ISO-10303-21;
HEADER;
/* Generated by software containing ST-Developer
 * from STEP Tools, Inc. (www.steptools.com) 
 */

FILE_DESCRIPTION(
/* description */ (''),
/* implementation_level */ '2;1');

FILE_NAME(
/* name */ 'Assembly Screw 2.step',
/* time_stamp */ '2026-10-28T16:47:13+01:00',
/* author */ (''),
/* organization */ (''),
/* preprocessor_version */ 'ST-DEVELOPER v20.2',
/* originating_system */ 'Autodesk Translation Framework v15.17.0.0',
/* authorisation */ '');

FILE_SCHEMA (('AUTOMOTIVE_DESIGN { 1 0 10303 214 3 1 1 }'));
ENDSEC;

DATA;
#10=MECHANICAL_DESIGN_GEOMETRIC_PRESENTATION_REPRESENTATION('',(#4607),#459242);
#198=ELLIPSE('',#99479,0.027499979201819,0.0194466400235264);
#199=ELLIPSE('',#99481,0.0274999792018223,0.0194466400235272);
#200=ELLIPSE('',#99483,0.0274999792017924,0.0194466400235207);
#201=ELLIPSE('',#99485,0.0274999792018212,0.0194466400235271);
#202=ELLIPSE('',#99487,0.0274999792018093,0.0194466400235266);
#203=ELLIPSE('',#99489,0.0274999792018116,0.0194466400235246);
#204=ELLIPSE('',#99491,0.0274999792018137,0.0194466400235258);
#205=ELLIPSE('',#99493,0.0274999792018285,0.019446640023529);
#206=ELLIPSE('',#99495,0.0274999792018225,0.0194466400235274);
#207=ELLIPSE('',#99497,0.0274999792018218,0.0194466400235291);
#208=ELLIPSE('',#99499,0.0274999792018109,0.019446640023525);
#209=ELLIPSE('',#99501,0.0274999792018031,0.0194466400235235);
#210=ELLIPSE('',#99503,0.0274999792018403,0.0194466400235318);
#211=ELLIPSE('',#99505,0.0274999792018273,0.0194466400235287);
#212=ELLIPSE('',#99507,0.0274999792018071,0.0194466400235239);
#213=ELLIPSE('',#99509,0.0274999792018003,0.0194466400235229);
#214=ELLIPSE('',#99511,0.0274999792018132,0.0194466400235249);
#215=ELLIPSE('',#99513,0.0274999792018307,0.0194466400235292);
#216=ELLIPSE('',#99515,0.0274999792018211,0.0194466400235281);
#217=ELLIPSE('',#99517,0.027499979201803,0.0194466400235226);
#218=ELLIPSE('',#99519,0.027499979201819,0.019446640023527);
#219=ELLIPSE('',#99521,0.0274999792018149,0.0194466400235247);
#220=ELLIPSE('',#99523,0.0274999792018479,0.019446640023533);
#221=ELLIPSE('',#99525,0.0274999792018327,0.0194466400235312);
#222=ELLIPSE('',#99527,0.0274999792018231,0.0194466400235292);
#223=ELLIPSE('',#99529,0.0274999792018213,0.0194466400235274);
#224=ELLIPSE('',#99531,0.0274999792018071,0.0194466400235238);
#225=ELLIPSE('',#99533,0.0274999792018454,0.0194466400235312);
#226=ELLIPSE('',#99535,0.0274999792018473,0.0194466400235348);
#227=ELLIPSE('',#99537,0.0274999792017789,0.0194466400235172);
#228=ELLIPSE('',#99539,0.0274999792017695,0.0194466400235156);
#229=ELLIPSE('',#99541,0.0274999792018213,0.0194466400235258);
#230=ELLIPSE('',#99543,0.0274999792018424,0.0194466400235306);
#231=ELLIPSE('',#99545,0.0274999792018183,0.0194466400235275);
#232=ELLIPSE('',#99547,0.0274999792018239,0.0194466400235288);
#233=ELLIPSE('',#99549,0.02749997920184,0.0194466400235311);
#234=ELLIPSE('',#99551,0.0274999792018135,0.0194466400235251);
#235=ELLIPSE('',#99553,0.0274999792017894,0.019446640023519);
#236=ELLIPSE('',#99555,0.0274999792018526,0.0194466400235354);
#237=ELLIPSE('',#99557,0.0274999792017924,0.0194466400235216);
#238=ELLIPSE('',#99559,0.0274999792018348,0.0194466400235303);
#239=ELLIPSE('',#99561,0.0274999792018408,0.0194466400235337);
#240=ELLIPSE('',#99563,0.0274999792018198,0.0194466400235256);
#241=ELLIPSE('',#99565,0.0274999792018384,0.0194466400235318);
#242=ELLIPSE('',#99567,0.027499979201788,0.0194466400235206);
#243=ELLIPSE('',#99569,0.0274999792018338,0.0194466400235292);
#244=ELLIPSE('',#99571,0.027499979201835,0.0194466400235291);
#245=ELLIPSE('',#99573,0.0274999792018021,0.0194466400235238);
#246=ELLIPSE('',#99575,0.0274999792018534,0.0194466400235355);
#247=ELLIPSE('',#99580,0.0274999792018521,0.0194466400235337);
#248=ELLIPSE('',#99582,0.027499979201854,0.0194466400235346);
#249=ELLIPSE('',#99584,0.0274999792018411,0.0194466400235325);
#250=ELLIPSE('',#99586,0.0274999792017827,0.0194466400235186);
#251=ELLIPSE('',#99588,0.0274999792018246,0.0194466400235274);
#252=ELLIPSE('',#99590,0.0274999792018228,0.0194466400235272);
#253=ELLIPSE('',#99592,0.0274999792018508,0.0194466400235342);
#254=ELLIPSE('',#99594,0.027499979201825,0.019446640023528);
#255=ELLIPSE('',#99596,0.0274999792018088,0.0194466400235245);
#256=ELLIPSE('',#99598,0.0274999792018039,0.0194466400235234);
#257=ELLIPSE('',#99600,0.0274999792018231,0.0194466400235278);
#258=ELLIPSE('',#99602,0.0274999792018028,0.0194466400235229);
#259=ELLIPSE('',#99604,0.0274999792018038,0.019446640023523);
#260=ELLIPSE('',#99606,0.0274999792018027,0.0194466400235246);
#261=ELLIPSE('',#99608,0.0274999792018087,0.0194466400235226);
#262=ELLIPSE('',#99610,0.027499979201824,0.0194466400235279);
#263=ELLIPSE('',#99612,0.0274999792018275,0.0194466400235301);
#264=ELLIPSE('',#99614,0.0274999792018072,0.019446640023524);
#265=ELLIPSE('',#99616,0.0274999792018082,0.0194466400235244);
#266=ELLIPSE('',#99618,0.0274999792018318,0.0194466400235293);
#267=ELLIPSE('',#99620,0.0274999792017886,0.0194466400235195);
#268=ELLIPSE('',#99622,0.0274999792018619,0.0194466400235365);
#269=ELLIPSE('',#99624,0.0274999792018085,0.0194466400235243);
#270=ELLIPSE('',#99626,0.0274999792018058,0.0194466400235241);
#271=ELLIPSE('',#99628,0.0274999792018022,0.0194466400235246);
#272=ELLIPSE('',#99630,0.02749997920182,0.0194466400235268);
#273=ELLIPSE('',#99632,0.0274999792017819,0.0194466400235169);
#274=ELLIPSE('',#99634,0.0274999792018284,0.0194466400235286);
#275=ELLIPSE('',#99636,0.0274999792018055,0.0194466400235254);
#276=ELLIPSE('',#99638,0.0274999792018053,0.0194466400235236);
#277=ELLIPSE('',#99640,0.0274999792018291,0.0194466400235292);
#278=ELLIPSE('',#99642,0.0274999792018261,0.0194466400235284);
#279=ELLIPSE('',#99644,0.0274999792018197,0.0194466400235282);
#280=ELLIPSE('',#99646,0.0274999792018074,0.0194466400235247);
#281=ELLIPSE('',#99648,0.0274999792018118,0.0194466400235253);
#282=ELLIPSE('',#99650,0.0274999792018347,0.0194466400235298);
#283=ELLIPSE('',#99652,0.0274999792017871,0.0194466400235192);
#284=ELLIPSE('',#99654,0.0274999792018461,0.0194466400235328);
#285=ELLIPSE('',#99656,0.0274999792018429,0.0194466400235337);
#286=ELLIPSE('',#99658,0.0274999792018179,0.0194466400235262);
#287=ELLIPSE('',#99660,0.0274999792018226,0.0194466400235276);
#288=ELLIPSE('',#99662,0.0274999792018338,0.0194466400235298);
#289=ELLIPSE('',#99664,0.027499979201791,0.0194466400235187);
#290=ELLIPSE('',#99666,0.0274999792018158,0.0194466400235259);
#291=ELLIPSE('',#99668,0.0274999792018309,0.0194466400235295);
#292=ELLIPSE('',#99670,0.0274999792018025,0.0194466400235224);
#293=ELLIPSE('',#99672,0.0274999792018289,0.0194466400235288);
#294=ELLIPSE('',#99674,0.0274999792018066,0.0194466400235238);
#295=ELLIPSE('',#99676,0.027499979201837,0.0194466400235302);
#296=ELLIPSE('',#99682,0.0377939546271109,0.0250703601820978);
#297=ELLIPSE('',#99684,0.0378695219465235,0.0250983059764406);
#298=ELLIPSE('',#99686,0.0377939546270395,0.0250703601820702);
#299=ELLIPSE('',#99688,0.037869521946444,0.0250983059764107);
#300=ELLIPSE('',#99690,0.0377939546272685,0.0250703601821445);
#301=ELLIPSE('',#99692,0.0378695219466119,0.0250983059764672);
#302=ELLIPSE('',#99694,0.0377939546269576,0.0250703601820378);
#303=ELLIPSE('',#99696,0.0378695219464082,0.0250983059763933);
#304=ELLIPSE('',#99698,0.0377939546267997,0.0250703601819834);
#305=ELLIPSE('',#99700,0.0378695219464645,0.0250983059764194);
#306=ELLIPSE('',#99702,0.0377939546267974,0.0250703601819848);
#307=ELLIPSE('',#99704,0.0378695219466849,0.0250983059764935);
#308=ELLIPSE('',#99706,0.0377939546269491,0.0250703601820439);
#309=ELLIPSE('',#99708,0.0378695219464801,0.0250983059764239);
#310=ELLIPSE('',#99710,0.0377939546268274,0.0250703601820047);
#311=ELLIPSE('',#99712,0.0378695219465395,0.0250983059764457);
#312=ELLIPSE('',#99714,0.0377939546270607,0.0250703601820776);
#313=ELLIPSE('',#99716,0.0378695219463676,0.02509830597638);
#314=ELLIPSE('',#99718,0.0377939546270672,0.0250703601820751);
#315=ELLIPSE('',#99720,0.0378695219465767,0.0250983059764549);
#316=ELLIPSE('',#99722,0.0377939546270847,0.0250703601820898);
#317=ELLIPSE('',#99724,0.0378695219463306,0.0250983059763689);
#318=ELLIPSE('',#99726,0.0377939546271058,0.0250703601820951);
#319=ELLIPSE('',#99728,0.0378695219463806,0.0250983059763838);
#320=ELLIPSE('',#99730,0.0377939546273992,0.0250703601821958);
#321=ELLIPSE('',#99732,0.0378695219463341,0.0250983059763734);
#322=ELLIPSE('',#99734,0.0377939546267671,0.0250703601819788);
#323=ELLIPSE('',#99736,0.0378695219467491,0.0250983059765119);
#324=ELLIPSE('',#99738,0.037793954627011,0.0250703601820574);
#325=ELLIPSE('',#99740,0.0378695219464796,0.0250983059764208);
#326=ELLIPSE('',#99742,0.0377939546271938,0.0250703601821272);
#327=ELLIPSE('',#99744,0.0378695219464403,0.0250983059764047);
#328=ELLIPSE('',#99746,0.0377939546272078,0.0250703601821293);
#329=ELLIPSE('',#99748,0.0378695219462217,0.0250983059763317);
#330=ELLIPSE('',#99750,0.0377939546274431,0.0250703601822155);
#331=ELLIPSE('',#99752,0.0378695219465727,0.025098305976455);
#332=ELLIPSE('',#99754,0.0377939546272413,0.0250703601821465);
#333=ELLIPSE('',#99756,0.0378695219465893,0.0250983059764576);
#334=ELLIPSE('',#99758,0.0377939546268262,0.0250703601819944);
#335=ELLIPSE('',#99760,0.037869521946427,0.0250983059763988);
#336=ELLIPSE('',#99762,0.0377939546267704,0.0250703601819765);
#337=ELLIPSE('',#99764,0.0378695219464597,0.0250983059764122);
#338=ELLIPSE('',#99766,0.0377939546267808,0.0250703601819798);
#339=ELLIPSE('',#99768,0.0378695219460054,0.025098305976261);
#340=ELLIPSE('',#99770,0.0377939546271222,0.0250703601820998);
#341=ELLIPSE('',#99772,0.0378695219467645,0.0250983059765208);
#342=ELLIPSE('',#99774,0.0377939546272981,0.025070360182163);
#343=ELLIPSE('',#99776,0.0378695219464416,0.0250983059764082);
#344=ELLIPSE('',#99778,0.0377939546270981,0.0250703601820953);
#345=ELLIPSE('',#99780,0.0378695219463879,0.0250983059763866);
#346=ELLIPSE('',#99782,0.0377939546269133,0.0250703601820331);
#347=ELLIPSE('',#99784,0.03786952194643,0.0250983059764058);
#348=ELLIPSE('',#99786,0.037793954627311,0.0250703601821679);
#349=ELLIPSE('',#99788,0.0378695219464575,0.0250983059764103);
#350=ELLIPSE('',#99790,0.037793954626787,0.0250703601819827);
#351=ELLIPSE('',#99792,0.0378695219465744,0.0250983059764543);
#352=ELLIPSE('',#99794,0.037793954627,0.0250703601820628);
#353=ELLIPSE('',#99796,0.0378695219464972,0.0250983059764296);
#354=ELLIPSE('',#99798,0.0377939546271824,0.0250703601821208);
#355=ELLIPSE('',#99800,0.0378695219463181,0.0250983059763621);
#356=ELLIPSE('',#99802,0.0377939546270806,0.02507036018209);
#357=ELLIPSE('',#99804,0.0378695219464793,0.025098305976419);
#358=ELLIPSE('',#99806,0.0377939546271536,0.0250703601821112);
#359=ELLIPSE('',#99808,0.0378695219464171,0.0250983059764114);
#360=ELLIPSE('',#99810,0.0377939546268865,0.0250703601820144);
#361=ELLIPSE('',#99812,0.0378695219466686,0.0250983059764919);
#362=ELLIPSE('',#99814,0.0377939546269507,0.0250703601820383);
#363=ELLIPSE('',#99816,0.0378695219467058,0.0250983059764957);
#364=ELLIPSE('',#99818,0.0377939546272764,0.0250703601821624);
#365=ELLIPSE('',#99820,0.0378695219461522,0.0250983059763082);
#366=ELLIPSE('',#99822,0.0377939546272405,0.0250703601821427);
#367=ELLIPSE('',#99824,0.0378695219465727,0.0250983059764577);
#368=ELLIPSE('',#99826,0.0377939546272697,0.0250703601821556);
#369=ELLIPSE('',#99828,0.0378695219465898,0.0250983059764639);
#370=ELLIPSE('',#99830,0.0377939546271452,0.0250703601821021);
#371=ELLIPSE('',#99832,0.0378695219464919,0.0250983059764311);
#372=ELLIPSE('',#99834,0.0377939546270735,0.0250703601820848);
#373=ELLIPSE('',#99836,0.0378695219467591,0.0250983059765092);
#374=ELLIPSE('',#99838,0.0377939546272653,0.0250703601821518);
#375=ELLIPSE('',#99840,0.0378695219467233,0.0250983059764915);
#376=ELLIPSE('',#99842,0.0377939546271496,0.0250703601821116);
#377=ELLIPSE('',#99844,0.037869521946483,0.0250983059764293);
#378=ELLIPSE('',#99846,0.0377939546268239,0.0250703601819968);
#379=ELLIPSE('',#99848,0.0378695219468845,0.0250983059765543);
#380=ELLIPSE('',#99850,0.0377939546266337,0.0250703601819282);
#381=ELLIPSE('',#99852,0.0378695219461948,0.0250983059763309);
#382=ELLIPSE('',#99854,0.0377939546269812,0.025070360182053);
#383=ELLIPSE('',#99856,0.0378695219463886,0.0250983059763826);
#384=ELLIPSE('',#99858,0.037793954627197,0.025070360182132);
#385=ELLIPSE('',#99860,0.0378695219465481,0.0250983059764459);
#386=ELLIPSE('',#99862,0.0377939546267804,0.0250703601819784);
#387=ELLIPSE('',#99864,0.0378695219459524,0.0250983059762446);
#388=ELLIPSE('',#99866,0.0377939546270476,0.0250703601820695);
#389=ELLIPSE('',#99868,0.0378695219469002,0.0250983059765617);
#390=ELLIPSE('',#99870,0.0377939546271249,0.0250703601820983);
#391=ELLIPSE('',#99872,0.037869521946226,0.0250983059763336);
#392=ELLIPSE('',#99874,0.0377939546270712,0.0250703601820862);
#393=ELLIPSE('',#99876,0.0378695219466723,0.0250983059764892);
#394=ELLIPSE('',#99879,0.0377939546273518,0.0250703601821778);
#395=ELLIPSE('',#99881,0.037869521947147,0.0250983059766503);
#396=ELLIPSE('',#99883,0.0377939546273672,0.0250703601821858);
#397=ELLIPSE('',#99885,0.0378695219471249,0.0250983059766443);
#398=ELLIPSE('',#99887,0.0377939546272684,0.0250703601821527);
#399=ELLIPSE('',#99889,0.0378695219465376,0.0250983059764453);
#400=ELLIPSE('',#99891,0.0377939546267177,0.0250703601819543);
#401=ELLIPSE('',#99893,0.0378695219465633,0.0250983059764556);
#402=ELLIPSE('',#99895,0.0377939546267279,0.0250703601819634);
#403=ELLIPSE('',#99897,0.0378695219465408,0.0250983059764424);
#404=ELLIPSE('',#99899,0.0377939546271458,0.0250703601821111);
#405=ELLIPSE('',#99901,0.037869521946556,0.0250983059764535);
#406=ELLIPSE('',#99903,0.0377939546272391,0.0250703601821381);
#407=ELLIPSE('',#99905,0.0378695219461841,0.0250983059763208);
#408=ELLIPSE('',#99907,0.0377939546271602,0.0250703601821172);
#409=ELLIPSE('',#99909,0.0378695219469737,0.0250983059765869);
#410=ELLIPSE('',#99911,0.0377939546268286,0.025070360181992);
#411=ELLIPSE('',#99913,0.0378695219464023,0.0250983059763922);
#412=ELLIPSE('',#99915,0.0377939546271851,0.0250703601821223);
#413=ELLIPSE('',#99917,0.0378695219460789,0.0250983059762906);
#414=ELLIPSE('',#99919,0.037793954627282,0.0250703601821508);
#415=ELLIPSE('',#99921,0.0378695219465084,0.0250983059764242);
#416=ELLIPSE('',#99923,0.0377939546267815,0.0250703601819804);
#417=ELLIPSE('',#99925,0.0378695219463702,0.0250983059763883);
#418=ELLIPSE('',#99927,0.0377939546265622,0.025070360181903);
#419=ELLIPSE('',#99929,0.0378695219464024,0.0250983059764034);
#420=ELLIPSE('',#99931,0.0377939546270649,0.0250703601820832);
#421=ELLIPSE('',#99933,0.037869521946096,0.0250983059762913);
#422=ELLIPSE('',#99935,0.0377939546270451,0.0250703601820666);
#423=ELLIPSE('',#99937,0.0378695219465469,0.0250983059764424);
#424=ELLIPSE('',#99939,0.0377939546274933,0.025070360182228);
#425=ELLIPSE('',#99941,0.0378695219459719,0.0250983059762507);
#426=ELLIPSE('',#99943,0.037793954626721,0.0250703601819633);
#427=ELLIPSE('',#99945,0.0378695219467833,0.0250983059765231);
#428=ELLIPSE('',#99947,0.0377939546272019,0.0250703601821268);
#429=ELLIPSE('',#99949,0.0378695219465463,0.0250983059764481);
#430=ELLIPSE('',#99951,0.0377939546273632,0.0250703601821844);
#431=ELLIPSE('',#99953,0.0378695219468885,0.0250983059765562);
#432=ELLIPSE('',#99955,0.0377939546272644,0.0250703601821503);
#433=ELLIPSE('',#99957,0.0378695219465198,0.0250983059764359);
#434=ELLIPSE('',#99959,0.0377939546270628,0.025070360182078);
#435=ELLIPSE('',#99961,0.0378695219461977,0.02509830597633);
#436=ELLIPSE('',#99963,0.0377939546271482,0.0250703601821143);
#437=ELLIPSE('',#99965,0.0378695219465306,0.0250983059764382);
#438=ELLIPSE('',#99967,0.0377939546267965,0.0250703601819846);
#439=ELLIPSE('',#99969,0.0378695219466369,0.0250983059764776);
#440=ELLIPSE('',#99971,0.0377939546272131,0.0250703601821351);
#441=ELLIPSE('',#99973,0.0378695219464218,0.0250983059764017);
#442=ELLIPSE('',#99975,0.0377939546270981,0.0250703601820953);
#443=ELLIPSE('',#99977,0.0378695219460318,0.0250983059762701);
#444=ELLIPSE('',#99979,0.0377939546271911,0.0250703601821247);
#445=ELLIPSE('',#99981,0.0378695219466486,0.0250983059764816);
#446=ELLIPSE('',#99983,0.0377939546272545,0.0250703601821443);
#447=ELLIPSE('',#99985,0.0378695219464022,0.0250983059763928);
#448=ELLIPSE('',#99987,0.0377939546270471,0.0250703601820705);
#449=ELLIPSE('',#99989,0.0378695219464218,0.025098305976405);
#450=ELLIPSE('',#99991,0.037793954627098,0.0250703601820907);
#451=ELLIPSE('',#99993,0.03786952194662,0.0250983059764673);
#452=ELLIPSE('',#99995,0.0377939546268382,0.0250703601819987);
#453=ELLIPSE('',#99997,0.0378695219465927,0.0250983059764667);
#454=ELLIPSE('',#99999,0.0377939546271273,0.0250703601821041);
#455=ELLIPSE('',#100001,0.0378695219461789,0.0250983059763172);
#456=ELLIPSE('',#100003,0.0377939546268529,0.0250703601820112);
#457=ELLIPSE('',#100005,0.0378695219465492,0.0250983059764485);
#458=ELLIPSE('',#100007,0.0377939546268233,0.0250703601819974);
#459=ELLIPSE('',#100009,0.0378695219464527,0.0250983059764105);
#460=ELLIPSE('',#100011,0.0377939546267064,0.0250703601819536);
#461=ELLIPSE('',#100013,0.0378695219465347,0.0250983059764463);
#462=ELLIPSE('',#100015,0.0377939546271184,0.0250703601820973);
#463=ELLIPSE('',#100017,0.0378695219464462,0.0250983059764076);
#464=ELLIPSE('',#100019,0.0377939546269241,0.0250703601820279);
#465=ELLIPSE('',#100021,0.037869521946493,0.0250983059764276);
#466=ELLIPSE('',#100023,0.0377939546272981,0.025070360182169);
#467=ELLIPSE('',#100025,0.037869521946465,0.0250983059764108);
#468=ELLIPSE('',#100027,0.037793954627171,0.0250703601821197);
#469=ELLIPSE('',#100029,0.0378695219462166,0.0250983059763296);
#470=ELLIPSE('',#100031,0.0377939546272262,0.0250703601821393);
#471=ELLIPSE('',#100033,0.0378695219463891,0.0250983059763892);
#472=ELLIPSE('',#100035,0.0377939546270739,0.0250703601820887);
#473=ELLIPSE('',#100037,0.0378695219466546,0.0250983059764808);
#474=ELLIPSE('',#100039,0.0377939546270089,0.0250703601820585);
#475=ELLIPSE('',#100041,0.0378695219463441,0.0250983059763761);
#476=ELLIPSE('',#100043,0.0377939546270472,0.0250703601820732);
#477=ELLIPSE('',#100045,0.0378695219463518,0.0250983059763784);
#478=ELLIPSE('',#100047,0.0377939546271573,0.0250703601821169);
#479=ELLIPSE('',#100049,0.0378695219466952,0.0250983059764971);
#480=ELLIPSE('',#100051,0.0377939546271577,0.0250703601821112);
#481=ELLIPSE('',#100053,0.0378695219462776,0.0250983059763517);
#482=ELLIPSE('',#100055,0.0377939546271348,0.0250703601821107);
#483=ELLIPSE('',#100057,0.0378695219464613,0.0250983059764109);
#484=ELLIPSE('',#100059,0.0377939546271653,0.0250703601821089);
#485=ELLIPSE('',#100061,0.0378695219465757,0.0250983059764537);
#486=ELLIPSE('',#100063,0.0377939546272274,0.0250703601821409);
#487=ELLIPSE('',#100065,0.0378695219463364,0.0250983059763705);
#488=ELLIPSE('',#100067,0.0377939546269824,0.0250703601820482);
#489=ELLIPSE('',#100069,0.0378695219463565,0.0250983059763739);
#490=ELLIPSE('',#100071,0.0377939546272586,0.0250703601821497);
#491=ELLIPSE('',#100073,0.037869521946479,0.0250983059764217);
#492=ELLIPSE('',#100075,0.0594717522093815,0.0552292627679723);
#493=ELLIPSE('',#100076,0.0523574408941029,0.0489195958911169);
#494=ELLIPSE('',#100078,0.0523574408930336,0.048919595889694);
#495=ELLIPSE('',#100079,0.0594717522063949,0.0552292627663424);
#496=ELLIPSE('',#100081,0.059471752210527,0.0552292627685546);
#497=ELLIPSE('',#100082,0.0523574408933772,0.0489195958901572);
#498=ELLIPSE('',#100084,0.0594717522080122,0.0552292627672104);
#499=ELLIPSE('',#100085,0.0523574408945968,0.0489195958918944);
#500=ELLIPSE('',#100087,0.0594717522099653,0.0552292627682868);
#501=ELLIPSE('',#100088,0.0523574408935738,0.0489195958903706);
#502=ELLIPSE('',#100090,0.0594717522071289,0.0552292627667538);
#503=ELLIPSE('',#100091,0.0523574408941314,0.0489195958911761);
#504=ELLIPSE('',#100093,0.0594717522078325,0.0552292627671278);
#505=ELLIPSE('',#100094,0.0523574408930899,0.0489195958898256);
#506=ELLIPSE('',#100096,0.0594717522074437,0.0552292627669329);
#507=ELLIPSE('',#100097,0.0523574408948173,0.0489195958920454);
#508=ELLIPSE('',#100099,0.0594717522075256,0.0552292627669854);
#509=ELLIPSE('',#100100,0.0523574408932733,0.0489195958900324);
#510=ELLIPSE('',#100102,0.0594717522088852,0.0552292627677376);
#511=ELLIPSE('',#100103,0.0523574408934708,0.0489195958902787);
#512=ELLIPSE('',#100105,0.0594717522104183,0.0552292627685669);
#513=ELLIPSE('',#100106,0.0523574408933491,0.0489195958901329);
#514=ELLIPSE('',#100108,0.059471752206937,0.0552292627666515);
#515=ELLIPSE('',#100109,0.0523574408941294,0.0489195958912471);
#516=ELLIPSE('',#100111,0.0594717522082379,0.055229262767351);
#517=ELLIPSE('',#100112,0.052357440893126,0.0489195958898559);
#518=ELLIPSE('',#100114,0.0594717522082644,0.0552292627674078);
#519=ELLIPSE('',#100115,0.0523574408934445,0.0489195958902684);
#520=ELLIPSE('',#100117,0.0594717522068689,0.0552292627666162);
#521=ELLIPSE('',#100118,0.0523574408922878,0.0489195958887345);
#522=ELLIPSE('',#100120,0.0594717522080172,0.055229262767222);
#523=ELLIPSE('',#100121,0.0523574408943491,0.0489195958914509);
#524=ELLIPSE('',#100123,0.0594717522070147,0.055229262766697);
#525=ELLIPSE('',#100124,0.0523574408928524,0.0489195958894166);
#526=ELLIPSE('',#100126,0.059471752206359,0.0552292627663632);
#527=ELLIPSE('',#100127,0.0523574408936573,0.0489195958905023);
#528=ELLIPSE('',#100129,0.0594717522080242,0.0552292627672641);
#529=ELLIPSE('',#100130,0.0523574408925724,0.0489195958890778);
#530=ELLIPSE('',#100132,0.0594717522087728,0.0552292627676604);
#531=ELLIPSE('',#100133,0.0523574408942549,0.0489195958913365);
#532=ELLIPSE('',#100135,0.0594717522117556,0.0552292627692794);
#533=ELLIPSE('',#100136,0.0523574408925802,0.0489195958890979);
#534=ELLIPSE('',#100138,0.0594717522092905,0.055229262767912);
#535=ELLIPSE('',#100139,0.0523574408935547,0.0489195958904525);
#536=ELLIPSE('',#100141,0.0594717522079891,0.0552292627672496);
#537=ELLIPSE('',#100142,0.0523574408925326,0.0489195958890156);
#538=ELLIPSE('',#100144,0.059471752209349,0.05522926276795);
#539=ELLIPSE('',#100145,0.0523574408931156,0.048919595889817);
#540=ELLIPSE('',#100147,0.0594717522060788,0.0552292627661841);
#541=ELLIPSE('',#100148,0.0523574408937248,0.0489195958905856);
#542=ELLIPSE('',#100150,0.0594717522076025,0.0552292627670435);
#543=ELLIPSE('',#100151,0.0523574408931184,0.0489195958898577);
#544=ELLIPSE('',#100153,0.0594717522085552,0.0552292627675089);
#545=ELLIPSE('',#100154,0.0523574408942864,0.0489195958914513);
#546=ELLIPSE('',#100156,0.0594717522095339,0.0552292627680599);
#547=ELLIPSE('',#100157,0.0523574408933161,0.0489195958900139);
#548=ELLIPSE('',#100159,0.0594717522094596,0.0552292627679749);
#549=ELLIPSE('',#100160,0.0523574408929958,0.0489195958896259);
#550=ELLIPSE('',#100162,0.0594717522107856,0.0552292627686926);
#551=ELLIPSE('',#100163,0.052357440893669,0.0489195958905554);
#552=ELLIPSE('',#100165,0.059471752207577,0.0552292627670372);
#553=ELLIPSE('',#100166,0.0523574408935437,0.0489195958903441);
#554=ELLIPSE('',#100168,0.0594717522095802,0.0552292627680481);
#555=ELLIPSE('',#100169,0.0523574408924447,0.0489195958888946);
#556=ELLIPSE('',#100171,0.0594717522083012,0.0552292627673983);
#557=ELLIPSE('',#100172,0.052357440892708,0.0489195958892621);
#558=ELLIPSE('',#100174,0.0594717522076934,0.0552292627670944);
#559=ELLIPSE('',#100175,0.0523574408938724,0.0489195958907808);
#560=ELLIPSE('',#100177,0.0594717522081998,0.0552292627673637);
#561=ELLIPSE('',#100178,0.0523574408925381,0.0489195958889725);
#562=ELLIPSE('',#100180,0.0594717522060484,0.0552292627661945);
#563=ELLIPSE('',#100181,0.0523574408917811,0.0489195958880099);
#564=ELLIPSE('',#100183,0.0594717522096474,0.0552292627681111);
#565=ELLIPSE('',#100184,0.0523574408933097,0.0489195958901172);
#566=ELLIPSE('',#100186,0.0594717522073831,0.0552292627668932);
#567=ELLIPSE('',#100187,0.0523574408935224,0.0489195958904008);
#568=ELLIPSE('',#100189,0.0594717522078441,0.0552292627671437);
#569=ELLIPSE('',#100190,0.0523574408939627,0.0489195958908927);
#570=ELLIPSE('',#100192,0.0594717522112087,0.0552292627689124);
#571=ELLIPSE('',#100193,0.0523574408926999,0.0489195958892166);
#572=ELLIPSE('',#100195,0.0594717522077727,0.0552292627671321);
#573=ELLIPSE('',#100196,0.0523574408945673,0.0489195958917693);
#574=ELLIPSE('',#100198,0.0594717522067864,0.0552292627665967);
#575=ELLIPSE('',#100199,0.052357440893046,0.048919595889673);
#576=ELLIPSE('',#100201,0.0594717522070521,0.0552292627667294);
#577=ELLIPSE('',#100202,0.052357440893711,0.0489195958906244);
#578=ELLIPSE('',#100204,0.0594717522074139,0.055229262766935);
#579=ELLIPSE('',#100205,0.0523574408936527,0.0489195958906036);
#580=ELLIPSE('',#100207,0.0594717522106702,0.0552292627686464);
#581=ELLIPSE('',#100208,0.0523574408925687,0.0489195958890896);
#582=ELLIPSE('',#100210,0.0594717522061032,0.0552292627662244);
#583=ELLIPSE('',#100211,0.0523574408933305,0.0489195958901204);
#584=ELLIPSE('',#100213,0.0594717522078377,0.0552292627671592);
#585=ELLIPSE('',#100214,0.0523574408934019,0.0489195958902017);
#586=ELLIPSE('',#100216,0.0594717522095676,0.0552292627680807);
#587=ELLIPSE('',#100217,0.0523574408935074,0.048919595890387);
#588=ELLIPSE('',#100219,0.0594717522063091,0.0552292627662996);
#589=ELLIPSE('',#100220,0.0523574408934654,0.0489195958902804);
#590=ELLIPSE('',#100222,0.0594717522078024,0.055229262767126);
#591=ELLIPSE('',#100223,0.0523574408931717,0.048919595889865);
#592=ELLIPSE('',#100225,0.0594717522062108,0.0552292627662818);
#593=ELLIPSE('',#100226,0.0523574408944596,0.048919595891611);
#594=ELLIPSE('',#100228,0.0594717522059097,0.055229262766132);
#595=ELLIPSE('',#100229,0.0523574408929005,0.0489195958895422);
#596=ELLIPSE('',#100231,0.0594717522087653,0.0552292627676661);
#597=ELLIPSE('',#100232,0.052357440892832,0.0489195958893877);
#598=ELLIPSE('',#100234,0.0594717522108721,0.0552292627687884);
#599=ELLIPSE('',#100235,0.0523574408940629,0.0489195958911095);
#600=ELLIPSE('',#100237,0.0594717522082771,0.0552292627674181);
#601=ELLIPSE('',#100238,0.0523574408928738,0.0489195958895351);
#602=ELLIPSE('',#100240,0.0594717522078313,0.0552292627671469);
#603=ELLIPSE('',#100241,0.0523574408941011,0.0489195958911154);
#604=ELLIPSE('',#100243,0.0594717522081063,0.0552292627673198);
#605=ELLIPSE('',#100244,0.0523574408937338,0.0489195958906628);
#606=ELLIPSE('',#100246,0.0594717522056887,0.0552292627659561);
#607=ELLIPSE('',#100247,0.0523574408928622,0.0489195958894712);
#608=ELLIPSE('',#100249,0.0594717522088224,0.0552292627677157);
#609=ELLIPSE('',#100250,0.0523574408944811,0.0489195958916444);
#610=ELLIPSE('',#100252,0.0594717522089922,0.0552292627677814);
#611=ELLIPSE('',#100253,0.0523574408947637,0.0489195958920602);
#612=ELLIPSE('',#100255,0.0594717522120167,0.0552292627693562);
#613=ELLIPSE('',#100256,0.0523574408934261,0.0489195958901972);
#614=ELLIPSE('',#100258,0.0594717522125058,0.0552292627696656);
#615=ELLIPSE('',#100259,0.052357440893374,0.048919595890127);
#616=ELLIPSE('',#100261,0.0594717522094242,0.0552292627680217);
#617=ELLIPSE('',#100262,0.0523574408935378,0.0489195958903875);
#618=ELLIPSE('',#100264,0.0594717522087569,0.0552292627676444);
#619=ELLIPSE('',#100265,0.052357440892614,0.0489195958891282);
#620=ELLIPSE('',#100267,0.0594717522092211,0.0552292627678974);
#621=ELLIPSE('',#100268,0.0523574408936857,0.0489195958905767);
#622=ELLIPSE('',#100270,0.0523574408929943,0.0489195958897697);
#623=ELLIPSE('',#100271,0.0594717522085673,0.0552292627675639);
#624=ELLIPSE('',#100273,0.0523574408939794,0.0489195958909905);
#625=ELLIPSE('',#100274,0.0594717522101173,0.0552292627683671);
#626=ELLIPSE('',#100276,0.052357440892821,0.0489195958893363);
#627=ELLIPSE('',#100277,0.0594717522076746,0.0552292627670676);
#628=ELLIPSE('',#100279,0.0523574408943176,0.048919595891439);
#629=ELLIPSE('',#100280,0.0594717522097422,0.0552292627682068);
#630=ELLIPSE('',#100282,0.0523574408948324,0.0489195958921146);
#631=ELLIPSE('',#100283,0.0594717522092244,0.0552292627678736);
#632=ELLIPSE('',#100285,0.0523574408928958,0.0489195958894956);
#633=ELLIPSE('',#100286,0.059471752209436,0.0552292627679566);
#634=ELLIPSE('',#100288,0.0523574408927136,0.0489195958892958);
#635=ELLIPSE('',#100289,0.0594717522101865,0.0552292627683888);
#636=ELLIPSE('',#100291,0.0523574408933246,0.0489195958900545);
#637=ELLIPSE('',#100292,0.0594717522084889,0.0552292627675033);
#638=ELLIPSE('',#100294,0.0523574408929252,0.0489195958895466);
#639=ELLIPSE('',#100295,0.0594717522067242,0.0552292627665378);
#640=ELLIPSE('',#100297,0.0523574408935323,0.0489195958904197);
#641=ELLIPSE('',#100298,0.0594717522084362,0.0552292627674681);
#642=ELLIPSE('',#100300,0.0523574408934523,0.048919595890263);
#643=ELLIPSE('',#100301,0.0594717522090756,0.0552292627677804);
#644=ELLIPSE('',#100303,0.052357440893078,0.0489195958897325);
#645=ELLIPSE('',#100304,0.0594717522116622,0.055229262769157);
#646=ELLIPSE('',#100306,0.0523574408933239,0.0489195958901453);
#647=ELLIPSE('',#100307,0.0594717522098756,0.0552292627682184);
#648=ELLIPSE('',#100309,0.0523574408931826,0.0489195958898953);
#649=ELLIPSE('',#100310,0.05947175220972,0.0552292627681239);
#650=ELLIPSE('',#100312,0.0523574408929838,0.0489195958896346);
#651=ELLIPSE('',#100313,0.0594717522045155,0.0552292627653588);
#652=ELLIPSE('',#100315,0.0523574408926991,0.0489195958892291);
#653=ELLIPSE('',#100316,0.0594717522098512,0.0552292627682459);
#654=ELLIPSE('',#100318,0.0523574408937797,0.0489195958907056);
#655=ELLIPSE('',#100319,0.0594717522087746,0.0552292627676573);
#656=ELLIPSE('',#100321,0.0523574408945519,0.0489195958917232);
#657=ELLIPSE('',#100322,0.0594717522092935,0.0552292627679665);
#658=ELLIPSE('',#100324,0.0523574408931019,0.0489195958897895);
#659=ELLIPSE('',#100325,0.059471752208446,0.0552292627674902);
#660=ELLIPSE('',#100327,0.0523574408941714,0.0489195958912245);
#661=ELLIPSE('',#100328,0.0594717522091084,0.0552292627678568);
#662=ELLIPSE('',#100330,0.0523574408940044,0.0489195958909118);
#663=ELLIPSE('',#100331,0.0594717522068734,0.0552292627666293);
#664=ELLIPSE('',#100333,0.0523574408937834,0.0489195958907224);
#665=ELLIPSE('',#100334,0.0594717522098918,0.0552292627682498);
#666=ELLIPSE('',#100336,0.0523574408935842,0.0489195958904222);
#667=ELLIPSE('',#100337,0.0594717522076412,0.0552292627670567);
#668=ELLIPSE('',#100339,0.0523574408937256,0.0489195958906133);
#669=ELLIPSE('',#100340,0.0594717522070184,0.0552292627667054);
#670=ELLIPSE('',#100342,0.0523574408927693,0.0489195958892124);
#671=ELLIPSE('',#100343,0.0594717522081041,0.0552292627672715);
#672=ELLIPSE('',#100345,0.0523574408933158,0.0489195958900367);
#673=ELLIPSE('',#100346,0.0594717522063655,0.0552292627663595);
#674=ELLIPSE('',#100348,0.0523574408935146,0.0489195958902675);
#675=ELLIPSE('',#100349,0.0594717522087871,0.0552292627676304);
#676=ELLIPSE('',#100351,0.0523574408942678,0.0489195958913386);
#677=ELLIPSE('',#100352,0.0594717522065507,0.0552292627664879);
#678=ELLIPSE('',#100354,0.0523574408935429,0.0489195958904555);
#679=ELLIPSE('',#100355,0.0594717522103784,0.0552292627684482);
#680=ELLIPSE('',#100357,0.0523574408931172,0.0489195958897559);
#681=ELLIPSE('',#100358,0.0594717522069347,0.0552292627666673);
#682=ELLIPSE('',#100360,0.0523574408936834,0.0489195958906288);
#683=ELLIPSE('',#100361,0.0594717522080242,0.0552292627672641);
#684=ELLIPSE('',#100363,0.059471752207151,0.0552292627668208);
#685=ELLIPSE('',#100364,0.0523574408926382,0.0489195958891156);
#686=ELLIPSE('',#100368,0.0496327928416145,0.0434076000955403);
#687=ELLIPSE('',#100370,0.0425526869750752,0.039014288226265);
#688=ELLIPSE('',#100383,0.0594717522070795,0.0552292627667962);
#689=ELLIPSE('',#100384,0.0523574408936573,0.0489195958905023);
#690=ELLIPSE('',#100402,0.0192307675635318,0.0124961950671783);
#691=ELLIPSE('',#100406,0.0192307675634953,0.0124961950670989);
#692=ELLIPSE('',#100418,0.0425526869738727,0.0390142882252431);
#693=ELLIPSE('',#100420,0.0496327928421636,0.0434076000958099);
#694=ELLIPSE('',#100423,0.0192307675634341,0.0124961950670948);
#695=ELLIPSE('',#100424,0.0192307675633307,0.0124961950669426);
#696=ELLIPSE('',#100441,0.0425526869750512,0.0390142882262157);
#697=ELLIPSE('',#100443,0.0496327928428896,0.0434076000962082);
#698=ELLIPSE('',#100446,0.0192307675634649,0.0124961950671064);
#699=ELLIPSE('',#100447,0.0192307675632899,0.0124961950669237);
#700=ELLIPSE('',#100464,0.0425526869732722,0.0390142882247097);
#701=ELLIPSE('',#100466,0.0496327928411177,0.0434076000953248);
#702=ELLIPSE('',#100469,0.0192307675635973,0.0124961950671957);
#703=ELLIPSE('',#100470,0.0192307675633788,0.0124961950669941);
#704=ELLIPSE('',#100487,0.042552686974379,0.0390142882257283);
#705=ELLIPSE('',#100489,0.0496327928396385,0.0434076000945822);
#706=ELLIPSE('',#100492,0.0192307675633234,0.0124961950669785);
#707=ELLIPSE('',#100493,0.0192307675635267,0.0124961950671152);
#708=ELLIPSE('',#100510,0.0425526869749281,0.0390142882261518);
#709=ELLIPSE('',#100512,0.0496327928406238,0.0434076000950604);
#710=ELLIPSE('',#100515,0.0192307675632406,0.0124961950669363);
#711=ELLIPSE('',#100516,0.0192307675635317,0.0124961950671101);
#712=ELLIPSE('',#100533,0.0425526869741915,0.0390142882254985);
#713=ELLIPSE('',#100535,0.0496327928403701,0.0434076000948868);
#714=ELLIPSE('',#100538,0.0192307675638857,0.0124961950674675);
#715=ELLIPSE('',#100539,0.0192307675637902,0.0124961950673144);
#716=ELLIPSE('',#100556,0.0425526869735336,0.0390142882250337);
#717=ELLIPSE('',#100558,0.0496327928395447,0.0434076000945563);
#718=ELLIPSE('',#100561,0.0192307675636895,0.0124961950672939);
#719=ELLIPSE('',#100562,0.0192307675635296,0.0124961950671171);
#720=ELLIPSE('',#100579,0.0425526869736662,0.0390142882251435);
#721=ELLIPSE('',#100581,0.0496327928443886,0.0434076000968867);
#722=ELLIPSE('',#100584,0.0192307675636211,0.0124961950672701);
#723=ELLIPSE('',#100585,0.0192307675635263,0.0124961950670976);
#724=ELLIPSE('',#100602,0.042552686973854,0.0390142882252422);
#725=ELLIPSE('',#100604,0.049632792838296,0.0434076000939053);
#726=ELLIPSE('',#100607,0.0192307675635304,0.0124961950671889);
#727=ELLIPSE('',#100608,0.0192307675630496,0.0124961950667192);
#728=ELLIPSE('',#100625,0.0425526869739649,0.0390142882253226);
#729=ELLIPSE('',#100627,0.0496327928427627,0.0434076000960995);
#730=ELLIPSE('',#100630,0.0192307675628893,0.0124961950666526);
#731=ELLIPSE('',#100631,0.0192307675635299,0.0124961950671293);
#732=ELLIPSE('',#100648,0.0425526869747805,0.0390142882260044);
#733=ELLIPSE('',#100650,0.049632792841599,0.0434076000955309);
#734=ELLIPSE('',#100653,0.0192307675637578,0.0124961950673562);
#735=ELLIPSE('',#100654,0.0192307675639124,0.012496195067421);
#736=ELLIPSE('',#100671,0.0425526869743715,0.0390142882256719);
#737=ELLIPSE('',#100673,0.0496327928404835,0.043407600094977);
#738=ELLIPSE('',#100676,0.0192307675632384,0.012496195066941);
#739=ELLIPSE('',#100677,0.0192307675635312,0.0124961950671388);
#740=ELLIPSE('',#100694,0.0425526869740824,0.0390142882254308);
#741=ELLIPSE('',#100696,0.0496327928393061,0.0434076000944058);
#742=ELLIPSE('',#100699,0.019230767563583,0.0124961950672037);
#743=ELLIPSE('',#100700,0.0192307675632949,0.0124961950669026);
#744=ELLIPSE('',#100717,0.0425526869744841,0.0390142882257579);
#745=ELLIPSE('',#100719,0.0496327928399138,0.0434076000947192);
#746=ELLIPSE('',#100722,0.0192307675631686,0.0124961950668521);
#747=ELLIPSE('',#100723,0.0192307675635192,0.0124961950671158);
#748=ELLIPSE('',#100740,0.0425526869733499,0.0390142882248535);
#749=ELLIPSE('',#100742,0.0496327928401791,0.0434076000948666);
#750=ELLIPSE('',#100745,0.0192307675633233,0.0124961950669949);
#751=ELLIPSE('',#100746,0.0192307675638509,0.012496195067394);
#752=ELLIPSE('',#100763,0.0425526869753439,0.0390142882264477);
#753=ELLIPSE('',#100765,0.0496327928419698,0.0434076000956947);
#754=ELLIPSE('',#100768,0.0192307675639329,0.0124961950675036);
#755=ELLIPSE('',#100769,0.0192307675637545,0.0124961950673123);
#756=ELLIPSE('',#100786,0.0425526869744145,0.0390142882257717);
#757=ELLIPSE('',#100788,0.0496327928401159,0.0434076000948093);
#758=ELLIPSE('',#100791,0.0192307675636705,0.0124961950673185);
#759=ELLIPSE('',#100792,0.0192307675636708,0.0124961950672442);
#760=ELLIPSE('',#100809,0.0425526869732906,0.0390142882248623);
#761=ELLIPSE('',#100811,0.04963279284165,0.0434076000955818);
#762=ELLIPSE('',#100814,0.0192307675631284,0.012496195066834);
#763=ELLIPSE('',#100815,0.0192307675635161,0.012496195067104);
#764=ELLIPSE('',#100832,0.0425526869746155,0.0390142882259526);
#765=ELLIPSE('',#100834,0.0496327928399284,0.0434076000947457);
#766=ELLIPSE('',#100837,0.019230767563741,0.0124961950673528);
#767=ELLIPSE('',#100838,0.0192307675636219,0.0124961950671777);
#768=ELLIPSE('',#100855,0.0425526869749252,0.0390142882261626);
#769=ELLIPSE('',#100857,0.0496327928407413,0.0434076000951222);
#770=ELLIPSE('',#100860,0.0192307675635523,0.012496195067215);
#771=ELLIPSE('',#100861,0.0192307675633197,0.0124961950669376);
#772=ELLIPSE('',#100878,0.0425526869747909,0.0390142882260437);
#773=ELLIPSE('',#100880,0.0496327928410715,0.043407600095254);
#774=ELLIPSE('',#100883,0.0192307675635571,0.0124961950671645);
#775=ELLIPSE('',#100884,0.0192307675637541,0.0124961950673131);
#776=ELLIPSE('',#100901,0.0425526869737034,0.0390142882252059);
#777=ELLIPSE('',#100903,0.0496327928401919,0.0434076000948428);
#778=ELLIPSE('',#100906,0.0192307675631893,0.0124961950668821);
#779=ELLIPSE('',#100907,0.0192307675632753,0.0124961950669121);
#780=ELLIPSE('',#100924,0.0425526869745075,0.0390142882257448);
#781=ELLIPSE('',#100926,0.0496327928397759,0.0434076000946169);
#782=ELLIPSE('',#100929,0.0192307675634038,0.0124961950670969);
#783=ELLIPSE('',#100930,0.0192307675637935,0.0124961950673019);
#784=ELLIPSE('',#100947,0.0425526869742738,0.0390142882255607);
#785=ELLIPSE('',#100949,0.0496327928432332,0.0434076000963396);
#786=ELLIPSE('',#100952,0.0192307675634102,0.0124961950670913);
#787=ELLIPSE('',#100953,0.019230767563503,0.012496195067078);
#788=ELLIPSE('',#100970,0.0425526869742644,0.0390142882255844);
#789=ELLIPSE('',#100972,0.0496327928394013,0.043407600094468);
#790=ELLIPSE('',#100975,0.0192307675630013,0.0124961950667316);
#791=ELLIPSE('',#100976,0.0192307675636216,0.0124961950672165);
#792=ELLIPSE('',#100993,0.0425526869761727,0.0390142882271604);
#793=ELLIPSE('',#100995,0.0496327928412727,0.0434076000953756);
#794=ELLIPSE('',#100998,0.0192307675631514,0.0124961950668792);
#795=ELLIPSE('',#100999,0.019230767563722,0.0124961950672546);
#796=ELLIPSE('',#101016,0.0425526869747384,0.0390142882259681);
#797=ELLIPSE('',#101018,0.0496327928446237,0.0434076000970921);
#798=ELLIPSE('',#101021,0.0192307675632903,0.0124961950669737);
#799=ELLIPSE('',#101022,0.019230767563666,0.0124961950672293);
#800=ELLIPSE('',#101039,0.0425526869737097,0.0390142882251084);
#801=ELLIPSE('',#101041,0.0496327928425481,0.0434076000960501);
#802=ELLIPSE('',#101044,0.0192307675631588,0.0124961950668712);
#803=ELLIPSE('',#101045,0.0192307675640625,0.0124961950675836);
#804=ELLIPSE('',#101062,0.0425526869745639,0.0390142882258298);
#805=ELLIPSE('',#101064,0.0496327928409908,0.043407600095271);
#806=ELLIPSE('',#101067,0.0192307675634594,0.0124961950671047);
#807=ELLIPSE('',#101068,0.0192307675634831,0.0124961950671005);
#808=ELLIPSE('',#101085,0.0425526869762421,0.0390142882271955);
#809=ELLIPSE('',#101087,0.0496327928398201,0.0434076000947202);
#810=ELLIPSE('',#101090,0.0192307675634189,0.0124961950670756);
#811=ELLIPSE('',#101091,0.0192307675636712,0.0124961950672523);
#812=ELLIPSE('',#101108,0.0425526869751123,0.0390142882263016);
#813=ELLIPSE('',#101110,0.0496327928428975,0.0434076000961352);
#814=ELLIPSE('',#101113,0.0192307675638601,0.0124961950674287);
#815=ELLIPSE('',#101114,0.0192307675633655,0.0124961950669765);
#816=ELLIPSE('',#101131,0.042552686974957,0.039014288226131);
#817=ELLIPSE('',#101133,0.0496327928377014,0.0434076000936218);
#818=ELLIPSE('',#101136,0.0192307675633611,0.0124961950670825);
#819=ELLIPSE('',#101137,0.0192307675636668,0.0124961950672304);
#820=ELLIPSE('',#101154,0.0425526869741348,0.0390142882255173);
#821=ELLIPSE('',#101156,0.0496327928422112,0.0434076000958298);
#822=ELLIPSE('',#101159,0.0192307675636596,0.0124961950672704);
#823=ELLIPSE('',#101160,0.0192307675634132,0.0124961950670193);
#824=ELLIPSE('',#101177,0.0425526869757438,0.0390142882268549);
#825=ELLIPSE('',#101179,0.049632792839498,0.0434076000944692);
#826=ELLIPSE('',#101182,0.0192307675636907,0.0124961950673134);
#827=ELLIPSE('',#101183,0.0192307675632347,0.0124961950668581);
#828=ELLIPSE('',#101200,0.0425526869756515,0.0390142882267198);
#829=ELLIPSE('',#101202,0.0496327928408119,0.0434076000951749);
#830=ELLIPSE('',#101205,0.019230767563772,0.0124961950673667);
#831=ELLIPSE('',#101206,0.0192307675640002,0.0124961950674824);
#832=ELLIPSE('',#101223,0.0425526869742298,0.0390142882257123);
#833=ELLIPSE('',#101225,0.0496327928392884,0.0434076000944368);
#834=ELLIPSE('',#101228,0.0192307675638603,0.0124961950674543);
#835=ELLIPSE('',#101229,0.0192307675640063,0.0124961950675154);
#836=ELLIPSE('',#101246,0.0425526869754304,0.039014288226562);
#837=ELLIPSE('',#101248,0.0496327928399952,0.0434076000947494);
#838=ELLIPSE('',#101251,0.0192307675631104,0.0124961950668259);
#839=ELLIPSE('',#101252,0.0192307675637105,0.0124961950672723);
#840=ELLIPSE('',#101269,0.0425526869751533,0.0390142882263134);
#841=ELLIPSE('',#101271,0.0496327928434795,0.0434076000964837);
#842=ELLIPSE('',#101274,0.0192307675635219,0.012496195067161);
#843=ELLIPSE('',#101275,0.0192307675636582,0.0124961950672209);
#844=ELLIPSE('',#101292,0.0425526869738089,0.0390142882252893);
#845=ELLIPSE('',#101294,0.0496327928415335,0.0434076000954915);
#846=ELLIPSE('',#101297,0.0192307675636047,0.0124961950672229);
#847=ELLIPSE('',#101298,0.0192307675637509,0.0124961950672977);
#848=ELLIPSE('',#101315,0.0425526869748406,0.0390142882260696);
#849=ELLIPSE('',#101317,0.0496327928416895,0.0434076000955919);
#850=ELLIPSE('',#101320,0.0192307675636503,0.0124961950672501);
#851=ELLIPSE('',#101321,0.0192307675637744,0.0124961950673005);
#852=ELLIPSE('',#101338,0.0425526869748277,0.0390142882260173);
#853=ELLIPSE('',#101340,0.0496327928393208,0.0434076000944356);
#854=ELLIPSE('',#101343,0.019230767563307,0.0124961950669749);
#855=ELLIPSE('',#101344,0.0192307675635884,0.0124961950671878);
#856=ELLIPSE('',#101361,0.0425526869745431,0.0390142882258003);
#857=ELLIPSE('',#101363,0.049632792839495,0.0434076000945007);
#858=ELLIPSE('',#101366,0.0192307675636009,0.0124961950672421);
#859=ELLIPSE('',#101367,0.0192307675639625,0.0124961950674852);
#860=ELLIPSE('',#101384,0.0425526869740447,0.0390142882253699);
#861=ELLIPSE('',#101386,0.0496327928390667,0.043407600094334);
#862=ELLIPSE('',#101389,0.0192307675635503,0.012496195067186);
#863=ELLIPSE('',#101390,0.0192307675639065,0.0124961950674353);
#864=ELLIPSE('',#101407,0.042552686974613,0.0390142882258343);
#865=ELLIPSE('',#101409,0.0496327928417377,0.0434076000955981);
#866=ELLIPSE('',#101412,0.0192307675632349,0.0124961950669307);
#867=ELLIPSE('',#101413,0.0192307675636638,0.012496195067226);
#868=ELLIPSE('',#101430,0.0425526869746227,0.0390142882258163);
#869=ELLIPSE('',#101432,0.0496327928412397,0.043407600095381);
#870=ELLIPSE('',#101435,0.0192307675631595,0.0124961950668576);
#871=ELLIPSE('',#101436,0.019230767563481,0.012496195067064);
#872=ELLIPSE('',#101453,0.0425526869750388,0.0390142882262424);
#873=ELLIPSE('',#101455,0.0496327928405082,0.0434076000950075);
#874=ELLIPSE('',#101458,0.0192307675638917,0.0124961950674706);
#875=ELLIPSE('',#101459,0.0192307675638487,0.01249619506737);
#876=ELLIPSE('',#101476,0.0425526869741601,0.0390142882255349);
#877=ELLIPSE('',#101478,0.0496327928403301,0.0434076000948956);
#878=ELLIPSE('',#101481,0.0192307675637445,0.0124961950673484);
#879=ELLIPSE('',#101482,0.0192307675638341,0.0124961950673598);
#880=ELLIPSE('',#101499,0.0425526869743731,0.0390142882256932);
#881=ELLIPSE('',#101501,0.049632792839551,0.0434076000945117);
#882=ELLIPSE('',#101504,0.0192307675633938,0.0124961950670532);
#883=ELLIPSE('',#101505,0.0192307675634615,0.0124961950670706);
#884=ELLIPSE('',#101522,0.0425526869753327,0.0390142882265068);
#885=ELLIPSE('',#101524,0.0496327928392813,0.0434076000943744);
#886=ELLIPSE('',#101527,0.0192307675634685,0.0124961950671455);
#887=ELLIPSE('',#101528,0.0192307675636214,0.01249619506719);
#888=ELLIPSE('',#101545,0.0425526869753598,0.039014288226546);
#889=ELLIPSE('',#101547,0.0496327928418455,0.0434076000956737);
#890=ELLIPSE('',#101550,0.0192307675632718,0.0124961950669572);
#891=ELLIPSE('',#101551,0.0192307675635591,0.0124961950671161);
#892=ELLIPSE('',#101568,0.0425526869738626,0.0390142882253316);
#893=ELLIPSE('',#101570,0.0496327928412948,0.0434076000954059);
#894=ELLIPSE('',#101573,0.0192307675634556,0.0124961950670978);
#895=ELLIPSE('',#101574,0.0192307675636301,0.0124961950672015);
#896=ELLIPSE('',#101591,0.0425526869756818,0.0390142882267155);
#897=ELLIPSE('',#101593,0.0496327928431759,0.0434076000963139);
#898=ELLIPSE('',#101596,0.0192307675635293,0.0124961950671862);
#899=ELLIPSE('',#101597,0.0192307675636501,0.0124961950672362);
#900=ELLIPSE('',#101614,0.0425526869746175,0.0390142882259505);
#901=ELLIPSE('',#101616,0.049632792837045,0.0434076000933051);
#902=ELLIPSE('',#101619,0.0192307675633792,0.0124961950670546);
#903=ELLIPSE('',#101620,0.0192307675635501,0.0124961950671421);
#904=ELLIPSE('',#101637,0.0425526869752923,0.0390142882263946);
#905=ELLIPSE('',#101639,0.0496327928408134,0.0434076000951231);
#906=ELLIPSE('',#101642,0.0192307675636319,0.0124961950672612);
#907=ELLIPSE('',#101643,0.0192307675636181,0.0124961950671656);
#908=ELLIPSE('',#101660,0.0425526869742864,0.0390142882256438);
#909=ELLIPSE('',#101662,0.0496327928417663,0.0434076000956443);
#910=ELLIPSE('',#101665,0.0192307675637982,0.012496195067383);
#911=ELLIPSE('',#101666,0.0192307675638904,0.012496195067438);
#912=ELLIPSE('',#101683,0.0425526869752358,0.0390142882264552);
#913=ELLIPSE('',#101685,0.0496327928396165,0.0434076000945633);
#914=ELLIPSE('',#101688,0.019230767563197,0.0124961950669256);
#915=ELLIPSE('',#101689,0.0192307675639446,0.0124961950674674);
#916=ELLIPSE('',#101706,0.0425526869754807,0.0390142882265653);
#917=ELLIPSE('',#101708,0.0496327928408132,0.0434076000951034);
#918=ELLIPSE('',#101711,0.0192307675635509,0.0124961950671871);
#919=ELLIPSE('',#101712,0.0192307675641415,0.0124961950676206);
#920=ELLIPSE('',#101729,0.0425526869749276,0.0390142882262301);
#921=ELLIPSE('',#101731,0.0496327928440629,0.0434076000967274);
#922=ELLIPSE('',#101734,0.019230767563645,0.0124961950672504);
#923=ELLIPSE('',#101735,0.0192307675638628,0.0124961950674008);
#924=ELLIPSE('',#101752,0.0425526869745453,0.0390142882258204);
#925=ELLIPSE('',#101754,0.0496327928416776,0.0434076000955951);
#926=ELLIPSE('',#101757,0.0192307675636142,0.0124961950672563);
#927=ELLIPSE('',#101758,0.0192307675632203,0.0124961950668388);
#928=ELLIPSE('',#101775,0.0425526869749915,0.0390142882261663);
#929=ELLIPSE('',#101777,0.0496327928438602,0.0434076000966784);
#930=ELLIPSE('',#101780,0.0192307675633165,0.0124961950669919);
#931=ELLIPSE('',#101781,0.01923076756384,0.0124961950673881);
#932=ELLIPSE('',#101798,0.0425526869744079,0.0390142882256586);
#933=ELLIPSE('',#101800,0.0496327928408126,0.0434076000951567);
#934=ELLIPSE('',#101803,0.0192307675637739,0.0124961950674063);
#935=ELLIPSE('',#101804,0.0192307675637082,0.0124961950672627);
#936=ELLIPSE('',#101821,0.0425526869734033,0.0390142882248949);
#937=ELLIPSE('',#101823,0.0496327928401318,0.0434076000948125);
#938=ELLIPSE('',#101826,0.0192307675635592,0.0124961950672023);
#939=ELLIPSE('',#101827,0.0192307675639849,0.0124961950674855);
#940=ELLIPSE('',#101844,0.042552686975287,0.0390142882264506);
#941=ELLIPSE('',#101846,0.0496327928407087,0.043407600095097);
#942=ELLIPSE('',#101849,0.0192307675633303,0.0124961950670066);
#943=ELLIPSE('',#101850,0.0192307675633735,0.0124961950670145);
#944=ELLIPSE('',#101867,0.0425526869737294,0.0390142882251553);
#945=ELLIPSE('',#101869,0.0496327928412784,0.0434076000953894);
#946=ELLIPSE('',#101872,0.0192307675636036,0.0124961950672486);
#947=ELLIPSE('',#101873,0.0192307675637504,0.0124961950672888);
#948=ELLIPSE('',#101890,0.0425526869748891,0.039014288226071);
#949=ELLIPSE('',#101892,0.0496327928397892,0.0434076000946233);
#950=ELLIPSE('',#101895,0.0192307675635607,0.0124961950671772);
#951=ELLIPSE('',#101896,0.0192307675637951,0.0124961950673368);
#952=ELLIPSE('',#101913,0.0425526869755134,0.0390142882265691);
#953=ELLIPSE('',#101915,0.0496327928419113,0.0434076000957154);
#954=ELLIPSE('',#101918,0.0192307675634443,0.0124961950671131);
#955=ELLIPSE('',#101919,0.0192307675636348,0.0124961950672014);
#956=ELLIPSE('',#101936,0.042552686974117,0.0390142882255079);
#957=ELLIPSE('',#101938,0.0496327928414422,0.0434076000954564);
#958=ELLIPSE('',#101941,0.0192307675635264,0.0124961950671719);
#959=ELLIPSE('',#101942,0.0192307675631223,0.0124961950667821);
#960=ELLIPSE('',#101959,0.0425526869740302,0.0390142882253675);
#961=ELLIPSE('',#101961,0.049632792844195,0.0434076000968254);
#962=ELLIPSE('',#101964,0.0192307675632831,0.0124961950669592);
#963=ELLIPSE('',#101965,0.0192307675637101,0.0124961950672638);
#964=ELLIPSE('',#101982,0.0425526869744749,0.0390142882257445);
#965=ELLIPSE('',#101984,0.0496327928427934,0.0434076000960854);
#966=ELLIPSE('',#101987,0.0192307675634205,0.0124961950670957);
#967=ELLIPSE('',#101988,0.0192307675635492,0.012496195067125);
#968=ELLIPSE('',#102005,0.042552686973661,0.0390142882250711);
#969=ELLIPSE('',#102007,0.0496327928417467,0.0434076000956492);
#970=ELLIPSE('',#102010,0.0192307675638008,0.0124961950674073);
#971=ELLIPSE('',#102011,0.0192307675632246,0.0124961950668404);
#972=ELLIPSE('',#102028,0.0425526869754936,0.0390142882266065);
#973=ELLIPSE('',#102030,0.0496327928427154,0.0434076000961266);
#974=ELLIPSE('',#102033,0.0192307675637723,0.0124961950673811);
#975=ELLIPSE('',#102034,0.0192307675634061,0.0124961950670075);
#976=ELLIPSE('',#102051,0.0425526869745814,0.0390142882258619);
#977=ELLIPSE('',#102053,0.0496327928401041,0.0434076000948024);
#978=ELLIPSE('',#102056,0.0192307675635512,0.0124961950671918);
#979=ELLIPSE('',#102057,0.0192307675634758,0.0124961950670549);
#980=ELLIPSE('',#102074,0.0425526869738501,0.0390142882253079);
#981=ELLIPSE('',#102076,0.0496327928405524,0.0434076000950126);
#982=ELLIPSE('',#102079,0.0192307675632594,0.0124961950669426);
#983=ELLIPSE('',#102080,0.019230767563644,0.0124961950672196);
#984=ELLIPSE('',#102097,0.0425526869746686,0.0390142882259405);
#985=ELLIPSE('',#102099,0.0496327928412873,0.0434076000953856);
#986=ELLIPSE('',#102102,0.0192307675633519,0.0124961950670217);
#987=ELLIPSE('',#102103,0.0192307675635051,0.012496195067098);
#988=ELLIPSE('',#102120,0.0425526869738852,0.0390142882252857);
#989=ELLIPSE('',#102122,0.0496327928420414,0.0434076000957133);
#990=ELLIPSE('',#102125,0.0192307675637008,0.0124961950673219);
#991=ELLIPSE('',#102126,0.019230767563814,0.0124961950673542);
#992=ELLIPSE('',#102143,0.0425526869754299,0.0390142882265886);
#993=ELLIPSE('',#102145,0.0496327928386749,0.0434076000941317);
#994=ELLIPSE('',#102148,0.0192307675633133,0.0124961950669842);
#995=ELLIPSE('',#102149,0.0192307675636375,0.0124961950671983);
#996=ELLIPSE('',#102166,0.0425526869745743,0.0390142882257796);
#997=ELLIPSE('',#102168,0.0496327928421313,0.043407600095765);
#998=ELLIPSE('',#102171,0.0192307675631128,0.0124961950668294);
#999=ELLIPSE('',#102172,0.0192307675634278,0.0124961950670298);
#1000=ELLIPSE('',#102189,0.0425526869737158,0.0390142882251488);
#1001=ELLIPSE('',#102191,0.0496327928430415,0.0434076000962617);
#1002=ELLIPSE('',#102194,0.0192307675635778,0.0124961950672225);
#1003=ELLIPSE('',#102195,0.019230767563536,0.0124961950671344);
#1004=ELLIPSE('',#102212,0.0425526869745159,0.0390142882257335);
#1005=ELLIPSE('',#102214,0.0496327928416729,0.0434076000956114);
#1006=ELLIPSE('',#102217,0.0192307675629175,0.0124961950666397);
#1007=ELLIPSE('',#102218,0.0192307675639304,0.0124961950674491);
#1008=ELLIPSE('',#102235,0.0425526869749957,0.0390142882261683);
#1009=ELLIPSE('',#102237,0.0496327928395604,0.0434076000945359);
#1010=ELLIPSE('',#102240,0.0192307675634575,0.0124961950671176);
#1011=ELLIPSE('',#102241,0.0192307675637056,0.0124961950672668);
#1012=ELLIPSE('',#102258,0.0425526869750752,0.039014288226265);
#1013=ELLIPSE('',#102260,0.0496327928416145,0.0434076000955403);
#1014=ELLIPSE('',#102263,0.0192307675635318,0.0124961950671783);
#1015=ELLIPSE('',#102264,0.019230767563965,0.012496195067492);
#1016=ELLIPSE('',#102281,0.0425526869753011,0.0390142882264729);
#1017=ELLIPSE('',#102283,0.0496327928402229,0.0434076000948783);
#1018=ELLIPSE('',#102286,0.0192307675628003,0.0124961950665828);
#1019=ELLIPSE('',#102287,0.0192307675639499,0.0124961950674749);
#1020=ELLIPSE('',#102304,0.0425526869746192,0.0390142882259507);
#1021=ELLIPSE('',#102306,0.0496327928388132,0.0434076000941526);
#1022=ELLIPSE('',#102309,0.0192307675632284,0.0124961950669226);
#1023=ELLIPSE('',#102310,0.0192307675632992,0.0124961950669107);
#1024=ELLIPSE('',#102327,0.0425526869730377,0.0390142882245624);
#1025=ELLIPSE('',#102329,0.0496327928419789,0.0434076000957078);
#1026=ELLIPSE('',#102332,0.0192307675636472,0.012496195067296);
#1027=ELLIPSE('',#102333,0.0192307675638403,0.0124961950673552);
#1028=ELLIPSE('',#102350,0.0425526869748947,0.0390142882261328);
#1029=ELLIPSE('',#102352,0.0496327928390325,0.0434076000943003);
#1030=ELLIPSE('',#102355,0.0192307675634255,0.0124961950670811);
#1031=ELLIPSE('',#102356,0.0192307675635047,0.0124961950670899);
#1032=ELLIPSE('',#102373,0.0425526869747593,0.0390142882260281);
#1033=ELLIPSE('',#102375,0.0496327928439498,0.0434076000966843);
#1034=ELLIPSE('',#102378,0.0192307675631962,0.0124961950669167);
#1035=ELLIPSE('',#102379,0.0192307675637204,0.0124961950672605);
#1036=ELLIPSE('',#102396,0.0425526869755656,0.0390142882266576);
#1037=ELLIPSE('',#102398,0.0496327928402873,0.0434076000948886);
#1038=ELLIPSE('',#102401,0.0192307675633131,0.0124961950669589);
#1039=ELLIPSE('',#102402,0.0192307675637082,0.0124961950672744);
#1040=ELLIPSE('',#102419,0.0425526869745731,0.0390142882258727);
#1041=ELLIPSE('',#102421,0.0496327928400867,0.0434076000948188);
#1042=ELLIPSE('',#102424,0.0192307675635455,0.0124961950671794);
#1043=ELLIPSE('',#102425,0.0192307675635274,0.0124961950671071);
#1044=ELLIPSE('',#102442,0.0425526869749222,0.0390142882261123);
#1045=ELLIPSE('',#102444,0.0496327928431116,0.0434076000963298);
#1046=ELLIPSE('',#102447,0.0192307675635483,0.0124961950671917);
#1047=ELLIPSE('',#102448,0.0192307675640448,0.0124961950675534);
#1048=ELLIPSE('',#102465,0.0425526869742523,0.0390142882255338);
#1049=ELLIPSE('',#102467,0.0496327928418504,0.0434076000956289);
#1050=ELLIPSE('',#102470,0.0192307675635763,0.0124961950672184);
#1051=ELLIPSE('',#102471,0.0192307675639207,0.0124961950674505);
#1052=ELLIPSE('',#102488,0.0425526869744852,0.0390142882257258);
#1053=ELLIPSE('',#102490,0.0496327928436922,0.0434076000965822);
#1054=ELLIPSE('',#102493,0.0192307675635066,0.0124961950671226);
#1055=ELLIPSE('',#102494,0.0192307675639793,0.0124961950675183);
#1056=ELLIPSE('',#102511,0.0425526869738252,0.0390142882252166);
#1057=ELLIPSE('',#102513,0.0496327928419966,0.0434076000957468);
#1058=ELLIPSE('',#102516,0.0192307675630665,0.0124961950667913);
#1059=ELLIPSE('',#102517,0.0192307675639641,0.0124961950674707);
#1060=ELLIPSE('',#102534,0.0425526869765007,0.039014288227406);
#1061=ELLIPSE('',#102536,0.0496327928408136,0.0434076000951572);
#1062=ELLIPSE('',#102539,0.0192307675633216,0.012496195066993);
#1063=ELLIPSE('',#102540,0.0192307675635825,0.0124961950671522);
#1064=ELLIPSE('',#102557,0.0425526869734816,0.0390142882249933);
#1065=ELLIPSE('',#102559,0.0496327928387264,0.043407600094146);
#1066=ELLIPSE('',#102562,0.0192307675637256,0.012496195067343);
#1067=ELLIPSE('',#102563,0.0192307675635382,0.0124961950671278);
#1068=ELLIPSE('',#102580,0.0425526869735161,0.0390142882249432);
#1069=ELLIPSE('',#102582,0.0496327928400537,0.043407600094742);
#1070=ELLIPSE('',#102585,0.0192307675635381,0.0124961950671603);
#1071=ELLIPSE('',#102586,0.0192307675638612,0.0124961950674075);
#1072=ELLIPSE('',#102603,0.0425526869739921,0.0390142882253723);
#1073=ELLIPSE('',#102605,0.0496327928392701,0.0434076000943856);
#1074=ELLIPSE('',#102608,0.019230767563548,0.0124961950671943);
#1075=ELLIPSE('',#102609,0.0192307675638532,0.0124961950673877);
#1076=ELLIPSE('',#102626,0.0425526869752034,0.039014288226399);
#1077=ELLIPSE('',#102628,0.0496327928432613,0.0434076000963658);
#1078=ELLIPSE('',#102631,0.019230767563464,0.0124961950671191);
#1079=ELLIPSE('',#102632,0.0192307675637455,0.0124961950673029);
#1864=TOROIDAL_SURFACE('',#99456,1.625,0.125);
#1865=TOROIDAL_SURFACE('',#99468,2.50721825406948,0.0550000000000003);
#1866=TOROIDAL_SURFACE('',#99474,2.695,0.0550000000000007);
#1867=TOROIDAL_SURFACE('',#99677,2.50721825406948,0.0549999999999999);
#1868=TOROIDAL_SURFACE('',#100074,2.695,0.0550000000000003);
#1869=TOROIDAL_SURFACE('',#100077,2.695,0.0550000000000003);
#1870=TOROIDAL_SURFACE('',#100080,2.695,0.0550000000000003);
#1871=TOROIDAL_SURFACE('',#100083,2.695,0.0550000000000003);
#1872=TOROIDAL_SURFACE('',#100086,2.695,0.0550000000000003);
#1873=TOROIDAL_SURFACE('',#100089,2.695,0.0550000000000003);
#1874=TOROIDAL_SURFACE('',#100092,2.695,0.0550000000000003);
#1875=TOROIDAL_SURFACE('',#100095,2.695,0.0550000000000003);
#1876=TOROIDAL_SURFACE('',#100098,2.695,0.0550000000000003);
#1877=TOROIDAL_SURFACE('',#100101,2.695,0.0550000000000003);
#1878=TOROIDAL_SURFACE('',#100104,2.695,0.0550000000000003);
#1879=TOROIDAL_SURFACE('',#100107,2.695,0.0550000000000003);
#1880=TOROIDAL_SURFACE('',#100110,2.695,0.0550000000000003);
#1881=TOROIDAL_SURFACE('',#100113,2.695,0.0550000000000003);
#1882=TOROIDAL_SURFACE('',#100116,2.695,0.0550000000000003);
#1883=TOROIDAL_SURFACE('',#100119,2.695,0.0550000000000003);
#1884=TOROIDAL_SURFACE('',#100122,2.695,0.0550000000000003);
#1885=TOROIDAL_SURFACE('',#100125,2.695,0.0550000000000003);
#1886=TOROIDAL_SURFACE('',#100128,2.695,0.0550000000000003);
#1887=TOROIDAL_SURFACE('',#100131,2.695,0.0550000000000003);
#1888=TOROIDAL_SURFACE('',#100134,2.695,0.0550000000000003);
#1889=TOROIDAL_SURFACE('',#100137,2.695,0.0550000000000003);
#1890=TOROIDAL_SURFACE('',#100140,2.695,0.0550000000000003);
#1891=TOROIDAL_SURFACE('',#100143,2.695,0.0550000000000003);
#1892=TOROIDAL_SURFACE('',#100146,2.695,0.0550000000000003);
#1893=TOROIDAL_SURFACE('',#100149,2.695,0.0550000000000003);
#1894=TOROIDAL_SURFACE('',#100152,2.695,0.0550000000000003);
#1895=TOROIDAL_SURFACE('',#100155,2.695,0.0550000000000003);
#1896=TOROIDAL_SURFACE('',#100158,2.695,0.0550000000000003);
#1897=TOROIDAL_SURFACE('',#100161,2.695,0.0550000000000003);
#1898=TOROIDAL_SURFACE('',#100164,2.695,0.0550000000000003);
#1899=TOROIDAL_SURFACE('',#100167,2.695,0.0550000000000003);
#1900=TOROIDAL_SURFACE('',#100170,2.695,0.0550000000000003);
#1901=TOROIDAL_SURFACE('',#100173,2.695,0.0550000000000003);
#1902=TOROIDAL_SURFACE('',#100176,2.695,0.0550000000000003);
#1903=TOROIDAL_SURFACE('',#100179,2.695,0.0550000000000003);
#1904=TOROIDAL_SURFACE('',#100182,2.695,0.0550000000000003);
#1905=TOROIDAL_SURFACE('',#100185,2.695,0.0550000000000003);
#1906=TOROIDAL_SURFACE('',#100188,2.695,0.0550000000000003);
#1907=TOROIDAL_SURFACE('',#100191,2.695,0.0550000000000003);
#1908=TOROIDAL_SURFACE('',#100194,2.695,0.0550000000000003);
#1909=TOROIDAL_SURFACE('',#100197,2.695,0.0550000000000003);
#1910=TOROIDAL_SURFACE('',#100200,2.695,0.0550000000000003);
#1911=TOROIDAL_SURFACE('',#100203,2.695,0.0550000000000003);
#1912=TOROIDAL_SURFACE('',#100206,2.695,0.0550000000000003);
#1913=TOROIDAL_SURFACE('',#100209,2.695,0.0550000000000003);
#1914=TOROIDAL_SURFACE('',#100212,2.695,0.0550000000000003);
#1915=TOROIDAL_SURFACE('',#100215,2.695,0.0550000000000003);
#1916=TOROIDAL_SURFACE('',#100218,2.695,0.0550000000000003);
#1917=TOROIDAL_SURFACE('',#100221,2.695,0.0550000000000003);
#1918=TOROIDAL_SURFACE('',#100224,2.695,0.0550000000000003);
#1919=TOROIDAL_SURFACE('',#100227,2.695,0.0550000000000003);
#1920=TOROIDAL_SURFACE('',#100230,2.695,0.0550000000000003);
#1921=TOROIDAL_SURFACE('',#100233,2.695,0.0550000000000003);
#1922=TOROIDAL_SURFACE('',#100236,2.695,0.0550000000000003);
#1923=TOROIDAL_SURFACE('',#100239,2.695,0.0550000000000003);
#1924=TOROIDAL_SURFACE('',#100242,2.695,0.0550000000000003);
#1925=TOROIDAL_SURFACE('',#100245,2.695,0.0550000000000003);
#1926=TOROIDAL_SURFACE('',#100248,2.695,0.0550000000000003);
#1927=TOROIDAL_SURFACE('',#100251,2.695,0.0550000000000003);
#1928=TOROIDAL_SURFACE('',#100254,2.695,0.0550000000000003);
#1929=TOROIDAL_SURFACE('',#100257,2.695,0.0550000000000003);
#1930=TOROIDAL_SURFACE('',#100260,2.695,0.0550000000000003);
#1931=TOROIDAL_SURFACE('',#100263,2.695,0.0550000000000003);
#1932=TOROIDAL_SURFACE('',#100266,2.695,0.0550000000000003);
#1933=TOROIDAL_SURFACE('',#100269,2.695,0.0550000000000003);
#1934=TOROIDAL_SURFACE('',#100272,2.695,0.0550000000000003);
#1935=TOROIDAL_SURFACE('',#100275,2.695,0.0550000000000003);
#1936=TOROIDAL_SURFACE('',#100278,2.695,0.0550000000000003);
#1937=TOROIDAL_SURFACE('',#100281,2.695,0.0550000000000003);
#1938=TOROIDAL_SURFACE('',#100284,2.695,0.0550000000000003);
#1939=TOROIDAL_SURFACE('',#100287,2.695,0.0550000000000003);
#1940=TOROIDAL_SURFACE('',#100290,2.695,0.0550000000000003);
#1941=TOROIDAL_SURFACE('',#100293,2.695,0.0550000000000003);
#1942=TOROIDAL_SURFACE('',#100296,2.695,0.0550000000000003);
#1943=TOROIDAL_SURFACE('',#100299,2.695,0.0550000000000003);
#1944=TOROIDAL_SURFACE('',#100302,2.695,0.0550000000000003);
#1945=TOROIDAL_SURFACE('',#100305,2.695,0.0550000000000003);
#1946=TOROIDAL_SURFACE('',#100308,2.695,0.0550000000000003);
#1947=TOROIDAL_SURFACE('',#100311,2.695,0.0550000000000003);
#1948=TOROIDAL_SURFACE('',#100314,2.695,0.0550000000000003);
#1949=TOROIDAL_SURFACE('',#100317,2.695,0.0550000000000003);
#1950=TOROIDAL_SURFACE('',#100320,2.695,0.0550000000000003);
#1951=TOROIDAL_SURFACE('',#100323,2.695,0.0550000000000003);
#1952=TOROIDAL_SURFACE('',#100326,2.695,0.0550000000000003);
#1953=TOROIDAL_SURFACE('',#100329,2.695,0.0550000000000003);
#1954=TOROIDAL_SURFACE('',#100332,2.695,0.0550000000000003);
#1955=TOROIDAL_SURFACE('',#100335,2.695,0.0550000000000003);
#1956=TOROIDAL_SURFACE('',#100338,2.695,0.0550000000000003);
#1957=TOROIDAL_SURFACE('',#100341,2.695,0.0550000000000003);
#1958=TOROIDAL_SURFACE('',#100344,2.695,0.0550000000000003);
#1959=TOROIDAL_SURFACE('',#100347,2.695,0.0550000000000003);
#1960=TOROIDAL_SURFACE('',#100350,2.695,0.0550000000000003);
#1961=TOROIDAL_SURFACE('',#100353,2.695,0.0550000000000003);
#1962=TOROIDAL_SURFACE('',#100356,2.695,0.0550000000000003);
#1963=TOROIDAL_SURFACE('',#100359,2.695,0.0550000000000003);
#1964=TOROIDAL_SURFACE('',#100362,2.695,0.0550000000000003);
#1965=TOROIDAL_SURFACE('',#100382,2.695,0.0550000000000003);
#1966=TOROIDAL_SURFACE('',#100409,2.7375,0.0125);
#1967=TOROIDAL_SURFACE('',#100425,2.7375,0.0125);
#1968=TOROIDAL_SURFACE('',#100448,2.7375,0.0125);
#1969=TOROIDAL_SURFACE('',#100471,2.7375,0.0125);
#1970=TOROIDAL_SURFACE('',#100494,2.7375,0.0125);
#1971=TOROIDAL_SURFACE('',#100517,2.7375,0.0125);
#1972=TOROIDAL_SURFACE('',#100540,2.7375,0.0125);
#1973=TOROIDAL_SURFACE('',#100563,2.7375,0.0125);
#1974=TOROIDAL_SURFACE('',#100586,2.7375,0.0125);
#1975=TOROIDAL_SURFACE('',#100609,2.7375,0.0125);
#1976=TOROIDAL_SURFACE('',#100632,2.7375,0.0125);
#1977=TOROIDAL_SURFACE('',#100655,2.7375,0.0125);
#1978=TOROIDAL_SURFACE('',#100678,2.7375,0.0125);
#1979=TOROIDAL_SURFACE('',#100701,2.7375,0.0125);
#1980=TOROIDAL_SURFACE('',#100724,2.7375,0.0125);
#1981=TOROIDAL_SURFACE('',#100747,2.7375,0.0125);
#1982=TOROIDAL_SURFACE('',#100770,2.7375,0.0125);
#1983=TOROIDAL_SURFACE('',#100793,2.7375,0.0125);
#1984=TOROIDAL_SURFACE('',#100816,2.7375,0.0125);
#1985=TOROIDAL_SURFACE('',#100839,2.7375,0.0125);
#1986=TOROIDAL_SURFACE('',#100862,2.7375,0.0125);
#1987=TOROIDAL_SURFACE('',#100885,2.7375,0.0125);
#1988=TOROIDAL_SURFACE('',#100908,2.7375,0.0125);
#1989=TOROIDAL_SURFACE('',#100931,2.7375,0.0125);
#1990=TOROIDAL_SURFACE('',#100954,2.7375,0.0125);
#1991=TOROIDAL_SURFACE('',#100977,2.7375,0.0125);
#1992=TOROIDAL_SURFACE('',#101000,2.7375,0.0125);
#1993=TOROIDAL_SURFACE('',#101023,2.7375,0.0125);
#1994=TOROIDAL_SURFACE('',#101046,2.7375,0.0125);
#1995=TOROIDAL_SURFACE('',#101069,2.7375,0.0125);
#1996=TOROIDAL_SURFACE('',#101092,2.7375,0.0125);
#1997=TOROIDAL_SURFACE('',#101115,2.7375,0.0125);
#1998=TOROIDAL_SURFACE('',#101138,2.7375,0.0125);
#1999=TOROIDAL_SURFACE('',#101161,2.7375,0.0125);
#2000=TOROIDAL_SURFACE('',#101184,2.7375,0.0125);
#2001=TOROIDAL_SURFACE('',#101207,2.7375,0.0125);
#2002=TOROIDAL_SURFACE('',#101230,2.7375,0.0125);
#2003=TOROIDAL_SURFACE('',#101253,2.7375,0.0125);
#2004=TOROIDAL_SURFACE('',#101276,2.7375,0.0125);
#2005=TOROIDAL_SURFACE('',#101299,2.7375,0.0125);
#2006=TOROIDAL_SURFACE('',#101322,2.7375,0.0125);
#2007=TOROIDAL_SURFACE('',#101345,2.7375,0.0125);
#2008=TOROIDAL_SURFACE('',#101368,2.7375,0.0125);
#2009=TOROIDAL_SURFACE('',#101391,2.7375,0.0125);
#2010=TOROIDAL_SURFACE('',#101414,2.7375,0.0125);
#2011=TOROIDAL_SURFACE('',#101437,2.7375,0.0125);
#2012=TOROIDAL_SURFACE('',#101460,2.7375,0.0125);
#2013=TOROIDAL_SURFACE('',#101483,2.7375,0.0125);
#2014=TOROIDAL_SURFACE('',#101506,2.7375,0.0125);
#2015=TOROIDAL_SURFACE('',#101529,2.7375,0.0125);
#2016=TOROIDAL_SURFACE('',#101552,2.7375,0.0125);
#2017=TOROIDAL_SURFACE('',#101575,2.7375,0.0125);
#2018=TOROIDAL_SURFACE('',#101598,2.7375,0.0125);
#2019=TOROIDAL_SURFACE('',#101621,2.7375,0.0125);
#2020=TOROIDAL_SURFACE('',#101644,2.7375,0.0125);
#2021=TOROIDAL_SURFACE('',#101667,2.7375,0.0125);
#2022=TOROIDAL_SURFACE('',#101690,2.7375,0.0125);
#2023=TOROIDAL_SURFACE('',#101713,2.7375,0.0125);
#2024=TOROIDAL_SURFACE('',#101736,2.7375,0.0125);
#2025=TOROIDAL_SURFACE('',#101759,2.7375,0.0125);
#2026=TOROIDAL_SURFACE('',#101782,2.7375,0.0125);
#2027=TOROIDAL_SURFACE('',#101805,2.7375,0.0125);
#2028=TOROIDAL_SURFACE('',#101828,2.7375,0.0125);
#2029=TOROIDAL_SURFACE('',#101851,2.7375,0.0125);
#2030=TOROIDAL_SURFACE('',#101874,2.7375,0.0125);
#2031=TOROIDAL_SURFACE('',#101897,2.7375,0.0125);
#2032=TOROIDAL_SURFACE('',#101920,2.7375,0.0125);
#2033=TOROIDAL_SURFACE('',#101943,2.7375,0.0125);
#2034=TOROIDAL_SURFACE('',#101966,2.7375,0.0125);
#2035=TOROIDAL_SURFACE('',#101989,2.7375,0.0125);
#2036=TOROIDAL_SURFACE('',#102012,2.7375,0.0125);
#2037=TOROIDAL_SURFACE('',#102035,2.7375,0.0125);
#2038=TOROIDAL_SURFACE('',#102058,2.7375,0.0125);
#2039=TOROIDAL_SURFACE('',#102081,2.7375,0.0125);
#2040=TOROIDAL_SURFACE('',#102104,2.7375,0.0125);
#2041=TOROIDAL_SURFACE('',#102127,2.7375,0.0125);
#2042=TOROIDAL_SURFACE('',#102150,2.7375,0.0125);
#2043=TOROIDAL_SURFACE('',#102173,2.7375,0.0125);
#2044=TOROIDAL_SURFACE('',#102196,2.7375,0.0125);
#2045=TOROIDAL_SURFACE('',#102219,2.7375,0.0125);
#2046=TOROIDAL_SURFACE('',#102242,2.7375,0.0125);
#2047=TOROIDAL_SURFACE('',#102265,2.7375,0.0125);
#2048=TOROIDAL_SURFACE('',#102288,2.7375,0.0125);
#2049=TOROIDAL_SURFACE('',#102311,2.7375,0.0125);
#2050=TOROIDAL_SURFACE('',#102334,2.7375,0.0125);
#2051=TOROIDAL_SURFACE('',#102357,2.7375,0.0125);
#2052=TOROIDAL_SURFACE('',#102380,2.7375,0.0125);
#2053=TOROIDAL_SURFACE('',#102403,2.7375,0.0125);
#2054=TOROIDAL_SURFACE('',#102426,2.7375,0.0125);
#2055=TOROIDAL_SURFACE('',#102449,2.7375,0.0125);
#2056=TOROIDAL_SURFACE('',#102472,2.7375,0.0125);
#2057=TOROIDAL_SURFACE('',#102495,2.7375,0.0125);
#2058=TOROIDAL_SURFACE('',#102518,2.7375,0.0125);
#2059=TOROIDAL_SURFACE('',#102541,2.7375,0.0125);
#2060=TOROIDAL_SURFACE('',#102564,2.7375,0.0125);
#2061=TOROIDAL_SURFACE('',#102587,2.7375,0.0125);
#2062=TOROIDAL_SURFACE('',#102610,2.7375,0.0125);
#2063=TOROIDAL_SURFACE('',#102633,2.7375,0.0125);
#2319=(
BOUNDED_SURFACE()
B_SPLINE_SURFACE(1,2,((#378429,#378430,#378431,#378432,#378433,#378434,
#378435,#378436,#378437,#378438,#378439,#378440,#378441,#378442,#378443,
#378444,#378445,#378446,#378447,#378448,#378449,#378450,#378451,#378452,
#378453,#378454,#378455,#378456,#378457,#378458,#378459,#378460,#378461,
#378462,#378463,#378464,#378465,#378466,#378467,#378468,#378469,#378470,
#378471,#378472,#378473,#378474,#378475,#378476,#378477,#378478,#378479,
#378480,#378481,#378482,#378483,#378484,#378485,#378486,#378487,#378488,
#378489,#378490,#378491,#378492,#378493,#378494,#378495,#378496,#378497,
#378498,#378499,#378500,#378501,#378502,#378503,#378504,#378505,#378506,
#378507,#378508,#378509,#378510,#378511,#378512,#378513,#378514,#378515,
#378516,#378517,#378518,#378519,#378520,#378521,#378522,#378523,#378524,
#378525,#378526,#378527,#378528,#378529,#378530,#378531,#378532,#378533,
#378534,#378535,#378536,#378537,#378538,#378539,#378540,#378541,#378542,
#378543,#378544,#378545,#378546,#378547,#378548,#378549,#378550,#378551,
#378552,#378553,#378554,#378555,#378556,#378557,#378558,#378559,#378560,
#378561,#378562,#378563,#378564,#378565,#378566,#378567,#378568,#378569,
#378570,#378571,#378572,#378573,#378574,#378575,#378576,#378577,#378578,
#378579,#378580,#378581,#378582,#378583,#378584,#378585,#378586,#378587,
#378588,#378589,#378590,#378591,#378592,#378593,#378594,#378595,#378596,
#378597,#378598,#378599,#378600,#378601,#378602,#378603,#378604,#378605,
#378606,#378607,#378608,#378609,#378610,#378611,#378612,#378613,#378614,
#378615,#378616,#378617,#378618,#378619,#378620,#378621,#378622,#378623,
#378624,#378625,#378626,#378627,#378628,#378629,#378630,#378631,#378632,
#378633,#378634,#378635,#378636,#378637,#378638,#378639,#378640,#378641,
#378642,#378643,#378644,#378645,#378646,#378647,#378648,#378649,#378650,
#378651,#378652,#378653,#378654,#378655,#378656,#378657,#378658,#378659,
#378660,#378661,#378662,#378663,#378664,#378665,#378666,#378667,#378668,
#378669,#378670,#378671,#378672,#378673,#378674,#378675,#378676,#378677,
#378678,#378679,#378680,#378681,#378682,#378683,#378684,#378685,#378686,
#378687,#378688,#378689,#378690,#378691,#378692,#378693,#378694,#378695,
#378696,#378697,#378698,#378699,#378700,#378701,#378702,#378703,#378704,
#378705,#378706,#378707,#378708,#378709,#378710,#378711,#378712,#378713,
#378714,#378715,#378716,#378717,#378718,#378719,#378720,#378721,#378722,
#378723,#378724,#378725,#378726,#378727,#378728,#378729,#378730,#378731,
#378732,#378733,#378734,#378735,#378736,#378737,#378738,#378739,#378740,
#378741,#378742,#378743,#378744,#378745,#378746,#378747,#378748,#378749,
#378750,#378751,#378752,#378753,#378754,#378755,#378756,#378757,#378758,
#378759,#378760,#378761,#378762,#378763,#378764,#378765,#378766,#378767,
#378768,#378769,#378770,#378771,#378772,#378773,#378774,#378775,#378776,
#378777,#378778,#378779,#378780,#378781,#378782,#378783,#378784,#378785,
#378786,#378787,#378788,#378789,#378790,#378791,#378792,#378793,#378794,
#378795,#378796,#378797,#378798,#378799,#378800,#378801),(#378802,#378803,
#378804,#378805,#378806,#378807,#378808,#378809,#378810,#378811,#378812,
#378813,#378814,#378815,#378816,#378817,#378818,#378819,#378820,#378821,
#378822,#378823,#378824,#378825,#378826,#378827,#378828,#378829,#378830,
#378831,#378832,#378833,#378834,#378835,#378836,#378837,#378838,#378839,
#378840,#378841,#378842,#378843,#378844,#378845,#378846,#378847,#378848,
#378849,#378850,#378851,#378852,#378853,#378854,#378855,#378856,#378857,
#378858,#378859,#378860,#378861,#378862,#378863,#378864,#378865,#378866,
#378867,#378868,#378869,#378870,#378871,#378872,#378873,#378874,#378875,
#378876,#378877,#378878,#378879,#378880,#378881,#378882,#378883,#378884,
#378885,#378886,#378887,#378888,#378889,#378890,#378891,#378892,#378893,
#378894,#378895,#378896,#378897,#378898,#378899,#378900,#378901,#378902,
#378903,#378904,#378905,#378906,#378907,#378908,#378909,#378910,#378911,
#378912,#378913,#378914,#378915,#378916,#378917,#378918,#378919,#378920,
#378921,#378922,#378923,#378924,#378925,#378926,#378927,#378928,#378929,
#378930,#378931,#378932,#378933,#378934,#378935,#378936,#378937,#378938,
#378939,#378940,#378941,#378942,#378943,#378944,#378945,#378946,#378947,
#378948,#378949,#378950,#378951,#378952,#378953,#378954,#378955,#378956,
#378957,#378958,#378959,#378960,#378961,#378962,#378963,#378964,#378965,
#378966,#378967,#378968,#378969,#378970,#378971,#378972,#378973,#378974,
#378975,#378976,#378977,#378978,#378979,#378980,#378981,#378982,#378983,
#378984,#378985,#378986,#378987,#378988,#378989,#378990,#378991,#378992,
#378993,#378994,#378995,#378996,#378997,#378998,#378999,#379000,#379001,
#379002,#379003,#379004,#379005,#379006,#379007,#379008,#379009,#379010,
#379011,#379012,#379013,#379014,#379015,#379016,#379017,#379018,#379019,
#379020,#379021,#379022,#379023,#379024,#379025,#379026,#379027,#379028,
#379029,#379030,#379031,#379032,#379033,#379034,#379035,#379036,#379037,
#379038,#379039,#379040,#379041,#379042,#379043,#379044,#379045,#379046,
#379047,#379048,#379049,#379050,#379051,#379052,#379053,#379054,#379055,
#379056,#379057,#379058,#379059,#379060,#379061,#379062,#379063,#379064,
#379065,#379066,#379067,#379068,#379069,#379070,#379071,#379072,#379073,
#379074,#379075,#379076,#379077,#379078,#379079,#379080,#379081,#379082,
#379083,#379084,#379085,#379086,#379087,#379088,#379089,#379090,#379091,
#379092,#379093,#379094,#379095,#379096,#379097,#379098,#379099,#379100,
#379101,#379102,#379103,#379104,#379105,#379106,#379107,#379108,#379109,
#379110,#379111,#379112,#379113,#379114,#379115,#379116,#379117,#379118,
#379119,#379120,#379121,#379122,#379123,#379124,#379125,#379126,#379127,
#379128,#379129,#379130,#379131,#379132,#379133,#379134,#379135,#379136,
#379137,#379138,#379139,#379140,#379141,#379142,#379143,#379144,#379145,
#379146,#379147,#379148,#379149,#379150,#379151,#379152,#379153,#379154,
#379155,#379156,#379157,#379158,#379159,#379160,#379161,#379162,#379163,
#379164,#379165,#379166,#379167,#379168,#379169,#379170,#379171,#379172,
#379173,#379174)),.UNSPECIFIED.,.F.,.F.,.F.)
B_SPLINE_SURFACE_WITH_KNOTS((2,2),(3,2,2,2,2,2,2,2,2,2,2,2,2,2,2,2,2,2,
2,2,2,2,2,2,2,2,2,2,2,2,2,2,2,2,2,2,2,2,2,2,2,2,2,2,2,2,2,2,2,2,2,2,2,2,
2,2,2,2,2,2,2,2,2,2,2,2,2,2,2,2,2,2,2,2,2,2,2,2,2,2,2,2,2,2,2,2,2,2,2,2,
2,2,2,2,2,2,2,2,2,2,2,2,2,2,2,2,2,2,2,2,2,2,2,2,2,2,2,2,2,2,2,2,2,2,2,2,
2,2,2,2,2,2,2,2,2,2,2,2,2,2,2,2,2,2,2,2,2,2,2,2,2,2,2,2,2,2,2,2,2,2,2,2,
2,2,2,2,2,2,2,2,2,2,2,2,2,2,2,2,2,2,2,2,2,2,2,2,3),(0.,1.),(0.,0.00537634408602151,
0.010752688172043,0.0161290322580645,0.021505376344086,0.0268817204301075,
0.032258064516129,0.0376344086021505,0.043010752688172,0.0483870967741935,
0.0537634408602151,0.0591397849462366,0.0645161290322581,0.0698924731182796,
0.0752688172043011,0.0806451612903226,0.0860215053763441,0.0913978494623656,
0.0967741935483871,0.102150537634409,0.10752688172043,0.112903225806452,
0.118279569892473,0.123655913978495,0.129032258064516,0.134408602150538,
0.139784946236559,0.145161290322581,0.150537634408602,0.155913978494624,
0.161290322580645,0.166666666666667,0.172043010752688,0.17741935483871,
0.182795698924731,0.188172043010753,0.193548387096774,0.198924731182796,
0.204301075268817,0.209677419354839,0.21505376344086,0.220430107526882,
0.225806451612903,0.231182795698925,0.236559139784946,0.241935483870968,
0.247311827956989,0.252688172043011,0.258064516129032,0.263440860215054,
0.268817204301075,0.274193548387097,0.279569892473118,0.28494623655914,
0.290322580645161,0.295698924731183,0.301075268817204,0.306451612903226,
0.311827956989247,0.317204301075269,0.32258064516129,0.327956989247312,
0.333333333333333,0.338709677419355,0.344086021505376,0.349462365591398,
0.354838709677419,0.360215053763441,0.365591397849462,0.370967741935484,
0.376344086021505,0.381720430107527,0.387096774193548,0.39247311827957,
0.397849462365591,0.403225806451613,0.408602150537634,0.413978494623656,
0.419354838709677,0.424731182795699,0.43010752688172,0.435483870967742,
0.440860215053763,0.446236559139785,0.451612903225806,0.456989247311828,
0.462365591397849,0.467741935483871,0.473118279569892,0.478494623655914,
0.483870967741935,0.489247311827957,0.494623655913978,0.5,0.505376344086022,
0.510752688172043,0.516129032258065,0.521505376344086,0.526881720430108,
0.532258064516129,0.537634408602151,0.543010752688172,0.548387096774194,
0.553763440860215,0.559139784946237,0.564516129032258,0.56989247311828,
0.575268817204301,0.580645161290323,0.586021505376344,0.591397849462366,
0.596774193548387,0.602150537634409,0.60752688172043,0.612903225806452,
0.618279569892473,0.623655913978495,0.629032258064516,0.634408602150538,
0.639784946236559,0.645161290322581,0.650537634408602,0.655913978494624,
0.661290322580645,0.666666666666667,0.672043010752688,0.67741935483871,
0.682795698924731,0.688172043010753,0.693548387096774,0.698924731182796,
0.704301075268817,0.709677419354839,0.71505376344086,0.720430107526882,
0.725806451612903,0.731182795698925,0.736559139784946,0.741935483870968,
0.747311827956989,0.752688172043011,0.758064516129032,0.763440860215054,
0.768817204301075,0.774193548387097,0.779569892473118,0.78494623655914,
0.790322580645161,0.795698924731183,0.801075268817204,0.806451612903226,
0.811827956989247,0.817204301075269,0.82258064516129,0.827956989247312,
0.833333333333333,0.838709677419355,0.844086021505376,0.849462365591398,
0.854838709677419,0.860215053763441,0.865591397849462,0.870967741935484,
0.876344086021505,0.881720430107527,0.887096774193548,0.89247311827957,
0.897849462365591,0.903225806451613,0.908602150537634,0.913978494623656,
0.919354838709677,0.924731182795699,0.93010752688172,0.935483870967742,
0.940860215053763,0.946236559139785,0.951612903225806,0.956989247311828,
0.962365591397849,0.967741935483871,0.973118279569892,0.978494623655914,
0.983870967741935,0.989247311827957,0.994623655913978,1.),.UNSPECIFIED.)
GEOMETRIC_REPRESENTATION_ITEM()
RATIONAL_B_SPLINE_SURFACE(((1.,0.866025403784439,1.,0.866025403784439,1.,
0.866025403784439,1.,0.866025403784439,1.,0.866025403784439,1.,0.866025403784439,
1.,0.866025403784439,1.,0.866025403784439,1.,0.866025403784439,1.,0.866025403784439,
1.,0.866025403784439,1.,0.866025403784439,1.,0.866025403784439,1.,0.866025403784439,
1.,0.866025403784439,1.,0.866025403784439,1.,0.866025403784439,1.,0.866025403784439,
1.,0.866025403784439,1.,0.866025403784439,1.,0.866025403784439,1.,0.866025403784439,
1.,0.866025403784439,1.,0.866025403784439,1.,0.866025403784439,1.,0.866025403784439,
1.,0.866025403784439,1.,0.866025403784439,1.,0.866025403784439,1.,0.866025403784439,
1.,0.866025403784439,1.,0.866025403784439,1.,0.866025403784439,1.,0.866025403784439,
1.,0.866025403784439,1.,0.866025403784439,1.,0.866025403784439,1.,0.866025403784439,
1.,0.866025403784439,1.,0.866025403784439,1.,0.866025403784439,1.,0.866025403784439,
1.,0.866025403784439,1.,0.866025403784439,1.,0.866025403784439,1.,0.866025403784439,
1.,0.866025403784439,1.,0.866025403784439,1.,0.866025403784439,1.,0.866025403784439,
1.,0.866025403784439,1.,0.866025403784439,1.,0.866025403784439,1.,0.866025403784439,
1.,0.866025403784439,1.,0.866025403784439,1.,0.866025403784439,1.,0.866025403784439,
1.,0.866025403784439,1.,0.866025403784439,1.,0.866025403784439,1.,0.866025403784439,
1.,0.866025403784439,1.,0.866025403784439,1.,0.866025403784439,1.,0.866025403784439,
1.,0.866025403784439,1.,0.866025403784439,1.,0.866025403784439,1.,0.866025403784439,
1.,0.866025403784439,1.,0.866025403784439,1.,0.866025403784439,1.,0.866025403784439,
1.,0.866025403784439,1.,0.866025403784439,1.,0.866025403784439,1.,0.866025403784439,
1.,0.866025403784439,1.,0.866025403784439,1.,0.866025403784439,1.,0.866025403784439,
1.,0.866025403784439,1.,0.866025403784439,1.,0.866025403784439,1.,0.866025403784439,
1.,0.866025403784439,1.,0.866025403784439,1.,0.866025403784439,1.,0.866025403784439,
1.,0.866025403784439,1.,0.866025403784439,1.,0.866025403784439,1.,0.866025403784439,
1.,0.866025403784439,1.,0.866025403784439,1.,0.866025403784439,1.,0.866025403784439,
1.,0.866025403784439,1.,0.866025403784439,1.,0.866025403784439,1.,0.866025403784439,
1.,0.866025403784439,1.,0.866025403784439,1.,0.866025403784439,1.,0.866025403784439,
1.,0.866025403784439,1.,0.866025403784439,1.,0.866025403784439,1.,0.866025403784439,
1.,0.866025403784439,1.,0.866025403784439,1.,0.866025403784439,1.,0.866025403784439,
1.,0.866025403784439,1.,0.866025403784439,1.,0.866025403784439,1.,0.866025403784439,
1.,0.866025403784439,1.,0.866025403784439,1.,0.866025403784439,1.,0.866025403784439,
1.,0.866025403784439,1.,0.866025403784439,1.,0.866025403784439,1.,0.866025403784439,
1.,0.866025403784439,1.,0.866025403784439,1.,0.866025403784439,1.,0.866025403784439,
1.,0.866025403784439,1.,0.866025403784439,1.,0.866025403784439,1.,0.866025403784439,
1.,0.866025403784439,1.,0.866025403784439,1.,0.866025403784439,1.,0.866025403784439,
1.,0.866025403784439,1.,0.866025403784439,1.,0.866025403784439,1.,0.866025403784439,
1.,0.866025403784439,1.,0.866025403784439,1.,0.866025403784439,1.,0.866025403784439,
1.,0.866025403784439,1.,0.866025403784439,1.,0.866025403784439,1.,0.866025403784439,
1.,0.866025403784439,1.,0.866025403784439,1.,0.866025403784439,1.,0.866025403784439,
1.,0.866025403784439,1.,0.866025403784439,1.,0.866025403784439,1.,0.866025403784439,
1.,0.866025403784439,1.,0.866025403784439,1.,0.866025403784439,1.,0.866025403784439,
1.,0.866025403784439,1.,0.866025403784439,1.,0.866025403784439,1.,0.866025403784439,
1.,0.866025403784439,1.,0.866025403784439,1.,0.866025403784439,1.,0.866025403784439,
1.,0.866025403784439,1.,0.866025403784439,1.,0.866025403784439,1.,0.866025403784439,
1.,0.866025403784439,1.,0.866025403784439,1.,0.866025403784439,1.,0.866025403784439,
1.,0.866025403784439,1.,0.866025403784439,1.,0.866025403784439,1.,0.866025403784439,
1.,0.866025403784439,1.,0.866025403784439,1.,0.866025403784439,1.,0.866025403784439,
1.),(1.,0.866025403784439,1.,0.866025403784439,1.,0.866025403784439,1.,
0.866025403784439,1.,0.866025403784439,1.,0.866025403784439,1.,0.866025403784439,
1.,0.866025403784439,1.,0.866025403784439,1.,0.866025403784439,1.,0.866025403784439,
1.,0.866025403784439,1.,0.866025403784439,1.,0.866025403784439,1.,0.866025403784439,
1.,0.866025403784439,1.,0.866025403784439,1.,0.866025403784439,1.,0.866025403784439,
1.,0.866025403784439,1.,0.866025403784439,1.,0.866025403784439,1.,0.866025403784439,
1.,0.866025403784439,1.,0.866025403784439,1.,0.866025403784439,1.,0.866025403784439,
1.,0.866025403784439,1.,0.866025403784439,1.,0.866025403784439,1.,0.866025403784439,
1.,0.866025403784439,1.,0.866025403784439,1.,0.866025403784439,1.,0.866025403784439,
1.,0.866025403784439,1.,0.866025403784439,1.,0.866025403784439,1.,0.866025403784439,
1.,0.866025403784439,1.,0.866025403784439,1.,0.866025403784439,1.,0.866025403784439,
1.,0.866025403784439,1.,0.866025403784439,1.,0.866025403784439,1.,0.866025403784439,
1.,0.866025403784439,1.,0.866025403784439,1.,0.866025403784439,1.,0.866025403784439,
1.,0.866025403784439,1.,0.866025403784439,1.,0.866025403784439,1.,0.866025403784439,
1.,0.866025403784439,1.,0.866025403784439,1.,0.866025403784439,1.,0.866025403784439,
1.,0.866025403784439,1.,0.866025403784439,1.,0.866025403784439,1.,0.866025403784439,
1.,0.866025403784439,1.,0.866025403784439,1.,0.866025403784439,1.,0.866025403784439,
1.,0.866025403784439,1.,0.866025403784439,1.,0.866025403784439,1.,0.866025403784439,
1.,0.866025403784439,1.,0.866025403784439,1.,0.866025403784439,1.,0.866025403784439,
1.,0.866025403784439,1.,0.866025403784439,1.,0.866025403784439,1.,0.866025403784439,
1.,0.866025403784439,1.,0.866025403784439,1.,0.866025403784439,1.,0.866025403784439,
1.,0.866025403784439,1.,0.866025403784439,1.,0.866025403784439,1.,0.866025403784439,
1.,0.866025403784439,1.,0.866025403784439,1.,0.866025403784439,1.,0.866025403784439,
1.,0.866025403784439,1.,0.866025403784439,1.,0.866025403784439,1.,0.866025403784439,
1.,0.866025403784439,1.,0.866025403784439,1.,0.866025403784439,1.,0.866025403784439,
1.,0.866025403784439,1.,0.866025403784439,1.,0.866025403784439,1.,0.866025403784439,
1.,0.866025403784439,1.,0.866025403784439,1.,0.866025403784439,1.,0.866025403784439,
1.,0.866025403784439,1.,0.866025403784439,1.,0.866025403784439,1.,0.866025403784439,
1.,0.866025403784439,1.,0.866025403784439,1.,0.866025403784439,1.,0.866025403784439,
1.,0.866025403784439,1.,0.866025403784439,1.,0.866025403784439,1.,0.866025403784439,
1.,0.866025403784439,1.,0.866025403784439,1.,0.866025403784439,1.,0.866025403784439,
1.,0.866025403784439,1.,0.866025403784439,1.,0.866025403784439,1.,0.866025403784439,
1.,0.866025403784439,1.,0.866025403784439,1.,0.866025403784439,1.,0.866025403784439,
1.,0.866025403784439,1.,0.866025403784439,1.,0.866025403784439,1.,0.866025403784439,
1.,0.866025403784439,1.,0.866025403784439,1.,0.866025403784439,1.,0.866025403784439,
1.,0.866025403784439,1.,0.866025403784439,1.,0.866025403784439,1.,0.866025403784439,
1.,0.866025403784439,1.,0.866025403784439,1.,0.866025403784439,1.,0.866025403784439,
1.,0.866025403784439,1.,0.866025403784439,1.,0.866025403784439,1.,0.866025403784439,
1.,0.866025403784439,1.,0.866025403784439,1.,0.866025403784439,1.,0.866025403784439,
1.,0.866025403784439,1.,0.866025403784439,1.,0.866025403784439,1.,0.866025403784439,
1.,0.866025403784439,1.,0.866025403784439,1.,0.866025403784439,1.,0.866025403784439,
1.,0.866025403784439,1.,0.866025403784439,1.,0.866025403784439,1.,0.866025403784439,
1.,0.866025403784439,1.,0.866025403784439,1.,0.866025403784439,1.,0.866025403784439,
1.,0.866025403784439,1.,0.866025403784439,1.,0.866025403784439,1.,0.866025403784439,
1.,0.866025403784439,1.,0.866025403784439,1.,0.866025403784439,1.,0.866025403784439,
1.,0.866025403784439,1.,0.866025403784439,1.,0.866025403784439,1.,0.866025403784439,
1.,0.866025403784439,1.,0.866025403784439,1.,0.866025403784439,1.)))
REPRESENTATION_ITEM('')
SURFACE()
);
#2320=(
BOUNDED_SURFACE()
B_SPLINE_SURFACE(1,2,((#379175,#379176,#379177,#379178,#379179,#379180,
#379181,#379182,#379183,#379184,#379185,#379186,#379187,#379188,#379189,
#379190,#379191,#379192,#379193,#379194,#379195,#379196,#379197,#379198,
#379199,#379200,#379201,#379202,#379203,#379204,#379205,#379206,#379207,
#379208,#379209,#379210,#379211,#379212,#379213,#379214,#379215,#379216,
#379217,#379218,#379219,#379220,#379221,#379222,#379223,#379224,#379225,
#379226,#379227,#379228,#379229,#379230,#379231,#379232,#379233,#379234,
#379235,#379236,#379237,#379238,#379239,#379240,#379241,#379242,#379243,
#379244,#379245,#379246,#379247,#379248,#379249,#379250,#379251,#379252,
#379253,#379254,#379255,#379256,#379257,#379258,#379259,#379260,#379261,
#379262,#379263,#379264,#379265,#379266,#379267,#379268,#379269,#379270,
#379271,#379272,#379273,#379274,#379275,#379276,#379277,#379278,#379279,
#379280,#379281,#379282,#379283,#379284,#379285,#379286,#379287,#379288,
#379289,#379290,#379291,#379292,#379293,#379294,#379295,#379296,#379297,
#379298,#379299,#379300,#379301,#379302,#379303,#379304,#379305,#379306,
#379307,#379308,#379309,#379310,#379311,#379312,#379313,#379314,#379315,
#379316,#379317,#379318,#379319,#379320,#379321,#379322,#379323,#379324,
#379325,#379326,#379327,#379328,#379329,#379330,#379331,#379332,#379333,
#379334,#379335,#379336,#379337,#379338,#379339,#379340,#379341,#379342,
#379343,#379344,#379345,#379346,#379347,#379348,#379349,#379350,#379351,
#379352,#379353,#379354,#379355,#379356,#379357,#379358,#379359,#379360,
#379361,#379362,#379363,#379364,#379365,#379366,#379367,#379368,#379369,
#379370,#379371,#379372,#379373,#379374,#379375,#379376,#379377,#379378,
#379379,#379380,#379381,#379382,#379383,#379384,#379385,#379386,#379387,
#379388,#379389,#379390,#379391,#379392,#379393,#379394,#379395,#379396,
#379397,#379398,#379399,#379400,#379401,#379402,#379403,#379404,#379405,
#379406,#379407,#379408,#379409,#379410,#379411,#379412,#379413,#379414,
#379415,#379416,#379417,#379418,#379419,#379420,#379421,#379422,#379423,
#379424,#379425,#379426,#379427,#379428,#379429,#379430,#379431,#379432,
#379433,#379434,#379435,#379436,#379437,#379438,#379439,#379440,#379441,
#379442,#379443,#379444,#379445,#379446,#379447,#379448,#379449,#379450,
#379451,#379452,#379453,#379454,#379455,#379456,#379457,#379458,#379459,
#379460,#379461,#379462,#379463,#379464,#379465,#379466,#379467,#379468,
#379469,#379470,#379471,#379472,#379473,#379474,#379475,#379476,#379477,
#379478,#379479,#379480,#379481,#379482,#379483,#379484,#379485,#379486,
#379487,#379488,#379489,#379490,#379491,#379492,#379493,#379494,#379495,
#379496,#379497,#379498,#379499,#379500,#379501,#379502,#379503,#379504,
#379505,#379506,#379507,#379508,#379509,#379510,#379511,#379512,#379513,
#379514,#379515,#379516,#379517,#379518,#379519,#379520,#379521,#379522,
#379523,#379524,#379525,#379526,#379527,#379528,#379529,#379530,#379531,
#379532,#379533,#379534,#379535,#379536,#379537,#379538,#379539,#379540,
#379541,#379542,#379543,#379544,#379545,#379546,#379547),(#379548,#379549,
#379550,#379551,#379552,#379553,#379554,#379555,#379556,#379557,#379558,
#379559,#379560,#379561,#379562,#379563,#379564,#379565,#379566,#379567,
#379568,#379569,#379570,#379571,#379572,#379573,#379574,#379575,#379576,
#379577,#379578,#379579,#379580,#379581,#379582,#379583,#379584,#379585,
#379586,#379587,#379588,#379589,#379590,#379591,#379592,#379593,#379594,
#379595,#379596,#379597,#379598,#379599,#379600,#379601,#379602,#379603,
#379604,#379605,#379606,#379607,#379608,#379609,#379610,#379611,#379612,
#379613,#379614,#379615,#379616,#379617,#379618,#379619,#379620,#379621,
#379622,#379623,#379624,#379625,#379626,#379627,#379628,#379629,#379630,
#379631,#379632,#379633,#379634,#379635,#379636,#379637,#379638,#379639,
#379640,#379641,#379642,#379643,#379644,#379645,#379646,#379647,#379648,
#379649,#379650,#379651,#379652,#379653,#379654,#379655,#379656,#379657,
#379658,#379659,#379660,#379661,#379662,#379663,#379664,#379665,#379666,
#379667,#379668,#379669,#379670,#379671,#379672,#379673,#379674,#379675,
#379676,#379677,#379678,#379679,#379680,#379681,#379682,#379683,#379684,
#379685,#379686,#379687,#379688,#379689,#379690,#379691,#379692,#379693,
#379694,#379695,#379696,#379697,#379698,#379699,#379700,#379701,#379702,
#379703,#379704,#379705,#379706,#379707,#379708,#379709,#379710,#379711,
#379712,#379713,#379714,#379715,#379716,#379717,#379718,#379719,#379720,
#379721,#379722,#379723,#379724,#379725,#379726,#379727,#379728,#379729,
#379730,#379731,#379732,#379733,#379734,#379735,#379736,#379737,#379738,
#379739,#379740,#379741,#379742,#379743,#379744,#379745,#379746,#379747,
#379748,#379749,#379750,#379751,#379752,#379753,#379754,#379755,#379756,
#379757,#379758,#379759,#379760,#379761,#379762,#379763,#379764,#379765,
#379766,#379767,#379768,#379769,#379770,#379771,#379772,#379773,#379774,
#379775,#379776,#379777,#379778,#379779,#379780,#379781,#379782,#379783,
#379784,#379785,#379786,#379787,#379788,#379789,#379790,#379791,#379792,
#379793,#379794,#379795,#379796,#379797,#379798,#379799,#379800,#379801,
#379802,#379803,#379804,#379805,#379806,#379807,#379808,#379809,#379810,
#379811,#379812,#379813,#379814,#379815,#379816,#379817,#379818,#379819,
#379820,#379821,#379822,#379823,#379824,#379825,#379826,#379827,#379828,
#379829,#379830,#379831,#379832,#379833,#379834,#379835,#379836,#379837,
#379838,#379839,#379840,#379841,#379842,#379843,#379844,#379845,#379846,
#379847,#379848,#379849,#379850,#379851,#379852,#379853,#379854,#379855,
#379856,#379857,#379858,#379859,#379860,#379861,#379862,#379863,#379864,
#379865,#379866,#379867,#379868,#379869,#379870,#379871,#379872,#379873,
#379874,#379875,#379876,#379877,#379878,#379879,#379880,#379881,#379882,
#379883,#379884,#379885,#379886,#379887,#379888,#379889,#379890,#379891,
#379892,#379893,#379894,#379895,#379896,#379897,#379898,#379899,#379900,
#379901,#379902,#379903,#379904,#379905,#379906,#379907,#379908,#379909,
#379910,#379911,#379912,#379913,#379914,#379915,#379916,#379917,#379918,
#379919,#379920)),.UNSPECIFIED.,.F.,.F.,.F.)
B_SPLINE_SURFACE_WITH_KNOTS((2,2),(3,2,2,2,2,2,2,2,2,2,2,2,2,2,2,2,2,2,
2,2,2,2,2,2,2,2,2,2,2,2,2,2,2,2,2,2,2,2,2,2,2,2,2,2,2,2,2,2,2,2,2,2,2,2,
2,2,2,2,2,2,2,2,2,2,2,2,2,2,2,2,2,2,2,2,2,2,2,2,2,2,2,2,2,2,2,2,2,2,2,2,
2,2,2,2,2,2,2,2,2,2,2,2,2,2,2,2,2,2,2,2,2,2,2,2,2,2,2,2,2,2,2,2,2,2,2,2,
2,2,2,2,2,2,2,2,2,2,2,2,2,2,2,2,2,2,2,2,2,2,2,2,2,2,2,2,2,2,2,2,2,2,2,2,
2,2,2,2,2,2,2,2,2,2,2,2,2,2,2,2,2,2,2,2,2,2,2,2,3),(0.,1.00002458575229),
(0.,0.00537634408602151,0.010752688172043,0.0161290322580645,0.021505376344086,
0.0268817204301075,0.032258064516129,0.0376344086021505,0.043010752688172,
0.0483870967741935,0.0537634408602151,0.0591397849462366,0.0645161290322581,
0.0698924731182796,0.0752688172043011,0.0806451612903226,0.0860215053763441,
0.0913978494623656,0.0967741935483871,0.102150537634409,0.10752688172043,
0.112903225806452,0.118279569892473,0.123655913978495,0.129032258064516,
0.134408602150538,0.139784946236559,0.145161290322581,0.150537634408602,
0.155913978494624,0.161290322580645,0.166666666666667,0.172043010752688,
0.17741935483871,0.182795698924731,0.188172043010753,0.193548387096774,
0.198924731182796,0.204301075268817,0.209677419354839,0.21505376344086,
0.220430107526882,0.225806451612903,0.231182795698925,0.236559139784946,
0.241935483870968,0.247311827956989,0.252688172043011,0.258064516129032,
0.263440860215054,0.268817204301075,0.274193548387097,0.279569892473118,
0.28494623655914,0.290322580645161,0.295698924731183,0.301075268817204,
0.306451612903226,0.311827956989247,0.317204301075269,0.32258064516129,
0.327956989247312,0.333333333333333,0.338709677419355,0.344086021505376,
0.349462365591398,0.354838709677419,0.360215053763441,0.365591397849462,
0.370967741935484,0.376344086021505,0.381720430107527,0.387096774193548,
0.39247311827957,0.397849462365591,0.403225806451613,0.408602150537634,
0.413978494623656,0.419354838709677,0.424731182795699,0.43010752688172,
0.435483870967742,0.440860215053763,0.446236559139785,0.451612903225806,
0.456989247311828,0.462365591397849,0.467741935483871,0.473118279569892,
0.478494623655914,0.483870967741935,0.489247311827957,0.494623655913978,
0.5,0.505376344086022,0.510752688172043,0.516129032258065,0.521505376344086,
0.526881720430108,0.532258064516129,0.537634408602151,0.543010752688172,
0.548387096774194,0.553763440860215,0.559139784946237,0.564516129032258,
0.56989247311828,0.575268817204301,0.580645161290323,0.586021505376344,
0.591397849462366,0.596774193548387,0.602150537634409,0.60752688172043,
0.612903225806452,0.618279569892473,0.623655913978495,0.629032258064516,
0.634408602150538,0.639784946236559,0.645161290322581,0.650537634408602,
0.655913978494624,0.661290322580645,0.666666666666667,0.672043010752688,
0.67741935483871,0.682795698924731,0.688172043010753,0.693548387096774,
0.698924731182796,0.704301075268817,0.709677419354839,0.71505376344086,
0.720430107526882,0.725806451612903,0.731182795698925,0.736559139784946,
0.741935483870968,0.747311827956989,0.752688172043011,0.758064516129032,
0.763440860215054,0.768817204301075,0.774193548387097,0.779569892473118,
0.78494623655914,0.790322580645161,0.795698924731183,0.801075268817204,
0.806451612903226,0.811827956989247,0.817204301075269,0.82258064516129,
0.827956989247312,0.833333333333333,0.838709677419355,0.844086021505376,
0.849462365591398,0.854838709677419,0.860215053763441,0.865591397849462,
0.870967741935484,0.876344086021505,0.881720430107527,0.887096774193548,
0.89247311827957,0.897849462365591,0.903225806451613,0.908602150537634,
0.913978494623656,0.919354838709677,0.924731182795699,0.93010752688172,
0.935483870967742,0.940860215053763,0.946236559139785,0.951612903225806,
0.956989247311828,0.962365591397849,0.967741935483871,0.973118279569892,
0.978494623655914,0.983870967741935,0.989247311827957,0.994623655913978,
1.),.UNSPECIFIED.)
GEOMETRIC_REPRESENTATION_ITEM()
RATIONAL_B_SPLINE_SURFACE(((1.,0.866025403784439,1.,0.866025403784439,1.,
0.866025403784439,1.,0.866025403784439,1.,0.866025403784439,1.,0.866025403784439,
1.,0.866025403784439,1.,0.866025403784439,1.,0.866025403784439,1.,0.866025403784439,
1.,0.866025403784439,1.,0.866025403784439,1.,0.866025403784439,1.,0.866025403784439,
1.,0.866025403784439,1.,0.866025403784439,1.,0.866025403784439,1.,0.866025403784439,
1.,0.866025403784439,1.,0.866025403784439,1.,0.866025403784439,1.,0.866025403784439,
1.,0.866025403784439,1.,0.866025403784439,1.,0.866025403784439,1.,0.866025403784439,
1.,0.866025403784439,1.,0.866025403784439,1.,0.866025403784439,1.,0.866025403784439,
1.,0.866025403784439,1.,0.866025403784439,1.,0.866025403784439,1.,0.866025403784439,
1.,0.866025403784439,1.,0.866025403784439,1.,0.866025403784439,1.,0.866025403784439,
1.,0.866025403784439,1.,0.866025403784439,1.,0.866025403784439,1.,0.866025403784439,
1.,0.866025403784439,1.,0.866025403784439,1.,0.866025403784439,1.,0.866025403784439,
1.,0.866025403784439,1.,0.866025403784439,1.,0.866025403784439,1.,0.866025403784439,
1.,0.866025403784439,1.,0.866025403784439,1.,0.866025403784439,1.,0.866025403784439,
1.,0.866025403784439,1.,0.866025403784439,1.,0.866025403784439,1.,0.866025403784439,
1.,0.866025403784439,1.,0.866025403784439,1.,0.866025403784439,1.,0.866025403784439,
1.,0.866025403784439,1.,0.866025403784439,1.,0.866025403784439,1.,0.866025403784439,
1.,0.866025403784439,1.,0.866025403784439,1.,0.866025403784439,1.,0.866025403784439,
1.,0.866025403784439,1.,0.866025403784439,1.,0.866025403784439,1.,0.866025403784439,
1.,0.866025403784439,1.,0.866025403784439,1.,0.866025403784439,1.,0.866025403784439,
1.,0.866025403784439,1.,0.866025403784439,1.,0.866025403784439,1.,0.866025403784439,
1.,0.866025403784439,1.,0.866025403784439,1.,0.866025403784439,1.,0.866025403784439,
1.,0.866025403784439,1.,0.866025403784439,1.,0.866025403784439,1.,0.866025403784439,
1.,0.866025403784439,1.,0.866025403784439,1.,0.866025403784439,1.,0.866025403784439,
1.,0.866025403784439,1.,0.866025403784439,1.,0.866025403784439,1.,0.866025403784439,
1.,0.866025403784439,1.,0.866025403784439,1.,0.866025403784439,1.,0.866025403784439,
1.,0.866025403784439,1.,0.866025403784439,1.,0.866025403784439,1.,0.866025403784439,
1.,0.866025403784439,1.,0.866025403784439,1.,0.866025403784439,1.,0.866025403784439,
1.,0.866025403784439,1.,0.866025403784439,1.,0.866025403784439,1.,0.866025403784439,
1.,0.866025403784439,1.,0.866025403784439,1.,0.866025403784439,1.,0.866025403784439,
1.,0.866025403784439,1.,0.866025403784439,1.,0.866025403784439,1.,0.866025403784439,
1.,0.866025403784439,1.,0.866025403784439,1.,0.866025403784439,1.,0.866025403784439,
1.,0.866025403784439,1.,0.866025403784439,1.,0.866025403784439,1.,0.866025403784439,
1.,0.866025403784439,1.,0.866025403784439,1.,0.866025403784439,1.,0.866025403784439,
1.,0.866025403784439,1.,0.866025403784439,1.,0.866025403784439,1.,0.866025403784439,
1.,0.866025403784439,1.,0.866025403784439,1.,0.866025403784439,1.,0.866025403784439,
1.,0.866025403784439,1.,0.866025403784439,1.,0.866025403784439,1.,0.866025403784439,
1.,0.866025403784439,1.,0.866025403784439,1.,0.866025403784439,1.,0.866025403784439,
1.,0.866025403784439,1.,0.866025403784439,1.,0.866025403784439,1.,0.866025403784439,
1.,0.866025403784439,1.,0.866025403784439,1.,0.866025403784439,1.,0.866025403784439,
1.,0.866025403784439,1.,0.866025403784439,1.,0.866025403784439,1.,0.866025403784439,
1.,0.866025403784439,1.,0.866025403784439,1.,0.866025403784439,1.,0.866025403784439,
1.,0.866025403784439,1.,0.866025403784439,1.,0.866025403784439,1.,0.866025403784439,
1.,0.866025403784439,1.,0.866025403784439,1.,0.866025403784439,1.,0.866025403784439,
1.,0.866025403784439,1.,0.866025403784439,1.,0.866025403784439,1.,0.866025403784439,
1.,0.866025403784439,1.,0.866025403784439,1.,0.866025403784439,1.,0.866025403784439,
1.,0.866025403784439,1.,0.866025403784439,1.,0.866025403784439,1.,0.866025403784439,
1.),(1.,0.866025403784439,1.,0.866025403784439,1.,0.866025403784439,1.,
0.866025403784439,1.,0.866025403784439,1.,0.866025403784439,1.,0.866025403784439,
1.,0.866025403784439,1.,0.866025403784439,1.,0.866025403784439,1.,0.866025403784439,
1.,0.866025403784439,1.,0.866025403784439,1.,0.866025403784439,1.,0.866025403784439,
1.,0.866025403784439,1.,0.866025403784439,1.,0.866025403784439,1.,0.866025403784439,
1.,0.866025403784439,1.,0.866025403784439,1.,0.866025403784439,1.,0.866025403784439,
1.,0.866025403784439,1.,0.866025403784439,1.,0.866025403784439,1.,0.866025403784439,
1.,0.866025403784439,1.,0.866025403784439,1.,0.866025403784439,1.,0.866025403784439,
1.,0.866025403784439,1.,0.866025403784439,1.,0.866025403784439,1.,0.866025403784439,
1.,0.866025403784439,1.,0.866025403784439,1.,0.866025403784439,1.,0.866025403784439,
1.,0.866025403784439,1.,0.866025403784439,1.,0.866025403784439,1.,0.866025403784439,
1.,0.866025403784439,1.,0.866025403784439,1.,0.866025403784439,1.,0.866025403784439,
1.,0.866025403784439,1.,0.866025403784439,1.,0.866025403784439,1.,0.866025403784439,
1.,0.866025403784439,1.,0.866025403784439,1.,0.866025403784439,1.,0.866025403784439,
1.,0.866025403784439,1.,0.866025403784439,1.,0.866025403784439,1.,0.866025403784439,
1.,0.866025403784439,1.,0.866025403784439,1.,0.866025403784439,1.,0.866025403784439,
1.,0.866025403784439,1.,0.866025403784439,1.,0.866025403784439,1.,0.866025403784439,
1.,0.866025403784439,1.,0.866025403784439,1.,0.866025403784439,1.,0.866025403784439,
1.,0.866025403784439,1.,0.866025403784439,1.,0.866025403784439,1.,0.866025403784439,
1.,0.866025403784439,1.,0.866025403784439,1.,0.866025403784439,1.,0.866025403784439,
1.,0.866025403784439,1.,0.866025403784439,1.,0.866025403784439,1.,0.866025403784439,
1.,0.866025403784439,1.,0.866025403784439,1.,0.866025403784439,1.,0.866025403784439,
1.,0.866025403784439,1.,0.866025403784439,1.,0.866025403784439,1.,0.866025403784439,
1.,0.866025403784439,1.,0.866025403784439,1.,0.866025403784439,1.,0.866025403784439,
1.,0.866025403784439,1.,0.866025403784439,1.,0.866025403784439,1.,0.866025403784439,
1.,0.866025403784439,1.,0.866025403784439,1.,0.866025403784439,1.,0.866025403784439,
1.,0.866025403784439,1.,0.866025403784439,1.,0.866025403784439,1.,0.866025403784439,
1.,0.866025403784439,1.,0.866025403784439,1.,0.866025403784439,1.,0.866025403784439,
1.,0.866025403784439,1.,0.866025403784439,1.,0.866025403784439,1.,0.866025403784439,
1.,0.866025403784439,1.,0.866025403784439,1.,0.866025403784439,1.,0.866025403784439,
1.,0.866025403784439,1.,0.866025403784439,1.,0.866025403784439,1.,0.866025403784439,
1.,0.866025403784439,1.,0.866025403784439,1.,0.866025403784439,1.,0.866025403784439,
1.,0.866025403784439,1.,0.866025403784439,1.,0.866025403784439,1.,0.866025403784439,
1.,0.866025403784439,1.,0.866025403784439,1.,0.866025403784439,1.,0.866025403784439,
1.,0.866025403784439,1.,0.866025403784439,1.,0.866025403784439,1.,0.866025403784439,
1.,0.866025403784439,1.,0.866025403784439,1.,0.866025403784439,1.,0.866025403784439,
1.,0.866025403784439,1.,0.866025403784439,1.,0.866025403784439,1.,0.866025403784439,
1.,0.866025403784439,1.,0.866025403784439,1.,0.866025403784439,1.,0.866025403784439,
1.,0.866025403784439,1.,0.866025403784439,1.,0.866025403784439,1.,0.866025403784439,
1.,0.866025403784439,1.,0.866025403784439,1.,0.866025403784439,1.,0.866025403784439,
1.,0.866025403784439,1.,0.866025403784439,1.,0.866025403784439,1.,0.866025403784439,
1.,0.866025403784439,1.,0.866025403784439,1.,0.866025403784439,1.,0.866025403784439,
1.,0.866025403784439,1.,0.866025403784439,1.,0.866025403784439,1.,0.866025403784439,
1.,0.866025403784439,1.,0.866025403784439,1.,0.866025403784439,1.,0.866025403784439,
1.,0.866025403784439,1.,0.866025403784439,1.,0.866025403784439,1.,0.866025403784439,
1.,0.866025403784439,1.,0.866025403784439,1.,0.866025403784439,1.,0.866025403784439,
1.,0.866025403784439,1.,0.866025403784439,1.,0.866025403784439,1.)))
REPRESENTATION_ITEM('')
SURFACE()
);
#2321=(
BOUNDED_SURFACE()
B_SPLINE_SURFACE(3,2,((#379934,#379935,#379936),(#379937,#379938,#379939),
(#379940,#379941,#379942),(#379943,#379944,#379945)),.UNSPECIFIED.,.F.,
 .F.,.F.)
B_SPLINE_SURFACE_WITH_KNOTS((4,4),(3,3),(0.00135801595889393,0.00148409170619832),
(0.,1.),.UNSPECIFIED.)
GEOMETRIC_REPRESENTATION_ITEM()
RATIONAL_B_SPLINE_SURFACE(((1.,0.818301933966443,1.),(1.,0.817226613172337,
1.),(1.,0.816179643373948,1.),(1.,0.815159387863655,1.)))
REPRESENTATION_ITEM('')
SURFACE()
);
#2322=(
BOUNDED_SURFACE()
B_SPLINE_SURFACE(3,2,((#379981,#379982,#379983),(#379984,#379985,#379986),
(#379987,#379988,#379989),(#379990,#379991,#379992)),.UNSPECIFIED.,.F.,
 .F.,.F.)
B_SPLINE_SURFACE_WITH_KNOTS((4,4),(3,3),(-1.54744435122076E-6,1.54744435122076E-5),
(-0.0151698983610561,1.),.UNSPECIFIED.)
GEOMETRIC_REPRESENTATION_ITEM()
RATIONAL_B_SPLINE_SURFACE(((1.02018382472812,0.334740937357287,1.),(1.00401234488797,
0.867753072813418,1.),(1.00033622856778,0.988917903080862,1.),(1.,1.,1.)))
REPRESENTATION_ITEM('')
SURFACE()
);
#2323=(
BOUNDED_SURFACE()
B_SPLINE_SURFACE(3,2,((#379994,#379995,#379996),(#379997,#379998,#379999),
(#380000,#380001,#380002),(#380003,#380004,#380005)),.UNSPECIFIED.,.F.,
 .F.,.F.)
B_SPLINE_SURFACE_WITH_KNOTS((4,4),(3,3),(1.55009486301137E-5,4.92065510474431E-5),
(-8.13759512746712E-5,1.),.UNSPECIFIED.)
GEOMETRIC_REPRESENTATION_ITEM()
RATIONAL_B_SPLINE_SURFACE(((1.0000237291233,0.85420063959972,1.),(1.0000142358599,
0.912530301180549,1.),(1.00000710550469,0.956341495377441,1.),(1.00001238975905,
0.923873338137039,1.)))
REPRESENTATION_ITEM('')
SURFACE()
);
#2324=(
BOUNDED_SURFACE()
B_SPLINE_SURFACE(3,2,((#380007,#380008,#380009),(#380010,#380011,#380012),
(#380013,#380014,#380015),(#380016,#380017,#380018)),.UNSPECIFIED.,.F.,
 .F.,.F.)
B_SPLINE_SURFACE_WITH_KNOTS((4,4),(3,3),(-3.39934179457821E-6,3.73927597403565E-5),
(-0.00186004067418894,1.00069373317436),.UNSPECIFIED.)
GEOMETRIC_REPRESENTATION_ITEM()
RATIONAL_B_SPLINE_SURFACE(((1.00072100136055,0.806051963875345,1.0002685964269),
(1.00060048440154,0.838470803558665,1.00022369994495),(1.00053106448795,
0.857144632272366,1.00019783877218),(1.00054515072852,0.853355459539107,
1.00020308635436)))
REPRESENTATION_ITEM('')
SURFACE()
);
#2325=(
BOUNDED_SURFACE()
B_SPLINE_SURFACE(3,2,((#380020,#380021,#380022),(#380023,#380024,#380025),
(#380026,#380027,#380028),(#380029,#380030,#380031)),.UNSPECIFIED.,.F.,
 .F.,.F.)
B_SPLINE_SURFACE_WITH_KNOTS((4,4),(3,3),(0.00137194782501028,0.00149814269699235),
(0.,1.),.UNSPECIFIED.)
GEOMETRIC_REPRESENTATION_ITEM()
RATIONAL_B_SPLINE_SURFACE(((1.,0.815158509402307,1.),(1.,0.816179044148172,
1.),(1.,0.817226308119919,1.),(1.,0.818301939488809,1.)))
REPRESENTATION_ITEM('')
SURFACE()
);
#2326=(
BOUNDED_SURFACE()
B_SPLINE_SURFACE(3,2,((#380068,#380069,#380070),(#380071,#380072,#380073),
(#380074,#380075,#380076),(#380077,#380078,#380079)),.UNSPECIFIED.,.F.,
 .F.,.F.)
B_SPLINE_SURFACE_WITH_KNOTS((4,4),(3,3),(0.,9.54361881492174E-5),(0.,1.),
 .UNSPECIFIED.)
GEOMETRIC_REPRESENTATION_ITEM()
RATIONAL_B_SPLINE_SURFACE(((1.,0.816715621142057,1.),(1.,0.815907587407932,
1.),(1.,0.81511595934521,1.),(1.,0.814339887349193,1.)))
REPRESENTATION_ITEM('')
SURFACE()
);
#2327=(
BOUNDED_SURFACE()
B_SPLINE_SURFACE(3,2,((#380081,#380082,#380083),(#380084,#380085,#380086),
(#380087,#380088,#380089),(#380090,#380091,#380092)),.UNSPECIFIED.,.F.,
 .F.,.F.)
B_SPLINE_SURFACE_WITH_KNOTS((4,4),(3,3),(2.02993869230509E-5,5.39756952686906E-5),
(-0.000116281069492499,1.),.UNSPECIFIED.)
GEOMETRIC_REPRESENTATION_ITEM()
RATIONAL_B_SPLINE_SURFACE(((1.00001770479723,0.923870681143041,1.),(1.00001014104055,
0.956394275543438,1.),(1.00002037300271,0.912397594905722,1.),(1.00003390859456,
0.85419555086991,1.)))
REPRESENTATION_ITEM('')
SURFACE()
);
#2328=(
BOUNDED_SURFACE()
B_SPLINE_SURFACE(3,2,((#380094,#380095,#380096),(#380097,#380098,#380099),
(#380100,#380101,#380102),(#380103,#380104,#380105)),.UNSPECIFIED.,.F.,
 .F.,.F.)
B_SPLINE_SURFACE_WITH_KNOTS((4,4),(3,3),(0.,4.68197758448209E-5),(0.,1.),
 .UNSPECIFIED.)
GEOMETRIC_REPRESENTATION_ITEM()
RATIONAL_B_SPLINE_SURFACE(((1.,0.816715621142057,1.),(1.,0.953638980025206,
1.),(1.,0.954506925408047,1.),(1.,0.816715621142055,1.)))
REPRESENTATION_ITEM('')
SURFACE()
);
#2329=(
BOUNDED_SURFACE()
B_SPLINE_SURFACE(3,2,((#380109,#380110,#380111),(#380112,#380113,#380114),
(#380115,#380116,#380117),(#380118,#380119,#380120)),.UNSPECIFIED.,.F.,
 .F.,.F.)
B_SPLINE_SURFACE_WITH_KNOTS((4,4),(3,3),(0.,9.54361881492177E-5),(0.,1.),
 .UNSPECIFIED.)
GEOMETRIC_REPRESENTATION_ITEM()
RATIONAL_B_SPLINE_SURFACE(((1.,0.814339887349193,1.),(1.,0.815115959345207,
1.),(1.,0.815907587407933,1.),(1.,0.816715621142057,1.)))
REPRESENTATION_ITEM('')
SURFACE()
);
#2330=(
BOUNDED_SURFACE()
B_SPLINE_SURFACE(3,2,((#380122,#380123,#380124),(#380125,#380126,#380127),
(#380128,#380129,#380130),(#380131,#380132,#380133)),.UNSPECIFIED.,.F.,
 .F.,.F.)
B_SPLINE_SURFACE_WITH_KNOTS((4,4),(3,3),(-3.39528393502487E-6,3.73481232852736E-5),
(-0.0016501803328463,1.),.UNSPECIFIED.)
GEOMETRIC_REPRESENTATION_ITEM()
RATIONAL_B_SPLINE_SURFACE(((1.00048354385553,0.853487571660461,1.),(1.00047110510908,
0.857256476851525,1.),(1.00053193201093,0.83882609665593,1.),(1.00063970687709,
0.806170615310181,1.)))
REPRESENTATION_ITEM('')
SURFACE()
);
#2331=(
BOUNDED_SURFACE()
B_SPLINE_SURFACE(3,2,((#380225,#380226,#380227),(#380228,#380229,#380230),
(#380231,#380232,#380233),(#380234,#380235,#380236)),.UNSPECIFIED.,.F.,
 .F.,.F.)
B_SPLINE_SURFACE_WITH_KNOTS((4,4),(3,3),(0.00135801595889393,0.00148409170619832),
(0.,1.),.UNSPECIFIED.)
GEOMETRIC_REPRESENTATION_ITEM()
RATIONAL_B_SPLINE_SURFACE(((1.,0.818301933966445,1.),(1.,0.817226613172352,
1.),(1.,0.816179643373942,1.),(1.,0.815159387863666,1.)))
REPRESENTATION_ITEM('')
SURFACE()
);
#2332=(
BOUNDED_SURFACE()
B_SPLINE_SURFACE(3,2,((#380275,#380276,#380277),(#380278,#380279,#380280),
(#380281,#380282,#380283),(#380284,#380285,#380286)),.UNSPECIFIED.,.F.,
 .F.,.F.)
B_SPLINE_SURFACE_WITH_KNOTS((4,4),(3,3),(-1.54744435122067E-6,1.54744435122073E-5),
(-0.015169898363932,1.),.UNSPECIFIED.)
GEOMETRIC_REPRESENTATION_ITEM()
RATIONAL_B_SPLINE_SURFACE(((1.02018382473201,0.334740937355304,1.),(1.00401234488873,
0.867753072813129,1.),(1.00033622856785,0.988917903080821,1.),(1.,1.,1.)))
REPRESENTATION_ITEM('')
SURFACE()
);
#2333=(
BOUNDED_SURFACE()
B_SPLINE_SURFACE(3,2,((#380288,#380289,#380290),(#380291,#380292,#380293),
(#380294,#380295,#380296),(#380297,#380298,#380299)),.UNSPECIFIED.,.F.,
 .F.,.F.)
B_SPLINE_SURFACE_WITH_KNOTS((4,4),(3,3),(0.00137194782501028,0.00149814269699235),
(0.,1.),.UNSPECIFIED.)
GEOMETRIC_REPRESENTATION_ITEM()
RATIONAL_B_SPLINE_SURFACE(((1.,0.815158509402316,1.),(1.,0.816179044148162,
1.),(1.,0.817226308119924,1.),(1.,0.818301939488816,1.)))
REPRESENTATION_ITEM('')
SURFACE()
);
#2334=(
BOUNDED_SURFACE()
B_SPLINE_SURFACE(3,2,((#380343,#380344,#380345),(#380346,#380347,#380348),
(#380349,#380350,#380351),(#380352,#380353,#380354)),.UNSPECIFIED.,.F.,
 .F.,.F.)
B_SPLINE_SURFACE_WITH_KNOTS((4,4),(3,3),(1.55009486301137E-5,4.92065510474432E-5),
(-8.13759515860464E-5,1.),.UNSPECIFIED.)
GEOMETRIC_REPRESENTATION_ITEM()
RATIONAL_B_SPLINE_SURFACE(((1.00002372912339,0.854200639599671,1.),(1.00001423585995,
0.91253030118053,1.),(1.00000710550472,0.956341495377424,1.),(1.0000123897591,
0.923873338137017,1.)))
REPRESENTATION_ITEM('')
SURFACE()
);
#2335=(
BOUNDED_SURFACE()
B_SPLINE_SURFACE(3,2,((#380358,#380359,#380360),(#380361,#380362,#380363),
(#380364,#380365,#380366),(#380367,#380368,#380369)),.UNSPECIFIED.,.F.,
 .F.,.F.)
B_SPLINE_SURFACE_WITH_KNOTS((4,4),(3,3),(-3.3993417945781E-6,3.73927597403567E-5),
(-0.00186004067406598,1.00069373317433),.UNSPECIFIED.)
GEOMETRIC_REPRESENTATION_ITEM()
RATIONAL_B_SPLINE_SURFACE(((1.0007210013605,0.806051963875402,1.00026859642688),
(1.0006004844015,0.838470803558646,1.00022369994494),(1.00053106448791,
0.85714463227243,1.00019783877218),(1.00054515072849,0.853355459539126,
1.00020308635435)))
REPRESENTATION_ITEM('')
SURFACE()
);
#2336=(
BOUNDED_SURFACE()
B_SPLINE_SURFACE(3,2,((#380371,#380372,#380373),(#380374,#380375,#380376),
(#380377,#380378,#380379),(#380380,#380381,#380382)),.UNSPECIFIED.,.F.,
 .F.,.F.)
B_SPLINE_SURFACE_WITH_KNOTS((4,4),(3,3),(1.62630325872826E-19,9.54361881492175E-5),
(0.,1.),.UNSPECIFIED.)
GEOMETRIC_REPRESENTATION_ITEM()
RATIONAL_B_SPLINE_SURFACE(((1.,0.816715621142059,1.),(1.,0.815907587407935,
1.),(1.,0.815115959345216,1.),(1.,0.814339887349207,1.)))
REPRESENTATION_ITEM('')
SURFACE()
);
#2337=(
BOUNDED_SURFACE()
B_SPLINE_SURFACE(3,2,((#380384,#380385,#380386),(#380387,#380388,#380389),
(#380390,#380391,#380392),(#380393,#380394,#380395)),.UNSPECIFIED.,.F.,
 .F.,.F.)
B_SPLINE_SURFACE_WITH_KNOTS((4,4),(3,3),(9.48676900924816E-20,4.68197758448212E-5),
(0.,1.),.UNSPECIFIED.)
GEOMETRIC_REPRESENTATION_ITEM()
RATIONAL_B_SPLINE_SURFACE(((1.,0.81671562114204,1.),(1.,0.953638980025222,
1.),(1.,0.954506925408046,1.),(1.,0.816715621142051,1.)))
REPRESENTATION_ITEM('')
SURFACE()
);
#2338=(
BOUNDED_SURFACE()
B_SPLINE_SURFACE(3,2,((#380397,#380398,#380399),(#380400,#380401,#380402),
(#380403,#380404,#380405),(#380406,#380407,#380408)),.UNSPECIFIED.,.F.,
 .F.,.F.)
B_SPLINE_SURFACE_WITH_KNOTS((4,4),(3,3),(5.42101086242752E-20,9.54361881492177E-5),
(0.,1.),.UNSPECIFIED.)
GEOMETRIC_REPRESENTATION_ITEM()
RATIONAL_B_SPLINE_SURFACE(((1.,0.814339887349192,1.),(1.,0.815115959345195,
1.),(1.,0.815907587407961,1.),(1.,0.81671562114204,1.)))
REPRESENTATION_ITEM('')
SURFACE()
);
#2339=(
BOUNDED_SURFACE()
B_SPLINE_SURFACE(3,2,((#380410,#380411,#380412),(#380413,#380414,#380415),
(#380416,#380417,#380418),(#380419,#380420,#380421)),.UNSPECIFIED.,.F.,
 .F.,.F.)
B_SPLINE_SURFACE_WITH_KNOTS((4,4),(3,3),(-3.39528393502487E-6,3.73481232852731E-5),
(-0.00165018033312054,1.),.UNSPECIFIED.)
GEOMETRIC_REPRESENTATION_ITEM()
RATIONAL_B_SPLINE_SURFACE(((1.00048354385561,0.853487571660432,1.),(1.00047110510916,
0.857256476851472,1.),(1.00053193201102,0.838826096655894,1.),(1.00063970687719,
0.806170615310123,1.)))
REPRESENTATION_ITEM('')
SURFACE()
);
#2340=(
BOUNDED_SURFACE()
B_SPLINE_SURFACE(3,2,((#380425,#380426,#380427),(#380428,#380429,#380430),
(#380431,#380432,#380433),(#380434,#380435,#380436)),.UNSPECIFIED.,.F.,
 .F.,.F.)
B_SPLINE_SURFACE_WITH_KNOTS((4,4),(3,3),(2.02993869230509E-5,5.39756952686907E-5),
(-0.000116281069872552,1.),.UNSPECIFIED.)
GEOMETRIC_REPRESENTATION_ITEM()
RATIONAL_B_SPLINE_SURFACE(((1.00001770479729,0.923870681143009,1.),(1.00001014104058,
0.956394275543428,1.),(1.00002037300278,0.912397594905674,1.),(1.00003390859467,
0.85419555086986,1.)))
REPRESENTATION_ITEM('')
SURFACE()
);
#2341=(
BOUNDED_SURFACE()
B_SPLINE_SURFACE(3,2,((#380529,#380530,#380531),(#380532,#380533,#380534),
(#380535,#380536,#380537),(#380538,#380539,#380540)),.UNSPECIFIED.,.F.,
 .F.,.F.)
B_SPLINE_SURFACE_WITH_KNOTS((4,4),(3,3),(0.00135801595889393,0.00148409170619832),
(0.,1.),.UNSPECIFIED.)
GEOMETRIC_REPRESENTATION_ITEM()
RATIONAL_B_SPLINE_SURFACE(((1.,0.818301933966445,1.),(1.,0.817226613172355,
1.),(1.,0.81617964337394,1.),(1.,0.815159387863663,1.)))
REPRESENTATION_ITEM('')
SURFACE()
);
#2342=(
BOUNDED_SURFACE()
B_SPLINE_SURFACE(3,2,((#380579,#380580,#380581),(#380582,#380583,#380584),
(#380585,#380586,#380587),(#380588,#380589,#380590)),.UNSPECIFIED.,.F.,
 .F.,.F.)
B_SPLINE_SURFACE_WITH_KNOTS((4,4),(3,3),(-1.54744435122007E-6,1.54744435122084E-5),
(-0.0151698983689038,1.),.UNSPECIFIED.)
GEOMETRIC_REPRESENTATION_ITEM()
RATIONAL_B_SPLINE_SURFACE(((1.02018382473872,0.334740937352125,1.),(1.00401234489007,
0.86775307281241,1.),(1.00033622856796,0.988917903080806,1.),(1.,1.,1.)))
REPRESENTATION_ITEM('')
SURFACE()
);
#2343=(
BOUNDED_SURFACE()
B_SPLINE_SURFACE(3,2,((#380592,#380593,#380594),(#380595,#380596,#380597),
(#380598,#380599,#380600),(#380601,#380602,#380603)),.UNSPECIFIED.,.F.,
 .F.,.F.)
B_SPLINE_SURFACE_WITH_KNOTS((4,4),(3,3),(0.00137194782501028,0.00149814269699235),
(0.,1.),.UNSPECIFIED.)
GEOMETRIC_REPRESENTATION_ITEM()
RATIONAL_B_SPLINE_SURFACE(((1.,0.815158509402318,1.),(1.,0.816179044148178,
1.),(1.,0.817226308119925,1.),(1.,0.818301939488807,1.)))
REPRESENTATION_ITEM('')
SURFACE()
);
#2344=(
BOUNDED_SURFACE()
B_SPLINE_SURFACE(3,2,((#380647,#380648,#380649),(#380650,#380651,#380652),
(#380653,#380654,#380655),(#380656,#380657,#380658)),.UNSPECIFIED.,.F.,
 .F.,.F.)
B_SPLINE_SURFACE_WITH_KNOTS((4,4),(3,3),(1.55009486301137E-5,4.92065510474435E-5),
(-8.13759514786794E-5,1.),.UNSPECIFIED.)
GEOMETRIC_REPRESENTATION_ITEM()
RATIONAL_B_SPLINE_SURFACE(((1.00002372912336,0.854200639599684,1.),(1.00001423585993,
0.912530301180555,1.),(1.00000710550471,0.956341495377423,1.),(1.00001238975908,
0.923873338137021,1.)))
REPRESENTATION_ITEM('')
SURFACE()
);
#2345=(
BOUNDED_SURFACE()
B_SPLINE_SURFACE(3,2,((#380662,#380663,#380664),(#380665,#380666,#380667),
(#380668,#380669,#380670),(#380671,#380672,#380673)),.UNSPECIFIED.,.F.,
 .F.,.F.)
B_SPLINE_SURFACE_WITH_KNOTS((4,4),(3,3),(-3.39934179457836E-6,3.73927597403564E-5),
(-0.00186004067423522,1.00069373317444),.UNSPECIFIED.)
GEOMETRIC_REPRESENTATION_ITEM()
RATIONAL_B_SPLINE_SURFACE(((1.00072100136056,0.806051963875341,1.00026859642693),
(1.00060048440156,0.838470803558606,1.00022369994497),(1.00053106448796,
0.85714463227239,1.00019783877221),(1.00054515072854,0.853355459539081,
1.00020308635438)))
REPRESENTATION_ITEM('')
SURFACE()
);
#2346=(
BOUNDED_SURFACE()
B_SPLINE_SURFACE(3,2,((#380675,#380676,#380677),(#380678,#380679,#380680),
(#380681,#380682,#380683),(#380684,#380685,#380686)),.UNSPECIFIED.,.F.,
 .F.,.F.)
B_SPLINE_SURFACE_WITH_KNOTS((4,4),(3,3),(2.71050543121376E-19,9.54361881492173E-5),
(0.,1.),.UNSPECIFIED.)
GEOMETRIC_REPRESENTATION_ITEM()
RATIONAL_B_SPLINE_SURFACE(((1.,0.816715621142052,1.),(1.,0.815907587407943,
1.),(1.,0.815115959345205,1.),(1.,0.814339887349196,1.)))
REPRESENTATION_ITEM('')
SURFACE()
);
#2347=(
BOUNDED_SURFACE()
B_SPLINE_SURFACE(3,2,((#380688,#380689,#380690),(#380691,#380692,#380693),
(#380694,#380695,#380696),(#380697,#380698,#380699)),.UNSPECIFIED.,.F.,
 .F.,.F.)
B_SPLINE_SURFACE_WITH_KNOTS((4,4),(3,3),(4.74338450462408E-20,4.6819775844821E-5),
(0.,1.),.UNSPECIFIED.)
GEOMETRIC_REPRESENTATION_ITEM()
RATIONAL_B_SPLINE_SURFACE(((1.,0.816715621142047,1.),(1.,0.953638980025206,
1.),(1.,0.954506925408053,1.),(1.,0.816715621142052,1.)))
REPRESENTATION_ITEM('')
SURFACE()
);
#2348=(
BOUNDED_SURFACE()
B_SPLINE_SURFACE(3,2,((#380701,#380702,#380703),(#380704,#380705,#380706),
(#380707,#380708,#380709),(#380710,#380711,#380712)),.UNSPECIFIED.,.F.,
 .F.,.F.)
B_SPLINE_SURFACE_WITH_KNOTS((4,4),(3,3),(-1.62630325872826E-19,9.54361881492177E-5),
(0.,1.),.UNSPECIFIED.)
GEOMETRIC_REPRESENTATION_ITEM()
RATIONAL_B_SPLINE_SURFACE(((1.,0.814339887349194,1.),(1.,0.815115959345216,
1.),(1.,0.815907587407934,1.),(1.,0.816715621142047,1.)))
REPRESENTATION_ITEM('')
SURFACE()
);
#2349=(
BOUNDED_SURFACE()
B_SPLINE_SURFACE(3,2,((#380714,#380715,#380716),(#380717,#380718,#380719),
(#380720,#380721,#380722),(#380723,#380724,#380725)),.UNSPECIFIED.,.F.,
 .F.,.F.)
B_SPLINE_SURFACE_WITH_KNOTS((4,4),(3,3),(-3.39528393502481E-6,3.73481232852726E-5),
(-0.00165018033327409,1.),.UNSPECIFIED.)
GEOMETRIC_REPRESENTATION_ITEM()
RATIONAL_B_SPLINE_SURFACE(((1.00048354385565,0.853487571660394,1.),(1.0004711051092,
0.857256476851478,1.),(1.00053193201107,0.838826096655851,1.),(1.00063970687725,
0.806170615310114,1.)))
REPRESENTATION_ITEM('')
SURFACE()
);
#2350=(
BOUNDED_SURFACE()
B_SPLINE_SURFACE(3,2,((#380729,#380730,#380731),(#380732,#380733,#380734),
(#380735,#380736,#380737),(#380738,#380739,#380740)),.UNSPECIFIED.,.F.,
 .F.,.F.)
B_SPLINE_SURFACE_WITH_KNOTS((4,4),(3,3),(2.0299386923051E-5,5.39756952687117E-5),
(-0.000116281068889452,1.),.UNSPECIFIED.)
GEOMETRIC_REPRESENTATION_ITEM()
RATIONAL_B_SPLINE_SURFACE(((1.00001770479714,0.923870681143094,1.),(1.0000101410405,
0.95639427554349,1.),(1.0000203730026,0.912397594905705,1.),(1.00003390859439,
0.85419555086989,1.)))
REPRESENTATION_ITEM('')
SURFACE()
);
#2351=(
BOUNDED_SURFACE()
B_SPLINE_SURFACE(3,2,((#380833,#380834,#380835),(#380836,#380837,#380838),
(#380839,#380840,#380841),(#380842,#380843,#380844)),.UNSPECIFIED.,.F.,
 .F.,.F.)
B_SPLINE_SURFACE_WITH_KNOTS((4,4),(3,3),(0.00135801595889393,0.00148409170619832),
(0.,1.),.UNSPECIFIED.)
GEOMETRIC_REPRESENTATION_ITEM()
RATIONAL_B_SPLINE_SURFACE(((1.,0.818301933966442,1.),(1.,0.817226613172345,
1.),(1.,0.81617964337394,1.),(1.,0.815159387863652,1.)))
REPRESENTATION_ITEM('')
SURFACE()
);
#2352=(
BOUNDED_SURFACE()
B_SPLINE_SURFACE(3,2,((#380883,#380884,#380885),(#380886,#380887,#380888),
(#380889,#380890,#380891),(#380892,#380893,#380894)),.UNSPECIFIED.,.F.,
 .F.,.F.)
B_SPLINE_SURFACE_WITH_KNOTS((4,4),(3,3),(-1.54744435122067E-6,1.54744435122072E-5),
(-0.0151698983630455,1.0151698983594),.UNSPECIFIED.)
GEOMETRIC_REPRESENTATION_ITEM()
RATIONAL_B_SPLINE_SURFACE(((1.02018382473081,0.324498219413325,1.02018382472589),
(1.00401234488849,0.865716921710696,1.00401234488751),(1.00033622856783,
0.98874727662963,1.00033622856775),(1.,1.,1.)))
REPRESENTATION_ITEM('')
SURFACE()
);
#2353=(
BOUNDED_SURFACE()
B_SPLINE_SURFACE(3,2,((#380896,#380897,#380898),(#380899,#380900,#380901),
(#380902,#380903,#380904),(#380905,#380906,#380907)),.UNSPECIFIED.,.F.,
 .F.,.F.)
B_SPLINE_SURFACE_WITH_KNOTS((4,4),(3,3),(0.00137194782501028,0.00149814269699235),
(0.,1.),.UNSPECIFIED.)
GEOMETRIC_REPRESENTATION_ITEM()
RATIONAL_B_SPLINE_SURFACE(((1.,0.815158509402329,1.),(1.,0.816179044148147,
1.),(1.,0.817226308119943,1.),(1.,0.818301939488811,1.)))
REPRESENTATION_ITEM('')
SURFACE()
);
#2354=(
BOUNDED_SURFACE()
B_SPLINE_SURFACE(3,2,((#380951,#380952,#380953),(#380954,#380955,#380956),
(#380957,#380958,#380959),(#380960,#380961,#380962)),.UNSPECIFIED.,.F.,
 .F.,.F.)
B_SPLINE_SURFACE_WITH_KNOTS((4,4),(3,3),(1.55009486301137E-5,4.9206551047443E-5),
(-8.13759513938222E-5,1.),.UNSPECIFIED.)
GEOMETRIC_REPRESENTATION_ITEM()
RATIONAL_B_SPLINE_SURFACE(((1.00002372912333,0.854200639599693,1.),(1.00001423585992,
0.912530301180551,1.),(1.0000071055047,0.956341495377431,1.),(1.00001238975907,
0.923873338137031,1.)))
REPRESENTATION_ITEM('')
SURFACE()
);
#2355=(
BOUNDED_SURFACE()
B_SPLINE_SURFACE(3,2,((#380966,#380967,#380968),(#380969,#380970,#380971),
(#380972,#380973,#380974),(#380975,#380976,#380977)),.UNSPECIFIED.,.F.,
 .F.,.F.)
B_SPLINE_SURFACE_WITH_KNOTS((4,4),(3,3),(-3.39934179457771E-6,3.73927597403564E-5),
(-0.00186004067387202,1.00069373317419),.UNSPECIFIED.)
GEOMETRIC_REPRESENTATION_ITEM()
RATIONAL_B_SPLINE_SURFACE(((1.00072100136042,0.806051963875442,1.00026859642683),
(1.00060048440144,0.838470803558734,1.00022369994489),(1.00053106448786,
0.857144632272446,1.00019783877213),(1.00054515072843,0.853355459539176,
1.00020308635431)))
REPRESENTATION_ITEM('')
SURFACE()
);
#2356=(
BOUNDED_SURFACE()
B_SPLINE_SURFACE(3,2,((#380979,#380980,#380981),(#380982,#380983,#380984),
(#380985,#380986,#380987),(#380988,#380989,#380990)),.UNSPECIFIED.,.F.,
 .F.,.F.)
B_SPLINE_SURFACE_WITH_KNOTS((4,4),(3,3),(-5.42101086242752E-20,9.54361881492173E-5),
(0.,1.),.UNSPECIFIED.)
GEOMETRIC_REPRESENTATION_ITEM()
RATIONAL_B_SPLINE_SURFACE(((1.,0.816715621142041,1.),(1.,0.815907587407945,
1.),(1.,0.815115959345203,1.),(1.,0.814339887349193,1.)))
REPRESENTATION_ITEM('')
SURFACE()
);
#2357=(
BOUNDED_SURFACE()
B_SPLINE_SURFACE(3,2,((#380992,#380993,#380994),(#380995,#380996,#380997),
(#380998,#380999,#381000),(#381001,#381002,#381003)),.UNSPECIFIED.,.F.,
 .F.,.F.)
B_SPLINE_SURFACE_WITH_KNOTS((4,4),(3,3),(-6.94567016748526E-20,4.68197758448209E-5),
(0.,1.),.UNSPECIFIED.)
GEOMETRIC_REPRESENTATION_ITEM()
RATIONAL_B_SPLINE_SURFACE(((1.,0.816715621142046,1.),(1.,0.953638980025212,
1.),(1.,0.954506925408061,1.),(1.,0.816715621142055,1.)))
REPRESENTATION_ITEM('')
SURFACE()
);
#2358=(
BOUNDED_SURFACE()
B_SPLINE_SURFACE(3,2,((#381005,#381006,#381007),(#381008,#381009,#381010),
(#381011,#381012,#381013),(#381014,#381015,#381016)),.UNSPECIFIED.,.F.,
 .F.,.F.)
B_SPLINE_SURFACE_WITH_KNOTS((4,4),(3,3),(0.,9.54361881492177E-5),(0.,1.),
 .UNSPECIFIED.)
GEOMETRIC_REPRESENTATION_ITEM()
RATIONAL_B_SPLINE_SURFACE(((1.,0.814339887349197,1.),(1.,0.815115959345203,
1.),(1.,0.815907587407944,1.),(1.,0.816715621142052,1.)))
REPRESENTATION_ITEM('')
SURFACE()
);
#2359=(
BOUNDED_SURFACE()
B_SPLINE_SURFACE(3,2,((#381018,#381019,#381020),(#381021,#381022,#381023),
(#381024,#381025,#381026),(#381027,#381028,#381029)),.UNSPECIFIED.,.F.,
 .F.,.F.)
B_SPLINE_SURFACE_WITH_KNOTS((4,4),(3,3),(-3.39528393502478E-6,3.73481232852734E-5),
(-0.00165018033339765,1.),.UNSPECIFIED.)
GEOMETRIC_REPRESENTATION_ITEM()
RATIONAL_B_SPLINE_SURFACE(((1.00048354385569,0.853487571660387,1.),(1.00047110510924,
0.857256476851426,1.),(1.00053193201111,0.838826096655854,1.),(1.0006397068773,
0.806170615310073,1.)))
REPRESENTATION_ITEM('')
SURFACE()
);
#2360=(
BOUNDED_SURFACE()
B_SPLINE_SURFACE(3,2,((#381033,#381034,#381035),(#381036,#381037,#381038),
(#381039,#381040,#381041),(#381042,#381043,#381044)),.UNSPECIFIED.,.F.,
 .F.,.F.)
B_SPLINE_SURFACE_WITH_KNOTS((4,4),(3,3),(2.02993869230509E-5,5.39756952687123E-5),
(-0.000116281069965564,1.),.UNSPECIFIED.)
GEOMETRIC_REPRESENTATION_ITEM()
RATIONAL_B_SPLINE_SURFACE(((1.0000177047973,0.923870681143007,1.),(1.00001014104059,
0.956394275543447,1.),(1.00002037300279,0.912397594905618,1.),(1.0000339085947,
0.854195550869732,1.)))
REPRESENTATION_ITEM('')
SURFACE()
);
#2361=(
BOUNDED_SURFACE()
B_SPLINE_SURFACE(3,2,((#381137,#381138,#381139),(#381140,#381141,#381142),
(#381143,#381144,#381145),(#381146,#381147,#381148)),.UNSPECIFIED.,.F.,
 .F.,.F.)
B_SPLINE_SURFACE_WITH_KNOTS((4,4),(3,3),(0.00135801595889393,0.00148409170619832),
(0.,1.),.UNSPECIFIED.)
GEOMETRIC_REPRESENTATION_ITEM()
RATIONAL_B_SPLINE_SURFACE(((1.,0.818301933966441,1.),(1.,0.81722661317235,
1.),(1.,0.816179643373941,1.),(1.,0.815159387863647,1.)))
REPRESENTATION_ITEM('')
SURFACE()
);
#2362=(
BOUNDED_SURFACE()
B_SPLINE_SURFACE(3,2,((#381187,#381188,#381189),(#381190,#381191,#381192),
(#381193,#381194,#381195),(#381196,#381197,#381198)),.UNSPECIFIED.,.F.,
 .F.,.F.)
B_SPLINE_SURFACE_WITH_KNOTS((4,4),(3,3),(-1.5474443512207E-6,1.54744435122068E-5),
(-0.0151698983641212,1.01516989835814),.UNSPECIFIED.)
GEOMETRIC_REPRESENTATION_ITEM()
RATIONAL_B_SPLINE_SURFACE(((1.02018382473226,0.324498219413555,1.02018382472418),
(1.00401234488878,0.865716921710647,1.00401234488718),(1.00033622856785,
0.988747276629687,1.00033622856772),(1.,1.,1.)))
REPRESENTATION_ITEM('')
SURFACE()
);
#2363=(
BOUNDED_SURFACE()
B_SPLINE_SURFACE(3,2,((#381200,#381201,#381202),(#381203,#381204,#381205),
(#381206,#381207,#381208),(#381209,#381210,#381211)),.UNSPECIFIED.,.F.,
 .F.,.F.)
B_SPLINE_SURFACE_WITH_KNOTS((4,4),(3,3),(0.00137194782501028,0.00149814269699235),
(0.,1.),.UNSPECIFIED.)
GEOMETRIC_REPRESENTATION_ITEM()
RATIONAL_B_SPLINE_SURFACE(((1.,0.815158509402315,1.),(1.,0.816179044148158,
1.),(1.,0.817226308119926,1.),(1.,0.818301939488807,1.)))
REPRESENTATION_ITEM('')
SURFACE()
);
#2364=(
BOUNDED_SURFACE()
B_SPLINE_SURFACE(3,2,((#381255,#381256,#381257),(#381258,#381259,#381260),
(#381261,#381262,#381263),(#381264,#381265,#381266)),.UNSPECIFIED.,.F.,
 .F.,.F.)
B_SPLINE_SURFACE_WITH_KNOTS((4,4),(3,3),(1.55009486301137E-5,4.9206551047443E-5),
(-8.13759514042935E-5,1.),.UNSPECIFIED.)
GEOMETRIC_REPRESENTATION_ITEM()
RATIONAL_B_SPLINE_SURFACE(((1.00002372912333,0.854200639599698,1.),(1.00001423585992,
0.912530301180538,1.),(1.0000071055047,0.956341495377442,1.),(1.00001238975907,
0.923873338137026,1.)))
REPRESENTATION_ITEM('')
SURFACE()
);
#2365=(
BOUNDED_SURFACE()
B_SPLINE_SURFACE(3,2,((#381270,#381271,#381272),(#381273,#381274,#381275),
(#381276,#381277,#381278),(#381279,#381280,#381281)),.UNSPECIFIED.,.F.,
 .F.,.F.)
B_SPLINE_SURFACE_WITH_KNOTS((4,4),(3,3),(-3.39934179457819E-6,3.73927597403567E-5),
(-0.00186004067378984,1.00069373317421),.UNSPECIFIED.)
GEOMETRIC_REPRESENTATION_ITEM()
RATIONAL_B_SPLINE_SURFACE(((1.00072100136039,0.80605196387545,1.00026859642684),
(1.00060048440141,0.838470803558752,1.0002236999449),(1.00053106448783,
0.85714463227244,1.00019783877214),(1.00054515072841,0.853355459539185,
1.00020308635432)))
REPRESENTATION_ITEM('')
SURFACE()
);
#2366=(
BOUNDED_SURFACE()
B_SPLINE_SURFACE(3,2,((#381283,#381284,#381285),(#381286,#381287,#381288),
(#381289,#381290,#381291),(#381292,#381293,#381294)),.UNSPECIFIED.,.F.,
 .F.,.F.)
B_SPLINE_SURFACE_WITH_KNOTS((4,4),(3,3),(-5.42101086242752E-20,9.54361881492172E-5),
(0.,1.),.UNSPECIFIED.)
GEOMETRIC_REPRESENTATION_ITEM()
RATIONAL_B_SPLINE_SURFACE(((1.,0.816715621142048,1.),(1.,0.815907587407955,
1.),(1.,0.815115959345183,1.),(1.,0.814339887349201,1.)))
REPRESENTATION_ITEM('')
SURFACE()
);
#2367=(
BOUNDED_SURFACE()
B_SPLINE_SURFACE(3,2,((#381296,#381297,#381298),(#381299,#381300,#381301),
(#381302,#381303,#381304),(#381305,#381306,#381307)),.UNSPECIFIED.,.F.,
 .F.,.F.)
B_SPLINE_SURFACE_WITH_KNOTS((4,4),(3,3),(2.87991202066462E-20,4.6819775844821E-5),
(0.,1.),.UNSPECIFIED.)
GEOMETRIC_REPRESENTATION_ITEM()
RATIONAL_B_SPLINE_SURFACE(((1.,0.816715621142047,1.),(1.,0.953638980025212,
1.),(1.,0.954506925408053,1.),(1.,0.816715621142048,1.)))
REPRESENTATION_ITEM('')
SURFACE()
);
#2368=(
BOUNDED_SURFACE()
B_SPLINE_SURFACE(3,2,((#381309,#381310,#381311),(#381312,#381313,#381314),
(#381315,#381316,#381317),(#381318,#381319,#381320)),.UNSPECIFIED.,.F.,
 .F.,.F.)
B_SPLINE_SURFACE_WITH_KNOTS((4,4),(3,3),(-1.62630325872826E-19,9.54361881492175E-5),
(0.,1.),.UNSPECIFIED.)
GEOMETRIC_REPRESENTATION_ITEM()
RATIONAL_B_SPLINE_SURFACE(((1.,0.814339887349191,1.),(1.,0.815115959345201,
1.),(1.,0.81590758740795,1.),(1.,0.816715621142048,1.)))
REPRESENTATION_ITEM('')
SURFACE()
);
#2369=(
BOUNDED_SURFACE()
B_SPLINE_SURFACE(3,2,((#381322,#381323,#381324),(#381325,#381326,#381327),
(#381328,#381329,#381330),(#381331,#381332,#381333)),.UNSPECIFIED.,.F.,
 .F.,.F.)
B_SPLINE_SURFACE_WITH_KNOTS((4,4),(3,3),(-3.39528393502376E-6,3.73481232852727E-5),
(-0.00165018033296025,1.),.UNSPECIFIED.)
GEOMETRIC_REPRESENTATION_ITEM()
RATIONAL_B_SPLINE_SURFACE(((1.00048354385556,0.853487571660445,1.),(1.00047110510911,
0.857256476851498,1.),(1.00053193201097,0.838826096655924,1.),(1.00063970687713,
0.806170615310152,1.)))
REPRESENTATION_ITEM('')
SURFACE()
);
#2370=(
BOUNDED_SURFACE()
B_SPLINE_SURFACE(3,2,((#381337,#381338,#381339),(#381340,#381341,#381342),
(#381343,#381344,#381345),(#381346,#381347,#381348)),.UNSPECIFIED.,.F.,
 .F.,.F.)
B_SPLINE_SURFACE_WITH_KNOTS((4,4),(3,3),(2.0299386923051E-5,5.39756952686909E-5),
(-0.000116281070037132,1.),.UNSPECIFIED.)
GEOMETRIC_REPRESENTATION_ITEM()
RATIONAL_B_SPLINE_SURFACE(((1.00001770479732,0.923870681143002,1.),(1.0000101410406,
0.956394275543398,1.),(1.0000203730028,0.91239759490568,1.),(1.00003390859472,
0.854195550869837,1.)))
REPRESENTATION_ITEM('')
SURFACE()
);
#2371=(
BOUNDED_SURFACE()
B_SPLINE_SURFACE(3,2,((#381441,#381442,#381443),(#381444,#381445,#381446),
(#381447,#381448,#381449),(#381450,#381451,#381452)),.UNSPECIFIED.,.F.,
 .F.,.F.)
B_SPLINE_SURFACE_WITH_KNOTS((4,4),(3,3),(0.00135801595889393,0.00148409170619832),
(0.,1.),.UNSPECIFIED.)
GEOMETRIC_REPRESENTATION_ITEM()
RATIONAL_B_SPLINE_SURFACE(((1.,0.818301933966442,1.),(1.,0.817226613172349,
1.),(1.,0.816179643373945,1.),(1.,0.815159387863655,1.)))
REPRESENTATION_ITEM('')
SURFACE()
);
#2372=(
BOUNDED_SURFACE()
B_SPLINE_SURFACE(3,2,((#381491,#381492,#381493),(#381494,#381495,#381496),
(#381497,#381498,#381499),(#381500,#381501,#381502)),.UNSPECIFIED.,.F.,
 .F.,.F.)
B_SPLINE_SURFACE_WITH_KNOTS((4,4),(3,3),(-1.54744435122081E-6,1.54744435122079E-5),
(-0.0151698983621951,1.),.UNSPECIFIED.)
GEOMETRIC_REPRESENTATION_ITEM()
RATIONAL_B_SPLINE_SURFACE(((1.02018382472966,0.334740937356506,1.),(1.00401234488827,
0.867753072813274,1.),(1.00033622856781,0.988917903080871,1.),(1.,1.,1.)))
REPRESENTATION_ITEM('')
SURFACE()
);
#2373=(
BOUNDED_SURFACE()
B_SPLINE_SURFACE(3,2,((#381504,#381505,#381506),(#381507,#381508,#381509),
(#381510,#381511,#381512),(#381513,#381514,#381515)),.UNSPECIFIED.,.F.,
 .F.,.F.)
B_SPLINE_SURFACE_WITH_KNOTS((4,4),(3,3),(0.00137194782501028,0.00149814269699235),
(0.,1.),.UNSPECIFIED.)
GEOMETRIC_REPRESENTATION_ITEM()
RATIONAL_B_SPLINE_SURFACE(((1.,0.815158509402317,1.),(1.,0.81617904414816,
1.),(1.,0.817226308119932,1.),(1.,0.818301939488811,1.)))
REPRESENTATION_ITEM('')
SURFACE()
);
#2374=(
BOUNDED_SURFACE()
B_SPLINE_SURFACE(3,2,((#381559,#381560,#381561),(#381562,#381563,#381564),
(#381565,#381566,#381567),(#381568,#381569,#381570)),.UNSPECIFIED.,.F.,
 .F.,.F.)
B_SPLINE_SURFACE_WITH_KNOTS((4,4),(3,3),(1.55009486301137E-5,4.92065510474435E-5),
(-8.13759516055901E-5,1.),.UNSPECIFIED.)
GEOMETRIC_REPRESENTATION_ITEM()
RATIONAL_B_SPLINE_SURFACE(((1.00002372912339,0.854200639599675,1.),(1.00001423585996,
0.91253030118052,1.),(1.00000710550472,0.956341495377425,1.),(1.0000123897591,
0.923873338137014,1.)))
REPRESENTATION_ITEM('')
SURFACE()
);
#2375=(
BOUNDED_SURFACE()
B_SPLINE_SURFACE(3,2,((#381574,#381575,#381576),(#381577,#381578,#381579),
(#381580,#381581,#381582),(#381583,#381584,#381585)),.UNSPECIFIED.,.F.,
 .F.,.F.)
B_SPLINE_SURFACE_WITH_KNOTS((4,4),(3,3),(-3.39934179457775E-6,3.73927597403566E-5),
(-0.00186004067423228,1.00069373317438),.UNSPECIFIED.)
GEOMETRIC_REPRESENTATION_ITEM()
RATIONAL_B_SPLINE_SURFACE(((1.00072100136056,0.806051963875337,1.0002685964269),
(1.00060048440155,0.838470803558647,1.00022369994495),(1.00053106448796,
0.857144632272365,1.00019783877219),(1.00054515072854,0.853355459539096,
1.00020308635436)))
REPRESENTATION_ITEM('')
SURFACE()
);
#2376=(
BOUNDED_SURFACE()
B_SPLINE_SURFACE(3,2,((#381587,#381588,#381589),(#381590,#381591,#381592),
(#381593,#381594,#381595),(#381596,#381597,#381598)),.UNSPECIFIED.,.F.,
 .F.,.F.)
B_SPLINE_SURFACE_WITH_KNOTS((4,4),(3,3),(-3.79470760369927E-19,9.54361881492172E-5),
(0.,1.),.UNSPECIFIED.)
GEOMETRIC_REPRESENTATION_ITEM()
RATIONAL_B_SPLINE_SURFACE(((1.,0.81671562114205,1.),(1.,0.815907587407947,
1.),(1.,0.815115959345205,1.),(1.,0.814339887349194,1.)))
REPRESENTATION_ITEM('')
SURFACE()
);
#2377=(
BOUNDED_SURFACE()
B_SPLINE_SURFACE(3,2,((#381600,#381601,#381602),(#381603,#381604,#381605),
(#381606,#381607,#381608),(#381609,#381610,#381611)),.UNSPECIFIED.,.F.,
 .F.,.F.)
B_SPLINE_SURFACE_WITH_KNOTS((4,4),(3,3),(-1.27054942088145E-19,4.68197758448207E-5),
(0.,1.),.UNSPECIFIED.)
GEOMETRIC_REPRESENTATION_ITEM()
RATIONAL_B_SPLINE_SURFACE(((1.,0.816715621142049,1.),(1.,0.953638980025204,
1.),(1.,0.954506925408054,1.),(1.,0.816715621142057,1.)))
REPRESENTATION_ITEM('')
SURFACE()
);
#2378=(
BOUNDED_SURFACE()
B_SPLINE_SURFACE(3,2,((#381613,#381614,#381615),(#381616,#381617,#381618),
(#381619,#381620,#381621),(#381622,#381623,#381624)),.UNSPECIFIED.,.F.,
 .F.,.F.)
B_SPLINE_SURFACE_WITH_KNOTS((4,4),(3,3),(-1.0842021724855E-19,9.54361881492175E-5),
(0.,1.),.UNSPECIFIED.)
GEOMETRIC_REPRESENTATION_ITEM()
RATIONAL_B_SPLINE_SURFACE(((1.,0.814339887349193,1.),(1.,0.81511595934522,
1.),(1.,0.815907587407938,1.),(1.,0.81671562114205,1.)))
REPRESENTATION_ITEM('')
SURFACE()
);
#2379=(
BOUNDED_SURFACE()
B_SPLINE_SURFACE(3,2,((#381626,#381627,#381628),(#381629,#381630,#381631),
(#381632,#381633,#381634),(#381635,#381636,#381637)),.UNSPECIFIED.,.F.,
 .F.,.F.)
B_SPLINE_SURFACE_WITH_KNOTS((4,4),(3,3),(-3.39528393502485E-6,3.73481232852735E-5),
(-0.00165018033289677,1.),.UNSPECIFIED.)
GEOMETRIC_REPRESENTATION_ITEM()
RATIONAL_B_SPLINE_SURFACE(((1.00048354385554,0.853487571660458,1.),(1.0004711051091,
0.857256476851515,1.),(1.00053193201095,0.838826096655935,1.),(1.00063970687711,
0.806170615310171,1.)))
REPRESENTATION_ITEM('')
SURFACE()
);
#2380=(
BOUNDED_SURFACE()
B_SPLINE_SURFACE(3,2,((#381641,#381642,#381643),(#381644,#381645,#381646),
(#381647,#381648,#381649),(#381650,#381651,#381652)),.UNSPECIFIED.,.F.,
 .F.,.F.)
B_SPLINE_SURFACE_WITH_KNOTS((4,4),(3,3),(2.02993869230508E-5,5.39756952686903E-5),
(-0.000116281069679975,1.),.UNSPECIFIED.)
GEOMETRIC_REPRESENTATION_ITEM()
RATIONAL_B_SPLINE_SURFACE(((1.00001770479726,0.923870681143028,1.),(1.00001014104057,
0.956394275543431,1.),(1.00002037300274,0.912397594905693,1.),(1.00003390859462,
0.854195550869887,1.)))
REPRESENTATION_ITEM('')
SURFACE()
);
#2381=(
BOUNDED_SURFACE()
B_SPLINE_SURFACE(3,2,((#381745,#381746,#381747),(#381748,#381749,#381750),
(#381751,#381752,#381753),(#381754,#381755,#381756)),.UNSPECIFIED.,.F.,
 .F.,.F.)
B_SPLINE_SURFACE_WITH_KNOTS((4,4),(3,3),(0.00135801595889393,0.00148409170619832),
(0.,1.),.UNSPECIFIED.)
GEOMETRIC_REPRESENTATION_ITEM()
RATIONAL_B_SPLINE_SURFACE(((1.,0.818301933966442,1.),(1.,0.817226613172351,
1.),(1.,0.816179643373944,1.),(1.,0.815159387863653,1.)))
REPRESENTATION_ITEM('')
SURFACE()
);
#2382=(
BOUNDED_SURFACE()
B_SPLINE_SURFACE(3,2,((#381795,#381796,#381797),(#381798,#381799,#381800),
(#381801,#381802,#381803),(#381804,#381805,#381806)),.UNSPECIFIED.,.F.,
 .F.,.F.)
B_SPLINE_SURFACE_WITH_KNOTS((4,4),(3,3),(-1.54744435122086E-6,1.54744435122087E-5),
(-0.0151698983707459,1.01516989835136),.UNSPECIFIED.)
GEOMETRIC_REPRESENTATION_ITEM()
RATIONAL_B_SPLINE_SURFACE(((1.02018382474121,0.324498219413668,1.02018382471503),
(1.00401234489057,0.865716921710515,1.00401234488536),(1.000336228568,0.988747276629717,
1.00033622856756),(1.,1.,1.)))
REPRESENTATION_ITEM('')
SURFACE()
);
#2383=(
BOUNDED_SURFACE()
B_SPLINE_SURFACE(3,2,((#381808,#381809,#381810),(#381811,#381812,#381813),
(#381814,#381815,#381816),(#381817,#381818,#381819)),.UNSPECIFIED.,.F.,
 .F.,.F.)
B_SPLINE_SURFACE_WITH_KNOTS((4,4),(3,3),(0.00137194782501028,0.00149814269699235),
(0.,1.),.UNSPECIFIED.)
GEOMETRIC_REPRESENTATION_ITEM()
RATIONAL_B_SPLINE_SURFACE(((1.,0.815158509402316,1.),(1.,0.816179044148168,
1.),(1.,0.817226308119923,1.),(1.,0.81830193948881,1.)))
REPRESENTATION_ITEM('')
SURFACE()
);
#2384=(
BOUNDED_SURFACE()
B_SPLINE_SURFACE(3,2,((#381863,#381864,#381865),(#381866,#381867,#381868),
(#381869,#381870,#381871),(#381872,#381873,#381874)),.UNSPECIFIED.,.F.,
 .F.,.F.)
B_SPLINE_SURFACE_WITH_KNOTS((4,4),(3,3),(1.55009486301137E-5,4.92065510474433E-5),
(-8.13759517471266E-5,1.),.UNSPECIFIED.)
GEOMETRIC_REPRESENTATION_ITEM()
RATIONAL_B_SPLINE_SURFACE(((1.00002372912343,0.854200639599643,1.),(1.00001423585998,
0.912530301180509,1.),(1.00000710550473,0.956341495377418,1.),(1.00001238975912,
0.923873338136999,1.)))
REPRESENTATION_ITEM('')
SURFACE()
);
#2385=(
BOUNDED_SURFACE()
B_SPLINE_SURFACE(3,2,((#381878,#381879,#381880),(#381881,#381882,#381883),
(#381884,#381885,#381886),(#381887,#381888,#381889)),.UNSPECIFIED.,.F.,
 .F.,.F.)
B_SPLINE_SURFACE_WITH_KNOTS((4,4),(3,3),(-3.39934179457816E-6,3.73927597403566E-5),
(-0.00186004067451563,1.00069373317446),.UNSPECIFIED.)
GEOMETRIC_REPRESENTATION_ITEM()
RATIONAL_B_SPLINE_SURFACE(((1.00072100136067,0.806051963875284,1.00026859642693),
(1.00060048440165,0.838470803558566,1.00022369994498),(1.00053106448804,
0.857144632272327,1.00019783877221),(1.00054515072862,0.853355459539038,
1.00020308635439)))
REPRESENTATION_ITEM('')
SURFACE()
);
#2386=(
BOUNDED_SURFACE()
B_SPLINE_SURFACE(3,2,((#381891,#381892,#381893),(#381894,#381895,#381896),
(#381897,#381898,#381899),(#381900,#381901,#381902)),.UNSPECIFIED.,.F.,
 .F.,.F.)
B_SPLINE_SURFACE_WITH_KNOTS((4,4),(3,3),(2.16840434497101E-19,9.54361881492174E-5),
(0.,1.),.UNSPECIFIED.)
GEOMETRIC_REPRESENTATION_ITEM()
RATIONAL_B_SPLINE_SURFACE(((1.,0.816715621142049,1.),(1.,0.815907587407941,
1.),(1.,0.8151159593452,1.),(1.,0.814339887349195,1.)))
REPRESENTATION_ITEM('')
SURFACE()
);
#2387=(
BOUNDED_SURFACE()
B_SPLINE_SURFACE(3,2,((#381904,#381905,#381906),(#381907,#381908,#381909),
(#381910,#381911,#381912),(#381913,#381914,#381915)),.UNSPECIFIED.,.F.,
 .F.,.F.)
B_SPLINE_SURFACE_WITH_KNOTS((4,4),(3,3),(2.71050543121376E-20,4.68197758448213E-5),
(0.,1.),.UNSPECIFIED.)
GEOMETRIC_REPRESENTATION_ITEM()
RATIONAL_B_SPLINE_SURFACE(((1.,0.816715621142051,1.),(1.,0.953638980025212,
1.),(1.,0.954506925408045,1.),(1.,0.816715621142055,1.)))
REPRESENTATION_ITEM('')
SURFACE()
);
#2388=(
BOUNDED_SURFACE()
B_SPLINE_SURFACE(3,2,((#381917,#381918,#381919),(#381920,#381921,#381922),
(#381923,#381924,#381925),(#381926,#381927,#381928)),.UNSPECIFIED.,.F.,
 .F.,.F.)
B_SPLINE_SURFACE_WITH_KNOTS((4,4),(3,3),(0.,9.54361881492176E-5),(0.,1.),
 .UNSPECIFIED.)
GEOMETRIC_REPRESENTATION_ITEM()
RATIONAL_B_SPLINE_SURFACE(((1.,0.814339887349193,1.),(1.,0.815115959345204,
1.),(1.,0.815907587407941,1.),(1.,0.816715621142051,1.)))
REPRESENTATION_ITEM('')
SURFACE()
);
#2389=(
BOUNDED_SURFACE()
B_SPLINE_SURFACE(3,2,((#381930,#381931,#381932),(#381933,#381934,#381935),
(#381936,#381937,#381938),(#381939,#381940,#381941)),.UNSPECIFIED.,.F.,
 .F.,.F.)
B_SPLINE_SURFACE_WITH_KNOTS((4,4),(3,3),(-3.39528393502491E-6,3.73481232852736E-5),
(-0.0016501803332037,1.),.UNSPECIFIED.)
GEOMETRIC_REPRESENTATION_ITEM()
RATIONAL_B_SPLINE_SURFACE(((1.00048354385563,0.853487571660408,1.),(1.00047110510918,
0.857256476851472,1.),(1.00053193201105,0.83882609665589,1.),(1.00063970687722,
0.806170615310104,1.)))
REPRESENTATION_ITEM('')
SURFACE()
);
#2390=(
BOUNDED_SURFACE()
B_SPLINE_SURFACE(3,2,((#381945,#381946,#381947),(#381948,#381949,#381950),
(#381951,#381952,#381953),(#381954,#381955,#381956)),.UNSPECIFIED.,.F.,
 .F.,.F.)
B_SPLINE_SURFACE_WITH_KNOTS((4,4),(3,3),(2.02993869230507E-5,5.397569526869E-5),
(-0.00011628106952024,1.),.UNSPECIFIED.)
GEOMETRIC_REPRESENTATION_ITEM()
RATIONAL_B_SPLINE_SURFACE(((1.00001770479724,0.923870681143042,1.),(1.00001014104055,
0.956394275543437,1.),(1.00002037300271,0.912397594905713,1.),(1.00003390859457,
0.854195550869909,1.)))
REPRESENTATION_ITEM('')
SURFACE()
);
#2391=(
BOUNDED_SURFACE()
B_SPLINE_SURFACE(3,2,((#382049,#382050,#382051),(#382052,#382053,#382054),
(#382055,#382056,#382057),(#382058,#382059,#382060)),.UNSPECIFIED.,.F.,
 .F.,.F.)
B_SPLINE_SURFACE_WITH_KNOTS((4,4),(3,3),(0.00135801595889393,0.00148409170619832),
(0.,1.),.UNSPECIFIED.)
GEOMETRIC_REPRESENTATION_ITEM()
RATIONAL_B_SPLINE_SURFACE(((1.,0.818301933966448,1.),(1.,0.81722661317234,
1.),(1.,0.816179643373967,1.),(1.,0.815159387863657,1.)))
REPRESENTATION_ITEM('')
SURFACE()
);
#2392=(
BOUNDED_SURFACE()
B_SPLINE_SURFACE(3,2,((#382099,#382100,#382101),(#382102,#382103,#382104),
(#382105,#382106,#382107),(#382108,#382109,#382110)),.UNSPECIFIED.,.F.,
 .F.,.F.)
B_SPLINE_SURFACE_WITH_KNOTS((4,4),(3,3),(-1.54744435121997E-6,1.54744435122078E-5),
(-0.0151698983613011,1.01516989836171),.UNSPECIFIED.)
GEOMETRIC_REPRESENTATION_ITEM()
RATIONAL_B_SPLINE_SURFACE(((1.02018382472845,0.324498219413089,1.020183824729),
(1.00401234488803,0.865716921710524,1.00401234488814),(1.00033622856779,
0.988747276629642,1.0003362285678),(1.,1.,1.)))
REPRESENTATION_ITEM('')
SURFACE()
);
#2393=(
BOUNDED_SURFACE()
B_SPLINE_SURFACE(3,2,((#382112,#382113,#382114),(#382115,#382116,#382117),
(#382118,#382119,#382120),(#382121,#382122,#382123)),.UNSPECIFIED.,.F.,
 .F.,.F.)
B_SPLINE_SURFACE_WITH_KNOTS((4,4),(3,3),(0.00137194782501028,0.00149814269699235),
(0.,1.),.UNSPECIFIED.)
GEOMETRIC_REPRESENTATION_ITEM()
RATIONAL_B_SPLINE_SURFACE(((1.,0.815158509402318,1.),(1.,0.816179044148161,
1.),(1.,0.817226308119937,1.),(1.,0.818301939488799,1.)))
REPRESENTATION_ITEM('')
SURFACE()
);
#2394=(
BOUNDED_SURFACE()
B_SPLINE_SURFACE(3,2,((#382167,#382168,#382169),(#382170,#382171,#382172),
(#382173,#382174,#382175),(#382176,#382177,#382178)),.UNSPECIFIED.,.F.,
 .F.,.F.)
B_SPLINE_SURFACE_WITH_KNOTS((4,4),(3,3),(1.55009486301137E-5,4.92065510474436E-5),
(-8.13759516876729E-5,1.),.UNSPECIFIED.)
GEOMETRIC_REPRESENTATION_ITEM()
RATIONAL_B_SPLINE_SURFACE(((1.00002372912342,0.854200639599655,1.),(1.00001423585997,
0.912530301180514,1.),(1.00000710550473,0.95634149537743,1.),(1.00001238975912,
0.923873338137006,1.)))
REPRESENTATION_ITEM('')
SURFACE()
);
#2395=(
BOUNDED_SURFACE()
B_SPLINE_SURFACE(3,2,((#382182,#382183,#382184),(#382185,#382186,#382187),
(#382188,#382189,#382190),(#382191,#382192,#382193)),.UNSPECIFIED.,.F.,
 .F.,.F.)
B_SPLINE_SURFACE_WITH_KNOTS((4,4),(3,3),(-3.39934179457829E-6,3.73927597403564E-5),
(-0.00186004067411874,1.00069373317431),.UNSPECIFIED.)
GEOMETRIC_REPRESENTATION_ITEM()
RATIONAL_B_SPLINE_SURFACE(((1.00072100136052,0.806051963875365,1.00026859642688),
(1.00060048440152,0.838470803558694,1.00022369994493),(1.00053106448793,
0.857144632272389,1.00019783877217),(1.0005451507285,0.85335545953913,1.00020308635434)))
REPRESENTATION_ITEM('')
SURFACE()
);
#2396=(
BOUNDED_SURFACE()
B_SPLINE_SURFACE(3,2,((#382195,#382196,#382197),(#382198,#382199,#382200),
(#382201,#382202,#382203),(#382204,#382205,#382206)),.UNSPECIFIED.,.F.,
 .F.,.F.)
B_SPLINE_SURFACE_WITH_KNOTS((4,4),(3,3),(-1.0842021724855E-19,9.54361881492172E-5),
(0.,1.),.UNSPECIFIED.)
GEOMETRIC_REPRESENTATION_ITEM()
RATIONAL_B_SPLINE_SURFACE(((1.,0.816715621142054,1.),(1.,0.815907587407943,
1.),(1.,0.815115959345211,1.),(1.,0.814339887349197,1.)))
REPRESENTATION_ITEM('')
SURFACE()
);
#2397=(
BOUNDED_SURFACE()
B_SPLINE_SURFACE(3,2,((#382208,#382209,#382210),(#382211,#382212,#382213),
(#382214,#382215,#382216),(#382217,#382218,#382219)),.UNSPECIFIED.,.F.,
 .F.,.F.)
B_SPLINE_SURFACE_WITH_KNOTS((4,4),(3,3),(1.54159996400283E-19,4.68197758448204E-5),
(0.,1.),.UNSPECIFIED.)
GEOMETRIC_REPRESENTATION_ITEM()
RATIONAL_B_SPLINE_SURFACE(((1.,0.816715621142047,1.),(1.,0.953638980025207,
1.),(1.,0.954506925408052,1.),(1.,0.816715621142061,1.)))
REPRESENTATION_ITEM('')
SURFACE()
);
#2398=(
BOUNDED_SURFACE()
B_SPLINE_SURFACE(3,2,((#382221,#382222,#382223),(#382224,#382225,#382226),
(#382227,#382228,#382229),(#382230,#382231,#382232)),.UNSPECIFIED.,.F.,
 .F.,.F.)
B_SPLINE_SURFACE_WITH_KNOTS((4,4),(3,3),(2.16840434497101E-19,9.54361881492178E-5),
(0.,1.),.UNSPECIFIED.)
GEOMETRIC_REPRESENTATION_ITEM()
RATIONAL_B_SPLINE_SURFACE(((1.,0.814339887349196,1.),(1.,0.81511595934521,
1.),(1.,0.815907587407939,1.),(1.,0.816715621142047,1.)))
REPRESENTATION_ITEM('')
SURFACE()
);
#2399=(
BOUNDED_SURFACE()
B_SPLINE_SURFACE(3,2,((#382234,#382235,#382236),(#382237,#382238,#382239),
(#382240,#382241,#382242),(#382243,#382244,#382245)),.UNSPECIFIED.,.F.,
 .F.,.F.)
B_SPLINE_SURFACE_WITH_KNOTS((4,4),(3,3),(-3.39528393502487E-6,3.73481232852735E-5),
(-0.00165018033261962,1.),.UNSPECIFIED.)
GEOMETRIC_REPRESENTATION_ITEM()
RATIONAL_B_SPLINE_SURFACE(((1.00048354385546,0.853487571660497,1.),(1.00047110510902,
0.857256476851547,1.),(1.00053193201086,0.838826096655987,1.),(1.000639706877,
0.806170615310215,1.)))
REPRESENTATION_ITEM('')
SURFACE()
);
#2400=(
BOUNDED_SURFACE()
B_SPLINE_SURFACE(3,2,((#382249,#382250,#382251),(#382252,#382253,#382254),
(#382255,#382256,#382257),(#382258,#382259,#382260)),.UNSPECIFIED.,.F.,
 .F.,.F.)
B_SPLINE_SURFACE_WITH_KNOTS((4,4),(3,3),(2.02993869230507E-5,5.397569526869E-5),
(-0.000116281069878473,1.),.UNSPECIFIED.)
GEOMETRIC_REPRESENTATION_ITEM()
RATIONAL_B_SPLINE_SURFACE(((1.00001770479729,0.923870681143011,1.),(1.00001014104059,
0.956394275543423,1.),(1.00002037300278,0.912397594905672,1.),(1.00003390859468,
0.854195550869864,1.)))
REPRESENTATION_ITEM('')
SURFACE()
);
#2401=(
BOUNDED_SURFACE()
B_SPLINE_SURFACE(3,2,((#382353,#382354,#382355),(#382356,#382357,#382358),
(#382359,#382360,#382361),(#382362,#382363,#382364)),.UNSPECIFIED.,.F.,
 .F.,.F.)
B_SPLINE_SURFACE_WITH_KNOTS((4,4),(3,3),(0.00135801595889393,0.00148409170619832),
(0.,1.),.UNSPECIFIED.)
GEOMETRIC_REPRESENTATION_ITEM()
RATIONAL_B_SPLINE_SURFACE(((1.,0.818301933966445,1.),(1.,0.817226613172353,
1.),(1.,0.816179643373947,1.),(1.,0.815159387863659,1.)))
REPRESENTATION_ITEM('')
SURFACE()
);
#2402=(
BOUNDED_SURFACE()
B_SPLINE_SURFACE(3,2,((#382403,#382404,#382405),(#382406,#382407,#382408),
(#382409,#382410,#382411),(#382412,#382413,#382414)),.UNSPECIFIED.,.F.,
 .F.,.F.)
B_SPLINE_SURFACE_WITH_KNOTS((4,4),(3,3),(5.0821976835258E-20,1.54744435122074E-5),
(0.,1.),.UNSPECIFIED.)
GEOMETRIC_REPRESENTATION_ITEM()
RATIONAL_B_SPLINE_SURFACE(((1.,0.478041569704972,1.),(1.,0.890533857552081,
1.),(1.,0.990075913815901,1.),(1.,1.,1.)))
REPRESENTATION_ITEM('')
SURFACE()
);
#2403=(
BOUNDED_SURFACE()
B_SPLINE_SURFACE(3,2,((#382416,#382417,#382418),(#382419,#382420,#382421),
(#382422,#382423,#382424),(#382425,#382426,#382427)),.UNSPECIFIED.,.F.,
 .F.,.F.)
B_SPLINE_SURFACE_WITH_KNOTS((4,4),(3,3),(0.00137194782501028,0.00149814269699235),
(0.,1.),.UNSPECIFIED.)
GEOMETRIC_REPRESENTATION_ITEM()
RATIONAL_B_SPLINE_SURFACE(((1.,0.815158509402316,1.),(1.,0.81617904414817,
1.),(1.,0.817226308119927,1.),(1.,0.818301939488812,1.)))
REPRESENTATION_ITEM('')
SURFACE()
);
#2404=(
BOUNDED_SURFACE()
B_SPLINE_SURFACE(3,2,((#382471,#382472,#382473),(#382474,#382475,#382476),
(#382477,#382478,#382479),(#382480,#382481,#382482)),.UNSPECIFIED.,.F.,
 .F.,.F.)
B_SPLINE_SURFACE_WITH_KNOTS((4,4),(3,3),(1.55009486301137E-5,4.92065510474426E-5),
(-8.13759511169527E-5,1.),.UNSPECIFIED.)
GEOMETRIC_REPRESENTATION_ITEM()
RATIONAL_B_SPLINE_SURFACE(((1.00002372912325,0.854200639599739,1.),(1.00001423585987,
0.912530301180574,1.),(1.00000710550468,0.956341495377443,1.),(1.00001238975903,
0.92387333813705,1.)))
REPRESENTATION_ITEM('')
SURFACE()
);
#2405=(
BOUNDED_SURFACE()
B_SPLINE_SURFACE(3,2,((#382486,#382487,#382488),(#382489,#382490,#382491),
(#382492,#382493,#382494),(#382495,#382496,#382497)),.UNSPECIFIED.,.F.,
 .F.,.F.)
B_SPLINE_SURFACE_WITH_KNOTS((4,4),(3,3),(-3.39934179457774E-6,3.73927597403568E-5),
(-0.00186004067399766,1.00069373317424),.UNSPECIFIED.)
GEOMETRIC_REPRESENTATION_ITEM()
RATIONAL_B_SPLINE_SURFACE(((1.00072100136047,0.806051963875431,1.00026859642685),
(1.00060048440148,0.838470803558688,1.00022369994491),(1.00053106448789,
0.857144632272437,1.00019783877215),(1.00054515072847,0.853355459539152,
1.00020308635432)))
REPRESENTATION_ITEM('')
SURFACE()
);
#2406=(
BOUNDED_SURFACE()
B_SPLINE_SURFACE(3,2,((#382499,#382500,#382501),(#382502,#382503,#382504),
(#382505,#382506,#382507),(#382508,#382509,#382510)),.UNSPECIFIED.,.F.,
 .F.,.F.)
B_SPLINE_SURFACE_WITH_KNOTS((4,4),(3,3),(-2.71050543121376E-19,9.54361881492173E-5),
(0.,1.),.UNSPECIFIED.)
GEOMETRIC_REPRESENTATION_ITEM()
RATIONAL_B_SPLINE_SURFACE(((1.,0.81671562114205,1.),(1.,0.815907587407946,
1.),(1.,0.815115959345205,1.),(1.,0.814339887349197,1.)))
REPRESENTATION_ITEM('')
SURFACE()
);
#2407=(
BOUNDED_SURFACE()
B_SPLINE_SURFACE(3,2,((#382512,#382513,#382514),(#382515,#382516,#382517),
(#382518,#382519,#382520),(#382521,#382522,#382523)),.UNSPECIFIED.,.F.,
 .F.,.F.)
B_SPLINE_SURFACE_WITH_KNOTS((4,4),(3,3),(1.06726151354042E-19,4.68197758448204E-5),
(0.,1.),.UNSPECIFIED.)
GEOMETRIC_REPRESENTATION_ITEM()
RATIONAL_B_SPLINE_SURFACE(((1.,0.816715621142051,1.),(1.,0.9536389800252,
1.),(1.,0.954506925408061,1.),(1.,0.81671562114205,1.)))
REPRESENTATION_ITEM('')
SURFACE()
);
#2408=(
BOUNDED_SURFACE()
B_SPLINE_SURFACE(3,2,((#382525,#382526,#382527),(#382528,#382529,#382530),
(#382531,#382532,#382533),(#382534,#382535,#382536)),.UNSPECIFIED.,.F.,
 .F.,.F.)
B_SPLINE_SURFACE_WITH_KNOTS((4,4),(3,3),(5.42101086242752E-20,9.54361881492178E-5),
(0.,1.),.UNSPECIFIED.)
GEOMETRIC_REPRESENTATION_ITEM()
RATIONAL_B_SPLINE_SURFACE(((1.,0.814339887349194,1.),(1.,0.81511595934521,
1.),(1.,0.81590758740794,1.),(1.,0.816715621142051,1.)))
REPRESENTATION_ITEM('')
SURFACE()
);
#2409=(
BOUNDED_SURFACE()
B_SPLINE_SURFACE(3,2,((#382538,#382539,#382540),(#382541,#382542,#382543),
(#382544,#382545,#382546),(#382547,#382548,#382549)),.UNSPECIFIED.,.F.,
 .F.,.F.)
B_SPLINE_SURFACE_WITH_KNOTS((4,4),(3,3),(-3.3952839350248E-6,3.73481232852729E-5),
(-0.00165018033267285,1.),.UNSPECIFIED.)
GEOMETRIC_REPRESENTATION_ITEM()
RATIONAL_B_SPLINE_SURFACE(((1.00048354385548,0.853487571660492,1.),(1.00047110510903,
0.857256476851548,1.),(1.00053193201088,0.838826096655974,1.),(1.00063970687702,
0.80617061531021,1.)))
REPRESENTATION_ITEM('')
SURFACE()
);
#2410=(
BOUNDED_SURFACE()
B_SPLINE_SURFACE(3,2,((#382553,#382554,#382555),(#382556,#382557,#382558),
(#382559,#382560,#382561),(#382562,#382563,#382564)),.UNSPECIFIED.,.F.,
 .F.,.F.)
B_SPLINE_SURFACE_WITH_KNOTS((4,4),(3,3),(2.02993869230509E-5,5.39756952686904E-5),
(-0.000116281069613679,1.),.UNSPECIFIED.)
GEOMETRIC_REPRESENTATION_ITEM()
RATIONAL_B_SPLINE_SURFACE(((1.00001770479725,0.923870681143035,1.),(1.00001014104056,
0.956394275543439,1.),(1.00002037300273,0.91239759490569,1.),(1.0000339085946,
0.854195550869901,1.)))
REPRESENTATION_ITEM('')
SURFACE()
);
#2411=(
BOUNDED_SURFACE()
B_SPLINE_SURFACE(3,2,((#382657,#382658,#382659),(#382660,#382661,#382662),
(#382663,#382664,#382665),(#382666,#382667,#382668)),.UNSPECIFIED.,.F.,
 .F.,.F.)
B_SPLINE_SURFACE_WITH_KNOTS((4,4),(3,3),(0.00135801595889393,0.00148409170619832),
(0.,1.),.UNSPECIFIED.)
GEOMETRIC_REPRESENTATION_ITEM()
RATIONAL_B_SPLINE_SURFACE(((1.,0.818301933966442,1.),(1.,0.81722661317236,
1.),(1.,0.816179643373935,1.),(1.,0.815159387863652,1.)))
REPRESENTATION_ITEM('')
SURFACE()
);
#2412=(
BOUNDED_SURFACE()
B_SPLINE_SURFACE(3,2,((#382707,#382708,#382709),(#382710,#382711,#382712),
(#382713,#382714,#382715),(#382716,#382717,#382718)),.UNSPECIFIED.,.F.,
 .F.,.F.)
B_SPLINE_SURFACE_WITH_KNOTS((4,4),(3,3),(-1.54744435122025E-6,1.54744435122093E-5),
(-0.0151698983649992,1.),.UNSPECIFIED.)
GEOMETRIC_REPRESENTATION_ITEM()
RATIONAL_B_SPLINE_SURFACE(((1.02018382473345,0.334740937354653,1.),(1.00401234488902,
0.867753072812965,1.),(1.00033622856787,0.988917903080835,1.),(1.,1.,1.)))
REPRESENTATION_ITEM('')
SURFACE()
);
#2413=(
BOUNDED_SURFACE()
B_SPLINE_SURFACE(3,2,((#382720,#382721,#382722),(#382723,#382724,#382725),
(#382726,#382727,#382728),(#382729,#382730,#382731)),.UNSPECIFIED.,.F.,
 .F.,.F.)
B_SPLINE_SURFACE_WITH_KNOTS((4,4),(3,3),(0.00137194782501028,0.00149814269699235),
(0.,1.),.UNSPECIFIED.)
GEOMETRIC_REPRESENTATION_ITEM()
RATIONAL_B_SPLINE_SURFACE(((1.,0.815158509402317,1.),(1.,0.816179044148177,
1.),(1.,0.817226308119917,1.),(1.,0.81830193948881,1.)))
REPRESENTATION_ITEM('')
SURFACE()
);
#2414=(
BOUNDED_SURFACE()
B_SPLINE_SURFACE(3,2,((#382775,#382776,#382777),(#382778,#382779,#382780),
(#382781,#382782,#382783),(#382784,#382785,#382786)),.UNSPECIFIED.,.F.,
 .F.,.F.)
B_SPLINE_SURFACE_WITH_KNOTS((4,4),(3,3),(1.55009486301137E-5,4.92065510474434E-5),
(-8.13759515751784E-5,1.),.UNSPECIFIED.)
GEOMETRIC_REPRESENTATION_ITEM()
RATIONAL_B_SPLINE_SURFACE(((1.00002372912338,0.854200639599668,1.),(1.00001423585995,
0.912530301180522,1.),(1.00000710550472,0.95634149537743,1.),(1.0000123897591,
0.923873338137017,1.)))
REPRESENTATION_ITEM('')
SURFACE()
);
#2415=(
BOUNDED_SURFACE()
B_SPLINE_SURFACE(3,2,((#382790,#382791,#382792),(#382793,#382794,#382795),
(#382796,#382797,#382798),(#382799,#382800,#382801)),.UNSPECIFIED.,.F.,
 .F.,.F.)
B_SPLINE_SURFACE_WITH_KNOTS((4,4),(3,3),(-3.39934179457739E-6,3.73927597403563E-5),
(-0.00186004067473832,1.00069373317447),.UNSPECIFIED.)
GEOMETRIC_REPRESENTATION_ITEM()
RATIONAL_B_SPLINE_SURFACE(((1.00072100136076,0.806051963875238,1.00026859642694),
(1.00060048440172,0.838470803558532,1.00022369994498),(1.0005310644881,
0.857144632272293,1.00019783877222),(1.00054515072868,0.853355459539006,
1.00020308635439)))
REPRESENTATION_ITEM('')
SURFACE()
);
#2416=(
BOUNDED_SURFACE()
B_SPLINE_SURFACE(3,2,((#382803,#382804,#382805),(#382806,#382807,#382808),
(#382809,#382810,#382811),(#382812,#382813,#382814)),.UNSPECIFIED.,.F.,
 .F.,.F.)
B_SPLINE_SURFACE_WITH_KNOTS((4,4),(3,3),(-2.16840434497101E-19,9.54361881492172E-5),
(0.,1.),.UNSPECIFIED.)
GEOMETRIC_REPRESENTATION_ITEM()
RATIONAL_B_SPLINE_SURFACE(((1.,0.816715621142048,1.),(1.,0.815907587407942,
1.),(1.,0.81511595934521,1.),(1.,0.814339887349192,1.)))
REPRESENTATION_ITEM('')
SURFACE()
);
#2417=(
BOUNDED_SURFACE()
B_SPLINE_SURFACE(3,2,((#382816,#382817,#382818),(#382819,#382820,#382821),
(#382822,#382823,#382824),(#382825,#382826,#382827)),.UNSPECIFIED.,.F.,
 .F.,.F.)
B_SPLINE_SURFACE_WITH_KNOTS((4,4),(3,3),(4.40457132572236E-20,4.68197758448206E-5),
(0.,1.),.UNSPECIFIED.)
GEOMETRIC_REPRESENTATION_ITEM()
RATIONAL_B_SPLINE_SURFACE(((1.,0.816715621142052,1.),(1.,0.953638980025205,
1.),(1.,0.954506925408055,1.),(1.,0.816715621142055,1.)))
REPRESENTATION_ITEM('')
SURFACE()
);
#2418=(
BOUNDED_SURFACE()
B_SPLINE_SURFACE(3,2,((#382829,#382830,#382831),(#382832,#382833,#382834),
(#382835,#382836,#382837),(#382838,#382839,#382840)),.UNSPECIFIED.,.F.,
 .F.,.F.)
B_SPLINE_SURFACE_WITH_KNOTS((4,4),(3,3),(0.,9.54361881492178E-5),(0.,1.),
 .UNSPECIFIED.)
GEOMETRIC_REPRESENTATION_ITEM()
RATIONAL_B_SPLINE_SURFACE(((1.,0.8143398873492,1.),(1.,0.815115959345208,
1.),(1.,0.815907587407944,1.),(1.,0.816715621142052,1.)))
REPRESENTATION_ITEM('')
SURFACE()
);
#2419=(
BOUNDED_SURFACE()
B_SPLINE_SURFACE(3,2,((#382842,#382843,#382844),(#382845,#382846,#382847),
(#382848,#382849,#382850),(#382851,#382852,#382853)),.UNSPECIFIED.,.F.,
 .F.,.F.)
B_SPLINE_SURFACE_WITH_KNOTS((4,4),(3,3),(-3.3952839350249E-6,3.73481232852737E-5),
(-0.00165018033328263,1.),.UNSPECIFIED.)
GEOMETRIC_REPRESENTATION_ITEM()
RATIONAL_B_SPLINE_SURFACE(((1.00048354385566,0.853487571660404,1.),(1.00047110510921,
0.857256476851462,1.),(1.00053193201107,0.838826096655865,1.),(1.00063970687725,
0.806170615310108,0.999999999999999)))
REPRESENTATION_ITEM('')
SURFACE()
);
#2420=(
BOUNDED_SURFACE()
B_SPLINE_SURFACE(3,2,((#382857,#382858,#382859),(#382860,#382861,#382862),
(#382863,#382864,#382865),(#382866,#382867,#382868)),.UNSPECIFIED.,.F.,
 .F.,.F.)
B_SPLINE_SURFACE_WITH_KNOTS((4,4),(3,3),(2.02993869230504E-5,5.39756952686903E-5),
(-0.000116281069376645,1.),.UNSPECIFIED.)
GEOMETRIC_REPRESENTATION_ITEM()
RATIONAL_B_SPLINE_SURFACE(((1.00001770479722,0.923870681143052,1.),(1.00001014104054,
0.956394275543437,1.),(1.00002037300269,0.912397594905733,1.),(1.00003390859453,
0.854195550869932,1.)))
REPRESENTATION_ITEM('')
SURFACE()
);
#2421=(
BOUNDED_SURFACE()
B_SPLINE_SURFACE(3,2,((#382961,#382962,#382963),(#382964,#382965,#382966),
(#382967,#382968,#382969),(#382970,#382971,#382972)),.UNSPECIFIED.,.F.,
 .F.,.F.)
B_SPLINE_SURFACE_WITH_KNOTS((4,4),(3,3),(0.00135801595889393,0.00148409170619832),
(0.,1.),.UNSPECIFIED.)
GEOMETRIC_REPRESENTATION_ITEM()
RATIONAL_B_SPLINE_SURFACE(((1.,0.818301933966446,1.),(1.,0.817226613172346,
1.),(1.,0.816179643373951,1.),(1.,0.815159387863661,1.)))
REPRESENTATION_ITEM('')
SURFACE()
);
#2422=(
BOUNDED_SURFACE()
B_SPLINE_SURFACE(3,2,((#383011,#383012,#383013),(#383014,#383015,#383016),
(#383017,#383018,#383019),(#383020,#383021,#383022)),.UNSPECIFIED.,.F.,
 .F.,.F.)
B_SPLINE_SURFACE_WITH_KNOTS((4,4),(3,3),(-1.54744435122008E-6,1.54744435122076E-5),
(-0.0151698983742707,1.01516989834804),.UNSPECIFIED.)
GEOMETRIC_REPRESENTATION_ITEM()
RATIONAL_B_SPLINE_SURFACE(((1.02018382474597,0.32449821941359,1.02018382471054),
(1.00401234489151,0.865716921710459,1.00401234488447),(1.00033622856808,
0.988747276629742,1.00033622856749),(1.,1.,1.)))
REPRESENTATION_ITEM('')
SURFACE()
);
#2423=(
BOUNDED_SURFACE()
B_SPLINE_SURFACE(3,2,((#383024,#383025,#383026),(#383027,#383028,#383029),
(#383030,#383031,#383032),(#383033,#383034,#383035)),.UNSPECIFIED.,.F.,
 .F.,.F.)
B_SPLINE_SURFACE_WITH_KNOTS((4,4),(3,3),(0.00137194782501028,0.00149814269699235),
(0.,1.),.UNSPECIFIED.)
GEOMETRIC_REPRESENTATION_ITEM()
RATIONAL_B_SPLINE_SURFACE(((1.,0.81515850940232,1.),(1.,0.816179044148172,
1.),(1.,0.817226308119918,1.),(1.,0.818301939488811,1.)))
REPRESENTATION_ITEM('')
SURFACE()
);
#2424=(
BOUNDED_SURFACE()
B_SPLINE_SURFACE(3,2,((#383079,#383080,#383081),(#383082,#383083,#383084),
(#383085,#383086,#383087),(#383088,#383089,#383090)),.UNSPECIFIED.,.F.,
 .F.,.F.)
B_SPLINE_SURFACE_WITH_KNOTS((4,4),(3,3),(1.55009486301137E-5,4.92065510474435E-5),
(-8.13759513091309E-5,1.),.UNSPECIFIED.)
GEOMETRIC_REPRESENTATION_ITEM()
RATIONAL_B_SPLINE_SURFACE(((1.00002372912331,0.854200639599711,1.),(1.0000142358599,
0.912530301180553,1.),(1.00000710550469,0.956341495377436,1.),(1.00001238975906,
0.923873338137037,1.)))
REPRESENTATION_ITEM('')
SURFACE()
);
#2425=(
BOUNDED_SURFACE()
B_SPLINE_SURFACE(3,2,((#383094,#383095,#383096),(#383097,#383098,#383099),
(#383100,#383101,#383102),(#383103,#383104,#383105)),.UNSPECIFIED.,.F.,
 .F.,.F.)
B_SPLINE_SURFACE_WITH_KNOTS((4,4),(3,3),(-3.39934179457783E-6,3.73927597403565E-5),
(-0.00186004067468424,1.00069373317467),.UNSPECIFIED.)
GEOMETRIC_REPRESENTATION_ITEM()
RATIONAL_B_SPLINE_SURFACE(((1.00072100136074,0.806051963875206,1.00026859642702),
(1.0006004844017,0.838470803558528,1.00022369994505),(1.00053106448809,
0.857144632272264,1.00019783877227),(1.00054515072867,0.853355459538992,
1.00020308635445)))
REPRESENTATION_ITEM('')
SURFACE()
);
#2426=(
BOUNDED_SURFACE()
B_SPLINE_SURFACE(3,2,((#383107,#383108,#383109),(#383110,#383111,#383112),
(#383113,#383114,#383115),(#383116,#383117,#383118)),.UNSPECIFIED.,.F.,
 .F.,.F.)
B_SPLINE_SURFACE_WITH_KNOTS((4,4),(3,3),(4.33680868994202E-19,9.54361881492176E-5),
(0.,1.),.UNSPECIFIED.)
GEOMETRIC_REPRESENTATION_ITEM()
RATIONAL_B_SPLINE_SURFACE(((1.,0.81671562114205,1.),(1.,0.815907587407954,
1.),(1.,0.815115959345207,1.),(1.,0.814339887349196,1.)))
REPRESENTATION_ITEM('')
SURFACE()
);
#2427=(
BOUNDED_SURFACE()
B_SPLINE_SURFACE(3,2,((#383120,#383121,#383122),(#383123,#383124,#383125),
(#383126,#383127,#383128),(#383129,#383130,#383131)),.UNSPECIFIED.,.F.,
 .F.,.F.)
B_SPLINE_SURFACE_WITH_KNOTS((4,4),(3,3),(1.03338019565025E-19,4.68197758448208E-5),
(0.,1.),.UNSPECIFIED.)
GEOMETRIC_REPRESENTATION_ITEM()
RATIONAL_B_SPLINE_SURFACE(((1.,0.816715621142044,1.),(1.,0.953638980025212,
1.),(1.,0.954506925408053,1.),(1.,0.81671562114205,1.)))
REPRESENTATION_ITEM('')
SURFACE()
);
#2428=(
BOUNDED_SURFACE()
B_SPLINE_SURFACE(3,2,((#383133,#383134,#383135),(#383136,#383137,#383138),
(#383139,#383140,#383141),(#383142,#383143,#383144)),.UNSPECIFIED.,.F.,
 .F.,.F.)
B_SPLINE_SURFACE_WITH_KNOTS((4,4),(3,3),(1.62630325872826E-19,9.54361881492179E-5),
(0.,1.),.UNSPECIFIED.)
GEOMETRIC_REPRESENTATION_ITEM()
RATIONAL_B_SPLINE_SURFACE(((1.,0.81433988734919,1.),(1.,0.815115959345206,
1.),(1.,0.815907587407942,1.),(1.,0.816715621142044,1.)))
REPRESENTATION_ITEM('')
SURFACE()
);
#2429=(
BOUNDED_SURFACE()
B_SPLINE_SURFACE(3,2,((#383146,#383147,#383148),(#383149,#383150,#383151),
(#383152,#383153,#383154),(#383155,#383156,#383157)),.UNSPECIFIED.,.F.,
 .F.,.F.)
B_SPLINE_SURFACE_WITH_KNOTS((4,4),(3,3),(-3.39528393502381E-6,3.73481232852734E-5),
(-0.0016501803331559,1.),.UNSPECIFIED.)
GEOMETRIC_REPRESENTATION_ITEM()
RATIONAL_B_SPLINE_SURFACE(((1.00048354385562,0.853487571660411,1.),(1.00047110510917,
0.857256476851486,1.),(1.00053193201103,0.838826096655886,1.),(1.00063970687721,
0.806170615310118,1.)))
REPRESENTATION_ITEM('')
SURFACE()
);
#2430=(
BOUNDED_SURFACE()
B_SPLINE_SURFACE(3,2,((#383161,#383162,#383163),(#383164,#383165,#383166),
(#383167,#383168,#383169),(#383170,#383171,#383172)),.UNSPECIFIED.,.F.,
 .F.,.F.)
B_SPLINE_SURFACE_WITH_KNOTS((4,4),(3,3),(2.02993869230506E-5,5.39756952686892E-5),
(-0.000116281070440117,1.),.UNSPECIFIED.)
GEOMETRIC_REPRESENTATION_ITEM()
RATIONAL_B_SPLINE_SURFACE(((1.00001770479738,0.923870681142973,1.),(1.00001014104063,
0.956394275543383,1.),(1.00002037300287,0.912397594905633,1.),(1.00003390859484,
0.854195550869773,1.)))
REPRESENTATION_ITEM('')
SURFACE()
);
#2431=(
BOUNDED_SURFACE()
B_SPLINE_SURFACE(3,2,((#383265,#383266,#383267),(#383268,#383269,#383270),
(#383271,#383272,#383273),(#383274,#383275,#383276)),.UNSPECIFIED.,.F.,
 .F.,.F.)
B_SPLINE_SURFACE_WITH_KNOTS((4,4),(3,3),(0.00135801595889393,0.00148409170619832),
(0.,1.),.UNSPECIFIED.)
GEOMETRIC_REPRESENTATION_ITEM()
RATIONAL_B_SPLINE_SURFACE(((1.,0.818301933966448,1.),(1.,0.817226613172323,
1.),(1.,0.816179643373976,1.),(1.,0.815159387863649,1.)))
REPRESENTATION_ITEM('')
SURFACE()
);
#2432=(
BOUNDED_SURFACE()
B_SPLINE_SURFACE(3,2,((#383315,#383316,#383317),(#383318,#383319,#383320),
(#383321,#383322,#383323),(#383324,#383325,#383326)),.UNSPECIFIED.,.F.,
 .F.,.F.)
B_SPLINE_SURFACE_WITH_KNOTS((4,4),(3,3),(-1.54744435122076E-6,1.54744435122075E-5),
(-0.0151698983599064,1.01516989836254),.UNSPECIFIED.)
GEOMETRIC_REPRESENTATION_ITEM()
RATIONAL_B_SPLINE_SURFACE(((1.02018382472657,0.324498219413438,1.02018382473013),
(1.00401234488766,0.865716921710524,1.00401234488836),(1.00033622856776,
0.988747276629706,1.00033622856781),(1.,1.,1.)))
REPRESENTATION_ITEM('')
SURFACE()
);
#2433=(
BOUNDED_SURFACE()
B_SPLINE_SURFACE(3,2,((#383328,#383329,#383330),(#383331,#383332,#383333),
(#383334,#383335,#383336),(#383337,#383338,#383339)),.UNSPECIFIED.,.F.,
 .F.,.F.)
B_SPLINE_SURFACE_WITH_KNOTS((4,4),(3,3),(0.00137194782501028,0.00149814269699235),
(0.,1.),.UNSPECIFIED.)
GEOMETRIC_REPRESENTATION_ITEM()
RATIONAL_B_SPLINE_SURFACE(((1.,0.815158509402314,1.),(1.,0.816179044148168,
1.),(1.,0.817226308119925,1.),(1.,0.818301939488811,1.)))
REPRESENTATION_ITEM('')
SURFACE()
);
#2434=(
BOUNDED_SURFACE()
B_SPLINE_SURFACE(3,2,((#383383,#383384,#383385),(#383386,#383387,#383388),
(#383389,#383390,#383391),(#383392,#383393,#383394)),.UNSPECIFIED.,.F.,
 .F.,.F.)
B_SPLINE_SURFACE_WITH_KNOTS((4,4),(3,3),(1.55009486301138E-5,4.92065510474435E-5),
(-8.1375951280074E-5,1.),.UNSPECIFIED.)
GEOMETRIC_REPRESENTATION_ITEM()
RATIONAL_B_SPLINE_SURFACE(((1.0000237291233,0.854200639599717,1.),(1.0000142358599,
0.912530301180554,1.),(1.00000710550469,0.956341495377434,1.),(1.00001238975905,
0.923873338137037,1.)))
REPRESENTATION_ITEM('')
SURFACE()
);
#2435=(
BOUNDED_SURFACE()
B_SPLINE_SURFACE(3,2,((#383398,#383399,#383400),(#383401,#383402,#383403),
(#383404,#383405,#383406),(#383407,#383408,#383409)),.UNSPECIFIED.,.F.,
 .F.,.F.)
B_SPLINE_SURFACE_WITH_KNOTS((4,4),(3,3),(-3.39934179457824E-6,3.73927597403564E-5),
(-0.00186004067418031,1.00069373317447),.UNSPECIFIED.)
GEOMETRIC_REPRESENTATION_ITEM()
RATIONAL_B_SPLINE_SURFACE(((1.00072100136054,0.80605196387533,1.00026859642694),
(1.00060048440154,0.838470803558632,1.00022369994498),(1.00053106448795,
0.85714463227236,1.00019783877221),(1.00054515072852,0.853355459539088,
1.00020308635439)))
REPRESENTATION_ITEM('')
SURFACE()
);
#2436=(
BOUNDED_SURFACE()
B_SPLINE_SURFACE(3,2,((#383411,#383412,#383413),(#383414,#383415,#383416),
(#383417,#383418,#383419),(#383420,#383421,#383422)),.UNSPECIFIED.,.F.,
 .F.,.F.)
B_SPLINE_SURFACE_WITH_KNOTS((4,4),(3,3),(-5.42101086242752E-20,9.54361881492176E-5),
(0.,1.),.UNSPECIFIED.)
GEOMETRIC_REPRESENTATION_ITEM()
RATIONAL_B_SPLINE_SURFACE(((1.,0.816715621142047,1.),(1.,0.815907587407942,
1.),(1.,0.815115959345202,1.),(1.,0.814339887349191,1.)))
REPRESENTATION_ITEM('')
SURFACE()
);
#2437=(
BOUNDED_SURFACE()
B_SPLINE_SURFACE(3,2,((#383424,#383425,#383426),(#383427,#383428,#383429),
(#383430,#383431,#383432),(#383433,#383434,#383435)),.UNSPECIFIED.,.F.,
 .F.,.F.)
B_SPLINE_SURFACE_WITH_KNOTS((4,4),(3,3),(-8.13151629364128E-20,4.6819775844821E-5),
(0.,1.),.UNSPECIFIED.)
GEOMETRIC_REPRESENTATION_ITEM()
RATIONAL_B_SPLINE_SURFACE(((1.,0.816715621142044,1.),(1.,0.953638980025209,
1.),(1.,0.954506925408053,1.),(1.,0.816715621142054,1.)))
REPRESENTATION_ITEM('')
SURFACE()
);
#2438=(
BOUNDED_SURFACE()
B_SPLINE_SURFACE(3,2,((#383437,#383438,#383439),(#383440,#383441,#383442),
(#383443,#383444,#383445),(#383446,#383447,#383448)),.UNSPECIFIED.,.F.,
 .F.,.F.)
B_SPLINE_SURFACE_WITH_KNOTS((4,4),(3,3),(0.,9.54361881492175E-5),(0.,1.),
 .UNSPECIFIED.)
GEOMETRIC_REPRESENTATION_ITEM()
RATIONAL_B_SPLINE_SURFACE(((1.,0.814339887349196,1.),(1.,0.815115959345203,
1.),(1.,0.815907587407943,1.),(1.,0.816715621142047,1.)))
REPRESENTATION_ITEM('')
SURFACE()
);
#2439=(
BOUNDED_SURFACE()
B_SPLINE_SURFACE(3,2,((#383450,#383451,#383452),(#383453,#383454,#383455),
(#383456,#383457,#383458),(#383459,#383460,#383461)),.UNSPECIFIED.,.F.,
 .F.,.F.)
B_SPLINE_SURFACE_WITH_KNOTS((4,4),(3,3),(-3.39528393502484E-6,3.73481232852734E-5),
(-0.0016501803333211,1.),.UNSPECIFIED.)
GEOMETRIC_REPRESENTATION_ITEM()
RATIONAL_B_SPLINE_SURFACE(((1.00048354385567,0.853487571660387,1.),(1.00047110510922,
0.85725647685146,1.),(1.00053193201109,0.838826096655864,1.),(1.00063970687727,
0.806170615310083,1.)))
REPRESENTATION_ITEM('')
SURFACE()
);
#2440=(
BOUNDED_SURFACE()
B_SPLINE_SURFACE(3,2,((#383465,#383466,#383467),(#383468,#383469,#383470),
(#383471,#383472,#383473),(#383474,#383475,#383476)),.UNSPECIFIED.,.F.,
 .F.,.F.)
B_SPLINE_SURFACE_WITH_KNOTS((4,4),(3,3),(2.02993869230507E-5,5.397569526869E-5),
(-0.000116281069781334,1.),.UNSPECIFIED.)
GEOMETRIC_REPRESENTATION_ITEM()
RATIONAL_B_SPLINE_SURFACE(((1.00001770479728,0.923870681143021,1.),(1.00001014104058,
0.956394275543415,1.),(1.00002037300276,0.912397594905702,1.),(1.00003390859465,
0.85419555086987,1.)))
REPRESENTATION_ITEM('')
SURFACE()
);
#2441=(
BOUNDED_SURFACE()
B_SPLINE_SURFACE(3,2,((#383569,#383570,#383571),(#383572,#383573,#383574),
(#383575,#383576,#383577),(#383578,#383579,#383580)),.UNSPECIFIED.,.F.,
 .F.,.F.)
B_SPLINE_SURFACE_WITH_KNOTS((4,4),(3,3),(0.00135801595889393,0.00148409170619832),
(0.,1.),.UNSPECIFIED.)
GEOMETRIC_REPRESENTATION_ITEM()
RATIONAL_B_SPLINE_SURFACE(((1.,0.818301933966444,1.),(1.,0.817226613172353,
1.),(1.,0.816179643373948,1.),(1.,0.815159387863653,1.)))
REPRESENTATION_ITEM('')
SURFACE()
);
#2442=(
BOUNDED_SURFACE()
B_SPLINE_SURFACE(3,2,((#383619,#383620,#383621),(#383622,#383623,#383624),
(#383625,#383626,#383627),(#383628,#383629,#383630)),.UNSPECIFIED.,.F.,
 .F.,.F.)
B_SPLINE_SURFACE_WITH_KNOTS((4,4),(3,3),(3.19754937588498E-20,1.54744435122089E-5),
(0.,1.),.UNSPECIFIED.)
GEOMETRIC_REPRESENTATION_ITEM()
RATIONAL_B_SPLINE_SURFACE(((1.,0.478041569704873,1.),(1.,0.890533857552073,
1.),(1.,0.990075913815892,1.),(1.,1.,1.)))
REPRESENTATION_ITEM('')
SURFACE()
);
#2443=(
BOUNDED_SURFACE()
B_SPLINE_SURFACE(3,2,((#383632,#383633,#383634),(#383635,#383636,#383637),
(#383638,#383639,#383640),(#383641,#383642,#383643)),.UNSPECIFIED.,.F.,
 .F.,.F.)
B_SPLINE_SURFACE_WITH_KNOTS((4,4),(3,3),(0.00137194782501028,0.00149814269699235),
(0.,1.),.UNSPECIFIED.)
GEOMETRIC_REPRESENTATION_ITEM()
RATIONAL_B_SPLINE_SURFACE(((1.,0.815158509402317,1.),(1.,0.816179044148181,
1.),(1.,0.817226308119919,1.),(1.,0.818301939488807,1.)))
REPRESENTATION_ITEM('')
SURFACE()
);
#2444=(
BOUNDED_SURFACE()
B_SPLINE_SURFACE(3,2,((#383687,#383688,#383689),(#383690,#383691,#383692),
(#383693,#383694,#383695),(#383696,#383697,#383698)),.UNSPECIFIED.,.F.,
 .F.,.F.)
B_SPLINE_SURFACE_WITH_KNOTS((4,4),(3,3),(1.55009486301138E-5,4.92065510474436E-5),
(-8.13759515716345E-5,1.),.UNSPECIFIED.)
GEOMETRIC_REPRESENTATION_ITEM()
RATIONAL_B_SPLINE_SURFACE(((1.00002372912338,0.854200639599673,1.),(1.00001423585995,
0.912530301180534,1.),(1.00000710550472,0.956341495377423,1.),(1.0000123897591,
0.923873338137018,1.)))
REPRESENTATION_ITEM('')
SURFACE()
);
#2445=(
BOUNDED_SURFACE()
B_SPLINE_SURFACE(3,2,((#383702,#383703,#383704),(#383705,#383706,#383707),
(#383708,#383709,#383710),(#383711,#383712,#383713)),.UNSPECIFIED.,.F.,
 .F.,.F.)
B_SPLINE_SURFACE_WITH_KNOTS((4,4),(3,3),(-3.39934179457829E-6,3.73927597403563E-5),
(-0.00186004067487366,1.00069373317464),.UNSPECIFIED.)
GEOMETRIC_REPRESENTATION_ITEM()
RATIONAL_B_SPLINE_SURFACE(((1.00072100136081,0.806051963875175,1.000268596427),
(1.00060048440176,0.838470803558498,1.00022369994504),(1.00053106448814,
0.857144632272234,1.00019783877226),(1.00054515072872,0.853355459538972,
1.00020308635444)))
REPRESENTATION_ITEM('')
SURFACE()
);
#2446=(
BOUNDED_SURFACE()
B_SPLINE_SURFACE(3,2,((#383715,#383716,#383717),(#383718,#383719,#383720),
(#383721,#383722,#383723),(#383724,#383725,#383726)),.UNSPECIFIED.,.F.,
 .F.,.F.)
B_SPLINE_SURFACE_WITH_KNOTS((4,4),(3,3),(-5.42101086242752E-20,9.54361881492173E-5),
(0.,1.),.UNSPECIFIED.)
GEOMETRIC_REPRESENTATION_ITEM()
RATIONAL_B_SPLINE_SURFACE(((1.,0.816715621142058,1.),(1.,0.815907587407942,
1.),(1.,0.815115959345203,1.),(1.,0.814339887349202,1.)))
REPRESENTATION_ITEM('')
SURFACE()
);
#2447=(
BOUNDED_SURFACE()
B_SPLINE_SURFACE(3,2,((#383728,#383729,#383730),(#383731,#383732,#383733),
(#383734,#383735,#383736),(#383737,#383738,#383739)),.UNSPECIFIED.,.F.,
 .F.,.F.)
B_SPLINE_SURFACE_WITH_KNOTS((4,4),(3,3),(1.91429446079472E-19,4.68197758448213E-5),
(0.,1.),.UNSPECIFIED.)
GEOMETRIC_REPRESENTATION_ITEM()
RATIONAL_B_SPLINE_SURFACE(((1.,0.816715621142044,1.),(1.,0.953638980025207,
1.),(1.,0.954506925408054,1.),(1.,0.816715621142053,1.)))
REPRESENTATION_ITEM('')
SURFACE()
);
#2448=(
BOUNDED_SURFACE()
B_SPLINE_SURFACE(3,2,((#383741,#383742,#383743),(#383744,#383745,#383746),
(#383747,#383748,#383749),(#383750,#383751,#383752)),.UNSPECIFIED.,.F.,
 .F.,.F.)
B_SPLINE_SURFACE_WITH_KNOTS((4,4),(3,3),(-2.16840434497101E-19,9.54361881492177E-5),
(0.,1.),.UNSPECIFIED.)
GEOMETRIC_REPRESENTATION_ITEM()
RATIONAL_B_SPLINE_SURFACE(((1.,0.814339887349197,1.),(1.,0.815115959345205,
1.),(1.,0.815907587407944,1.),(1.,0.816715621142047,1.)))
REPRESENTATION_ITEM('')
SURFACE()
);
#2449=(
BOUNDED_SURFACE()
B_SPLINE_SURFACE(3,2,((#383754,#383755,#383756),(#383757,#383758,#383759),
(#383760,#383761,#383762),(#383763,#383764,#383765)),.UNSPECIFIED.,.F.,
 .F.,.F.)
B_SPLINE_SURFACE_WITH_KNOTS((4,4),(3,3),(-3.39528393502379E-6,3.73481232852736E-5),
(-0.00165018033327137,1.),.UNSPECIFIED.)
GEOMETRIC_REPRESENTATION_ITEM()
RATIONAL_B_SPLINE_SURFACE(((1.00048354385565,0.85348757166041,1.),(1.0004711051092,
0.857256476851454,1.),(1.00053193201107,0.83882609665588,1.),(1.00063970687725,
0.806170615310096,1.)))
REPRESENTATION_ITEM('')
SURFACE()
);
#2450=(
BOUNDED_SURFACE()
B_SPLINE_SURFACE(3,2,((#383769,#383770,#383771),(#383772,#383773,#383774),
(#383775,#383776,#383777),(#383778,#383779,#383780)),.UNSPECIFIED.,.F.,
 .F.,.F.)
B_SPLINE_SURFACE_WITH_KNOTS((4,4),(3,3),(2.02993869230508E-5,5.39756952686894E-5),
(-0.000116281069403863,1.),.UNSPECIFIED.)
GEOMETRIC_REPRESENTATION_ITEM()
RATIONAL_B_SPLINE_SURFACE(((1.00001770479722,0.923870681143049,1.),(1.00001014104054,
0.956394275543439,1.),(1.00002037300269,0.912397594905726,1.),(1.00003390859454,
0.854195550869924,1.)))
REPRESENTATION_ITEM('')
SURFACE()
);
#2451=(
BOUNDED_SURFACE()
B_SPLINE_SURFACE(3,2,((#383873,#383874,#383875),(#383876,#383877,#383878),
(#383879,#383880,#383881),(#383882,#383883,#383884)),.UNSPECIFIED.,.F.,
 .F.,.F.)
B_SPLINE_SURFACE_WITH_KNOTS((4,4),(3,3),(0.00135801595889393,0.00148409170619832),
(0.,1.),.UNSPECIFIED.)
GEOMETRIC_REPRESENTATION_ITEM()
RATIONAL_B_SPLINE_SURFACE(((1.,0.818301933966444,1.),(1.,0.817226613172333,
1.),(1.,0.816179643373965,1.),(1.,0.815159387863653,1.)))
REPRESENTATION_ITEM('')
SURFACE()
);
#2452=(
BOUNDED_SURFACE()
B_SPLINE_SURFACE(3,2,((#383923,#383924,#383925),(#383926,#383927,#383928),
(#383929,#383930,#383931),(#383932,#383933,#383934)),.UNSPECIFIED.,.F.,
 .F.,.F.)
B_SPLINE_SURFACE_WITH_KNOTS((4,4),(3,3),(-1.5474443512208E-6,1.54744435122078E-5),
(-0.0151698983643226,1.01516989835825),.UNSPECIFIED.)
GEOMETRIC_REPRESENTATION_ITEM()
RATIONAL_B_SPLINE_SURFACE(((1.02018382473254,0.324498219413273,1.02018382472433),
(1.00401234488884,0.865716921710659,1.00401234488721),(1.00033622856786,
0.988747276629648,1.00033622856772),(1.,1.,1.)))
REPRESENTATION_ITEM('')
SURFACE()
);
#2453=(
BOUNDED_SURFACE()
B_SPLINE_SURFACE(3,2,((#383936,#383937,#383938),(#383939,#383940,#383941),
(#383942,#383943,#383944),(#383945,#383946,#383947)),.UNSPECIFIED.,.F.,
 .F.,.F.)
B_SPLINE_SURFACE_WITH_KNOTS((4,4),(3,3),(0.00137194782501028,0.00149814269699235),
(0.,1.),.UNSPECIFIED.)
GEOMETRIC_REPRESENTATION_ITEM()
RATIONAL_B_SPLINE_SURFACE(((1.,0.815158509402318,1.),(1.,0.816179044148162,
1.),(1.,0.81722630811993,1.),(1.,0.818301939488811,1.)))
REPRESENTATION_ITEM('')
SURFACE()
);
#2454=(
BOUNDED_SURFACE()
B_SPLINE_SURFACE(3,2,((#383991,#383992,#383993),(#383994,#383995,#383996),
(#383997,#383998,#383999),(#384000,#384001,#384002)),.UNSPECIFIED.,.F.,
 .F.,.F.)
B_SPLINE_SURFACE_WITH_KNOTS((4,4),(3,3),(1.55009486301137E-5,4.9206551047443E-5),
(-8.13759512068241E-5,1.),.UNSPECIFIED.)
GEOMETRIC_REPRESENTATION_ITEM()
RATIONAL_B_SPLINE_SURFACE(((1.00002372912328,0.854200639599729,1.),(1.00001423585989,
0.912530301180557,1.),(1.00000710550468,0.956341495377445,1.),(1.00001238975904,
0.923873338137045,1.)))
REPRESENTATION_ITEM('')
SURFACE()
);
#2455=(
BOUNDED_SURFACE()
B_SPLINE_SURFACE(3,2,((#384006,#384007,#384008),(#384009,#384010,#384011),
(#384012,#384013,#384014),(#384015,#384016,#384017)),.UNSPECIFIED.,.F.,
 .F.,.F.)
B_SPLINE_SURFACE_WITH_KNOTS((4,4),(3,3),(-3.39934179457836E-6,3.73927597403565E-5),
(-0.00186004067393548,1.0006937331742),.UNSPECIFIED.)
GEOMETRIC_REPRESENTATION_ITEM()
RATIONAL_B_SPLINE_SURFACE(((1.00072100136045,0.80605196387545,1.00026859642683),
(1.00060048440146,0.838470803558697,1.00022369994489),(1.00053106448788,
0.857144632272436,1.00019783877214),(1.00054515072845,0.853355459539174,
1.00020308635431)))
REPRESENTATION_ITEM('')
SURFACE()
);
#2456=(
BOUNDED_SURFACE()
B_SPLINE_SURFACE(3,2,((#384019,#384020,#384021),(#384022,#384023,#384024),
(#384025,#384026,#384027),(#384028,#384029,#384030)),.UNSPECIFIED.,.F.,
 .F.,.F.)
B_SPLINE_SURFACE_WITH_KNOTS((4,4),(3,3),(-5.42101086242752E-20,9.54361881492175E-5),
(0.,1.),.UNSPECIFIED.)
GEOMETRIC_REPRESENTATION_ITEM()
RATIONAL_B_SPLINE_SURFACE(((1.,0.81671562114205,1.),(1.,0.815907587407945,
1.),(1.,0.815115959345207,1.),(1.,0.814339887349188,1.)))
REPRESENTATION_ITEM('')
SURFACE()
);
#2457=(
BOUNDED_SURFACE()
B_SPLINE_SURFACE(3,2,((#384032,#384033,#384034),(#384035,#384036,#384037),
(#384038,#384039,#384040),(#384041,#384042,#384043)),.UNSPECIFIED.,.F.,
 .F.,.F.)
B_SPLINE_SURFACE_WITH_KNOTS((4,4),(3,3),(5.25160427297666E-20,4.68197758448206E-5),
(0.,1.),.UNSPECIFIED.)
GEOMETRIC_REPRESENTATION_ITEM()
RATIONAL_B_SPLINE_SURFACE(((1.,0.816715621142045,1.),(1.,0.953638980025207,
1.),(1.,0.954506925408054,1.),(1.,0.816715621142054,1.)))
REPRESENTATION_ITEM('')
SURFACE()
);
#2458=(
BOUNDED_SURFACE()
B_SPLINE_SURFACE(3,2,((#384045,#384046,#384047),(#384048,#384049,#384050),
(#384051,#384052,#384053),(#384054,#384055,#384056)),.UNSPECIFIED.,.F.,
 .F.,.F.)
B_SPLINE_SURFACE_WITH_KNOTS((4,4),(3,3),(5.42101086242752E-20,9.54361881492178E-5),
(0.,1.),.UNSPECIFIED.)
GEOMETRIC_REPRESENTATION_ITEM()
RATIONAL_B_SPLINE_SURFACE(((1.,0.814339887349191,1.),(1.,0.815115959345209,
1.),(1.,0.815907587407936,1.),(1.,0.816715621142049,1.)))
REPRESENTATION_ITEM('')
SURFACE()
);
#2459=(
BOUNDED_SURFACE()
B_SPLINE_SURFACE(3,2,((#384058,#384059,#384060),(#384061,#384062,#384063),
(#384064,#384065,#384066),(#384067,#384068,#384069)),.UNSPECIFIED.,.F.,
 .F.,.F.)
B_SPLINE_SURFACE_WITH_KNOTS((4,4),(3,3),(-3.39528393502487E-6,3.73481232852724E-5),
(-0.00165018033260751,1.),.UNSPECIFIED.)
GEOMETRIC_REPRESENTATION_ITEM()
RATIONAL_B_SPLINE_SURFACE(((1.00048354385546,0.853487571660499,1.),(1.00047110510901,
0.857256476851543,1.),(1.00053193201086,0.838826096655999,1.),(1.00063970687699,
0.806170615310219,0.999999999999999)))
REPRESENTATION_ITEM('')
SURFACE()
);
#2460=(
BOUNDED_SURFACE()
B_SPLINE_SURFACE(3,2,((#384073,#384074,#384075),(#384076,#384077,#384078),
(#384079,#384080,#384081),(#384082,#384083,#384084)),.UNSPECIFIED.,.F.,
 .F.,.F.)
B_SPLINE_SURFACE_WITH_KNOTS((4,4),(3,3),(2.02993869230509E-5,5.39756952686904E-5),
(-0.000116281069838297,1.),.UNSPECIFIED.)
GEOMETRIC_REPRESENTATION_ITEM()
RATIONAL_B_SPLINE_SURFACE(((1.00001770479729,0.923870681143015,1.),(1.00001014104058,
0.956394275543424,1.),(1.00002037300277,0.912397594905687,1.),(1.00003390859466,
0.854195550869865,1.)))
REPRESENTATION_ITEM('')
SURFACE()
);
#2461=(
BOUNDED_SURFACE()
B_SPLINE_SURFACE(3,2,((#384177,#384178,#384179),(#384180,#384181,#384182),
(#384183,#384184,#384185),(#384186,#384187,#384188)),.UNSPECIFIED.,.F.,
 .F.,.F.)
B_SPLINE_SURFACE_WITH_KNOTS((4,4),(3,3),(0.00135801595889393,0.00148409170619832),
(0.,1.),.UNSPECIFIED.)
GEOMETRIC_REPRESENTATION_ITEM()
RATIONAL_B_SPLINE_SURFACE(((1.,0.818301933966448,1.),(1.,0.817226613172348,
1.),(1.,0.81617964337395,1.),(1.,0.815159387863654,1.)))
REPRESENTATION_ITEM('')
SURFACE()
);
#2462=(
BOUNDED_SURFACE()
B_SPLINE_SURFACE(3,2,((#384227,#384228,#384229),(#384230,#384231,#384232),
(#384233,#384234,#384235),(#384236,#384237,#384238)),.UNSPECIFIED.,.F.,
 .F.,.F.)
B_SPLINE_SURFACE_WITH_KNOTS((4,4),(3,3),(-1.5474443512208E-6,1.5474443512208E-5),
(-0.0151698983683404,1.01516989835403),.UNSPECIFIED.)
GEOMETRIC_REPRESENTATION_ITEM()
RATIONAL_B_SPLINE_SURFACE(((1.02018382473796,0.324498219413477,1.02018382471863),
(1.00401234488992,0.865716921710568,1.00401234488608),(1.00033622856795,
0.988747276629655,1.00033622856762),(1.,1.,1.)))
REPRESENTATION_ITEM('')
SURFACE()
);
#2463=(
BOUNDED_SURFACE()
B_SPLINE_SURFACE(3,2,((#384240,#384241,#384242),(#384243,#384244,#384245),
(#384246,#384247,#384248),(#384249,#384250,#384251)),.UNSPECIFIED.,.F.,
 .F.,.F.)
B_SPLINE_SURFACE_WITH_KNOTS((4,4),(3,3),(0.00137194782501028,0.00149814269699235),
(0.,1.),.UNSPECIFIED.)
GEOMETRIC_REPRESENTATION_ITEM()
RATIONAL_B_SPLINE_SURFACE(((1.,0.815158509402319,1.),(1.,0.816179044148174,
1.),(1.,0.817226308119916,1.),(1.,0.818301939488812,1.)))
REPRESENTATION_ITEM('')
SURFACE()
);
#2464=(
BOUNDED_SURFACE()
B_SPLINE_SURFACE(3,2,((#384295,#384296,#384297),(#384298,#384299,#384300),
(#384301,#384302,#384303),(#384304,#384305,#384306)),.UNSPECIFIED.,.F.,
 .F.,.F.)
B_SPLINE_SURFACE_WITH_KNOTS((4,4),(3,3),(1.55009486301138E-5,4.9206551047444E-5),
(-8.13759517028193E-5,1.),.UNSPECIFIED.)
GEOMETRIC_REPRESENTATION_ITEM()
RATIONAL_B_SPLINE_SURFACE(((1.00002372912342,0.854200639599655,1.),(1.00001423585997,
0.912530301180528,1.),(1.00000710550473,0.956341495377415,1.),(1.00001238975912,
0.923873338137004,1.)))
REPRESENTATION_ITEM('')
SURFACE()
);
#2465=(
BOUNDED_SURFACE()
B_SPLINE_SURFACE(3,2,((#384310,#384311,#384312),(#384313,#384314,#384315),
(#384316,#384317,#384318),(#384319,#384320,#384321)),.UNSPECIFIED.,.F.,
 .F.,.F.)
B_SPLINE_SURFACE_WITH_KNOTS((4,4),(3,3),(-3.39934179457804E-6,3.73927597403566E-5),
(-0.00186004067478799,1.00069373317431),.UNSPECIFIED.)
GEOMETRIC_REPRESENTATION_ITEM()
RATIONAL_B_SPLINE_SURFACE(((1.00072100136078,0.806051963875266,1.00026859642688),
(1.00060048440173,0.838470803558537,1.00022369994493),(1.00053106448812,
0.857144632272323,1.00019783877217),(1.0005451507287,0.85335545953902,1.00020308635434)))
REPRESENTATION_ITEM('')
SURFACE()
);
#2466=(
BOUNDED_SURFACE()
B_SPLINE_SURFACE(3,2,((#384323,#384324,#384325),(#384326,#384327,#384328),
(#384329,#384330,#384331),(#384332,#384333,#384334)),.UNSPECIFIED.,.F.,
 .F.,.F.)
B_SPLINE_SURFACE_WITH_KNOTS((4,4),(3,3),(0.,9.54361881492173E-5),(0.,1.),
 .UNSPECIFIED.)
GEOMETRIC_REPRESENTATION_ITEM()
RATIONAL_B_SPLINE_SURFACE(((1.,0.816715621142051,1.),(1.,0.815907587407942,
1.),(1.,0.815115959345209,1.),(1.,0.814339887349193,1.)))
REPRESENTATION_ITEM('')
SURFACE()
);
#2467=(
BOUNDED_SURFACE()
B_SPLINE_SURFACE(3,2,((#384336,#384337,#384338),(#384339,#384340,#384341),
(#384342,#384343,#384344),(#384345,#384346,#384347)),.UNSPECIFIED.,.F.,
 .F.,.F.)
B_SPLINE_SURFACE_WITH_KNOTS((4,4),(3,3),(1.01643953670516E-20,4.68197758448216E-5),
(0.,1.),.UNSPECIFIED.)
GEOMETRIC_REPRESENTATION_ITEM()
RATIONAL_B_SPLINE_SURFACE(((1.,0.816715621142039,1.),(1.,0.95363898002521,
1.),(1.,0.954506925408058,1.),(1.,0.816715621142055,1.)))
REPRESENTATION_ITEM('')
SURFACE()
);
#2468=(
BOUNDED_SURFACE()
B_SPLINE_SURFACE(3,2,((#384349,#384350,#384351),(#384352,#384353,#384354),
(#384355,#384356,#384357),(#384358,#384359,#384360)),.UNSPECIFIED.,.F.,
 .F.,.F.)
B_SPLINE_SURFACE_WITH_KNOTS((4,4),(3,3),(0.,9.54361881492177E-5),(0.,1.),
 .UNSPECIFIED.)
GEOMETRIC_REPRESENTATION_ITEM()
RATIONAL_B_SPLINE_SURFACE(((1.,0.814339887349194,1.),(1.,0.815115959345197,
1.),(1.,0.815907587407955,1.),(1.,0.816715621142046,1.)))
REPRESENTATION_ITEM('')
SURFACE()
);
#2469=(
BOUNDED_SURFACE()
B_SPLINE_SURFACE(3,2,((#384362,#384363,#384364),(#384365,#384366,#384367),
(#384368,#384369,#384370),(#384371,#384372,#384373)),.UNSPECIFIED.,.F.,
 .F.,.F.)
B_SPLINE_SURFACE_WITH_KNOTS((4,4),(3,3),(-3.39528393502377E-6,3.73481232852734E-5),
(-0.00165018033340471,1.),.UNSPECIFIED.)
GEOMETRIC_REPRESENTATION_ITEM()
RATIONAL_B_SPLINE_SURFACE(((1.00048354385569,0.853487571660383,1.),(1.00047110510924,
0.857256476851451,1.),(1.00053193201111,0.838826096655851,1.),(1.0006397068773,
0.806170615310069,1.)))
REPRESENTATION_ITEM('')
SURFACE()
);
#2470=(
BOUNDED_SURFACE()
B_SPLINE_SURFACE(3,2,((#384377,#384378,#384379),(#384380,#384381,#384382),
(#384383,#384384,#384385),(#384386,#384387,#384388)),.UNSPECIFIED.,.F.,
 .F.,.F.)
B_SPLINE_SURFACE_WITH_KNOTS((4,4),(3,3),(2.02993869230508E-5,5.397569526869E-5),
(-0.000116281070011194,1.),.UNSPECIFIED.)
GEOMETRIC_REPRESENTATION_ITEM()
RATIONAL_B_SPLINE_SURFACE(((1.00001770479731,0.923870681143,1.),(1.0000101410406,
0.956394275543404,1.),(1.0000203730028,0.912397594905675,1.),(1.00003390859471,
0.854195550869839,1.)))
REPRESENTATION_ITEM('')
SURFACE()
);
#2471=(
BOUNDED_SURFACE()
B_SPLINE_SURFACE(3,2,((#384481,#384482,#384483),(#384484,#384485,#384486),
(#384487,#384488,#384489),(#384490,#384491,#384492)),.UNSPECIFIED.,.F.,
 .F.,.F.)
B_SPLINE_SURFACE_WITH_KNOTS((4,4),(3,3),(0.00135801595889393,0.00148409170619832),
(0.,1.),.UNSPECIFIED.)
GEOMETRIC_REPRESENTATION_ITEM()
RATIONAL_B_SPLINE_SURFACE(((1.,0.818301933966444,1.),(1.,0.81722661317233,
1.),(1.,0.816179643373973,1.),(1.,0.815159387863652,1.)))
REPRESENTATION_ITEM('')
SURFACE()
);
#2472=(
BOUNDED_SURFACE()
B_SPLINE_SURFACE(3,2,((#384531,#384532,#384533),(#384534,#384535,#384536),
(#384537,#384538,#384539),(#384540,#384541,#384542)),.UNSPECIFIED.,.F.,
 .F.,.F.)
B_SPLINE_SURFACE_WITH_KNOTS((4,4),(3,3),(-1.54744435122086E-6,1.54744435122084E-5),
(-0.0151698983566559,1.01516989836567),.UNSPECIFIED.)
GEOMETRIC_REPRESENTATION_ITEM()
RATIONAL_B_SPLINE_SURFACE(((1.02018382472218,0.324498219413471,1.02018382473435),
(1.00401234488678,0.865716921710634,1.0040123448892),(1.00033622856768,
0.988747276629699,1.00033622856788),(1.,1.,1.)))
REPRESENTATION_ITEM('')
SURFACE()
);
#2473=(
BOUNDED_SURFACE()
B_SPLINE_SURFACE(3,2,((#384544,#384545,#384546),(#384547,#384548,#384549),
(#384550,#384551,#384552),(#384553,#384554,#384555)),.UNSPECIFIED.,.F.,
 .F.,.F.)
B_SPLINE_SURFACE_WITH_KNOTS((4,4),(3,3),(0.00137194782501028,0.00149814269699235),
(0.,1.),.UNSPECIFIED.)
GEOMETRIC_REPRESENTATION_ITEM()
RATIONAL_B_SPLINE_SURFACE(((1.,0.815158509402317,1.),(1.,0.816179044148182,
1.),(1.,0.817226308119902,1.),(1.,0.81830193948882,1.)))
REPRESENTATION_ITEM('')
SURFACE()
);
#2474=(
BOUNDED_SURFACE()
B_SPLINE_SURFACE(3,2,((#384599,#384600,#384601),(#384602,#384603,#384604),
(#384605,#384606,#384607),(#384608,#384609,#384610)),.UNSPECIFIED.,.F.,
 .F.,.F.)
B_SPLINE_SURFACE_WITH_KNOTS((4,4),(3,3),(1.55009486301137E-5,4.92065510474432E-5),
(-8.13759511476216E-5,1.),.UNSPECIFIED.)
GEOMETRIC_REPRESENTATION_ITEM()
RATIONAL_B_SPLINE_SURFACE(((1.00002372912326,0.854200639599733,1.),(1.00001423585988,
0.912530301180572,1.),(1.00000710550468,0.956341495377445,1.),(1.00001238975903,
0.923873338137047,1.)))
REPRESENTATION_ITEM('')
SURFACE()
);
#2475=(
BOUNDED_SURFACE()
B_SPLINE_SURFACE(3,2,((#384614,#384615,#384616),(#384617,#384618,#384619),
(#384620,#384621,#384622),(#384623,#384624,#384625)),.UNSPECIFIED.,.F.,
 .F.,.F.)
B_SPLINE_SURFACE_WITH_KNOTS((4,4),(3,3),(-3.39934179457803E-6,3.73927597403565E-5),
(-0.00186004067432212,1.00069373317451),.UNSPECIFIED.)
GEOMETRIC_REPRESENTATION_ITEM()
RATIONAL_B_SPLINE_SURFACE(((1.0007210013606,0.806051963875291,1.00026859642695),
(1.00060048440158,0.838470803558606,1.00022369994499),(1.00053106448799,
0.857144632272342,1.00019783877223),(1.00054515072856,0.853355459539061,
1.0002030863544)))
REPRESENTATION_ITEM('')
SURFACE()
);
#2476=(
BOUNDED_SURFACE()
B_SPLINE_SURFACE(3,2,((#384627,#384628,#384629),(#384630,#384631,#384632),
(#384633,#384634,#384635),(#384636,#384637,#384638)),.UNSPECIFIED.,.F.,
 .F.,.F.)
B_SPLINE_SURFACE_WITH_KNOTS((4,4),(3,3),(-2.16840434497101E-19,9.54361881492172E-5),
(0.,1.),.UNSPECIFIED.)
GEOMETRIC_REPRESENTATION_ITEM()
RATIONAL_B_SPLINE_SURFACE(((1.,0.816715621142053,1.),(1.,0.815907587407932,
1.),(1.,0.815115959345205,1.),(1.,0.814339887349196,1.)))
REPRESENTATION_ITEM('')
SURFACE()
);
#2477=(
BOUNDED_SURFACE()
B_SPLINE_SURFACE(3,2,((#384640,#384641,#384642),(#384643,#384644,#384645),
(#384646,#384647,#384648),(#384649,#384650,#384651)),.UNSPECIFIED.,.F.,
 .F.,.F.)
B_SPLINE_SURFACE_WITH_KNOTS((4,4),(3,3),(2.21922632180627E-19,4.68197758448208E-5),
(0.,1.),.UNSPECIFIED.)
GEOMETRIC_REPRESENTATION_ITEM()
RATIONAL_B_SPLINE_SURFACE(((1.,0.81671562114205,1.),(1.,0.9536389800252,
1.),(1.,0.954506925408054,1.),(1.,0.816715621142053,1.)))
REPRESENTATION_ITEM('')
SURFACE()
);
#2478=(
BOUNDED_SURFACE()
B_SPLINE_SURFACE(3,2,((#384653,#384654,#384655),(#384656,#384657,#384658),
(#384659,#384660,#384661),(#384662,#384663,#384664)),.UNSPECIFIED.,.F.,
 .F.,.F.)
B_SPLINE_SURFACE_WITH_KNOTS((4,4),(3,3),(-3.79470760369927E-19,9.54361881492173E-5),
(0.,1.),.UNSPECIFIED.)
GEOMETRIC_REPRESENTATION_ITEM()
RATIONAL_B_SPLINE_SURFACE(((1.,0.814339887349193,1.),(1.,0.81511595934522,
1.),(1.,0.815907587407937,1.),(1.,0.81671562114205,1.)))
REPRESENTATION_ITEM('')
SURFACE()
);
#2479=(
BOUNDED_SURFACE()
B_SPLINE_SURFACE(3,2,((#384666,#384667,#384668),(#384669,#384670,#384671),
(#384672,#384673,#384674),(#384675,#384676,#384677)),.UNSPECIFIED.,.F.,
 .F.,.F.)
B_SPLINE_SURFACE_WITH_KNOTS((4,4),(3,3),(-3.39528393502489E-6,3.73481232852735E-5),
(-0.00165018033256893,1.),.UNSPECIFIED.)
GEOMETRIC_REPRESENTATION_ITEM()
RATIONAL_B_SPLINE_SURFACE(((1.00048354385545,0.853487571660496,1.),(1.000471105109,
0.857256476851579,1.),(1.00053193201084,0.838826096655986,1.),(1.00063970687698,
0.806170615310235,1.)))
REPRESENTATION_ITEM('')
SURFACE()
);
#2480=(
BOUNDED_SURFACE()
B_SPLINE_SURFACE(3,2,((#384681,#384682,#384683),(#384684,#384685,#384686),
(#384687,#384688,#384689),(#384690,#384691,#384692)),.UNSPECIFIED.,.F.,
 .F.,.F.)
B_SPLINE_SURFACE_WITH_KNOTS((4,4),(3,3),(2.0299386923051E-5,5.39756952687128E-5),
(-0.000116281069528885,1.),.UNSPECIFIED.)
GEOMETRIC_REPRESENTATION_ITEM()
RATIONAL_B_SPLINE_SURFACE(((1.00001770479724,0.923870681143037,1.),(1.00001014104055,
0.956394275543469,1.),(1.00002037300272,0.912397594905643,1.),(1.00003390859457,
0.854195550869799,1.)))
REPRESENTATION_ITEM('')
SURFACE()
);
#2481=(
BOUNDED_SURFACE()
B_SPLINE_SURFACE(3,2,((#384785,#384786,#384787),(#384788,#384789,#384790),
(#384791,#384792,#384793),(#384794,#384795,#384796)),.UNSPECIFIED.,.F.,
 .F.,.F.)
B_SPLINE_SURFACE_WITH_KNOTS((4,4),(3,3),(0.00135801595889393,0.00148409170619832),
(0.,1.),.UNSPECIFIED.)
GEOMETRIC_REPRESENTATION_ITEM()
RATIONAL_B_SPLINE_SURFACE(((1.,0.818301933966446,1.),(1.,0.817226613172343,
1.),(1.,0.816179643373963,1.),(1.,0.815159387863655,1.)))
REPRESENTATION_ITEM('')
SURFACE()
);
#2482=(
BOUNDED_SURFACE()
B_SPLINE_SURFACE(3,2,((#384835,#384836,#384837),(#384838,#384839,#384840),
(#384841,#384842,#384843),(#384844,#384845,#384846)),.UNSPECIFIED.,.F.,
 .F.,.F.)
B_SPLINE_SURFACE_WITH_KNOTS((4,4),(3,3),(3.15519772852227E-20,1.54744435122079E-5),
(0.,1.),.UNSPECIFIED.)
GEOMETRIC_REPRESENTATION_ITEM()
RATIONAL_B_SPLINE_SURFACE(((1.,0.478041569704962,1.),(1.,0.890533857552089,
1.),(1.,0.990075913815913,1.),(1.,1.,1.)))
REPRESENTATION_ITEM('')
SURFACE()
);
#2483=(
BOUNDED_SURFACE()
B_SPLINE_SURFACE(3,2,((#384848,#384849,#384850),(#384851,#384852,#384853),
(#384854,#384855,#384856),(#384857,#384858,#384859)),.UNSPECIFIED.,.F.,
 .F.,.F.)
B_SPLINE_SURFACE_WITH_KNOTS((4,4),(3,3),(0.00137194782501028,0.00149814269699235),
(0.,1.),.UNSPECIFIED.)
GEOMETRIC_REPRESENTATION_ITEM()
RATIONAL_B_SPLINE_SURFACE(((1.,0.815158509402321,1.),(1.,0.816179044148162,
1.),(1.,0.817226308119932,1.),(1.,0.818301939488813,1.)))
REPRESENTATION_ITEM('')
SURFACE()
);
#2484=(
BOUNDED_SURFACE()
B_SPLINE_SURFACE(3,2,((#384903,#384904,#384905),(#384906,#384907,#384908),
(#384909,#384910,#384911),(#384912,#384913,#384914)),.UNSPECIFIED.,.F.,
 .F.,.F.)
B_SPLINE_SURFACE_WITH_KNOTS((4,4),(3,3),(1.55009486301137E-5,4.92065510474437E-5),
(-8.13759516774955E-5,1.),.UNSPECIFIED.)
GEOMETRIC_REPRESENTATION_ITEM()
RATIONAL_B_SPLINE_SURFACE(((1.00002372912341,0.854200639599657,1.),(1.00001423585997,
0.912530301180526,1.),(1.00000710550473,0.956341495377421,1.),(1.00001238975911,
0.923873338137008,1.)))
REPRESENTATION_ITEM('')
SURFACE()
);
#2485=(
BOUNDED_SURFACE()
B_SPLINE_SURFACE(3,2,((#384918,#384919,#384920),(#384921,#384922,#384923),
(#384924,#384925,#384926),(#384927,#384928,#384929)),.UNSPECIFIED.,.F.,
 .F.,.F.)
B_SPLINE_SURFACE_WITH_KNOTS((4,4),(3,3),(-3.39934179457824E-6,3.73927597403566E-5),
(-0.00186004067402246,1.00069373317468),.UNSPECIFIED.)
GEOMETRIC_REPRESENTATION_ITEM()
RATIONAL_B_SPLINE_SURFACE(((1.00072100136048,0.806051963875315,1.00026859642702),
(1.00060048440149,0.838470803558637,1.00022369994505),(1.0005310644879,
0.857144632272356,1.00019783877227),(1.00054515072847,0.853355459539086,
1.00020308635445)))
REPRESENTATION_ITEM('')
SURFACE()
);
#2486=(
BOUNDED_SURFACE()
B_SPLINE_SURFACE(3,2,((#384931,#384932,#384933),(#384934,#384935,#384936),
(#384937,#384938,#384939),(#384940,#384941,#384942)),.UNSPECIFIED.,.F.,
 .F.,.F.)
B_SPLINE_SURFACE_WITH_KNOTS((4,4),(3,3),(1.62630325872826E-19,9.54361881492175E-5),
(0.,1.),.UNSPECIFIED.)
GEOMETRIC_REPRESENTATION_ITEM()
RATIONAL_B_SPLINE_SURFACE(((1.,0.816715621142049,1.),(1.,0.815907587407945,
1.),(1.,0.815115959345202,1.),(1.,0.814339887349198,1.)))
REPRESENTATION_ITEM('')
SURFACE()
);
#2487=(
BOUNDED_SURFACE()
B_SPLINE_SURFACE(3,2,((#384944,#384945,#384946),(#384947,#384948,#384949),
(#384950,#384951,#384952),(#384953,#384954,#384955)),.UNSPECIFIED.,.F.,
 .F.,.F.)
B_SPLINE_SURFACE_WITH_KNOTS((4,4),(3,3),(5.59041745187838E-20,4.68197758448204E-5),
(0.,1.),.UNSPECIFIED.)
GEOMETRIC_REPRESENTATION_ITEM()
RATIONAL_B_SPLINE_SURFACE(((1.,0.81671562114205,1.),(1.,0.953638980025201,
1.),(1.,0.954506925408057,1.),(1.,0.816715621142055,1.)))
REPRESENTATION_ITEM('')
SURFACE()
);
#2488=(
BOUNDED_SURFACE()
B_SPLINE_SURFACE(3,2,((#384957,#384958,#384959),(#384960,#384961,#384962),
(#384963,#384964,#384965),(#384966,#384967,#384968)),.UNSPECIFIED.,.F.,
 .F.,.F.)
B_SPLINE_SURFACE_WITH_KNOTS((4,4),(3,3),(-5.42101086242752E-20,9.54361881492176E-5),
(0.,1.),.UNSPECIFIED.)
GEOMETRIC_REPRESENTATION_ITEM()
RATIONAL_B_SPLINE_SURFACE(((1.,0.814339887349194,1.),(1.,0.815115959345203,
1.),(1.,0.815907587407944,1.),(1.,0.81671562114205,1.)))
REPRESENTATION_ITEM('')
SURFACE()
);
#2489=(
BOUNDED_SURFACE()
B_SPLINE_SURFACE(3,2,((#384970,#384971,#384972),(#384973,#384974,#384975),
(#384976,#384977,#384978),(#384979,#384980,#384981)),.UNSPECIFIED.,.F.,
 .F.,.F.)
B_SPLINE_SURFACE_WITH_KNOTS((4,4),(3,3),(-3.3952839350249E-6,3.73481232852735E-5),
(-0.00165018033317863,1.),.UNSPECIFIED.)
GEOMETRIC_REPRESENTATION_ITEM()
RATIONAL_B_SPLINE_SURFACE(((1.00048354385562,0.853487571660423,1.),(1.00047110510918,
0.857256476851474,1.),(1.00053193201104,0.838826096655891,1.),(1.00063970687721,
0.806170615310117,1.)))
REPRESENTATION_ITEM('')
SURFACE()
);
#2490=(
BOUNDED_SURFACE()
B_SPLINE_SURFACE(3,2,((#384985,#384986,#384987),(#384988,#384989,#384990),
(#384991,#384992,#384993),(#384994,#384995,#384996)),.UNSPECIFIED.,.F.,
 .F.,.F.)
B_SPLINE_SURFACE_WITH_KNOTS((4,4),(3,3),(2.0299386923051E-5,5.39756952687133E-5),
(-0.000116281070167084,1.),.UNSPECIFIED.)
GEOMETRIC_REPRESENTATION_ITEM()
RATIONAL_B_SPLINE_SURFACE(((1.00001770479734,0.923870681142993,1.),(1.00001014104061,
0.95639427554343,1.),(1.00002037300283,0.912397594905591,1.),(1.00003390859476,
0.854195550869707,1.)))
REPRESENTATION_ITEM('')
SURFACE()
);
#2491=(
BOUNDED_SURFACE()
B_SPLINE_SURFACE(3,2,((#385089,#385090,#385091),(#385092,#385093,#385094),
(#385095,#385096,#385097),(#385098,#385099,#385100)),.UNSPECIFIED.,.F.,
 .F.,.F.)
B_SPLINE_SURFACE_WITH_KNOTS((4,4),(3,3),(0.00135801595889393,0.00148409170619832),
(0.,1.),.UNSPECIFIED.)
GEOMETRIC_REPRESENTATION_ITEM()
RATIONAL_B_SPLINE_SURFACE(((1.,0.818301933966444,1.),(1.,0.817226613172343,
1.),(1.,0.816179643373956,1.),(1.,0.815159387863651,1.)))
REPRESENTATION_ITEM('')
SURFACE()
);
#2492=(
BOUNDED_SURFACE()
B_SPLINE_SURFACE(3,2,((#385139,#385140,#385141),(#385142,#385143,#385144),
(#385145,#385146,#385147),(#385148,#385149,#385150)),.UNSPECIFIED.,.F.,
 .F.,.F.)
B_SPLINE_SURFACE_WITH_KNOTS((4,4),(3,3),(-1.54744435122067E-6,1.5474443512207E-5),
(-0.0151698983643363,1.01516989835806),.UNSPECIFIED.)
GEOMETRIC_REPRESENTATION_ITEM()
RATIONAL_B_SPLINE_SURFACE(((1.02018382473255,0.324498219413463,1.02018382472407),
(1.00401234488884,0.865716921710598,1.00401234488716),(1.00033622856786,
0.988747276629678,1.00033622856771),(1.,1.,1.)))
REPRESENTATION_ITEM('')
SURFACE()
);
#2493=(
BOUNDED_SURFACE()
B_SPLINE_SURFACE(3,2,((#385152,#385153,#385154),(#385155,#385156,#385157),
(#385158,#385159,#385160),(#385161,#385162,#385163)),.UNSPECIFIED.,.F.,
 .F.,.F.)
B_SPLINE_SURFACE_WITH_KNOTS((4,4),(3,3),(0.00137194782501028,0.00149814269699235),
(0.,1.),.UNSPECIFIED.)
GEOMETRIC_REPRESENTATION_ITEM()
RATIONAL_B_SPLINE_SURFACE(((1.,0.815158509402313,1.),(1.,0.816179044148164,
1.),(1.,0.81722630811993,1.),(1.,0.818301939488796,1.)))
REPRESENTATION_ITEM('')
SURFACE()
);
#2494=(
BOUNDED_SURFACE()
B_SPLINE_SURFACE(3,2,((#385207,#385208,#385209),(#385210,#385211,#385212),
(#385213,#385214,#385215),(#385216,#385217,#385218)),.UNSPECIFIED.,.F.,
 .F.,.F.)
B_SPLINE_SURFACE_WITH_KNOTS((4,4),(3,3),(1.55009486301137E-5,4.92065510474435E-5),
(-8.13759514913963E-5,1.),.UNSPECIFIED.)
GEOMETRIC_REPRESENTATION_ITEM()
RATIONAL_B_SPLINE_SURFACE(((1.00002372912336,0.85420063959969,1.),(1.00001423585994,
0.91253030118053,1.),(1.00000710550471,0.95634149537743,1.),(1.00001238975909,
0.923873338137023,1.)))
REPRESENTATION_ITEM('')
SURFACE()
);
#2495=(
BOUNDED_SURFACE()
B_SPLINE_SURFACE(3,2,((#385222,#385223,#385224),(#385225,#385226,#385227),
(#385228,#385229,#385230),(#385231,#385232,#385233)),.UNSPECIFIED.,.F.,
 .F.,.F.)
B_SPLINE_SURFACE_WITH_KNOTS((4,4),(3,3),(-3.39934179457805E-6,3.73927597403566E-5),
(-0.00186004067409043,1.00069373317417),.UNSPECIFIED.)
GEOMETRIC_REPRESENTATION_ITEM()
RATIONAL_B_SPLINE_SURFACE(((1.00072100136051,0.806051963875405,1.00026859642682),
(1.00060048440151,0.838470803558699,1.00022369994488),(1.00053106448792,
0.857144632272416,1.00019783877213),(1.00054515072849,0.85335545953915,
1.0002030863543)))
REPRESENTATION_ITEM('')
SURFACE()
);
#2496=(
BOUNDED_SURFACE()
B_SPLINE_SURFACE(3,2,((#385235,#385236,#385237),(#385238,#385239,#385240),
(#385241,#385242,#385243),(#385244,#385245,#385246)),.UNSPECIFIED.,.F.,
 .F.,.F.)
B_SPLINE_SURFACE_WITH_KNOTS((4,4),(3,3),(0.,9.54361881492173E-5),(0.,1.),
 .UNSPECIFIED.)
GEOMETRIC_REPRESENTATION_ITEM()
RATIONAL_B_SPLINE_SURFACE(((1.,0.816715621142048,1.),(1.,0.81590758740794,
1.),(1.,0.815115959345199,1.),(1.,0.814339887349196,1.)))
REPRESENTATION_ITEM('')
SURFACE()
);
#2497=(
BOUNDED_SURFACE()
B_SPLINE_SURFACE(3,2,((#385248,#385249,#385250),(#385251,#385252,#385253),
(#385254,#385255,#385256),(#385257,#385258,#385259)),.UNSPECIFIED.,.F.,
 .F.,.F.)
B_SPLINE_SURFACE_WITH_KNOTS((4,4),(3,3),(1.47383732822248E-19,4.68197758448205E-5),
(0.,1.),.UNSPECIFIED.)
GEOMETRIC_REPRESENTATION_ITEM()
RATIONAL_B_SPLINE_SURFACE(((1.,0.816715621142046,1.),(1.,0.953638980025211,
1.),(1.,0.954506925408045,1.),(1.,0.81671562114205,1.)))
REPRESENTATION_ITEM('')
SURFACE()
);
#2498=(
BOUNDED_SURFACE()
B_SPLINE_SURFACE(3,2,((#385261,#385262,#385263),(#385264,#385265,#385266),
(#385267,#385268,#385269),(#385270,#385271,#385272)),.UNSPECIFIED.,.F.,
 .F.,.F.)
B_SPLINE_SURFACE_WITH_KNOTS((4,4),(3,3),(-1.0842021724855E-19,9.5436188149218E-5),
(0.,1.),.UNSPECIFIED.)
GEOMETRIC_REPRESENTATION_ITEM()
RATIONAL_B_SPLINE_SURFACE(((1.,0.814339887349195,1.),(1.,0.815115959345212,
1.),(1.,0.815907587407936,1.),(1.,0.816715621142046,1.)))
REPRESENTATION_ITEM('')
SURFACE()
);
#2499=(
BOUNDED_SURFACE()
B_SPLINE_SURFACE(3,2,((#385274,#385275,#385276),(#385277,#385278,#385279),
(#385280,#385281,#385282),(#385283,#385284,#385285)),.UNSPECIFIED.,.F.,
 .F.,.F.)
B_SPLINE_SURFACE_WITH_KNOTS((4,4),(3,3),(-3.39528393502485E-6,3.73481232852731E-5),
(-0.00165018033290614,1.),.UNSPECIFIED.)
GEOMETRIC_REPRESENTATION_ITEM()
RATIONAL_B_SPLINE_SURFACE(((1.00048354385554,0.853487571660454,1.),(1.0004711051091,
0.857256476851504,1.),(1.00053193201095,0.838826096655941,1.),(1.00063970687711,
0.806170615310158,1.)))
REPRESENTATION_ITEM('')
SURFACE()
);
#2500=(
BOUNDED_SURFACE()
B_SPLINE_SURFACE(3,2,((#385289,#385290,#385291),(#385292,#385293,#385294),
(#385295,#385296,#385297),(#385298,#385299,#385300)),.UNSPECIFIED.,.F.,
 .F.,.F.)
B_SPLINE_SURFACE_WITH_KNOTS((4,4),(3,3),(2.02993869230509E-5,5.39756952686903E-5),
(-0.000116281069964736,1.),.UNSPECIFIED.)
GEOMETRIC_REPRESENTATION_ITEM()
RATIONAL_B_SPLINE_SURFACE(((1.0000177047973,0.923870681143004,1.),(1.00001014104059,
0.956394275543417,1.),(1.00002037300279,0.912397594905668,1.),(1.0000339085947,
0.854195550869854,1.)))
REPRESENTATION_ITEM('')
SURFACE()
);
#2501=(
BOUNDED_SURFACE()
B_SPLINE_SURFACE(3,2,((#385393,#385394,#385395),(#385396,#385397,#385398),
(#385399,#385400,#385401),(#385402,#385403,#385404)),.UNSPECIFIED.,.F.,
 .F.,.F.)
B_SPLINE_SURFACE_WITH_KNOTS((4,4),(3,3),(0.00135801595889393,0.00148409170619832),
(0.,1.),.UNSPECIFIED.)
GEOMETRIC_REPRESENTATION_ITEM()
RATIONAL_B_SPLINE_SURFACE(((1.,0.818301933966441,1.),(1.,0.817226613172338,
1.),(1.,0.816179643373964,1.),(1.,0.815159387863657,1.)))
REPRESENTATION_ITEM('')
SURFACE()
);
#2502=(
BOUNDED_SURFACE()
B_SPLINE_SURFACE(3,2,((#385443,#385444,#385445),(#385446,#385447,#385448),
(#385449,#385450,#385451),(#385452,#385453,#385454)),.UNSPECIFIED.,.F.,
 .F.,.F.)
B_SPLINE_SURFACE_WITH_KNOTS((4,4),(3,3),(-1.54744435122076E-6,1.54744435122078E-5),
(-0.0151698983634891,1.),.UNSPECIFIED.)
GEOMETRIC_REPRESENTATION_ITEM()
RATIONAL_B_SPLINE_SURFACE(((1.02018382473141,0.334740937355592,1.),(1.00401234488861,
0.86775307281324,1.),(1.00033622856784,0.988917903080779,1.),(1.,1.,1.)))
REPRESENTATION_ITEM('')
SURFACE()
);
#2503=(
BOUNDED_SURFACE()
B_SPLINE_SURFACE(3,2,((#385456,#385457,#385458),(#385459,#385460,#385461),
(#385462,#385463,#385464),(#385465,#385466,#385467)),.UNSPECIFIED.,.F.,
 .F.,.F.)
B_SPLINE_SURFACE_WITH_KNOTS((4,4),(3,3),(0.00137194782501028,0.00149814269699235),
(0.,1.),.UNSPECIFIED.)
GEOMETRIC_REPRESENTATION_ITEM()
RATIONAL_B_SPLINE_SURFACE(((1.,0.815158509402317,1.),(1.,0.816179044148157,
1.),(1.,0.817226308119947,1.),(1.,0.818301939488798,1.)))
REPRESENTATION_ITEM('')
SURFACE()
);
#2504=(
BOUNDED_SURFACE()
B_SPLINE_SURFACE(3,2,((#385511,#385512,#385513),(#385514,#385515,#385516),
(#385517,#385518,#385519),(#385520,#385521,#385522)),.UNSPECIFIED.,.F.,
 .F.,.F.)
B_SPLINE_SURFACE_WITH_KNOTS((4,4),(3,3),(1.55009486301138E-5,4.92065510474432E-5),
(-8.13759517454961E-5,1.),.UNSPECIFIED.)
GEOMETRIC_REPRESENTATION_ITEM()
RATIONAL_B_SPLINE_SURFACE(((1.00002372912343,0.854200639599646,1.),(1.00001423585998,
0.912530301180508,1.),(1.00000710550473,0.956341495377424,1.),(1.00001238975912,
0.923873338137003,1.)))
REPRESENTATION_ITEM('')
SURFACE()
);
#2505=(
BOUNDED_SURFACE()
B_SPLINE_SURFACE(3,2,((#385526,#385527,#385528),(#385529,#385530,#385531),
(#385532,#385533,#385534),(#385535,#385536,#385537)),.UNSPECIFIED.,.F.,
 .F.,.F.)
B_SPLINE_SURFACE_WITH_KNOTS((4,4),(3,3),(-3.39934179457826E-6,3.73927597403565E-5),
(-0.00186004067384692,1.00069373317454),.UNSPECIFIED.)
GEOMETRIC_REPRESENTATION_ITEM()
RATIONAL_B_SPLINE_SURFACE(((1.00072100136041,0.806051963875379,1.00026859642697),
(1.00060048440143,0.838470803558679,1.00022369994501),(1.00053106448785,
0.857144632272401,1.00019783877224),(1.00054515072842,0.853355459539132,
1.00020308635441)))
REPRESENTATION_ITEM('')
SURFACE()
);
#2506=(
BOUNDED_SURFACE()
B_SPLINE_SURFACE(3,2,((#385539,#385540,#385541),(#385542,#385543,#385544),
(#385545,#385546,#385547),(#385548,#385549,#385550)),.UNSPECIFIED.,.F.,
 .F.,.F.)
B_SPLINE_SURFACE_WITH_KNOTS((4,4),(3,3),(0.,9.54361881492173E-5),(0.,1.),
 .UNSPECIFIED.)
GEOMETRIC_REPRESENTATION_ITEM()
RATIONAL_B_SPLINE_SURFACE(((1.,0.816715621142047,1.),(1.,0.815907587407945,
1.),(1.,0.815115959345206,1.),(1.,0.814339887349193,1.)))
REPRESENTATION_ITEM('')
SURFACE()
);
#2507=(
BOUNDED_SURFACE()
B_SPLINE_SURFACE(3,2,((#385552,#385553,#385554),(#385555,#385556,#385557),
(#385558,#385559,#385560),(#385561,#385562,#385563)),.UNSPECIFIED.,.F.,
 .F.,.F.)
B_SPLINE_SURFACE_WITH_KNOTS((4,4),(3,3),(1.16890546721093E-19,4.68197758448207E-5),
(0.,1.),.UNSPECIFIED.)
GEOMETRIC_REPRESENTATION_ITEM()
RATIONAL_B_SPLINE_SURFACE(((1.,0.816715621142051,1.),(1.,0.953638980025205,
1.),(1.,0.954506925408056,1.),(1.,0.81671562114205,1.)))
REPRESENTATION_ITEM('')
SURFACE()
);
#2508=(
BOUNDED_SURFACE()
B_SPLINE_SURFACE(3,2,((#385565,#385566,#385567),(#385568,#385569,#385570),
(#385571,#385572,#385573),(#385574,#385575,#385576)),.UNSPECIFIED.,.F.,
 .F.,.F.)
B_SPLINE_SURFACE_WITH_KNOTS((4,4),(3,3),(-1.62630325872826E-19,9.54361881492177E-5),
(0.,1.),.UNSPECIFIED.)
GEOMETRIC_REPRESENTATION_ITEM()
RATIONAL_B_SPLINE_SURFACE(((1.,0.814339887349195,1.),(1.,0.815115959345206,
1.),(1.,0.81590758740794,1.),(1.,0.816715621142051,1.)))
REPRESENTATION_ITEM('')
SURFACE()
);
#2509=(
BOUNDED_SURFACE()
B_SPLINE_SURFACE(3,2,((#385578,#385579,#385580),(#385581,#385582,#385583),
(#385584,#385585,#385586),(#385587,#385588,#385589)),.UNSPECIFIED.,.F.,
 .F.,.F.)
B_SPLINE_SURFACE_WITH_KNOTS((4,4),(3,3),(-3.39528393502489E-6,3.7348123285274E-5),
(-0.00165018033282777,1.),.UNSPECIFIED.)
GEOMETRIC_REPRESENTATION_ITEM()
RATIONAL_B_SPLINE_SURFACE(((1.00048354385552,0.853487571660468,1.),(1.00047110510908,
0.857256476851526,1.),(1.00053193201093,0.838826096655947,1.),(1.00063970687708,
0.806170615310178,0.999999999999999)))
REPRESENTATION_ITEM('')
SURFACE()
);
#2510=(
BOUNDED_SURFACE()
B_SPLINE_SURFACE(3,2,((#385593,#385594,#385595),(#385596,#385597,#385598),
(#385599,#385600,#385601),(#385602,#385603,#385604)),.UNSPECIFIED.,.F.,
 .F.,.F.)
B_SPLINE_SURFACE_WITH_KNOTS((4,4),(3,3),(2.0299386923051E-5,5.3975695268712E-5),
(-0.000116281069906644,1.),.UNSPECIFIED.)
GEOMETRIC_REPRESENTATION_ITEM()
RATIONAL_B_SPLINE_SURFACE(((1.0000177047973,0.923870681143011,1.),(1.00001014104059,
0.956394275543454,1.),(1.00002037300278,0.912397594905597,1.),(1.00003390859468,
0.854195550869745,1.)))
REPRESENTATION_ITEM('')
SURFACE()
);
#2511=(
BOUNDED_SURFACE()
B_SPLINE_SURFACE(3,2,((#385697,#385698,#385699),(#385700,#385701,#385702),
(#385703,#385704,#385705),(#385706,#385707,#385708)),.UNSPECIFIED.,.F.,
 .F.,.F.)
B_SPLINE_SURFACE_WITH_KNOTS((4,4),(3,3),(0.00135801595889393,0.00148409170619832),
(0.,1.),.UNSPECIFIED.)
GEOMETRIC_REPRESENTATION_ITEM()
RATIONAL_B_SPLINE_SURFACE(((1.,0.818301933966441,1.),(1.,0.817226613172349,
1.),(1.,0.816179643373946,1.),(1.,0.815159387863657,1.)))
REPRESENTATION_ITEM('')
SURFACE()
);
#2512=(
BOUNDED_SURFACE()
B_SPLINE_SURFACE(3,2,((#385747,#385748,#385749),(#385750,#385751,#385752),
(#385753,#385754,#385755),(#385756,#385757,#385758)),.UNSPECIFIED.,.F.,
 .F.,.F.)
B_SPLINE_SURFACE_WITH_KNOTS((4,4),(3,3),(-1.54744435122074E-6,1.54744435122074E-5),
(-0.0151698983623385,1.01516989836002),.UNSPECIFIED.)
GEOMETRIC_REPRESENTATION_ITEM()
RATIONAL_B_SPLINE_SURFACE(((1.02018382472986,0.324498219413466,1.02018382472673),
(1.00401234488831,0.865716921710605,1.00401234488769),(1.00033622856781,
0.98874727662968,1.00033622856776),(1.,1.,1.)))
REPRESENTATION_ITEM('')
SURFACE()
);
#2513=(
BOUNDED_SURFACE()
B_SPLINE_SURFACE(3,2,((#385760,#385761,#385762),(#385763,#385764,#385765),
(#385766,#385767,#385768),(#385769,#385770,#385771)),.UNSPECIFIED.,.F.,
 .F.,.F.)
B_SPLINE_SURFACE_WITH_KNOTS((4,4),(3,3),(0.00137194782501028,0.00149814269699235),
(0.,1.),.UNSPECIFIED.)
GEOMETRIC_REPRESENTATION_ITEM()
RATIONAL_B_SPLINE_SURFACE(((1.,0.815158509402318,1.),(1.,0.816179044148164,
1.),(1.,0.817226308119924,1.),(1.,0.818301939488807,1.)))
REPRESENTATION_ITEM('')
SURFACE()
);
#2514=(
BOUNDED_SURFACE()
B_SPLINE_SURFACE(3,2,((#385815,#385816,#385817),(#385818,#385819,#385820),
(#385821,#385822,#385823),(#385824,#385825,#385826)),.UNSPECIFIED.,.F.,
 .F.,.F.)
B_SPLINE_SURFACE_WITH_KNOTS((4,4),(3,3),(1.55009486301137E-5,4.92065510474427E-5),
(-8.13759513362642E-5,1.),.UNSPECIFIED.)
GEOMETRIC_REPRESENTATION_ITEM()
RATIONAL_B_SPLINE_SURFACE(((1.00002372912331,0.854200639599707,1.),(1.00001423585991,
0.912530301180549,1.),(1.0000071055047,0.956341495377444,1.),(1.00001238975906,
0.923873338137031,1.)))
REPRESENTATION_ITEM('')
SURFACE()
);
#2515=(
BOUNDED_SURFACE()
B_SPLINE_SURFACE(3,2,((#385830,#385831,#385832),(#385833,#385834,#385835),
(#385836,#385837,#385838),(#385839,#385840,#385841)),.UNSPECIFIED.,.F.,
 .F.,.F.)
B_SPLINE_SURFACE_WITH_KNOTS((4,4),(3,3),(-3.39934179457806E-6,3.73927597403565E-5),
(-0.00186004067400375,1.00069373317447),.UNSPECIFIED.)
GEOMETRIC_REPRESENTATION_ITEM()
RATIONAL_B_SPLINE_SURFACE(((1.00072100136047,0.806051963875356,1.00026859642694),
(1.00060048440148,0.838470803558668,1.00022369994498),(1.00053106448789,
0.857144632272387,1.00019783877222),(1.00054515072847,0.85335545953912,
1.00020308635439)))
REPRESENTATION_ITEM('')
SURFACE()
);
#2516=(
BOUNDED_SURFACE()
B_SPLINE_SURFACE(3,2,((#385843,#385844,#385845),(#385846,#385847,#385848),
(#385849,#385850,#385851),(#385852,#385853,#385854)),.UNSPECIFIED.,.F.,
 .F.,.F.)
B_SPLINE_SURFACE_WITH_KNOTS((4,4),(3,3),(5.42101086242752E-20,9.54361881492175E-5),
(0.,1.),.UNSPECIFIED.)
GEOMETRIC_REPRESENTATION_ITEM()
RATIONAL_B_SPLINE_SURFACE(((1.,0.81671562114205,1.),(1.,0.815907587407938,
1.),(1.,0.815115959345202,1.),(1.,0.814339887349195,1.)))
REPRESENTATION_ITEM('')
SURFACE()
);
#2517=(
BOUNDED_SURFACE()
B_SPLINE_SURFACE(3,2,((#385856,#385857,#385858),(#385859,#385860,#385861),
(#385862,#385863,#385864),(#385865,#385866,#385867)),.UNSPECIFIED.,.F.,
 .F.,.F.)
B_SPLINE_SURFACE_WITH_KNOTS((4,4),(3,3),(1.18584612615602E-19,4.68197758448209E-5),
(0.,1.),.UNSPECIFIED.)
GEOMETRIC_REPRESENTATION_ITEM()
RATIONAL_B_SPLINE_SURFACE(((1.,0.816715621142049,1.),(1.,0.953638980025195,
1.),(1.,0.954506925408062,1.),(1.,0.816715621142057,1.)))
REPRESENTATION_ITEM('')
SURFACE()
);
#2518=(
BOUNDED_SURFACE()
B_SPLINE_SURFACE(3,2,((#385869,#385870,#385871),(#385872,#385873,#385874),
(#385875,#385876,#385877),(#385878,#385879,#385880)),.UNSPECIFIED.,.F.,
 .F.,.F.)
B_SPLINE_SURFACE_WITH_KNOTS((4,4),(3,3),(-1.62630325872826E-19,9.54361881492177E-5),
(0.,1.),.UNSPECIFIED.)
GEOMETRIC_REPRESENTATION_ITEM()
RATIONAL_B_SPLINE_SURFACE(((1.,0.81433988734919,1.),(1.,0.815115959345207,
1.),(1.,0.815907587407944,1.),(1.,0.816715621142049,1.)))
REPRESENTATION_ITEM('')
SURFACE()
);
#2519=(
BOUNDED_SURFACE()
B_SPLINE_SURFACE(3,2,((#385882,#385883,#385884),(#385885,#385886,#385887),
(#385888,#385889,#385890),(#385891,#385892,#385893)),.UNSPECIFIED.,.F.,
 .F.,.F.)
B_SPLINE_SURFACE_WITH_KNOTS((4,4),(3,3),(-3.39528393502492E-6,3.73481232852737E-5),
(-0.00165018033286106,1.),.UNSPECIFIED.)
GEOMETRIC_REPRESENTATION_ITEM()
RATIONAL_B_SPLINE_SURFACE(((1.00048354385553,0.853487571660456,1.),(1.00047110510909,
0.857256476851521,1.),(1.00053193201094,0.838826096655938,1.),(1.00063970687709,
0.806170615310175,1.)))
REPRESENTATION_ITEM('')
SURFACE()
);
#2520=(
BOUNDED_SURFACE()
B_SPLINE_SURFACE(3,2,((#385897,#385898,#385899),(#385900,#385901,#385902),
(#385903,#385904,#385905),(#385906,#385907,#385908)),.UNSPECIFIED.,.F.,
 .F.,.F.)
B_SPLINE_SURFACE_WITH_KNOTS((4,4),(3,3),(2.02993869230507E-5,5.39756952687127E-5),
(-0.000116281069855912,1.),.UNSPECIFIED.)
GEOMETRIC_REPRESENTATION_ITEM()
RATIONAL_B_SPLINE_SURFACE(((1.00001770479729,0.923870681143013,1.),(1.00001014104058,
0.956394275543447,1.),(1.00002037300277,0.912397594905622,1.),(1.00003390859467,
0.854195550869747,1.)))
REPRESENTATION_ITEM('')
SURFACE()
);
#2521=(
BOUNDED_SURFACE()
B_SPLINE_SURFACE(3,2,((#386001,#386002,#386003),(#386004,#386005,#386006),
(#386007,#386008,#386009),(#386010,#386011,#386012)),.UNSPECIFIED.,.F.,
 .F.,.F.)
B_SPLINE_SURFACE_WITH_KNOTS((4,4),(3,3),(0.00135801595889393,0.00148409170619832),
(0.,1.),.UNSPECIFIED.)
GEOMETRIC_REPRESENTATION_ITEM()
RATIONAL_B_SPLINE_SURFACE(((1.,0.818301933966445,1.),(1.,0.817226613172353,
1.),(1.,0.816179643373944,1.),(1.,0.815159387863655,1.)))
REPRESENTATION_ITEM('')
SURFACE()
);
#2522=(
BOUNDED_SURFACE()
B_SPLINE_SURFACE(3,2,((#386051,#386052,#386053),(#386054,#386055,#386056),
(#386057,#386058,#386059),(#386060,#386061,#386062)),.UNSPECIFIED.,.F.,
 .F.,.F.)
B_SPLINE_SURFACE_WITH_KNOTS((4,4),(3,3),(-1.54744435122071E-6,1.54744435122078E-5),
(-0.0151698983634562,1.),.UNSPECIFIED.)
GEOMETRIC_REPRESENTATION_ITEM()
RATIONAL_B_SPLINE_SURFACE(((1.02018382473136,0.334740937355685,1.),(1.00401234488861,
0.867753072813108,1.),(1.00033622856783,0.988917903080856,1.),(1.,1.,1.)))
REPRESENTATION_ITEM('')
SURFACE()
);
#2523=(
BOUNDED_SURFACE()
B_SPLINE_SURFACE(3,2,((#386064,#386065,#386066),(#386067,#386068,#386069),
(#386070,#386071,#386072),(#386073,#386074,#386075)),.UNSPECIFIED.,.F.,
 .F.,.F.)
B_SPLINE_SURFACE_WITH_KNOTS((4,4),(3,3),(0.00137194782501028,0.00149814269699235),
(0.,1.),.UNSPECIFIED.)
GEOMETRIC_REPRESENTATION_ITEM()
RATIONAL_B_SPLINE_SURFACE(((1.,0.815158509402317,1.),(1.,0.816179044148167,
1.),(1.,0.817226308119926,1.),(1.,0.818301939488808,1.)))
REPRESENTATION_ITEM('')
SURFACE()
);
#2524=(
BOUNDED_SURFACE()
B_SPLINE_SURFACE(3,2,((#386119,#386120,#386121),(#386122,#386123,#386124),
(#386125,#386126,#386127),(#386128,#386129,#386130)),.UNSPECIFIED.,.F.,
 .F.,.F.)
B_SPLINE_SURFACE_WITH_KNOTS((4,4),(3,3),(1.55009486301137E-5,4.92065510474429E-5),
(-8.13759514961233E-5,1.),.UNSPECIFIED.)
GEOMETRIC_REPRESENTATION_ITEM()
RATIONAL_B_SPLINE_SURFACE(((1.00002372912336,0.854200639599683,1.),(1.00001423585994,
0.912530301180529,1.),(1.00000710550471,0.956341495377432,1.),(1.00001238975909,
0.923873338137021,1.)))
REPRESENTATION_ITEM('')
SURFACE()
);
#2525=(
BOUNDED_SURFACE()
B_SPLINE_SURFACE(3,2,((#386134,#386135,#386136),(#386137,#386138,#386139),
(#386140,#386141,#386142),(#386143,#386144,#386145)),.UNSPECIFIED.,.F.,
 .F.,.F.)
B_SPLINE_SURFACE_WITH_KNOTS((4,4),(3,3),(-3.39934179457838E-6,3.73927597403565E-5),
(-0.00186004067399421,1.00069373317385),.UNSPECIFIED.)
GEOMETRIC_REPRESENTATION_ITEM()
RATIONAL_B_SPLINE_SURFACE(((1.00072100136047,0.806051963875509,1.0002685964267),
(1.00060048440148,0.838470803558736,1.00022369994478),(1.00053106448789,
0.857144632272504,1.00019783877204),(1.00054515072847,0.853355459539207,
1.00020308635421)))
REPRESENTATION_ITEM('')
SURFACE()
);
#2526=(
BOUNDED_SURFACE()
B_SPLINE_SURFACE(3,2,((#386147,#386148,#386149),(#386150,#386151,#386152),
(#386153,#386154,#386155),(#386156,#386157,#386158)),.UNSPECIFIED.,.F.,
 .F.,.F.)
B_SPLINE_SURFACE_WITH_KNOTS((4,4),(3,3),(0.,9.54361881492174E-5),(0.,1.),
 .UNSPECIFIED.)
GEOMETRIC_REPRESENTATION_ITEM()
RATIONAL_B_SPLINE_SURFACE(((1.,0.816715621142053,1.),(1.,0.81590758740794,
1.),(1.,0.815115959345204,1.),(1.,0.814339887349195,1.)))
REPRESENTATION_ITEM('')
SURFACE()
);
#2527=(
BOUNDED_SURFACE()
B_SPLINE_SURFACE(3,2,((#386160,#386161,#386162),(#386163,#386164,#386165),
(#386166,#386167,#386168),(#386169,#386170,#386171)),.UNSPECIFIED.,.F.,
 .F.,.F.)
B_SPLINE_SURFACE_WITH_KNOTS((4,4),(3,3),(-1.76182853028894E-19,4.68197758448203E-5),
(0.,1.),.UNSPECIFIED.)
GEOMETRIC_REPRESENTATION_ITEM()
RATIONAL_B_SPLINE_SURFACE(((1.,0.816715621142051,1.),(1.,0.953638980025202,
1.),(1.,0.954506925408056,1.),(1.,0.816715621142056,1.)))
REPRESENTATION_ITEM('')
SURFACE()
);
#2528=(
BOUNDED_SURFACE()
B_SPLINE_SURFACE(3,2,((#386173,#386174,#386175),(#386176,#386177,#386178),
(#386179,#386180,#386181),(#386182,#386183,#386184)),.UNSPECIFIED.,.F.,
 .F.,.F.)
B_SPLINE_SURFACE_WITH_KNOTS((4,4),(3,3),(-2.71050543121376E-19,9.54361881492173E-5),
(0.,1.),.UNSPECIFIED.)
GEOMETRIC_REPRESENTATION_ITEM()
RATIONAL_B_SPLINE_SURFACE(((1.,0.814339887349194,1.),(1.,0.815115959345203,
1.),(1.,0.815907587407945,1.),(1.,0.816715621142049,1.)))
REPRESENTATION_ITEM('')
SURFACE()
);
#2529=(
BOUNDED_SURFACE()
B_SPLINE_SURFACE(3,2,((#386186,#386187,#386188),(#386189,#386190,#386191),
(#386192,#386193,#386194),(#386195,#386196,#386197)),.UNSPECIFIED.,.F.,
 .F.,.F.)
B_SPLINE_SURFACE_WITH_KNOTS((4,4),(3,3),(-3.39528393502482E-6,3.73481232852729E-5),
(-0.00165018033288066,1.),.UNSPECIFIED.)
GEOMETRIC_REPRESENTATION_ITEM()
RATIONAL_B_SPLINE_SURFACE(((1.00048354385554,0.853487571660457,1.),(1.00047110510909,
0.85725647685152,1.),(1.00053193201094,0.838826096655938,1.),(1.0006397068771,
0.80617061531017,1.)))
REPRESENTATION_ITEM('')
SURFACE()
);
#2530=(
BOUNDED_SURFACE()
B_SPLINE_SURFACE(3,2,((#386201,#386202,#386203),(#386204,#386205,#386206),
(#386207,#386208,#386209),(#386210,#386211,#386212)),.UNSPECIFIED.,.F.,
 .F.,.F.)
B_SPLINE_SURFACE_WITH_KNOTS((4,4),(3,3),(2.02993869230509E-5,5.39756952687121E-5),
(-0.000116281069688478,1.),.UNSPECIFIED.)
GEOMETRIC_REPRESENTATION_ITEM()
RATIONAL_B_SPLINE_SURFACE(((1.00001770479726,0.923870681143028,1.),(1.00001014104057,
0.956394275543453,1.),(1.00002037300274,0.912397594905643,1.),(1.00003390859462,
0.854195550869773,1.)))
REPRESENTATION_ITEM('')
SURFACE()
);
#2531=(
BOUNDED_SURFACE()
B_SPLINE_SURFACE(3,2,((#386305,#386306,#386307),(#386308,#386309,#386310),
(#386311,#386312,#386313),(#386314,#386315,#386316)),.UNSPECIFIED.,.F.,
 .F.,.F.)
B_SPLINE_SURFACE_WITH_KNOTS((4,4),(3,3),(0.00135801595889393,0.00148409170619832),
(0.,1.),.UNSPECIFIED.)
GEOMETRIC_REPRESENTATION_ITEM()
RATIONAL_B_SPLINE_SURFACE(((1.,0.818301933966445,1.),(1.,0.817226613172355,
1.),(1.,0.816179643373943,1.),(1.,0.815159387863657,1.)))
REPRESENTATION_ITEM('')
SURFACE()
);
#2532=(
BOUNDED_SURFACE()
B_SPLINE_SURFACE(3,2,((#386355,#386356,#386357),(#386358,#386359,#386360),
(#386361,#386362,#386363),(#386364,#386365,#386366)),.UNSPECIFIED.,.F.,
 .F.,.F.)
B_SPLINE_SURFACE_WITH_KNOTS((4,4),(3,3),(-1.54744435122083E-6,1.54744435122081E-5),
(-0.0151698983585689,1.01516989836374),.UNSPECIFIED.)
GEOMETRIC_REPRESENTATION_ITEM()
RATIONAL_B_SPLINE_SURFACE(((1.02018382472476,0.324498219413556,1.02018382473175),
(1.0040123448873,0.865716921710493,1.00401234488869),(1.00033622856772,
0.988747276629742,1.00033622856784),(1.,1.,1.)))
REPRESENTATION_ITEM('')
SURFACE()
);
#2533=(
BOUNDED_SURFACE()
B_SPLINE_SURFACE(3,2,((#386368,#386369,#386370),(#386371,#386372,#386373),
(#386374,#386375,#386376),(#386377,#386378,#386379)),.UNSPECIFIED.,.F.,
 .F.,.F.)
B_SPLINE_SURFACE_WITH_KNOTS((4,4),(3,3),(0.00137194782501028,0.00149814269699235),
(0.,1.),.UNSPECIFIED.)
GEOMETRIC_REPRESENTATION_ITEM()
RATIONAL_B_SPLINE_SURFACE(((1.,0.815158509402318,1.),(1.,0.816179044148175,
1.),(1.,0.817226308119926,1.),(1.,0.818301939488811,1.)))
REPRESENTATION_ITEM('')
SURFACE()
);
#2534=(
BOUNDED_SURFACE()
B_SPLINE_SURFACE(3,2,((#386423,#386424,#386425),(#386426,#386427,#386428),
(#386429,#386430,#386431),(#386432,#386433,#386434)),.UNSPECIFIED.,.F.,
 .F.,.F.)
B_SPLINE_SURFACE_WITH_KNOTS((4,4),(3,3),(1.55009486301138E-5,4.92065510474436E-5),
(-8.13759515694668E-5,1.),.UNSPECIFIED.)
GEOMETRIC_REPRESENTATION_ITEM()
RATIONAL_B_SPLINE_SURFACE(((1.00002372912338,0.854200639599671,1.),(1.00001423585995,
0.912530301180525,1.),(1.00000710550472,0.956341495377431,1.),(1.0000123897591,
0.923873338137017,1.)))
REPRESENTATION_ITEM('')
SURFACE()
);
#2535=(
BOUNDED_SURFACE()
B_SPLINE_SURFACE(3,2,((#386438,#386439,#386440),(#386441,#386442,#386443),
(#386444,#386445,#386446),(#386447,#386448,#386449)),.UNSPECIFIED.,.F.,
 .F.,.F.)
B_SPLINE_SURFACE_WITH_KNOTS((4,4),(3,3),(-3.39934179457811E-6,3.73927597403567E-5),
(-0.0018600406746428,1.00069373317446),.UNSPECIFIED.)
GEOMETRIC_REPRESENTATION_ITEM()
RATIONAL_B_SPLINE_SURFACE(((1.00072100136072,0.806051963875256,1.00026859642693),
(1.00060048440169,0.838470803558557,1.00022369994498),(1.00053106448808,
0.857144632272301,1.00019783877221),(1.00054515072866,0.853355459539024,
1.00020308635439)))
REPRESENTATION_ITEM('')
SURFACE()
);
#2536=(
BOUNDED_SURFACE()
B_SPLINE_SURFACE(3,2,((#386451,#386452,#386453),(#386454,#386455,#386456),
(#386457,#386458,#386459),(#386460,#386461,#386462)),.UNSPECIFIED.,.F.,
 .F.,.F.)
B_SPLINE_SURFACE_WITH_KNOTS((4,4),(3,3),(2.71050543121376E-19,9.54361881492177E-5),
(0.,1.),.UNSPECIFIED.)
GEOMETRIC_REPRESENTATION_ITEM()
RATIONAL_B_SPLINE_SURFACE(((1.,0.816715621142051,1.),(1.,0.815907587407941,
1.),(1.,0.815115959345211,1.),(1.,0.814339887349194,1.)))
REPRESENTATION_ITEM('')
SURFACE()
);
#2537=(
BOUNDED_SURFACE()
B_SPLINE_SURFACE(3,2,((#386464,#386465,#386466),(#386467,#386468,#386469),
(#386470,#386471,#386472),(#386473,#386474,#386475)),.UNSPECIFIED.,.F.,
 .F.,.F.)
B_SPLINE_SURFACE_WITH_KNOTS((4,4),(3,3),(-4.91279109407494E-20,4.68197758448206E-5),
(0.,1.),.UNSPECIFIED.)
GEOMETRIC_REPRESENTATION_ITEM()
RATIONAL_B_SPLINE_SURFACE(((1.,0.81671562114205,1.),(1.,0.953638980025202,
1.),(1.,0.954506925408066,1.),(1.,0.816715621142053,1.)))
REPRESENTATION_ITEM('')
SURFACE()
);
#2538=(
BOUNDED_SURFACE()
B_SPLINE_SURFACE(3,2,((#386477,#386478,#386479),(#386480,#386481,#386482),
(#386483,#386484,#386485),(#386486,#386487,#386488)),.UNSPECIFIED.,.F.,
 .F.,.F.)
B_SPLINE_SURFACE_WITH_KNOTS((4,4),(3,3),(0.,9.54361881492175E-5),(0.,1.),
 .UNSPECIFIED.)
GEOMETRIC_REPRESENTATION_ITEM()
RATIONAL_B_SPLINE_SURFACE(((1.,0.814339887349197,1.),(1.,0.815115959345201,
1.),(1.,0.815907587407948,1.),(1.,0.81671562114205,1.)))
REPRESENTATION_ITEM('')
SURFACE()
);
#2539=(
BOUNDED_SURFACE()
B_SPLINE_SURFACE(3,2,((#386490,#386491,#386492),(#386493,#386494,#386495),
(#386496,#386497,#386498),(#386499,#386500,#386501)),.UNSPECIFIED.,.F.,
 .F.,.F.)
B_SPLINE_SURFACE_WITH_KNOTS((4,4),(3,3),(-3.39528393502379E-6,3.73481232852733E-5),
(-0.00165018033281,1.),.UNSPECIFIED.)
GEOMETRIC_REPRESENTATION_ITEM()
RATIONAL_B_SPLINE_SURFACE(((1.00048354385552,0.853487571660465,1.),(1.00047110510907,
0.857256476851538,1.),(1.00053193201092,0.838826096655939,1.),(1.00063970687707,
0.806170615310189,0.999999999999999)))
REPRESENTATION_ITEM('')
SURFACE()
);
#2540=(
BOUNDED_SURFACE()
B_SPLINE_SURFACE(3,2,((#386505,#386506,#386507),(#386508,#386509,#386510),
(#386511,#386512,#386513),(#386514,#386515,#386516)),.UNSPECIFIED.,.F.,
 .F.,.F.)
B_SPLINE_SURFACE_WITH_KNOTS((4,4),(3,3),(2.02993869230507E-5,5.3975695268713E-5),
(-0.000116281070062206,1.),.UNSPECIFIED.)
GEOMETRIC_REPRESENTATION_ITEM()
RATIONAL_B_SPLINE_SURFACE(((1.00001770479732,0.923870681143,1.),(1.0000101410406,
0.956394275543443,1.),(1.00002037300281,0.912397594905605,1.),(1.00003390859473,
0.854195550869708,1.)))
REPRESENTATION_ITEM('')
SURFACE()
);
#2541=(
BOUNDED_SURFACE()
B_SPLINE_SURFACE(3,2,((#386609,#386610,#386611),(#386612,#386613,#386614),
(#386615,#386616,#386617),(#386618,#386619,#386620)),.UNSPECIFIED.,.F.,
 .F.,.F.)
B_SPLINE_SURFACE_WITH_KNOTS((4,4),(3,3),(0.00135801595889393,0.00148409170619832),
(0.,1.),.UNSPECIFIED.)
GEOMETRIC_REPRESENTATION_ITEM()
RATIONAL_B_SPLINE_SURFACE(((1.,0.818301933966441,1.),(1.,0.817226613172342,
1.),(1.,0.816179643373956,1.),(1.,0.815159387863641,1.)))
REPRESENTATION_ITEM('')
SURFACE()
);
#2542=(
BOUNDED_SURFACE()
B_SPLINE_SURFACE(3,2,((#386659,#386660,#386661),(#386662,#386663,#386664),
(#386665,#386666,#386667),(#386668,#386669,#386670)),.UNSPECIFIED.,.F.,
 .F.,.F.)
B_SPLINE_SURFACE_WITH_KNOTS((4,4),(3,3),(-1.54744435122073E-6,1.54744435122074E-5),
(-0.0151698983629041,1.01516989835958),.UNSPECIFIED.)
GEOMETRIC_REPRESENTATION_ITEM()
RATIONAL_B_SPLINE_SURFACE(((1.02018382473062,0.324498219413462,1.02018382472613),
(1.00401234488846,0.865716921710508,1.00401234488757),(1.00033622856782,
0.988747276629692,1.00033622856775),(1.,1.,1.)))
REPRESENTATION_ITEM('')
SURFACE()
);
#2543=(
BOUNDED_SURFACE()
B_SPLINE_SURFACE(3,2,((#386672,#386673,#386674),(#386675,#386676,#386677),
(#386678,#386679,#386680),(#386681,#386682,#386683)),.UNSPECIFIED.,.F.,
 .F.,.F.)
B_SPLINE_SURFACE_WITH_KNOTS((4,4),(3,3),(0.00137194782501028,0.00149814269699235),
(0.,1.),.UNSPECIFIED.)
GEOMETRIC_REPRESENTATION_ITEM()
RATIONAL_B_SPLINE_SURFACE(((1.,0.815158509402317,1.),(1.,0.816179044148162,
1.),(1.,0.817226308119928,1.),(1.,0.818301939488809,1.)))
REPRESENTATION_ITEM('')
SURFACE()
);
#2544=(
BOUNDED_SURFACE()
B_SPLINE_SURFACE(3,2,((#386727,#386728,#386729),(#386730,#386731,#386732),
(#386733,#386734,#386735),(#386736,#386737,#386738)),.UNSPECIFIED.,.F.,
 .F.,.F.)
B_SPLINE_SURFACE_WITH_KNOTS((4,4),(3,3),(1.55009486301137E-5,4.92065510474433E-5),
(-8.13759518888895E-5,1.),.UNSPECIFIED.)
GEOMETRIC_REPRESENTATION_ITEM()
RATIONAL_B_SPLINE_SURFACE(((1.00002372912348,0.854200639599625,1.),(1.00001423586001,
0.912530301180506,1.),(1.00000710550474,0.956341495377407,1.),(1.00001238975915,
0.923873338136996,1.)))
REPRESENTATION_ITEM('')
SURFACE()
);
#2545=(
BOUNDED_SURFACE()
B_SPLINE_SURFACE(3,2,((#386742,#386743,#386744),(#386745,#386746,#386747),
(#386748,#386749,#386750),(#386751,#386752,#386753)),.UNSPECIFIED.,.F.,
 .F.,.F.)
B_SPLINE_SURFACE_WITH_KNOTS((4,4),(3,3),(-3.39934179457743E-6,3.73927597403565E-5),
(-0.0018600406739329,1.00069373317448),.UNSPECIFIED.)
GEOMETRIC_REPRESENTATION_ITEM()
RATIONAL_B_SPLINE_SURFACE(((1.00072100136045,0.806051963875354,1.00026859642694),
(1.00060048440146,0.838470803558705,1.00022369994498),(1.00053106448787,
0.857144632272372,1.00019783877222),(1.00054515072845,0.853355459539128,
1.00020308635439)))
REPRESENTATION_ITEM('')
SURFACE()
);
#2546=(
BOUNDED_SURFACE()
B_SPLINE_SURFACE(3,2,((#386755,#386756,#386757),(#386758,#386759,#386760),
(#386761,#386762,#386763),(#386764,#386765,#386766)),.UNSPECIFIED.,.F.,
 .F.,.F.)
B_SPLINE_SURFACE_WITH_KNOTS((4,4),(3,3),(0.,9.54361881492174E-5),(0.,1.),
 .UNSPECIFIED.)
GEOMETRIC_REPRESENTATION_ITEM()
RATIONAL_B_SPLINE_SURFACE(((1.,0.816715621142047,1.),(1.,0.815907587407938,
1.),(1.,0.815115959345211,1.),(1.,0.81433988734918,1.)))
REPRESENTATION_ITEM('')
SURFACE()
);
#2547=(
BOUNDED_SURFACE()
B_SPLINE_SURFACE(3,2,((#386768,#386769,#386770),(#386771,#386772,#386773),
(#386774,#386775,#386776),(#386777,#386778,#386779)),.UNSPECIFIED.,.F.,
 .F.,.F.)
B_SPLINE_SURFACE_WITH_KNOTS((4,4),(3,3),(5.59041745187838E-20,4.68197758448209E-5),
(0.,1.),.UNSPECIFIED.)
GEOMETRIC_REPRESENTATION_ITEM()
RATIONAL_B_SPLINE_SURFACE(((1.,0.81671562114205,1.),(1.,0.953638980025216,
1.),(1.,0.954506925408045,1.),(1.,0.816715621142053,1.)))
REPRESENTATION_ITEM('')
SURFACE()
);
#2548=(
BOUNDED_SURFACE()
B_SPLINE_SURFACE(3,2,((#386781,#386782,#386783),(#386784,#386785,#386786),
(#386787,#386788,#386789),(#386790,#386791,#386792)),.UNSPECIFIED.,.F.,
 .F.,.F.)
B_SPLINE_SURFACE_WITH_KNOTS((4,4),(3,3),(-2.16840434497101E-19,9.54361881492178E-5),
(0.,1.),.UNSPECIFIED.)
GEOMETRIC_REPRESENTATION_ITEM()
RATIONAL_B_SPLINE_SURFACE(((1.,0.814339887349194,1.),(1.,0.815115959345191,
1.),(1.,0.815907587407956,1.),(1.,0.81671562114205,1.)))
REPRESENTATION_ITEM('')
SURFACE()
);
#2549=(
BOUNDED_SURFACE()
B_SPLINE_SURFACE(3,2,((#386794,#386795,#386796),(#386797,#386798,#386799),
(#386800,#386801,#386802),(#386803,#386804,#386805)),.UNSPECIFIED.,.F.,
 .F.,.F.)
B_SPLINE_SURFACE_WITH_KNOTS((4,4),(3,3),(-3.39528393502388E-6,3.73481232852735E-5),
(-0.00165018033239079,1.),.UNSPECIFIED.)
GEOMETRIC_REPRESENTATION_ITEM()
RATIONAL_B_SPLINE_SURFACE(((1.00048354385539,0.853487571660534,1.),(1.00047110510895,
0.857256476851569,1.),(1.00053193201079,0.838826096656041,1.),(1.00063970687691,
0.806170615310252,1.)))
REPRESENTATION_ITEM('')
SURFACE()
);
#2550=(
BOUNDED_SURFACE()
B_SPLINE_SURFACE(3,2,((#386809,#386810,#386811),(#386812,#386813,#386814),
(#386815,#386816,#386817),(#386818,#386819,#386820)),.UNSPECIFIED.,.F.,
 .F.,.F.)
B_SPLINE_SURFACE_WITH_KNOTS((4,4),(3,3),(2.02993869230509E-5,5.39756952687124E-5),
(-0.000116281070051072,1.),.UNSPECIFIED.)
GEOMETRIC_REPRESENTATION_ITEM()
RATIONAL_B_SPLINE_SURFACE(((1.00001770479732,0.923870681143,1.),(1.0000101410406,
0.956394275543444,1.),(1.00002037300281,0.912397594905592,1.),(1.00003390859473,
0.854195550869727,1.)))
REPRESENTATION_ITEM('')
SURFACE()
);
#2551=(
BOUNDED_SURFACE()
B_SPLINE_SURFACE(3,2,((#386913,#386914,#386915),(#386916,#386917,#386918),
(#386919,#386920,#386921),(#386922,#386923,#386924)),.UNSPECIFIED.,.F.,
 .F.,.F.)
B_SPLINE_SURFACE_WITH_KNOTS((4,4),(3,3),(0.00135801595889393,0.00148409170619832),
(0.,1.),.UNSPECIFIED.)
GEOMETRIC_REPRESENTATION_ITEM()
RATIONAL_B_SPLINE_SURFACE(((1.,0.818301933966444,1.),(1.,0.817226613172349,
1.),(1.,0.816179643373945,1.),(1.,0.815159387863654,1.)))
REPRESENTATION_ITEM('')
SURFACE()
);
#2552=(
BOUNDED_SURFACE()
B_SPLINE_SURFACE(3,2,((#386963,#386964,#386965),(#386966,#386967,#386968),
(#386969,#386970,#386971),(#386972,#386973,#386974)),.UNSPECIFIED.,.F.,
 .F.,.F.)
B_SPLINE_SURFACE_WITH_KNOTS((4,4),(3,3),(-1.54744435121951E-6,1.5474443512209E-5),
(-0.0151698983658987,1.),.UNSPECIFIED.)
GEOMETRIC_REPRESENTATION_ITEM()
RATIONAL_B_SPLINE_SURFACE(((1.02018382473466,0.334740937354148,1.),(1.00401234488927,
0.867753072812766,1.),(1.00033622856789,0.988917903080833,1.),(1.,1.,1.)))
REPRESENTATION_ITEM('')
SURFACE()
);
#2553=(
BOUNDED_SURFACE()
B_SPLINE_SURFACE(3,2,((#386976,#386977,#386978),(#386979,#386980,#386981),
(#386982,#386983,#386984),(#386985,#386986,#386987)),.UNSPECIFIED.,.F.,
 .F.,.F.)
B_SPLINE_SURFACE_WITH_KNOTS((4,4),(3,3),(0.00137194782501028,0.00149814269699235),
(0.,1.),.UNSPECIFIED.)
GEOMETRIC_REPRESENTATION_ITEM()
RATIONAL_B_SPLINE_SURFACE(((1.,0.815158509402322,1.),(1.,0.816179044148155,
1.),(1.,0.817226308119924,1.),(1.,0.818301939488806,1.)))
REPRESENTATION_ITEM('')
SURFACE()
);
#2554=(
BOUNDED_SURFACE()
B_SPLINE_SURFACE(3,2,((#387031,#387032,#387033),(#387034,#387035,#387036),
(#387037,#387038,#387039),(#387040,#387041,#387042)),.UNSPECIFIED.,.F.,
 .F.,.F.)
B_SPLINE_SURFACE_WITH_KNOTS((4,4),(3,3),(1.55009486301137E-5,4.92065510474438E-5),
(-8.13759515736558E-5,1.),.UNSPECIFIED.)
GEOMETRIC_REPRESENTATION_ITEM()
RATIONAL_B_SPLINE_SURFACE(((1.00002372912338,0.854200639599664,1.),(1.00001423585995,
0.912530301180544,1.),(1.00000710550472,0.956341495377414,1.),(1.0000123897591,
0.923873338137018,1.)))
REPRESENTATION_ITEM('')
SURFACE()
);
#2555=(
BOUNDED_SURFACE()
B_SPLINE_SURFACE(3,2,((#387046,#387047,#387048),(#387049,#387050,#387051),
(#387052,#387053,#387054),(#387055,#387056,#387057)),.UNSPECIFIED.,.F.,
 .F.,.F.)
B_SPLINE_SURFACE_WITH_KNOTS((4,4),(3,3),(-3.39934179457825E-6,3.73927597403565E-5),
(-0.00186004067397268,1.00069373317423),.UNSPECIFIED.)
GEOMETRIC_REPRESENTATION_ITEM()
RATIONAL_B_SPLINE_SURFACE(((1.00072100136046,0.806051963875417,1.00026859642684),
(1.00060048440147,0.838470803558705,1.0002236999449),(1.00053106448789,
0.857144632272435,1.00019783877215),(1.00054515072846,0.853355459539152,
1.00020308635432)))
REPRESENTATION_ITEM('')
SURFACE()
);
#2556=(
BOUNDED_SURFACE()
B_SPLINE_SURFACE(3,2,((#387059,#387060,#387061),(#387062,#387063,#387064),
(#387065,#387066,#387067),(#387068,#387069,#387070)),.UNSPECIFIED.,.F.,
 .F.,.F.)
B_SPLINE_SURFACE_WITH_KNOTS((4,4),(3,3),(0.,9.54361881492175E-5),(0.,1.),
 .UNSPECIFIED.)
GEOMETRIC_REPRESENTATION_ITEM()
RATIONAL_B_SPLINE_SURFACE(((1.,0.81671562114206,1.),(1.,0.81590758740792,
1.),(1.,0.815115959345222,1.),(1.,0.814339887349192,1.)))
REPRESENTATION_ITEM('')
SURFACE()
);
#2557=(
BOUNDED_SURFACE()
B_SPLINE_SURFACE(3,2,((#387072,#387073,#387074),(#387075,#387076,#387077),
(#387078,#387079,#387080),(#387081,#387082,#387083)),.UNSPECIFIED.,.F.,
 .F.,.F.)
B_SPLINE_SURFACE_WITH_KNOTS((4,4),(3,3),(1.64324391767334E-19,4.68197758448208E-5),
(0.,1.),.UNSPECIFIED.)
GEOMETRIC_REPRESENTATION_ITEM()
RATIONAL_B_SPLINE_SURFACE(((1.,0.816715621142038,1.),(1.,0.953638980025226,
1.),(1.,0.954506925408039,1.),(1.,0.816715621142058,1.)))
REPRESENTATION_ITEM('')
SURFACE()
);
#2558=(
BOUNDED_SURFACE()
B_SPLINE_SURFACE(3,2,((#387085,#387086,#387087),(#387088,#387089,#387090),
(#387091,#387092,#387093),(#387094,#387095,#387096)),.UNSPECIFIED.,.F.,
 .F.,.F.)
B_SPLINE_SURFACE_WITH_KNOTS((4,4),(3,3),(1.62630325872826E-19,9.5436188149218E-5),
(0.,1.),.UNSPECIFIED.)
GEOMETRIC_REPRESENTATION_ITEM()
RATIONAL_B_SPLINE_SURFACE(((1.,0.814339887349191,1.),(1.,0.815115959345203,
1.),(1.,0.815907587407944,1.),(1.,0.816715621142039,1.)))
REPRESENTATION_ITEM('')
SURFACE()
);
#2559=(
BOUNDED_SURFACE()
B_SPLINE_SURFACE(3,2,((#387098,#387099,#387100),(#387101,#387102,#387103),
(#387104,#387105,#387106),(#387107,#387108,#387109)),.UNSPECIFIED.,.F.,
 .F.,.F.)
B_SPLINE_SURFACE_WITH_KNOTS((4,4),(3,3),(-3.39528393502273E-6,3.73481232852735E-5),
(-0.00165018033329502,1.),.UNSPECIFIED.)
GEOMETRIC_REPRESENTATION_ITEM()
RATIONAL_B_SPLINE_SURFACE(((1.00048354385566,0.853487571660388,0.999999999999999),
(1.00047110510921,0.857256476851473,1.),(1.00053193201108,0.838826096655837,
1.),(1.00063970687726,0.80617061531011,1.)))
REPRESENTATION_ITEM('')
SURFACE()
);
#2560=(
BOUNDED_SURFACE()
B_SPLINE_SURFACE(3,2,((#387113,#387114,#387115),(#387116,#387117,#387118),
(#387119,#387120,#387121),(#387122,#387123,#387124)),.UNSPECIFIED.,.F.,
 .F.,.F.)
B_SPLINE_SURFACE_WITH_KNOTS((4,4),(3,3),(2.02993869230509E-5,5.39756952687125E-5),
(-0.000116281069404188,1.),.UNSPECIFIED.)
GEOMETRIC_REPRESENTATION_ITEM()
RATIONAL_B_SPLINE_SURFACE(((1.00001770479722,0.923870681143052,1.),(1.00001014104054,
0.95639427554346,1.),(1.00002037300269,0.912397594905661,1.),(1.00003390859454,
0.854195550869813,1.)))
REPRESENTATION_ITEM('')
SURFACE()
);
#2561=(
BOUNDED_SURFACE()
B_SPLINE_SURFACE(3,2,((#387217,#387218,#387219),(#387220,#387221,#387222),
(#387223,#387224,#387225),(#387226,#387227,#387228)),.UNSPECIFIED.,.F.,
 .F.,.F.)
B_SPLINE_SURFACE_WITH_KNOTS((4,4),(3,3),(0.00135801595889393,0.00148409170619832),
(0.,1.),.UNSPECIFIED.)
GEOMETRIC_REPRESENTATION_ITEM()
RATIONAL_B_SPLINE_SURFACE(((1.,0.818301933966441,1.),(1.,0.817226613172353,
1.),(1.,0.816179643373937,1.),(1.,0.815159387863654,1.)))
REPRESENTATION_ITEM('')
SURFACE()
);
#2562=(
BOUNDED_SURFACE()
B_SPLINE_SURFACE(3,2,((#387267,#387268,#387269),(#387270,#387271,#387272),
(#387273,#387274,#387275),(#387276,#387277,#387278)),.UNSPECIFIED.,.F.,
 .F.,.F.)
B_SPLINE_SURFACE_WITH_KNOTS((4,4),(3,3),(-1.54744435122068E-6,1.54744435122067E-5),
(-0.0151698983720345,1.),.UNSPECIFIED.)
GEOMETRIC_REPRESENTATION_ITEM()
RATIONAL_B_SPLINE_SURFACE(((1.02018382474295,0.334740937350091,1.),(1.00401234489091,
0.867753072811983,1.),(1.00033622856803,0.988917903080762,1.),(1.,1.,1.)))
REPRESENTATION_ITEM('')
SURFACE()
);
#2563=(
BOUNDED_SURFACE()
B_SPLINE_SURFACE(3,2,((#387280,#387281,#387282),(#387283,#387284,#387285),
(#387286,#387287,#387288),(#387289,#387290,#387291)),.UNSPECIFIED.,.F.,
 .F.,.F.)
B_SPLINE_SURFACE_WITH_KNOTS((4,4),(3,3),(0.00137194782501028,0.00149814269699235),
(0.,1.),.UNSPECIFIED.)
GEOMETRIC_REPRESENTATION_ITEM()
RATIONAL_B_SPLINE_SURFACE(((1.,0.815158509402319,1.),(1.,0.816179044148152,
1.),(1.,0.817226308119945,1.),(1.,0.818301939488801,1.)))
REPRESENTATION_ITEM('')
SURFACE()
);
#2564=(
BOUNDED_SURFACE()
B_SPLINE_SURFACE(3,2,((#387335,#387336,#387337),(#387338,#387339,#387340),
(#387341,#387342,#387343),(#387344,#387345,#387346)),.UNSPECIFIED.,.F.,
 .F.,.F.)
B_SPLINE_SURFACE_WITH_KNOTS((4,4),(3,3),(1.55009486301137E-5,4.92065510474429E-5),
(-8.13759515085778E-5,1.),.UNSPECIFIED.)
GEOMETRIC_REPRESENTATION_ITEM()
RATIONAL_B_SPLINE_SURFACE(((1.00002372912336,0.854200639599683,1.),(1.00001423585994,
0.912530301180521,1.),(1.00000710550471,0.956341495377441,1.),(1.00001238975909,
0.923873338137018,1.)))
REPRESENTATION_ITEM('')
SURFACE()
);
#2565=(
BOUNDED_SURFACE()
B_SPLINE_SURFACE(3,2,((#387350,#387351,#387352),(#387353,#387354,#387355),
(#387356,#387357,#387358),(#387359,#387360,#387361)),.UNSPECIFIED.,.F.,
 .F.,.F.)
B_SPLINE_SURFACE_WITH_KNOTS((4,4),(3,3),(-3.39934179457791E-6,3.73927597403567E-5),
(-0.00186004067370867,1.00069373317445),.UNSPECIFIED.)
GEOMETRIC_REPRESENTATION_ITEM()
RATIONAL_B_SPLINE_SURFACE(((1.00072100136036,0.806051963875422,1.00026859642693),
(1.00060048440138,0.838470803558717,1.00022369994497),(1.00053106448781,
0.857144632272427,1.00019783877221),(1.00054515072838,0.853355459539162,
1.00020308635438)))
REPRESENTATION_ITEM('')
SURFACE()
);
#2566=(
BOUNDED_SURFACE()
B_SPLINE_SURFACE(3,2,((#387363,#387364,#387365),(#387366,#387367,#387368),
(#387369,#387370,#387371),(#387372,#387373,#387374)),.UNSPECIFIED.,.F.,
 .F.,.F.)
B_SPLINE_SURFACE_WITH_KNOTS((4,4),(3,3),(-2.71050543121376E-19,9.54361881492173E-5),
(0.,1.),.UNSPECIFIED.)
GEOMETRIC_REPRESENTATION_ITEM()
RATIONAL_B_SPLINE_SURFACE(((1.,0.816715621142049,1.),(1.,0.815907587407939,
1.),(1.,0.815115959345212,1.),(1.,0.814339887349184,1.)))
REPRESENTATION_ITEM('')
SURFACE()
);
#2567=(
BOUNDED_SURFACE()
B_SPLINE_SURFACE(3,2,((#387376,#387377,#387378),(#387379,#387380,#387381),
(#387382,#387383,#387384),(#387385,#387386,#387387)),.UNSPECIFIED.,.F.,
 .F.,.F.)
B_SPLINE_SURFACE_WITH_KNOTS((4,4),(3,3),(-2.71050543121376E-20,4.68197758448208E-5),
(0.,1.),.UNSPECIFIED.)
GEOMETRIC_REPRESENTATION_ITEM()
RATIONAL_B_SPLINE_SURFACE(((1.,0.816715621142045,1.),(1.,0.953638980025206,
1.),(1.,0.954506925408058,1.),(1.,0.816715621142055,1.)))
REPRESENTATION_ITEM('')
SURFACE()
);
#2568=(
BOUNDED_SURFACE()
B_SPLINE_SURFACE(3,2,((#387389,#387390,#387391),(#387392,#387393,#387394),
(#387395,#387396,#387397),(#387398,#387399,#387400)),.UNSPECIFIED.,.F.,
 .F.,.F.)
B_SPLINE_SURFACE_WITH_KNOTS((4,4),(3,3),(-2.16840434497101E-19,9.54361881492175E-5),
(0.,1.),.UNSPECIFIED.)
GEOMETRIC_REPRESENTATION_ITEM()
RATIONAL_B_SPLINE_SURFACE(((1.,0.814339887349195,1.),(1.,0.815115959345194,
1.),(1.,0.815907587407954,1.),(1.,0.816715621142052,1.)))
REPRESENTATION_ITEM('')
SURFACE()
);
#2569=(
BOUNDED_SURFACE()
B_SPLINE_SURFACE(3,2,((#387402,#387403,#387404),(#387405,#387406,#387407),
(#387408,#387409,#387410),(#387411,#387412,#387413)),.UNSPECIFIED.,.F.,
 .F.,.F.)
B_SPLINE_SURFACE_WITH_KNOTS((4,4),(3,3),(-3.39528393502381E-6,3.73481232852725E-5),
(-0.00165018033340393,1.),.UNSPECIFIED.)
GEOMETRIC_REPRESENTATION_ITEM()
RATIONAL_B_SPLINE_SURFACE(((1.00048354385569,0.85348757166039,1.),(1.00047110510924,
0.857256476851414,1.),(1.00053193201111,0.83882609665589,1.),(1.0006397068773,
0.806170615310054,1.)))
REPRESENTATION_ITEM('')
SURFACE()
);
#2570=(
BOUNDED_SURFACE()
B_SPLINE_SURFACE(3,2,((#387417,#387418,#387419),(#387420,#387421,#387422),
(#387423,#387424,#387425),(#387426,#387427,#387428)),.UNSPECIFIED.,.F.,
 .F.,.F.)
B_SPLINE_SURFACE_WITH_KNOTS((4,4),(3,3),(2.02993869230509E-5,5.39756952687122E-5),
(-0.000116281069851099,1.),.UNSPECIFIED.)
GEOMETRIC_REPRESENTATION_ITEM()
RATIONAL_B_SPLINE_SURFACE(((1.00001770479729,0.923870681143016,1.),(1.00001014104058,
0.956394275543448,1.),(1.00002037300277,0.912397594905624,1.),(1.00003390859467,
0.854195550869753,1.)))
REPRESENTATION_ITEM('')
SURFACE()
);
#2571=(
BOUNDED_SURFACE()
B_SPLINE_SURFACE(3,2,((#387521,#387522,#387523),(#387524,#387525,#387526),
(#387527,#387528,#387529),(#387530,#387531,#387532)),.UNSPECIFIED.,.F.,
 .F.,.F.)
B_SPLINE_SURFACE_WITH_KNOTS((4,4),(3,3),(0.00135801595889393,0.00148409170619832),
(0.,1.),.UNSPECIFIED.)
GEOMETRIC_REPRESENTATION_ITEM()
RATIONAL_B_SPLINE_SURFACE(((1.,0.818301933966442,1.),(1.,0.817226613172339,
1.),(1.,0.816179643373948,1.),(1.,0.815159387863652,1.)))
REPRESENTATION_ITEM('')
SURFACE()
);
#2572=(
BOUNDED_SURFACE()
B_SPLINE_SURFACE(3,2,((#387571,#387572,#387573),(#387574,#387575,#387576),
(#387577,#387578,#387579),(#387580,#387581,#387582)),.UNSPECIFIED.,.F.,
 .F.,.F.)
B_SPLINE_SURFACE_WITH_KNOTS((4,4),(3,3),(-1.54744435122023E-6,1.54744435122092E-5),
(-0.0151698983759789,1.),.UNSPECIFIED.)
GEOMETRIC_REPRESENTATION_ITEM()
RATIONAL_B_SPLINE_SURFACE(((1.02018382474828,0.334740937347494,1.),(1.00401234489197,
0.867753072811548,1.),(1.00033622856812,0.988917903080688,1.),(1.,1.,1.)))
REPRESENTATION_ITEM('')
SURFACE()
);
#2573=(
BOUNDED_SURFACE()
B_SPLINE_SURFACE(3,2,((#387584,#387585,#387586),(#387587,#387588,#387589),
(#387590,#387591,#387592),(#387593,#387594,#387595)),.UNSPECIFIED.,.F.,
 .F.,.F.)
B_SPLINE_SURFACE_WITH_KNOTS((4,4),(3,3),(0.00137194782501028,0.00149814269699235),
(0.,1.),.UNSPECIFIED.)
GEOMETRIC_REPRESENTATION_ITEM()
RATIONAL_B_SPLINE_SURFACE(((1.,0.81515850940232,1.),(1.,0.816179044148172,
1.),(1.,0.817226308119932,1.),(1.,0.818301939488812,1.)))
REPRESENTATION_ITEM('')
SURFACE()
);
#2574=(
BOUNDED_SURFACE()
B_SPLINE_SURFACE(3,2,((#387639,#387640,#387641),(#387642,#387643,#387644),
(#387645,#387646,#387647),(#387648,#387649,#387650)),.UNSPECIFIED.,.F.,
 .F.,.F.)
B_SPLINE_SURFACE_WITH_KNOTS((4,4),(3,3),(1.55009486301137E-5,4.92065510474435E-5),
(-8.13759514590226E-5,1.),.UNSPECIFIED.)
GEOMETRIC_REPRESENTATION_ITEM()
RATIONAL_B_SPLINE_SURFACE(((1.00002372912335,0.854200639599691,1.),(1.00001423585993,
0.912530301180533,1.),(1.00000710550471,0.956341495377436,1.),(1.00001238975908,
0.923873338137026,1.)))
REPRESENTATION_ITEM('')
SURFACE()
);
#2575=(
BOUNDED_SURFACE()
B_SPLINE_SURFACE(3,2,((#387654,#387655,#387656),(#387657,#387658,#387659),
(#387660,#387661,#387662),(#387663,#387664,#387665)),.UNSPECIFIED.,.F.,
 .F.,.F.)
B_SPLINE_SURFACE_WITH_KNOTS((4,4),(3,3),(-3.39934179457859E-6,3.73927597403564E-5),
(-0.0018600406738678,1.00069373317437),.UNSPECIFIED.)
GEOMETRIC_REPRESENTATION_ITEM()
RATIONAL_B_SPLINE_SURFACE(((1.00072100136042,0.80605196387541,1.0002685964269),
(1.00060048440144,0.838470803558693,1.00022369994495),(1.00053106448786,
0.857144632272428,1.00019783877219),(1.00054515072843,0.853355459539146,
1.00020308635436)))
REPRESENTATION_ITEM('')
SURFACE()
);
#2576=(
BOUNDED_SURFACE()
B_SPLINE_SURFACE(3,2,((#387667,#387668,#387669),(#387670,#387671,#387672),
(#387673,#387674,#387675),(#387676,#387677,#387678)),.UNSPECIFIED.,.F.,
 .F.,.F.)
B_SPLINE_SURFACE_WITH_KNOTS((4,4),(3,3),(3.25260651745651E-19,9.54361881492174E-5),
(0.,1.),.UNSPECIFIED.)
GEOMETRIC_REPRESENTATION_ITEM()
RATIONAL_B_SPLINE_SURFACE(((1.,0.816715621142049,1.),(1.,0.815907587407951,
1.),(1.,0.815115959345193,1.),(1.,0.814339887349191,1.)))
REPRESENTATION_ITEM('')
SURFACE()
);
#2577=(
BOUNDED_SURFACE()
B_SPLINE_SURFACE(3,2,((#387680,#387681,#387682),(#387683,#387684,#387685),
(#387686,#387687,#387688),(#387689,#387690,#387691)),.UNSPECIFIED.,.F.,
 .F.,.F.)
B_SPLINE_SURFACE_WITH_KNOTS((4,4),(3,3),(2.84603070277445E-19,4.68197758448212E-5),
(0.,1.),.UNSPECIFIED.)
GEOMETRIC_REPRESENTATION_ITEM()
RATIONAL_B_SPLINE_SURFACE(((1.,0.816715621142052,1.),(1.,0.953638980025206,
1.),(1.,0.954506925408059,1.),(1.,0.816715621142047,1.)))
REPRESENTATION_ITEM('')
SURFACE()
);
#2578=(
BOUNDED_SURFACE()
B_SPLINE_SURFACE(3,2,((#387693,#387694,#387695),(#387696,#387697,#387698),
(#387699,#387700,#387701),(#387702,#387703,#387704)),.UNSPECIFIED.,.F.,
 .F.,.F.)
B_SPLINE_SURFACE_WITH_KNOTS((4,4),(3,3),(5.42101086242752E-20,9.54361881492178E-5),
(0.,1.),.UNSPECIFIED.)
GEOMETRIC_REPRESENTATION_ITEM()
RATIONAL_B_SPLINE_SURFACE(((1.,0.814339887349196,1.),(1.,0.815115959345201,
1.),(1.,0.81590758740795,1.),(1.,0.816715621142052,1.)))
REPRESENTATION_ITEM('')
SURFACE()
);
#2579=(
BOUNDED_SURFACE()
B_SPLINE_SURFACE(3,2,((#387706,#387707,#387708),(#387709,#387710,#387711),
(#387712,#387713,#387714),(#387715,#387716,#387717)),.UNSPECIFIED.,.F.,
 .F.,.F.)
B_SPLINE_SURFACE_WITH_KNOTS((4,4),(3,3),(-3.39528393502485E-6,3.73481232852734E-5),
(-0.00165018033328164,1.),.UNSPECIFIED.)
GEOMETRIC_REPRESENTATION_ITEM()
RATIONAL_B_SPLINE_SURFACE(((1.00048354385565,0.853487571660389,1.),(1.00047110510921,
0.857256476851473,1.),(1.00053193201107,0.838826096655867,1.),(1.00063970687725,
0.806170615310098,0.999999999999999)))
REPRESENTATION_ITEM('')
SURFACE()
);
#2580=(
BOUNDED_SURFACE()
B_SPLINE_SURFACE(3,2,((#387721,#387722,#387723),(#387724,#387725,#387726),
(#387727,#387728,#387729),(#387730,#387731,#387732)),.UNSPECIFIED.,.F.,
 .F.,.F.)
B_SPLINE_SURFACE_WITH_KNOTS((4,4),(3,3),(2.02993869230509E-5,5.39756952687131E-5),
(-0.000116281069453101,1.),.UNSPECIFIED.)
GEOMETRIC_REPRESENTATION_ITEM()
RATIONAL_B_SPLINE_SURFACE(((1.00001770479723,0.923870681143048,1.),(1.00001014104055,
0.956394275543459,1.),(1.0000203730027,0.912397594905651,1.),(1.00003390859455,
0.854195550869809,1.)))
REPRESENTATION_ITEM('')
SURFACE()
);
#2581=(
BOUNDED_SURFACE()
B_SPLINE_SURFACE(3,2,((#387825,#387826,#387827),(#387828,#387829,#387830),
(#387831,#387832,#387833),(#387834,#387835,#387836)),.UNSPECIFIED.,.F.,
 .F.,.F.)
B_SPLINE_SURFACE_WITH_KNOTS((4,4),(3,3),(0.00135801595889393,0.00148409170619832),
(0.,1.),.UNSPECIFIED.)
GEOMETRIC_REPRESENTATION_ITEM()
RATIONAL_B_SPLINE_SURFACE(((1.,0.818301933966442,1.),(1.,0.817226613172366,
1.),(1.,0.816179643373922,1.),(1.,0.815159387863662,1.)))
REPRESENTATION_ITEM('')
SURFACE()
);
#2582=(
BOUNDED_SURFACE()
B_SPLINE_SURFACE(3,2,((#387875,#387876,#387877),(#387878,#387879,#387880),
(#387881,#387882,#387883),(#387884,#387885,#387886)),.UNSPECIFIED.,.F.,
 .F.,.F.)
B_SPLINE_SURFACE_WITH_KNOTS((4,4),(3,3),(-1.54744435122083E-6,1.54744435122081E-5),
(-0.0151698983611594,1.0151698983615),.UNSPECIFIED.)
GEOMETRIC_REPRESENTATION_ITEM()
RATIONAL_B_SPLINE_SURFACE(((1.02018382472826,0.324498219413338,1.02018382472872),
(1.00401234488799,0.865716921710435,1.00401234488809),(1.00033622856778,
0.988747276629712,1.00033622856779),(1.,1.,1.)))
REPRESENTATION_ITEM('')
SURFACE()
);
#2583=(
BOUNDED_SURFACE()
B_SPLINE_SURFACE(3,2,((#387888,#387889,#387890),(#387891,#387892,#387893),
(#387894,#387895,#387896),(#387897,#387898,#387899)),.UNSPECIFIED.,.F.,
 .F.,.F.)
B_SPLINE_SURFACE_WITH_KNOTS((4,4),(3,3),(0.00137194782501028,0.00149814269699235),
(0.,1.),.UNSPECIFIED.)
GEOMETRIC_REPRESENTATION_ITEM()
RATIONAL_B_SPLINE_SURFACE(((1.,0.815158509402319,1.),(1.,0.816179044148163,
1.),(1.,0.817226308119931,1.),(1.,0.818301939488809,1.)))
REPRESENTATION_ITEM('')
SURFACE()
);
#2584=(
BOUNDED_SURFACE()
B_SPLINE_SURFACE(3,2,((#387943,#387944,#387945),(#387946,#387947,#387948),
(#387949,#387950,#387951),(#387952,#387953,#387954)),.UNSPECIFIED.,.F.,
 .F.,.F.)
B_SPLINE_SURFACE_WITH_KNOTS((4,4),(3,3),(1.55009486301137E-5,4.92065510474435E-5),
(-8.13759514136358E-5,1.),.UNSPECIFIED.)
GEOMETRIC_REPRESENTATION_ITEM()
RATIONAL_B_SPLINE_SURFACE(((1.00002372912334,0.854200639599699,1.),(1.00001423585992,
0.912530301180534,1.),(1.0000071055047,0.956341495377437,1.),(1.00001238975907,
0.923873338137028,1.)))
REPRESENTATION_ITEM('')
SURFACE()
);
#2585=(
BOUNDED_SURFACE()
B_SPLINE_SURFACE(3,2,((#387958,#387959,#387960),(#387961,#387962,#387963),
(#387964,#387965,#387966),(#387967,#387968,#387969)),.UNSPECIFIED.,.F.,
 .F.,.F.)
B_SPLINE_SURFACE_WITH_KNOTS((4,4),(3,3),(-3.39934179457858E-6,3.73927597403564E-5),
(-0.00186004067417087,1.0006937331743),.UNSPECIFIED.)
GEOMETRIC_REPRESENTATION_ITEM()
RATIONAL_B_SPLINE_SURFACE(((1.00072100136054,0.806051963875373,1.00026859642687),
(1.00060048440153,0.838470803558666,1.00022369994493),(1.00053106448794,
0.857144632272389,1.00019783877217),(1.00054515072852,0.853355459539116,
1.00020308635434)))
REPRESENTATION_ITEM('')
SURFACE()
);
#2586=(
BOUNDED_SURFACE()
B_SPLINE_SURFACE(3,2,((#387971,#387972,#387973),(#387974,#387975,#387976),
(#387977,#387978,#387979),(#387980,#387981,#387982)),.UNSPECIFIED.,.F.,
 .F.,.F.)
B_SPLINE_SURFACE_WITH_KNOTS((4,4),(3,3),(1.62630325872826E-19,9.54361881492172E-5),
(0.,1.),.UNSPECIFIED.)
GEOMETRIC_REPRESENTATION_ITEM()
RATIONAL_B_SPLINE_SURFACE(((1.,0.816715621142049,1.),(1.,0.815907587407932,
1.),(1.,0.815115959345205,1.),(1.,0.814339887349192,1.)))
REPRESENTATION_ITEM('')
SURFACE()
);
#2587=(
BOUNDED_SURFACE()
B_SPLINE_SURFACE(3,2,((#387984,#387985,#387986),(#387987,#387988,#387989),
(#387990,#387991,#387992),(#387993,#387994,#387995)),.UNSPECIFIED.,.F.,
 .F.,.F.)
B_SPLINE_SURFACE_WITH_KNOTS((4,4),(3,3),(1.25360876193636E-19,4.6819775844821E-5),
(0.,1.),.UNSPECIFIED.)
GEOMETRIC_REPRESENTATION_ITEM()
RATIONAL_B_SPLINE_SURFACE(((1.,0.816715621142052,1.),(1.,0.953638980025202,
1.),(1.,0.954506925408057,1.),(1.,0.816715621142041,1.)))
REPRESENTATION_ITEM('')
SURFACE()
);
#2588=(
BOUNDED_SURFACE()
B_SPLINE_SURFACE(3,2,((#387997,#387998,#387999),(#388000,#388001,#388002),
(#388003,#388004,#388005),(#388006,#388007,#388008)),.UNSPECIFIED.,.F.,
 .F.,.F.)
B_SPLINE_SURFACE_WITH_KNOTS((4,4),(3,3),(-5.42101086242752E-20,9.54361881492177E-5),
(0.,1.),.UNSPECIFIED.)
GEOMETRIC_REPRESENTATION_ITEM()
RATIONAL_B_SPLINE_SURFACE(((1.,0.814339887349194,1.),(1.,0.815115959345217,
1.),(1.,0.815907587407937,1.),(1.,0.816715621142052,1.)))
REPRESENTATION_ITEM('')
SURFACE()
);
#2589=(
BOUNDED_SURFACE()
B_SPLINE_SURFACE(3,2,((#388010,#388011,#388012),(#388013,#388014,#388015),
(#388016,#388017,#388018),(#388019,#388020,#388021)),.UNSPECIFIED.,.F.,
 .F.,.F.)
B_SPLINE_SURFACE_WITH_KNOTS((4,4),(3,3),(-3.3952839350248E-6,3.73481232852735E-5),
(-0.00165018033333831,1.),.UNSPECIFIED.)
GEOMETRIC_REPRESENTATION_ITEM()
RATIONAL_B_SPLINE_SURFACE(((1.00048354385567,0.853487571660397,1.),(1.00047110510922,
0.857256476851433,1.),(1.00053193201109,0.83882609665588,1.),(1.00063970687728,
0.80617061531008,1.)))
REPRESENTATION_ITEM('')
SURFACE()
);
#2590=(
BOUNDED_SURFACE()
B_SPLINE_SURFACE(3,2,((#388025,#388026,#388027),(#388028,#388029,#388030),
(#388031,#388032,#388033),(#388034,#388035,#388036)),.UNSPECIFIED.,.F.,
 .F.,.F.)
B_SPLINE_SURFACE_WITH_KNOTS((4,4),(3,3),(2.0299386923051E-5,5.39756952687129E-5),
(-0.000116281069825858,1.),.UNSPECIFIED.)
GEOMETRIC_REPRESENTATION_ITEM()
RATIONAL_B_SPLINE_SURFACE(((1.00001770479728,0.923870681143017,1.),(1.00001014104058,
0.956394275543444,1.),(1.00002037300277,0.912397594905627,1.),(1.00003390859466,
0.854195550869749,1.)))
REPRESENTATION_ITEM('')
SURFACE()
);
#2591=(
BOUNDED_SURFACE()
B_SPLINE_SURFACE(3,2,((#388129,#388130,#388131),(#388132,#388133,#388134),
(#388135,#388136,#388137),(#388138,#388139,#388140)),.UNSPECIFIED.,.F.,
 .F.,.F.)
B_SPLINE_SURFACE_WITH_KNOTS((4,4),(3,3),(0.00135801595889393,0.00148409170619832),
(0.,1.),.UNSPECIFIED.)
GEOMETRIC_REPRESENTATION_ITEM()
RATIONAL_B_SPLINE_SURFACE(((1.,0.818301933966442,1.),(1.,0.817226613172345,
1.),(1.,0.816179643373941,1.),(1.,0.815159387863652,1.)))
REPRESENTATION_ITEM('')
SURFACE()
);
#2592=(
BOUNDED_SURFACE()
B_SPLINE_SURFACE(3,2,((#388179,#388180,#388181),(#388182,#388183,#388184),
(#388185,#388186,#388187),(#388188,#388189,#388190)),.UNSPECIFIED.,.F.,
 .F.,.F.)
B_SPLINE_SURFACE_WITH_KNOTS((4,4),(3,3),(-1.54744435122098E-6,1.54744435122099E-5),
(-0.0151698983702731,1.),.UNSPECIFIED.)
GEOMETRIC_REPRESENTATION_ITEM()
RATIONAL_B_SPLINE_SURFACE(((1.02018382474057,0.334740937351171,1.),(1.00401234489044,
0.86775307281218,1.),(1.00033622856799,0.988917903080774,1.),(1.,1.,1.)))
REPRESENTATION_ITEM('')
SURFACE()
);
#2593=(
BOUNDED_SURFACE()
B_SPLINE_SURFACE(3,2,((#388192,#388193,#388194),(#388195,#388196,#388197),
(#388198,#388199,#388200),(#388201,#388202,#388203)),.UNSPECIFIED.,.F.,
 .F.,.F.)
B_SPLINE_SURFACE_WITH_KNOTS((4,4),(3,3),(0.00137194782501028,0.00149814269699235),
(0.,1.),.UNSPECIFIED.)
GEOMETRIC_REPRESENTATION_ITEM()
RATIONAL_B_SPLINE_SURFACE(((1.,0.815158509402318,1.),(1.,0.816179044148197,
1.),(1.,0.817226308119904,1.),(1.,0.818301939488812,1.)))
REPRESENTATION_ITEM('')
SURFACE()
);
#2594=(
BOUNDED_SURFACE()
B_SPLINE_SURFACE(3,2,((#388247,#388248,#388249),(#388250,#388251,#388252),
(#388253,#388254,#388255),(#388256,#388257,#388258)),.UNSPECIFIED.,.F.,
 .F.,.F.)
B_SPLINE_SURFACE_WITH_KNOTS((4,4),(3,3),(1.55009486301137E-5,4.92065510474437E-5),
(-8.13759516110161E-5,1.),.UNSPECIFIED.)
GEOMETRIC_REPRESENTATION_ITEM()
RATIONAL_B_SPLINE_SURFACE(((1.00002372912339,0.85420063959966,1.),(1.00001423585996,
0.91253030118053,1.),(1.00000710550472,0.956341495377427,1.),(1.0000123897591,
0.923873338137008,1.)))
REPRESENTATION_ITEM('')
SURFACE()
);
#2595=(
BOUNDED_SURFACE()
B_SPLINE_SURFACE(3,2,((#388262,#388263,#388264),(#388265,#388266,#388267),
(#388268,#388269,#388270),(#388271,#388272,#388273)),.UNSPECIFIED.,.F.,
 .F.,.F.)
B_SPLINE_SURFACE_WITH_KNOTS((4,4),(3,3),(-3.39934179457838E-6,3.73927597403563E-5),
(-0.00186004067450901,1.00069373317437),.UNSPECIFIED.)
GEOMETRIC_REPRESENTATION_ITEM()
RATIONAL_B_SPLINE_SURFACE(((1.00072100136067,0.8060519638753,1.0002685964269),
(1.00060048440164,0.83847080355858,1.00022369994495),(1.00053106448804,
0.857144632272337,1.00019783877219),(1.00054515072862,0.853355459539053,
1.00020308635436)))
REPRESENTATION_ITEM('')
SURFACE()
);
#2596=(
BOUNDED_SURFACE()
B_SPLINE_SURFACE(3,2,((#388275,#388276,#388277),(#388278,#388279,#388280),
(#388281,#388282,#388283),(#388284,#388285,#388286)),.UNSPECIFIED.,.F.,
 .F.,.F.)
B_SPLINE_SURFACE_WITH_KNOTS((4,4),(3,3),(4.33680868994202E-19,9.54361881492176E-5),
(0.,1.),.UNSPECIFIED.)
GEOMETRIC_REPRESENTATION_ITEM()
RATIONAL_B_SPLINE_SURFACE(((1.,0.816715621142048,1.),(1.,0.815907587407924,
1.),(1.,0.815115959345207,1.),(1.,0.8143398873492,1.)))
REPRESENTATION_ITEM('')
SURFACE()
);
#2597=(
BOUNDED_SURFACE()
B_SPLINE_SURFACE(3,2,((#388288,#388289,#388290),(#388291,#388292,#388293),
(#388294,#388295,#388296),(#388297,#388298,#388299)),.UNSPECIFIED.,.F.,
 .F.,.F.)
B_SPLINE_SURFACE_WITH_KNOTS((4,4),(3,3),(6.26804380968182E-20,4.68197758448211E-5),
(0.,1.),.UNSPECIFIED.)
GEOMETRIC_REPRESENTATION_ITEM()
RATIONAL_B_SPLINE_SURFACE(((1.,0.816715621142051,1.),(1.,0.953638980025213,
1.),(1.,0.954506925408048,1.),(1.,0.816715621142054,1.)))
REPRESENTATION_ITEM('')
SURFACE()
);
#2598=(
BOUNDED_SURFACE()
B_SPLINE_SURFACE(3,2,((#388301,#388302,#388303),(#388304,#388305,#388306),
(#388307,#388308,#388309),(#388310,#388311,#388312)),.UNSPECIFIED.,.F.,
 .F.,.F.)
B_SPLINE_SURFACE_WITH_KNOTS((4,4),(3,3),(-1.62630325872826E-19,9.54361881492177E-5),
(0.,1.),.UNSPECIFIED.)
GEOMETRIC_REPRESENTATION_ITEM()
RATIONAL_B_SPLINE_SURFACE(((1.,0.814339887349196,1.),(1.,0.815115959345208,
1.),(1.,0.815907587407945,1.),(1.,0.816715621142051,1.)))
REPRESENTATION_ITEM('')
SURFACE()
);
#2599=(
BOUNDED_SURFACE()
B_SPLINE_SURFACE(3,2,((#388314,#388315,#388316),(#388317,#388318,#388319),
(#388320,#388321,#388322),(#388323,#388324,#388325)),.UNSPECIFIED.,.F.,
 .F.,.F.)
B_SPLINE_SURFACE_WITH_KNOTS((4,4),(3,3),(-3.39528393502485E-6,3.73481232852728E-5),
(-0.00165018033331429,1.),.UNSPECIFIED.)
GEOMETRIC_REPRESENTATION_ITEM()
RATIONAL_B_SPLINE_SURFACE(((1.00048354385566,0.85348757166039,1.),(1.00047110510922,
0.857256476851484,1.),(1.00053193201108,0.838826096655838,1.),(1.00063970687727,
0.806170615310114,1.)))
REPRESENTATION_ITEM('')
SURFACE()
);
#2600=(
BOUNDED_SURFACE()
B_SPLINE_SURFACE(3,2,((#388329,#388330,#388331),(#388332,#388333,#388334),
(#388335,#388336,#388337),(#388338,#388339,#388340)),.UNSPECIFIED.,.F.,
 .F.,.F.)
B_SPLINE_SURFACE_WITH_KNOTS((4,4),(3,3),(2.02993869230509E-5,5.39756952687124E-5),
(-0.000116281070022815,1.),.UNSPECIFIED.)
GEOMETRIC_REPRESENTATION_ITEM()
RATIONAL_B_SPLINE_SURFACE(((1.00001770479731,0.923870681143008,1.),(1.0000101410406,
0.956394275543434,1.),(1.0000203730028,0.912397594905605,1.),(1.00003390859472,
0.854195550869727,1.)))
REPRESENTATION_ITEM('')
SURFACE()
);
#2601=(
BOUNDED_SURFACE()
B_SPLINE_SURFACE(3,2,((#388433,#388434,#388435),(#388436,#388437,#388438),
(#388439,#388440,#388441),(#388442,#388443,#388444)),.UNSPECIFIED.,.F.,
 .F.,.F.)
B_SPLINE_SURFACE_WITH_KNOTS((4,4),(3,3),(0.00135801595889393,0.00148409170619832),
(0.,1.),.UNSPECIFIED.)
GEOMETRIC_REPRESENTATION_ITEM()
RATIONAL_B_SPLINE_SURFACE(((1.,0.818301933966433,1.),(1.,0.817226613172354,
1.),(1.,0.816179643373948,1.),(1.,0.815159387863654,1.)))
REPRESENTATION_ITEM('')
SURFACE()
);
#2602=(
BOUNDED_SURFACE()
B_SPLINE_SURFACE(3,2,((#388483,#388484,#388485),(#388486,#388487,#388488),
(#388489,#388490,#388491),(#388492,#388493,#388494)),.UNSPECIFIED.,.F.,
 .F.,.F.)
B_SPLINE_SURFACE_WITH_KNOTS((4,4),(3,3),(5.90805480709874E-20,1.54744435122067E-5),
(0.,1.),.UNSPECIFIED.)
GEOMETRIC_REPRESENTATION_ITEM()
RATIONAL_B_SPLINE_SURFACE(((1.,0.478041569704953,1.),(1.,0.890533857552143,
1.),(1.,0.990075913815874,1.),(1.,1.,1.)))
REPRESENTATION_ITEM('')
SURFACE()
);
#2603=(
BOUNDED_SURFACE()
B_SPLINE_SURFACE(3,2,((#388496,#388497,#388498),(#388499,#388500,#388501),
(#388502,#388503,#388504),(#388505,#388506,#388507)),.UNSPECIFIED.,.F.,
 .F.,.F.)
B_SPLINE_SURFACE_WITH_KNOTS((4,4),(3,3),(0.00137194782501028,0.00149814269699235),
(0.,1.),.UNSPECIFIED.)
GEOMETRIC_REPRESENTATION_ITEM()
RATIONAL_B_SPLINE_SURFACE(((1.,0.81515850940233,1.),(1.,0.816179044148154,
1.),(1.,0.817226308119924,1.),(1.,0.818301939488809,1.)))
REPRESENTATION_ITEM('')
SURFACE()
);
#2604=(
BOUNDED_SURFACE()
B_SPLINE_SURFACE(3,2,((#388551,#388552,#388553),(#388554,#388555,#388556),
(#388557,#388558,#388559),(#388560,#388561,#388562)),.UNSPECIFIED.,.F.,
 .F.,.F.)
B_SPLINE_SURFACE_WITH_KNOTS((4,4),(3,3),(1.55009486301137E-5,4.92065510474431E-5),
(-8.13759513751905E-5,1.),.UNSPECIFIED.)
GEOMETRIC_REPRESENTATION_ITEM()
RATIONAL_B_SPLINE_SURFACE(((1.00002372912332,0.854200639599697,1.),(1.00001423585992,
0.912530301180547,1.),(1.0000071055047,0.956341495377435,1.),(1.00001238975907,
0.923873338137029,1.)))
REPRESENTATION_ITEM('')
SURFACE()
);
#2605=(
BOUNDED_SURFACE()
B_SPLINE_SURFACE(3,2,((#388566,#388567,#388568),(#388569,#388570,#388571),
(#388572,#388573,#388574),(#388575,#388576,#388577)),.UNSPECIFIED.,.F.,
 .F.,.F.)
B_SPLINE_SURFACE_WITH_KNOTS((4,4),(3,3),(-3.39934179457832E-6,3.73927597403566E-5),
(-0.00186004067413571,1.00069373317433),.UNSPECIFIED.)
GEOMETRIC_REPRESENTATION_ITEM()
RATIONAL_B_SPLINE_SURFACE(((1.00072100136053,0.806051963875365,1.00026859642689),
(1.00060048440152,0.838470803558657,1.00022369994494),(1.00053106448793,
0.857144632272392,1.00019783877218),(1.00054515072851,0.853355459539125,
1.00020308635435)))
REPRESENTATION_ITEM('')
SURFACE()
);
#2606=(
BOUNDED_SURFACE()
B_SPLINE_SURFACE(3,2,((#388579,#388580,#388581),(#388582,#388583,#388584),
(#388585,#388586,#388587),(#388588,#388589,#388590)),.UNSPECIFIED.,.F.,
 .F.,.F.)
B_SPLINE_SURFACE_WITH_KNOTS((4,4),(3,3),(1.0842021724855E-19,9.54361881492174E-5),
(0.,1.),.UNSPECIFIED.)
GEOMETRIC_REPRESENTATION_ITEM()
RATIONAL_B_SPLINE_SURFACE(((1.,0.816715621142049,1.),(1.,0.815907587407935,
1.),(1.,0.815115959345209,1.),(1.,0.814339887349194,1.)))
REPRESENTATION_ITEM('')
SURFACE()
);
#2607=(
BOUNDED_SURFACE()
B_SPLINE_SURFACE(3,2,((#388592,#388593,#388594),(#388595,#388596,#388597),
(#388598,#388599,#388600),(#388601,#388602,#388603)),.UNSPECIFIED.,.F.,
 .F.,.F.)
B_SPLINE_SURFACE_WITH_KNOTS((4,4),(3,3),(-3.06625926906057E-19,4.68197758448209E-5),
(0.,1.),.UNSPECIFIED.)
GEOMETRIC_REPRESENTATION_ITEM()
RATIONAL_B_SPLINE_SURFACE(((1.,0.816715621142046,1.),(1.,0.953638980025209,
1.),(1.,0.954506925408055,1.),(1.,0.81671562114205,1.)))
REPRESENTATION_ITEM('')
SURFACE()
);
#2608=(
BOUNDED_SURFACE()
B_SPLINE_SURFACE(3,2,((#388605,#388606,#388607),(#388608,#388609,#388610),
(#388611,#388612,#388613),(#388614,#388615,#388616)),.UNSPECIFIED.,.F.,
 .F.,.F.)
B_SPLINE_SURFACE_WITH_KNOTS((4,4),(3,3),(-5.42101086242752E-20,9.54361881492177E-5),
(0.,1.),.UNSPECIFIED.)
GEOMETRIC_REPRESENTATION_ITEM()
RATIONAL_B_SPLINE_SURFACE(((1.,0.814339887349194,1.),(1.,0.81511595934521,
1.),(1.,0.815907587407933,1.),(1.,0.816715621142052,1.)))
REPRESENTATION_ITEM('')
SURFACE()
);
#2609=(
BOUNDED_SURFACE()
B_SPLINE_SURFACE(3,2,((#388618,#388619,#388620),(#388621,#388622,#388623),
(#388624,#388625,#388626),(#388627,#388628,#388629)),.UNSPECIFIED.,.F.,
 .F.,.F.)
B_SPLINE_SURFACE_WITH_KNOTS((4,4),(3,3),(-3.3952839350248E-6,3.73481232852734E-5),
(-0.00165018033261607,1.),.UNSPECIFIED.)
GEOMETRIC_REPRESENTATION_ITEM()
RATIONAL_B_SPLINE_SURFACE(((1.00048354385546,0.853487571660518,1.),(1.00047110510902,
0.857256476851525,1.),(1.00053193201086,0.83882609665601,1.),(1.000639706877,
0.806170615310205,1.)))
REPRESENTATION_ITEM('')
SURFACE()
);
#2610=(
BOUNDED_SURFACE()
B_SPLINE_SURFACE(3,2,((#388633,#388634,#388635),(#388636,#388637,#388638),
(#388639,#388640,#388641),(#388642,#388643,#388644)),.UNSPECIFIED.,.F.,
 .F.,.F.)
B_SPLINE_SURFACE_WITH_KNOTS((4,4),(3,3),(2.02993869230509E-5,5.39756952687129E-5),
(-0.000116281069137242,1.),.UNSPECIFIED.)
GEOMETRIC_REPRESENTATION_ITEM()
RATIONAL_B_SPLINE_SURFACE(((1.00001770479718,0.923870681143067,1.),(1.00001014104052,
0.95639427554348,1.),(1.00002037300265,0.912397594905681,1.),(1.00003390859446,
0.854195550869853,1.)))
REPRESENTATION_ITEM('')
SURFACE()
);
#2611=(
BOUNDED_SURFACE()
B_SPLINE_SURFACE(3,2,((#388737,#388738,#388739),(#388740,#388741,#388742),
(#388743,#388744,#388745),(#388746,#388747,#388748)),.UNSPECIFIED.,.F.,
 .F.,.F.)
B_SPLINE_SURFACE_WITH_KNOTS((4,4),(3,3),(0.00135801595889393,0.00148409170619832),
(0.,1.),.UNSPECIFIED.)
GEOMETRIC_REPRESENTATION_ITEM()
RATIONAL_B_SPLINE_SURFACE(((1.,0.818301933966445,1.),(1.,0.817226613172342,
1.),(1.,0.816179643373966,1.),(1.,0.815159387863652,1.)))
REPRESENTATION_ITEM('')
SURFACE()
);
#2612=(
BOUNDED_SURFACE()
B_SPLINE_SURFACE(3,2,((#388787,#388788,#388789),(#388790,#388791,#388792),
(#388793,#388794,#388795),(#388796,#388797,#388798)),.UNSPECIFIED.,.F.,
 .F.,.F.)
B_SPLINE_SURFACE_WITH_KNOTS((4,4),(3,3),(-1.54744435122073E-6,1.54744435122074E-5),
(-0.0151698983599587,1.),.UNSPECIFIED.)
GEOMETRIC_REPRESENTATION_ITEM()
RATIONAL_B_SPLINE_SURFACE(((1.02018382472664,0.334740937357953,1.),(1.00401234488767,
0.867753072813686,1.),(1.00033622856776,0.98891790308083,1.),(1.,1.,1.)))
REPRESENTATION_ITEM('')
SURFACE()
);
#2613=(
BOUNDED_SURFACE()
B_SPLINE_SURFACE(3,2,((#388800,#388801,#388802),(#388803,#388804,#388805),
(#388806,#388807,#388808),(#388809,#388810,#388811)),.UNSPECIFIED.,.F.,
 .F.,.F.)
B_SPLINE_SURFACE_WITH_KNOTS((4,4),(3,3),(0.00137194782501028,0.00149814269699235),
(0.,1.),.UNSPECIFIED.)
GEOMETRIC_REPRESENTATION_ITEM()
RATIONAL_B_SPLINE_SURFACE(((1.,0.815158509402319,1.),(1.,0.81617904414817,
1.),(1.,0.817226308119905,1.),(1.,0.818301939488816,1.)))
REPRESENTATION_ITEM('')
SURFACE()
);
#2614=(
BOUNDED_SURFACE()
B_SPLINE_SURFACE(3,2,((#388855,#388856,#388857),(#388858,#388859,#388860),
(#388861,#388862,#388863),(#388864,#388865,#388866)),.UNSPECIFIED.,.F.,
 .F.,.F.)
B_SPLINE_SURFACE_WITH_KNOTS((4,4),(3,3),(1.55009486301137E-5,4.92065510474434E-5),
(-8.1375951256704E-5,1.),.UNSPECIFIED.)
GEOMETRIC_REPRESENTATION_ITEM()
RATIONAL_B_SPLINE_SURFACE(((1.00002372912329,0.854200639599719,1.),(1.0000142358599,
0.912530301180564,1.),(1.00000710550469,0.956341495377436,1.),(1.00001238975905,
0.923873338137045,1.)))
REPRESENTATION_ITEM('')
SURFACE()
);
#2615=(
BOUNDED_SURFACE()
B_SPLINE_SURFACE(3,2,((#388870,#388871,#388872),(#388873,#388874,#388875),
(#388876,#388877,#388878),(#388879,#388880,#388881)),.UNSPECIFIED.,.F.,
 .F.,.F.)
B_SPLINE_SURFACE_WITH_KNOTS((4,4),(3,3),(-3.39934179457825E-6,3.73927597403566E-5),
(-0.00186004067440102,1.00069373317436),.UNSPECIFIED.)
GEOMETRIC_REPRESENTATION_ITEM()
RATIONAL_B_SPLINE_SURFACE(((1.00072100136063,0.806051963875328,1.0002685964269),
(1.00060048440161,0.838470803558596,1.00022369994495),(1.00053106448801,
0.857144632272367,1.00019783877219),(1.00054515072859,0.853355459539074,
1.00020308635436)))
REPRESENTATION_ITEM('')
SURFACE()
);
#2616=(
BOUNDED_SURFACE()
B_SPLINE_SURFACE(3,2,((#388883,#388884,#388885),(#388886,#388887,#388888),
(#388889,#388890,#388891),(#388892,#388893,#388894)),.UNSPECIFIED.,.F.,
 .F.,.F.)
B_SPLINE_SURFACE_WITH_KNOTS((4,4),(3,3),(3.79470760369927E-19,9.54361881492177E-5),
(0.,1.),.UNSPECIFIED.)
GEOMETRIC_REPRESENTATION_ITEM()
RATIONAL_B_SPLINE_SURFACE(((1.,0.816715621142054,1.),(1.,0.815907587407937,
1.),(1.,0.81511595934522,1.),(1.,0.814339887349198,1.)))
REPRESENTATION_ITEM('')
SURFACE()
);
#2617=(
BOUNDED_SURFACE()
B_SPLINE_SURFACE(3,2,((#388896,#388897,#388898),(#388899,#388900,#388901),
(#388902,#388903,#388904),(#388905,#388906,#388907)),.UNSPECIFIED.,.F.,
 .F.,.F.)
B_SPLINE_SURFACE_WITH_KNOTS((4,4),(3,3),(1.05032085459533E-19,4.68197758448214E-5),
(0.,1.),.UNSPECIFIED.)
GEOMETRIC_REPRESENTATION_ITEM()
RATIONAL_B_SPLINE_SURFACE(((1.,0.816715621142049,1.),(1.,0.953638980025221,
1.),(1.,0.954506925408039,1.),(1.,0.816715621142054,1.)))
REPRESENTATION_ITEM('')
SURFACE()
);
#2618=(
BOUNDED_SURFACE()
B_SPLINE_SURFACE(3,2,((#388909,#388910,#388911),(#388912,#388913,#388914),
(#388915,#388916,#388917),(#388918,#388919,#388920)),.UNSPECIFIED.,.F.,
 .F.,.F.)
B_SPLINE_SURFACE_WITH_KNOTS((4,4),(3,3),(-5.42101086242752E-20,9.54361881492178E-5),
(0.,1.),.UNSPECIFIED.)
GEOMETRIC_REPRESENTATION_ITEM()
RATIONAL_B_SPLINE_SURFACE(((1.,0.814339887349192,1.),(1.,0.815115959345194,
1.),(1.,0.815907587407953,1.),(1.,0.816715621142049,1.)))
REPRESENTATION_ITEM('')
SURFACE()
);
#2619=(
BOUNDED_SURFACE()
B_SPLINE_SURFACE(3,2,((#388922,#388923,#388924),(#388925,#388926,#388927),
(#388928,#388929,#388930),(#388931,#388932,#388933)),.UNSPECIFIED.,.F.,
 .F.,.F.)
B_SPLINE_SURFACE_WITH_KNOTS((4,4),(3,3),(-3.39528393502487E-6,3.73481232852734E-5),
(-0.00165018033251935,1.),.UNSPECIFIED.)
GEOMETRIC_REPRESENTATION_ITEM()
RATIONAL_B_SPLINE_SURFACE(((1.00048354385543,0.85348757166049,1.),(1.00047110510899,
0.857256476851603,1.),(1.00053193201083,0.83882609665598,1.),(1.00063970687696,
0.806170615310246,1.)))
REPRESENTATION_ITEM('')
SURFACE()
);
#2620=(
BOUNDED_SURFACE()
B_SPLINE_SURFACE(3,2,((#388937,#388938,#388939),(#388940,#388941,#388942),
(#388943,#388944,#388945),(#388946,#388947,#388948)),.UNSPECIFIED.,.F.,
 .F.,.F.)
B_SPLINE_SURFACE_WITH_KNOTS((4,4),(3,3),(2.02993869230509E-5,5.39756952686905E-5),
(-0.000116281069650204,1.),.UNSPECIFIED.)
GEOMETRIC_REPRESENTATION_ITEM()
RATIONAL_B_SPLINE_SURFACE(((1.00001770479726,0.923870681143031,1.),(1.00001014104057,
0.956394275543426,1.),(1.00002037300274,0.912397594905714,1.),(1.00003390859461,
0.854195550869881,1.)))
REPRESENTATION_ITEM('')
SURFACE()
);
#2621=(
BOUNDED_SURFACE()
B_SPLINE_SURFACE(3,2,((#389041,#389042,#389043),(#389044,#389045,#389046),
(#389047,#389048,#389049),(#389050,#389051,#389052)),.UNSPECIFIED.,.F.,
 .F.,.F.)
B_SPLINE_SURFACE_WITH_KNOTS((4,4),(3,3),(0.00135801595889393,0.00148409170619832),
(0.,1.),.UNSPECIFIED.)
GEOMETRIC_REPRESENTATION_ITEM()
RATIONAL_B_SPLINE_SURFACE(((1.,0.818301933966442,1.),(1.,0.817226613172343,
1.),(1.,0.816179643373952,1.),(1.,0.815159387863653,1.)))
REPRESENTATION_ITEM('')
SURFACE()
);
#2622=(
BOUNDED_SURFACE()
B_SPLINE_SURFACE(3,2,((#389091,#389092,#389093),(#389094,#389095,#389096),
(#389097,#389098,#389099),(#389100,#389101,#389102)),.UNSPECIFIED.,.F.,
 .F.,.F.)
B_SPLINE_SURFACE_WITH_KNOTS((4,4),(3,3),(-1.54744435122082E-6,1.5474443512208E-5),
(-0.0151698983619477,1.),.UNSPECIFIED.)
GEOMETRIC_REPRESENTATION_ITEM()
RATIONAL_B_SPLINE_SURFACE(((1.02018382472933,0.334740937356649,1.),(1.0040123448882,
0.867753072813339,1.),(1.0003362285678,0.988917903080829,1.),(1.,1.,1.)))
REPRESENTATION_ITEM('')
SURFACE()
);
#2623=(
BOUNDED_SURFACE()
B_SPLINE_SURFACE(3,2,((#389104,#389105,#389106),(#389107,#389108,#389109),
(#389110,#389111,#389112),(#389113,#389114,#389115)),.UNSPECIFIED.,.F.,
 .F.,.F.)
B_SPLINE_SURFACE_WITH_KNOTS((4,4),(3,3),(0.00137194782501028,0.00149814269699235),
(0.,1.),.UNSPECIFIED.)
GEOMETRIC_REPRESENTATION_ITEM()
RATIONAL_B_SPLINE_SURFACE(((1.,0.815158509402328,1.),(1.,0.816179044148159,
1.),(1.,0.81722630811993,1.),(1.,0.818301939488807,1.)))
REPRESENTATION_ITEM('')
SURFACE()
);
#2624=(
BOUNDED_SURFACE()
B_SPLINE_SURFACE(3,2,((#389159,#389160,#389161),(#389162,#389163,#389164),
(#389165,#389166,#389167),(#389168,#389169,#389170)),.UNSPECIFIED.,.F.,
 .F.,.F.)
B_SPLINE_SURFACE_WITH_KNOTS((4,4),(3,3),(1.55009486301137E-5,4.9206551047443E-5),
(-8.13759515487E-5,1.),.UNSPECIFIED.)
GEOMETRIC_REPRESENTATION_ITEM()
RATIONAL_B_SPLINE_SURFACE(((1.00002372912338,0.854200639599678,1.),(1.00001423585995,
0.912530301180521,1.),(1.00000710550471,0.956341495377438,1.),(1.00001238975909,
0.923873338137016,1.)))
REPRESENTATION_ITEM('')
SURFACE()
);
#2625=(
BOUNDED_SURFACE()
B_SPLINE_SURFACE(3,2,((#389174,#389175,#389176),(#389177,#389178,#389179),
(#389180,#389181,#389182),(#389183,#389184,#389185)),.UNSPECIFIED.,.F.,
 .F.,.F.)
B_SPLINE_SURFACE_WITH_KNOTS((4,4),(3,3),(-3.39934179457848E-6,3.73927597403565E-5),
(-0.00186004067432748,1.00069373317439),.UNSPECIFIED.)
GEOMETRIC_REPRESENTATION_ITEM()
RATIONAL_B_SPLINE_SURFACE(((1.0007210013606,0.806051963875316,1.00026859642691),
(1.00060048440158,0.838470803558609,1.00022369994495),(1.00053106448799,
0.857144632272371,1.00019783877219),(1.00054515072856,0.85335545953907,
1.00020308635437)))
REPRESENTATION_ITEM('')
SURFACE()
);
#2626=(
BOUNDED_SURFACE()
B_SPLINE_SURFACE(3,2,((#389187,#389188,#389189),(#389190,#389191,#389192),
(#389193,#389194,#389195),(#389196,#389197,#389198)),.UNSPECIFIED.,.F.,
 .F.,.F.)
B_SPLINE_SURFACE_WITH_KNOTS((4,4),(3,3),(-1.62630325872826E-19,9.5436188149217E-5),
(0.,1.),.UNSPECIFIED.)
GEOMETRIC_REPRESENTATION_ITEM()
RATIONAL_B_SPLINE_SURFACE(((1.,0.816715621142048,1.),(1.,0.815907587407941,
1.),(1.,0.815115959345207,1.),(1.,0.814339887349185,1.)))
REPRESENTATION_ITEM('')
SURFACE()
);
#2627=(
BOUNDED_SURFACE()
B_SPLINE_SURFACE(3,2,((#389200,#389201,#389202),(#389203,#389204,#389205),
(#389206,#389207,#389208),(#389209,#389210,#389211)),.UNSPECIFIED.,.F.,
 .F.,.F.)
B_SPLINE_SURFACE_WITH_KNOTS((4,4),(3,3),(-1.60936259978317E-19,4.68197758448207E-5),
(0.,1.),.UNSPECIFIED.)
GEOMETRIC_REPRESENTATION_ITEM()
RATIONAL_B_SPLINE_SURFACE(((1.,0.816715621142048,1.),(1.,0.953638980025212,
1.),(1.,0.954506925408048,1.),(1.,0.816715621142053,1.)))
REPRESENTATION_ITEM('')
SURFACE()
);
#2628=(
BOUNDED_SURFACE()
B_SPLINE_SURFACE(3,2,((#389213,#389214,#389215),(#389216,#389217,#389218),
(#389219,#389220,#389221),(#389222,#389223,#389224)),.UNSPECIFIED.,.F.,
 .F.,.F.)
B_SPLINE_SURFACE_WITH_KNOTS((4,4),(3,3),(5.42101086242752E-20,9.54361881492175E-5),
(0.,1.),.UNSPECIFIED.)
GEOMETRIC_REPRESENTATION_ITEM()
RATIONAL_B_SPLINE_SURFACE(((1.,0.814339887349189,1.),(1.,0.815115959345207,
1.),(1.,0.815907587407939,1.),(1.,0.816715621142047,1.)))
REPRESENTATION_ITEM('')
SURFACE()
);
#2629=(
BOUNDED_SURFACE()
B_SPLINE_SURFACE(3,2,((#389226,#389227,#389228),(#389229,#389230,#389231),
(#389232,#389233,#389234),(#389235,#389236,#389237)),.UNSPECIFIED.,.F.,
 .F.,.F.)
B_SPLINE_SURFACE_WITH_KNOTS((4,4),(3,3),(-3.39528393502488E-6,3.73481232852735E-5),
(-0.00165018033272199,1.),.UNSPECIFIED.)
GEOMETRIC_REPRESENTATION_ITEM()
RATIONAL_B_SPLINE_SURFACE(((1.00048354385549,0.853487571660471,1.),(1.00047110510905,
0.85725647685156,1.),(1.00053193201089,0.838826096655951,1.),(1.00063970687704,
0.806170615310205,1.)))
REPRESENTATION_ITEM('')
SURFACE()
);
#2630=(
BOUNDED_SURFACE()
B_SPLINE_SURFACE(3,2,((#389241,#389242,#389243),(#389244,#389245,#389246),
(#389247,#389248,#389249),(#389250,#389251,#389252)),.UNSPECIFIED.,.F.,
 .F.,.F.)
B_SPLINE_SURFACE_WITH_KNOTS((4,4),(3,3),(2.0299386923051E-5,5.39756952686902E-5),
(-0.00011628106966309,1.),.UNSPECIFIED.)
GEOMETRIC_REPRESENTATION_ITEM()
RATIONAL_B_SPLINE_SURFACE(((1.00001770479726,0.92387068114303,1.),(1.00001014104057,
0.956394275543435,1.),(1.00002037300274,0.912397594905691,1.),(1.00003390859461,
0.8541955508699,1.)))
REPRESENTATION_ITEM('')
SURFACE()
);
#2631=(
BOUNDED_SURFACE()
B_SPLINE_SURFACE(3,2,((#389345,#389346,#389347),(#389348,#389349,#389350),
(#389351,#389352,#389353),(#389354,#389355,#389356)),.UNSPECIFIED.,.F.,
 .F.,.F.)
B_SPLINE_SURFACE_WITH_KNOTS((4,4),(3,3),(0.00135801595889393,0.00148409170619832),
(0.,1.),.UNSPECIFIED.)
GEOMETRIC_REPRESENTATION_ITEM()
RATIONAL_B_SPLINE_SURFACE(((1.,0.818301933966445,1.),(1.,0.817226613172347,
1.),(1.,0.816179643373956,1.),(1.,0.815159387863658,1.)))
REPRESENTATION_ITEM('')
SURFACE()
);
#2632=(
BOUNDED_SURFACE()
B_SPLINE_SURFACE(3,2,((#389395,#389396,#389397),(#389398,#389399,#389400),
(#389401,#389402,#389403),(#389404,#389405,#389406)),.UNSPECIFIED.,.F.,
 .F.,.F.)
B_SPLINE_SURFACE_WITH_KNOTS((4,4),(3,3),(-1.54744435122081E-6,1.54744435122075E-5),
(-0.0151698983637362,1.),.UNSPECIFIED.)
GEOMETRIC_REPRESENTATION_ITEM()
RATIONAL_B_SPLINE_SURFACE(((1.02018382473174,0.334740937355544,1.),(1.00401234488868,
0.86775307281305,1.),(1.00033622856784,0.988917903080849,1.),(1.,1.,1.)))
REPRESENTATION_ITEM('')
SURFACE()
);
#2633=(
BOUNDED_SURFACE()
B_SPLINE_SURFACE(3,2,((#389408,#389409,#389410),(#389411,#389412,#389413),
(#389414,#389415,#389416),(#389417,#389418,#389419)),.UNSPECIFIED.,.F.,
 .F.,.F.)
B_SPLINE_SURFACE_WITH_KNOTS((4,4),(3,3),(0.00137194782501028,0.00149814269699235),
(0.,1.),.UNSPECIFIED.)
GEOMETRIC_REPRESENTATION_ITEM()
RATIONAL_B_SPLINE_SURFACE(((1.,0.815158509402313,1.),(1.,0.816179044148172,
1.),(1.,0.817226308119923,1.),(1.,0.818301939488807,1.)))
REPRESENTATION_ITEM('')
SURFACE()
);
#2634=(
BOUNDED_SURFACE()
B_SPLINE_SURFACE(3,2,((#389463,#389464,#389465),(#389466,#389467,#389468),
(#389469,#389470,#389471),(#389472,#389473,#389474)),.UNSPECIFIED.,.F.,
 .F.,.F.)
B_SPLINE_SURFACE_WITH_KNOTS((4,4),(3,3),(1.55009486301137E-5,4.9206551047443E-5),
(-8.13759514700875E-5,1.),.UNSPECIFIED.)
GEOMETRIC_REPRESENTATION_ITEM()
RATIONAL_B_SPLINE_SURFACE(((1.00002372912335,0.854200639599689,1.),(1.00001423585993,
0.912530301180527,1.),(1.00000710550471,0.956341495377435,1.),(1.00001238975908,
0.923873338137022,1.)))
REPRESENTATION_ITEM('')
SURFACE()
);
#2635=(
BOUNDED_SURFACE()
B_SPLINE_SURFACE(3,2,((#389478,#389479,#389480),(#389481,#389482,#389483),
(#389484,#389485,#389486),(#389487,#389488,#389489)),.UNSPECIFIED.,.F.,
 .F.,.F.)
B_SPLINE_SURFACE_WITH_KNOTS((4,4),(3,3),(-3.39934179457819E-6,3.73927597403566E-5),
(-0.00186004067485636,1.0006937331747),.UNSPECIFIED.)
GEOMETRIC_REPRESENTATION_ITEM()
RATIONAL_B_SPLINE_SURFACE(((1.00072100136081,0.806051963875156,1.00026859642703),
(1.00060048440176,0.838470803558486,1.00022369994506),(1.00053106448814,
0.857144632272242,1.00019783877228),(1.00054515072872,0.853355459538962,
1.00020308635446)))
REPRESENTATION_ITEM('')
SURFACE()
);
#2636=(
BOUNDED_SURFACE()
B_SPLINE_SURFACE(3,2,((#389491,#389492,#389493),(#389494,#389495,#389496),
(#389497,#389498,#389499),(#389500,#389501,#389502)),.UNSPECIFIED.,.F.,
 .F.,.F.)
B_SPLINE_SURFACE_WITH_KNOTS((4,4),(3,3),(-5.42101086242752E-20,9.54361881492174E-5),
(0.,1.),.UNSPECIFIED.)
GEOMETRIC_REPRESENTATION_ITEM()
RATIONAL_B_SPLINE_SURFACE(((1.,0.816715621142055,1.),(1.,0.815907587407937,
1.),(1.,0.815115959345214,1.),(1.,0.814339887349196,1.)))
REPRESENTATION_ITEM('')
SURFACE()
);
#2637=(
BOUNDED_SURFACE()
B_SPLINE_SURFACE(3,2,((#389504,#389505,#389506),(#389507,#389508,#389509),
(#389510,#389511,#389512),(#389513,#389514,#389515)),.UNSPECIFIED.,.F.,
 .F.,.F.)
B_SPLINE_SURFACE_WITH_KNOTS((4,4),(3,3),(7.96210970419042E-20,4.68197758448209E-5),
(0.,1.),.UNSPECIFIED.)
GEOMETRIC_REPRESENTATION_ITEM()
RATIONAL_B_SPLINE_SURFACE(((1.,0.816715621142049,1.),(1.,0.953638980025211,
1.),(1.,0.954506925408045,1.),(1.,0.816715621142055,1.)))
REPRESENTATION_ITEM('')
SURFACE()
);
#2638=(
BOUNDED_SURFACE()
B_SPLINE_SURFACE(3,2,((#389517,#389518,#389519),(#389520,#389521,#389522),
(#389523,#389524,#389525),(#389526,#389527,#389528)),.UNSPECIFIED.,.F.,
 .F.,.F.)
B_SPLINE_SURFACE_WITH_KNOTS((4,4),(3,3),(1.62630325872826E-19,9.54361881492178E-5),
(0.,1.),.UNSPECIFIED.)
GEOMETRIC_REPRESENTATION_ITEM()
RATIONAL_B_SPLINE_SURFACE(((1.,0.814339887349188,1.),(1.,0.815115959345215,
1.),(1.,0.815907587407936,1.),(1.,0.816715621142051,1.)))
REPRESENTATION_ITEM('')
SURFACE()
);
#2639=(
BOUNDED_SURFACE()
B_SPLINE_SURFACE(3,2,((#389530,#389531,#389532),(#389533,#389534,#389535),
(#389536,#389537,#389538),(#389539,#389540,#389541)),.UNSPECIFIED.,.F.,
 .F.,.F.)
B_SPLINE_SURFACE_WITH_KNOTS((4,4),(3,3),(-3.3952839350249E-6,3.73481232852728E-5),
(-0.00165018033345588,1.),.UNSPECIFIED.)
GEOMETRIC_REPRESENTATION_ITEM()
RATIONAL_B_SPLINE_SURFACE(((1.00048354385571,0.853487571660368,1.),(1.00047110510926,
0.857256476851443,1.),(1.00053193201113,0.838826096655833,1.),(1.00063970687732,
0.806170615310063,1.)))
REPRESENTATION_ITEM('')
SURFACE()
);
#2640=(
BOUNDED_SURFACE()
B_SPLINE_SURFACE(3,2,((#389545,#389546,#389547),(#389548,#389549,#389550),
(#389551,#389552,#389553),(#389554,#389555,#389556)),.UNSPECIFIED.,.F.,
 .F.,.F.)
B_SPLINE_SURFACE_WITH_KNOTS((4,4),(3,3),(2.02993869230511E-5,5.39756952686902E-5),
(-0.000116281069626685,1.),.UNSPECIFIED.)
GEOMETRIC_REPRESENTATION_ITEM()
RATIONAL_B_SPLINE_SURFACE(((1.00001770479725,0.923870681143031,1.),(1.00001014104056,
0.956394275543432,1.),(1.00002037300273,0.9123975949057,1.),(1.0000339085946,
0.854195550869898,1.)))
REPRESENTATION_ITEM('')
SURFACE()
);
#2641=(
BOUNDED_SURFACE()
B_SPLINE_SURFACE(3,2,((#389649,#389650,#389651),(#389652,#389653,#389654),
(#389655,#389656,#389657),(#389658,#389659,#389660)),.UNSPECIFIED.,.F.,
 .F.,.F.)
B_SPLINE_SURFACE_WITH_KNOTS((4,4),(3,3),(0.00135801595889393,0.00148409170619832),
(0.,1.),.UNSPECIFIED.)
GEOMETRIC_REPRESENTATION_ITEM()
RATIONAL_B_SPLINE_SURFACE(((1.,0.818301933966445,1.),(1.,0.817226613172353,
1.),(1.,0.81617964337395,1.),(1.,0.815159387863655,1.)))
REPRESENTATION_ITEM('')
SURFACE()
);
#2642=(
BOUNDED_SURFACE()
B_SPLINE_SURFACE(3,2,((#389699,#389700,#389701),(#389702,#389703,#389704),
(#389705,#389706,#389707),(#389708,#389709,#389710)),.UNSPECIFIED.,.F.,
 .F.,.F.)
B_SPLINE_SURFACE_WITH_KNOTS((4,4),(3,3),(-1.54744435122017E-6,1.54744435122086E-5),
(0.,1.01516989835332),.UNSPECIFIED.)
GEOMETRIC_REPRESENTATION_ITEM()
RATIONAL_B_SPLINE_SURFACE(((1.,0.33474093736242,1.02018382471767),(1.,0.867753072814264,
1.00401234488589),(1.,0.988917903081015,1.00033622856761),(1.,1.,1.)))
REPRESENTATION_ITEM('')
SURFACE()
);
#2643=(
BOUNDED_SURFACE()
B_SPLINE_SURFACE(3,2,((#389712,#389713,#389714),(#389715,#389716,#389717),
(#389718,#389719,#389720),(#389721,#389722,#389723)),.UNSPECIFIED.,.F.,
 .F.,.F.)
B_SPLINE_SURFACE_WITH_KNOTS((4,4),(3,3),(0.00137194782501028,0.00149814269699235),
(0.,1.),.UNSPECIFIED.)
GEOMETRIC_REPRESENTATION_ITEM()
RATIONAL_B_SPLINE_SURFACE(((1.,0.815158509402318,1.),(1.,0.816179044148163,
1.),(1.,0.817226308119936,1.),(1.,0.818301939488807,1.)))
REPRESENTATION_ITEM('')
SURFACE()
);
#2644=(
BOUNDED_SURFACE()
B_SPLINE_SURFACE(3,2,((#389767,#389768,#389769),(#389770,#389771,#389772),
(#389773,#389774,#389775),(#389776,#389777,#389778)),.UNSPECIFIED.,.F.,
 .F.,.F.)
B_SPLINE_SURFACE_WITH_KNOTS((4,4),(3,3),(1.55009486301137E-5,4.92065510474438E-5),
(-8.13759517499485E-5,1.),.UNSPECIFIED.)
GEOMETRIC_REPRESENTATION_ITEM()
RATIONAL_B_SPLINE_SURFACE(((1.00002372912343,0.854200639599646,1.),(1.00001423585998,
0.912530301180521,1.),(1.00000710550473,0.956341495377413,1.),(1.00001238975913,
0.923873338137004,1.)))
REPRESENTATION_ITEM('')
SURFACE()
);
#2645=(
BOUNDED_SURFACE()
B_SPLINE_SURFACE(3,2,((#389782,#389783,#389784),(#389785,#389786,#389787),
(#389788,#389789,#389790),(#389791,#389792,#389793)),.UNSPECIFIED.,.F.,
 .F.,.F.)
B_SPLINE_SURFACE_WITH_KNOTS((4,4),(3,3),(-3.39934179457862E-6,3.73927597403562E-5),
(-0.00186004067474084,1.00069373317454),.UNSPECIFIED.)
GEOMETRIC_REPRESENTATION_ITEM()
RATIONAL_B_SPLINE_SURFACE(((1.00072100136076,0.806051963875226,1.00026859642696),
(1.00060048440172,0.838470803558517,1.000223699945),(1.00053106448811,0.85714463227229,
1.00019783877223),(1.00054515072869,0.853355459538998,1.00020308635441)))
REPRESENTATION_ITEM('')
SURFACE()
);
#2646=(
BOUNDED_SURFACE()
B_SPLINE_SURFACE(3,2,((#389795,#389796,#389797),(#389798,#389799,#389800),
(#389801,#389802,#389803),(#389804,#389805,#389806)),.UNSPECIFIED.,.F.,
 .F.,.F.)
B_SPLINE_SURFACE_WITH_KNOTS((4,4),(3,3),(-1.0842021724855E-19,9.54361881492172E-5),
(0.,1.),.UNSPECIFIED.)
GEOMETRIC_REPRESENTATION_ITEM()
RATIONAL_B_SPLINE_SURFACE(((1.,0.816715621142051,1.),(1.,0.815907587407944,
1.),(1.,0.815115959345209,1.),(1.,0.814339887349197,1.)))
REPRESENTATION_ITEM('')
SURFACE()
);
#2647=(
BOUNDED_SURFACE()
B_SPLINE_SURFACE(3,2,((#389808,#389809,#389810),(#389811,#389812,#389813),
(#389814,#389815,#389816),(#389817,#389818,#389819)),.UNSPECIFIED.,.F.,
 .F.,.F.)
B_SPLINE_SURFACE_WITH_KNOTS((4,4),(3,3),(-1.96511643762998E-19,4.68197758448206E-5),
(0.,1.),.UNSPECIFIED.)
GEOMETRIC_REPRESENTATION_ITEM()
RATIONAL_B_SPLINE_SURFACE(((1.,0.816715621142045,1.),(1.,0.953638980025211,
1.),(1.,0.954506925408055,1.),(1.,0.816715621142051,1.)))
REPRESENTATION_ITEM('')
SURFACE()
);
#2648=(
BOUNDED_SURFACE()
B_SPLINE_SURFACE(3,2,((#389821,#389822,#389823),(#389824,#389825,#389826),
(#389827,#389828,#389829),(#389830,#389831,#389832)),.UNSPECIFIED.,.F.,
 .F.,.F.)
B_SPLINE_SURFACE_WITH_KNOTS((4,4),(3,3),(0.,9.54361881492177E-5),(0.,1.),
 .UNSPECIFIED.)
GEOMETRIC_REPRESENTATION_ITEM()
RATIONAL_B_SPLINE_SURFACE(((1.,0.814339887349196,1.),(1.,0.815115959345193,
1.),(1.,0.815907587407952,1.),(1.,0.816715621142047,1.)))
REPRESENTATION_ITEM('')
SURFACE()
);
#2649=(
BOUNDED_SURFACE()
B_SPLINE_SURFACE(3,2,((#389834,#389835,#389836),(#389837,#389838,#389839),
(#389840,#389841,#389842),(#389843,#389844,#389845)),.UNSPECIFIED.,.F.,
 .F.,.F.)
B_SPLINE_SURFACE_WITH_KNOTS((4,4),(3,3),(-3.39528393502488E-6,3.73481232852735E-5),
(-0.00165018033331416,1.),.UNSPECIFIED.)
GEOMETRIC_REPRESENTATION_ITEM()
RATIONAL_B_SPLINE_SURFACE(((1.00048354385566,0.853487571660399,1.),(1.00047110510922,
0.857256476851447,1.),(1.00053193201108,0.838826096655879,1.),(1.00063970687727,
0.806170615310081,1.)))
REPRESENTATION_ITEM('')
SURFACE()
);
#2650=(
BOUNDED_SURFACE()
B_SPLINE_SURFACE(3,2,((#389849,#389850,#389851),(#389852,#389853,#389854),
(#389855,#389856,#389857),(#389858,#389859,#389860)),.UNSPECIFIED.,.F.,
 .F.,.F.)
B_SPLINE_SURFACE_WITH_KNOTS((4,4),(3,3),(2.02993869230507E-5,5.39756952686892E-5),
(-0.000116281069916757,1.),.UNSPECIFIED.)
GEOMETRIC_REPRESENTATION_ITEM()
RATIONAL_B_SPLINE_SURFACE(((1.0000177047973,0.92387068114301,1.),(1.00001014104059,
0.956394275543412,1.),(1.00002037300278,0.912397594905679,1.),(1.00003390859469,
0.854195550869856,1.)))
REPRESENTATION_ITEM('')
SURFACE()
);
#2651=(
BOUNDED_SURFACE()
B_SPLINE_SURFACE(3,2,((#389953,#389954,#389955),(#389956,#389957,#389958),
(#389959,#389960,#389961),(#389962,#389963,#389964)),.UNSPECIFIED.,.F.,
 .F.,.F.)
B_SPLINE_SURFACE_WITH_KNOTS((4,4),(3,3),(0.00135801595889393,0.00148409170619832),
(0.,1.),.UNSPECIFIED.)
GEOMETRIC_REPRESENTATION_ITEM()
RATIONAL_B_SPLINE_SURFACE(((1.,0.818301933966448,1.),(1.,0.817226613172342,
1.),(1.,0.81617964337396,1.),(1.,0.81515938786366,1.)))
REPRESENTATION_ITEM('')
SURFACE()
);
#2652=(
BOUNDED_SURFACE()
B_SPLINE_SURFACE(3,2,((#390003,#390004,#390005),(#390006,#390007,#390008),
(#390009,#390010,#390011),(#390012,#390013,#390014)),.UNSPECIFIED.,.F.,
 .F.,.F.)
B_SPLINE_SURFACE_WITH_KNOTS((4,4),(3,3),(-1.54744435122075E-6,1.5474443512208E-5),
(-0.0151698983620152,1.),.UNSPECIFIED.)
GEOMETRIC_REPRESENTATION_ITEM()
RATIONAL_B_SPLINE_SURFACE(((1.02018382472942,0.334740937356621,1.),(1.00401234488822,
0.867753072813288,1.),(1.0003362285678,0.988917903080855,1.),(1.,1.,1.)))
REPRESENTATION_ITEM('')
SURFACE()
);
#2653=(
BOUNDED_SURFACE()
B_SPLINE_SURFACE(3,2,((#390016,#390017,#390018),(#390019,#390020,#390021),
(#390022,#390023,#390024),(#390025,#390026,#390027)),.UNSPECIFIED.,.F.,
 .F.,.F.)
B_SPLINE_SURFACE_WITH_KNOTS((4,4),(3,3),(0.00137194782501028,0.00149814269699235),
(0.,1.),.UNSPECIFIED.)
GEOMETRIC_REPRESENTATION_ITEM()
RATIONAL_B_SPLINE_SURFACE(((1.,0.815158509402316,1.),(1.,0.81617904414816,
1.),(1.,0.817226308119934,1.),(1.,0.818301939488799,1.)))
REPRESENTATION_ITEM('')
SURFACE()
);
#2654=(
BOUNDED_SURFACE()
B_SPLINE_SURFACE(3,2,((#390071,#390072,#390073),(#390074,#390075,#390076),
(#390077,#390078,#390079),(#390080,#390081,#390082)),.UNSPECIFIED.,.F.,
 .F.,.F.)
B_SPLINE_SURFACE_WITH_KNOTS((4,4),(3,3),(1.55009486301137E-5,4.92065510474438E-5),
(-8.13759515447854E-5,1.),.UNSPECIFIED.)
GEOMETRIC_REPRESENTATION_ITEM()
RATIONAL_B_SPLINE_SURFACE(((1.00002372912337,0.854200639599677,1.),(1.00001423585995,
0.912530301180528,1.),(1.00000710550471,0.956341495377429,1.),(1.00001238975909,
0.923873338137019,1.)))
REPRESENTATION_ITEM('')
SURFACE()
);
#2655=(
BOUNDED_SURFACE()
B_SPLINE_SURFACE(3,2,((#390086,#390087,#390088),(#390089,#390090,#390091),
(#390092,#390093,#390094),(#390095,#390096,#390097)),.UNSPECIFIED.,.F.,
 .F.,.F.)
B_SPLINE_SURFACE_WITH_KNOTS((4,4),(3,3),(-3.39934179457828E-6,3.73927597403566E-5),
(-0.00186004067387787,1.00069373317419),.UNSPECIFIED.)
GEOMETRIC_REPRESENTATION_ITEM()
RATIONAL_B_SPLINE_SURFACE(((1.00072100136043,0.806051963875447,1.00026859642683),
(1.00060048440144,0.838470803558726,1.00022369994489),(1.00053106448786,
0.857144632272452,1.00019783877214),(1.00054515072843,0.853355459539179,
1.00020308635431)))
REPRESENTATION_ITEM('')
SURFACE()
);
#2656=(
BOUNDED_SURFACE()
B_SPLINE_SURFACE(3,2,((#390099,#390100,#390101),(#390102,#390103,#390104),
(#390105,#390106,#390107),(#390108,#390109,#390110)),.UNSPECIFIED.,.F.,
 .F.,.F.)
B_SPLINE_SURFACE_WITH_KNOTS((4,4),(3,3),(-1.0842021724855E-19,9.54361881492174E-5),
(0.,1.),.UNSPECIFIED.)
GEOMETRIC_REPRESENTATION_ITEM()
RATIONAL_B_SPLINE_SURFACE(((1.,0.816715621142051,1.),(1.,0.815907587407947,
1.),(1.,0.815115959345208,1.),(1.,0.814339887349195,1.)))
REPRESENTATION_ITEM('')
SURFACE()
);
#2657=(
BOUNDED_SURFACE()
B_SPLINE_SURFACE(3,2,((#390112,#390113,#390114),(#390115,#390116,#390117),
(#390118,#390119,#390120),(#390121,#390122,#390123)),.UNSPECIFIED.,.F.,
 .F.,.F.)
B_SPLINE_SURFACE_WITH_KNOTS((4,4),(3,3),(-8.470329472543E-21,4.68197758448207E-5),
(0.,1.),.UNSPECIFIED.)
GEOMETRIC_REPRESENTATION_ITEM()
RATIONAL_B_SPLINE_SURFACE(((1.,0.816715621142051,1.),(1.,0.953638980025211,
1.),(1.,0.954506925408046,1.),(1.,0.816715621142051,1.)))
REPRESENTATION_ITEM('')
SURFACE()
);
#2658=(
BOUNDED_SURFACE()
B_SPLINE_SURFACE(3,2,((#390125,#390126,#390127),(#390128,#390129,#390130),
(#390131,#390132,#390133),(#390134,#390135,#390136)),.UNSPECIFIED.,.F.,
 .F.,.F.)
B_SPLINE_SURFACE_WITH_KNOTS((4,4),(3,3),(-5.42101086242752E-20,9.54361881492177E-5),
(0.,1.),.UNSPECIFIED.)
GEOMETRIC_REPRESENTATION_ITEM()
RATIONAL_B_SPLINE_SURFACE(((1.,0.814339887349193,1.),(1.,0.815115959345206,
1.),(1.,0.815907587407936,1.),(1.,0.816715621142051,1.)))
REPRESENTATION_ITEM('')
SURFACE()
);
#2659=(
BOUNDED_SURFACE()
B_SPLINE_SURFACE(3,2,((#390138,#390139,#390140),(#390141,#390142,#390143),
(#390144,#390145,#390146),(#390147,#390148,#390149)),.UNSPECIFIED.,.F.,
 .F.,.F.)
B_SPLINE_SURFACE_WITH_KNOTS((4,4),(3,3),(-3.39528393502381E-6,3.73481232852733E-5),
(-0.00165018033288198,1.),.UNSPECIFIED.)
GEOMETRIC_REPRESENTATION_ITEM()
RATIONAL_B_SPLINE_SURFACE(((1.00048354385554,0.853487571660452,1.),(1.00047110510909,
0.857256476851522,1.),(1.00053193201094,0.838826096655925,1.),(1.0006397068771,
0.806170615310169,1.)))
REPRESENTATION_ITEM('')
SURFACE()
);
#2660=(
BOUNDED_SURFACE()
B_SPLINE_SURFACE(3,2,((#390153,#390154,#390155),(#390156,#390157,#390158),
(#390159,#390160,#390161),(#390162,#390163,#390164)),.UNSPECIFIED.,.F.,
 .F.,.F.)
B_SPLINE_SURFACE_WITH_KNOTS((4,4),(3,3),(2.02993869230506E-5,5.39756952686901E-5),
(-0.000116281069653534,1.),.UNSPECIFIED.)
GEOMETRIC_REPRESENTATION_ITEM()
RATIONAL_B_SPLINE_SURFACE(((1.00001770479726,0.92387068114303,1.),(1.00001014104057,
0.956394275543427,1.),(1.00002037300274,0.912397594905703,1.),(1.00003390859461,
0.854195550869894,1.)))
REPRESENTATION_ITEM('')
SURFACE()
);
#2661=(
BOUNDED_SURFACE()
B_SPLINE_SURFACE(3,2,((#390257,#390258,#390259),(#390260,#390261,#390262),
(#390263,#390264,#390265),(#390266,#390267,#390268)),.UNSPECIFIED.,.F.,
 .F.,.F.)
B_SPLINE_SURFACE_WITH_KNOTS((4,4),(3,3),(0.00135801595889393,0.00148409170619832),
(0.,1.),.UNSPECIFIED.)
GEOMETRIC_REPRESENTATION_ITEM()
RATIONAL_B_SPLINE_SURFACE(((1.,0.818301933966444,1.),(1.,0.817226613172336,
1.),(1.,0.816179643373953,1.),(1.,0.815159387863656,1.)))
REPRESENTATION_ITEM('')
SURFACE()
);
#2662=(
BOUNDED_SURFACE()
B_SPLINE_SURFACE(3,2,((#390307,#390308,#390309),(#390310,#390311,#390312),
(#390313,#390314,#390315),(#390316,#390317,#390318)),.UNSPECIFIED.,.F.,
 .F.,.F.)
B_SPLINE_SURFACE_WITH_KNOTS((4,4),(3,3),(-1.54744435122082E-6,1.54744435122076E-5),
(-0.0151698983580317,1.),.UNSPECIFIED.)
GEOMETRIC_REPRESENTATION_ITEM()
RATIONAL_B_SPLINE_SURFACE(((1.02018382472404,0.334740937359278,1.),(1.00401234488715,
0.867753072813855,1.),(1.00033622856771,0.988917903080905,1.),(1.,1.,1.)))
REPRESENTATION_ITEM('')
SURFACE()
);
#2663=(
BOUNDED_SURFACE()
B_SPLINE_SURFACE(3,2,((#390320,#390321,#390322),(#390323,#390324,#390325),
(#390326,#390327,#390328),(#390329,#390330,#390331)),.UNSPECIFIED.,.F.,
 .F.,.F.)
B_SPLINE_SURFACE_WITH_KNOTS((4,4),(3,3),(0.00137194782501028,0.00149814269699235),
(0.,1.),.UNSPECIFIED.)
GEOMETRIC_REPRESENTATION_ITEM()
RATIONAL_B_SPLINE_SURFACE(((1.,0.815158509402318,1.),(1.,0.81617904414817,
1.),(1.,0.817226308119915,1.),(1.,0.818301939488809,1.)))
REPRESENTATION_ITEM('')
SURFACE()
);
#2664=(
BOUNDED_SURFACE()
B_SPLINE_SURFACE(3,2,((#390375,#390376,#390377),(#390378,#390379,#390380),
(#390381,#390382,#390383),(#390384,#390385,#390386)),.UNSPECIFIED.,.F.,
 .F.,.F.)
B_SPLINE_SURFACE_WITH_KNOTS((4,4),(3,3),(1.55009486301137E-5,4.92065510474432E-5),
(-8.13759517235604E-5,1.),.UNSPECIFIED.)
GEOMETRIC_REPRESENTATION_ITEM()
RATIONAL_B_SPLINE_SURFACE(((1.00002372912343,0.854200639599652,1.),(1.00001423585998,
0.912530301180515,1.),(1.00000710550473,0.956341495377416,1.),(1.00001238975912,
0.923873338137006,1.)))
REPRESENTATION_ITEM('')
SURFACE()
);
#2665=(
BOUNDED_SURFACE()
B_SPLINE_SURFACE(3,2,((#390390,#390391,#390392),(#390393,#390394,#390395),
(#390396,#390397,#390398),(#390399,#390400,#390401)),.UNSPECIFIED.,.F.,
 .F.,.F.)
B_SPLINE_SURFACE_WITH_KNOTS((4,4),(3,3),(-3.39934179457832E-6,3.73927597403565E-5),
(-0.00186004067364305,1.00069373317418),.UNSPECIFIED.)
GEOMETRIC_REPRESENTATION_ITEM()
RATIONAL_B_SPLINE_SURFACE(((1.00072100136033,0.806051963875482,1.00026859642682),
(1.00060048440136,0.838470803558797,1.00022369994489),(1.00053106448779,
0.857144632272455,1.00019783877213),(1.00054515072836,0.853355459539217,
1.0002030863543)))
REPRESENTATION_ITEM('')
SURFACE()
);
#2666=(
BOUNDED_SURFACE()
B_SPLINE_SURFACE(3,2,((#390403,#390404,#390405),(#390406,#390407,#390408),
(#390409,#390410,#390411),(#390412,#390413,#390414)),.UNSPECIFIED.,.F.,
 .F.,.F.)
B_SPLINE_SURFACE_WITH_KNOTS((4,4),(3,3),(-2.71050543121376E-19,9.54361881492173E-5),
(0.,1.),.UNSPECIFIED.)
GEOMETRIC_REPRESENTATION_ITEM()
RATIONAL_B_SPLINE_SURFACE(((1.,0.816715621142051,1.),(1.,0.815907587407946,
1.),(1.,0.815115959345203,1.),(1.,0.814339887349205,1.)))
REPRESENTATION_ITEM('')
SURFACE()
);
#2667=(
BOUNDED_SURFACE()
B_SPLINE_SURFACE(3,2,((#390416,#390417,#390418),(#390419,#390420,#390421),
(#390422,#390423,#390424),(#390425,#390426,#390427)),.UNSPECIFIED.,.F.,
 .F.,.F.)
B_SPLINE_SURFACE_WITH_KNOTS((4,4),(3,3),(-7.28448334638698E-20,4.68197758448207E-5),
(0.,1.),.UNSPECIFIED.)
GEOMETRIC_REPRESENTATION_ITEM()
RATIONAL_B_SPLINE_SURFACE(((1.,0.81671562114205,1.),(1.,0.953638980025219,
1.),(1.,0.954506925408033,1.),(1.,0.816715621142067,1.)))
REPRESENTATION_ITEM('')
SURFACE()
);
#2668=(
BOUNDED_SURFACE()
B_SPLINE_SURFACE(3,2,((#390429,#390430,#390431),(#390432,#390433,#390434),
(#390435,#390436,#390437),(#390438,#390439,#390440)),.UNSPECIFIED.,.F.,
 .F.,.F.)
B_SPLINE_SURFACE_WITH_KNOTS((4,4),(3,3),(5.42101086242752E-20,9.54361881492178E-5),
(0.,1.),.UNSPECIFIED.)
GEOMETRIC_REPRESENTATION_ITEM()
RATIONAL_B_SPLINE_SURFACE(((1.,0.814339887349195,1.),(1.,0.815115959345213,
1.),(1.,0.815907587407941,1.),(1.,0.81671562114205,1.)))
REPRESENTATION_ITEM('')
SURFACE()
);
#2669=(
BOUNDED_SURFACE()
B_SPLINE_SURFACE(3,2,((#390442,#390443,#390444),(#390445,#390446,#390447),
(#390448,#390449,#390450),(#390451,#390452,#390453)),.UNSPECIFIED.,.F.,
 .F.,.F.)
B_SPLINE_SURFACE_WITH_KNOTS((4,4),(3,3),(-3.39528393502482E-6,3.73481232852735E-5),
(-0.00165018033334558,1.),.UNSPECIFIED.)
GEOMETRIC_REPRESENTATION_ITEM()
RATIONAL_B_SPLINE_SURFACE(((1.00048354385567,0.853487571660392,1.),(1.00047110510922,
0.857256476851449,1.),(1.00053193201109,0.838826096655861,1.),(1.00063970687728,
0.806170615310092,0.999999999999999)))
REPRESENTATION_ITEM('')
SURFACE()
);
#2670=(
BOUNDED_SURFACE()
B_SPLINE_SURFACE(3,2,((#390457,#390458,#390459),(#390460,#390461,#390462),
(#390463,#390464,#390465),(#390466,#390467,#390468)),.UNSPECIFIED.,.F.,
 .F.,.F.)
B_SPLINE_SURFACE_WITH_KNOTS((4,4),(3,3),(2.02993869230509E-5,5.39756952687131E-5),
(-0.000116281069912844,1.),.UNSPECIFIED.)
GEOMETRIC_REPRESENTATION_ITEM()
RATIONAL_B_SPLINE_SURFACE(((1.0000177047973,0.923870681143008,1.),(1.00001014104059,
0.956394275543449,1.),(1.00002037300278,0.912397594905614,1.),(1.00003390859469,
0.854195550869742,1.)))
REPRESENTATION_ITEM('')
SURFACE()
);
#2671=(
BOUNDED_SURFACE()
B_SPLINE_SURFACE(3,2,((#390561,#390562,#390563),(#390564,#390565,#390566),
(#390567,#390568,#390569),(#390570,#390571,#390572)),.UNSPECIFIED.,.F.,
 .F.,.F.)
B_SPLINE_SURFACE_WITH_KNOTS((4,4),(3,3),(0.00135801595889393,0.00148409170619832),
(0.,1.),.UNSPECIFIED.)
GEOMETRIC_REPRESENTATION_ITEM()
RATIONAL_B_SPLINE_SURFACE(((1.,0.818301933966435,1.),(1.,0.817226613172361,
1.),(1.,0.816179643373941,1.),(1.,0.815159387863655,1.)))
REPRESENTATION_ITEM('')
SURFACE()
);
#2672=(
BOUNDED_SURFACE()
B_SPLINE_SURFACE(3,2,((#390611,#390612,#390613),(#390614,#390615,#390616),
(#390617,#390618,#390619),(#390620,#390621,#390622)),.UNSPECIFIED.,.F.,
 .F.,.F.)
B_SPLINE_SURFACE_WITH_KNOTS((4,4),(3,3),(-1.547444351221E-6,1.547444351221E-5),
(-0.0151698983664584,1.),.UNSPECIFIED.)
GEOMETRIC_REPRESENTATION_ITEM()
RATIONAL_B_SPLINE_SURFACE(((1.02018382473542,0.334740937353579,1.),(1.00401234488941,
0.867753072812758,1.),(1.0003362285679,0.988917903080774,1.),(1.,1.,1.)))
REPRESENTATION_ITEM('')
SURFACE()
);
#2673=(
BOUNDED_SURFACE()
B_SPLINE_SURFACE(3,2,((#390624,#390625,#390626),(#390627,#390628,#390629),
(#390630,#390631,#390632),(#390633,#390634,#390635)),.UNSPECIFIED.,.F.,
 .F.,.F.)
B_SPLINE_SURFACE_WITH_KNOTS((4,4),(3,3),(0.00137194782501028,0.00149814269699235),
(0.,1.),.UNSPECIFIED.)
GEOMETRIC_REPRESENTATION_ITEM()
RATIONAL_B_SPLINE_SURFACE(((1.,0.815158509402311,1.),(1.,0.81617904414817,
1.),(1.,0.817226308119933,1.),(1.,0.818301939488804,1.)))
REPRESENTATION_ITEM('')
SURFACE()
);
#2674=(
BOUNDED_SURFACE()
B_SPLINE_SURFACE(3,2,((#390679,#390680,#390681),(#390682,#390683,#390684),
(#390685,#390686,#390687),(#390688,#390689,#390690)),.UNSPECIFIED.,.F.,
 .F.,.F.)
B_SPLINE_SURFACE_WITH_KNOTS((4,4),(3,3),(1.55009486301137E-5,4.92065510474437E-5),
(-8.13759512625954E-5,1.),.UNSPECIFIED.)
GEOMETRIC_REPRESENTATION_ITEM()
RATIONAL_B_SPLINE_SURFACE(((1.00002372912329,0.854200639599705,1.),(1.0000142358599,
0.912530301180581,1.),(1.00000710550469,0.956341495377423,1.),(1.00001238975905,
0.92387333813704,1.)))
REPRESENTATION_ITEM('')
SURFACE()
);
#2675=(
BOUNDED_SURFACE()
B_SPLINE_SURFACE(3,2,((#390694,#390695,#390696),(#390697,#390698,#390699),
(#390700,#390701,#390702),(#390703,#390704,#390705)),.UNSPECIFIED.,.F.,
 .F.,.F.)
B_SPLINE_SURFACE_WITH_KNOTS((4,4),(3,3),(-3.3993417945781E-6,3.73927597403565E-5),
(-0.00186004067444186,1.00069373317443),.UNSPECIFIED.)
GEOMETRIC_REPRESENTATION_ITEM()
RATIONAL_B_SPLINE_SURFACE(((1.00072100136064,0.806051963875309,1.00026859642692),
(1.00060048440162,0.838470803558578,1.00022369994497),(1.00053106448802,
0.857144632272335,1.00019783877221),(1.0005451507286,0.85335545953907,1.00020308635438)))
REPRESENTATION_ITEM('')
SURFACE()
);
#2676=(
BOUNDED_SURFACE()
B_SPLINE_SURFACE(3,2,((#390707,#390708,#390709),(#390710,#390711,#390712),
(#390713,#390714,#390715),(#390716,#390717,#390718)),.UNSPECIFIED.,.F.,
 .F.,.F.)
B_SPLINE_SURFACE_WITH_KNOTS((4,4),(3,3),(-1.62630325872826E-19,9.54361881492174E-5),
(0.,1.),.UNSPECIFIED.)
GEOMETRIC_REPRESENTATION_ITEM()
RATIONAL_B_SPLINE_SURFACE(((1.,0.816715621142052,1.),(1.,0.815907587407941,
1.),(1.,0.815115959345206,1.),(1.,0.814339887349205,1.)))
REPRESENTATION_ITEM('')
SURFACE()
);
#2677=(
BOUNDED_SURFACE()
B_SPLINE_SURFACE(3,2,((#390720,#390721,#390722),(#390723,#390724,#390725),
(#390726,#390727,#390728),(#390729,#390730,#390731)),.UNSPECIFIED.,.F.,
 .F.,.F.)
B_SPLINE_SURFACE_WITH_KNOTS((4,4),(3,3),(-1.62630325872826E-19,4.68197758448203E-5),
(0.,1.),.UNSPECIFIED.)
GEOMETRIC_REPRESENTATION_ITEM()
RATIONAL_B_SPLINE_SURFACE(((1.,0.81671562114205,1.),(1.,0.953638980025207,
1.),(1.,0.954506925408057,1.),(1.,0.816715621142054,1.)))
REPRESENTATION_ITEM('')
SURFACE()
);
#2678=(
BOUNDED_SURFACE()
B_SPLINE_SURFACE(3,2,((#390733,#390734,#390735),(#390736,#390737,#390738),
(#390739,#390740,#390741),(#390742,#390743,#390744)),.UNSPECIFIED.,.F.,
 .F.,.F.)
B_SPLINE_SURFACE_WITH_KNOTS((4,4),(3,3),(0.,9.54361881492176E-5),(0.,1.),
 .UNSPECIFIED.)
GEOMETRIC_REPRESENTATION_ITEM()
RATIONAL_B_SPLINE_SURFACE(((1.,0.814339887349195,1.),(1.,0.815115959345205,
1.),(1.,0.815907587407934,1.),(1.,0.816715621142051,1.)))
REPRESENTATION_ITEM('')
SURFACE()
);
#2679=(
BOUNDED_SURFACE()
B_SPLINE_SURFACE(3,2,((#390746,#390747,#390748),(#390749,#390750,#390751),
(#390752,#390753,#390754),(#390755,#390756,#390757)),.UNSPECIFIED.,.F.,
 .F.,.F.)
B_SPLINE_SURFACE_WITH_KNOTS((4,4),(3,3),(-3.39528393502488E-6,3.73481232852733E-5),
(-0.00165018033319236,1.),.UNSPECIFIED.)
GEOMETRIC_REPRESENTATION_ITEM()
RATIONAL_B_SPLINE_SURFACE(((1.00048354385563,0.853487571660413,1.),(1.00047110510918,
0.857256476851468,1.),(1.00053193201104,0.838826096655893,1.),(1.00063970687722,
0.806170615310112,1.)))
REPRESENTATION_ITEM('')
SURFACE()
);
#2680=(
BOUNDED_SURFACE()
B_SPLINE_SURFACE(3,2,((#390761,#390762,#390763),(#390764,#390765,#390766),
(#390767,#390768,#390769),(#390770,#390771,#390772)),.UNSPECIFIED.,.F.,
 .F.,.F.)
B_SPLINE_SURFACE_WITH_KNOTS((4,4),(3,3),(2.0299386923051E-5,5.39756952687122E-5),
(-0.000116281069487411,1.),.UNSPECIFIED.)
GEOMETRIC_REPRESENTATION_ITEM()
RATIONAL_B_SPLINE_SURFACE(((1.00001770479723,0.923870681143045,1.),(1.00001014104055,
0.956394275543472,1.),(1.00002037300271,0.91239759490564,1.),(1.00003390859456,
0.854195550869798,1.)))
REPRESENTATION_ITEM('')
SURFACE()
);
#2681=(
BOUNDED_SURFACE()
B_SPLINE_SURFACE(3,2,((#390865,#390866,#390867),(#390868,#390869,#390870),
(#390871,#390872,#390873),(#390874,#390875,#390876)),.UNSPECIFIED.,.F.,
 .F.,.F.)
B_SPLINE_SURFACE_WITH_KNOTS((4,4),(3,3),(0.00135801595889393,0.00148409170619832),
(0.,1.),.UNSPECIFIED.)
GEOMETRIC_REPRESENTATION_ITEM()
RATIONAL_B_SPLINE_SURFACE(((1.,0.818301933966441,1.),(1.,0.817226613172357,
1.),(1.,0.816179643373942,1.),(1.,0.815159387863654,1.)))
REPRESENTATION_ITEM('')
SURFACE()
);
#2682=(
BOUNDED_SURFACE()
B_SPLINE_SURFACE(3,2,((#390915,#390916,#390917),(#390918,#390919,#390920),
(#390921,#390922,#390923),(#390924,#390925,#390926)),.UNSPECIFIED.,.F.,
 .F.,.F.)
B_SPLINE_SURFACE_WITH_KNOTS((4,4),(3,3),(-1.5474443512208E-6,1.54744435122079E-5),
(-0.0151698983560359,1.01516989836669),.UNSPECIFIED.)
GEOMETRIC_REPRESENTATION_ITEM()
RATIONAL_B_SPLINE_SURFACE(((1.02018382472135,0.324498219413126,1.02018382473574),
(1.00401234488662,0.865716921710547,1.00401234488948),(1.00033622856767,
0.988747276629689,1.00033622856791),(1.,1.,1.)))
REPRESENTATION_ITEM('')
SURFACE()
);
#2683=(
BOUNDED_SURFACE()
B_SPLINE_SURFACE(3,2,((#390928,#390929,#390930),(#390931,#390932,#390933),
(#390934,#390935,#390936),(#390937,#390938,#390939)),.UNSPECIFIED.,.F.,
 .F.,.F.)
B_SPLINE_SURFACE_WITH_KNOTS((4,4),(3,3),(0.00137194782501028,0.00149814269699235),
(0.,1.),.UNSPECIFIED.)
GEOMETRIC_REPRESENTATION_ITEM()
RATIONAL_B_SPLINE_SURFACE(((1.,0.81515850940232,1.),(1.,0.816179044148155,
1.),(1.,0.817226308119932,1.),(1.,0.818301939488814,1.)))
REPRESENTATION_ITEM('')
SURFACE()
);
#2684=(
BOUNDED_SURFACE()
B_SPLINE_SURFACE(3,2,((#390983,#390984,#390985),(#390986,#390987,#390988),
(#390989,#390990,#390991),(#390992,#390993,#390994)),.UNSPECIFIED.,.F.,
 .F.,.F.)
B_SPLINE_SURFACE_WITH_KNOTS((4,4),(3,3),(1.55009486301137E-5,4.92065510474433E-5),
(-8.13759512421491E-5,1.),.UNSPECIFIED.)
GEOMETRIC_REPRESENTATION_ITEM()
RATIONAL_B_SPLINE_SURFACE(((1.00002372912329,0.854200639599716,1.),(1.00001423585989,
0.912530301180567,1.),(1.00000710550469,0.956341495377428,1.),(1.00001238975905,
0.923873338137046,1.)))
REPRESENTATION_ITEM('')
SURFACE()
);
#2685=(
BOUNDED_SURFACE()
B_SPLINE_SURFACE(3,2,((#390998,#390999,#391000),(#391001,#391002,#391003),
(#391004,#391005,#391006),(#391007,#391008,#391009)),.UNSPECIFIED.,.F.,
 .F.,.F.)
B_SPLINE_SURFACE_WITH_KNOTS((4,4),(3,3),(-3.39934179457794E-6,3.73927597403566E-5),
(-0.00186004067499191,1.0006937331745),.UNSPECIFIED.)
GEOMETRIC_REPRESENTATION_ITEM()
RATIONAL_B_SPLINE_SURFACE(((1.00072100136086,0.806051963875182,1.00026859642695),
(1.0006004844018,0.838470803558485,1.00022369994499),(1.00053106448818,
0.857144632272248,1.00019783877222),(1.00054515072876,0.853355459538966,
1.0002030863544)))
REPRESENTATION_ITEM('')
SURFACE()
);
#2686=(
BOUNDED_SURFACE()
B_SPLINE_SURFACE(3,2,((#391011,#391012,#391013),(#391014,#391015,#391016),
(#391017,#391018,#391019),(#391020,#391021,#391022)),.UNSPECIFIED.,.F.,
 .F.,.F.)
B_SPLINE_SURFACE_WITH_KNOTS((4,4),(3,3),(1.0842021724855E-19,9.54361881492177E-5),
(0.,1.),.UNSPECIFIED.)
GEOMETRIC_REPRESENTATION_ITEM()
RATIONAL_B_SPLINE_SURFACE(((1.,0.816715621142048,1.),(1.,0.815907587407943,
1.),(1.,0.815115959345211,1.),(1.,0.814339887349192,1.)))
REPRESENTATION_ITEM('')
SURFACE()
);
#2687=(
BOUNDED_SURFACE()
B_SPLINE_SURFACE(3,2,((#391024,#391025,#391026),(#391027,#391028,#391029),
(#391030,#391031,#391032),(#391033,#391034,#391035)),.UNSPECIFIED.,.F.,
 .F.,.F.)
B_SPLINE_SURFACE_WITH_KNOTS((4,4),(3,3),(-1.35525271560688E-20,4.68197758448202E-5),
(0.,1.),.UNSPECIFIED.)
GEOMETRIC_REPRESENTATION_ITEM()
RATIONAL_B_SPLINE_SURFACE(((1.,0.816715621142053,1.),(1.,0.953638980025202,
1.),(1.,0.954506925408059,1.),(1.,0.816715621142055,1.)))
REPRESENTATION_ITEM('')
SURFACE()
);
#2688=(
BOUNDED_SURFACE()
B_SPLINE_SURFACE(3,2,((#391037,#391038,#391039),(#391040,#391041,#391042),
(#391043,#391044,#391045),(#391046,#391047,#391048)),.UNSPECIFIED.,.F.,
 .F.,.F.)
B_SPLINE_SURFACE_WITH_KNOTS((4,4),(3,3),(2.16840434497101E-19,9.54361881492179E-5),
(0.,1.),.UNSPECIFIED.)
GEOMETRIC_REPRESENTATION_ITEM()
RATIONAL_B_SPLINE_SURFACE(((1.,0.814339887349196,1.),(1.,0.81511595934521,
1.),(1.,0.815907587407947,1.),(1.,0.816715621142053,1.)))
REPRESENTATION_ITEM('')
SURFACE()
);
#2689=(
BOUNDED_SURFACE()
B_SPLINE_SURFACE(3,2,((#391050,#391051,#391052),(#391053,#391054,#391055),
(#391056,#391057,#391058),(#391059,#391060,#391061)),.UNSPECIFIED.,.F.,
 .F.,.F.)
B_SPLINE_SURFACE_WITH_KNOTS((4,4),(3,3),(-3.39528393502263E-6,3.73481232852728E-5),
(-0.00165018033282337,1.),.UNSPECIFIED.)
GEOMETRIC_REPRESENTATION_ITEM()
RATIONAL_B_SPLINE_SURFACE(((1.00048354385552,0.853487571660466,0.999999999999999),
(1.00047110510907,0.857256476851539,1.),(1.00053193201092,0.838826096655945,
1.),(1.00063970687708,0.806170615310179,0.999999999999999)))
REPRESENTATION_ITEM('')
SURFACE()
);
#2690=(
BOUNDED_SURFACE()
B_SPLINE_SURFACE(3,2,((#391065,#391066,#391067),(#391068,#391069,#391070),
(#391071,#391072,#391073),(#391074,#391075,#391076)),.UNSPECIFIED.,.F.,
 .F.,.F.)
B_SPLINE_SURFACE_WITH_KNOTS((4,4),(3,3),(2.0299386923051E-5,5.39756952687123E-5),
(-0.000116281069803118,1.),.UNSPECIFIED.)
GEOMETRIC_REPRESENTATION_ITEM()
RATIONAL_B_SPLINE_SURFACE(((1.00001770479728,0.923870681143023,1.),(1.00001014104058,
0.956394275543449,1.),(1.00002037300276,0.912397594905616,1.),(1.00003390859465,
0.854195550869764,1.)))
REPRESENTATION_ITEM('')
SURFACE()
);
#2691=(
BOUNDED_SURFACE()
B_SPLINE_SURFACE(3,2,((#391169,#391170,#391171),(#391172,#391173,#391174),
(#391175,#391176,#391177),(#391178,#391179,#391180)),.UNSPECIFIED.,.F.,
 .F.,.F.)
B_SPLINE_SURFACE_WITH_KNOTS((4,4),(3,3),(0.00135801595889393,0.00148409170619832),
(0.,1.),.UNSPECIFIED.)
GEOMETRIC_REPRESENTATION_ITEM()
RATIONAL_B_SPLINE_SURFACE(((1.,0.818301933966442,1.),(1.,0.817226613172347,
1.),(1.,0.816179643373956,1.),(1.,0.815159387863651,1.)))
REPRESENTATION_ITEM('')
SURFACE()
);
#2692=(
BOUNDED_SURFACE()
B_SPLINE_SURFACE(3,2,((#391219,#391220,#391221),(#391222,#391223,#391224),
(#391225,#391226,#391227),(#391228,#391229,#391230)),.UNSPECIFIED.,.F.,
 .F.,.F.)
B_SPLINE_SURFACE_WITH_KNOTS((4,4),(3,3),(-1.54744435122076E-6,1.54744435122077E-5),
(-0.015169898366694,1.015169898356),.UNSPECIFIED.)
GEOMETRIC_REPRESENTATION_ITEM()
RATIONAL_B_SPLINE_SURFACE(((1.02018382473574,0.32449821941326,1.0201838247213),
(1.00401234488948,0.865716921710591,1.00401234488661),(1.00033622856791,
0.988747276629664,1.00033622856767),(1.,1.,1.)))
REPRESENTATION_ITEM('')
SURFACE()
);
#2693=(
BOUNDED_SURFACE()
B_SPLINE_SURFACE(3,2,((#391232,#391233,#391234),(#391235,#391236,#391237),
(#391238,#391239,#391240),(#391241,#391242,#391243)),.UNSPECIFIED.,.F.,
 .F.,.F.)
B_SPLINE_SURFACE_WITH_KNOTS((4,4),(3,3),(0.00137194782501028,0.00149814269699235),
(0.,1.),.UNSPECIFIED.)
GEOMETRIC_REPRESENTATION_ITEM()
RATIONAL_B_SPLINE_SURFACE(((1.,0.815158509402324,1.),(1.,0.816179044148158,
1.),(1.,0.817226308119934,1.),(1.,0.818301939488811,1.)))
REPRESENTATION_ITEM('')
SURFACE()
);
#2694=(
BOUNDED_SURFACE()
B_SPLINE_SURFACE(3,2,((#391287,#391288,#391289),(#391290,#391291,#391292),
(#391293,#391294,#391295),(#391296,#391297,#391298)),.UNSPECIFIED.,.F.,
 .F.,.F.)
B_SPLINE_SURFACE_WITH_KNOTS((4,4),(3,3),(1.55009486301137E-5,4.92065510474431E-5),
(-8.1375951403725E-5,1.),.UNSPECIFIED.)
GEOMETRIC_REPRESENTATION_ITEM()
RATIONAL_B_SPLINE_SURFACE(((1.00002372912333,0.854200639599696,1.),(1.00001423585992,
0.912530301180547,1.),(1.0000071055047,0.956341495377436,1.),(1.00001238975907,
0.923873338137027,1.)))
REPRESENTATION_ITEM('')
SURFACE()
);
#2695=(
BOUNDED_SURFACE()
B_SPLINE_SURFACE(3,2,((#391302,#391303,#391304),(#391305,#391306,#391307),
(#391308,#391309,#391310),(#391311,#391312,#391313)),.UNSPECIFIED.,.F.,
 .F.,.F.)
B_SPLINE_SURFACE_WITH_KNOTS((4,4),(3,3),(-3.39934179457726E-6,3.73927597403567E-5),
(-0.00186004067386771,1.00069373317438),.UNSPECIFIED.)
GEOMETRIC_REPRESENTATION_ITEM()
RATIONAL_B_SPLINE_SURFACE(((1.00072100136042,0.806051963875403,1.0002685964269),
(1.00060048440144,0.838470803558709,1.00022369994495),(1.00053106448786,
0.857144632272417,1.00019783877219),(1.00054515072843,0.853355459539146,
1.00020308635436)))
REPRESENTATION_ITEM('')
SURFACE()
);
#2696=(
BOUNDED_SURFACE()
B_SPLINE_SURFACE(3,2,((#391315,#391316,#391317),(#391318,#391319,#391320),
(#391321,#391322,#391323),(#391324,#391325,#391326)),.UNSPECIFIED.,.F.,
 .F.,.F.)
B_SPLINE_SURFACE_WITH_KNOTS((4,4),(3,3),(0.,9.54361881492175E-5),(0.,1.),
 .UNSPECIFIED.)
GEOMETRIC_REPRESENTATION_ITEM()
RATIONAL_B_SPLINE_SURFACE(((1.,0.816715621142048,1.),(1.,0.815907587407944,
1.),(1.,0.815115959345201,1.),(1.,0.814339887349192,1.)))
REPRESENTATION_ITEM('')
SURFACE()
);
#2697=(
BOUNDED_SURFACE()
B_SPLINE_SURFACE(3,2,((#391328,#391329,#391330),(#391331,#391332,#391333),
(#391334,#391335,#391336),(#391337,#391338,#391339)),.UNSPECIFIED.,.F.,
 .F.,.F.)
B_SPLINE_SURFACE_WITH_KNOTS((4,4),(3,3),(-2.03287907341032E-20,4.68197758448202E-5),
(0.,1.),.UNSPECIFIED.)
GEOMETRIC_REPRESENTATION_ITEM()
RATIONAL_B_SPLINE_SURFACE(((1.,0.816715621142051,1.),(1.,0.953638980025202,
1.),(1.,0.954506925408062,1.),(1.,0.816715621142055,1.)))
REPRESENTATION_ITEM('')
SURFACE()
);
#2698=(
BOUNDED_SURFACE()
B_SPLINE_SURFACE(3,2,((#391341,#391342,#391343),(#391344,#391345,#391346),
(#391347,#391348,#391349),(#391350,#391351,#391352)),.UNSPECIFIED.,.F.,
 .F.,.F.)
B_SPLINE_SURFACE_WITH_KNOTS((4,4),(3,3),(-1.0842021724855E-19,9.54361881492179E-5),
(0.,1.),.UNSPECIFIED.)
GEOMETRIC_REPRESENTATION_ITEM()
RATIONAL_B_SPLINE_SURFACE(((1.,0.814339887349194,1.),(1.,0.815115959345207,
1.),(1.,0.815907587407945,1.),(1.,0.816715621142051,1.)))
REPRESENTATION_ITEM('')
SURFACE()
);
#2699=(
BOUNDED_SURFACE()
B_SPLINE_SURFACE(3,2,((#391354,#391355,#391356),(#391357,#391358,#391359),
(#391360,#391361,#391362),(#391363,#391364,#391365)),.UNSPECIFIED.,.F.,
 .F.,.F.)
B_SPLINE_SURFACE_WITH_KNOTS((4,4),(3,3),(-3.39528393502489E-6,3.73481232852729E-5),
(-0.00165018033268899,1.),.UNSPECIFIED.)
GEOMETRIC_REPRESENTATION_ITEM()
RATIONAL_B_SPLINE_SURFACE(((1.00048354385548,0.853487571660492,1.),(1.00047110510904,
0.85725647685155,1.),(1.00053193201088,0.838826096655953,1.),(1.00063970687702,
0.806170615310211,1.)))
REPRESENTATION_ITEM('')
SURFACE()
);
#2700=(
BOUNDED_SURFACE()
B_SPLINE_SURFACE(3,2,((#391369,#391370,#391371),(#391372,#391373,#391374),
(#391375,#391376,#391377),(#391378,#391379,#391380)),.UNSPECIFIED.,.F.,
 .F.,.F.)
B_SPLINE_SURFACE_WITH_KNOTS((4,4),(3,3),(2.02993869230509E-5,5.39756952687132E-5),
(-0.000116281069788604,1.),.UNSPECIFIED.)
GEOMETRIC_REPRESENTATION_ITEM()
RATIONAL_B_SPLINE_SURFACE(((1.00001770479728,0.923870681143019,1.),(1.00001014104058,
0.956394275543461,1.),(1.00002037300276,0.912397594905618,1.),(1.00003390859465,
0.854195550869757,1.)))
REPRESENTATION_ITEM('')
SURFACE()
);
#2701=(
BOUNDED_SURFACE()
B_SPLINE_SURFACE(3,2,((#391473,#391474,#391475),(#391476,#391477,#391478),
(#391479,#391480,#391481),(#391482,#391483,#391484)),.UNSPECIFIED.,.F.,
 .F.,.F.)
B_SPLINE_SURFACE_WITH_KNOTS((4,4),(3,3),(0.00135801595889393,0.00148409170619832),
(0.,1.),.UNSPECIFIED.)
GEOMETRIC_REPRESENTATION_ITEM()
RATIONAL_B_SPLINE_SURFACE(((1.,0.818301933966439,1.),(1.,0.817226613172347,
1.),(1.,0.816179643373954,1.),(1.,0.815159387863651,1.)))
REPRESENTATION_ITEM('')
SURFACE()
);
#2702=(
BOUNDED_SURFACE()
B_SPLINE_SURFACE(3,2,((#391523,#391524,#391525),(#391526,#391527,#391528),
(#391529,#391530,#391531),(#391532,#391533,#391534)),.UNSPECIFIED.,.F.,
 .F.,.F.)
B_SPLINE_SURFACE_WITH_KNOTS((4,4),(3,3),(-1.54744435122088E-6,1.54744435122086E-5),
(0.,1.01516989836117),.UNSPECIFIED.)
GEOMETRIC_REPRESENTATION_ITEM()
RATIONAL_B_SPLINE_SURFACE(((1.,0.33474093735719,1.02018382472828),(1.,0.867753072813379,
1.004012344888),(1.,0.988917903080892,1.00033622856778),(1.,1.,1.)))
REPRESENTATION_ITEM('')
SURFACE()
);
#2703=(
BOUNDED_SURFACE()
B_SPLINE_SURFACE(3,2,((#391536,#391537,#391538),(#391539,#391540,#391541),
(#391542,#391543,#391544),(#391545,#391546,#391547)),.UNSPECIFIED.,.F.,
 .F.,.F.)
B_SPLINE_SURFACE_WITH_KNOTS((4,4),(3,3),(0.00137194782501028,0.00149814269699235),
(0.,1.),.UNSPECIFIED.)
GEOMETRIC_REPRESENTATION_ITEM()
RATIONAL_B_SPLINE_SURFACE(((1.,0.815158509402315,1.),(1.,0.816179044148166,
1.),(1.,0.817226308119922,1.),(1.,0.81830193948881,1.)))
REPRESENTATION_ITEM('')
SURFACE()
);
#2704=(
BOUNDED_SURFACE()
B_SPLINE_SURFACE(3,2,((#391591,#391592,#391593),(#391594,#391595,#391596),
(#391597,#391598,#391599),(#391600,#391601,#391602)),.UNSPECIFIED.,.F.,
 .F.,.F.)
B_SPLINE_SURFACE_WITH_KNOTS((4,4),(3,3),(1.55009486301138E-5,4.92065510474433E-5),
(-8.13759515113838E-5,1.),.UNSPECIFIED.)
GEOMETRIC_REPRESENTATION_ITEM()
RATIONAL_B_SPLINE_SURFACE(((1.00002372912336,0.854200639599683,1.),(1.00001423585994,
0.912530301180536,1.),(1.00000710550471,0.956341495377428,1.),(1.00001238975909,
0.92387333813702,1.)))
REPRESENTATION_ITEM('')
SURFACE()
);
#2705=(
BOUNDED_SURFACE()
B_SPLINE_SURFACE(3,2,((#391606,#391607,#391608),(#391609,#391610,#391611),
(#391612,#391613,#391614),(#391615,#391616,#391617)),.UNSPECIFIED.,.F.,
 .F.,.F.)
B_SPLINE_SURFACE_WITH_KNOTS((4,4),(3,3),(-3.39934179457829E-6,3.73927597403567E-5),
(-0.00186004067439069,1.00069373317447),.UNSPECIFIED.)
GEOMETRIC_REPRESENTATION_ITEM()
RATIONAL_B_SPLINE_SURFACE(((1.00072100136063,0.806051963875286,1.00026859642694),
(1.00060048440161,0.838470803558599,1.00022369994498),(1.00053106448801,
0.857144632272333,1.00019783877221),(1.00054515072858,0.853355459539056,
1.00020308635439)))
REPRESENTATION_ITEM('')
SURFACE()
);
#2706=(
BOUNDED_SURFACE()
B_SPLINE_SURFACE(3,2,((#391619,#391620,#391621),(#391622,#391623,#391624),
(#391625,#391626,#391627),(#391628,#391629,#391630)),.UNSPECIFIED.,.F.,
 .F.,.F.)
B_SPLINE_SURFACE_WITH_KNOTS((4,4),(3,3),(0.,9.54361881492173E-5),(0.,1.),
 .UNSPECIFIED.)
GEOMETRIC_REPRESENTATION_ITEM()
RATIONAL_B_SPLINE_SURFACE(((1.,0.816715621142043,1.),(1.,0.815907587407943,
1.),(1.,0.815115959345201,1.),(1.,0.814339887349192,1.)))
REPRESENTATION_ITEM('')
SURFACE()
);
#2707=(
BOUNDED_SURFACE()
B_SPLINE_SURFACE(3,2,((#391632,#391633,#391634),(#391635,#391636,#391637),
(#391638,#391639,#391640),(#391641,#391642,#391643)),.UNSPECIFIED.,.F.,
 .F.,.F.)
B_SPLINE_SURFACE_WITH_KNOTS((4,4),(3,3),(3.72694496791892E-20,4.68197758448211E-5),
(0.,1.),.UNSPECIFIED.)
GEOMETRIC_REPRESENTATION_ITEM()
RATIONAL_B_SPLINE_SURFACE(((1.,0.816715621142048,1.),(1.,0.953638980025199,
1.),(1.,0.954506925408065,1.),(1.,0.81671562114205,1.)))
REPRESENTATION_ITEM('')
SURFACE()
);
#2708=(
BOUNDED_SURFACE()
B_SPLINE_SURFACE(3,2,((#391645,#391646,#391647),(#391648,#391649,#391650),
(#391651,#391652,#391653),(#391654,#391655,#391656)),.UNSPECIFIED.,.F.,
 .F.,.F.)
B_SPLINE_SURFACE_WITH_KNOTS((4,4),(3,3),(5.42101086242752E-20,9.54361881492175E-5),
(0.,1.),.UNSPECIFIED.)
GEOMETRIC_REPRESENTATION_ITEM()
RATIONAL_B_SPLINE_SURFACE(((1.,0.814339887349195,1.),(1.,0.815115959345203,
1.),(1.,0.815907587407943,1.),(1.,0.816715621142048,1.)))
REPRESENTATION_ITEM('')
SURFACE()
);
#2709=(
BOUNDED_SURFACE()
B_SPLINE_SURFACE(3,2,((#391658,#391659,#391660),(#391661,#391662,#391663),
(#391664,#391665,#391666),(#391667,#391668,#391669)),.UNSPECIFIED.,.F.,
 .F.,.F.)
B_SPLINE_SURFACE_WITH_KNOTS((4,4),(3,3),(-3.39528393502494E-6,3.73481232852736E-5),
(-0.00165018033281065,1.),.UNSPECIFIED.)
GEOMETRIC_REPRESENTATION_ITEM()
RATIONAL_B_SPLINE_SURFACE(((1.00048354385552,0.853487571660464,1.),(1.00047110510907,
0.857256476851531,1.),(1.00053193201092,0.838826096655946,1.),(1.00063970687707,
0.806170615310178,1.)))
REPRESENTATION_ITEM('')
SURFACE()
);
#2710=(
BOUNDED_SURFACE()
B_SPLINE_SURFACE(3,2,((#391673,#391674,#391675),(#391676,#391677,#391678),
(#391679,#391680,#391681),(#391682,#391683,#391684)),.UNSPECIFIED.,.F.,
 .F.,.F.)
B_SPLINE_SURFACE_WITH_KNOTS((4,4),(3,3),(2.02993869230512E-5,5.39756952686905E-5),
(-0.000116281069867502,1.),.UNSPECIFIED.)
GEOMETRIC_REPRESENTATION_ITEM()
RATIONAL_B_SPLINE_SURFACE(((1.00001770479729,0.923870681143014,1.),(1.00001014104058,
0.956394275543423,1.),(1.00002037300277,0.912397594905681,1.),(1.00003390859467,
0.854195550869863,1.)))
REPRESENTATION_ITEM('')
SURFACE()
);
#2711=(
BOUNDED_SURFACE()
B_SPLINE_SURFACE(3,2,((#391777,#391778,#391779),(#391780,#391781,#391782),
(#391783,#391784,#391785),(#391786,#391787,#391788)),.UNSPECIFIED.,.F.,
 .F.,.F.)
B_SPLINE_SURFACE_WITH_KNOTS((4,4),(3,3),(0.00135801595889393,0.00148409170619832),
(0.,1.),.UNSPECIFIED.)
GEOMETRIC_REPRESENTATION_ITEM()
RATIONAL_B_SPLINE_SURFACE(((1.,0.818301933966447,1.),(1.,0.817226613172343,
1.),(1.,0.816179643373953,1.),(1.,0.815159387863653,1.)))
REPRESENTATION_ITEM('')
SURFACE()
);
#2712=(
BOUNDED_SURFACE()
B_SPLINE_SURFACE(3,2,((#391827,#391828,#391829),(#391830,#391831,#391832),
(#391833,#391834,#391835),(#391836,#391837,#391838)),.UNSPECIFIED.,.F.,
 .F.,.F.)
B_SPLINE_SURFACE_WITH_KNOTS((4,4),(3,3),(-1.54744435122076E-6,1.54744435122075E-5),
(-0.0151698983634846,1.),.UNSPECIFIED.)
GEOMETRIC_REPRESENTATION_ITEM()
RATIONAL_B_SPLINE_SURFACE(((1.0201838247314,0.334740937355646,1.),(1.00401234488862,
0.867753072813101,1.),(1.00033622856784,0.9889179030808,1.),(1.,1.,1.)))
REPRESENTATION_ITEM('')
SURFACE()
);
#2713=(
BOUNDED_SURFACE()
B_SPLINE_SURFACE(3,2,((#391840,#391841,#391842),(#391843,#391844,#391845),
(#391846,#391847,#391848),(#391849,#391850,#391851)),.UNSPECIFIED.,.F.,
 .F.,.F.)
B_SPLINE_SURFACE_WITH_KNOTS((4,4),(3,3),(0.00137194782501028,0.00149814269699235),
(0.,1.),.UNSPECIFIED.)
GEOMETRIC_REPRESENTATION_ITEM()
RATIONAL_B_SPLINE_SURFACE(((1.,0.815158509402315,1.),(1.,0.816179044148159,
1.),(1.,0.817226308119933,1.),(1.,0.818301939488797,1.)))
REPRESENTATION_ITEM('')
SURFACE()
);
#2714=(
BOUNDED_SURFACE()
B_SPLINE_SURFACE(3,2,((#391895,#391896,#391897),(#391898,#391899,#391900),
(#391901,#391902,#391903),(#391904,#391905,#391906)),.UNSPECIFIED.,.F.,
 .F.,.F.)
B_SPLINE_SURFACE_WITH_KNOTS((4,4),(3,3),(1.55009486301138E-5,4.9206551047444E-5),
(-8.13759513100112E-5,1.),.UNSPECIFIED.)
GEOMETRIC_REPRESENTATION_ITEM()
RATIONAL_B_SPLINE_SURFACE(((1.00002372912331,0.854200639599707,1.),(1.0000142358599,
0.912530301180563,1.),(1.00000710550469,0.956341495377437,1.),(1.00001238975906,
0.923873338137034,1.)))
REPRESENTATION_ITEM('')
SURFACE()
);
#2715=(
BOUNDED_SURFACE()
B_SPLINE_SURFACE(3,2,((#391910,#391911,#391912),(#391913,#391914,#391915),
(#391916,#391917,#391918),(#391919,#391920,#391921)),.UNSPECIFIED.,.F.,
 .F.,.F.)
B_SPLINE_SURFACE_WITH_KNOTS((4,4),(3,3),(-3.39934179457842E-6,3.73927597403566E-5),
(-0.00186004067399086,1.00069373317438),.UNSPECIFIED.)
GEOMETRIC_REPRESENTATION_ITEM()
RATIONAL_B_SPLINE_SURFACE(((1.00072100136047,0.806051963875379,1.0002685964269),
(1.00060048440148,0.838470803558684,1.00022369994495),(1.00053106448789,
0.857144632272404,1.00019783877219),(1.00054515072847,0.853355459539131,
1.00020308635436)))
REPRESENTATION_ITEM('')
SURFACE()
);
#2716=(
BOUNDED_SURFACE()
B_SPLINE_SURFACE(3,2,((#391923,#391924,#391925),(#391926,#391927,#391928),
(#391929,#391930,#391931),(#391932,#391933,#391934)),.UNSPECIFIED.,.F.,
 .F.,.F.)
B_SPLINE_SURFACE_WITH_KNOTS((4,4),(3,3),(-5.42101086242752E-20,9.54361881492174E-5),
(0.,1.),.UNSPECIFIED.)
GEOMETRIC_REPRESENTATION_ITEM()
RATIONAL_B_SPLINE_SURFACE(((1.,0.81671562114205,1.),(1.,0.815907587407946,
1.),(1.,0.815115959345202,1.),(1.,0.814339887349197,1.)))
REPRESENTATION_ITEM('')
SURFACE()
);
#2717=(
BOUNDED_SURFACE()
B_SPLINE_SURFACE(3,2,((#391936,#391937,#391938),(#391939,#391940,#391941),
(#391942,#391943,#391944),(#391945,#391946,#391947)),.UNSPECIFIED.,.F.,
 .F.,.F.)
B_SPLINE_SURFACE_WITH_KNOTS((4,4),(3,3),(6.60685698858354E-20,4.68197758448206E-5),
(0.,1.),.UNSPECIFIED.)
GEOMETRIC_REPRESENTATION_ITEM()
RATIONAL_B_SPLINE_SURFACE(((1.,0.816715621142048,1.),(1.,0.95363898002521,
1.),(1.,0.954506925408056,1.),(1.,0.816715621142053,1.)))
REPRESENTATION_ITEM('')
SURFACE()
);
#2718=(
BOUNDED_SURFACE()
B_SPLINE_SURFACE(3,2,((#391949,#391950,#391951),(#391952,#391953,#391954),
(#391955,#391956,#391957),(#391958,#391959,#391960)),.UNSPECIFIED.,.F.,
 .F.,.F.)
B_SPLINE_SURFACE_WITH_KNOTS((4,4),(3,3),(5.42101086242752E-20,9.54361881492175E-5),
(0.,1.),.UNSPECIFIED.)
GEOMETRIC_REPRESENTATION_ITEM()
RATIONAL_B_SPLINE_SURFACE(((1.,0.814339887349195,1.),(1.,0.815115959345198,
1.),(1.,0.815907587407947,1.),(1.,0.816715621142048,1.)))
REPRESENTATION_ITEM('')
SURFACE()
);
#2719=(
BOUNDED_SURFACE()
B_SPLINE_SURFACE(3,2,((#391962,#391963,#391964),(#391965,#391966,#391967),
(#391968,#391969,#391970),(#391971,#391972,#391973)),.UNSPECIFIED.,.F.,
 .F.,.F.)
B_SPLINE_SURFACE_WITH_KNOTS((4,4),(3,3),(-3.39528393502485E-6,3.73481232852736E-5),
(-0.0016501803329349,1.),.UNSPECIFIED.)
GEOMETRIC_REPRESENTATION_ITEM()
RATIONAL_B_SPLINE_SURFACE(((1.00048354385555,0.853487571660447,1.),(1.00047110510911,
0.857256476851509,1.),(1.00053193201096,0.838826096655926,1.),(1.00063970687712,
0.806170615310158,1.)))
REPRESENTATION_ITEM('')
SURFACE()
);
#2720=(
BOUNDED_SURFACE()
B_SPLINE_SURFACE(3,2,((#391977,#391978,#391979),(#391980,#391981,#391982),
(#391983,#391984,#391985),(#391986,#391987,#391988)),.UNSPECIFIED.,.F.,
 .F.,.F.)
B_SPLINE_SURFACE_WITH_KNOTS((4,4),(3,3),(2.02993869230509E-5,5.39756952686908E-5),
(-0.000116281069783489,1.),.UNSPECIFIED.)
GEOMETRIC_REPRESENTATION_ITEM()
RATIONAL_B_SPLINE_SURFACE(((1.00001770479728,0.92387068114302,1.),(1.00001014104058,
0.956394275543422,1.),(1.00002037300276,0.912397594905689,1.),(1.00003390859465,
0.854195550869876,1.)))
REPRESENTATION_ITEM('')
SURFACE()
);
#2721=(
BOUNDED_SURFACE()
B_SPLINE_SURFACE(3,2,((#392081,#392082,#392083),(#392084,#392085,#392086),
(#392087,#392088,#392089),(#392090,#392091,#392092)),.UNSPECIFIED.,.F.,
 .F.,.F.)
B_SPLINE_SURFACE_WITH_KNOTS((4,4),(3,3),(0.00135801595889393,0.00148409170619832),
(0.,1.),.UNSPECIFIED.)
GEOMETRIC_REPRESENTATION_ITEM()
RATIONAL_B_SPLINE_SURFACE(((1.,0.818301933966443,1.),(1.,0.817226613172345,
1.),(1.,0.816179643373947,1.),(1.,0.815159387863655,1.)))
REPRESENTATION_ITEM('')
SURFACE()
);
#2722=(
BOUNDED_SURFACE()
B_SPLINE_SURFACE(3,2,((#392131,#392132,#392133),(#392134,#392135,#392136),
(#392137,#392138,#392139),(#392140,#392141,#392142)),.UNSPECIFIED.,.F.,
 .F.,.F.)
B_SPLINE_SURFACE_WITH_KNOTS((4,4),(3,3),(-1.54744435122035E-6,1.54744435122103E-5),
(-0.0151698983687994,1.01516989835352),.UNSPECIFIED.)
GEOMETRIC_REPRESENTATION_ITEM()
RATIONAL_B_SPLINE_SURFACE(((1.02018382473858,0.324498219413536,1.02018382471794),
(1.00401234489005,0.865716921710479,1.00401234488594),(1.00033622856796,
0.9887472766297,1.00033622856761),(1.,1.,1.)))
REPRESENTATION_ITEM('')
SURFACE()
);
#2723=(
BOUNDED_SURFACE()
B_SPLINE_SURFACE(3,2,((#392144,#392145,#392146),(#392147,#392148,#392149),
(#392150,#392151,#392152),(#392153,#392154,#392155)),.UNSPECIFIED.,.F.,
 .F.,.F.)
B_SPLINE_SURFACE_WITH_KNOTS((4,4),(3,3),(0.00137194782501028,0.00149814269699235),
(0.,1.),.UNSPECIFIED.)
GEOMETRIC_REPRESENTATION_ITEM()
RATIONAL_B_SPLINE_SURFACE(((1.,0.81515850940232,1.),(1.,0.816179044148184,
1.),(1.,0.817226308119919,1.),(1.,0.818301939488813,1.)))
REPRESENTATION_ITEM('')
SURFACE()
);
#2724=(
BOUNDED_SURFACE()
B_SPLINE_SURFACE(3,2,((#392199,#392200,#392201),(#392202,#392203,#392204),
(#392205,#392206,#392207),(#392208,#392209,#392210)),.UNSPECIFIED.,.F.,
 .F.,.F.)
B_SPLINE_SURFACE_WITH_KNOTS((4,4),(3,3),(1.55009486301137E-5,4.92065510474437E-5),
(-8.13759513857627E-5,1.),.UNSPECIFIED.)
GEOMETRIC_REPRESENTATION_ITEM()
RATIONAL_B_SPLINE_SURFACE(((1.00002372912333,0.854200639599689,1.),(1.00001423585992,
0.912530301180556,1.),(1.0000071055047,0.956341495377434,1.),(1.00001238975907,
0.923873338137031,1.)))
REPRESENTATION_ITEM('')
SURFACE()
);
#2725=(
BOUNDED_SURFACE()
B_SPLINE_SURFACE(3,2,((#392214,#392215,#392216),(#392217,#392218,#392219),
(#392220,#392221,#392222),(#392223,#392224,#392225)),.UNSPECIFIED.,.F.,
 .F.,.F.)
B_SPLINE_SURFACE_WITH_KNOTS((4,4),(3,3),(-3.39934179457847E-6,3.73927597403563E-5),
(-0.00186004067427395,1.0006937331744),.UNSPECIFIED.)
GEOMETRIC_REPRESENTATION_ITEM()
RATIONAL_B_SPLINE_SURFACE(((1.00072100136058,0.806051963875343,1.00026859642691),
(1.00060048440157,0.838470803558615,1.00022369994496),(1.00053106448797,
0.857144632272372,1.00019783877219),(1.00054515072855,0.85335545953908,
1.00020308635437)))
REPRESENTATION_ITEM('')
SURFACE()
);
#2726=(
BOUNDED_SURFACE()
B_SPLINE_SURFACE(3,2,((#392227,#392228,#392229),(#392230,#392231,#392232),
(#392233,#392234,#392235),(#392236,#392237,#392238)),.UNSPECIFIED.,.F.,
 .F.,.F.)
B_SPLINE_SURFACE_WITH_KNOTS((4,4),(3,3),(-5.42101086242752E-20,9.54361881492172E-5),
(0.,1.),.UNSPECIFIED.)
GEOMETRIC_REPRESENTATION_ITEM()
RATIONAL_B_SPLINE_SURFACE(((1.,0.816715621142052,1.),(1.,0.81590758740794,
1.),(1.,0.815115959345208,1.),(1.,0.814339887349189,1.)))
REPRESENTATION_ITEM('')
SURFACE()
);
#2727=(
BOUNDED_SURFACE()
B_SPLINE_SURFACE(3,2,((#392240,#392241,#392242),(#392243,#392244,#392245),
(#392246,#392247,#392248),(#392249,#392250,#392251)),.UNSPECIFIED.,.F.,
 .F.,.F.)
B_SPLINE_SURFACE_WITH_KNOTS((4,4),(3,3),(1.52465930505774E-20,4.68197758448212E-5),
(0.,1.),.UNSPECIFIED.)
GEOMETRIC_REPRESENTATION_ITEM()
RATIONAL_B_SPLINE_SURFACE(((1.,0.816715621142048,1.),(1.,0.953638980025214,
1.),(1.,0.95450692540805,1.),(1.,0.816715621142054,1.)))
REPRESENTATION_ITEM('')
SURFACE()
);
#2728=(
BOUNDED_SURFACE()
B_SPLINE_SURFACE(3,2,((#392253,#392254,#392255),(#392256,#392257,#392258),
(#392259,#392260,#392261),(#392262,#392263,#392264)),.UNSPECIFIED.,.F.,
 .F.,.F.)
B_SPLINE_SURFACE_WITH_KNOTS((4,4),(3,3),(2.16840434497101E-19,9.54361881492177E-5),
(0.,1.),.UNSPECIFIED.)
GEOMETRIC_REPRESENTATION_ITEM()
RATIONAL_B_SPLINE_SURFACE(((1.,0.814339887349197,1.),(1.,0.815115959345207,
1.),(1.,0.81590758740794,1.),(1.,0.816715621142055,1.)))
REPRESENTATION_ITEM('')
SURFACE()
);
#2729=(
BOUNDED_SURFACE()
B_SPLINE_SURFACE(3,2,((#392266,#392267,#392268),(#392269,#392270,#392271),
(#392272,#392273,#392274),(#392275,#392276,#392277)),.UNSPECIFIED.,.F.,
 .F.,.F.)
B_SPLINE_SURFACE_WITH_KNOTS((4,4),(3,3),(-3.39528393502276E-6,3.73481232852735E-5),
(-0.00165018033333829,1.),.UNSPECIFIED.)
GEOMETRIC_REPRESENTATION_ITEM()
RATIONAL_B_SPLINE_SURFACE(((1.00048354385567,0.8534875716604,1.),(1.00047110510922,
0.857256476851447,1.),(1.00053193201109,0.838826096655876,1.),(1.00063970687728,
0.806170615310078,1.)))
REPRESENTATION_ITEM('')
SURFACE()
);
#2730=(
BOUNDED_SURFACE()
B_SPLINE_SURFACE(3,2,((#392281,#392282,#392283),(#392284,#392285,#392286),
(#392287,#392288,#392289),(#392290,#392291,#392292)),.UNSPECIFIED.,.F.,
 .F.,.F.)
B_SPLINE_SURFACE_WITH_KNOTS((4,4),(3,3),(2.0299386923051E-5,5.39756952687117E-5),
(-0.00011628106978846,1.),.UNSPECIFIED.)
GEOMETRIC_REPRESENTATION_ITEM()
RATIONAL_B_SPLINE_SURFACE(((1.00001770479728,0.92387068114302,1.),(1.00001014104058,
0.95639427554344,1.),(1.00002037300276,0.912397594905636,1.),(1.00003390859465,
0.85419555086975,1.)))
REPRESENTATION_ITEM('')
SURFACE()
);
#2731=(
BOUNDED_SURFACE()
B_SPLINE_SURFACE(3,2,((#392385,#392386,#392387),(#392388,#392389,#392390),
(#392391,#392392,#392393),(#392394,#392395,#392396)),.UNSPECIFIED.,.F.,
 .F.,.F.)
B_SPLINE_SURFACE_WITH_KNOTS((4,4),(3,3),(0.00135801595889393,0.00148409170619832),
(0.,1.),.UNSPECIFIED.)
GEOMETRIC_REPRESENTATION_ITEM()
RATIONAL_B_SPLINE_SURFACE(((1.,0.818301933966443,1.),(1.,0.817226613172348,
1.),(1.,0.816179643373948,1.),(1.,0.815159387863653,1.)))
REPRESENTATION_ITEM('')
SURFACE()
);
#2732=(
BOUNDED_SURFACE()
B_SPLINE_SURFACE(3,2,((#392435,#392436,#392437),(#392438,#392439,#392440),
(#392441,#392442,#392443),(#392444,#392445,#392446)),.UNSPECIFIED.,.F.,
 .F.,.F.)
B_SPLINE_SURFACE_WITH_KNOTS((4,4),(3,3),(-1.54744435122077E-6,1.54744435122075E-5),
(-0.0151698983695553,1.01516989835249),.UNSPECIFIED.)
GEOMETRIC_REPRESENTATION_ITEM()
RATIONAL_B_SPLINE_SURFACE(((1.0201838247396,0.324498219413675,1.02018382471655),
(1.00401234489024,0.865716921710634,1.00401234488566),(1.00033622856797,
0.988747276629691,1.00033622856759),(1.,1.,1.)))
REPRESENTATION_ITEM('')
SURFACE()
);
#2733=(
BOUNDED_SURFACE()
B_SPLINE_SURFACE(3,2,((#392448,#392449,#392450),(#392451,#392452,#392453),
(#392454,#392455,#392456),(#392457,#392458,#392459)),.UNSPECIFIED.,.F.,
 .F.,.F.)
B_SPLINE_SURFACE_WITH_KNOTS((4,4),(3,3),(0.00137194782501028,0.00149814269699235),
(0.,1.),.UNSPECIFIED.)
GEOMETRIC_REPRESENTATION_ITEM()
RATIONAL_B_SPLINE_SURFACE(((1.,0.815158509402309,1.),(1.,0.816179044148166,
1.),(1.,0.81722630811991,1.),(1.,0.818301939488811,1.)))
REPRESENTATION_ITEM('')
SURFACE()
);
#2734=(
BOUNDED_SURFACE()
B_SPLINE_SURFACE(3,2,((#392503,#392504,#392505),(#392506,#392507,#392508),
(#392509,#392510,#392511),(#392512,#392513,#392514)),.UNSPECIFIED.,.F.,
 .F.,.F.)
B_SPLINE_SURFACE_WITH_KNOTS((4,4),(3,3),(1.55009486301137E-5,4.92065510474435E-5),
(-8.13759514726279E-5,1.),.UNSPECIFIED.)
GEOMETRIC_REPRESENTATION_ITEM()
RATIONAL_B_SPLINE_SURFACE(((1.00002372912335,0.854200639599686,1.),(1.00001423585993,
0.91253030118053,1.),(1.00000710550471,0.956341495377435,1.),(1.00001238975908,
0.923873338137022,1.)))
REPRESENTATION_ITEM('')
SURFACE()
);
#2735=(
BOUNDED_SURFACE()
B_SPLINE_SURFACE(3,2,((#392518,#392519,#392520),(#392521,#392522,#392523),
(#392524,#392525,#392526),(#392527,#392528,#392529)),.UNSPECIFIED.,.F.,
 .F.,.F.)
B_SPLINE_SURFACE_WITH_KNOTS((4,4),(3,3),(-3.39934179457794E-6,3.73927597403566E-5),
(-0.00186004067473901,1.00069373317458),.UNSPECIFIED.)
GEOMETRIC_REPRESENTATION_ITEM()
RATIONAL_B_SPLINE_SURFACE(((1.00072100136076,0.806051963875218,1.00026859642698),
(1.00060048440172,0.838470803558506,1.00022369994502),(1.00053106448811,
0.857144632272285,1.00019783877225),(1.00054515072869,0.853355459538985,
1.00020308635442)))
REPRESENTATION_ITEM('')
SURFACE()
);
#2736=(
BOUNDED_SURFACE()
B_SPLINE_SURFACE(3,2,((#392531,#392532,#392533),(#392534,#392535,#392536),
(#392537,#392538,#392539),(#392540,#392541,#392542)),.UNSPECIFIED.,.F.,
 .F.,.F.)
B_SPLINE_SURFACE_WITH_KNOTS((4,4),(3,3),(1.0842021724855E-19,9.54361881492175E-5),
(0.,1.),.UNSPECIFIED.)
GEOMETRIC_REPRESENTATION_ITEM()
RATIONAL_B_SPLINE_SURFACE(((1.,0.816715621142047,1.),(1.,0.815907587407942,
1.),(1.,0.815115959345205,1.),(1.,0.814339887349193,1.)))
REPRESENTATION_ITEM('')
SURFACE()
);
#2737=(
BOUNDED_SURFACE()
B_SPLINE_SURFACE(3,2,((#392544,#392545,#392546),(#392547,#392548,#392549),
(#392550,#392551,#392552),(#392553,#392554,#392555)),.UNSPECIFIED.,.F.,
 .F.,.F.)
B_SPLINE_SURFACE_WITH_KNOTS((4,4),(3,3),(2.71050543121376E-19,4.68197758448202E-5),
(0.,1.),.UNSPECIFIED.)
GEOMETRIC_REPRESENTATION_ITEM()
RATIONAL_B_SPLINE_SURFACE(((1.,0.81671562114206,1.),(1.,0.953638980025188,
1.),(1.,0.954506925408073,1.),(1.,0.81671562114205,1.)))
REPRESENTATION_ITEM('')
SURFACE()
);
#2738=(
BOUNDED_SURFACE()
B_SPLINE_SURFACE(3,2,((#392557,#392558,#392559),(#392560,#392561,#392562),
(#392563,#392564,#392565),(#392566,#392567,#392568)),.UNSPECIFIED.,.F.,
 .F.,.F.)
B_SPLINE_SURFACE_WITH_KNOTS((4,4),(3,3),(2.16840434497101E-19,9.54361881492178E-5),
(0.,1.),.UNSPECIFIED.)
GEOMETRIC_REPRESENTATION_ITEM()
RATIONAL_B_SPLINE_SURFACE(((1.,0.814339887349199,1.),(1.,0.815115959345194,
1.),(1.,0.81590758740794,1.),(1.,0.816715621142048,1.)))
REPRESENTATION_ITEM('')
SURFACE()
);
#2739=(
BOUNDED_SURFACE()
B_SPLINE_SURFACE(3,2,((#392570,#392571,#392572),(#392573,#392574,#392575),
(#392576,#392577,#392578),(#392579,#392580,#392581)),.UNSPECIFIED.,.F.,
 .F.,.F.)
B_SPLINE_SURFACE_WITH_KNOTS((4,4),(3,3),(-3.39528393502482E-6,3.73481232852722E-5),
(-0.00165018033345345,1.),.UNSPECIFIED.)
GEOMETRIC_REPRESENTATION_ITEM()
RATIONAL_B_SPLINE_SURFACE(((1.0004835438557,0.853487571660372,1.),(1.00047110510926,
0.857256476851432,1.),(1.00053193201113,0.838826096655844,1.),(1.00063970687732,
0.806170615310062,1.)))
REPRESENTATION_ITEM('')
SURFACE()
);
#2740=(
BOUNDED_SURFACE()
B_SPLINE_SURFACE(3,2,((#392585,#392586,#392587),(#392588,#392589,#392590),
(#392591,#392592,#392593),(#392594,#392595,#392596)),.UNSPECIFIED.,.F.,
 .F.,.F.)
B_SPLINE_SURFACE_WITH_KNOTS((4,4),(3,3),(2.02993869230509E-5,5.39756952687131E-5),
(-0.000116281070764672,1.),.UNSPECIFIED.)
GEOMETRIC_REPRESENTATION_ITEM()
RATIONAL_B_SPLINE_SURFACE(((1.00001770479743,0.923870681142944,1.),(1.00001014104066,
0.956394275543422,1.),(1.00002037300293,0.912397594905522,1.),(1.00003390859493,
0.854195550869619,1.)))
REPRESENTATION_ITEM('')
SURFACE()
);
#2741=(
BOUNDED_SURFACE()
B_SPLINE_SURFACE(3,2,((#392689,#392690,#392691),(#392692,#392693,#392694),
(#392695,#392696,#392697),(#392698,#392699,#392700)),.UNSPECIFIED.,.F.,
 .F.,.F.)
B_SPLINE_SURFACE_WITH_KNOTS((4,4),(3,3),(0.00135801595889393,0.00148409170619832),
(0.,1.),.UNSPECIFIED.)
GEOMETRIC_REPRESENTATION_ITEM()
RATIONAL_B_SPLINE_SURFACE(((1.,0.818301933966439,1.),(1.,0.817226613172351,
1.),(1.,0.816179643373943,1.),(1.,0.81515938786366,1.)))
REPRESENTATION_ITEM('')
SURFACE()
);
#2742=(
BOUNDED_SURFACE()
B_SPLINE_SURFACE(3,2,((#392739,#392740,#392741),(#392742,#392743,#392744),
(#392745,#392746,#392747),(#392748,#392749,#392750)),.UNSPECIFIED.,.F.,
 .F.,.F.)
B_SPLINE_SURFACE_WITH_KNOTS((4,4),(3,3),(-1.54744435122084E-6,1.54744435122079E-5),
(-0.0151698983650642,1.),.UNSPECIFIED.)
GEOMETRIC_REPRESENTATION_ITEM()
RATIONAL_B_SPLINE_SURFACE(((1.02018382473354,0.334740937354608,1.),(1.00401234488904,
0.867753072812928,1.),(1.00033622856787,0.988917903080853,1.),(1.,1.,1.)))
REPRESENTATION_ITEM('')
SURFACE()
);
#2743=(
BOUNDED_SURFACE()
B_SPLINE_SURFACE(3,2,((#392752,#392753,#392754),(#392755,#392756,#392757),
(#392758,#392759,#392760),(#392761,#392762,#392763)),.UNSPECIFIED.,.F.,
 .F.,.F.)
B_SPLINE_SURFACE_WITH_KNOTS((4,4),(3,3),(0.00137194782501028,0.00149814269699235),
(0.,1.),.UNSPECIFIED.)
GEOMETRIC_REPRESENTATION_ITEM()
RATIONAL_B_SPLINE_SURFACE(((1.,0.81515850940232,1.),(1.,0.81617904414816,
1.),(1.,0.817226308119934,1.),(1.,0.818301939488798,1.)))
REPRESENTATION_ITEM('')
SURFACE()
);
#2744=(
BOUNDED_SURFACE()
B_SPLINE_SURFACE(3,2,((#392807,#392808,#392809),(#392810,#392811,#392812),
(#392813,#392814,#392815),(#392816,#392817,#392818)),.UNSPECIFIED.,.F.,
 .F.,.F.)
B_SPLINE_SURFACE_WITH_KNOTS((4,4),(3,3),(1.55009486301137E-5,4.92065510474422E-5),
(-8.13759512240223E-5,1.),.UNSPECIFIED.)
GEOMETRIC_REPRESENTATION_ITEM()
RATIONAL_B_SPLINE_SURFACE(((1.00002372912328,0.854200639599726,1.),(1.00001423585989,
0.912530301180556,1.),(1.00000710550469,0.956341495377445,1.),(1.00001238975904,
0.923873338137043,1.)))
REPRESENTATION_ITEM('')
SURFACE()
);
#2745=(
BOUNDED_SURFACE()
B_SPLINE_SURFACE(3,2,((#392822,#392823,#392824),(#392825,#392826,#392827),
(#392828,#392829,#392830),(#392831,#392832,#392833)),.UNSPECIFIED.,.F.,
 .F.,.F.)
B_SPLINE_SURFACE_WITH_KNOTS((4,4),(3,3),(-3.39934179457808E-6,3.73927597403565E-5),
(-0.00186004067398835,1.00069373317426),.UNSPECIFIED.)
GEOMETRIC_REPRESENTATION_ITEM()
RATIONAL_B_SPLINE_SURFACE(((1.00072100136047,0.806051963875403,1.00026859642685),
(1.00060048440148,0.838470803558706,1.00022369994491),(1.00053106448789,
0.857144632272425,1.00019783877215),(1.00054515072846,0.853355459539151,
1.00020308635433)))
REPRESENTATION_ITEM('')
SURFACE()
);
#2746=(
BOUNDED_SURFACE()
B_SPLINE_SURFACE(3,2,((#392835,#392836,#392837),(#392838,#392839,#392840),
(#392841,#392842,#392843),(#392844,#392845,#392846)),.UNSPECIFIED.,.F.,
 .F.,.F.)
B_SPLINE_SURFACE_WITH_KNOTS((4,4),(3,3),(1.62630325872826E-19,9.54361881492174E-5),
(0.,1.),.UNSPECIFIED.)
GEOMETRIC_REPRESENTATION_ITEM()
RATIONAL_B_SPLINE_SURFACE(((1.,0.81671562114205,1.),(1.,0.815907587407942,
1.),(1.,0.815115959345204,1.),(1.,0.814339887349196,1.)))
REPRESENTATION_ITEM('')
SURFACE()
);
#2747=(
BOUNDED_SURFACE()
B_SPLINE_SURFACE(3,2,((#392848,#392849,#392850),(#392851,#392852,#392853),
(#392854,#392855,#392856),(#392857,#392858,#392859)),.UNSPECIFIED.,.F.,
 .F.,.F.)
B_SPLINE_SURFACE_WITH_KNOTS((4,4),(3,3),(-4.67562186884374E-19,4.68197758448209E-5),
(0.,1.),.UNSPECIFIED.)
GEOMETRIC_REPRESENTATION_ITEM()
RATIONAL_B_SPLINE_SURFACE(((1.,0.816715621142041,1.),(1.,0.953638980025197,
1.),(1.,0.954506925408066,1.),(1.,0.816715621142053,1.)))
REPRESENTATION_ITEM('')
SURFACE()
);
#2748=(
BOUNDED_SURFACE()
B_SPLINE_SURFACE(3,2,((#392861,#392862,#392863),(#392864,#392865,#392866),
(#392867,#392868,#392869),(#392870,#392871,#392872)),.UNSPECIFIED.,.F.,
 .F.,.F.)
B_SPLINE_SURFACE_WITH_KNOTS((4,4),(3,3),(0.,9.54361881492174E-5),(0.,1.),
 .UNSPECIFIED.)
GEOMETRIC_REPRESENTATION_ITEM()
RATIONAL_B_SPLINE_SURFACE(((1.,0.814339887349195,1.),(1.,0.815115959345201,
1.),(1.,0.815907587407948,1.),(1.,0.816715621142047,1.)))
REPRESENTATION_ITEM('')
SURFACE()
);
#2749=(
BOUNDED_SURFACE()
B_SPLINE_SURFACE(3,2,((#392874,#392875,#392876),(#392877,#392878,#392879),
(#392880,#392881,#392882),(#392883,#392884,#392885)),.UNSPECIFIED.,.F.,
 .F.,.F.)
B_SPLINE_SURFACE_WITH_KNOTS((4,4),(3,3),(-3.39528393502486E-6,3.73481232852734E-5),
(-0.00165018033326623,1.),.UNSPECIFIED.)
GEOMETRIC_REPRESENTATION_ITEM()
RATIONAL_B_SPLINE_SURFACE(((1.00048354385565,0.853487571660407,1.),(1.0004711051092,
0.857256476851465,1.),(1.00053193201107,0.838826096655872,1.),(1.00063970687725,
0.806170615310097,1.)))
REPRESENTATION_ITEM('')
SURFACE()
);
#2750=(
BOUNDED_SURFACE()
B_SPLINE_SURFACE(3,2,((#392889,#392890,#392891),(#392892,#392893,#392894),
(#392895,#392896,#392897),(#392898,#392899,#392900)),.UNSPECIFIED.,.F.,
 .F.,.F.)
B_SPLINE_SURFACE_WITH_KNOTS((4,4),(3,3),(2.02993869230514E-5,5.39756952687133E-5),
(-0.000116281069893436,1.),.UNSPECIFIED.)
GEOMETRIC_REPRESENTATION_ITEM()
RATIONAL_B_SPLINE_SURFACE(((1.00001770479729,0.923870681143013,1.),(1.00001014104059,
0.956394275543435,1.),(1.00002037300278,0.912397594905628,1.),(1.00003390859468,
0.85419555086974,1.)))
REPRESENTATION_ITEM('')
SURFACE()
);
#2751=(
BOUNDED_SURFACE()
B_SPLINE_SURFACE(3,2,((#392993,#392994,#392995),(#392996,#392997,#392998),
(#392999,#393000,#393001),(#393002,#393003,#393004)),.UNSPECIFIED.,.F.,
 .F.,.F.)
B_SPLINE_SURFACE_WITH_KNOTS((4,4),(3,3),(0.00135801595889393,0.00148409170619832),
(0.,1.),.UNSPECIFIED.)
GEOMETRIC_REPRESENTATION_ITEM()
RATIONAL_B_SPLINE_SURFACE(((1.,0.818301933966445,1.),(1.,0.817226613172342,
1.),(1.,0.816179643373954,1.),(1.,0.815159387863652,1.)))
REPRESENTATION_ITEM('')
SURFACE()
);
#2752=(
BOUNDED_SURFACE()
B_SPLINE_SURFACE(3,2,((#393043,#393044,#393045),(#393046,#393047,#393048),
(#393049,#393050,#393051),(#393052,#393053,#393054)),.UNSPECIFIED.,.F.,
 .F.,.F.)
B_SPLINE_SURFACE_WITH_KNOTS((4,4),(3,3),(-1.54744435122082E-6,1.54744435122082E-5),
(-0.015169898361537,1.01516989836005),.UNSPECIFIED.)
GEOMETRIC_REPRESENTATION_ITEM()
RATIONAL_B_SPLINE_SURFACE(((1.02018382472877,0.324498219414025,1.02018382472676),
(1.00401234488809,0.865716921710696,1.00401234488769),(1.00033622856779,
0.988747276629713,1.00033622856776),(1.,1.,1.)))
REPRESENTATION_ITEM('')
SURFACE()
);
#2753=(
BOUNDED_SURFACE()
B_SPLINE_SURFACE(3,2,((#393056,#393057,#393058),(#393059,#393060,#393061),
(#393062,#393063,#393064),(#393065,#393066,#393067)),.UNSPECIFIED.,.F.,
 .F.,.F.)
B_SPLINE_SURFACE_WITH_KNOTS((4,4),(3,3),(0.00137194782501028,0.00149814269699235),
(0.,1.),.UNSPECIFIED.)
GEOMETRIC_REPRESENTATION_ITEM()
RATIONAL_B_SPLINE_SURFACE(((1.,0.815158509402316,1.),(1.,0.816179044148173,
1.),(1.,0.817226308119922,1.),(1.,0.818301939488805,1.)))
REPRESENTATION_ITEM('')
SURFACE()
);
#2754=(
BOUNDED_SURFACE()
B_SPLINE_SURFACE(3,2,((#393111,#393112,#393113),(#393114,#393115,#393116),
(#393117,#393118,#393119),(#393120,#393121,#393122)),.UNSPECIFIED.,.F.,
 .F.,.F.)
B_SPLINE_SURFACE_WITH_KNOTS((4,4),(3,3),(1.55009486301137E-5,4.92065510474434E-5),
(-8.13759516301738E-5,1.),.UNSPECIFIED.)
GEOMETRIC_REPRESENTATION_ITEM()
RATIONAL_B_SPLINE_SURFACE(((1.0000237291234,0.854200639599662,1.),(1.00001423585996,
0.912530301180526,1.),(1.00000710550472,0.956341495377425,1.),(1.00001238975911,
0.92387333813701,1.)))
REPRESENTATION_ITEM('')
SURFACE()
);
#2755=(
BOUNDED_SURFACE()
B_SPLINE_SURFACE(3,2,((#393126,#393127,#393128),(#393129,#393130,#393131),
(#393132,#393133,#393134),(#393135,#393136,#393137)),.UNSPECIFIED.,.F.,
 .F.,.F.)
B_SPLINE_SURFACE_WITH_KNOTS((4,4),(3,3),(-3.39934179457814E-6,3.73927597403564E-5),
(-0.00186004067407364,1.00069373317444),.UNSPECIFIED.)
GEOMETRIC_REPRESENTATION_ITEM()
RATIONAL_B_SPLINE_SURFACE(((1.0007210013605,0.806051963875375,1.00026859642693),
(1.0006004844015,0.838470803558624,1.00022369994497),(1.00053106448791,
0.857144632272406,1.00019783877221),(1.00054515072849,0.853355459539101,
1.00020308635438)))
REPRESENTATION_ITEM('')
SURFACE()
);
#2756=(
BOUNDED_SURFACE()
B_SPLINE_SURFACE(3,2,((#393139,#393140,#393141),(#393142,#393143,#393144),
(#393145,#393146,#393147),(#393148,#393149,#393150)),.UNSPECIFIED.,.F.,
 .F.,.F.)
B_SPLINE_SURFACE_WITH_KNOTS((4,4),(3,3),(1.0842021724855E-19,9.54361881492174E-5),
(0.,1.),.UNSPECIFIED.)
GEOMETRIC_REPRESENTATION_ITEM()
RATIONAL_B_SPLINE_SURFACE(((1.,0.816715621142047,1.),(1.,0.815907587407939,
1.),(1.,0.815115959345212,1.),(1.,0.814339887349189,1.)))
REPRESENTATION_ITEM('')
SURFACE()
);
#2757=(
BOUNDED_SURFACE()
B_SPLINE_SURFACE(3,2,((#393152,#393153,#393154),(#393155,#393156,#393157),
(#393158,#393159,#393160),(#393161,#393162,#393163)),.UNSPECIFIED.,.F.,
 .F.,.F.)
B_SPLINE_SURFACE_WITH_KNOTS((4,4),(3,3),(1.01643953670516E-20,4.68197758448205E-5),
(0.,1.),.UNSPECIFIED.)
GEOMETRIC_REPRESENTATION_ITEM()
RATIONAL_B_SPLINE_SURFACE(((1.,0.816715621142046,1.),(1.,0.953638980025195,
1.),(1.,0.954506925408074,1.),(1.,0.81671562114205,1.)))
REPRESENTATION_ITEM('')
SURFACE()
);
#2758=(
BOUNDED_SURFACE()
B_SPLINE_SURFACE(3,2,((#393165,#393166,#393167),(#393168,#393169,#393170),
(#393171,#393172,#393173),(#393174,#393175,#393176)),.UNSPECIFIED.,.F.,
 .F.,.F.)
B_SPLINE_SURFACE_WITH_KNOTS((4,4),(3,3),(0.,9.54361881492176E-5),(0.,1.),
 .UNSPECIFIED.)
GEOMETRIC_REPRESENTATION_ITEM()
RATIONAL_B_SPLINE_SURFACE(((1.,0.814339887349195,1.),(1.,0.8151159593452,
1.),(1.,0.815907587407945,1.),(1.,0.816715621142046,1.)))
REPRESENTATION_ITEM('')
SURFACE()
);
#2759=(
BOUNDED_SURFACE()
B_SPLINE_SURFACE(3,2,((#393178,#393179,#393180),(#393181,#393182,#393183),
(#393184,#393185,#393186),(#393187,#393188,#393189)),.UNSPECIFIED.,.F.,
 .F.,.F.)
B_SPLINE_SURFACE_WITH_KNOTS((4,4),(3,3),(-3.39528393502486E-6,3.73481232852736E-5),
(-0.00165018033290617,1.),.UNSPECIFIED.)
GEOMETRIC_REPRESENTATION_ITEM()
RATIONAL_B_SPLINE_SURFACE(((1.00048354385554,0.853487571660446,1.),(1.0004711051091,
0.857256476851517,1.),(1.00053193201095,0.838826096655916,1.),(1.00063970687711,
0.806170615310169,1.)))
REPRESENTATION_ITEM('')
SURFACE()
);
#2760=(
BOUNDED_SURFACE()
B_SPLINE_SURFACE(3,2,((#393193,#393194,#393195),(#393196,#393197,#393198),
(#393199,#393200,#393201),(#393202,#393203,#393204)),.UNSPECIFIED.,.F.,
 .F.,.F.)
B_SPLINE_SURFACE_WITH_KNOTS((4,4),(3,3),(2.02993869230511E-5,5.39756952686905E-5),
(-0.000116281070107644,1.),.UNSPECIFIED.)
GEOMETRIC_REPRESENTATION_ITEM()
RATIONAL_B_SPLINE_SURFACE(((1.00001770479733,0.923870681142993,1.),(1.00001014104061,
0.956394275543421,1.),(1.00002037300282,0.912397594905653,1.),(1.00003390859474,
0.854195550869826,1.)))
REPRESENTATION_ITEM('')
SURFACE()
);
#2761=(
BOUNDED_SURFACE()
B_SPLINE_SURFACE(3,2,((#393297,#393298,#393299),(#393300,#393301,#393302),
(#393303,#393304,#393305),(#393306,#393307,#393308)),.UNSPECIFIED.,.F.,
 .F.,.F.)
B_SPLINE_SURFACE_WITH_KNOTS((4,4),(3,3),(0.00135801595889393,0.00148409170619832),
(0.,1.),.UNSPECIFIED.)
GEOMETRIC_REPRESENTATION_ITEM()
RATIONAL_B_SPLINE_SURFACE(((1.,0.818301933966446,1.),(1.,0.817226613172339,
1.),(1.,0.816179643373962,1.),(1.,0.815159387863655,1.)))
REPRESENTATION_ITEM('')
SURFACE()
);
#2762=(
BOUNDED_SURFACE()
B_SPLINE_SURFACE(3,2,((#393347,#393348,#393349),(#393350,#393351,#393352),
(#393353,#393354,#393355),(#393356,#393357,#393358)),.UNSPECIFIED.,.F.,
 .F.,.F.)
B_SPLINE_SURFACE_WITH_KNOTS((4,4),(3,3),(-1.5474443512208E-6,1.54744435122079E-5),
(-0.0151698983606426,1.01516989836206),.UNSPECIFIED.)
GEOMETRIC_REPRESENTATION_ITEM()
RATIONAL_B_SPLINE_SURFACE(((1.02018382472757,0.32449821941319,1.02018382472948),
(1.00401234488785,0.865716921710622,1.00401234488823),(1.00033622856777,
0.988747276629658,1.00033622856781),(1.,1.,1.)))
REPRESENTATION_ITEM('')
SURFACE()
);
#2763=(
BOUNDED_SURFACE()
B_SPLINE_SURFACE(3,2,((#393360,#393361,#393362),(#393363,#393364,#393365),
(#393366,#393367,#393368),(#393369,#393370,#393371)),.UNSPECIFIED.,.F.,
 .F.,.F.)
B_SPLINE_SURFACE_WITH_KNOTS((4,4),(3,3),(0.00137194782501028,0.00149814269699235),
(0.,1.),.UNSPECIFIED.)
GEOMETRIC_REPRESENTATION_ITEM()
RATIONAL_B_SPLINE_SURFACE(((1.,0.815158509402323,1.),(1.,0.816179044148176,
1.),(1.,0.817226308119921,1.),(1.,0.818301939488808,1.)))
REPRESENTATION_ITEM('')
SURFACE()
);
#2764=(
BOUNDED_SURFACE()
B_SPLINE_SURFACE(3,2,((#393415,#393416,#393417),(#393418,#393419,#393420),
(#393421,#393422,#393423),(#393424,#393425,#393426)),.UNSPECIFIED.,.F.,
 .F.,.F.)
B_SPLINE_SURFACE_WITH_KNOTS((4,4),(3,3),(1.55009486301137E-5,4.92065510474429E-5),
(-8.13759515703415E-5,1.),.UNSPECIFIED.)
GEOMETRIC_REPRESENTATION_ITEM()
RATIONAL_B_SPLINE_SURFACE(((1.00002372912338,0.854200639599671,1.),(1.00001423585995,
0.912530301180536,1.),(1.00000710550472,0.956341495377421,1.),(1.0000123897591,
0.923873338137016,1.)))
REPRESENTATION_ITEM('')
SURFACE()
);
#2765=(
BOUNDED_SURFACE()
B_SPLINE_SURFACE(3,2,((#393430,#393431,#393432),(#393433,#393434,#393435),
(#393436,#393437,#393438),(#393439,#393440,#393441)),.UNSPECIFIED.,.F.,
 .F.,.F.)
B_SPLINE_SURFACE_WITH_KNOTS((4,4),(3,3),(-3.39934179457827E-6,3.73927597403564E-5),
(-0.00186004067416749,1.00069373317441),.UNSPECIFIED.)
GEOMETRIC_REPRESENTATION_ITEM()
RATIONAL_B_SPLINE_SURFACE(((1.00072100136054,0.806051963875334,1.00026859642691),
(1.00060048440153,0.838470803558673,1.00022369994496),(1.00053106448794,
0.857144632272363,1.0001978387722),(1.00054515072852,0.853355459539107,
1.00020308635437)))
REPRESENTATION_ITEM('')
SURFACE()
);
#2766=(
BOUNDED_SURFACE()
B_SPLINE_SURFACE(3,2,((#393443,#393444,#393445),(#393446,#393447,#393448),
(#393449,#393450,#393451),(#393452,#393453,#393454)),.UNSPECIFIED.,.F.,
 .F.,.F.)
B_SPLINE_SURFACE_WITH_KNOTS((4,4),(3,3),(5.42101086242752E-20,9.54361881492173E-5),
(0.,1.),.UNSPECIFIED.)
GEOMETRIC_REPRESENTATION_ITEM()
RATIONAL_B_SPLINE_SURFACE(((1.,0.816715621142053,1.),(1.,0.815907587407943,
1.),(1.,0.815115959345204,1.),(1.,0.814339887349193,1.)))
REPRESENTATION_ITEM('')
SURFACE()
);
#2767=(
BOUNDED_SURFACE()
B_SPLINE_SURFACE(3,2,((#393456,#393457,#393458),(#393459,#393460,#393461),
(#393462,#393463,#393464),(#393465,#393466,#393467)),.UNSPECIFIED.,.F.,
 .F.,.F.)
B_SPLINE_SURFACE_WITH_KNOTS((4,4),(3,3),(-7.45388993583784E-20,4.68197758448203E-5),
(0.,1.),.UNSPECIFIED.)
GEOMETRIC_REPRESENTATION_ITEM()
RATIONAL_B_SPLINE_SURFACE(((1.,0.816715621142046,1.),(1.,0.953638980025215,
1.),(1.,0.954506925408046,1.),(1.,0.816715621142056,1.)))
REPRESENTATION_ITEM('')
SURFACE()
);
#2768=(
BOUNDED_SURFACE()
B_SPLINE_SURFACE(3,2,((#393469,#393470,#393471),(#393472,#393473,#393474),
(#393475,#393476,#393477),(#393478,#393479,#393480)),.UNSPECIFIED.,.F.,
 .F.,.F.)
B_SPLINE_SURFACE_WITH_KNOTS((4,4),(3,3),(-1.0842021724855E-19,9.54361881492176E-5),
(0.,1.),.UNSPECIFIED.)
GEOMETRIC_REPRESENTATION_ITEM()
RATIONAL_B_SPLINE_SURFACE(((1.,0.814339887349194,1.),(1.,0.815115959345214,
1.),(1.,0.81590758740794,1.),(1.,0.816715621142046,1.)))
REPRESENTATION_ITEM('')
SURFACE()
);
#2769=(
BOUNDED_SURFACE()
B_SPLINE_SURFACE(3,2,((#393482,#393483,#393484),(#393485,#393486,#393487),
(#393488,#393489,#393490),(#393491,#393492,#393493)),.UNSPECIFIED.,.F.,
 .F.,.F.)
B_SPLINE_SURFACE_WITH_KNOTS((4,4),(3,3),(-3.39528393502488E-6,3.73481232852734E-5),
(-0.00165018033329553,1.),.UNSPECIFIED.)
GEOMETRIC_REPRESENTATION_ITEM()
RATIONAL_B_SPLINE_SURFACE(((1.00048354385566,0.85348757166039,1.),(1.00047110510921,
0.857256476851485,1.),(1.00053193201108,0.838826096655847,1.),(1.00063970687726,
0.8061706153101,1.)))
REPRESENTATION_ITEM('')
SURFACE()
);
#2770=(
BOUNDED_SURFACE()
B_SPLINE_SURFACE(3,2,((#393497,#393498,#393499),(#393500,#393501,#393502),
(#393503,#393504,#393505),(#393506,#393507,#393508)),.UNSPECIFIED.,.F.,
 .F.,.F.)
B_SPLINE_SURFACE_WITH_KNOTS((4,4),(3,3),(2.02993869230509E-5,5.39756952686905E-5),
(-0.000116281069641126,1.),.UNSPECIFIED.)
GEOMETRIC_REPRESENTATION_ITEM()
RATIONAL_B_SPLINE_SURFACE(((1.00001770479726,0.923870681143033,1.),(1.00001014104056,
0.95639427554342,1.),(1.00002037300274,0.912397594905708,1.),(1.00003390859461,
0.854195550869891,1.)))
REPRESENTATION_ITEM('')
SURFACE()
);
#2771=(
BOUNDED_SURFACE()
B_SPLINE_SURFACE(3,2,((#393601,#393602,#393603),(#393604,#393605,#393606),
(#393607,#393608,#393609),(#393610,#393611,#393612)),.UNSPECIFIED.,.F.,
 .F.,.F.)
B_SPLINE_SURFACE_WITH_KNOTS((4,4),(3,3),(0.00135801595889393,0.00148409170619832),
(0.,1.),.UNSPECIFIED.)
GEOMETRIC_REPRESENTATION_ITEM()
RATIONAL_B_SPLINE_SURFACE(((1.,0.818301933966445,1.),(1.,0.817226613172349,
1.),(1.,0.816179643373947,1.),(1.,0.815159387863652,1.)))
REPRESENTATION_ITEM('')
SURFACE()
);
#2772=(
BOUNDED_SURFACE()
B_SPLINE_SURFACE(3,2,((#393651,#393652,#393653),(#393654,#393655,#393656),
(#393657,#393658,#393659),(#393660,#393661,#393662)),.UNSPECIFIED.,.F.,
 .F.,.F.)
B_SPLINE_SURFACE_WITH_KNOTS((4,4),(3,3),(-1.54744435122075E-6,1.54744435122076E-5),
(-0.0151698983615748,1.),.UNSPECIFIED.)
GEOMETRIC_REPRESENTATION_ITEM()
RATIONAL_B_SPLINE_SURFACE(((1.02018382472883,0.334740937356857,1.),(1.0040123448881,
0.867753072813479,1.),(1.00033622856779,0.988917903080847,1.),(1.,1.,1.)))
REPRESENTATION_ITEM('')
SURFACE()
);
#2773=(
BOUNDED_SURFACE()
B_SPLINE_SURFACE(3,2,((#393664,#393665,#393666),(#393667,#393668,#393669),
(#393670,#393671,#393672),(#393673,#393674,#393675)),.UNSPECIFIED.,.F.,
 .F.,.F.)
B_SPLINE_SURFACE_WITH_KNOTS((4,4),(3,3),(0.00137194782501028,0.00149814269699235),
(0.,1.),.UNSPECIFIED.)
GEOMETRIC_REPRESENTATION_ITEM()
RATIONAL_B_SPLINE_SURFACE(((1.,0.815158509402314,1.),(1.,0.816179044148167,
1.),(1.,0.817226308119939,1.),(1.,0.818301939488801,1.)))
REPRESENTATION_ITEM('')
SURFACE()
);
#2774=(
BOUNDED_SURFACE()
B_SPLINE_SURFACE(3,2,((#393719,#393720,#393721),(#393722,#393723,#393724),
(#393725,#393726,#393727),(#393728,#393729,#393730)),.UNSPECIFIED.,.F.,
 .F.,.F.)
B_SPLINE_SURFACE_WITH_KNOTS((4,4),(3,3),(1.55009486301137E-5,4.92065510474427E-5),
(-8.1375951387387E-5,1.),.UNSPECIFIED.)
GEOMETRIC_REPRESENTATION_ITEM()
RATIONAL_B_SPLINE_SURFACE(((1.00002372912333,0.854200639599705,1.),(1.00001423585992,
0.912530301180535,1.),(1.0000071055047,0.95634149537744,1.),(1.00001238975907,
0.923873338137029,1.)))
REPRESENTATION_ITEM('')
SURFACE()
);
#2775=(
BOUNDED_SURFACE()
B_SPLINE_SURFACE(3,2,((#393734,#393735,#393736),(#393737,#393738,#393739),
(#393740,#393741,#393742),(#393743,#393744,#393745)),.UNSPECIFIED.,.F.,
 .F.,.F.)
B_SPLINE_SURFACE_WITH_KNOTS((4,4),(3,3),(-3.39934179457817E-6,3.73927597403564E-5),
(-0.00186004067389001,1.00069373317438),.UNSPECIFIED.)
GEOMETRIC_REPRESENTATION_ITEM()
RATIONAL_B_SPLINE_SURFACE(((1.00072100136043,0.806051963875405,1.0002685964269),
(1.00060048440144,0.838470803558679,1.00022369994495),(1.00053106448786,
0.857144632272429,1.00019783877219),(1.00054515072844,0.853355459539144,
1.00020308635436)))
REPRESENTATION_ITEM('')
SURFACE()
);
#2776=(
BOUNDED_SURFACE()
B_SPLINE_SURFACE(3,2,((#393747,#393748,#393749),(#393750,#393751,#393752),
(#393753,#393754,#393755),(#393756,#393757,#393758)),.UNSPECIFIED.,.F.,
 .F.,.F.)
B_SPLINE_SURFACE_WITH_KNOTS((4,4),(3,3),(5.42101086242752E-20,9.54361881492175E-5),
(0.,1.),.UNSPECIFIED.)
GEOMETRIC_REPRESENTATION_ITEM()
RATIONAL_B_SPLINE_SURFACE(((1.,0.816715621142047,1.),(1.,0.815907587407949,
1.),(1.,0.8151159593452,1.),(1.,0.814339887349195,1.)))
REPRESENTATION_ITEM('')
SURFACE()
);
#2777=(
BOUNDED_SURFACE()
B_SPLINE_SURFACE(3,2,((#393760,#393761,#393762),(#393763,#393764,#393765),
(#393766,#393767,#393768),(#393769,#393770,#393771)),.UNSPECIFIED.,.F.,
 .F.,.F.)
B_SPLINE_SURFACE_WITH_KNOTS((4,4),(3,3),(3.55753837846806E-20,4.68197758448214E-5),
(0.,1.),.UNSPECIFIED.)
GEOMETRIC_REPRESENTATION_ITEM()
RATIONAL_B_SPLINE_SURFACE(((1.,0.816715621142045,1.),(1.,0.953638980025214,
1.),(1.,0.954506925408051,1.),(1.,0.816715621142053,1.)))
REPRESENTATION_ITEM('')
SURFACE()
);
#2778=(
BOUNDED_SURFACE()
B_SPLINE_SURFACE(3,2,((#393773,#393774,#393775),(#393776,#393777,#393778),
(#393779,#393780,#393781),(#393782,#393783,#393784)),.UNSPECIFIED.,.F.,
 .F.,.F.)
B_SPLINE_SURFACE_WITH_KNOTS((4,4),(3,3),(1.62630325872826E-19,9.54361881492177E-5),
(0.,1.),.UNSPECIFIED.)
GEOMETRIC_REPRESENTATION_ITEM()
RATIONAL_B_SPLINE_SURFACE(((1.,0.814339887349193,1.),(1.,0.81511595934521,
1.),(1.,0.815907587407938,1.),(1.,0.816715621142048,1.)))
REPRESENTATION_ITEM('')
SURFACE()
);
#2779=(
BOUNDED_SURFACE()
B_SPLINE_SURFACE(3,2,((#393786,#393787,#393788),(#393789,#393790,#393791),
(#393792,#393793,#393794),(#393795,#393796,#393797)),.UNSPECIFIED.,.F.,
 .F.,.F.)
B_SPLINE_SURFACE_WITH_KNOTS((4,4),(3,3),(-3.39528393502492E-6,3.73481232852736E-5),
(-0.00165018033285678,1.),.UNSPECIFIED.)
GEOMETRIC_REPRESENTATION_ITEM()
RATIONAL_B_SPLINE_SURFACE(((1.00048354385553,0.85348757166045,1.),(1.00047110510908,
0.857256476851541,1.),(1.00053193201094,0.838826096655928,1.),(1.00063970687709,
0.806170615310183,1.)))
REPRESENTATION_ITEM('')
SURFACE()
);
#2780=(
BOUNDED_SURFACE()
B_SPLINE_SURFACE(3,2,((#393801,#393802,#393803),(#393804,#393805,#393806),
(#393807,#393808,#393809),(#393810,#393811,#393812)),.UNSPECIFIED.,.F.,
 .F.,.F.)
B_SPLINE_SURFACE_WITH_KNOTS((4,4),(3,3),(2.02993869230514E-5,5.39756952686908E-5),
(-0.000116281069724157,1.),.UNSPECIFIED.)
GEOMETRIC_REPRESENTATION_ITEM()
RATIONAL_B_SPLINE_SURFACE(((1.00001770479727,0.923870681143026,1.),(1.00001014104057,
0.95639427554342,1.),(1.00002037300275,0.912397594905702,1.),(1.00003390859463,
0.854195550869877,1.)))
REPRESENTATION_ITEM('')
SURFACE()
);
#2781=(
BOUNDED_SURFACE()
B_SPLINE_SURFACE(3,2,((#393905,#393906,#393907),(#393908,#393909,#393910),
(#393911,#393912,#393913),(#393914,#393915,#393916)),.UNSPECIFIED.,.F.,
 .F.,.F.)
B_SPLINE_SURFACE_WITH_KNOTS((4,4),(3,3),(0.00135801595889393,0.00148409170619832),
(0.,1.),.UNSPECIFIED.)
GEOMETRIC_REPRESENTATION_ITEM()
RATIONAL_B_SPLINE_SURFACE(((1.,0.818301933966443,1.),(1.,0.817226613172343,
1.),(1.,0.816179643373959,1.),(1.,0.815159387863654,1.)))
REPRESENTATION_ITEM('')
SURFACE()
);
#2782=(
BOUNDED_SURFACE()
B_SPLINE_SURFACE(3,2,((#393955,#393956,#393957),(#393958,#393959,#393960),
(#393961,#393962,#393963),(#393964,#393965,#393966)),.UNSPECIFIED.,.F.,
 .F.,.F.)
B_SPLINE_SURFACE_WITH_KNOTS((4,4),(3,3),(-1.54744435122069E-6,1.54744435122075E-5),
(-0.0151698983646716,1.01516989835781),.UNSPECIFIED.)
GEOMETRIC_REPRESENTATION_ITEM()
RATIONAL_B_SPLINE_SURFACE(((1.02018382473301,0.324498219413436,1.02018382472374),
(1.00401234488893,0.865716921710573,1.00401234488709),(1.00033622856786,
0.988747276629695,1.00033622856771),(1.,1.,1.)))
REPRESENTATION_ITEM('')
SURFACE()
);
#2783=(
BOUNDED_SURFACE()
B_SPLINE_SURFACE(3,2,((#393968,#393969,#393970),(#393971,#393972,#393973),
(#393974,#393975,#393976),(#393977,#393978,#393979)),.UNSPECIFIED.,.F.,
 .F.,.F.)
B_SPLINE_SURFACE_WITH_KNOTS((4,4),(3,3),(0.00137194782501028,0.00149814269699235),
(0.,1.),.UNSPECIFIED.)
GEOMETRIC_REPRESENTATION_ITEM()
RATIONAL_B_SPLINE_SURFACE(((1.,0.815158509402317,1.),(1.,0.816179044148163,
1.),(1.,0.817226308119931,1.),(1.,0.818301939488807,1.)))
REPRESENTATION_ITEM('')
SURFACE()
);
#2784=(
BOUNDED_SURFACE()
B_SPLINE_SURFACE(3,2,((#394023,#394024,#394025),(#394026,#394027,#394028),
(#394029,#394030,#394031),(#394032,#394033,#394034)),.UNSPECIFIED.,.F.,
 .F.,.F.)
B_SPLINE_SURFACE_WITH_KNOTS((4,4),(3,3),(1.55009486301137E-5,4.92065510474434E-5),
(-8.13759515344749E-5,1.),.UNSPECIFIED.)
GEOMETRIC_REPRESENTATION_ITEM()
RATIONAL_B_SPLINE_SURFACE(((1.00002372912337,0.854200639599674,1.),(1.00001423585994,
0.912530301180545,1.),(1.00000710550471,0.956341495377423,1.),(1.00001238975909,
0.92387333813702,1.)))
REPRESENTATION_ITEM('')
SURFACE()
);
#2785=(
BOUNDED_SURFACE()
B_SPLINE_SURFACE(3,2,((#394038,#394039,#394040),(#394041,#394042,#394043),
(#394044,#394045,#394046),(#394047,#394048,#394049)),.UNSPECIFIED.,.F.,
 .F.,.F.)
B_SPLINE_SURFACE_WITH_KNOTS((4,4),(3,3),(-3.39934179457785E-6,3.73927597403566E-5),
(-0.00186004067389604,1.00069373317456),.UNSPECIFIED.)
GEOMETRIC_REPRESENTATION_ITEM()
RATIONAL_B_SPLINE_SURFACE(((1.00072100136043,0.80605196387536,1.00026859642697),
(1.00060048440145,0.838470803558678,1.00022369994501),(1.00053106448786,
0.857144632272387,1.00019783877224),(1.00054515072844,0.853355459539119,
1.00020308635442)))
REPRESENTATION_ITEM('')
SURFACE()
);
#2786=(
BOUNDED_SURFACE()
B_SPLINE_SURFACE(3,2,((#394051,#394052,#394053),(#394054,#394055,#394056),
(#394057,#394058,#394059),(#394060,#394061,#394062)),.UNSPECIFIED.,.F.,
 .F.,.F.)
B_SPLINE_SURFACE_WITH_KNOTS((4,4),(3,3),(-5.42101086242752E-20,9.54361881492175E-5),
(0.,1.),.UNSPECIFIED.)
GEOMETRIC_REPRESENTATION_ITEM()
RATIONAL_B_SPLINE_SURFACE(((1.,0.81671562114205,1.),(1.,0.815907587407957,
1.),(1.,0.815115959345192,1.),(1.,0.814339887349193,1.)))
REPRESENTATION_ITEM('')
SURFACE()
);
#2787=(
BOUNDED_SURFACE()
B_SPLINE_SURFACE(3,2,((#394064,#394065,#394066),(#394067,#394068,#394069),
(#394070,#394071,#394072),(#394073,#394074,#394075)),.UNSPECIFIED.,.F.,
 .F.,.F.)
B_SPLINE_SURFACE_WITH_KNOTS((4,4),(3,3),(2.79520872593919E-19,4.68197758448212E-5),
(0.,1.),.UNSPECIFIED.)
GEOMETRIC_REPRESENTATION_ITEM()
RATIONAL_B_SPLINE_SURFACE(((1.,0.81671562114205,1.),(1.,0.953638980025211,
1.),(1.,0.954506925408057,1.),(1.,0.81671562114205,1.)))
REPRESENTATION_ITEM('')
SURFACE()
);
#2788=(
BOUNDED_SURFACE()
B_SPLINE_SURFACE(3,2,((#394077,#394078,#394079),(#394080,#394081,#394082),
(#394083,#394084,#394085),(#394086,#394087,#394088)),.UNSPECIFIED.,.F.,
 .F.,.F.)
B_SPLINE_SURFACE_WITH_KNOTS((4,4),(3,3),(0.,9.54361881492179E-5),(0.,1.),
 .UNSPECIFIED.)
GEOMETRIC_REPRESENTATION_ITEM()
RATIONAL_B_SPLINE_SURFACE(((1.,0.814339887349193,1.),(1.,0.815115959345207,
1.),(1.,0.815907587407936,1.),(1.,0.81671562114205,1.)))
REPRESENTATION_ITEM('')
SURFACE()
);
#2789=(
BOUNDED_SURFACE()
B_SPLINE_SURFACE(3,2,((#394090,#394091,#394092),(#394093,#394094,#394095),
(#394096,#394097,#394098),(#394099,#394100,#394101)),.UNSPECIFIED.,.F.,
 .F.,.F.)
B_SPLINE_SURFACE_WITH_KNOTS((4,4),(3,3),(-3.39528393502486E-6,3.73481232852728E-5),
(-0.00165018033346268,1.),.UNSPECIFIED.)
GEOMETRIC_REPRESENTATION_ITEM()
RATIONAL_B_SPLINE_SURFACE(((1.00048354385571,0.853487571660363,1.),(1.00047110510926,
0.857256476851452,1.),(1.00053193201113,0.838826096655833,1.),(1.00063970687733,
0.80617061531006,1.)))
REPRESENTATION_ITEM('')
SURFACE()
);
#2790=(
BOUNDED_SURFACE()
B_SPLINE_SURFACE(3,2,((#394105,#394106,#394107),(#394108,#394109,#394110),
(#394111,#394112,#394113),(#394114,#394115,#394116)),.UNSPECIFIED.,.F.,
 .F.,.F.)
B_SPLINE_SURFACE_WITH_KNOTS((4,4),(3,3),(2.02993869230509E-5,5.39756952686905E-5),
(-0.000116281070001636,1.),.UNSPECIFIED.)
GEOMETRIC_REPRESENTATION_ITEM()
RATIONAL_B_SPLINE_SURFACE(((1.00001770479731,0.923870681143004,1.),(1.0000101410406,
0.956394275543415,1.),(1.0000203730028,0.912397594905674,1.),(1.00003390859471,
0.854195550869838,1.)))
REPRESENTATION_ITEM('')
SURFACE()
);
#2791=(
BOUNDED_SURFACE()
B_SPLINE_SURFACE(3,2,((#394209,#394210,#394211),(#394212,#394213,#394214),
(#394215,#394216,#394217),(#394218,#394219,#394220)),.UNSPECIFIED.,.F.,
 .F.,.F.)
B_SPLINE_SURFACE_WITH_KNOTS((4,4),(3,3),(0.00135801595889393,0.00148409170619832),
(0.,1.),.UNSPECIFIED.)
GEOMETRIC_REPRESENTATION_ITEM()
RATIONAL_B_SPLINE_SURFACE(((1.,0.818301933966442,1.),(1.,0.817226613172347,
1.),(1.,0.816179643373947,1.),(1.,0.815159387863655,1.)))
REPRESENTATION_ITEM('')
SURFACE()
);
#2792=(
BOUNDED_SURFACE()
B_SPLINE_SURFACE(3,2,((#394259,#394260,#394261),(#394262,#394263,#394264),
(#394265,#394266,#394267),(#394268,#394269,#394270)),.UNSPECIFIED.,.F.,
 .F.,.F.)
B_SPLINE_SURFACE_WITH_KNOTS((4,4),(3,3),(3.43048343637992E-20,1.54744435122082E-5),
(0.,1.),.UNSPECIFIED.)
GEOMETRIC_REPRESENTATION_ITEM()
RATIONAL_B_SPLINE_SURFACE(((1.,0.478041569704948,1.),(1.,0.890533857552087,
1.),(1.,0.990075913815913,1.),(1.,1.,1.)))
REPRESENTATION_ITEM('')
SURFACE()
);
#2793=(
BOUNDED_SURFACE()
B_SPLINE_SURFACE(3,2,((#394272,#394273,#394274),(#394275,#394276,#394277),
(#394278,#394279,#394280),(#394281,#394282,#394283)),.UNSPECIFIED.,.F.,
 .F.,.F.)
B_SPLINE_SURFACE_WITH_KNOTS((4,4),(3,3),(0.00137194782501028,0.00149814269699235),
(0.,1.),.UNSPECIFIED.)
GEOMETRIC_REPRESENTATION_ITEM()
RATIONAL_B_SPLINE_SURFACE(((1.,0.815158509402316,1.),(1.,0.816179044148169,
1.),(1.,0.817226308119927,1.),(1.,0.818301939488802,1.)))
REPRESENTATION_ITEM('')
SURFACE()
);
#2794=(
BOUNDED_SURFACE()
B_SPLINE_SURFACE(3,2,((#394327,#394328,#394329),(#394330,#394331,#394332),
(#394333,#394334,#394335),(#394336,#394337,#394338)),.UNSPECIFIED.,.F.,
 .F.,.F.)
B_SPLINE_SURFACE_WITH_KNOTS((4,4),(3,3),(1.55009486301137E-5,4.92065510474435E-5),
(-8.1375951522669E-5,1.),.UNSPECIFIED.)
GEOMETRIC_REPRESENTATION_ITEM()
RATIONAL_B_SPLINE_SURFACE(((1.00002372912337,0.854200639599685,1.),(1.00001423585994,
0.912530301180533,1.),(1.00000710550471,0.956341495377427,1.),(1.00001238975909,
0.92387333813702,1.)))
REPRESENTATION_ITEM('')
SURFACE()
);
#2795=(
BOUNDED_SURFACE()
B_SPLINE_SURFACE(3,2,((#394342,#394343,#394344),(#394345,#394346,#394347),
(#394348,#394349,#394350),(#394351,#394352,#394353)),.UNSPECIFIED.,.F.,
 .F.,.F.)
B_SPLINE_SURFACE_WITH_KNOTS((4,4),(3,3),(-3.39934179457797E-6,3.73927597403568E-5),
(-0.00186004067438382,1.00069373317431),.UNSPECIFIED.)
GEOMETRIC_REPRESENTATION_ITEM()
RATIONAL_B_SPLINE_SURFACE(((1.00072100136062,0.806051963875329,1.00026859642688),
(1.0006004844016,0.83847080355862,1.00022369994493),(1.000531064488,0.857144632272351,
1.00019783877217),(1.00054515072858,0.85335545953909,1.00020308635434)))
REPRESENTATION_ITEM('')
SURFACE()
);
#2796=(
BOUNDED_SURFACE()
B_SPLINE_SURFACE(3,2,((#394355,#394356,#394357),(#394358,#394359,#394360),
(#394361,#394362,#394363),(#394364,#394365,#394366)),.UNSPECIFIED.,.F.,
 .F.,.F.)
B_SPLINE_SURFACE_WITH_KNOTS((4,4),(3,3),(-2.71050543121376E-19,9.54361881492169E-5),
(0.,1.),.UNSPECIFIED.)
GEOMETRIC_REPRESENTATION_ITEM()
RATIONAL_B_SPLINE_SURFACE(((1.,0.81671562114205,1.),(1.,0.815907587407938,
1.),(1.,0.81511595934521,1.),(1.,0.814339887349194,1.)))
REPRESENTATION_ITEM('')
SURFACE()
);
#2797=(
BOUNDED_SURFACE()
B_SPLINE_SURFACE(3,2,((#394368,#394369,#394370),(#394371,#394372,#394373),
(#394374,#394375,#394376),(#394377,#394378,#394379)),.UNSPECIFIED.,.F.,
 .F.,.F.)
B_SPLINE_SURFACE_WITH_KNOTS((4,4),(3,3),(-2.37169225231204E-20,4.68197758448205E-5),
(0.,1.),.UNSPECIFIED.)
GEOMETRIC_REPRESENTATION_ITEM()
RATIONAL_B_SPLINE_SURFACE(((1.,0.816715621142046,1.),(1.,0.953638980025212,
1.),(1.,0.954506925408045,1.),(1.,0.816715621142057,1.)))
REPRESENTATION_ITEM('')
SURFACE()
);
#2798=(
BOUNDED_SURFACE()
B_SPLINE_SURFACE(3,2,((#394381,#394382,#394383),(#394384,#394385,#394386),
(#394387,#394388,#394389),(#394390,#394391,#394392)),.UNSPECIFIED.,.F.,
 .F.,.F.)
B_SPLINE_SURFACE_WITH_KNOTS((4,4),(3,3),(1.62630325872826E-19,9.54361881492178E-5),
(0.,1.),.UNSPECIFIED.)
GEOMETRIC_REPRESENTATION_ITEM()
RATIONAL_B_SPLINE_SURFACE(((1.,0.814339887349195,1.),(1.,0.815115959345209,
1.),(1.,0.81590758740794,1.),(1.,0.816715621142049,1.)))
REPRESENTATION_ITEM('')
SURFACE()
);
#2799=(
BOUNDED_SURFACE()
B_SPLINE_SURFACE(3,2,((#394394,#394395,#394396),(#394397,#394398,#394399),
(#394400,#394401,#394402),(#394403,#394404,#394405)),.UNSPECIFIED.,.F.,
 .F.,.F.)
B_SPLINE_SURFACE_WITH_KNOTS((4,4),(3,3),(-3.39528393502483E-6,3.73481232852736E-5),
(-0.00165018033284259,1.),.UNSPECIFIED.)
GEOMETRIC_REPRESENTATION_ITEM()
RATIONAL_B_SPLINE_SURFACE(((1.00048354385553,0.853487571660465,1.),(1.00047110510908,
0.857256476851521,1.),(1.00053193201093,0.838826096655951,1.),(1.00063970687708,
0.806170615310176,1.)))
REPRESENTATION_ITEM('')
SURFACE()
);
#2800=(
BOUNDED_SURFACE()
B_SPLINE_SURFACE(3,2,((#394409,#394410,#394411),(#394412,#394413,#394414),
(#394415,#394416,#394417),(#394418,#394419,#394420)),.UNSPECIFIED.,.F.,
 .F.,.F.)
B_SPLINE_SURFACE_WITH_KNOTS((4,4),(3,3),(2.02993869230506E-5,5.39756952686903E-5),
(-0.000116281070056919,1.),.UNSPECIFIED.)
GEOMETRIC_REPRESENTATION_ITEM()
RATIONAL_B_SPLINE_SURFACE(((1.00001770479732,0.923870681142999,1.),(1.0000101410406,
0.95639427554342,1.),(1.00002037300281,0.912397594905655,1.),(1.00003390859473,
0.854195550869835,1.)))
REPRESENTATION_ITEM('')
SURFACE()
);
#2801=(
BOUNDED_SURFACE()
B_SPLINE_SURFACE(3,2,((#394513,#394514,#394515),(#394516,#394517,#394518),
(#394519,#394520,#394521),(#394522,#394523,#394524)),.UNSPECIFIED.,.F.,
 .F.,.F.)
B_SPLINE_SURFACE_WITH_KNOTS((4,4),(3,3),(0.00135801595889393,0.00148409170619832),
(0.,1.),.UNSPECIFIED.)
GEOMETRIC_REPRESENTATION_ITEM()
RATIONAL_B_SPLINE_SURFACE(((1.,0.818301933966447,1.),(1.,0.817226613172351,
1.),(1.,0.816179643373952,1.),(1.,0.815159387863656,1.)))
REPRESENTATION_ITEM('')
SURFACE()
);
#2802=(
BOUNDED_SURFACE()
B_SPLINE_SURFACE(3,2,((#394563,#394564,#394565),(#394566,#394567,#394568),
(#394569,#394570,#394571),(#394572,#394573,#394574)),.UNSPECIFIED.,.F.,
 .F.,.F.)
B_SPLINE_SURFACE_WITH_KNOTS((4,4),(3,3),(-1.54744435122069E-6,1.54744435122074E-5),
(-0.0151698983592225,1.),.UNSPECIFIED.)
GEOMETRIC_REPRESENTATION_ITEM()
RATIONAL_B_SPLINE_SURFACE(((1.02018382472565,0.334740937358353,1.),(1.00401234488747,
0.867753072813766,1.),(1.00033622856774,0.988917903080832,1.),(1.,1.,1.)))
REPRESENTATION_ITEM('')
SURFACE()
);
#2803=(
BOUNDED_SURFACE()
B_SPLINE_SURFACE(3,2,((#394576,#394577,#394578),(#394579,#394580,#394581),
(#394582,#394583,#394584),(#394585,#394586,#394587)),.UNSPECIFIED.,.F.,
 .F.,.F.)
B_SPLINE_SURFACE_WITH_KNOTS((4,4),(3,3),(0.00137194782501028,0.00149814269699235),
(0.,1.),.UNSPECIFIED.)
GEOMETRIC_REPRESENTATION_ITEM()
RATIONAL_B_SPLINE_SURFACE(((1.,0.81515850940232,1.),(1.,0.816179044148164,
1.),(1.,0.817226308119926,1.),(1.,0.818301939488812,1.)))
REPRESENTATION_ITEM('')
SURFACE()
);
#2804=(
BOUNDED_SURFACE()
B_SPLINE_SURFACE(3,2,((#394631,#394632,#394633),(#394634,#394635,#394636),
(#394637,#394638,#394639),(#394640,#394641,#394642)),.UNSPECIFIED.,.F.,
 .F.,.F.)
B_SPLINE_SURFACE_WITH_KNOTS((4,4),(3,3),(1.55009486301137E-5,4.9206551047443E-5),
(-8.13759512517913E-5,1.),.UNSPECIFIED.)
GEOMETRIC_REPRESENTATION_ITEM()
RATIONAL_B_SPLINE_SURFACE(((1.00002372912329,0.85420063959972,1.),(1.00001423585989,
0.912530301180554,1.),(1.00000710550469,0.956341495377446,1.),(1.00001238975905,
0.923873338137039,1.)))
REPRESENTATION_ITEM('')
SURFACE()
);
#2805=(
BOUNDED_SURFACE()
B_SPLINE_SURFACE(3,2,((#394646,#394647,#394648),(#394649,#394650,#394651),
(#394652,#394653,#394654),(#394655,#394656,#394657)),.UNSPECIFIED.,.F.,
 .F.,.F.)
B_SPLINE_SURFACE_WITH_KNOTS((4,4),(3,3),(-3.39934179457793E-6,3.73927597403567E-5),
(-0.00186004067460027,1.00069373317475),.UNSPECIFIED.)
GEOMETRIC_REPRESENTATION_ITEM()
RATIONAL_B_SPLINE_SURFACE(((1.00072100136071,0.806051963875212,1.00026859642704),
(1.00060048440167,0.838470803558519,1.00022369994507),(1.00053106448807,
0.857144632272275,1.00019783877229),(1.00054515072864,0.853355459538997,
1.00020308635447)))
REPRESENTATION_ITEM('')
SURFACE()
);
#2806=(
BOUNDED_SURFACE()
B_SPLINE_SURFACE(3,2,((#394659,#394660,#394661),(#394662,#394663,#394664),
(#394665,#394666,#394667),(#394668,#394669,#394670)),.UNSPECIFIED.,.F.,
 .F.,.F.)
B_SPLINE_SURFACE_WITH_KNOTS((4,4),(3,3),(-1.62630325872826E-19,9.54361881492172E-5),
(0.,1.),.UNSPECIFIED.)
GEOMETRIC_REPRESENTATION_ITEM()
RATIONAL_B_SPLINE_SURFACE(((1.,0.816715621142052,1.),(1.,0.815907587407936,
1.),(1.,0.815115959345212,1.),(1.,0.814339887349197,1.)))
REPRESENTATION_ITEM('')
SURFACE()
);
#2807=(
BOUNDED_SURFACE()
B_SPLINE_SURFACE(3,2,((#394672,#394673,#394674),(#394675,#394676,#394677),
(#394678,#394679,#394680),(#394681,#394682,#394683)),.UNSPECIFIED.,.F.,
 .F.,.F.)
B_SPLINE_SURFACE_WITH_KNOTS((4,4),(3,3),(5.9292306307801E-20,4.68197758448215E-5),
(0.,1.),.UNSPECIFIED.)
GEOMETRIC_REPRESENTATION_ITEM()
RATIONAL_B_SPLINE_SURFACE(((1.,0.816715621142048,1.),(1.,0.953638980025212,
1.),(1.,0.95450692540805,1.),(1.,0.816715621142047,1.)))
REPRESENTATION_ITEM('')
SURFACE()
);
#2808=(
BOUNDED_SURFACE()
B_SPLINE_SURFACE(3,2,((#394685,#394686,#394687),(#394688,#394689,#394690),
(#394691,#394692,#394693),(#394694,#394695,#394696)),.UNSPECIFIED.,.F.,
 .F.,.F.)
B_SPLINE_SURFACE_WITH_KNOTS((4,4),(3,3),(-1.0842021724855E-19,9.54361881492175E-5),
(0.,1.),.UNSPECIFIED.)
GEOMETRIC_REPRESENTATION_ITEM()
RATIONAL_B_SPLINE_SURFACE(((1.,0.814339887349196,1.),(1.,0.815115959345207,
1.),(1.,0.815907587407945,1.),(1.,0.816715621142051,1.)))
REPRESENTATION_ITEM('')
SURFACE()
);
#2809=(
BOUNDED_SURFACE()
B_SPLINE_SURFACE(3,2,((#394698,#394699,#394700),(#394701,#394702,#394703),
(#394704,#394705,#394706),(#394707,#394708,#394709)),.UNSPECIFIED.,.F.,
 .F.,.F.)
B_SPLINE_SURFACE_WITH_KNOTS((4,4),(3,3),(-3.39528393502488E-6,3.73481232852737E-5),
(-0.00165018033318095,1.),.UNSPECIFIED.)
GEOMETRIC_REPRESENTATION_ITEM()
RATIONAL_B_SPLINE_SURFACE(((1.00048354385562,0.853487571660418,1.),(1.00047110510918,
0.857256476851478,1.),(1.00053193201104,0.838826096655891,1.),(1.00063970687722,
0.806170615310113,1.)))
REPRESENTATION_ITEM('')
SURFACE()
);
#2810=(
BOUNDED_SURFACE()
B_SPLINE_SURFACE(3,2,((#394713,#394714,#394715),(#394716,#394717,#394718),
(#394719,#394720,#394721),(#394722,#394723,#394724)),.UNSPECIFIED.,.F.,
 .F.,.F.)
B_SPLINE_SURFACE_WITH_KNOTS((4,4),(3,3),(2.02993869230509E-5,5.39756952686907E-5),
(-0.000116281069535401,1.),.UNSPECIFIED.)
GEOMETRIC_REPRESENTATION_ITEM()
RATIONAL_B_SPLINE_SURFACE(((1.00001770479724,0.923870681143039,1.),(1.00001014104056,
0.956394275543436,1.),(1.00002037300272,0.912397594905709,1.),(1.00003390859458,
0.854195550869909,1.)))
REPRESENTATION_ITEM('')
SURFACE()
);
#2811=(
BOUNDED_SURFACE()
B_SPLINE_SURFACE(3,2,((#394817,#394818,#394819),(#394820,#394821,#394822),
(#394823,#394824,#394825),(#394826,#394827,#394828)),.UNSPECIFIED.,.F.,
 .F.,.F.)
B_SPLINE_SURFACE_WITH_KNOTS((4,4),(3,3),(0.00135801595889393,0.00148409170619832),
(0.,1.),.UNSPECIFIED.)
GEOMETRIC_REPRESENTATION_ITEM()
RATIONAL_B_SPLINE_SURFACE(((1.,0.818301933966442,1.),(1.,0.817226613172344,
1.),(1.,0.816179643373945,1.),(1.,0.815159387863654,1.)))
REPRESENTATION_ITEM('')
SURFACE()
);
#2812=(
BOUNDED_SURFACE()
B_SPLINE_SURFACE(3,2,((#394867,#394868,#394869),(#394870,#394871,#394872),
(#394873,#394874,#394875),(#394876,#394877,#394878)),.UNSPECIFIED.,.F.,
 .F.,.F.)
B_SPLINE_SURFACE_WITH_KNOTS((4,4),(3,3),(-1.54744435122077E-6,1.54744435122079E-5),
(0.,1.01516989836551),.UNSPECIFIED.)
GEOMETRIC_REPRESENTATION_ITEM()
RATIONAL_B_SPLINE_SURFACE(((1.,0.334740937354324,1.02018382473414),(1.,
0.867753072812859,1.00401234488916),(1.,0.988917903080846,1.00033622856788),
(1.,1.,1.)))
REPRESENTATION_ITEM('')
SURFACE()
);
#2813=(
BOUNDED_SURFACE()
B_SPLINE_SURFACE(3,2,((#394880,#394881,#394882),(#394883,#394884,#394885),
(#394886,#394887,#394888),(#394889,#394890,#394891)),.UNSPECIFIED.,.F.,
 .F.,.F.)
B_SPLINE_SURFACE_WITH_KNOTS((4,4),(3,3),(0.00137194782501028,0.00149814269699235),
(0.,1.),.UNSPECIFIED.)
GEOMETRIC_REPRESENTATION_ITEM()
RATIONAL_B_SPLINE_SURFACE(((1.,0.815158509402316,1.),(1.,0.816179044148155,
1.),(1.,0.817226308119926,1.),(1.,0.818301939488808,1.)))
REPRESENTATION_ITEM('')
SURFACE()
);
#2814=(
BOUNDED_SURFACE()
B_SPLINE_SURFACE(3,2,((#394935,#394936,#394937),(#394938,#394939,#394940),
(#394941,#394942,#394943),(#394944,#394945,#394946)),.UNSPECIFIED.,.F.,
 .F.,.F.)
B_SPLINE_SURFACE_WITH_KNOTS((4,4),(3,3),(1.55009486301137E-5,4.92065510474433E-5),
(-8.13759514709342E-5,1.),.UNSPECIFIED.)
GEOMETRIC_REPRESENTATION_ITEM()
RATIONAL_B_SPLINE_SURFACE(((1.00002372912335,0.854200639599687,1.),(1.00001423585993,
0.912530301180535,1.),(1.00000710550471,0.956341495377432,1.),(1.00001238975908,
0.923873338137023,1.)))
REPRESENTATION_ITEM('')
SURFACE()
);
#2815=(
BOUNDED_SURFACE()
B_SPLINE_SURFACE(3,2,((#394950,#394951,#394952),(#394953,#394954,#394955),
(#394956,#394957,#394958),(#394959,#394960,#394961)),.UNSPECIFIED.,.F.,
 .F.,.F.)
B_SPLINE_SURFACE_WITH_KNOTS((4,4),(3,3),(-3.39934179457828E-6,3.73927597403565E-5),
(-0.00186004067401879,1.00069373317445),.UNSPECIFIED.)
GEOMETRIC_REPRESENTATION_ITEM()
RATIONAL_B_SPLINE_SURFACE(((1.00072100136048,0.806051963875363,1.00026859642693),
(1.00060048440149,0.838470803558657,1.00022369994497),(1.0005310644879,
0.857144632272393,1.00019783877221),(1.00054515072847,0.85335545953911,
1.00020308635438)))
REPRESENTATION_ITEM('')
SURFACE()
);
#2816=(
BOUNDED_SURFACE()
B_SPLINE_SURFACE(3,2,((#394963,#394964,#394965),(#394966,#394967,#394968),
(#394969,#394970,#394971),(#394972,#394973,#394974)),.UNSPECIFIED.,.F.,
 .F.,.F.)
B_SPLINE_SURFACE_WITH_KNOTS((4,4),(3,3),(1.62630325872826E-19,9.54361881492177E-5),
(0.,1.),.UNSPECIFIED.)
GEOMETRIC_REPRESENTATION_ITEM()
RATIONAL_B_SPLINE_SURFACE(((1.,0.816715621142046,1.),(1.,0.815907587407939,
1.),(1.,0.815115959345208,1.),(1.,0.814339887349188,1.)))
REPRESENTATION_ITEM('')
SURFACE()
);
#2817=(
BOUNDED_SURFACE()
B_SPLINE_SURFACE(3,2,((#394976,#394977,#394978),(#394979,#394980,#394981),
(#394982,#394983,#394984),(#394985,#394986,#394987)),.UNSPECIFIED.,.F.,
 .F.,.F.)
B_SPLINE_SURFACE_WITH_KNOTS((4,4),(3,3),(9.99498877760074E-20,4.68197758448203E-5),
(0.,1.),.UNSPECIFIED.)
GEOMETRIC_REPRESENTATION_ITEM()
RATIONAL_B_SPLINE_SURFACE(((1.,0.816715621142051,1.),(1.,0.953638980025203,
1.),(1.,0.954506925408057,1.),(1.,0.816715621142053,1.)))
REPRESENTATION_ITEM('')
SURFACE()
);
#2818=(
BOUNDED_SURFACE()
B_SPLINE_SURFACE(3,2,((#394989,#394990,#394991),(#394992,#394993,#394994),
(#394995,#394996,#394997),(#394998,#394999,#395000)),.UNSPECIFIED.,.F.,
 .F.,.F.)
B_SPLINE_SURFACE_WITH_KNOTS((4,4),(3,3),(-1.0842021724855E-19,9.54361881492176E-5),
(0.,1.),.UNSPECIFIED.)
GEOMETRIC_REPRESENTATION_ITEM()
RATIONAL_B_SPLINE_SURFACE(((1.,0.814339887349193,1.),(1.,0.815115959345199,
1.),(1.,0.815907587407946,1.),(1.,0.816715621142045,1.)))
REPRESENTATION_ITEM('')
SURFACE()
);
#2819=(
BOUNDED_SURFACE()
B_SPLINE_SURFACE(3,2,((#395002,#395003,#395004),(#395005,#395006,#395007),
(#395008,#395009,#395010),(#395011,#395012,#395013)),.UNSPECIFIED.,.F.,
 .F.,.F.)
B_SPLINE_SURFACE_WITH_KNOTS((4,4),(3,3),(-3.39528393502487E-6,3.73481232852732E-5),
(-0.00165018033287617,1.),.UNSPECIFIED.)
GEOMETRIC_REPRESENTATION_ITEM()
RATIONAL_B_SPLINE_SURFACE(((1.00048354385554,0.85348757166045,1.),(1.00047110510909,
0.857256476851514,1.),(1.00053193201094,0.838826096655938,1.),(1.0006397068771,
0.806170615310168,1.)))
REPRESENTATION_ITEM('')
SURFACE()
);
#2820=(
BOUNDED_SURFACE()
B_SPLINE_SURFACE(3,2,((#395017,#395018,#395019),(#395020,#395021,#395022),
(#395023,#395024,#395025),(#395026,#395027,#395028)),.UNSPECIFIED.,.F.,
 .F.,.F.)
B_SPLINE_SURFACE_WITH_KNOTS((4,4),(3,3),(2.02993869230513E-5,5.397569526869E-5),
(-0.000116281070601051,1.),.UNSPECIFIED.)
GEOMETRIC_REPRESENTATION_ITEM()
RATIONAL_B_SPLINE_SURFACE(((1.0000177047974,0.923870681142957,1.),(1.00001014104065,
0.956394275543391,1.),(1.0000203730029,0.912397594905618,1.),(1.00003390859489,
0.854195550869751,1.)))
REPRESENTATION_ITEM('')
SURFACE()
);
#2821=(
BOUNDED_SURFACE()
B_SPLINE_SURFACE(3,2,((#395121,#395122,#395123),(#395124,#395125,#395126),
(#395127,#395128,#395129),(#395130,#395131,#395132)),.UNSPECIFIED.,.F.,
 .F.,.F.)
B_SPLINE_SURFACE_WITH_KNOTS((4,4),(3,3),(0.00135801595889393,0.00148409170619832),
(0.,1.),.UNSPECIFIED.)
GEOMETRIC_REPRESENTATION_ITEM()
RATIONAL_B_SPLINE_SURFACE(((1.,0.818301933966445,1.),(1.,0.817226613172345,
1.),(1.,0.816179643373958,1.),(1.,0.815159387863655,1.)))
REPRESENTATION_ITEM('')
SURFACE()
);
#2822=(
BOUNDED_SURFACE()
B_SPLINE_SURFACE(3,2,((#395171,#395172,#395173),(#395174,#395175,#395176),
(#395177,#395178,#395179),(#395180,#395181,#395182)),.UNSPECIFIED.,.F.,
 .F.,.F.)
B_SPLINE_SURFACE_WITH_KNOTS((4,4),(3,3),(-1.54744435122066E-6,1.54744435122077E-5),
(-0.0151698983594881,1.0151698983631),.UNSPECIFIED.)
GEOMETRIC_REPRESENTATION_ITEM()
RATIONAL_B_SPLINE_SURFACE(((1.02018382472601,0.324498219413288,1.02018382473088),
(1.00401234488754,0.865716921710537,1.00401234488851),(1.00033622856775,
0.988747276629672,1.00033622856783),(1.,1.,1.)))
REPRESENTATION_ITEM('')
SURFACE()
);
#2823=(
BOUNDED_SURFACE()
B_SPLINE_SURFACE(3,2,((#395184,#395185,#395186),(#395187,#395188,#395189),
(#395190,#395191,#395192),(#395193,#395194,#395195)),.UNSPECIFIED.,.F.,
 .F.,.F.)
B_SPLINE_SURFACE_WITH_KNOTS((4,4),(3,3),(0.00137194782501028,0.00149814269699235),
(0.,1.),.UNSPECIFIED.)
GEOMETRIC_REPRESENTATION_ITEM()
RATIONAL_B_SPLINE_SURFACE(((1.,0.815158509402318,1.),(1.,0.816179044148161,
1.),(1.,0.817226308119921,1.),(1.,0.818301939488807,1.)))
REPRESENTATION_ITEM('')
SURFACE()
);
#2824=(
BOUNDED_SURFACE()
B_SPLINE_SURFACE(3,2,((#395239,#395240,#395241),(#395242,#395243,#395244),
(#395245,#395246,#395247),(#395248,#395249,#395250)),.UNSPECIFIED.,.F.,
 .F.,.F.)
B_SPLINE_SURFACE_WITH_KNOTS((4,4),(3,3),(1.55009486301137E-5,4.92065510474435E-5),
(-8.13759515122868E-5,1.),.UNSPECIFIED.)
GEOMETRIC_REPRESENTATION_ITEM()
RATIONAL_B_SPLINE_SURFACE(((1.00002372912337,0.85420063959968,1.),(1.00001423585994,
0.912530301180539,1.),(1.00000710550471,0.956341495377423,1.),(1.00001238975909,
0.923873338137018,1.)))
REPRESENTATION_ITEM('')
SURFACE()
);
#2825=(
BOUNDED_SURFACE()
B_SPLINE_SURFACE(3,2,((#395254,#395255,#395256),(#395257,#395258,#395259),
(#395260,#395261,#395262),(#395263,#395264,#395265)),.UNSPECIFIED.,.F.,
 .F.,.F.)
B_SPLINE_SURFACE_WITH_KNOTS((4,4),(3,3),(-3.39934179457826E-6,3.73927597403567E-5),
(-0.00186004067395861,1.00069373317436),.UNSPECIFIED.)
GEOMETRIC_REPRESENTATION_ITEM()
RATIONAL_B_SPLINE_SURFACE(((1.00072100136046,0.806051963875392,1.0002685964269),
(1.00060048440147,0.838470803558698,1.00022369994495),(1.00053106448788,
0.857144632272418,1.00019783877219),(1.00054515072846,0.85335545953914,
1.00020308635436)))
REPRESENTATION_ITEM('')
SURFACE()
);
#2826=(
BOUNDED_SURFACE()
B_SPLINE_SURFACE(3,2,((#395267,#395268,#395269),(#395270,#395271,#395272),
(#395273,#395274,#395275),(#395276,#395277,#395278)),.UNSPECIFIED.,.F.,
 .F.,.F.)
B_SPLINE_SURFACE_WITH_KNOTS((4,4),(3,3),(-1.62630325872826E-19,9.54361881492171E-5),
(0.,1.),.UNSPECIFIED.)
GEOMETRIC_REPRESENTATION_ITEM()
RATIONAL_B_SPLINE_SURFACE(((1.,0.816715621142051,1.),(1.,0.815907587407945,
1.),(1.,0.815115959345208,1.),(1.,0.814339887349197,1.)))
REPRESENTATION_ITEM('')
SURFACE()
);
#2827=(
BOUNDED_SURFACE()
B_SPLINE_SURFACE(3,2,((#395280,#395281,#395282),(#395283,#395284,#395285),
(#395286,#395287,#395288),(#395289,#395290,#395291)),.UNSPECIFIED.,.F.,
 .F.,.F.)
B_SPLINE_SURFACE_WITH_KNOTS((4,4),(3,3),(4.57397791517322E-20,4.68197758448206E-5),
(0.,1.),.UNSPECIFIED.)
GEOMETRIC_REPRESENTATION_ITEM()
RATIONAL_B_SPLINE_SURFACE(((1.,0.81671562114205,1.),(1.,0.953638980025207,
1.),(1.,0.954506925408057,1.),(1.,0.816715621142058,1.)))
REPRESENTATION_ITEM('')
SURFACE()
);
#2828=(
BOUNDED_SURFACE()
B_SPLINE_SURFACE(3,2,((#395293,#395294,#395295),(#395296,#395297,#395298),
(#395299,#395300,#395301),(#395302,#395303,#395304)),.UNSPECIFIED.,.F.,
 .F.,.F.)
B_SPLINE_SURFACE_WITH_KNOTS((4,4),(3,3),(1.0842021724855E-19,9.54361881492178E-5),
(0.,1.),.UNSPECIFIED.)
GEOMETRIC_REPRESENTATION_ITEM()
RATIONAL_B_SPLINE_SURFACE(((1.,0.814339887349192,1.),(1.,0.815115959345201,
1.),(1.,0.815907587407939,1.),(1.,0.816715621142047,1.)))
REPRESENTATION_ITEM('')
SURFACE()
);
#2829=(
BOUNDED_SURFACE()
B_SPLINE_SURFACE(3,2,((#395306,#395307,#395308),(#395309,#395310,#395311),
(#395312,#395313,#395314),(#395315,#395316,#395317)),.UNSPECIFIED.,.F.,
 .F.,.F.)
B_SPLINE_SURFACE_WITH_KNOTS((4,4),(3,3),(-3.39528393502489E-6,3.73481232852737E-5),
(-0.00165018033293757,1.),.UNSPECIFIED.)
GEOMETRIC_REPRESENTATION_ITEM()
RATIONAL_B_SPLINE_SURFACE(((1.00048354385555,0.853487571660446,1.),(1.00047110510911,
0.857256476851515,1.),(1.00053193201096,0.838826096655921,1.),(1.00063970687712,
0.806170615310158,1.)))
REPRESENTATION_ITEM('')
SURFACE()
);
#2830=(
BOUNDED_SURFACE()
B_SPLINE_SURFACE(3,2,((#395321,#395322,#395323),(#395324,#395325,#395326),
(#395327,#395328,#395329),(#395330,#395331,#395332)),.UNSPECIFIED.,.F.,
 .F.,.F.)
B_SPLINE_SURFACE_WITH_KNOTS((4,4),(3,3),(2.02993869230509E-5,5.39756952686902E-5),
(-0.000116281069873628,1.),.UNSPECIFIED.)
GEOMETRIC_REPRESENTATION_ITEM()
RATIONAL_B_SPLINE_SURFACE(((1.00001770479729,0.923870681143014,1.),(1.00001014104058,
0.95639427554342,1.),(1.00002037300278,0.912397594905681,1.),(1.00003390859467,
0.854195550869857,1.)))
REPRESENTATION_ITEM('')
SURFACE()
);
#2831=(
BOUNDED_SURFACE()
B_SPLINE_SURFACE(3,2,((#395425,#395426,#395427),(#395428,#395429,#395430),
(#395431,#395432,#395433),(#395434,#395435,#395436)),.UNSPECIFIED.,.F.,
 .F.,.F.)
B_SPLINE_SURFACE_WITH_KNOTS((4,4),(3,3),(0.00135801595889393,0.00148409170619832),
(0.,1.),.UNSPECIFIED.)
GEOMETRIC_REPRESENTATION_ITEM()
RATIONAL_B_SPLINE_SURFACE(((1.,0.818301933966442,1.),(1.,0.817226613172343,
1.),(1.,0.816179643373955,1.),(1.,0.815159387863651,1.)))
REPRESENTATION_ITEM('')
SURFACE()
);
#2832=(
BOUNDED_SURFACE()
B_SPLINE_SURFACE(3,2,((#395475,#395476,#395477),(#395478,#395479,#395480),
(#395481,#395482,#395483),(#395484,#395485,#395486)),.UNSPECIFIED.,.F.,
 .F.,.F.)
B_SPLINE_SURFACE_WITH_KNOTS((4,4),(3,3),(-1.54744435122069E-6,1.54744435122075E-5),
(-0.0151698983687385,1.01516989835399),.UNSPECIFIED.)
GEOMETRIC_REPRESENTATION_ITEM()
RATIONAL_B_SPLINE_SURFACE(((1.0201838247385,0.324498219413267,1.02018382471858),
(1.00401234489003,0.865716921710468,1.00401234488607),(1.00033622856795,
0.988747276629697,1.00033622856762),(1.,1.,1.)))
REPRESENTATION_ITEM('')
SURFACE()
);
#2833=(
BOUNDED_SURFACE()
B_SPLINE_SURFACE(3,2,((#395488,#395489,#395490),(#395491,#395492,#395493),
(#395494,#395495,#395496),(#395497,#395498,#395499)),.UNSPECIFIED.,.F.,
 .F.,.F.)
B_SPLINE_SURFACE_WITH_KNOTS((4,4),(3,3),(0.00137194782501028,0.00149814269699235),
(0.,1.),.UNSPECIFIED.)
GEOMETRIC_REPRESENTATION_ITEM()
RATIONAL_B_SPLINE_SURFACE(((1.,0.815158509402313,1.),(1.,0.816179044148156,
1.),(1.,0.817226308119923,1.),(1.,0.818301939488804,1.)))
REPRESENTATION_ITEM('')
SURFACE()
);
#2834=(
BOUNDED_SURFACE()
B_SPLINE_SURFACE(3,2,((#395543,#395544,#395545),(#395546,#395547,#395548),
(#395549,#395550,#395551),(#395552,#395553,#395554)),.UNSPECIFIED.,.F.,
 .F.,.F.)
B_SPLINE_SURFACE_WITH_KNOTS((4,4),(3,3),(1.55009486301137E-5,4.92065510474425E-5),
(-8.1375951558491E-5,1.),.UNSPECIFIED.)
GEOMETRIC_REPRESENTATION_ITEM()
RATIONAL_B_SPLINE_SURFACE(((1.00002372912338,0.854200639599676,1.),(1.00001423585995,
0.91253030118053,1.),(1.00000710550471,0.956341495377426,1.),(1.0000123897591,
0.923873338137015,1.)))
REPRESENTATION_ITEM('')
SURFACE()
);
#2835=(
BOUNDED_SURFACE()
B_SPLINE_SURFACE(3,2,((#395558,#395559,#395560),(#395561,#395562,#395563),
(#395564,#395565,#395566),(#395567,#395568,#395569)),.UNSPECIFIED.,.F.,
 .F.,.F.)
B_SPLINE_SURFACE_WITH_KNOTS((4,4),(3,3),(-3.3993417945782E-6,3.73927597403566E-5),
(-0.00186004067410343,1.00069373317431),.UNSPECIFIED.)
GEOMETRIC_REPRESENTATION_ITEM()
RATIONAL_B_SPLINE_SURFACE(((1.00072100136051,0.806051963875371,1.00026859642688),
(1.00060048440151,0.838470803558661,1.00022369994493),(1.00053106448792,
0.857144632272405,1.00019783877217),(1.0005451507285,0.853355459539116,
1.00020308635434)))
REPRESENTATION_ITEM('')
SURFACE()
);
#2836=(
BOUNDED_SURFACE()
B_SPLINE_SURFACE(3,2,((#395571,#395572,#395573),(#395574,#395575,#395576),
(#395577,#395578,#395579),(#395580,#395581,#395582)),.UNSPECIFIED.,.F.,
 .F.,.F.)
B_SPLINE_SURFACE_WITH_KNOTS((4,4),(3,3),(-2.16840434497101E-19,9.54361881492175E-5),
(0.,1.),.UNSPECIFIED.)
GEOMETRIC_REPRESENTATION_ITEM()
RATIONAL_B_SPLINE_SURFACE(((1.,0.816715621142046,1.),(1.,0.815907587407944,
1.),(1.,0.815115959345203,1.),(1.,0.814339887349189,1.)))
REPRESENTATION_ITEM('')
SURFACE()
);
#2837=(
BOUNDED_SURFACE()
B_SPLINE_SURFACE(3,2,((#395584,#395585,#395586),(#395587,#395588,#395589),
(#395590,#395591,#395592),(#395593,#395594,#395595)),.UNSPECIFIED.,.F.,
 .F.,.F.)
B_SPLINE_SURFACE_WITH_KNOTS((4,4),(3,3),(3.3881317890172E-20,4.68197758448206E-5),
(0.,1.),.UNSPECIFIED.)
GEOMETRIC_REPRESENTATION_ITEM()
RATIONAL_B_SPLINE_SURFACE(((1.,0.816715621142054,1.),(1.,0.953638980025203,
1.),(1.,0.954506925408048,1.),(1.,0.81671562114206,1.)))
REPRESENTATION_ITEM('')
SURFACE()
);
#2838=(
BOUNDED_SURFACE()
B_SPLINE_SURFACE(3,2,((#395597,#395598,#395599),(#395600,#395601,#395602),
(#395603,#395604,#395605),(#395606,#395607,#395608)),.UNSPECIFIED.,.F.,
 .F.,.F.)
B_SPLINE_SURFACE_WITH_KNOTS((4,4),(3,3),(1.62630325872826E-19,9.54361881492176E-5),
(0.,1.),.UNSPECIFIED.)
GEOMETRIC_REPRESENTATION_ITEM()
RATIONAL_B_SPLINE_SURFACE(((1.,0.814339887349188,1.),(1.,0.815115959345208,
1.),(1.,0.815907587407938,1.),(1.,0.816715621142049,1.)))
REPRESENTATION_ITEM('')
SURFACE()
);
#2839=(
BOUNDED_SURFACE()
B_SPLINE_SURFACE(3,2,((#395610,#395611,#395612),(#395613,#395614,#395615),
(#395616,#395617,#395618),(#395619,#395620,#395621)),.UNSPECIFIED.,.F.,
 .F.,.F.)
B_SPLINE_SURFACE_WITH_KNOTS((4,4),(3,3),(-3.3952839350249E-6,3.73481232852737E-5),
(-0.00165018033274544,1.),.UNSPECIFIED.)
GEOMETRIC_REPRESENTATION_ITEM()
RATIONAL_B_SPLINE_SURFACE(((1.0004835438555,0.853487571660473,1.),(1.00047110510905,
0.857256476851541,1.),(1.0005319320109,0.838826096655948,1.),(1.00063970687705,
0.806170615310199,1.)))
REPRESENTATION_ITEM('')
SURFACE()
);
#2840=(
BOUNDED_SURFACE()
B_SPLINE_SURFACE(3,2,((#395625,#395626,#395627),(#395628,#395629,#395630),
(#395631,#395632,#395633),(#395634,#395635,#395636)),.UNSPECIFIED.,.F.,
 .F.,.F.)
B_SPLINE_SURFACE_WITH_KNOTS((4,4),(3,3),(2.02993869230511E-5,5.39756952686902E-5),
(-0.000116281070168245,1.),.UNSPECIFIED.)
GEOMETRIC_REPRESENTATION_ITEM()
RATIONAL_B_SPLINE_SURFACE(((1.00001770479734,0.92387068114299,1.),(1.00001014104061,
0.956394275543405,1.),(1.00002037300283,0.912397594905657,1.),(1.00003390859476,
0.854195550869819,1.)))
REPRESENTATION_ITEM('')
SURFACE()
);
#2841=(
BOUNDED_SURFACE()
B_SPLINE_SURFACE(3,2,((#395729,#395730,#395731),(#395732,#395733,#395734),
(#395735,#395736,#395737),(#395738,#395739,#395740)),.UNSPECIFIED.,.F.,
 .F.,.F.)
B_SPLINE_SURFACE_WITH_KNOTS((4,4),(3,3),(0.00135801595889393,0.00148409170619832),
(0.,1.),.UNSPECIFIED.)
GEOMETRIC_REPRESENTATION_ITEM()
RATIONAL_B_SPLINE_SURFACE(((1.,0.818301933966444,1.),(1.,0.817226613172339,
1.),(1.,0.816179643373955,1.),(1.,0.815159387863653,1.)))
REPRESENTATION_ITEM('')
SURFACE()
);
#2842=(
BOUNDED_SURFACE()
B_SPLINE_SURFACE(3,2,((#395779,#395780,#395781),(#395782,#395783,#395784),
(#395785,#395786,#395787),(#395788,#395789,#395790)),.UNSPECIFIED.,.F.,
 .F.,.F.)
B_SPLINE_SURFACE_WITH_KNOTS((4,4),(3,3),(-1.54744435122071E-6,1.54744435122069E-5),
(-0.0151698983631405,1.01516989835935),.UNSPECIFIED.)
GEOMETRIC_REPRESENTATION_ITEM()
RATIONAL_B_SPLINE_SURFACE(((1.02018382473094,0.324498219413405,1.02018382472582),
(1.00401234488852,0.865716921710534,1.00401234488751),(1.00033622856783,
0.988747276629699,1.00033622856774),(1.,1.,1.)))
REPRESENTATION_ITEM('')
SURFACE()
);
#2843=(
BOUNDED_SURFACE()
B_SPLINE_SURFACE(3,2,((#395792,#395793,#395794),(#395795,#395796,#395797),
(#395798,#395799,#395800),(#395801,#395802,#395803)),.UNSPECIFIED.,.F.,
 .F.,.F.)
B_SPLINE_SURFACE_WITH_KNOTS((4,4),(3,3),(0.00137194782501028,0.00149814269699235),
(0.,1.),.UNSPECIFIED.)
GEOMETRIC_REPRESENTATION_ITEM()
RATIONAL_B_SPLINE_SURFACE(((1.,0.815158509402317,1.),(1.,0.816179044148151,
1.),(1.,0.817226308119928,1.),(1.,0.818301939488808,1.)))
REPRESENTATION_ITEM('')
SURFACE()
);
#2844=(
BOUNDED_SURFACE()
B_SPLINE_SURFACE(3,2,((#395847,#395848,#395849),(#395850,#395851,#395852),
(#395853,#395854,#395855),(#395856,#395857,#395858)),.UNSPECIFIED.,.F.,
 .F.,.F.)
B_SPLINE_SURFACE_WITH_KNOTS((4,4),(3,3),(1.55009486301137E-5,4.9206551047443E-5),
(-8.13759515172332E-5,1.),.UNSPECIFIED.)
GEOMETRIC_REPRESENTATION_ITEM()
RATIONAL_B_SPLINE_SURFACE(((1.00002372912337,0.854200639599675,1.),(1.00001423585994,
0.912530301180543,1.),(1.00000710550471,0.956341495377428,1.),(1.00001238975909,
0.923873338137019,1.)))
REPRESENTATION_ITEM('')
SURFACE()
);
#2845=(
BOUNDED_SURFACE()
B_SPLINE_SURFACE(3,2,((#395862,#395863,#395864),(#395865,#395866,#395867),
(#395868,#395869,#395870),(#395871,#395872,#395873)),.UNSPECIFIED.,.F.,
 .F.,.F.)
B_SPLINE_SURFACE_WITH_KNOTS((4,4),(3,3),(-3.39934179457809E-6,3.73927597403566E-5),
(-0.0018600406740949,1.00069373317436),.UNSPECIFIED.)
GEOMETRIC_REPRESENTATION_ITEM()
RATIONAL_B_SPLINE_SURFACE(((1.00072100136051,0.806051963875365,1.0002685964269),
(1.00060048440151,0.83847080355867,1.00022369994495),(1.00053106448792,
0.85714463227239,1.00019783877218),(1.0005451507285,0.853355459539117,1.00020308635436)))
REPRESENTATION_ITEM('')
SURFACE()
);
#2846=(
BOUNDED_SURFACE()
B_SPLINE_SURFACE(3,2,((#395875,#395876,#395877),(#395878,#395879,#395880),
(#395881,#395882,#395883),(#395884,#395885,#395886)),.UNSPECIFIED.,.F.,
 .F.,.F.)
B_SPLINE_SURFACE_WITH_KNOTS((4,4),(3,3),(-5.42101086242752E-20,9.54361881492176E-5),
(0.,1.),.UNSPECIFIED.)
GEOMETRIC_REPRESENTATION_ITEM()
RATIONAL_B_SPLINE_SURFACE(((1.,0.816715621142048,1.),(1.,0.81590758740794,
1.),(1.,0.815115959345207,1.),(1.,0.814339887349192,1.)))
REPRESENTATION_ITEM('')
SURFACE()
);
#2847=(
BOUNDED_SURFACE()
B_SPLINE_SURFACE(3,2,((#395888,#395889,#395890),(#395891,#395892,#395893),
(#395894,#395895,#395896),(#395897,#395898,#395899)),.UNSPECIFIED.,.F.,
 .F.,.F.)
B_SPLINE_SURFACE_WITH_KNOTS((4,4),(3,3),(1.03338019565025E-19,4.68197758448208E-5),
(0.,1.),.UNSPECIFIED.)
GEOMETRIC_REPRESENTATION_ITEM()
RATIONAL_B_SPLINE_SURFACE(((1.,0.816715621142046,1.),(1.,0.953638980025206,
1.),(1.,0.954506925408053,1.),(1.,0.816715621142057,1.)))
REPRESENTATION_ITEM('')
SURFACE()
);
#2848=(
BOUNDED_SURFACE()
B_SPLINE_SURFACE(3,2,((#395901,#395902,#395903),(#395904,#395905,#395906),
(#395907,#395908,#395909),(#395910,#395911,#395912)),.UNSPECIFIED.,.F.,
 .F.,.F.)
B_SPLINE_SURFACE_WITH_KNOTS((4,4),(3,3),(5.42101086242752E-20,9.54361881492177E-5),
(0.,1.),.UNSPECIFIED.)
GEOMETRIC_REPRESENTATION_ITEM()
RATIONAL_B_SPLINE_SURFACE(((1.,0.814339887349189,1.),(1.,0.815115959345208,
1.),(1.,0.815907587407936,1.),(1.,0.816715621142047,1.)))
REPRESENTATION_ITEM('')
SURFACE()
);
#2849=(
BOUNDED_SURFACE()
B_SPLINE_SURFACE(3,2,((#395914,#395915,#395916),(#395917,#395918,#395919),
(#395920,#395921,#395922),(#395923,#395924,#395925)),.UNSPECIFIED.,.F.,
 .F.,.F.)
B_SPLINE_SURFACE_WITH_KNOTS((4,4),(3,3),(-3.39528393502485E-6,3.73481232852736E-5),
(-0.00165018033331714,1.),.UNSPECIFIED.)
GEOMETRIC_REPRESENTATION_ITEM()
RATIONAL_B_SPLINE_SURFACE(((1.00048354385567,0.853487571660372,1.),(1.00047110510922,
0.857256476851477,1.),(1.00053193201108,0.838826096655848,1.),(1.00063970687727,
0.80617061531009,1.)))
REPRESENTATION_ITEM('')
SURFACE()
);
#2850=(
BOUNDED_SURFACE()
B_SPLINE_SURFACE(3,2,((#395929,#395930,#395931),(#395932,#395933,#395934),
(#395935,#395936,#395937),(#395938,#395939,#395940)),.UNSPECIFIED.,.F.,
 .F.,.F.)
B_SPLINE_SURFACE_WITH_KNOTS((4,4),(3,3),(2.02993869230511E-5,5.39756952686902E-5),
(-0.000116281069525557,1.),.UNSPECIFIED.)
GEOMETRIC_REPRESENTATION_ITEM()
RATIONAL_B_SPLINE_SURFACE(((1.00001770479724,0.923870681143036,1.),(1.00001014104055,
0.956394275543452,1.),(1.00002037300272,0.912397594905699,1.),(1.00003390859457,
0.854195550869911,1.)))
REPRESENTATION_ITEM('')
SURFACE()
);
#2851=(
BOUNDED_SURFACE()
B_SPLINE_SURFACE(3,2,((#396033,#396034,#396035),(#396036,#396037,#396038),
(#396039,#396040,#396041),(#396042,#396043,#396044)),.UNSPECIFIED.,.F.,
 .F.,.F.)
B_SPLINE_SURFACE_WITH_KNOTS((4,4),(3,3),(0.00135801595889393,0.00148409170619832),
(0.,1.),.UNSPECIFIED.)
GEOMETRIC_REPRESENTATION_ITEM()
RATIONAL_B_SPLINE_SURFACE(((1.,0.818301933966435,1.),(1.,0.817226613172344,
1.),(1.,0.816179643373953,1.),(1.,0.815159387863652,1.)))
REPRESENTATION_ITEM('')
SURFACE()
);
#2852=(
BOUNDED_SURFACE()
B_SPLINE_SURFACE(3,2,((#396083,#396084,#396085),(#396086,#396087,#396088),
(#396089,#396090,#396091),(#396092,#396093,#396094)),.UNSPECIFIED.,.F.,
 .F.,.F.)
B_SPLINE_SURFACE_WITH_KNOTS((4,4),(3,3),(-1.54744435122072E-6,1.54744435122074E-5),
(-0.0151698983584628,1.),.UNSPECIFIED.)
GEOMETRIC_REPRESENTATION_ITEM()
RATIONAL_B_SPLINE_SURFACE(((1.02018382472462,0.334740937358972,1.),(1.00401234488727,
0.867753072813783,1.),(1.00033622856772,0.988917903080908,1.),(1.,1.,1.)))
REPRESENTATION_ITEM('')
SURFACE()
);
#2853=(
BOUNDED_SURFACE()
B_SPLINE_SURFACE(3,2,((#396096,#396097,#396098),(#396099,#396100,#396101),
(#396102,#396103,#396104),(#396105,#396106,#396107)),.UNSPECIFIED.,.F.,
 .F.,.F.)
B_SPLINE_SURFACE_WITH_KNOTS((4,4),(3,3),(0.00137194782501028,0.00149814269699235),
(0.,1.),.UNSPECIFIED.)
GEOMETRIC_REPRESENTATION_ITEM()
RATIONAL_B_SPLINE_SURFACE(((1.,0.815158509402318,1.),(1.,0.816179044148147,
1.),(1.,0.817226308119945,1.),(1.,0.818301939488798,1.)))
REPRESENTATION_ITEM('')
SURFACE()
);
#2854=(
BOUNDED_SURFACE()
B_SPLINE_SURFACE(3,2,((#396151,#396152,#396153),(#396154,#396155,#396156),
(#396157,#396158,#396159),(#396160,#396161,#396162)),.UNSPECIFIED.,.F.,
 .F.,.F.)
B_SPLINE_SURFACE_WITH_KNOTS((4,4),(3,3),(1.55009486301138E-5,4.92065510474431E-5),
(-8.13759513618527E-5,1.),.UNSPECIFIED.)
GEOMETRIC_REPRESENTATION_ITEM()
RATIONAL_B_SPLINE_SURFACE(((1.00002372912332,0.854200639599699,1.),(1.00001423585991,
0.912530301180549,1.),(1.0000071055047,0.956341495377427,1.),(1.00001238975907,
0.923873338137033,1.)))
REPRESENTATION_ITEM('')
SURFACE()
);
#2855=(
BOUNDED_SURFACE()
B_SPLINE_SURFACE(3,2,((#396166,#396167,#396168),(#396169,#396170,#396171),
(#396172,#396173,#396174),(#396175,#396176,#396177)),.UNSPECIFIED.,.F.,
 .F.,.F.)
B_SPLINE_SURFACE_WITH_KNOTS((4,4),(3,3),(-3.39934179457828E-6,3.73927597403566E-5),
(-0.00186004067405741,1.00069373317425),.UNSPECIFIED.)
GEOMETRIC_REPRESENTATION_ITEM()
RATIONAL_B_SPLINE_SURFACE(((1.0007210013605,0.80605196387541,1.00026859642685),
(1.0006004844015,0.838470803558664,1.00022369994491),(1.00053106448791,
0.857144632272433,1.00019783877215),(1.00054515072849,0.853355459539133,
1.00020308635433)))
REPRESENTATION_ITEM('')
SURFACE()
);
#2856=(
BOUNDED_SURFACE()
B_SPLINE_SURFACE(3,2,((#396179,#396180,#396181),(#396182,#396183,#396184),
(#396185,#396186,#396187),(#396188,#396189,#396190)),.UNSPECIFIED.,.F.,
 .F.,.F.)
B_SPLINE_SURFACE_WITH_KNOTS((4,4),(3,3),(5.42101086242752E-20,9.54361881492173E-5),
(0.,1.),.UNSPECIFIED.)
GEOMETRIC_REPRESENTATION_ITEM()
RATIONAL_B_SPLINE_SURFACE(((1.,0.816715621142047,1.),(1.,0.815907587407945,
1.),(1.,0.815115959345203,1.),(1.,0.814339887349192,1.)))
REPRESENTATION_ITEM('')
SURFACE()
);
#2857=(
BOUNDED_SURFACE()
B_SPLINE_SURFACE(3,2,((#396192,#396193,#396194),(#396195,#396196,#396197),
(#396198,#396199,#396200),(#396201,#396202,#396203)),.UNSPECIFIED.,.F.,
 .F.,.F.)
B_SPLINE_SURFACE_WITH_KNOTS((4,4),(3,3),(-1.6940658945086E-19,4.68197758448211E-5),
(0.,1.),.UNSPECIFIED.)
GEOMETRIC_REPRESENTATION_ITEM()
RATIONAL_B_SPLINE_SURFACE(((1.,0.816715621142047,1.),(1.,0.953638980025217,
1.),(1.,0.954506925408042,1.),(1.,0.816715621142054,1.)))
REPRESENTATION_ITEM('')
SURFACE()
);
#2858=(
BOUNDED_SURFACE()
B_SPLINE_SURFACE(3,2,((#396205,#396206,#396207),(#396208,#396209,#396210),
(#396211,#396212,#396213),(#396214,#396215,#396216)),.UNSPECIFIED.,.F.,
 .F.,.F.)
B_SPLINE_SURFACE_WITH_KNOTS((4,4),(3,3),(5.42101086242752E-20,9.54361881492176E-5),
(0.,1.),.UNSPECIFIED.)
GEOMETRIC_REPRESENTATION_ITEM()
RATIONAL_B_SPLINE_SURFACE(((1.,0.814339887349192,1.),(1.,0.815115959345213,
1.),(1.,0.815907587407945,1.),(1.,0.816715621142048,1.)))
REPRESENTATION_ITEM('')
SURFACE()
);
#2859=(
BOUNDED_SURFACE()
B_SPLINE_SURFACE(3,2,((#396218,#396219,#396220),(#396221,#396222,#396223),
(#396224,#396225,#396226),(#396227,#396228,#396229)),.UNSPECIFIED.,.F.,
 .F.,.F.)
B_SPLINE_SURFACE_WITH_KNOTS((4,4),(3,3),(-3.39528393502489E-6,3.73481232852737E-5),
(-0.00165018033303416,1.),.UNSPECIFIED.)
GEOMETRIC_REPRESENTATION_ITEM()
RATIONAL_B_SPLINE_SURFACE(((1.00048354385558,0.853487571660428,1.),(1.00047110510914,
0.857256476851519,1.),(1.00053193201099,0.838826096655876,1.),(1.00063970687716,
0.80617061531015,0.999999999999999)))
REPRESENTATION_ITEM('')
SURFACE()
);
#2860=(
BOUNDED_SURFACE()
B_SPLINE_SURFACE(3,2,((#396233,#396234,#396235),(#396236,#396237,#396238),
(#396239,#396240,#396241),(#396242,#396243,#396244)),.UNSPECIFIED.,.F.,
 .F.,.F.)
B_SPLINE_SURFACE_WITH_KNOTS((4,4),(3,3),(2.02993869230509E-5,5.39756952686906E-5),
(-0.000116281069786927,1.),.UNSPECIFIED.)
GEOMETRIC_REPRESENTATION_ITEM()
RATIONAL_B_SPLINE_SURFACE(((1.00001770479728,0.923870681143016,1.),(1.00001014104058,
0.956394275543437,1.),(1.00002037300276,0.912397594905671,1.),(1.00003390859465,
0.854195550869887,1.)))
REPRESENTATION_ITEM('')
SURFACE()
);
#2861=(
BOUNDED_SURFACE()
B_SPLINE_SURFACE(3,2,((#396337,#396338,#396339),(#396340,#396341,#396342),
(#396343,#396344,#396345),(#396346,#396347,#396348)),.UNSPECIFIED.,.F.,
 .F.,.F.)
B_SPLINE_SURFACE_WITH_KNOTS((4,4),(3,3),(0.00135801595889393,0.00148409170619832),
(0.,1.),.UNSPECIFIED.)
GEOMETRIC_REPRESENTATION_ITEM()
RATIONAL_B_SPLINE_SURFACE(((1.,0.818301933966445,1.),(1.,0.817226613172349,
1.),(1.,0.816179643373948,1.),(1.,0.815159387863656,1.)))
REPRESENTATION_ITEM('')
SURFACE()
);
#2862=(
BOUNDED_SURFACE()
B_SPLINE_SURFACE(3,2,((#396387,#396388,#396389),(#396390,#396391,#396392),
(#396393,#396394,#396395),(#396396,#396397,#396398)),.UNSPECIFIED.,.F.,
 .F.,.F.)
B_SPLINE_SURFACE_WITH_KNOTS((4,4),(3,3),(-1.54744435122057E-6,1.54744435122063E-5),
(-0.0151698983656125,1.01516989835623),.UNSPECIFIED.)
GEOMETRIC_REPRESENTATION_ITEM()
RATIONAL_B_SPLINE_SURFACE(((1.02018382473428,0.32449821941383,1.02018382472161),
(1.00401234488918,0.865716921710735,1.00401234488667),(1.00033622856789,
0.988747276629634,1.00033622856767),(1.,1.,1.)))
REPRESENTATION_ITEM('')
SURFACE()
);
#2863=(
BOUNDED_SURFACE()
B_SPLINE_SURFACE(3,2,((#396400,#396401,#396402),(#396403,#396404,#396405),
(#396406,#396407,#396408),(#396409,#396410,#396411)),.UNSPECIFIED.,.F.,
 .F.,.F.)
B_SPLINE_SURFACE_WITH_KNOTS((4,4),(3,3),(0.00137194782501028,0.00149814269699235),
(0.,1.),.UNSPECIFIED.)
GEOMETRIC_REPRESENTATION_ITEM()
RATIONAL_B_SPLINE_SURFACE(((1.,0.815158509402319,1.),(1.,0.81617904414816,
1.),(1.,0.817226308119937,1.),(1.,0.81830193948881,1.)))
REPRESENTATION_ITEM('')
SURFACE()
);
#2864=(
BOUNDED_SURFACE()
B_SPLINE_SURFACE(3,2,((#396455,#396456,#396457),(#396458,#396459,#396460),
(#396461,#396462,#396463),(#396464,#396465,#396466)),.UNSPECIFIED.,.F.,
 .F.,.F.)
B_SPLINE_SURFACE_WITH_KNOTS((4,4),(3,3),(1.55009486301137E-5,4.92065510474434E-5),
(-8.137595126164E-5,1.),.UNSPECIFIED.)
GEOMETRIC_REPRESENTATION_ITEM()
RATIONAL_B_SPLINE_SURFACE(((1.00002372912329,0.854200639599716,1.),(1.0000142358599,
0.912530301180545,1.),(1.00000710550469,0.956341495377451,1.),(1.00001238975905,
0.923873338137038,1.)))
REPRESENTATION_ITEM('')
SURFACE()
);
#2865=(
BOUNDED_SURFACE()
B_SPLINE_SURFACE(3,2,((#396470,#396471,#396472),(#396473,#396474,#396475),
(#396476,#396477,#396478),(#396479,#396480,#396481)),.UNSPECIFIED.,.F.,
 .F.,.F.)
B_SPLINE_SURFACE_WITH_KNOTS((4,4),(3,3),(-3.39934179457798E-6,3.73927597403568E-5),
(-0.00186004067401208,1.0006937331744),.UNSPECIFIED.)
GEOMETRIC_REPRESENTATION_ITEM()
RATIONAL_B_SPLINE_SURFACE(((1.00072100136048,0.806051963875378,1.00026859642691),
(1.00060048440148,0.838470803558667,1.00022369994496),(1.0005310644879,
0.857144632272393,1.00019783877219),(1.00054515072847,0.85335545953913,
1.00020308635437)))
REPRESENTATION_ITEM('')
SURFACE()
);
#2866=(
BOUNDED_SURFACE()
B_SPLINE_SURFACE(3,2,((#396483,#396484,#396485),(#396486,#396487,#396488),
(#396489,#396490,#396491),(#396492,#396493,#396494)),.UNSPECIFIED.,.F.,
 .F.,.F.)
B_SPLINE_SURFACE_WITH_KNOTS((4,4),(3,3),(-2.71050543121376E-19,9.54361881492172E-5),
(0.,1.),.UNSPECIFIED.)
GEOMETRIC_REPRESENTATION_ITEM()
RATIONAL_B_SPLINE_SURFACE(((1.,0.816715621142058,1.),(1.,0.815907587407936,
1.),(1.,0.815115959345221,1.),(1.,0.814339887349188,1.)))
REPRESENTATION_ITEM('')
SURFACE()
);
#2867=(
BOUNDED_SURFACE()
B_SPLINE_SURFACE(3,2,((#396496,#396497,#396498),(#396499,#396500,#396501),
(#396502,#396503,#396504),(#396505,#396506,#396507)),.UNSPECIFIED.,.F.,
 .F.,.F.)
B_SPLINE_SURFACE_WITH_KNOTS((4,4),(3,3),(-3.06625926906057E-19,4.68197758448208E-5),
(0.,1.),.UNSPECIFIED.)
GEOMETRIC_REPRESENTATION_ITEM()
RATIONAL_B_SPLINE_SURFACE(((1.,0.816715621142045,1.),(1.,0.953638980025204,
1.),(1.,0.954506925408053,1.),(1.,0.816715621142051,1.)))
REPRESENTATION_ITEM('')
SURFACE()
);
#2868=(
BOUNDED_SURFACE()
B_SPLINE_SURFACE(3,2,((#396509,#396510,#396511),(#396512,#396513,#396514),
(#396515,#396516,#396517),(#396518,#396519,#396520)),.UNSPECIFIED.,.F.,
 .F.,.F.)
B_SPLINE_SURFACE_WITH_KNOTS((4,4),(3,3),(-3.25260651745651E-19,9.54361881492173E-5),
(0.,1.),.UNSPECIFIED.)
GEOMETRIC_REPRESENTATION_ITEM()
RATIONAL_B_SPLINE_SURFACE(((1.,0.814339887349194,1.),(1.,0.815115959345209,
1.),(1.,0.815907587407937,1.),(1.,0.816715621142051,1.)))
REPRESENTATION_ITEM('')
SURFACE()
);
#2869=(
BOUNDED_SURFACE()
B_SPLINE_SURFACE(3,2,((#396522,#396523,#396524),(#396525,#396526,#396527),
(#396528,#396529,#396530),(#396531,#396532,#396533)),.UNSPECIFIED.,.F.,
 .F.,.F.)
B_SPLINE_SURFACE_WITH_KNOTS((4,4),(3,3),(-3.39528393502371E-6,3.73481232852731E-5),
(-0.00165018033284349,1.),.UNSPECIFIED.)
GEOMETRIC_REPRESENTATION_ITEM()
RATIONAL_B_SPLINE_SURFACE(((1.00048354385553,0.853487571660481,1.),(1.00047110510908,
0.857256476851499,1.),(1.00053193201093,0.838826096655967,1.),(1.00063970687708,
0.806170615310163,1.)))
REPRESENTATION_ITEM('')
SURFACE()
);
#2870=(
BOUNDED_SURFACE()
B_SPLINE_SURFACE(3,2,((#396537,#396538,#396539),(#396540,#396541,#396542),
(#396543,#396544,#396545),(#396546,#396547,#396548)),.UNSPECIFIED.,.F.,
 .F.,.F.)
B_SPLINE_SURFACE_WITH_KNOTS((4,4),(3,3),(2.02993869230509E-5,5.3975695268713E-5),
(-0.000116281069995185,1.),.UNSPECIFIED.)
GEOMETRIC_REPRESENTATION_ITEM()
RATIONAL_B_SPLINE_SURFACE(((1.00001770479731,0.923870681143002,1.),(1.0000101410406,
0.956394275543429,1.),(1.0000203730028,0.912397594905616,1.),(1.00003390859471,
0.854195550869726,1.)))
REPRESENTATION_ITEM('')
SURFACE()
);
#2871=(
BOUNDED_SURFACE()
B_SPLINE_SURFACE(3,2,((#396641,#396642,#396643),(#396644,#396645,#396646),
(#396647,#396648,#396649),(#396650,#396651,#396652)),.UNSPECIFIED.,.F.,
 .F.,.F.)
B_SPLINE_SURFACE_WITH_KNOTS((4,4),(3,3),(0.00135801595889393,0.00148409170619832),
(0.,1.),.UNSPECIFIED.)
GEOMETRIC_REPRESENTATION_ITEM()
RATIONAL_B_SPLINE_SURFACE(((1.,0.81830193396645,1.),(1.,0.817226613172347,
1.),(1.,0.816179643373947,1.),(1.,0.815159387863661,1.)))
REPRESENTATION_ITEM('')
SURFACE()
);
#2872=(
BOUNDED_SURFACE()
B_SPLINE_SURFACE(3,2,((#396691,#396692,#396693),(#396694,#396695,#396696),
(#396697,#396698,#396699),(#396700,#396701,#396702)),.UNSPECIFIED.,.F.,
 .F.,.F.)
B_SPLINE_SURFACE_WITH_KNOTS((4,4),(3,3),(-1.54744435122069E-6,1.54744435122069E-5),
(-0.0151698983596124,1.01516989836293),.UNSPECIFIED.)
GEOMETRIC_REPRESENTATION_ITEM()
RATIONAL_B_SPLINE_SURFACE(((1.02018382472617,0.324498219413415,1.02018382473066),
(1.00401234488758,0.865716921710511,1.00401234488847),(1.00033622856775,
0.988747276629721,1.00033622856782),(1.,1.,1.)))
REPRESENTATION_ITEM('')
SURFACE()
);
#2873=(
BOUNDED_SURFACE()
B_SPLINE_SURFACE(3,2,((#396704,#396705,#396706),(#396707,#396708,#396709),
(#396710,#396711,#396712),(#396713,#396714,#396715)),.UNSPECIFIED.,.F.,
 .F.,.F.)
B_SPLINE_SURFACE_WITH_KNOTS((4,4),(3,3),(0.00137194782501028,0.00149814269699235),
(0.,1.),.UNSPECIFIED.)
GEOMETRIC_REPRESENTATION_ITEM()
RATIONAL_B_SPLINE_SURFACE(((1.,0.815158509402317,1.),(1.,0.816179044148172,
1.),(1.,0.817226308119915,1.),(1.,0.818301939488811,1.)))
REPRESENTATION_ITEM('')
SURFACE()
);
#2874=(
BOUNDED_SURFACE()
B_SPLINE_SURFACE(3,2,((#396759,#396760,#396761),(#396762,#396763,#396764),
(#396765,#396766,#396767),(#396768,#396769,#396770)),.UNSPECIFIED.,.F.,
 .F.,.F.)
B_SPLINE_SURFACE_WITH_KNOTS((4,4),(3,3),(1.55009486301137E-5,4.92065510474434E-5),
(-8.1375951822287E-5,1.),.UNSPECIFIED.)
GEOMETRIC_REPRESENTATION_ITEM()
RATIONAL_B_SPLINE_SURFACE(((1.00002372912346,0.854200639599639,1.),(1.00001423585999,
0.912530301180504,1.),(1.00000710550474,0.95634149537741,1.),(1.00001238975914,
0.923873338137001,1.)))
REPRESENTATION_ITEM('')
SURFACE()
);
#2875=(
BOUNDED_SURFACE()
B_SPLINE_SURFACE(3,2,((#396774,#396775,#396776),(#396777,#396778,#396779),
(#396780,#396781,#396782),(#396783,#396784,#396785)),.UNSPECIFIED.,.F.,
 .F.,.F.)
B_SPLINE_SURFACE_WITH_KNOTS((4,4),(3,3),(-3.39934179457806E-6,3.73927597403567E-5),
(-0.00186004067406807,1.00069373317433),.UNSPECIFIED.)
GEOMETRIC_REPRESENTATION_ITEM()
RATIONAL_B_SPLINE_SURFACE(((1.0007210013605,0.806051963875368,1.00026859642689),
(1.0006004844015,0.838470803558668,1.00022369994494),(1.00053106448791,
0.857144632272412,1.00019783877218),(1.00054515072849,0.853355459539114,
1.00020308635435)))
REPRESENTATION_ITEM('')
SURFACE()
);
#2876=(
BOUNDED_SURFACE()
B_SPLINE_SURFACE(3,2,((#396787,#396788,#396789),(#396790,#396791,#396792),
(#396793,#396794,#396795),(#396796,#396797,#396798)),.UNSPECIFIED.,.F.,
 .F.,.F.)
B_SPLINE_SURFACE_WITH_KNOTS((4,4),(3,3),(-5.42101086242752E-20,9.54361881492173E-5),
(0.,1.),.UNSPECIFIED.)
GEOMETRIC_REPRESENTATION_ITEM()
RATIONAL_B_SPLINE_SURFACE(((1.,0.81671562114205,1.),(1.,0.815907587407947,
1.),(1.,0.815115959345199,1.),(1.,0.814339887349193,1.)))
REPRESENTATION_ITEM('')
SURFACE()
);
#2877=(
BOUNDED_SURFACE()
B_SPLINE_SURFACE(3,2,((#396800,#396801,#396802),(#396803,#396804,#396805),
(#396806,#396807,#396808),(#396809,#396810,#396811)),.UNSPECIFIED.,.F.,
 .F.,.F.)
B_SPLINE_SURFACE_WITH_KNOTS((4,4),(3,3),(7.79270311473956E-20,4.6819775844821E-5),
(0.,1.),.UNSPECIFIED.)
GEOMETRIC_REPRESENTATION_ITEM()
RATIONAL_B_SPLINE_SURFACE(((1.,0.81671562114205,1.),(1.,0.953638980025221,
1.),(1.,0.954506925408034,1.),(1.,0.816715621142064,1.)))
REPRESENTATION_ITEM('')
SURFACE()
);
#2878=(
BOUNDED_SURFACE()
B_SPLINE_SURFACE(3,2,((#396813,#396814,#396815),(#396816,#396817,#396818),
(#396819,#396820,#396821),(#396822,#396823,#396824)),.UNSPECIFIED.,.F.,
 .F.,.F.)
B_SPLINE_SURFACE_WITH_KNOTS((4,4),(3,3),(1.0842021724855E-19,9.54361881492179E-5),
(0.,1.),.UNSPECIFIED.)
GEOMETRIC_REPRESENTATION_ITEM()
RATIONAL_B_SPLINE_SURFACE(((1.,0.814339887349205,1.),(1.,0.815115959345194,
1.),(1.,0.815907587407962,1.),(1.,0.816715621142051,1.)))
REPRESENTATION_ITEM('')
SURFACE()
);
#2879=(
BOUNDED_SURFACE()
B_SPLINE_SURFACE(3,2,((#396826,#396827,#396828),(#396829,#396830,#396831),
(#396832,#396833,#396834),(#396835,#396836,#396837)),.UNSPECIFIED.,.F.,
 .F.,.F.)
B_SPLINE_SURFACE_WITH_KNOTS((4,4),(3,3),(-3.39528393502484E-6,3.73481232852731E-5),
(-0.00165018033298142,1.),.UNSPECIFIED.)
GEOMETRIC_REPRESENTATION_ITEM()
RATIONAL_B_SPLINE_SURFACE(((1.00048354385557,0.853487571660459,1.),(1.00047110510912,
0.857256476851485,1.),(1.00053193201098,0.838826096655939,1.),(1.00063970687714,
0.806170615310147,1.)))
REPRESENTATION_ITEM('')
SURFACE()
);
#2880=(
BOUNDED_SURFACE()
B_SPLINE_SURFACE(3,2,((#396841,#396842,#396843),(#396844,#396845,#396846),
(#396847,#396848,#396849),(#396850,#396851,#396852)),.UNSPECIFIED.,.F.,
 .F.,.F.)
B_SPLINE_SURFACE_WITH_KNOTS((4,4),(3,3),(2.02993869230509E-5,5.3975695268712E-5),
(-0.00011628106945422,1.),.UNSPECIFIED.)
GEOMETRIC_REPRESENTATION_ITEM()
RATIONAL_B_SPLINE_SURFACE(((1.00001770479723,0.923870681143046,1.),(1.00001014104055,
0.956394275543465,1.),(1.0000203730027,0.912397594905649,1.),(1.00003390859455,
0.854195550869809,1.)))
REPRESENTATION_ITEM('')
SURFACE()
);
#2881=(
BOUNDED_SURFACE()
B_SPLINE_SURFACE(3,2,((#396945,#396946,#396947),(#396948,#396949,#396950),
(#396951,#396952,#396953),(#396954,#396955,#396956)),.UNSPECIFIED.,.F.,
 .F.,.F.)
B_SPLINE_SURFACE_WITH_KNOTS((4,4),(3,3),(0.00135801595889393,0.00148409170619832),
(0.,1.),.UNSPECIFIED.)
GEOMETRIC_REPRESENTATION_ITEM()
RATIONAL_B_SPLINE_SURFACE(((1.,0.818301933966443,1.),(1.,0.817226613172376,
1.),(1.,0.816179643373924,1.),(1.,0.815159387863663,1.)))
REPRESENTATION_ITEM('')
SURFACE()
);
#2882=(
BOUNDED_SURFACE()
B_SPLINE_SURFACE(3,2,((#396995,#396996,#396997),(#396998,#396999,#397000),
(#397001,#397002,#397003),(#397004,#397005,#397006)),.UNSPECIFIED.,.F.,
 .F.,.F.)
B_SPLINE_SURFACE_WITH_KNOTS((4,4),(3,3),(-1.5474443512208E-6,1.54744435122078E-5),
(-0.0151698983647775,1.),.UNSPECIFIED.)
GEOMETRIC_REPRESENTATION_ITEM()
RATIONAL_B_SPLINE_SURFACE(((1.02018382473315,0.334740937354771,1.),(1.00401234488896,
0.867753072812997,1.),(1.00033622856787,0.988917903080786,1.),(1.,1.,1.)))
REPRESENTATION_ITEM('')
SURFACE()
);
#2883=(
BOUNDED_SURFACE()
B_SPLINE_SURFACE(3,2,((#397008,#397009,#397010),(#397011,#397012,#397013),
(#397014,#397015,#397016),(#397017,#397018,#397019)),.UNSPECIFIED.,.F.,
 .F.,.F.)
B_SPLINE_SURFACE_WITH_KNOTS((4,4),(3,3),(0.00137194782501028,0.00149814269699235),
(0.,1.),.UNSPECIFIED.)
GEOMETRIC_REPRESENTATION_ITEM()
RATIONAL_B_SPLINE_SURFACE(((1.,0.815158509402318,1.),(1.,0.816179044148164,
1.),(1.,0.81722630811994,1.),(1.,0.818301939488808,1.)))
REPRESENTATION_ITEM('')
SURFACE()
);
#2884=(
BOUNDED_SURFACE()
B_SPLINE_SURFACE(3,2,((#397063,#397064,#397065),(#397066,#397067,#397068),
(#397069,#397070,#397071),(#397072,#397073,#397074)),.UNSPECIFIED.,.F.,
 .F.,.F.)
B_SPLINE_SURFACE_WITH_KNOTS((4,4),(3,3),(1.55009486301137E-5,4.92065510474432E-5),
(-8.13759513958142E-5,1.),.UNSPECIFIED.)
GEOMETRIC_REPRESENTATION_ITEM()
RATIONAL_B_SPLINE_SURFACE(((1.00002372912333,0.854200639599695,1.),(1.00001423585992,
0.912530301180542,1.),(1.0000071055047,0.956341495377438,1.),(1.00001238975907,
0.923873338137029,1.)))
REPRESENTATION_ITEM('')
SURFACE()
);
#2885=(
BOUNDED_SURFACE()
B_SPLINE_SURFACE(3,2,((#397078,#397079,#397080),(#397081,#397082,#397083),
(#397084,#397085,#397086),(#397087,#397088,#397089)),.UNSPECIFIED.,.F.,
 .F.,.F.)
B_SPLINE_SURFACE_WITH_KNOTS((4,4),(3,3),(-3.39934179457826E-6,3.73927597403565E-5),
(-0.00186004067394221,1.00069373317415),.UNSPECIFIED.)
GEOMETRIC_REPRESENTATION_ITEM()
RATIONAL_B_SPLINE_SURFACE(((1.00072100136045,0.806051963875464,1.00026859642681),
(1.00060048440146,0.838470803558715,1.00022369994488),(1.00053106448788,
0.857144632272451,1.00019783877212),(1.00054515072845,0.853355459539171,
1.0002030863543)))
REPRESENTATION_ITEM('')
SURFACE()
);
#2886=(
BOUNDED_SURFACE()
B_SPLINE_SURFACE(3,2,((#397091,#397092,#397093),(#397094,#397095,#397096),
(#397097,#397098,#397099),(#397100,#397101,#397102)),.UNSPECIFIED.,.F.,
 .F.,.F.)
B_SPLINE_SURFACE_WITH_KNOTS((4,4),(3,3),(-2.71050543121376E-19,9.54361881492172E-5),
(0.,1.),.UNSPECIFIED.)
GEOMETRIC_REPRESENTATION_ITEM()
RATIONAL_B_SPLINE_SURFACE(((1.,0.81671562114205,1.),(1.,0.815907587407935,
1.),(1.,0.815115959345205,1.),(1.,0.814339887349194,1.)))
REPRESENTATION_ITEM('')
SURFACE()
);
#2887=(
BOUNDED_SURFACE()
B_SPLINE_SURFACE(3,2,((#397104,#397105,#397106),(#397107,#397108,#397109),
(#397110,#397111,#397112),(#397113,#397114,#397115)),.UNSPECIFIED.,.F.,
 .F.,.F.)
B_SPLINE_SURFACE_WITH_KNOTS((4,4),(3,3),(1.38913403349705E-19,4.68197758448206E-5),
(0.,1.),.UNSPECIFIED.)
GEOMETRIC_REPRESENTATION_ITEM()
RATIONAL_B_SPLINE_SURFACE(((1.,0.816715621142052,1.),(1.,0.953638980025209,
1.),(1.,0.954506925408051,1.),(1.,0.816715621142057,1.)))
REPRESENTATION_ITEM('')
SURFACE()
);
#2888=(
BOUNDED_SURFACE()
B_SPLINE_SURFACE(3,2,((#397117,#397118,#397119),(#397120,#397121,#397122),
(#397123,#397124,#397125),(#397126,#397127,#397128)),.UNSPECIFIED.,.F.,
 .F.,.F.)
B_SPLINE_SURFACE_WITH_KNOTS((4,4),(3,3),(-1.0842021724855E-19,9.54361881492178E-5),
(0.,1.),.UNSPECIFIED.)
GEOMETRIC_REPRESENTATION_ITEM()
RATIONAL_B_SPLINE_SURFACE(((1.,0.814339887349202,1.),(1.,0.815115959345215,
1.),(1.,0.815907587407934,1.),(1.,0.816715621142051,1.)))
REPRESENTATION_ITEM('')
SURFACE()
);
#2889=(
BOUNDED_SURFACE()
B_SPLINE_SURFACE(3,2,((#397130,#397131,#397132),(#397133,#397134,#397135),
(#397136,#397137,#397138),(#397139,#397140,#397141)),.UNSPECIFIED.,.F.,
 .F.,.F.)
B_SPLINE_SURFACE_WITH_KNOTS((4,4),(3,3),(-3.39528393502384E-6,3.73481232852732E-5),
(-0.00165018033264819,1.),.UNSPECIFIED.)
GEOMETRIC_REPRESENTATION_ITEM()
RATIONAL_B_SPLINE_SURFACE(((1.00048354385547,0.853487571660489,1.),(1.00047110510903,
0.857256476851558,1.),(1.00053193201087,0.838826096655971,1.),(1.00063970687701,
0.806170615310218,1.)))
REPRESENTATION_ITEM('')
SURFACE()
);
#2890=(
BOUNDED_SURFACE()
B_SPLINE_SURFACE(3,2,((#397145,#397146,#397147),(#397148,#397149,#397150),
(#397151,#397152,#397153),(#397154,#397155,#397156)),.UNSPECIFIED.,.F.,
 .F.,.F.)
B_SPLINE_SURFACE_WITH_KNOTS((4,4),(3,3),(2.0299386923051E-5,5.39756952687132E-5),
(-0.000116281069686216,1.),.UNSPECIFIED.)
GEOMETRIC_REPRESENTATION_ITEM()
RATIONAL_B_SPLINE_SURFACE(((1.00001770479726,0.923870681143028,1.),(1.00001014104057,
0.956394275543452,1.),(1.00002037300274,0.912397594905648,1.),(1.00003390859462,
0.85419555086976,1.)))
REPRESENTATION_ITEM('')
SURFACE()
);
#2891=(
BOUNDED_SURFACE()
B_SPLINE_SURFACE(3,2,((#397249,#397250,#397251),(#397252,#397253,#397254),
(#397255,#397256,#397257),(#397258,#397259,#397260)),.UNSPECIFIED.,.F.,
 .F.,.F.)
B_SPLINE_SURFACE_WITH_KNOTS((4,4),(3,3),(0.00135801595889393,0.00148409170619832),
(0.,1.),.UNSPECIFIED.)
GEOMETRIC_REPRESENTATION_ITEM()
RATIONAL_B_SPLINE_SURFACE(((1.,0.818301933966443,1.),(1.,0.81722661317235,
1.),(1.,0.816179643373951,1.),(1.,0.815159387863653,1.)))
REPRESENTATION_ITEM('')
SURFACE()
);
#2892=(
BOUNDED_SURFACE()
B_SPLINE_SURFACE(3,2,((#397299,#397300,#397301),(#397302,#397303,#397304),
(#397305,#397306,#397307),(#397308,#397309,#397310)),.UNSPECIFIED.,.F.,
 .F.,.F.)
B_SPLINE_SURFACE_WITH_KNOTS((4,4),(3,3),(-1.54744435122068E-6,1.54744435122077E-5),
(-0.0151698983618832,1.01516989836046),.UNSPECIFIED.)
GEOMETRIC_REPRESENTATION_ITEM()
RATIONAL_B_SPLINE_SURFACE(((1.02018382472924,0.324498219413552,1.02018382472731),
(1.00401234488819,0.865716921710482,1.00401234488781),(1.0003362285678,
0.98874727662976,1.00033622856777),(1.,1.,1.)))
REPRESENTATION_ITEM('')
SURFACE()
);
#2893=(
BOUNDED_SURFACE()
B_SPLINE_SURFACE(3,2,((#397312,#397313,#397314),(#397315,#397316,#397317),
(#397318,#397319,#397320),(#397321,#397322,#397323)),.UNSPECIFIED.,.F.,
 .F.,.F.)
B_SPLINE_SURFACE_WITH_KNOTS((4,4),(3,3),(0.00137194782501028,0.00149814269699235),
(0.,1.),.UNSPECIFIED.)
GEOMETRIC_REPRESENTATION_ITEM()
RATIONAL_B_SPLINE_SURFACE(((1.,0.815158509402319,1.),(1.,0.816179044148173,
1.),(1.,0.817226308119922,1.),(1.,0.818301939488809,1.)))
REPRESENTATION_ITEM('')
SURFACE()
);
#2894=(
BOUNDED_SURFACE()
B_SPLINE_SURFACE(3,2,((#397367,#397368,#397369),(#397370,#397371,#397372),
(#397373,#397374,#397375),(#397376,#397377,#397378)),.UNSPECIFIED.,.F.,
 .F.,.F.)
B_SPLINE_SURFACE_WITH_KNOTS((4,4),(3,3),(1.55009486301137E-5,4.92065510474431E-5),
(-8.13759512503572E-5,1.),.UNSPECIFIED.)
GEOMETRIC_REPRESENTATION_ITEM()
RATIONAL_B_SPLINE_SURFACE(((1.00002372912329,0.854200639599723,1.),(1.00001423585989,
0.912530301180552,1.),(1.00000710550469,0.956341495377439,1.),(1.00001238975905,
0.923873338137042,1.)))
REPRESENTATION_ITEM('')
SURFACE()
);
#2895=(
BOUNDED_SURFACE()
B_SPLINE_SURFACE(3,2,((#397382,#397383,#397384),(#397385,#397386,#397387),
(#397388,#397389,#397390),(#397391,#397392,#397393)),.UNSPECIFIED.,.F.,
 .F.,.F.)
B_SPLINE_SURFACE_WITH_KNOTS((4,4),(3,3),(-3.39934179457864E-6,3.73927597403564E-5),
(-0.00186004067415249,1.00069373317438),.UNSPECIFIED.)
GEOMETRIC_REPRESENTATION_ITEM()
RATIONAL_B_SPLINE_SURFACE(((1.00072100136053,0.806051963875349,1.0002685964269),
(1.00060048440153,0.838470803558665,1.00022369994495),(1.00053106448794,
0.857144632272378,1.00019783877219),(1.00054515072851,0.853355459539108,
1.00020308635436)))
REPRESENTATION_ITEM('')
SURFACE()
);
#2896=(
BOUNDED_SURFACE()
B_SPLINE_SURFACE(3,2,((#397395,#397396,#397397),(#397398,#397399,#397400),
(#397401,#397402,#397403),(#397404,#397405,#397406)),.UNSPECIFIED.,.F.,
 .F.,.F.)
B_SPLINE_SURFACE_WITH_KNOTS((4,4),(3,3),(5.42101086242752E-20,9.54361881492173E-5),
(0.,1.),.UNSPECIFIED.)
GEOMETRIC_REPRESENTATION_ITEM()
RATIONAL_B_SPLINE_SURFACE(((1.,0.81671562114205,1.),(1.,0.815907587407942,
1.),(1.,0.815115959345208,1.),(1.,0.814339887349183,1.)))
REPRESENTATION_ITEM('')
SURFACE()
);
#2897=(
BOUNDED_SURFACE()
B_SPLINE_SURFACE(3,2,((#397408,#397409,#397410),(#397411,#397412,#397413),
(#397414,#397415,#397416),(#397417,#397418,#397419)),.UNSPECIFIED.,.F.,
 .F.,.F.)
B_SPLINE_SURFACE_WITH_KNOTS((4,4),(3,3),(-1.01643953670516E-20,4.68197758448209E-5),
(0.,1.),.UNSPECIFIED.)
GEOMETRIC_REPRESENTATION_ITEM()
RATIONAL_B_SPLINE_SURFACE(((1.,0.816715621142051,1.),(1.,0.953638980025216,
1.),(1.,0.954506925408042,1.),(1.,0.816715621142057,1.)))
REPRESENTATION_ITEM('')
SURFACE()
);
#2898=(
BOUNDED_SURFACE()
B_SPLINE_SURFACE(3,2,((#397421,#397422,#397423),(#397424,#397425,#397426),
(#397427,#397428,#397429),(#397430,#397431,#397432)),.UNSPECIFIED.,.F.,
 .F.,.F.)
B_SPLINE_SURFACE_WITH_KNOTS((4,4),(3,3),(-5.42101086242752E-20,9.54361881492176E-5),
(0.,1.),.UNSPECIFIED.)
GEOMETRIC_REPRESENTATION_ITEM()
RATIONAL_B_SPLINE_SURFACE(((1.,0.814339887349195,1.),(1.,0.8151159593452,
1.),(1.,0.815907587407949,1.),(1.,0.816715621142051,1.)))
REPRESENTATION_ITEM('')
SURFACE()
);
#2899=(
BOUNDED_SURFACE()
B_SPLINE_SURFACE(3,2,((#397434,#397435,#397436),(#397437,#397438,#397439),
(#397440,#397441,#397442),(#397443,#397444,#397445)),.UNSPECIFIED.,.F.,
 .F.,.F.)
B_SPLINE_SURFACE_WITH_KNOTS((4,4),(3,3),(-3.3952839350248E-6,3.73481232852737E-5),
(-0.00165018033327807,1.),.UNSPECIFIED.)
GEOMETRIC_REPRESENTATION_ITEM()
RATIONAL_B_SPLINE_SURFACE(((1.00048354385565,0.853487571660403,1.),(1.00047110510921,
0.857256476851452,1.),(1.00053193201107,0.838826096655878,1.),(1.00063970687725,
0.806170615310095,1.)))
REPRESENTATION_ITEM('')
SURFACE()
);
#2900=(
BOUNDED_SURFACE()
B_SPLINE_SURFACE(3,2,((#397449,#397450,#397451),(#397452,#397453,#397454),
(#397455,#397456,#397457),(#397458,#397459,#397460)),.UNSPECIFIED.,.F.,
 .F.,.F.)
B_SPLINE_SURFACE_WITH_KNOTS((4,4),(3,3),(2.02993869230509E-5,5.39756952687128E-5),
(-0.000116281069711852,1.),.UNSPECIFIED.)
GEOMETRIC_REPRESENTATION_ITEM()
RATIONAL_B_SPLINE_SURFACE(((1.00001770479727,0.923870681143028,1.),(1.00001014104057,
0.956394275543455,1.),(1.00002037300275,0.912397594905626,1.),(1.00003390859463,
0.854195550869769,1.)))
REPRESENTATION_ITEM('')
SURFACE()
);
#2901=(
BOUNDED_SURFACE()
B_SPLINE_SURFACE(3,2,((#397553,#397554,#397555),(#397556,#397557,#397558),
(#397559,#397560,#397561),(#397562,#397563,#397564)),.UNSPECIFIED.,.F.,
 .F.,.F.)
B_SPLINE_SURFACE_WITH_KNOTS((4,4),(3,3),(0.00135801595889393,0.00148409170619832),
(0.,1.),.UNSPECIFIED.)
GEOMETRIC_REPRESENTATION_ITEM()
RATIONAL_B_SPLINE_SURFACE(((1.,0.818301933966442,1.),(1.,0.817226613172341,
1.),(1.,0.816179643373949,1.),(1.,0.815159387863656,1.)))
REPRESENTATION_ITEM('')
SURFACE()
);
#2902=(
BOUNDED_SURFACE()
B_SPLINE_SURFACE(3,2,((#397603,#397604,#397605),(#397606,#397607,#397608),
(#397609,#397610,#397611),(#397612,#397613,#397614)),.UNSPECIFIED.,.F.,
 .F.,.F.)
B_SPLINE_SURFACE_WITH_KNOTS((4,4),(3,3),(-1.54744435121991E-6,1.54744435122074E-5),
(-0.0151698983710202,1.),.UNSPECIFIED.)
GEOMETRIC_REPRESENTATION_ITEM()
RATIONAL_B_SPLINE_SURFACE(((1.02018382474158,0.334740937350775,1.),(1.00401234489064,
0.867753072812127,1.),(1.00033622856801,0.988917903080755,1.),(1.,1.,1.)))
REPRESENTATION_ITEM('')
SURFACE()
);
#2903=(
BOUNDED_SURFACE()
B_SPLINE_SURFACE(3,2,((#397616,#397617,#397618),(#397619,#397620,#397621),
(#397622,#397623,#397624),(#397625,#397626,#397627)),.UNSPECIFIED.,.F.,
 .F.,.F.)
B_SPLINE_SURFACE_WITH_KNOTS((4,4),(3,3),(0.00137194782501028,0.00149814269699235),
(0.,1.),.UNSPECIFIED.)
GEOMETRIC_REPRESENTATION_ITEM()
RATIONAL_B_SPLINE_SURFACE(((1.,0.815158509402318,1.),(1.,0.816179044148172,
1.),(1.,0.81722630811991,1.),(1.,0.818301939488818,1.)))
REPRESENTATION_ITEM('')
SURFACE()
);
#2904=(
BOUNDED_SURFACE()
B_SPLINE_SURFACE(3,2,((#397671,#397672,#397673),(#397674,#397675,#397676),
(#397677,#397678,#397679),(#397680,#397681,#397682)),.UNSPECIFIED.,.F.,
 .F.,.F.)
B_SPLINE_SURFACE_WITH_KNOTS((4,4),(3,3),(1.55009486301137E-5,4.92065510474433E-5),
(-8.13759517002211E-5,1.),.UNSPECIFIED.)
GEOMETRIC_REPRESENTATION_ITEM()
RATIONAL_B_SPLINE_SURFACE(((1.00002372912342,0.85420063959964,1.),(1.00001423585997,
0.912530301180541,1.),(1.00000710550473,0.956341495377402,1.),(1.00001238975912,
0.923873338137012,1.)))
REPRESENTATION_ITEM('')
SURFACE()
);
#2905=(
BOUNDED_SURFACE()
B_SPLINE_SURFACE(3,2,((#397686,#397687,#397688),(#397689,#397690,#397691),
(#397692,#397693,#397694),(#397695,#397696,#397697)),.UNSPECIFIED.,.F.,
 .F.,.F.)
B_SPLINE_SURFACE_WITH_KNOTS((4,4),(3,3),(-3.39934179457822E-6,3.73927597403565E-5),
(-0.00186004067409689,1.00069373317422),.UNSPECIFIED.)
GEOMETRIC_REPRESENTATION_ITEM()
RATIONAL_B_SPLINE_SURFACE(((1.00072100136051,0.806051963875408,1.00026859642684),
(1.00060048440151,0.838470803558674,1.0002236999449),(1.00053106448792,
0.857144632272417,1.00019783877215),(1.0005451507285,0.853355459539137,
1.00020308635432)))
REPRESENTATION_ITEM('')
SURFACE()
);
#2906=(
BOUNDED_SURFACE()
B_SPLINE_SURFACE(3,2,((#397699,#397700,#397701),(#397702,#397703,#397704),
(#397705,#397706,#397707),(#397708,#397709,#397710)),.UNSPECIFIED.,.F.,
 .F.,.F.)
B_SPLINE_SURFACE_WITH_KNOTS((4,4),(3,3),(0.,9.54361881492174E-5),(0.,1.),
 .UNSPECIFIED.)
GEOMETRIC_REPRESENTATION_ITEM()
RATIONAL_B_SPLINE_SURFACE(((1.,0.81671562114205,1.),(1.,0.815907587407957,
1.),(1.,0.815115959345199,1.),(1.,0.814339887349194,1.)))
REPRESENTATION_ITEM('')
SURFACE()
);
#2907=(
BOUNDED_SURFACE()
B_SPLINE_SURFACE(3,2,((#397712,#397713,#397714),(#397715,#397716,#397717),
(#397718,#397719,#397720),(#397721,#397722,#397723)),.UNSPECIFIED.,.F.,
 .F.,.F.)
B_SPLINE_SURFACE_WITH_KNOTS((4,4),(3,3),(-2.03287907341032E-20,4.68197758448207E-5),
(0.,1.),.UNSPECIFIED.)
GEOMETRIC_REPRESENTATION_ITEM()
RATIONAL_B_SPLINE_SURFACE(((1.,0.816715621142051,1.),(1.,0.953638980025206,
1.),(1.,0.95450692540804,1.),(1.,0.81671562114206,1.)))
REPRESENTATION_ITEM('')
SURFACE()
);
#2908=(
BOUNDED_SURFACE()
B_SPLINE_SURFACE(3,2,((#397725,#397726,#397727),(#397728,#397729,#397730),
(#397731,#397732,#397733),(#397734,#397735,#397736)),.UNSPECIFIED.,.F.,
 .F.,.F.)
B_SPLINE_SURFACE_WITH_KNOTS((4,4),(3,3),(-1.0842021724855E-19,9.54361881492177E-5),
(0.,1.),.UNSPECIFIED.)
GEOMETRIC_REPRESENTATION_ITEM()
RATIONAL_B_SPLINE_SURFACE(((1.,0.814339887349194,1.),(1.,0.815115959345219,
1.),(1.,0.81590758740793,1.),(1.,0.816715621142051,1.)))
REPRESENTATION_ITEM('')
SURFACE()
);
#2909=(
BOUNDED_SURFACE()
B_SPLINE_SURFACE(3,2,((#397738,#397739,#397740),(#397741,#397742,#397743),
(#397744,#397745,#397746),(#397747,#397748,#397749)),.UNSPECIFIED.,.F.,
 .F.,.F.)
B_SPLINE_SURFACE_WITH_KNOTS((4,4),(3,3),(-3.39528393502491E-6,3.73481232852735E-5),
(-0.00165018033281841,1.),.UNSPECIFIED.)
GEOMETRIC_REPRESENTATION_ITEM()
RATIONAL_B_SPLINE_SURFACE(((1.00048354385552,0.853487571660464,1.),(1.00047110510907,
0.85725647685154,1.),(1.00053193201092,0.838826096655927,1.),(1.00063970687707,
0.8061706153102,1.)))
REPRESENTATION_ITEM('')
SURFACE()
);
#2910=(
BOUNDED_SURFACE()
B_SPLINE_SURFACE(3,2,((#397753,#397754,#397755),(#397756,#397757,#397758),
(#397759,#397760,#397761),(#397762,#397763,#397764)),.UNSPECIFIED.,.F.,
 .F.,.F.)
B_SPLINE_SURFACE_WITH_KNOTS((4,4),(3,3),(2.02993869230509E-5,5.39756952687121E-5),
(-0.000116281069798229,1.),.UNSPECIFIED.)
GEOMETRIC_REPRESENTATION_ITEM()
RATIONAL_B_SPLINE_SURFACE(((1.00001770479728,0.92387068114302,1.),(1.00001014104058,
0.956394275543454,1.),(1.00002037300276,0.912397594905629,1.),(1.00003390859465,
0.854195550869759,1.)))
REPRESENTATION_ITEM('')
SURFACE()
);
#2911=(
BOUNDED_SURFACE()
B_SPLINE_SURFACE(3,2,((#397857,#397858,#397859),(#397860,#397861,#397862),
(#397863,#397864,#397865),(#397866,#397867,#397868)),.UNSPECIFIED.,.F.,
 .F.,.F.)
B_SPLINE_SURFACE_WITH_KNOTS((4,4),(3,3),(0.00135801595889393,0.00148409170619832),
(0.,1.),.UNSPECIFIED.)
GEOMETRIC_REPRESENTATION_ITEM()
RATIONAL_B_SPLINE_SURFACE(((1.,0.818301933966453,1.),(1.,0.817226613172341,
1.),(1.,0.816179643373938,1.),(1.,0.815159387863655,1.)))
REPRESENTATION_ITEM('')
SURFACE()
);
#2912=(
BOUNDED_SURFACE()
B_SPLINE_SURFACE(3,2,((#397907,#397908,#397909),(#397910,#397911,#397912),
(#397913,#397914,#397915),(#397916,#397917,#397918)),.UNSPECIFIED.,.F.,
 .F.,.F.)
B_SPLINE_SURFACE_WITH_KNOTS((4,4),(3,3),(-1.54744435122067E-6,1.54744435122074E-5),
(-0.0151698983708486,1.01516989835091),.UNSPECIFIED.)
GEOMETRIC_REPRESENTATION_ITEM()
RATIONAL_B_SPLINE_SURFACE(((1.02018382474135,0.324498219413826,1.02018382471442),
(1.00401234489059,0.865716921710718,1.00401234488524),(1.000336228568,0.9887472766297,
1.00033622856755),(1.,1.,1.)))
REPRESENTATION_ITEM('')
SURFACE()
);
#2913=(
BOUNDED_SURFACE()
B_SPLINE_SURFACE(3,2,((#397920,#397921,#397922),(#397923,#397924,#397925),
(#397926,#397927,#397928),(#397929,#397930,#397931)),.UNSPECIFIED.,.F.,
 .F.,.F.)
B_SPLINE_SURFACE_WITH_KNOTS((4,4),(3,3),(0.00137194782501028,0.00149814269699235),
(0.,1.),.UNSPECIFIED.)
GEOMETRIC_REPRESENTATION_ITEM()
RATIONAL_B_SPLINE_SURFACE(((1.,0.815158509402318,1.),(1.,0.816179044148168,
1.),(1.,0.817226308119929,1.),(1.,0.818301939488811,1.)))
REPRESENTATION_ITEM('')
SURFACE()
);
#2914=(
BOUNDED_SURFACE()
B_SPLINE_SURFACE(3,2,((#397975,#397976,#397977),(#397978,#397979,#397980),
(#397981,#397982,#397983),(#397984,#397985,#397986)),.UNSPECIFIED.,.F.,
 .F.,.F.)
B_SPLINE_SURFACE_WITH_KNOTS((4,4),(3,3),(1.55009486301137E-5,4.92065510474431E-5),
(-8.13759513342479E-5,1.),.UNSPECIFIED.)
GEOMETRIC_REPRESENTATION_ITEM()
RATIONAL_B_SPLINE_SURFACE(((1.00002372912331,0.854200639599702,1.),(1.00001423585991,
0.912530301180565,1.),(1.00000710550469,0.95634149537742,1.),(1.00001238975906,
0.923873338137036,1.)))
REPRESENTATION_ITEM('')
SURFACE()
);
#2915=(
BOUNDED_SURFACE()
B_SPLINE_SURFACE(3,2,((#397990,#397991,#397992),(#397993,#397994,#397995),
(#397996,#397997,#397998),(#397999,#398000,#398001)),.UNSPECIFIED.,.F.,
 .F.,.F.)
B_SPLINE_SURFACE_WITH_KNOTS((4,4),(3,3),(-3.39934179457801E-6,3.73927597403567E-5),
(-0.00186004067410277,1.00069373317419),.UNSPECIFIED.)
GEOMETRIC_REPRESENTATION_ITEM()
RATIONAL_B_SPLINE_SURFACE(((1.00072100136051,0.806051963875423,1.00026859642683),
(1.00060048440151,0.838470803558641,1.00022369994489),(1.00053106448792,
0.857144632272466,1.00019783877214),(1.0005451507285,0.853355459539117,
1.00020308635431)))
REPRESENTATION_ITEM('')
SURFACE()
);
#2916=(
BOUNDED_SURFACE()
B_SPLINE_SURFACE(3,2,((#398003,#398004,#398005),(#398006,#398007,#398008),
(#398009,#398010,#398011),(#398012,#398013,#398014)),.UNSPECIFIED.,.F.,
 .F.,.F.)
B_SPLINE_SURFACE_WITH_KNOTS((4,4),(3,3),(0.,9.54361881492176E-5),(0.,1.),
 .UNSPECIFIED.)
GEOMETRIC_REPRESENTATION_ITEM()
RATIONAL_B_SPLINE_SURFACE(((1.,0.816715621142051,1.),(1.,0.815907587407931,
1.),(1.,0.815115959345217,1.),(1.,0.814339887349183,1.)))
REPRESENTATION_ITEM('')
SURFACE()
);
#2917=(
BOUNDED_SURFACE()
B_SPLINE_SURFACE(3,2,((#398016,#398017,#398018),(#398019,#398020,#398021),
(#398022,#398023,#398024),(#398025,#398026,#398027)),.UNSPECIFIED.,.F.,
 .F.,.F.)
B_SPLINE_SURFACE_WITH_KNOTS((4,4),(3,3),(-1.37219337455197E-19,4.68197758448213E-5),
(0.,1.),.UNSPECIFIED.)
GEOMETRIC_REPRESENTATION_ITEM()
RATIONAL_B_SPLINE_SURFACE(((1.,0.816715621142045,1.),(1.,0.953638980025202,
1.),(1.,0.95450692540806,1.),(1.,0.816715621142052,1.)))
REPRESENTATION_ITEM('')
SURFACE()
);
#2918=(
BOUNDED_SURFACE()
B_SPLINE_SURFACE(3,2,((#398029,#398030,#398031),(#398032,#398033,#398034),
(#398035,#398036,#398037),(#398038,#398039,#398040)),.UNSPECIFIED.,.F.,
 .F.,.F.)
B_SPLINE_SURFACE_WITH_KNOTS((4,4),(3,3),(-1.0842021724855E-19,9.54361881492175E-5),
(0.,1.),.UNSPECIFIED.)
GEOMETRIC_REPRESENTATION_ITEM()
RATIONAL_B_SPLINE_SURFACE(((1.,0.814339887349196,1.),(1.,0.81511595934521,
1.),(1.,0.815907587407948,1.),(1.,0.816715621142052,1.)))
REPRESENTATION_ITEM('')
SURFACE()
);
#2919=(
BOUNDED_SURFACE()
B_SPLINE_SURFACE(3,2,((#398042,#398043,#398044),(#398045,#398046,#398047),
(#398048,#398049,#398050),(#398051,#398052,#398053)),.UNSPECIFIED.,.F.,
 .F.,.F.)
B_SPLINE_SURFACE_WITH_KNOTS((4,4),(3,3),(-3.39528393502481E-6,3.73481232852722E-5),
(-0.0016501803332717,1.),.UNSPECIFIED.)
GEOMETRIC_REPRESENTATION_ITEM()
RATIONAL_B_SPLINE_SURFACE(((1.00048354385565,0.853487571660418,1.),(1.0004711051092,
0.857256476851432,1.),(1.00053193201107,0.838826096655909,1.),(1.00063970687725,
0.806170615310093,1.)))
REPRESENTATION_ITEM('')
SURFACE()
);
#2920=(
BOUNDED_SURFACE()
B_SPLINE_SURFACE(3,2,((#398057,#398058,#398059),(#398060,#398061,#398062),
(#398063,#398064,#398065),(#398066,#398067,#398068)),.UNSPECIFIED.,.F.,
 .F.,.F.)
B_SPLINE_SURFACE_WITH_KNOTS((4,4),(3,3),(2.0299386923051E-5,5.39756952687124E-5),
(-0.00011628106957775,1.),.UNSPECIFIED.)
GEOMETRIC_REPRESENTATION_ITEM()
RATIONAL_B_SPLINE_SURFACE(((1.00001770479725,0.923870681143034,1.),(1.00001014104056,
0.95639427554345,1.),(1.00002037300272,0.912397594905659,1.),(1.00003390859459,
0.854195550869787,1.)))
REPRESENTATION_ITEM('')
SURFACE()
);
#2921=(
BOUNDED_SURFACE()
B_SPLINE_SURFACE(3,2,((#398161,#398162,#398163),(#398164,#398165,#398166),
(#398167,#398168,#398169),(#398170,#398171,#398172)),.UNSPECIFIED.,.F.,
 .F.,.F.)
B_SPLINE_SURFACE_WITH_KNOTS((4,4),(3,3),(0.00135801595889393,0.00148409170619832),
(0.,1.),.UNSPECIFIED.)
GEOMETRIC_REPRESENTATION_ITEM()
RATIONAL_B_SPLINE_SURFACE(((1.,0.81830193396644,1.),(1.,0.817226613172329,
1.),(1.,0.816179643373962,1.),(1.,0.815159387863652,1.)))
REPRESENTATION_ITEM('')
SURFACE()
);
#2922=(
BOUNDED_SURFACE()
B_SPLINE_SURFACE(3,2,((#398211,#398212,#398213),(#398214,#398215,#398216),
(#398217,#398218,#398219),(#398220,#398221,#398222)),.UNSPECIFIED.,.F.,
 .F.,.F.)
B_SPLINE_SURFACE_WITH_KNOTS((4,4),(3,3),(-1.54744435122089E-6,1.5474443512209E-5),
(-0.0151698983635135,1.01516989835912),.UNSPECIFIED.)
GEOMETRIC_REPRESENTATION_ITEM()
RATIONAL_B_SPLINE_SURFACE(((1.02018382473144,0.32449821941329,1.02018382472551),
(1.00401234488862,0.865716921710548,1.00401234488744),(1.00033622856784,
0.988747276629661,1.00033622856774),(1.,1.,1.)))
REPRESENTATION_ITEM('')
SURFACE()
);
#2923=(
BOUNDED_SURFACE()
B_SPLINE_SURFACE(3,2,((#398224,#398225,#398226),(#398227,#398228,#398229),
(#398230,#398231,#398232),(#398233,#398234,#398235)),.UNSPECIFIED.,.F.,
 .F.,.F.)
B_SPLINE_SURFACE_WITH_KNOTS((4,4),(3,3),(0.00137194782501028,0.00149814269699235),
(0.,1.),.UNSPECIFIED.)
GEOMETRIC_REPRESENTATION_ITEM()
RATIONAL_B_SPLINE_SURFACE(((1.,0.815158509402317,1.),(1.,0.816179044148169,
1.),(1.,0.817226308119919,1.),(1.,0.818301939488809,1.)))
REPRESENTATION_ITEM('')
SURFACE()
);
#2924=(
BOUNDED_SURFACE()
B_SPLINE_SURFACE(3,2,((#398279,#398280,#398281),(#398282,#398283,#398284),
(#398285,#398286,#398287),(#398288,#398289,#398290)),.UNSPECIFIED.,.F.,
 .F.,.F.)
B_SPLINE_SURFACE_WITH_KNOTS((4,4),(3,3),(1.55009486301137E-5,4.92065510474432E-5),
(-8.1375951632858E-5,1.),.UNSPECIFIED.)
GEOMETRIC_REPRESENTATION_ITEM()
RATIONAL_B_SPLINE_SURFACE(((1.0000237291234,0.854200639599664,1.),(1.00001423585996,
0.912530301180503,1.),(1.00000710550472,0.956341495377435,1.),(1.00001238975911,
0.923873338137011,1.)))
REPRESENTATION_ITEM('')
SURFACE()
);
#2925=(
BOUNDED_SURFACE()
B_SPLINE_SURFACE(3,2,((#398294,#398295,#398296),(#398297,#398298,#398299),
(#398300,#398301,#398302),(#398303,#398304,#398305)),.UNSPECIFIED.,.F.,
 .F.,.F.)
B_SPLINE_SURFACE_WITH_KNOTS((4,4),(3,3),(-3.39934179457874E-6,3.73927597403563E-5),
(-0.00186004067438938,1.00069373317449),.UNSPECIFIED.)
GEOMETRIC_REPRESENTATION_ITEM()
RATIONAL_B_SPLINE_SURFACE(((1.00072100136062,0.806051963875284,1.00026859642694),
(1.0006004844016,0.83847080355859,1.00022369994499),(1.000531064488,0.857144632272337,
1.00019783877222),(1.00054515072858,0.853355459539054,1.0002030863544)))
REPRESENTATION_ITEM('')
SURFACE()
);
#2926=(
BOUNDED_SURFACE()
B_SPLINE_SURFACE(3,2,((#398307,#398308,#398309),(#398310,#398311,#398312),
(#398313,#398314,#398315),(#398316,#398317,#398318)),.UNSPECIFIED.,.F.,
 .F.,.F.)
B_SPLINE_SURFACE_WITH_KNOTS((4,4),(3,3),(-1.0842021724855E-19,9.54361881492171E-5),
(0.,1.),.UNSPECIFIED.)
GEOMETRIC_REPRESENTATION_ITEM()
RATIONAL_B_SPLINE_SURFACE(((1.,0.816715621142048,1.),(1.,0.815907587407952,
1.),(1.,0.815115959345191,1.),(1.,0.814339887349191,1.)))
REPRESENTATION_ITEM('')
SURFACE()
);
#2927=(
BOUNDED_SURFACE()
B_SPLINE_SURFACE(3,2,((#398320,#398321,#398322),(#398323,#398324,#398325),
(#398326,#398327,#398328),(#398329,#398330,#398331)),.UNSPECIFIED.,.F.,
 .F.,.F.)
B_SPLINE_SURFACE_WITH_KNOTS((4,4),(3,3),(3.64224167319349E-19,4.68197758448205E-5),
(0.,1.),.UNSPECIFIED.)
GEOMETRIC_REPRESENTATION_ITEM()
RATIONAL_B_SPLINE_SURFACE(((1.,0.816715621142056,1.),(1.,0.953638980025198,
1.),(1.,0.954506925408059,1.),(1.,0.816715621142056,1.)))
REPRESENTATION_ITEM('')
SURFACE()
);
#2928=(
BOUNDED_SURFACE()
B_SPLINE_SURFACE(3,2,((#398333,#398334,#398335),(#398336,#398337,#398338),
(#398339,#398340,#398341),(#398342,#398343,#398344)),.UNSPECIFIED.,.F.,
 .F.,.F.)
B_SPLINE_SURFACE_WITH_KNOTS((4,4),(3,3),(1.0842021724855E-19,9.54361881492179E-5),
(0.,1.),.UNSPECIFIED.)
GEOMETRIC_REPRESENTATION_ITEM()
RATIONAL_B_SPLINE_SURFACE(((1.,0.814339887349194,1.),(1.,0.815115959345204,
1.),(1.,0.815907587407948,1.),(1.,0.81671562114205,1.)))
REPRESENTATION_ITEM('')
SURFACE()
);
#2929=(
BOUNDED_SURFACE()
B_SPLINE_SURFACE(3,2,((#398346,#398347,#398348),(#398349,#398350,#398351),
(#398352,#398353,#398354),(#398355,#398356,#398357)),.UNSPECIFIED.,.F.,
 .F.,.F.)
B_SPLINE_SURFACE_WITH_KNOTS((4,4),(3,3),(-3.39528393502483E-6,3.73481232852738E-5),
(-0.00165018033340518,1.),.UNSPECIFIED.)
GEOMETRIC_REPRESENTATION_ITEM()
RATIONAL_B_SPLINE_SURFACE(((1.00048354385569,0.853487571660378,1.),(1.00047110510924,
0.857256476851447,1.),(1.00053193201111,0.83882609665586,1.),(1.0006397068773,
0.806170615310066,1.)))
REPRESENTATION_ITEM('')
SURFACE()
);
#2930=(
BOUNDED_SURFACE()
B_SPLINE_SURFACE(3,2,((#398361,#398362,#398363),(#398364,#398365,#398366),
(#398367,#398368,#398369),(#398370,#398371,#398372)),.UNSPECIFIED.,.F.,
 .F.,.F.)
B_SPLINE_SURFACE_WITH_KNOTS((4,4),(3,3),(2.02993869230509E-5,5.39756952687129E-5),
(-0.000116281069815165,1.),.UNSPECIFIED.)
GEOMETRIC_REPRESENTATION_ITEM()
RATIONAL_B_SPLINE_SURFACE(((1.00001770479728,0.923870681143013,1.),(1.00001014104058,
0.956394275543449,1.),(1.00002037300277,0.91239759490563,1.),(1.00003390859466,
0.85419555086975,1.)))
REPRESENTATION_ITEM('')
SURFACE()
);
#2931=(
BOUNDED_SURFACE()
B_SPLINE_SURFACE(3,2,((#398465,#398466,#398467),(#398468,#398469,#398470),
(#398471,#398472,#398473),(#398474,#398475,#398476)),.UNSPECIFIED.,.F.,
 .F.,.F.)
B_SPLINE_SURFACE_WITH_KNOTS((4,4),(3,3),(0.00135801595889393,0.00148409170619832),
(0.,1.),.UNSPECIFIED.)
GEOMETRIC_REPRESENTATION_ITEM()
RATIONAL_B_SPLINE_SURFACE(((1.,0.818301933966442,1.),(1.,0.817226613172341,
1.),(1.,0.81617964337395,1.),(1.,0.815159387863652,1.)))
REPRESENTATION_ITEM('')
SURFACE()
);
#2932=(
BOUNDED_SURFACE()
B_SPLINE_SURFACE(3,2,((#398515,#398516,#398517),(#398518,#398519,#398520),
(#398521,#398522,#398523),(#398524,#398525,#398526)),.UNSPECIFIED.,.F.,
 .F.,.F.)
B_SPLINE_SURFACE_WITH_KNOTS((4,4),(3,3),(-1.54744435122074E-6,1.54744435122072E-5),
(-0.015169898358919,1.01516989836333),.UNSPECIFIED.)
GEOMETRIC_REPRESENTATION_ITEM()
RATIONAL_B_SPLINE_SURFACE(((1.02018382472524,0.324498219413669,1.02018382473119),
(1.00401234488739,0.865716921710439,1.00401234488858),(1.00033622856773,
0.988747276629761,1.00033622856783),(1.,1.,1.)))
REPRESENTATION_ITEM('')
SURFACE()
);
#2933=(
BOUNDED_SURFACE()
B_SPLINE_SURFACE(3,2,((#398528,#398529,#398530),(#398531,#398532,#398533),
(#398534,#398535,#398536),(#398537,#398538,#398539)),.UNSPECIFIED.,.F.,
 .F.,.F.)
B_SPLINE_SURFACE_WITH_KNOTS((4,4),(3,3),(0.00137194782501028,0.00149814269699235),
(0.,1.),.UNSPECIFIED.)
GEOMETRIC_REPRESENTATION_ITEM()
RATIONAL_B_SPLINE_SURFACE(((1.,0.815158509402318,1.),(1.,0.816179044148164,
1.),(1.,0.817226308119921,1.),(1.,0.818301939488808,1.)))
REPRESENTATION_ITEM('')
SURFACE()
);
#2934=(
BOUNDED_SURFACE()
B_SPLINE_SURFACE(3,2,((#398583,#398584,#398585),(#398586,#398587,#398588),
(#398589,#398590,#398591),(#398592,#398593,#398594)),.UNSPECIFIED.,.F.,
 .F.,.F.)
B_SPLINE_SURFACE_WITH_KNOTS((4,4),(3,3),(1.55009486301137E-5,4.92065510474435E-5),
(-8.13759518653072E-5,1.),.UNSPECIFIED.)
GEOMETRIC_REPRESENTATION_ITEM()
RATIONAL_B_SPLINE_SURFACE(((1.00002372912347,0.854200639599629,1.),(1.00001423586,
0.912530301180511,1.),(1.00000710550474,0.956341495377406,1.),(1.00001238975914,
0.923873338136994,1.)))
REPRESENTATION_ITEM('')
SURFACE()
);
#2935=(
BOUNDED_SURFACE()
B_SPLINE_SURFACE(3,2,((#398598,#398599,#398600),(#398601,#398602,#398603),
(#398604,#398605,#398606),(#398607,#398608,#398609)),.UNSPECIFIED.,.F.,
 .F.,.F.)
B_SPLINE_SURFACE_WITH_KNOTS((4,4),(3,3),(-3.39934179457845E-6,3.73927597403565E-5),
(-0.00186004067405994,1.00069373317426),.UNSPECIFIED.)
GEOMETRIC_REPRESENTATION_ITEM()
RATIONAL_B_SPLINE_SURFACE(((1.0007210013605,0.806051963875394,1.00026859642686),
(1.0006004844015,0.83847080355868,1.00022369994491),(1.00053106448791,0.857144632272414,
1.00019783877215),(1.00054515072849,0.853355459539135,1.00020308635433)))
REPRESENTATION_ITEM('')
SURFACE()
);
#2936=(
BOUNDED_SURFACE()
B_SPLINE_SURFACE(3,2,((#398611,#398612,#398613),(#398614,#398615,#398616),
(#398617,#398618,#398619),(#398620,#398621,#398622)),.UNSPECIFIED.,.F.,
 .F.,.F.)
B_SPLINE_SURFACE_WITH_KNOTS((4,4),(3,3),(-5.42101086242752E-20,9.54361881492175E-5),
(0.,1.),.UNSPECIFIED.)
GEOMETRIC_REPRESENTATION_ITEM()
RATIONAL_B_SPLINE_SURFACE(((1.,0.816715621142049,1.),(1.,0.815907587407938,
1.),(1.,0.815115959345205,1.),(1.,0.81433988734919,1.)))
REPRESENTATION_ITEM('')
SURFACE()
);
#2937=(
BOUNDED_SURFACE()
B_SPLINE_SURFACE(3,2,((#398624,#398625,#398626),(#398627,#398628,#398629),
(#398630,#398631,#398632),(#398633,#398634,#398635)),.UNSPECIFIED.,.F.,
 .F.,.F.)
B_SPLINE_SURFACE_WITH_KNOTS((4,4),(3,3),(2.64274279543342E-19,4.68197758448213E-5),
(0.,1.),.UNSPECIFIED.)
GEOMETRIC_REPRESENTATION_ITEM()
RATIONAL_B_SPLINE_SURFACE(((1.,0.81671562114205,1.),(1.,0.953638980025202,
1.),(1.,0.95450692540806,1.),(1.,0.816715621142055,1.)))
REPRESENTATION_ITEM('')
SURFACE()
);
#2938=(
BOUNDED_SURFACE()
B_SPLINE_SURFACE(3,2,((#398637,#398638,#398639),(#398640,#398641,#398642),
(#398643,#398644,#398645),(#398646,#398647,#398648)),.UNSPECIFIED.,.F.,
 .F.,.F.)
B_SPLINE_SURFACE_WITH_KNOTS((4,4),(3,3),(-1.0842021724855E-19,9.54361881492178E-5),
(0.,1.),.UNSPECIFIED.)
GEOMETRIC_REPRESENTATION_ITEM()
RATIONAL_B_SPLINE_SURFACE(((1.,0.814339887349194,1.),(1.,0.815115959345202,
1.),(1.,0.815907587407945,1.),(1.,0.81671562114205,1.)))
REPRESENTATION_ITEM('')
SURFACE()
);
#2939=(
BOUNDED_SURFACE()
B_SPLINE_SURFACE(3,2,((#398650,#398651,#398652),(#398653,#398654,#398655),
(#398656,#398657,#398658),(#398659,#398660,#398661)),.UNSPECIFIED.,.F.,
 .F.,.F.)
B_SPLINE_SURFACE_WITH_KNOTS((4,4),(3,3),(-3.39528393502484E-6,3.73481232852732E-5),
(-0.00165018033312451,1.),.UNSPECIFIED.)
GEOMETRIC_REPRESENTATION_ITEM()
RATIONAL_B_SPLINE_SURFACE(((1.00048354385561,0.853487571660429,1.),(1.00047110510916,
0.857256476851488,1.),(1.00053193201102,0.838826096655901,1.),(1.00063970687719,
0.806170615310121,1.)))
REPRESENTATION_ITEM('')
SURFACE()
);
#2940=(
BOUNDED_SURFACE()
B_SPLINE_SURFACE(3,2,((#398665,#398666,#398667),(#398668,#398669,#398670),
(#398671,#398672,#398673),(#398674,#398675,#398676)),.UNSPECIFIED.,.F.,
 .F.,.F.)
B_SPLINE_SURFACE_WITH_KNOTS((4,4),(3,3),(2.02993869230509E-5,5.39756952687132E-5),
(-0.000116281069764964,1.),.UNSPECIFIED.)
GEOMETRIC_REPRESENTATION_ITEM()
RATIONAL_B_SPLINE_SURFACE(((1.00001770479727,0.923870681143023,1.),(1.00001014104058,
0.956394275543448,1.),(1.00002037300276,0.912397594905643,1.),(1.00003390859464,
0.854195550869757,1.)))
REPRESENTATION_ITEM('')
SURFACE()
);
#2941=(
BOUNDED_SURFACE()
B_SPLINE_SURFACE(3,2,((#398769,#398770,#398771),(#398772,#398773,#398774),
(#398775,#398776,#398777),(#398778,#398779,#398780)),.UNSPECIFIED.,.F.,
 .F.,.F.)
B_SPLINE_SURFACE_WITH_KNOTS((4,4),(3,3),(0.00135801595889393,0.00148409170619832),
(0.,1.),.UNSPECIFIED.)
GEOMETRIC_REPRESENTATION_ITEM()
RATIONAL_B_SPLINE_SURFACE(((1.,0.818301933966446,1.),(1.,0.817226613172346,
1.),(1.,0.816179643373953,1.),(1.,0.815159387863655,1.)))
REPRESENTATION_ITEM('')
SURFACE()
);
#2942=(
BOUNDED_SURFACE()
B_SPLINE_SURFACE(3,2,((#398819,#398820,#398821),(#398822,#398823,#398824),
(#398825,#398826,#398827),(#398828,#398829,#398830)),.UNSPECIFIED.,.F.,
 .F.,.F.)
B_SPLINE_SURFACE_WITH_KNOTS((4,4),(3,3),(-1.54744435122087E-6,1.54744435122095E-5),
(-0.0151698983679368,1.015169898355),.UNSPECIFIED.)
GEOMETRIC_REPRESENTATION_ITEM()
RATIONAL_B_SPLINE_SURFACE(((1.02018382473742,0.324498219413098,1.02018382471995),
(1.00401234488981,0.865716921710379,1.00401234488634),(1.00033622856794,
0.988747276629715,1.00033622856764),(1.,1.,1.)))
REPRESENTATION_ITEM('')
SURFACE()
);
#2943=(
BOUNDED_SURFACE()
B_SPLINE_SURFACE(3,2,((#398832,#398833,#398834),(#398835,#398836,#398837),
(#398838,#398839,#398840),(#398841,#398842,#398843)),.UNSPECIFIED.,.F.,
 .F.,.F.)
B_SPLINE_SURFACE_WITH_KNOTS((4,4),(3,3),(0.00137194782501028,0.00149814269699235),
(0.,1.),.UNSPECIFIED.)
GEOMETRIC_REPRESENTATION_ITEM()
RATIONAL_B_SPLINE_SURFACE(((1.,0.815158509402317,1.),(1.,0.81617904414817,
1.),(1.,0.817226308119926,1.),(1.,0.818301939488808,1.)))
REPRESENTATION_ITEM('')
SURFACE()
);
#2944=(
BOUNDED_SURFACE()
B_SPLINE_SURFACE(3,2,((#398887,#398888,#398889),(#398890,#398891,#398892),
(#398893,#398894,#398895),(#398896,#398897,#398898)),.UNSPECIFIED.,.F.,
 .F.,.F.)
B_SPLINE_SURFACE_WITH_KNOTS((4,4),(3,3),(1.55009486301137E-5,4.92065510474438E-5),
(-8.13759514719951E-5,1.),.UNSPECIFIED.)
GEOMETRIC_REPRESENTATION_ITEM()
RATIONAL_B_SPLINE_SURFACE(((1.00002372912335,0.854200639599683,1.),(1.00001423585993,
0.912530301180541,1.),(1.00000710550471,0.956341495377434,1.),(1.00001238975908,
0.923873338137023,1.)))
REPRESENTATION_ITEM('')
SURFACE()
);
#2945=(
BOUNDED_SURFACE()
B_SPLINE_SURFACE(3,2,((#398902,#398903,#398904),(#398905,#398906,#398907),
(#398908,#398909,#398910),(#398911,#398912,#398913)),.UNSPECIFIED.,.F.,
 .F.,.F.)
B_SPLINE_SURFACE_WITH_KNOTS((4,4),(3,3),(-3.39934179457794E-6,3.73927597403563E-5),
(-0.00186004067477698,1.00069373317471),.UNSPECIFIED.)
GEOMETRIC_REPRESENTATION_ITEM()
RATIONAL_B_SPLINE_SURFACE(((1.00072100136078,0.80605196387518,1.00026859642703),
(1.00060048440173,0.838470803558503,1.00022369994506),(1.00053106448812,
0.857144632272239,1.00019783877228),(1.0005451507287,0.853355459538978,
1.00020308635446)))
REPRESENTATION_ITEM('')
SURFACE()
);
#2946=(
BOUNDED_SURFACE()
B_SPLINE_SURFACE(3,2,((#398915,#398916,#398917),(#398918,#398919,#398920),
(#398921,#398922,#398923),(#398924,#398925,#398926)),.UNSPECIFIED.,.F.,
 .F.,.F.)
B_SPLINE_SURFACE_WITH_KNOTS((4,4),(3,3),(-1.0842021724855E-19,9.54361881492173E-5),
(0.,1.),.UNSPECIFIED.)
GEOMETRIC_REPRESENTATION_ITEM()
RATIONAL_B_SPLINE_SURFACE(((1.,0.816715621142054,1.),(1.,0.815907587407935,
1.),(1.,0.815115959345215,1.),(1.,0.814339887349195,1.)))
REPRESENTATION_ITEM('')
SURFACE()
);
#2947=(
BOUNDED_SURFACE()
B_SPLINE_SURFACE(3,2,((#398928,#398929,#398930),(#398931,#398932,#398933),
(#398934,#398935,#398936),(#398937,#398938,#398939)),.UNSPECIFIED.,.F.,
 .F.,.F.)
B_SPLINE_SURFACE_WITH_KNOTS((4,4),(3,3),(-1.8126505071242E-19,4.68197758448207E-5),
(0.,1.),.UNSPECIFIED.)
GEOMETRIC_REPRESENTATION_ITEM()
RATIONAL_B_SPLINE_SURFACE(((1.,0.816715621142049,1.),(1.,0.953638980025206,
1.),(1.,0.954506925408054,1.),(1.,0.816715621142056,1.)))
REPRESENTATION_ITEM('')
SURFACE()
);
#2948=(
BOUNDED_SURFACE()
B_SPLINE_SURFACE(3,2,((#398941,#398942,#398943),(#398944,#398945,#398946),
(#398947,#398948,#398949),(#398950,#398951,#398952)),.UNSPECIFIED.,.F.,
 .F.,.F.)
B_SPLINE_SURFACE_WITH_KNOTS((4,4),(3,3),(2.16840434497101E-19,9.54361881492176E-5),
(0.,1.),.UNSPECIFIED.)
GEOMETRIC_REPRESENTATION_ITEM()
RATIONAL_B_SPLINE_SURFACE(((1.,0.814339887349194,1.),(1.,0.815115959345205,
1.),(1.,0.815907587407941,1.),(1.,0.816715621142049,1.)))
REPRESENTATION_ITEM('')
SURFACE()
);
#2949=(
BOUNDED_SURFACE()
B_SPLINE_SURFACE(3,2,((#398954,#398955,#398956),(#398957,#398958,#398959),
(#398960,#398961,#398962),(#398963,#398964,#398965)),.UNSPECIFIED.,.F.,
 .F.,.F.)
B_SPLINE_SURFACE_WITH_KNOTS((4,4),(3,3),(-3.39528393502485E-6,3.7348123285274E-5),
(-0.00165018033347468,1.),.UNSPECIFIED.)
GEOMETRIC_REPRESENTATION_ITEM()
RATIONAL_B_SPLINE_SURFACE(((1.00048354385571,0.853487571660368,1.),(1.00047110510926,
0.857256476851433,1.),(1.00053193201114,0.838826096655843,1.),(1.00063970687733,
0.80617061531005,0.999999999999999)))
REPRESENTATION_ITEM('')
SURFACE()
);
#2950=(
BOUNDED_SURFACE()
B_SPLINE_SURFACE(3,2,((#398969,#398970,#398971),(#398972,#398973,#398974),
(#398975,#398976,#398977),(#398978,#398979,#398980)),.UNSPECIFIED.,.F.,
 .F.,.F.)
B_SPLINE_SURFACE_WITH_KNOTS((4,4),(3,3),(2.02993869230511E-5,5.39756952687125E-5),
(-0.000116281069576731,1.),.UNSPECIFIED.)
GEOMETRIC_REPRESENTATION_ITEM()
RATIONAL_B_SPLINE_SURFACE(((1.00001770479725,0.923870681143036,1.),(1.00001014104056,
0.956394275543457,1.),(1.00002037300272,0.912397594905648,1.),(1.00003390859459,
0.854195550869787,1.)))
REPRESENTATION_ITEM('')
SURFACE()
);
#2951=(
BOUNDED_SURFACE()
B_SPLINE_SURFACE(3,2,((#399073,#399074,#399075),(#399076,#399077,#399078),
(#399079,#399080,#399081),(#399082,#399083,#399084)),.UNSPECIFIED.,.F.,
 .F.,.F.)
B_SPLINE_SURFACE_WITH_KNOTS((4,4),(3,3),(0.00135801595889393,0.00148409170619832),
(0.,1.),.UNSPECIFIED.)
GEOMETRIC_REPRESENTATION_ITEM()
RATIONAL_B_SPLINE_SURFACE(((1.,0.818301933966439,1.),(1.,0.817226613172357,
1.),(1.,0.816179643373936,1.),(1.,0.815159387863655,1.)))
REPRESENTATION_ITEM('')
SURFACE()
);
#2952=(
BOUNDED_SURFACE()
B_SPLINE_SURFACE(3,2,((#399123,#399124,#399125),(#399126,#399127,#399128),
(#399129,#399130,#399131),(#399132,#399133,#399134)),.UNSPECIFIED.,.F.,
 .F.,.F.)
B_SPLINE_SURFACE_WITH_KNOTS((4,4),(3,3),(-1.54744435122104E-6,1.54744435122105E-5),
(-0.015169898368822,1.01516989835412),.UNSPECIFIED.)
GEOMETRIC_REPRESENTATION_ITEM()
RATIONAL_B_SPLINE_SURFACE(((1.02018382473861,0.324498219413095,1.02018382471876),
(1.00401234489005,0.865716921710323,1.00401234488611),(1.00033622856795,
0.98874727662973,1.00033622856762),(1.,1.,1.)))
REPRESENTATION_ITEM('')
SURFACE()
);
#2953=(
BOUNDED_SURFACE()
B_SPLINE_SURFACE(3,2,((#399136,#399137,#399138),(#399139,#399140,#399141),
(#399142,#399143,#399144),(#399145,#399146,#399147)),.UNSPECIFIED.,.F.,
 .F.,.F.)
B_SPLINE_SURFACE_WITH_KNOTS((4,4),(3,3),(0.00137194782501028,0.00149814269699235),
(0.,1.),.UNSPECIFIED.)
GEOMETRIC_REPRESENTATION_ITEM()
RATIONAL_B_SPLINE_SURFACE(((1.,0.815158509402313,1.),(1.,0.816179044148173,
1.),(1.,0.817226308119917,1.),(1.,0.818301939488807,1.)))
REPRESENTATION_ITEM('')
SURFACE()
);
#2954=(
BOUNDED_SURFACE()
B_SPLINE_SURFACE(3,2,((#399191,#399192,#399193),(#399194,#399195,#399196),
(#399197,#399198,#399199),(#399200,#399201,#399202)),.UNSPECIFIED.,.F.,
 .F.,.F.)
B_SPLINE_SURFACE_WITH_KNOTS((4,4),(3,3),(1.55009486301138E-5,4.92065510474443E-5),
(-8.13759510935406E-5,1.),.UNSPECIFIED.)
GEOMETRIC_REPRESENTATION_ITEM()
RATIONAL_B_SPLINE_SURFACE(((1.00002372912324,0.854200639599743,1.),(1.00001423585987,
0.912530301180569,1.),(1.00000710550467,0.956341495377446,1.),(1.00001238975903,
0.923873338137053,1.)))
REPRESENTATION_ITEM('')
SURFACE()
);
#2955=(
BOUNDED_SURFACE()
B_SPLINE_SURFACE(3,2,((#399206,#399207,#399208),(#399209,#399210,#399211),
(#399212,#399213,#399214),(#399215,#399216,#399217)),.UNSPECIFIED.,.F.,
 .F.,.F.)
B_SPLINE_SURFACE_WITH_KNOTS((4,4),(3,3),(-3.39934179457821E-6,3.73927597403565E-5),
(-0.00186004067401852,1.00069373317405),.UNSPECIFIED.)
GEOMETRIC_REPRESENTATION_ITEM()
RATIONAL_B_SPLINE_SURFACE(((1.00072100136048,0.80605196387546,1.00026859642678),
(1.00060048440149,0.838470803558704,1.00022369994485),(1.0005310644879,
0.85714463227246,1.0001978387721),(1.00054515072847,0.853355459539171,1.00020308635427)))
REPRESENTATION_ITEM('')
SURFACE()
);
#2956=(
BOUNDED_SURFACE()
B_SPLINE_SURFACE(3,2,((#399219,#399220,#399221),(#399222,#399223,#399224),
(#399225,#399226,#399227),(#399228,#399229,#399230)),.UNSPECIFIED.,.F.,
 .F.,.F.)
B_SPLINE_SURFACE_WITH_KNOTS((4,4),(3,3),(-1.62630325872826E-19,9.54361881492172E-5),
(0.,1.),.UNSPECIFIED.)
GEOMETRIC_REPRESENTATION_ITEM()
RATIONAL_B_SPLINE_SURFACE(((1.,0.816715621142047,1.),(1.,0.815907587407934,
1.),(1.,0.815115959345204,1.),(1.,0.814339887349192,1.)))
REPRESENTATION_ITEM('')
SURFACE()
);
#2957=(
BOUNDED_SURFACE()
B_SPLINE_SURFACE(3,2,((#399232,#399233,#399234),(#399235,#399236,#399237),
(#399238,#399239,#399240),(#399241,#399242,#399243)),.UNSPECIFIED.,.F.,
 .F.,.F.)
B_SPLINE_SURFACE_WITH_KNOTS((4,4),(3,3),(-1.89735380184963E-19,4.68197758448202E-5),
(0.,1.),.UNSPECIFIED.)
GEOMETRIC_REPRESENTATION_ITEM()
RATIONAL_B_SPLINE_SURFACE(((1.,0.816715621142049,1.),(1.,0.953638980025202,
1.),(1.,0.954506925408058,1.),(1.,0.816715621142054,1.)))
REPRESENTATION_ITEM('')
SURFACE()
);
#2958=(
BOUNDED_SURFACE()
B_SPLINE_SURFACE(3,2,((#399245,#399246,#399247),(#399248,#399249,#399250),
(#399251,#399252,#399253),(#399254,#399255,#399256)),.UNSPECIFIED.,.F.,
 .F.,.F.)
B_SPLINE_SURFACE_WITH_KNOTS((4,4),(3,3),(-5.42101086242752E-20,9.54361881492178E-5),
(0.,1.),.UNSPECIFIED.)
GEOMETRIC_REPRESENTATION_ITEM()
RATIONAL_B_SPLINE_SURFACE(((1.,0.81433988734919,1.),(1.,0.815115959345203,
1.),(1.,0.815907587407937,1.),(1.,0.816715621142049,1.)))
REPRESENTATION_ITEM('')
SURFACE()
);
#2959=(
BOUNDED_SURFACE()
B_SPLINE_SURFACE(3,2,((#399258,#399259,#399260),(#399261,#399262,#399263),
(#399264,#399265,#399266),(#399267,#399268,#399269)),.UNSPECIFIED.,.F.,
 .F.,.F.)
B_SPLINE_SURFACE_WITH_KNOTS((4,4),(3,3),(-3.39528393502489E-6,3.73481232852725E-5),
(-0.00165018033329913,1.),.UNSPECIFIED.)
GEOMETRIC_REPRESENTATION_ITEM()
RATIONAL_B_SPLINE_SURFACE(((1.00048354385566,0.853487571660391,1.),(1.00047110510921,
0.857256476851463,1.),(1.00053193201108,0.838826096655849,1.),(1.00063970687726,
0.80617061531011,0.999999999999999)))
REPRESENTATION_ITEM('')
SURFACE()
);
#2960=(
BOUNDED_SURFACE()
B_SPLINE_SURFACE(3,2,((#399273,#399274,#399275),(#399276,#399277,#399278),
(#399279,#399280,#399281),(#399282,#399283,#399284)),.UNSPECIFIED.,.F.,
 .F.,.F.)
B_SPLINE_SURFACE_WITH_KNOTS((4,4),(3,3),(2.02993869230512E-5,5.39756952687125E-5),
(-0.000116281069426136,1.),.UNSPECIFIED.)
GEOMETRIC_REPRESENTATION_ITEM()
RATIONAL_B_SPLINE_SURFACE(((1.00001770479722,0.92387068114305,1.),(1.00001014104055,
0.956394275543467,1.),(1.0000203730027,0.912397594905656,1.),(1.00003390859454,
0.854195550869809,1.)))
REPRESENTATION_ITEM('')
SURFACE()
);
#2961=(
BOUNDED_SURFACE()
B_SPLINE_SURFACE(3,2,((#399377,#399378,#399379),(#399380,#399381,#399382),
(#399383,#399384,#399385),(#399386,#399387,#399388)),.UNSPECIFIED.,.F.,
 .F.,.F.)
B_SPLINE_SURFACE_WITH_KNOTS((4,4),(3,3),(0.00135801595889393,0.00148409170619832),
(0.,1.),.UNSPECIFIED.)
GEOMETRIC_REPRESENTATION_ITEM()
RATIONAL_B_SPLINE_SURFACE(((1.,0.818301933966445,1.),(1.,0.817226613172349,
1.),(1.,0.816179643373958,1.),(1.,0.815159387863658,1.)))
REPRESENTATION_ITEM('')
SURFACE()
);
#2962=(
BOUNDED_SURFACE()
B_SPLINE_SURFACE(3,2,((#399427,#399428,#399429),(#399430,#399431,#399432),
(#399433,#399434,#399435),(#399436,#399437,#399438)),.UNSPECIFIED.,.F.,
 .F.,.F.)
B_SPLINE_SURFACE_WITH_KNOTS((4,4),(3,3),(3.91752738105114E-20,1.54744435122074E-5),
(0.,1.),.UNSPECIFIED.)
GEOMETRIC_REPRESENTATION_ITEM()
RATIONAL_B_SPLINE_SURFACE(((1.,0.478041569704954,1.),(1.,0.890533857552083,
1.),(1.,0.990075913815909,1.),(1.,1.,1.)))
REPRESENTATION_ITEM('')
SURFACE()
);
#2963=(
BOUNDED_SURFACE()
B_SPLINE_SURFACE(3,2,((#399440,#399441,#399442),(#399443,#399444,#399445),
(#399446,#399447,#399448),(#399449,#399450,#399451)),.UNSPECIFIED.,.F.,
 .F.,.F.)
B_SPLINE_SURFACE_WITH_KNOTS((4,4),(3,3),(0.00137194782501028,0.00149814269699235),
(0.,1.),.UNSPECIFIED.)
GEOMETRIC_REPRESENTATION_ITEM()
RATIONAL_B_SPLINE_SURFACE(((1.,0.815158509402317,1.),(1.,0.816179044148163,
1.),(1.,0.817226308119927,1.),(1.,0.818301939488798,1.)))
REPRESENTATION_ITEM('')
SURFACE()
);
#2964=(
BOUNDED_SURFACE()
B_SPLINE_SURFACE(3,2,((#399495,#399496,#399497),(#399498,#399499,#399500),
(#399501,#399502,#399503),(#399504,#399505,#399506)),.UNSPECIFIED.,.F.,
 .F.,.F.)
B_SPLINE_SURFACE_WITH_KNOTS((4,4),(3,3),(1.55009486301137E-5,4.92065510474427E-5),
(-8.13759517743486E-5,1.),.UNSPECIFIED.)
GEOMETRIC_REPRESENTATION_ITEM()
RATIONAL_B_SPLINE_SURFACE(((1.00002372912344,0.854200639599642,1.),(1.00001423585999,
0.912530301180501,1.),(1.00000710550473,0.95634149537743,1.),(1.00001238975913,
0.923873338136998,1.)))
REPRESENTATION_ITEM('')
SURFACE()
);
#2965=(
BOUNDED_SURFACE()
B_SPLINE_SURFACE(3,2,((#399510,#399511,#399512),(#399513,#399514,#399515),
(#399516,#399517,#399518),(#399519,#399520,#399521)),.UNSPECIFIED.,.F.,
 .F.,.F.)
B_SPLINE_SURFACE_WITH_KNOTS((4,4),(3,3),(-3.39934179457844E-6,3.73927597403567E-5),
(-0.00186004067380532,1.00069373317436),.UNSPECIFIED.)
GEOMETRIC_REPRESENTATION_ITEM()
RATIONAL_B_SPLINE_SURFACE(((1.0007210013604,0.806051963875427,1.00026859642689),
(1.00060048440142,0.838470803558702,1.00022369994494),(1.00053106448784,
0.857144632272448,1.00019783877218),(1.00054515072841,0.853355459539161,
1.00020308635436)))
REPRESENTATION_ITEM('')
SURFACE()
);
#2966=(
BOUNDED_SURFACE()
B_SPLINE_SURFACE(3,2,((#399523,#399524,#399525),(#399526,#399527,#399528),
(#399529,#399530,#399531),(#399532,#399533,#399534)),.UNSPECIFIED.,.F.,
 .F.,.F.)
B_SPLINE_SURFACE_WITH_KNOTS((4,4),(3,3),(-5.42101086242752E-20,9.54361881492172E-5),
(0.,1.),.UNSPECIFIED.)
GEOMETRIC_REPRESENTATION_ITEM()
RATIONAL_B_SPLINE_SURFACE(((1.,0.816715621142047,1.),(1.,0.815907587407954,
1.),(1.,0.815115959345199,1.),(1.,0.814339887349199,1.)))
REPRESENTATION_ITEM('')
SURFACE()
);
#2967=(
BOUNDED_SURFACE()
B_SPLINE_SURFACE(3,2,((#399536,#399537,#399538),(#399539,#399540,#399541),
(#399542,#399543,#399544),(#399545,#399546,#399547)),.UNSPECIFIED.,.F.,
 .F.,.F.)
B_SPLINE_SURFACE_WITH_KNOTS((4,4),(3,3),(-4.60785923306339E-19,4.68197758448207E-5),
(0.,1.),.UNSPECIFIED.)
GEOMETRIC_REPRESENTATION_ITEM()
RATIONAL_B_SPLINE_SURFACE(((1.,0.816715621142045,1.),(1.,0.953638980025201,
1.),(1.,0.954506925408062,1.),(1.,0.816715621142047,1.)))
REPRESENTATION_ITEM('')
SURFACE()
);
#2968=(
BOUNDED_SURFACE()
B_SPLINE_SURFACE(3,2,((#399549,#399550,#399551),(#399552,#399553,#399554),
(#399555,#399556,#399557),(#399558,#399559,#399560)),.UNSPECIFIED.,.F.,
 .F.,.F.)
B_SPLINE_SURFACE_WITH_KNOTS((4,4),(3,3),(-1.0842021724855E-19,9.54361881492174E-5),
(0.,1.),.UNSPECIFIED.)
GEOMETRIC_REPRESENTATION_ITEM()
RATIONAL_B_SPLINE_SURFACE(((1.,0.814339887349193,1.),(1.,0.815115959345205,
1.),(1.,0.815907587407938,1.),(1.,0.816715621142051,1.)))
REPRESENTATION_ITEM('')
SURFACE()
);
#2969=(
BOUNDED_SURFACE()
B_SPLINE_SURFACE(3,2,((#399562,#399563,#399564),(#399565,#399566,#399567),
(#399568,#399569,#399570),(#399571,#399572,#399573)),.UNSPECIFIED.,.F.,
 .F.,.F.)
B_SPLINE_SURFACE_WITH_KNOTS((4,4),(3,3),(-3.39528393502485E-6,3.73481232852737E-5),
(-0.00165018033257718,1.),.UNSPECIFIED.)
GEOMETRIC_REPRESENTATION_ITEM()
RATIONAL_B_SPLINE_SURFACE(((1.00048354385545,0.853487571660499,1.),(1.000471105109,
0.85725647685156,1.),(1.00053193201085,0.838826096655988,1.),(1.00063970687698,
0.806170615310227,1.)))
REPRESENTATION_ITEM('')
SURFACE()
);
#2970=(
BOUNDED_SURFACE()
B_SPLINE_SURFACE(3,2,((#399577,#399578,#399579),(#399580,#399581,#399582),
(#399583,#399584,#399585),(#399586,#399587,#399588)),.UNSPECIFIED.,.F.,
 .F.,.F.)
B_SPLINE_SURFACE_WITH_KNOTS((4,4),(3,3),(2.0299386923051E-5,5.39756952687121E-5),
(-0.000116281070730535,1.),.UNSPECIFIED.)
GEOMETRIC_REPRESENTATION_ITEM()
RATIONAL_B_SPLINE_SURFACE(((1.00001770479742,0.923870681142948,1.),(1.00001014104066,
0.9563942755434,1.),(1.00002037300293,0.912397594905555,1.),(1.00003390859492,
0.854195550869617,1.)))
REPRESENTATION_ITEM('')
SURFACE()
);
#2971=(
BOUNDED_SURFACE()
B_SPLINE_SURFACE(3,2,((#399681,#399682,#399683),(#399684,#399685,#399686),
(#399687,#399688,#399689),(#399690,#399691,#399692)),.UNSPECIFIED.,.F.,
 .F.,.F.)
B_SPLINE_SURFACE_WITH_KNOTS((4,4),(3,3),(0.00135801595889393,0.00148409170619832),
(0.,1.),.UNSPECIFIED.)
GEOMETRIC_REPRESENTATION_ITEM()
RATIONAL_B_SPLINE_SURFACE(((1.,0.818301933966444,1.),(1.,0.817226613172335,
1.),(1.,0.816179643373969,1.),(1.,0.815159387863651,1.)))
REPRESENTATION_ITEM('')
SURFACE()
);
#2972=(
BOUNDED_SURFACE()
B_SPLINE_SURFACE(3,2,((#399731,#399732,#399733),(#399734,#399735,#399736),
(#399737,#399738,#399739),(#399740,#399741,#399742)),.UNSPECIFIED.,.F.,
 .F.,.F.)
B_SPLINE_SURFACE_WITH_KNOTS((4,4),(3,3),(-1.54744435122074E-6,1.54744435122078E-5),
(-0.0151698983613399,1.01516989836114),.UNSPECIFIED.)
GEOMETRIC_REPRESENTATION_ITEM()
RATIONAL_B_SPLINE_SURFACE(((1.02018382472851,0.324498219413358,1.02018382472825),
(1.00401234488804,0.865716921710615,1.00401234488799),(1.00033622856779,
0.988747276629691,1.00033622856778),(1.,1.,1.)))
REPRESENTATION_ITEM('')
SURFACE()
);
#2973=(
BOUNDED_SURFACE()
B_SPLINE_SURFACE(3,2,((#399744,#399745,#399746),(#399747,#399748,#399749),
(#399750,#399751,#399752),(#399753,#399754,#399755)),.UNSPECIFIED.,.F.,
 .F.,.F.)
B_SPLINE_SURFACE_WITH_KNOTS((4,4),(3,3),(0.00137194782501028,0.00149814269699235),
(0.,1.),.UNSPECIFIED.)
GEOMETRIC_REPRESENTATION_ITEM()
RATIONAL_B_SPLINE_SURFACE(((1.,0.815158509402308,1.),(1.,0.816179044148165,
1.),(1.,0.817226308119931,1.),(1.,0.818301939488802,1.)))
REPRESENTATION_ITEM('')
SURFACE()
);
#2974=(
BOUNDED_SURFACE()
B_SPLINE_SURFACE(3,2,((#399799,#399800,#399801),(#399802,#399803,#399804),
(#399805,#399806,#399807),(#399808,#399809,#399810)),.UNSPECIFIED.,.F.,
 .F.,.F.)
B_SPLINE_SURFACE_WITH_KNOTS((4,4),(3,3),(1.55009486301137E-5,4.92065510474429E-5),
(-8.13759509738754E-5,1.),.UNSPECIFIED.)
GEOMETRIC_REPRESENTATION_ITEM()
RATIONAL_B_SPLINE_SURFACE(((1.00002372912321,0.854200639599766,1.),(1.00001423585985,
0.912530301180572,1.),(1.00000710550466,0.956341495377455,1.),(1.00001238975901,
0.923873338137061,1.)))
REPRESENTATION_ITEM('')
SURFACE()
);
#2975=(
BOUNDED_SURFACE()
B_SPLINE_SURFACE(3,2,((#399814,#399815,#399816),(#399817,#399818,#399819),
(#399820,#399821,#399822),(#399823,#399824,#399825)),.UNSPECIFIED.,.F.,
 .F.,.F.)
B_SPLINE_SURFACE_WITH_KNOTS((4,4),(3,3),(-3.39934179457793E-6,3.73927597403565E-5),
(-0.0018600406739492,1.00069373317436),.UNSPECIFIED.)
GEOMETRIC_REPRESENTATION_ITEM()
RATIONAL_B_SPLINE_SURFACE(((1.00072100136045,0.806051963875388,1.0002685964269),
(1.00060048440146,0.8384708035587,1.00022369994495),(1.00053106448788,0.857144632272405,
1.00019783877218),(1.00054515072845,0.853355459539143,1.00020308635436)))
REPRESENTATION_ITEM('')
SURFACE()
);
#2976=(
BOUNDED_SURFACE()
B_SPLINE_SURFACE(3,2,((#399827,#399828,#399829),(#399830,#399831,#399832),
(#399833,#399834,#399835),(#399836,#399837,#399838)),.UNSPECIFIED.,.F.,
 .F.,.F.)
B_SPLINE_SURFACE_WITH_KNOTS((4,4),(3,3),(1.0842021724855E-19,9.54361881492174E-5),
(0.,1.),.UNSPECIFIED.)
GEOMETRIC_REPRESENTATION_ITEM()
RATIONAL_B_SPLINE_SURFACE(((1.,0.816715621142051,1.),(1.,0.815907587407938,
1.),(1.,0.815115959345202,1.),(1.,0.814339887349196,1.)))
REPRESENTATION_ITEM('')
SURFACE()
);
#2977=(
BOUNDED_SURFACE()
B_SPLINE_SURFACE(3,2,((#399840,#399841,#399842),(#399843,#399844,#399845),
(#399846,#399847,#399848),(#399849,#399850,#399851)),.UNSPECIFIED.,.F.,
 .F.,.F.)
B_SPLINE_SURFACE_WITH_KNOTS((4,4),(3,3),(1.47383732822248E-19,4.68197758448205E-5),
(0.,1.),.UNSPECIFIED.)
GEOMETRIC_REPRESENTATION_ITEM()
RATIONAL_B_SPLINE_SURFACE(((1.,0.81671562114205,1.),(1.,0.953638980025207,
1.),(1.,0.95450692540805,1.),(1.,0.816715621142057,1.)))
REPRESENTATION_ITEM('')
SURFACE()
);
#2978=(
BOUNDED_SURFACE()
B_SPLINE_SURFACE(3,2,((#399853,#399854,#399855),(#399856,#399857,#399858),
(#399859,#399860,#399861),(#399862,#399863,#399864)),.UNSPECIFIED.,.F.,
 .F.,.F.)
B_SPLINE_SURFACE_WITH_KNOTS((4,4),(3,3),(1.0842021724855E-19,9.54361881492178E-5),
(0.,1.),.UNSPECIFIED.)
GEOMETRIC_REPRESENTATION_ITEM()
RATIONAL_B_SPLINE_SURFACE(((1.,0.814339887349195,1.),(1.,0.815115959345184,
1.),(1.,0.815907587407959,1.),(1.,0.81671562114205,1.)))
REPRESENTATION_ITEM('')
SURFACE()
);
#2979=(
BOUNDED_SURFACE()
B_SPLINE_SURFACE(3,2,((#399866,#399867,#399868),(#399869,#399870,#399871),
(#399872,#399873,#399874),(#399875,#399876,#399877)),.UNSPECIFIED.,.F.,
 .F.,.F.)
B_SPLINE_SURFACE_WITH_KNOTS((4,4),(3,3),(-3.3952839350249E-6,3.73481232852728E-5),
(-0.00165018033329724,1.),.UNSPECIFIED.)
GEOMETRIC_REPRESENTATION_ITEM()
RATIONAL_B_SPLINE_SURFACE(((1.00048354385566,0.853487571660387,1.),(1.00047110510921,
0.857256476851467,1.),(1.00053193201108,0.838826096655857,1.),(1.00063970687726,
0.806170615310098,1.)))
REPRESENTATION_ITEM('')
SURFACE()
);
#2980=(
BOUNDED_SURFACE()
B_SPLINE_SURFACE(3,2,((#399881,#399882,#399883),(#399884,#399885,#399886),
(#399887,#399888,#399889),(#399890,#399891,#399892)),.UNSPECIFIED.,.F.,
 .F.,.F.)
B_SPLINE_SURFACE_WITH_KNOTS((4,4),(3,3),(2.02993869230513E-5,5.39756952686905E-5),
(-0.000116281069768348,1.),.UNSPECIFIED.)
GEOMETRIC_REPRESENTATION_ITEM()
RATIONAL_B_SPLINE_SURFACE(((1.00001770479727,0.923870681143019,1.),(1.00001014104058,
0.956394275543429,1.),(1.00002037300276,0.912397594905682,1.),(1.00003390859464,
0.854195550869875,1.)))
REPRESENTATION_ITEM('')
SURFACE()
);
#2981=(
BOUNDED_SURFACE()
B_SPLINE_SURFACE(3,2,((#399985,#399986,#399987),(#399988,#399989,#399990),
(#399991,#399992,#399993),(#399994,#399995,#399996)),.UNSPECIFIED.,.F.,
 .F.,.F.)
B_SPLINE_SURFACE_WITH_KNOTS((4,4),(3,3),(0.00135801595889393,0.00148409170619832),
(0.,1.),.UNSPECIFIED.)
GEOMETRIC_REPRESENTATION_ITEM()
RATIONAL_B_SPLINE_SURFACE(((1.,0.818301933966446,1.),(1.,0.817226613172338,
1.),(1.,0.816179643373962,1.),(1.,0.815159387863655,1.)))
REPRESENTATION_ITEM('')
SURFACE()
);
#2982=(
BOUNDED_SURFACE()
B_SPLINE_SURFACE(3,2,((#400035,#400036,#400037),(#400038,#400039,#400040),
(#400041,#400042,#400043),(#400044,#400045,#400046)),.UNSPECIFIED.,.F.,
 .F.,.F.)
B_SPLINE_SURFACE_WITH_KNOTS((4,4),(3,3),(-1.54744435122077E-6,1.54744435122077E-5),
(-0.0151698983622635,1.0151698983599),.UNSPECIFIED.)
GEOMETRIC_REPRESENTATION_ITEM()
RATIONAL_B_SPLINE_SURFACE(((1.02018382472975,0.324498219413619,1.02018382472657),
(1.00401234488829,0.865716921710638,1.00401234488765),(1.00033622856781,
0.988747276629694,1.00033622856776),(1.,1.,1.)))
REPRESENTATION_ITEM('')
SURFACE()
);
#2983=(
BOUNDED_SURFACE()
B_SPLINE_SURFACE(3,2,((#400048,#400049,#400050),(#400051,#400052,#400053),
(#400054,#400055,#400056),(#400057,#400058,#400059)),.UNSPECIFIED.,.F.,
 .F.,.F.)
B_SPLINE_SURFACE_WITH_KNOTS((4,4),(3,3),(0.00137194782501028,0.00149814269699235),
(0.,1.),.UNSPECIFIED.)
GEOMETRIC_REPRESENTATION_ITEM()
RATIONAL_B_SPLINE_SURFACE(((1.,0.815158509402316,1.),(1.,0.816179044148169,
1.),(1.,0.817226308119926,1.),(1.,0.8183019394888,1.)))
REPRESENTATION_ITEM('')
SURFACE()
);
#2984=(
BOUNDED_SURFACE()
B_SPLINE_SURFACE(3,2,((#400103,#400104,#400105),(#400106,#400107,#400108),
(#400109,#400110,#400111),(#400112,#400113,#400114)),.UNSPECIFIED.,.F.,
 .F.,.F.)
B_SPLINE_SURFACE_WITH_KNOTS((4,4),(3,3),(1.55009486301137E-5,4.9206551047443E-5),
(-8.13759515176208E-5,1.),.UNSPECIFIED.)
GEOMETRIC_REPRESENTATION_ITEM()
RATIONAL_B_SPLINE_SURFACE(((1.00002372912337,0.85420063959968,1.),(1.00001423585994,
0.912530301180536,1.),(1.00000710550471,0.956341495377428,1.),(1.00001238975909,
0.923873338137019,1.)))
REPRESENTATION_ITEM('')
SURFACE()
);
#2985=(
BOUNDED_SURFACE()
B_SPLINE_SURFACE(3,2,((#400118,#400119,#400120),(#400121,#400122,#400123),
(#400124,#400125,#400126),(#400127,#400128,#400129)),.UNSPECIFIED.,.F.,
 .F.,.F.)
B_SPLINE_SURFACE_WITH_KNOTS((4,4),(3,3),(-3.39934179457841E-6,3.73927597403565E-5),
(-0.00186004067418672,1.00069373317461),.UNSPECIFIED.)
GEOMETRIC_REPRESENTATION_ITEM()
RATIONAL_B_SPLINE_SURFACE(((1.00072100136055,0.806051963875299,1.00026859642699),
(1.00060048440154,0.838470803558624,1.00022369994503),(1.00053106448795,
0.857144632272335,1.00019783877226),(1.00054515072852,0.853355459539078,
1.00020308635443)))
REPRESENTATION_ITEM('')
SURFACE()
);
#2986=(
BOUNDED_SURFACE()
B_SPLINE_SURFACE(3,2,((#400131,#400132,#400133),(#400134,#400135,#400136),
(#400137,#400138,#400139),(#400140,#400141,#400142)),.UNSPECIFIED.,.F.,
 .F.,.F.)
B_SPLINE_SURFACE_WITH_KNOTS((4,4),(3,3),(-1.62630325872826E-19,9.54361881492173E-5),
(0.,1.),.UNSPECIFIED.)
GEOMETRIC_REPRESENTATION_ITEM()
RATIONAL_B_SPLINE_SURFACE(((1.,0.816715621142052,1.),(1.,0.815907587407943,
1.),(1.,0.815115959345206,1.),(1.,0.814339887349198,1.)))
REPRESENTATION_ITEM('')
SURFACE()
);
#2987=(
BOUNDED_SURFACE()
B_SPLINE_SURFACE(3,2,((#400144,#400145,#400146),(#400147,#400148,#400149),
(#400150,#400151,#400152),(#400153,#400154,#400155)),.UNSPECIFIED.,.F.,
 .F.,.F.)
B_SPLINE_SURFACE_WITH_KNOTS((4,4),(3,3),(-1.86347248395946E-19,4.68197758448201E-5),
(0.,1.),.UNSPECIFIED.)
GEOMETRIC_REPRESENTATION_ITEM()
RATIONAL_B_SPLINE_SURFACE(((1.,0.81671562114205,1.),(1.,0.953638980025198,
1.),(1.,0.954506925408061,1.),(1.,0.816715621142052,1.)))
REPRESENTATION_ITEM('')
SURFACE()
);
#2988=(
BOUNDED_SURFACE()
B_SPLINE_SURFACE(3,2,((#400157,#400158,#400159),(#400160,#400161,#400162),
(#400163,#400164,#400165),(#400166,#400167,#400168)),.UNSPECIFIED.,.F.,
 .F.,.F.)
B_SPLINE_SURFACE_WITH_KNOTS((4,4),(3,3),(1.0842021724855E-19,9.54361881492174E-5),
(0.,1.),.UNSPECIFIED.)
GEOMETRIC_REPRESENTATION_ITEM()
RATIONAL_B_SPLINE_SURFACE(((1.,0.814339887349194,1.),(1.,0.815115959345208,
1.),(1.,0.815907587407941,1.),(1.,0.81671562114205,1.)))
REPRESENTATION_ITEM('')
SURFACE()
);
#2989=(
BOUNDED_SURFACE()
B_SPLINE_SURFACE(3,2,((#400170,#400171,#400172),(#400173,#400174,#400175),
(#400176,#400177,#400178),(#400179,#400180,#400181)),.UNSPECIFIED.,.F.,
 .F.,.F.)
B_SPLINE_SURFACE_WITH_KNOTS((4,4),(3,3),(-3.39528393502491E-6,3.73481232852729E-5),
(-0.00165018033330832,1.),.UNSPECIFIED.)
GEOMETRIC_REPRESENTATION_ITEM()
RATIONAL_B_SPLINE_SURFACE(((1.00048354385566,0.853487571660394,1.),(1.00047110510921,
0.857256476851454,1.),(1.00053193201108,0.838826096655882,1.),(1.00063970687726,
0.806170615310084,1.)))
REPRESENTATION_ITEM('')
SURFACE()
);
#2990=(
BOUNDED_SURFACE()
B_SPLINE_SURFACE(3,2,((#400185,#400186,#400187),(#400188,#400189,#400190),
(#400191,#400192,#400193),(#400194,#400195,#400196)),.UNSPECIFIED.,.F.,
 .F.,.F.)
B_SPLINE_SURFACE_WITH_KNOTS((4,4),(3,3),(2.02993869230508E-5,5.39756952687126E-5),
(-0.000116281069690976,1.),.UNSPECIFIED.)
GEOMETRIC_REPRESENTATION_ITEM()
RATIONAL_B_SPLINE_SURFACE(((1.00001770479726,0.923870681143028,1.),(1.00001014104057,
0.956394275543463,1.),(1.00002037300274,0.912397594905633,1.),(1.00003390859462,
0.854195550869773,1.)))
REPRESENTATION_ITEM('')
SURFACE()
);
#2991=(
BOUNDED_SURFACE()
B_SPLINE_SURFACE(3,2,((#400289,#400290,#400291),(#400292,#400293,#400294),
(#400295,#400296,#400297),(#400298,#400299,#400300)),.UNSPECIFIED.,.F.,
 .F.,.F.)
B_SPLINE_SURFACE_WITH_KNOTS((4,4),(3,3),(0.00135801595889393,0.00148409170619832),
(0.,1.),.UNSPECIFIED.)
GEOMETRIC_REPRESENTATION_ITEM()
RATIONAL_B_SPLINE_SURFACE(((1.,0.818301933966441,1.),(1.,0.817226613172331,
1.),(1.,0.816179643373969,1.),(1.,0.815159387863649,1.)))
REPRESENTATION_ITEM('')
SURFACE()
);
#2992=(
BOUNDED_SURFACE()
B_SPLINE_SURFACE(3,2,((#400339,#400340,#400341),(#400342,#400343,#400344),
(#400345,#400346,#400347),(#400348,#400349,#400350)),.UNSPECIFIED.,.F.,
 .F.,.F.)
B_SPLINE_SURFACE_WITH_KNOTS((4,4),(3,3),(-1.54744435121998E-6,1.54744435122074E-5),
(0.,1.01516989835084),.UNSPECIFIED.)
GEOMETRIC_REPRESENTATION_ITEM()
RATIONAL_B_SPLINE_SURFACE(((1.,0.334740937363976,1.02018382471433),(1.,
0.867753072814783,1.00401234488522),(1.,0.98891790308095,1.00033622856755),
(1.,1.,1.)))
REPRESENTATION_ITEM('')
SURFACE()
);
#2993=(
BOUNDED_SURFACE()
B_SPLINE_SURFACE(3,2,((#400352,#400353,#400354),(#400355,#400356,#400357),
(#400358,#400359,#400360),(#400361,#400362,#400363)),.UNSPECIFIED.,.F.,
 .F.,.F.)
B_SPLINE_SURFACE_WITH_KNOTS((4,4),(3,3),(0.00137194782501028,0.00149814269699235),
(0.,1.),.UNSPECIFIED.)
GEOMETRIC_REPRESENTATION_ITEM()
RATIONAL_B_SPLINE_SURFACE(((1.,0.815158509402317,1.),(1.,0.816179044148169,
1.),(1.,0.81722630811993,1.),(1.,0.818301939488802,1.)))
REPRESENTATION_ITEM('')
SURFACE()
);
#2994=(
BOUNDED_SURFACE()
B_SPLINE_SURFACE(3,2,((#400407,#400408,#400409),(#400410,#400411,#400412),
(#400413,#400414,#400415),(#400416,#400417,#400418)),.UNSPECIFIED.,.F.,
 .F.,.F.)
B_SPLINE_SURFACE_WITH_KNOTS((4,4),(3,3),(1.55009486301137E-5,4.92065510474433E-5),
(-8.1375951657446E-5,1.),.UNSPECIFIED.)
GEOMETRIC_REPRESENTATION_ITEM()
RATIONAL_B_SPLINE_SURFACE(((1.00002372912341,0.854200639599655,1.),(1.00001423585997,
0.912530301180528,1.),(1.00000710550472,0.956341495377426,1.),(1.00001238975911,
0.92387333813701,1.)))
REPRESENTATION_ITEM('')
SURFACE()
);
#2995=(
BOUNDED_SURFACE()
B_SPLINE_SURFACE(3,2,((#400422,#400423,#400424),(#400425,#400426,#400427),
(#400428,#400429,#400430),(#400431,#400432,#400433)),.UNSPECIFIED.,.F.,
 .F.,.F.)
B_SPLINE_SURFACE_WITH_KNOTS((4,4),(3,3),(-3.39934179457807E-6,3.73927597403566E-5),
(-0.00186004067478061,1.00069373317481),.UNSPECIFIED.)
GEOMETRIC_REPRESENTATION_ITEM()
RATIONAL_B_SPLINE_SURFACE(((1.00072100136078,0.806051963875142,1.00026859642707),
(1.00060048440173,0.838470803558472,1.00022369994509),(1.00053106448812,
0.857144632272242,1.00019783877231),(1.0005451507287,0.853355459538941,
1.00020308635449)))
REPRESENTATION_ITEM('')
SURFACE()
);
#2996=(
BOUNDED_SURFACE()
B_SPLINE_SURFACE(3,2,((#400435,#400436,#400437),(#400438,#400439,#400440),
(#400441,#400442,#400443),(#400444,#400445,#400446)),.UNSPECIFIED.,.F.,
 .F.,.F.)
B_SPLINE_SURFACE_WITH_KNOTS((4,4),(3,3),(0.,9.54361881492173E-5),(0.,1.),
 .UNSPECIFIED.)
GEOMETRIC_REPRESENTATION_ITEM()
RATIONAL_B_SPLINE_SURFACE(((1.,0.81671562114205,1.),(1.,0.815907587407937,
1.),(1.,0.815115959345202,1.),(1.,0.814339887349193,1.)))
REPRESENTATION_ITEM('')
SURFACE()
);
#2997=(
BOUNDED_SURFACE()
B_SPLINE_SURFACE(3,2,((#400448,#400449,#400450),(#400451,#400452,#400453),
(#400454,#400455,#400456),(#400457,#400458,#400459)),.UNSPECIFIED.,.F.,
 .F.,.F.)
B_SPLINE_SURFACE_WITH_KNOTS((4,4),(3,3),(4.47233396150271E-19,4.68197758448205E-5),
(0.,1.),.UNSPECIFIED.)
GEOMETRIC_REPRESENTATION_ITEM()
RATIONAL_B_SPLINE_SURFACE(((1.,0.81671562114205,1.),(1.,0.953638980025206,
1.),(1.,0.954506925408054,1.),(1.,0.816715621142053,1.)))
REPRESENTATION_ITEM('')
SURFACE()
);
#2998=(
BOUNDED_SURFACE()
B_SPLINE_SURFACE(3,2,((#400461,#400462,#400463),(#400464,#400465,#400466),
(#400467,#400468,#400469),(#400470,#400471,#400472)),.UNSPECIFIED.,.F.,
 .F.,.F.)
B_SPLINE_SURFACE_WITH_KNOTS((4,4),(3,3),(-2.16840434497101E-19,9.54361881492177E-5),
(0.,1.),.UNSPECIFIED.)
GEOMETRIC_REPRESENTATION_ITEM()
RATIONAL_B_SPLINE_SURFACE(((1.,0.814339887349193,1.),(1.,0.815115959345207,
1.),(1.,0.815907587407941,1.),(1.,0.81671562114205,1.)))
REPRESENTATION_ITEM('')
SURFACE()
);
#2999=(
BOUNDED_SURFACE()
B_SPLINE_SURFACE(3,2,((#400474,#400475,#400476),(#400477,#400478,#400479),
(#400480,#400481,#400482),(#400483,#400484,#400485)),.UNSPECIFIED.,.F.,
 .F.,.F.)
B_SPLINE_SURFACE_WITH_KNOTS((4,4),(3,3),(-3.39528393502376E-6,3.73481232852733E-5),
(-0.00165018033265501,1.),.UNSPECIFIED.)
GEOMETRIC_REPRESENTATION_ITEM()
RATIONAL_B_SPLINE_SURFACE(((1.00048354385547,0.853487571660489,1.),(1.00047110510903,
0.857256476851551,1.),(1.00053193201087,0.838826096655975,1.),(1.00063970687701,
0.806170615310217,1.)))
REPRESENTATION_ITEM('')
SURFACE()
);
#3000=(
BOUNDED_SURFACE()
B_SPLINE_SURFACE(3,2,((#400489,#400490,#400491),(#400492,#400493,#400494),
(#400495,#400496,#400497),(#400498,#400499,#400500)),.UNSPECIFIED.,.F.,
 .F.,.F.)
B_SPLINE_SURFACE_WITH_KNOTS((4,4),(3,3),(2.02993869230507E-5,5.3975695268713E-5),
(-0.000116281069929633,1.),.UNSPECIFIED.)
GEOMETRIC_REPRESENTATION_ITEM()
RATIONAL_B_SPLINE_SURFACE(((1.0000177047973,0.923870681143012,1.),(1.00001014104059,
0.956394275543438,1.),(1.00002037300279,0.912397594905633,1.),(1.00003390859469,
0.854195550869724,1.)))
REPRESENTATION_ITEM('')
SURFACE()
);
#3001=(
BOUNDED_SURFACE()
B_SPLINE_SURFACE(3,2,((#400593,#400594,#400595),(#400596,#400597,#400598),
(#400599,#400600,#400601),(#400602,#400603,#400604)),.UNSPECIFIED.,.F.,
 .F.,.F.)
B_SPLINE_SURFACE_WITH_KNOTS((4,4),(3,3),(0.00135801595889393,0.00148409170619832),
(0.,1.),.UNSPECIFIED.)
GEOMETRIC_REPRESENTATION_ITEM()
RATIONAL_B_SPLINE_SURFACE(((1.,0.818301933966445,1.),(1.,0.817226613172345,
1.),(1.,0.816179643373948,1.),(1.,0.815159387863651,1.)))
REPRESENTATION_ITEM('')
SURFACE()
);
#3002=(
BOUNDED_SURFACE()
B_SPLINE_SURFACE(3,2,((#400643,#400644,#400645),(#400646,#400647,#400648),
(#400649,#400650,#400651),(#400652,#400653,#400654)),.UNSPECIFIED.,.F.,
 .F.,.F.)
B_SPLINE_SURFACE_WITH_KNOTS((4,4),(3,3),(-1.54744435122071E-6,1.5474443512207E-5),
(-0.0151698983637522,1.),.UNSPECIFIED.)
GEOMETRIC_REPRESENTATION_ITEM()
RATIONAL_B_SPLINE_SURFACE(((1.02018382473177,0.334740937355425,1.),(1.00401234488869,
0.867753072813156,1.),(1.00033622856784,0.988917903080815,1.),(1.,1.,1.)))
REPRESENTATION_ITEM('')
SURFACE()
);
#3003=(
BOUNDED_SURFACE()
B_SPLINE_SURFACE(3,2,((#400656,#400657,#400658),(#400659,#400660,#400661),
(#400662,#400663,#400664),(#400665,#400666,#400667)),.UNSPECIFIED.,.F.,
 .F.,.F.)
B_SPLINE_SURFACE_WITH_KNOTS((4,4),(3,3),(0.00137194782501028,0.00149814269699235),
(0.,1.),.UNSPECIFIED.)
GEOMETRIC_REPRESENTATION_ITEM()
RATIONAL_B_SPLINE_SURFACE(((1.,0.815158509402319,1.),(1.,0.816179044148169,
1.),(1.,0.817226308119925,1.),(1.,0.818301939488808,1.)))
REPRESENTATION_ITEM('')
SURFACE()
);
#3004=(
BOUNDED_SURFACE()
B_SPLINE_SURFACE(3,2,((#400711,#400712,#400713),(#400714,#400715,#400716),
(#400717,#400718,#400719),(#400720,#400721,#400722)),.UNSPECIFIED.,.F.,
 .F.,.F.)
B_SPLINE_SURFACE_WITH_KNOTS((4,4),(3,3),(1.55009486301137E-5,4.92065510474432E-5),
(-8.13759513806331E-5,1.),.UNSPECIFIED.)
GEOMETRIC_REPRESENTATION_ITEM()
RATIONAL_B_SPLINE_SURFACE(((1.00002372912333,0.854200639599697,1.),(1.00001423585992,
0.912530301180547,1.),(1.0000071055047,0.956341495377435,1.),(1.00001238975907,
0.92387333813703,1.)))
REPRESENTATION_ITEM('')
SURFACE()
);
#3005=(
BOUNDED_SURFACE()
B_SPLINE_SURFACE(3,2,((#400726,#400727,#400728),(#400729,#400730,#400731),
(#400732,#400733,#400734),(#400735,#400736,#400737)),.UNSPECIFIED.,.F.,
 .F.,.F.)
B_SPLINE_SURFACE_WITH_KNOTS((4,4),(3,3),(-3.39934179457817E-6,3.73927597403566E-5),
(-0.00186004067470975,1.00069373317475),.UNSPECIFIED.)
GEOMETRIC_REPRESENTATION_ITEM()
RATIONAL_B_SPLINE_SURFACE(((1.00072100136075,0.806051963875176,1.00026859642705),
(1.00060048440171,0.838470803558489,1.00022369994507),(1.0005310644881,
0.857144632272263,1.0001978387723),(1.00054515072868,0.853355459538963,
1.00020308635447)))
REPRESENTATION_ITEM('')
SURFACE()
);
#3006=(
BOUNDED_SURFACE()
B_SPLINE_SURFACE(3,2,((#400739,#400740,#400741),(#400742,#400743,#400744),
(#400745,#400746,#400747),(#400748,#400749,#400750)),.UNSPECIFIED.,.F.,
 .F.,.F.)
B_SPLINE_SURFACE_WITH_KNOTS((4,4),(3,3),(1.0842021724855E-19,9.54361881492173E-5),
(0.,1.),.UNSPECIFIED.)
GEOMETRIC_REPRESENTATION_ITEM()
RATIONAL_B_SPLINE_SURFACE(((1.,0.816715621142048,1.),(1.,0.815907587407936,
1.),(1.,0.815115959345214,1.),(1.,0.81433988734919,1.)))
REPRESENTATION_ITEM('')
SURFACE()
);
#3007=(
BOUNDED_SURFACE()
B_SPLINE_SURFACE(3,2,((#400752,#400753,#400754),(#400755,#400756,#400757),
(#400758,#400759,#400760),(#400761,#400762,#400763)),.UNSPECIFIED.,.F.,
 .F.,.F.)
B_SPLINE_SURFACE_WITH_KNOTS((4,4),(3,3),(1.01643953670516E-20,4.68197758448207E-5),
(0.,1.),.UNSPECIFIED.)
GEOMETRIC_REPRESENTATION_ITEM()
RATIONAL_B_SPLINE_SURFACE(((1.,0.816715621142052,1.),(1.,0.9536389800252,
1.),(1.,0.954506925408064,1.),(1.,0.816715621142051,1.)))
REPRESENTATION_ITEM('')
SURFACE()
);
#3008=(
BOUNDED_SURFACE()
B_SPLINE_SURFACE(3,2,((#400765,#400766,#400767),(#400768,#400769,#400770),
(#400771,#400772,#400773),(#400774,#400775,#400776)),.UNSPECIFIED.,.F.,
 .F.,.F.)
B_SPLINE_SURFACE_WITH_KNOTS((4,4),(3,3),(0.,9.5436188149218E-5),(0.,1.),
 .UNSPECIFIED.)
GEOMETRIC_REPRESENTATION_ITEM()
RATIONAL_B_SPLINE_SURFACE(((1.,0.814339887349194,1.),(1.,0.815115959345198,
1.),(1.,0.815907587407943,1.),(1.,0.816715621142052,1.)))
REPRESENTATION_ITEM('')
SURFACE()
);
#3009=(
BOUNDED_SURFACE()
B_SPLINE_SURFACE(3,2,((#400778,#400779,#400780),(#400781,#400782,#400783),
(#400784,#400785,#400786),(#400787,#400788,#400789)),.UNSPECIFIED.,.F.,
 .F.,.F.)
B_SPLINE_SURFACE_WITH_KNOTS((4,4),(3,3),(-3.39528393502483E-6,3.73481232852733E-5),
(-0.00165018033317789,1.),.UNSPECIFIED.)
GEOMETRIC_REPRESENTATION_ITEM()
RATIONAL_B_SPLINE_SURFACE(((1.00048354385562,0.853487571660412,1.),(1.00047110510918,
0.857256476851481,1.),(1.00053193201104,0.838826096655889,1.),(1.00063970687721,
0.806170615310112,1.)))
REPRESENTATION_ITEM('')
SURFACE()
);
#3010=(
BOUNDED_SURFACE()
B_SPLINE_SURFACE(3,2,((#400793,#400794,#400795),(#400796,#400797,#400798),
(#400799,#400800,#400801),(#400802,#400803,#400804)),.UNSPECIFIED.,.F.,
 .F.,.F.)
B_SPLINE_SURFACE_WITH_KNOTS((4,4),(3,3),(2.02993869230513E-5,5.39756952686903E-5),
(-0.000116281069625813,1.),.UNSPECIFIED.)
GEOMETRIC_REPRESENTATION_ITEM()
RATIONAL_B_SPLINE_SURFACE(((1.00001770479725,0.923870681143032,1.),(1.00001014104056,
0.956394275543427,1.),(1.00002037300273,0.912397594905699,1.),(1.0000339085946,
0.8541955508699,1.)))
REPRESENTATION_ITEM('')
SURFACE()
);
#3011=(
BOUNDED_SURFACE()
B_SPLINE_SURFACE(3,2,((#400897,#400898,#400899),(#400900,#400901,#400902),
(#400903,#400904,#400905),(#400906,#400907,#400908)),.UNSPECIFIED.,.F.,
 .F.,.F.)
B_SPLINE_SURFACE_WITH_KNOTS((4,4),(3,3),(0.00135801595889393,0.00148409170619832),
(0.,1.),.UNSPECIFIED.)
GEOMETRIC_REPRESENTATION_ITEM()
RATIONAL_B_SPLINE_SURFACE(((1.,0.818301933966444,1.),(1.,0.817226613172345,
1.),(1.,0.816179643373944,1.),(1.,0.815159387863653,1.)))
REPRESENTATION_ITEM('')
SURFACE()
);
#3012=(
BOUNDED_SURFACE()
B_SPLINE_SURFACE(3,2,((#400947,#400948,#400949),(#400950,#400951,#400952),
(#400953,#400954,#400955),(#400956,#400957,#400958)),.UNSPECIFIED.,.F.,
 .F.,.F.)
B_SPLINE_SURFACE_WITH_KNOTS((4,4),(3,3),(-1.54744435122073E-6,1.54744435122075E-5),
(-0.0151698983625013,1.),.UNSPECIFIED.)
GEOMETRIC_REPRESENTATION_ITEM()
RATIONAL_B_SPLINE_SURFACE(((1.02018382473008,0.334740937356303,1.),(1.00401234488835,
0.867753072813278,1.),(1.00033622856781,0.98891790308083,1.),(1.,1.,1.)))
REPRESENTATION_ITEM('')
SURFACE()
);
#3013=(
BOUNDED_SURFACE()
B_SPLINE_SURFACE(3,2,((#400960,#400961,#400962),(#400963,#400964,#400965),
(#400966,#400967,#400968),(#400969,#400970,#400971)),.UNSPECIFIED.,.F.,
 .F.,.F.)
B_SPLINE_SURFACE_WITH_KNOTS((4,4),(3,3),(0.00137194782501028,0.00149814269699235),
(0.,1.),.UNSPECIFIED.)
GEOMETRIC_REPRESENTATION_ITEM()
RATIONAL_B_SPLINE_SURFACE(((1.,0.815158509402321,1.),(1.,0.816179044148159,
1.),(1.,0.817226308119919,1.),(1.,0.818301939488811,1.)))
REPRESENTATION_ITEM('')
SURFACE()
);
#3014=(
BOUNDED_SURFACE()
B_SPLINE_SURFACE(3,2,((#401015,#401016,#401017),(#401018,#401019,#401020),
(#401021,#401022,#401023),(#401024,#401025,#401026)),.UNSPECIFIED.,.F.,
 .F.,.F.)
B_SPLINE_SURFACE_WITH_KNOTS((4,4),(3,3),(1.55009486301137E-5,4.92065510474426E-5),
(-8.13759514346884E-5,1.),.UNSPECIFIED.)
GEOMETRIC_REPRESENTATION_ITEM()
RATIONAL_B_SPLINE_SURFACE(((1.00002372912334,0.854200639599699,1.),(1.00001423585993,
0.912530301180536,1.),(1.0000071055047,0.956341495377432,1.),(1.00001238975908,
0.923873338137028,1.)))
REPRESENTATION_ITEM('')
SURFACE()
);
#3015=(
BOUNDED_SURFACE()
B_SPLINE_SURFACE(3,2,((#401030,#401031,#401032),(#401033,#401034,#401035),
(#401036,#401037,#401038),(#401039,#401040,#401041)),.UNSPECIFIED.,.F.,
 .F.,.F.)
B_SPLINE_SURFACE_WITH_KNOTS((4,4),(3,3),(-3.39934179457863E-6,3.73927597403564E-5),
(-0.00186004067392485,1.00069373317437),.UNSPECIFIED.)
GEOMETRIC_REPRESENTATION_ITEM()
RATIONAL_B_SPLINE_SURFACE(((1.00072100136044,0.806051963875394,1.0002685964269),
(1.00060048440145,0.838470803558699,1.00022369994495),(1.00053106448787,
0.8571446322724,1.00019783877219),(1.00054515072845,0.853355459539153,1.00020308635436)))
REPRESENTATION_ITEM('')
SURFACE()
);
#3016=(
BOUNDED_SURFACE()
B_SPLINE_SURFACE(3,2,((#401043,#401044,#401045),(#401046,#401047,#401048),
(#401049,#401050,#401051),(#401052,#401053,#401054)),.UNSPECIFIED.,.F.,
 .F.,.F.)
B_SPLINE_SURFACE_WITH_KNOTS((4,4),(3,3),(-5.42101086242752E-20,9.54361881492172E-5),
(0.,1.),.UNSPECIFIED.)
GEOMETRIC_REPRESENTATION_ITEM()
RATIONAL_B_SPLINE_SURFACE(((1.,0.81671562114205,1.),(1.,0.815907587407929,
1.),(1.,0.815115959345219,1.),(1.,0.814339887349188,1.)))
REPRESENTATION_ITEM('')
SURFACE()
);
#3017=(
BOUNDED_SURFACE()
B_SPLINE_SURFACE(3,2,((#401056,#401057,#401058),(#401059,#401060,#401061),
(#401062,#401063,#401064),(#401065,#401066,#401067)),.UNSPECIFIED.,.F.,
 .F.,.F.)
B_SPLINE_SURFACE_WITH_KNOTS((4,4),(3,3),(1.0842021724855E-19,4.6819775844821E-5),
(0.,1.),.UNSPECIFIED.)
GEOMETRIC_REPRESENTATION_ITEM()
RATIONAL_B_SPLINE_SURFACE(((1.,0.816715621142049,1.),(1.,0.953638980025214,
1.),(1.,0.954506925408049,1.),(1.,0.81671562114205,1.)))
REPRESENTATION_ITEM('')
SURFACE()
);
#3018=(
BOUNDED_SURFACE()
B_SPLINE_SURFACE(3,2,((#401069,#401070,#401071),(#401072,#401073,#401074),
(#401075,#401076,#401077),(#401078,#401079,#401080)),.UNSPECIFIED.,.F.,
 .F.,.F.)
B_SPLINE_SURFACE_WITH_KNOTS((4,4),(3,3),(0.,9.54361881492176E-5),(0.,1.),
 .UNSPECIFIED.)
GEOMETRIC_REPRESENTATION_ITEM()
RATIONAL_B_SPLINE_SURFACE(((1.,0.814339887349192,1.),(1.,0.815115959345197,
1.),(1.,0.815907587407954,1.),(1.,0.816715621142049,1.)))
REPRESENTATION_ITEM('')
SURFACE()
);
#3019=(
BOUNDED_SURFACE()
B_SPLINE_SURFACE(3,2,((#401082,#401083,#401084),(#401085,#401086,#401087),
(#401088,#401089,#401090),(#401091,#401092,#401093)),.UNSPECIFIED.,.F.,
 .F.,.F.)
B_SPLINE_SURFACE_WITH_KNOTS((4,4),(3,3),(-3.39528393502374E-6,3.73481232852735E-5),
(-0.00165018033314802,1.),.UNSPECIFIED.)
GEOMETRIC_REPRESENTATION_ITEM()
RATIONAL_B_SPLINE_SURFACE(((1.00048354385562,0.853487571660416,1.),(1.00047110510917,
0.857256476851484,1.),(1.00053193201103,0.838826096655888,1.),(1.0006397068772,
0.806170615310112,1.)))
REPRESENTATION_ITEM('')
SURFACE()
);
#3020=(
BOUNDED_SURFACE()
B_SPLINE_SURFACE(3,2,((#401097,#401098,#401099),(#401100,#401101,#401102),
(#401103,#401104,#401105),(#401106,#401107,#401108)),.UNSPECIFIED.,.F.,
 .F.,.F.)
B_SPLINE_SURFACE_WITH_KNOTS((4,4),(3,3),(2.02993869230511E-5,5.39756952686907E-5),
(-0.000116281069653282,1.),.UNSPECIFIED.)
GEOMETRIC_REPRESENTATION_ITEM()
RATIONAL_B_SPLINE_SURFACE(((1.00001770479726,0.92387068114303,1.),(1.00001014104057,
0.956394275543435,1.),(1.00002037300274,0.912397594905695,1.),(1.00003390859461,
0.854195550869892,1.)))
REPRESENTATION_ITEM('')
SURFACE()
);
#3021=(
BOUNDED_SURFACE()
B_SPLINE_SURFACE(3,2,((#401201,#401202,#401203),(#401204,#401205,#401206),
(#401207,#401208,#401209),(#401210,#401211,#401212)),.UNSPECIFIED.,.F.,
 .F.,.F.)
B_SPLINE_SURFACE_WITH_KNOTS((4,4),(3,3),(0.00135801595889393,0.00148409170619832),
(0.,1.),.UNSPECIFIED.)
GEOMETRIC_REPRESENTATION_ITEM()
RATIONAL_B_SPLINE_SURFACE(((1.,0.818301933966434,1.),(1.,0.817226613172369,
1.),(1.,0.816179643373941,1.),(1.,0.815159387863662,1.)))
REPRESENTATION_ITEM('')
SURFACE()
);
#3022=(
BOUNDED_SURFACE()
B_SPLINE_SURFACE(3,2,((#401251,#401252,#401253),(#401254,#401255,#401256),
(#401257,#401258,#401259),(#401260,#401261,#401262)),.UNSPECIFIED.,.F.,
 .F.,.F.)
B_SPLINE_SURFACE_WITH_KNOTS((4,4),(3,3),(-1.54744435122073E-6,1.54744435122075E-5),
(-0.0151698983614576,1.01516989836034),.UNSPECIFIED.)
GEOMETRIC_REPRESENTATION_ITEM()
RATIONAL_B_SPLINE_SURFACE(((1.02018382472867,0.32449821941385,1.02018382472716),
(1.00401234488807,0.86571692171071,1.00401234488777),(1.00033622856779,
0.988747276629654,1.00033622856777),(1.,1.,1.)))
REPRESENTATION_ITEM('')
SURFACE()
);
#3023=(
BOUNDED_SURFACE()
B_SPLINE_SURFACE(3,2,((#401264,#401265,#401266),(#401267,#401268,#401269),
(#401270,#401271,#401272),(#401273,#401274,#401275)),.UNSPECIFIED.,.F.,
 .F.,.F.)
B_SPLINE_SURFACE_WITH_KNOTS((4,4),(3,3),(0.00137194782501028,0.00149814269699235),
(0.,1.),.UNSPECIFIED.)
GEOMETRIC_REPRESENTATION_ITEM()
RATIONAL_B_SPLINE_SURFACE(((1.,0.815158509402314,1.),(1.,0.816179044148169,
1.),(1.,0.817226308119935,1.),(1.,0.818301939488798,1.)))
REPRESENTATION_ITEM('')
SURFACE()
);
#3024=(
BOUNDED_SURFACE()
B_SPLINE_SURFACE(3,2,((#401319,#401320,#401321),(#401322,#401323,#401324),
(#401325,#401326,#401327),(#401328,#401329,#401330)),.UNSPECIFIED.,.F.,
 .F.,.F.)
B_SPLINE_SURFACE_WITH_KNOTS((4,4),(3,3),(1.55009486301137E-5,4.9206551047443E-5),
(-8.13759512452905E-5,1.),.UNSPECIFIED.)
GEOMETRIC_REPRESENTATION_ITEM()
RATIONAL_B_SPLINE_SURFACE(((1.00002372912329,0.85420063959972,1.),(1.00001423585989,
0.912530301180559,1.),(1.00000710550469,0.95634149537744,1.),(1.00001238975905,
0.923873338137041,1.)))
REPRESENTATION_ITEM('')
SURFACE()
);
#3025=(
BOUNDED_SURFACE()
B_SPLINE_SURFACE(3,2,((#401334,#401335,#401336),(#401337,#401338,#401339),
(#401340,#401341,#401342),(#401343,#401344,#401345)),.UNSPECIFIED.,.F.,
 .F.,.F.)
B_SPLINE_SURFACE_WITH_KNOTS((4,4),(3,3),(-3.39934179457794E-6,3.73927597403568E-5),
(-0.00186004067403676,1.00069373317385),.UNSPECIFIED.)
GEOMETRIC_REPRESENTATION_ITEM()
RATIONAL_B_SPLINE_SURFACE(((1.00072100136049,0.806051963875495,1.0002685964267),
(1.00060048440149,0.838470803558738,1.00022369994478),(1.0005310644879,
0.8571446322725,1.00019783877204),(1.00054515072848,0.853355459539201,1.00020308635421)))
REPRESENTATION_ITEM('')
SURFACE()
);
#3026=(
BOUNDED_SURFACE()
B_SPLINE_SURFACE(3,2,((#401347,#401348,#401349),(#401350,#401351,#401352),
(#401353,#401354,#401355),(#401356,#401357,#401358)),.UNSPECIFIED.,.F.,
 .F.,.F.)
B_SPLINE_SURFACE_WITH_KNOTS((4,4),(3,3),(0.,9.54361881492172E-5),(0.,1.),
 .UNSPECIFIED.)
GEOMETRIC_REPRESENTATION_ITEM()
RATIONAL_B_SPLINE_SURFACE(((1.,0.816715621142058,1.),(1.,0.815907587407938,
1.),(1.,0.815115959345213,1.),(1.,0.814339887349197,1.)))
REPRESENTATION_ITEM('')
SURFACE()
);
#3027=(
BOUNDED_SURFACE()
B_SPLINE_SURFACE(3,2,((#401360,#401361,#401362),(#401363,#401364,#401365),
(#401366,#401367,#401368),(#401369,#401370,#401371)),.UNSPECIFIED.,.F.,
 .F.,.F.)
B_SPLINE_SURFACE_WITH_KNOTS((4,4),(3,3),(1.91429446079472E-19,4.68197758448204E-5),
(0.,1.),.UNSPECIFIED.)
GEOMETRIC_REPRESENTATION_ITEM()
RATIONAL_B_SPLINE_SURFACE(((1.,0.816715621142047,1.),(1.,0.953638980025218,
1.),(1.,0.954506925408038,1.),(1.,0.816715621142058,1.)))
REPRESENTATION_ITEM('')
SURFACE()
);
#3028=(
BOUNDED_SURFACE()
B_SPLINE_SURFACE(3,2,((#401373,#401374,#401375),(#401376,#401377,#401378),
(#401379,#401380,#401381),(#401382,#401383,#401384)),.UNSPECIFIED.,.F.,
 .F.,.F.)
B_SPLINE_SURFACE_WITH_KNOTS((4,4),(3,3),(1.62630325872826E-19,9.54361881492179E-5),
(0.,1.),.UNSPECIFIED.)
GEOMETRIC_REPRESENTATION_ITEM()
RATIONAL_B_SPLINE_SURFACE(((1.,0.814339887349189,1.),(1.,0.815115959345212,
1.),(1.,0.81590758740794,1.),(1.,0.816715621142047,1.)))
REPRESENTATION_ITEM('')
SURFACE()
);
#3029=(
BOUNDED_SURFACE()
B_SPLINE_SURFACE(3,2,((#401386,#401387,#401388),(#401389,#401390,#401391),
(#401392,#401393,#401394),(#401395,#401396,#401397)),.UNSPECIFIED.,.F.,
 .F.,.F.)
B_SPLINE_SURFACE_WITH_KNOTS((4,4),(3,3),(-3.39528393502484E-6,3.73481232852723E-5),
(-0.00165018033327953,1.),.UNSPECIFIED.)
GEOMETRIC_REPRESENTATION_ITEM()
RATIONAL_B_SPLINE_SURFACE(((1.00048354385565,0.85348757166039,1.),(1.00047110510921,
0.857256476851472,1.),(1.00053193201107,0.838826096655868,1.),(1.00063970687725,
0.8061706153101,1.)))
REPRESENTATION_ITEM('')
SURFACE()
);
#3030=(
BOUNDED_SURFACE()
B_SPLINE_SURFACE(3,2,((#401401,#401402,#401403),(#401404,#401405,#401406),
(#401407,#401408,#401409),(#401410,#401411,#401412)),.UNSPECIFIED.,.F.,
 .F.,.F.)
B_SPLINE_SURFACE_WITH_KNOTS((4,4),(3,3),(2.02993869230511E-5,5.39756952686904E-5),
(-0.000116281070078735,1.),.UNSPECIFIED.)
GEOMETRIC_REPRESENTATION_ITEM()
RATIONAL_B_SPLINE_SURFACE(((1.00001770479732,0.923870681142998,1.),(1.0000101410406,
0.956394275543412,1.),(1.00002037300281,0.912397594905667,1.),(1.00003390859473,
0.854195550869826,1.)))
REPRESENTATION_ITEM('')
SURFACE()
);
#3031=(
BOUNDED_SURFACE()
B_SPLINE_SURFACE(3,2,((#401505,#401506,#401507),(#401508,#401509,#401510),
(#401511,#401512,#401513),(#401514,#401515,#401516)),.UNSPECIFIED.,.F.,
 .F.,.F.)
B_SPLINE_SURFACE_WITH_KNOTS((4,4),(3,3),(0.00135801595889393,0.00148409170619832),
(0.,1.),.UNSPECIFIED.)
GEOMETRIC_REPRESENTATION_ITEM()
RATIONAL_B_SPLINE_SURFACE(((1.,0.818301933966433,1.),(1.,0.81722661317235,
1.),(1.,0.816179643373951,1.),(1.,0.815159387863659,1.)))
REPRESENTATION_ITEM('')
SURFACE()
);
#3032=(
BOUNDED_SURFACE()
B_SPLINE_SURFACE(3,2,((#401555,#401556,#401557),(#401558,#401559,#401560),
(#401561,#401562,#401563),(#401564,#401565,#401566)),.UNSPECIFIED.,.F.,
 .F.,.F.)
B_SPLINE_SURFACE_WITH_KNOTS((4,4),(3,3),(-1.54744435122067E-6,1.54744435122071E-5),
(-0.0151698983645437,1.01516989835833),.UNSPECIFIED.)
GEOMETRIC_REPRESENTATION_ITEM()
RATIONAL_B_SPLINE_SURFACE(((1.02018382473283,0.324498219413116,1.02018382472444),
(1.0040123448889,0.86571692171053,1.00401234488723),(1.00033622856786,0.988747276629684,
1.00033622856772),(1.,1.,1.)))
REPRESENTATION_ITEM('')
SURFACE()
);
#3033=(
BOUNDED_SURFACE()
B_SPLINE_SURFACE(3,2,((#401568,#401569,#401570),(#401571,#401572,#401573),
(#401574,#401575,#401576),(#401577,#401578,#401579)),.UNSPECIFIED.,.F.,
 .F.,.F.)
B_SPLINE_SURFACE_WITH_KNOTS((4,4),(3,3),(0.00137194782501028,0.00149814269699235),
(0.,1.),.UNSPECIFIED.)
GEOMETRIC_REPRESENTATION_ITEM()
RATIONAL_B_SPLINE_SURFACE(((1.,0.815158509402314,1.),(1.,0.81617904414816,
1.),(1.,0.817226308119927,1.),(1.,0.818301939488808,1.)))
REPRESENTATION_ITEM('')
SURFACE()
);
#3034=(
BOUNDED_SURFACE()
B_SPLINE_SURFACE(3,2,((#401623,#401624,#401625),(#401626,#401627,#401628),
(#401629,#401630,#401631),(#401632,#401633,#401634)),.UNSPECIFIED.,.F.,
 .F.,.F.)
B_SPLINE_SURFACE_WITH_KNOTS((4,4),(3,3),(1.55009486301138E-5,4.92065510474435E-5),
(-8.13759512394683E-5,1.),.UNSPECIFIED.)
GEOMETRIC_REPRESENTATION_ITEM()
RATIONAL_B_SPLINE_SURFACE(((1.00002372912329,0.854200639599714,1.),(1.00001423585989,
0.912530301180566,1.),(1.00000710550469,0.956341495377436,1.),(1.00001238975905,
0.92387333813704,1.)))
REPRESENTATION_ITEM('')
SURFACE()
);
#3035=(
BOUNDED_SURFACE()
B_SPLINE_SURFACE(3,2,((#401638,#401639,#401640),(#401641,#401642,#401643),
(#401644,#401645,#401646),(#401647,#401648,#401649)),.UNSPECIFIED.,.F.,
 .F.,.F.)
B_SPLINE_SURFACE_WITH_KNOTS((4,4),(3,3),(-3.39934179457784E-6,3.73927597403568E-5),
(-0.001860040674796,1.00069373317472),.UNSPECIFIED.)
GEOMETRIC_REPRESENTATION_ITEM()
RATIONAL_B_SPLINE_SURFACE(((1.00072100136078,0.806051963875152,1.00026859642704),
(1.00060048440174,0.838470803558502,1.00022369994506),(1.00053106448812,
0.857144632272237,1.00019783877229),(1.0005451507287,0.85335545953896,1.00020308635446)))
REPRESENTATION_ITEM('')
SURFACE()
);
#3036=(
BOUNDED_SURFACE()
B_SPLINE_SURFACE(3,2,((#401651,#401652,#401653),(#401654,#401655,#401656),
(#401657,#401658,#401659),(#401660,#401661,#401662)),.UNSPECIFIED.,.F.,
 .F.,.F.)
B_SPLINE_SURFACE_WITH_KNOTS((4,4),(3,3),(-1.62630325872826E-19,9.54361881492172E-5),
(0.,1.),.UNSPECIFIED.)
GEOMETRIC_REPRESENTATION_ITEM()
RATIONAL_B_SPLINE_SURFACE(((1.,0.816715621142042,1.),(1.,0.815907587407949,
1.),(1.,0.815115959345201,1.),(1.,0.814339887349195,1.)))
REPRESENTATION_ITEM('')
SURFACE()
);
#3037=(
BOUNDED_SURFACE()
B_SPLINE_SURFACE(3,2,((#401664,#401665,#401666),(#401667,#401668,#401669),
(#401670,#401671,#401672),(#401673,#401674,#401675)),.UNSPECIFIED.,.F.,
 .F.,.F.)
B_SPLINE_SURFACE_WITH_KNOTS((4,4),(3,3),(4.2351647362715E-20,4.6819775844821E-5),
(0.,1.),.UNSPECIFIED.)
GEOMETRIC_REPRESENTATION_ITEM()
RATIONAL_B_SPLINE_SURFACE(((1.,0.816715621142047,1.),(1.,0.953638980025218,
1.),(1.,0.954506925408044,1.),(1.,0.816715621142054,1.)))
REPRESENTATION_ITEM('')
SURFACE()
);
#3038=(
BOUNDED_SURFACE()
B_SPLINE_SURFACE(3,2,((#401677,#401678,#401679),(#401680,#401681,#401682),
(#401683,#401684,#401685),(#401686,#401687,#401688)),.UNSPECIFIED.,.F.,
 .F.,.F.)
B_SPLINE_SURFACE_WITH_KNOTS((4,4),(3,3),(-1.0842021724855E-19,9.54361881492177E-5),
(0.,1.),.UNSPECIFIED.)
GEOMETRIC_REPRESENTATION_ITEM()
RATIONAL_B_SPLINE_SURFACE(((1.,0.814339887349196,1.),(1.,0.815115959345204,
1.),(1.,0.81590758740794,1.),(1.,0.816715621142047,1.)))
REPRESENTATION_ITEM('')
SURFACE()
);
#3039=(
BOUNDED_SURFACE()
B_SPLINE_SURFACE(3,2,((#401690,#401691,#401692),(#401693,#401694,#401695),
(#401696,#401697,#401698),(#401699,#401700,#401701)),.UNSPECIFIED.,.F.,
 .F.,.F.)
B_SPLINE_SURFACE_WITH_KNOTS((4,4),(3,3),(-3.39528393502374E-6,3.73481232852733E-5),
(-0.00165018033334311,1.),.UNSPECIFIED.)
GEOMETRIC_REPRESENTATION_ITEM()
RATIONAL_B_SPLINE_SURFACE(((1.00048354385567,0.853487571660385,1.),(1.00047110510922,
0.857256476851452,1.),(1.00053193201109,0.838826096655862,1.),(1.00063970687728,
0.80617061531008,1.)))
REPRESENTATION_ITEM('')
SURFACE()
);
#3040=(
BOUNDED_SURFACE()
B_SPLINE_SURFACE(3,2,((#401705,#401706,#401707),(#401708,#401709,#401710),
(#401711,#401712,#401713),(#401714,#401715,#401716)),.UNSPECIFIED.,.F.,
 .F.,.F.)
B_SPLINE_SURFACE_WITH_KNOTS((4,4),(3,3),(2.02993869230507E-5,5.39756952686899E-5),
(-0.000116281069940536,1.),.UNSPECIFIED.)
GEOMETRIC_REPRESENTATION_ITEM()
RATIONAL_B_SPLINE_SURFACE(((1.0000177047973,0.923870681143011,1.),(1.00001014104059,
0.95639427554341,1.),(1.00002037300279,0.912397594905685,1.),(1.00003390859469,
0.854195550869851,1.)))
REPRESENTATION_ITEM('')
SURFACE()
);
#3041=(
BOUNDED_SURFACE()
B_SPLINE_SURFACE(3,2,((#401809,#401810,#401811),(#401812,#401813,#401814),
(#401815,#401816,#401817),(#401818,#401819,#401820)),.UNSPECIFIED.,.F.,
 .F.,.F.)
B_SPLINE_SURFACE_WITH_KNOTS((4,4),(3,3),(0.00135801595889393,0.00148409170619832),
(0.,1.),.UNSPECIFIED.)
GEOMETRIC_REPRESENTATION_ITEM()
RATIONAL_B_SPLINE_SURFACE(((1.,0.818301933966449,1.),(1.,0.817226613172348,
1.),(1.,0.816179643373952,1.),(1.,0.815159387863656,1.)))
REPRESENTATION_ITEM('')
SURFACE()
);
#3042=(
BOUNDED_SURFACE()
B_SPLINE_SURFACE(3,2,((#401859,#401860,#401861),(#401862,#401863,#401864),
(#401865,#401866,#401867),(#401868,#401869,#401870)),.UNSPECIFIED.,.F.,
 .F.,.F.)
B_SPLINE_SURFACE_WITH_KNOTS((4,4),(3,3),(-1.5474443512208E-6,1.54744435122078E-5),
(-0.0151698983646347,1.),.UNSPECIFIED.)
GEOMETRIC_REPRESENTATION_ITEM()
RATIONAL_B_SPLINE_SURFACE(((1.02018382473296,0.334740937354848,1.),(1.00401234488892,
0.867753072812993,1.),(1.00033622856786,0.988917903080814,1.),(1.,1.,1.)))
REPRESENTATION_ITEM('')
SURFACE()
);
#3043=(
BOUNDED_SURFACE()
B_SPLINE_SURFACE(3,2,((#401872,#401873,#401874),(#401875,#401876,#401877),
(#401878,#401879,#401880),(#401881,#401882,#401883)),.UNSPECIFIED.,.F.,
 .F.,.F.)
B_SPLINE_SURFACE_WITH_KNOTS((4,4),(3,3),(0.00137194782501028,0.00149814269699235),
(0.,1.),.UNSPECIFIED.)
GEOMETRIC_REPRESENTATION_ITEM()
RATIONAL_B_SPLINE_SURFACE(((1.,0.81515850940232,1.),(1.,0.816179044148161,
1.),(1.,0.817226308119925,1.),(1.,0.818301939488814,1.)))
REPRESENTATION_ITEM('')
SURFACE()
);
#3044=(
BOUNDED_SURFACE()
B_SPLINE_SURFACE(3,2,((#401927,#401928,#401929),(#401930,#401931,#401932),
(#401933,#401934,#401935),(#401936,#401937,#401938)),.UNSPECIFIED.,.F.,
 .F.,.F.)
B_SPLINE_SURFACE_WITH_KNOTS((4,4),(3,3),(1.55009486301137E-5,4.92065510474434E-5),
(-8.13759515589481E-5,1.),.UNSPECIFIED.)
GEOMETRIC_REPRESENTATION_ITEM()
RATIONAL_B_SPLINE_SURFACE(((1.00002372912338,0.854200639599674,1.),(1.00001423585995,
0.912530301180525,1.),(1.00000710550471,0.956341495377429,1.),(1.0000123897591,
0.923873338137018,1.)))
REPRESENTATION_ITEM('')
SURFACE()
);
#3045=(
BOUNDED_SURFACE()
B_SPLINE_SURFACE(3,2,((#401942,#401943,#401944),(#401945,#401946,#401947),
(#401948,#401949,#401950),(#401951,#401952,#401953)),.UNSPECIFIED.,.F.,
 .F.,.F.)
B_SPLINE_SURFACE_WITH_KNOTS((4,4),(3,3),(-3.39934179457785E-6,3.73927597403568E-5),
(-0.00186004067443997,1.00069373317459),.UNSPECIFIED.)
GEOMETRIC_REPRESENTATION_ITEM()
RATIONAL_B_SPLINE_SURFACE(((1.00072100136064,0.806051963875255,1.00026859642698),
(1.00060048440162,0.838470803558584,1.00022369994502),(1.00053106448802,
0.857144632272302,1.00019783877225),(1.0005451507286,0.853355459539047,
1.00020308635443)))
REPRESENTATION_ITEM('')
SURFACE()
);
#3046=(
BOUNDED_SURFACE()
B_SPLINE_SURFACE(3,2,((#401955,#401956,#401957),(#401958,#401959,#401960),
(#401961,#401962,#401963),(#401964,#401965,#401966)),.UNSPECIFIED.,.F.,
 .F.,.F.)
B_SPLINE_SURFACE_WITH_KNOTS((4,4),(3,3),(2.16840434497101E-19,9.54361881492174E-5),
(0.,1.),.UNSPECIFIED.)
GEOMETRIC_REPRESENTATION_ITEM()
RATIONAL_B_SPLINE_SURFACE(((1.,0.816715621142055,1.),(1.,0.815907587407941,
1.),(1.,0.815115959345212,1.),(1.,0.814339887349196,1.)))
REPRESENTATION_ITEM('')
SURFACE()
);
#3047=(
BOUNDED_SURFACE()
B_SPLINE_SURFACE(3,2,((#401968,#401969,#401970),(#401971,#401972,#401973),
(#401974,#401975,#401976),(#401977,#401978,#401979)),.UNSPECIFIED.,.F.,
 .F.,.F.)
B_SPLINE_SURFACE_WITH_KNOTS((4,4),(3,3),(3.10014058695074E-19,4.68197758448212E-5),
(0.,1.),.UNSPECIFIED.)
GEOMETRIC_REPRESENTATION_ITEM()
RATIONAL_B_SPLINE_SURFACE(((1.,0.816715621142044,1.),(1.,0.95363898002522,
1.),(1.,0.954506925408041,1.),(1.,0.816715621142055,1.)))
REPRESENTATION_ITEM('')
SURFACE()
);
#3048=(
BOUNDED_SURFACE()
B_SPLINE_SURFACE(3,2,((#401981,#401982,#401983),(#401984,#401985,#401986),
(#401987,#401988,#401989),(#401990,#401991,#401992)),.UNSPECIFIED.,.F.,
 .F.,.F.)
B_SPLINE_SURFACE_WITH_KNOTS((4,4),(3,3),(2.16840434497101E-19,9.54361881492178E-5),
(0.,1.),.UNSPECIFIED.)
GEOMETRIC_REPRESENTATION_ITEM()
RATIONAL_B_SPLINE_SURFACE(((1.,0.814339887349193,1.),(1.,0.815115959345206,
1.),(1.,0.815907587407946,1.),(1.,0.816715621142047,1.)))
REPRESENTATION_ITEM('')
SURFACE()
);
#3049=(
BOUNDED_SURFACE()
B_SPLINE_SURFACE(3,2,((#401994,#401995,#401996),(#401997,#401998,#401999),
(#402000,#402001,#402002),(#402003,#402004,#402005)),.UNSPECIFIED.,.F.,
 .F.,.F.)
B_SPLINE_SURFACE_WITH_KNOTS((4,4),(3,3),(-3.39528393502495E-6,3.7348123285273E-5),
(-0.00165018033346878,1.),.UNSPECIFIED.)
GEOMETRIC_REPRESENTATION_ITEM()
RATIONAL_B_SPLINE_SURFACE(((1.00048354385571,0.853487571660368,1.),(1.00047110510926,
0.857256476851447,1.),(1.00053193201113,0.838826096655836,1.),(1.00063970687733,
0.806170615310062,1.)))
REPRESENTATION_ITEM('')
SURFACE()
);
#3050=(
BOUNDED_SURFACE()
B_SPLINE_SURFACE(3,2,((#402009,#402010,#402011),(#402012,#402013,#402014),
(#402015,#402016,#402017),(#402018,#402019,#402020)),.UNSPECIFIED.,.F.,
 .F.,.F.)
B_SPLINE_SURFACE_WITH_KNOTS((4,4),(3,3),(2.02993869230511E-5,5.39756952686901E-5),
(-0.000116281069764521,1.),.UNSPECIFIED.)
GEOMETRIC_REPRESENTATION_ITEM()
RATIONAL_B_SPLINE_SURFACE(((1.00001770479727,0.92387068114302,1.),(1.00001014104058,
0.956394275543423,1.),(1.00002037300276,0.912397594905696,1.),(1.00003390859464,
0.854195550869868,1.)))
REPRESENTATION_ITEM('')
SURFACE()
);
#3051=(
BOUNDED_SURFACE()
B_SPLINE_SURFACE(3,2,((#402113,#402114,#402115),(#402116,#402117,#402118),
(#402119,#402120,#402121),(#402122,#402123,#402124)),.UNSPECIFIED.,.F.,
 .F.,.F.)
B_SPLINE_SURFACE_WITH_KNOTS((4,4),(3,3),(0.00135801595889393,0.00148409170619832),
(0.,1.),.UNSPECIFIED.)
GEOMETRIC_REPRESENTATION_ITEM()
RATIONAL_B_SPLINE_SURFACE(((1.,0.818301933966446,1.),(1.,0.817226613172357,
1.),(1.,0.81617964337394,1.),(1.,0.815159387863662,1.)))
REPRESENTATION_ITEM('')
SURFACE()
);
#3052=(
BOUNDED_SURFACE()
B_SPLINE_SURFACE(3,2,((#402163,#402164,#402165),(#402166,#402167,#402168),
(#402169,#402170,#402171),(#402172,#402173,#402174)),.UNSPECIFIED.,.F.,
 .F.,.F.)
B_SPLINE_SURFACE_WITH_KNOTS((4,4),(3,3),(-1.54744435122075E-6,1.5474443512207E-5),
(0.,1.01516989835802),.UNSPECIFIED.)
GEOMETRIC_REPRESENTATION_ITEM()
RATIONAL_B_SPLINE_SURFACE(((1.,0.33474093735925,1.02018382472402),(1.,0.867753072813741,
1.00401234488715),(1.,0.988917903080923,1.00033622856771),(1.,1.,1.)))
REPRESENTATION_ITEM('')
SURFACE()
);
#3053=(
BOUNDED_SURFACE()
B_SPLINE_SURFACE(3,2,((#402176,#402177,#402178),(#402179,#402180,#402181),
(#402182,#402183,#402184),(#402185,#402186,#402187)),.UNSPECIFIED.,.F.,
 .F.,.F.)
B_SPLINE_SURFACE_WITH_KNOTS((4,4),(3,3),(0.00137194782501028,0.00149814269699235),
(0.,1.),.UNSPECIFIED.)
GEOMETRIC_REPRESENTATION_ITEM()
RATIONAL_B_SPLINE_SURFACE(((1.,0.815158509402314,1.),(1.,0.816179044148173,
1.),(1.,0.817226308119935,1.),(1.,0.818301939488801,1.)))
REPRESENTATION_ITEM('')
SURFACE()
);
#3054=(
BOUNDED_SURFACE()
B_SPLINE_SURFACE(3,2,((#402231,#402232,#402233),(#402234,#402235,#402236),
(#402237,#402238,#402239),(#402240,#402241,#402242)),.UNSPECIFIED.,.F.,
 .F.,.F.)
B_SPLINE_SURFACE_WITH_KNOTS((4,4),(3,3),(1.55009486301137E-5,4.92065510474435E-5),
(-8.13759513899056E-5,1.),.UNSPECIFIED.)
GEOMETRIC_REPRESENTATION_ITEM()
RATIONAL_B_SPLINE_SURFACE(((1.00002372912333,0.854200639599704,1.),(1.00001423585992,
0.912530301180536,1.),(1.0000071055047,0.956341495377438,1.),(1.00001238975907,
0.923873338137032,1.)))
REPRESENTATION_ITEM('')
SURFACE()
);
#3055=(
BOUNDED_SURFACE()
B_SPLINE_SURFACE(3,2,((#402246,#402247,#402248),(#402249,#402250,#402251),
(#402252,#402253,#402254),(#402255,#402256,#402257)),.UNSPECIFIED.,.F.,
 .F.,.F.)
B_SPLINE_SURFACE_WITH_KNOTS((4,4),(3,3),(-3.39934179457833E-6,3.73927597403565E-5),
(-0.00186004067416003,1.00069373317436),.UNSPECIFIED.)
GEOMETRIC_REPRESENTATION_ITEM()
RATIONAL_B_SPLINE_SURFACE(((1.00072100136054,0.80605196387537,1.00026859642689),
(1.00060048440153,0.838470803558641,1.00022369994495),(1.00053106448794,
0.8571446322724,1.00019783877218),(1.00054515072851,0.853355459539105,1.00020308635436)))
REPRESENTATION_ITEM('')
SURFACE()
);
#3056=(
BOUNDED_SURFACE()
B_SPLINE_SURFACE(3,2,((#402259,#402260,#402261),(#402262,#402263,#402264),
(#402265,#402266,#402267),(#402268,#402269,#402270)),.UNSPECIFIED.,.F.,
 .F.,.F.)
B_SPLINE_SURFACE_WITH_KNOTS((4,4),(3,3),(-2.16840434497101E-19,9.54361881492173E-5),
(0.,1.),.UNSPECIFIED.)
GEOMETRIC_REPRESENTATION_ITEM()
RATIONAL_B_SPLINE_SURFACE(((1.,0.81671562114205,1.),(1.,0.815907587407941,
1.),(1.,0.815115959345207,1.),(1.,0.814339887349197,1.)))
REPRESENTATION_ITEM('')
SURFACE()
);
#3057=(
BOUNDED_SURFACE()
B_SPLINE_SURFACE(3,2,((#402272,#402273,#402274),(#402275,#402276,#402277),
(#402278,#402279,#402280),(#402281,#402282,#402283)),.UNSPECIFIED.,.F.,
 .F.,.F.)
B_SPLINE_SURFACE_WITH_KNOTS((4,4),(3,3),(-2.87991202066462E-19,4.68197758448209E-5),
(0.,1.),.UNSPECIFIED.)
GEOMETRIC_REPRESENTATION_ITEM()
RATIONAL_B_SPLINE_SURFACE(((1.,0.816715621142049,1.),(1.,0.953638980025204,
1.),(1.,0.954506925408058,1.),(1.,0.816715621142057,1.)))
REPRESENTATION_ITEM('')
SURFACE()
);
#3058=(
BOUNDED_SURFACE()
B_SPLINE_SURFACE(3,2,((#402285,#402286,#402287),(#402288,#402289,#402290),
(#402291,#402292,#402293),(#402294,#402295,#402296)),.UNSPECIFIED.,.F.,
 .F.,.F.)
B_SPLINE_SURFACE_WITH_KNOTS((4,4),(3,3),(1.62630325872826E-19,9.54361881492178E-5),
(0.,1.),.UNSPECIFIED.)
GEOMETRIC_REPRESENTATION_ITEM()
RATIONAL_B_SPLINE_SURFACE(((1.,0.814339887349197,1.),(1.,0.815115959345213,
1.),(1.,0.815907587407937,1.),(1.,0.816715621142052,1.)))
REPRESENTATION_ITEM('')
SURFACE()
);
#3059=(
BOUNDED_SURFACE()
B_SPLINE_SURFACE(3,2,((#402298,#402299,#402300),(#402301,#402302,#402303),
(#402304,#402305,#402306),(#402307,#402308,#402309)),.UNSPECIFIED.,.F.,
 .F.,.F.)
B_SPLINE_SURFACE_WITH_KNOTS((4,4),(3,3),(-3.39528393502494E-6,3.73481232852724E-5),
(-0.00165018033326561,1.),.UNSPECIFIED.)
GEOMETRIC_REPRESENTATION_ITEM()
RATIONAL_B_SPLINE_SURFACE(((1.00048354385565,0.853487571660401,1.),(1.0004711051092,
0.857256476851465,1.),(1.00053193201107,0.838826096655876,1.),(1.00063970687725,
0.8061706153101,1.)))
REPRESENTATION_ITEM('')
SURFACE()
);
#3060=(
BOUNDED_SURFACE()
B_SPLINE_SURFACE(3,2,((#402313,#402314,#402315),(#402316,#402317,#402318),
(#402319,#402320,#402321),(#402322,#402323,#402324)),.UNSPECIFIED.,.F.,
 .F.,.F.)
B_SPLINE_SURFACE_WITH_KNOTS((4,4),(3,3),(2.02993869230509E-5,5.39756952686898E-5),
(-0.000116281069845253,1.),.UNSPECIFIED.)
GEOMETRIC_REPRESENTATION_ITEM()
RATIONAL_B_SPLINE_SURFACE(((1.00001770479729,0.923870681143014,1.),(1.00001014104058,
0.956394275543427,1.),(1.00002037300277,0.912397594905681,1.),(1.00003390859467,
0.854195550869864,1.)))
REPRESENTATION_ITEM('')
SURFACE()
);
#3061=(
BOUNDED_SURFACE()
B_SPLINE_SURFACE(3,2,((#402417,#402418,#402419),(#402420,#402421,#402422),
(#402423,#402424,#402425),(#402426,#402427,#402428)),.UNSPECIFIED.,.F.,
 .F.,.F.)
B_SPLINE_SURFACE_WITH_KNOTS((4,4),(3,3),(0.00135801595889393,0.00148409170619832),
(0.,1.),.UNSPECIFIED.)
GEOMETRIC_REPRESENTATION_ITEM()
RATIONAL_B_SPLINE_SURFACE(((1.,0.818301933966443,1.),(1.,0.817226613172338,
1.),(1.,0.816179643373947,1.),(1.,0.815159387863652,1.)))
REPRESENTATION_ITEM('')
SURFACE()
);
#3062=(
BOUNDED_SURFACE()
B_SPLINE_SURFACE(3,2,((#402467,#402468,#402469),(#402470,#402471,#402472),
(#402473,#402474,#402475),(#402476,#402477,#402478)),.UNSPECIFIED.,.F.,
 .F.,.F.)
B_SPLINE_SURFACE_WITH_KNOTS((4,4),(3,3),(-1.54744435122089E-6,1.54744435122086E-5),
(-0.0151698983679409,1.),.UNSPECIFIED.)
GEOMETRIC_REPRESENTATION_ITEM()
RATIONAL_B_SPLINE_SURFACE(((1.02018382473742,0.334740937352698,1.),(1.00401234488981,
0.867753072812613,1.),(1.00033622856794,0.988917903080764,1.),(1.,1.,1.)))
REPRESENTATION_ITEM('')
SURFACE()
);
#3063=(
BOUNDED_SURFACE()
B_SPLINE_SURFACE(3,2,((#402480,#402481,#402482),(#402483,#402484,#402485),
(#402486,#402487,#402488),(#402489,#402490,#402491)),.UNSPECIFIED.,.F.,
 .F.,.F.)
B_SPLINE_SURFACE_WITH_KNOTS((4,4),(3,3),(0.00137194782501028,0.00149814269699235),
(0.,1.),.UNSPECIFIED.)
GEOMETRIC_REPRESENTATION_ITEM()
RATIONAL_B_SPLINE_SURFACE(((1.,0.815158509402319,1.),(1.,0.81617904414817,
1.),(1.,0.817226308119927,1.),(1.,0.818301939488815,1.)))
REPRESENTATION_ITEM('')
SURFACE()
);
#3064=(
BOUNDED_SURFACE()
B_SPLINE_SURFACE(3,2,((#402535,#402536,#402537),(#402538,#402539,#402540),
(#402541,#402542,#402543),(#402544,#402545,#402546)),.UNSPECIFIED.,.F.,
 .F.,.F.)
B_SPLINE_SURFACE_WITH_KNOTS((4,4),(3,3),(1.55009486301137E-5,4.92065510474433E-5),
(-8.13759512715114E-5,1.),.UNSPECIFIED.)
GEOMETRIC_REPRESENTATION_ITEM()
RATIONAL_B_SPLINE_SURFACE(((1.00002372912329,0.85420063959972,1.),(1.0000142358599,
0.912530301180555,1.),(1.00000710550469,0.956341495377441,1.),(1.00001238975905,
0.923873338137036,1.)))
REPRESENTATION_ITEM('')
SURFACE()
);
#3065=(
BOUNDED_SURFACE()
B_SPLINE_SURFACE(3,2,((#402550,#402551,#402552),(#402553,#402554,#402555),
(#402556,#402557,#402558),(#402559,#402560,#402561)),.UNSPECIFIED.,.F.,
 .F.,.F.)
B_SPLINE_SURFACE_WITH_KNOTS((4,4),(3,3),(-3.39934179457849E-6,3.73927597403563E-5),
(-0.00186004067427479,1.00069373317438),.UNSPECIFIED.)
GEOMETRIC_REPRESENTATION_ITEM()
RATIONAL_B_SPLINE_SURFACE(((1.00072100136058,0.806051963875348,1.0002685964269),
(1.00060048440157,0.838470803558596,1.00022369994495),(1.00053106448797,
0.857144632272381,1.00019783877219),(1.00054515072855,0.853355459539078,
1.00020308635436)))
REPRESENTATION_ITEM('')
SURFACE()
);
#3066=(
BOUNDED_SURFACE()
B_SPLINE_SURFACE(3,2,((#402563,#402564,#402565),(#402566,#402567,#402568),
(#402569,#402570,#402571),(#402572,#402573,#402574)),.UNSPECIFIED.,.F.,
 .F.,.F.)
B_SPLINE_SURFACE_WITH_KNOTS((4,4),(3,3),(-3.79470760369927E-19,9.54361881492171E-5),
(0.,1.),.UNSPECIFIED.)
GEOMETRIC_REPRESENTATION_ITEM()
RATIONAL_B_SPLINE_SURFACE(((1.,0.816715621142048,1.),(1.,0.815907587407932,
1.),(1.,0.815115959345209,1.),(1.,0.81433988734919,1.)))
REPRESENTATION_ITEM('')
SURFACE()
);
#3067=(
BOUNDED_SURFACE()
B_SPLINE_SURFACE(3,2,((#402576,#402577,#402578),(#402579,#402580,#402581),
(#402582,#402583,#402584),(#402585,#402586,#402587)),.UNSPECIFIED.,.F.,
 .F.,.F.)
B_SPLINE_SURFACE_WITH_KNOTS((4,4),(3,3),(-1.28749007982654E-19,4.68197758448209E-5),
(0.,1.),.UNSPECIFIED.)
GEOMETRIC_REPRESENTATION_ITEM()
RATIONAL_B_SPLINE_SURFACE(((1.,0.816715621142051,1.),(1.,0.953638980025206,
1.),(1.,0.954506925408048,1.),(1.,0.816715621142061,1.)))
REPRESENTATION_ITEM('')
SURFACE()
);
#3068=(
BOUNDED_SURFACE()
B_SPLINE_SURFACE(3,2,((#402589,#402590,#402591),(#402592,#402593,#402594),
(#402595,#402596,#402597),(#402598,#402599,#402600)),.UNSPECIFIED.,.F.,
 .F.,.F.)
B_SPLINE_SURFACE_WITH_KNOTS((4,4),(3,3),(-1.0842021724855E-19,9.54361881492177E-5),
(0.,1.),.UNSPECIFIED.)
GEOMETRIC_REPRESENTATION_ITEM()
RATIONAL_B_SPLINE_SURFACE(((1.,0.814339887349197,1.),(1.,0.815115959345209,
1.),(1.,0.815907587407942,1.),(1.,0.816715621142054,1.)))
REPRESENTATION_ITEM('')
SURFACE()
);
#3069=(
BOUNDED_SURFACE()
B_SPLINE_SURFACE(3,2,((#402602,#402603,#402604),(#402605,#402606,#402607),
(#402608,#402609,#402610),(#402611,#402612,#402613)),.UNSPECIFIED.,.F.,
 .F.,.F.)
B_SPLINE_SURFACE_WITH_KNOTS((4,4),(3,3),(-3.39528393502479E-6,3.73481232852735E-5),
(-0.00165018033315628,1.),.UNSPECIFIED.)
GEOMETRIC_REPRESENTATION_ITEM()
RATIONAL_B_SPLINE_SURFACE(((1.00048354385562,0.853487571660415,1.),(1.00047110510917,
0.857256476851483,1.),(1.00053193201103,0.838826096655902,1.),(1.00063970687721,
0.806170615310112,0.999999999999999)))
REPRESENTATION_ITEM('')
SURFACE()
);
#3070=(
BOUNDED_SURFACE()
B_SPLINE_SURFACE(3,2,((#402617,#402618,#402619),(#402620,#402621,#402622),
(#402623,#402624,#402625),(#402626,#402627,#402628)),.UNSPECIFIED.,.F.,
 .F.,.F.)
B_SPLINE_SURFACE_WITH_KNOTS((4,4),(3,3),(2.02993869230511E-5,5.39756952686902E-5),
(-0.000116281069516842,1.),.UNSPECIFIED.)
GEOMETRIC_REPRESENTATION_ITEM()
RATIONAL_B_SPLINE_SURFACE(((1.00001770479724,0.923870681143042,1.),(1.00001014104055,
0.956394275543434,1.),(1.00002037300271,0.912397594905713,1.),(1.00003390859457,
0.85419555086991,1.)))
REPRESENTATION_ITEM('')
SURFACE()
);
#3071=(
BOUNDED_SURFACE()
B_SPLINE_SURFACE(3,2,((#402721,#402722,#402723),(#402724,#402725,#402726),
(#402727,#402728,#402729),(#402730,#402731,#402732)),.UNSPECIFIED.,.F.,
 .F.,.F.)
B_SPLINE_SURFACE_WITH_KNOTS((4,4),(3,3),(0.00135801595889393,0.00148409170619832),
(0.,1.),.UNSPECIFIED.)
GEOMETRIC_REPRESENTATION_ITEM()
RATIONAL_B_SPLINE_SURFACE(((1.,0.818301933966441,1.),(1.,0.817226613172343,
1.),(1.,0.816179643373954,1.),(1.,0.815159387863651,1.)))
REPRESENTATION_ITEM('')
SURFACE()
);
#3072=(
BOUNDED_SURFACE()
B_SPLINE_SURFACE(3,2,((#402771,#402772,#402773),(#402774,#402775,#402776),
(#402777,#402778,#402779),(#402780,#402781,#402782)),.UNSPECIFIED.,.F.,
 .F.,.F.)
B_SPLINE_SURFACE_WITH_KNOTS((4,4),(3,3),(-1.54744435122074E-6,1.54744435122071E-5),
(-0.0151698983619576,1.01516989836059),.UNSPECIFIED.)
GEOMETRIC_REPRESENTATION_ITEM()
RATIONAL_B_SPLINE_SURFACE(((1.02018382472934,0.324498219413315,1.02018382472749),
(1.0040123448882,0.865716921710694,1.00401234488783),(1.0003362285678,0.988747276629597,
1.00033622856777),(1.,1.,1.)))
REPRESENTATION_ITEM('')
SURFACE()
);
#3073=(
BOUNDED_SURFACE()
B_SPLINE_SURFACE(3,2,((#402784,#402785,#402786),(#402787,#402788,#402789),
(#402790,#402791,#402792),(#402793,#402794,#402795)),.UNSPECIFIED.,.F.,
 .F.,.F.)
B_SPLINE_SURFACE_WITH_KNOTS((4,4),(3,3),(0.00137194782501028,0.00149814269699235),
(0.,1.),.UNSPECIFIED.)
GEOMETRIC_REPRESENTATION_ITEM()
RATIONAL_B_SPLINE_SURFACE(((1.,0.815158509402318,1.),(1.,0.816179044148166,
1.),(1.,0.817226308119925,1.),(1.,0.818301939488809,1.)))
REPRESENTATION_ITEM('')
SURFACE()
);
#3074=(
BOUNDED_SURFACE()
B_SPLINE_SURFACE(3,2,((#402839,#402840,#402841),(#402842,#402843,#402844),
(#402845,#402846,#402847),(#402848,#402849,#402850)),.UNSPECIFIED.,.F.,
 .F.,.F.)
B_SPLINE_SURFACE_WITH_KNOTS((4,4),(3,3),(1.55009486301137E-5,4.9206551047443E-5),
(-8.13759517604745E-5,1.),.UNSPECIFIED.)
GEOMETRIC_REPRESENTATION_ITEM()
RATIONAL_B_SPLINE_SURFACE(((1.00002372912344,0.854200639599649,1.),(1.00001423585998,
0.912530301180504,1.),(1.00000710550473,0.956341495377428,1.),(1.00001238975913,
0.923873338137001,1.)))
REPRESENTATION_ITEM('')
SURFACE()
);
#3075=(
BOUNDED_SURFACE()
B_SPLINE_SURFACE(3,2,((#402854,#402855,#402856),(#402857,#402858,#402859),
(#402860,#402861,#402862),(#402863,#402864,#402865)),.UNSPECIFIED.,.F.,
 .F.,.F.)
B_SPLINE_SURFACE_WITH_KNOTS((4,4),(3,3),(-3.39934179457832E-6,3.73927597403565E-5),
(-0.00186004067362119,1.00069373317417),.UNSPECIFIED.)
GEOMETRIC_REPRESENTATION_ITEM()
RATIONAL_B_SPLINE_SURFACE(((1.00072100136033,0.806051963875496,1.00026859642682),
(1.00060048440136,0.838470803558756,1.00022369994489),(1.00053106448778,
0.857144632272493,1.00019783877213),(1.00054515072836,0.853355459539209,
1.0002030863543)))
REPRESENTATION_ITEM('')
SURFACE()
);
#3076=(
BOUNDED_SURFACE()
B_SPLINE_SURFACE(3,2,((#402867,#402868,#402869),(#402870,#402871,#402872),
(#402873,#402874,#402875),(#402876,#402877,#402878)),.UNSPECIFIED.,.F.,
 .F.,.F.)
B_SPLINE_SURFACE_WITH_KNOTS((4,4),(3,3),(5.42101086242752E-20,9.54361881492173E-5),
(0.,1.),.UNSPECIFIED.)
GEOMETRIC_REPRESENTATION_ITEM()
RATIONAL_B_SPLINE_SURFACE(((1.,0.816715621142048,1.),(1.,0.815907587407936,
1.),(1.,0.81511595934521,1.),(1.,0.81433988734919,1.)))
REPRESENTATION_ITEM('')
SURFACE()
);
#3077=(
BOUNDED_SURFACE()
B_SPLINE_SURFACE(3,2,((#402880,#402881,#402882),(#402883,#402884,#402885),
(#402886,#402887,#402888),(#402889,#402890,#402891)),.UNSPECIFIED.,.F.,
 .F.,.F.)
B_SPLINE_SURFACE_WITH_KNOTS((4,4),(3,3),(1.54159996400283E-19,4.68197758448206E-5),
(0.,1.),.UNSPECIFIED.)
GEOMETRIC_REPRESENTATION_ITEM()
RATIONAL_B_SPLINE_SURFACE(((1.,0.81671562114205,1.),(1.,0.953638980025216,
1.),(1.,0.954506925408041,1.),(1.,0.816715621142061,1.)))
REPRESENTATION_ITEM('')
SURFACE()
);
#3078=(
BOUNDED_SURFACE()
B_SPLINE_SURFACE(3,2,((#402893,#402894,#402895),(#402896,#402897,#402898),
(#402899,#402900,#402901),(#402902,#402903,#402904)),.UNSPECIFIED.,.F.,
 .F.,.F.)
B_SPLINE_SURFACE_WITH_KNOTS((4,4),(3,3),(-1.62630325872826E-19,9.54361881492177E-5),
(0.,1.),.UNSPECIFIED.)
GEOMETRIC_REPRESENTATION_ITEM()
RATIONAL_B_SPLINE_SURFACE(((1.,0.814339887349192,1.),(1.,0.815115959345203,
1.),(1.,0.815907587407944,1.),(1.,0.816715621142047,1.)))
REPRESENTATION_ITEM('')
SURFACE()
);
#3079=(
BOUNDED_SURFACE()
B_SPLINE_SURFACE(3,2,((#402906,#402907,#402908),(#402909,#402910,#402911),
(#402912,#402913,#402914),(#402915,#402916,#402917)),.UNSPECIFIED.,.F.,
 .F.,.F.)
B_SPLINE_SURFACE_WITH_KNOTS((4,4),(3,3),(-3.39528393502487E-6,3.73481232852725E-5),
(-0.00165018033253464,1.),.UNSPECIFIED.)
GEOMETRIC_REPRESENTATION_ITEM()
RATIONAL_B_SPLINE_SURFACE(((1.00048354385544,0.853487571660502,1.),(1.00047110510899,
0.857256476851569,1.),(1.00053193201083,0.83882609665599,1.),(1.00063970687696,
0.806170615310237,1.)))
REPRESENTATION_ITEM('')
SURFACE()
);
#3080=(
BOUNDED_SURFACE()
B_SPLINE_SURFACE(3,2,((#402921,#402922,#402923),(#402924,#402925,#402926),
(#402927,#402928,#402929),(#402930,#402931,#402932)),.UNSPECIFIED.,.F.,
 .F.,.F.)
B_SPLINE_SURFACE_WITH_KNOTS((4,4),(3,3),(2.02993869230508E-5,5.39756952686905E-5),
(-0.000116281070005832,1.),.UNSPECIFIED.)
GEOMETRIC_REPRESENTATION_ITEM()
RATIONAL_B_SPLINE_SURFACE(((1.00001770479731,0.923870681143002,1.),(1.0000101410406,
0.956394275543423,1.),(1.0000203730028,0.912397594905659,1.),(1.00003390859471,
0.854195550869846,1.)))
REPRESENTATION_ITEM('')
SURFACE()
);
#3081=(
BOUNDED_SURFACE()
B_SPLINE_SURFACE(3,2,((#403025,#403026,#403027),(#403028,#403029,#403030),
(#403031,#403032,#403033),(#403034,#403035,#403036)),.UNSPECIFIED.,.F.,
 .F.,.F.)
B_SPLINE_SURFACE_WITH_KNOTS((4,4),(3,3),(0.00135801595889393,0.00148409170619832),
(0.,1.),.UNSPECIFIED.)
GEOMETRIC_REPRESENTATION_ITEM()
RATIONAL_B_SPLINE_SURFACE(((1.,0.818301933966442,1.),(1.,0.817226613172342,
1.),(1.,0.816179643373958,1.),(1.,0.815159387863653,1.)))
REPRESENTATION_ITEM('')
SURFACE()
);
#3082=(
BOUNDED_SURFACE()
B_SPLINE_SURFACE(3,2,((#403075,#403076,#403077),(#403078,#403079,#403080),
(#403081,#403082,#403083),(#403084,#403085,#403086)),.UNSPECIFIED.,.F.,
 .F.,.F.)
B_SPLINE_SURFACE_WITH_KNOTS((4,4),(3,3),(-1.54744435122088E-6,1.54744435122089E-5),
(-0.0151698983713734,1.),.UNSPECIFIED.)
GEOMETRIC_REPRESENTATION_ITEM()
RATIONAL_B_SPLINE_SURFACE(((1.02018382474206,0.334740937350499,1.),(1.00401234489073,
0.86775307281208,1.),(1.00033622856801,0.988917903080762,1.),(1.,1.,1.)))
REPRESENTATION_ITEM('')
SURFACE()
);
#3083=(
BOUNDED_SURFACE()
B_SPLINE_SURFACE(3,2,((#403088,#403089,#403090),(#403091,#403092,#403093),
(#403094,#403095,#403096),(#403097,#403098,#403099)),.UNSPECIFIED.,.F.,
 .F.,.F.)
B_SPLINE_SURFACE_WITH_KNOTS((4,4),(3,3),(0.00137194782501028,0.00149814269699235),
(0.,1.),.UNSPECIFIED.)
GEOMETRIC_REPRESENTATION_ITEM()
RATIONAL_B_SPLINE_SURFACE(((1.,0.815158509402318,1.),(1.,0.816179044148161,
1.),(1.,0.817226308119928,1.),(1.,0.818301939488811,1.)))
REPRESENTATION_ITEM('')
SURFACE()
);
#3084=(
BOUNDED_SURFACE()
B_SPLINE_SURFACE(3,2,((#403143,#403144,#403145),(#403146,#403147,#403148),
(#403149,#403150,#403151),(#403152,#403153,#403154)),.UNSPECIFIED.,.F.,
 .F.,.F.)
B_SPLINE_SURFACE_WITH_KNOTS((4,4),(3,3),(1.55009486301138E-5,4.92065510474435E-5),
(-8.13759517814764E-5,1.),.UNSPECIFIED.)
GEOMETRIC_REPRESENTATION_ITEM()
RATIONAL_B_SPLINE_SURFACE(((1.00002372912344,0.854200639599645,1.),(1.00001423585999,
0.91253030118051,1.),(1.00000710550473,0.956341495377427,1.),(1.00001238975913,
0.923873338136997,1.)))
REPRESENTATION_ITEM('')
SURFACE()
);
#3085=(
BOUNDED_SURFACE()
B_SPLINE_SURFACE(3,2,((#403158,#403159,#403160),(#403161,#403162,#403163),
(#403164,#403165,#403166),(#403167,#403168,#403169)),.UNSPECIFIED.,.F.,
 .F.,.F.)
B_SPLINE_SURFACE_WITH_KNOTS((4,4),(3,3),(-3.39934179457815E-6,3.73927597403564E-5),
(-0.00186004067386607,1.0006937331742),.UNSPECIFIED.)
GEOMETRIC_REPRESENTATION_ITEM()
RATIONAL_B_SPLINE_SURFACE(((1.00072100136042,0.806051963875458,1.00026859642683),
(1.00060048440144,0.838470803558717,1.0002236999449),(1.00053106448786,
0.857144632272456,1.00019783877214),(1.00054515072843,0.853355459539174,
1.00020308635431)))
REPRESENTATION_ITEM('')
SURFACE()
);
#3086=(
BOUNDED_SURFACE()
B_SPLINE_SURFACE(3,2,((#403171,#403172,#403173),(#403174,#403175,#403176),
(#403177,#403178,#403179),(#403180,#403181,#403182)),.UNSPECIFIED.,.F.,
 .F.,.F.)
B_SPLINE_SURFACE_WITH_KNOTS((4,4),(3,3),(0.,9.54361881492175E-5),(0.,1.),
 .UNSPECIFIED.)
GEOMETRIC_REPRESENTATION_ITEM()
RATIONAL_B_SPLINE_SURFACE(((1.,0.816715621142046,1.),(1.,0.815907587407946,
1.),(1.,0.8151159593452,1.),(1.,0.814339887349193,1.)))
REPRESENTATION_ITEM('')
SURFACE()
);
#3087=(
BOUNDED_SURFACE()
B_SPLINE_SURFACE(3,2,((#403184,#403185,#403186),(#403187,#403188,#403189),
(#403190,#403191,#403192),(#403193,#403194,#403195)),.UNSPECIFIED.,.F.,
 .F.,.F.)
B_SPLINE_SURFACE_WITH_KNOTS((4,4),(3,3),(1.15196480826585E-19,4.68197758448212E-5),
(0.,1.),.UNSPECIFIED.)
GEOMETRIC_REPRESENTATION_ITEM()
RATIONAL_B_SPLINE_SURFACE(((1.,0.816715621142048,1.),(1.,0.953638980025211,
1.),(1.,0.954506925408052,1.),(1.,0.816715621142046,1.)))
REPRESENTATION_ITEM('')
SURFACE()
);
#3088=(
BOUNDED_SURFACE()
B_SPLINE_SURFACE(3,2,((#403197,#403198,#403199),(#403200,#403201,#403202),
(#403203,#403204,#403205),(#403206,#403207,#403208)),.UNSPECIFIED.,.F.,
 .F.,.F.)
B_SPLINE_SURFACE_WITH_KNOTS((4,4),(3,3),(1.0842021724855E-19,9.54361881492177E-5),
(0.,1.),.UNSPECIFIED.)
GEOMETRIC_REPRESENTATION_ITEM()
RATIONAL_B_SPLINE_SURFACE(((1.,0.814339887349194,1.),(1.,0.815115959345202,
1.),(1.,0.815907587407943,1.),(1.,0.81671562114205,1.)))
REPRESENTATION_ITEM('')
SURFACE()
);
#3089=(
BOUNDED_SURFACE()
B_SPLINE_SURFACE(3,2,((#403210,#403211,#403212),(#403213,#403214,#403215),
(#403216,#403217,#403218),(#403219,#403220,#403221)),.UNSPECIFIED.,.F.,
 .F.,.F.)
B_SPLINE_SURFACE_WITH_KNOTS((4,4),(3,3),(-3.39528393502489E-6,3.73481232852738E-5),
(-0.00165018033274941,1.),.UNSPECIFIED.)
GEOMETRIC_REPRESENTATION_ITEM()
RATIONAL_B_SPLINE_SURFACE(((1.0004835438555,0.853487571660473,1.),(1.00047110510905,
0.857256476851541,1.),(1.0005319320109,0.838826096655956,1.),(1.00063970687705,
0.806170615310195,1.)))
REPRESENTATION_ITEM('')
SURFACE()
);
#3090=(
BOUNDED_SURFACE()
B_SPLINE_SURFACE(3,2,((#403225,#403226,#403227),(#403228,#403229,#403230),
(#403231,#403232,#403233),(#403234,#403235,#403236)),.UNSPECIFIED.,.F.,
 .F.,.F.)
B_SPLINE_SURFACE_WITH_KNOTS((4,4),(3,3),(2.02993869230509E-5,5.39756952686902E-5),
(-0.000116281069780791,1.),.UNSPECIFIED.)
GEOMETRIC_REPRESENTATION_ITEM()
RATIONAL_B_SPLINE_SURFACE(((1.00001770479728,0.923870681143022,1.),(1.00001014104058,
0.956394275543426,1.),(1.00002037300276,0.912397594905692,1.),(1.00003390859465,
0.854195550869869,1.)))
REPRESENTATION_ITEM('')
SURFACE()
);
#3091=(
BOUNDED_SURFACE()
B_SPLINE_SURFACE(3,2,((#403329,#403330,#403331),(#403332,#403333,#403334),
(#403335,#403336,#403337),(#403338,#403339,#403340)),.UNSPECIFIED.,.F.,
 .F.,.F.)
B_SPLINE_SURFACE_WITH_KNOTS((4,4),(3,3),(0.00135801595889393,0.00148409170619832),
(0.,1.),.UNSPECIFIED.)
GEOMETRIC_REPRESENTATION_ITEM()
RATIONAL_B_SPLINE_SURFACE(((1.,0.818301933966445,1.),(1.,0.817226613172349,
1.),(1.,0.816179643373942,1.),(1.,0.81515938786366,1.)))
REPRESENTATION_ITEM('')
SURFACE()
);
#3092=(
BOUNDED_SURFACE()
B_SPLINE_SURFACE(3,2,((#403379,#403380,#403381),(#403382,#403383,#403384),
(#403385,#403386,#403387),(#403388,#403389,#403390)),.UNSPECIFIED.,.F.,
 .F.,.F.)
B_SPLINE_SURFACE_WITH_KNOTS((4,4),(3,3),(-1.5474443512208E-6,1.54744435122077E-5),
(-0.0151698983618865,1.01516989836038),.UNSPECIFIED.)
GEOMETRIC_REPRESENTATION_ITEM()
RATIONAL_B_SPLINE_SURFACE(((1.02018382472925,0.324498219413554,1.02018382472721),
(1.00401234488819,0.865716921710617,1.00401234488778),(1.0003362285678,
0.988747276629687,1.00033622856777),(1.,1.,1.)))
REPRESENTATION_ITEM('')
SURFACE()
);
#3093=(
BOUNDED_SURFACE()
B_SPLINE_SURFACE(3,2,((#403392,#403393,#403394),(#403395,#403396,#403397),
(#403398,#403399,#403400),(#403401,#403402,#403403)),.UNSPECIFIED.,.F.,
 .F.,.F.)
B_SPLINE_SURFACE_WITH_KNOTS((4,4),(3,3),(0.00137194782501028,0.00149814269699235),
(0.,1.),.UNSPECIFIED.)
GEOMETRIC_REPRESENTATION_ITEM()
RATIONAL_B_SPLINE_SURFACE(((1.,0.815158509402316,1.),(1.,0.816179044148174,
1.),(1.,0.817226308119917,1.),(1.,0.818301939488799,1.)))
REPRESENTATION_ITEM('')
SURFACE()
);
#3094=(
BOUNDED_SURFACE()
B_SPLINE_SURFACE(3,2,((#403447,#403448,#403449),(#403450,#403451,#403452),
(#403453,#403454,#403455),(#403456,#403457,#403458)),.UNSPECIFIED.,.F.,
 .F.,.F.)
B_SPLINE_SURFACE_WITH_KNOTS((4,4),(3,3),(1.55009486301137E-5,4.92065510474433E-5),
(-8.13759517061083E-5,1.),.UNSPECIFIED.)
GEOMETRIC_REPRESENTATION_ITEM()
RATIONAL_B_SPLINE_SURFACE(((1.00002372912342,0.854200639599651,1.),(1.00001423585997,
0.912530301180521,1.),(1.00000710550473,0.956341495377419,1.),(1.00001238975912,
0.923873338137002,1.)))
REPRESENTATION_ITEM('')
SURFACE()
);
#3095=(
BOUNDED_SURFACE()
B_SPLINE_SURFACE(3,2,((#403462,#403463,#403464),(#403465,#403466,#403467),
(#403468,#403469,#403470),(#403471,#403472,#403473)),.UNSPECIFIED.,.F.,
 .F.,.F.)
B_SPLINE_SURFACE_WITH_KNOTS((4,4),(3,3),(-3.3993417945782E-6,3.73927597403566E-5),
(-0.00186004067396171,1.00069373317445),.UNSPECIFIED.)
GEOMETRIC_REPRESENTATION_ITEM()
RATIONAL_B_SPLINE_SURFACE(((1.00072100136046,0.80605196387537,1.00026859642693),
(1.00060048440147,0.8384708035587,1.00022369994497),(1.00053106448788,0.857144632272388,
1.00019783877221),(1.00054515072846,0.853355459539131,1.00020308635438)))
REPRESENTATION_ITEM('')
SURFACE()
);
#3096=(
BOUNDED_SURFACE()
B_SPLINE_SURFACE(3,2,((#403475,#403476,#403477),(#403478,#403479,#403480),
(#403481,#403482,#403483),(#403484,#403485,#403486)),.UNSPECIFIED.,.F.,
 .F.,.F.)
B_SPLINE_SURFACE_WITH_KNOTS((4,4),(3,3),(3.25260651745651E-19,9.54361881492175E-5),
(0.,1.),.UNSPECIFIED.)
GEOMETRIC_REPRESENTATION_ITEM()
RATIONAL_B_SPLINE_SURFACE(((1.,0.81671562114205,1.),(1.,0.815907587407942,
1.),(1.,0.815115959345214,1.),(1.,0.814339887349196,1.)))
REPRESENTATION_ITEM('')
SURFACE()
);
#3097=(
BOUNDED_SURFACE()
B_SPLINE_SURFACE(3,2,((#403488,#403489,#403490),(#403491,#403492,#403493),
(#403494,#403495,#403496),(#403497,#403498,#403499)),.UNSPECIFIED.,.F.,
 .F.,.F.)
B_SPLINE_SURFACE_WITH_KNOTS((4,4),(3,3),(1.8126505071242E-19,4.68197758448212E-5),
(0.,1.),.UNSPECIFIED.)
GEOMETRIC_REPRESENTATION_ITEM()
RATIONAL_B_SPLINE_SURFACE(((1.,0.816715621142049,1.),(1.,0.953638980025205,
1.),(1.,0.954506925408058,1.),(1.,0.816715621142051,1.)))
REPRESENTATION_ITEM('')
SURFACE()
);
#3098=(
BOUNDED_SURFACE()
B_SPLINE_SURFACE(3,2,((#403501,#403502,#403503),(#403504,#403505,#403506),
(#403507,#403508,#403509),(#403510,#403511,#403512)),.UNSPECIFIED.,.F.,
 .F.,.F.)
B_SPLINE_SURFACE_WITH_KNOTS((4,4),(3,3),(2.71050543121376E-19,9.54361881492178E-5),
(0.,1.),.UNSPECIFIED.)
GEOMETRIC_REPRESENTATION_ITEM()
RATIONAL_B_SPLINE_SURFACE(((1.,0.814339887349193,1.),(1.,0.815115959345211,
1.),(1.,0.815907587407943,1.),(1.,0.816715621142048,1.)))
REPRESENTATION_ITEM('')
SURFACE()
);
#3099=(
BOUNDED_SURFACE()
B_SPLINE_SURFACE(3,2,((#403514,#403515,#403516),(#403517,#403518,#403519),
(#403520,#403521,#403522),(#403523,#403524,#403525)),.UNSPECIFIED.,.F.,
 .F.,.F.)
B_SPLINE_SURFACE_WITH_KNOTS((4,4),(3,3),(-3.39528393502497E-6,3.73481232852735E-5),
(-0.00165018033334449,1.),.UNSPECIFIED.)
GEOMETRIC_REPRESENTATION_ITEM()
RATIONAL_B_SPLINE_SURFACE(((1.00048354385567,0.853487571660367,1.),(1.00047110510922,
0.857256476851486,1.),(1.00053193201109,0.838826096655839,1.),(1.00063970687728,
0.806170615310088,1.)))
REPRESENTATION_ITEM('')
SURFACE()
);
#3100=(
BOUNDED_SURFACE()
B_SPLINE_SURFACE(3,2,((#403529,#403530,#403531),(#403532,#403533,#403534),
(#403535,#403536,#403537),(#403538,#403539,#403540)),.UNSPECIFIED.,.F.,
 .F.,.F.)
B_SPLINE_SURFACE_WITH_KNOTS((4,4),(3,3),(2.0299386923051E-5,5.39756952686908E-5),
(-0.000116281069556606,1.),.UNSPECIFIED.)
GEOMETRIC_REPRESENTATION_ITEM()
RATIONAL_B_SPLINE_SURFACE(((1.00001770479724,0.923870681143038,1.),(1.00001014104056,
0.956394275543434,1.),(1.00002037300272,0.912397594905709,1.),(1.00003390859458,
0.854195550869906,1.)))
REPRESENTATION_ITEM('')
SURFACE()
);
#3101=(
BOUNDED_SURFACE()
B_SPLINE_SURFACE(3,2,((#403633,#403634,#403635),(#403636,#403637,#403638),
(#403639,#403640,#403641),(#403642,#403643,#403644)),.UNSPECIFIED.,.F.,
 .F.,.F.)
B_SPLINE_SURFACE_WITH_KNOTS((4,4),(3,3),(0.00135801595889393,0.00148409170619832),
(0.,1.),.UNSPECIFIED.)
GEOMETRIC_REPRESENTATION_ITEM()
RATIONAL_B_SPLINE_SURFACE(((1.,0.818301933966442,1.),(1.,0.817226613172335,
1.),(1.,0.816179643373966,1.),(1.,0.815159387863648,1.)))
REPRESENTATION_ITEM('')
SURFACE()
);
#3102=(
BOUNDED_SURFACE()
B_SPLINE_SURFACE(3,2,((#403683,#403684,#403685),(#403686,#403687,#403688),
(#403689,#403690,#403691),(#403692,#403693,#403694)),.UNSPECIFIED.,.F.,
 .F.,.F.)
B_SPLINE_SURFACE_WITH_KNOTS((4,4),(3,3),(-1.54744435122071E-6,1.54744435122068E-5),
(-0.0151698983644995,1.01516989835826),.UNSPECIFIED.)
GEOMETRIC_REPRESENTATION_ITEM()
RATIONAL_B_SPLINE_SURFACE(((1.02018382473277,0.32449821941328,1.02018382472435),
(1.00401234488889,0.865716921710489,1.00401234488721),(1.00033622856786,
0.988747276629715,1.00033622856772),(1.,1.,1.)))
REPRESENTATION_ITEM('')
SURFACE()
);
#3103=(
BOUNDED_SURFACE()
B_SPLINE_SURFACE(3,2,((#403696,#403697,#403698),(#403699,#403700,#403701),
(#403702,#403703,#403704),(#403705,#403706,#403707)),.UNSPECIFIED.,.F.,
 .F.,.F.)
B_SPLINE_SURFACE_WITH_KNOTS((4,4),(3,3),(0.00137194782501028,0.00149814269699235),
(0.,1.),.UNSPECIFIED.)
GEOMETRIC_REPRESENTATION_ITEM()
RATIONAL_B_SPLINE_SURFACE(((1.,0.815158509402313,1.),(1.,0.816179044148176,
1.),(1.,0.817226308119907,1.),(1.,0.818301939488817,1.)))
REPRESENTATION_ITEM('')
SURFACE()
);
#3104=(
BOUNDED_SURFACE()
B_SPLINE_SURFACE(3,2,((#403751,#403752,#403753),(#403754,#403755,#403756),
(#403757,#403758,#403759),(#403760,#403761,#403762)),.UNSPECIFIED.,.F.,
 .F.,.F.)
B_SPLINE_SURFACE_WITH_KNOTS((4,4),(3,3),(1.55009486301137E-5,4.92065510474431E-5),
(-8.13759512659326E-5,1.),.UNSPECIFIED.)
GEOMETRIC_REPRESENTATION_ITEM()
RATIONAL_B_SPLINE_SURFACE(((1.00002372912329,0.854200639599712,1.),(1.0000142358599,
0.912530301180562,1.),(1.00000710550469,0.95634149537744,1.),(1.00001238975905,
0.923873338137042,1.)))
REPRESENTATION_ITEM('')
SURFACE()
);
#3105=(
BOUNDED_SURFACE()
B_SPLINE_SURFACE(3,2,((#403766,#403767,#403768),(#403769,#403770,#403771),
(#403772,#403773,#403774),(#403775,#403776,#403777)),.UNSPECIFIED.,.F.,
 .F.,.F.)
B_SPLINE_SURFACE_WITH_KNOTS((4,4),(3,3),(-3.3993417945782E-6,3.73927597403566E-5),
(-0.00186004067380188,1.00069373317431),.UNSPECIFIED.)
GEOMETRIC_REPRESENTATION_ITEM()
RATIONAL_B_SPLINE_SURFACE(((1.0007210013604,0.806051963875434,1.00026859642688),
(1.00060048440142,0.838470803558721,1.00022369994493),(1.00053106448784,
0.857144632272437,1.00019783877217),(1.00054515072841,0.853355459539169,
1.00020308635434)))
REPRESENTATION_ITEM('')
SURFACE()
);
#3106=(
BOUNDED_SURFACE()
B_SPLINE_SURFACE(3,2,((#403779,#403780,#403781),(#403782,#403783,#403784),
(#403785,#403786,#403787),(#403788,#403789,#403790)),.UNSPECIFIED.,.F.,
 .F.,.F.)
B_SPLINE_SURFACE_WITH_KNOTS((4,4),(3,3),(-5.42101086242752E-20,9.54361881492174E-5),
(0.,1.),.UNSPECIFIED.)
GEOMETRIC_REPRESENTATION_ITEM()
RATIONAL_B_SPLINE_SURFACE(((1.,0.816715621142048,1.),(1.,0.815907587407946,
1.),(1.,0.815115959345197,1.),(1.,0.814339887349194,1.)))
REPRESENTATION_ITEM('')
SURFACE()
);
#3107=(
BOUNDED_SURFACE()
B_SPLINE_SURFACE(3,2,((#403792,#403793,#403794),(#403795,#403796,#403797),
(#403798,#403799,#403800),(#403801,#403802,#403803)),.UNSPECIFIED.,.F.,
 .F.,.F.)
B_SPLINE_SURFACE_WITH_KNOTS((4,4),(3,3),(-1.79570984817912E-19,4.6819775844821E-5),
(0.,1.),.UNSPECIFIED.)
GEOMETRIC_REPRESENTATION_ITEM()
RATIONAL_B_SPLINE_SURFACE(((1.,0.816715621142045,1.),(1.,0.953638980025212,
1.),(1.,0.954506925408055,1.),(1.,0.816715621142048,1.)))
REPRESENTATION_ITEM('')
SURFACE()
);
#3108=(
BOUNDED_SURFACE()
B_SPLINE_SURFACE(3,2,((#403805,#403806,#403807),(#403808,#403809,#403810),
(#403811,#403812,#403813),(#403814,#403815,#403816)),.UNSPECIFIED.,.F.,
 .F.,.F.)
B_SPLINE_SURFACE_WITH_KNOTS((4,4),(3,3),(-1.0842021724855E-19,9.54361881492175E-5),
(0.,1.),.UNSPECIFIED.)
GEOMETRIC_REPRESENTATION_ITEM()
RATIONAL_B_SPLINE_SURFACE(((1.,0.814339887349193,1.),(1.,0.815115959345213,
1.),(1.,0.815907587407938,1.),(1.,0.816715621142047,1.)))
REPRESENTATION_ITEM('')
SURFACE()
);
#3109=(
BOUNDED_SURFACE()
B_SPLINE_SURFACE(3,2,((#403818,#403819,#403820),(#403821,#403822,#403823),
(#403824,#403825,#403826),(#403827,#403828,#403829)),.UNSPECIFIED.,.F.,
 .F.,.F.)
B_SPLINE_SURFACE_WITH_KNOTS((4,4),(3,3),(-3.39528393502377E-6,3.73481232852734E-5),
(-0.00165018033347931,1.),.UNSPECIFIED.)
GEOMETRIC_REPRESENTATION_ITEM()
RATIONAL_B_SPLINE_SURFACE(((1.00048354385571,0.853487571660351,1.),(1.00047110510926,
0.857256476851438,1.),(1.00053193201114,0.838826096655829,1.),(1.00063970687733,
0.806170615310052,1.)))
REPRESENTATION_ITEM('')
SURFACE()
);
#3110=(
BOUNDED_SURFACE()
B_SPLINE_SURFACE(3,2,((#403833,#403834,#403835),(#403836,#403837,#403838),
(#403839,#403840,#403841),(#403842,#403843,#403844)),.UNSPECIFIED.,.F.,
 .F.,.F.)
B_SPLINE_SURFACE_WITH_KNOTS((4,4),(3,3),(2.02993869230509E-5,5.39756952687133E-5),
(-0.000116281070048236,1.),.UNSPECIFIED.)
GEOMETRIC_REPRESENTATION_ITEM()
RATIONAL_B_SPLINE_SURFACE(((1.00001770479732,0.923870681142996,1.),(1.0000101410406,
0.95639427554344,1.),(1.00002037300281,0.912397594905617,1.),(1.00003390859473,
0.854195550869708,1.)))
REPRESENTATION_ITEM('')
SURFACE()
);
#3111=(
BOUNDED_SURFACE()
B_SPLINE_SURFACE(3,2,((#403937,#403938,#403939),(#403940,#403941,#403942),
(#403943,#403944,#403945),(#403946,#403947,#403948)),.UNSPECIFIED.,.F.,
 .F.,.F.)
B_SPLINE_SURFACE_WITH_KNOTS((4,4),(3,3),(0.00135801595889393,0.00148409170619832),
(0.,1.),.UNSPECIFIED.)
GEOMETRIC_REPRESENTATION_ITEM()
RATIONAL_B_SPLINE_SURFACE(((1.,0.818301933966445,1.),(1.,0.817226613172346,
1.),(1.,0.81617964337396,1.),(1.,0.815159387863655,1.)))
REPRESENTATION_ITEM('')
SURFACE()
);
#3112=(
BOUNDED_SURFACE()
B_SPLINE_SURFACE(3,2,((#403987,#403988,#403989),(#403990,#403991,#403992),
(#403993,#403994,#403995),(#403996,#403997,#403998)),.UNSPECIFIED.,.F.,
 .F.,.F.)
B_SPLINE_SURFACE_WITH_KNOTS((4,4),(3,3),(-1.54744435122081E-6,1.54744435122075E-5),
(-0.015169898363464,1.0151698983591),.UNSPECIFIED.)
GEOMETRIC_REPRESENTATION_ITEM()
RATIONAL_B_SPLINE_SURFACE(((1.02018382473138,0.324498219413331,1.02018382472549),
(1.00401234488861,0.865716921710593,1.00401234488744),(1.00033622856784,
0.988747276629696,1.00033622856774),(1.,1.,1.)))
REPRESENTATION_ITEM('')
SURFACE()
);
#3113=(
BOUNDED_SURFACE()
B_SPLINE_SURFACE(3,2,((#404000,#404001,#404002),(#404003,#404004,#404005),
(#404006,#404007,#404008),(#404009,#404010,#404011)),.UNSPECIFIED.,.F.,
 .F.,.F.)
B_SPLINE_SURFACE_WITH_KNOTS((4,4),(3,3),(0.00137194782501028,0.00149814269699235),
(0.,1.),.UNSPECIFIED.)
GEOMETRIC_REPRESENTATION_ITEM()
RATIONAL_B_SPLINE_SURFACE(((1.,0.815158509402319,1.),(1.,0.816179044148164,
1.),(1.,0.817226308119929,1.),(1.,0.818301939488808,1.)))
REPRESENTATION_ITEM('')
SURFACE()
);
#3114=(
BOUNDED_SURFACE()
B_SPLINE_SURFACE(3,2,((#404055,#404056,#404057),(#404058,#404059,#404060),
(#404061,#404062,#404063),(#404064,#404065,#404066)),.UNSPECIFIED.,.F.,
 .F.,.F.)
B_SPLINE_SURFACE_WITH_KNOTS((4,4),(3,3),(1.55009486301137E-5,4.9206551047443E-5),
(-8.13759512613473E-5,1.),.UNSPECIFIED.)
GEOMETRIC_REPRESENTATION_ITEM()
RATIONAL_B_SPLINE_SURFACE(((1.00002372912329,0.854200639599707,1.),(1.0000142358599,
0.912530301180568,1.),(1.00000710550469,0.956341495377435,1.),(1.00001238975905,
0.923873338137041,1.)))
REPRESENTATION_ITEM('')
SURFACE()
);
#3115=(
BOUNDED_SURFACE()
B_SPLINE_SURFACE(3,2,((#404070,#404071,#404072),(#404073,#404074,#404075),
(#404076,#404077,#404078),(#404079,#404080,#404081)),.UNSPECIFIED.,.F.,
 .F.,.F.)
B_SPLINE_SURFACE_WITH_KNOTS((4,4),(3,3),(-3.39934179457856E-6,3.73927597403564E-5),
(-0.0018600406739503,1.0006937331742),.UNSPECIFIED.)
GEOMETRIC_REPRESENTATION_ITEM()
RATIONAL_B_SPLINE_SURFACE(((1.00072100136045,0.806051963875425,1.00026859642683),
(1.00060048440146,0.838470803558715,1.0002236999449),(1.00053106448788,
0.857144632272439,1.00019783877214),(1.00054515072845,0.853355459539172,
1.00020308635431)))
REPRESENTATION_ITEM('')
SURFACE()
);
#3116=(
BOUNDED_SURFACE()
B_SPLINE_SURFACE(3,2,((#404083,#404084,#404085),(#404086,#404087,#404088),
(#404089,#404090,#404091),(#404092,#404093,#404094)),.UNSPECIFIED.,.F.,
 .F.,.F.)
B_SPLINE_SURFACE_WITH_KNOTS((4,4),(3,3),(1.62630325872826E-19,9.54361881492171E-5),
(0.,1.),.UNSPECIFIED.)
GEOMETRIC_REPRESENTATION_ITEM()
RATIONAL_B_SPLINE_SURFACE(((1.,0.816715621142057,1.),(1.,0.815907587407945,
1.),(1.,0.815115959345199,1.),(1.,0.814339887349194,1.)))
REPRESENTATION_ITEM('')
SURFACE()
);
#3117=(
BOUNDED_SURFACE()
B_SPLINE_SURFACE(3,2,((#404096,#404097,#404098),(#404099,#404100,#404101),
(#404102,#404103,#404104),(#404105,#404106,#404107)),.UNSPECIFIED.,.F.,
 .F.,.F.)
B_SPLINE_SURFACE_WITH_KNOTS((4,4),(3,3),(-2.5410988417629E-20,4.68197758448212E-5),
(0.,1.),.UNSPECIFIED.)
GEOMETRIC_REPRESENTATION_ITEM()
RATIONAL_B_SPLINE_SURFACE(((1.,0.81671562114206,1.),(1.,0.953638980025189,
1.),(1.,0.954506925408053,1.),(1.,0.816715621142049,1.)))
REPRESENTATION_ITEM('')
SURFACE()
);
#3118=(
BOUNDED_SURFACE()
B_SPLINE_SURFACE(3,2,((#404109,#404110,#404111),(#404112,#404113,#404114),
(#404115,#404116,#404117),(#404118,#404119,#404120)),.UNSPECIFIED.,.F.,
 .F.,.F.)
B_SPLINE_SURFACE_WITH_KNOTS((4,4),(3,3),(0.,9.54361881492177E-5),(0.,1.),
 .UNSPECIFIED.)
GEOMETRIC_REPRESENTATION_ITEM()
RATIONAL_B_SPLINE_SURFACE(((1.,0.814339887349206,1.),(1.,0.815115959345194,
1.),(1.,0.815907587407949,1.),(1.,0.816715621142061,1.)))
REPRESENTATION_ITEM('')
SURFACE()
);
#3119=(
BOUNDED_SURFACE()
B_SPLINE_SURFACE(3,2,((#404122,#404123,#404124),(#404125,#404126,#404127),
(#404128,#404129,#404130),(#404131,#404132,#404133)),.UNSPECIFIED.,.F.,
 .F.,.F.)
B_SPLINE_SURFACE_WITH_KNOTS((4,4),(3,3),(-3.39528393502479E-6,3.73481232852728E-5),
(-0.0016501803332698,1.),.UNSPECIFIED.)
GEOMETRIC_REPRESENTATION_ITEM()
RATIONAL_B_SPLINE_SURFACE(((1.00048354385565,0.853487571660401,1.),(1.0004711051092,
0.857256476851457,1.),(1.00053193201107,0.83882609665588,1.),(1.00063970687725,
0.806170615310097,1.)))
REPRESENTATION_ITEM('')
SURFACE()
);
#3120=(
BOUNDED_SURFACE()
B_SPLINE_SURFACE(3,2,((#404137,#404138,#404139),(#404140,#404141,#404142),
(#404143,#404144,#404145),(#404146,#404147,#404148)),.UNSPECIFIED.,.F.,
 .F.,.F.)
B_SPLINE_SURFACE_WITH_KNOTS((4,4),(3,3),(2.0299386923051E-5,5.39756952687124E-5),
(-0.000116281069954705,1.),.UNSPECIFIED.)
GEOMETRIC_REPRESENTATION_ITEM()
RATIONAL_B_SPLINE_SURFACE(((1.0000177047973,0.923870681143004,1.),(1.00001014104059,
0.956394275543448,1.),(1.00002037300279,0.912397594905612,1.),(1.0000339085947,
0.854195550869733,1.)))
REPRESENTATION_ITEM('')
SURFACE()
);
#3121=(
BOUNDED_SURFACE()
B_SPLINE_SURFACE(3,2,((#404241,#404242,#404243),(#404244,#404245,#404246),
(#404247,#404248,#404249),(#404250,#404251,#404252)),.UNSPECIFIED.,.F.,
 .F.,.F.)
B_SPLINE_SURFACE_WITH_KNOTS((4,4),(3,3),(0.00135801595889393,0.00148409170619832),
(0.,1.),.UNSPECIFIED.)
GEOMETRIC_REPRESENTATION_ITEM()
RATIONAL_B_SPLINE_SURFACE(((1.,0.818301933966446,1.),(1.,0.817226613172337,
1.),(1.,0.816179643373957,1.),(1.,0.815159387863657,1.)))
REPRESENTATION_ITEM('')
SURFACE()
);
#3122=(
BOUNDED_SURFACE()
B_SPLINE_SURFACE(3,2,((#404291,#404292,#404293),(#404294,#404295,#404296),
(#404297,#404298,#404299),(#404300,#404301,#404302)),.UNSPECIFIED.,.F.,
 .F.,.F.)
B_SPLINE_SURFACE_WITH_KNOTS((4,4),(3,3),(-1.54744435122086E-6,1.54744435122091E-5),
(-0.0151698983689157,1.0151698983533),.UNSPECIFIED.)
GEOMETRIC_REPRESENTATION_ITEM()
RATIONAL_B_SPLINE_SURFACE(((1.02018382473874,0.324498219413532,1.02018382471765),
(1.00401234489008,0.865716921710509,1.00401234488588),(1.00033622856796,
0.988747276629715,1.00033622856761),(1.,1.,1.)))
REPRESENTATION_ITEM('')
SURFACE()
);
#3123=(
BOUNDED_SURFACE()
B_SPLINE_SURFACE(3,2,((#404304,#404305,#404306),(#404307,#404308,#404309),
(#404310,#404311,#404312),(#404313,#404314,#404315)),.UNSPECIFIED.,.F.,
 .F.,.F.)
B_SPLINE_SURFACE_WITH_KNOTS((4,4),(3,3),(0.00137194782501028,0.00149814269699235),
(0.,1.),.UNSPECIFIED.)
GEOMETRIC_REPRESENTATION_ITEM()
RATIONAL_B_SPLINE_SURFACE(((1.,0.815158509402316,1.),(1.,0.816179044148173,
1.),(1.,0.81722630811992,1.),(1.,0.818301939488806,1.)))
REPRESENTATION_ITEM('')
SURFACE()
);
#3124=(
BOUNDED_SURFACE()
B_SPLINE_SURFACE(3,2,((#404359,#404360,#404361),(#404362,#404363,#404364),
(#404365,#404366,#404367),(#404368,#404369,#404370)),.UNSPECIFIED.,.F.,
 .F.,.F.)
B_SPLINE_SURFACE_WITH_KNOTS((4,4),(3,3),(1.55009486301137E-5,4.92065510474437E-5),
(-8.13759512178582E-5,1.),.UNSPECIFIED.)
GEOMETRIC_REPRESENTATION_ITEM()
RATIONAL_B_SPLINE_SURFACE(((1.00002372912328,0.854200639599716,1.),(1.00001423585989,
0.912530301180565,1.),(1.00000710550468,0.956341495377443,1.),(1.00001238975904,
0.923873338137041,1.)))
REPRESENTATION_ITEM('')
SURFACE()
);
#3125=(
BOUNDED_SURFACE()
B_SPLINE_SURFACE(3,2,((#404374,#404375,#404376),(#404377,#404378,#404379),
(#404380,#404381,#404382),(#404383,#404384,#404385)),.UNSPECIFIED.,.F.,
 .F.,.F.)
B_SPLINE_SURFACE_WITH_KNOTS((4,4),(3,3),(-3.3993417945784E-6,3.73927597403564E-5),
(-0.00186004067426403,1.0006937331744),.UNSPECIFIED.)
GEOMETRIC_REPRESENTATION_ITEM()
RATIONAL_B_SPLINE_SURFACE(((1.00072100136058,0.806051963875325,1.00026859642691),
(1.00060048440156,0.838470803558652,1.00022369994496),(1.00053106448797,
0.85714463227235,1.00019783877219),(1.00054515072855,0.853355459539107,
1.00020308635437)))
REPRESENTATION_ITEM('')
SURFACE()
);
#3126=(
BOUNDED_SURFACE()
B_SPLINE_SURFACE(3,2,((#404387,#404388,#404389),(#404390,#404391,#404392),
(#404393,#404394,#404395),(#404396,#404397,#404398)),.UNSPECIFIED.,.F.,
 .F.,.F.)
B_SPLINE_SURFACE_WITH_KNOTS((4,4),(3,3),(1.0842021724855E-19,9.54361881492173E-5),
(0.,1.),.UNSPECIFIED.)
GEOMETRIC_REPRESENTATION_ITEM()
RATIONAL_B_SPLINE_SURFACE(((1.,0.816715621142061,1.),(1.,0.815907587407937,
1.),(1.,0.815115959345211,1.),(1.,0.814339887349197,1.)))
REPRESENTATION_ITEM('')
SURFACE()
);
#3127=(
BOUNDED_SURFACE()
B_SPLINE_SURFACE(3,2,((#404400,#404401,#404402),(#404403,#404404,#404405),
(#404406,#404407,#404408),(#404409,#404410,#404411)),.UNSPECIFIED.,.F.,
 .F.,.F.)
B_SPLINE_SURFACE_WITH_KNOTS((4,4),(3,3),(6.7762635780344E-20,4.6819775844821E-5),
(0.,1.),.UNSPECIFIED.)
GEOMETRIC_REPRESENTATION_ITEM()
RATIONAL_B_SPLINE_SURFACE(((1.,0.816715621142037,1.),(1.,0.953638980025224,
1.),(1.,0.954506925408043,1.),(1.,0.816715621142053,1.)))
REPRESENTATION_ITEM('')
SURFACE()
);
#3128=(
BOUNDED_SURFACE()
B_SPLINE_SURFACE(3,2,((#404413,#404414,#404415),(#404416,#404417,#404418),
(#404419,#404420,#404421),(#404422,#404423,#404424)),.UNSPECIFIED.,.F.,
 .F.,.F.)
B_SPLINE_SURFACE_WITH_KNOTS((4,4),(3,3),(-2.16840434497101E-19,9.54361881492175E-5),
(0.,1.),.UNSPECIFIED.)
GEOMETRIC_REPRESENTATION_ITEM()
RATIONAL_B_SPLINE_SURFACE(((1.,0.814339887349194,1.),(1.,0.815115959345198,
1.),(1.,0.815907587407953,1.),(1.,0.816715621142038,1.)))
REPRESENTATION_ITEM('')
SURFACE()
);
#3129=(
BOUNDED_SURFACE()
B_SPLINE_SURFACE(3,2,((#404426,#404427,#404428),(#404429,#404430,#404431),
(#404432,#404433,#404434),(#404435,#404436,#404437)),.UNSPECIFIED.,.F.,
 .F.,.F.)
B_SPLINE_SURFACE_WITH_KNOTS((4,4),(3,3),(-3.39528393502481E-6,3.73481232852735E-5),
(-0.00165018033338635,1.),.UNSPECIFIED.)
GEOMETRIC_REPRESENTATION_ITEM()
RATIONAL_B_SPLINE_SURFACE(((1.00048354385569,0.853487571660377,1.),(1.00047110510924,
0.857256476851453,1.),(1.00053193201111,0.838826096655834,1.),(1.0006397068773,
0.806170615310088,1.)))
REPRESENTATION_ITEM('')
SURFACE()
);
#3130=(
BOUNDED_SURFACE()
B_SPLINE_SURFACE(3,2,((#404441,#404442,#404443),(#404444,#404445,#404446),
(#404447,#404448,#404449),(#404450,#404451,#404452)),.UNSPECIFIED.,.F.,
 .F.,.F.)
B_SPLINE_SURFACE_WITH_KNOTS((4,4),(3,3),(2.0299386923051E-5,5.39756952687122E-5),
(-0.000116281070054044,1.),.UNSPECIFIED.)
GEOMETRIC_REPRESENTATION_ITEM()
RATIONAL_B_SPLINE_SURFACE(((1.00001770479732,0.923870681142996,1.),(1.0000101410406,
0.956394275543441,1.),(1.00002037300281,0.912397594905597,1.),(1.00003390859473,
0.854195550869718,1.)))
REPRESENTATION_ITEM('')
SURFACE()
);
#3131=(
BOUNDED_SURFACE()
B_SPLINE_SURFACE(3,2,((#404545,#404546,#404547),(#404548,#404549,#404550),
(#404551,#404552,#404553),(#404554,#404555,#404556)),.UNSPECIFIED.,.F.,
 .F.,.F.)
B_SPLINE_SURFACE_WITH_KNOTS((4,4),(3,3),(0.00135801595889393,0.00148409170619832),
(0.,1.),.UNSPECIFIED.)
GEOMETRIC_REPRESENTATION_ITEM()
RATIONAL_B_SPLINE_SURFACE(((1.,0.818301933966443,1.),(1.,0.817226613172337,
1.),(1.,0.816179643373948,1.),(1.,0.815159387863655,1.)))
REPRESENTATION_ITEM('')
SURFACE()
);
#3132=(
BOUNDED_SURFACE()
B_SPLINE_SURFACE(3,2,((#404595,#404596,#404597),(#404598,#404599,#404600),
(#404601,#404602,#404603),(#404604,#404605,#404606)),.UNSPECIFIED.,.F.,
 .F.,.F.)
B_SPLINE_SURFACE_WITH_KNOTS((4,4),(3,3),(-1.54744435122076E-6,1.54744435122076E-5),
(-0.0151698983610561,1.),.UNSPECIFIED.)
GEOMETRIC_REPRESENTATION_ITEM()
RATIONAL_B_SPLINE_SURFACE(((1.02018382472812,0.334740937357287,1.),(1.00401234488797,
0.867753072813418,1.),(1.00033622856778,0.988917903080862,1.),(1.,1.,1.)))
REPRESENTATION_ITEM('')
SURFACE()
);
#3133=(
BOUNDED_SURFACE()
B_SPLINE_SURFACE(3,2,((#404608,#404609,#404610),(#404611,#404612,#404613),
(#404614,#404615,#404616),(#404617,#404618,#404619)),.UNSPECIFIED.,.F.,
 .F.,.F.)
B_SPLINE_SURFACE_WITH_KNOTS((4,4),(3,3),(0.00137194782501028,0.00149814269699235),
(0.,1.),.UNSPECIFIED.)
GEOMETRIC_REPRESENTATION_ITEM()
RATIONAL_B_SPLINE_SURFACE(((1.,0.815158509402307,1.),(1.,0.816179044148172,
1.),(1.,0.817226308119919,1.),(1.,0.818301939488809,1.)))
REPRESENTATION_ITEM('')
SURFACE()
);
#3134=(
BOUNDED_SURFACE()
B_SPLINE_SURFACE(3,2,((#404663,#404664,#404665),(#404666,#404667,#404668),
(#404669,#404670,#404671),(#404672,#404673,#404674)),.UNSPECIFIED.,.F.,
 .F.,.F.)
B_SPLINE_SURFACE_WITH_KNOTS((4,4),(3,3),(1.55009486301137E-5,4.92065510474431E-5),
(-8.13759512799104E-5,1.),.UNSPECIFIED.)
GEOMETRIC_REPRESENTATION_ITEM()
RATIONAL_B_SPLINE_SURFACE(((1.0000237291233,0.854200639599719,1.),(1.0000142358599,
0.912530301180548,1.),(1.00000710550469,0.956341495377441,1.),(1.00001238975905,
0.923873338137039,1.)))
REPRESENTATION_ITEM('')
SURFACE()
);
#3135=(
BOUNDED_SURFACE()
B_SPLINE_SURFACE(3,2,((#404678,#404679,#404680),(#404681,#404682,#404683),
(#404684,#404685,#404686),(#404687,#404688,#404689)),.UNSPECIFIED.,.F.,
 .F.,.F.)
B_SPLINE_SURFACE_WITH_KNOTS((4,4),(3,3),(-3.39934179457821E-6,3.73927597403565E-5),
(-0.00186004067423112,1.00069373317435),.UNSPECIFIED.)
GEOMETRIC_REPRESENTATION_ITEM()
RATIONAL_B_SPLINE_SURFACE(((1.00072100136056,0.806051963875339,1.00026859642689),
(1.00060048440155,0.83847080355866,1.00022369994494),(1.00053106448796,
0.857144632272363,1.00019783877218),(1.00054515072854,0.853355459539103,
1.00020308635435)))
REPRESENTATION_ITEM('')
SURFACE()
);
#3136=(
BOUNDED_SURFACE()
B_SPLINE_SURFACE(3,2,((#404691,#404692,#404693),(#404694,#404695,#404696),
(#404697,#404698,#404699),(#404700,#404701,#404702)),.UNSPECIFIED.,.F.,
 .F.,.F.)
B_SPLINE_SURFACE_WITH_KNOTS((4,4),(3,3),(0.,9.54361881492174E-5),(0.,1.),
 .UNSPECIFIED.)
GEOMETRIC_REPRESENTATION_ITEM()
RATIONAL_B_SPLINE_SURFACE(((1.,0.816715621142057,1.),(1.,0.815907587407932,
1.),(1.,0.81511595934521,1.),(1.,0.814339887349193,1.)))
REPRESENTATION_ITEM('')
SURFACE()
);
#3137=(
BOUNDED_SURFACE()
B_SPLINE_SURFACE(3,2,((#404704,#404705,#404706),(#404707,#404708,#404709),
(#404710,#404711,#404712),(#404713,#404714,#404715)),.UNSPECIFIED.,.F.,
 .F.,.F.)
B_SPLINE_SURFACE_WITH_KNOTS((4,4),(3,3),(0.,4.68197758448209E-5),(0.,1.),
 .UNSPECIFIED.)
GEOMETRIC_REPRESENTATION_ITEM()
RATIONAL_B_SPLINE_SURFACE(((1.,0.816715621142057,1.),(1.,0.953638980025206,
1.),(1.,0.954506925408047,1.),(1.,0.816715621142055,1.)))
REPRESENTATION_ITEM('')
SURFACE()
);
#3138=(
BOUNDED_SURFACE()
B_SPLINE_SURFACE(3,2,((#404717,#404718,#404719),(#404720,#404721,#404722),
(#404723,#404724,#404725),(#404726,#404727,#404728)),.UNSPECIFIED.,.F.,
 .F.,.F.)
B_SPLINE_SURFACE_WITH_KNOTS((4,4),(3,3),(0.,9.54361881492177E-5),(0.,1.),
 .UNSPECIFIED.)
GEOMETRIC_REPRESENTATION_ITEM()
RATIONAL_B_SPLINE_SURFACE(((1.,0.814339887349193,1.),(1.,0.815115959345207,
1.),(1.,0.815907587407933,1.),(1.,0.816715621142057,1.)))
REPRESENTATION_ITEM('')
SURFACE()
);
#3139=(
BOUNDED_SURFACE()
B_SPLINE_SURFACE(3,2,((#404730,#404731,#404732),(#404733,#404734,#404735),
(#404736,#404737,#404738),(#404739,#404740,#404741)),.UNSPECIFIED.,.F.,
 .F.,.F.)
B_SPLINE_SURFACE_WITH_KNOTS((4,4),(3,3),(-3.39528393502487E-6,3.73481232852736E-5),
(-0.00165018033284231,1.),.UNSPECIFIED.)
GEOMETRIC_REPRESENTATION_ITEM()
RATIONAL_B_SPLINE_SURFACE(((1.00048354385553,0.853487571660461,1.),(1.00047110510908,
0.857256476851525,1.),(1.00053193201093,0.83882609665593,1.),(1.00063970687708,
0.806170615310182,1.)))
REPRESENTATION_ITEM('')
SURFACE()
);
#3140=(
BOUNDED_SURFACE()
B_SPLINE_SURFACE(3,2,((#404745,#404746,#404747),(#404748,#404749,#404750),
(#404751,#404752,#404753),(#404754,#404755,#404756)),.UNSPECIFIED.,.F.,
 .F.,.F.)
B_SPLINE_SURFACE_WITH_KNOTS((4,4),(3,3),(2.02993869230509E-5,5.39756952686906E-5),
(-0.000116281069559425,1.),.UNSPECIFIED.)
GEOMETRIC_REPRESENTATION_ITEM()
RATIONAL_B_SPLINE_SURFACE(((1.00001770479724,0.923870681143036,1.),(1.00001014104056,
0.956394275543435,1.),(1.00002037300272,0.912397594905716,1.),(1.00003390859458,
0.854195550869901,1.)))
REPRESENTATION_ITEM('')
SURFACE()
);
#3141=(
BOUNDED_SURFACE()
B_SPLINE_SURFACE(3,2,((#404849,#404850,#404851),(#404852,#404853,#404854),
(#404855,#404856,#404857),(#404858,#404859,#404860)),.UNSPECIFIED.,.F.,
 .F.,.F.)
B_SPLINE_SURFACE_WITH_KNOTS((4,4),(3,3),(0.00135801595889393,0.00148409170619832),
(0.,1.),.UNSPECIFIED.)
GEOMETRIC_REPRESENTATION_ITEM()
RATIONAL_B_SPLINE_SURFACE(((1.,0.818301933966444,1.),(1.,0.817226613172348,
1.),(1.,0.816179643373956,1.),(1.,0.815159387863656,1.)))
REPRESENTATION_ITEM('')
SURFACE()
);
#3142=(
BOUNDED_SURFACE()
B_SPLINE_SURFACE(3,2,((#404899,#404900,#404901),(#404902,#404903,#404904),
(#404905,#404906,#404907),(#404908,#404909,#404910)),.UNSPECIFIED.,.F.,
 .F.,.F.)
B_SPLINE_SURFACE_WITH_KNOTS((4,4),(3,3),(4.06575814682064E-20,1.54744435122071E-5),
(0.,1.),.UNSPECIFIED.)
GEOMETRIC_REPRESENTATION_ITEM()
RATIONAL_B_SPLINE_SURFACE(((1.,0.478041569704941,1.),(1.,0.890533857552089,
1.),(1.,0.990075913815898,1.),(1.,1.,1.)))
REPRESENTATION_ITEM('')
SURFACE()
);
#3143=(
BOUNDED_SURFACE()
B_SPLINE_SURFACE(3,2,((#404912,#404913,#404914),(#404915,#404916,#404917),
(#404918,#404919,#404920),(#404921,#404922,#404923)),.UNSPECIFIED.,.F.,
 .F.,.F.)
B_SPLINE_SURFACE_WITH_KNOTS((4,4),(3,3),(0.00137194782501028,0.00149814269699235),
(0.,1.),.UNSPECIFIED.)
GEOMETRIC_REPRESENTATION_ITEM()
RATIONAL_B_SPLINE_SURFACE(((1.,0.815158509402317,1.),(1.,0.816179044148144,
1.),(1.,0.817226308119948,1.),(1.,0.818301939488799,1.)))
REPRESENTATION_ITEM('')
SURFACE()
);
#3144=(
BOUNDED_SURFACE()
B_SPLINE_SURFACE(3,2,((#404967,#404968,#404969),(#404970,#404971,#404972),
(#404973,#404974,#404975),(#404976,#404977,#404978)),.UNSPECIFIED.,.F.,
 .F.,.F.)
B_SPLINE_SURFACE_WITH_KNOTS((4,4),(3,3),(1.55009486301137E-5,4.92065510474435E-5),
(-8.13759517818879E-5,1.),.UNSPECIFIED.)
GEOMETRIC_REPRESENTATION_ITEM()
RATIONAL_B_SPLINE_SURFACE(((1.00002372912344,0.854200639599641,1.),(1.00001423585999,
0.912530301180507,1.),(1.00000710550473,0.956341495377427,1.),(1.00001238975913,
0.923873338136997,1.)))
REPRESENTATION_ITEM('')
SURFACE()
);
#3145=(
BOUNDED_SURFACE()
B_SPLINE_SURFACE(3,2,((#404982,#404983,#404984),(#404985,#404986,#404987),
(#404988,#404989,#404990),(#404991,#404992,#404993)),.UNSPECIFIED.,.F.,
 .F.,.F.)
B_SPLINE_SURFACE_WITH_KNOTS((4,4),(3,3),(-3.39934179457839E-6,3.73927597403565E-5),
(-0.00186004067408013,1.00069373317433),.UNSPECIFIED.)
GEOMETRIC_REPRESENTATION_ITEM()
RATIONAL_B_SPLINE_SURFACE(((1.0007210013605,0.806051963875374,1.00026859642689),
(1.0006004844015,0.838470803558685,1.00022369994494),(1.00053106448792,
0.857144632272391,1.00019783877218),(1.00054515072849,0.85335545953913,
1.00020308635435)))
REPRESENTATION_ITEM('')
SURFACE()
);
#3146=(
BOUNDED_SURFACE()
B_SPLINE_SURFACE(3,2,((#404995,#404996,#404997),(#404998,#404999,#405000),
(#405001,#405002,#405003),(#405004,#405005,#405006)),.UNSPECIFIED.,.F.,
 .F.,.F.)
B_SPLINE_SURFACE_WITH_KNOTS((4,4),(3,3),(-1.62630325872826E-19,9.54361881492173E-5),
(0.,1.),.UNSPECIFIED.)
GEOMETRIC_REPRESENTATION_ITEM()
RATIONAL_B_SPLINE_SURFACE(((1.,0.816715621142041,1.),(1.,0.815907587407958,
1.),(1.,0.815115959345198,1.),(1.,0.814339887349188,1.)))
REPRESENTATION_ITEM('')
SURFACE()
);
#3147=(
BOUNDED_SURFACE()
B_SPLINE_SURFACE(3,2,((#405008,#405009,#405010),(#405011,#405012,#405013),
(#405014,#405015,#405016),(#405017,#405018,#405019)),.UNSPECIFIED.,.F.,
 .F.,.F.)
B_SPLINE_SURFACE_WITH_KNOTS((4,4),(3,3),(-2.18534500391609E-19,4.68197758448207E-5),
(0.,1.),.UNSPECIFIED.)
GEOMETRIC_REPRESENTATION_ITEM()
RATIONAL_B_SPLINE_SURFACE(((1.,0.816715621142048,1.),(1.,0.953638980025177,
1.),(1.,0.954506925408093,1.),(1.,0.816715621142042,1.)))
REPRESENTATION_ITEM('')
SURFACE()
);
#3148=(
BOUNDED_SURFACE()
B_SPLINE_SURFACE(3,2,((#405021,#405022,#405023),(#405024,#405025,#405026),
(#405027,#405028,#405029),(#405030,#405031,#405032)),.UNSPECIFIED.,.F.,
 .F.,.F.)
B_SPLINE_SURFACE_WITH_KNOTS((4,4),(3,3),(1.62630325872826E-19,9.54361881492177E-5),
(0.,1.),.UNSPECIFIED.)
GEOMETRIC_REPRESENTATION_ITEM()
RATIONAL_B_SPLINE_SURFACE(((1.,0.814339887349193,1.),(1.,0.815115959345219,
1.),(1.,0.815907587407931,1.),(1.,0.816715621142048,1.)))
REPRESENTATION_ITEM('')
SURFACE()
);
#3149=(
BOUNDED_SURFACE()
B_SPLINE_SURFACE(3,2,((#405034,#405035,#405036),(#405037,#405038,#405039),
(#405040,#405041,#405042),(#405043,#405044,#405045)),.UNSPECIFIED.,.F.,
 .F.,.F.)
B_SPLINE_SURFACE_WITH_KNOTS((4,4),(3,3),(-3.39528393502487E-6,3.73481232852729E-5),
(-0.00165018033325894,1.),.UNSPECIFIED.)
GEOMETRIC_REPRESENTATION_ITEM()
RATIONAL_B_SPLINE_SURFACE(((1.00048354385565,0.853487571660394,1.),(1.0004711051092,
0.857256476851486,1.),(1.00053193201107,0.838826096655843,1.),(1.00063970687725,
0.806170615310116,1.)))
REPRESENTATION_ITEM('')
SURFACE()
);
#3150=(
BOUNDED_SURFACE()
B_SPLINE_SURFACE(3,2,((#405049,#405050,#405051),(#405052,#405053,#405054),
(#405055,#405056,#405057),(#405058,#405059,#405060)),.UNSPECIFIED.,.F.,
 .F.,.F.)
B_SPLINE_SURFACE_WITH_KNOTS((4,4),(3,3),(2.02993869230509E-5,5.3975695268713E-5),
(-0.000116281070087646,1.),.UNSPECIFIED.)
GEOMETRIC_REPRESENTATION_ITEM()
RATIONAL_B_SPLINE_SURFACE(((1.00001770479732,0.923870681142998,1.),(1.0000101410406,
0.956394275543433,1.),(1.00002037300281,0.912397594905605,1.),(1.00003390859474,
0.854195550869712,1.)))
REPRESENTATION_ITEM('')
SURFACE()
);
#3151=(
BOUNDED_SURFACE()
B_SPLINE_SURFACE(3,2,((#405153,#405154,#405155),(#405156,#405157,#405158),
(#405159,#405160,#405161),(#405162,#405163,#405164)),.UNSPECIFIED.,.F.,
 .F.,.F.)
B_SPLINE_SURFACE_WITH_KNOTS((4,4),(3,3),(0.00135801595889393,0.00148409170619832),
(0.,1.),.UNSPECIFIED.)
GEOMETRIC_REPRESENTATION_ITEM()
RATIONAL_B_SPLINE_SURFACE(((1.,0.818301933966444,1.),(1.,0.817226613172336,
1.),(1.,0.816179643373948,1.),(1.,0.815159387863655,1.)))
REPRESENTATION_ITEM('')
SURFACE()
);
#3152=(
BOUNDED_SURFACE()
B_SPLINE_SURFACE(3,2,((#405203,#405204,#405205),(#405206,#405207,#405208),
(#405209,#405210,#405211),(#405212,#405213,#405214)),.UNSPECIFIED.,.F.,
 .F.,.F.)
B_SPLINE_SURFACE_WITH_KNOTS((4,4),(3,3),(-1.54744435122067E-6,1.54744435122073E-5),
(-0.0151698983595576,1.),.UNSPECIFIED.)
GEOMETRIC_REPRESENTATION_ITEM()
RATIONAL_B_SPLINE_SURFACE(((1.0201838247261,0.33474093735822,1.),(1.00401234488756,
0.867753072813637,1.),(1.00033622856775,0.988917903080848,1.),(1.,1.,1.)))
REPRESENTATION_ITEM('')
SURFACE()
);
#3153=(
BOUNDED_SURFACE()
B_SPLINE_SURFACE(3,2,((#405216,#405217,#405218),(#405219,#405220,#405221),
(#405222,#405223,#405224),(#405225,#405226,#405227)),.UNSPECIFIED.,.F.,
 .F.,.F.)
B_SPLINE_SURFACE_WITH_KNOTS((4,4),(3,3),(0.00137194782501028,0.00149814269699235),
(0.,1.),.UNSPECIFIED.)
GEOMETRIC_REPRESENTATION_ITEM()
RATIONAL_B_SPLINE_SURFACE(((1.,0.81515850940232,1.),(1.,0.816179044148172,
1.),(1.,0.81722630811993,1.),(1.,0.818301939488811,1.)))
REPRESENTATION_ITEM('')
SURFACE()
);
#3154=(
BOUNDED_SURFACE()
B_SPLINE_SURFACE(3,2,((#405271,#405272,#405273),(#405274,#405275,#405276),
(#405277,#405278,#405279),(#405280,#405281,#405282)),.UNSPECIFIED.,.F.,
 .F.,.F.)
B_SPLINE_SURFACE_WITH_KNOTS((4,4),(3,3),(1.55009486301137E-5,4.92065510474429E-5),
(-8.1375951146008E-5,1.),.UNSPECIFIED.)
GEOMETRIC_REPRESENTATION_ITEM()
RATIONAL_B_SPLINE_SURFACE(((1.00002372912326,0.854200639599736,1.),(1.00001423585988,
0.912530301180571,1.),(1.00000710550468,0.956341495377441,1.),(1.00001238975903,
0.92387333813705,1.)))
REPRESENTATION_ITEM('')
SURFACE()
);
#3155=(
BOUNDED_SURFACE()
B_SPLINE_SURFACE(3,2,((#405286,#405287,#405288),(#405289,#405290,#405291),
(#405292,#405293,#405294),(#405295,#405296,#405297)),.UNSPECIFIED.,.F.,
 .F.,.F.)
B_SPLINE_SURFACE_WITH_KNOTS((4,4),(3,3),(-3.39934179457831E-6,3.73927597403567E-5),
(-0.00186004067387599,1.00069373317442),.UNSPECIFIED.)
GEOMETRIC_REPRESENTATION_ITEM()
RATIONAL_B_SPLINE_SURFACE(((1.00072100136043,0.806051963875394,1.00026859642692),
(1.00060048440144,0.8384708035587,1.00022369994497),(1.00053106448786,0.857144632272403,
1.0001978387722),(1.00054515072843,0.853355459539154,1.00020308635438)))
REPRESENTATION_ITEM('')
SURFACE()
);
#3156=(
BOUNDED_SURFACE()
B_SPLINE_SURFACE(3,2,((#405299,#405300,#405301),(#405302,#405303,#405304),
(#405305,#405306,#405307),(#405308,#405309,#405310)),.UNSPECIFIED.,.F.,
 .F.,.F.)
B_SPLINE_SURFACE_WITH_KNOTS((4,4),(3,3),(0.,9.54361881492172E-5),(0.,1.),
 .UNSPECIFIED.)
GEOMETRIC_REPRESENTATION_ITEM()
RATIONAL_B_SPLINE_SURFACE(((1.,0.816715621142041,1.),(1.,0.815907587407948,
1.),(1.,0.8151159593452,1.),(1.,0.81433988734919,1.)))
REPRESENTATION_ITEM('')
SURFACE()
);
#3157=(
BOUNDED_SURFACE()
B_SPLINE_SURFACE(3,2,((#405312,#405313,#405314),(#405315,#405316,#405317),
(#405318,#405319,#405320),(#405321,#405322,#405323)),.UNSPECIFIED.,.F.,
 .F.,.F.)
B_SPLINE_SURFACE_WITH_KNOTS((4,4),(3,3),(2.3039296165317E-19,4.68197758448208E-5),
(0.,1.),.UNSPECIFIED.)
GEOMETRIC_REPRESENTATION_ITEM()
RATIONAL_B_SPLINE_SURFACE(((1.,0.816715621142044,1.),(1.,0.95363898002521,
1.),(1.,0.954506925408057,1.),(1.,0.816715621142057,1.)))
REPRESENTATION_ITEM('')
SURFACE()
);
#3158=(
BOUNDED_SURFACE()
B_SPLINE_SURFACE(3,2,((#405325,#405326,#405327),(#405328,#405329,#405330),
(#405331,#405332,#405333),(#405334,#405335,#405336)),.UNSPECIFIED.,.F.,
 .F.,.F.)
B_SPLINE_SURFACE_WITH_KNOTS((4,4),(3,3),(-5.42101086242752E-20,9.54361881492175E-5),
(0.,1.),.UNSPECIFIED.)
GEOMETRIC_REPRESENTATION_ITEM()
RATIONAL_B_SPLINE_SURFACE(((1.,0.814339887349189,1.),(1.,0.81511595934523,
1.),(1.,0.815907587407935,1.),(1.,0.816715621142044,1.)))
REPRESENTATION_ITEM('')
SURFACE()
);
#3159=(
BOUNDED_SURFACE()
B_SPLINE_SURFACE(3,2,((#405338,#405339,#405340),(#405341,#405342,#405343),
(#405344,#405345,#405346),(#405347,#405348,#405349)),.UNSPECIFIED.,.F.,
 .F.,.F.)
B_SPLINE_SURFACE_WITH_KNOTS((4,4),(3,3),(-3.3952839350249E-6,3.73481232852736E-5),
(-0.00165018033293838,1.),.UNSPECIFIED.)
GEOMETRIC_REPRESENTATION_ITEM()
RATIONAL_B_SPLINE_SURFACE(((1.00048354385555,0.853487571660468,1.),(1.00047110510911,
0.857256476851485,1.),(1.00053193201096,0.83882609665595,1.),(1.00063970687712,
0.806170615310157,1.)))
REPRESENTATION_ITEM('')
SURFACE()
);
#3160=(
BOUNDED_SURFACE()
B_SPLINE_SURFACE(3,2,((#405353,#405354,#405355),(#405356,#405357,#405358),
(#405359,#405360,#405361),(#405362,#405363,#405364)),.UNSPECIFIED.,.F.,
 .F.,.F.)
B_SPLINE_SURFACE_WITH_KNOTS((4,4),(3,3),(2.0299386923051E-5,5.3975695268713E-5),
(-0.000116281069768265,1.),.UNSPECIFIED.)
GEOMETRIC_REPRESENTATION_ITEM()
RATIONAL_B_SPLINE_SURFACE(((1.00001770479727,0.923870681143019,1.),(1.00001014104058,
0.95639427554345,1.),(1.00002037300276,0.912397594905637,1.),(1.00003390859464,
0.854195550869751,1.)))
REPRESENTATION_ITEM('')
SURFACE()
);
#3161=(
BOUNDED_SURFACE()
B_SPLINE_SURFACE(3,2,((#405457,#405458,#405459),(#405460,#405461,#405462),
(#405463,#405464,#405465),(#405466,#405467,#405468)),.UNSPECIFIED.,.F.,
 .F.,.F.)
B_SPLINE_SURFACE_WITH_KNOTS((4,4),(3,3),(0.00135801595889393,0.00148409170619832),
(0.,1.),.UNSPECIFIED.)
GEOMETRIC_REPRESENTATION_ITEM()
RATIONAL_B_SPLINE_SURFACE(((1.,0.818301933966443,1.),(1.,0.817226613172352,
1.),(1.,0.816179643373961,1.),(1.,0.815159387863647,1.)))
REPRESENTATION_ITEM('')
SURFACE()
);
#3162=(
BOUNDED_SURFACE()
B_SPLINE_SURFACE(3,2,((#405507,#405508,#405509),(#405510,#405511,#405512),
(#405513,#405514,#405515),(#405516,#405517,#405518)),.UNSPECIFIED.,.F.,
 .F.,.F.)
B_SPLINE_SURFACE_WITH_KNOTS((4,4),(3,3),(-1.54744435122026E-6,1.54744435122097E-5),
(-0.0151698983659335,1.),.UNSPECIFIED.)
GEOMETRIC_REPRESENTATION_ITEM()
RATIONAL_B_SPLINE_SURFACE(((1.02018382473471,0.334740937354024,1.),(1.00401234488928,
0.867753072812738,1.),(1.00033622856789,0.988917903080813,1.),(1.,1.,1.)))
REPRESENTATION_ITEM('')
SURFACE()
);
#3163=(
BOUNDED_SURFACE()
B_SPLINE_SURFACE(3,2,((#405520,#405521,#405522),(#405523,#405524,#405525),
(#405526,#405527,#405528),(#405529,#405530,#405531)),.UNSPECIFIED.,.F.,
 .F.,.F.)
B_SPLINE_SURFACE_WITH_KNOTS((4,4),(3,3),(0.00137194782501028,0.00149814269699235),
(0.,1.),.UNSPECIFIED.)
GEOMETRIC_REPRESENTATION_ITEM()
RATIONAL_B_SPLINE_SURFACE(((1.,0.815158509402312,1.),(1.,0.816179044148169,
1.),(1.,0.817226308119936,1.),(1.,0.818301939488803,1.)))
REPRESENTATION_ITEM('')
SURFACE()
);
#3164=(
BOUNDED_SURFACE()
B_SPLINE_SURFACE(3,2,((#405575,#405576,#405577),(#405578,#405579,#405580),
(#405581,#405582,#405583),(#405584,#405585,#405586)),.UNSPECIFIED.,.F.,
 .F.,.F.)
B_SPLINE_SURFACE_WITH_KNOTS((4,4),(3,3),(1.55009486301137E-5,4.92065510474438E-5),
(-8.13759512935703E-5,1.),.UNSPECIFIED.)
GEOMETRIC_REPRESENTATION_ITEM()
RATIONAL_B_SPLINE_SURFACE(((1.0000237291233,0.854200639599709,1.),(1.0000142358599,
0.912530301180559,1.),(1.00000710550469,0.956341495377438,1.),(1.00001238975906,
0.923873338137037,1.)))
REPRESENTATION_ITEM('')
SURFACE()
);
#3165=(
BOUNDED_SURFACE()
B_SPLINE_SURFACE(3,2,((#405590,#405591,#405592),(#405593,#405594,#405595),
(#405596,#405597,#405598),(#405599,#405600,#405601)),.UNSPECIFIED.,.F.,
 .F.,.F.)
B_SPLINE_SURFACE_WITH_KNOTS((4,4),(3,3),(-3.39934179457839E-6,3.73927597403563E-5),
(-0.00186004067454099,1.00069373317433),.UNSPECIFIED.)
GEOMETRIC_REPRESENTATION_ITEM()
RATIONAL_B_SPLINE_SURFACE(((1.00072100136068,0.80605196387532,1.00026859642688),
(1.00060048440165,0.838470803558564,1.00022369994494),(1.00053106448805,
0.857144632272353,1.00019783877218),(1.00054515072863,0.853355459539056,
1.00020308635435)))
REPRESENTATION_ITEM('')
SURFACE()
);
#3166=(
BOUNDED_SURFACE()
B_SPLINE_SURFACE(3,2,((#405603,#405604,#405605),(#405606,#405607,#405608),
(#405609,#405610,#405611),(#405612,#405613,#405614)),.UNSPECIFIED.,.F.,
 .F.,.F.)
B_SPLINE_SURFACE_WITH_KNOTS((4,4),(3,3),(-5.42101086242752E-20,9.54361881492174E-5),
(0.,1.),.UNSPECIFIED.)
GEOMETRIC_REPRESENTATION_ITEM()
RATIONAL_B_SPLINE_SURFACE(((1.,0.816715621142051,1.),(1.,0.815907587407935,
1.),(1.,0.815115959345206,1.),(1.,0.814339887349197,1.)))
REPRESENTATION_ITEM('')
SURFACE()
);
#3167=(
BOUNDED_SURFACE()
B_SPLINE_SURFACE(3,2,((#405616,#405617,#405618),(#405619,#405620,#405621),
(#405622,#405623,#405624),(#405625,#405626,#405627)),.UNSPECIFIED.,.F.,
 .F.,.F.)
B_SPLINE_SURFACE_WITH_KNOTS((4,4),(3,3),(-1.6940658945086E-19,4.68197758448204E-5),
(0.,1.),.UNSPECIFIED.)
GEOMETRIC_REPRESENTATION_ITEM()
RATIONAL_B_SPLINE_SURFACE(((1.,0.81671562114205,1.),(1.,0.953638980025204,
1.),(1.,0.954506925408062,1.),(1.,0.81671562114205,1.)))
REPRESENTATION_ITEM('')
SURFACE()
);
#3168=(
BOUNDED_SURFACE()
B_SPLINE_SURFACE(3,2,((#405629,#405630,#405631),(#405632,#405633,#405634),
(#405635,#405636,#405637),(#405638,#405639,#405640)),.UNSPECIFIED.,.F.,
 .F.,.F.)
B_SPLINE_SURFACE_WITH_KNOTS((4,4),(3,3),(-3.25260651745651E-19,9.54361881492175E-5),
(0.,1.),.UNSPECIFIED.)
GEOMETRIC_REPRESENTATION_ITEM()
RATIONAL_B_SPLINE_SURFACE(((1.,0.814339887349189,1.),(1.,0.815115959345215,
1.),(1.,0.815907587407932,1.),(1.,0.81671562114205,1.)))
REPRESENTATION_ITEM('')
SURFACE()
);
#3169=(
BOUNDED_SURFACE()
B_SPLINE_SURFACE(3,2,((#405642,#405643,#405644),(#405645,#405646,#405647),
(#405648,#405649,#405650),(#405651,#405652,#405653)),.UNSPECIFIED.,.F.,
 .F.,.F.)
B_SPLINE_SURFACE_WITH_KNOTS((4,4),(3,3),(-3.39528393502489E-6,3.73481232852736E-5),
(-0.00165018033330409,1.),.UNSPECIFIED.)
GEOMETRIC_REPRESENTATION_ITEM()
RATIONAL_B_SPLINE_SURFACE(((1.00048354385566,0.853487571660407,1.),(1.00047110510921,
0.857256476851462,1.),(1.00053193201108,0.838826096655856,1.),(1.00063970687726,
0.806170615310109,1.)))
REPRESENTATION_ITEM('')
SURFACE()
);
#3170=(
BOUNDED_SURFACE()
B_SPLINE_SURFACE(3,2,((#405657,#405658,#405659),(#405660,#405661,#405662),
(#405663,#405664,#405665),(#405666,#405667,#405668)),.UNSPECIFIED.,.F.,
 .F.,.F.)
B_SPLINE_SURFACE_WITH_KNOTS((4,4),(3,3),(2.02993869230511E-5,5.39756952687126E-5),
(-0.000116281069505731,1.),.UNSPECIFIED.)
GEOMETRIC_REPRESENTATION_ITEM()
RATIONAL_B_SPLINE_SURFACE(((1.00001770479723,0.923870681143043,1.),(1.00001014104055,
0.956394275543463,1.),(1.00002037300271,0.912397594905643,1.),(1.00003390859457,
0.854195550869798,1.)))
REPRESENTATION_ITEM('')
SURFACE()
);
#3171=(
BOUNDED_SURFACE()
B_SPLINE_SURFACE(3,2,((#405761,#405762,#405763),(#405764,#405765,#405766),
(#405767,#405768,#405769),(#405770,#405771,#405772)),.UNSPECIFIED.,.F.,
 .F.,.F.)
B_SPLINE_SURFACE_WITH_KNOTS((4,4),(3,3),(0.00135801595889393,0.00148409170619832),
(0.,1.),.UNSPECIFIED.)
GEOMETRIC_REPRESENTATION_ITEM()
RATIONAL_B_SPLINE_SURFACE(((1.,0.818301933966442,1.),(1.,0.817226613172354,
1.),(1.,0.816179643373949,1.),(1.,0.815159387863654,1.)))
REPRESENTATION_ITEM('')
SURFACE()
);
#3172=(
BOUNDED_SURFACE()
B_SPLINE_SURFACE(3,2,((#405811,#405812,#405813),(#405814,#405815,#405816),
(#405817,#405818,#405819),(#405820,#405821,#405822)),.UNSPECIFIED.,.F.,
 .F.,.F.)
B_SPLINE_SURFACE_WITH_KNOTS((4,4),(3,3),(-1.54744435122082E-6,1.54744435122081E-5),
(-0.015169898361091,1.),.UNSPECIFIED.)
GEOMETRIC_REPRESENTATION_ITEM()
RATIONAL_B_SPLINE_SURFACE(((1.02018382472817,0.334740937357215,1.),(1.00401234488797,
0.867753072813476,1.),(1.00033622856778,0.988917903080883,1.),(1.,1.,1.)))
REPRESENTATION_ITEM('')
SURFACE()
);
#3173=(
BOUNDED_SURFACE()
B_SPLINE_SURFACE(3,2,((#405824,#405825,#405826),(#405827,#405828,#405829),
(#405830,#405831,#405832),(#405833,#405834,#405835)),.UNSPECIFIED.,.F.,
 .F.,.F.)
B_SPLINE_SURFACE_WITH_KNOTS((4,4),(3,3),(0.00137194782501028,0.00149814269699235),
(0.,1.),.UNSPECIFIED.)
GEOMETRIC_REPRESENTATION_ITEM()
RATIONAL_B_SPLINE_SURFACE(((1.,0.815158509402314,1.),(1.,0.816179044148165,
1.),(1.,0.817226308119932,1.),(1.,0.818301939488806,1.)))
REPRESENTATION_ITEM('')
SURFACE()
);
#3174=(
BOUNDED_SURFACE()
B_SPLINE_SURFACE(3,2,((#405879,#405880,#405881),(#405882,#405883,#405884),
(#405885,#405886,#405887),(#405888,#405889,#405890)),.UNSPECIFIED.,.F.,
 .F.,.F.)
B_SPLINE_SURFACE_WITH_KNOTS((4,4),(3,3),(1.55009486301137E-5,4.92065510474431E-5),
(-8.13759513357166E-5,1.),.UNSPECIFIED.)
GEOMETRIC_REPRESENTATION_ITEM()
RATIONAL_B_SPLINE_SURFACE(((1.00002372912331,0.854200639599699,1.),(1.00001423585991,
0.912530301180558,1.),(1.00000710550469,0.956341495377437,1.),(1.00001238975906,
0.92387333813703,1.)))
REPRESENTATION_ITEM('')
SURFACE()
);
#3175=(
BOUNDED_SURFACE()
B_SPLINE_SURFACE(3,2,((#405894,#405895,#405896),(#405897,#405898,#405899),
(#405900,#405901,#405902),(#405903,#405904,#405905)),.UNSPECIFIED.,.F.,
 .F.,.F.)
B_SPLINE_SURFACE_WITH_KNOTS((4,4),(3,3),(-3.39934179457816E-6,3.73927597403566E-5),
(-0.0018600406740343,1.00069373317451),.UNSPECIFIED.)
GEOMETRIC_REPRESENTATION_ITEM()
RATIONAL_B_SPLINE_SURFACE(((1.00072100136049,0.806051963875347,1.00026859642695),
(1.00060048440149,0.838470803558664,1.00022369994499),(1.0005310644879,
0.857144632272365,1.00019783877223),(1.00054515072848,0.853355459539118,
1.0002030863544)))
REPRESENTATION_ITEM('')
SURFACE()
);
#3176=(
BOUNDED_SURFACE()
B_SPLINE_SURFACE(3,2,((#405907,#405908,#405909),(#405910,#405911,#405912),
(#405913,#405914,#405915),(#405916,#405917,#405918)),.UNSPECIFIED.,.F.,
 .F.,.F.)
B_SPLINE_SURFACE_WITH_KNOTS((4,4),(3,3),(-5.42101086242752E-20,9.54361881492174E-5),
(0.,1.),.UNSPECIFIED.)
GEOMETRIC_REPRESENTATION_ITEM()
RATIONAL_B_SPLINE_SURFACE(((1.,0.816715621142048,1.),(1.,0.81590758740793,
1.),(1.,0.815115959345223,1.),(1.,0.814339887349182,1.)))
REPRESENTATION_ITEM('')
SURFACE()
);
#3177=(
BOUNDED_SURFACE()
B_SPLINE_SURFACE(3,2,((#405920,#405921,#405922),(#405923,#405924,#405925),
(#405926,#405927,#405928),(#405929,#405930,#405931)),.UNSPECIFIED.,.F.,
 .F.,.F.)
B_SPLINE_SURFACE_WITH_KNOTS((4,4),(3,3),(-1.52465930505774E-20,4.6819775844821E-5),
(0.,1.),.UNSPECIFIED.)
GEOMETRIC_REPRESENTATION_ITEM()
RATIONAL_B_SPLINE_SURFACE(((1.,0.816715621142048,1.),(1.,0.953638980025194,
1.),(1.,0.954506925408067,1.),(1.,0.81671562114205,1.)))
REPRESENTATION_ITEM('')
SURFACE()
);
#3178=(
BOUNDED_SURFACE()
B_SPLINE_SURFACE(3,2,((#405933,#405934,#405935),(#405936,#405937,#405938),
(#405939,#405940,#405941),(#405942,#405943,#405944)),.UNSPECIFIED.,.F.,
 .F.,.F.)
B_SPLINE_SURFACE_WITH_KNOTS((4,4),(3,3),(-5.42101086242752E-20,9.54361881492175E-5),
(0.,1.),.UNSPECIFIED.)
GEOMETRIC_REPRESENTATION_ITEM()
RATIONAL_B_SPLINE_SURFACE(((1.,0.814339887349192,1.),(1.,0.815115959345209,
1.),(1.,0.815907587407939,1.),(1.,0.816715621142048,1.)))
REPRESENTATION_ITEM('')
SURFACE()
);
#3179=(
BOUNDED_SURFACE()
B_SPLINE_SURFACE(3,2,((#405946,#405947,#405948),(#405949,#405950,#405951),
(#405952,#405953,#405954),(#405955,#405956,#405957)),.UNSPECIFIED.,.F.,
 .F.,.F.)
B_SPLINE_SURFACE_WITH_KNOTS((4,4),(3,3),(-3.39528393502372E-6,3.73481232852733E-5),
(-0.00165018033253919,1.),.UNSPECIFIED.)
GEOMETRIC_REPRESENTATION_ITEM()
RATIONAL_B_SPLINE_SURFACE(((1.00048354385544,0.853487571660503,1.),(1.00047110510899,
0.857256476851567,1.),(1.00053193201083,0.838826096655973,1.),(1.00063970687697,
0.806170615310248,1.)))
REPRESENTATION_ITEM('')
SURFACE()
);
#3180=(
BOUNDED_SURFACE()
B_SPLINE_SURFACE(3,2,((#405961,#405962,#405963),(#405964,#405965,#405966),
(#405967,#405968,#405969),(#405970,#405971,#405972)),.UNSPECIFIED.,.F.,
 .F.,.F.)
B_SPLINE_SURFACE_WITH_KNOTS((4,4),(3,3),(2.0299386923051E-5,5.39756952687123E-5),
(-0.000116281069828518,1.),.UNSPECIFIED.)
GEOMETRIC_REPRESENTATION_ITEM()
RATIONAL_B_SPLINE_SURFACE(((1.00001770479728,0.923870681143012,1.),(1.00001014104058,
0.956394275543464,1.),(1.00002037300277,0.912397594905604,1.),(1.00003390859466,
0.854195550869756,1.)))
REPRESENTATION_ITEM('')
SURFACE()
);
#3181=(
BOUNDED_SURFACE()
B_SPLINE_SURFACE(3,2,((#406065,#406066,#406067),(#406068,#406069,#406070),
(#406071,#406072,#406073),(#406074,#406075,#406076)),.UNSPECIFIED.,.F.,
 .F.,.F.)
B_SPLINE_SURFACE_WITH_KNOTS((4,4),(3,3),(0.00135801595889393,0.00148409170619832),
(0.,1.),.UNSPECIFIED.)
GEOMETRIC_REPRESENTATION_ITEM()
RATIONAL_B_SPLINE_SURFACE(((1.,0.818301933966443,1.),(1.,0.817226613172342,
1.),(1.,0.816179643373952,1.),(1.,0.815159387863651,1.)))
REPRESENTATION_ITEM('')
SURFACE()
);
#3182=(
BOUNDED_SURFACE()
B_SPLINE_SURFACE(3,2,((#406115,#406116,#406117),(#406118,#406119,#406120),
(#406121,#406122,#406123),(#406124,#406125,#406126)),.UNSPECIFIED.,.F.,
 .F.,.F.)
B_SPLINE_SURFACE_WITH_KNOTS((4,4),(3,3),(-1.54744435122067E-6,1.54744435122067E-5),
(-0.0151698983602967,1.),.UNSPECIFIED.)
GEOMETRIC_REPRESENTATION_ITEM()
RATIONAL_B_SPLINE_SURFACE(((1.0201838247271,0.334740937357766,1.),(1.00401234488776,
0.867753072813545,1.),(1.00033622856776,0.988917903080887,1.),(1.,1.,1.)))
REPRESENTATION_ITEM('')
SURFACE()
);
#3183=(
BOUNDED_SURFACE()
B_SPLINE_SURFACE(3,2,((#406128,#406129,#406130),(#406131,#406132,#406133),
(#406134,#406135,#406136),(#406137,#406138,#406139)),.UNSPECIFIED.,.F.,
 .F.,.F.)
B_SPLINE_SURFACE_WITH_KNOTS((4,4),(3,3),(0.00137194782501028,0.00149814269699235),
(0.,1.),.UNSPECIFIED.)
GEOMETRIC_REPRESENTATION_ITEM()
RATIONAL_B_SPLINE_SURFACE(((1.,0.815158509402321,1.),(1.,0.816179044148165,
1.),(1.,0.817226308119932,1.),(1.,0.818301939488811,1.)))
REPRESENTATION_ITEM('')
SURFACE()
);
#3184=(
BOUNDED_SURFACE()
B_SPLINE_SURFACE(3,2,((#406183,#406184,#406185),(#406186,#406187,#406188),
(#406189,#406190,#406191),(#406192,#406193,#406194)),.UNSPECIFIED.,.F.,
 .F.,.F.)
B_SPLINE_SURFACE_WITH_KNOTS((4,4),(3,3),(1.55009486301137E-5,4.92065510474429E-5),
(-8.13759516652293E-5,1.),.UNSPECIFIED.)
GEOMETRIC_REPRESENTATION_ITEM()
RATIONAL_B_SPLINE_SURFACE(((1.00002372912341,0.854200639599659,1.),(1.00001423585997,
0.912530301180516,1.),(1.00000710550472,0.95634149537743,1.),(1.00001238975911,
0.923873338137006,1.)))
REPRESENTATION_ITEM('')
SURFACE()
);
#3185=(
BOUNDED_SURFACE()
B_SPLINE_SURFACE(3,2,((#406198,#406199,#406200),(#406201,#406202,#406203),
(#406204,#406205,#406206),(#406207,#406208,#406209)),.UNSPECIFIED.,.F.,
 .F.,.F.)
B_SPLINE_SURFACE_WITH_KNOTS((4,4),(3,3),(-3.39934179457825E-6,3.73927597403566E-5),
(-0.00186004067403026,1.00069373317436),.UNSPECIFIED.)
GEOMETRIC_REPRESENTATION_ITEM()
RATIONAL_B_SPLINE_SURFACE(((1.00072100136049,0.806051963875376,1.00026859642689),
(1.00060048440149,0.838470803558669,1.00022369994495),(1.0005310644879,
0.857144632272403,1.00019783877218),(1.00054515072848,0.853355459539127,
1.00020308635436)))
REPRESENTATION_ITEM('')
SURFACE()
);
#3186=(
BOUNDED_SURFACE()
B_SPLINE_SURFACE(3,2,((#406211,#406212,#406213),(#406214,#406215,#406216),
(#406217,#406218,#406219),(#406220,#406221,#406222)),.UNSPECIFIED.,.F.,
 .F.,.F.)
B_SPLINE_SURFACE_WITH_KNOTS((4,4),(3,3),(-5.42101086242752E-20,9.54361881492172E-5),
(0.,1.),.UNSPECIFIED.)
GEOMETRIC_REPRESENTATION_ITEM()
RATIONAL_B_SPLINE_SURFACE(((1.,0.81671562114205,1.),(1.,0.815907587407941,
1.),(1.,0.815115959345202,1.),(1.,0.814339887349194,1.)))
REPRESENTATION_ITEM('')
SURFACE()
);
#3187=(
BOUNDED_SURFACE()
B_SPLINE_SURFACE(3,2,((#406224,#406225,#406226),(#406227,#406228,#406229),
(#406230,#406231,#406232),(#406233,#406234,#406235)),.UNSPECIFIED.,.F.,
 .F.,.F.)
B_SPLINE_SURFACE_WITH_KNOTS((4,4),(3,3),(-2.03287907341032E-20,4.68197758448218E-5),
(0.,1.),.UNSPECIFIED.)
GEOMETRIC_REPRESENTATION_ITEM()
RATIONAL_B_SPLINE_SURFACE(((1.,0.816715621142045,1.),(1.,0.953638980025206,
1.),(1.,0.954506925408059,1.),(1.,0.816715621142049,1.)))
REPRESENTATION_ITEM('')
SURFACE()
);
#3188=(
BOUNDED_SURFACE()
B_SPLINE_SURFACE(3,2,((#406237,#406238,#406239),(#406240,#406241,#406242),
(#406243,#406244,#406245),(#406246,#406247,#406248)),.UNSPECIFIED.,.F.,
 .F.,.F.)
B_SPLINE_SURFACE_WITH_KNOTS((4,4),(3,3),(0.,9.54361881492173E-5),(0.,1.),
 .UNSPECIFIED.)
GEOMETRIC_REPRESENTATION_ITEM()
RATIONAL_B_SPLINE_SURFACE(((1.,0.814339887349198,1.),(1.,0.815115959345204,
1.),(1.,0.815907587407952,1.),(1.,0.816715621142052,1.)))
REPRESENTATION_ITEM('')
SURFACE()
);
#3189=(
BOUNDED_SURFACE()
B_SPLINE_SURFACE(3,2,((#406250,#406251,#406252),(#406253,#406254,#406255),
(#406256,#406257,#406258),(#406259,#406260,#406261)),.UNSPECIFIED.,.F.,
 .F.,.F.)
B_SPLINE_SURFACE_WITH_KNOTS((4,4),(3,3),(-3.39528393502492E-6,3.73481232852737E-5),
(-0.00165018033268536,1.),.UNSPECIFIED.)
GEOMETRIC_REPRESENTATION_ITEM()
RATIONAL_B_SPLINE_SURFACE(((1.00048354385548,0.853487571660492,1.),(1.00047110510904,
0.857256476851538,1.),(1.00053193201088,0.838826096655981,1.),(1.00063970687702,
0.806170615310209,1.)))
REPRESENTATION_ITEM('')
SURFACE()
);
#3190=(
BOUNDED_SURFACE()
B_SPLINE_SURFACE(3,2,((#406265,#406266,#406267),(#406268,#406269,#406270),
(#406271,#406272,#406273),(#406274,#406275,#406276)),.UNSPECIFIED.,.F.,
 .F.,.F.)
B_SPLINE_SURFACE_WITH_KNOTS((4,4),(3,3),(2.0299386923051E-5,5.39756952687129E-5),
(-0.000116281069912106,1.),.UNSPECIFIED.)
GEOMETRIC_REPRESENTATION_ITEM()
RATIONAL_B_SPLINE_SURFACE(((1.0000177047973,0.923870681143004,1.),(1.00001014104059,
0.956394275543463,1.),(1.00002037300278,0.912397594905594,1.),(1.00003390859469,
0.854195550869741,1.)))
REPRESENTATION_ITEM('')
SURFACE()
);
#3191=(
BOUNDED_SURFACE()
B_SPLINE_SURFACE(3,2,((#406369,#406370,#406371),(#406372,#406373,#406374),
(#406375,#406376,#406377),(#406378,#406379,#406380)),.UNSPECIFIED.,.F.,
 .F.,.F.)
B_SPLINE_SURFACE_WITH_KNOTS((4,4),(3,3),(0.00135801595889393,0.00148409170619832),
(0.,1.),.UNSPECIFIED.)
GEOMETRIC_REPRESENTATION_ITEM()
RATIONAL_B_SPLINE_SURFACE(((1.,0.818301933966445,1.),(1.,0.81722661317235,
1.),(1.,0.816179643373955,1.),(1.,0.815159387863658,1.)))
REPRESENTATION_ITEM('')
SURFACE()
);
#3192=(
BOUNDED_SURFACE()
B_SPLINE_SURFACE(3,2,((#406419,#406420,#406421),(#406422,#406423,#406424),
(#406425,#406426,#406427),(#406428,#406429,#406430)),.UNSPECIFIED.,.F.,
 .F.,.F.)
B_SPLINE_SURFACE_WITH_KNOTS((4,4),(3,3),(-1.54744435122074E-6,1.54744435122073E-5),
(-0.015169898360452,1.),.UNSPECIFIED.)
GEOMETRIC_REPRESENTATION_ITEM()
RATIONAL_B_SPLINE_SURFACE(((1.02018382472731,0.334740937357643,1.),(1.0040123448878,
0.86775307281355,1.),(1.00033622856777,0.988917903080834,1.),(1.,1.,1.)))
REPRESENTATION_ITEM('')
SURFACE()
);
#3193=(
BOUNDED_SURFACE()
B_SPLINE_SURFACE(3,2,((#406432,#406433,#406434),(#406435,#406436,#406437),
(#406438,#406439,#406440),(#406441,#406442,#406443)),.UNSPECIFIED.,.F.,
 .F.,.F.)
B_SPLINE_SURFACE_WITH_KNOTS((4,4),(3,3),(0.00137194782501028,0.00149814269699235),
(0.,1.),.UNSPECIFIED.)
GEOMETRIC_REPRESENTATION_ITEM()
RATIONAL_B_SPLINE_SURFACE(((1.,0.815158509402315,1.),(1.,0.816179044148178,
1.),(1.,0.817226308119919,1.),(1.,0.81830193948881,1.)))
REPRESENTATION_ITEM('')
SURFACE()
);
#3194=(
BOUNDED_SURFACE()
B_SPLINE_SURFACE(3,2,((#406487,#406488,#406489),(#406490,#406491,#406492),
(#406493,#406494,#406495),(#406496,#406497,#406498)),.UNSPECIFIED.,.F.,
 .F.,.F.)
B_SPLINE_SURFACE_WITH_KNOTS((4,4),(3,3),(1.55009486301138E-5,4.92065510474426E-5),
(-8.13759513231332E-5,1.),.UNSPECIFIED.)
GEOMETRIC_REPRESENTATION_ITEM()
RATIONAL_B_SPLINE_SURFACE(((1.00002372912331,0.85420063959971,1.),(1.00001423585991,
0.912530301180546,1.),(1.00000710550469,0.956341495377441,1.),(1.00001238975906,
0.923873338137034,1.)))
REPRESENTATION_ITEM('')
SURFACE()
);
#3195=(
BOUNDED_SURFACE()
B_SPLINE_SURFACE(3,2,((#406502,#406503,#406504),(#406505,#406506,#406507),
(#406508,#406509,#406510),(#406511,#406512,#406513)),.UNSPECIFIED.,.F.,
 .F.,.F.)
B_SPLINE_SURFACE_WITH_KNOTS((4,4),(3,3),(-3.39934179457787E-6,3.73927597403566E-5),
(-0.00186004067382816,1.00069373317414),.UNSPECIFIED.)
GEOMETRIC_REPRESENTATION_ITEM()
RATIONAL_B_SPLINE_SURFACE(((1.00072100136041,0.806051963875452,1.00026859642681),
(1.00060048440142,0.838470803558758,1.00022369994488),(1.00053106448784,
0.857144632272456,1.00019783877212),(1.00054515072842,0.853355459539199,
1.00020308635429)))
REPRESENTATION_ITEM('')
SURFACE()
);
#3196=(
BOUNDED_SURFACE()
B_SPLINE_SURFACE(3,2,((#406515,#406516,#406517),(#406518,#406519,#406520),
(#406521,#406522,#406523),(#406524,#406525,#406526)),.UNSPECIFIED.,.F.,
 .F.,.F.)
B_SPLINE_SURFACE_WITH_KNOTS((4,4),(3,3),(2.16840434497101E-19,9.54361881492174E-5),
(0.,1.),.UNSPECIFIED.)
GEOMETRIC_REPRESENTATION_ITEM()
RATIONAL_B_SPLINE_SURFACE(((1.,0.81671562114205,1.),(1.,0.815907587407943,
1.),(1.,0.815115959345212,1.),(1.,0.814339887349199,1.)))
REPRESENTATION_ITEM('')
SURFACE()
);
#3197=(
BOUNDED_SURFACE()
B_SPLINE_SURFACE(3,2,((#406528,#406529,#406530),(#406531,#406532,#406533),
(#406534,#406535,#406536),(#406537,#406538,#406539)),.UNSPECIFIED.,.F.,
 .F.,.F.)
B_SPLINE_SURFACE_WITH_KNOTS((4,4),(3,3),(-2.72744609015885E-19,4.68197758448208E-5),
(0.,1.),.UNSPECIFIED.)
GEOMETRIC_REPRESENTATION_ITEM()
RATIONAL_B_SPLINE_SURFACE(((1.,0.816715621142048,1.),(1.,0.953638980025201,
1.),(1.,0.954506925408066,1.),(1.,0.81671562114205,1.)))
REPRESENTATION_ITEM('')
SURFACE()
);
#3198=(
BOUNDED_SURFACE()
B_SPLINE_SURFACE(3,2,((#406541,#406542,#406543),(#406544,#406545,#406546),
(#406547,#406548,#406549),(#406550,#406551,#406552)),.UNSPECIFIED.,.F.,
 .F.,.F.)
B_SPLINE_SURFACE_WITH_KNOTS((4,4),(3,3),(-3.79470760369927E-19,9.54361881492174E-5),
(0.,1.),.UNSPECIFIED.)
GEOMETRIC_REPRESENTATION_ITEM()
RATIONAL_B_SPLINE_SURFACE(((1.,0.814339887349195,1.),(1.,0.8151159593452,
1.),(1.,0.815907587407948,1.),(1.,0.816715621142048,1.)))
REPRESENTATION_ITEM('')
SURFACE()
);
#3199=(
BOUNDED_SURFACE()
B_SPLINE_SURFACE(3,2,((#406554,#406555,#406556),(#406557,#406558,#406559),
(#406560,#406561,#406562),(#406563,#406564,#406565)),.UNSPECIFIED.,.F.,
 .F.,.F.)
B_SPLINE_SURFACE_WITH_KNOTS((4,4),(3,3),(-3.39528393502476E-6,3.73481232852733E-5),
(-0.00165018033344203,1.),.UNSPECIFIED.)
GEOMETRIC_REPRESENTATION_ITEM()
RATIONAL_B_SPLINE_SURFACE(((1.0004835438557,0.853487571660372,1.),(1.00047110510925,
0.85725647685145,1.),(1.00053193201113,0.838826096655834,1.),(1.00063970687732,
0.806170615310065,1.)))
REPRESENTATION_ITEM('')
SURFACE()
);
#3200=(
BOUNDED_SURFACE()
B_SPLINE_SURFACE(3,2,((#406569,#406570,#406571),(#406572,#406573,#406574),
(#406575,#406576,#406577),(#406578,#406579,#406580)),.UNSPECIFIED.,.F.,
 .F.,.F.)
B_SPLINE_SURFACE_WITH_KNOTS((4,4),(3,3),(2.02993869230512E-5,5.39756952687121E-5),
(-0.000116281069696749,1.),.UNSPECIFIED.)
GEOMETRIC_REPRESENTATION_ITEM()
RATIONAL_B_SPLINE_SURFACE(((1.00001770479726,0.923870681143028,1.),(1.00001014104057,
0.956394275543456,1.),(1.00002037300274,0.912397594905636,1.),(1.00003390859462,
0.854195550869775,1.)))
REPRESENTATION_ITEM('')
SURFACE()
);
#3201=(
BOUNDED_SURFACE()
B_SPLINE_SURFACE(3,2,((#406673,#406674,#406675),(#406676,#406677,#406678),
(#406679,#406680,#406681),(#406682,#406683,#406684)),.UNSPECIFIED.,.F.,
 .F.,.F.)
B_SPLINE_SURFACE_WITH_KNOTS((4,4),(3,3),(0.00135801595889393,0.00148409170619832),
(0.,1.),.UNSPECIFIED.)
GEOMETRIC_REPRESENTATION_ITEM()
RATIONAL_B_SPLINE_SURFACE(((1.,0.818301933966447,1.),(1.,0.81722661317234,
1.),(1.,0.816179643373958,1.),(1.,0.815159387863653,1.)))
REPRESENTATION_ITEM('')
SURFACE()
);
#3202=(
BOUNDED_SURFACE()
B_SPLINE_SURFACE(3,2,((#406723,#406724,#406725),(#406726,#406727,#406728),
(#406729,#406730,#406731),(#406732,#406733,#406734)),.UNSPECIFIED.,.F.,
 .F.,.F.)
B_SPLINE_SURFACE_WITH_KNOTS((4,4),(3,3),(-1.54744435122086E-6,1.54744435122082E-5),
(-0.0151698983584593,1.),.UNSPECIFIED.)
GEOMETRIC_REPRESENTATION_ITEM()
RATIONAL_B_SPLINE_SURFACE(((1.02018382472462,0.334740937358951,1.),(1.00401234488727,
0.867753072813709,1.),(1.00033622856772,0.988917903080944,1.),(1.,1.,1.)))
REPRESENTATION_ITEM('')
SURFACE()
);
#3203=(
BOUNDED_SURFACE()
B_SPLINE_SURFACE(3,2,((#406736,#406737,#406738),(#406739,#406740,#406741),
(#406742,#406743,#406744),(#406745,#406746,#406747)),.UNSPECIFIED.,.F.,
 .F.,.F.)
B_SPLINE_SURFACE_WITH_KNOTS((4,4),(3,3),(0.00137194782501028,0.00149814269699235),
(0.,1.),.UNSPECIFIED.)
GEOMETRIC_REPRESENTATION_ITEM()
RATIONAL_B_SPLINE_SURFACE(((1.,0.815158509402315,1.),(1.,0.816179044148163,
1.),(1.,0.817226308119928,1.),(1.,0.818301939488807,1.)))
REPRESENTATION_ITEM('')
SURFACE()
);
#3204=(
BOUNDED_SURFACE()
B_SPLINE_SURFACE(3,2,((#406791,#406792,#406793),(#406794,#406795,#406796),
(#406797,#406798,#406799),(#406800,#406801,#406802)),.UNSPECIFIED.,.F.,
 .F.,.F.)
B_SPLINE_SURFACE_WITH_KNOTS((4,4),(3,3),(1.55009486301138E-5,4.92065510474432E-5),
(-8.13759515373864E-5,1.),.UNSPECIFIED.)
GEOMETRIC_REPRESENTATION_ITEM()
RATIONAL_B_SPLINE_SURFACE(((1.00002372912337,0.854200639599679,1.),(1.00001423585994,
0.912530301180528,1.),(1.00000710550471,0.956341495377432,1.),(1.00001238975909,
0.923873338137018,1.)))
REPRESENTATION_ITEM('')
SURFACE()
);
#3205=(
BOUNDED_SURFACE()
B_SPLINE_SURFACE(3,2,((#406806,#406807,#406808),(#406809,#406810,#406811),
(#406812,#406813,#406814),(#406815,#406816,#406817)),.UNSPECIFIED.,.F.,
 .F.,.F.)
B_SPLINE_SURFACE_WITH_KNOTS((4,4),(3,3),(-3.39934179457858E-6,3.73927597403565E-5),
(-0.00186004067447938,1.00069373317472),.UNSPECIFIED.)
GEOMETRIC_REPRESENTATION_ITEM()
RATIONAL_B_SPLINE_SURFACE(((1.00072100136066,0.806051963875218,1.00026859642704),
(1.00060048440163,0.838470803558548,1.00022369994506),(1.00053106448803,
0.857144632272291,1.00019783877229),(1.00054515072861,0.853355459539002,
1.00020308635446)))
REPRESENTATION_ITEM('')
SURFACE()
);
#3206=(
BOUNDED_SURFACE()
B_SPLINE_SURFACE(3,2,((#406819,#406820,#406821),(#406822,#406823,#406824),
(#406825,#406826,#406827),(#406828,#406829,#406830)),.UNSPECIFIED.,.F.,
 .F.,.F.)
B_SPLINE_SURFACE_WITH_KNOTS((4,4),(3,3),(-5.42101086242752E-20,9.54361881492173E-5),
(0.,1.),.UNSPECIFIED.)
GEOMETRIC_REPRESENTATION_ITEM()
RATIONAL_B_SPLINE_SURFACE(((1.,0.81671562114205,1.),(1.,0.815907587407935,
1.),(1.,0.815115959345209,1.),(1.,0.814339887349193,1.)))
REPRESENTATION_ITEM('')
SURFACE()
);
#3207=(
BOUNDED_SURFACE()
B_SPLINE_SURFACE(3,2,((#406832,#406833,#406834),(#406835,#406836,#406837),
(#406838,#406839,#406840),(#406841,#406842,#406843)),.UNSPECIFIED.,.F.,
 .F.,.F.)
B_SPLINE_SURFACE_WITH_KNOTS((4,4),(3,3),(9.14795583034644E-20,4.68197758448201E-5),
(0.,1.),.UNSPECIFIED.)
GEOMETRIC_REPRESENTATION_ITEM()
RATIONAL_B_SPLINE_SURFACE(((1.,0.816715621142048,1.),(1.,0.953638980025215,
1.),(1.,0.954506925408048,1.),(1.,0.81671562114206,1.)))
REPRESENTATION_ITEM('')
SURFACE()
);
#3208=(
BOUNDED_SURFACE()
B_SPLINE_SURFACE(3,2,((#406845,#406846,#406847),(#406848,#406849,#406850),
(#406851,#406852,#406853),(#406854,#406855,#406856)),.UNSPECIFIED.,.F.,
 .F.,.F.)
B_SPLINE_SURFACE_WITH_KNOTS((4,4),(3,3),(0.,9.54361881492178E-5),(0.,1.),
 .UNSPECIFIED.)
GEOMETRIC_REPRESENTATION_ITEM()
RATIONAL_B_SPLINE_SURFACE(((1.,0.814339887349195,1.),(1.,0.815115959345203,
1.),(1.,0.815907587407945,1.),(1.,0.816715621142048,1.)))
REPRESENTATION_ITEM('')
SURFACE()
);
#3209=(
BOUNDED_SURFACE()
B_SPLINE_SURFACE(3,2,((#406858,#406859,#406860),(#406861,#406862,#406863),
(#406864,#406865,#406866),(#406867,#406868,#406869)),.UNSPECIFIED.,.F.,
 .F.,.F.)
B_SPLINE_SURFACE_WITH_KNOTS((4,4),(3,3),(-3.39528393502485E-6,3.73481232852737E-5),
(-0.001650180332763,1.),.UNSPECIFIED.)
GEOMETRIC_REPRESENTATION_ITEM()
RATIONAL_B_SPLINE_SURFACE(((1.0004835438555,0.853487571660472,1.),(1.00047110510906,
0.857256476851533,1.),(1.00053193201091,0.838826096655957,1.),(1.00063970687705,
0.806170615310193,0.999999999999999)))
REPRESENTATION_ITEM('')
SURFACE()
);
#3210=(
BOUNDED_SURFACE()
B_SPLINE_SURFACE(3,2,((#406873,#406874,#406875),(#406876,#406877,#406878),
(#406879,#406880,#406881),(#406882,#406883,#406884)),.UNSPECIFIED.,.F.,
 .F.,.F.)
B_SPLINE_SURFACE_WITH_KNOTS((4,4),(3,3),(2.02993869230511E-5,5.39756952687121E-5),
(-0.000116281069947723,1.),.UNSPECIFIED.)
GEOMETRIC_REPRESENTATION_ITEM()
RATIONAL_B_SPLINE_SURFACE(((1.0000177047973,0.923870681143008,1.),(1.00001014104059,
0.956394275543438,1.),(1.00002037300279,0.912397594905621,1.),(1.0000339085947,
0.854195550869734,1.)))
REPRESENTATION_ITEM('')
SURFACE()
);
#3211=(
BOUNDED_SURFACE()
B_SPLINE_SURFACE(3,2,((#406977,#406978,#406979),(#406980,#406981,#406982),
(#406983,#406984,#406985),(#406986,#406987,#406988)),.UNSPECIFIED.,.F.,
 .F.,.F.)
B_SPLINE_SURFACE_WITH_KNOTS((4,4),(3,3),(0.00135801595889393,0.00148409170619832),
(0.,1.),.UNSPECIFIED.)
GEOMETRIC_REPRESENTATION_ITEM()
RATIONAL_B_SPLINE_SURFACE(((1.,0.818301933966446,1.),(1.,0.817226613172351,
1.),(1.,0.816179643373943,1.),(1.,0.815159387863657,1.)))
REPRESENTATION_ITEM('')
SURFACE()
);
#3212=(
BOUNDED_SURFACE()
B_SPLINE_SURFACE(3,2,((#407027,#407028,#407029),(#407030,#407031,#407032),
(#407033,#407034,#407035),(#407036,#407037,#407038)),.UNSPECIFIED.,.F.,
 .F.,.F.)
B_SPLINE_SURFACE_WITH_KNOTS((4,4),(3,3),(-1.54744435122082E-6,1.5474443512208E-5),
(-0.0151698983592207,1.01516989836348),.UNSPECIFIED.)
GEOMETRIC_REPRESENTATION_ITEM()
RATIONAL_B_SPLINE_SURFACE(((1.02018382472565,0.324498219413281,1.02018382473139),
(1.00401234488747,0.865716921710482,1.00401234488862),(1.00033622856774,
0.98874727662973,1.00033622856783),(1.,1.,1.)))
REPRESENTATION_ITEM('')
SURFACE()
);
#3213=(
BOUNDED_SURFACE()
B_SPLINE_SURFACE(3,2,((#407040,#407041,#407042),(#407043,#407044,#407045),
(#407046,#407047,#407048),(#407049,#407050,#407051)),.UNSPECIFIED.,.F.,
 .F.,.F.)
B_SPLINE_SURFACE_WITH_KNOTS((4,4),(3,3),(0.00137194782501028,0.00149814269699235),
(0.,1.),.UNSPECIFIED.)
GEOMETRIC_REPRESENTATION_ITEM()
RATIONAL_B_SPLINE_SURFACE(((1.,0.815158509402314,1.),(1.,0.816179044148161,
1.),(1.,0.817226308119928,1.),(1.,0.818301939488807,1.)))
REPRESENTATION_ITEM('')
SURFACE()
);
#3214=(
BOUNDED_SURFACE()
B_SPLINE_SURFACE(3,2,((#407095,#407096,#407097),(#407098,#407099,#407100),
(#407101,#407102,#407103),(#407104,#407105,#407106)),.UNSPECIFIED.,.F.,
 .F.,.F.)
B_SPLINE_SURFACE_WITH_KNOTS((4,4),(3,3),(1.55009486301137E-5,4.92065510474436E-5),
(-8.13759513776842E-5,1.),.UNSPECIFIED.)
GEOMETRIC_REPRESENTATION_ITEM()
RATIONAL_B_SPLINE_SURFACE(((1.00002372912333,0.854200639599703,1.),(1.00001423585992,
0.912530301180543,1.),(1.0000071055047,0.956341495377434,1.),(1.00001238975907,
0.92387333813703,1.)))
REPRESENTATION_ITEM('')
SURFACE()
);
#3215=(
BOUNDED_SURFACE()
B_SPLINE_SURFACE(3,2,((#407110,#407111,#407112),(#407113,#407114,#407115),
(#407116,#407117,#407118),(#407119,#407120,#407121)),.UNSPECIFIED.,.F.,
 .F.,.F.)
B_SPLINE_SURFACE_WITH_KNOTS((4,4),(3,3),(-3.39934179457812E-6,3.73927597403563E-5),
(-0.00186004067419253,1.00069373317458),.UNSPECIFIED.)
GEOMETRIC_REPRESENTATION_ITEM()
RATIONAL_B_SPLINE_SURFACE(((1.00072100136055,0.806051963875307,1.00026859642698),
(1.00060048440154,0.838470803558622,1.00022369994502),(1.00053106448795,
0.85714463227235,1.00019783877225),(1.00054515072852,0.853355459539066,
1.00020308635442)))
REPRESENTATION_ITEM('')
SURFACE()
);
#3216=(
BOUNDED_SURFACE()
B_SPLINE_SURFACE(3,2,((#407123,#407124,#407125),(#407126,#407127,#407128),
(#407129,#407130,#407131),(#407132,#407133,#407134)),.UNSPECIFIED.,.F.,
 .F.,.F.)
B_SPLINE_SURFACE_WITH_KNOTS((4,4),(3,3),(1.0842021724855E-19,9.54361881492175E-5),
(0.,1.),.UNSPECIFIED.)
GEOMETRIC_REPRESENTATION_ITEM()
RATIONAL_B_SPLINE_SURFACE(((1.,0.816715621142052,1.),(1.,0.815907587407936,
1.),(1.,0.815115959345211,1.),(1.,0.814339887349192,1.)))
REPRESENTATION_ITEM('')
SURFACE()
);
#3217=(
BOUNDED_SURFACE()
B_SPLINE_SURFACE(3,2,((#407136,#407137,#407138),(#407139,#407140,#407141),
(#407142,#407143,#407144),(#407145,#407146,#407147)),.UNSPECIFIED.,.F.,
 .F.,.F.)
B_SPLINE_SURFACE_WITH_KNOTS((4,4),(3,3),(-2.50721752387273E-19,4.68197758448202E-5),
(0.,1.),.UNSPECIFIED.)
GEOMETRIC_REPRESENTATION_ITEM()
RATIONAL_B_SPLINE_SURFACE(((1.,0.816715621142048,1.),(1.,0.953638980025203,
1.),(1.,0.95450692540806,1.),(1.,0.816715621142054,1.)))
REPRESENTATION_ITEM('')
SURFACE()
);
#3218=(
BOUNDED_SURFACE()
B_SPLINE_SURFACE(3,2,((#407149,#407150,#407151),(#407152,#407153,#407154),
(#407155,#407156,#407157),(#407158,#407159,#407160)),.UNSPECIFIED.,.F.,
 .F.,.F.)
B_SPLINE_SURFACE_WITH_KNOTS((4,4),(3,3),(2.16840434497101E-19,9.54361881492177E-5),
(0.,1.),.UNSPECIFIED.)
GEOMETRIC_REPRESENTATION_ITEM()
RATIONAL_B_SPLINE_SURFACE(((1.,0.81433988734919,1.),(1.,0.815115959345201,
1.),(1.,0.81590758740794,1.),(1.,0.816715621142048,1.)))
REPRESENTATION_ITEM('')
SURFACE()
);
#3219=(
BOUNDED_SURFACE()
B_SPLINE_SURFACE(3,2,((#407162,#407163,#407164),(#407165,#407166,#407167),
(#407168,#407169,#407170),(#407171,#407172,#407173)),.UNSPECIFIED.,.F.,
 .F.,.F.)
B_SPLINE_SURFACE_WITH_KNOTS((4,4),(3,3),(-3.39528393502494E-6,3.73481232852734E-5),
(-0.00165018033333615,1.),.UNSPECIFIED.)
GEOMETRIC_REPRESENTATION_ITEM()
RATIONAL_B_SPLINE_SURFACE(((1.00048354385567,0.853487571660389,1.),(1.00047110510922,
0.857256476851451,1.),(1.00053193201109,0.838826096655853,1.),(1.00063970687728,
0.806170615310085,1.)))
REPRESENTATION_ITEM('')
SURFACE()
);
#3220=(
BOUNDED_SURFACE()
B_SPLINE_SURFACE(3,2,((#407177,#407178,#407179),(#407180,#407181,#407182),
(#407183,#407184,#407185),(#407186,#407187,#407188)),.UNSPECIFIED.,.F.,
 .F.,.F.)
B_SPLINE_SURFACE_WITH_KNOTS((4,4),(3,3),(2.02993869230512E-5,5.39756952687125E-5),
(-0.000116281069885172,1.),.UNSPECIFIED.)
GEOMETRIC_REPRESENTATION_ITEM()
RATIONAL_B_SPLINE_SURFACE(((1.00001770479729,0.923870681143012,1.),(1.00001014104059,
0.956394275543446,1.),(1.00002037300278,0.912397594905608,1.),(1.00003390859468,
0.854195550869753,1.)))
REPRESENTATION_ITEM('')
SURFACE()
);
#3221=(
BOUNDED_SURFACE()
B_SPLINE_SURFACE(3,2,((#407281,#407282,#407283),(#407284,#407285,#407286),
(#407287,#407288,#407289),(#407290,#407291,#407292)),.UNSPECIFIED.,.F.,
 .F.,.F.)
B_SPLINE_SURFACE_WITH_KNOTS((4,4),(3,3),(0.00135801595889393,0.00148409170619832),
(0.,1.),.UNSPECIFIED.)
GEOMETRIC_REPRESENTATION_ITEM()
RATIONAL_B_SPLINE_SURFACE(((1.,0.818301933966446,1.),(1.,0.817226613172354,
1.),(1.,0.816179643373942,1.),(1.,0.815159387863656,1.)))
REPRESENTATION_ITEM('')
SURFACE()
);
#3222=(
BOUNDED_SURFACE()
B_SPLINE_SURFACE(3,2,((#407331,#407332,#407333),(#407334,#407335,#407336),
(#407337,#407338,#407339),(#407340,#407341,#407342)),.UNSPECIFIED.,.F.,
 .F.,.F.)
B_SPLINE_SURFACE_WITH_KNOTS((4,4),(3,3),(-1.54744435122079E-6,1.54744435122076E-5),
(-0.0151698983713926,1.),.UNSPECIFIED.)
GEOMETRIC_REPRESENTATION_ITEM()
RATIONAL_B_SPLINE_SURFACE(((1.02018382474208,0.334740937350454,1.),(1.00401234489074,
0.867753072812112,1.),(1.00033622856801,0.988917903080724,1.),(1.,1.,1.)))
REPRESENTATION_ITEM('')
SURFACE()
);
#3223=(
BOUNDED_SURFACE()
B_SPLINE_SURFACE(3,2,((#407344,#407345,#407346),(#407347,#407348,#407349),
(#407350,#407351,#407352),(#407353,#407354,#407355)),.UNSPECIFIED.,.F.,
 .F.,.F.)
B_SPLINE_SURFACE_WITH_KNOTS((4,4),(3,3),(0.00137194782501028,0.00149814269699235),
(0.,1.),.UNSPECIFIED.)
GEOMETRIC_REPRESENTATION_ITEM()
RATIONAL_B_SPLINE_SURFACE(((1.,0.815158509402318,1.),(1.,0.816179044148164,
1.),(1.,0.817226308119933,1.),(1.,0.818301939488801,1.)))
REPRESENTATION_ITEM('')
SURFACE()
);
#3224=(
BOUNDED_SURFACE()
B_SPLINE_SURFACE(3,2,((#407399,#407400,#407401),(#407402,#407403,#407404),
(#407405,#407406,#407407),(#407408,#407409,#407410)),.UNSPECIFIED.,.F.,
 .F.,.F.)
B_SPLINE_SURFACE_WITH_KNOTS((4,4),(3,3),(1.55009486301138E-5,4.92065510474433E-5),
(-8.13759511895836E-5,1.),.UNSPECIFIED.)
GEOMETRIC_REPRESENTATION_ITEM()
RATIONAL_B_SPLINE_SURFACE(((1.00002372912327,0.854200639599731,1.),(1.00001423585988,
0.91253030118056,1.),(1.00000710550468,0.956341495377448,1.),(1.00001238975904,
0.923873338137045,1.)))
REPRESENTATION_ITEM('')
SURFACE()
);
#3225=(
BOUNDED_SURFACE()
B_SPLINE_SURFACE(3,2,((#407414,#407415,#407416),(#407417,#407418,#407419),
(#407420,#407421,#407422),(#407423,#407424,#407425)),.UNSPECIFIED.,.F.,
 .F.,.F.)
B_SPLINE_SURFACE_WITH_KNOTS((4,4),(3,3),(-3.39934179457792E-6,3.73927597403563E-5),
(-0.00186004067408231,1.00069373317463),.UNSPECIFIED.)
GEOMETRIC_REPRESENTATION_ITEM()
RATIONAL_B_SPLINE_SURFACE(((1.00072100136051,0.806051963875312,1.000268596427),
(1.00060048440151,0.838470803558632,1.00022369994503),(1.00053106448792,
0.857144632272357,1.00019783877226),(1.00054515072849,0.853355459539082,
1.00020308635444)))
REPRESENTATION_ITEM('')
SURFACE()
);
#3226=(
BOUNDED_SURFACE()
B_SPLINE_SURFACE(3,2,((#407427,#407428,#407429),(#407430,#407431,#407432),
(#407433,#407434,#407435),(#407436,#407437,#407438)),.UNSPECIFIED.,.F.,
 .F.,.F.)
B_SPLINE_SURFACE_WITH_KNOTS((4,4),(3,3),(2.71050543121376E-19,9.54361881492175E-5),
(0.,1.),.UNSPECIFIED.)
GEOMETRIC_REPRESENTATION_ITEM()
RATIONAL_B_SPLINE_SURFACE(((1.,0.81671562114205,1.),(1.,0.81590758740794,
1.),(1.,0.815115959345207,1.),(1.,0.814339887349193,1.)))
REPRESENTATION_ITEM('')
SURFACE()
);
#3227=(
BOUNDED_SURFACE()
B_SPLINE_SURFACE(3,2,((#407440,#407441,#407442),(#407443,#407444,#407445),
(#407446,#407447,#407448),(#407449,#407450,#407451)),.UNSPECIFIED.,.F.,
 .F.,.F.)
B_SPLINE_SURFACE_WITH_KNOTS((4,4),(3,3),(-2.71050543121376E-20,4.68197758448206E-5),
(0.,1.),.UNSPECIFIED.)
GEOMETRIC_REPRESENTATION_ITEM()
RATIONAL_B_SPLINE_SURFACE(((1.,0.816715621142048,1.),(1.,0.953638980025207,
1.),(1.,0.954506925408056,1.),(1.,0.81671562114205,1.)))
REPRESENTATION_ITEM('')
SURFACE()
);
#3228=(
BOUNDED_SURFACE()
B_SPLINE_SURFACE(3,2,((#407453,#407454,#407455),(#407456,#407457,#407458),
(#407459,#407460,#407461),(#407462,#407463,#407464)),.UNSPECIFIED.,.F.,
 .F.,.F.)
B_SPLINE_SURFACE_WITH_KNOTS((4,4),(3,3),(0.,9.54361881492175E-5),(0.,1.),
 .UNSPECIFIED.)
GEOMETRIC_REPRESENTATION_ITEM()
RATIONAL_B_SPLINE_SURFACE(((1.,0.814339887349194,1.),(1.,0.815115959345203,
1.),(1.,0.815907587407944,1.),(1.,0.816715621142048,1.)))
REPRESENTATION_ITEM('')
SURFACE()
);
#3229=(
BOUNDED_SURFACE()
B_SPLINE_SURFACE(3,2,((#407466,#407467,#407468),(#407469,#407470,#407471),
(#407472,#407473,#407474),(#407475,#407476,#407477)),.UNSPECIFIED.,.F.,
 .F.,.F.)
B_SPLINE_SURFACE_WITH_KNOTS((4,4),(3,3),(-3.39528393502488E-6,3.7348123285273E-5),
(-0.00165018033331949,1.),.UNSPECIFIED.)
GEOMETRIC_REPRESENTATION_ITEM()
RATIONAL_B_SPLINE_SURFACE(((1.00048354385567,0.853487571660389,1.),(1.00047110510922,
0.857256476851462,1.),(1.00053193201109,0.838826096655859,1.),(1.00063970687727,
0.806170615310095,1.)))
REPRESENTATION_ITEM('')
SURFACE()
);
#3230=(
BOUNDED_SURFACE()
B_SPLINE_SURFACE(3,2,((#407481,#407482,#407483),(#407484,#407485,#407486),
(#407487,#407488,#407489),(#407490,#407491,#407492)),.UNSPECIFIED.,.F.,
 .F.,.F.)
B_SPLINE_SURFACE_WITH_KNOTS((4,4),(3,3),(2.02993869230515E-5,5.39756952687123E-5),
(-0.000116281070470176,1.),.UNSPECIFIED.)
GEOMETRIC_REPRESENTATION_ITEM()
RATIONAL_B_SPLINE_SURFACE(((1.00001770479738,0.923870681142967,1.),(1.00001014104064,
0.95639427554342,1.),(1.00002037300288,0.912397594905563,1.),(1.00003390859485,
0.854195550869658,1.)))
REPRESENTATION_ITEM('')
SURFACE()
);
#3231=(
BOUNDED_SURFACE()
B_SPLINE_SURFACE(3,2,((#407585,#407586,#407587),(#407588,#407589,#407590),
(#407591,#407592,#407593),(#407594,#407595,#407596)),.UNSPECIFIED.,.F.,
 .F.,.F.)
B_SPLINE_SURFACE_WITH_KNOTS((4,4),(3,3),(0.00135801595889393,0.00148409170619832),
(0.,1.),.UNSPECIFIED.)
GEOMETRIC_REPRESENTATION_ITEM()
RATIONAL_B_SPLINE_SURFACE(((1.,0.818301933966439,1.),(1.,0.817226613172349,
1.),(1.,0.816179643373947,1.),(1.,0.815159387863649,1.)))
REPRESENTATION_ITEM('')
SURFACE()
);
#3232=(
BOUNDED_SURFACE()
B_SPLINE_SURFACE(3,2,((#407635,#407636,#407637),(#407638,#407639,#407640),
(#407641,#407642,#407643),(#407644,#407645,#407646)),.UNSPECIFIED.,.F.,
 .F.,.F.)
B_SPLINE_SURFACE_WITH_KNOTS((4,4),(3,3),(1.24937359720009E-20,1.5474443512209E-5),
(0.,1.),.UNSPECIFIED.)
GEOMETRIC_REPRESENTATION_ITEM()
RATIONAL_B_SPLINE_SURFACE(((1.,0.478041569704913,1.),(1.,0.890533857551977,
1.),(1.,0.990075913815931,1.),(1.,1.,1.)))
REPRESENTATION_ITEM('')
SURFACE()
);
#3233=(
BOUNDED_SURFACE()
B_SPLINE_SURFACE(3,2,((#407648,#407649,#407650),(#407651,#407652,#407653),
(#407654,#407655,#407656),(#407657,#407658,#407659)),.UNSPECIFIED.,.F.,
 .F.,.F.)
B_SPLINE_SURFACE_WITH_KNOTS((4,4),(3,3),(0.00137194782501028,0.00149814269699235),
(0.,1.),.UNSPECIFIED.)
GEOMETRIC_REPRESENTATION_ITEM()
RATIONAL_B_SPLINE_SURFACE(((1.,0.81515850940232,1.),(1.,0.816179044148162,
1.),(1.,0.817226308119929,1.),(1.,0.818301939488808,1.)))
REPRESENTATION_ITEM('')
SURFACE()
);
#3234=(
BOUNDED_SURFACE()
B_SPLINE_SURFACE(3,2,((#407703,#407704,#407705),(#407706,#407707,#407708),
(#407709,#407710,#407711),(#407712,#407713,#407714)),.UNSPECIFIED.,.F.,
 .F.,.F.)
B_SPLINE_SURFACE_WITH_KNOTS((4,4),(3,3),(1.55009486301137E-5,4.9206551047444E-5),
(-8.13759515126626E-5,1.),.UNSPECIFIED.)
GEOMETRIC_REPRESENTATION_ITEM()
RATIONAL_B_SPLINE_SURFACE(((1.00002372912336,0.854200639599676,1.),(1.00001423585994,
0.912530301180537,1.),(1.00000710550471,0.956341495377424,1.),(1.00001238975909,
0.923873338137019,1.)))
REPRESENTATION_ITEM('')
SURFACE()
);
#3235=(
BOUNDED_SURFACE()
B_SPLINE_SURFACE(3,2,((#407718,#407719,#407720),(#407721,#407722,#407723),
(#407724,#407725,#407726),(#407727,#407728,#407729)),.UNSPECIFIED.,.F.,
 .F.,.F.)
B_SPLINE_SURFACE_WITH_KNOTS((4,4),(3,3),(-3.39934179457807E-6,3.73927597403565E-5),
(-0.00186004067470178,1.00069373317451),.UNSPECIFIED.)
GEOMETRIC_REPRESENTATION_ITEM()
RATIONAL_B_SPLINE_SURFACE(((1.00072100136075,0.806051963875235,1.00026859642695),
(1.00060048440171,0.838470803558528,1.00022369994499),(1.00053106448809,
0.85714463227229,1.00019783877223),(1.00054515072867,0.853355459539005,
1.0002030863544)))
REPRESENTATION_ITEM('')
SURFACE()
);
#3236=(
BOUNDED_SURFACE()
B_SPLINE_SURFACE(3,2,((#407731,#407732,#407733),(#407734,#407735,#407736),
(#407737,#407738,#407739),(#407740,#407741,#407742)),.UNSPECIFIED.,.F.,
 .F.,.F.)
B_SPLINE_SURFACE_WITH_KNOTS((4,4),(3,3),(2.16840434497101E-19,9.54361881492175E-5),
(0.,1.),.UNSPECIFIED.)
GEOMETRIC_REPRESENTATION_ITEM()
RATIONAL_B_SPLINE_SURFACE(((1.,0.816715621142047,1.),(1.,0.815907587407948,
1.),(1.,0.815115959345199,1.),(1.,0.814339887349196,1.)))
REPRESENTATION_ITEM('')
SURFACE()
);
#3237=(
BOUNDED_SURFACE()
B_SPLINE_SURFACE(3,2,((#407744,#407745,#407746),(#407747,#407748,#407749),
(#407750,#407751,#407752),(#407753,#407754,#407755)),.UNSPECIFIED.,.F.,
 .F.,.F.)
B_SPLINE_SURFACE_WITH_KNOTS((4,4),(3,3),(1.71100655345369E-19,4.68197758448206E-5),
(0.,1.),.UNSPECIFIED.)
GEOMETRIC_REPRESENTATION_ITEM()
RATIONAL_B_SPLINE_SURFACE(((1.,0.816715621142055,1.),(1.,0.9536389800252,
1.),(1.,0.95450692540806,1.),(1.,0.816715621142053,1.)))
REPRESENTATION_ITEM('')
SURFACE()
);
#3238=(
BOUNDED_SURFACE()
B_SPLINE_SURFACE(3,2,((#407757,#407758,#407759),(#407760,#407761,#407762),
(#407763,#407764,#407765),(#407766,#407767,#407768)),.UNSPECIFIED.,.F.,
 .F.,.F.)
B_SPLINE_SURFACE_WITH_KNOTS((4,4),(3,3),(-1.62630325872826E-19,9.54361881492177E-5),
(0.,1.),.UNSPECIFIED.)
GEOMETRIC_REPRESENTATION_ITEM()
RATIONAL_B_SPLINE_SURFACE(((1.,0.814339887349195,1.),(1.,0.81511595934521,
1.),(1.,0.815907587407946,1.),(1.,0.816715621142055,1.)))
REPRESENTATION_ITEM('')
SURFACE()
);
#3239=(
BOUNDED_SURFACE()
B_SPLINE_SURFACE(3,2,((#407770,#407771,#407772),(#407773,#407774,#407775),
(#407776,#407777,#407778),(#407779,#407780,#407781)),.UNSPECIFIED.,.F.,
 .F.,.F.)
B_SPLINE_SURFACE_WITH_KNOTS((4,4),(3,3),(-3.3952839350238E-6,3.73481232852729E-5),
(-0.00165018033326818,1.),.UNSPECIFIED.)
GEOMETRIC_REPRESENTATION_ITEM()
RATIONAL_B_SPLINE_SURFACE(((1.00048354385565,0.853487571660405,1.),(1.0004711051092,
0.85725647685147,1.),(1.00053193201107,0.838826096655865,1.),(1.00063970687725,
0.806170615310107,1.)))
REPRESENTATION_ITEM('')
SURFACE()
);
#3240=(
BOUNDED_SURFACE()
B_SPLINE_SURFACE(3,2,((#407785,#407786,#407787),(#407788,#407789,#407790),
(#407791,#407792,#407793),(#407794,#407795,#407796)),.UNSPECIFIED.,.F.,
 .F.,.F.)
B_SPLINE_SURFACE_WITH_KNOTS((4,4),(3,3),(2.02993869230506E-5,5.39756952687124E-5),
(-0.000116281069760664,1.),.UNSPECIFIED.)
GEOMETRIC_REPRESENTATION_ITEM()
RATIONAL_B_SPLINE_SURFACE(((1.00001770479727,0.923870681143024,1.),(1.00001014104057,
0.956394275543451,1.),(1.00002037300276,0.912397594905623,1.),(1.00003390859464,
0.854195550869758,1.)))
REPRESENTATION_ITEM('')
SURFACE()
);
#3241=(
BOUNDED_SURFACE()
B_SPLINE_SURFACE(3,2,((#407889,#407890,#407891),(#407892,#407893,#407894),
(#407895,#407896,#407897),(#407898,#407899,#407900)),.UNSPECIFIED.,.F.,
 .F.,.F.)
B_SPLINE_SURFACE_WITH_KNOTS((4,4),(3,3),(0.00135801595889393,0.00148409170619832),
(0.,1.),.UNSPECIFIED.)
GEOMETRIC_REPRESENTATION_ITEM()
RATIONAL_B_SPLINE_SURFACE(((1.,0.818301933966445,1.),(1.,0.817226613172328,
1.),(1.,0.816179643373974,1.),(1.,0.815159387863655,1.)))
REPRESENTATION_ITEM('')
SURFACE()
);
#3242=(
BOUNDED_SURFACE()
B_SPLINE_SURFACE(3,2,((#407939,#407940,#407941),(#407942,#407943,#407944),
(#407945,#407946,#407947),(#407948,#407949,#407950)),.UNSPECIFIED.,.F.,
 .F.,.F.)
B_SPLINE_SURFACE_WITH_KNOTS((4,4),(3,3),(-1.5474443512208E-6,1.54744435122079E-5),
(-0.0151698983581421,1.),.UNSPECIFIED.)
GEOMETRIC_REPRESENTATION_ITEM()
RATIONAL_B_SPLINE_SURFACE(((1.02018382472419,0.334740937359151,1.),(1.00401234488718,
0.86775307281386,1.),(1.00033622856772,0.988917903080911,1.),(1.,1.,1.)))
REPRESENTATION_ITEM('')
SURFACE()
);
#3243=(
BOUNDED_SURFACE()
B_SPLINE_SURFACE(3,2,((#407952,#407953,#407954),(#407955,#407956,#407957),
(#407958,#407959,#407960),(#407961,#407962,#407963)),.UNSPECIFIED.,.F.,
 .F.,.F.)
B_SPLINE_SURFACE_WITH_KNOTS((4,4),(3,3),(0.00137194782501028,0.00149814269699235),
(0.,1.),.UNSPECIFIED.)
GEOMETRIC_REPRESENTATION_ITEM()
RATIONAL_B_SPLINE_SURFACE(((1.,0.815158509402316,1.),(1.,0.816179044148151,
1.),(1.,0.817226308119921,1.),(1.,0.818301939488809,1.)))
REPRESENTATION_ITEM('')
SURFACE()
);
#3244=(
BOUNDED_SURFACE()
B_SPLINE_SURFACE(3,2,((#408007,#408008,#408009),(#408010,#408011,#408012),
(#408013,#408014,#408015),(#408016,#408017,#408018)),.UNSPECIFIED.,.F.,
 .F.,.F.)
B_SPLINE_SURFACE_WITH_KNOTS((4,4),(3,3),(1.55009486301138E-5,4.92065510474427E-5),
(-8.13759513980918E-5,1.),.UNSPECIFIED.)
GEOMETRIC_REPRESENTATION_ITEM()
RATIONAL_B_SPLINE_SURFACE(((1.00002372912333,0.854200639599699,1.),(1.00001423585992,
0.912530301180542,1.),(1.0000071055047,0.956341495377437,1.),(1.00001238975907,
0.923873338137028,1.)))
REPRESENTATION_ITEM('')
SURFACE()
);
#3245=(
BOUNDED_SURFACE()
B_SPLINE_SURFACE(3,2,((#408022,#408023,#408024),(#408025,#408026,#408027),
(#408028,#408029,#408030),(#408031,#408032,#408033)),.UNSPECIFIED.,.F.,
 .F.,.F.)
B_SPLINE_SURFACE_WITH_KNOTS((4,4),(3,3),(-3.3993417945781E-6,3.73927597403565E-5),
(-0.00186004067393523,1.00069373317419),.UNSPECIFIED.)
GEOMETRIC_REPRESENTATION_ITEM()
RATIONAL_B_SPLINE_SURFACE(((1.00072100136045,0.806051963875439,1.00026859642683),
(1.00060048440146,0.838470803558701,1.00022369994489),(1.00053106448788,
0.857144632272456,1.00019783877214),(1.00054515072845,0.853355459539164,
1.00020308635431)))
REPRESENTATION_ITEM('')
SURFACE()
);
#3246=(
BOUNDED_SURFACE()
B_SPLINE_SURFACE(3,2,((#408035,#408036,#408037),(#408038,#408039,#408040),
(#408041,#408042,#408043),(#408044,#408045,#408046)),.UNSPECIFIED.,.F.,
 .F.,.F.)
B_SPLINE_SURFACE_WITH_KNOTS((4,4),(3,3),(-1.62630325872826E-19,9.54361881492173E-5),
(0.,1.),.UNSPECIFIED.)
GEOMETRIC_REPRESENTATION_ITEM()
RATIONAL_B_SPLINE_SURFACE(((1.,0.81671562114205,1.),(1.,0.815907587407941,
1.),(1.,0.815115959345208,1.),(1.,0.814339887349192,1.)))
REPRESENTATION_ITEM('')
SURFACE()
);
#3247=(
BOUNDED_SURFACE()
B_SPLINE_SURFACE(3,2,((#408048,#408049,#408050),(#408051,#408052,#408053),
(#408054,#408055,#408056),(#408057,#408058,#408059)),.UNSPECIFIED.,.F.,
 .F.,.F.)
B_SPLINE_SURFACE_WITH_KNOTS((4,4),(3,3),(7.45388993583784E-20,4.68197758448203E-5),
(0.,1.),.UNSPECIFIED.)
GEOMETRIC_REPRESENTATION_ITEM()
RATIONAL_B_SPLINE_SURFACE(((1.,0.816715621142041,1.),(1.,0.953638980025206,
1.),(1.,0.954506925408059,1.),(1.,0.816715621142055,1.)))
REPRESENTATION_ITEM('')
SURFACE()
);
#3248=(
BOUNDED_SURFACE()
B_SPLINE_SURFACE(3,2,((#408061,#408062,#408063),(#408064,#408065,#408066),
(#408067,#408068,#408069),(#408070,#408071,#408072)),.UNSPECIFIED.,.F.,
 .F.,.F.)
B_SPLINE_SURFACE_WITH_KNOTS((4,4),(3,3),(-1.0842021724855E-19,9.54361881492176E-5),
(0.,1.),.UNSPECIFIED.)
GEOMETRIC_REPRESENTATION_ITEM()
RATIONAL_B_SPLINE_SURFACE(((1.,0.814339887349189,1.),(1.,0.815115959345212,
1.),(1.,0.815907587407938,1.),(1.,0.816715621142046,1.)))
REPRESENTATION_ITEM('')
SURFACE()
);
#3249=(
BOUNDED_SURFACE()
B_SPLINE_SURFACE(3,2,((#408074,#408075,#408076),(#408077,#408078,#408079),
(#408080,#408081,#408082),(#408083,#408084,#408085)),.UNSPECIFIED.,.F.,
 .F.,.F.)
B_SPLINE_SURFACE_WITH_KNOTS((4,4),(3,3),(-3.39528393502485E-6,3.73481232852729E-5),
(-0.00165018033279177,1.),.UNSPECIFIED.)
GEOMETRIC_REPRESENTATION_ITEM()
RATIONAL_B_SPLINE_SURFACE(((1.00048354385551,0.853487571660467,1.),(1.00047110510907,
0.857256476851533,1.),(1.00053193201091,0.838826096655952,1.),(1.00063970687706,
0.806170615310181,0.999999999999999)))
REPRESENTATION_ITEM('')
SURFACE()
);
#3250=(
BOUNDED_SURFACE()
B_SPLINE_SURFACE(3,2,((#408089,#408090,#408091),(#408092,#408093,#408094),
(#408095,#408096,#408097),(#408098,#408099,#408100)),.UNSPECIFIED.,.F.,
 .F.,.F.)
B_SPLINE_SURFACE_WITH_KNOTS((4,4),(3,3),(2.0299386923051E-5,5.39756952686906E-5),
(-0.000116281069637203,1.),.UNSPECIFIED.)
GEOMETRIC_REPRESENTATION_ITEM()
RATIONAL_B_SPLINE_SURFACE(((1.00001770479725,0.92387068114303,1.),(1.00001014104056,
0.956394275543433,1.),(1.00002037300273,0.912397594905709,1.),(1.00003390859461,
0.854195550869884,1.)))
REPRESENTATION_ITEM('')
SURFACE()
);
#3251=(
BOUNDED_SURFACE()
B_SPLINE_SURFACE(3,2,((#408193,#408194,#408195),(#408196,#408197,#408198),
(#408199,#408200,#408201),(#408202,#408203,#408204)),.UNSPECIFIED.,.F.,
 .F.,.F.)
B_SPLINE_SURFACE_WITH_KNOTS((4,4),(3,3),(0.00135801595889393,0.00148409170619832),
(0.,1.),.UNSPECIFIED.)
GEOMETRIC_REPRESENTATION_ITEM()
RATIONAL_B_SPLINE_SURFACE(((1.,0.818301933966446,1.),(1.,0.817226613172344,
1.),(1.,0.81617964337396,1.),(1.,0.815159387863656,1.)))
REPRESENTATION_ITEM('')
SURFACE()
);
#3252=(
BOUNDED_SURFACE()
B_SPLINE_SURFACE(3,2,((#408243,#408244,#408245),(#408246,#408247,#408248),
(#408249,#408250,#408251),(#408252,#408253,#408254)),.UNSPECIFIED.,.F.,
 .F.,.F.)
B_SPLINE_SURFACE_WITH_KNOTS((4,4),(3,3),(-1.54744435122072E-6,1.54744435122074E-5),
(-0.0151698983608262,1.),.UNSPECIFIED.)
GEOMETRIC_REPRESENTATION_ITEM()
RATIONAL_B_SPLINE_SURFACE(((1.02018382472781,0.33474093735738,1.),(1.0040123448879,
0.867753072813488,1.),(1.00033622856778,0.988917903080869,1.),(1.,1.,1.)))
REPRESENTATION_ITEM('')
SURFACE()
);
#3253=(
BOUNDED_SURFACE()
B_SPLINE_SURFACE(3,2,((#408256,#408257,#408258),(#408259,#408260,#408261),
(#408262,#408263,#408264),(#408265,#408266,#408267)),.UNSPECIFIED.,.F.,
 .F.,.F.)
B_SPLINE_SURFACE_WITH_KNOTS((4,4),(3,3),(0.00137194782501028,0.00149814269699235),
(0.,1.),.UNSPECIFIED.)
GEOMETRIC_REPRESENTATION_ITEM()
RATIONAL_B_SPLINE_SURFACE(((1.,0.815158509402327,1.),(1.,0.816179044148159,
1.),(1.,0.817226308119928,1.),(1.,0.818301939488813,1.)))
REPRESENTATION_ITEM('')
SURFACE()
);
#3254=(
BOUNDED_SURFACE()
B_SPLINE_SURFACE(3,2,((#408311,#408312,#408313),(#408314,#408315,#408316),
(#408317,#408318,#408319),(#408320,#408321,#408322)),.UNSPECIFIED.,.F.,
 .F.,.F.)
B_SPLINE_SURFACE_WITH_KNOTS((4,4),(3,3),(1.55009486301138E-5,4.92065510474431E-5),
(-8.13759512660296E-5,1.),.UNSPECIFIED.)
GEOMETRIC_REPRESENTATION_ITEM()
RATIONAL_B_SPLINE_SURFACE(((1.00002372912329,0.854200639599717,1.),(1.0000142358599,
0.912530301180557,1.),(1.00000710550469,0.956341495377438,1.),(1.00001238975905,
0.92387333813704,1.)))
REPRESENTATION_ITEM('')
SURFACE()
);
#3255=(
BOUNDED_SURFACE()
B_SPLINE_SURFACE(3,2,((#408326,#408327,#408328),(#408329,#408330,#408331),
(#408332,#408333,#408334),(#408335,#408336,#408337)),.UNSPECIFIED.,.F.,
 .F.,.F.)
B_SPLINE_SURFACE_WITH_KNOTS((4,4),(3,3),(-3.39934179457814E-6,3.73927597403565E-5),
(-0.00186004067420733,1.00069373317452),.UNSPECIFIED.)
GEOMETRIC_REPRESENTATION_ITEM()
RATIONAL_B_SPLINE_SURFACE(((1.00072100136055,0.806051963875316,1.00026859642696),
(1.00060048440155,0.838470803558624,1.000223699945),(1.00053106448795,0.857144632272353,
1.00019783877223),(1.00054515072853,0.853355459539081,1.00020308635441)))
REPRESENTATION_ITEM('')
SURFACE()
);
#3256=(
BOUNDED_SURFACE()
B_SPLINE_SURFACE(3,2,((#408339,#408340,#408341),(#408342,#408343,#408344),
(#408345,#408346,#408347),(#408348,#408349,#408350)),.UNSPECIFIED.,.F.,
 .F.,.F.)
B_SPLINE_SURFACE_WITH_KNOTS((4,4),(3,3),(-5.42101086242752E-20,9.54361881492175E-5),
(0.,1.),.UNSPECIFIED.)
GEOMETRIC_REPRESENTATION_ITEM()
RATIONAL_B_SPLINE_SURFACE(((1.,0.816715621142055,1.),(1.,0.81590758740794,
1.),(1.,0.815115959345211,1.),(1.,0.814339887349194,1.)))
REPRESENTATION_ITEM('')
SURFACE()
);
#3257=(
BOUNDED_SURFACE()
B_SPLINE_SURFACE(3,2,((#408352,#408353,#408354),(#408355,#408356,#408357),
(#408358,#408359,#408360),(#408361,#408362,#408363)),.UNSPECIFIED.,.F.,
 .F.,.F.)
B_SPLINE_SURFACE_WITH_KNOTS((4,4),(3,3),(0.,4.68197758448204E-5),(0.,1.),
 .UNSPECIFIED.)
GEOMETRIC_REPRESENTATION_ITEM()
RATIONAL_B_SPLINE_SURFACE(((1.,0.816715621142046,1.),(1.,0.953638980025203,
1.),(1.,0.954506925408058,1.),(1.,0.816715621142054,1.)))
REPRESENTATION_ITEM('')
SURFACE()
);
#3258=(
BOUNDED_SURFACE()
B_SPLINE_SURFACE(3,2,((#408365,#408366,#408367),(#408368,#408369,#408370),
(#408371,#408372,#408373),(#408374,#408375,#408376)),.UNSPECIFIED.,.F.,
 .F.,.F.)
B_SPLINE_SURFACE_WITH_KNOTS((4,4),(3,3),(-1.62630325872826E-19,9.54361881492175E-5),
(0.,1.),.UNSPECIFIED.)
GEOMETRIC_REPRESENTATION_ITEM()
RATIONAL_B_SPLINE_SURFACE(((1.,0.814339887349194,1.),(1.,0.815115959345217,
1.),(1.,0.815907587407947,1.),(1.,0.816715621142046,1.)))
REPRESENTATION_ITEM('')
SURFACE()
);
#3259=(
BOUNDED_SURFACE()
B_SPLINE_SURFACE(3,2,((#408378,#408379,#408380),(#408381,#408382,#408383),
(#408384,#408385,#408386),(#408387,#408388,#408389)),.UNSPECIFIED.,.F.,
 .F.,.F.)
B_SPLINE_SURFACE_WITH_KNOTS((4,4),(3,3),(-3.39528393502482E-6,3.73481232852737E-5),
(-0.00165018033328133,1.),.UNSPECIFIED.)
GEOMETRIC_REPRESENTATION_ITEM()
RATIONAL_B_SPLINE_SURFACE(((1.00048354385565,0.853487571660392,1.),(1.00047110510921,
0.857256476851488,1.),(1.00053193201107,0.838826096655856,1.),(1.00063970687725,
0.8061706153101,1.)))
REPRESENTATION_ITEM('')
SURFACE()
);
#3260=(
BOUNDED_SURFACE()
B_SPLINE_SURFACE(3,2,((#408393,#408394,#408395),(#408396,#408397,#408398),
(#408399,#408400,#408401),(#408402,#408403,#408404)),.UNSPECIFIED.,.F.,
 .F.,.F.)
B_SPLINE_SURFACE_WITH_KNOTS((4,4),(3,3),(2.02993869230512E-5,5.39756952686903E-5),
(-0.000116281070068554,1.),.UNSPECIFIED.)
GEOMETRIC_REPRESENTATION_ITEM()
RATIONAL_B_SPLINE_SURFACE(((1.00001770479732,0.923870681143002,1.),(1.0000101410406,
0.956394275543405,1.),(1.00002037300281,0.91239759490567,1.),(1.00003390859473,
0.854195550869827,1.)))
REPRESENTATION_ITEM('')
SURFACE()
);
#3261=(
BOUNDED_SURFACE()
B_SPLINE_SURFACE(3,2,((#408497,#408498,#408499),(#408500,#408501,#408502),
(#408503,#408504,#408505),(#408506,#408507,#408508)),.UNSPECIFIED.,.F.,
 .F.,.F.)
B_SPLINE_SURFACE_WITH_KNOTS((4,4),(3,3),(0.00135801595889393,0.00148409170619832),
(0.,1.),.UNSPECIFIED.)
GEOMETRIC_REPRESENTATION_ITEM()
RATIONAL_B_SPLINE_SURFACE(((1.,0.818301933966445,1.),(1.,0.81722661317235,
1.),(1.,0.816179643373944,1.),(1.,0.815159387863652,1.)))
REPRESENTATION_ITEM('')
SURFACE()
);
#3262=(
BOUNDED_SURFACE()
B_SPLINE_SURFACE(3,2,((#408547,#408548,#408549),(#408550,#408551,#408552),
(#408553,#408554,#408555),(#408556,#408557,#408558)),.UNSPECIFIED.,.F.,
 .F.,.F.)
B_SPLINE_SURFACE_WITH_KNOTS((4,4),(3,3),(-1.54744435122071E-6,1.54744435122076E-5),
(-0.0151698983676148,1.),.UNSPECIFIED.)
GEOMETRIC_REPRESENTATION_ITEM()
RATIONAL_B_SPLINE_SURFACE(((1.02018382473698,0.3347409373529,1.),(1.00401234488972,
0.867753072812631,1.),(1.00033622856793,0.98891790308079,1.),(1.,1.,1.)))
REPRESENTATION_ITEM('')
SURFACE()
);
#3263=(
BOUNDED_SURFACE()
B_SPLINE_SURFACE(3,2,((#408560,#408561,#408562),(#408563,#408564,#408565),
(#408566,#408567,#408568),(#408569,#408570,#408571)),.UNSPECIFIED.,.F.,
 .F.,.F.)
B_SPLINE_SURFACE_WITH_KNOTS((4,4),(3,3),(0.00137194782501028,0.00149814269699235),
(0.,1.),.UNSPECIFIED.)
GEOMETRIC_REPRESENTATION_ITEM()
RATIONAL_B_SPLINE_SURFACE(((1.,0.815158509402318,1.),(1.,0.816179044148164,
1.),(1.,0.817226308119926,1.),(1.,0.818301939488811,1.)))
REPRESENTATION_ITEM('')
SURFACE()
);
#3264=(
BOUNDED_SURFACE()
B_SPLINE_SURFACE(3,2,((#408615,#408616,#408617),(#408618,#408619,#408620),
(#408621,#408622,#408623),(#408624,#408625,#408626)),.UNSPECIFIED.,.F.,
 .F.,.F.)
B_SPLINE_SURFACE_WITH_KNOTS((4,4),(3,3),(1.55009486301137E-5,4.92065510474429E-5),
(-8.13759514211941E-5,1.),.UNSPECIFIED.)
GEOMETRIC_REPRESENTATION_ITEM()
RATIONAL_B_SPLINE_SURFACE(((1.00002372912334,0.8542006395997,1.),(1.00001423585992,
0.912530301180531,1.),(1.0000071055047,0.956341495377438,1.),(1.00001238975908,
0.923873338137026,1.)))
REPRESENTATION_ITEM('')
SURFACE()
);
#3265=(
BOUNDED_SURFACE()
B_SPLINE_SURFACE(3,2,((#408630,#408631,#408632),(#408633,#408634,#408635),
(#408636,#408637,#408638),(#408639,#408640,#408641)),.UNSPECIFIED.,.F.,
 .F.,.F.)
B_SPLINE_SURFACE_WITH_KNOTS((4,4),(3,3),(-3.39934179457818E-6,3.73927597403565E-5),
(-0.00186004067459443,1.00069373317435),.UNSPECIFIED.)
GEOMETRIC_REPRESENTATION_ITEM()
RATIONAL_B_SPLINE_SURFACE(((1.0007210013607,0.80605196387529,1.00026859642689),
(1.00060048440167,0.838470803558563,1.00022369994494),(1.00053106448806,
0.85714463227233,1.00019783877218),(1.00054515072864,0.853355459539047,
1.00020308635435)))
REPRESENTATION_ITEM('')
SURFACE()
);
#3266=(
BOUNDED_SURFACE()
B_SPLINE_SURFACE(3,2,((#408643,#408644,#408645),(#408646,#408647,#408648),
(#408649,#408650,#408651),(#408652,#408653,#408654)),.UNSPECIFIED.,.F.,
 .F.,.F.)
B_SPLINE_SURFACE_WITH_KNOTS((4,4),(3,3),(5.42101086242752E-20,9.54361881492175E-5),
(0.,1.),.UNSPECIFIED.)
GEOMETRIC_REPRESENTATION_ITEM()
RATIONAL_B_SPLINE_SURFACE(((1.,0.816715621142041,1.),(1.,0.815907587407951,
1.),(1.,0.815115959345192,1.),(1.,0.81433988734919,1.)))
REPRESENTATION_ITEM('')
SURFACE()
);
#3267=(
BOUNDED_SURFACE()
B_SPLINE_SURFACE(3,2,((#408656,#408657,#408658),(#408659,#408660,#408661),
(#408662,#408663,#408664),(#408665,#408666,#408667)),.UNSPECIFIED.,.F.,
 .F.,.F.)
B_SPLINE_SURFACE_WITH_KNOTS((4,4),(3,3),(6.94567016748526E-20,4.68197758448217E-5),
(0.,1.),.UNSPECIFIED.)
GEOMETRIC_REPRESENTATION_ITEM()
RATIONAL_B_SPLINE_SURFACE(((1.,0.816715621142048,1.),(1.,0.953638980025213,
1.),(1.,0.954506925408052,1.),(1.,0.816715621142053,1.)))
REPRESENTATION_ITEM('')
SURFACE()
);
#3268=(
BOUNDED_SURFACE()
B_SPLINE_SURFACE(3,2,((#408669,#408670,#408671),(#408672,#408673,#408674),
(#408675,#408676,#408677),(#408678,#408679,#408680)),.UNSPECIFIED.,.F.,
 .F.,.F.)
B_SPLINE_SURFACE_WITH_KNOTS((4,4),(3,3),(-5.42101086242752E-20,9.54361881492176E-5),
(0.,1.),.UNSPECIFIED.)
GEOMETRIC_REPRESENTATION_ITEM()
RATIONAL_B_SPLINE_SURFACE(((1.,0.81433988734919,1.),(1.,0.815115959345202,
1.),(1.,0.815907587407945,1.),(1.,0.816715621142048,1.)))
REPRESENTATION_ITEM('')
SURFACE()
);
#3269=(
BOUNDED_SURFACE()
B_SPLINE_SURFACE(3,2,((#408682,#408683,#408684),(#408685,#408686,#408687),
(#408688,#408689,#408690),(#408691,#408692,#408693)),.UNSPECIFIED.,.F.,
 .F.,.F.)
B_SPLINE_SURFACE_WITH_KNOTS((4,4),(3,3),(-3.39528393502486E-6,3.73481232852737E-5),
(-0.00165018033291492,1.),.UNSPECIFIED.)
GEOMETRIC_REPRESENTATION_ITEM()
RATIONAL_B_SPLINE_SURFACE(((1.00048354385555,0.853487571660454,1.),(1.0004711051091,
0.857256476851512,1.),(1.00053193201096,0.838826096655924,1.),(1.00063970687711,
0.806170615310167,1.)))
REPRESENTATION_ITEM('')
SURFACE()
);
#3270=(
BOUNDED_SURFACE()
B_SPLINE_SURFACE(3,2,((#408697,#408698,#408699),(#408700,#408701,#408702),
(#408703,#408704,#408705),(#408706,#408707,#408708)),.UNSPECIFIED.,.F.,
 .F.,.F.)
B_SPLINE_SURFACE_WITH_KNOTS((4,4),(3,3),(2.02993869230508E-5,5.39756952686901E-5),
(-0.000116281069843854,1.),.UNSPECIFIED.)
GEOMETRIC_REPRESENTATION_ITEM()
RATIONAL_B_SPLINE_SURFACE(((1.00001770479729,0.923870681143018,1.),(1.00001014104058,
0.956394275543418,1.),(1.00002037300277,0.912397594905681,1.),(1.00003390859467,
0.854195550869865,1.)))
REPRESENTATION_ITEM('')
SURFACE()
);
#3271=(
BOUNDED_SURFACE()
B_SPLINE_SURFACE(3,2,((#408801,#408802,#408803),(#408804,#408805,#408806),
(#408807,#408808,#408809),(#408810,#408811,#408812)),.UNSPECIFIED.,.F.,
 .F.,.F.)
B_SPLINE_SURFACE_WITH_KNOTS((4,4),(3,3),(0.00135801595889393,0.00148409170619832),
(0.,1.),.UNSPECIFIED.)
GEOMETRIC_REPRESENTATION_ITEM()
RATIONAL_B_SPLINE_SURFACE(((1.,0.818301933966443,1.),(1.,0.817226613172335,
1.),(1.,0.816179643373956,1.),(1.,0.815159387863654,1.)))
REPRESENTATION_ITEM('')
SURFACE()
);
#3272=(
BOUNDED_SURFACE()
B_SPLINE_SURFACE(3,2,((#408851,#408852,#408853),(#408854,#408855,#408856),
(#408857,#408858,#408859),(#408860,#408861,#408862)),.UNSPECIFIED.,.F.,
 .F.,.F.)
B_SPLINE_SURFACE_WITH_KNOTS((4,4),(3,3),(-1.54744435122086E-6,1.54744435122079E-5),
(-0.015169898363146,1.),.UNSPECIFIED.)
GEOMETRIC_REPRESENTATION_ITEM()
RATIONAL_B_SPLINE_SURFACE(((1.02018382473095,0.334740937355848,1.),(1.00401234488852,
0.867753072813226,1.),(1.00033622856783,0.988917903080852,1.),(1.,1.,1.)))
REPRESENTATION_ITEM('')
SURFACE()
);
#3273=(
BOUNDED_SURFACE()
B_SPLINE_SURFACE(3,2,((#408864,#408865,#408866),(#408867,#408868,#408869),
(#408870,#408871,#408872),(#408873,#408874,#408875)),.UNSPECIFIED.,.F.,
 .F.,.F.)
B_SPLINE_SURFACE_WITH_KNOTS((4,4),(3,3),(0.00137194782501028,0.00149814269699235),
(0.,1.),.UNSPECIFIED.)
GEOMETRIC_REPRESENTATION_ITEM()
RATIONAL_B_SPLINE_SURFACE(((1.,0.815158509402317,1.),(1.,0.816179044148165,
1.),(1.,0.817226308119923,1.),(1.,0.81830193948881,1.)))
REPRESENTATION_ITEM('')
SURFACE()
);
#3274=(
BOUNDED_SURFACE()
B_SPLINE_SURFACE(3,2,((#408919,#408920,#408921),(#408922,#408923,#408924),
(#408925,#408926,#408927),(#408928,#408929,#408930)),.UNSPECIFIED.,.F.,
 .F.,.F.)
B_SPLINE_SURFACE_WITH_KNOTS((4,4),(3,3),(1.55009486301137E-5,4.92065510474431E-5),
(-8.13759512802933E-5,1.),.UNSPECIFIED.)
GEOMETRIC_REPRESENTATION_ITEM()
RATIONAL_B_SPLINE_SURFACE(((1.0000237291233,0.85420063959972,1.),(1.0000142358599,
0.912530301180552,1.),(1.00000710550469,0.956341495377443,1.),(1.00001238975905,
0.923873338137036,1.)))
REPRESENTATION_ITEM('')
SURFACE()
);
#3275=(
BOUNDED_SURFACE()
B_SPLINE_SURFACE(3,2,((#408934,#408935,#408936),(#408937,#408938,#408939),
(#408940,#408941,#408942),(#408943,#408944,#408945)),.UNSPECIFIED.,.F.,
 .F.,.F.)
B_SPLINE_SURFACE_WITH_KNOTS((4,4),(3,3),(-3.39934179457827E-6,3.73927597403564E-5),
(-0.00186004067454373,1.0006937331745),.UNSPECIFIED.)
GEOMETRIC_REPRESENTATION_ITEM()
RATIONAL_B_SPLINE_SURFACE(((1.00072100136068,0.806051963875258,1.00026859642695),
(1.00060048440166,0.838470803558567,1.00022369994499),(1.00053106448805,
0.85714463227231,1.00019783877222),(1.00054515072863,0.853355459539032,
1.0002030863544)))
REPRESENTATION_ITEM('')
SURFACE()
);
#3276=(
BOUNDED_SURFACE()
B_SPLINE_SURFACE(3,2,((#408947,#408948,#408949),(#408950,#408951,#408952),
(#408953,#408954,#408955),(#408956,#408957,#408958)),.UNSPECIFIED.,.F.,
 .F.,.F.)
B_SPLINE_SURFACE_WITH_KNOTS((4,4),(3,3),(1.62630325872826E-19,9.54361881492177E-5),
(0.,1.),.UNSPECIFIED.)
GEOMETRIC_REPRESENTATION_ITEM()
RATIONAL_B_SPLINE_SURFACE(((1.,0.81671562114205,1.),(1.,0.815907587407935,
1.),(1.,0.815115959345204,1.),(1.,0.814339887349198,1.)))
REPRESENTATION_ITEM('')
SURFACE()
);
#3277=(
BOUNDED_SURFACE()
B_SPLINE_SURFACE(3,2,((#408960,#408961,#408962),(#408963,#408964,#408965),
(#408966,#408967,#408968),(#408969,#408970,#408971)),.UNSPECIFIED.,.F.,
 .F.,.F.)
B_SPLINE_SURFACE_WITH_KNOTS((4,4),(3,3),(-2.87991202066462E-20,4.68197758448205E-5),
(0.,1.),.UNSPECIFIED.)
GEOMETRIC_REPRESENTATION_ITEM()
RATIONAL_B_SPLINE_SURFACE(((1.,0.816715621142046,1.),(1.,0.953638980025209,
1.),(1.,0.954506925408056,1.),(1.,0.816715621142056,1.)))
REPRESENTATION_ITEM('')
SURFACE()
);
#3278=(
BOUNDED_SURFACE()
B_SPLINE_SURFACE(3,2,((#408973,#408974,#408975),(#408976,#408977,#408978),
(#408979,#408980,#408981),(#408982,#408983,#408984)),.UNSPECIFIED.,.F.,
 .F.,.F.)
B_SPLINE_SURFACE_WITH_KNOTS((4,4),(3,3),(1.0842021724855E-19,9.54361881492178E-5),
(0.,1.),.UNSPECIFIED.)
GEOMETRIC_REPRESENTATION_ITEM()
RATIONAL_B_SPLINE_SURFACE(((1.,0.814339887349193,1.),(1.,0.815115959345203,
1.),(1.,0.815907587407949,1.),(1.,0.81671562114205,1.)))
REPRESENTATION_ITEM('')
SURFACE()
);
#3279=(
BOUNDED_SURFACE()
B_SPLINE_SURFACE(3,2,((#408986,#408987,#408988),(#408989,#408990,#408991),
(#408992,#408993,#408994),(#408995,#408996,#408997)),.UNSPECIFIED.,.F.,
 .F.,.F.)
B_SPLINE_SURFACE_WITH_KNOTS((4,4),(3,3),(-3.39528393502482E-6,3.73481232852731E-5),
(-0.00165018033344248,1.),.UNSPECIFIED.)
GEOMETRIC_REPRESENTATION_ITEM()
RATIONAL_B_SPLINE_SURFACE(((1.0004835438557,0.85348757166038,1.),(1.00047110510925,
0.857256476851433,1.),(1.00053193201113,0.838826096655854,1.),(1.00063970687732,
0.806170615310058,1.)))
REPRESENTATION_ITEM('')
SURFACE()
);
#3280=(
BOUNDED_SURFACE()
B_SPLINE_SURFACE(3,2,((#409001,#409002,#409003),(#409004,#409005,#409006),
(#409007,#409008,#409009),(#409010,#409011,#409012)),.UNSPECIFIED.,.F.,
 .F.,.F.)
B_SPLINE_SURFACE_WITH_KNOTS((4,4),(3,3),(2.02993869230511E-5,5.39756952686911E-5),
(-0.000116281070020795,1.),.UNSPECIFIED.)
GEOMETRIC_REPRESENTATION_ITEM()
RATIONAL_B_SPLINE_SURFACE(((1.00001770479731,0.923870681143002,1.),(1.0000101410406,
0.956394275543419,1.),(1.0000203730028,0.912397594905663,1.),(1.00003390859472,
0.854195550869841,1.)))
REPRESENTATION_ITEM('')
SURFACE()
);
#3281=(
BOUNDED_SURFACE()
B_SPLINE_SURFACE(3,2,((#409105,#409106,#409107),(#409108,#409109,#409110),
(#409111,#409112,#409113),(#409114,#409115,#409116)),.UNSPECIFIED.,.F.,
 .F.,.F.)
B_SPLINE_SURFACE_WITH_KNOTS((4,4),(3,3),(0.00135801595889393,0.00148409170619832),
(0.,1.),.UNSPECIFIED.)
GEOMETRIC_REPRESENTATION_ITEM()
RATIONAL_B_SPLINE_SURFACE(((1.,0.818301933966442,1.),(1.,0.817226613172329,
1.),(1.,0.816179643373963,1.),(1.,0.81515938786365,1.)))
REPRESENTATION_ITEM('')
SURFACE()
);
#3282=(
BOUNDED_SURFACE()
B_SPLINE_SURFACE(3,2,((#409155,#409156,#409157),(#409158,#409159,#409160),
(#409161,#409162,#409163),(#409164,#409165,#409166)),.UNSPECIFIED.,.F.,
 .F.,.F.)
B_SPLINE_SURFACE_WITH_KNOTS((4,4),(3,3),(-1.54744435122071E-6,1.5474443512207E-5),
(-0.015169898364808,1.),.UNSPECIFIED.)
GEOMETRIC_REPRESENTATION_ITEM()
RATIONAL_B_SPLINE_SURFACE(((1.02018382473319,0.334740937354758,1.),(1.00401234488897,
0.867753072813005,1.),(1.00033622856787,0.988917903080771,1.),(1.,1.,1.)))
REPRESENTATION_ITEM('')
SURFACE()
);
#3283=(
BOUNDED_SURFACE()
B_SPLINE_SURFACE(3,2,((#409168,#409169,#409170),(#409171,#409172,#409173),
(#409174,#409175,#409176),(#409177,#409178,#409179)),.UNSPECIFIED.,.F.,
 .F.,.F.)
B_SPLINE_SURFACE_WITH_KNOTS((4,4),(3,3),(0.00137194782501028,0.00149814269699235),
(0.,1.),.UNSPECIFIED.)
GEOMETRIC_REPRESENTATION_ITEM()
RATIONAL_B_SPLINE_SURFACE(((1.,0.815158509402313,1.),(1.,0.816179044148174,
1.),(1.,0.817226308119912,1.),(1.,0.818301939488812,1.)))
REPRESENTATION_ITEM('')
SURFACE()
);
#3284=(
BOUNDED_SURFACE()
B_SPLINE_SURFACE(3,2,((#409223,#409224,#409225),(#409226,#409227,#409228),
(#409229,#409230,#409231),(#409232,#409233,#409234)),.UNSPECIFIED.,.F.,
 .F.,.F.)
B_SPLINE_SURFACE_WITH_KNOTS((4,4),(3,3),(1.55009486301138E-5,4.92065510474437E-5),
(-8.13759515121529E-5,1.),.UNSPECIFIED.)
GEOMETRIC_REPRESENTATION_ITEM()
RATIONAL_B_SPLINE_SURFACE(((1.00002372912336,0.854200639599686,1.),(1.00001423585994,
0.912530301180531,1.),(1.00000710550471,0.956341495377431,1.),(1.00001238975909,
0.923873338137019,1.)))
REPRESENTATION_ITEM('')
SURFACE()
);
#3285=(
BOUNDED_SURFACE()
B_SPLINE_SURFACE(3,2,((#409238,#409239,#409240),(#409241,#409242,#409243),
(#409244,#409245,#409246),(#409247,#409248,#409249)),.UNSPECIFIED.,.F.,
 .F.,.F.)
B_SPLINE_SURFACE_WITH_KNOTS((4,4),(3,3),(-3.39934179457835E-6,3.73927597403565E-5),
(-0.0018600406742466,1.0006937331745),.UNSPECIFIED.)
GEOMETRIC_REPRESENTATION_ITEM()
RATIONAL_B_SPLINE_SURFACE(((1.00072100136057,0.806051963875303,1.00026859642695),
(1.00060048440156,0.838470803558628,1.00022369994499),(1.00053106448796,
0.857144632272343,1.00019783877222),(1.00054515072854,0.853355459539073,
1.0002030863544)))
REPRESENTATION_ITEM('')
SURFACE()
);
#3286=(
BOUNDED_SURFACE()
B_SPLINE_SURFACE(3,2,((#409251,#409252,#409253),(#409254,#409255,#409256),
(#409257,#409258,#409259),(#409260,#409261,#409262)),.UNSPECIFIED.,.F.,
 .F.,.F.)
B_SPLINE_SURFACE_WITH_KNOTS((4,4),(3,3),(-5.42101086242752E-20,9.54361881492175E-5),
(0.,1.),.UNSPECIFIED.)
GEOMETRIC_REPRESENTATION_ITEM()
RATIONAL_B_SPLINE_SURFACE(((1.,0.816715621142046,1.),(1.,0.815907587407942,
1.),(1.,0.815115959345197,1.),(1.,0.814339887349194,1.)))
REPRESENTATION_ITEM('')
SURFACE()
);
#3287=(
BOUNDED_SURFACE()
B_SPLINE_SURFACE(3,2,((#409264,#409265,#409266),(#409267,#409268,#409269),
(#409270,#409271,#409272),(#409273,#409274,#409275)),.UNSPECIFIED.,.F.,
 .F.,.F.)
B_SPLINE_SURFACE_WITH_KNOTS((4,4),(3,3),(-2.37169225231204E-20,4.68197758448207E-5),
(0.,1.),.UNSPECIFIED.)
GEOMETRIC_REPRESENTATION_ITEM()
RATIONAL_B_SPLINE_SURFACE(((1.,0.816715621142046,1.),(1.,0.953638980025198,
1.),(1.,0.954506925408069,1.),(1.,0.816715621142046,1.)))
REPRESENTATION_ITEM('')
SURFACE()
);
#3288=(
BOUNDED_SURFACE()
B_SPLINE_SURFACE(3,2,((#409277,#409278,#409279),(#409280,#409281,#409282),
(#409283,#409284,#409285),(#409286,#409287,#409288)),.UNSPECIFIED.,.F.,
 .F.,.F.)
B_SPLINE_SURFACE_WITH_KNOTS((4,4),(3,3),(5.42101086242752E-20,9.54361881492178E-5),
(0.,1.),.UNSPECIFIED.)
GEOMETRIC_REPRESENTATION_ITEM()
RATIONAL_B_SPLINE_SURFACE(((1.,0.814339887349192,1.),(1.,0.815115959345201,
1.),(1.,0.815907587407946,1.),(1.,0.816715621142046,1.)))
REPRESENTATION_ITEM('')
SURFACE()
);
#3289=(
BOUNDED_SURFACE()
B_SPLINE_SURFACE(3,2,((#409290,#409291,#409292),(#409293,#409294,#409295),
(#409296,#409297,#409298),(#409299,#409300,#409301)),.UNSPECIFIED.,.F.,
 .F.,.F.)
B_SPLINE_SURFACE_WITH_KNOTS((4,4),(3,3),(-3.39528393502488E-6,3.73481232852737E-5),
(-0.00165018033279429,1.),.UNSPECIFIED.)
GEOMETRIC_REPRESENTATION_ITEM()
RATIONAL_B_SPLINE_SURFACE(((1.00048354385551,0.853487571660467,1.),(1.00047110510907,
0.857256476851531,1.),(1.00053193201092,0.838826096655951,1.),(1.00063970687707,
0.806170615310183,1.)))
REPRESENTATION_ITEM('')
SURFACE()
);
#3290=(
BOUNDED_SURFACE()
B_SPLINE_SURFACE(3,2,((#409305,#409306,#409307),(#409308,#409309,#409310),
(#409311,#409312,#409313),(#409314,#409315,#409316)),.UNSPECIFIED.,.F.,
 .F.,.F.)
B_SPLINE_SURFACE_WITH_KNOTS((4,4),(3,3),(2.0299386923051E-5,5.39756952686907E-5),
(-0.000116281069868689,1.),.UNSPECIFIED.)
GEOMETRIC_REPRESENTATION_ITEM()
RATIONAL_B_SPLINE_SURFACE(((1.00001770479729,0.923870681143011,1.),(1.00001014104058,
0.95639427554342,1.),(1.00002037300278,0.912397594905679,1.),(1.00003390859467,
0.854195550869862,1.)))
REPRESENTATION_ITEM('')
SURFACE()
);
#3291=(
BOUNDED_SURFACE()
B_SPLINE_SURFACE(3,2,((#409409,#409410,#409411),(#409412,#409413,#409414),
(#409415,#409416,#409417),(#409418,#409419,#409420)),.UNSPECIFIED.,.F.,
 .F.,.F.)
B_SPLINE_SURFACE_WITH_KNOTS((4,4),(3,3),(0.00135801595889393,0.00148409170619832),
(0.,1.),.UNSPECIFIED.)
GEOMETRIC_REPRESENTATION_ITEM()
RATIONAL_B_SPLINE_SURFACE(((1.,0.818301933966443,1.),(1.,0.817226613172361,
1.),(1.,0.816179643373939,1.),(1.,0.815159387863656,1.)))
REPRESENTATION_ITEM('')
SURFACE()
);
#3292=(
BOUNDED_SURFACE()
B_SPLINE_SURFACE(3,2,((#409459,#409460,#409461),(#409462,#409463,#409464),
(#409465,#409466,#409467),(#409468,#409469,#409470)),.UNSPECIFIED.,.F.,
 .F.,.F.)
B_SPLINE_SURFACE_WITH_KNOTS((4,4),(3,3),(-1.5474443512207E-6,1.54744435122074E-5),
(-0.015169898372212,1.),.UNSPECIFIED.)
GEOMETRIC_REPRESENTATION_ITEM()
RATIONAL_B_SPLINE_SURFACE(((1.02018382474319,0.33474093734983,1.),(1.00401234489096,
0.867753072812112,1.),(1.00033622856803,0.988917903080659,1.),(1.,1.,1.)))
REPRESENTATION_ITEM('')
SURFACE()
);
#3293=(
BOUNDED_SURFACE()
B_SPLINE_SURFACE(3,2,((#409472,#409473,#409474),(#409475,#409476,#409477),
(#409478,#409479,#409480),(#409481,#409482,#409483)),.UNSPECIFIED.,.F.,
 .F.,.F.)
B_SPLINE_SURFACE_WITH_KNOTS((4,4),(3,3),(0.00137194782501028,0.00149814269699235),
(0.,1.),.UNSPECIFIED.)
GEOMETRIC_REPRESENTATION_ITEM()
RATIONAL_B_SPLINE_SURFACE(((1.,0.815158509402317,1.),(1.,0.816179044148169,
1.),(1.,0.817226308119918,1.),(1.,0.81830193948881,1.)))
REPRESENTATION_ITEM('')
SURFACE()
);
#3294=(
BOUNDED_SURFACE()
B_SPLINE_SURFACE(3,2,((#409527,#409528,#409529),(#409530,#409531,#409532),
(#409533,#409534,#409535),(#409536,#409537,#409538)),.UNSPECIFIED.,.F.,
 .F.,.F.)
B_SPLINE_SURFACE_WITH_KNOTS((4,4),(3,3),(1.55009486301137E-5,4.92065510474436E-5),
(-8.13759515650707E-5,1.),.UNSPECIFIED.)
GEOMETRIC_REPRESENTATION_ITEM()
RATIONAL_B_SPLINE_SURFACE(((1.00002372912338,0.85420063959967,1.),(1.00001423585995,
0.912530301180529,1.),(1.00000710550471,0.956341495377431,1.),(1.0000123897591,
0.923873338137015,1.)))
REPRESENTATION_ITEM('')
SURFACE()
);
#3295=(
BOUNDED_SURFACE()
B_SPLINE_SURFACE(3,2,((#409542,#409543,#409544),(#409545,#409546,#409547),
(#409548,#409549,#409550),(#409551,#409552,#409553)),.UNSPECIFIED.,.F.,
 .F.,.F.)
B_SPLINE_SURFACE_WITH_KNOTS((4,4),(3,3),(-3.3993417945787E-6,3.73927597403563E-5),
(-0.00186004067399629,1.00069373317423),.UNSPECIFIED.)
GEOMETRIC_REPRESENTATION_ITEM()
RATIONAL_B_SPLINE_SURFACE(((1.00072100136047,0.806051963875404,1.00026859642685),
(1.00060048440148,0.838470803558721,1.0002236999449),(1.00053106448789,
0.857144632272418,1.00019783877215),(1.00054515072847,0.853355459539159,
1.00020308635432)))
REPRESENTATION_ITEM('')
SURFACE()
);
#3296=(
BOUNDED_SURFACE()
B_SPLINE_SURFACE(3,2,((#409555,#409556,#409557),(#409558,#409559,#409560),
(#409561,#409562,#409563),(#409564,#409565,#409566)),.UNSPECIFIED.,.F.,
 .F.,.F.)
B_SPLINE_SURFACE_WITH_KNOTS((4,4),(3,3),(1.0842021724855E-19,9.54361881492172E-5),
(0.,1.),.UNSPECIFIED.)
GEOMETRIC_REPRESENTATION_ITEM()
RATIONAL_B_SPLINE_SURFACE(((1.,0.816715621142052,1.),(1.,0.81590758740794,
1.),(1.,0.815115959345197,1.),(1.,0.814339887349202,1.)))
REPRESENTATION_ITEM('')
SURFACE()
);
#3297=(
BOUNDED_SURFACE()
B_SPLINE_SURFACE(3,2,((#409568,#409569,#409570),(#409571,#409572,#409573),
(#409574,#409575,#409576),(#409577,#409578,#409579)),.UNSPECIFIED.,.F.,
 .F.,.F.)
B_SPLINE_SURFACE_WITH_KNOTS((4,4),(3,3),(5.9292306307801E-20,4.68197758448208E-5),
(0.,1.),.UNSPECIFIED.)
GEOMETRIC_REPRESENTATION_ITEM()
RATIONAL_B_SPLINE_SURFACE(((1.,0.816715621142048,1.),(1.,0.953638980025209,
1.),(1.,0.954506925408052,1.),(1.,0.816715621142059,1.)))
REPRESENTATION_ITEM('')
SURFACE()
);
#3298=(
BOUNDED_SURFACE()
B_SPLINE_SURFACE(3,2,((#409581,#409582,#409583),(#409584,#409585,#409586),
(#409587,#409588,#409589),(#409590,#409591,#409592)),.UNSPECIFIED.,.F.,
 .F.,.F.)
B_SPLINE_SURFACE_WITH_KNOTS((4,4),(3,3),(-5.42101086242752E-20,9.54361881492178E-5),
(0.,1.),.UNSPECIFIED.)
GEOMETRIC_REPRESENTATION_ITEM()
RATIONAL_B_SPLINE_SURFACE(((1.,0.814339887349196,1.),(1.,0.815115959345204,
1.),(1.,0.815907587407944,1.),(1.,0.816715621142048,1.)))
REPRESENTATION_ITEM('')
SURFACE()
);
#3299=(
BOUNDED_SURFACE()
B_SPLINE_SURFACE(3,2,((#409594,#409595,#409596),(#409597,#409598,#409599),
(#409600,#409601,#409602),(#409603,#409604,#409605)),.UNSPECIFIED.,.F.,
 .F.,.F.)
B_SPLINE_SURFACE_WITH_KNOTS((4,4),(3,3),(-3.39528393502484E-6,3.7348123285273E-5),
(-0.00165018033307088,1.),.UNSPECIFIED.)
GEOMETRIC_REPRESENTATION_ITEM()
RATIONAL_B_SPLINE_SURFACE(((1.00048354385559,0.85348757166043,1.),(1.00047110510915,
0.857256476851486,1.),(1.000531932011,0.838826096655913,1.),(1.00063970687717,
0.806170615310131,1.)))
REPRESENTATION_ITEM('')
SURFACE()
);
#3300=(
BOUNDED_SURFACE()
B_SPLINE_SURFACE(3,2,((#409609,#409610,#409611),(#409612,#409613,#409614),
(#409615,#409616,#409617),(#409618,#409619,#409620)),.UNSPECIFIED.,.F.,
 .F.,.F.)
B_SPLINE_SURFACE_WITH_KNOTS((4,4),(3,3),(2.02993869230509E-5,5.39756952686903E-5),
(-0.000116281069956809,1.),.UNSPECIFIED.)
GEOMETRIC_REPRESENTATION_ITEM()
RATIONAL_B_SPLINE_SURFACE(((1.0000177047973,0.923870681143007,1.),(1.00001014104059,
0.956394275543409,1.),(1.00002037300279,0.912397594905683,1.),(1.0000339085947,
0.854195550869847,1.)))
REPRESENTATION_ITEM('')
SURFACE()
);
#4261=(
BOUNDED_CURVE()
B_SPLINE_CURVE(2,(#371613,#371614,#371615),.UNSPECIFIED.,.F.,.F.)
B_SPLINE_CURVE_WITH_KNOTS((3,3),(0.0121665790178462,0.0161290322580645),
 .UNSPECIFIED.)
CURVE()
GEOMETRIC_REPRESENTATION_ITEM()
RATIONAL_B_SPLINE_CURVE((0.948065210722606,0.901258538444081,1.))
REPRESENTATION_ITEM('')
);
#4262=(
BOUNDED_CURVE()
B_SPLINE_CURVE(2,(#371621,#371622,#371623,#371624,#371625,#371626,#371627,
#371628,#371629,#371630,#371631,#371632,#371633),.UNSPECIFIED.,.F.,.F.)
B_SPLINE_CURVE_WITH_KNOTS((3,2,2,2,2,2,3),(0.0161290322580645,0.021505376344086,
0.0268817204301075,0.032258064516129,0.0376344086021505,0.043010752688172,
0.0483870967741935),.UNSPECIFIED.)
CURVE()
GEOMETRIC_REPRESENTATION_ITEM()
RATIONAL_B_SPLINE_CURVE((1.,0.866025403784439,1.,0.866025403784439,1.,0.866025403784439,
1.,0.866025403784439,1.,0.866025403784439,1.,0.866025403784439,1.))
REPRESENTATION_ITEM('')
);
#4263=(
BOUNDED_CURVE()
B_SPLINE_CURVE(2,(#371634,#371635,#371636,#371637,#371638,#371639,#371640,
#371641,#371642,#371643,#371644,#371645,#371646),.UNSPECIFIED.,.F.,.F.)
B_SPLINE_CURVE_WITH_KNOTS((3,2,2,2,2,2,3),(0.0161290322580645,0.021505376344086,
0.0268817204301075,0.032258064516129,0.0376344086021506,0.0430107526881721,
0.0483870967741936),.UNSPECIFIED.)
CURVE()
GEOMETRIC_REPRESENTATION_ITEM()
RATIONAL_B_SPLINE_CURVE((1.,0.866025403784439,1.,0.866025403784439,1.,0.866025403784439,
1.,0.866025403784439,1.,0.866025403784439,1.,0.866025403784439,1.))
REPRESENTATION_ITEM('')
);
#4264=(
BOUNDED_CURVE()
B_SPLINE_CURVE(2,(#371651,#371652,#371653,#371654,#371655,#371656,#371657,
#371658,#371659,#371660,#371661,#371662,#371663),.UNSPECIFIED.,.F.,.F.)
B_SPLINE_CURVE_WITH_KNOTS((3,2,2,2,2,2,3),(0.0483870967741935,0.0537634408602151,
0.0591397849462366,0.0645161290322581,0.0698924731182796,0.0752688172043011,
0.0806451612903226),.UNSPECIFIED.)
CURVE()
GEOMETRIC_REPRESENTATION_ITEM()
RATIONAL_B_SPLINE_CURVE((1.,0.866025403784439,1.,0.866025403784439,1.,0.866025403784439,
1.,0.866025403784439,1.,0.866025403784439,1.,0.866025403784439,1.))
REPRESENTATION_ITEM('')
);
#4265=(
BOUNDED_CURVE()
B_SPLINE_CURVE(2,(#371664,#371665,#371666,#371667,#371668,#371669,#371670,
#371671,#371672,#371673,#371674,#371675,#371676),.UNSPECIFIED.,.F.,.F.)
B_SPLINE_CURVE_WITH_KNOTS((3,2,2,2,2,2,3),(0.0483870967741936,0.0537634408602151,
0.0591397849462366,0.0645161290322581,0.0698924731182796,0.0752688172043011,
0.0806451612903226),.UNSPECIFIED.)
CURVE()
GEOMETRIC_REPRESENTATION_ITEM()
RATIONAL_B_SPLINE_CURVE((1.,0.866025403784439,1.,0.866025403784439,1.,0.866025403784439,
1.,0.866025403784439,1.,0.866025403784439,1.,0.866025403784439,1.))
REPRESENTATION_ITEM('')
);
#4266=(
BOUNDED_CURVE()
B_SPLINE_CURVE(2,(#371681,#371682,#371683,#371684,#371685,#371686,#371687,
#371688,#371689,#371690,#371691,#371692,#371693),.UNSPECIFIED.,.F.,.F.)
B_SPLINE_CURVE_WITH_KNOTS((3,2,2,2,2,2,3),(0.0806451612903226,0.0860215053763441,
0.0913978494623656,0.0967741935483871,0.102150537634409,0.10752688172043,
0.112903225806452),.UNSPECIFIED.)
CURVE()
GEOMETRIC_REPRESENTATION_ITEM()
RATIONAL_B_SPLINE_CURVE((1.,0.866025403784439,1.,0.866025403784439,1.,0.866025403784439,
1.,0.866025403784439,1.,0.866025403784439,1.,0.866025403784439,1.))
REPRESENTATION_ITEM('')
);
#4267=(
BOUNDED_CURVE()
B_SPLINE_CURVE(2,(#371694,#371695,#371696,#371697,#371698,#371699,#371700,
#371701,#371702,#371703,#371704,#371705,#371706),.UNSPECIFIED.,.F.,.F.)
B_SPLINE_CURVE_WITH_KNOTS((3,2,2,2,2,2,3),(0.0806451612903226,0.0860215053763441,
0.0913978494623656,0.0967741935483871,0.102150537634409,0.10752688172043,
0.112903225806452),.UNSPECIFIED.)
CURVE()
GEOMETRIC_REPRESENTATION_ITEM()
RATIONAL_B_SPLINE_CURVE((1.,0.866025403784439,1.,0.866025403784439,1.,0.866025403784439,
1.,0.866025403784439,1.,0.866025403784439,1.,0.866025403784439,1.))
REPRESENTATION_ITEM('')
);
#4268=(
BOUNDED_CURVE()
B_SPLINE_CURVE(2,(#371711,#371712,#371713,#371714,#371715,#371716,#371717,
#371718,#371719,#371720,#371721,#371722,#371723),.UNSPECIFIED.,.F.,.F.)
B_SPLINE_CURVE_WITH_KNOTS((3,2,2,2,2,2,3),(0.112903225806452,0.118279569892473,
0.123655913978495,0.129032258064516,0.134408602150538,0.139784946236559,
0.145161290322581),.UNSPECIFIED.)
CURVE()
GEOMETRIC_REPRESENTATION_ITEM()
RATIONAL_B_SPLINE_CURVE((1.,0.866025403784439,1.,0.866025403784439,1.,0.866025403784439,
1.,0.866025403784439,1.,0.866025403784439,1.,0.866025403784439,1.))
REPRESENTATION_ITEM('')
);
#4269=(
BOUNDED_CURVE()
B_SPLINE_CURVE(2,(#371724,#371725,#371726,#371727,#371728,#371729,#371730,
#371731,#371732,#371733,#371734,#371735,#371736),.UNSPECIFIED.,.F.,.F.)
B_SPLINE_CURVE_WITH_KNOTS((3,2,2,2,2,2,3),(0.112903225806452,0.118279569892473,
0.123655913978495,0.129032258064516,0.134408602150538,0.139784946236559,
0.145161290322581),.UNSPECIFIED.)
CURVE()
GEOMETRIC_REPRESENTATION_ITEM()
RATIONAL_B_SPLINE_CURVE((1.,0.866025403784439,1.,0.866025403784439,1.,0.866025403784439,
1.,0.866025403784439,1.,0.866025403784439,1.,0.866025403784439,1.))
REPRESENTATION_ITEM('')
);
#4270=(
BOUNDED_CURVE()
B_SPLINE_CURVE(2,(#371741,#371742,#371743,#371744,#371745,#371746,#371747,
#371748,#371749,#371750,#371751,#371752,#371753),.UNSPECIFIED.,.F.,.F.)
B_SPLINE_CURVE_WITH_KNOTS((3,2,2,2,2,2,3),(0.145161290322581,0.150537634408602,
0.155913978494624,0.161290322580645,0.166666666666667,0.172043010752688,
0.17741935483871),.UNSPECIFIED.)
CURVE()
GEOMETRIC_REPRESENTATION_ITEM()
RATIONAL_B_SPLINE_CURVE((1.,0.866025403784439,1.,0.866025403784439,1.,0.866025403784439,
1.,0.866025403784439,1.,0.866025403784439,1.,0.866025403784439,1.))
REPRESENTATION_ITEM('')
);
#4271=(
BOUNDED_CURVE()
B_SPLINE_CURVE(2,(#371754,#371755,#371756,#371757,#371758,#371759,#371760,
#371761,#371762,#371763,#371764,#371765,#371766),.UNSPECIFIED.,.F.,.F.)
B_SPLINE_CURVE_WITH_KNOTS((3,2,2,2,2,2,3),(0.145161290322581,0.150537634408602,
0.155913978494624,0.161290322580645,0.166666666666667,0.172043010752688,
0.17741935483871),.UNSPECIFIED.)
CURVE()
GEOMETRIC_REPRESENTATION_ITEM()
RATIONAL_B_SPLINE_CURVE((1.,0.866025403784439,1.,0.866025403784439,1.,0.866025403784439,
1.,0.866025403784439,1.,0.866025403784439,1.,0.866025403784439,1.))
REPRESENTATION_ITEM('')
);
#4272=(
BOUNDED_CURVE()
B_SPLINE_CURVE(2,(#371771,#371772,#371773,#371774,#371775,#371776,#371777,
#371778,#371779,#371780,#371781,#371782,#371783),.UNSPECIFIED.,.F.,.F.)
B_SPLINE_CURVE_WITH_KNOTS((3,2,2,2,2,2,3),(0.17741935483871,0.182795698924731,
0.188172043010753,0.193548387096774,0.198924731182796,0.204301075268817,
0.209677419354839),.UNSPECIFIED.)
CURVE()
GEOMETRIC_REPRESENTATION_ITEM()
RATIONAL_B_SPLINE_CURVE((1.,0.866025403784439,1.,0.866025403784439,1.,0.866025403784439,
1.,0.866025403784439,1.,0.866025403784439,1.,0.866025403784439,1.))
REPRESENTATION_ITEM('')
);
#4273=(
BOUNDED_CURVE()
B_SPLINE_CURVE(2,(#371784,#371785,#371786,#371787,#371788,#371789,#371790,
#371791,#371792,#371793,#371794,#371795,#371796),.UNSPECIFIED.,.F.,.F.)
B_SPLINE_CURVE_WITH_KNOTS((3,2,2,2,2,2,3),(0.17741935483871,0.182795698924731,
0.188172043010753,0.193548387096774,0.198924731182796,0.204301075268817,
0.209677419354839),.UNSPECIFIED.)
CURVE()
GEOMETRIC_REPRESENTATION_ITEM()
RATIONAL_B_SPLINE_CURVE((1.,0.866025403784439,1.,0.866025403784439,1.,0.866025403784439,
1.,0.866025403784439,1.,0.866025403784439,1.,0.866025403784439,1.))
REPRESENTATION_ITEM('')
);
#4274=(
BOUNDED_CURVE()
B_SPLINE_CURVE(2,(#371801,#371802,#371803,#371804,#371805,#371806,#371807,
#371808,#371809,#371810,#371811,#371812,#371813),.UNSPECIFIED.,.F.,.F.)
B_SPLINE_CURVE_WITH_KNOTS((3,2,2,2,2,2,3),(0.209677419354839,0.21505376344086,
0.220430107526882,0.225806451612903,0.231182795698925,0.236559139784946,
0.241935483870968),.UNSPECIFIED.)
CURVE()
GEOMETRIC_REPRESENTATION_ITEM()
RATIONAL_B_SPLINE_CURVE((1.,0.866025403784439,1.,0.866025403784439,1.,0.866025403784439,
1.,0.866025403784439,1.,0.866025403784439,1.,0.866025403784439,1.))
REPRESENTATION_ITEM('')
);
#4275=(
BOUNDED_CURVE()
B_SPLINE_CURVE(2,(#371814,#371815,#371816,#371817,#371818,#371819,#371820,
#371821,#371822,#371823,#371824,#371825,#371826),.UNSPECIFIED.,.F.,.F.)
B_SPLINE_CURVE_WITH_KNOTS((3,2,2,2,2,2,3),(0.209677419354839,0.21505376344086,
0.220430107526882,0.225806451612903,0.231182795698925,0.236559139784946,
0.241935483870968),.UNSPECIFIED.)
CURVE()
GEOMETRIC_REPRESENTATION_ITEM()
RATIONAL_B_SPLINE_CURVE((1.,0.866025403784439,1.,0.866025403784439,1.,0.866025403784439,
1.,0.866025403784439,1.,0.866025403784439,1.,0.866025403784439,1.))
REPRESENTATION_ITEM('')
);
#4276=(
BOUNDED_CURVE()
B_SPLINE_CURVE(2,(#371831,#371832,#371833,#371834,#371835,#371836,#371837,
#371838,#371839,#371840,#371841,#371842,#371843),.UNSPECIFIED.,.F.,.F.)
B_SPLINE_CURVE_WITH_KNOTS((3,2,2,2,2,2,3),(0.241935483870968,0.247311827956989,
0.252688172043011,0.258064516129032,0.263440860215054,0.268817204301075,
0.274193548387097),.UNSPECIFIED.)
CURVE()
GEOMETRIC_REPRESENTATION_ITEM()
RATIONAL_B_SPLINE_CURVE((1.,0.866025403784439,1.,0.866025403784439,1.,0.866025403784439,
1.,0.866025403784439,1.,0.866025403784439,1.,0.866025403784439,1.))
REPRESENTATION_ITEM('')
);
#4277=(
BOUNDED_CURVE()
B_SPLINE_CURVE(2,(#371844,#371845,#371846,#371847,#371848,#371849,#371850,
#371851,#371852,#371853,#371854,#371855,#371856),.UNSPECIFIED.,.F.,.F.)
B_SPLINE_CURVE_WITH_KNOTS((3,2,2,2,2,2,3),(0.241935483870968,0.247311827956989,
0.252688172043011,0.258064516129032,0.263440860215054,0.268817204301075,
0.274193548387097),.UNSPECIFIED.)
CURVE()
GEOMETRIC_REPRESENTATION_ITEM()
RATIONAL_B_SPLINE_CURVE((1.,0.866025403784439,1.,0.866025403784439,1.,0.866025403784439,
1.,0.866025403784439,1.,0.866025403784439,1.,0.866025403784439,1.))
REPRESENTATION_ITEM('')
);
#4278=(
BOUNDED_CURVE()
B_SPLINE_CURVE(2,(#371861,#371862,#371863,#371864,#371865,#371866,#371867,
#371868,#371869,#371870,#371871,#371872,#371873),.UNSPECIFIED.,.F.,.F.)
B_SPLINE_CURVE_WITH_KNOTS((3,2,2,2,2,2,3),(0.274193548387097,0.279569892473118,
0.28494623655914,0.290322580645161,0.295698924731183,0.301075268817204,
0.306451612903226),.UNSPECIFIED.)
CURVE()
GEOMETRIC_REPRESENTATION_ITEM()
RATIONAL_B_SPLINE_CURVE((1.,0.866025403784439,1.,0.866025403784439,1.,0.866025403784439,
1.,0.866025403784439,1.,0.866025403784439,1.,0.866025403784439,1.))
REPRESENTATION_ITEM('')
);
#4279=(
BOUNDED_CURVE()
B_SPLINE_CURVE(2,(#371874,#371875,#371876,#371877,#371878,#371879,#371880,
#371881,#371882,#371883,#371884,#371885,#371886),.UNSPECIFIED.,.F.,.F.)
B_SPLINE_CURVE_WITH_KNOTS((3,2,2,2,2,2,3),(0.274193548387097,0.279569892473118,
0.28494623655914,0.290322580645161,0.295698924731183,0.301075268817204,
0.306451612903226),.UNSPECIFIED.)
CURVE()
GEOMETRIC_REPRESENTATION_ITEM()
RATIONAL_B_SPLINE_CURVE((1.,0.866025403784439,1.,0.866025403784439,1.,0.866025403784439,
1.,0.866025403784439,1.,0.866025403784439,1.,0.866025403784439,1.))
REPRESENTATION_ITEM('')
);
#4280=(
BOUNDED_CURVE()
B_SPLINE_CURVE(2,(#371891,#371892,#371893,#371894,#371895,#371896,#371897,
#371898,#371899,#371900,#371901,#371902,#371903),.UNSPECIFIED.,.F.,.F.)
B_SPLINE_CURVE_WITH_KNOTS((3,2,2,2,2,2,3),(0.306451612903226,0.311827956989247,
0.317204301075269,0.32258064516129,0.327956989247312,0.333333333333333,
0.338709677419355),.UNSPECIFIED.)
CURVE()
GEOMETRIC_REPRESENTATION_ITEM()
RATIONAL_B_SPLINE_CURVE((1.,0.866025403784439,1.,0.866025403784439,1.,0.866025403784439,
1.,0.866025403784439,1.,0.866025403784439,1.,0.866025403784439,1.))
REPRESENTATION_ITEM('')
);
#4281=(
BOUNDED_CURVE()
B_SPLINE_CURVE(2,(#371904,#371905,#371906,#371907,#371908,#371909,#371910,
#371911,#371912,#371913,#371914,#371915,#371916),.UNSPECIFIED.,.F.,.F.)
B_SPLINE_CURVE_WITH_KNOTS((3,2,2,2,2,2,3),(0.306451612903226,0.311827956989247,
0.317204301075269,0.32258064516129,0.327956989247312,0.333333333333333,
0.338709677419355),.UNSPECIFIED.)
CURVE()
GEOMETRIC_REPRESENTATION_ITEM()
RATIONAL_B_SPLINE_CURVE((1.,0.866025403784439,1.,0.866025403784439,1.,0.866025403784439,
1.,0.866025403784439,1.,0.866025403784439,1.,0.866025403784439,1.))
REPRESENTATION_ITEM('')
);
#4282=(
BOUNDED_CURVE()
B_SPLINE_CURVE(2,(#371921,#371922,#371923,#371924,#371925,#371926,#371927,
#371928,#371929,#371930,#371931,#371932,#371933),.UNSPECIFIED.,.F.,.F.)
B_SPLINE_CURVE_WITH_KNOTS((3,2,2,2,2,2,3),(0.338709677419355,0.344086021505376,
0.349462365591398,0.354838709677419,0.360215053763441,0.365591397849462,
0.370967741935484),.UNSPECIFIED.)
CURVE()
GEOMETRIC_REPRESENTATION_ITEM()
RATIONAL_B_SPLINE_CURVE((1.,0.866025403784439,1.,0.866025403784439,1.,0.866025403784439,
1.,0.866025403784439,1.,0.866025403784439,1.,0.866025403784439,1.))
REPRESENTATION_ITEM('')
);
#4283=(
BOUNDED_CURVE()
B_SPLINE_CURVE(2,(#371934,#371935,#371936,#371937,#371938,#371939,#371940,
#371941,#371942,#371943,#371944,#371945,#371946),.UNSPECIFIED.,.F.,.F.)
B_SPLINE_CURVE_WITH_KNOTS((3,2,2,2,2,2,3),(0.338709677419355,0.344086021505376,
0.349462365591398,0.354838709677419,0.360215053763441,0.365591397849462,
0.370967741935484),.UNSPECIFIED.)
CURVE()
GEOMETRIC_REPRESENTATION_ITEM()
RATIONAL_B_SPLINE_CURVE((1.,0.866025403784439,1.,0.866025403784439,1.,0.866025403784439,
1.,0.866025403784439,1.,0.866025403784439,1.,0.866025403784439,1.))
REPRESENTATION_ITEM('')
);
#4284=(
BOUNDED_CURVE()
B_SPLINE_CURVE(2,(#371951,#371952,#371953,#371954,#371955,#371956,#371957,
#371958,#371959,#371960,#371961,#371962,#371963),.UNSPECIFIED.,.F.,.F.)
B_SPLINE_CURVE_WITH_KNOTS((3,2,2,2,2,2,3),(0.370967741935484,0.376344086021505,
0.381720430107527,0.387096774193548,0.39247311827957,0.397849462365591,
0.403225806451613),.UNSPECIFIED.)
CURVE()
GEOMETRIC_REPRESENTATION_ITEM()
RATIONAL_B_SPLINE_CURVE((1.,0.866025403784439,1.,0.866025403784439,1.,0.866025403784439,
1.,0.866025403784439,1.,0.866025403784439,1.,0.866025403784439,1.))
REPRESENTATION_ITEM('')
);
#4285=(
BOUNDED_CURVE()
B_SPLINE_CURVE(2,(#371964,#371965,#371966,#371967,#371968,#371969,#371970,
#371971,#371972,#371973,#371974,#371975,#371976),.UNSPECIFIED.,.F.,.F.)
B_SPLINE_CURVE_WITH_KNOTS((3,2,2,2,2,2,3),(0.370967741935484,0.376344086021505,
0.381720430107527,0.387096774193548,0.39247311827957,0.397849462365591,
0.403225806451613),.UNSPECIFIED.)
CURVE()
GEOMETRIC_REPRESENTATION_ITEM()
RATIONAL_B_SPLINE_CURVE((1.,0.866025403784439,1.,0.866025403784439,1.,0.866025403784439,
1.,0.866025403784439,1.,0.866025403784439,1.,0.866025403784439,1.))
REPRESENTATION_ITEM('')
);
#4286=(
BOUNDED_CURVE()
B_SPLINE_CURVE(2,(#371981,#371982,#371983,#371984,#371985,#371986,#371987,
#371988,#371989,#371990,#371991,#371992,#371993),.UNSPECIFIED.,.F.,.F.)
B_SPLINE_CURVE_WITH_KNOTS((3,2,2,2,2,2,3),(0.403225806451613,0.408602150537634,
0.413978494623656,0.419354838709677,0.424731182795699,0.43010752688172,
0.435483870967742),.UNSPECIFIED.)
CURVE()
GEOMETRIC_REPRESENTATION_ITEM()
RATIONAL_B_SPLINE_CURVE((1.,0.866025403784439,1.,0.866025403784439,1.,0.866025403784439,
1.,0.866025403784439,1.,0.866025403784439,1.,0.866025403784439,1.))
REPRESENTATION_ITEM('')
);
#4287=(
BOUNDED_CURVE()
B_SPLINE_CURVE(2,(#371994,#371995,#371996,#371997,#371998,#371999,#372000,
#372001,#372002,#372003,#372004,#372005,#372006),.UNSPECIFIED.,.F.,.F.)
B_SPLINE_CURVE_WITH_KNOTS((3,2,2,2,2,2,3),(0.403225806451613,0.408602150537634,
0.413978494623656,0.419354838709677,0.424731182795699,0.43010752688172,
0.435483870967742),.UNSPECIFIED.)
CURVE()
GEOMETRIC_REPRESENTATION_ITEM()
RATIONAL_B_SPLINE_CURVE((1.,0.866025403784439,1.,0.866025403784439,1.,0.866025403784439,
1.,0.866025403784439,1.,0.866025403784439,1.,0.866025403784439,1.))
REPRESENTATION_ITEM('')
);
#4288=(
BOUNDED_CURVE()
B_SPLINE_CURVE(2,(#372011,#372012,#372013,#372014,#372015,#372016,#372017,
#372018,#372019,#372020,#372021,#372022,#372023),.UNSPECIFIED.,.F.,.F.)
B_SPLINE_CURVE_WITH_KNOTS((3,2,2,2,2,2,3),(0.435483870967742,0.440860215053763,
0.446236559139785,0.451612903225806,0.456989247311828,0.462365591397849,
0.467741935483871),.UNSPECIFIED.)
CURVE()
GEOMETRIC_REPRESENTATION_ITEM()
RATIONAL_B_SPLINE_CURVE((1.,0.866025403784439,1.,0.866025403784439,1.,0.866025403784439,
1.,0.866025403784439,1.,0.866025403784439,1.,0.866025403784439,1.))
REPRESENTATION_ITEM('')
);
#4289=(
BOUNDED_CURVE()
B_SPLINE_CURVE(2,(#372024,#372025,#372026,#372027,#372028,#372029,#372030,
#372031,#372032,#372033,#372034,#372035,#372036),.UNSPECIFIED.,.F.,.F.)
B_SPLINE_CURVE_WITH_KNOTS((3,2,2,2,2,2,3),(0.435483870967742,0.440860215053763,
0.446236559139785,0.451612903225806,0.456989247311828,0.462365591397849,
0.467741935483871),.UNSPECIFIED.)
CURVE()
GEOMETRIC_REPRESENTATION_ITEM()
RATIONAL_B_SPLINE_CURVE((1.,0.866025403784439,1.,0.866025403784439,1.,0.866025403784439,
1.,0.866025403784439,1.,0.866025403784439,1.,0.866025403784439,1.))
REPRESENTATION_ITEM('')
);
#4290=(
BOUNDED_CURVE()
B_SPLINE_CURVE(2,(#372041,#372042,#372043,#372044,#372045,#372046,#372047,
#372048,#372049,#372050,#372051,#372052,#372053),.UNSPECIFIED.,.F.,.F.)
B_SPLINE_CURVE_WITH_KNOTS((3,2,2,2,2,2,3),(0.467741935483871,0.473118279569892,
0.478494623655914,0.483870967741935,0.489247311827957,0.494623655913979,
0.5),.UNSPECIFIED.)
CURVE()
GEOMETRIC_REPRESENTATION_ITEM()
RATIONAL_B_SPLINE_CURVE((1.,0.866025403784439,1.,0.866025403784439,1.,0.866025403784439,
1.,0.866025403784439,1.,0.866025403784439,1.,0.866025403784439,1.))
REPRESENTATION_ITEM('')
);
#4291=(
BOUNDED_CURVE()
B_SPLINE_CURVE(2,(#372054,#372055,#372056,#372057,#372058,#372059,#372060,
#372061,#372062,#372063,#372064,#372065,#372066),.UNSPECIFIED.,.F.,.F.)
B_SPLINE_CURVE_WITH_KNOTS((3,2,2,2,2,2,3),(0.467741935483871,0.473118279569892,
0.478494623655914,0.483870967741935,0.489247311827957,0.494623655913978,
0.5),.UNSPECIFIED.)
CURVE()
GEOMETRIC_REPRESENTATION_ITEM()
RATIONAL_B_SPLINE_CURVE((1.,0.866025403784439,1.,0.866025403784439,1.,0.866025403784439,
1.,0.866025403784439,1.,0.866025403784439,1.,0.866025403784439,1.))
REPRESENTATION_ITEM('')
);
#4292=(
BOUNDED_CURVE()
B_SPLINE_CURVE(2,(#372071,#372072,#372073,#372074,#372075,#372076,#372077,
#372078,#372079,#372080,#372081,#372082,#372083),.UNSPECIFIED.,.F.,.F.)
B_SPLINE_CURVE_WITH_KNOTS((3,2,2,2,2,2,3),(0.5,0.505376344086022,0.510752688172043,
0.516129032258065,0.521505376344086,0.526881720430108,0.532258064516129),
 .UNSPECIFIED.)
CURVE()
GEOMETRIC_REPRESENTATION_ITEM()
RATIONAL_B_SPLINE_CURVE((1.,0.866025403784439,1.,0.866025403784439,1.,0.866025403784439,
1.,0.866025403784439,1.,0.866025403784439,1.,0.866025403784439,1.))
REPRESENTATION_ITEM('')
);
#4293=(
BOUNDED_CURVE()
B_SPLINE_CURVE(2,(#372084,#372085,#372086,#372087,#372088,#372089,#372090,
#372091,#372092,#372093,#372094,#372095,#372096),.UNSPECIFIED.,.F.,.F.)
B_SPLINE_CURVE_WITH_KNOTS((3,2,2,2,2,2,3),(0.5,0.505376344086022,0.510752688172043,
0.516129032258065,0.521505376344086,0.526881720430108,0.532258064516129),
 .UNSPECIFIED.)
CURVE()
GEOMETRIC_REPRESENTATION_ITEM()
RATIONAL_B_SPLINE_CURVE((1.,0.866025403784439,1.,0.866025403784439,1.,0.866025403784439,
1.,0.866025403784439,1.,0.866025403784439,1.,0.866025403784439,1.))
REPRESENTATION_ITEM('')
);
#4294=(
BOUNDED_CURVE()
B_SPLINE_CURVE(2,(#372101,#372102,#372103,#372104,#372105,#372106,#372107,
#372108,#372109,#372110,#372111,#372112,#372113),.UNSPECIFIED.,.F.,.F.)
B_SPLINE_CURVE_WITH_KNOTS((3,2,2,2,2,2,3),(0.532258064516129,0.537634408602151,
0.543010752688172,0.548387096774194,0.553763440860215,0.559139784946237,
0.564516129032258),.UNSPECIFIED.)
CURVE()
GEOMETRIC_REPRESENTATION_ITEM()
RATIONAL_B_SPLINE_CURVE((1.,0.866025403784439,1.,0.866025403784439,1.,0.866025403784439,
1.,0.866025403784439,1.,0.866025403784439,1.,0.866025403784439,1.))
REPRESENTATION_ITEM('')
);
#4295=(
BOUNDED_CURVE()
B_SPLINE_CURVE(2,(#372114,#372115,#372116,#372117,#372118,#372119,#372120,
#372121,#372122,#372123,#372124,#372125,#372126),.UNSPECIFIED.,.F.,.F.)
B_SPLINE_CURVE_WITH_KNOTS((3,2,2,2,2,2,3),(0.532258064516129,0.537634408602151,
0.543010752688172,0.548387096774194,0.553763440860215,0.559139784946237,
0.564516129032258),.UNSPECIFIED.)
CURVE()
GEOMETRIC_REPRESENTATION_ITEM()
RATIONAL_B_SPLINE_CURVE((1.,0.866025403784439,1.,0.866025403784439,1.,0.866025403784439,
1.,0.866025403784439,1.,0.866025403784439,1.,0.866025403784439,1.))
REPRESENTATION_ITEM('')
);
#4296=(
BOUNDED_CURVE()
B_SPLINE_CURVE(2,(#372131,#372132,#372133,#372134,#372135,#372136,#372137,
#372138,#372139,#372140,#372141,#372142,#372143),.UNSPECIFIED.,.F.,.F.)
B_SPLINE_CURVE_WITH_KNOTS((3,2,2,2,2,2,3),(0.564516129032258,0.56989247311828,
0.575268817204301,0.580645161290323,0.586021505376344,0.591397849462366,
0.596774193548387),.UNSPECIFIED.)
CURVE()
GEOMETRIC_REPRESENTATION_ITEM()
RATIONAL_B_SPLINE_CURVE((1.,0.866025403784439,1.,0.866025403784439,1.,0.866025403784439,
1.,0.866025403784439,1.,0.866025403784439,1.,0.866025403784439,1.))
REPRESENTATION_ITEM('')
);
#4297=(
BOUNDED_CURVE()
B_SPLINE_CURVE(2,(#372144,#372145,#372146,#372147,#372148,#372149,#372150,
#372151,#372152,#372153,#372154,#372155,#372156),.UNSPECIFIED.,.F.,.F.)
B_SPLINE_CURVE_WITH_KNOTS((3,2,2,2,2,2,3),(0.564516129032258,0.56989247311828,
0.575268817204301,0.580645161290323,0.586021505376344,0.591397849462366,
0.596774193548387),.UNSPECIFIED.)
CURVE()
GEOMETRIC_REPRESENTATION_ITEM()
RATIONAL_B_SPLINE_CURVE((1.,0.866025403784439,1.,0.866025403784439,1.,0.866025403784439,
1.,0.866025403784439,1.,0.866025403784439,1.,0.866025403784439,1.))
REPRESENTATION_ITEM('')
);
#4298=(
BOUNDED_CURVE()
B_SPLINE_CURVE(2,(#372161,#372162,#372163,#372164,#372165,#372166,#372167,
#372168,#372169,#372170,#372171,#372172,#372173),.UNSPECIFIED.,.F.,.F.)
B_SPLINE_CURVE_WITH_KNOTS((3,2,2,2,2,2,3),(0.596774193548387,0.602150537634409,
0.60752688172043,0.612903225806452,0.618279569892473,0.623655913978495,
0.629032258064516),.UNSPECIFIED.)
CURVE()
GEOMETRIC_REPRESENTATION_ITEM()
RATIONAL_B_SPLINE_CURVE((1.,0.866025403784439,1.,0.866025403784439,1.,0.866025403784439,
1.,0.866025403784439,1.,0.866025403784439,1.,0.866025403784439,1.))
REPRESENTATION_ITEM('')
);
#4299=(
BOUNDED_CURVE()
B_SPLINE_CURVE(2,(#372174,#372175,#372176,#372177,#372178,#372179,#372180,
#372181,#372182,#372183,#372184,#372185,#372186),.UNSPECIFIED.,.F.,.F.)
B_SPLINE_CURVE_WITH_KNOTS((3,2,2,2,2,2,3),(0.596774193548387,0.602150537634409,
0.60752688172043,0.612903225806452,0.618279569892473,0.623655913978495,
0.629032258064516),.UNSPECIFIED.)
CURVE()
GEOMETRIC_REPRESENTATION_ITEM()
RATIONAL_B_SPLINE_CURVE((1.,0.866025403784439,1.,0.866025403784439,1.,0.866025403784439,
1.,0.866025403784439,1.,0.866025403784439,1.,0.866025403784439,1.))
REPRESENTATION_ITEM('')
);
#4300=(
BOUNDED_CURVE()
B_SPLINE_CURVE(2,(#372191,#372192,#372193,#372194,#372195,#372196,#372197,
#372198,#372199,#372200,#372201,#372202,#372203),.UNSPECIFIED.,.F.,.F.)
B_SPLINE_CURVE_WITH_KNOTS((3,2,2,2,2,2,3),(0.629032258064516,0.634408602150538,
0.639784946236559,0.645161290322581,0.650537634408602,0.655913978494624,
0.661290322580645),.UNSPECIFIED.)
CURVE()
GEOMETRIC_REPRESENTATION_ITEM()
RATIONAL_B_SPLINE_CURVE((1.,0.866025403784439,1.,0.866025403784439,1.,0.866025403784439,
1.,0.866025403784439,1.,0.866025403784439,1.,0.866025403784439,1.))
REPRESENTATION_ITEM('')
);
#4301=(
BOUNDED_CURVE()
B_SPLINE_CURVE(2,(#372204,#372205,#372206,#372207,#372208,#372209,#372210,
#372211,#372212,#372213,#372214,#372215,#372216),.UNSPECIFIED.,.F.,.F.)
B_SPLINE_CURVE_WITH_KNOTS((3,2,2,2,2,2,3),(0.629032258064516,0.634408602150538,
0.639784946236559,0.645161290322581,0.650537634408602,0.655913978494624,
0.661290322580645),.UNSPECIFIED.)
CURVE()
GEOMETRIC_REPRESENTATION_ITEM()
RATIONAL_B_SPLINE_CURVE((1.,0.866025403784439,1.,0.866025403784439,1.,0.866025403784439,
1.,0.866025403784439,1.,0.866025403784439,1.,0.866025403784439,1.))
REPRESENTATION_ITEM('')
);
#4302=(
BOUNDED_CURVE()
B_SPLINE_CURVE(2,(#372221,#372222,#372223,#372224,#372225,#372226,#372227,
#372228,#372229,#372230,#372231,#372232,#372233),.UNSPECIFIED.,.F.,.F.)
B_SPLINE_CURVE_WITH_KNOTS((3,2,2,2,2,2,3),(0.661290322580645,0.666666666666667,
0.672043010752688,0.67741935483871,0.682795698924731,0.688172043010753,
0.693548387096774),.UNSPECIFIED.)
CURVE()
GEOMETRIC_REPRESENTATION_ITEM()
RATIONAL_B_SPLINE_CURVE((1.,0.866025403784439,1.,0.866025403784439,1.,0.866025403784439,
1.,0.866025403784439,1.,0.866025403784439,1.,0.866025403784439,1.))
REPRESENTATION_ITEM('')
);
#4303=(
BOUNDED_CURVE()
B_SPLINE_CURVE(2,(#372234,#372235,#372236,#372237,#372238,#372239,#372240,
#372241,#372242,#372243,#372244,#372245,#372246),.UNSPECIFIED.,.F.,.F.)
B_SPLINE_CURVE_WITH_KNOTS((3,2,2,2,2,2,3),(0.661290322580645,0.666666666666667,
0.672043010752688,0.67741935483871,0.682795698924731,0.688172043010753,
0.693548387096774),.UNSPECIFIED.)
CURVE()
GEOMETRIC_REPRESENTATION_ITEM()
RATIONAL_B_SPLINE_CURVE((1.,0.866025403784439,1.,0.866025403784439,1.,0.866025403784439,
1.,0.866025403784439,1.,0.866025403784439,1.,0.866025403784439,1.))
REPRESENTATION_ITEM('')
);
#4304=(
BOUNDED_CURVE()
B_SPLINE_CURVE(2,(#372251,#372252,#372253,#372254,#372255,#372256,#372257,
#372258,#372259,#372260,#372261,#372262,#372263),.UNSPECIFIED.,.F.,.F.)
B_SPLINE_CURVE_WITH_KNOTS((3,2,2,2,2,2,3),(0.693548387096774,0.698924731182796,
0.704301075268817,0.709677419354839,0.71505376344086,0.720430107526882,
0.725806451612903),.UNSPECIFIED.)
CURVE()
GEOMETRIC_REPRESENTATION_ITEM()
RATIONAL_B_SPLINE_CURVE((1.,0.866025403784439,1.,0.866025403784439,1.,0.866025403784439,
1.,0.866025403784439,1.,0.866025403784439,1.,0.866025403784439,1.))
REPRESENTATION_ITEM('')
);
#4305=(
BOUNDED_CURVE()
B_SPLINE_CURVE(2,(#372264,#372265,#372266,#372267,#372268,#372269,#372270,
#372271,#372272,#372273,#372274,#372275,#372276),.UNSPECIFIED.,.F.,.F.)
B_SPLINE_CURVE_WITH_KNOTS((3,2,2,2,2,2,3),(0.693548387096774,0.698924731182796,
0.704301075268817,0.709677419354839,0.71505376344086,0.720430107526882,
0.725806451612903),.UNSPECIFIED.)
CURVE()
GEOMETRIC_REPRESENTATION_ITEM()
RATIONAL_B_SPLINE_CURVE((1.,0.866025403784439,1.,0.866025403784439,1.,0.866025403784439,
1.,0.866025403784439,1.,0.866025403784439,1.,0.866025403784439,1.))
REPRESENTATION_ITEM('')
);
#4306=(
BOUNDED_CURVE()
B_SPLINE_CURVE(2,(#372281,#372282,#372283,#372284,#372285,#372286,#372287,
#372288,#372289,#372290,#372291,#372292,#372293),.UNSPECIFIED.,.F.,.F.)
B_SPLINE_CURVE_WITH_KNOTS((3,2,2,2,2,2,3),(0.725806451612903,0.731182795698925,
0.736559139784946,0.741935483870968,0.747311827956989,0.752688172043011,
0.758064516129032),.UNSPECIFIED.)
CURVE()
GEOMETRIC_REPRESENTATION_ITEM()
RATIONAL_B_SPLINE_CURVE((1.,0.866025403784439,1.,0.866025403784439,1.,0.866025403784439,
1.,0.866025403784439,1.,0.866025403784439,1.,0.866025403784439,1.))
REPRESENTATION_ITEM('')
);
#4307=(
BOUNDED_CURVE()
B_SPLINE_CURVE(2,(#372294,#372295,#372296,#372297,#372298,#372299,#372300,
#372301,#372302,#372303,#372304,#372305,#372306),.UNSPECIFIED.,.F.,.F.)
B_SPLINE_CURVE_WITH_KNOTS((3,2,2,2,2,2,3),(0.725806451612903,0.731182795698925,
0.736559139784946,0.741935483870968,0.747311827956989,0.752688172043011,
0.758064516129032),.UNSPECIFIED.)
CURVE()
GEOMETRIC_REPRESENTATION_ITEM()
RATIONAL_B_SPLINE_CURVE((1.,0.866025403784439,1.,0.866025403784439,1.,0.866025403784439,
1.,0.866025403784439,1.,0.866025403784439,1.,0.866025403784439,1.))
REPRESENTATION_ITEM('')
);
#4308=(
BOUNDED_CURVE()
B_SPLINE_CURVE(2,(#372311,#372312,#372313,#372314,#372315,#372316,#372317,
#372318,#372319,#372320,#372321,#372322,#372323),.UNSPECIFIED.,.F.,.F.)
B_SPLINE_CURVE_WITH_KNOTS((3,2,2,2,2,2,3),(0.758064516129032,0.763440860215054,
0.768817204301075,0.774193548387097,0.779569892473118,0.78494623655914,
0.790322580645161),.UNSPECIFIED.)
CURVE()
GEOMETRIC_REPRESENTATION_ITEM()
RATIONAL_B_SPLINE_CURVE((1.,0.866025403784439,1.,0.866025403784439,1.,0.866025403784439,
1.,0.866025403784439,1.,0.866025403784439,1.,0.866025403784439,1.))
REPRESENTATION_ITEM('')
);
#4309=(
BOUNDED_CURVE()
B_SPLINE_CURVE(2,(#372324,#372325,#372326,#372327,#372328,#372329,#372330,
#372331,#372332,#372333,#372334,#372335,#372336),.UNSPECIFIED.,.F.,.F.)
B_SPLINE_CURVE_WITH_KNOTS((3,2,2,2,2,2,3),(0.758064516129032,0.763440860215054,
0.768817204301075,0.774193548387097,0.779569892473118,0.78494623655914,
0.790322580645161),.UNSPECIFIED.)
CURVE()
GEOMETRIC_REPRESENTATION_ITEM()
RATIONAL_B_SPLINE_CURVE((1.,0.866025403784439,1.,0.866025403784439,1.,0.866025403784439,
1.,0.866025403784439,1.,0.866025403784439,1.,0.866025403784439,1.))
REPRESENTATION_ITEM('')
);
#4310=(
BOUNDED_CURVE()
B_SPLINE_CURVE(2,(#372341,#372342,#372343,#372344,#372345,#372346,#372347,
#372348,#372349,#372350,#372351,#372352,#372353),.UNSPECIFIED.,.F.,.F.)
B_SPLINE_CURVE_WITH_KNOTS((3,2,2,2,2,2,3),(0.790322580645161,0.795698924731183,
0.801075268817204,0.806451612903226,0.811827956989247,0.817204301075269,
0.82258064516129),.UNSPECIFIED.)
CURVE()
GEOMETRIC_REPRESENTATION_ITEM()
RATIONAL_B_SPLINE_CURVE((1.,0.866025403784439,1.,0.866025403784439,1.,0.866025403784439,
1.,0.866025403784439,1.,0.866025403784439,1.,0.866025403784439,1.))
REPRESENTATION_ITEM('')
);
#4311=(
BOUNDED_CURVE()
B_SPLINE_CURVE(2,(#372354,#372355,#372356,#372357,#372358,#372359,#372360,
#372361,#372362,#372363,#372364,#372365,#372366),.UNSPECIFIED.,.F.,.F.)
B_SPLINE_CURVE_WITH_KNOTS((3,2,2,2,2,2,3),(0.790322580645161,0.795698924731183,
0.801075268817204,0.806451612903226,0.811827956989247,0.817204301075269,
0.82258064516129),.UNSPECIFIED.)
CURVE()
GEOMETRIC_REPRESENTATION_ITEM()
RATIONAL_B_SPLINE_CURVE((1.,0.866025403784439,1.,0.866025403784439,1.,0.866025403784439,
1.,0.866025403784439,1.,0.866025403784439,1.,0.866025403784439,1.))
REPRESENTATION_ITEM('')
);
#4312=(
BOUNDED_CURVE()
B_SPLINE_CURVE(2,(#372371,#372372,#372373,#372374,#372375,#372376,#372377,
#372378,#372379,#372380,#372381,#372382,#372383),.UNSPECIFIED.,.F.,.F.)
B_SPLINE_CURVE_WITH_KNOTS((3,2,2,2,2,2,3),(0.82258064516129,0.827956989247312,
0.833333333333333,0.838709677419355,0.844086021505376,0.849462365591398,
0.854838709677419),.UNSPECIFIED.)
CURVE()
GEOMETRIC_REPRESENTATION_ITEM()
RATIONAL_B_SPLINE_CURVE((1.,0.866025403784439,1.,0.866025403784439,1.,0.866025403784439,
1.,0.866025403784439,1.,0.866025403784439,1.,0.866025403784439,1.))
REPRESENTATION_ITEM('')
);
#4313=(
BOUNDED_CURVE()
B_SPLINE_CURVE(2,(#372384,#372385,#372386,#372387,#372388,#372389,#372390,
#372391,#372392,#372393,#372394,#372395,#372396),.UNSPECIFIED.,.F.,.F.)
B_SPLINE_CURVE_WITH_KNOTS((3,2,2,2,2,2,3),(0.82258064516129,0.827956989247312,
0.833333333333333,0.838709677419355,0.844086021505376,0.849462365591398,
0.854838709677419),.UNSPECIFIED.)
CURVE()
GEOMETRIC_REPRESENTATION_ITEM()
RATIONAL_B_SPLINE_CURVE((1.,0.866025403784439,1.,0.866025403784439,1.,0.866025403784439,
1.,0.866025403784439,1.,0.866025403784439,1.,0.866025403784439,1.))
REPRESENTATION_ITEM('')
);
#4314=(
BOUNDED_CURVE()
B_SPLINE_CURVE(2,(#372401,#372402,#372403,#372404,#372405,#372406,#372407,
#372408,#372409,#372410,#372411,#372412,#372413),.UNSPECIFIED.,.F.,.F.)
B_SPLINE_CURVE_WITH_KNOTS((3,2,2,2,2,2,3),(0.854838709677419,0.860215053763441,
0.865591397849462,0.870967741935484,0.876344086021505,0.881720430107527,
0.887096774193548),.UNSPECIFIED.)
CURVE()
GEOMETRIC_REPRESENTATION_ITEM()
RATIONAL_B_SPLINE_CURVE((1.,0.866025403784439,1.,0.866025403784439,1.,0.866025403784439,
1.,0.866025403784439,1.,0.866025403784439,1.,0.866025403784439,1.))
REPRESENTATION_ITEM('')
);
#4315=(
BOUNDED_CURVE()
B_SPLINE_CURVE(2,(#372414,#372415,#372416,#372417,#372418,#372419,#372420,
#372421,#372422,#372423,#372424,#372425,#372426),.UNSPECIFIED.,.F.,.F.)
B_SPLINE_CURVE_WITH_KNOTS((3,2,2,2,2,2,3),(0.854838709677419,0.860215053763441,
0.865591397849462,0.870967741935484,0.876344086021505,0.881720430107527,
0.887096774193548),.UNSPECIFIED.)
CURVE()
GEOMETRIC_REPRESENTATION_ITEM()
RATIONAL_B_SPLINE_CURVE((1.,0.866025403784439,1.,0.866025403784439,1.,0.866025403784439,
1.,0.866025403784439,1.,0.866025403784439,1.,0.866025403784439,1.))
REPRESENTATION_ITEM('')
);
#4316=(
BOUNDED_CURVE()
B_SPLINE_CURVE(2,(#372431,#372432,#372433,#372434,#372435,#372436,#372437,
#372438,#372439,#372440,#372441,#372442,#372443),.UNSPECIFIED.,.F.,.F.)
B_SPLINE_CURVE_WITH_KNOTS((3,2,2,2,2,2,3),(0.887096774193548,0.89247311827957,
0.897849462365591,0.903225806451613,0.908602150537634,0.913978494623656,
0.919354838709677),.UNSPECIFIED.)
CURVE()
GEOMETRIC_REPRESENTATION_ITEM()
RATIONAL_B_SPLINE_CURVE((1.,0.866025403784439,1.,0.866025403784439,1.,0.866025403784439,
1.,0.866025403784439,1.,0.866025403784439,1.,0.866025403784439,1.))
REPRESENTATION_ITEM('')
);
#4317=(
BOUNDED_CURVE()
B_SPLINE_CURVE(2,(#372444,#372445,#372446,#372447,#372448,#372449,#372450,
#372451,#372452,#372453,#372454,#372455,#372456),.UNSPECIFIED.,.F.,.F.)
B_SPLINE_CURVE_WITH_KNOTS((3,2,2,2,2,2,3),(0.887096774193548,0.89247311827957,
0.897849462365591,0.903225806451613,0.908602150537634,0.913978494623656,
0.919354838709677),.UNSPECIFIED.)
CURVE()
GEOMETRIC_REPRESENTATION_ITEM()
RATIONAL_B_SPLINE_CURVE((1.,0.866025403784439,1.,0.866025403784439,1.,0.866025403784439,
1.,0.866025403784439,1.,0.866025403784439,1.,0.866025403784439,1.))
REPRESENTATION_ITEM('')
);
#4318=(
BOUNDED_CURVE()
B_SPLINE_CURVE(2,(#374793,#374794,#374795),.UNSPECIFIED.,.F.,.F.)
B_SPLINE_CURVE_WITH_KNOTS((3,3),(0.127655147271297,0.35532436269275),
 .UNSPECIFIED.)
CURVE()
GEOMETRIC_REPRESENTATION_ITEM()
RATIONAL_B_SPLINE_CURVE((1.3712812921102,1.58341924626904,1.3712812921102))
REPRESENTATION_ITEM('')
);
#4319=(
BOUNDED_CURVE()
B_SPLINE_CURVE(2,(#378380,#378381,#378382),.UNSPECIFIED.,.F.,.F.)
B_SPLINE_CURVE_WITH_KNOTS((3,3),(-0.355324362692751,-0.127655147271297),
 .UNSPECIFIED.)
CURVE()
GEOMETRIC_REPRESENTATION_ITEM()
RATIONAL_B_SPLINE_CURVE((1.3712812921102,1.58341924626904,1.3712812921102))
REPRESENTATION_ITEM('')
);
#4320=(
BOUNDED_CURVE()
B_SPLINE_CURVE(2,(#378388,#378389,#378390),.UNSPECIFIED.,.F.,.F.)
B_SPLINE_CURVE_WITH_KNOTS((3,3),(-0.355324362692751,-0.127655147271297),
 .UNSPECIFIED.)
CURVE()
GEOMETRIC_REPRESENTATION_ITEM()
RATIONAL_B_SPLINE_CURVE((1.3712812921102,1.58341924626905,1.37128129211021))
REPRESENTATION_ITEM('')
);
#4321=(
BOUNDED_CURVE()
B_SPLINE_CURVE(2,(#378394,#378395,#378396),.UNSPECIFIED.,.F.,.F.)
B_SPLINE_CURVE_WITH_KNOTS((3,3),(-0.35532436269275,-0.127655147271297),
 .UNSPECIFIED.)
CURVE()
GEOMETRIC_REPRESENTATION_ITEM()
RATIONAL_B_SPLINE_CURVE((1.37128129211021,1.58341924626905,1.37128129211021))
REPRESENTATION_ITEM('')
);
#4322=(
BOUNDED_CURVE()
B_SPLINE_CURVE(2,(#378400,#378401,#378402),.UNSPECIFIED.,.F.,.F.)
B_SPLINE_CURVE_WITH_KNOTS((3,3),(-0.355324362692751,-0.127655147271297),
 .UNSPECIFIED.)
CURVE()
GEOMETRIC_REPRESENTATION_ITEM()
RATIONAL_B_SPLINE_CURVE((1.37128129211021,1.58341924626905,1.37128129211021))
REPRESENTATION_ITEM('')
);
#4323=(
BOUNDED_CURVE()
B_SPLINE_CURVE(2,(#378405,#378406,#378407),.UNSPECIFIED.,.F.,.F.)
B_SPLINE_CURVE_WITH_KNOTS((3,3),(-0.35532436269275,-0.127655147271297),
 .UNSPECIFIED.)
CURVE()
GEOMETRIC_REPRESENTATION_ITEM()
RATIONAL_B_SPLINE_CURVE((1.37128129211021,1.58341924626905,1.37128129211021))
REPRESENTATION_ITEM('')
);
#4324=(
BOUNDED_CURVE()
B_SPLINE_CURVE(2,(#378417,#378418,#378419,#378420,#378421,#378422,#378423),
 .UNSPECIFIED.,.F.,.F.)
B_SPLINE_CURVE_WITH_KNOTS((3,2,2,3),(0.919354838709677,0.924731182795699,
0.93010752688172,0.930718281243958),.UNSPECIFIED.)
CURVE()
GEOMETRIC_REPRESENTATION_ITEM()
RATIONAL_B_SPLINE_CURVE((1.,0.866025403784439,1.,0.866025403784439,1.,0.984780444153422,
0.973018780873198))
REPRESENTATION_ITEM('')
);
#4325=(
BOUNDED_CURVE()
B_SPLINE_CURVE(2,(#378424,#378425,#378426,#378427,#378428),
 .UNSPECIFIED.,.F.,.F.)
B_SPLINE_CURVE_WITH_KNOTS((3,2,3),(0.919354838709677,0.924731182795699,
0.926677363777307),.UNSPECIFIED.)
CURVE()
GEOMETRIC_REPRESENTATION_ITEM()
RATIONAL_B_SPLINE_CURVE((1.,0.866025403784439,1.,0.951502581121761,0.938116290834902))
REPRESENTATION_ITEM('')
);
#4419=SHAPE_REPRESENTATION_RELATIONSHIP('SRR','None',#459345,#4440);
#4440=ADVANCED_BREP_SHAPE_REPRESENTATION('',(#4487),#459234);
#4487=MANIFOLD_SOLID_BREP('Body',#94665);
#4607=STYLED_ITEM('',(#459533),#4487);
#4903=CONICAL_SURFACE('',#99447,999.999999999989,0.785398163397443);
#4904=CONICAL_SURFACE('',#99449,1.17524047358083,0.785398163397453);
#4905=CONICAL_SURFACE('',#99451,1.17524047358083,0.785398163397453);
#4906=CONICAL_SURFACE('',#99454,999.999999999989,0.785398163397443);
#4907=CONICAL_SURFACE('',#99459,1.25,1.0471975511966);
#4908=CONICAL_SURFACE('',#99466,1.44337567297406,0.78539816339745);
#4909=CONICAL_SURFACE('',#99472,2.54610912703474,0.785398163397439);
#4910=CONICAL_SURFACE('',#99477,2.73389087296526,0.785398163397455);
#4911=CONICAL_SURFACE('',#100392,1.44337567297406,0.78539816339745);
#4912=CONICAL_SURFACE('',#100393,1.44337567297406,0.78539816339745);
#4913=CONICAL_SURFACE('',#100394,1.44337567297406,0.78539816339745);
#4914=CONICAL_SURFACE('',#100395,1.44337567297406,0.78539816339745);
#4915=CONICAL_SURFACE('',#100396,1.44337567297406,0.78539816339745);
#4916=CONICAL_SURFACE('',#100400,2.75,0.78539816339745);
#4917=CONICAL_SURFACE('',#100439,2.75,0.78539816339745);
#4918=CONICAL_SURFACE('',#100462,2.75,0.78539816339745);
#4919=CONICAL_SURFACE('',#100485,2.75,0.78539816339745);
#4920=CONICAL_SURFACE('',#100508,2.75,0.78539816339745);
#4921=CONICAL_SURFACE('',#100531,2.75,0.78539816339745);
#4922=CONICAL_SURFACE('',#100554,2.75,0.78539816339745);
#4923=CONICAL_SURFACE('',#100577,2.75,0.78539816339745);
#4924=CONICAL_SURFACE('',#100600,2.75,0.78539816339745);
#4925=CONICAL_SURFACE('',#100623,2.75,0.78539816339745);
#4926=CONICAL_SURFACE('',#100646,2.75,0.78539816339745);
#4927=CONICAL_SURFACE('',#100669,2.75,0.78539816339745);
#4928=CONICAL_SURFACE('',#100692,2.75,0.78539816339745);
#4929=CONICAL_SURFACE('',#100715,2.75,0.78539816339745);
#4930=CONICAL_SURFACE('',#100738,2.75,0.78539816339745);
#4931=CONICAL_SURFACE('',#100761,2.75,0.78539816339745);
#4932=CONICAL_SURFACE('',#100784,2.75,0.78539816339745);
#4933=CONICAL_SURFACE('',#100807,2.75,0.78539816339745);
#4934=CONICAL_SURFACE('',#100830,2.75,0.78539816339745);
#4935=CONICAL_SURFACE('',#100853,2.75,0.78539816339745);
#4936=CONICAL_SURFACE('',#100876,2.75,0.78539816339745);
#4937=CONICAL_SURFACE('',#100899,2.75,0.78539816339745);
#4938=CONICAL_SURFACE('',#100922,2.75,0.78539816339745);
#4939=CONICAL_SURFACE('',#100945,2.75,0.78539816339745);
#4940=CONICAL_SURFACE('',#100968,2.75,0.78539816339745);
#4941=CONICAL_SURFACE('',#100991,2.75,0.78539816339745);
#4942=CONICAL_SURFACE('',#101014,2.75,0.78539816339745);
#4943=CONICAL_SURFACE('',#101037,2.75,0.78539816339745);
#4944=CONICAL_SURFACE('',#101060,2.75,0.78539816339745);
#4945=CONICAL_SURFACE('',#101083,2.75,0.78539816339745);
#4946=CONICAL_SURFACE('',#101106,2.75,0.78539816339745);
#4947=CONICAL_SURFACE('',#101129,2.75,0.78539816339745);
#4948=CONICAL_SURFACE('',#101152,2.75,0.78539816339745);
#4949=CONICAL_SURFACE('',#101175,2.75,0.78539816339745);
#4950=CONICAL_SURFACE('',#101198,2.75,0.78539816339745);
#4951=CONICAL_SURFACE('',#101221,2.75,0.78539816339745);
#4952=CONICAL_SURFACE('',#101244,2.75,0.78539816339745);
#4953=CONICAL_SURFACE('',#101267,2.75,0.78539816339745);
#4954=CONICAL_SURFACE('',#101290,2.75,0.78539816339745);
#4955=CONICAL_SURFACE('',#101313,2.75,0.78539816339745);
#4956=CONICAL_SURFACE('',#101336,2.75,0.78539816339745);
#4957=CONICAL_SURFACE('',#101359,2.75,0.78539816339745);
#4958=CONICAL_SURFACE('',#101382,2.75,0.78539816339745);
#4959=CONICAL_SURFACE('',#101405,2.75,0.78539816339745);
#4960=CONICAL_SURFACE('',#101428,2.75,0.78539816339745);
#4961=CONICAL_SURFACE('',#101451,2.75,0.78539816339745);
#4962=CONICAL_SURFACE('',#101474,2.75,0.78539816339745);
#4963=CONICAL_SURFACE('',#101497,2.75,0.78539816339745);
#4964=CONICAL_SURFACE('',#101520,2.75,0.78539816339745);
#4965=CONICAL_SURFACE('',#101543,2.75,0.78539816339745);
#4966=CONICAL_SURFACE('',#101566,2.75,0.78539816339745);
#4967=CONICAL_SURFACE('',#101589,2.75,0.78539816339745);
#4968=CONICAL_SURFACE('',#101612,2.75,0.78539816339745);
#4969=CONICAL_SURFACE('',#101635,2.75,0.78539816339745);
#4970=CONICAL_SURFACE('',#101658,2.75,0.78539816339745);
#4971=CONICAL_SURFACE('',#101681,2.75,0.78539816339745);
#4972=CONICAL_SURFACE('',#101704,2.75,0.78539816339745);
#4973=CONICAL_SURFACE('',#101727,2.75,0.78539816339745);
#4974=CONICAL_SURFACE('',#101750,2.75,0.78539816339745);
#4975=CONICAL_SURFACE('',#101773,2.75,0.78539816339745);
#4976=CONICAL_SURFACE('',#101796,2.75,0.78539816339745);
#4977=CONICAL_SURFACE('',#101819,2.75,0.78539816339745);
#4978=CONICAL_SURFACE('',#101842,2.75,0.78539816339745);
#4979=CONICAL_SURFACE('',#101865,2.75,0.78539816339745);
#4980=CONICAL_SURFACE('',#101888,2.75,0.78539816339745);
#4981=CONICAL_SURFACE('',#101911,2.75,0.78539816339745);
#4982=CONICAL_SURFACE('',#101934,2.75,0.78539816339745);
#4983=CONICAL_SURFACE('',#101957,2.75,0.78539816339745);
#4984=CONICAL_SURFACE('',#101980,2.75,0.78539816339745);
#4985=CONICAL_SURFACE('',#102003,2.75,0.78539816339745);
#4986=CONICAL_SURFACE('',#102026,2.75,0.78539816339745);
#4987=CONICAL_SURFACE('',#102049,2.75,0.78539816339745);
#4988=CONICAL_SURFACE('',#102072,2.75,0.78539816339745);
#4989=CONICAL_SURFACE('',#102095,2.75,0.78539816339745);
#4990=CONICAL_SURFACE('',#102118,2.75,0.78539816339745);
#4991=CONICAL_SURFACE('',#102141,2.75,0.78539816339745);
#4992=CONICAL_SURFACE('',#102164,2.75,0.78539816339745);
#4993=CONICAL_SURFACE('',#102187,2.75,0.78539816339745);
#4994=CONICAL_SURFACE('',#102210,2.75,0.78539816339745);
#4995=CONICAL_SURFACE('',#102233,2.75,0.78539816339745);
#4996=CONICAL_SURFACE('',#102256,2.75,0.78539816339745);
#4997=CONICAL_SURFACE('',#102279,2.75,0.78539816339745);
#4998=CONICAL_SURFACE('',#102302,2.75,0.78539816339745);
#4999=CONICAL_SURFACE('',#102325,2.75,0.78539816339745);
#5000=CONICAL_SURFACE('',#102348,2.75,0.78539816339745);
#5001=CONICAL_SURFACE('',#102371,2.75,0.78539816339745);
#5002=CONICAL_SURFACE('',#102394,2.75,0.78539816339745);
#5003=CONICAL_SURFACE('',#102417,2.75,0.78539816339745);
#5004=CONICAL_SURFACE('',#102440,2.75,0.78539816339745);
#5005=CONICAL_SURFACE('',#102463,2.75,0.78539816339745);
#5006=CONICAL_SURFACE('',#102486,2.75,0.78539816339745);
#5007=CONICAL_SURFACE('',#102509,2.75,0.78539816339745);
#5008=CONICAL_SURFACE('',#102532,2.75,0.78539816339745);
#5009=CONICAL_SURFACE('',#102555,2.75,0.78539816339745);
#5010=CONICAL_SURFACE('',#102578,2.75,0.78539816339745);
#5011=CONICAL_SURFACE('',#102601,2.75,0.78539816339745);
#5012=CONICAL_SURFACE('',#102624,2.75,0.78539816339745);
#5013=CONICAL_SURFACE('',#102647,2.75,0.78539816339745);
#5226=FACE_BOUND('',#14649,.T.);
#5227=FACE_BOUND('',#14664,.T.);
#5726=PLANE('',#100367);
#5727=PLANE('',#100369);
#5728=PLANE('',#100371);
#5729=PLANE('',#100372);
#5730=PLANE('',#100373);
#5731=PLANE('',#100374);
#5732=PLANE('',#100375);
#5733=PLANE('',#100376);
#5734=PLANE('',#100385);
#5735=PLANE('',#100386);
#5736=PLANE('',#100387);
#5737=PLANE('',#100388);
#5738=PLANE('',#100389);
#5739=PLANE('',#100390);
#5740=PLANE('',#100391);
#5741=PLANE('',#100397);
#5742=PLANE('',#100398);
#5743=PLANE('',#100417);
#5744=PLANE('',#100419);
#5745=PLANE('',#100440);
#5746=PLANE('',#100442);
#5747=PLANE('',#100463);
#5748=PLANE('',#100465);
#5749=PLANE('',#100486);
#5750=PLANE('',#100488);
#5751=PLANE('',#100509);
#5752=PLANE('',#100511);
#5753=PLANE('',#100532);
#5754=PLANE('',#100534);
#5755=PLANE('',#100555);
#5756=PLANE('',#100557);
#5757=PLANE('',#100578);
#5758=PLANE('',#100580);
#5759=PLANE('',#100601);
#5760=PLANE('',#100603);
#5761=PLANE('',#100624);
#5762=PLANE('',#100626);
#5763=PLANE('',#100647);
#5764=PLANE('',#100649);
#5765=PLANE('',#100670);
#5766=PLANE('',#100672);
#5767=PLANE('',#100693);
#5768=PLANE('',#100695);
#5769=PLANE('',#100716);
#5770=PLANE('',#100718);
#5771=PLANE('',#100739);
#5772=PLANE('',#100741);
#5773=PLANE('',#100762);
#5774=PLANE('',#100764);
#5775=PLANE('',#100785);
#5776=PLANE('',#100787);
#5777=PLANE('',#100808);
#5778=PLANE('',#100810);
#5779=PLANE('',#100831);
#5780=PLANE('',#100833);
#5781=PLANE('',#100854);
#5782=PLANE('',#100856);
#5783=PLANE('',#100877);
#5784=PLANE('',#100879);
#5785=PLANE('',#100900);
#5786=PLANE('',#100902);
#5787=PLANE('',#100923);
#5788=PLANE('',#100925);
#5789=PLANE('',#100946);
#5790=PLANE('',#100948);
#5791=PLANE('',#100969);
#5792=PLANE('',#100971);
#5793=PLANE('',#100992);
#5794=PLANE('',#100994);
#5795=PLANE('',#101015);
#5796=PLANE('',#101017);
#5797=PLANE('',#101038);
#5798=PLANE('',#101040);
#5799=PLANE('',#101061);
#5800=PLANE('',#101063);
#5801=PLANE('',#101084);
#5802=PLANE('',#101086);
#5803=PLANE('',#101107);
#5804=PLANE('',#101109);
#5805=PLANE('',#101130);
#5806=PLANE('',#101132);
#5807=PLANE('',#101153);
#5808=PLANE('',#101155);
#5809=PLANE('',#101176);
#5810=PLANE('',#101178);
#5811=PLANE('',#101199);
#5812=PLANE('',#101201);
#5813=PLANE('',#101222);
#5814=PLANE('',#101224);
#5815=PLANE('',#101245);
#5816=PLANE('',#101247);
#5817=PLANE('',#101268);
#5818=PLANE('',#101270);
#5819=PLANE('',#101291);
#5820=PLANE('',#101293);
#5821=PLANE('',#101314);
#5822=PLANE('',#101316);
#5823=PLANE('',#101337);
#5824=PLANE('',#101339);
#5825=PLANE('',#101360);
#5826=PLANE('',#101362);
#5827=PLANE('',#101383);
#5828=PLANE('',#101385);
#5829=PLANE('',#101406);
#5830=PLANE('',#101408);
#5831=PLANE('',#101429);
#5832=PLANE('',#101431);
#5833=PLANE('',#101452);
#5834=PLANE('',#101454);
#5835=PLANE('',#101475);
#5836=PLANE('',#101477);
#5837=PLANE('',#101498);
#5838=PLANE('',#101500);
#5839=PLANE('',#101521);
#5840=PLANE('',#101523);
#5841=PLANE('',#101544);
#5842=PLANE('',#101546);
#5843=PLANE('',#101567);
#5844=PLANE('',#101569);
#5845=PLANE('',#101590);
#5846=PLANE('',#101592);
#5847=PLANE('',#101613);
#5848=PLANE('',#101615);
#5849=PLANE('',#101636);
#5850=PLANE('',#101638);
#5851=PLANE('',#101659);
#5852=PLANE('',#101661);
#5853=PLANE('',#101682);
#5854=PLANE('',#101684);
#5855=PLANE('',#101705);
#5856=PLANE('',#101707);
#5857=PLANE('',#101728);
#5858=PLANE('',#101730);
#5859=PLANE('',#101751);
#5860=PLANE('',#101753);
#5861=PLANE('',#101774);
#5862=PLANE('',#101776);
#5863=PLANE('',#101797);
#5864=PLANE('',#101799);
#5865=PLANE('',#101820);
#5866=PLANE('',#101822);
#5867=PLANE('',#101843);
#5868=PLANE('',#101845);
#5869=PLANE('',#101866);
#5870=PLANE('',#101868);
#5871=PLANE('',#101889);
#5872=PLANE('',#101891);
#5873=PLANE('',#101912);
#5874=PLANE('',#101914);
#5875=PLANE('',#101935);
#5876=PLANE('',#101937);
#5877=PLANE('',#101958);
#5878=PLANE('',#101960);
#5879=PLANE('',#101981);
#5880=PLANE('',#101983);
#5881=PLANE('',#102004);
#5882=PLANE('',#102006);
#5883=PLANE('',#102027);
#5884=PLANE('',#102029);
#5885=PLANE('',#102050);
#5886=PLANE('',#102052);
#5887=PLANE('',#102073);
#5888=PLANE('',#102075);
#5889=PLANE('',#102096);
#5890=PLANE('',#102098);
#5891=PLANE('',#102119);
#5892=PLANE('',#102121);
#5893=PLANE('',#102142);
#5894=PLANE('',#102144);
#5895=PLANE('',#102165);
#5896=PLANE('',#102167);
#5897=PLANE('',#102188);
#5898=PLANE('',#102190);
#5899=PLANE('',#102211);
#5900=PLANE('',#102213);
#5901=PLANE('',#102234);
#5902=PLANE('',#102236);
#5903=PLANE('',#102257);
#5904=PLANE('',#102259);
#5905=PLANE('',#102280);
#5906=PLANE('',#102282);
#5907=PLANE('',#102303);
#5908=PLANE('',#102305);
#5909=PLANE('',#102326);
#5910=PLANE('',#102328);
#5911=PLANE('',#102349);
#5912=PLANE('',#102351);
#5913=PLANE('',#102372);
#5914=PLANE('',#102374);
#5915=PLANE('',#102395);
#5916=PLANE('',#102397);
#5917=PLANE('',#102418);
#5918=PLANE('',#102420);
#5919=PLANE('',#102441);
#5920=PLANE('',#102443);
#5921=PLANE('',#102464);
#5922=PLANE('',#102466);
#5923=PLANE('',#102487);
#5924=PLANE('',#102489);
#5925=PLANE('',#102510);
#5926=PLANE('',#102512);
#5927=PLANE('',#102533);
#5928=PLANE('',#102535);
#5929=PLANE('',#102556);
#5930=PLANE('',#102558);
#5931=PLANE('',#102579);
#5932=PLANE('',#102581);
#5933=PLANE('',#102602);
#5934=PLANE('',#102604);
#5935=PLANE('',#102625);
#5936=PLANE('',#102627);
#8551=FACE_OUTER_BOUND('',#14472,.T.);
#8552=FACE_OUTER_BOUND('',#14473,.T.);
#8553=FACE_OUTER_BOUND('',#14474,.T.);
#8554=FACE_OUTER_BOUND('',#14475,.T.);
#8555=FACE_OUTER_BOUND('',#14476,.T.);
#8556=FACE_OUTER_BOUND('',#14477,.T.);
#8557=FACE_OUTER_BOUND('',#14478,.T.);
#8558=FACE_OUTER_BOUND('',#14479,.T.);
#8559=FACE_OUTER_BOUND('',#14480,.T.);
#8560=FACE_OUTER_BOUND('',#14481,.T.);
#8561=FACE_OUTER_BOUND('',#14482,.T.);
#8562=FACE_OUTER_BOUND('',#14483,.T.);
#8563=FACE_OUTER_BOUND('',#14484,.T.);
#8564=FACE_OUTER_BOUND('',#14485,.T.);
#8565=FACE_OUTER_BOUND('',#14486,.T.);
#8566=FACE_OUTER_BOUND('',#14487,.T.);
#8567=FACE_OUTER_BOUND('',#14488,.T.);
#8568=FACE_OUTER_BOUND('',#14489,.T.);
#8569=FACE_OUTER_BOUND('',#14490,.T.);
#8570=FACE_OUTER_BOUND('',#14491,.T.);
#8571=FACE_OUTER_BOUND('',#14492,.T.);
#8572=FACE_OUTER_BOUND('',#14493,.T.);
#8573=FACE_OUTER_BOUND('',#14494,.T.);
#8574=FACE_OUTER_BOUND('',#14495,.T.);
#8575=FACE_OUTER_BOUND('',#14496,.T.);
#8576=FACE_OUTER_BOUND('',#14497,.T.);
#8577=FACE_OUTER_BOUND('',#14498,.T.);
#8578=FACE_OUTER_BOUND('',#14499,.T.);
#8579=FACE_OUTER_BOUND('',#14500,.T.);
#8580=FACE_OUTER_BOUND('',#14501,.T.);
#8581=FACE_OUTER_BOUND('',#14502,.T.);
#8582=FACE_OUTER_BOUND('',#14503,.T.);
#8583=FACE_OUTER_BOUND('',#14504,.T.);
#8584=FACE_OUTER_BOUND('',#14505,.T.);
#8585=FACE_OUTER_BOUND('',#14506,.T.);
#8586=FACE_OUTER_BOUND('',#14507,.T.);
#8587=FACE_OUTER_BOUND('',#14508,.T.);
#8588=FACE_OUTER_BOUND('',#14509,.T.);
#8589=FACE_OUTER_BOUND('',#14510,.T.);
#8590=FACE_OUTER_BOUND('',#14511,.T.);
#8591=FACE_OUTER_BOUND('',#14512,.T.);
#8592=FACE_OUTER_BOUND('',#14513,.T.);
#8593=FACE_OUTER_BOUND('',#14514,.T.);
#8594=FACE_OUTER_BOUND('',#14515,.T.);
#8595=FACE_OUTER_BOUND('',#14516,.T.);
#8596=FACE_OUTER_BOUND('',#14517,.T.);
#8597=FACE_OUTER_BOUND('',#14518,.T.);
#8598=FACE_OUTER_BOUND('',#14519,.T.);
#8599=FACE_OUTER_BOUND('',#14520,.T.);
#8600=FACE_OUTER_BOUND('',#14521,.T.);
#8601=FACE_OUTER_BOUND('',#14522,.T.);
#8602=FACE_OUTER_BOUND('',#14523,.T.);
#8603=FACE_OUTER_BOUND('',#14524,.T.);
#8604=FACE_OUTER_BOUND('',#14525,.T.);
#8605=FACE_OUTER_BOUND('',#14526,.T.);
#8606=FACE_OUTER_BOUND('',#14527,.T.);
#8607=FACE_OUTER_BOUND('',#14528,.T.);
#8608=FACE_OUTER_BOUND('',#14529,.T.);
#8609=FACE_OUTER_BOUND('',#14530,.T.);
#8610=FACE_OUTER_BOUND('',#14531,.T.);
#8611=FACE_OUTER_BOUND('',#14532,.T.);
#8612=FACE_OUTER_BOUND('',#14533,.T.);
#8613=FACE_OUTER_BOUND('',#14534,.T.);
#8614=FACE_OUTER_BOUND('',#14535,.T.);
#8615=FACE_OUTER_BOUND('',#14536,.T.);
#8616=FACE_OUTER_BOUND('',#14537,.T.);
#8617=FACE_OUTER_BOUND('',#14538,.T.);
#8618=FACE_OUTER_BOUND('',#14539,.T.);
#8619=FACE_OUTER_BOUND('',#14540,.T.);
#8620=FACE_OUTER_BOUND('',#14541,.T.);
#8621=FACE_OUTER_BOUND('',#14542,.T.);
#8622=FACE_OUTER_BOUND('',#14543,.T.);
#8623=FACE_OUTER_BOUND('',#14544,.T.);
#8624=FACE_OUTER_BOUND('',#14545,.T.);
#8625=FACE_OUTER_BOUND('',#14546,.T.);
#8626=FACE_OUTER_BOUND('',#14547,.T.);
#8627=FACE_OUTER_BOUND('',#14548,.T.);
#8628=FACE_OUTER_BOUND('',#14549,.T.);
#8629=FACE_OUTER_BOUND('',#14550,.T.);
#8630=FACE_OUTER_BOUND('',#14551,.T.);
#8631=FACE_OUTER_BOUND('',#14552,.T.);
#8632=FACE_OUTER_BOUND('',#14553,.T.);
#8633=FACE_OUTER_BOUND('',#14554,.T.);
#8634=FACE_OUTER_BOUND('',#14555,.T.);
#8635=FACE_OUTER_BOUND('',#14556,.T.);
#8636=FACE_OUTER_BOUND('',#14557,.T.);
#8637=FACE_OUTER_BOUND('',#14558,.T.);
#8638=FACE_OUTER_BOUND('',#14559,.T.);
#8639=FACE_OUTER_BOUND('',#14560,.T.);
#8640=FACE_OUTER_BOUND('',#14561,.T.);
#8641=FACE_OUTER_BOUND('',#14562,.T.);
#8642=FACE_OUTER_BOUND('',#14563,.T.);
#8643=FACE_OUTER_BOUND('',#14564,.T.);
#8644=FACE_OUTER_BOUND('',#14565,.T.);
#8645=FACE_OUTER_BOUND('',#14566,.T.);
#8646=FACE_OUTER_BOUND('',#14567,.T.);
#8647=FACE_OUTER_BOUND('',#14568,.T.);
#8648=FACE_OUTER_BOUND('',#14569,.T.);
#8649=FACE_OUTER_BOUND('',#14570,.T.);
#8650=FACE_OUTER_BOUND('',#14571,.T.);
#8651=FACE_OUTER_BOUND('',#14572,.T.);
#8652=FACE_OUTER_BOUND('',#14573,.T.);
#8653=FACE_OUTER_BOUND('',#14574,.T.);
#8654=FACE_OUTER_BOUND('',#14575,.T.);
#8655=FACE_OUTER_BOUND('',#14576,.T.);
#8656=FACE_OUTER_BOUND('',#14577,.T.);
#8657=FACE_OUTER_BOUND('',#14578,.T.);
#8658=FACE_OUTER_BOUND('',#14579,.T.);
#8659=FACE_OUTER_BOUND('',#14580,.T.);
#8660=FACE_OUTER_BOUND('',#14581,.T.);
#8661=FACE_OUTER_BOUND('',#14582,.T.);
#8662=FACE_OUTER_BOUND('',#14583,.T.);
#8663=FACE_OUTER_BOUND('',#14584,.T.);
#8664=FACE_OUTER_BOUND('',#14585,.T.);
#8665=FACE_OUTER_BOUND('',#14586,.T.);
#8666=FACE_OUTER_BOUND('',#14587,.T.);
#8667=FACE_OUTER_BOUND('',#14588,.T.);
#8668=FACE_OUTER_BOUND('',#14589,.T.);
#8669=FACE_OUTER_BOUND('',#14590,.T.);
#8670=FACE_OUTER_BOUND('',#14591,.T.);
#8671=FACE_OUTER_BOUND('',#14592,.T.);
#8672=FACE_OUTER_BOUND('',#14593,.T.);
#8673=FACE_OUTER_BOUND('',#14594,.T.);
#8674=FACE_OUTER_BOUND('',#14595,.T.);
#8675=FACE_OUTER_BOUND('',#14596,.T.);
#8676=FACE_OUTER_BOUND('',#14597,.T.);
#8677=FACE_OUTER_BOUND('',#14598,.T.);
#8678=FACE_OUTER_BOUND('',#14599,.T.);
#8679=FACE_OUTER_BOUND('',#14600,.T.);
#8680=FACE_OUTER_BOUND('',#14601,.T.);
#8681=FACE_OUTER_BOUND('',#14602,.T.);
#8682=FACE_OUTER_BOUND('',#14603,.T.);
#8683=FACE_OUTER_BOUND('',#14604,.T.);
#8684=FACE_OUTER_BOUND('',#14605,.T.);
#8685=FACE_OUTER_BOUND('',#14606,.T.);
#8686=FACE_OUTER_BOUND('',#14607,.T.);
#8687=FACE_OUTER_BOUND('',#14608,.T.);
#8688=FACE_OUTER_BOUND('',#14609,.T.);
#8689=FACE_OUTER_BOUND('',#14610,.T.);
#8690=FACE_OUTER_BOUND('',#14611,.T.);
#8691=FACE_OUTER_BOUND('',#14612,.T.);
#8692=FACE_OUTER_BOUND('',#14613,.T.);
#8693=FACE_OUTER_BOUND('',#14614,.T.);
#8694=FACE_OUTER_BOUND('',#14615,.T.);
#8695=FACE_OUTER_BOUND('',#14616,.T.);
#8696=FACE_OUTER_BOUND('',#14617,.T.);
#8697=FACE_OUTER_BOUND('',#14618,.T.);
#8698=FACE_OUTER_BOUND('',#14619,.T.);
#8699=FACE_OUTER_BOUND('',#14620,.T.);
#8700=FACE_OUTER_BOUND('',#14621,.T.);
#8701=FACE_OUTER_BOUND('',#14622,.T.);
#8702=FACE_OUTER_BOUND('',#14623,.T.);
#8703=FACE_OUTER_BOUND('',#14624,.T.);
#8704=FACE_OUTER_BOUND('',#14625,.T.);
#8705=FACE_OUTER_BOUND('',#14626,.T.);
#8706=FACE_OUTER_BOUND('',#14627,.T.);
#8707=FACE_OUTER_BOUND('',#14628,.T.);
#8708=FACE_OUTER_BOUND('',#14629,.T.);
#8709=FACE_OUTER_BOUND('',#14630,.T.);
#8710=FACE_OUTER_BOUND('',#14631,.T.);
#8711=FACE_OUTER_BOUND('',#14632,.T.);
#8712=FACE_OUTER_BOUND('',#14633,.T.);
#8713=FACE_OUTER_BOUND('',#14634,.T.);
#8714=FACE_OUTER_BOUND('',#14635,.T.);
#8715=FACE_OUTER_BOUND('',#14636,.T.);
#8716=FACE_OUTER_BOUND('',#14637,.T.);
#8717=FACE_OUTER_BOUND('',#14638,.T.);
#8718=FACE_OUTER_BOUND('',#14639,.T.);
#8719=FACE_OUTER_BOUND('',#14640,.T.);
#8720=FACE_OUTER_BOUND('',#14641,.T.);
#8721=FACE_OUTER_BOUND('',#14642,.T.);
#8722=FACE_OUTER_BOUND('',#14643,.T.);
#8723=FACE_OUTER_BOUND('',#14644,.T.);
#8724=FACE_OUTER_BOUND('',#14645,.T.);
#8725=FACE_OUTER_BOUND('',#14646,.T.);
#8726=FACE_OUTER_BOUND('',#14647,.T.);
#8727=FACE_OUTER_BOUND('',#14648,.T.);
#8728=FACE_OUTER_BOUND('',#14650,.T.);
#8729=FACE_OUTER_BOUND('',#14651,.T.);
#8730=FACE_OUTER_BOUND('',#14652,.T.);
#8731=FACE_OUTER_BOUND('',#14653,.T.);
#8732=FACE_OUTER_BOUND('',#14654,.T.);
#8733=FACE_OUTER_BOUND('',#14655,.T.);
#8734=FACE_OUTER_BOUND('',#14656,.T.);
#8735=FACE_OUTER_BOUND('',#14657,.T.);
#8736=FACE_OUTER_BOUND('',#14658,.T.);
#8737=FACE_OUTER_BOUND('',#14659,.T.);
#8738=FACE_OUTER_BOUND('',#14660,.T.);
#8739=FACE_OUTER_BOUND('',#14661,.T.);
#8740=FACE_OUTER_BOUND('',#14662,.T.);
#8741=FACE_OUTER_BOUND('',#14663,.T.);
#8742=FACE_OUTER_BOUND('',#14665,.T.);
#8743=FACE_OUTER_BOUND('',#14666,.T.);
#8744=FACE_OUTER_BOUND('',#14667,.T.);
#8745=FACE_OUTER_BOUND('',#14668,.T.);
#8746=FACE_OUTER_BOUND('',#14669,.T.);
#8747=FACE_OUTER_BOUND('',#14670,.T.);
#8748=FACE_OUTER_BOUND('',#14671,.T.);
#8749=FACE_OUTER_BOUND('',#14672,.T.);
#8750=FACE_OUTER_BOUND('',#14673,.T.);
#8751=FACE_OUTER_BOUND('',#14674,.T.);
#8752=FACE_OUTER_BOUND('',#14675,.T.);
#8753=FACE_OUTER_BOUND('',#14676,.T.);
#8754=FACE_OUTER_BOUND('',#14677,.T.);
#8755=FACE_OUTER_BOUND('',#14678,.T.);
#8756=FACE_OUTER_BOUND('',#14679,.T.);
#8757=FACE_OUTER_BOUND('',#14680,.T.);
#8758=FACE_OUTER_BOUND('',#14681,.T.);
#8759=FACE_OUTER_BOUND('',#14682,.T.);
#8760=FACE_OUTER_BOUND('',#14683,.T.);
#8761=FACE_OUTER_BOUND('',#14684,.T.);
#8762=FACE_OUTER_BOUND('',#14685,.T.);
#8763=FACE_OUTER_BOUND('',#14686,.T.);
#8764=FACE_OUTER_BOUND('',#14687,.T.);
#8765=FACE_OUTER_BOUND('',#14688,.T.);
#8766=FACE_OUTER_BOUND('',#14689,.T.);
#8767=FACE_OUTER_BOUND('',#14690,.T.);
#8768=FACE_OUTER_BOUND('',#14691,.T.);
#8769=FACE_OUTER_BOUND('',#14692,.T.);
#8770=FACE_OUTER_BOUND('',#14693,.T.);
#8771=FACE_OUTER_BOUND('',#14694,.T.);
#8772=FACE_OUTER_BOUND('',#14695,.T.);
#8773=FACE_OUTER_BOUND('',#14696,.T.);
#8774=FACE_OUTER_BOUND('',#14697,.T.);
#8775=FACE_OUTER_BOUND('',#14698,.T.);
#8776=FACE_OUTER_BOUND('',#14699,.T.);
#8777=FACE_OUTER_BOUND('',#14700,.T.);
#8778=FACE_OUTER_BOUND('',#14701,.T.);
#8779=FACE_OUTER_BOUND('',#14702,.T.);
#8780=FACE_OUTER_BOUND('',#14703,.T.);
#8781=FACE_OUTER_BOUND('',#14704,.T.);
#8782=FACE_OUTER_BOUND('',#14705,.T.);
#8783=FACE_OUTER_BOUND('',#14706,.T.);
#8784=FACE_OUTER_BOUND('',#14707,.T.);
#8785=FACE_OUTER_BOUND('',#14708,.T.);
#8786=FACE_OUTER_BOUND('',#14709,.T.);
#8787=FACE_OUTER_BOUND('',#14710,.T.);
#8788=FACE_OUTER_BOUND('',#14711,.T.);
#8789=FACE_OUTER_BOUND('',#14712,.T.);
#8790=FACE_OUTER_BOUND('',#14713,.T.);
#8791=FACE_OUTER_BOUND('',#14714,.T.);
#8792=FACE_OUTER_BOUND('',#14715,.T.);
#8793=FACE_OUTER_BOUND('',#14716,.T.);
#8794=FACE_OUTER_BOUND('',#14717,.T.);
#8795=FACE_OUTER_BOUND('',#14718,.T.);
#8796=FACE_OUTER_BOUND('',#14719,.T.);
#8797=FACE_OUTER_BOUND('',#14720,.T.);
#8798=FACE_OUTER_BOUND('',#14721,.T.);
#8799=FACE_OUTER_BOUND('',#14722,.T.);
#8800=FACE_OUTER_BOUND('',#14723,.T.);
#8801=FACE_OUTER_BOUND('',#14724,.T.);
#8802=FACE_OUTER_BOUND('',#14725,.T.);
#8803=FACE_OUTER_BOUND('',#14726,.T.);
#8804=FACE_OUTER_BOUND('',#14727,.T.);
#8805=FACE_OUTER_BOUND('',#14728,.T.);
#8806=FACE_OUTER_BOUND('',#14729,.T.);
#8807=FACE_OUTER_BOUND('',#14730,.T.);
#8808=FACE_OUTER_BOUND('',#14731,.T.);
#8809=FACE_OUTER_BOUND('',#14732,.T.);
#8810=FACE_OUTER_BOUND('',#14733,.T.);
#8811=FACE_OUTER_BOUND('',#14734,.T.);
#8812=FACE_OUTER_BOUND('',#14735,.T.);
#8813=FACE_OUTER_BOUND('',#14736,.T.);
#8814=FACE_OUTER_BOUND('',#14737,.T.);
#8815=FACE_OUTER_BOUND('',#14738,.T.);
#8816=FACE_OUTER_BOUND('',#14739,.T.);
#8817=FACE_OUTER_BOUND('',#14740,.T.);
#8818=FACE_OUTER_BOUND('',#14741,.T.);
#8819=FACE_OUTER_BOUND('',#14742,.T.);
#8820=FACE_OUTER_BOUND('',#14743,.T.);
#8821=FACE_OUTER_BOUND('',#14744,.T.);
#8822=FACE_OUTER_BOUND('',#14745,.T.);
#8823=FACE_OUTER_BOUND('',#14746,.T.);
#8824=FACE_OUTER_BOUND('',#14747,.T.);
#8825=FACE_OUTER_BOUND('',#14748,.T.);
#8826=FACE_OUTER_BOUND('',#14749,.T.);
#8827=FACE_OUTER_BOUND('',#14750,.T.);
#8828=FACE_OUTER_BOUND('',#14751,.T.);
#8829=FACE_OUTER_BOUND('',#14752,.T.);
#8830=FACE_OUTER_BOUND('',#14753,.T.);
#8831=FACE_OUTER_BOUND('',#14754,.T.);
#8832=FACE_OUTER_BOUND('',#14755,.T.);
#8833=FACE_OUTER_BOUND('',#14756,.T.);
#8834=FACE_OUTER_BOUND('',#14757,.T.);
#8835=FACE_OUTER_BOUND('',#14758,.T.);
#8836=FACE_OUTER_BOUND('',#14759,.T.);
#8837=FACE_OUTER_BOUND('',#14760,.T.);
#8838=FACE_OUTER_BOUND('',#14761,.T.);
#8839=FACE_OUTER_BOUND('',#14762,.T.);
#8840=FACE_OUTER_BOUND('',#14763,.T.);
#8841=FACE_OUTER_BOUND('',#14764,.T.);
#8842=FACE_OUTER_BOUND('',#14765,.T.);
#8843=FACE_OUTER_BOUND('',#14766,.T.);
#8844=FACE_OUTER_BOUND('',#14767,.T.);
#8845=FACE_OUTER_BOUND('',#14768,.T.);
#8846=FACE_OUTER_BOUND('',#14769,.T.);
#8847=FACE_OUTER_BOUND('',#14770,.T.);
#8848=FACE_OUTER_BOUND('',#14771,.T.);
#8849=FACE_OUTER_BOUND('',#14772,.T.);
#8850=FACE_OUTER_BOUND('',#14773,.T.);
#8851=FACE_OUTER_BOUND('',#14774,.T.);
#8852=FACE_OUTER_BOUND('',#14775,.T.);
#8853=FACE_OUTER_BOUND('',#14776,.T.);
#8854=FACE_OUTER_BOUND('',#14777,.T.);
#8855=FACE_OUTER_BOUND('',#14778,.T.);
#8856=FACE_OUTER_BOUND('',#14779,.T.);
#8857=FACE_OUTER_BOUND('',#14780,.T.);
#8858=FACE_OUTER_BOUND('',#14781,.T.);
#8859=FACE_OUTER_BOUND('',#14782,.T.);
#8860=FACE_OUTER_BOUND('',#14783,.T.);
#8861=FACE_OUTER_BOUND('',#14784,.T.);
#8862=FACE_OUTER_BOUND('',#14785,.T.);
#8863=FACE_OUTER_BOUND('',#14786,.T.);
#8864=FACE_OUTER_BOUND('',#14787,.T.);
#8865=FACE_OUTER_BOUND('',#14788,.T.);
#8866=FACE_OUTER_BOUND('',#14789,.T.);
#8867=FACE_OUTER_BOUND('',#14790,.T.);
#8868=FACE_OUTER_BOUND('',#14791,.T.);
#8869=FACE_OUTER_BOUND('',#14792,.T.);
#8870=FACE_OUTER_BOUND('',#14793,.T.);
#8871=FACE_OUTER_BOUND('',#14794,.T.);
#8872=FACE_OUTER_BOUND('',#14795,.T.);
#8873=FACE_OUTER_BOUND('',#14796,.T.);
#8874=FACE_OUTER_BOUND('',#14797,.T.);
#8875=FACE_OUTER_BOUND('',#14798,.T.);
#8876=FACE_OUTER_BOUND('',#14799,.T.);
#8877=FACE_OUTER_BOUND('',#14800,.T.);
#8878=FACE_OUTER_BOUND('',#14801,.T.);
#8879=FACE_OUTER_BOUND('',#14802,.T.);
#8880=FACE_OUTER_BOUND('',#14803,.T.);
#8881=FACE_OUTER_BOUND('',#14804,.T.);
#8882=FACE_OUTER_BOUND('',#14805,.T.);
#8883=FACE_OUTER_BOUND('',#14806,.T.);
#8884=FACE_OUTER_BOUND('',#14807,.T.);
#8885=FACE_OUTER_BOUND('',#14808,.T.);
#8886=FACE_OUTER_BOUND('',#14809,.T.);
#8887=FACE_OUTER_BOUND('',#14810,.T.);
#8888=FACE_OUTER_BOUND('',#14811,.T.);
#8889=FACE_OUTER_BOUND('',#14812,.T.);
#8890=FACE_OUTER_BOUND('',#14813,.T.);
#8891=FACE_OUTER_BOUND('',#14814,.T.);
#8892=FACE_OUTER_BOUND('',#14815,.T.);
#8893=FACE_OUTER_BOUND('',#14816,.T.);
#8894=FACE_OUTER_BOUND('',#14817,.T.);
#8895=FACE_OUTER_BOUND('',#14818,.T.);
#8896=FACE_OUTER_BOUND('',#14819,.T.);
#8897=FACE_OUTER_BOUND('',#14820,.T.);
#8898=FACE_OUTER_BOUND('',#14821,.T.);
#8899=FACE_OUTER_BOUND('',#14822,.T.);
#8900=FACE_OUTER_BOUND('',#14823,.T.);
#8901=FACE_OUTER_BOUND('',#14824,.T.);
#8902=FACE_OUTER_BOUND('',#14825,.T.);
#8903=FACE_OUTER_BOUND('',#14826,.T.);
#8904=FACE_OUTER_BOUND('',#14827,.T.);
#8905=FACE_OUTER_BOUND('',#14828,.T.);
#8906=FACE_OUTER_BOUND('',#14829,.T.);
#8907=FACE_OUTER_BOUND('',#14830,.T.);
#8908=FACE_OUTER_BOUND('',#14831,.T.);
#8909=FACE_OUTER_BOUND('',#14832,.T.);
#8910=FACE_OUTER_BOUND('',#14833,.T.);
#8911=FACE_OUTER_BOUND('',#14834,.T.);
#8912=FACE_OUTER_BOUND('',#14835,.T.);
#8913=FACE_OUTER_BOUND('',#14836,.T.);
#8914=FACE_OUTER_BOUND('',#14837,.T.);
#8915=FACE_OUTER_BOUND('',#14838,.T.);
#8916=FACE_OUTER_BOUND('',#14839,.T.);
#8917=FACE_OUTER_BOUND('',#14840,.T.);
#8918=FACE_OUTER_BOUND('',#14841,.T.);
#8919=FACE_OUTER_BOUND('',#14842,.T.);
#8920=FACE_OUTER_BOUND('',#14843,.T.);
#8921=FACE_OUTER_BOUND('',#14844,.T.);
#8922=FACE_OUTER_BOUND('',#14845,.T.);
#8923=FACE_OUTER_BOUND('',#14846,.T.);
#8924=FACE_OUTER_BOUND('',#14847,.T.);
#8925=FACE_OUTER_BOUND('',#14848,.T.);
#8926=FACE_OUTER_BOUND('',#14849,.T.);
#8927=FACE_OUTER_BOUND('',#14850,.T.);
#8928=FACE_OUTER_BOUND('',#14851,.T.);
#8929=FACE_OUTER_BOUND('',#14852,.T.);
#8930=FACE_OUTER_BOUND('',#14853,.T.);
#8931=FACE_OUTER_BOUND('',#14854,.T.);
#8932=FACE_OUTER_BOUND('',#14855,.T.);
#8933=FACE_OUTER_BOUND('',#14856,.T.);
#8934=FACE_OUTER_BOUND('',#14857,.T.);
#8935=FACE_OUTER_BOUND('',#14858,.T.);
#8936=FACE_OUTER_BOUND('',#14859,.T.);
#8937=FACE_OUTER_BOUND('',#14860,.T.);
#8938=FACE_OUTER_BOUND('',#14861,.T.);
#8939=FACE_OUTER_BOUND('',#14862,.T.);
#8940=FACE_OUTER_BOUND('',#14863,.T.);
#8941=FACE_OUTER_BOUND('',#14864,.T.);
#8942=FACE_OUTER_BOUND('',#14865,.T.);
#8943=FACE_OUTER_BOUND('',#14866,.T.);
#8944=FACE_OUTER_BOUND('',#14867,.T.);
#8945=FACE_OUTER_BOUND('',#14868,.T.);
#8946=FACE_OUTER_BOUND('',#14869,.T.);
#8947=FACE_OUTER_BOUND('',#14870,.T.);
#8948=FACE_OUTER_BOUND('',#14871,.T.);
#8949=FACE_OUTER_BOUND('',#14872,.T.);
#8950=FACE_OUTER_BOUND('',#14873,.T.);
#8951=FACE_OUTER_BOUND('',#14874,.T.);
#8952=FACE_OUTER_BOUND('',#14875,.T.);
#8953=FACE_OUTER_BOUND('',#14876,.T.);
#8954=FACE_OUTER_BOUND('',#14877,.T.);
#8955=FACE_OUTER_BOUND('',#14878,.T.);
#8956=FACE_OUTER_BOUND('',#14879,.T.);
#8957=FACE_OUTER_BOUND('',#14880,.T.);
#8958=FACE_OUTER_BOUND('',#14881,.T.);
#8959=FACE_OUTER_BOUND('',#14882,.T.);
#8960=FACE_OUTER_BOUND('',#14883,.T.);
#8961=FACE_OUTER_BOUND('',#14884,.T.);
#8962=FACE_OUTER_BOUND('',#14885,.T.);
#8963=FACE_OUTER_BOUND('',#14886,.T.);
#8964=FACE_OUTER_BOUND('',#14887,.T.);
#8965=FACE_OUTER_BOUND('',#14888,.T.);
#8966=FACE_OUTER_BOUND('',#14889,.T.);
#8967=FACE_OUTER_BOUND('',#14890,.T.);
#8968=FACE_OUTER_BOUND('',#14891,.T.);
#8969=FACE_OUTER_BOUND('',#14892,.T.);
#8970=FACE_OUTER_BOUND('',#14893,.T.);
#8971=FACE_OUTER_BOUND('',#14894,.T.);
#8972=FACE_OUTER_BOUND('',#14895,.T.);
#8973=FACE_OUTER_BOUND('',#14896,.T.);
#8974=FACE_OUTER_BOUND('',#14897,.T.);
#8975=FACE_OUTER_BOUND('',#14898,.T.);
#8976=FACE_OUTER_BOUND('',#14899,.T.);
#8977=FACE_OUTER_BOUND('',#14900,.T.);
#8978=FACE_OUTER_BOUND('',#14901,.T.);
#8979=FACE_OUTER_BOUND('',#14902,.T.);
#8980=FACE_OUTER_BOUND('',#14903,.T.);
#8981=FACE_OUTER_BOUND('',#14904,.T.);
#8982=FACE_OUTER_BOUND('',#14905,.T.);
#8983=FACE_OUTER_BOUND('',#14906,.T.);
#8984=FACE_OUTER_BOUND('',#14907,.T.);
#8985=FACE_OUTER_BOUND('',#14908,.T.);
#8986=FACE_OUTER_BOUND('',#14909,.T.);
#8987=FACE_OUTER_BOUND('',#14910,.T.);
#8988=FACE_OUTER_BOUND('',#14911,.T.);
#8989=FACE_OUTER_BOUND('',#14912,.T.);
#8990=FACE_OUTER_BOUND('',#14913,.T.);
#8991=FACE_OUTER_BOUND('',#14914,.T.);
#8992=FACE_OUTER_BOUND('',#14915,.T.);
#8993=FACE_OUTER_BOUND('',#14916,.T.);
#8994=FACE_OUTER_BOUND('',#14917,.T.);
#8995=FACE_OUTER_BOUND('',#14918,.T.);
#8996=FACE_OUTER_BOUND('',#14919,.T.);
#8997=FACE_OUTER_BOUND('',#14920,.T.);
#8998=FACE_OUTER_BOUND('',#14921,.T.);
#8999=FACE_OUTER_BOUND('',#14922,.T.);
#9000=FACE_OUTER_BOUND('',#14923,.T.);
#9001=FACE_OUTER_BOUND('',#14924,.T.);
#9002=FACE_OUTER_BOUND('',#14925,.T.);
#9003=FACE_OUTER_BOUND('',#14926,.T.);
#9004=FACE_OUTER_BOUND('',#14927,.T.);
#9005=FACE_OUTER_BOUND('',#14928,.T.);
#9006=FACE_OUTER_BOUND('',#14929,.T.);
#9007=FACE_OUTER_BOUND('',#14930,.T.);
#9008=FACE_OUTER_BOUND('',#14931,.T.);
#9009=FACE_OUTER_BOUND('',#14932,.T.);
#9010=FACE_OUTER_BOUND('',#14933,.T.);
#9011=FACE_OUTER_BOUND('',#14934,.T.);
#9012=FACE_OUTER_BOUND('',#14935,.T.);
#9013=FACE_OUTER_BOUND('',#14936,.T.);
#9014=FACE_OUTER_BOUND('',#14937,.T.);
#9015=FACE_OUTER_BOUND('',#14938,.T.);
#9016=FACE_OUTER_BOUND('',#14939,.T.);
#9017=FACE_OUTER_BOUND('',#14940,.T.);
#9018=FACE_OUTER_BOUND('',#14941,.T.);
#9019=FACE_OUTER_BOUND('',#14942,.T.);
#9020=FACE_OUTER_BOUND('',#14943,.T.);
#9021=FACE_OUTER_BOUND('',#14944,.T.);
#9022=FACE_OUTER_BOUND('',#14945,.T.);
#9023=FACE_OUTER_BOUND('',#14946,.T.);
#9024=FACE_OUTER_BOUND('',#14947,.T.);
#9025=FACE_OUTER_BOUND('',#14948,.T.);
#9026=FACE_OUTER_BOUND('',#14949,.T.);
#9027=FACE_OUTER_BOUND('',#14950,.T.);
#9028=FACE_OUTER_BOUND('',#14951,.T.);
#9029=FACE_OUTER_BOUND('',#14952,.T.);
#9030=FACE_OUTER_BOUND('',#14953,.T.);
#9031=FACE_OUTER_BOUND('',#14954,.T.);
#9032=FACE_OUTER_BOUND('',#14955,.T.);
#9033=FACE_OUTER_BOUND('',#14956,.T.);
#9034=FACE_OUTER_BOUND('',#14957,.T.);
#9035=FACE_OUTER_BOUND('',#14958,.T.);
#9036=FACE_OUTER_BOUND('',#14959,.T.);
#9037=FACE_OUTER_BOUND('',#14960,.T.);
#9038=FACE_OUTER_BOUND('',#14961,.T.);
#9039=FACE_OUTER_BOUND('',#14962,.T.);
#9040=FACE_OUTER_BOUND('',#14963,.T.);
#9041=FACE_OUTER_BOUND('',#14964,.T.);
#9042=FACE_OUTER_BOUND('',#14965,.T.);
#9043=FACE_OUTER_BOUND('',#14966,.T.);
#9044=FACE_OUTER_BOUND('',#14967,.T.);
#9045=FACE_OUTER_BOUND('',#14968,.T.);
#9046=FACE_OUTER_BOUND('',#14969,.T.);
#9047=FACE_OUTER_BOUND('',#14970,.T.);
#9048=FACE_OUTER_BOUND('',#14971,.T.);
#9049=FACE_OUTER_BOUND('',#14972,.T.);
#9050=FACE_OUTER_BOUND('',#14973,.T.);
#9051=FACE_OUTER_BOUND('',#14974,.T.);
#9052=FACE_OUTER_BOUND('',#14975,.T.);
#9053=FACE_OUTER_BOUND('',#14976,.T.);
#9054=FACE_OUTER_BOUND('',#14977,.T.);
#9055=FACE_OUTER_BOUND('',#14978,.T.);
#9056=FACE_OUTER_BOUND('',#14979,.T.);
#9057=FACE_OUTER_BOUND('',#14980,.T.);
#9058=FACE_OUTER_BOUND('',#14981,.T.);
#9059=FACE_OUTER_BOUND('',#14982,.T.);
#9060=FACE_OUTER_BOUND('',#14983,.T.);
#9061=FACE_OUTER_BOUND('',#14984,.T.);
#9062=FACE_OUTER_BOUND('',#14985,.T.);
#9063=FACE_OUTER_BOUND('',#14986,.T.);
#9064=FACE_OUTER_BOUND('',#14987,.T.);
#9065=FACE_OUTER_BOUND('',#14988,.T.);
#9066=FACE_OUTER_BOUND('',#14989,.T.);
#9067=FACE_OUTER_BOUND('',#14990,.T.);
#9068=FACE_OUTER_BOUND('',#14991,.T.);
#9069=FACE_OUTER_BOUND('',#14992,.T.);
#9070=FACE_OUTER_BOUND('',#14993,.T.);
#9071=FACE_OUTER_BOUND('',#14994,.T.);
#9072=FACE_OUTER_BOUND('',#14995,.T.);
#9073=FACE_OUTER_BOUND('',#14996,.T.);
#9074=FACE_OUTER_BOUND('',#14997,.T.);
#9075=FACE_OUTER_BOUND('',#14998,.T.);
#9076=FACE_OUTER_BOUND('',#14999,.T.);
#9077=FACE_OUTER_BOUND('',#15000,.T.);
#9078=FACE_OUTER_BOUND('',#15001,.T.);
#9079=FACE_OUTER_BOUND('',#15002,.T.);
#9080=FACE_OUTER_BOUND('',#15003,.T.);
#9081=FACE_OUTER_BOUND('',#15004,.T.);
#9082=FACE_OUTER_BOUND('',#15005,.T.);
#9083=FACE_OUTER_BOUND('',#15006,.T.);
#9084=FACE_OUTER_BOUND('',#15007,.T.);
#9085=FACE_OUTER_BOUND('',#15008,.T.);
#9086=FACE_OUTER_BOUND('',#15009,.T.);
#9087=FACE_OUTER_BOUND('',#15010,.T.);
#9088=FACE_OUTER_BOUND('',#15011,.T.);
#9089=FACE_OUTER_BOUND('',#15012,.T.);
#9090=FACE_OUTER_BOUND('',#15013,.T.);
#9091=FACE_OUTER_BOUND('',#15014,.T.);
#9092=FACE_OUTER_BOUND('',#15015,.T.);
#9093=FACE_OUTER_BOUND('',#15016,.T.);
#9094=FACE_OUTER_BOUND('',#15017,.T.);
#9095=FACE_OUTER_BOUND('',#15018,.T.);
#9096=FACE_OUTER_BOUND('',#15019,.T.);
#9097=FACE_OUTER_BOUND('',#15020,.T.);
#9098=FACE_OUTER_BOUND('',#15021,.T.);
#9099=FACE_OUTER_BOUND('',#15022,.T.);
#9100=FACE_OUTER_BOUND('',#15023,.T.);
#9101=FACE_OUTER_BOUND('',#15024,.T.);
#9102=FACE_OUTER_BOUND('',#15025,.T.);
#9103=FACE_OUTER_BOUND('',#15026,.T.);
#9104=FACE_OUTER_BOUND('',#15027,.T.);
#9105=FACE_OUTER_BOUND('',#15028,.T.);
#9106=FACE_OUTER_BOUND('',#15029,.T.);
#9107=FACE_OUTER_BOUND('',#15030,.T.);
#9108=FACE_OUTER_BOUND('',#15031,.T.);
#9109=FACE_OUTER_BOUND('',#15032,.T.);
#9110=FACE_OUTER_BOUND('',#15033,.T.);
#9111=FACE_OUTER_BOUND('',#15034,.T.);
#9112=FACE_OUTER_BOUND('',#15035,.T.);
#9113=FACE_OUTER_BOUND('',#15036,.T.);
#9114=FACE_OUTER_BOUND('',#15037,.T.);
#9115=FACE_OUTER_BOUND('',#15038,.T.);
#9116=FACE_OUTER_BOUND('',#15039,.T.);
#9117=FACE_OUTER_BOUND('',#15040,.T.);
#9118=FACE_OUTER_BOUND('',#15041,.T.);
#9119=FACE_OUTER_BOUND('',#15042,.T.);
#9120=FACE_OUTER_BOUND('',#15043,.T.);
#9121=FACE_OUTER_BOUND('',#15044,.T.);
#9122=FACE_OUTER_BOUND('',#15045,.T.);
#9123=FACE_OUTER_BOUND('',#15046,.T.);
#9124=FACE_OUTER_BOUND('',#15047,.T.);
#9125=FACE_OUTER_BOUND('',#15048,.T.);
#9126=FACE_OUTER_BOUND('',#15049,.T.);
#9127=FACE_OUTER_BOUND('',#15050,.T.);
#9128=FACE_OUTER_BOUND('',#15051,.T.);
#9129=FACE_OUTER_BOUND('',#15052,.T.);
#9130=FACE_OUTER_BOUND('',#15053,.T.);
#9131=FACE_OUTER_BOUND('',#15054,.T.);
#9132=FACE_OUTER_BOUND('',#15055,.T.);
#9133=FACE_OUTER_BOUND('',#15056,.T.);
#9134=FACE_OUTER_BOUND('',#15057,.T.);
#9135=FACE_OUTER_BOUND('',#15058,.T.);
#9136=FACE_OUTER_BOUND('',#15059,.T.);
#9137=FACE_OUTER_BOUND('',#15060,.T.);
#9138=FACE_OUTER_BOUND('',#15061,.T.);
#9139=FACE_OUTER_BOUND('',#15062,.T.);
#9140=FACE_OUTER_BOUND('',#15063,.T.);
#9141=FACE_OUTER_BOUND('',#15064,.T.);
#9142=FACE_OUTER_BOUND('',#15065,.T.);
#9143=FACE_OUTER_BOUND('',#15066,.T.);
#9144=FACE_OUTER_BOUND('',#15067,.T.);
#9145=FACE_OUTER_BOUND('',#15068,.T.);
#9146=FACE_OUTER_BOUND('',#15069,.T.);
#9147=FACE_OUTER_BOUND('',#15070,.T.);
#9148=FACE_OUTER_BOUND('',#15071,.T.);
#9149=FACE_OUTER_BOUND('',#15072,.T.);
#9150=FACE_OUTER_BOUND('',#15073,.T.);
#9151=FACE_OUTER_BOUND('',#15074,.T.);
#9152=FACE_OUTER_BOUND('',#15075,.T.);
#9153=FACE_OUTER_BOUND('',#15076,.T.);
#9154=FACE_OUTER_BOUND('',#15077,.T.);
#9155=FACE_OUTER_BOUND('',#15078,.T.);
#9156=FACE_OUTER_BOUND('',#15079,.T.);
#9157=FACE_OUTER_BOUND('',#15080,.T.);
#9158=FACE_OUTER_BOUND('',#15081,.T.);
#9159=FACE_OUTER_BOUND('',#15082,.T.);
#9160=FACE_OUTER_BOUND('',#15083,.T.);
#9161=FACE_OUTER_BOUND('',#15084,.T.);
#9162=FACE_OUTER_BOUND('',#15085,.T.);
#9163=FACE_OUTER_BOUND('',#15086,.T.);
#9164=FACE_OUTER_BOUND('',#15087,.T.);
#9165=FACE_OUTER_BOUND('',#15088,.T.);
#9166=FACE_OUTER_BOUND('',#15089,.T.);
#9167=FACE_OUTER_BOUND('',#15090,.T.);
#9168=FACE_OUTER_BOUND('',#15091,.T.);
#9169=FACE_OUTER_BOUND('',#15092,.T.);
#9170=FACE_OUTER_BOUND('',#15093,.T.);
#9171=FACE_OUTER_BOUND('',#15094,.T.);
#9172=FACE_OUTER_BOUND('',#15095,.T.);
#9173=FACE_OUTER_BOUND('',#15096,.T.);
#9174=FACE_OUTER_BOUND('',#15097,.T.);
#9175=FACE_OUTER_BOUND('',#15098,.T.);
#9176=FACE_OUTER_BOUND('',#15099,.T.);
#9177=FACE_OUTER_BOUND('',#15100,.T.);
#9178=FACE_OUTER_BOUND('',#15101,.T.);
#9179=FACE_OUTER_BOUND('',#15102,.T.);
#9180=FACE_OUTER_BOUND('',#15103,.T.);
#9181=FACE_OUTER_BOUND('',#15104,.T.);
#9182=FACE_OUTER_BOUND('',#15105,.T.);
#9183=FACE_OUTER_BOUND('',#15106,.T.);
#9184=FACE_OUTER_BOUND('',#15107,.T.);
#9185=FACE_OUTER_BOUND('',#15108,.T.);
#9186=FACE_OUTER_BOUND('',#15109,.T.);
#9187=FACE_OUTER_BOUND('',#15110,.T.);
#9188=FACE_OUTER_BOUND('',#15111,.T.);
#9189=FACE_OUTER_BOUND('',#15112,.T.);
#9190=FACE_OUTER_BOUND('',#15113,.T.);
#9191=FACE_OUTER_BOUND('',#15114,.T.);
#9192=FACE_OUTER_BOUND('',#15115,.T.);
#9193=FACE_OUTER_BOUND('',#15116,.T.);
#9194=FACE_OUTER_BOUND('',#15117,.T.);
#9195=FACE_OUTER_BOUND('',#15118,.T.);
#9196=FACE_OUTER_BOUND('',#15119,.T.);
#9197=FACE_OUTER_BOUND('',#15120,.T.);
#9198=FACE_OUTER_BOUND('',#15121,.T.);
#9199=FACE_OUTER_BOUND('',#15122,.T.);
#9200=FACE_OUTER_BOUND('',#15123,.T.);
#9201=FACE_OUTER_BOUND('',#15124,.T.);
#9202=FACE_OUTER_BOUND('',#15125,.T.);
#9203=FACE_OUTER_BOUND('',#15126,.T.);
#9204=FACE_OUTER_BOUND('',#15127,.T.);
#9205=FACE_OUTER_BOUND('',#15128,.T.);
#9206=FACE_OUTER_BOUND('',#15129,.T.);
#9207=FACE_OUTER_BOUND('',#15130,.T.);
#9208=FACE_OUTER_BOUND('',#15131,.T.);
#9209=FACE_OUTER_BOUND('',#15132,.T.);
#9210=FACE_OUTER_BOUND('',#15133,.T.);
#9211=FACE_OUTER_BOUND('',#15134,.T.);
#9212=FACE_OUTER_BOUND('',#15135,.T.);
#9213=FACE_OUTER_BOUND('',#15136,.T.);
#9214=FACE_OUTER_BOUND('',#15137,.T.);
#9215=FACE_OUTER_BOUND('',#15138,.T.);
#9216=FACE_OUTER_BOUND('',#15139,.T.);
#9217=FACE_OUTER_BOUND('',#15140,.T.);
#9218=FACE_OUTER_BOUND('',#15141,.T.);
#9219=FACE_OUTER_BOUND('',#15142,.T.);
#9220=FACE_OUTER_BOUND('',#15143,.T.);
#9221=FACE_OUTER_BOUND('',#15144,.T.);
#9222=FACE_OUTER_BOUND('',#15145,.T.);
#9223=FACE_OUTER_BOUND('',#15146,.T.);
#9224=FACE_OUTER_BOUND('',#15147,.T.);
#9225=FACE_OUTER_BOUND('',#15148,.T.);
#9226=FACE_OUTER_BOUND('',#15149,.T.);
#9227=FACE_OUTER_BOUND('',#15150,.T.);
#9228=FACE_OUTER_BOUND('',#15151,.T.);
#9229=FACE_OUTER_BOUND('',#15152,.T.);
#9230=FACE_OUTER_BOUND('',#15153,.T.);
#9231=FACE_OUTER_BOUND('',#15154,.T.);
#9232=FACE_OUTER_BOUND('',#15155,.T.);
#9233=FACE_OUTER_BOUND('',#15156,.T.);
#9234=FACE_OUTER_BOUND('',#15157,.T.);
#9235=FACE_OUTER_BOUND('',#15158,.T.);
#9236=FACE_OUTER_BOUND('',#15159,.T.);
#9237=FACE_OUTER_BOUND('',#15160,.T.);
#9238=FACE_OUTER_BOUND('',#15161,.T.);
#9239=FACE_OUTER_BOUND('',#15162,.T.);
#9240=FACE_OUTER_BOUND('',#15163,.T.);
#9241=FACE_OUTER_BOUND('',#15164,.T.);
#9242=FACE_OUTER_BOUND('',#15165,.T.);
#9243=FACE_OUTER_BOUND('',#15166,.T.);
#9244=FACE_OUTER_BOUND('',#15167,.T.);
#9245=FACE_OUTER_BOUND('',#15168,.T.);
#9246=FACE_OUTER_BOUND('',#15169,.T.);
#9247=FACE_OUTER_BOUND('',#15170,.T.);
#9248=FACE_OUTER_BOUND('',#15171,.T.);
#9249=FACE_OUTER_BOUND('',#15172,.T.);
#9250=FACE_OUTER_BOUND('',#15173,.T.);
#9251=FACE_OUTER_BOUND('',#15174,.T.);
#9252=FACE_OUTER_BOUND('',#15175,.T.);
#9253=FACE_OUTER_BOUND('',#15176,.T.);
#9254=FACE_OUTER_BOUND('',#15177,.T.);
#9255=FACE_OUTER_BOUND('',#15178,.T.);
#9256=FACE_OUTER_BOUND('',#15179,.T.);
#9257=FACE_OUTER_BOUND('',#15180,.T.);
#9258=FACE_OUTER_BOUND('',#15181,.T.);
#9259=FACE_OUTER_BOUND('',#15182,.T.);
#9260=FACE_OUTER_BOUND('',#15183,.T.);
#9261=FACE_OUTER_BOUND('',#15184,.T.);
#9262=FACE_OUTER_BOUND('',#15185,.T.);
#9263=FACE_OUTER_BOUND('',#15186,.T.);
#9264=FACE_OUTER_BOUND('',#15187,.T.);
#9265=FACE_OUTER_BOUND('',#15188,.T.);
#9266=FACE_OUTER_BOUND('',#15189,.T.);
#9267=FACE_OUTER_BOUND('',#15190,.T.);
#9268=FACE_OUTER_BOUND('',#15191,.T.);
#9269=FACE_OUTER_BOUND('',#15192,.T.);
#9270=FACE_OUTER_BOUND('',#15193,.T.);
#9271=FACE_OUTER_BOUND('',#15194,.T.);
#9272=FACE_OUTER_BOUND('',#15195,.T.);
#9273=FACE_OUTER_BOUND('',#15196,.T.);
#9274=FACE_OUTER_BOUND('',#15197,.T.);
#9275=FACE_OUTER_BOUND('',#15198,.T.);
#9276=FACE_OUTER_BOUND('',#15199,.T.);
#9277=FACE_OUTER_BOUND('',#15200,.T.);
#9278=FACE_OUTER_BOUND('',#15201,.T.);
#9279=FACE_OUTER_BOUND('',#15202,.T.);
#9280=FACE_OUTER_BOUND('',#15203,.T.);
#9281=FACE_OUTER_BOUND('',#15204,.T.);
#9282=FACE_OUTER_BOUND('',#15205,.T.);
#9283=FACE_OUTER_BOUND('',#15206,.T.);
#9284=FACE_OUTER_BOUND('',#15207,.T.);
#9285=FACE_OUTER_BOUND('',#15208,.T.);
#9286=FACE_OUTER_BOUND('',#15209,.T.);
#9287=FACE_OUTER_BOUND('',#15210,.T.);
#9288=FACE_OUTER_BOUND('',#15211,.T.);
#9289=FACE_OUTER_BOUND('',#15212,.T.);
#9290=FACE_OUTER_BOUND('',#15213,.T.);
#9291=FACE_OUTER_BOUND('',#15214,.T.);
#9292=FACE_OUTER_BOUND('',#15215,.T.);
#9293=FACE_OUTER_BOUND('',#15216,.T.);
#9294=FACE_OUTER_BOUND('',#15217,.T.);
#9295=FACE_OUTER_BOUND('',#15218,.T.);
#9296=FACE_OUTER_BOUND('',#15219,.T.);
#9297=FACE_OUTER_BOUND('',#15220,.T.);
#9298=FACE_OUTER_BOUND('',#15221,.T.);
#9299=FACE_OUTER_BOUND('',#15222,.T.);
#9300=FACE_OUTER_BOUND('',#15223,.T.);
#9301=FACE_OUTER_BOUND('',#15224,.T.);
#9302=FACE_OUTER_BOUND('',#15225,.T.);
#9303=FACE_OUTER_BOUND('',#15226,.T.);
#9304=FACE_OUTER_BOUND('',#15227,.T.);
#9305=FACE_OUTER_BOUND('',#15228,.T.);
#9306=FACE_OUTER_BOUND('',#15229,.T.);
#9307=FACE_OUTER_BOUND('',#15230,.T.);
#9308=FACE_OUTER_BOUND('',#15231,.T.);
#9309=FACE_OUTER_BOUND('',#15232,.T.);
#9310=FACE_OUTER_BOUND('',#15233,.T.);
#9311=FACE_OUTER_BOUND('',#15234,.T.);
#9312=FACE_OUTER_BOUND('',#15235,.T.);
#9313=FACE_OUTER_BOUND('',#15236,.T.);
#9314=FACE_OUTER_BOUND('',#15237,.T.);
#9315=FACE_OUTER_BOUND('',#15238,.T.);
#9316=FACE_OUTER_BOUND('',#15239,.T.);
#9317=FACE_OUTER_BOUND('',#15240,.T.);
#9318=FACE_OUTER_BOUND('',#15241,.T.);
#9319=FACE_OUTER_BOUND('',#15242,.T.);
#9320=FACE_OUTER_BOUND('',#15243,.T.);
#9321=FACE_OUTER_BOUND('',#15244,.T.);
#9322=FACE_OUTER_BOUND('',#15245,.T.);
#9323=FACE_OUTER_BOUND('',#15246,.T.);
#9324=FACE_OUTER_BOUND('',#15247,.T.);
#9325=FACE_OUTER_BOUND('',#15248,.T.);
#9326=FACE_OUTER_BOUND('',#15249,.T.);
#9327=FACE_OUTER_BOUND('',#15250,.T.);
#9328=FACE_OUTER_BOUND('',#15251,.T.);
#9329=FACE_OUTER_BOUND('',#15252,.T.);
#9330=FACE_OUTER_BOUND('',#15253,.T.);
#9331=FACE_OUTER_BOUND('',#15254,.T.);
#9332=FACE_OUTER_BOUND('',#15255,.T.);
#9333=FACE_OUTER_BOUND('',#15256,.T.);
#9334=FACE_OUTER_BOUND('',#15257,.T.);
#9335=FACE_OUTER_BOUND('',#15258,.T.);
#9336=FACE_OUTER_BOUND('',#15259,.T.);
#9337=FACE_OUTER_BOUND('',#15260,.T.);
#9338=FACE_OUTER_BOUND('',#15261,.T.);
#9339=FACE_OUTER_BOUND('',#15262,.T.);
#9340=FACE_OUTER_BOUND('',#15263,.T.);
#9341=FACE_OUTER_BOUND('',#15264,.T.);
#9342=FACE_OUTER_BOUND('',#15265,.T.);
#9343=FACE_OUTER_BOUND('',#15266,.T.);
#9344=FACE_OUTER_BOUND('',#15267,.T.);
#9345=FACE_OUTER_BOUND('',#15268,.T.);
#9346=FACE_OUTER_BOUND('',#15269,.T.);
#9347=FACE_OUTER_BOUND('',#15270,.T.);
#9348=FACE_OUTER_BOUND('',#15271,.T.);
#9349=FACE_OUTER_BOUND('',#15272,.T.);
#9350=FACE_OUTER_BOUND('',#15273,.T.);
#9351=FACE_OUTER_BOUND('',#15274,.T.);
#9352=FACE_OUTER_BOUND('',#15275,.T.);
#9353=FACE_OUTER_BOUND('',#15276,.T.);
#9354=FACE_OUTER_BOUND('',#15277,.T.);
#9355=FACE_OUTER_BOUND('',#15278,.T.);
#9356=FACE_OUTER_BOUND('',#15279,.T.);
#9357=FACE_OUTER_BOUND('',#15280,.T.);
#9358=FACE_OUTER_BOUND('',#15281,.T.);
#9359=FACE_OUTER_BOUND('',#15282,.T.);
#9360=FACE_OUTER_BOUND('',#15283,.T.);
#9361=FACE_OUTER_BOUND('',#15284,.T.);
#9362=FACE_OUTER_BOUND('',#15285,.T.);
#9363=FACE_OUTER_BOUND('',#15286,.T.);
#9364=FACE_OUTER_BOUND('',#15287,.T.);
#9365=FACE_OUTER_BOUND('',#15288,.T.);
#9366=FACE_OUTER_BOUND('',#15289,.T.);
#9367=FACE_OUTER_BOUND('',#15290,.T.);
#9368=FACE_OUTER_BOUND('',#15291,.T.);
#9369=FACE_OUTER_BOUND('',#15292,.T.);
#9370=FACE_OUTER_BOUND('',#15293,.T.);
#9371=FACE_OUTER_BOUND('',#15294,.T.);
#9372=FACE_OUTER_BOUND('',#15295,.T.);
#9373=FACE_OUTER_BOUND('',#15296,.T.);
#9374=FACE_OUTER_BOUND('',#15297,.T.);
#9375=FACE_OUTER_BOUND('',#15298,.T.);
#9376=FACE_OUTER_BOUND('',#15299,.T.);
#9377=FACE_OUTER_BOUND('',#15300,.T.);
#9378=FACE_OUTER_BOUND('',#15301,.T.);
#9379=FACE_OUTER_BOUND('',#15302,.T.);
#9380=FACE_OUTER_BOUND('',#15303,.T.);
#9381=FACE_OUTER_BOUND('',#15304,.T.);
#9382=FACE_OUTER_BOUND('',#15305,.T.);
#9383=FACE_OUTER_BOUND('',#15306,.T.);
#9384=FACE_OUTER_BOUND('',#15307,.T.);
#9385=FACE_OUTER_BOUND('',#15308,.T.);
#9386=FACE_OUTER_BOUND('',#15309,.T.);
#9387=FACE_OUTER_BOUND('',#15310,.T.);
#9388=FACE_OUTER_BOUND('',#15311,.T.);
#9389=FACE_OUTER_BOUND('',#15312,.T.);
#9390=FACE_OUTER_BOUND('',#15313,.T.);
#9391=FACE_OUTER_BOUND('',#15314,.T.);
#9392=FACE_OUTER_BOUND('',#15315,.T.);
#9393=FACE_OUTER_BOUND('',#15316,.T.);
#9394=FACE_OUTER_BOUND('',#15317,.T.);
#9395=FACE_OUTER_BOUND('',#15318,.T.);
#9396=FACE_OUTER_BOUND('',#15319,.T.);
#9397=FACE_OUTER_BOUND('',#15320,.T.);
#9398=FACE_OUTER_BOUND('',#15321,.T.);
#9399=FACE_OUTER_BOUND('',#15322,.T.);
#9400=FACE_OUTER_BOUND('',#15323,.T.);
#9401=FACE_OUTER_BOUND('',#15324,.T.);
#9402=FACE_OUTER_BOUND('',#15325,.T.);
#9403=FACE_OUTER_BOUND('',#15326,.T.);
#9404=FACE_OUTER_BOUND('',#15327,.T.);
#9405=FACE_OUTER_BOUND('',#15328,.T.);
#9406=FACE_OUTER_BOUND('',#15329,.T.);
#9407=FACE_OUTER_BOUND('',#15330,.T.);
#9408=FACE_OUTER_BOUND('',#15331,.T.);
#9409=FACE_OUTER_BOUND('',#15332,.T.);
#9410=FACE_OUTER_BOUND('',#15333,.T.);
#9411=FACE_OUTER_BOUND('',#15334,.T.);
#9412=FACE_OUTER_BOUND('',#15335,.T.);
#9413=FACE_OUTER_BOUND('',#15336,.T.);
#9414=FACE_OUTER_BOUND('',#15337,.T.);
#9415=FACE_OUTER_BOUND('',#15338,.T.);
#9416=FACE_OUTER_BOUND('',#15339,.T.);
#9417=FACE_OUTER_BOUND('',#15340,.T.);
#9418=FACE_OUTER_BOUND('',#15341,.T.);
#9419=FACE_OUTER_BOUND('',#15342,.T.);
#9420=FACE_OUTER_BOUND('',#15343,.T.);
#9421=FACE_OUTER_BOUND('',#15344,.T.);
#9422=FACE_OUTER_BOUND('',#15345,.T.);
#9423=FACE_OUTER_BOUND('',#15346,.T.);
#9424=FACE_OUTER_BOUND('',#15347,.T.);
#9425=FACE_OUTER_BOUND('',#15348,.T.);
#9426=FACE_OUTER_BOUND('',#15349,.T.);
#9427=FACE_OUTER_BOUND('',#15350,.T.);
#9428=FACE_OUTER_BOUND('',#15351,.T.);
#9429=FACE_OUTER_BOUND('',#15352,.T.);
#9430=FACE_OUTER_BOUND('',#15353,.T.);
#9431=FACE_OUTER_BOUND('',#15354,.T.);
#9432=FACE_OUTER_BOUND('',#15355,.T.);
#9433=FACE_OUTER_BOUND('',#15356,.T.);
#9434=FACE_OUTER_BOUND('',#15357,.T.);
#9435=FACE_OUTER_BOUND('',#15358,.T.);
#9436=FACE_OUTER_BOUND('',#15359,.T.);
#9437=FACE_OUTER_BOUND('',#15360,.T.);
#9438=FACE_OUTER_BOUND('',#15361,.T.);
#9439=FACE_OUTER_BOUND('',#15362,.T.);
#9440=FACE_OUTER_BOUND('',#15363,.T.);
#9441=FACE_OUTER_BOUND('',#15364,.T.);
#9442=FACE_OUTER_BOUND('',#15365,.T.);
#9443=FACE_OUTER_BOUND('',#15366,.T.);
#9444=FACE_OUTER_BOUND('',#15367,.T.);
#9445=FACE_OUTER_BOUND('',#15368,.T.);
#9446=FACE_OUTER_BOUND('',#15369,.T.);
#9447=FACE_OUTER_BOUND('',#15370,.T.);
#9448=FACE_OUTER_BOUND('',#15371,.T.);
#9449=FACE_OUTER_BOUND('',#15372,.T.);
#9450=FACE_OUTER_BOUND('',#15373,.T.);
#9451=FACE_OUTER_BOUND('',#15374,.T.);
#9452=FACE_OUTER_BOUND('',#15375,.T.);
#9453=FACE_OUTER_BOUND('',#15376,.T.);
#9454=FACE_OUTER_BOUND('',#15377,.T.);
#9455=FACE_OUTER_BOUND('',#15378,.T.);
#9456=FACE_OUTER_BOUND('',#15379,.T.);
#9457=FACE_OUTER_BOUND('',#15380,.T.);
#9458=FACE_OUTER_BOUND('',#15381,.T.);
#9459=FACE_OUTER_BOUND('',#15382,.T.);
#9460=FACE_OUTER_BOUND('',#15383,.T.);
#9461=FACE_OUTER_BOUND('',#15384,.T.);
#9462=FACE_OUTER_BOUND('',#15385,.T.);
#9463=FACE_OUTER_BOUND('',#15386,.T.);
#9464=FACE_OUTER_BOUND('',#15387,.T.);
#9465=FACE_OUTER_BOUND('',#15388,.T.);
#9466=FACE_OUTER_BOUND('',#15389,.T.);
#9467=FACE_OUTER_BOUND('',#15390,.T.);
#9468=FACE_OUTER_BOUND('',#15391,.T.);
#9469=FACE_OUTER_BOUND('',#15392,.T.);
#9470=FACE_OUTER_BOUND('',#15393,.T.);
#9471=FACE_OUTER_BOUND('',#15394,.T.);
#9472=FACE_OUTER_BOUND('',#15395,.T.);
#9473=FACE_OUTER_BOUND('',#15396,.T.);
#9474=FACE_OUTER_BOUND('',#15397,.T.);
#9475=FACE_OUTER_BOUND('',#15398,.T.);
#9476=FACE_OUTER_BOUND('',#15399,.T.);
#9477=FACE_OUTER_BOUND('',#15400,.T.);
#9478=FACE_OUTER_BOUND('',#15401,.T.);
#9479=FACE_OUTER_BOUND('',#15402,.T.);
#9480=FACE_OUTER_BOUND('',#15403,.T.);
#9481=FACE_OUTER_BOUND('',#15404,.T.);
#9482=FACE_OUTER_BOUND('',#15405,.T.);
#9483=FACE_OUTER_BOUND('',#15406,.T.);
#9484=FACE_OUTER_BOUND('',#15407,.T.);
#9485=FACE_OUTER_BOUND('',#15408,.T.);
#9486=FACE_OUTER_BOUND('',#15409,.T.);
#9487=FACE_OUTER_BOUND('',#15410,.T.);
#9488=FACE_OUTER_BOUND('',#15411,.T.);
#9489=FACE_OUTER_BOUND('',#15412,.T.);
#9490=FACE_OUTER_BOUND('',#15413,.T.);
#9491=FACE_OUTER_BOUND('',#15414,.T.);
#9492=FACE_OUTER_BOUND('',#15415,.T.);
#9493=FACE_OUTER_BOUND('',#15416,.T.);
#9494=FACE_OUTER_BOUND('',#15417,.T.);
#9495=FACE_OUTER_BOUND('',#15418,.T.);
#9496=FACE_OUTER_BOUND('',#15419,.T.);
#9497=FACE_OUTER_BOUND('',#15420,.T.);
#9498=FACE_OUTER_BOUND('',#15421,.T.);
#9499=FACE_OUTER_BOUND('',#15422,.T.);
#9500=FACE_OUTER_BOUND('',#15423,.T.);
#9501=FACE_OUTER_BOUND('',#15424,.T.);
#9502=FACE_OUTER_BOUND('',#15425,.T.);
#9503=FACE_OUTER_BOUND('',#15426,.T.);
#9504=FACE_OUTER_BOUND('',#15427,.T.);
#9505=FACE_OUTER_BOUND('',#15428,.T.);
#9506=FACE_OUTER_BOUND('',#15429,.T.);
#9507=FACE_OUTER_BOUND('',#15430,.T.);
#9508=FACE_OUTER_BOUND('',#15431,.T.);
#9509=FACE_OUTER_BOUND('',#15432,.T.);
#9510=FACE_OUTER_BOUND('',#15433,.T.);
#9511=FACE_OUTER_BOUND('',#15434,.T.);
#9512=FACE_OUTER_BOUND('',#15435,.T.);
#9513=FACE_OUTER_BOUND('',#15436,.T.);
#9514=FACE_OUTER_BOUND('',#15437,.T.);
#9515=FACE_OUTER_BOUND('',#15438,.T.);
#9516=FACE_OUTER_BOUND('',#15439,.T.);
#9517=FACE_OUTER_BOUND('',#15440,.T.);
#9518=FACE_OUTER_BOUND('',#15441,.T.);
#9519=FACE_OUTER_BOUND('',#15442,.T.);
#9520=FACE_OUTER_BOUND('',#15443,.T.);
#9521=FACE_OUTER_BOUND('',#15444,.T.);
#9522=FACE_OUTER_BOUND('',#15445,.T.);
#9523=FACE_OUTER_BOUND('',#15446,.T.);
#9524=FACE_OUTER_BOUND('',#15447,.T.);
#9525=FACE_OUTER_BOUND('',#15448,.T.);
#9526=FACE_OUTER_BOUND('',#15449,.T.);
#9527=FACE_OUTER_BOUND('',#15450,.T.);
#9528=FACE_OUTER_BOUND('',#15451,.T.);
#9529=FACE_OUTER_BOUND('',#15452,.T.);
#9530=FACE_OUTER_BOUND('',#15453,.T.);
#9531=FACE_OUTER_BOUND('',#15454,.T.);
#9532=FACE_OUTER_BOUND('',#15455,.T.);
#9533=FACE_OUTER_BOUND('',#15456,.T.);
#9534=FACE_OUTER_BOUND('',#15457,.T.);
#9535=FACE_OUTER_BOUND('',#15458,.T.);
#9536=FACE_OUTER_BOUND('',#15459,.T.);
#9537=FACE_OUTER_BOUND('',#15460,.T.);
#9538=FACE_OUTER_BOUND('',#15461,.T.);
#9539=FACE_OUTER_BOUND('',#15462,.T.);
#9540=FACE_OUTER_BOUND('',#15463,.T.);
#9541=FACE_OUTER_BOUND('',#15464,.T.);
#9542=FACE_OUTER_BOUND('',#15465,.T.);
#9543=FACE_OUTER_BOUND('',#15466,.T.);
#9544=FACE_OUTER_BOUND('',#15467,.T.);
#9545=FACE_OUTER_BOUND('',#15468,.T.);
#9546=FACE_OUTER_BOUND('',#15469,.T.);
#9547=FACE_OUTER_BOUND('',#15470,.T.);
#9548=FACE_OUTER_BOUND('',#15471,.T.);
#9549=FACE_OUTER_BOUND('',#15472,.T.);
#9550=FACE_OUTER_BOUND('',#15473,.T.);
#9551=FACE_OUTER_BOUND('',#15474,.T.);
#9552=FACE_OUTER_BOUND('',#15475,.T.);
#9553=FACE_OUTER_BOUND('',#15476,.T.);
#9554=FACE_OUTER_BOUND('',#15477,.T.);
#9555=FACE_OUTER_BOUND('',#15478,.T.);
#9556=FACE_OUTER_BOUND('',#15479,.T.);
#9557=FACE_OUTER_BOUND('',#15480,.T.);
#9558=FACE_OUTER_BOUND('',#15481,.T.);
#9559=FACE_OUTER_BOUND('',#15482,.T.);
#9560=FACE_OUTER_BOUND('',#15483,.T.);
#9561=FACE_OUTER_BOUND('',#15484,.T.);
#9562=FACE_OUTER_BOUND('',#15485,.T.);
#9563=FACE_OUTER_BOUND('',#15486,.T.);
#9564=FACE_OUTER_BOUND('',#15487,.T.);
#9565=FACE_OUTER_BOUND('',#15488,.T.);
#9566=FACE_OUTER_BOUND('',#15489,.T.);
#9567=FACE_OUTER_BOUND('',#15490,.T.);
#9568=FACE_OUTER_BOUND('',#15491,.T.);
#9569=FACE_OUTER_BOUND('',#15492,.T.);
#9570=FACE_OUTER_BOUND('',#15493,.T.);
#9571=FACE_OUTER_BOUND('',#15494,.T.);
#9572=FACE_OUTER_BOUND('',#15495,.T.);
#9573=FACE_OUTER_BOUND('',#15496,.T.);
#9574=FACE_OUTER_BOUND('',#15497,.T.);
#9575=FACE_OUTER_BOUND('',#15498,.T.);
#9576=FACE_OUTER_BOUND('',#15499,.T.);
#9577=FACE_OUTER_BOUND('',#15500,.T.);
#9578=FACE_OUTER_BOUND('',#15501,.T.);
#9579=FACE_OUTER_BOUND('',#15502,.T.);
#9580=FACE_OUTER_BOUND('',#15503,.T.);
#9581=FACE_OUTER_BOUND('',#15504,.T.);
#9582=FACE_OUTER_BOUND('',#15505,.T.);
#9583=FACE_OUTER_BOUND('',#15506,.T.);
#9584=FACE_OUTER_BOUND('',#15507,.T.);
#9585=FACE_OUTER_BOUND('',#15508,.T.);
#9586=FACE_OUTER_BOUND('',#15509,.T.);
#9587=FACE_OUTER_BOUND('',#15510,.T.);
#9588=FACE_OUTER_BOUND('',#15511,.T.);
#9589=FACE_OUTER_BOUND('',#15512,.T.);
#9590=FACE_OUTER_BOUND('',#15513,.T.);
#9591=FACE_OUTER_BOUND('',#15514,.T.);
#9592=FACE_OUTER_BOUND('',#15515,.T.);
#9593=FACE_OUTER_BOUND('',#15516,.T.);
#9594=FACE_OUTER_BOUND('',#15517,.T.);
#9595=FACE_OUTER_BOUND('',#15518,.T.);
#9596=FACE_OUTER_BOUND('',#15519,.T.);
#9597=FACE_OUTER_BOUND('',#15520,.T.);
#9598=FACE_OUTER_BOUND('',#15521,.T.);
#9599=FACE_OUTER_BOUND('',#15522,.T.);
#9600=FACE_OUTER_BOUND('',#15523,.T.);
#9601=FACE_OUTER_BOUND('',#15524,.T.);
#9602=FACE_OUTER_BOUND('',#15525,.T.);
#9603=FACE_OUTER_BOUND('',#15526,.T.);
#9604=FACE_OUTER_BOUND('',#15527,.T.);
#9605=FACE_OUTER_BOUND('',#15528,.T.);
#9606=FACE_OUTER_BOUND('',#15529,.T.);
#9607=FACE_OUTER_BOUND('',#15530,.T.);
#9608=FACE_OUTER_BOUND('',#15531,.T.);
#9609=FACE_OUTER_BOUND('',#15532,.T.);
#9610=FACE_OUTER_BOUND('',#15533,.T.);
#9611=FACE_OUTER_BOUND('',#15534,.T.);
#9612=FACE_OUTER_BOUND('',#15535,.T.);
#9613=FACE_OUTER_BOUND('',#15536,.T.);
#9614=FACE_OUTER_BOUND('',#15537,.T.);
#9615=FACE_OUTER_BOUND('',#15538,.T.);
#9616=FACE_OUTER_BOUND('',#15539,.T.);
#9617=FACE_OUTER_BOUND('',#15540,.T.);
#9618=FACE_OUTER_BOUND('',#15541,.T.);
#9619=FACE_OUTER_BOUND('',#15542,.T.);
#9620=FACE_OUTER_BOUND('',#15543,.T.);
#9621=FACE_OUTER_BOUND('',#15544,.T.);
#9622=FACE_OUTER_BOUND('',#15545,.T.);
#9623=FACE_OUTER_BOUND('',#15546,.T.);
#9624=FACE_OUTER_BOUND('',#15547,.T.);
#9625=FACE_OUTER_BOUND('',#15548,.T.);
#9626=FACE_OUTER_BOUND('',#15549,.T.);
#9627=FACE_OUTER_BOUND('',#15550,.T.);
#9628=FACE_OUTER_BOUND('',#15551,.T.);
#9629=FACE_OUTER_BOUND('',#15552,.T.);
#9630=FACE_OUTER_BOUND('',#15553,.T.);
#9631=FACE_OUTER_BOUND('',#15554,.T.);
#9632=FACE_OUTER_BOUND('',#15555,.T.);
#9633=FACE_OUTER_BOUND('',#15556,.T.);
#9634=FACE_OUTER_BOUND('',#15557,.T.);
#9635=FACE_OUTER_BOUND('',#15558,.T.);
#9636=FACE_OUTER_BOUND('',#15559,.T.);
#9637=FACE_OUTER_BOUND('',#15560,.T.);
#9638=FACE_OUTER_BOUND('',#15561,.T.);
#9639=FACE_OUTER_BOUND('',#15562,.T.);
#9640=FACE_OUTER_BOUND('',#15563,.T.);
#9641=FACE_OUTER_BOUND('',#15564,.T.);
#9642=FACE_OUTER_BOUND('',#15565,.T.);
#9643=FACE_OUTER_BOUND('',#15566,.T.);
#9644=FACE_OUTER_BOUND('',#15567,.T.);
#9645=FACE_OUTER_BOUND('',#15568,.T.);
#9646=FACE_OUTER_BOUND('',#15569,.T.);
#9647=FACE_OUTER_BOUND('',#15570,.T.);
#9648=FACE_OUTER_BOUND('',#15571,.T.);
#9649=FACE_OUTER_BOUND('',#15572,.T.);
#9650=FACE_OUTER_BOUND('',#15573,.T.);
#9651=FACE_OUTER_BOUND('',#15574,.T.);
#9652=FACE_OUTER_BOUND('',#15575,.T.);
#9653=FACE_OUTER_BOUND('',#15576,.T.);
#9654=FACE_OUTER_BOUND('',#15577,.T.);
#9655=FACE_OUTER_BOUND('',#15578,.T.);
#9656=FACE_OUTER_BOUND('',#15579,.T.);
#9657=FACE_OUTER_BOUND('',#15580,.T.);
#9658=FACE_OUTER_BOUND('',#15581,.T.);
#9659=FACE_OUTER_BOUND('',#15582,.T.);
#9660=FACE_OUTER_BOUND('',#15583,.T.);
#9661=FACE_OUTER_BOUND('',#15584,.T.);
#9662=FACE_OUTER_BOUND('',#15585,.T.);
#9663=FACE_OUTER_BOUND('',#15586,.T.);
#9664=FACE_OUTER_BOUND('',#15587,.T.);
#9665=FACE_OUTER_BOUND('',#15588,.T.);
#9666=FACE_OUTER_BOUND('',#15589,.T.);
#9667=FACE_OUTER_BOUND('',#15590,.T.);
#9668=FACE_OUTER_BOUND('',#15591,.T.);
#9669=FACE_OUTER_BOUND('',#15592,.T.);
#9670=FACE_OUTER_BOUND('',#15593,.T.);
#9671=FACE_OUTER_BOUND('',#15594,.T.);
#9672=FACE_OUTER_BOUND('',#15595,.T.);
#9673=FACE_OUTER_BOUND('',#15596,.T.);
#9674=FACE_OUTER_BOUND('',#15597,.T.);
#9675=FACE_OUTER_BOUND('',#15598,.T.);
#9676=FACE_OUTER_BOUND('',#15599,.T.);
#9677=FACE_OUTER_BOUND('',#15600,.T.);
#9678=FACE_OUTER_BOUND('',#15601,.T.);
#9679=FACE_OUTER_BOUND('',#15602,.T.);
#9680=FACE_OUTER_BOUND('',#15603,.T.);
#9681=FACE_OUTER_BOUND('',#15604,.T.);
#9682=FACE_OUTER_BOUND('',#15605,.T.);
#9683=FACE_OUTER_BOUND('',#15606,.T.);
#9684=FACE_OUTER_BOUND('',#15607,.T.);
#9685=FACE_OUTER_BOUND('',#15608,.T.);
#9686=FACE_OUTER_BOUND('',#15609,.T.);
#9687=FACE_OUTER_BOUND('',#15610,.T.);
#9688=FACE_OUTER_BOUND('',#15611,.T.);
#9689=FACE_OUTER_BOUND('',#15612,.T.);
#9690=FACE_OUTER_BOUND('',#15613,.T.);
#9691=FACE_OUTER_BOUND('',#15614,.T.);
#9692=FACE_OUTER_BOUND('',#15615,.T.);
#9693=FACE_OUTER_BOUND('',#15616,.T.);
#9694=FACE_OUTER_BOUND('',#15617,.T.);
#9695=FACE_OUTER_BOUND('',#15618,.T.);
#9696=FACE_OUTER_BOUND('',#15619,.T.);
#9697=FACE_OUTER_BOUND('',#15620,.T.);
#9698=FACE_OUTER_BOUND('',#15621,.T.);
#9699=FACE_OUTER_BOUND('',#15622,.T.);
#9700=FACE_OUTER_BOUND('',#15623,.T.);
#9701=FACE_OUTER_BOUND('',#15624,.T.);
#9702=FACE_OUTER_BOUND('',#15625,.T.);
#9703=FACE_OUTER_BOUND('',#15626,.T.);
#9704=FACE_OUTER_BOUND('',#15627,.T.);
#9705=FACE_OUTER_BOUND('',#15628,.T.);
#9706=FACE_OUTER_BOUND('',#15629,.T.);
#9707=FACE_OUTER_BOUND('',#15630,.T.);
#9708=FACE_OUTER_BOUND('',#15631,.T.);
#9709=FACE_OUTER_BOUND('',#15632,.T.);
#9710=FACE_OUTER_BOUND('',#15633,.T.);
#9711=FACE_OUTER_BOUND('',#15634,.T.);
#9712=FACE_OUTER_BOUND('',#15635,.T.);
#9713=FACE_OUTER_BOUND('',#15636,.T.);
#9714=FACE_OUTER_BOUND('',#15637,.T.);
#9715=FACE_OUTER_BOUND('',#15638,.T.);
#9716=FACE_OUTER_BOUND('',#15639,.T.);
#9717=FACE_OUTER_BOUND('',#15640,.T.);
#9718=FACE_OUTER_BOUND('',#15641,.T.);
#9719=FACE_OUTER_BOUND('',#15642,.T.);
#9720=FACE_OUTER_BOUND('',#15643,.T.);
#9721=FACE_OUTER_BOUND('',#15644,.T.);
#9722=FACE_OUTER_BOUND('',#15645,.T.);
#9723=FACE_OUTER_BOUND('',#15646,.T.);
#9724=FACE_OUTER_BOUND('',#15647,.T.);
#9725=FACE_OUTER_BOUND('',#15648,.T.);
#9726=FACE_OUTER_BOUND('',#15649,.T.);
#9727=FACE_OUTER_BOUND('',#15650,.T.);
#9728=FACE_OUTER_BOUND('',#15651,.T.);
#9729=FACE_OUTER_BOUND('',#15652,.T.);
#9730=FACE_OUTER_BOUND('',#15653,.T.);
#9731=FACE_OUTER_BOUND('',#15654,.T.);
#9732=FACE_OUTER_BOUND('',#15655,.T.);
#9733=FACE_OUTER_BOUND('',#15656,.T.);
#9734=FACE_OUTER_BOUND('',#15657,.T.);
#9735=FACE_OUTER_BOUND('',#15658,.T.);
#9736=FACE_OUTER_BOUND('',#15659,.T.);
#9737=FACE_OUTER_BOUND('',#15660,.T.);
#9738=FACE_OUTER_BOUND('',#15661,.T.);
#9739=FACE_OUTER_BOUND('',#15662,.T.);
#9740=FACE_OUTER_BOUND('',#15663,.T.);
#9741=FACE_OUTER_BOUND('',#15664,.T.);
#9742=FACE_OUTER_BOUND('',#15665,.T.);
#9743=FACE_OUTER_BOUND('',#15666,.T.);
#9744=FACE_OUTER_BOUND('',#15667,.T.);
#9745=FACE_OUTER_BOUND('',#15668,.T.);
#9746=FACE_OUTER_BOUND('',#15669,.T.);
#9747=FACE_OUTER_BOUND('',#15670,.T.);
#9748=FACE_OUTER_BOUND('',#15671,.T.);
#9749=FACE_OUTER_BOUND('',#15672,.T.);
#9750=FACE_OUTER_BOUND('',#15673,.T.);
#9751=FACE_OUTER_BOUND('',#15674,.T.);
#9752=FACE_OUTER_BOUND('',#15675,.T.);
#9753=FACE_OUTER_BOUND('',#15676,.T.);
#9754=FACE_OUTER_BOUND('',#15677,.T.);
#9755=FACE_OUTER_BOUND('',#15678,.T.);
#9756=FACE_OUTER_BOUND('',#15679,.T.);
#9757=FACE_OUTER_BOUND('',#15680,.T.);
#9758=FACE_OUTER_BOUND('',#15681,.T.);
#9759=FACE_OUTER_BOUND('',#15682,.T.);
#9760=FACE_OUTER_BOUND('',#15683,.T.);
#9761=FACE_OUTER_BOUND('',#15684,.T.);
#9762=FACE_OUTER_BOUND('',#15685,.T.);
#9763=FACE_OUTER_BOUND('',#15686,.T.);
#9764=FACE_OUTER_BOUND('',#15687,.T.);
#9765=FACE_OUTER_BOUND('',#15688,.T.);
#9766=FACE_OUTER_BOUND('',#15689,.T.);
#9767=FACE_OUTER_BOUND('',#15690,.T.);
#9768=FACE_OUTER_BOUND('',#15691,.T.);
#9769=FACE_OUTER_BOUND('',#15692,.T.);
#9770=FACE_OUTER_BOUND('',#15693,.T.);
#9771=FACE_OUTER_BOUND('',#15694,.T.);
#9772=FACE_OUTER_BOUND('',#15695,.T.);
#9773=FACE_OUTER_BOUND('',#15696,.T.);
#9774=FACE_OUTER_BOUND('',#15697,.T.);
#9775=FACE_OUTER_BOUND('',#15698,.T.);
#9776=FACE_OUTER_BOUND('',#15699,.T.);
#9777=FACE_OUTER_BOUND('',#15700,.T.);
#9778=FACE_OUTER_BOUND('',#15701,.T.);
#9779=FACE_OUTER_BOUND('',#15702,.T.);
#9780=FACE_OUTER_BOUND('',#15703,.T.);
#9781=FACE_OUTER_BOUND('',#15704,.T.);
#9782=FACE_OUTER_BOUND('',#15705,.T.);
#9783=FACE_OUTER_BOUND('',#15706,.T.);
#9784=FACE_OUTER_BOUND('',#15707,.T.);
#9785=FACE_OUTER_BOUND('',#15708,.T.);
#9786=FACE_OUTER_BOUND('',#15709,.T.);
#9787=FACE_OUTER_BOUND('',#15710,.T.);
#9788=FACE_OUTER_BOUND('',#15711,.T.);
#9789=FACE_OUTER_BOUND('',#15712,.T.);
#9790=FACE_OUTER_BOUND('',#15713,.T.);
#9791=FACE_OUTER_BOUND('',#15714,.T.);
#9792=FACE_OUTER_BOUND('',#15715,.T.);
#9793=FACE_OUTER_BOUND('',#15716,.T.);
#9794=FACE_OUTER_BOUND('',#15717,.T.);
#9795=FACE_OUTER_BOUND('',#15718,.T.);
#9796=FACE_OUTER_BOUND('',#15719,.T.);
#9797=FACE_OUTER_BOUND('',#15720,.T.);
#9798=FACE_OUTER_BOUND('',#15721,.T.);
#9799=FACE_OUTER_BOUND('',#15722,.T.);
#9800=FACE_OUTER_BOUND('',#15723,.T.);
#9801=FACE_OUTER_BOUND('',#15724,.T.);
#9802=FACE_OUTER_BOUND('',#15725,.T.);
#9803=FACE_OUTER_BOUND('',#15726,.T.);
#9804=FACE_OUTER_BOUND('',#15727,.T.);
#9805=FACE_OUTER_BOUND('',#15728,.T.);
#9806=FACE_OUTER_BOUND('',#15729,.T.);
#9807=FACE_OUTER_BOUND('',#15730,.T.);
#9808=FACE_OUTER_BOUND('',#15731,.T.);
#9809=FACE_OUTER_BOUND('',#15732,.T.);
#9810=FACE_OUTER_BOUND('',#15733,.T.);
#9811=FACE_OUTER_BOUND('',#15734,.T.);
#9812=FACE_OUTER_BOUND('',#15735,.T.);
#9813=FACE_OUTER_BOUND('',#15736,.T.);
#9814=FACE_OUTER_BOUND('',#15737,.T.);
#9815=FACE_OUTER_BOUND('',#15738,.T.);
#9816=FACE_OUTER_BOUND('',#15739,.T.);
#9817=FACE_OUTER_BOUND('',#15740,.T.);
#9818=FACE_OUTER_BOUND('',#15741,.T.);
#9819=FACE_OUTER_BOUND('',#15742,.T.);
#9820=FACE_OUTER_BOUND('',#15743,.T.);
#9821=FACE_OUTER_BOUND('',#15744,.T.);
#9822=FACE_OUTER_BOUND('',#15745,.T.);
#9823=FACE_OUTER_BOUND('',#15746,.T.);
#9824=FACE_OUTER_BOUND('',#15747,.T.);
#9825=FACE_OUTER_BOUND('',#15748,.T.);
#9826=FACE_OUTER_BOUND('',#15749,.T.);
#9827=FACE_OUTER_BOUND('',#15750,.T.);
#9828=FACE_OUTER_BOUND('',#15751,.T.);
#9829=FACE_OUTER_BOUND('',#15752,.T.);
#9830=FACE_OUTER_BOUND('',#15753,.T.);
#9831=FACE_OUTER_BOUND('',#15754,.T.);
#9832=FACE_OUTER_BOUND('',#15755,.T.);
#9833=FACE_OUTER_BOUND('',#15756,.T.);
#9834=FACE_OUTER_BOUND('',#15757,.T.);
#9835=FACE_OUTER_BOUND('',#15758,.T.);
#9836=FACE_OUTER_BOUND('',#15759,.T.);
#9837=FACE_OUTER_BOUND('',#15760,.T.);
#9838=FACE_OUTER_BOUND('',#15761,.T.);
#9839=FACE_OUTER_BOUND('',#15762,.T.);
#9840=FACE_OUTER_BOUND('',#15763,.T.);
#9841=FACE_OUTER_BOUND('',#15764,.T.);
#9842=FACE_OUTER_BOUND('',#15765,.T.);
#9843=FACE_OUTER_BOUND('',#15766,.T.);
#9844=FACE_OUTER_BOUND('',#15767,.T.);
#9845=FACE_OUTER_BOUND('',#15768,.T.);
#9846=FACE_OUTER_BOUND('',#15769,.T.);
#9847=FACE_OUTER_BOUND('',#15770,.T.);
#9848=FACE_OUTER_BOUND('',#15771,.T.);
#9849=FACE_OUTER_BOUND('',#15772,.T.);
#9850=FACE_OUTER_BOUND('',#15773,.T.);
#9851=FACE_OUTER_BOUND('',#15774,.T.);
#9852=FACE_OUTER_BOUND('',#15775,.T.);
#9853=FACE_OUTER_BOUND('',#15776,.T.);
#9854=FACE_OUTER_BOUND('',#15777,.T.);
#9855=FACE_OUTER_BOUND('',#15778,.T.);
#9856=FACE_OUTER_BOUND('',#15779,.T.);
#9857=FACE_OUTER_BOUND('',#15780,.T.);
#9858=FACE_OUTER_BOUND('',#15781,.T.);
#9859=FACE_OUTER_BOUND('',#15782,.T.);
#9860=FACE_OUTER_BOUND('',#15783,.T.);
#9861=FACE_OUTER_BOUND('',#15784,.T.);
#9862=FACE_OUTER_BOUND('',#15785,.T.);
#9863=FACE_OUTER_BOUND('',#15786,.T.);
#9864=FACE_OUTER_BOUND('',#15787,.T.);
#9865=FACE_OUTER_BOUND('',#15788,.T.);
#9866=FACE_OUTER_BOUND('',#15789,.T.);
#9867=FACE_OUTER_BOUND('',#15790,.T.);
#9868=FACE_OUTER_BOUND('',#15791,.T.);
#9869=FACE_OUTER_BOUND('',#15792,.T.);
#9870=FACE_OUTER_BOUND('',#15793,.T.);
#9871=FACE_OUTER_BOUND('',#15794,.T.);
#9872=FACE_OUTER_BOUND('',#15795,.T.);
#9873=FACE_OUTER_BOUND('',#15796,.T.);
#9874=FACE_OUTER_BOUND('',#15797,.T.);
#9875=FACE_OUTER_BOUND('',#15798,.T.);
#9876=FACE_OUTER_BOUND('',#15799,.T.);
#9877=FACE_OUTER_BOUND('',#15800,.T.);
#9878=FACE_OUTER_BOUND('',#15801,.T.);
#9879=FACE_OUTER_BOUND('',#15802,.T.);
#9880=FACE_OUTER_BOUND('',#15803,.T.);
#9881=FACE_OUTER_BOUND('',#15804,.T.);
#9882=FACE_OUTER_BOUND('',#15805,.T.);
#9883=FACE_OUTER_BOUND('',#15806,.T.);
#9884=FACE_OUTER_BOUND('',#15807,.T.);
#9885=FACE_OUTER_BOUND('',#15808,.T.);
#9886=FACE_OUTER_BOUND('',#15809,.T.);
#9887=FACE_OUTER_BOUND('',#15810,.T.);
#9888=FACE_OUTER_BOUND('',#15811,.T.);
#9889=FACE_OUTER_BOUND('',#15812,.T.);
#9890=FACE_OUTER_BOUND('',#15813,.T.);
#9891=FACE_OUTER_BOUND('',#15814,.T.);
#9892=FACE_OUTER_BOUND('',#15815,.T.);
#9893=FACE_OUTER_BOUND('',#15816,.T.);
#9894=FACE_OUTER_BOUND('',#15817,.T.);
#9895=FACE_OUTER_BOUND('',#15818,.T.);
#9896=FACE_OUTER_BOUND('',#15819,.T.);
#9897=FACE_OUTER_BOUND('',#15820,.T.);
#9898=FACE_OUTER_BOUND('',#15821,.T.);
#9899=FACE_OUTER_BOUND('',#15822,.T.);
#9900=FACE_OUTER_BOUND('',#15823,.T.);
#9901=FACE_OUTER_BOUND('',#15824,.T.);
#9902=FACE_OUTER_BOUND('',#15825,.T.);
#9903=FACE_OUTER_BOUND('',#15826,.T.);
#9904=FACE_OUTER_BOUND('',#15827,.T.);
#9905=FACE_OUTER_BOUND('',#15828,.T.);
#9906=FACE_OUTER_BOUND('',#15829,.T.);
#9907=FACE_OUTER_BOUND('',#15830,.T.);
#9908=FACE_OUTER_BOUND('',#15831,.T.);
#9909=FACE_OUTER_BOUND('',#15832,.T.);
#9910=FACE_OUTER_BOUND('',#15833,.T.);
#9911=FACE_OUTER_BOUND('',#15834,.T.);
#9912=FACE_OUTER_BOUND('',#15835,.T.);
#9913=FACE_OUTER_BOUND('',#15836,.T.);
#9914=FACE_OUTER_BOUND('',#15837,.T.);
#9915=FACE_OUTER_BOUND('',#15838,.T.);
#9916=FACE_OUTER_BOUND('',#15839,.T.);
#9917=FACE_OUTER_BOUND('',#15840,.T.);
#9918=FACE_OUTER_BOUND('',#15841,.T.);
#9919=FACE_OUTER_BOUND('',#15842,.T.);
#9920=FACE_OUTER_BOUND('',#15843,.T.);
#9921=FACE_OUTER_BOUND('',#15844,.T.);
#9922=FACE_OUTER_BOUND('',#15845,.T.);
#9923=FACE_OUTER_BOUND('',#15846,.T.);
#9924=FACE_OUTER_BOUND('',#15847,.T.);
#9925=FACE_OUTER_BOUND('',#15848,.T.);
#9926=FACE_OUTER_BOUND('',#15849,.T.);
#9927=FACE_OUTER_BOUND('',#15850,.T.);
#9928=FACE_OUTER_BOUND('',#15851,.T.);
#9929=FACE_OUTER_BOUND('',#15852,.T.);
#9930=FACE_OUTER_BOUND('',#15853,.T.);
#9931=FACE_OUTER_BOUND('',#15854,.T.);
#9932=FACE_OUTER_BOUND('',#15855,.T.);
#9933=FACE_OUTER_BOUND('',#15856,.T.);
#9934=FACE_OUTER_BOUND('',#15857,.T.);
#9935=FACE_OUTER_BOUND('',#15858,.T.);
#9936=FACE_OUTER_BOUND('',#15859,.T.);
#9937=FACE_OUTER_BOUND('',#15860,.T.);
#9938=FACE_OUTER_BOUND('',#15861,.T.);
#9939=FACE_OUTER_BOUND('',#15862,.T.);
#9940=FACE_OUTER_BOUND('',#15863,.T.);
#9941=FACE_OUTER_BOUND('',#15864,.T.);
#9942=FACE_OUTER_BOUND('',#15865,.T.);
#9943=FACE_OUTER_BOUND('',#15866,.T.);
#9944=FACE_OUTER_BOUND('',#15867,.T.);
#9945=FACE_OUTER_BOUND('',#15868,.T.);
#9946=FACE_OUTER_BOUND('',#15869,.T.);
#9947=FACE_OUTER_BOUND('',#15870,.T.);
#9948=FACE_OUTER_BOUND('',#15871,.T.);
#9949=FACE_OUTER_BOUND('',#15872,.T.);
#9950=FACE_OUTER_BOUND('',#15873,.T.);
#9951=FACE_OUTER_BOUND('',#15874,.T.);
#9952=FACE_OUTER_BOUND('',#15875,.T.);
#9953=FACE_OUTER_BOUND('',#15876,.T.);
#9954=FACE_OUTER_BOUND('',#15877,.T.);
#9955=FACE_OUTER_BOUND('',#15878,.T.);
#9956=FACE_OUTER_BOUND('',#15879,.T.);
#9957=FACE_OUTER_BOUND('',#15880,.T.);
#9958=FACE_OUTER_BOUND('',#15881,.T.);
#9959=FACE_OUTER_BOUND('',#15882,.T.);
#9960=FACE_OUTER_BOUND('',#15883,.T.);
#9961=FACE_OUTER_BOUND('',#15884,.T.);
#9962=FACE_OUTER_BOUND('',#15885,.T.);
#9963=FACE_OUTER_BOUND('',#15886,.T.);
#9964=FACE_OUTER_BOUND('',#15887,.T.);
#9965=FACE_OUTER_BOUND('',#15888,.T.);
#9966=FACE_OUTER_BOUND('',#15889,.T.);
#9967=FACE_OUTER_BOUND('',#15890,.T.);
#9968=FACE_OUTER_BOUND('',#15891,.T.);
#9969=FACE_OUTER_BOUND('',#15892,.T.);
#9970=FACE_OUTER_BOUND('',#15893,.T.);
#9971=FACE_OUTER_BOUND('',#15894,.T.);
#9972=FACE_OUTER_BOUND('',#15895,.T.);
#9973=FACE_OUTER_BOUND('',#15896,.T.);
#9974=FACE_OUTER_BOUND('',#15897,.T.);
#9975=FACE_OUTER_BOUND('',#15898,.T.);
#9976=FACE_OUTER_BOUND('',#15899,.T.);
#9977=FACE_OUTER_BOUND('',#15900,.T.);
#9978=FACE_OUTER_BOUND('',#15901,.T.);
#9979=FACE_OUTER_BOUND('',#15902,.T.);
#9980=FACE_OUTER_BOUND('',#15903,.T.);
#9981=FACE_OUTER_BOUND('',#15904,.T.);
#9982=FACE_OUTER_BOUND('',#15905,.T.);
#9983=FACE_OUTER_BOUND('',#15906,.T.);
#9984=FACE_OUTER_BOUND('',#15907,.T.);
#9985=FACE_OUTER_BOUND('',#15908,.T.);
#9986=FACE_OUTER_BOUND('',#15909,.T.);
#9987=FACE_OUTER_BOUND('',#15910,.T.);
#9988=FACE_OUTER_BOUND('',#15911,.T.);
#9989=FACE_OUTER_BOUND('',#15912,.T.);
#9990=FACE_OUTER_BOUND('',#15913,.T.);
#9991=FACE_OUTER_BOUND('',#15914,.T.);
#9992=FACE_OUTER_BOUND('',#15915,.T.);
#9993=FACE_OUTER_BOUND('',#15916,.T.);
#9994=FACE_OUTER_BOUND('',#15917,.T.);
#9995=FACE_OUTER_BOUND('',#15918,.T.);
#9996=FACE_OUTER_BOUND('',#15919,.T.);
#9997=FACE_OUTER_BOUND('',#15920,.T.);
#9998=FACE_OUTER_BOUND('',#15921,.T.);
#9999=FACE_OUTER_BOUND('',#15922,.T.);
#10000=FACE_OUTER_BOUND('',#15923,.T.);
#10001=FACE_OUTER_BOUND('',#15924,.T.);
#10002=FACE_OUTER_BOUND('',#15925,.T.);
#10003=FACE_OUTER_BOUND('',#15926,.T.);
#10004=FACE_OUTER_BOUND('',#15927,.T.);
#10005=FACE_OUTER_BOUND('',#15928,.T.);
#10006=FACE_OUTER_BOUND('',#15929,.T.);
#10007=FACE_OUTER_BOUND('',#15930,.T.);
#10008=FACE_OUTER_BOUND('',#15931,.T.);
#10009=FACE_OUTER_BOUND('',#15932,.T.);
#10010=FACE_OUTER_BOUND('',#15933,.T.);
#10011=FACE_OUTER_BOUND('',#15934,.T.);
#10012=FACE_OUTER_BOUND('',#15935,.T.);
#10013=FACE_OUTER_BOUND('',#15936,.T.);
#10014=FACE_OUTER_BOUND('',#15937,.T.);
#10015=FACE_OUTER_BOUND('',#15938,.T.);
#10016=FACE_OUTER_BOUND('',#15939,.T.);
#10017=FACE_OUTER_BOUND('',#15940,.T.);
#10018=FACE_OUTER_BOUND('',#15941,.T.);
#10019=FACE_OUTER_BOUND('',#15942,.T.);
#10020=FACE_OUTER_BOUND('',#15943,.T.);
#10021=FACE_OUTER_BOUND('',#15944,.T.);
#10022=FACE_OUTER_BOUND('',#15945,.T.);
#10023=FACE_OUTER_BOUND('',#15946,.T.);
#10024=FACE_OUTER_BOUND('',#15947,.T.);
#10025=FACE_OUTER_BOUND('',#15948,.T.);
#10026=FACE_OUTER_BOUND('',#15949,.T.);
#10027=FACE_OUTER_BOUND('',#15950,.T.);
#10028=FACE_OUTER_BOUND('',#15951,.T.);
#10029=FACE_OUTER_BOUND('',#15952,.T.);
#10030=FACE_OUTER_BOUND('',#15953,.T.);
#10031=FACE_OUTER_BOUND('',#15954,.T.);
#10032=FACE_OUTER_BOUND('',#15955,.T.);
#10033=FACE_OUTER_BOUND('',#15956,.T.);
#10034=FACE_OUTER_BOUND('',#15957,.T.);
#10035=FACE_OUTER_BOUND('',#15958,.T.);
#10036=FACE_OUTER_BOUND('',#15959,.T.);
#10037=FACE_OUTER_BOUND('',#15960,.T.);
#10038=FACE_OUTER_BOUND('',#15961,.T.);
#10039=FACE_OUTER_BOUND('',#15962,.T.);
#10040=FACE_OUTER_BOUND('',#15963,.T.);
#10041=FACE_OUTER_BOUND('',#15964,.T.);
#10042=FACE_OUTER_BOUND('',#15965,.T.);
#10043=FACE_OUTER_BOUND('',#15966,.T.);
#10044=FACE_OUTER_BOUND('',#15967,.T.);
#10045=FACE_OUTER_BOUND('',#15968,.T.);
#10046=FACE_OUTER_BOUND('',#15969,.T.);
#10047=FACE_OUTER_BOUND('',#15970,.T.);
#10048=FACE_OUTER_BOUND('',#15971,.T.);
#10049=FACE_OUTER_BOUND('',#15972,.T.);
#10050=FACE_OUTER_BOUND('',#15973,.T.);
#10051=FACE_OUTER_BOUND('',#15974,.T.);
#10052=FACE_OUTER_BOUND('',#15975,.T.);
#10053=FACE_OUTER_BOUND('',#15976,.T.);
#10054=FACE_OUTER_BOUND('',#15977,.T.);
#10055=FACE_OUTER_BOUND('',#15978,.T.);
#10056=FACE_OUTER_BOUND('',#15979,.T.);
#10057=FACE_OUTER_BOUND('',#15980,.T.);
#10058=FACE_OUTER_BOUND('',#15981,.T.);
#10059=FACE_OUTER_BOUND('',#15982,.T.);
#10060=FACE_OUTER_BOUND('',#15983,.T.);
#10061=FACE_OUTER_BOUND('',#15984,.T.);
#10062=FACE_OUTER_BOUND('',#15985,.T.);
#10063=FACE_OUTER_BOUND('',#15986,.T.);
#10064=FACE_OUTER_BOUND('',#15987,.T.);
#10065=FACE_OUTER_BOUND('',#15988,.T.);
#10066=FACE_OUTER_BOUND('',#15989,.T.);
#10067=FACE_OUTER_BOUND('',#15990,.T.);
#10068=FACE_OUTER_BOUND('',#15991,.T.);
#10069=FACE_OUTER_BOUND('',#15992,.T.);
#10070=FACE_OUTER_BOUND('',#15993,.T.);
#10071=FACE_OUTER_BOUND('',#15994,.T.);
#10072=FACE_OUTER_BOUND('',#15995,.T.);
#10073=FACE_OUTER_BOUND('',#15996,.T.);
#10074=FACE_OUTER_BOUND('',#15997,.T.);
#10075=FACE_OUTER_BOUND('',#15998,.T.);
#10076=FACE_OUTER_BOUND('',#15999,.T.);
#10077=FACE_OUTER_BOUND('',#16000,.T.);
#10078=FACE_OUTER_BOUND('',#16001,.T.);
#10079=FACE_OUTER_BOUND('',#16002,.T.);
#10080=FACE_OUTER_BOUND('',#16003,.T.);
#10081=FACE_OUTER_BOUND('',#16004,.T.);
#10082=FACE_OUTER_BOUND('',#16005,.T.);
#10083=FACE_OUTER_BOUND('',#16006,.T.);
#10084=FACE_OUTER_BOUND('',#16007,.T.);
#10085=FACE_OUTER_BOUND('',#16008,.T.);
#10086=FACE_OUTER_BOUND('',#16009,.T.);
#10087=FACE_OUTER_BOUND('',#16010,.T.);
#10088=FACE_OUTER_BOUND('',#16011,.T.);
#10089=FACE_OUTER_BOUND('',#16012,.T.);
#10090=FACE_OUTER_BOUND('',#16013,.T.);
#10091=FACE_OUTER_BOUND('',#16014,.T.);
#10092=FACE_OUTER_BOUND('',#16015,.T.);
#10093=FACE_OUTER_BOUND('',#16016,.T.);
#10094=FACE_OUTER_BOUND('',#16017,.T.);
#10095=FACE_OUTER_BOUND('',#16018,.T.);
#10096=FACE_OUTER_BOUND('',#16019,.T.);
#10097=FACE_OUTER_BOUND('',#16020,.T.);
#10098=FACE_OUTER_BOUND('',#16021,.T.);
#10099=FACE_OUTER_BOUND('',#16022,.T.);
#10100=FACE_OUTER_BOUND('',#16023,.T.);
#10101=FACE_OUTER_BOUND('',#16024,.T.);
#10102=FACE_OUTER_BOUND('',#16025,.T.);
#10103=FACE_OUTER_BOUND('',#16026,.T.);
#10104=FACE_OUTER_BOUND('',#16027,.T.);
#10105=FACE_OUTER_BOUND('',#16028,.T.);
#10106=FACE_OUTER_BOUND('',#16029,.T.);
#10107=FACE_OUTER_BOUND('',#16030,.T.);
#10108=FACE_OUTER_BOUND('',#16031,.T.);
#10109=FACE_OUTER_BOUND('',#16032,.T.);
#10110=FACE_OUTER_BOUND('',#16033,.T.);
#10111=FACE_OUTER_BOUND('',#16034,.T.);
#10112=FACE_OUTER_BOUND('',#16035,.T.);
#10113=FACE_OUTER_BOUND('',#16036,.T.);
#10114=FACE_OUTER_BOUND('',#16037,.T.);
#10115=FACE_OUTER_BOUND('',#16038,.T.);
#10116=FACE_OUTER_BOUND('',#16039,.T.);
#10117=FACE_OUTER_BOUND('',#16040,.T.);
#10118=FACE_OUTER_BOUND('',#16041,.T.);
#10119=FACE_OUTER_BOUND('',#16042,.T.);
#10120=FACE_OUTER_BOUND('',#16043,.T.);
#10121=FACE_OUTER_BOUND('',#16044,.T.);
#10122=FACE_OUTER_BOUND('',#16045,.T.);
#10123=FACE_OUTER_BOUND('',#16046,.T.);
#10124=FACE_OUTER_BOUND('',#16047,.T.);
#10125=FACE_OUTER_BOUND('',#16048,.T.);
#10126=FACE_OUTER_BOUND('',#16049,.T.);
#10127=FACE_OUTER_BOUND('',#16050,.T.);
#10128=FACE_OUTER_BOUND('',#16051,.T.);
#10129=FACE_OUTER_BOUND('',#16052,.T.);
#10130=FACE_OUTER_BOUND('',#16053,.T.);
#10131=FACE_OUTER_BOUND('',#16054,.T.);
#10132=FACE_OUTER_BOUND('',#16055,.T.);
#10133=FACE_OUTER_BOUND('',#16056,.T.);
#10134=FACE_OUTER_BOUND('',#16057,.T.);
#10135=FACE_OUTER_BOUND('',#16058,.T.);
#10136=FACE_OUTER_BOUND('',#16059,.T.);
#10137=FACE_OUTER_BOUND('',#16060,.T.);
#10138=FACE_OUTER_BOUND('',#16061,.T.);
#10139=FACE_OUTER_BOUND('',#16062,.T.);
#10140=FACE_OUTER_BOUND('',#16063,.T.);
#10141=FACE_OUTER_BOUND('',#16064,.T.);
#10142=FACE_OUTER_BOUND('',#16065,.T.);
#10143=FACE_OUTER_BOUND('',#16066,.T.);
#10144=FACE_OUTER_BOUND('',#16067,.T.);
#10145=FACE_OUTER_BOUND('',#16068,.T.);
#10146=FACE_OUTER_BOUND('',#16069,.T.);
#10147=FACE_OUTER_BOUND('',#16070,.T.);
#10148=FACE_OUTER_BOUND('',#16071,.T.);
#10149=FACE_OUTER_BOUND('',#16072,.T.);
#10150=FACE_OUTER_BOUND('',#16073,.T.);
#10151=FACE_OUTER_BOUND('',#16074,.T.);
#10152=FACE_OUTER_BOUND('',#16075,.T.);
#10153=FACE_OUTER_BOUND('',#16076,.T.);
#10154=FACE_OUTER_BOUND('',#16077,.T.);
#10155=FACE_OUTER_BOUND('',#16078,.T.);
#10156=FACE_OUTER_BOUND('',#16079,.T.);
#10157=FACE_OUTER_BOUND('',#16080,.T.);
#10158=FACE_OUTER_BOUND('',#16081,.T.);
#10159=FACE_OUTER_BOUND('',#16082,.T.);
#10160=FACE_OUTER_BOUND('',#16083,.T.);
#10161=FACE_OUTER_BOUND('',#16084,.T.);
#10162=FACE_OUTER_BOUND('',#16085,.T.);
#10163=FACE_OUTER_BOUND('',#16086,.T.);
#10164=FACE_OUTER_BOUND('',#16087,.T.);
#10165=FACE_OUTER_BOUND('',#16088,.T.);
#10166=FACE_OUTER_BOUND('',#16089,.T.);
#10167=FACE_OUTER_BOUND('',#16090,.T.);
#10168=FACE_OUTER_BOUND('',#16091,.T.);
#10169=FACE_OUTER_BOUND('',#16092,.T.);
#10170=FACE_OUTER_BOUND('',#16093,.T.);
#10171=FACE_OUTER_BOUND('',#16094,.T.);
#10172=FACE_OUTER_BOUND('',#16095,.T.);
#10173=FACE_OUTER_BOUND('',#16096,.T.);
#10174=FACE_OUTER_BOUND('',#16097,.T.);
#10175=FACE_OUTER_BOUND('',#16098,.T.);
#10176=FACE_OUTER_BOUND('',#16099,.T.);
#10177=FACE_OUTER_BOUND('',#16100,.T.);
#10178=FACE_OUTER_BOUND('',#16101,.T.);
#10179=FACE_OUTER_BOUND('',#16102,.T.);
#10180=FACE_OUTER_BOUND('',#16103,.T.);
#10181=FACE_OUTER_BOUND('',#16104,.T.);
#10182=FACE_OUTER_BOUND('',#16105,.T.);
#10183=FACE_OUTER_BOUND('',#16106,.T.);
#10184=FACE_OUTER_BOUND('',#16107,.T.);
#10185=FACE_OUTER_BOUND('',#16108,.T.);
#10186=FACE_OUTER_BOUND('',#16109,.T.);
#10187=FACE_OUTER_BOUND('',#16110,.T.);
#10188=FACE_OUTER_BOUND('',#16111,.T.);
#10189=FACE_OUTER_BOUND('',#16112,.T.);
#10190=FACE_OUTER_BOUND('',#16113,.T.);
#10191=FACE_OUTER_BOUND('',#16114,.T.);
#10192=FACE_OUTER_BOUND('',#16115,.T.);
#10193=FACE_OUTER_BOUND('',#16116,.T.);
#10194=FACE_OUTER_BOUND('',#16117,.T.);
#10195=FACE_OUTER_BOUND('',#16118,.T.);
#10196=FACE_OUTER_BOUND('',#16119,.T.);
#10197=FACE_OUTER_BOUND('',#16120,.T.);
#10198=FACE_OUTER_BOUND('',#16121,.T.);
#10199=FACE_OUTER_BOUND('',#16122,.T.);
#10200=FACE_OUTER_BOUND('',#16123,.T.);
#10201=FACE_OUTER_BOUND('',#16124,.T.);
#10202=FACE_OUTER_BOUND('',#16125,.T.);
#10203=FACE_OUTER_BOUND('',#16126,.T.);
#10204=FACE_OUTER_BOUND('',#16127,.T.);
#10205=FACE_OUTER_BOUND('',#16128,.T.);
#10206=FACE_OUTER_BOUND('',#16129,.T.);
#10207=FACE_OUTER_BOUND('',#16130,.T.);
#10208=FACE_OUTER_BOUND('',#16131,.T.);
#10209=FACE_OUTER_BOUND('',#16132,.T.);
#10210=FACE_OUTER_BOUND('',#16133,.T.);
#10211=FACE_OUTER_BOUND('',#16134,.T.);
#10212=FACE_OUTER_BOUND('',#16135,.T.);
#10213=FACE_OUTER_BOUND('',#16136,.T.);
#10214=FACE_OUTER_BOUND('',#16137,.T.);
#10215=FACE_OUTER_BOUND('',#16138,.T.);
#10216=FACE_OUTER_BOUND('',#16139,.T.);
#10217=FACE_OUTER_BOUND('',#16140,.T.);
#10218=FACE_OUTER_BOUND('',#16141,.T.);
#10219=FACE_OUTER_BOUND('',#16142,.T.);
#10220=FACE_OUTER_BOUND('',#16143,.T.);
#10221=FACE_OUTER_BOUND('',#16144,.T.);
#10222=FACE_OUTER_BOUND('',#16145,.T.);
#10223=FACE_OUTER_BOUND('',#16146,.T.);
#10224=FACE_OUTER_BOUND('',#16147,.T.);
#10225=FACE_OUTER_BOUND('',#16148,.T.);
#10226=FACE_OUTER_BOUND('',#16149,.T.);
#10227=FACE_OUTER_BOUND('',#16150,.T.);
#10228=FACE_OUTER_BOUND('',#16151,.T.);
#10229=FACE_OUTER_BOUND('',#16152,.T.);
#10230=FACE_OUTER_BOUND('',#16153,.T.);
#10231=FACE_OUTER_BOUND('',#16154,.T.);
#10232=FACE_OUTER_BOUND('',#16155,.T.);
#10233=FACE_OUTER_BOUND('',#16156,.T.);
#10234=FACE_OUTER_BOUND('',#16157,.T.);
#10235=FACE_OUTER_BOUND('',#16158,.T.);
#10236=FACE_OUTER_BOUND('',#16159,.T.);
#10237=FACE_OUTER_BOUND('',#16160,.T.);
#10238=FACE_OUTER_BOUND('',#16161,.T.);
#10239=FACE_OUTER_BOUND('',#16162,.T.);
#10240=FACE_OUTER_BOUND('',#16163,.T.);
#10241=FACE_OUTER_BOUND('',#16164,.T.);
#10242=FACE_OUTER_BOUND('',#16165,.T.);
#10243=FACE_OUTER_BOUND('',#16166,.T.);
#10244=FACE_OUTER_BOUND('',#16167,.T.);
#10245=FACE_OUTER_BOUND('',#16168,.T.);
#10246=FACE_OUTER_BOUND('',#16169,.T.);
#10247=FACE_OUTER_BOUND('',#16170,.T.);
#10248=FACE_OUTER_BOUND('',#16171,.T.);
#10249=FACE_OUTER_BOUND('',#16172,.T.);
#10250=FACE_OUTER_BOUND('',#16173,.T.);
#10251=FACE_OUTER_BOUND('',#16174,.T.);
#10252=FACE_OUTER_BOUND('',#16175,.T.);
#10253=FACE_OUTER_BOUND('',#16176,.T.);
#10254=FACE_OUTER_BOUND('',#16177,.T.);
#10255=FACE_OUTER_BOUND('',#16178,.T.);
#10256=FACE_OUTER_BOUND('',#16179,.T.);
#10257=FACE_OUTER_BOUND('',#16180,.T.);
#10258=FACE_OUTER_BOUND('',#16181,.T.);
#10259=FACE_OUTER_BOUND('',#16182,.T.);
#10260=FACE_OUTER_BOUND('',#16183,.T.);
#10261=FACE_OUTER_BOUND('',#16184,.T.);
#10262=FACE_OUTER_BOUND('',#16185,.T.);
#10263=FACE_OUTER_BOUND('',#16186,.T.);
#10264=FACE_OUTER_BOUND('',#16187,.T.);
#10265=FACE_OUTER_BOUND('',#16188,.T.);
#10266=FACE_OUTER_BOUND('',#16189,.T.);
#10267=FACE_OUTER_BOUND('',#16190,.T.);
#10268=FACE_OUTER_BOUND('',#16191,.T.);
#10269=FACE_OUTER_BOUND('',#16192,.T.);
#10270=FACE_OUTER_BOUND('',#16193,.T.);
#10271=FACE_OUTER_BOUND('',#16194,.T.);
#10272=FACE_OUTER_BOUND('',#16195,.T.);
#10273=FACE_OUTER_BOUND('',#16196,.T.);
#10274=FACE_OUTER_BOUND('',#16197,.T.);
#10275=FACE_OUTER_BOUND('',#16198,.T.);
#10276=FACE_OUTER_BOUND('',#16199,.T.);
#10277=FACE_OUTER_BOUND('',#16200,.T.);
#10278=FACE_OUTER_BOUND('',#16201,.T.);
#10279=FACE_OUTER_BOUND('',#16202,.T.);
#10280=FACE_OUTER_BOUND('',#16203,.T.);
#10281=FACE_OUTER_BOUND('',#16204,.T.);
#10282=FACE_OUTER_BOUND('',#16205,.T.);
#10283=FACE_OUTER_BOUND('',#16206,.T.);
#10284=FACE_OUTER_BOUND('',#16207,.T.);
#10285=FACE_OUTER_BOUND('',#16208,.T.);
#10286=FACE_OUTER_BOUND('',#16209,.T.);
#10287=FACE_OUTER_BOUND('',#16210,.T.);
#10288=FACE_OUTER_BOUND('',#16211,.T.);
#10289=FACE_OUTER_BOUND('',#16212,.T.);
#10290=FACE_OUTER_BOUND('',#16213,.T.);
#10291=FACE_OUTER_BOUND('',#16214,.T.);
#10292=FACE_OUTER_BOUND('',#16215,.T.);
#10293=FACE_OUTER_BOUND('',#16216,.T.);
#10294=FACE_OUTER_BOUND('',#16217,.T.);
#10295=FACE_OUTER_BOUND('',#16218,.T.);
#10296=FACE_OUTER_BOUND('',#16219,.T.);
#10297=FACE_OUTER_BOUND('',#16220,.T.);
#10298=FACE_OUTER_BOUND('',#16221,.T.);
#10299=FACE_OUTER_BOUND('',#16222,.T.);
#10300=FACE_OUTER_BOUND('',#16223,.T.);
#10301=FACE_OUTER_BOUND('',#16224,.T.);
#10302=FACE_OUTER_BOUND('',#16225,.T.);
#10303=FACE_OUTER_BOUND('',#16226,.T.);
#10304=FACE_OUTER_BOUND('',#16227,.T.);
#10305=FACE_OUTER_BOUND('',#16228,.T.);
#10306=FACE_OUTER_BOUND('',#16229,.T.);
#10307=FACE_OUTER_BOUND('',#16230,.T.);
#10308=FACE_OUTER_BOUND('',#16231,.T.);
#10309=FACE_OUTER_BOUND('',#16232,.T.);
#10310=FACE_OUTER_BOUND('',#16233,.T.);
#10311=FACE_OUTER_BOUND('',#16234,.T.);
#10312=FACE_OUTER_BOUND('',#16235,.T.);
#10313=FACE_OUTER_BOUND('',#16236,.T.);
#10314=FACE_OUTER_BOUND('',#16237,.T.);
#10315=FACE_OUTER_BOUND('',#16238,.T.);
#10316=FACE_OUTER_BOUND('',#16239,.T.);
#10317=FACE_OUTER_BOUND('',#16240,.T.);
#10318=FACE_OUTER_BOUND('',#16241,.T.);
#10319=FACE_OUTER_BOUND('',#16242,.T.);
#10320=FACE_OUTER_BOUND('',#16243,.T.);
#10321=FACE_OUTER_BOUND('',#16244,.T.);
#10322=FACE_OUTER_BOUND('',#16245,.T.);
#10323=FACE_OUTER_BOUND('',#16246,.T.);
#10324=FACE_OUTER_BOUND('',#16247,.T.);
#10325=FACE_OUTER_BOUND('',#16248,.T.);
#10326=FACE_OUTER_BOUND('',#16249,.T.);
#10327=FACE_OUTER_BOUND('',#16250,.T.);
#10328=FACE_OUTER_BOUND('',#16251,.T.);
#10329=FACE_OUTER_BOUND('',#16252,.T.);
#10330=FACE_OUTER_BOUND('',#16253,.T.);
#10331=FACE_OUTER_BOUND('',#16254,.T.);
#10332=FACE_OUTER_BOUND('',#16255,.T.);
#10333=FACE_OUTER_BOUND('',#16256,.T.);
#10334=FACE_OUTER_BOUND('',#16257,.T.);
#10335=FACE_OUTER_BOUND('',#16258,.T.);
#10336=FACE_OUTER_BOUND('',#16259,.T.);
#10337=FACE_OUTER_BOUND('',#16260,.T.);
#10338=FACE_OUTER_BOUND('',#16261,.T.);
#10339=FACE_OUTER_BOUND('',#16262,.T.);
#10340=FACE_OUTER_BOUND('',#16263,.T.);
#10341=FACE_OUTER_BOUND('',#16264,.T.);
#10342=FACE_OUTER_BOUND('',#16265,.T.);
#10343=FACE_OUTER_BOUND('',#16266,.T.);
#10344=FACE_OUTER_BOUND('',#16267,.T.);
#10345=FACE_OUTER_BOUND('',#16268,.T.);
#10346=FACE_OUTER_BOUND('',#16269,.T.);
#10347=FACE_OUTER_BOUND('',#16270,.T.);
#10348=FACE_OUTER_BOUND('',#16271,.T.);
#10349=FACE_OUTER_BOUND('',#16272,.T.);
#10350=FACE_OUTER_BOUND('',#16273,.T.);
#10351=FACE_OUTER_BOUND('',#16274,.T.);
#10352=FACE_OUTER_BOUND('',#16275,.T.);
#10353=FACE_OUTER_BOUND('',#16276,.T.);
#10354=FACE_OUTER_BOUND('',#16277,.T.);
#10355=FACE_OUTER_BOUND('',#16278,.T.);
#10356=FACE_OUTER_BOUND('',#16279,.T.);
#10357=FACE_OUTER_BOUND('',#16280,.T.);
#10358=FACE_OUTER_BOUND('',#16281,.T.);
#10359=FACE_OUTER_BOUND('',#16282,.T.);
#10360=FACE_OUTER_BOUND('',#16283,.T.);
#10361=FACE_OUTER_BOUND('',#16284,.T.);
#10362=FACE_OUTER_BOUND('',#16285,.T.);
#10363=FACE_OUTER_BOUND('',#16286,.T.);
#10364=FACE_OUTER_BOUND('',#16287,.T.);
#10365=FACE_OUTER_BOUND('',#16288,.T.);
#10366=FACE_OUTER_BOUND('',#16289,.T.);
#10367=FACE_OUTER_BOUND('',#16290,.T.);
#10368=FACE_OUTER_BOUND('',#16291,.T.);
#10369=FACE_OUTER_BOUND('',#16292,.T.);
#10370=FACE_OUTER_BOUND('',#16293,.T.);
#10371=FACE_OUTER_BOUND('',#16294,.T.);
#10372=FACE_OUTER_BOUND('',#16295,.T.);
#10373=FACE_OUTER_BOUND('',#16296,.T.);
#10374=FACE_OUTER_BOUND('',#16297,.T.);
#10375=FACE_OUTER_BOUND('',#16298,.T.);
#10376=FACE_OUTER_BOUND('',#16299,.T.);
#10377=FACE_OUTER_BOUND('',#16300,.T.);
#10378=FACE_OUTER_BOUND('',#16301,.T.);
#10379=FACE_OUTER_BOUND('',#16302,.T.);
#10380=FACE_OUTER_BOUND('',#16303,.T.);
#10381=FACE_OUTER_BOUND('',#16304,.T.);
#10382=FACE_OUTER_BOUND('',#16305,.T.);
#10383=FACE_OUTER_BOUND('',#16306,.T.);
#10384=FACE_OUTER_BOUND('',#16307,.T.);
#10385=FACE_OUTER_BOUND('',#16308,.T.);
#10386=FACE_OUTER_BOUND('',#16309,.T.);
#10387=FACE_OUTER_BOUND('',#16310,.T.);
#10388=FACE_OUTER_BOUND('',#16311,.T.);
#10389=FACE_OUTER_BOUND('',#16312,.T.);
#10390=FACE_OUTER_BOUND('',#16313,.T.);
#10391=FACE_OUTER_BOUND('',#16314,.T.);
#10392=FACE_OUTER_BOUND('',#16315,.T.);
#10393=FACE_OUTER_BOUND('',#16316,.T.);
#10394=FACE_OUTER_BOUND('',#16317,.T.);
#10395=FACE_OUTER_BOUND('',#16318,.T.);
#10396=FACE_OUTER_BOUND('',#16319,.T.);
#10397=FACE_OUTER_BOUND('',#16320,.T.);
#10398=FACE_OUTER_BOUND('',#16321,.T.);
#10399=FACE_OUTER_BOUND('',#16322,.T.);
#10400=FACE_OUTER_BOUND('',#16323,.T.);
#10401=FACE_OUTER_BOUND('',#16324,.T.);
#10402=FACE_OUTER_BOUND('',#16325,.T.);
#10403=FACE_OUTER_BOUND('',#16326,.T.);
#10404=FACE_OUTER_BOUND('',#16327,.T.);
#10405=FACE_OUTER_BOUND('',#16328,.T.);
#10406=FACE_OUTER_BOUND('',#16329,.T.);
#10407=FACE_OUTER_BOUND('',#16330,.T.);
#10408=FACE_OUTER_BOUND('',#16331,.T.);
#14472=EDGE_LOOP('',(#69924,#69925,#69926));
#14473=EDGE_LOOP('',(#69927,#69928,#69929,#69930));
#14474=EDGE_LOOP('',(#69931,#69932,#69933,#69934));
#14475=EDGE_LOOP('',(#69935,#69936,#69937,#69938));
#14476=EDGE_LOOP('',(#69939,#69940,#69941,#69942));
#14477=EDGE_LOOP('',(#69943,#69944,#69945,#69946));
#14478=EDGE_LOOP('',(#69947,#69948,#69949,#69950));
#14479=EDGE_LOOP('',(#69951,#69952,#69953,#69954));
#14480=EDGE_LOOP('',(#69955,#69956,#69957,#69958));
#14481=EDGE_LOOP('',(#69959,#69960,#69961,#69962));
#14482=EDGE_LOOP('',(#69963,#69964,#69965,#69966));
#14483=EDGE_LOOP('',(#69967,#69968,#69969,#69970));
#14484=EDGE_LOOP('',(#69971,#69972,#69973,#69974));
#14485=EDGE_LOOP('',(#69975,#69976,#69977,#69978));
#14486=EDGE_LOOP('',(#69979,#69980,#69981,#69982));
#14487=EDGE_LOOP('',(#69983,#69984,#69985,#69986));
#14488=EDGE_LOOP('',(#69987,#69988,#69989,#69990));
#14489=EDGE_LOOP('',(#69991,#69992,#69993,#69994));
#14490=EDGE_LOOP('',(#69995,#69996,#69997,#69998));
#14491=EDGE_LOOP('',(#69999,#70000,#70001,#70002));
#14492=EDGE_LOOP('',(#70003,#70004,#70005,#70006));
#14493=EDGE_LOOP('',(#70007,#70008,#70009,#70010));
#14494=EDGE_LOOP('',(#70011,#70012,#70013,#70014));
#14495=EDGE_LOOP('',(#70015,#70016,#70017,#70018));
#14496=EDGE_LOOP('',(#70019,#70020,#70021,#70022));
#14497=EDGE_LOOP('',(#70023,#70024,#70025,#70026));
#14498=EDGE_LOOP('',(#70027,#70028,#70029,#70030));
#14499=EDGE_LOOP('',(#70031,#70032,#70033,#70034));
#14500=EDGE_LOOP('',(#70035,#70036,#70037,#70038));
#14501=EDGE_LOOP('',(#70039,#70040,#70041,#70042,#70043,#70044,#70045,#70046));
#14502=EDGE_LOOP('',(#70047,#70048,#70049,#70050));
#14503=EDGE_LOOP('',(#70051,#70052,#70053,#70054));
#14504=EDGE_LOOP('',(#70055,#70056,#70057,#70058));
#14505=EDGE_LOOP('',(#70059,#70060,#70061,#70062));
#14506=EDGE_LOOP('',(#70063,#70064,#70065,#70066));
#14507=EDGE_LOOP('',(#70067,#70068,#70069,#70070));
#14508=EDGE_LOOP('',(#70071,#70072,#70073,#70074));
#14509=EDGE_LOOP('',(#70075,#70076,#70077,#70078));
#14510=EDGE_LOOP('',(#70079,#70080,#70081,#70082));
#14511=EDGE_LOOP('',(#70083,#70084,#70085,#70086));
#14512=EDGE_LOOP('',(#70087,#70088,#70089,#70090));
#14513=EDGE_LOOP('',(#70091,#70092,#70093,#70094));
#14514=EDGE_LOOP('',(#70095,#70096,#70097,#70098));
#14515=EDGE_LOOP('',(#70099,#70100,#70101,#70102));
#14516=EDGE_LOOP('',(#70103,#70104,#70105,#70106));
#14517=EDGE_LOOP('',(#70107,#70108,#70109,#70110));
#14518=EDGE_LOOP('',(#70111,#70112,#70113,#70114));
#14519=EDGE_LOOP('',(#70115,#70116,#70117,#70118));
#14520=EDGE_LOOP('',(#70119,#70120,#70121,#70122));
#14521=EDGE_LOOP('',(#70123,#70124,#70125,#70126));
#14522=EDGE_LOOP('',(#70127,#70128,#70129,#70130));
#14523=EDGE_LOOP('',(#70131,#70132,#70133,#70134));
#14524=EDGE_LOOP('',(#70135,#70136,#70137,#70138));
#14525=EDGE_LOOP('',(#70139,#70140,#70141,#70142));
#14526=EDGE_LOOP('',(#70143,#70144,#70145,#70146));
#14527=EDGE_LOOP('',(#70147,#70148,#70149,#70150));
#14528=EDGE_LOOP('',(#70151,#70152,#70153,#70154));
#14529=EDGE_LOOP('',(#70155,#70156,#70157,#70158));
#14530=EDGE_LOOP('',(#70159,#70160,#70161));
#14531=EDGE_LOOP('',(#70162,#70163,#70164,#70165,#70166));
#14532=EDGE_LOOP('',(#70167,#70168,#70169,#70170));
#14533=EDGE_LOOP('',(#70171,#70172,#70173,#70174));
#14534=EDGE_LOOP('',(#70175,#70176,#70177,#70178));
#14535=EDGE_LOOP('',(#70179,#70180,#70181,#70182,#70183,#70184,#70185,#70186));
#14536=EDGE_LOOP('',(#70187,#70188));
#14537=EDGE_LOOP('',(#70189,#70190,#70191,#70192));
#14538=EDGE_LOOP('',(#70193,#70194,#70195,#70196));
#14539=EDGE_LOOP('',(#70197,#70198,#70199,#70200));
#14540=EDGE_LOOP('',(#70201,#70202,#70203,#70204,#70205,#70206,#70207,#70208,
#70209,#70210,#70211,#70212,#70213,#70214,#70215,#70216,#70217,#70218,#70219,
#70220,#70221,#70222,#70223,#70224,#70225,#70226,#70227,#70228,#70229,#70230,
#70231,#70232,#70233,#70234,#70235,#70236,#70237,#70238,#70239,#70240,#70241,
#70242,#70243,#70244,#70245,#70246,#70247,#70248,#70249,#70250,#70251,#70252,
#70253,#70254,#70255,#70256,#70257,#70258,#70259,#70260,#70261,#70262,#70263,
#70264,#70265,#70266,#70267,#70268,#70269,#70270,#70271,#70272,#70273,#70274,
#70275,#70276,#70277,#70278,#70279,#70280,#70281,#70282,#70283,#70284,#70285,
#70286,#70287,#70288,#70289,#70290,#70291,#70292,#70293,#70294,#70295,#70296,
#70297,#70298,#70299,#70300,#70301,#70302,#70303,#70304,#70305,#70306,#70307,
#70308,#70309,#70310,#70311,#70312,#70313,#70314,#70315,#70316,#70317,#70318,
#70319,#70320,#70321,#70322,#70323,#70324,#70325,#70326,#70327,#70328,#70329,
#70330,#70331,#70332,#70333,#70334,#70335,#70336,#70337,#70338,#70339,#70340,
#70341,#70342,#70343,#70344,#70345,#70346,#70347,#70348,#70349,#70350,#70351,
#70352,#70353,#70354,#70355,#70356,#70357,#70358,#70359,#70360,#70361,#70362,
#70363,#70364,#70365,#70366,#70367,#70368,#70369,#70370,#70371,#70372,#70373,
#70374,#70375,#70376,#70377,#70378,#70379,#70380,#70381,#70382,#70383,#70384,
#70385,#70386,#70387,#70388,#70389,#70390,#70391,#70392,#70393,#70394,#70395,
#70396,#70397,#70398,#70399,#70400,#70401,#70402,#70403,#70404,#70405,#70406,
#70407,#70408,#70409,#70410,#70411,#70412,#70413,#70414,#70415,#70416,#70417,
#70418,#70419,#70420,#70421,#70422,#70423,#70424,#70425,#70426,#70427,#70428,
#70429,#70430,#70431,#70432,#70433,#70434,#70435,#70436,#70437,#70438,#70439,
#70440,#70441,#70442,#70443,#70444,#70445,#70446,#70447,#70448,#70449,#70450,
#70451,#70452,#70453,#70454,#70455,#70456,#70457,#70458,#70459,#70460,#70461,
#70462,#70463,#70464,#70465,#70466,#70467,#70468,#70469,#70470,#70471,#70472,
#70473,#70474,#70475,#70476,#70477,#70478,#70479,#70480,#70481,#70482,#70483,
#70484,#70485,#70486,#70487,#70488,#70489,#70490,#70491,#70492,#70493,#70494,
#70495,#70496,#70497,#70498,#70499,#70500,#70501,#70502,#70503,#70504,#70505,
#70506,#70507,#70508,#70509,#70510,#70511,#70512,#70513,#70514,#70515,#70516,
#70517,#70518,#70519,#70520,#70521,#70522,#70523,#70524,#70525,#70526,#70527,
#70528,#70529,#70530,#70531,#70532,#70533,#70534,#70535,#70536,#70537,#70538,
#70539,#70540,#70541,#70542,#70543,#70544,#70545,#70546,#70547,#70548,#70549,
#70550,#70551,#70552,#70553,#70554,#70555,#70556,#70557,#70558,#70559,#70560,
#70561,#70562,#70563,#70564,#70565,#70566,#70567,#70568,#70569,#70570,#70571,
#70572,#70573,#70574,#70575,#70576,#70577,#70578,#70579,#70580,#70581,#70582,
#70583,#70584,#70585,#70586,#70587,#70588,#70589,#70590,#70591,#70592,#70593,
#70594,#70595,#70596,#70597));
#14541=EDGE_LOOP('',(#70598,#70599,#70600,#70601,#70602));
#14542=EDGE_LOOP('',(#70603,#70604,#70605,#70606,#70607,#70608,#70609,#70610,
#70611,#70612,#70613,#70614,#70615,#70616,#70617,#70618,#70619,#70620,#70621,
#70622,#70623,#70624,#70625,#70626,#70627,#70628,#70629,#70630,#70631,#70632,
#70633,#70634,#70635,#70636,#70637,#70638,#70639,#70640,#70641,#70642,#70643,
#70644,#70645,#70646,#70647,#70648,#70649,#70650,#70651,#70652,#70653,#70654,
#70655,#70656,#70657,#70658,#70659,#70660,#70661,#70662,#70663,#70664,#70665,
#70666,#70667,#70668,#70669,#70670,#70671,#70672,#70673,#70674,#70675,#70676,
#70677,#70678,#70679,#70680,#70681,#70682,#70683,#70684,#70685,#70686,#70687,
#70688,#70689,#70690,#70691,#70692,#70693,#70694,#70695,#70696,#70697,#70698,
#70699,#70700,#70701,#70702,#70703,#70704,#70705,#70706,#70707,#70708,#70709,
#70710,#70711,#70712,#70713,#70714,#70715,#70716,#70717,#70718,#70719,#70720,
#70721,#70722,#70723,#70724,#70725,#70726,#70727,#70728,#70729,#70730,#70731,
#70732,#70733,#70734,#70735,#70736,#70737,#70738,#70739,#70740,#70741,#70742,
#70743,#70744,#70745,#70746,#70747,#70748,#70749,#70750,#70751,#70752,#70753,
#70754,#70755,#70756,#70757,#70758,#70759,#70760,#70761,#70762,#70763,#70764,
#70765,#70766,#70767,#70768,#70769,#70770,#70771,#70772,#70773,#70774,#70775,
#70776,#70777,#70778,#70779,#70780,#70781,#70782,#70783,#70784,#70785,#70786,
#70787,#70788,#70789,#70790,#70791,#70792,#70793,#70794,#70795,#70796,#70797,
#70798,#70799,#70800,#70801,#70802,#70803,#70804,#70805,#70806,#70807,#70808,
#70809,#70810,#70811,#70812,#70813,#70814,#70815,#70816,#70817,#70818,#70819,
#70820,#70821,#70822,#70823,#70824,#70825,#70826,#70827,#70828,#70829,#70830,
#70831,#70832,#70833,#70834,#70835,#70836,#70837,#70838,#70839,#70840,#70841,
#70842,#70843,#70844,#70845,#70846,#70847,#70848,#70849,#70850,#70851,#70852,
#70853,#70854,#70855,#70856,#70857,#70858,#70859,#70860,#70861,#70862,#70863,
#70864,#70865,#70866,#70867,#70868,#70869,#70870,#70871,#70872,#70873,#70874,
#70875,#70876,#70877,#70878,#70879,#70880,#70881,#70882,#70883,#70884,#70885,
#70886,#70887,#70888,#70889,#70890,#70891,#70892,#70893,#70894,#70895,#70896,
#70897,#70898,#70899,#70900,#70901,#70902,#70903,#70904,#70905,#70906,#70907,
#70908,#70909,#70910,#70911,#70912,#70913,#70914,#70915,#70916,#70917,#70918,
#70919,#70920,#70921,#70922,#70923,#70924,#70925,#70926,#70927,#70928,#70929,
#70930,#70931,#70932,#70933,#70934,#70935,#70936,#70937,#70938,#70939,#70940,
#70941,#70942,#70943,#70944,#70945,#70946,#70947,#70948,#70949,#70950,#70951,
#70952,#70953,#70954,#70955,#70956,#70957,#70958,#70959,#70960,#70961,#70962,
#70963,#70964,#70965,#70966,#70967,#70968,#70969,#70970,#70971,#70972,#70973,
#70974,#70975,#70976,#70977,#70978,#70979,#70980,#70981,#70982,#70983,#70984,
#70985,#70986,#70987,#70988,#70989,#70990,#70991,#70992,#70993,#70994,#70995,
#70996,#70997,#70998,#70999,#71000,#71001,#71002,#71003,#71004,#71005,#71006,
#71007,#71008,#71009,#71010,#71011,#71012,#71013,#71014,#71015,#71016,#71017,
#71018,#71019,#71020,#71021,#71022,#71023,#71024,#71025,#71026,#71027,#71028,
#71029,#71030,#71031,#71032,#71033,#71034,#71035,#71036,#71037,#71038,#71039,
#71040,#71041,#71042,#71043,#71044,#71045,#71046,#71047,#71048,#71049,#71050,
#71051,#71052,#71053,#71054,#71055,#71056,#71057,#71058,#71059,#71060,#71061,
#71062,#71063,#71064,#71065,#71066,#71067,#71068,#71069,#71070,#71071,#71072,
#71073,#71074,#71075,#71076,#71077,#71078,#71079,#71080,#71081,#71082,#71083,
#71084,#71085,#71086,#71087,#71088,#71089,#71090,#71091,#71092,#71093,#71094,
#71095,#71096,#71097,#71098,#71099,#71100,#71101,#71102,#71103,#71104,#71105,
#71106,#71107,#71108,#71109,#71110,#71111,#71112,#71113,#71114,#71115,#71116,
#71117,#71118,#71119,#71120,#71121,#71122,#71123,#71124,#71125,#71126,#71127,
#71128,#71129,#71130,#71131,#71132,#71133,#71134,#71135,#71136,#71137,#71138,
#71139,#71140,#71141,#71142,#71143,#71144,#71145,#71146,#71147,#71148,#71149,
#71150,#71151,#71152,#71153,#71154,#71155,#71156,#71157,#71158,#71159,#71160,
#71161,#71162,#71163,#71164,#71165,#71166,#71167,#71168,#71169,#71170,#71171,
#71172,#71173,#71174,#71175,#71176,#71177,#71178,#71179,#71180,#71181,#71182,
#71183,#71184,#71185,#71186,#71187,#71188,#71189,#71190,#71191,#71192,#71193,
#71194));
#14543=EDGE_LOOP('',(#71195,#71196,#71197,#71198,#71199));
#14544=EDGE_LOOP('',(#71200,#71201,#71202,#71203));
#14545=EDGE_LOOP('',(#71204,#71205,#71206,#71207));
#14546=EDGE_LOOP('',(#71208,#71209,#71210,#71211));
#14547=EDGE_LOOP('',(#71212,#71213,#71214,#71215));
#14548=EDGE_LOOP('',(#71216,#71217,#71218,#71219));
#14549=EDGE_LOOP('',(#71220,#71221,#71222,#71223));
#14550=EDGE_LOOP('',(#71224,#71225,#71226,#71227));
#14551=EDGE_LOOP('',(#71228,#71229,#71230,#71231));
#14552=EDGE_LOOP('',(#71232,#71233,#71234,#71235));
#14553=EDGE_LOOP('',(#71236,#71237,#71238,#71239));
#14554=EDGE_LOOP('',(#71240,#71241,#71242,#71243));
#14555=EDGE_LOOP('',(#71244,#71245,#71246,#71247));
#14556=EDGE_LOOP('',(#71248,#71249,#71250,#71251));
#14557=EDGE_LOOP('',(#71252,#71253,#71254,#71255));
#14558=EDGE_LOOP('',(#71256,#71257,#71258,#71259));
#14559=EDGE_LOOP('',(#71260,#71261,#71262,#71263));
#14560=EDGE_LOOP('',(#71264,#71265,#71266,#71267));
#14561=EDGE_LOOP('',(#71268,#71269,#71270,#71271));
#14562=EDGE_LOOP('',(#71272,#71273,#71274,#71275));
#14563=EDGE_LOOP('',(#71276,#71277,#71278,#71279));
#14564=EDGE_LOOP('',(#71280,#71281,#71282,#71283));
#14565=EDGE_LOOP('',(#71284,#71285,#71286,#71287));
#14566=EDGE_LOOP('',(#71288,#71289,#71290,#71291));
#14567=EDGE_LOOP('',(#71292,#71293,#71294,#71295));
#14568=EDGE_LOOP('',(#71296,#71297,#71298,#71299));
#14569=EDGE_LOOP('',(#71300,#71301,#71302,#71303));
#14570=EDGE_LOOP('',(#71304,#71305,#71306,#71307));
#14571=EDGE_LOOP('',(#71308,#71309,#71310,#71311));
#14572=EDGE_LOOP('',(#71312,#71313,#71314,#71315));
#14573=EDGE_LOOP('',(#71316,#71317,#71318,#71319));
#14574=EDGE_LOOP('',(#71320,#71321,#71322,#71323));
#14575=EDGE_LOOP('',(#71324,#71325,#71326,#71327));
#14576=EDGE_LOOP('',(#71328,#71329,#71330,#71331));
#14577=EDGE_LOOP('',(#71332,#71333,#71334,#71335));
#14578=EDGE_LOOP('',(#71336,#71337,#71338,#71339));
#14579=EDGE_LOOP('',(#71340,#71341,#71342,#71343));
#14580=EDGE_LOOP('',(#71344,#71345,#71346,#71347));
#14581=EDGE_LOOP('',(#71348,#71349,#71350,#71351));
#14582=EDGE_LOOP('',(#71352,#71353,#71354,#71355));
#14583=EDGE_LOOP('',(#71356,#71357,#71358,#71359));
#14584=EDGE_LOOP('',(#71360,#71361,#71362,#71363));
#14585=EDGE_LOOP('',(#71364,#71365,#71366,#71367,#71368));
#14586=EDGE_LOOP('',(#71369,#71370,#71371,#71372));
#14587=EDGE_LOOP('',(#71373,#71374,#71375,#71376));
#14588=EDGE_LOOP('',(#71377,#71378,#71379,#71380));
#14589=EDGE_LOOP('',(#71381,#71382,#71383,#71384));
#14590=EDGE_LOOP('',(#71385,#71386,#71387,#71388));
#14591=EDGE_LOOP('',(#71389,#71390,#71391,#71392));
#14592=EDGE_LOOP('',(#71393,#71394,#71395,#71396));
#14593=EDGE_LOOP('',(#71397,#71398,#71399,#71400));
#14594=EDGE_LOOP('',(#71401,#71402,#71403,#71404));
#14595=EDGE_LOOP('',(#71405,#71406,#71407,#71408));
#14596=EDGE_LOOP('',(#71409,#71410,#71411,#71412));
#14597=EDGE_LOOP('',(#71413,#71414,#71415,#71416));
#14598=EDGE_LOOP('',(#71417,#71418,#71419,#71420));
#14599=EDGE_LOOP('',(#71421,#71422,#71423,#71424));
#14600=EDGE_LOOP('',(#71425,#71426,#71427,#71428));
#14601=EDGE_LOOP('',(#71429,#71430,#71431,#71432));
#14602=EDGE_LOOP('',(#71433,#71434,#71435,#71436));
#14603=EDGE_LOOP('',(#71437,#71438,#71439,#71440));
#14604=EDGE_LOOP('',(#71441,#71442,#71443,#71444));
#14605=EDGE_LOOP('',(#71445,#71446,#71447,#71448));
#14606=EDGE_LOOP('',(#71449,#71450,#71451,#71452));
#14607=EDGE_LOOP('',(#71453,#71454,#71455,#71456));
#14608=EDGE_LOOP('',(#71457,#71458,#71459,#71460));
#14609=EDGE_LOOP('',(#71461,#71462,#71463,#71464));
#14610=EDGE_LOOP('',(#71465,#71466,#71467,#71468));
#14611=EDGE_LOOP('',(#71469,#71470,#71471,#71472));
#14612=EDGE_LOOP('',(#71473,#71474,#71475,#71476));
#14613=EDGE_LOOP('',(#71477,#71478,#71479,#71480));
#14614=EDGE_LOOP('',(#71481,#71482,#71483,#71484));
#14615=EDGE_LOOP('',(#71485,#71486,#71487,#71488));
#14616=EDGE_LOOP('',(#71489,#71490,#71491,#71492));
#14617=EDGE_LOOP('',(#71493,#71494,#71495,#71496));
#14618=EDGE_LOOP('',(#71497,#71498,#71499,#71500));
#14619=EDGE_LOOP('',(#71501,#71502,#71503,#71504));
#14620=EDGE_LOOP('',(#71505,#71506,#71507,#71508));
#14621=EDGE_LOOP('',(#71509,#71510,#71511,#71512));
#14622=EDGE_LOOP('',(#71513,#71514,#71515,#71516));
#14623=EDGE_LOOP('',(#71517,#71518,#71519,#71520));
#14624=EDGE_LOOP('',(#71521,#71522,#71523,#71524));
#14625=EDGE_LOOP('',(#71525,#71526,#71527,#71528));
#14626=EDGE_LOOP('',(#71529,#71530,#71531,#71532));
#14627=EDGE_LOOP('',(#71533,#71534,#71535,#71536));
#14628=EDGE_LOOP('',(#71537,#71538,#71539,#71540));
#14629=EDGE_LOOP('',(#71541,#71542,#71543,#71544));
#14630=EDGE_LOOP('',(#71545,#71546,#71547,#71548));
#14631=EDGE_LOOP('',(#71549,#71550,#71551,#71552));
#14632=EDGE_LOOP('',(#71553,#71554,#71555,#71556));
#14633=EDGE_LOOP('',(#71557,#71558,#71559,#71560));
#14634=EDGE_LOOP('',(#71561,#71562,#71563,#71564));
#14635=EDGE_LOOP('',(#71565,#71566,#71567,#71568));
#14636=EDGE_LOOP('',(#71569,#71570,#71571,#71572));
#14637=EDGE_LOOP('',(#71573,#71574,#71575,#71576));
#14638=EDGE_LOOP('',(#71577,#71578,#71579,#71580));
#14639=EDGE_LOOP('',(#71581,#71582,#71583,#71584));
#14640=EDGE_LOOP('',(#71585,#71586,#71587,#71588));
#14641=EDGE_LOOP('',(#71589,#71590,#71591,#71592,#71593));
#14642=EDGE_LOOP('',(#71594,#71595,#71596,#71597,#71598));
#14643=EDGE_LOOP('',(#71599,#71600,#71601));
#14644=EDGE_LOOP('',(#71602,#71603,#71604));
#14645=EDGE_LOOP('',(#71605,#71606,#71607));
#14646=EDGE_LOOP('',(#71608,#71609,#71610));
#14647=EDGE_LOOP('',(#71611,#71612,#71613));
#14648=EDGE_LOOP('',(#71614));
#14649=EDGE_LOOP('',(#71615,#71616,#71617,#71618,#71619,#71620));
#14650=EDGE_LOOP('',(#71621,#71622,#71623,#71624));
#14651=EDGE_LOOP('',(#71625,#71626,#71627,#71628,#71629));
#14652=EDGE_LOOP('',(#71630,#71631,#71632,#71633,#71634));
#14653=EDGE_LOOP('',(#71635,#71636,#71637,#71638,#71639));
#14654=EDGE_LOOP('',(#71640,#71641,#71642,#71643,#71644));
#14655=EDGE_LOOP('',(#71645,#71646,#71647,#71648,#71649));
#14656=EDGE_LOOP('',(#71650,#71651,#71652,#71653,#71654));
#14657=EDGE_LOOP('',(#71655,#71656,#71657));
#14658=EDGE_LOOP('',(#71658,#71659));
#14659=EDGE_LOOP('',(#71660,#71661));
#14660=EDGE_LOOP('',(#71662,#71663));
#14661=EDGE_LOOP('',(#71664,#71665));
#14662=EDGE_LOOP('',(#71666,#71667));
#14663=EDGE_LOOP('',(#71668));
#14664=EDGE_LOOP('',(#71669));
#14665=EDGE_LOOP('',(#71670,#71671,#71672));
#14666=EDGE_LOOP('',(#71673,#71674,#71675,#71676));
#14667=EDGE_LOOP('',(#71677,#71678,#71679,#71680,#71681,#71682,#71683,#71684,
#71685,#71686,#71687,#71688,#71689,#71690,#71691,#71692,#71693,#71694,#71695,
#71696,#71697,#71698,#71699,#71700,#71701,#71702,#71703,#71704,#71705,#71706,
#71707,#71708,#71709,#71710,#71711,#71712,#71713,#71714,#71715,#71716,#71717,
#71718,#71719,#71720,#71721,#71722,#71723,#71724,#71725,#71726,#71727,#71728,
#71729,#71730,#71731,#71732,#71733,#71734,#71735,#71736,#71737,#71738));
#14668=EDGE_LOOP('',(#71739,#71740,#71741,#71742,#71743,#71744,#71745,#71746,
#71747,#71748,#71749,#71750,#71751,#71752,#71753,#71754,#71755,#71756,#71757,
#71758,#71759,#71760,#71761,#71762,#71763,#71764,#71765,#71766,#71767,#71768,
#71769,#71770,#71771,#71772,#71773,#71774,#71775,#71776,#71777,#71778,#71779,
#71780,#71781,#71782,#71783,#71784,#71785,#71786,#71787,#71788,#71789,#71790,
#71791,#71792,#71793,#71794,#71795,#71796,#71797,#71798,#71799));
#14669=EDGE_LOOP('',(#71800,#71801,#71802));
#14670=EDGE_LOOP('',(#71803,#71804,#71805,#71806));
#14671=EDGE_LOOP('',(#71807,#71808,#71809,#71810));
#14672=EDGE_LOOP('',(#71811,#71812,#71813));
#14673=EDGE_LOOP('',(#71814,#71815,#71816,#71817));
#14674=EDGE_LOOP('',(#71818,#71819,#71820,#71821));
#14675=EDGE_LOOP('',(#71822,#71823,#71824,#71825));
#14676=EDGE_LOOP('',(#71826,#71827,#71828,#71829));
#14677=EDGE_LOOP('',(#71830,#71831,#71832,#71833));
#14678=EDGE_LOOP('',(#71834,#71835,#71836,#71837));
#14679=EDGE_LOOP('',(#71838,#71839,#71840,#71841));
#14680=EDGE_LOOP('',(#71842,#71843,#71844,#71845));
#14681=EDGE_LOOP('',(#71846,#71847,#71848,#71849));
#14682=EDGE_LOOP('',(#71850,#71851,#71852,#71853));
#14683=EDGE_LOOP('',(#71854,#71855,#71856,#71857,#71858));
#14684=EDGE_LOOP('',(#71859,#71860,#71861,#71862,#71863));
#14685=EDGE_LOOP('',(#71864,#71865,#71866,#71867));
#14686=EDGE_LOOP('',(#71868,#71869,#71870,#71871));
#14687=EDGE_LOOP('',(#71872,#71873,#71874));
#14688=EDGE_LOOP('',(#71875,#71876,#71877,#71878));
#14689=EDGE_LOOP('',(#71879,#71880,#71881,#71882));
#14690=EDGE_LOOP('',(#71883,#71884,#71885,#71886));
#14691=EDGE_LOOP('',(#71887,#71888,#71889,#71890));
#14692=EDGE_LOOP('',(#71891,#71892,#71893,#71894));
#14693=EDGE_LOOP('',(#71895,#71896,#71897,#71898));
#14694=EDGE_LOOP('',(#71899,#71900,#71901,#71902));
#14695=EDGE_LOOP('',(#71903,#71904,#71905,#71906));
#14696=EDGE_LOOP('',(#71907,#71908,#71909,#71910));
#14697=EDGE_LOOP('',(#71911,#71912,#71913,#71914));
#14698=EDGE_LOOP('',(#71915,#71916,#71917,#71918));
#14699=EDGE_LOOP('',(#71919,#71920,#71921));
#14700=EDGE_LOOP('',(#71922,#71923,#71924,#71925,#71926));
#14701=EDGE_LOOP('',(#71927,#71928,#71929,#71930,#71931));
#14702=EDGE_LOOP('',(#71932,#71933,#71934,#71935));
#14703=EDGE_LOOP('',(#71936,#71937,#71938,#71939));
#14704=EDGE_LOOP('',(#71940,#71941,#71942));
#14705=EDGE_LOOP('',(#71943,#71944,#71945,#71946));
#14706=EDGE_LOOP('',(#71947,#71948,#71949,#71950));
#14707=EDGE_LOOP('',(#71951,#71952,#71953,#71954));
#14708=EDGE_LOOP('',(#71955,#71956,#71957,#71958));
#14709=EDGE_LOOP('',(#71959,#71960,#71961,#71962));
#14710=EDGE_LOOP('',(#71963,#71964,#71965,#71966));
#14711=EDGE_LOOP('',(#71967,#71968,#71969,#71970));
#14712=EDGE_LOOP('',(#71971,#71972,#71973,#71974));
#14713=EDGE_LOOP('',(#71975,#71976,#71977,#71978));
#14714=EDGE_LOOP('',(#71979,#71980,#71981,#71982));
#14715=EDGE_LOOP('',(#71983,#71984,#71985,#71986));
#14716=EDGE_LOOP('',(#71987,#71988,#71989));
#14717=EDGE_LOOP('',(#71990,#71991,#71992,#71993,#71994));
#14718=EDGE_LOOP('',(#71995,#71996,#71997,#71998,#71999));
#14719=EDGE_LOOP('',(#72000,#72001,#72002,#72003));
#14720=EDGE_LOOP('',(#72004,#72005,#72006,#72007));
#14721=EDGE_LOOP('',(#72008,#72009,#72010));
#14722=EDGE_LOOP('',(#72011,#72012,#72013,#72014));
#14723=EDGE_LOOP('',(#72015,#72016,#72017,#72018));
#14724=EDGE_LOOP('',(#72019,#72020,#72021,#72022));
#14725=EDGE_LOOP('',(#72023,#72024,#72025,#72026));
#14726=EDGE_LOOP('',(#72027,#72028,#72029,#72030));
#14727=EDGE_LOOP('',(#72031,#72032,#72033,#72034));
#14728=EDGE_LOOP('',(#72035,#72036,#72037,#72038));
#14729=EDGE_LOOP('',(#72039,#72040,#72041,#72042));
#14730=EDGE_LOOP('',(#72043,#72044,#72045,#72046));
#14731=EDGE_LOOP('',(#72047,#72048,#72049,#72050));
#14732=EDGE_LOOP('',(#72051,#72052,#72053,#72054));
#14733=EDGE_LOOP('',(#72055,#72056,#72057));
#14734=EDGE_LOOP('',(#72058,#72059,#72060,#72061,#72062));
#14735=EDGE_LOOP('',(#72063,#72064,#72065,#72066,#72067));
#14736=EDGE_LOOP('',(#72068,#72069,#72070,#72071));
#14737=EDGE_LOOP('',(#72072,#72073,#72074,#72075));
#14738=EDGE_LOOP('',(#72076,#72077,#72078));
#14739=EDGE_LOOP('',(#72079,#72080,#72081,#72082));
#14740=EDGE_LOOP('',(#72083,#72084,#72085,#72086));
#14741=EDGE_LOOP('',(#72087,#72088,#72089,#72090));
#14742=EDGE_LOOP('',(#72091,#72092,#72093,#72094));
#14743=EDGE_LOOP('',(#72095,#72096,#72097,#72098));
#14744=EDGE_LOOP('',(#72099,#72100,#72101,#72102));
#14745=EDGE_LOOP('',(#72103,#72104,#72105,#72106));
#14746=EDGE_LOOP('',(#72107,#72108,#72109,#72110));
#14747=EDGE_LOOP('',(#72111,#72112,#72113,#72114));
#14748=EDGE_LOOP('',(#72115,#72116,#72117,#72118));
#14749=EDGE_LOOP('',(#72119,#72120,#72121,#72122));
#14750=EDGE_LOOP('',(#72123,#72124,#72125));
#14751=EDGE_LOOP('',(#72126,#72127,#72128,#72129,#72130));
#14752=EDGE_LOOP('',(#72131,#72132,#72133,#72134,#72135));
#14753=EDGE_LOOP('',(#72136,#72137,#72138,#72139));
#14754=EDGE_LOOP('',(#72140,#72141,#72142,#72143));
#14755=EDGE_LOOP('',(#72144,#72145,#72146));
#14756=EDGE_LOOP('',(#72147,#72148,#72149,#72150));
#14757=EDGE_LOOP('',(#72151,#72152,#72153,#72154));
#14758=EDGE_LOOP('',(#72155,#72156,#72157,#72158));
#14759=EDGE_LOOP('',(#72159,#72160,#72161,#72162));
#14760=EDGE_LOOP('',(#72163,#72164,#72165,#72166));
#14761=EDGE_LOOP('',(#72167,#72168,#72169,#72170));
#14762=EDGE_LOOP('',(#72171,#72172,#72173,#72174));
#14763=EDGE_LOOP('',(#72175,#72176,#72177,#72178));
#14764=EDGE_LOOP('',(#72179,#72180,#72181,#72182));
#14765=EDGE_LOOP('',(#72183,#72184,#72185,#72186));
#14766=EDGE_LOOP('',(#72187,#72188,#72189,#72190));
#14767=EDGE_LOOP('',(#72191,#72192,#72193));
#14768=EDGE_LOOP('',(#72194,#72195,#72196,#72197,#72198));
#14769=EDGE_LOOP('',(#72199,#72200,#72201,#72202,#72203));
#14770=EDGE_LOOP('',(#72204,#72205,#72206,#72207));
#14771=EDGE_LOOP('',(#72208,#72209,#72210,#72211));
#14772=EDGE_LOOP('',(#72212,#72213,#72214));
#14773=EDGE_LOOP('',(#72215,#72216,#72217,#72218));
#14774=EDGE_LOOP('',(#72219,#72220,#72221,#72222));
#14775=EDGE_LOOP('',(#72223,#72224,#72225,#72226));
#14776=EDGE_LOOP('',(#72227,#72228,#72229,#72230));
#14777=EDGE_LOOP('',(#72231,#72232,#72233,#72234));
#14778=EDGE_LOOP('',(#72235,#72236,#72237,#72238));
#14779=EDGE_LOOP('',(#72239,#72240,#72241,#72242));
#14780=EDGE_LOOP('',(#72243,#72244,#72245,#72246));
#14781=EDGE_LOOP('',(#72247,#72248,#72249,#72250));
#14782=EDGE_LOOP('',(#72251,#72252,#72253,#72254));
#14783=EDGE_LOOP('',(#72255,#72256,#72257,#72258));
#14784=EDGE_LOOP('',(#72259,#72260,#72261));
#14785=EDGE_LOOP('',(#72262,#72263,#72264,#72265,#72266));
#14786=EDGE_LOOP('',(#72267,#72268,#72269,#72270,#72271));
#14787=EDGE_LOOP('',(#72272,#72273,#72274,#72275));
#14788=EDGE_LOOP('',(#72276,#72277,#72278,#72279));
#14789=EDGE_LOOP('',(#72280,#72281,#72282));
#14790=EDGE_LOOP('',(#72283,#72284,#72285,#72286));
#14791=EDGE_LOOP('',(#72287,#72288,#72289,#72290));
#14792=EDGE_LOOP('',(#72291,#72292,#72293,#72294));
#14793=EDGE_LOOP('',(#72295,#72296,#72297,#72298));
#14794=EDGE_LOOP('',(#72299,#72300,#72301,#72302));
#14795=EDGE_LOOP('',(#72303,#72304,#72305,#72306));
#14796=EDGE_LOOP('',(#72307,#72308,#72309,#72310));
#14797=EDGE_LOOP('',(#72311,#72312,#72313,#72314));
#14798=EDGE_LOOP('',(#72315,#72316,#72317,#72318));
#14799=EDGE_LOOP('',(#72319,#72320,#72321,#72322));
#14800=EDGE_LOOP('',(#72323,#72324,#72325,#72326));
#14801=EDGE_LOOP('',(#72327,#72328,#72329));
#14802=EDGE_LOOP('',(#72330,#72331,#72332,#72333,#72334));
#14803=EDGE_LOOP('',(#72335,#72336,#72337,#72338,#72339));
#14804=EDGE_LOOP('',(#72340,#72341,#72342,#72343));
#14805=EDGE_LOOP('',(#72344,#72345,#72346,#72347));
#14806=EDGE_LOOP('',(#72348,#72349,#72350));
#14807=EDGE_LOOP('',(#72351,#72352,#72353,#72354));
#14808=EDGE_LOOP('',(#72355,#72356,#72357,#72358));
#14809=EDGE_LOOP('',(#72359,#72360,#72361,#72362));
#14810=EDGE_LOOP('',(#72363,#72364,#72365,#72366));
#14811=EDGE_LOOP('',(#72367,#72368,#72369,#72370));
#14812=EDGE_LOOP('',(#72371,#72372,#72373,#72374));
#14813=EDGE_LOOP('',(#72375,#72376,#72377,#72378));
#14814=EDGE_LOOP('',(#72379,#72380,#72381,#72382));
#14815=EDGE_LOOP('',(#72383,#72384,#72385,#72386));
#14816=EDGE_LOOP('',(#72387,#72388,#72389,#72390));
#14817=EDGE_LOOP('',(#72391,#72392,#72393,#72394));
#14818=EDGE_LOOP('',(#72395,#72396,#72397));
#14819=EDGE_LOOP('',(#72398,#72399,#72400,#72401,#72402));
#14820=EDGE_LOOP('',(#72403,#72404,#72405,#72406,#72407));
#14821=EDGE_LOOP('',(#72408,#72409,#72410,#72411));
#14822=EDGE_LOOP('',(#72412,#72413,#72414,#72415));
#14823=EDGE_LOOP('',(#72416,#72417,#72418));
#14824=EDGE_LOOP('',(#72419,#72420,#72421,#72422));
#14825=EDGE_LOOP('',(#72423,#72424,#72425,#72426));
#14826=EDGE_LOOP('',(#72427,#72428,#72429,#72430));
#14827=EDGE_LOOP('',(#72431,#72432,#72433,#72434));
#14828=EDGE_LOOP('',(#72435,#72436,#72437,#72438));
#14829=EDGE_LOOP('',(#72439,#72440,#72441,#72442));
#14830=EDGE_LOOP('',(#72443,#72444,#72445,#72446));
#14831=EDGE_LOOP('',(#72447,#72448,#72449,#72450));
#14832=EDGE_LOOP('',(#72451,#72452,#72453,#72454));
#14833=EDGE_LOOP('',(#72455,#72456,#72457,#72458));
#14834=EDGE_LOOP('',(#72459,#72460,#72461,#72462));
#14835=EDGE_LOOP('',(#72463,#72464,#72465));
#14836=EDGE_LOOP('',(#72466,#72467,#72468,#72469,#72470));
#14837=EDGE_LOOP('',(#72471,#72472,#72473,#72474,#72475));
#14838=EDGE_LOOP('',(#72476,#72477,#72478,#72479));
#14839=EDGE_LOOP('',(#72480,#72481,#72482,#72483));
#14840=EDGE_LOOP('',(#72484,#72485,#72486));
#14841=EDGE_LOOP('',(#72487,#72488,#72489,#72490));
#14842=EDGE_LOOP('',(#72491,#72492,#72493,#72494));
#14843=EDGE_LOOP('',(#72495,#72496,#72497,#72498));
#14844=EDGE_LOOP('',(#72499,#72500,#72501,#72502));
#14845=EDGE_LOOP('',(#72503,#72504,#72505,#72506));
#14846=EDGE_LOOP('',(#72507,#72508,#72509,#72510));
#14847=EDGE_LOOP('',(#72511,#72512,#72513,#72514));
#14848=EDGE_LOOP('',(#72515,#72516,#72517,#72518));
#14849=EDGE_LOOP('',(#72519,#72520,#72521,#72522));
#14850=EDGE_LOOP('',(#72523,#72524,#72525,#72526));
#14851=EDGE_LOOP('',(#72527,#72528,#72529,#72530));
#14852=EDGE_LOOP('',(#72531,#72532,#72533));
#14853=EDGE_LOOP('',(#72534,#72535,#72536,#72537,#72538));
#14854=EDGE_LOOP('',(#72539,#72540,#72541,#72542,#72543));
#14855=EDGE_LOOP('',(#72544,#72545,#72546,#72547));
#14856=EDGE_LOOP('',(#72548,#72549,#72550,#72551));
#14857=EDGE_LOOP('',(#72552,#72553,#72554));
#14858=EDGE_LOOP('',(#72555,#72556,#72557,#72558));
#14859=EDGE_LOOP('',(#72559,#72560,#72561,#72562));
#14860=EDGE_LOOP('',(#72563,#72564,#72565,#72566));
#14861=EDGE_LOOP('',(#72567,#72568,#72569,#72570));
#14862=EDGE_LOOP('',(#72571,#72572,#72573,#72574));
#14863=EDGE_LOOP('',(#72575,#72576,#72577,#72578));
#14864=EDGE_LOOP('',(#72579,#72580,#72581,#72582));
#14865=EDGE_LOOP('',(#72583,#72584,#72585,#72586));
#14866=EDGE_LOOP('',(#72587,#72588,#72589,#72590));
#14867=EDGE_LOOP('',(#72591,#72592,#72593,#72594));
#14868=EDGE_LOOP('',(#72595,#72596,#72597,#72598));
#14869=EDGE_LOOP('',(#72599,#72600,#72601));
#14870=EDGE_LOOP('',(#72602,#72603,#72604,#72605,#72606));
#14871=EDGE_LOOP('',(#72607,#72608,#72609,#72610,#72611));
#14872=EDGE_LOOP('',(#72612,#72613,#72614,#72615));
#14873=EDGE_LOOP('',(#72616,#72617,#72618,#72619));
#14874=EDGE_LOOP('',(#72620,#72621,#72622));
#14875=EDGE_LOOP('',(#72623,#72624,#72625,#72626));
#14876=EDGE_LOOP('',(#72627,#72628,#72629,#72630));
#14877=EDGE_LOOP('',(#72631,#72632,#72633,#72634));
#14878=EDGE_LOOP('',(#72635,#72636,#72637,#72638));
#14879=EDGE_LOOP('',(#72639,#72640,#72641,#72642));
#14880=EDGE_LOOP('',(#72643,#72644,#72645,#72646));
#14881=EDGE_LOOP('',(#72647,#72648,#72649,#72650));
#14882=EDGE_LOOP('',(#72651,#72652,#72653,#72654));
#14883=EDGE_LOOP('',(#72655,#72656,#72657,#72658));
#14884=EDGE_LOOP('',(#72659,#72660,#72661,#72662));
#14885=EDGE_LOOP('',(#72663,#72664,#72665,#72666));
#14886=EDGE_LOOP('',(#72667,#72668,#72669));
#14887=EDGE_LOOP('',(#72670,#72671,#72672,#72673,#72674));
#14888=EDGE_LOOP('',(#72675,#72676,#72677,#72678,#72679));
#14889=EDGE_LOOP('',(#72680,#72681,#72682,#72683));
#14890=EDGE_LOOP('',(#72684,#72685,#72686,#72687));
#14891=EDGE_LOOP('',(#72688,#72689,#72690));
#14892=EDGE_LOOP('',(#72691,#72692,#72693,#72694));
#14893=EDGE_LOOP('',(#72695,#72696,#72697,#72698));
#14894=EDGE_LOOP('',(#72699,#72700,#72701,#72702));
#14895=EDGE_LOOP('',(#72703,#72704,#72705,#72706));
#14896=EDGE_LOOP('',(#72707,#72708,#72709,#72710));
#14897=EDGE_LOOP('',(#72711,#72712,#72713,#72714));
#14898=EDGE_LOOP('',(#72715,#72716,#72717,#72718));
#14899=EDGE_LOOP('',(#72719,#72720,#72721,#72722));
#14900=EDGE_LOOP('',(#72723,#72724,#72725,#72726));
#14901=EDGE_LOOP('',(#72727,#72728,#72729,#72730));
#14902=EDGE_LOOP('',(#72731,#72732,#72733,#72734));
#14903=EDGE_LOOP('',(#72735,#72736,#72737));
#14904=EDGE_LOOP('',(#72738,#72739,#72740,#72741,#72742));
#14905=EDGE_LOOP('',(#72743,#72744,#72745,#72746,#72747));
#14906=EDGE_LOOP('',(#72748,#72749,#72750,#72751));
#14907=EDGE_LOOP('',(#72752,#72753,#72754,#72755));
#14908=EDGE_LOOP('',(#72756,#72757,#72758));
#14909=EDGE_LOOP('',(#72759,#72760,#72761,#72762));
#14910=EDGE_LOOP('',(#72763,#72764,#72765,#72766));
#14911=EDGE_LOOP('',(#72767,#72768,#72769,#72770));
#14912=EDGE_LOOP('',(#72771,#72772,#72773,#72774));
#14913=EDGE_LOOP('',(#72775,#72776,#72777,#72778));
#14914=EDGE_LOOP('',(#72779,#72780,#72781,#72782));
#14915=EDGE_LOOP('',(#72783,#72784,#72785,#72786));
#14916=EDGE_LOOP('',(#72787,#72788,#72789,#72790));
#14917=EDGE_LOOP('',(#72791,#72792,#72793,#72794));
#14918=EDGE_LOOP('',(#72795,#72796,#72797,#72798));
#14919=EDGE_LOOP('',(#72799,#72800,#72801,#72802));
#14920=EDGE_LOOP('',(#72803,#72804,#72805));
#14921=EDGE_LOOP('',(#72806,#72807,#72808,#72809,#72810));
#14922=EDGE_LOOP('',(#72811,#72812,#72813,#72814,#72815));
#14923=EDGE_LOOP('',(#72816,#72817,#72818,#72819));
#14924=EDGE_LOOP('',(#72820,#72821,#72822,#72823));
#14925=EDGE_LOOP('',(#72824,#72825,#72826));
#14926=EDGE_LOOP('',(#72827,#72828,#72829,#72830));
#14927=EDGE_LOOP('',(#72831,#72832,#72833,#72834));
#14928=EDGE_LOOP('',(#72835,#72836,#72837,#72838));
#14929=EDGE_LOOP('',(#72839,#72840,#72841,#72842));
#14930=EDGE_LOOP('',(#72843,#72844,#72845,#72846));
#14931=EDGE_LOOP('',(#72847,#72848,#72849,#72850));
#14932=EDGE_LOOP('',(#72851,#72852,#72853,#72854));
#14933=EDGE_LOOP('',(#72855,#72856,#72857,#72858));
#14934=EDGE_LOOP('',(#72859,#72860,#72861,#72862));
#14935=EDGE_LOOP('',(#72863,#72864,#72865,#72866));
#14936=EDGE_LOOP('',(#72867,#72868,#72869,#72870));
#14937=EDGE_LOOP('',(#72871,#72872,#72873));
#14938=EDGE_LOOP('',(#72874,#72875,#72876,#72877,#72878));
#14939=EDGE_LOOP('',(#72879,#72880,#72881,#72882,#72883));
#14940=EDGE_LOOP('',(#72884,#72885,#72886,#72887));
#14941=EDGE_LOOP('',(#72888,#72889,#72890,#72891));
#14942=EDGE_LOOP('',(#72892,#72893,#72894));
#14943=EDGE_LOOP('',(#72895,#72896,#72897,#72898));
#14944=EDGE_LOOP('',(#72899,#72900,#72901,#72902));
#14945=EDGE_LOOP('',(#72903,#72904,#72905,#72906));
#14946=EDGE_LOOP('',(#72907,#72908,#72909,#72910));
#14947=EDGE_LOOP('',(#72911,#72912,#72913,#72914));
#14948=EDGE_LOOP('',(#72915,#72916,#72917,#72918));
#14949=EDGE_LOOP('',(#72919,#72920,#72921,#72922));
#14950=EDGE_LOOP('',(#72923,#72924,#72925,#72926));
#14951=EDGE_LOOP('',(#72927,#72928,#72929,#72930));
#14952=EDGE_LOOP('',(#72931,#72932,#72933,#72934));
#14953=EDGE_LOOP('',(#72935,#72936,#72937,#72938));
#14954=EDGE_LOOP('',(#72939,#72940,#72941));
#14955=EDGE_LOOP('',(#72942,#72943,#72944,#72945,#72946));
#14956=EDGE_LOOP('',(#72947,#72948,#72949,#72950,#72951));
#14957=EDGE_LOOP('',(#72952,#72953,#72954,#72955));
#14958=EDGE_LOOP('',(#72956,#72957,#72958,#72959));
#14959=EDGE_LOOP('',(#72960,#72961,#72962));
#14960=EDGE_LOOP('',(#72963,#72964,#72965,#72966));
#14961=EDGE_LOOP('',(#72967,#72968,#72969,#72970));
#14962=EDGE_LOOP('',(#72971,#72972,#72973,#72974));
#14963=EDGE_LOOP('',(#72975,#72976,#72977,#72978));
#14964=EDGE_LOOP('',(#72979,#72980,#72981,#72982));
#14965=EDGE_LOOP('',(#72983,#72984,#72985,#72986));
#14966=EDGE_LOOP('',(#72987,#72988,#72989,#72990));
#14967=EDGE_LOOP('',(#72991,#72992,#72993,#72994));
#14968=EDGE_LOOP('',(#72995,#72996,#72997,#72998));
#14969=EDGE_LOOP('',(#72999,#73000,#73001,#73002));
#14970=EDGE_LOOP('',(#73003,#73004,#73005,#73006));
#14971=EDGE_LOOP('',(#73007,#73008,#73009));
#14972=EDGE_LOOP('',(#73010,#73011,#73012,#73013,#73014));
#14973=EDGE_LOOP('',(#73015,#73016,#73017,#73018,#73019));
#14974=EDGE_LOOP('',(#73020,#73021,#73022,#73023));
#14975=EDGE_LOOP('',(#73024,#73025,#73026,#73027));
#14976=EDGE_LOOP('',(#73028,#73029,#73030));
#14977=EDGE_LOOP('',(#73031,#73032,#73033,#73034));
#14978=EDGE_LOOP('',(#73035,#73036,#73037,#73038));
#14979=EDGE_LOOP('',(#73039,#73040,#73041,#73042));
#14980=EDGE_LOOP('',(#73043,#73044,#73045,#73046));
#14981=EDGE_LOOP('',(#73047,#73048,#73049,#73050));
#14982=EDGE_LOOP('',(#73051,#73052,#73053,#73054));
#14983=EDGE_LOOP('',(#73055,#73056,#73057,#73058));
#14984=EDGE_LOOP('',(#73059,#73060,#73061,#73062));
#14985=EDGE_LOOP('',(#73063,#73064,#73065,#73066));
#14986=EDGE_LOOP('',(#73067,#73068,#73069,#73070));
#14987=EDGE_LOOP('',(#73071,#73072,#73073,#73074));
#14988=EDGE_LOOP('',(#73075,#73076,#73077));
#14989=EDGE_LOOP('',(#73078,#73079,#73080,#73081,#73082));
#14990=EDGE_LOOP('',(#73083,#73084,#73085,#73086,#73087));
#14991=EDGE_LOOP('',(#73088,#73089,#73090,#73091));
#14992=EDGE_LOOP('',(#73092,#73093,#73094,#73095));
#14993=EDGE_LOOP('',(#73096,#73097,#73098));
#14994=EDGE_LOOP('',(#73099,#73100,#73101,#73102));
#14995=EDGE_LOOP('',(#73103,#73104,#73105,#73106));
#14996=EDGE_LOOP('',(#73107,#73108,#73109,#73110));
#14997=EDGE_LOOP('',(#73111,#73112,#73113,#73114));
#14998=EDGE_LOOP('',(#73115,#73116,#73117,#73118));
#14999=EDGE_LOOP('',(#73119,#73120,#73121,#73122));
#15000=EDGE_LOOP('',(#73123,#73124,#73125,#73126));
#15001=EDGE_LOOP('',(#73127,#73128,#73129,#73130));
#15002=EDGE_LOOP('',(#73131,#73132,#73133,#73134));
#15003=EDGE_LOOP('',(#73135,#73136,#73137,#73138));
#15004=EDGE_LOOP('',(#73139,#73140,#73141,#73142));
#15005=EDGE_LOOP('',(#73143,#73144,#73145));
#15006=EDGE_LOOP('',(#73146,#73147,#73148,#73149,#73150));
#15007=EDGE_LOOP('',(#73151,#73152,#73153,#73154,#73155));
#15008=EDGE_LOOP('',(#73156,#73157,#73158,#73159));
#15009=EDGE_LOOP('',(#73160,#73161,#73162,#73163));
#15010=EDGE_LOOP('',(#73164,#73165,#73166));
#15011=EDGE_LOOP('',(#73167,#73168,#73169,#73170));
#15012=EDGE_LOOP('',(#73171,#73172,#73173,#73174));
#15013=EDGE_LOOP('',(#73175,#73176,#73177,#73178));
#15014=EDGE_LOOP('',(#73179,#73180,#73181,#73182));
#15015=EDGE_LOOP('',(#73183,#73184,#73185,#73186));
#15016=EDGE_LOOP('',(#73187,#73188,#73189,#73190));
#15017=EDGE_LOOP('',(#73191,#73192,#73193,#73194));
#15018=EDGE_LOOP('',(#73195,#73196,#73197,#73198));
#15019=EDGE_LOOP('',(#73199,#73200,#73201,#73202));
#15020=EDGE_LOOP('',(#73203,#73204,#73205,#73206));
#15021=EDGE_LOOP('',(#73207,#73208,#73209,#73210));
#15022=EDGE_LOOP('',(#73211,#73212,#73213));
#15023=EDGE_LOOP('',(#73214,#73215,#73216,#73217,#73218));
#15024=EDGE_LOOP('',(#73219,#73220,#73221,#73222,#73223));
#15025=EDGE_LOOP('',(#73224,#73225,#73226,#73227));
#15026=EDGE_LOOP('',(#73228,#73229,#73230,#73231));
#15027=EDGE_LOOP('',(#73232,#73233,#73234));
#15028=EDGE_LOOP('',(#73235,#73236,#73237,#73238));
#15029=EDGE_LOOP('',(#73239,#73240,#73241,#73242));
#15030=EDGE_LOOP('',(#73243,#73244,#73245,#73246));
#15031=EDGE_LOOP('',(#73247,#73248,#73249,#73250));
#15032=EDGE_LOOP('',(#73251,#73252,#73253,#73254));
#15033=EDGE_LOOP('',(#73255,#73256,#73257,#73258));
#15034=EDGE_LOOP('',(#73259,#73260,#73261,#73262));
#15035=EDGE_LOOP('',(#73263,#73264,#73265,#73266));
#15036=EDGE_LOOP('',(#73267,#73268,#73269,#73270));
#15037=EDGE_LOOP('',(#73271,#73272,#73273,#73274));
#15038=EDGE_LOOP('',(#73275,#73276,#73277,#73278));
#15039=EDGE_LOOP('',(#73279,#73280,#73281));
#15040=EDGE_LOOP('',(#73282,#73283,#73284,#73285,#73286));
#15041=EDGE_LOOP('',(#73287,#73288,#73289,#73290,#73291));
#15042=EDGE_LOOP('',(#73292,#73293,#73294,#73295));
#15043=EDGE_LOOP('',(#73296,#73297,#73298,#73299));
#15044=EDGE_LOOP('',(#73300,#73301,#73302));
#15045=EDGE_LOOP('',(#73303,#73304,#73305,#73306));
#15046=EDGE_LOOP('',(#73307,#73308,#73309,#73310));
#15047=EDGE_LOOP('',(#73311,#73312,#73313,#73314));
#15048=EDGE_LOOP('',(#73315,#73316,#73317,#73318));
#15049=EDGE_LOOP('',(#73319,#73320,#73321,#73322));
#15050=EDGE_LOOP('',(#73323,#73324,#73325,#73326));
#15051=EDGE_LOOP('',(#73327,#73328,#73329,#73330));
#15052=EDGE_LOOP('',(#73331,#73332,#73333,#73334));
#15053=EDGE_LOOP('',(#73335,#73336,#73337,#73338));
#15054=EDGE_LOOP('',(#73339,#73340,#73341,#73342));
#15055=EDGE_LOOP('',(#73343,#73344,#73345,#73346));
#15056=EDGE_LOOP('',(#73347,#73348,#73349));
#15057=EDGE_LOOP('',(#73350,#73351,#73352,#73353,#73354));
#15058=EDGE_LOOP('',(#73355,#73356,#73357,#73358,#73359));
#15059=EDGE_LOOP('',(#73360,#73361,#73362,#73363));
#15060=EDGE_LOOP('',(#73364,#73365,#73366,#73367));
#15061=EDGE_LOOP('',(#73368,#73369,#73370));
#15062=EDGE_LOOP('',(#73371,#73372,#73373,#73374));
#15063=EDGE_LOOP('',(#73375,#73376,#73377,#73378));
#15064=EDGE_LOOP('',(#73379,#73380,#73381,#73382));
#15065=EDGE_LOOP('',(#73383,#73384,#73385,#73386));
#15066=EDGE_LOOP('',(#73387,#73388,#73389,#73390));
#15067=EDGE_LOOP('',(#73391,#73392,#73393,#73394));
#15068=EDGE_LOOP('',(#73395,#73396,#73397,#73398));
#15069=EDGE_LOOP('',(#73399,#73400,#73401,#73402));
#15070=EDGE_LOOP('',(#73403,#73404,#73405,#73406));
#15071=EDGE_LOOP('',(#73407,#73408,#73409,#73410));
#15072=EDGE_LOOP('',(#73411,#73412,#73413,#73414));
#15073=EDGE_LOOP('',(#73415,#73416,#73417));
#15074=EDGE_LOOP('',(#73418,#73419,#73420,#73421,#73422));
#15075=EDGE_LOOP('',(#73423,#73424,#73425,#73426,#73427));
#15076=EDGE_LOOP('',(#73428,#73429,#73430,#73431));
#15077=EDGE_LOOP('',(#73432,#73433,#73434,#73435));
#15078=EDGE_LOOP('',(#73436,#73437,#73438));
#15079=EDGE_LOOP('',(#73439,#73440,#73441,#73442));
#15080=EDGE_LOOP('',(#73443,#73444,#73445,#73446));
#15081=EDGE_LOOP('',(#73447,#73448,#73449,#73450));
#15082=EDGE_LOOP('',(#73451,#73452,#73453,#73454));
#15083=EDGE_LOOP('',(#73455,#73456,#73457,#73458));
#15084=EDGE_LOOP('',(#73459,#73460,#73461,#73462));
#15085=EDGE_LOOP('',(#73463,#73464,#73465,#73466));
#15086=EDGE_LOOP('',(#73467,#73468,#73469,#73470));
#15087=EDGE_LOOP('',(#73471,#73472,#73473,#73474));
#15088=EDGE_LOOP('',(#73475,#73476,#73477,#73478));
#15089=EDGE_LOOP('',(#73479,#73480,#73481,#73482));
#15090=EDGE_LOOP('',(#73483,#73484,#73485));
#15091=EDGE_LOOP('',(#73486,#73487,#73488,#73489,#73490));
#15092=EDGE_LOOP('',(#73491,#73492,#73493,#73494,#73495));
#15093=EDGE_LOOP('',(#73496,#73497,#73498,#73499));
#15094=EDGE_LOOP('',(#73500,#73501,#73502,#73503));
#15095=EDGE_LOOP('',(#73504,#73505,#73506));
#15096=EDGE_LOOP('',(#73507,#73508,#73509,#73510));
#15097=EDGE_LOOP('',(#73511,#73512,#73513,#73514));
#15098=EDGE_LOOP('',(#73515,#73516,#73517,#73518));
#15099=EDGE_LOOP('',(#73519,#73520,#73521,#73522));
#15100=EDGE_LOOP('',(#73523,#73524,#73525,#73526));
#15101=EDGE_LOOP('',(#73527,#73528,#73529,#73530));
#15102=EDGE_LOOP('',(#73531,#73532,#73533,#73534));
#15103=EDGE_LOOP('',(#73535,#73536,#73537,#73538));
#15104=EDGE_LOOP('',(#73539,#73540,#73541,#73542));
#15105=EDGE_LOOP('',(#73543,#73544,#73545,#73546));
#15106=EDGE_LOOP('',(#73547,#73548,#73549,#73550));
#15107=EDGE_LOOP('',(#73551,#73552,#73553));
#15108=EDGE_LOOP('',(#73554,#73555,#73556,#73557,#73558));
#15109=EDGE_LOOP('',(#73559,#73560,#73561,#73562,#73563));
#15110=EDGE_LOOP('',(#73564,#73565,#73566,#73567));
#15111=EDGE_LOOP('',(#73568,#73569,#73570,#73571));
#15112=EDGE_LOOP('',(#73572,#73573,#73574));
#15113=EDGE_LOOP('',(#73575,#73576,#73577,#73578));
#15114=EDGE_LOOP('',(#73579,#73580,#73581,#73582));
#15115=EDGE_LOOP('',(#73583,#73584,#73585,#73586));
#15116=EDGE_LOOP('',(#73587,#73588,#73589,#73590));
#15117=EDGE_LOOP('',(#73591,#73592,#73593,#73594));
#15118=EDGE_LOOP('',(#73595,#73596,#73597,#73598));
#15119=EDGE_LOOP('',(#73599,#73600,#73601,#73602));
#15120=EDGE_LOOP('',(#73603,#73604,#73605,#73606));
#15121=EDGE_LOOP('',(#73607,#73608,#73609,#73610));
#15122=EDGE_LOOP('',(#73611,#73612,#73613,#73614));
#15123=EDGE_LOOP('',(#73615,#73616,#73617,#73618));
#15124=EDGE_LOOP('',(#73619,#73620,#73621));
#15125=EDGE_LOOP('',(#73622,#73623,#73624,#73625,#73626));
#15126=EDGE_LOOP('',(#73627,#73628,#73629,#73630,#73631));
#15127=EDGE_LOOP('',(#73632,#73633,#73634,#73635));
#15128=EDGE_LOOP('',(#73636,#73637,#73638,#73639));
#15129=EDGE_LOOP('',(#73640,#73641,#73642));
#15130=EDGE_LOOP('',(#73643,#73644,#73645,#73646));
#15131=EDGE_LOOP('',(#73647,#73648,#73649,#73650));
#15132=EDGE_LOOP('',(#73651,#73652,#73653,#73654));
#15133=EDGE_LOOP('',(#73655,#73656,#73657,#73658));
#15134=EDGE_LOOP('',(#73659,#73660,#73661,#73662));
#15135=EDGE_LOOP('',(#73663,#73664,#73665,#73666));
#15136=EDGE_LOOP('',(#73667,#73668,#73669,#73670));
#15137=EDGE_LOOP('',(#73671,#73672,#73673,#73674));
#15138=EDGE_LOOP('',(#73675,#73676,#73677,#73678));
#15139=EDGE_LOOP('',(#73679,#73680,#73681,#73682));
#15140=EDGE_LOOP('',(#73683,#73684,#73685,#73686));
#15141=EDGE_LOOP('',(#73687,#73688,#73689));
#15142=EDGE_LOOP('',(#73690,#73691,#73692,#73693,#73694));
#15143=EDGE_LOOP('',(#73695,#73696,#73697,#73698,#73699));
#15144=EDGE_LOOP('',(#73700,#73701,#73702,#73703));
#15145=EDGE_LOOP('',(#73704,#73705,#73706,#73707));
#15146=EDGE_LOOP('',(#73708,#73709,#73710));
#15147=EDGE_LOOP('',(#73711,#73712,#73713,#73714));
#15148=EDGE_LOOP('',(#73715,#73716,#73717,#73718));
#15149=EDGE_LOOP('',(#73719,#73720,#73721,#73722));
#15150=EDGE_LOOP('',(#73723,#73724,#73725,#73726));
#15151=EDGE_LOOP('',(#73727,#73728,#73729,#73730));
#15152=EDGE_LOOP('',(#73731,#73732,#73733,#73734));
#15153=EDGE_LOOP('',(#73735,#73736,#73737,#73738));
#15154=EDGE_LOOP('',(#73739,#73740,#73741,#73742));
#15155=EDGE_LOOP('',(#73743,#73744,#73745,#73746));
#15156=EDGE_LOOP('',(#73747,#73748,#73749,#73750));
#15157=EDGE_LOOP('',(#73751,#73752,#73753,#73754));
#15158=EDGE_LOOP('',(#73755,#73756,#73757));
#15159=EDGE_LOOP('',(#73758,#73759,#73760,#73761,#73762));
#15160=EDGE_LOOP('',(#73763,#73764,#73765,#73766,#73767));
#15161=EDGE_LOOP('',(#73768,#73769,#73770,#73771));
#15162=EDGE_LOOP('',(#73772,#73773,#73774,#73775));
#15163=EDGE_LOOP('',(#73776,#73777,#73778));
#15164=EDGE_LOOP('',(#73779,#73780,#73781,#73782));
#15165=EDGE_LOOP('',(#73783,#73784,#73785,#73786));
#15166=EDGE_LOOP('',(#73787,#73788,#73789,#73790));
#15167=EDGE_LOOP('',(#73791,#73792,#73793,#73794));
#15168=EDGE_LOOP('',(#73795,#73796,#73797,#73798));
#15169=EDGE_LOOP('',(#73799,#73800,#73801,#73802));
#15170=EDGE_LOOP('',(#73803,#73804,#73805,#73806));
#15171=EDGE_LOOP('',(#73807,#73808,#73809,#73810));
#15172=EDGE_LOOP('',(#73811,#73812,#73813,#73814));
#15173=EDGE_LOOP('',(#73815,#73816,#73817,#73818));
#15174=EDGE_LOOP('',(#73819,#73820,#73821,#73822));
#15175=EDGE_LOOP('',(#73823,#73824,#73825));
#15176=EDGE_LOOP('',(#73826,#73827,#73828,#73829,#73830));
#15177=EDGE_LOOP('',(#73831,#73832,#73833,#73834,#73835));
#15178=EDGE_LOOP('',(#73836,#73837,#73838,#73839));
#15179=EDGE_LOOP('',(#73840,#73841,#73842,#73843));
#15180=EDGE_LOOP('',(#73844,#73845,#73846));
#15181=EDGE_LOOP('',(#73847,#73848,#73849,#73850));
#15182=EDGE_LOOP('',(#73851,#73852,#73853,#73854));
#15183=EDGE_LOOP('',(#73855,#73856,#73857,#73858));
#15184=EDGE_LOOP('',(#73859,#73860,#73861,#73862));
#15185=EDGE_LOOP('',(#73863,#73864,#73865,#73866));
#15186=EDGE_LOOP('',(#73867,#73868,#73869,#73870));
#15187=EDGE_LOOP('',(#73871,#73872,#73873,#73874));
#15188=EDGE_LOOP('',(#73875,#73876,#73877,#73878));
#15189=EDGE_LOOP('',(#73879,#73880,#73881,#73882));
#15190=EDGE_LOOP('',(#73883,#73884,#73885,#73886));
#15191=EDGE_LOOP('',(#73887,#73888,#73889,#73890));
#15192=EDGE_LOOP('',(#73891,#73892,#73893));
#15193=EDGE_LOOP('',(#73894,#73895,#73896,#73897,#73898));
#15194=EDGE_LOOP('',(#73899,#73900,#73901,#73902,#73903));
#15195=EDGE_LOOP('',(#73904,#73905,#73906,#73907));
#15196=EDGE_LOOP('',(#73908,#73909,#73910,#73911));
#15197=EDGE_LOOP('',(#73912,#73913,#73914));
#15198=EDGE_LOOP('',(#73915,#73916,#73917,#73918));
#15199=EDGE_LOOP('',(#73919,#73920,#73921,#73922));
#15200=EDGE_LOOP('',(#73923,#73924,#73925,#73926));
#15201=EDGE_LOOP('',(#73927,#73928,#73929,#73930));
#15202=EDGE_LOOP('',(#73931,#73932,#73933,#73934));
#15203=EDGE_LOOP('',(#73935,#73936,#73937,#73938));
#15204=EDGE_LOOP('',(#73939,#73940,#73941,#73942));
#15205=EDGE_LOOP('',(#73943,#73944,#73945,#73946));
#15206=EDGE_LOOP('',(#73947,#73948,#73949,#73950));
#15207=EDGE_LOOP('',(#73951,#73952,#73953,#73954));
#15208=EDGE_LOOP('',(#73955,#73956,#73957,#73958));
#15209=EDGE_LOOP('',(#73959,#73960,#73961));
#15210=EDGE_LOOP('',(#73962,#73963,#73964,#73965,#73966));
#15211=EDGE_LOOP('',(#73967,#73968,#73969,#73970,#73971));
#15212=EDGE_LOOP('',(#73972,#73973,#73974,#73975));
#15213=EDGE_LOOP('',(#73976,#73977,#73978,#73979));
#15214=EDGE_LOOP('',(#73980,#73981,#73982));
#15215=EDGE_LOOP('',(#73983,#73984,#73985,#73986));
#15216=EDGE_LOOP('',(#73987,#73988,#73989,#73990));
#15217=EDGE_LOOP('',(#73991,#73992,#73993,#73994));
#15218=EDGE_LOOP('',(#73995,#73996,#73997,#73998));
#15219=EDGE_LOOP('',(#73999,#74000,#74001,#74002));
#15220=EDGE_LOOP('',(#74003,#74004,#74005,#74006));
#15221=EDGE_LOOP('',(#74007,#74008,#74009,#74010));
#15222=EDGE_LOOP('',(#74011,#74012,#74013,#74014));
#15223=EDGE_LOOP('',(#74015,#74016,#74017,#74018));
#15224=EDGE_LOOP('',(#74019,#74020,#74021,#74022));
#15225=EDGE_LOOP('',(#74023,#74024,#74025,#74026));
#15226=EDGE_LOOP('',(#74027,#74028,#74029));
#15227=EDGE_LOOP('',(#74030,#74031,#74032,#74033,#74034));
#15228=EDGE_LOOP('',(#74035,#74036,#74037,#74038,#74039));
#15229=EDGE_LOOP('',(#74040,#74041,#74042,#74043));
#15230=EDGE_LOOP('',(#74044,#74045,#74046,#74047));
#15231=EDGE_LOOP('',(#74048,#74049,#74050));
#15232=EDGE_LOOP('',(#74051,#74052,#74053,#74054));
#15233=EDGE_LOOP('',(#74055,#74056,#74057,#74058));
#15234=EDGE_LOOP('',(#74059,#74060,#74061,#74062));
#15235=EDGE_LOOP('',(#74063,#74064,#74065,#74066));
#15236=EDGE_LOOP('',(#74067,#74068,#74069,#74070));
#15237=EDGE_LOOP('',(#74071,#74072,#74073,#74074));
#15238=EDGE_LOOP('',(#74075,#74076,#74077,#74078));
#15239=EDGE_LOOP('',(#74079,#74080,#74081,#74082));
#15240=EDGE_LOOP('',(#74083,#74084,#74085,#74086));
#15241=EDGE_LOOP('',(#74087,#74088,#74089,#74090));
#15242=EDGE_LOOP('',(#74091,#74092,#74093,#74094));
#15243=EDGE_LOOP('',(#74095,#74096,#74097));
#15244=EDGE_LOOP('',(#74098,#74099,#74100,#74101,#74102));
#15245=EDGE_LOOP('',(#74103,#74104,#74105,#74106,#74107));
#15246=EDGE_LOOP('',(#74108,#74109,#74110,#74111));
#15247=EDGE_LOOP('',(#74112,#74113,#74114,#74115));
#15248=EDGE_LOOP('',(#74116,#74117,#74118));
#15249=EDGE_LOOP('',(#74119,#74120,#74121,#74122));
#15250=EDGE_LOOP('',(#74123,#74124,#74125,#74126));
#15251=EDGE_LOOP('',(#74127,#74128,#74129,#74130));
#15252=EDGE_LOOP('',(#74131,#74132,#74133,#74134));
#15253=EDGE_LOOP('',(#74135,#74136,#74137,#74138));
#15254=EDGE_LOOP('',(#74139,#74140,#74141,#74142));
#15255=EDGE_LOOP('',(#74143,#74144,#74145,#74146));
#15256=EDGE_LOOP('',(#74147,#74148,#74149,#74150));
#15257=EDGE_LOOP('',(#74151,#74152,#74153,#74154));
#15258=EDGE_LOOP('',(#74155,#74156,#74157,#74158));
#15259=EDGE_LOOP('',(#74159,#74160,#74161,#74162));
#15260=EDGE_LOOP('',(#74163,#74164,#74165));
#15261=EDGE_LOOP('',(#74166,#74167,#74168,#74169,#74170));
#15262=EDGE_LOOP('',(#74171,#74172,#74173,#74174,#74175));
#15263=EDGE_LOOP('',(#74176,#74177,#74178,#74179));
#15264=EDGE_LOOP('',(#74180,#74181,#74182,#74183));
#15265=EDGE_LOOP('',(#74184,#74185,#74186));
#15266=EDGE_LOOP('',(#74187,#74188,#74189,#74190));
#15267=EDGE_LOOP('',(#74191,#74192,#74193,#74194));
#15268=EDGE_LOOP('',(#74195,#74196,#74197,#74198));
#15269=EDGE_LOOP('',(#74199,#74200,#74201,#74202));
#15270=EDGE_LOOP('',(#74203,#74204,#74205,#74206));
#15271=EDGE_LOOP('',(#74207,#74208,#74209,#74210));
#15272=EDGE_LOOP('',(#74211,#74212,#74213,#74214));
#15273=EDGE_LOOP('',(#74215,#74216,#74217,#74218));
#15274=EDGE_LOOP('',(#74219,#74220,#74221,#74222));
#15275=EDGE_LOOP('',(#74223,#74224,#74225,#74226));
#15276=EDGE_LOOP('',(#74227,#74228,#74229,#74230));
#15277=EDGE_LOOP('',(#74231,#74232,#74233));
#15278=EDGE_LOOP('',(#74234,#74235,#74236,#74237,#74238));
#15279=EDGE_LOOP('',(#74239,#74240,#74241,#74242,#74243));
#15280=EDGE_LOOP('',(#74244,#74245,#74246,#74247));
#15281=EDGE_LOOP('',(#74248,#74249,#74250,#74251));
#15282=EDGE_LOOP('',(#74252,#74253,#74254));
#15283=EDGE_LOOP('',(#74255,#74256,#74257,#74258));
#15284=EDGE_LOOP('',(#74259,#74260,#74261,#74262));
#15285=EDGE_LOOP('',(#74263,#74264,#74265,#74266));
#15286=EDGE_LOOP('',(#74267,#74268,#74269,#74270));
#15287=EDGE_LOOP('',(#74271,#74272,#74273,#74274));
#15288=EDGE_LOOP('',(#74275,#74276,#74277,#74278));
#15289=EDGE_LOOP('',(#74279,#74280,#74281,#74282));
#15290=EDGE_LOOP('',(#74283,#74284,#74285,#74286));
#15291=EDGE_LOOP('',(#74287,#74288,#74289,#74290));
#15292=EDGE_LOOP('',(#74291,#74292,#74293,#74294));
#15293=EDGE_LOOP('',(#74295,#74296,#74297,#74298));
#15294=EDGE_LOOP('',(#74299,#74300,#74301));
#15295=EDGE_LOOP('',(#74302,#74303,#74304,#74305,#74306));
#15296=EDGE_LOOP('',(#74307,#74308,#74309,#74310,#74311));
#15297=EDGE_LOOP('',(#74312,#74313,#74314,#74315));
#15298=EDGE_LOOP('',(#74316,#74317,#74318,#74319));
#15299=EDGE_LOOP('',(#74320,#74321,#74322));
#15300=EDGE_LOOP('',(#74323,#74324,#74325,#74326));
#15301=EDGE_LOOP('',(#74327,#74328,#74329,#74330));
#15302=EDGE_LOOP('',(#74331,#74332,#74333,#74334));
#15303=EDGE_LOOP('',(#74335,#74336,#74337,#74338));
#15304=EDGE_LOOP('',(#74339,#74340,#74341,#74342));
#15305=EDGE_LOOP('',(#74343,#74344,#74345,#74346));
#15306=EDGE_LOOP('',(#74347,#74348,#74349,#74350));
#15307=EDGE_LOOP('',(#74351,#74352,#74353,#74354));
#15308=EDGE_LOOP('',(#74355,#74356,#74357,#74358));
#15309=EDGE_LOOP('',(#74359,#74360,#74361,#74362));
#15310=EDGE_LOOP('',(#74363,#74364,#74365,#74366));
#15311=EDGE_LOOP('',(#74367,#74368,#74369));
#15312=EDGE_LOOP('',(#74370,#74371,#74372,#74373,#74374));
#15313=EDGE_LOOP('',(#74375,#74376,#74377,#74378,#74379));
#15314=EDGE_LOOP('',(#74380,#74381,#74382,#74383));
#15315=EDGE_LOOP('',(#74384,#74385,#74386,#74387));
#15316=EDGE_LOOP('',(#74388,#74389,#74390));
#15317=EDGE_LOOP('',(#74391,#74392,#74393,#74394));
#15318=EDGE_LOOP('',(#74395,#74396,#74397,#74398));
#15319=EDGE_LOOP('',(#74399,#74400,#74401,#74402));
#15320=EDGE_LOOP('',(#74403,#74404,#74405,#74406));
#15321=EDGE_LOOP('',(#74407,#74408,#74409,#74410));
#15322=EDGE_LOOP('',(#74411,#74412,#74413,#74414));
#15323=EDGE_LOOP('',(#74415,#74416,#74417,#74418));
#15324=EDGE_LOOP('',(#74419,#74420,#74421,#74422));
#15325=EDGE_LOOP('',(#74423,#74424,#74425,#74426));
#15326=EDGE_LOOP('',(#74427,#74428,#74429,#74430));
#15327=EDGE_LOOP('',(#74431,#74432,#74433,#74434));
#15328=EDGE_LOOP('',(#74435,#74436,#74437));
#15329=EDGE_LOOP('',(#74438,#74439,#74440,#74441,#74442));
#15330=EDGE_LOOP('',(#74443,#74444,#74445,#74446,#74447));
#15331=EDGE_LOOP('',(#74448,#74449,#74450,#74451));
#15332=EDGE_LOOP('',(#74452,#74453,#74454,#74455));
#15333=EDGE_LOOP('',(#74456,#74457,#74458));
#15334=EDGE_LOOP('',(#74459,#74460,#74461,#74462));
#15335=EDGE_LOOP('',(#74463,#74464,#74465,#74466));
#15336=EDGE_LOOP('',(#74467,#74468,#74469,#74470));
#15337=EDGE_LOOP('',(#74471,#74472,#74473,#74474));
#15338=EDGE_LOOP('',(#74475,#74476,#74477,#74478));
#15339=EDGE_LOOP('',(#74479,#74480,#74481,#74482));
#15340=EDGE_LOOP('',(#74483,#74484,#74485,#74486));
#15341=EDGE_LOOP('',(#74487,#74488,#74489,#74490));
#15342=EDGE_LOOP('',(#74491,#74492,#74493,#74494));
#15343=EDGE_LOOP('',(#74495,#74496,#74497,#74498));
#15344=EDGE_LOOP('',(#74499,#74500,#74501,#74502));
#15345=EDGE_LOOP('',(#74503,#74504,#74505));
#15346=EDGE_LOOP('',(#74506,#74507,#74508,#74509,#74510));
#15347=EDGE_LOOP('',(#74511,#74512,#74513,#74514,#74515));
#15348=EDGE_LOOP('',(#74516,#74517,#74518,#74519));
#15349=EDGE_LOOP('',(#74520,#74521,#74522,#74523));
#15350=EDGE_LOOP('',(#74524,#74525,#74526));
#15351=EDGE_LOOP('',(#74527,#74528,#74529,#74530));
#15352=EDGE_LOOP('',(#74531,#74532,#74533,#74534));
#15353=EDGE_LOOP('',(#74535,#74536,#74537,#74538));
#15354=EDGE_LOOP('',(#74539,#74540,#74541,#74542));
#15355=EDGE_LOOP('',(#74543,#74544,#74545,#74546));
#15356=EDGE_LOOP('',(#74547,#74548,#74549,#74550));
#15357=EDGE_LOOP('',(#74551,#74552,#74553,#74554));
#15358=EDGE_LOOP('',(#74555,#74556,#74557,#74558));
#15359=EDGE_LOOP('',(#74559,#74560,#74561,#74562));
#15360=EDGE_LOOP('',(#74563,#74564,#74565,#74566));
#15361=EDGE_LOOP('',(#74567,#74568,#74569,#74570));
#15362=EDGE_LOOP('',(#74571,#74572,#74573));
#15363=EDGE_LOOP('',(#74574,#74575,#74576,#74577,#74578));
#15364=EDGE_LOOP('',(#74579,#74580,#74581,#74582,#74583));
#15365=EDGE_LOOP('',(#74584,#74585,#74586,#74587));
#15366=EDGE_LOOP('',(#74588,#74589,#74590,#74591));
#15367=EDGE_LOOP('',(#74592,#74593,#74594));
#15368=EDGE_LOOP('',(#74595,#74596,#74597,#74598));
#15369=EDGE_LOOP('',(#74599,#74600,#74601,#74602));
#15370=EDGE_LOOP('',(#74603,#74604,#74605,#74606));
#15371=EDGE_LOOP('',(#74607,#74608,#74609,#74610));
#15372=EDGE_LOOP('',(#74611,#74612,#74613,#74614));
#15373=EDGE_LOOP('',(#74615,#74616,#74617,#74618));
#15374=EDGE_LOOP('',(#74619,#74620,#74621,#74622));
#15375=EDGE_LOOP('',(#74623,#74624,#74625,#74626));
#15376=EDGE_LOOP('',(#74627,#74628,#74629,#74630));
#15377=EDGE_LOOP('',(#74631,#74632,#74633,#74634));
#15378=EDGE_LOOP('',(#74635,#74636,#74637,#74638));
#15379=EDGE_LOOP('',(#74639,#74640,#74641));
#15380=EDGE_LOOP('',(#74642,#74643,#74644,#74645,#74646));
#15381=EDGE_LOOP('',(#74647,#74648,#74649,#74650,#74651));
#15382=EDGE_LOOP('',(#74652,#74653,#74654,#74655));
#15383=EDGE_LOOP('',(#74656,#74657,#74658,#74659));
#15384=EDGE_LOOP('',(#74660,#74661,#74662));
#15385=EDGE_LOOP('',(#74663,#74664,#74665,#74666));
#15386=EDGE_LOOP('',(#74667,#74668,#74669,#74670));
#15387=EDGE_LOOP('',(#74671,#74672,#74673,#74674));
#15388=EDGE_LOOP('',(#74675,#74676,#74677,#74678));
#15389=EDGE_LOOP('',(#74679,#74680,#74681,#74682));
#15390=EDGE_LOOP('',(#74683,#74684,#74685,#74686));
#15391=EDGE_LOOP('',(#74687,#74688,#74689,#74690));
#15392=EDGE_LOOP('',(#74691,#74692,#74693,#74694));
#15393=EDGE_LOOP('',(#74695,#74696,#74697,#74698));
#15394=EDGE_LOOP('',(#74699,#74700,#74701,#74702));
#15395=EDGE_LOOP('',(#74703,#74704,#74705,#74706));
#15396=EDGE_LOOP('',(#74707,#74708,#74709));
#15397=EDGE_LOOP('',(#74710,#74711,#74712,#74713,#74714));
#15398=EDGE_LOOP('',(#74715,#74716,#74717,#74718,#74719));
#15399=EDGE_LOOP('',(#74720,#74721,#74722,#74723));
#15400=EDGE_LOOP('',(#74724,#74725,#74726,#74727));
#15401=EDGE_LOOP('',(#74728,#74729,#74730));
#15402=EDGE_LOOP('',(#74731,#74732,#74733,#74734));
#15403=EDGE_LOOP('',(#74735,#74736,#74737,#74738));
#15404=EDGE_LOOP('',(#74739,#74740,#74741,#74742));
#15405=EDGE_LOOP('',(#74743,#74744,#74745,#74746));
#15406=EDGE_LOOP('',(#74747,#74748,#74749,#74750));
#15407=EDGE_LOOP('',(#74751,#74752,#74753,#74754));
#15408=EDGE_LOOP('',(#74755,#74756,#74757,#74758));
#15409=EDGE_LOOP('',(#74759,#74760,#74761,#74762));
#15410=EDGE_LOOP('',(#74763,#74764,#74765,#74766));
#15411=EDGE_LOOP('',(#74767,#74768,#74769,#74770));
#15412=EDGE_LOOP('',(#74771,#74772,#74773,#74774));
#15413=EDGE_LOOP('',(#74775,#74776,#74777));
#15414=EDGE_LOOP('',(#74778,#74779,#74780,#74781,#74782));
#15415=EDGE_LOOP('',(#74783,#74784,#74785,#74786,#74787));
#15416=EDGE_LOOP('',(#74788,#74789,#74790,#74791));
#15417=EDGE_LOOP('',(#74792,#74793,#74794,#74795));
#15418=EDGE_LOOP('',(#74796,#74797,#74798));
#15419=EDGE_LOOP('',(#74799,#74800,#74801,#74802));
#15420=EDGE_LOOP('',(#74803,#74804,#74805,#74806));
#15421=EDGE_LOOP('',(#74807,#74808,#74809,#74810));
#15422=EDGE_LOOP('',(#74811,#74812,#74813,#74814));
#15423=EDGE_LOOP('',(#74815,#74816,#74817,#74818));
#15424=EDGE_LOOP('',(#74819,#74820,#74821,#74822));
#15425=EDGE_LOOP('',(#74823,#74824,#74825,#74826));
#15426=EDGE_LOOP('',(#74827,#74828,#74829,#74830));
#15427=EDGE_LOOP('',(#74831,#74832,#74833,#74834));
#15428=EDGE_LOOP('',(#74835,#74836,#74837,#74838));
#15429=EDGE_LOOP('',(#74839,#74840,#74841,#74842));
#15430=EDGE_LOOP('',(#74843,#74844,#74845));
#15431=EDGE_LOOP('',(#74846,#74847,#74848,#74849,#74850));
#15432=EDGE_LOOP('',(#74851,#74852,#74853,#74854,#74855));
#15433=EDGE_LOOP('',(#74856,#74857,#74858,#74859));
#15434=EDGE_LOOP('',(#74860,#74861,#74862,#74863));
#15435=EDGE_LOOP('',(#74864,#74865,#74866));
#15436=EDGE_LOOP('',(#74867,#74868,#74869,#74870));
#15437=EDGE_LOOP('',(#74871,#74872,#74873,#74874));
#15438=EDGE_LOOP('',(#74875,#74876,#74877,#74878));
#15439=EDGE_LOOP('',(#74879,#74880,#74881,#74882));
#15440=EDGE_LOOP('',(#74883,#74884,#74885,#74886));
#15441=EDGE_LOOP('',(#74887,#74888,#74889,#74890));
#15442=EDGE_LOOP('',(#74891,#74892,#74893,#74894));
#15443=EDGE_LOOP('',(#74895,#74896,#74897,#74898));
#15444=EDGE_LOOP('',(#74899,#74900,#74901,#74902));
#15445=EDGE_LOOP('',(#74903,#74904,#74905,#74906));
#15446=EDGE_LOOP('',(#74907,#74908,#74909,#74910));
#15447=EDGE_LOOP('',(#74911,#74912,#74913));
#15448=EDGE_LOOP('',(#74914,#74915,#74916,#74917,#74918));
#15449=EDGE_LOOP('',(#74919,#74920,#74921,#74922,#74923));
#15450=EDGE_LOOP('',(#74924,#74925,#74926,#74927));
#15451=EDGE_LOOP('',(#74928,#74929,#74930,#74931));
#15452=EDGE_LOOP('',(#74932,#74933,#74934));
#15453=EDGE_LOOP('',(#74935,#74936,#74937,#74938));
#15454=EDGE_LOOP('',(#74939,#74940,#74941,#74942));
#15455=EDGE_LOOP('',(#74943,#74944,#74945,#74946));
#15456=EDGE_LOOP('',(#74947,#74948,#74949,#74950));
#15457=EDGE_LOOP('',(#74951,#74952,#74953,#74954));
#15458=EDGE_LOOP('',(#74955,#74956,#74957,#74958));
#15459=EDGE_LOOP('',(#74959,#74960,#74961,#74962));
#15460=EDGE_LOOP('',(#74963,#74964,#74965,#74966));
#15461=EDGE_LOOP('',(#74967,#74968,#74969,#74970));
#15462=EDGE_LOOP('',(#74971,#74972,#74973,#74974));
#15463=EDGE_LOOP('',(#74975,#74976,#74977,#74978));
#15464=EDGE_LOOP('',(#74979,#74980,#74981));
#15465=EDGE_LOOP('',(#74982,#74983,#74984,#74985,#74986));
#15466=EDGE_LOOP('',(#74987,#74988,#74989,#74990,#74991));
#15467=EDGE_LOOP('',(#74992,#74993,#74994,#74995));
#15468=EDGE_LOOP('',(#74996,#74997,#74998,#74999));
#15469=EDGE_LOOP('',(#75000,#75001,#75002));
#15470=EDGE_LOOP('',(#75003,#75004,#75005,#75006));
#15471=EDGE_LOOP('',(#75007,#75008,#75009,#75010));
#15472=EDGE_LOOP('',(#75011,#75012,#75013,#75014));
#15473=EDGE_LOOP('',(#75015,#75016,#75017,#75018));
#15474=EDGE_LOOP('',(#75019,#75020,#75021,#75022));
#15475=EDGE_LOOP('',(#75023,#75024,#75025,#75026));
#15476=EDGE_LOOP('',(#75027,#75028,#75029,#75030));
#15477=EDGE_LOOP('',(#75031,#75032,#75033,#75034));
#15478=EDGE_LOOP('',(#75035,#75036,#75037,#75038));
#15479=EDGE_LOOP('',(#75039,#75040,#75041,#75042));
#15480=EDGE_LOOP('',(#75043,#75044,#75045,#75046));
#15481=EDGE_LOOP('',(#75047,#75048,#75049));
#15482=EDGE_LOOP('',(#75050,#75051,#75052,#75053,#75054));
#15483=EDGE_LOOP('',(#75055,#75056,#75057,#75058,#75059));
#15484=EDGE_LOOP('',(#75060,#75061,#75062,#75063));
#15485=EDGE_LOOP('',(#75064,#75065,#75066,#75067));
#15486=EDGE_LOOP('',(#75068,#75069,#75070));
#15487=EDGE_LOOP('',(#75071,#75072,#75073,#75074));
#15488=EDGE_LOOP('',(#75075,#75076,#75077,#75078));
#15489=EDGE_LOOP('',(#75079,#75080,#75081,#75082));
#15490=EDGE_LOOP('',(#75083,#75084,#75085,#75086));
#15491=EDGE_LOOP('',(#75087,#75088,#75089,#75090));
#15492=EDGE_LOOP('',(#75091,#75092,#75093,#75094));
#15493=EDGE_LOOP('',(#75095,#75096,#75097,#75098));
#15494=EDGE_LOOP('',(#75099,#75100,#75101,#75102));
#15495=EDGE_LOOP('',(#75103,#75104,#75105,#75106));
#15496=EDGE_LOOP('',(#75107,#75108,#75109,#75110));
#15497=EDGE_LOOP('',(#75111,#75112,#75113,#75114));
#15498=EDGE_LOOP('',(#75115,#75116,#75117));
#15499=EDGE_LOOP('',(#75118,#75119,#75120,#75121,#75122));
#15500=EDGE_LOOP('',(#75123,#75124,#75125,#75126,#75127));
#15501=EDGE_LOOP('',(#75128,#75129,#75130,#75131));
#15502=EDGE_LOOP('',(#75132,#75133,#75134,#75135));
#15503=EDGE_LOOP('',(#75136,#75137,#75138));
#15504=EDGE_LOOP('',(#75139,#75140,#75141,#75142));
#15505=EDGE_LOOP('',(#75143,#75144,#75145,#75146));
#15506=EDGE_LOOP('',(#75147,#75148,#75149,#75150));
#15507=EDGE_LOOP('',(#75151,#75152,#75153,#75154));
#15508=EDGE_LOOP('',(#75155,#75156,#75157,#75158));
#15509=EDGE_LOOP('',(#75159,#75160,#75161,#75162));
#15510=EDGE_LOOP('',(#75163,#75164,#75165,#75166));
#15511=EDGE_LOOP('',(#75167,#75168,#75169,#75170));
#15512=EDGE_LOOP('',(#75171,#75172,#75173,#75174));
#15513=EDGE_LOOP('',(#75175,#75176,#75177,#75178));
#15514=EDGE_LOOP('',(#75179,#75180,#75181,#75182));
#15515=EDGE_LOOP('',(#75183,#75184,#75185));
#15516=EDGE_LOOP('',(#75186,#75187,#75188,#75189,#75190));
#15517=EDGE_LOOP('',(#75191,#75192,#75193,#75194,#75195));
#15518=EDGE_LOOP('',(#75196,#75197,#75198,#75199));
#15519=EDGE_LOOP('',(#75200,#75201,#75202,#75203));
#15520=EDGE_LOOP('',(#75204,#75205,#75206));
#15521=EDGE_LOOP('',(#75207,#75208,#75209,#75210));
#15522=EDGE_LOOP('',(#75211,#75212,#75213,#75214));
#15523=EDGE_LOOP('',(#75215,#75216,#75217,#75218));
#15524=EDGE_LOOP('',(#75219,#75220,#75221,#75222));
#15525=EDGE_LOOP('',(#75223,#75224,#75225,#75226));
#15526=EDGE_LOOP('',(#75227,#75228,#75229,#75230));
#15527=EDGE_LOOP('',(#75231,#75232,#75233,#75234));
#15528=EDGE_LOOP('',(#75235,#75236,#75237,#75238));
#15529=EDGE_LOOP('',(#75239,#75240,#75241,#75242));
#15530=EDGE_LOOP('',(#75243,#75244,#75245,#75246));
#15531=EDGE_LOOP('',(#75247,#75248,#75249,#75250));
#15532=EDGE_LOOP('',(#75251,#75252,#75253));
#15533=EDGE_LOOP('',(#75254,#75255,#75256,#75257,#75258));
#15534=EDGE_LOOP('',(#75259,#75260,#75261,#75262,#75263));
#15535=EDGE_LOOP('',(#75264,#75265,#75266,#75267));
#15536=EDGE_LOOP('',(#75268,#75269,#75270,#75271));
#15537=EDGE_LOOP('',(#75272,#75273,#75274));
#15538=EDGE_LOOP('',(#75275,#75276,#75277,#75278));
#15539=EDGE_LOOP('',(#75279,#75280,#75281,#75282));
#15540=EDGE_LOOP('',(#75283,#75284,#75285,#75286));
#15541=EDGE_LOOP('',(#75287,#75288,#75289,#75290));
#15542=EDGE_LOOP('',(#75291,#75292,#75293,#75294));
#15543=EDGE_LOOP('',(#75295,#75296,#75297,#75298));
#15544=EDGE_LOOP('',(#75299,#75300,#75301,#75302));
#15545=EDGE_LOOP('',(#75303,#75304,#75305,#75306));
#15546=EDGE_LOOP('',(#75307,#75308,#75309,#75310));
#15547=EDGE_LOOP('',(#75311,#75312,#75313,#75314));
#15548=EDGE_LOOP('',(#75315,#75316,#75317,#75318));
#15549=EDGE_LOOP('',(#75319,#75320,#75321));
#15550=EDGE_LOOP('',(#75322,#75323,#75324,#75325,#75326));
#15551=EDGE_LOOP('',(#75327,#75328,#75329,#75330,#75331));
#15552=EDGE_LOOP('',(#75332,#75333,#75334,#75335));
#15553=EDGE_LOOP('',(#75336,#75337,#75338,#75339));
#15554=EDGE_LOOP('',(#75340,#75341,#75342));
#15555=EDGE_LOOP('',(#75343,#75344,#75345,#75346));
#15556=EDGE_LOOP('',(#75347,#75348,#75349,#75350));
#15557=EDGE_LOOP('',(#75351,#75352,#75353,#75354));
#15558=EDGE_LOOP('',(#75355,#75356,#75357,#75358));
#15559=EDGE_LOOP('',(#75359,#75360,#75361,#75362));
#15560=EDGE_LOOP('',(#75363,#75364,#75365,#75366));
#15561=EDGE_LOOP('',(#75367,#75368,#75369,#75370));
#15562=EDGE_LOOP('',(#75371,#75372,#75373,#75374));
#15563=EDGE_LOOP('',(#75375,#75376,#75377,#75378));
#15564=EDGE_LOOP('',(#75379,#75380,#75381,#75382));
#15565=EDGE_LOOP('',(#75383,#75384,#75385,#75386));
#15566=EDGE_LOOP('',(#75387,#75388,#75389));
#15567=EDGE_LOOP('',(#75390,#75391,#75392,#75393,#75394));
#15568=EDGE_LOOP('',(#75395,#75396,#75397,#75398,#75399));
#15569=EDGE_LOOP('',(#75400,#75401,#75402,#75403));
#15570=EDGE_LOOP('',(#75404,#75405,#75406,#75407));
#15571=EDGE_LOOP('',(#75408,#75409,#75410));
#15572=EDGE_LOOP('',(#75411,#75412,#75413,#75414));
#15573=EDGE_LOOP('',(#75415,#75416,#75417,#75418));
#15574=EDGE_LOOP('',(#75419,#75420,#75421,#75422));
#15575=EDGE_LOOP('',(#75423,#75424,#75425,#75426));
#15576=EDGE_LOOP('',(#75427,#75428,#75429,#75430));
#15577=EDGE_LOOP('',(#75431,#75432,#75433,#75434));
#15578=EDGE_LOOP('',(#75435,#75436,#75437,#75438));
#15579=EDGE_LOOP('',(#75439,#75440,#75441,#75442));
#15580=EDGE_LOOP('',(#75443,#75444,#75445,#75446));
#15581=EDGE_LOOP('',(#75447,#75448,#75449,#75450));
#15582=EDGE_LOOP('',(#75451,#75452,#75453,#75454));
#15583=EDGE_LOOP('',(#75455,#75456,#75457));
#15584=EDGE_LOOP('',(#75458,#75459,#75460,#75461,#75462));
#15585=EDGE_LOOP('',(#75463,#75464,#75465,#75466,#75467));
#15586=EDGE_LOOP('',(#75468,#75469,#75470,#75471));
#15587=EDGE_LOOP('',(#75472,#75473,#75474,#75475));
#15588=EDGE_LOOP('',(#75476,#75477,#75478));
#15589=EDGE_LOOP('',(#75479,#75480,#75481,#75482));
#15590=EDGE_LOOP('',(#75483,#75484,#75485,#75486));
#15591=EDGE_LOOP('',(#75487,#75488,#75489,#75490));
#15592=EDGE_LOOP('',(#75491,#75492,#75493,#75494));
#15593=EDGE_LOOP('',(#75495,#75496,#75497,#75498));
#15594=EDGE_LOOP('',(#75499,#75500,#75501,#75502));
#15595=EDGE_LOOP('',(#75503,#75504,#75505,#75506));
#15596=EDGE_LOOP('',(#75507,#75508,#75509,#75510));
#15597=EDGE_LOOP('',(#75511,#75512,#75513,#75514));
#15598=EDGE_LOOP('',(#75515,#75516,#75517,#75518));
#15599=EDGE_LOOP('',(#75519,#75520,#75521,#75522));
#15600=EDGE_LOOP('',(#75523,#75524,#75525));
#15601=EDGE_LOOP('',(#75526,#75527,#75528,#75529,#75530));
#15602=EDGE_LOOP('',(#75531,#75532,#75533,#75534,#75535));
#15603=EDGE_LOOP('',(#75536,#75537,#75538,#75539));
#15604=EDGE_LOOP('',(#75540,#75541,#75542,#75543));
#15605=EDGE_LOOP('',(#75544,#75545,#75546));
#15606=EDGE_LOOP('',(#75547,#75548,#75549,#75550));
#15607=EDGE_LOOP('',(#75551,#75552,#75553,#75554));
#15608=EDGE_LOOP('',(#75555,#75556,#75557,#75558));
#15609=EDGE_LOOP('',(#75559,#75560,#75561,#75562));
#15610=EDGE_LOOP('',(#75563,#75564,#75565,#75566));
#15611=EDGE_LOOP('',(#75567,#75568,#75569,#75570));
#15612=EDGE_LOOP('',(#75571,#75572,#75573,#75574));
#15613=EDGE_LOOP('',(#75575,#75576,#75577,#75578));
#15614=EDGE_LOOP('',(#75579,#75580,#75581,#75582));
#15615=EDGE_LOOP('',(#75583,#75584,#75585,#75586));
#15616=EDGE_LOOP('',(#75587,#75588,#75589,#75590));
#15617=EDGE_LOOP('',(#75591,#75592,#75593));
#15618=EDGE_LOOP('',(#75594,#75595,#75596,#75597,#75598));
#15619=EDGE_LOOP('',(#75599,#75600,#75601,#75602,#75603));
#15620=EDGE_LOOP('',(#75604,#75605,#75606,#75607));
#15621=EDGE_LOOP('',(#75608,#75609,#75610,#75611));
#15622=EDGE_LOOP('',(#75612,#75613,#75614));
#15623=EDGE_LOOP('',(#75615,#75616,#75617,#75618));
#15624=EDGE_LOOP('',(#75619,#75620,#75621,#75622));
#15625=EDGE_LOOP('',(#75623,#75624,#75625,#75626));
#15626=EDGE_LOOP('',(#75627,#75628,#75629,#75630));
#15627=EDGE_LOOP('',(#75631,#75632,#75633,#75634));
#15628=EDGE_LOOP('',(#75635,#75636,#75637,#75638));
#15629=EDGE_LOOP('',(#75639,#75640,#75641,#75642));
#15630=EDGE_LOOP('',(#75643,#75644,#75645,#75646));
#15631=EDGE_LOOP('',(#75647,#75648,#75649,#75650));
#15632=EDGE_LOOP('',(#75651,#75652,#75653,#75654));
#15633=EDGE_LOOP('',(#75655,#75656,#75657,#75658));
#15634=EDGE_LOOP('',(#75659,#75660,#75661));
#15635=EDGE_LOOP('',(#75662,#75663,#75664,#75665,#75666));
#15636=EDGE_LOOP('',(#75667,#75668,#75669,#75670,#75671));
#15637=EDGE_LOOP('',(#75672,#75673,#75674,#75675));
#15638=EDGE_LOOP('',(#75676,#75677,#75678,#75679));
#15639=EDGE_LOOP('',(#75680,#75681,#75682));
#15640=EDGE_LOOP('',(#75683,#75684,#75685,#75686));
#15641=EDGE_LOOP('',(#75687,#75688,#75689,#75690));
#15642=EDGE_LOOP('',(#75691,#75692,#75693,#75694));
#15643=EDGE_LOOP('',(#75695,#75696,#75697,#75698));
#15644=EDGE_LOOP('',(#75699,#75700,#75701,#75702));
#15645=EDGE_LOOP('',(#75703,#75704,#75705,#75706));
#15646=EDGE_LOOP('',(#75707,#75708,#75709,#75710));
#15647=EDGE_LOOP('',(#75711,#75712,#75713,#75714));
#15648=EDGE_LOOP('',(#75715,#75716,#75717,#75718));
#15649=EDGE_LOOP('',(#75719,#75720,#75721,#75722));
#15650=EDGE_LOOP('',(#75723,#75724,#75725,#75726));
#15651=EDGE_LOOP('',(#75727,#75728,#75729));
#15652=EDGE_LOOP('',(#75730,#75731,#75732,#75733,#75734));
#15653=EDGE_LOOP('',(#75735,#75736,#75737,#75738,#75739));
#15654=EDGE_LOOP('',(#75740,#75741,#75742,#75743));
#15655=EDGE_LOOP('',(#75744,#75745,#75746,#75747));
#15656=EDGE_LOOP('',(#75748,#75749,#75750));
#15657=EDGE_LOOP('',(#75751,#75752,#75753,#75754));
#15658=EDGE_LOOP('',(#75755,#75756,#75757,#75758));
#15659=EDGE_LOOP('',(#75759,#75760,#75761,#75762));
#15660=EDGE_LOOP('',(#75763,#75764,#75765,#75766));
#15661=EDGE_LOOP('',(#75767,#75768,#75769,#75770));
#15662=EDGE_LOOP('',(#75771,#75772,#75773,#75774));
#15663=EDGE_LOOP('',(#75775,#75776,#75777,#75778));
#15664=EDGE_LOOP('',(#75779,#75780,#75781,#75782));
#15665=EDGE_LOOP('',(#75783,#75784,#75785,#75786));
#15666=EDGE_LOOP('',(#75787,#75788,#75789,#75790));
#15667=EDGE_LOOP('',(#75791,#75792,#75793,#75794));
#15668=EDGE_LOOP('',(#75795,#75796,#75797));
#15669=EDGE_LOOP('',(#75798,#75799,#75800,#75801,#75802));
#15670=EDGE_LOOP('',(#75803,#75804,#75805,#75806,#75807));
#15671=EDGE_LOOP('',(#75808,#75809,#75810,#75811));
#15672=EDGE_LOOP('',(#75812,#75813,#75814,#75815));
#15673=EDGE_LOOP('',(#75816,#75817,#75818));
#15674=EDGE_LOOP('',(#75819,#75820,#75821,#75822));
#15675=EDGE_LOOP('',(#75823,#75824,#75825,#75826));
#15676=EDGE_LOOP('',(#75827,#75828,#75829,#75830));
#15677=EDGE_LOOP('',(#75831,#75832,#75833,#75834));
#15678=EDGE_LOOP('',(#75835,#75836,#75837,#75838));
#15679=EDGE_LOOP('',(#75839,#75840,#75841,#75842));
#15680=EDGE_LOOP('',(#75843,#75844,#75845,#75846));
#15681=EDGE_LOOP('',(#75847,#75848,#75849,#75850));
#15682=EDGE_LOOP('',(#75851,#75852,#75853,#75854));
#15683=EDGE_LOOP('',(#75855,#75856,#75857,#75858));
#15684=EDGE_LOOP('',(#75859,#75860,#75861,#75862));
#15685=EDGE_LOOP('',(#75863,#75864,#75865));
#15686=EDGE_LOOP('',(#75866,#75867,#75868,#75869,#75870));
#15687=EDGE_LOOP('',(#75871,#75872,#75873,#75874,#75875));
#15688=EDGE_LOOP('',(#75876,#75877,#75878,#75879));
#15689=EDGE_LOOP('',(#75880,#75881,#75882,#75883));
#15690=EDGE_LOOP('',(#75884,#75885,#75886));
#15691=EDGE_LOOP('',(#75887,#75888,#75889,#75890));
#15692=EDGE_LOOP('',(#75891,#75892,#75893,#75894));
#15693=EDGE_LOOP('',(#75895,#75896,#75897,#75898));
#15694=EDGE_LOOP('',(#75899,#75900,#75901,#75902));
#15695=EDGE_LOOP('',(#75903,#75904,#75905,#75906));
#15696=EDGE_LOOP('',(#75907,#75908,#75909,#75910));
#15697=EDGE_LOOP('',(#75911,#75912,#75913,#75914));
#15698=EDGE_LOOP('',(#75915,#75916,#75917,#75918));
#15699=EDGE_LOOP('',(#75919,#75920,#75921,#75922));
#15700=EDGE_LOOP('',(#75923,#75924,#75925,#75926));
#15701=EDGE_LOOP('',(#75927,#75928,#75929,#75930));
#15702=EDGE_LOOP('',(#75931,#75932,#75933));
#15703=EDGE_LOOP('',(#75934,#75935,#75936,#75937,#75938));
#15704=EDGE_LOOP('',(#75939,#75940,#75941,#75942,#75943));
#15705=EDGE_LOOP('',(#75944,#75945,#75946,#75947));
#15706=EDGE_LOOP('',(#75948,#75949,#75950,#75951));
#15707=EDGE_LOOP('',(#75952,#75953,#75954));
#15708=EDGE_LOOP('',(#75955,#75956,#75957,#75958));
#15709=EDGE_LOOP('',(#75959,#75960,#75961,#75962));
#15710=EDGE_LOOP('',(#75963,#75964,#75965,#75966));
#15711=EDGE_LOOP('',(#75967,#75968,#75969,#75970));
#15712=EDGE_LOOP('',(#75971,#75972,#75973,#75974));
#15713=EDGE_LOOP('',(#75975,#75976,#75977,#75978));
#15714=EDGE_LOOP('',(#75979,#75980,#75981,#75982));
#15715=EDGE_LOOP('',(#75983,#75984,#75985,#75986));
#15716=EDGE_LOOP('',(#75987,#75988,#75989,#75990));
#15717=EDGE_LOOP('',(#75991,#75992,#75993,#75994));
#15718=EDGE_LOOP('',(#75995,#75996,#75997,#75998));
#15719=EDGE_LOOP('',(#75999,#76000,#76001));
#15720=EDGE_LOOP('',(#76002,#76003,#76004,#76005,#76006));
#15721=EDGE_LOOP('',(#76007,#76008,#76009,#76010,#76011));
#15722=EDGE_LOOP('',(#76012,#76013,#76014,#76015));
#15723=EDGE_LOOP('',(#76016,#76017,#76018,#76019));
#15724=EDGE_LOOP('',(#76020,#76021,#76022));
#15725=EDGE_LOOP('',(#76023,#76024,#76025,#76026));
#15726=EDGE_LOOP('',(#76027,#76028,#76029,#76030));
#15727=EDGE_LOOP('',(#76031,#76032,#76033,#76034));
#15728=EDGE_LOOP('',(#76035,#76036,#76037,#76038));
#15729=EDGE_LOOP('',(#76039,#76040,#76041,#76042));
#15730=EDGE_LOOP('',(#76043,#76044,#76045,#76046));
#15731=EDGE_LOOP('',(#76047,#76048,#76049,#76050));
#15732=EDGE_LOOP('',(#76051,#76052,#76053,#76054));
#15733=EDGE_LOOP('',(#76055,#76056,#76057,#76058));
#15734=EDGE_LOOP('',(#76059,#76060,#76061,#76062));
#15735=EDGE_LOOP('',(#76063,#76064,#76065,#76066));
#15736=EDGE_LOOP('',(#76067,#76068,#76069));
#15737=EDGE_LOOP('',(#76070,#76071,#76072,#76073,#76074));
#15738=EDGE_LOOP('',(#76075,#76076,#76077,#76078,#76079));
#15739=EDGE_LOOP('',(#76080,#76081,#76082,#76083));
#15740=EDGE_LOOP('',(#76084,#76085,#76086,#76087));
#15741=EDGE_LOOP('',(#76088,#76089,#76090));
#15742=EDGE_LOOP('',(#76091,#76092,#76093,#76094));
#15743=EDGE_LOOP('',(#76095,#76096,#76097,#76098));
#15744=EDGE_LOOP('',(#76099,#76100,#76101,#76102));
#15745=EDGE_LOOP('',(#76103,#76104,#76105,#76106));
#15746=EDGE_LOOP('',(#76107,#76108,#76109,#76110));
#15747=EDGE_LOOP('',(#76111,#76112,#76113,#76114));
#15748=EDGE_LOOP('',(#76115,#76116,#76117,#76118));
#15749=EDGE_LOOP('',(#76119,#76120,#76121,#76122));
#15750=EDGE_LOOP('',(#76123,#76124,#76125,#76126));
#15751=EDGE_LOOP('',(#76127,#76128,#76129,#76130));
#15752=EDGE_LOOP('',(#76131,#76132,#76133,#76134));
#15753=EDGE_LOOP('',(#76135,#76136,#76137));
#15754=EDGE_LOOP('',(#76138,#76139,#76140,#76141,#76142));
#15755=EDGE_LOOP('',(#76143,#76144,#76145,#76146,#76147));
#15756=EDGE_LOOP('',(#76148,#76149,#76150,#76151));
#15757=EDGE_LOOP('',(#76152,#76153,#76154,#76155));
#15758=EDGE_LOOP('',(#76156,#76157,#76158));
#15759=EDGE_LOOP('',(#76159,#76160,#76161,#76162));
#15760=EDGE_LOOP('',(#76163,#76164,#76165,#76166));
#15761=EDGE_LOOP('',(#76167,#76168,#76169,#76170));
#15762=EDGE_LOOP('',(#76171,#76172,#76173,#76174));
#15763=EDGE_LOOP('',(#76175,#76176,#76177,#76178));
#15764=EDGE_LOOP('',(#76179,#76180,#76181,#76182));
#15765=EDGE_LOOP('',(#76183,#76184,#76185,#76186));
#15766=EDGE_LOOP('',(#76187,#76188,#76189,#76190));
#15767=EDGE_LOOP('',(#76191,#76192,#76193,#76194));
#15768=EDGE_LOOP('',(#76195,#76196,#76197,#76198));
#15769=EDGE_LOOP('',(#76199,#76200,#76201,#76202));
#15770=EDGE_LOOP('',(#76203,#76204,#76205));
#15771=EDGE_LOOP('',(#76206,#76207,#76208,#76209,#76210));
#15772=EDGE_LOOP('',(#76211,#76212,#76213,#76214,#76215));
#15773=EDGE_LOOP('',(#76216,#76217,#76218,#76219));
#15774=EDGE_LOOP('',(#76220,#76221,#76222,#76223));
#15775=EDGE_LOOP('',(#76224,#76225,#76226));
#15776=EDGE_LOOP('',(#76227,#76228,#76229,#76230));
#15777=EDGE_LOOP('',(#76231,#76232,#76233,#76234));
#15778=EDGE_LOOP('',(#76235,#76236,#76237,#76238));
#15779=EDGE_LOOP('',(#76239,#76240,#76241,#76242));
#15780=EDGE_LOOP('',(#76243,#76244,#76245,#76246));
#15781=EDGE_LOOP('',(#76247,#76248,#76249,#76250));
#15782=EDGE_LOOP('',(#76251,#76252,#76253,#76254));
#15783=EDGE_LOOP('',(#76255,#76256,#76257,#76258));
#15784=EDGE_LOOP('',(#76259,#76260,#76261,#76262));
#15785=EDGE_LOOP('',(#76263,#76264,#76265,#76266));
#15786=EDGE_LOOP('',(#76267,#76268,#76269,#76270));
#15787=EDGE_LOOP('',(#76271,#76272,#76273));
#15788=EDGE_LOOP('',(#76274,#76275,#76276,#76277,#76278));
#15789=EDGE_LOOP('',(#76279,#76280,#76281,#76282,#76283));
#15790=EDGE_LOOP('',(#76284,#76285,#76286,#76287));
#15791=EDGE_LOOP('',(#76288,#76289,#76290,#76291));
#15792=EDGE_LOOP('',(#76292,#76293,#76294));
#15793=EDGE_LOOP('',(#76295,#76296,#76297,#76298));
#15794=EDGE_LOOP('',(#76299,#76300,#76301,#76302));
#15795=EDGE_LOOP('',(#76303,#76304,#76305,#76306));
#15796=EDGE_LOOP('',(#76307,#76308,#76309,#76310));
#15797=EDGE_LOOP('',(#76311,#76312,#76313,#76314));
#15798=EDGE_LOOP('',(#76315,#76316,#76317,#76318));
#15799=EDGE_LOOP('',(#76319,#76320,#76321,#76322));
#15800=EDGE_LOOP('',(#76323,#76324,#76325,#76326));
#15801=EDGE_LOOP('',(#76327,#76328,#76329,#76330));
#15802=EDGE_LOOP('',(#76331,#76332,#76333,#76334));
#15803=EDGE_LOOP('',(#76335,#76336,#76337,#76338));
#15804=EDGE_LOOP('',(#76339,#76340,#76341));
#15805=EDGE_LOOP('',(#76342,#76343,#76344,#76345,#76346));
#15806=EDGE_LOOP('',(#76347,#76348,#76349,#76350,#76351));
#15807=EDGE_LOOP('',(#76352,#76353,#76354,#76355));
#15808=EDGE_LOOP('',(#76356,#76357,#76358,#76359));
#15809=EDGE_LOOP('',(#76360,#76361,#76362));
#15810=EDGE_LOOP('',(#76363,#76364,#76365,#76366));
#15811=EDGE_LOOP('',(#76367,#76368,#76369,#76370));
#15812=EDGE_LOOP('',(#76371,#76372,#76373,#76374));
#15813=EDGE_LOOP('',(#76375,#76376,#76377,#76378));
#15814=EDGE_LOOP('',(#76379,#76380,#76381,#76382));
#15815=EDGE_LOOP('',(#76383,#76384,#76385,#76386));
#15816=EDGE_LOOP('',(#76387,#76388,#76389,#76390));
#15817=EDGE_LOOP('',(#76391,#76392,#76393,#76394));
#15818=EDGE_LOOP('',(#76395,#76396,#76397,#76398));
#15819=EDGE_LOOP('',(#76399,#76400,#76401,#76402));
#15820=EDGE_LOOP('',(#76403,#76404,#76405,#76406));
#15821=EDGE_LOOP('',(#76407,#76408,#76409));
#15822=EDGE_LOOP('',(#76410,#76411,#76412,#76413,#76414));
#15823=EDGE_LOOP('',(#76415,#76416,#76417,#76418,#76419));
#15824=EDGE_LOOP('',(#76420,#76421,#76422,#76423));
#15825=EDGE_LOOP('',(#76424,#76425,#76426,#76427));
#15826=EDGE_LOOP('',(#76428,#76429,#76430));
#15827=EDGE_LOOP('',(#76431,#76432,#76433,#76434));
#15828=EDGE_LOOP('',(#76435,#76436,#76437,#76438));
#15829=EDGE_LOOP('',(#76439,#76440,#76441,#76442));
#15830=EDGE_LOOP('',(#76443,#76444,#76445,#76446));
#15831=EDGE_LOOP('',(#76447,#76448,#76449,#76450));
#15832=EDGE_LOOP('',(#76451,#76452,#76453,#76454));
#15833=EDGE_LOOP('',(#76455,#76456,#76457,#76458));
#15834=EDGE_LOOP('',(#76459,#76460,#76461,#76462));
#15835=EDGE_LOOP('',(#76463,#76464,#76465,#76466));
#15836=EDGE_LOOP('',(#76467,#76468,#76469,#76470));
#15837=EDGE_LOOP('',(#76471,#76472,#76473,#76474));
#15838=EDGE_LOOP('',(#76475,#76476,#76477));
#15839=EDGE_LOOP('',(#76478,#76479,#76480,#76481,#76482));
#15840=EDGE_LOOP('',(#76483,#76484,#76485,#76486,#76487));
#15841=EDGE_LOOP('',(#76488,#76489,#76490,#76491));
#15842=EDGE_LOOP('',(#76492,#76493,#76494,#76495));
#15843=EDGE_LOOP('',(#76496,#76497,#76498));
#15844=EDGE_LOOP('',(#76499,#76500,#76501,#76502));
#15845=EDGE_LOOP('',(#76503,#76504,#76505,#76506));
#15846=EDGE_LOOP('',(#76507,#76508,#76509,#76510));
#15847=EDGE_LOOP('',(#76511,#76512,#76513,#76514));
#15848=EDGE_LOOP('',(#76515,#76516,#76517,#76518));
#15849=EDGE_LOOP('',(#76519,#76520,#76521,#76522));
#15850=EDGE_LOOP('',(#76523,#76524,#76525,#76526));
#15851=EDGE_LOOP('',(#76527,#76528,#76529,#76530));
#15852=EDGE_LOOP('',(#76531,#76532,#76533,#76534));
#15853=EDGE_LOOP('',(#76535,#76536,#76537,#76538));
#15854=EDGE_LOOP('',(#76539,#76540,#76541,#76542));
#15855=EDGE_LOOP('',(#76543,#76544,#76545));
#15856=EDGE_LOOP('',(#76546,#76547,#76548,#76549,#76550));
#15857=EDGE_LOOP('',(#76551,#76552,#76553,#76554,#76555));
#15858=EDGE_LOOP('',(#76556,#76557,#76558,#76559));
#15859=EDGE_LOOP('',(#76560,#76561,#76562,#76563));
#15860=EDGE_LOOP('',(#76564,#76565,#76566));
#15861=EDGE_LOOP('',(#76567,#76568,#76569,#76570));
#15862=EDGE_LOOP('',(#76571,#76572,#76573,#76574));
#15863=EDGE_LOOP('',(#76575,#76576,#76577,#76578));
#15864=EDGE_LOOP('',(#76579,#76580,#76581,#76582));
#15865=EDGE_LOOP('',(#76583,#76584,#76585,#76586));
#15866=EDGE_LOOP('',(#76587,#76588,#76589,#76590));
#15867=EDGE_LOOP('',(#76591,#76592,#76593,#76594));
#15868=EDGE_LOOP('',(#76595,#76596,#76597,#76598));
#15869=EDGE_LOOP('',(#76599,#76600,#76601,#76602));
#15870=EDGE_LOOP('',(#76603,#76604,#76605,#76606));
#15871=EDGE_LOOP('',(#76607,#76608,#76609,#76610));
#15872=EDGE_LOOP('',(#76611,#76612,#76613));
#15873=EDGE_LOOP('',(#76614,#76615,#76616,#76617,#76618));
#15874=EDGE_LOOP('',(#76619,#76620,#76621,#76622,#76623));
#15875=EDGE_LOOP('',(#76624,#76625,#76626,#76627));
#15876=EDGE_LOOP('',(#76628,#76629,#76630,#76631));
#15877=EDGE_LOOP('',(#76632,#76633,#76634));
#15878=EDGE_LOOP('',(#76635,#76636,#76637,#76638));
#15879=EDGE_LOOP('',(#76639,#76640,#76641,#76642));
#15880=EDGE_LOOP('',(#76643,#76644,#76645,#76646));
#15881=EDGE_LOOP('',(#76647,#76648,#76649,#76650));
#15882=EDGE_LOOP('',(#76651,#76652,#76653,#76654));
#15883=EDGE_LOOP('',(#76655,#76656,#76657,#76658));
#15884=EDGE_LOOP('',(#76659,#76660,#76661,#76662));
#15885=EDGE_LOOP('',(#76663,#76664,#76665,#76666));
#15886=EDGE_LOOP('',(#76667,#76668,#76669,#76670));
#15887=EDGE_LOOP('',(#76671,#76672,#76673,#76674));
#15888=EDGE_LOOP('',(#76675,#76676,#76677,#76678));
#15889=EDGE_LOOP('',(#76679,#76680,#76681));
#15890=EDGE_LOOP('',(#76682,#76683,#76684,#76685,#76686));
#15891=EDGE_LOOP('',(#76687,#76688,#76689,#76690,#76691));
#15892=EDGE_LOOP('',(#76692,#76693,#76694,#76695));
#15893=EDGE_LOOP('',(#76696,#76697,#76698,#76699));
#15894=EDGE_LOOP('',(#76700,#76701,#76702));
#15895=EDGE_LOOP('',(#76703,#76704,#76705,#76706));
#15896=EDGE_LOOP('',(#76707,#76708,#76709,#76710));
#15897=EDGE_LOOP('',(#76711,#76712,#76713,#76714));
#15898=EDGE_LOOP('',(#76715,#76716,#76717,#76718));
#15899=EDGE_LOOP('',(#76719,#76720,#76721,#76722));
#15900=EDGE_LOOP('',(#76723,#76724,#76725,#76726));
#15901=EDGE_LOOP('',(#76727,#76728,#76729,#76730));
#15902=EDGE_LOOP('',(#76731,#76732,#76733,#76734));
#15903=EDGE_LOOP('',(#76735,#76736,#76737,#76738));
#15904=EDGE_LOOP('',(#76739,#76740,#76741,#76742));
#15905=EDGE_LOOP('',(#76743,#76744,#76745,#76746));
#15906=EDGE_LOOP('',(#76747,#76748,#76749));
#15907=EDGE_LOOP('',(#76750,#76751,#76752,#76753,#76754));
#15908=EDGE_LOOP('',(#76755,#76756,#76757,#76758,#76759));
#15909=EDGE_LOOP('',(#76760,#76761,#76762,#76763));
#15910=EDGE_LOOP('',(#76764,#76765,#76766,#76767));
#15911=EDGE_LOOP('',(#76768,#76769,#76770));
#15912=EDGE_LOOP('',(#76771,#76772,#76773,#76774));
#15913=EDGE_LOOP('',(#76775,#76776,#76777,#76778));
#15914=EDGE_LOOP('',(#76779,#76780,#76781,#76782));
#15915=EDGE_LOOP('',(#76783,#76784,#76785,#76786));
#15916=EDGE_LOOP('',(#76787,#76788,#76789,#76790));
#15917=EDGE_LOOP('',(#76791,#76792,#76793,#76794));
#15918=EDGE_LOOP('',(#76795,#76796,#76797,#76798));
#15919=EDGE_LOOP('',(#76799,#76800,#76801,#76802));
#15920=EDGE_LOOP('',(#76803,#76804,#76805,#76806));
#15921=EDGE_LOOP('',(#76807,#76808,#76809,#76810));
#15922=EDGE_LOOP('',(#76811,#76812,#76813,#76814));
#15923=EDGE_LOOP('',(#76815,#76816,#76817));
#15924=EDGE_LOOP('',(#76818,#76819,#76820,#76821,#76822));
#15925=EDGE_LOOP('',(#76823,#76824,#76825,#76826,#76827));
#15926=EDGE_LOOP('',(#76828,#76829,#76830,#76831));
#15927=EDGE_LOOP('',(#76832,#76833,#76834,#76835));
#15928=EDGE_LOOP('',(#76836,#76837,#76838));
#15929=EDGE_LOOP('',(#76839,#76840,#76841,#76842));
#15930=EDGE_LOOP('',(#76843,#76844,#76845,#76846));
#15931=EDGE_LOOP('',(#76847,#76848,#76849,#76850));
#15932=EDGE_LOOP('',(#76851,#76852,#76853,#76854));
#15933=EDGE_LOOP('',(#76855,#76856,#76857,#76858));
#15934=EDGE_LOOP('',(#76859,#76860,#76861,#76862));
#15935=EDGE_LOOP('',(#76863,#76864,#76865,#76866));
#15936=EDGE_LOOP('',(#76867,#76868,#76869,#76870));
#15937=EDGE_LOOP('',(#76871,#76872,#76873,#76874));
#15938=EDGE_LOOP('',(#76875,#76876,#76877,#76878));
#15939=EDGE_LOOP('',(#76879,#76880,#76881,#76882));
#15940=EDGE_LOOP('',(#76883,#76884,#76885));
#15941=EDGE_LOOP('',(#76886,#76887,#76888,#76889,#76890));
#15942=EDGE_LOOP('',(#76891,#76892,#76893,#76894,#76895));
#15943=EDGE_LOOP('',(#76896,#76897,#76898,#76899));
#15944=EDGE_LOOP('',(#76900,#76901,#76902,#76903));
#15945=EDGE_LOOP('',(#76904,#76905,#76906));
#15946=EDGE_LOOP('',(#76907,#76908,#76909,#76910));
#15947=EDGE_LOOP('',(#76911,#76912,#76913,#76914));
#15948=EDGE_LOOP('',(#76915,#76916,#76917,#76918));
#15949=EDGE_LOOP('',(#76919,#76920,#76921,#76922));
#15950=EDGE_LOOP('',(#76923,#76924,#76925,#76926));
#15951=EDGE_LOOP('',(#76927,#76928,#76929,#76930));
#15952=EDGE_LOOP('',(#76931,#76932,#76933,#76934));
#15953=EDGE_LOOP('',(#76935,#76936,#76937,#76938));
#15954=EDGE_LOOP('',(#76939,#76940,#76941,#76942));
#15955=EDGE_LOOP('',(#76943,#76944,#76945,#76946));
#15956=EDGE_LOOP('',(#76947,#76948,#76949,#76950));
#15957=EDGE_LOOP('',(#76951,#76952,#76953));
#15958=EDGE_LOOP('',(#76954,#76955,#76956,#76957,#76958));
#15959=EDGE_LOOP('',(#76959,#76960,#76961,#76962,#76963));
#15960=EDGE_LOOP('',(#76964,#76965,#76966,#76967));
#15961=EDGE_LOOP('',(#76968,#76969,#76970,#76971));
#15962=EDGE_LOOP('',(#76972,#76973,#76974));
#15963=EDGE_LOOP('',(#76975,#76976,#76977,#76978));
#15964=EDGE_LOOP('',(#76979,#76980,#76981,#76982));
#15965=EDGE_LOOP('',(#76983,#76984,#76985,#76986));
#15966=EDGE_LOOP('',(#76987,#76988,#76989,#76990));
#15967=EDGE_LOOP('',(#76991,#76992,#76993,#76994));
#15968=EDGE_LOOP('',(#76995,#76996,#76997,#76998));
#15969=EDGE_LOOP('',(#76999,#77000,#77001,#77002));
#15970=EDGE_LOOP('',(#77003,#77004,#77005,#77006));
#15971=EDGE_LOOP('',(#77007,#77008,#77009,#77010));
#15972=EDGE_LOOP('',(#77011,#77012,#77013,#77014));
#15973=EDGE_LOOP('',(#77015,#77016,#77017,#77018));
#15974=EDGE_LOOP('',(#77019,#77020,#77021));
#15975=EDGE_LOOP('',(#77022,#77023,#77024,#77025,#77026));
#15976=EDGE_LOOP('',(#77027,#77028,#77029,#77030,#77031));
#15977=EDGE_LOOP('',(#77032,#77033,#77034,#77035));
#15978=EDGE_LOOP('',(#77036,#77037,#77038,#77039));
#15979=EDGE_LOOP('',(#77040,#77041,#77042));
#15980=EDGE_LOOP('',(#77043,#77044,#77045,#77046));
#15981=EDGE_LOOP('',(#77047,#77048,#77049,#77050));
#15982=EDGE_LOOP('',(#77051,#77052,#77053,#77054));
#15983=EDGE_LOOP('',(#77055,#77056,#77057,#77058));
#15984=EDGE_LOOP('',(#77059,#77060,#77061,#77062));
#15985=EDGE_LOOP('',(#77063,#77064,#77065,#77066));
#15986=EDGE_LOOP('',(#77067,#77068,#77069,#77070));
#15987=EDGE_LOOP('',(#77071,#77072,#77073,#77074));
#15988=EDGE_LOOP('',(#77075,#77076,#77077,#77078));
#15989=EDGE_LOOP('',(#77079,#77080,#77081,#77082));
#15990=EDGE_LOOP('',(#77083,#77084,#77085,#77086));
#15991=EDGE_LOOP('',(#77087,#77088,#77089));
#15992=EDGE_LOOP('',(#77090,#77091,#77092,#77093,#77094));
#15993=EDGE_LOOP('',(#77095,#77096,#77097,#77098,#77099));
#15994=EDGE_LOOP('',(#77100,#77101,#77102,#77103));
#15995=EDGE_LOOP('',(#77104,#77105,#77106,#77107));
#15996=EDGE_LOOP('',(#77108,#77109,#77110));
#15997=EDGE_LOOP('',(#77111,#77112,#77113,#77114));
#15998=EDGE_LOOP('',(#77115,#77116,#77117,#77118));
#15999=EDGE_LOOP('',(#77119,#77120,#77121,#77122));
#16000=EDGE_LOOP('',(#77123,#77124,#77125,#77126));
#16001=EDGE_LOOP('',(#77127,#77128,#77129,#77130));
#16002=EDGE_LOOP('',(#77131,#77132,#77133,#77134));
#16003=EDGE_LOOP('',(#77135,#77136,#77137,#77138));
#16004=EDGE_LOOP('',(#77139,#77140,#77141,#77142));
#16005=EDGE_LOOP('',(#77143,#77144,#77145,#77146));
#16006=EDGE_LOOP('',(#77147,#77148,#77149,#77150));
#16007=EDGE_LOOP('',(#77151,#77152,#77153,#77154));
#16008=EDGE_LOOP('',(#77155,#77156,#77157));
#16009=EDGE_LOOP('',(#77158,#77159,#77160,#77161,#77162));
#16010=EDGE_LOOP('',(#77163,#77164,#77165,#77166,#77167));
#16011=EDGE_LOOP('',(#77168,#77169,#77170,#77171));
#16012=EDGE_LOOP('',(#77172,#77173,#77174,#77175));
#16013=EDGE_LOOP('',(#77176,#77177,#77178));
#16014=EDGE_LOOP('',(#77179,#77180,#77181,#77182));
#16015=EDGE_LOOP('',(#77183,#77184,#77185,#77186));
#16016=EDGE_LOOP('',(#77187,#77188,#77189,#77190));
#16017=EDGE_LOOP('',(#77191,#77192,#77193,#77194));
#16018=EDGE_LOOP('',(#77195,#77196,#77197,#77198));
#16019=EDGE_LOOP('',(#77199,#77200,#77201,#77202));
#16020=EDGE_LOOP('',(#77203,#77204,#77205,#77206));
#16021=EDGE_LOOP('',(#77207,#77208,#77209,#77210));
#16022=EDGE_LOOP('',(#77211,#77212,#77213,#77214));
#16023=EDGE_LOOP('',(#77215,#77216,#77217,#77218));
#16024=EDGE_LOOP('',(#77219,#77220,#77221,#77222));
#16025=EDGE_LOOP('',(#77223,#77224,#77225));
#16026=EDGE_LOOP('',(#77226,#77227,#77228,#77229,#77230));
#16027=EDGE_LOOP('',(#77231,#77232,#77233,#77234,#77235));
#16028=EDGE_LOOP('',(#77236,#77237,#77238,#77239));
#16029=EDGE_LOOP('',(#77240,#77241,#77242,#77243));
#16030=EDGE_LOOP('',(#77244,#77245,#77246));
#16031=EDGE_LOOP('',(#77247,#77248,#77249,#77250));
#16032=EDGE_LOOP('',(#77251,#77252,#77253,#77254));
#16033=EDGE_LOOP('',(#77255,#77256,#77257,#77258));
#16034=EDGE_LOOP('',(#77259,#77260,#77261,#77262));
#16035=EDGE_LOOP('',(#77263,#77264,#77265,#77266));
#16036=EDGE_LOOP('',(#77267,#77268,#77269,#77270));
#16037=EDGE_LOOP('',(#77271,#77272,#77273,#77274));
#16038=EDGE_LOOP('',(#77275,#77276,#77277,#77278));
#16039=EDGE_LOOP('',(#77279,#77280,#77281,#77282));
#16040=EDGE_LOOP('',(#77283,#77284,#77285,#77286));
#16041=EDGE_LOOP('',(#77287,#77288,#77289,#77290));
#16042=EDGE_LOOP('',(#77291,#77292,#77293));
#16043=EDGE_LOOP('',(#77294,#77295,#77296,#77297,#77298));
#16044=EDGE_LOOP('',(#77299,#77300,#77301,#77302,#77303));
#16045=EDGE_LOOP('',(#77304,#77305,#77306,#77307));
#16046=EDGE_LOOP('',(#77308,#77309,#77310,#77311));
#16047=EDGE_LOOP('',(#77312,#77313,#77314));
#16048=EDGE_LOOP('',(#77315,#77316,#77317,#77318));
#16049=EDGE_LOOP('',(#77319,#77320,#77321,#77322));
#16050=EDGE_LOOP('',(#77323,#77324,#77325,#77326));
#16051=EDGE_LOOP('',(#77327,#77328,#77329,#77330));
#16052=EDGE_LOOP('',(#77331,#77332,#77333,#77334));
#16053=EDGE_LOOP('',(#77335,#77336,#77337,#77338));
#16054=EDGE_LOOP('',(#77339,#77340,#77341,#77342));
#16055=EDGE_LOOP('',(#77343,#77344,#77345,#77346));
#16056=EDGE_LOOP('',(#77347,#77348,#77349,#77350));
#16057=EDGE_LOOP('',(#77351,#77352,#77353,#77354));
#16058=EDGE_LOOP('',(#77355,#77356,#77357,#77358));
#16059=EDGE_LOOP('',(#77359,#77360,#77361));
#16060=EDGE_LOOP('',(#77362,#77363,#77364,#77365,#77366));
#16061=EDGE_LOOP('',(#77367,#77368,#77369,#77370,#77371));
#16062=EDGE_LOOP('',(#77372,#77373,#77374,#77375));
#16063=EDGE_LOOP('',(#77376,#77377,#77378,#77379));
#16064=EDGE_LOOP('',(#77380,#77381,#77382));
#16065=EDGE_LOOP('',(#77383,#77384,#77385,#77386));
#16066=EDGE_LOOP('',(#77387,#77388,#77389,#77390));
#16067=EDGE_LOOP('',(#77391,#77392,#77393,#77394));
#16068=EDGE_LOOP('',(#77395,#77396,#77397,#77398));
#16069=EDGE_LOOP('',(#77399,#77400,#77401,#77402));
#16070=EDGE_LOOP('',(#77403,#77404,#77405,#77406));
#16071=EDGE_LOOP('',(#77407,#77408,#77409,#77410));
#16072=EDGE_LOOP('',(#77411,#77412,#77413,#77414));
#16073=EDGE_LOOP('',(#77415,#77416,#77417,#77418));
#16074=EDGE_LOOP('',(#77419,#77420,#77421,#77422));
#16075=EDGE_LOOP('',(#77423,#77424,#77425,#77426));
#16076=EDGE_LOOP('',(#77427,#77428,#77429));
#16077=EDGE_LOOP('',(#77430,#77431,#77432,#77433,#77434));
#16078=EDGE_LOOP('',(#77435,#77436,#77437,#77438,#77439));
#16079=EDGE_LOOP('',(#77440,#77441,#77442,#77443));
#16080=EDGE_LOOP('',(#77444,#77445,#77446,#77447));
#16081=EDGE_LOOP('',(#77448,#77449,#77450));
#16082=EDGE_LOOP('',(#77451,#77452,#77453,#77454));
#16083=EDGE_LOOP('',(#77455,#77456,#77457,#77458));
#16084=EDGE_LOOP('',(#77459,#77460,#77461,#77462));
#16085=EDGE_LOOP('',(#77463,#77464,#77465,#77466));
#16086=EDGE_LOOP('',(#77467,#77468,#77469,#77470));
#16087=EDGE_LOOP('',(#77471,#77472,#77473,#77474));
#16088=EDGE_LOOP('',(#77475,#77476,#77477,#77478));
#16089=EDGE_LOOP('',(#77479,#77480,#77481,#77482));
#16090=EDGE_LOOP('',(#77483,#77484,#77485,#77486));
#16091=EDGE_LOOP('',(#77487,#77488,#77489,#77490));
#16092=EDGE_LOOP('',(#77491,#77492,#77493,#77494));
#16093=EDGE_LOOP('',(#77495,#77496,#77497));
#16094=EDGE_LOOP('',(#77498,#77499,#77500,#77501,#77502));
#16095=EDGE_LOOP('',(#77503,#77504,#77505,#77506,#77507));
#16096=EDGE_LOOP('',(#77508,#77509,#77510,#77511));
#16097=EDGE_LOOP('',(#77512,#77513,#77514,#77515));
#16098=EDGE_LOOP('',(#77516,#77517,#77518));
#16099=EDGE_LOOP('',(#77519,#77520,#77521,#77522));
#16100=EDGE_LOOP('',(#77523,#77524,#77525,#77526));
#16101=EDGE_LOOP('',(#77527,#77528,#77529,#77530));
#16102=EDGE_LOOP('',(#77531,#77532,#77533,#77534));
#16103=EDGE_LOOP('',(#77535,#77536,#77537,#77538));
#16104=EDGE_LOOP('',(#77539,#77540,#77541,#77542));
#16105=EDGE_LOOP('',(#77543,#77544,#77545,#77546));
#16106=EDGE_LOOP('',(#77547,#77548,#77549,#77550));
#16107=EDGE_LOOP('',(#77551,#77552,#77553,#77554));
#16108=EDGE_LOOP('',(#77555,#77556,#77557,#77558));
#16109=EDGE_LOOP('',(#77559,#77560,#77561,#77562));
#16110=EDGE_LOOP('',(#77563,#77564,#77565));
#16111=EDGE_LOOP('',(#77566,#77567,#77568,#77569,#77570));
#16112=EDGE_LOOP('',(#77571,#77572,#77573,#77574,#77575));
#16113=EDGE_LOOP('',(#77576,#77577,#77578,#77579));
#16114=EDGE_LOOP('',(#77580,#77581,#77582,#77583));
#16115=EDGE_LOOP('',(#77584,#77585,#77586));
#16116=EDGE_LOOP('',(#77587,#77588,#77589,#77590));
#16117=EDGE_LOOP('',(#77591,#77592,#77593,#77594));
#16118=EDGE_LOOP('',(#77595,#77596,#77597,#77598));
#16119=EDGE_LOOP('',(#77599,#77600,#77601,#77602));
#16120=EDGE_LOOP('',(#77603,#77604,#77605,#77606));
#16121=EDGE_LOOP('',(#77607,#77608,#77609,#77610));
#16122=EDGE_LOOP('',(#77611,#77612,#77613,#77614));
#16123=EDGE_LOOP('',(#77615,#77616,#77617,#77618));
#16124=EDGE_LOOP('',(#77619,#77620,#77621,#77622));
#16125=EDGE_LOOP('',(#77623,#77624,#77625,#77626));
#16126=EDGE_LOOP('',(#77627,#77628,#77629,#77630));
#16127=EDGE_LOOP('',(#77631,#77632,#77633));
#16128=EDGE_LOOP('',(#77634,#77635,#77636,#77637,#77638));
#16129=EDGE_LOOP('',(#77639,#77640,#77641,#77642,#77643));
#16130=EDGE_LOOP('',(#77644,#77645,#77646,#77647));
#16131=EDGE_LOOP('',(#77648,#77649,#77650,#77651));
#16132=EDGE_LOOP('',(#77652,#77653,#77654));
#16133=EDGE_LOOP('',(#77655,#77656,#77657,#77658));
#16134=EDGE_LOOP('',(#77659,#77660,#77661,#77662));
#16135=EDGE_LOOP('',(#77663,#77664,#77665,#77666));
#16136=EDGE_LOOP('',(#77667,#77668,#77669,#77670));
#16137=EDGE_LOOP('',(#77671,#77672,#77673,#77674));
#16138=EDGE_LOOP('',(#77675,#77676,#77677,#77678));
#16139=EDGE_LOOP('',(#77679,#77680,#77681,#77682));
#16140=EDGE_LOOP('',(#77683,#77684,#77685,#77686));
#16141=EDGE_LOOP('',(#77687,#77688,#77689,#77690));
#16142=EDGE_LOOP('',(#77691,#77692,#77693,#77694));
#16143=EDGE_LOOP('',(#77695,#77696,#77697,#77698));
#16144=EDGE_LOOP('',(#77699,#77700,#77701));
#16145=EDGE_LOOP('',(#77702,#77703,#77704,#77705,#77706));
#16146=EDGE_LOOP('',(#77707,#77708,#77709,#77710,#77711));
#16147=EDGE_LOOP('',(#77712,#77713,#77714,#77715));
#16148=EDGE_LOOP('',(#77716,#77717,#77718,#77719));
#16149=EDGE_LOOP('',(#77720,#77721,#77722));
#16150=EDGE_LOOP('',(#77723,#77724,#77725,#77726));
#16151=EDGE_LOOP('',(#77727,#77728,#77729,#77730));
#16152=EDGE_LOOP('',(#77731,#77732,#77733,#77734));
#16153=EDGE_LOOP('',(#77735,#77736,#77737,#77738));
#16154=EDGE_LOOP('',(#77739,#77740,#77741,#77742));
#16155=EDGE_LOOP('',(#77743,#77744,#77745,#77746));
#16156=EDGE_LOOP('',(#77747,#77748,#77749,#77750));
#16157=EDGE_LOOP('',(#77751,#77752,#77753,#77754));
#16158=EDGE_LOOP('',(#77755,#77756,#77757,#77758));
#16159=EDGE_LOOP('',(#77759,#77760,#77761,#77762));
#16160=EDGE_LOOP('',(#77763,#77764,#77765,#77766));
#16161=EDGE_LOOP('',(#77767,#77768,#77769));
#16162=EDGE_LOOP('',(#77770,#77771,#77772,#77773,#77774));
#16163=EDGE_LOOP('',(#77775,#77776,#77777,#77778,#77779));
#16164=EDGE_LOOP('',(#77780,#77781,#77782,#77783));
#16165=EDGE_LOOP('',(#77784,#77785,#77786,#77787));
#16166=EDGE_LOOP('',(#77788,#77789,#77790));
#16167=EDGE_LOOP('',(#77791,#77792,#77793,#77794));
#16168=EDGE_LOOP('',(#77795,#77796,#77797,#77798));
#16169=EDGE_LOOP('',(#77799,#77800,#77801,#77802));
#16170=EDGE_LOOP('',(#77803,#77804,#77805,#77806));
#16171=EDGE_LOOP('',(#77807,#77808,#77809,#77810));
#16172=EDGE_LOOP('',(#77811,#77812,#77813,#77814));
#16173=EDGE_LOOP('',(#77815,#77816,#77817,#77818));
#16174=EDGE_LOOP('',(#77819,#77820,#77821,#77822));
#16175=EDGE_LOOP('',(#77823,#77824,#77825,#77826));
#16176=EDGE_LOOP('',(#77827,#77828,#77829,#77830));
#16177=EDGE_LOOP('',(#77831,#77832,#77833,#77834));
#16178=EDGE_LOOP('',(#77835,#77836,#77837));
#16179=EDGE_LOOP('',(#77838,#77839,#77840,#77841,#77842));
#16180=EDGE_LOOP('',(#77843,#77844,#77845,#77846,#77847));
#16181=EDGE_LOOP('',(#77848,#77849,#77850,#77851));
#16182=EDGE_LOOP('',(#77852,#77853,#77854,#77855));
#16183=EDGE_LOOP('',(#77856,#77857,#77858));
#16184=EDGE_LOOP('',(#77859,#77860,#77861,#77862));
#16185=EDGE_LOOP('',(#77863,#77864,#77865,#77866));
#16186=EDGE_LOOP('',(#77867,#77868,#77869,#77870));
#16187=EDGE_LOOP('',(#77871,#77872,#77873,#77874));
#16188=EDGE_LOOP('',(#77875,#77876,#77877,#77878));
#16189=EDGE_LOOP('',(#77879,#77880,#77881,#77882));
#16190=EDGE_LOOP('',(#77883,#77884,#77885,#77886));
#16191=EDGE_LOOP('',(#77887,#77888,#77889,#77890));
#16192=EDGE_LOOP('',(#77891,#77892,#77893,#77894));
#16193=EDGE_LOOP('',(#77895,#77896,#77897,#77898));
#16194=EDGE_LOOP('',(#77899,#77900,#77901,#77902));
#16195=EDGE_LOOP('',(#77903,#77904,#77905));
#16196=EDGE_LOOP('',(#77906,#77907,#77908,#77909,#77910));
#16197=EDGE_LOOP('',(#77911,#77912,#77913,#77914,#77915));
#16198=EDGE_LOOP('',(#77916,#77917,#77918,#77919));
#16199=EDGE_LOOP('',(#77920,#77921,#77922,#77923));
#16200=EDGE_LOOP('',(#77924,#77925,#77926));
#16201=EDGE_LOOP('',(#77927,#77928,#77929,#77930));
#16202=EDGE_LOOP('',(#77931,#77932,#77933,#77934));
#16203=EDGE_LOOP('',(#77935,#77936,#77937,#77938));
#16204=EDGE_LOOP('',(#77939,#77940,#77941,#77942));
#16205=EDGE_LOOP('',(#77943,#77944,#77945,#77946));
#16206=EDGE_LOOP('',(#77947,#77948,#77949,#77950));
#16207=EDGE_LOOP('',(#77951,#77952,#77953,#77954));
#16208=EDGE_LOOP('',(#77955,#77956,#77957,#77958));
#16209=EDGE_LOOP('',(#77959,#77960,#77961,#77962));
#16210=EDGE_LOOP('',(#77963,#77964,#77965,#77966));
#16211=EDGE_LOOP('',(#77967,#77968,#77969,#77970));
#16212=EDGE_LOOP('',(#77971,#77972,#77973));
#16213=EDGE_LOOP('',(#77974,#77975,#77976,#77977,#77978));
#16214=EDGE_LOOP('',(#77979,#77980,#77981,#77982,#77983));
#16215=EDGE_LOOP('',(#77984,#77985,#77986,#77987));
#16216=EDGE_LOOP('',(#77988,#77989,#77990,#77991));
#16217=EDGE_LOOP('',(#77992,#77993,#77994));
#16218=EDGE_LOOP('',(#77995,#77996,#77997,#77998));
#16219=EDGE_LOOP('',(#77999,#78000,#78001,#78002));
#16220=EDGE_LOOP('',(#78003,#78004,#78005,#78006));
#16221=EDGE_LOOP('',(#78007,#78008,#78009,#78010));
#16222=EDGE_LOOP('',(#78011,#78012,#78013,#78014));
#16223=EDGE_LOOP('',(#78015,#78016,#78017,#78018));
#16224=EDGE_LOOP('',(#78019,#78020,#78021,#78022));
#16225=EDGE_LOOP('',(#78023,#78024,#78025,#78026));
#16226=EDGE_LOOP('',(#78027,#78028,#78029,#78030));
#16227=EDGE_LOOP('',(#78031,#78032,#78033,#78034));
#16228=EDGE_LOOP('',(#78035,#78036,#78037,#78038));
#16229=EDGE_LOOP('',(#78039,#78040,#78041));
#16230=EDGE_LOOP('',(#78042,#78043,#78044,#78045,#78046));
#16231=EDGE_LOOP('',(#78047,#78048,#78049,#78050,#78051));
#16232=EDGE_LOOP('',(#78052,#78053,#78054,#78055));
#16233=EDGE_LOOP('',(#78056,#78057,#78058,#78059));
#16234=EDGE_LOOP('',(#78060,#78061,#78062));
#16235=EDGE_LOOP('',(#78063,#78064,#78065,#78066));
#16236=EDGE_LOOP('',(#78067,#78068,#78069,#78070));
#16237=EDGE_LOOP('',(#78071,#78072,#78073,#78074));
#16238=EDGE_LOOP('',(#78075,#78076,#78077,#78078));
#16239=EDGE_LOOP('',(#78079,#78080,#78081,#78082));
#16240=EDGE_LOOP('',(#78083,#78084,#78085,#78086));
#16241=EDGE_LOOP('',(#78087,#78088,#78089,#78090));
#16242=EDGE_LOOP('',(#78091,#78092,#78093,#78094));
#16243=EDGE_LOOP('',(#78095,#78096,#78097,#78098));
#16244=EDGE_LOOP('',(#78099,#78100,#78101,#78102));
#16245=EDGE_LOOP('',(#78103,#78104,#78105,#78106));
#16246=EDGE_LOOP('',(#78107,#78108,#78109));
#16247=EDGE_LOOP('',(#78110,#78111,#78112,#78113,#78114));
#16248=EDGE_LOOP('',(#78115,#78116,#78117,#78118,#78119));
#16249=EDGE_LOOP('',(#78120,#78121,#78122,#78123));
#16250=EDGE_LOOP('',(#78124,#78125,#78126,#78127));
#16251=EDGE_LOOP('',(#78128,#78129,#78130));
#16252=EDGE_LOOP('',(#78131,#78132,#78133,#78134));
#16253=EDGE_LOOP('',(#78135,#78136,#78137,#78138));
#16254=EDGE_LOOP('',(#78139,#78140,#78141,#78142));
#16255=EDGE_LOOP('',(#78143,#78144,#78145,#78146));
#16256=EDGE_LOOP('',(#78147,#78148,#78149,#78150));
#16257=EDGE_LOOP('',(#78151,#78152,#78153,#78154));
#16258=EDGE_LOOP('',(#78155,#78156,#78157,#78158));
#16259=EDGE_LOOP('',(#78159,#78160,#78161,#78162));
#16260=EDGE_LOOP('',(#78163,#78164,#78165,#78166));
#16261=EDGE_LOOP('',(#78167,#78168,#78169,#78170));
#16262=EDGE_LOOP('',(#78171,#78172,#78173,#78174));
#16263=EDGE_LOOP('',(#78175,#78176,#78177));
#16264=EDGE_LOOP('',(#78178,#78179,#78180,#78181,#78182));
#16265=EDGE_LOOP('',(#78183,#78184,#78185,#78186,#78187));
#16266=EDGE_LOOP('',(#78188,#78189,#78190,#78191));
#16267=EDGE_LOOP('',(#78192,#78193,#78194,#78195));
#16268=EDGE_LOOP('',(#78196,#78197,#78198));
#16269=EDGE_LOOP('',(#78199,#78200,#78201,#78202));
#16270=EDGE_LOOP('',(#78203,#78204,#78205,#78206));
#16271=EDGE_LOOP('',(#78207,#78208,#78209,#78210));
#16272=EDGE_LOOP('',(#78211,#78212,#78213,#78214));
#16273=EDGE_LOOP('',(#78215,#78216,#78217,#78218));
#16274=EDGE_LOOP('',(#78219,#78220,#78221,#78222));
#16275=EDGE_LOOP('',(#78223,#78224,#78225,#78226));
#16276=EDGE_LOOP('',(#78227,#78228,#78229,#78230));
#16277=EDGE_LOOP('',(#78231,#78232,#78233,#78234));
#16278=EDGE_LOOP('',(#78235,#78236,#78237,#78238));
#16279=EDGE_LOOP('',(#78239,#78240,#78241,#78242));
#16280=EDGE_LOOP('',(#78243,#78244,#78245));
#16281=EDGE_LOOP('',(#78246,#78247,#78248,#78249,#78250));
#16282=EDGE_LOOP('',(#78251,#78252,#78253,#78254,#78255));
#16283=EDGE_LOOP('',(#78256,#78257,#78258,#78259));
#16284=EDGE_LOOP('',(#78260,#78261,#78262,#78263));
#16285=EDGE_LOOP('',(#78264,#78265,#78266));
#16286=EDGE_LOOP('',(#78267,#78268,#78269,#78270));
#16287=EDGE_LOOP('',(#78271,#78272,#78273,#78274));
#16288=EDGE_LOOP('',(#78275,#78276,#78277,#78278));
#16289=EDGE_LOOP('',(#78279,#78280,#78281,#78282));
#16290=EDGE_LOOP('',(#78283,#78284,#78285,#78286));
#16291=EDGE_LOOP('',(#78287,#78288,#78289,#78290));
#16292=EDGE_LOOP('',(#78291,#78292,#78293,#78294));
#16293=EDGE_LOOP('',(#78295,#78296,#78297,#78298));
#16294=EDGE_LOOP('',(#78299,#78300,#78301,#78302));
#16295=EDGE_LOOP('',(#78303,#78304,#78305,#78306));
#16296=EDGE_LOOP('',(#78307,#78308,#78309,#78310));
#16297=EDGE_LOOP('',(#78311,#78312,#78313));
#16298=EDGE_LOOP('',(#78314,#78315,#78316,#78317,#78318));
#16299=EDGE_LOOP('',(#78319,#78320,#78321,#78322,#78323));
#16300=EDGE_LOOP('',(#78324,#78325,#78326,#78327));
#16301=EDGE_LOOP('',(#78328,#78329,#78330,#78331));
#16302=EDGE_LOOP('',(#78332,#78333,#78334));
#16303=EDGE_LOOP('',(#78335,#78336,#78337,#78338));
#16304=EDGE_LOOP('',(#78339,#78340,#78341,#78342));
#16305=EDGE_LOOP('',(#78343,#78344,#78345,#78346));
#16306=EDGE_LOOP('',(#78347,#78348,#78349,#78350));
#16307=EDGE_LOOP('',(#78351,#78352,#78353,#78354));
#16308=EDGE_LOOP('',(#78355,#78356,#78357,#78358));
#16309=EDGE_LOOP('',(#78359,#78360,#78361,#78362));
#16310=EDGE_LOOP('',(#78363,#78364,#78365,#78366));
#16311=EDGE_LOOP('',(#78367,#78368,#78369,#78370));
#16312=EDGE_LOOP('',(#78371,#78372,#78373,#78374));
#16313=EDGE_LOOP('',(#78375,#78376,#78377,#78378));
#16314=EDGE_LOOP('',(#78379,#78380,#78381));
#16315=EDGE_LOOP('',(#78382,#78383,#78384,#78385,#78386));
#16316=EDGE_LOOP('',(#78387,#78388,#78389,#78390,#78391));
#16317=EDGE_LOOP('',(#78392,#78393,#78394,#78395));
#16318=EDGE_LOOP('',(#78396,#78397,#78398,#78399));
#16319=EDGE_LOOP('',(#78400,#78401,#78402));
#16320=EDGE_LOOP('',(#78403,#78404,#78405,#78406));
#16321=EDGE_LOOP('',(#78407,#78408,#78409,#78410));
#16322=EDGE_LOOP('',(#78411,#78412,#78413,#78414));
#16323=EDGE_LOOP('',(#78415,#78416,#78417,#78418));
#16324=EDGE_LOOP('',(#78419,#78420,#78421,#78422));
#16325=EDGE_LOOP('',(#78423,#78424,#78425,#78426));
#16326=EDGE_LOOP('',(#78427,#78428,#78429,#78430));
#16327=EDGE_LOOP('',(#78431,#78432,#78433,#78434));
#16328=EDGE_LOOP('',(#78435,#78436,#78437,#78438));
#16329=EDGE_LOOP('',(#78439,#78440,#78441,#78442));
#16330=EDGE_LOOP('',(#78443,#78444,#78445,#78446));
#16331=EDGE_LOOP('',(#78447,#78448,#78449));
#20606=CIRCLE('',#99387,1.17524047358083);
#20607=CIRCLE('',#99417,1.5);
#20608=CIRCLE('',#99418,1.5);
#20609=CIRCLE('',#99419,1.5);
#20610=CIRCLE('',#99448,1.17524047358085);
#20611=CIRCLE('',#99450,1.17524047358083);
#20612=CIRCLE('',#99452,1.17524047358083);
#20613=CIRCLE('',#99453,1.5);
#20614=CIRCLE('',#99457,0.125);
#20615=CIRCLE('',#99458,1.625);
#20616=CIRCLE('',#99460,1.25);
#20617=CIRCLE('',#99461,1.25);
#20618=CIRCLE('',#99462,1.25);
#20619=CIRCLE('',#99463,1.25);
#20620=CIRCLE('',#99464,1.25);
#20621=CIRCLE('',#99465,1.25);
#20622=CIRCLE('',#99467,1.44337567297406);
#20623=CIRCLE('',#99469,2.54610912703474);
#20624=CIRCLE('',#99470,0.0550000000000003);
#20625=CIRCLE('',#99471,2.50721825406948);
#20626=CIRCLE('',#99473,2.73389087296526);
#20627=CIRCLE('',#99475,2.75);
#20628=CIRCLE('',#99476,0.0550000000000007);
#20629=CIRCLE('',#99478,2.73389087296526);
#20630=CIRCLE('',#99480,2.73389087296526);
#20631=CIRCLE('',#99482,2.73389087296526);
#20632=CIRCLE('',#99484,2.73389087296526);
#20633=CIRCLE('',#99486,2.73389087296526);
#20634=CIRCLE('',#99488,2.73389087296526);
#20635=CIRCLE('',#99490,2.73389087296526);
#20636=CIRCLE('',#99492,2.73389087296526);
#20637=CIRCLE('',#99494,2.73389087296526);
#20638=CIRCLE('',#99496,2.73389087296526);
#20639=CIRCLE('',#99498,2.73389087296526);
#20640=CIRCLE('',#99500,2.73389087296526);
#20641=CIRCLE('',#99502,2.73389087296526);
#20642=CIRCLE('',#99504,2.73389087296526);
#20643=CIRCLE('',#99506,2.73389087296526);
#20644=CIRCLE('',#99508,2.73389087296526);
#20645=CIRCLE('',#99510,2.73389087296526);
#20646=CIRCLE('',#99512,2.73389087296526);
#20647=CIRCLE('',#99514,2.73389087296526);
#20648=CIRCLE('',#99516,2.73389087296526);
#20649=CIRCLE('',#99518,2.73389087296526);
#20650=CIRCLE('',#99520,2.73389087296526);
#20651=CIRCLE('',#99522,2.73389087296526);
#20652=CIRCLE('',#99524,2.73389087296526);
#20653=CIRCLE('',#99526,2.73389087296526);
#20654=CIRCLE('',#99528,2.73389087296526);
#20655=CIRCLE('',#99530,2.73389087296526);
#20656=CIRCLE('',#99532,2.73389087296526);
#20657=CIRCLE('',#99534,2.73389087296526);
#20658=CIRCLE('',#99536,2.73389087296526);
#20659=CIRCLE('',#99538,2.73389087296526);
#20660=CIRCLE('',#99540,2.73389087296526);
#20661=CIRCLE('',#99542,2.73389087296526);
#20662=CIRCLE('',#99544,2.73389087296526);
#20663=CIRCLE('',#99546,2.73389087296526);
#20664=CIRCLE('',#99548,2.73389087296526);
#20665=CIRCLE('',#99550,2.73389087296526);
#20666=CIRCLE('',#99552,2.73389087296526);
#20667=CIRCLE('',#99554,2.73389087296526);
#20668=CIRCLE('',#99556,2.73389087296526);
#20669=CIRCLE('',#99558,2.73389087296526);
#20670=CIRCLE('',#99560,2.73389087296526);
#20671=CIRCLE('',#99562,2.73389087296526);
#20672=CIRCLE('',#99564,2.73389087296526);
#20673=CIRCLE('',#99566,2.73389087296526);
#20674=CIRCLE('',#99568,2.73389087296526);
#20675=CIRCLE('',#99570,2.73389087296526);
#20676=CIRCLE('',#99572,2.73389087296526);
#20677=CIRCLE('',#99574,2.73389087296526);
#20678=CIRCLE('',#99576,2.73389087296526);
#20679=CIRCLE('',#99577,2.54610912703474);
#20680=CIRCLE('',#99578,2.54610912703474);
#20681=CIRCLE('',#99579,2.73389087296526);
#20682=CIRCLE('',#99581,2.73389087296526);
#20683=CIRCLE('',#99583,2.73389087296526);
#20684=CIRCLE('',#99585,2.73389087296526);
#20685=CIRCLE('',#99587,2.73389087296526);
#20686=CIRCLE('',#99589,2.73389087296526);
#20687=CIRCLE('',#99591,2.73389087296526);
#20688=CIRCLE('',#99593,2.73389087296526);
#20689=CIRCLE('',#99595,2.73389087296526);
#20690=CIRCLE('',#99597,2.73389087296526);
#20691=CIRCLE('',#99599,2.73389087296526);
#20692=CIRCLE('',#99601,2.73389087296526);
#20693=CIRCLE('',#99603,2.73389087296526);
#20694=CIRCLE('',#99605,2.73389087296526);
#20695=CIRCLE('',#99607,2.73389087296526);
#20696=CIRCLE('',#99609,2.73389087296526);
#20697=CIRCLE('',#99611,2.73389087296526);
#20698=CIRCLE('',#99613,2.73389087296526);
#20699=CIRCLE('',#99615,2.73389087296526);
#20700=CIRCLE('',#99617,2.73389087296526);
#20701=CIRCLE('',#99619,2.73389087296526);
#20702=CIRCLE('',#99621,2.73389087296526);
#20703=CIRCLE('',#99623,2.73389087296526);
#20704=CIRCLE('',#99625,2.73389087296526);
#20705=CIRCLE('',#99627,2.73389087296526);
#20706=CIRCLE('',#99629,2.73389087296526);
#20707=CIRCLE('',#99631,2.73389087296526);
#20708=CIRCLE('',#99633,2.73389087296526);
#20709=CIRCLE('',#99635,2.73389087296526);
#20710=CIRCLE('',#99637,2.73389087296526);
#20711=CIRCLE('',#99639,2.73389087296526);
#20712=CIRCLE('',#99641,2.73389087296526);
#20713=CIRCLE('',#99643,2.73389087296526);
#20714=CIRCLE('',#99645,2.73389087296526);
#20715=CIRCLE('',#99647,2.73389087296526);
#20716=CIRCLE('',#99649,2.73389087296526);
#20717=CIRCLE('',#99651,2.73389087296526);
#20718=CIRCLE('',#99653,2.73389087296526);
#20719=CIRCLE('',#99655,2.73389087296526);
#20720=CIRCLE('',#99657,2.73389087296526);
#20721=CIRCLE('',#99659,2.73389087296526);
#20722=CIRCLE('',#99661,2.73389087296526);
#20723=CIRCLE('',#99663,2.73389087296526);
#20724=CIRCLE('',#99665,2.73389087296526);
#20725=CIRCLE('',#99667,2.73389087296526);
#20726=CIRCLE('',#99669,2.73389087296526);
#20727=CIRCLE('',#99671,2.73389087296526);
#20728=CIRCLE('',#99673,2.73389087296526);
#20729=CIRCLE('',#99675,2.73389087296526);
#20730=CIRCLE('',#99678,2.50721825406948);
#20731=CIRCLE('',#99679,0.0549999999999999);
#20732=CIRCLE('',#99681,2.75);
#20733=CIRCLE('',#99683,2.75);
#20734=CIRCLE('',#99685,2.75);
#20735=CIRCLE('',#99687,2.75);
#20736=CIRCLE('',#99689,2.75);
#20737=CIRCLE('',#99691,2.75);
#20738=CIRCLE('',#99693,2.75);
#20739=CIRCLE('',#99695,2.75);
#20740=CIRCLE('',#99697,2.75);
#20741=CIRCLE('',#99699,2.75);
#20742=CIRCLE('',#99701,2.75);
#20743=CIRCLE('',#99703,2.75);
#20744=CIRCLE('',#99705,2.75);
#20745=CIRCLE('',#99707,2.75);
#20746=CIRCLE('',#99709,2.75);
#20747=CIRCLE('',#99711,2.75);
#20748=CIRCLE('',#99713,2.75);
#20749=CIRCLE('',#99715,2.75);
#20750=CIRCLE('',#99717,2.75);
#20751=CIRCLE('',#99719,2.75);
#20752=CIRCLE('',#99721,2.75);
#20753=CIRCLE('',#99723,2.75);
#20754=CIRCLE('',#99725,2.75);
#20755=CIRCLE('',#99727,2.75);
#20756=CIRCLE('',#99729,2.75);
#20757=CIRCLE('',#99731,2.75);
#20758=CIRCLE('',#99733,2.75);
#20759=CIRCLE('',#99735,2.75);
#20760=CIRCLE('',#99737,2.75);
#20761=CIRCLE('',#99739,2.75);
#20762=CIRCLE('',#99741,2.75);
#20763=CIRCLE('',#99743,2.75);
#20764=CIRCLE('',#99745,2.75);
#20765=CIRCLE('',#99747,2.75);
#20766=CIRCLE('',#99749,2.75);
#20767=CIRCLE('',#99751,2.75);
#20768=CIRCLE('',#99753,2.75);
#20769=CIRCLE('',#99755,2.75);
#20770=CIRCLE('',#99757,2.75);
#20771=CIRCLE('',#99759,2.75);
#20772=CIRCLE('',#99761,2.75);
#20773=CIRCLE('',#99763,2.75);
#20774=CIRCLE('',#99765,2.75);
#20775=CIRCLE('',#99767,2.75);
#20776=CIRCLE('',#99769,2.75);
#20777=CIRCLE('',#99771,2.75);
#20778=CIRCLE('',#99773,2.75);
#20779=CIRCLE('',#99775,2.75);
#20780=CIRCLE('',#99777,2.75);
#20781=CIRCLE('',#99779,2.75);
#20782=CIRCLE('',#99781,2.75);
#20783=CIRCLE('',#99783,2.75);
#20784=CIRCLE('',#99785,2.75);
#20785=CIRCLE('',#99787,2.75);
#20786=CIRCLE('',#99789,2.75);
#20787=CIRCLE('',#99791,2.75);
#20788=CIRCLE('',#99793,2.75);
#20789=CIRCLE('',#99795,2.75);
#20790=CIRCLE('',#99797,2.75);
#20791=CIRCLE('',#99799,2.75);
#20792=CIRCLE('',#99801,2.75);
#20793=CIRCLE('',#99803,2.75);
#20794=CIRCLE('',#99805,2.75);
#20795=CIRCLE('',#99807,2.75);
#20796=CIRCLE('',#99809,2.75);
#20797=CIRCLE('',#99811,2.75);
#20798=CIRCLE('',#99813,2.75);
#20799=CIRCLE('',#99815,2.75);
#20800=CIRCLE('',#99817,2.75);
#20801=CIRCLE('',#99819,2.75);
#20802=CIRCLE('',#99821,2.75);
#20803=CIRCLE('',#99823,2.75);
#20804=CIRCLE('',#99825,2.75);
#20805=CIRCLE('',#99827,2.75);
#20806=CIRCLE('',#99829,2.75);
#20807=CIRCLE('',#99831,2.75);
#20808=CIRCLE('',#99833,2.75);
#20809=CIRCLE('',#99835,2.75);
#20810=CIRCLE('',#99837,2.75);
#20811=CIRCLE('',#99839,2.75);
#20812=CIRCLE('',#99841,2.75);
#20813=CIRCLE('',#99843,2.75);
#20814=CIRCLE('',#99845,2.75);
#20815=CIRCLE('',#99847,2.75);
#20816=CIRCLE('',#99849,2.75);
#20817=CIRCLE('',#99851,2.75);
#20818=CIRCLE('',#99853,2.75);
#20819=CIRCLE('',#99855,2.75);
#20820=CIRCLE('',#99857,2.75);
#20821=CIRCLE('',#99859,2.75);
#20822=CIRCLE('',#99861,2.75);
#20823=CIRCLE('',#99863,2.75);
#20824=CIRCLE('',#99865,2.75);
#20825=CIRCLE('',#99867,2.75);
#20826=CIRCLE('',#99869,2.75);
#20827=CIRCLE('',#99871,2.75);
#20828=CIRCLE('',#99873,2.75);
#20829=CIRCLE('',#99875,2.75);
#20830=CIRCLE('',#99877,2.75);
#20831=CIRCLE('',#99878,2.75);
#20832=CIRCLE('',#99880,2.75);
#20833=CIRCLE('',#99882,2.75);
#20834=CIRCLE('',#99884,2.75);
#20835=CIRCLE('',#99886,2.75);
#20836=CIRCLE('',#99888,2.75);
#20837=CIRCLE('',#99890,2.75);
#20838=CIRCLE('',#99892,2.75);
#20839=CIRCLE('',#99894,2.75);
#20840=CIRCLE('',#99896,2.75);
#20841=CIRCLE('',#99898,2.75);
#20842=CIRCLE('',#99900,2.75);
#20843=CIRCLE('',#99902,2.75);
#20844=CIRCLE('',#99904,2.75);
#20845=CIRCLE('',#99906,2.75);
#20846=CIRCLE('',#99908,2.75);
#20847=CIRCLE('',#99910,2.75);
#20848=CIRCLE('',#99912,2.75);
#20849=CIRCLE('',#99914,2.75);
#20850=CIRCLE('',#99916,2.75);
#20851=CIRCLE('',#99918,2.75);
#20852=CIRCLE('',#99920,2.75);
#20853=CIRCLE('',#99922,2.75);
#20854=CIRCLE('',#99924,2.75);
#20855=CIRCLE('',#99926,2.75);
#20856=CIRCLE('',#99928,2.75);
#20857=CIRCLE('',#99930,2.75);
#20858=CIRCLE('',#99932,2.75);
#20859=CIRCLE('',#99934,2.75);
#20860=CIRCLE('',#99936,2.75);
#20861=CIRCLE('',#99938,2.75);
#20862=CIRCLE('',#99940,2.75);
#20863=CIRCLE('',#99942,2.75);
#20864=CIRCLE('',#99944,2.75);
#20865=CIRCLE('',#99946,2.75);
#20866=CIRCLE('',#99948,2.75);
#20867=CIRCLE('',#99950,2.75);
#20868=CIRCLE('',#99952,2.75);
#20869=CIRCLE('',#99954,2.75);
#20870=CIRCLE('',#99956,2.75);
#20871=CIRCLE('',#99958,2.75);
#20872=CIRCLE('',#99960,2.75);
#20873=CIRCLE('',#99962,2.75);
#20874=CIRCLE('',#99964,2.75);
#20875=CIRCLE('',#99966,2.75);
#20876=CIRCLE('',#99968,2.75);
#20877=CIRCLE('',#99970,2.75);
#20878=CIRCLE('',#99972,2.75);
#20879=CIRCLE('',#99974,2.75);
#20880=CIRCLE('',#99976,2.75);
#20881=CIRCLE('',#99978,2.75);
#20882=CIRCLE('',#99980,2.75);
#20883=CIRCLE('',#99982,2.75);
#20884=CIRCLE('',#99984,2.75);
#20885=CIRCLE('',#99986,2.75);
#20886=CIRCLE('',#99988,2.75);
#20887=CIRCLE('',#99990,2.75);
#20888=CIRCLE('',#99992,2.75);
#20889=CIRCLE('',#99994,2.75);
#20890=CIRCLE('',#99996,2.75);
#20891=CIRCLE('',#99998,2.75);
#20892=CIRCLE('',#100000,2.75);
#20893=CIRCLE('',#100002,2.75);
#20894=CIRCLE('',#100004,2.75);
#20895=CIRCLE('',#100006,2.75);
#20896=CIRCLE('',#100008,2.75);
#20897=CIRCLE('',#100010,2.75);
#20898=CIRCLE('',#100012,2.75);
#20899=CIRCLE('',#100014,2.75);
#20900=CIRCLE('',#100016,2.75);
#20901=CIRCLE('',#100018,2.75);
#20902=CIRCLE('',#100020,2.75);
#20903=CIRCLE('',#100022,2.75);
#20904=CIRCLE('',#100024,2.75);
#20905=CIRCLE('',#100026,2.75);
#20906=CIRCLE('',#100028,2.75);
#20907=CIRCLE('',#100030,2.75);
#20908=CIRCLE('',#100032,2.75);
#20909=CIRCLE('',#100034,2.75);
#20910=CIRCLE('',#100036,2.75);
#20911=CIRCLE('',#100038,2.75);
#20912=CIRCLE('',#100040,2.75);
#20913=CIRCLE('',#100042,2.75);
#20914=CIRCLE('',#100044,2.75);
#20915=CIRCLE('',#100046,2.75);
#20916=CIRCLE('',#100048,2.75);
#20917=CIRCLE('',#100050,2.75);
#20918=CIRCLE('',#100052,2.75);
#20919=CIRCLE('',#100054,2.75);
#20920=CIRCLE('',#100056,2.75);
#20921=CIRCLE('',#100058,2.75);
#20922=CIRCLE('',#100060,2.75);
#20923=CIRCLE('',#100062,2.75);
#20924=CIRCLE('',#100064,2.75);
#20925=CIRCLE('',#100066,2.75);
#20926=CIRCLE('',#100068,2.75);
#20927=CIRCLE('',#100070,2.75);
#20928=CIRCLE('',#100072,2.75);
#20929=CIRCLE('',#100366,0.00687499999999997);
#20930=CIRCLE('',#100377,1.44337567297406);
#20931=CIRCLE('',#100378,1.44337567297406);
#20932=CIRCLE('',#100379,1.44337567297406);
#20933=CIRCLE('',#100380,1.44337567297406);
#20934=CIRCLE('',#100381,1.44337567297406);
#20935=CIRCLE('',#100401,2.74633883476483);
#20936=CIRCLE('',#100404,0.0125);
#20937=CIRCLE('',#100405,0.0125);
#20938=CIRCLE('',#100407,0.0125000000000001);
#20939=CIRCLE('',#100408,0.0125000000000001);
#20940=CIRCLE('',#100410,0.0125000000000001);
#20941=CIRCLE('',#100411,0.0125000000000004);
#20942=CIRCLE('',#100412,0.0125);
#20943=CIRCLE('',#100413,0.0125000000000004);
#20944=CIRCLE('',#100415,0.0125);
#20945=CIRCLE('',#100416,0.0124999999999998);
#20946=CIRCLE('',#100422,0.00687499999999996);
#20947=CIRCLE('',#100426,0.0125000000000002);
#20948=CIRCLE('',#100427,2.74633883476483);
#20949=CIRCLE('',#100428,0.0124999999999998);
#20950=CIRCLE('',#100429,0.0125);
#20951=CIRCLE('',#100431,0.0125);
#20952=CIRCLE('',#100432,0.0125000000000001);
#20953=CIRCLE('',#100433,0.0125000000000003);
#20954=CIRCLE('',#100434,0.0125000000000003);
#20955=CIRCLE('',#100435,0.0124999999999998);
#20956=CIRCLE('',#100436,0.0125);
#20957=CIRCLE('',#100438,0.0125);
#20958=CIRCLE('',#100445,0.00687499999999999);
#20959=CIRCLE('',#100449,0.0124999999999998);
#20960=CIRCLE('',#100450,2.74633883476483);
#20961=CIRCLE('',#100451,0.0125000000000002);
#20962=CIRCLE('',#100452,0.0125);
#20963=CIRCLE('',#100454,0.0125);
#20964=CIRCLE('',#100455,0.0125000000000001);
#20965=CIRCLE('',#100456,0.0125000000000003);
#20966=CIRCLE('',#100457,0.0125000000000003);
#20967=CIRCLE('',#100458,0.0124999999999997);
#20968=CIRCLE('',#100459,0.0125);
#20969=CIRCLE('',#100461,0.0125);
#20970=CIRCLE('',#100468,0.00687499999999993);
#20971=CIRCLE('',#100472,0.0124999999999999);
#20972=CIRCLE('',#100473,2.74633883476483);
#20973=CIRCLE('',#100474,0.0124999999999999);
#20974=CIRCLE('',#100475,0.0125);
#20975=CIRCLE('',#100477,0.0125);
#20976=CIRCLE('',#100478,0.0124999999999999);
#20977=CIRCLE('',#100479,0.0125000000000004);
#20978=CIRCLE('',#100480,0.0125000000000004);
#20979=CIRCLE('',#100481,0.0124999999999999);
#20980=CIRCLE('',#100482,0.0125);
#20981=CIRCLE('',#100484,0.0125);
#20982=CIRCLE('',#100491,0.00687499999999995);
#20983=CIRCLE('',#100495,0.0124999999999999);
#20984=CIRCLE('',#100496,2.74633883476483);
#20985=CIRCLE('',#100497,0.0124999999999999);
#20986=CIRCLE('',#100498,0.0125);
#20987=CIRCLE('',#100500,0.0125);
#20988=CIRCLE('',#100501,0.0125);
#20989=CIRCLE('',#100502,0.0125000000000005);
#20990=CIRCLE('',#100503,0.0125000000000005);
#20991=CIRCLE('',#100504,0.0124999999999997);
#20992=CIRCLE('',#100505,0.0125);
#20993=CIRCLE('',#100507,0.0125000000000001);
#20994=CIRCLE('',#100514,0.00687499999999998);
#20995=CIRCLE('',#100518,0.0125);
#20996=CIRCLE('',#100519,2.74633883476483);
#20997=CIRCLE('',#100520,0.0125000000000002);
#20998=CIRCLE('',#100521,0.0125000000000001);
#20999=CIRCLE('',#100523,0.0125000000000001);
#21000=CIRCLE('',#100524,0.0125000000000001);
#21001=CIRCLE('',#100525,0.0125000000000004);
#21002=CIRCLE('',#100526,0.0125000000000004);
#21003=CIRCLE('',#100527,0.0124999999999998);
#21004=CIRCLE('',#100528,0.0125000000000001);
#21005=CIRCLE('',#100530,0.0125);
#21006=CIRCLE('',#100537,0.00687499999999991);
#21007=CIRCLE('',#100541,0.0125000000000002);
#21008=CIRCLE('',#100542,2.74633883476483);
#21009=CIRCLE('',#100543,0.0124999999999999);
#21010=CIRCLE('',#100544,0.0125);
#21011=CIRCLE('',#100546,0.0125);
#21012=CIRCLE('',#100547,0.0125);
#21013=CIRCLE('',#100548,0.0125000000000005);
#21014=CIRCLE('',#100549,0.0125000000000005);
#21015=CIRCLE('',#100550,0.0124999999999997);
#21016=CIRCLE('',#100551,0.0125);
#21017=CIRCLE('',#100553,0.0125);
#21018=CIRCLE('',#100560,0.00687500000000009);
#21019=CIRCLE('',#100564,0.0125000000000001);
#21020=CIRCLE('',#100565,2.74633883476483);
#21021=CIRCLE('',#100566,0.0125);
#21022=CIRCLE('',#100567,0.0124999999999999);
#21023=CIRCLE('',#100569,0.0124999999999999);
#21024=CIRCLE('',#100570,0.0125000000000001);
#21025=CIRCLE('',#100571,0.0125000000000004);
#21026=CIRCLE('',#100572,0.0125000000000004);
#21027=CIRCLE('',#100573,0.0124999999999998);
#21028=CIRCLE('',#100574,0.0124999999999999);
#21029=CIRCLE('',#100576,0.0125000000000001);
#21030=CIRCLE('',#100583,0.00687500000000007);
#21031=CIRCLE('',#100587,0.0124999999999999);
#21032=CIRCLE('',#100588,2.74633883476483);
#21033=CIRCLE('',#100589,0.0125);
#21034=CIRCLE('',#100590,0.0125000000000001);
#21035=CIRCLE('',#100592,0.0125000000000001);
#21036=CIRCLE('',#100593,0.0125);
#21037=CIRCLE('',#100594,0.0125000000000003);
#21038=CIRCLE('',#100595,0.0125000000000003);
#21039=CIRCLE('',#100596,0.0124999999999999);
#21040=CIRCLE('',#100597,0.0125000000000001);
#21041=CIRCLE('',#100599,0.0124999999999998);
#21042=CIRCLE('',#100606,0.00687500000000009);
#21043=CIRCLE('',#100610,0.0124999999999999);
#21044=CIRCLE('',#100611,2.74633883476483);
#21045=CIRCLE('',#100612,0.0125000000000001);
#21046=CIRCLE('',#100613,0.0125000000000001);
#21047=CIRCLE('',#100615,0.0125000000000001);
#21048=CIRCLE('',#100616,0.0125000000000001);
#21049=CIRCLE('',#100617,0.0125000000000004);
#21050=CIRCLE('',#100618,0.0125000000000004);
#21051=CIRCLE('',#100619,0.0124999999999998);
#21052=CIRCLE('',#100620,0.0125000000000001);
#21053=CIRCLE('',#100622,0.0125000000000001);
#21054=CIRCLE('',#100629,0.00687500000000004);
#21055=CIRCLE('',#100633,0.0124999999999999);
#21056=CIRCLE('',#100634,2.74633883476483);
#21057=CIRCLE('',#100635,0.0124999999999999);
#21058=CIRCLE('',#100636,0.0125000000000001);
#21059=CIRCLE('',#100638,0.0125000000000001);
#21060=CIRCLE('',#100639,0.0125000000000001);
#21061=CIRCLE('',#100640,0.0125000000000004);
#21062=CIRCLE('',#100641,0.0125000000000004);
#21063=CIRCLE('',#100642,0.0124999999999998);
#21064=CIRCLE('',#100643,0.0125000000000001);
#21065=CIRCLE('',#100645,0.0124999999999998);
#21066=CIRCLE('',#100652,0.00687500000000003);
#21067=CIRCLE('',#100656,0.0124999999999998);
#21068=CIRCLE('',#100657,2.74633883476483);
#21069=CIRCLE('',#100658,0.0125);
#21070=CIRCLE('',#100659,0.0125);
#21071=CIRCLE('',#100661,0.0125);
#21072=CIRCLE('',#100662,0.0124999999999999);
#21073=CIRCLE('',#100663,0.0125000000000003);
#21074=CIRCLE('',#100664,0.0125000000000003);
#21075=CIRCLE('',#100665,0.0124999999999998);
#21076=CIRCLE('',#100666,0.0125);
#21077=CIRCLE('',#100668,0.0125000000000001);
#21078=CIRCLE('',#100675,0.00687499999999996);
#21079=CIRCLE('',#100679,0.0124999999999999);
#21080=CIRCLE('',#100680,2.74633883476483);
#21081=CIRCLE('',#100681,0.0124999999999999);
#21082=CIRCLE('',#100682,0.0125);
#21083=CIRCLE('',#100684,0.0125);
#21084=CIRCLE('',#100685,0.0125);
#21085=CIRCLE('',#100686,0.0125000000000003);
#21086=CIRCLE('',#100687,0.0125000000000003);
#21087=CIRCLE('',#100688,0.0124999999999997);
#21088=CIRCLE('',#100689,0.0125);
#21089=CIRCLE('',#100691,0.0125000000000001);
#21090=CIRCLE('',#100698,0.00687499999999994);
#21091=CIRCLE('',#100702,0.0125000000000001);
#21092=CIRCLE('',#100703,2.74633883476483);
#21093=CIRCLE('',#100704,0.0124999999999999);
#21094=CIRCLE('',#100705,0.0125);
#21095=CIRCLE('',#100707,0.0125);
#21096=CIRCLE('',#100708,0.0125);
#21097=CIRCLE('',#100709,0.0125000000000004);
#21098=CIRCLE('',#100710,0.0125000000000004);
#21099=CIRCLE('',#100711,0.0124999999999998);
#21100=CIRCLE('',#100712,0.0125000000000001);
#21101=CIRCLE('',#100714,0.0125);
#21102=CIRCLE('',#100721,0.00687499999999994);
#21103=CIRCLE('',#100725,0.0125);
#21104=CIRCLE('',#100726,2.74633883476483);
#21105=CIRCLE('',#100727,0.0124999999999998);
#21106=CIRCLE('',#100728,0.0124999999999999);
#21107=CIRCLE('',#100730,0.0124999999999999);
#21108=CIRCLE('',#100731,0.0125);
#21109=CIRCLE('',#100732,0.0125000000000004);
#21110=CIRCLE('',#100733,0.0125000000000003);
#21111=CIRCLE('',#100734,0.0124999999999999);
#21112=CIRCLE('',#100735,0.0124999999999999);
#21113=CIRCLE('',#100737,0.0124999999999999);
#21114=CIRCLE('',#100744,0.00687500000000012);
#21115=CIRCLE('',#100748,0.0124999999999999);
#21116=CIRCLE('',#100749,2.74633883476483);
#21117=CIRCLE('',#100750,0.0125000000000002);
#21118=CIRCLE('',#100751,0.0125);
#21119=CIRCLE('',#100753,0.0125);
#21120=CIRCLE('',#100754,0.0125000000000001);
#21121=CIRCLE('',#100755,0.0125000000000005);
#21122=CIRCLE('',#100756,0.0125000000000005);
#21123=CIRCLE('',#100757,0.0124999999999998);
#21124=CIRCLE('',#100758,0.0125);
#21125=CIRCLE('',#100760,0.0125);
#21126=CIRCLE('',#100767,0.00687499999999988);
#21127=CIRCLE('',#100771,0.0125);
#21128=CIRCLE('',#100772,2.74633883476483);
#21129=CIRCLE('',#100773,0.0125000000000001);
#21130=CIRCLE('',#100774,0.0125);
#21131=CIRCLE('',#100776,0.0125);
#21132=CIRCLE('',#100777,0.0124999999999999);
#21133=CIRCLE('',#100778,0.0125000000000004);
#21134=CIRCLE('',#100779,0.0125000000000004);
#21135=CIRCLE('',#100780,0.0124999999999998);
#21136=CIRCLE('',#100781,0.0125);
#21137=CIRCLE('',#100783,0.0124999999999999);
#21138=CIRCLE('',#100790,0.00687500000000008);
#21139=CIRCLE('',#100794,0.0125);
#21140=CIRCLE('',#100795,2.74633883476483);
#21141=CIRCLE('',#100796,0.0124999999999999);
#21142=CIRCLE('',#100797,0.0125000000000001);
#21143=CIRCLE('',#100799,0.0125000000000001);
#21144=CIRCLE('',#100800,0.0124999999999998);
#21145=CIRCLE('',#100801,0.0125000000000005);
#21146=CIRCLE('',#100802,0.0125000000000005);
#21147=CIRCLE('',#100803,0.0124999999999998);
#21148=CIRCLE('',#100804,0.0125000000000001);
#21149=CIRCLE('',#100806,0.0124999999999999);
#21150=CIRCLE('',#100813,0.00687500000000005);
#21151=CIRCLE('',#100817,0.0125000000000001);
#21152=CIRCLE('',#100818,2.74633883476483);
#21153=CIRCLE('',#100819,0.0124999999999999);
#21154=CIRCLE('',#100820,0.0125);
#21155=CIRCLE('',#100822,0.0125);
#21156=CIRCLE('',#100823,0.0125000000000001);
#21157=CIRCLE('',#100824,0.0125000000000005);
#21158=CIRCLE('',#100825,0.0125000000000005);
#21159=CIRCLE('',#100826,0.0124999999999998);
#21160=CIRCLE('',#100827,0.0125);
#21161=CIRCLE('',#100829,0.0125);
#21162=CIRCLE('',#100836,0.00687499999999988);
#21163=CIRCLE('',#100840,0.0125000000000001);
#21164=CIRCLE('',#100841,2.74633883476483);
#21165=CIRCLE('',#100842,0.0124999999999998);
#21166=CIRCLE('',#100843,0.0125);
#21167=CIRCLE('',#100845,0.0125);
#21168=CIRCLE('',#100846,0.0124999999999998);
#21169=CIRCLE('',#100847,0.0125000000000005);
#21170=CIRCLE('',#100848,0.0125000000000005);
#21171=CIRCLE('',#100849,0.0124999999999999);
#21172=CIRCLE('',#100850,0.0125);
#21173=CIRCLE('',#100852,0.0125);
#21174=CIRCLE('',#100859,0.00687499999999997);
#21175=CIRCLE('',#100863,0.0125);
#21176=CIRCLE('',#100864,2.74633883476483);
#21177=CIRCLE('',#100865,0.0125);
#21178=CIRCLE('',#100866,0.0125);
#21179=CIRCLE('',#100868,0.0125);
#21180=CIRCLE('',#100869,0.0125000000000001);
#21181=CIRCLE('',#100870,0.0125000000000005);
#21182=CIRCLE('',#100871,0.0125000000000002);
#21183=CIRCLE('',#100872,0.0124999999999998);
#21184=CIRCLE('',#100873,0.0125);
#21185=CIRCLE('',#100875,0.0125);
#21186=CIRCLE('',#100882,0.00687499999999996);
#21187=CIRCLE('',#100886,0.0125);
#21188=CIRCLE('',#100887,2.74633883476483);
#21189=CIRCLE('',#100888,0.0125);
#21190=CIRCLE('',#100889,0.0125);
#21191=CIRCLE('',#100891,0.0125);
#21192=CIRCLE('',#100892,0.0125);
#21193=CIRCLE('',#100893,0.0125000000000004);
#21194=CIRCLE('',#100894,0.0125000000000004);
#21195=CIRCLE('',#100895,0.0124999999999997);
#21196=CIRCLE('',#100896,0.0125);
#21197=CIRCLE('',#100898,0.0125);
#21198=CIRCLE('',#100905,0.00687499999999993);
#21199=CIRCLE('',#100909,0.0125);
#21200=CIRCLE('',#100910,2.74633883476483);
#21201=CIRCLE('',#100911,0.0125);
#21202=CIRCLE('',#100912,0.0125);
#21203=CIRCLE('',#100914,0.0125);
#21204=CIRCLE('',#100915,0.0124999999999998);
#21205=CIRCLE('',#100916,0.0125000000000004);
#21206=CIRCLE('',#100917,0.0125000000000004);
#21207=CIRCLE('',#100918,0.0124999999999998);
#21208=CIRCLE('',#100919,0.0125);
#21209=CIRCLE('',#100921,0.0125);
#21210=CIRCLE('',#100928,0.00687500000000001);
#21211=CIRCLE('',#100932,0.0125);
#21212=CIRCLE('',#100933,2.74633883476484);
#21213=CIRCLE('',#100934,0.0125000000000002);
#21214=CIRCLE('',#100935,0.0125000000000001);
#21215=CIRCLE('',#100937,0.0125);
#21216=CIRCLE('',#100938,0.0125);
#21217=CIRCLE('',#100939,0.0125000000000003);
#21218=CIRCLE('',#100940,0.0125000000000003);
#21219=CIRCLE('',#100941,0.0124999999999997);
#21220=CIRCLE('',#100942,0.0125);
#21221=CIRCLE('',#100944,0.0125);
#21222=CIRCLE('',#100951,0.00687499999999995);
#21223=CIRCLE('',#100955,0.0125000000000001);
#21224=CIRCLE('',#100956,2.74633883476483);
#21225=CIRCLE('',#100957,0.0125000000000001);
#21226=CIRCLE('',#100958,0.0125);
#21227=CIRCLE('',#100960,0.0125);
#21228=CIRCLE('',#100961,0.0125);
#21229=CIRCLE('',#100962,0.0125000000000003);
#21230=CIRCLE('',#100963,0.0125000000000003);
#21231=CIRCLE('',#100964,0.0124999999999997);
#21232=CIRCLE('',#100965,0.0125);
#21233=CIRCLE('',#100967,0.0125);
#21234=CIRCLE('',#100974,0.00687499999999997);
#21235=CIRCLE('',#100978,0.0125);
#21236=CIRCLE('',#100979,2.74633883476483);
#21237=CIRCLE('',#100980,0.0125);
#21238=CIRCLE('',#100981,0.0125);
#21239=CIRCLE('',#100983,0.0125);
#21240=CIRCLE('',#100984,0.0125);
#21241=CIRCLE('',#100985,0.0125000000000004);
#21242=CIRCLE('',#100986,0.0125000000000004);
#21243=CIRCLE('',#100987,0.0124999999999997);
#21244=CIRCLE('',#100988,0.0125);
#21245=CIRCLE('',#100990,0.0125);
#21246=CIRCLE('',#100997,0.00687499999999996);
#21247=CIRCLE('',#101001,0.0125);
#21248=CIRCLE('',#101002,2.74633883476483);
#21249=CIRCLE('',#101003,0.0125);
#21250=CIRCLE('',#101004,0.0125);
#21251=CIRCLE('',#101006,0.0125);
#21252=CIRCLE('',#101007,0.0125);
#21253=CIRCLE('',#101008,0.0125000000000004);
#21254=CIRCLE('',#101009,0.0125000000000004);
#21255=CIRCLE('',#101010,0.0124999999999997);
#21256=CIRCLE('',#101011,0.0125);
#21257=CIRCLE('',#101013,0.0125);
#21258=CIRCLE('',#101020,0.00687500000000001);
#21259=CIRCLE('',#101024,0.0125);
#21260=CIRCLE('',#101025,2.74633883476483);
#21261=CIRCLE('',#101026,0.0125);
#21262=CIRCLE('',#101027,0.0125);
#21263=CIRCLE('',#101029,0.0125);
#21264=CIRCLE('',#101030,0.0125);
#21265=CIRCLE('',#101031,0.0125000000000003);
#21266=CIRCLE('',#101032,0.0125000000000003);
#21267=CIRCLE('',#101033,0.0124999999999997);
#21268=CIRCLE('',#101034,0.0125);
#21269=CIRCLE('',#101036,0.0125);
#21270=CIRCLE('',#101043,0.00687499999999995);
#21271=CIRCLE('',#101047,0.0125000000000001);
#21272=CIRCLE('',#101048,2.74633883476483);
#21273=CIRCLE('',#101049,0.0125);
#21274=CIRCLE('',#101050,0.0125);
#21275=CIRCLE('',#101052,0.0125);
#21276=CIRCLE('',#101053,0.0125);
#21277=CIRCLE('',#101054,0.0125000000000003);
#21278=CIRCLE('',#101055,0.0125000000000003);
#21279=CIRCLE('',#101056,0.0124999999999997);
#21280=CIRCLE('',#101057,0.0125);
#21281=CIRCLE('',#101059,0.0125);
#21282=CIRCLE('',#101066,0.00687499999999993);
#21283=CIRCLE('',#101070,0.0125);
#21284=CIRCLE('',#101071,2.74633883476483);
#21285=CIRCLE('',#101072,0.0124999999999999);
#21286=CIRCLE('',#101073,0.0125);
#21287=CIRCLE('',#101075,0.0125);
#21288=CIRCLE('',#101076,0.0125000000000001);
#21289=CIRCLE('',#101077,0.0125000000000004);
#21290=CIRCLE('',#101078,0.0125000000000004);
#21291=CIRCLE('',#101079,0.0124999999999998);
#21292=CIRCLE('',#101080,0.0125);
#21293=CIRCLE('',#101082,0.0125);
#21294=CIRCLE('',#101089,0.00687499999999996);
#21295=CIRCLE('',#101093,0.0124999999999999);
#21296=CIRCLE('',#101094,2.74633883476483);
#21297=CIRCLE('',#101095,0.0124999999999999);
#21298=CIRCLE('',#101096,0.0125000000000001);
#21299=CIRCLE('',#101098,0.0125000000000001);
#21300=CIRCLE('',#101099,0.0124999999999999);
#21301=CIRCLE('',#101100,0.0125000000000004);
#21302=CIRCLE('',#101101,0.0125000000000004);
#21303=CIRCLE('',#101102,0.0124999999999999);
#21304=CIRCLE('',#101103,0.0125000000000001);
#21305=CIRCLE('',#101105,0.0125000000000001);
#21306=CIRCLE('',#101112,0.00687499999999997);
#21307=CIRCLE('',#101116,0.0124999999999999);
#21308=CIRCLE('',#101117,2.74633883476483);
#21309=CIRCLE('',#101118,0.0124999999999999);
#21310=CIRCLE('',#101119,0.0125000000000001);
#21311=CIRCLE('',#101121,0.0125000000000001);
#21312=CIRCLE('',#101122,0.0125000000000001);
#21313=CIRCLE('',#101123,0.0125000000000005);
#21314=CIRCLE('',#101124,0.0125000000000005);
#21315=CIRCLE('',#101125,0.0124999999999998);
#21316=CIRCLE('',#101126,0.0125);
#21317=CIRCLE('',#101128,0.0124999999999999);
#21318=CIRCLE('',#101135,0.00687499999999988);
#21319=CIRCLE('',#101139,0.0125000000000001);
#21320=CIRCLE('',#101140,2.74633883476484);
#21321=CIRCLE('',#101141,0.0125);
#21322=CIRCLE('',#101142,0.0124999999999999);
#21323=CIRCLE('',#101144,0.0124999999999999);
#21324=CIRCLE('',#101145,0.0125000000000001);
#21325=CIRCLE('',#101146,0.0125000000000004);
#21326=CIRCLE('',#101147,0.0125000000000004);
#21327=CIRCLE('',#101148,0.0124999999999998);
#21328=CIRCLE('',#101149,0.0124999999999999);
#21329=CIRCLE('',#101151,0.0124999999999999);
#21330=CIRCLE('',#101158,0.00687500000000005);
#21331=CIRCLE('',#101162,0.0124999999999998);
#21332=CIRCLE('',#101163,2.74633883476483);
#21333=CIRCLE('',#101164,0.0125);
#21334=CIRCLE('',#101165,0.0125);
#21335=CIRCLE('',#101167,0.0125);
#21336=CIRCLE('',#101168,0.0125000000000001);
#21337=CIRCLE('',#101169,0.0125000000000005);
#21338=CIRCLE('',#101170,0.0125000000000005);
#21339=CIRCLE('',#101171,0.0124999999999997);
#21340=CIRCLE('',#101172,0.0125);
#21341=CIRCLE('',#101174,0.0125);
#21342=CIRCLE('',#101181,0.00687499999999999);
#21343=CIRCLE('',#101185,0.0124999999999999);
#21344=CIRCLE('',#101186,2.74633883476483);
#21345=CIRCLE('',#101187,0.0124999999999999);
#21346=CIRCLE('',#101188,0.0125);
#21347=CIRCLE('',#101190,0.0125);
#21348=CIRCLE('',#101191,0.0124999999999999);
#21349=CIRCLE('',#101192,0.0125000000000004);
#21350=CIRCLE('',#101193,0.0125000000000004);
#21351=CIRCLE('',#101194,0.0124999999999999);
#21352=CIRCLE('',#101195,0.0125);
#21353=CIRCLE('',#101197,0.0125);
#21354=CIRCLE('',#101204,0.00687499999999995);
#21355=CIRCLE('',#101208,0.0125);
#21356=CIRCLE('',#101209,2.74633883476483);
#21357=CIRCLE('',#101210,0.0124999999999999);
#21358=CIRCLE('',#101211,0.0125);
#21359=CIRCLE('',#101213,0.0125);
#21360=CIRCLE('',#101214,0.0125);
#21361=CIRCLE('',#101215,0.0125000000000006);
#21362=CIRCLE('',#101216,0.0125000000000002);
#21363=CIRCLE('',#101217,0.0124999999999997);
#21364=CIRCLE('',#101218,0.0125);
#21365=CIRCLE('',#101220,0.0125);
#21366=CIRCLE('',#101227,0.00687499999999988);
#21367=CIRCLE('',#101231,0.0124999999999998);
#21368=CIRCLE('',#101232,2.74633883476484);
#21369=CIRCLE('',#101233,0.0125000000000001);
#21370=CIRCLE('',#101234,0.0124999999999999);
#21371=CIRCLE('',#101236,0.0124999999999999);
#21372=CIRCLE('',#101237,0.0125000000000001);
#21373=CIRCLE('',#101238,0.0125000000000004);
#21374=CIRCLE('',#101239,0.0125000000000004);
#21375=CIRCLE('',#101240,0.0124999999999998);
#21376=CIRCLE('',#101241,0.0124999999999999);
#21377=CIRCLE('',#101243,0.0125000000000001);
#21378=CIRCLE('',#101250,0.00687499999999991);
#21379=CIRCLE('',#101254,0.0125);
#21380=CIRCLE('',#101255,2.74633883476483);
#21381=CIRCLE('',#101256,0.0124999999999998);
#21382=CIRCLE('',#101257,0.0125);
#21383=CIRCLE('',#101259,0.0124999999999999);
#21384=CIRCLE('',#101260,0.0125);
#21385=CIRCLE('',#101261,0.0125000000000005);
#21386=CIRCLE('',#101262,0.0125000000000005);
#21387=CIRCLE('',#101263,0.0124999999999997);
#21388=CIRCLE('',#101264,0.0125);
#21389=CIRCLE('',#101266,0.0124999999999999);
#21390=CIRCLE('',#101273,0.0068749999999999);
#21391=CIRCLE('',#101277,0.0125000000000001);
#21392=CIRCLE('',#101278,2.74633883476483);
#21393=CIRCLE('',#101279,0.0125000000000002);
#21394=CIRCLE('',#101280,0.0125000000000001);
#21395=CIRCLE('',#101282,0.0125000000000001);
#21396=CIRCLE('',#101283,0.0124999999999999);
#21397=CIRCLE('',#101284,0.0125000000000004);
#21398=CIRCLE('',#101285,0.0125000000000004);
#21399=CIRCLE('',#101286,0.0124999999999999);
#21400=CIRCLE('',#101287,0.0125);
#21401=CIRCLE('',#101289,0.0124999999999999);
#21402=CIRCLE('',#101296,0.00687499999999987);
#21403=CIRCLE('',#101300,0.0125);
#21404=CIRCLE('',#101301,2.74633883476483);
#21405=CIRCLE('',#101302,0.0125);
#21406=CIRCLE('',#101303,0.0125);
#21407=CIRCLE('',#101305,0.0125);
#21408=CIRCLE('',#101306,0.0125);
#21409=CIRCLE('',#101307,0.0125000000000003);
#21410=CIRCLE('',#101308,0.0125000000000003);
#21411=CIRCLE('',#101309,0.0124999999999997);
#21412=CIRCLE('',#101310,0.0125);
#21413=CIRCLE('',#101312,0.0125000000000001);
#21414=CIRCLE('',#101319,0.00687500000000009);
#21415=CIRCLE('',#101323,0.0125000000000002);
#21416=CIRCLE('',#101324,2.74633883476483);
#21417=CIRCLE('',#101325,0.0125);
#21418=CIRCLE('',#101326,0.0124999999999999);
#21419=CIRCLE('',#101328,0.0124999999999999);
#21420=CIRCLE('',#101329,0.0125000000000002);
#21421=CIRCLE('',#101330,0.0125000000000005);
#21422=CIRCLE('',#101331,0.0125000000000005);
#21423=CIRCLE('',#101332,0.0124999999999998);
#21424=CIRCLE('',#101333,0.0124999999999999);
#21425=CIRCLE('',#101335,0.0124999999999999);
#21426=CIRCLE('',#101342,0.00687499999999986);
#21427=CIRCLE('',#101346,0.0124999999999999);
#21428=CIRCLE('',#101347,2.74633883476483);
#21429=CIRCLE('',#101348,0.0125);
#21430=CIRCLE('',#101349,0.0124999999999999);
#21431=CIRCLE('',#101351,0.0124999999999999);
#21432=CIRCLE('',#101352,0.0124999999999999);
#21433=CIRCLE('',#101353,0.0125000000000005);
#21434=CIRCLE('',#101354,0.0125000000000005);
#21435=CIRCLE('',#101355,0.0124999999999998);
#21436=CIRCLE('',#101356,0.0124999999999999);
#21437=CIRCLE('',#101358,0.0125);
#21438=CIRCLE('',#101365,0.00687500000000003);
#21439=CIRCLE('',#101369,0.0125000000000002);
#21440=CIRCLE('',#101370,2.74633883476483);
#21441=CIRCLE('',#101371,0.0124999999999999);
#21442=CIRCLE('',#101372,0.0124999999999999);
#21443=CIRCLE('',#101374,0.0124999999999999);
#21444=CIRCLE('',#101375,0.0124999999999999);
#21445=CIRCLE('',#101376,0.0125000000000004);
#21446=CIRCLE('',#101377,0.0125000000000004);
#21447=CIRCLE('',#101378,0.0124999999999999);
#21448=CIRCLE('',#101379,0.0124999999999999);
#21449=CIRCLE('',#101381,0.0125);
#21450=CIRCLE('',#101388,0.00687499999999996);
#21451=CIRCLE('',#101392,0.0125);
#21452=CIRCLE('',#101393,2.74633883476483);
#21453=CIRCLE('',#101394,0.0124999999999999);
#21454=CIRCLE('',#101395,0.0124999999999998);
#21455=CIRCLE('',#101397,0.0124999999999998);
#21456=CIRCLE('',#101398,0.0125000000000001);
#21457=CIRCLE('',#101399,0.0125000000000003);
#21458=CIRCLE('',#101400,0.0125000000000003);
#21459=CIRCLE('',#101401,0.0124999999999998);
#21460=CIRCLE('',#101402,0.0124999999999998);
#21461=CIRCLE('',#101404,0.0125);
#21462=CIRCLE('',#101411,0.00687499999999994);
#21463=CIRCLE('',#101415,0.0125000000000001);
#21464=CIRCLE('',#101416,2.74633883476483);
#21465=CIRCLE('',#101417,0.0124999999999999);
#21466=CIRCLE('',#101418,0.0125);
#21467=CIRCLE('',#101420,0.0125);
#21468=CIRCLE('',#101421,0.0125);
#21469=CIRCLE('',#101422,0.0125000000000004);
#21470=CIRCLE('',#101423,0.0125000000000004);
#21471=CIRCLE('',#101424,0.0125);
#21472=CIRCLE('',#101425,0.0125000000000001);
#21473=CIRCLE('',#101427,0.0125);
#21474=CIRCLE('',#101434,0.00687499999999994);
#21475=CIRCLE('',#101438,0.0125000000000002);
#21476=CIRCLE('',#101439,2.74633883476483);
#21477=CIRCLE('',#101440,0.0125);
#21478=CIRCLE('',#101441,0.0125);
#21479=CIRCLE('',#101443,0.0125);
#21480=CIRCLE('',#101444,0.0124999999999999);
#21481=CIRCLE('',#101445,0.0125000000000005);
#21482=CIRCLE('',#101446,0.0125000000000005);
#21483=CIRCLE('',#101447,0.0124999999999998);
#21484=CIRCLE('',#101448,0.0125);
#21485=CIRCLE('',#101450,0.0125);
#21486=CIRCLE('',#101457,0.00687499999999985);
#21487=CIRCLE('',#101461,0.0125000000000001);
#21488=CIRCLE('',#101462,2.74633883476483);
#21489=CIRCLE('',#101463,0.0125000000000001);
#21490=CIRCLE('',#101464,0.0125);
#21491=CIRCLE('',#101466,0.0125);
#21492=CIRCLE('',#101467,0.0125);
#21493=CIRCLE('',#101468,0.0125000000000004);
#21494=CIRCLE('',#101469,0.0125000000000004);
#21495=CIRCLE('',#101470,0.0124999999999997);
#21496=CIRCLE('',#101471,0.0125);
#21497=CIRCLE('',#101473,0.0124999999999998);
#21498=CIRCLE('',#101480,0.00687500000000006);
#21499=CIRCLE('',#101484,0.0125);
#21500=CIRCLE('',#101485,2.74633883476483);
#21501=CIRCLE('',#101486,0.0125);
#21502=CIRCLE('',#101487,0.0125);
#21503=CIRCLE('',#101489,0.0125);
#21504=CIRCLE('',#101490,0.0125000000000001);
#21505=CIRCLE('',#101491,0.0125000000000004);
#21506=CIRCLE('',#101492,0.0125000000000004);
#21507=CIRCLE('',#101493,0.0124999999999998);
#21508=CIRCLE('',#101494,0.0125);
#21509=CIRCLE('',#101496,0.0125000000000001);
#21510=CIRCLE('',#101503,0.00687500000000008);
#21511=CIRCLE('',#101507,0.0124999999999999);
#21512=CIRCLE('',#101508,2.74633883476483);
#21513=CIRCLE('',#101509,0.0125);
#21514=CIRCLE('',#101510,0.0124999999999999);
#21515=CIRCLE('',#101512,0.0124999999999999);
#21516=CIRCLE('',#101513,0.0125000000000001);
#21517=CIRCLE('',#101514,0.0125000000000004);
#21518=CIRCLE('',#101515,0.0125000000000004);
#21519=CIRCLE('',#101516,0.0124999999999998);
#21520=CIRCLE('',#101517,0.0124999999999999);
#21521=CIRCLE('',#101519,0.0124999999999999);
#21522=CIRCLE('',#101526,0.00687500000000005);
#21523=CIRCLE('',#101530,0.0124999999999998);
#21524=CIRCLE('',#101531,2.74633883476483);
#21525=CIRCLE('',#101532,0.0125);
#21526=CIRCLE('',#101533,0.0124999999999998);
#21527=CIRCLE('',#101535,0.0124999999999998);
#21528=CIRCLE('',#101536,0.0125000000000001);
#21529=CIRCLE('',#101537,0.0125000000000005);
#21530=CIRCLE('',#101538,0.0125000000000005);
#21531=CIRCLE('',#101539,0.0124999999999997);
#21532=CIRCLE('',#101540,0.0124999999999998);
#21533=CIRCLE('',#101542,0.0125);
#21534=CIRCLE('',#101549,0.00687499999999988);
#21535=CIRCLE('',#101553,0.0124999999999998);
#21536=CIRCLE('',#101554,2.74633883476483);
#21537=CIRCLE('',#101555,0.0125000000000001);
#21538=CIRCLE('',#101556,0.0124999999999999);
#21539=CIRCLE('',#101558,0.0124999999999999);
#21540=CIRCLE('',#101559,0.0125000000000001);
#21541=CIRCLE('',#101560,0.0125000000000004);
#21542=CIRCLE('',#101561,0.0125000000000004);
#21543=CIRCLE('',#101562,0.0124999999999998);
#21544=CIRCLE('',#101563,0.0124999999999999);
#21545=CIRCLE('',#101565,0.0125);
#21546=CIRCLE('',#101572,0.00687499999999997);
#21547=CIRCLE('',#101576,0.0125);
#21548=CIRCLE('',#101577,2.74633883476483);
#21549=CIRCLE('',#101578,0.0124999999999999);
#21550=CIRCLE('',#101579,0.0125);
#21551=CIRCLE('',#101581,0.0125);
#21552=CIRCLE('',#101582,0.0125000000000001);
#21553=CIRCLE('',#101583,0.0125000000000005);
#21554=CIRCLE('',#101584,0.0125000000000005);
#21555=CIRCLE('',#101585,0.0124999999999998);
#21556=CIRCLE('',#101586,0.0125);
#21557=CIRCLE('',#101588,0.0125);
#21558=CIRCLE('',#101595,0.00687499999999996);
#21559=CIRCLE('',#101599,0.0125);
#21560=CIRCLE('',#101600,2.74633883476483);
#21561=CIRCLE('',#101601,0.0124999999999999);
#21562=CIRCLE('',#101602,0.0125);
#21563=CIRCLE('',#101604,0.0125);
#21564=CIRCLE('',#101605,0.0124999999999999);
#21565=CIRCLE('',#101606,0.0125000000000004);
#21566=CIRCLE('',#101607,0.0125000000000004);
#21567=CIRCLE('',#101608,0.0125);
#21568=CIRCLE('',#101609,0.0125);
#21569=CIRCLE('',#101611,0.0125);
#21570=CIRCLE('',#101618,0.00687499999999993);
#21571=CIRCLE('',#101622,0.0125);
#21572=CIRCLE('',#101623,2.74633883476483);
#21573=CIRCLE('',#101624,0.0125);
#21574=CIRCLE('',#101625,0.0125);
#21575=CIRCLE('',#101627,0.0125);
#21576=CIRCLE('',#101628,0.0125000000000001);
#21577=CIRCLE('',#101629,0.0125000000000004);
#21578=CIRCLE('',#101630,0.0125000000000004);
#21579=CIRCLE('',#101631,0.0124999999999998);
#21580=CIRCLE('',#101632,0.0125);
#21581=CIRCLE('',#101634,0.0125);
#21582=CIRCLE('',#101641,0.00687499999999995);
#21583=CIRCLE('',#101645,0.0125000000000001);
#21584=CIRCLE('',#101646,2.74633883476483);
#21585=CIRCLE('',#101647,0.0125);
#21586=CIRCLE('',#101648,0.0125);
#21587=CIRCLE('',#101650,0.0125);
#21588=CIRCLE('',#101651,0.0125);
#21589=CIRCLE('',#101652,0.0125000000000003);
#21590=CIRCLE('',#101653,0.0125000000000003);
#21591=CIRCLE('',#101654,0.0124999999999997);
#21592=CIRCLE('',#101655,0.0125);
#21593=CIRCLE('',#101657,0.0125);
#21594=CIRCLE('',#101664,0.00687499999999995);
#21595=CIRCLE('',#101668,0.0125);
#21596=CIRCLE('',#101669,2.74633883476483);
#21597=CIRCLE('',#101670,0.0125000000000001);
#21598=CIRCLE('',#101671,0.0125);
#21599=CIRCLE('',#101673,0.0125);
#21600=CIRCLE('',#101674,0.0125);
#21601=CIRCLE('',#101675,0.0125000000000003);
#21602=CIRCLE('',#101676,0.0125000000000003);
#21603=CIRCLE('',#101677,0.0124999999999997);
#21604=CIRCLE('',#101678,0.0125);
#21605=CIRCLE('',#101680,0.0125);
#21606=CIRCLE('',#101687,0.00687499999999996);
#21607=CIRCLE('',#101691,0.0125);
#21608=CIRCLE('',#101692,2.74633883476483);
#21609=CIRCLE('',#101693,0.0125);
#21610=CIRCLE('',#101694,0.0125);
#21611=CIRCLE('',#101696,0.0125);
#21612=CIRCLE('',#101697,0.0125);
#21613=CIRCLE('',#101698,0.0125000000000004);
#21614=CIRCLE('',#101699,0.0125000000000004);
#21615=CIRCLE('',#101700,0.0124999999999997);
#21616=CIRCLE('',#101701,0.0125);
#21617=CIRCLE('',#101703,0.0125);
#21618=CIRCLE('',#101710,0.00687499999999996);
#21619=CIRCLE('',#101714,0.0125);
#21620=CIRCLE('',#101715,2.74633883476483);
#21621=CIRCLE('',#101716,0.0125);
#21622=CIRCLE('',#101717,0.0125);
#21623=CIRCLE('',#101719,0.0125);
#21624=CIRCLE('',#101720,0.0125);
#21625=CIRCLE('',#101721,0.0125000000000004);
#21626=CIRCLE('',#101722,0.0125000000000004);
#21627=CIRCLE('',#101723,0.0124999999999997);
#21628=CIRCLE('',#101724,0.0125);
#21629=CIRCLE('',#101726,0.0125);
#21630=CIRCLE('',#101733,0.00687499999999995);
#21631=CIRCLE('',#101737,0.0125000000000001);
#21632=CIRCLE('',#101738,2.74633883476483);
#21633=CIRCLE('',#101739,0.0125);
#21634=CIRCLE('',#101740,0.0125);
#21635=CIRCLE('',#101742,0.0125);
#21636=CIRCLE('',#101743,0.0125);
#21637=CIRCLE('',#101744,0.0125000000000003);
#21638=CIRCLE('',#101745,0.0125000000000003);
#21639=CIRCLE('',#101746,0.0124999999999997);
#21640=CIRCLE('',#101747,0.0125);
#21641=CIRCLE('',#101749,0.0125);
#21642=CIRCLE('',#101756,0.00687500000000001);
#21643=CIRCLE('',#101760,0.0125);
#21644=CIRCLE('',#101761,2.74633883476483);
#21645=CIRCLE('',#101762,0.0125000000000002);
#21646=CIRCLE('',#101763,0.0125000000000001);
#21647=CIRCLE('',#101765,0.0125000000000001);
#21648=CIRCLE('',#101766,0.0125);
#21649=CIRCLE('',#101767,0.0125000000000003);
#21650=CIRCLE('',#101768,0.0125000000000003);
#21651=CIRCLE('',#101769,0.0124999999999997);
#21652=CIRCLE('',#101770,0.0125000000000001);
#21653=CIRCLE('',#101772,0.0125);
#21654=CIRCLE('',#101779,0.00687499999999993);
#21655=CIRCLE('',#101783,0.0125);
#21656=CIRCLE('',#101784,2.74633883476483);
#21657=CIRCLE('',#101785,0.0125);
#21658=CIRCLE('',#101786,0.0125);
#21659=CIRCLE('',#101788,0.0125);
#21660=CIRCLE('',#101789,0.0125000000000001);
#21661=CIRCLE('',#101790,0.0125000000000004);
#21662=CIRCLE('',#101791,0.0125000000000004);
#21663=CIRCLE('',#101792,0.0124999999999998);
#21664=CIRCLE('',#101793,0.0125);
#21665=CIRCLE('',#101795,0.0124999999999999);
#21666=CIRCLE('',#101802,0.00687499999999996);
#21667=CIRCLE('',#101806,0.0125);
#21668=CIRCLE('',#101807,2.74633883476483);
#21669=CIRCLE('',#101808,0.0125);
#21670=CIRCLE('',#101809,0.0125);
#21671=CIRCLE('',#101811,0.0125);
#21672=CIRCLE('',#101812,0.0125);
#21673=CIRCLE('',#101813,0.0125000000000004);
#21674=CIRCLE('',#101814,0.0125000000000004);
#21675=CIRCLE('',#101815,0.0125);
#21676=CIRCLE('',#101816,0.0125);
#21677=CIRCLE('',#101818,0.0125);
#21678=CIRCLE('',#101825,0.00687499999999997);
#21679=CIRCLE('',#101829,0.0124999999999999);
#21680=CIRCLE('',#101830,2.74633883476483);
#21681=CIRCLE('',#101831,0.0125);
#21682=CIRCLE('',#101832,0.0125);
#21683=CIRCLE('',#101834,0.0125);
#21684=CIRCLE('',#101835,0.0125000000000001);
#21685=CIRCLE('',#101836,0.0125000000000005);
#21686=CIRCLE('',#101837,0.0125000000000005);
#21687=CIRCLE('',#101838,0.0124999999999998);
#21688=CIRCLE('',#101839,0.0125);
#21689=CIRCLE('',#101841,0.0125);
#21690=CIRCLE('',#101848,0.00687499999999988);
#21691=CIRCLE('',#101852,0.0125000000000001);
#21692=CIRCLE('',#101853,2.74633883476483);
#21693=CIRCLE('',#101854,0.0124999999999998);
#21694=CIRCLE('',#101855,0.0125);
#21695=CIRCLE('',#101857,0.0125);
#21696=CIRCLE('',#101858,0.0125000000000001);
#21697=CIRCLE('',#101859,0.0125000000000005);
#21698=CIRCLE('',#101860,0.0125000000000005);
#21699=CIRCLE('',#101861,0.0124999999999998);
#21700=CIRCLE('',#101862,0.0125);
#21701=CIRCLE('',#101864,0.0125);
#21702=CIRCLE('',#101871,0.00687500000000005);
#21703=CIRCLE('',#101875,0.0125000000000001);
#21704=CIRCLE('',#101876,2.74633883476483);
#21705=CIRCLE('',#101877,0.0124999999999999);
#21706=CIRCLE('',#101878,0.0125);
#21707=CIRCLE('',#101880,0.0125);
#21708=CIRCLE('',#101881,0.0125000000000001);
#21709=CIRCLE('',#101882,0.0125000000000005);
#21710=CIRCLE('',#101883,0.0125000000000005);
#21711=CIRCLE('',#101884,0.0124999999999998);
#21712=CIRCLE('',#101885,0.0125);
#21713=CIRCLE('',#101887,0.0125);
#21714=CIRCLE('',#101894,0.00687500000000008);
#21715=CIRCLE('',#101898,0.0125);
#21716=CIRCLE('',#101899,2.74633883476483);
#21717=CIRCLE('',#101900,0.0124999999999999);
#21718=CIRCLE('',#101901,0.0125000000000001);
#21719=CIRCLE('',#101903,0.0125000000000001);
#21720=CIRCLE('',#101904,0.0125000000000001);
#21721=CIRCLE('',#101905,0.0125000000000005);
#21722=CIRCLE('',#101906,0.0125000000000005);
#21723=CIRCLE('',#101907,0.0124999999999998);
#21724=CIRCLE('',#101908,0.0125000000000001);
#21725=CIRCLE('',#101910,0.0125);
#21726=CIRCLE('',#101917,0.00687499999999988);
#21727=CIRCLE('',#101921,0.0125);
#21728=CIRCLE('',#101922,2.74633883476483);
#21729=CIRCLE('',#101923,0.0125000000000001);
#21730=CIRCLE('',#101924,0.0125);
#21731=CIRCLE('',#101926,0.0125);
#21732=CIRCLE('',#101927,0.0125000000000001);
#21733=CIRCLE('',#101928,0.0125000000000004);
#21734=CIRCLE('',#101929,0.0125000000000004);
#21735=CIRCLE('',#101930,0.0124999999999998);
#21736=CIRCLE('',#101931,0.0125);
#21737=CIRCLE('',#101933,0.0124999999999999);
#21738=CIRCLE('',#101940,0.00687499999999985);
#21739=CIRCLE('',#101944,0.0124999999999998);
#21740=CIRCLE('',#101945,2.74633883476483);
#21741=CIRCLE('',#101946,0.0125000000000001);
#21742=CIRCLE('',#101947,0.0125);
#21743=CIRCLE('',#101949,0.0125);
#21744=CIRCLE('',#101950,0.0125);
#21745=CIRCLE('',#101951,0.0125000000000004);
#21746=CIRCLE('',#101952,0.0125000000000004);
#21747=CIRCLE('',#101953,0.0124999999999998);
#21748=CIRCLE('',#101954,0.0125);
#21749=CIRCLE('',#101956,0.0125000000000002);
#21750=CIRCLE('',#101963,0.00687499999999994);
#21751=CIRCLE('',#101967,0.0125);
#21752=CIRCLE('',#101968,2.74633883476483);
#21753=CIRCLE('',#101969,0.0125000000000002);
#21754=CIRCLE('',#101970,0.0125);
#21755=CIRCLE('',#101972,0.0125);
#21756=CIRCLE('',#101973,0.0124999999999999);
#21757=CIRCLE('',#101974,0.0125000000000004);
#21758=CIRCLE('',#101975,0.0125000000000003);
#21759=CIRCLE('',#101976,0.0124999999999999);
#21760=CIRCLE('',#101977,0.0125);
#21761=CIRCLE('',#101979,0.0125);
#21762=CIRCLE('',#101986,0.00687500000000009);
#21763=CIRCLE('',#101990,0.0125000000000001);
#21764=CIRCLE('',#101991,2.74633883476483);
#21765=CIRCLE('',#101992,0.0124999999999999);
#21766=CIRCLE('',#101993,0.0124999999999998);
#21767=CIRCLE('',#101995,0.0124999999999998);
#21768=CIRCLE('',#101996,0.0125);
#21769=CIRCLE('',#101997,0.0125000000000004);
#21770=CIRCLE('',#101998,0.0125000000000004);
#21771=CIRCLE('',#101999,0.0124999999999998);
#21772=CIRCLE('',#102000,0.0125);
#21773=CIRCLE('',#102002,0.0125);
#21774=CIRCLE('',#102009,0.00687499999999996);
#21775=CIRCLE('',#102013,0.0124999999999999);
#21776=CIRCLE('',#102014,2.74633883476483);
#21777=CIRCLE('',#102015,0.0125);
#21778=CIRCLE('',#102016,0.0124999999999998);
#21779=CIRCLE('',#102018,0.0124999999999998);
#21780=CIRCLE('',#102019,0.0125);
#21781=CIRCLE('',#102020,0.0125000000000003);
#21782=CIRCLE('',#102021,0.0125000000000003);
#21783=CIRCLE('',#102022,0.0124999999999998);
#21784=CIRCLE('',#102023,0.0124999999999998);
#21785=CIRCLE('',#102025,0.0125000000000001);
#21786=CIRCLE('',#102032,0.00687500000000003);
#21787=CIRCLE('',#102036,0.0124999999999999);
#21788=CIRCLE('',#102037,2.74633883476483);
#21789=CIRCLE('',#102038,0.0125000000000002);
#21790=CIRCLE('',#102039,0.0125);
#21791=CIRCLE('',#102041,0.0125);
#21792=CIRCLE('',#102042,0.0124999999999999);
#21793=CIRCLE('',#102043,0.0125000000000004);
#21794=CIRCLE('',#102044,0.0125000000000004);
#21795=CIRCLE('',#102045,0.0124999999999998);
#21796=CIRCLE('',#102046,0.0125);
#21797=CIRCLE('',#102048,0.0124999999999999);
#21798=CIRCLE('',#102055,0.00687500000000004);
#21799=CIRCLE('',#102059,0.0125);
#21800=CIRCLE('',#102060,2.74633883476483);
#21801=CIRCLE('',#102061,0.0124999999999999);
#21802=CIRCLE('',#102062,0.0124999999999999);
#21803=CIRCLE('',#102064,0.0124999999999999);
#21804=CIRCLE('',#102065,0.0125000000000001);
#21805=CIRCLE('',#102066,0.0125000000000005);
#21806=CIRCLE('',#102067,0.0125000000000005);
#21807=CIRCLE('',#102068,0.0124999999999998);
#21808=CIRCLE('',#102069,0.0124999999999999);
#21809=CIRCLE('',#102071,0.0125000000000001);
#21810=CIRCLE('',#102078,0.00687500000000009);
#21811=CIRCLE('',#102082,0.0125);
#21812=CIRCLE('',#102083,2.74633883476483);
#21813=CIRCLE('',#102084,0.0125000000000001);
#21814=CIRCLE('',#102085,0.0124999999999999);
#21815=CIRCLE('',#102087,0.0124999999999999);
#21816=CIRCLE('',#102088,0.0125000000000001);
#21817=CIRCLE('',#102089,0.0125000000000004);
#21818=CIRCLE('',#102090,0.0125000000000004);
#21819=CIRCLE('',#102091,0.0124999999999998);
#21820=CIRCLE('',#102092,0.0124999999999999);
#21821=CIRCLE('',#102094,0.0124999999999999);
#21822=CIRCLE('',#102101,0.00687500000000007);
#21823=CIRCLE('',#102105,0.0124999999999999);
#21824=CIRCLE('',#102106,2.74633883476483);
#21825=CIRCLE('',#102107,0.0125);
#21826=CIRCLE('',#102108,0.0124999999999999);
#21827=CIRCLE('',#102110,0.0124999999999999);
#21828=CIRCLE('',#102111,0.0125);
#21829=CIRCLE('',#102112,0.0125000000000003);
#21830=CIRCLE('',#102113,0.0125000000000003);
#21831=CIRCLE('',#102114,0.0124999999999997);
#21832=CIRCLE('',#102115,0.0124999999999999);
#21833=CIRCLE('',#102117,0.0125);
#21834=CIRCLE('',#102124,0.00687500000000009);
#21835=CIRCLE('',#102128,0.0125000000000001);
#21836=CIRCLE('',#102129,2.74633883476483);
#21837=CIRCLE('',#102130,0.0125000000000001);
#21838=CIRCLE('',#102131,0.0125000000000001);
#21839=CIRCLE('',#102133,0.0125);
#21840=CIRCLE('',#102134,0.0125000000000001);
#21841=CIRCLE('',#102135,0.0125000000000004);
#21842=CIRCLE('',#102136,0.0125000000000004);
#21843=CIRCLE('',#102137,0.0124999999999998);
#21844=CIRCLE('',#102138,0.0125000000000001);
#21845=CIRCLE('',#102140,0.0124999999999999);
#21846=CIRCLE('',#102147,0.00687499999999991);
#21847=CIRCLE('',#102151,0.0125000000000002);
#21848=CIRCLE('',#102152,2.74633883476483);
#21849=CIRCLE('',#102153,0.0124999999999999);
#21850=CIRCLE('',#102154,0.0125);
#21851=CIRCLE('',#102156,0.0125);
#21852=CIRCLE('',#102157,0.0125);
#21853=CIRCLE('',#102158,0.0125000000000005);
#21854=CIRCLE('',#102159,0.0125000000000005);
#21855=CIRCLE('',#102160,0.0124999999999997);
#21856=CIRCLE('',#102161,0.0125);
#21857=CIRCLE('',#102163,0.0125);
#21858=CIRCLE('',#102170,0.00687499999999998);
#21859=CIRCLE('',#102174,0.0125);
#21860=CIRCLE('',#102175,2.74633883476483);
#21861=CIRCLE('',#102176,0.0124999999999998);
#21862=CIRCLE('',#102177,0.0124999999999999);
#21863=CIRCLE('',#102179,0.0124999999999999);
#21864=CIRCLE('',#102180,0.0125000000000001);
#21865=CIRCLE('',#102181,0.0125000000000004);
#21866=CIRCLE('',#102182,0.0125000000000004);
#21867=CIRCLE('',#102183,0.0124999999999998);
#21868=CIRCLE('',#102184,0.0124999999999999);
#21869=CIRCLE('',#102186,0.0125);
#21870=CIRCLE('',#102193,0.00687499999999995);
#21871=CIRCLE('',#102197,0.0124999999999999);
#21872=CIRCLE('',#102198,2.74633883476483);
#21873=CIRCLE('',#102199,0.0125);
#21874=CIRCLE('',#102200,0.0125);
#21875=CIRCLE('',#102202,0.0125);
#21876=CIRCLE('',#102203,0.0125);
#21877=CIRCLE('',#102204,0.0125000000000005);
#21878=CIRCLE('',#102205,0.0125000000000005);
#21879=CIRCLE('',#102206,0.0124999999999997);
#21880=CIRCLE('',#102207,0.0125);
#21881=CIRCLE('',#102209,0.0125000000000001);
#21882=CIRCLE('',#102216,0.00687499999999993);
#21883=CIRCLE('',#102220,0.0124999999999999);
#21884=CIRCLE('',#102221,2.74633883476483);
#21885=CIRCLE('',#102222,0.0124999999999999);
#21886=CIRCLE('',#102223,0.0125);
#21887=CIRCLE('',#102225,0.0125);
#21888=CIRCLE('',#102226,0.0124999999999999);
#21889=CIRCLE('',#102227,0.0125000000000004);
#21890=CIRCLE('',#102228,0.0125000000000004);
#21891=CIRCLE('',#102229,0.0124999999999999);
#21892=CIRCLE('',#102230,0.0125);
#21893=CIRCLE('',#102232,0.0125);
#21894=CIRCLE('',#102239,0.00687499999999999);
#21895=CIRCLE('',#102243,0.0124999999999998);
#21896=CIRCLE('',#102244,2.74633883476483);
#21897=CIRCLE('',#102245,0.0125000000000002);
#21898=CIRCLE('',#102246,0.0125);
#21899=CIRCLE('',#102248,0.0125);
#21900=CIRCLE('',#102249,0.0125000000000001);
#21901=CIRCLE('',#102250,0.0125000000000003);
#21902=CIRCLE('',#102251,0.0125000000000003);
#21903=CIRCLE('',#102252,0.0124999999999997);
#21904=CIRCLE('',#102253,0.0125);
#21905=CIRCLE('',#102255,0.0125);
#21906=CIRCLE('',#102262,0.00687499999999997);
#21907=CIRCLE('',#102266,0.0125000000000001);
#21908=CIRCLE('',#102267,2.74633883476483);
#21909=CIRCLE('',#102268,0.0125000000000001);
#21910=CIRCLE('',#102269,0.0125);
#21911=CIRCLE('',#102271,0.0125);
#21912=CIRCLE('',#102272,0.0125000000000001);
#21913=CIRCLE('',#102273,0.0125000000000004);
#21914=CIRCLE('',#102274,0.0125000000000004);
#21915=CIRCLE('',#102275,0.0124999999999998);
#21916=CIRCLE('',#102276,0.0125);
#21917=CIRCLE('',#102278,0.0125);
#21918=CIRCLE('',#102285,0.00687499999999996);
#21919=CIRCLE('',#102289,0.0124999999999998);
#21920=CIRCLE('',#102290,2.74633883476483);
#21921=CIRCLE('',#102291,0.0124999999999998);
#21922=CIRCLE('',#102292,0.0125);
#21923=CIRCLE('',#102294,0.0125);
#21924=CIRCLE('',#102295,0.0125000000000001);
#21925=CIRCLE('',#102296,0.0125000000000003);
#21926=CIRCLE('',#102297,0.0125000000000003);
#21927=CIRCLE('',#102298,0.0124999999999998);
#21928=CIRCLE('',#102299,0.0125);
#21929=CIRCLE('',#102301,0.0125);
#21930=CIRCLE('',#102308,0.00687499999999999);
#21931=CIRCLE('',#102312,0.0124999999999999);
#21932=CIRCLE('',#102313,2.74633883476483);
#21933=CIRCLE('',#102314,0.0124999999999999);
#21934=CIRCLE('',#102315,0.0125);
#21935=CIRCLE('',#102317,0.0125);
#21936=CIRCLE('',#102318,0.0124999999999999);
#21937=CIRCLE('',#102319,0.0125000000000004);
#21938=CIRCLE('',#102320,0.0125000000000004);
#21939=CIRCLE('',#102321,0.0124999999999999);
#21940=CIRCLE('',#102322,0.0125);
#21941=CIRCLE('',#102324,0.0125);
#21942=CIRCLE('',#102331,0.00687499999999995);
#21943=CIRCLE('',#102335,0.0125);
#21944=CIRCLE('',#102336,2.74633883476483);
#21945=CIRCLE('',#102337,0.0124999999999999);
#21946=CIRCLE('',#102338,0.0125);
#21947=CIRCLE('',#102340,0.0125);
#21948=CIRCLE('',#102341,0.0125);
#21949=CIRCLE('',#102342,0.0125000000000002);
#21950=CIRCLE('',#102343,0.0125000000000002);
#21951=CIRCLE('',#102344,0.0124999999999997);
#21952=CIRCLE('',#102345,0.0125);
#21953=CIRCLE('',#102347,0.0125);
#21954=CIRCLE('',#102354,0.00687499999999988);
#21955=CIRCLE('',#102358,0.0124999999999999);
#21956=CIRCLE('',#102359,2.74633883476483);
#21957=CIRCLE('',#102360,0.0125000000000001);
#21958=CIRCLE('',#102361,0.0125000000000001);
#21959=CIRCLE('',#102363,0.0125000000000001);
#21960=CIRCLE('',#102364,0.0125000000000001);
#21961=CIRCLE('',#102365,0.0125000000000004);
#21962=CIRCLE('',#102366,0.0125000000000004);
#21963=CIRCLE('',#102367,0.0124999999999998);
#21964=CIRCLE('',#102368,0.0125000000000001);
#21965=CIRCLE('',#102370,0.0125000000000001);
#21966=CIRCLE('',#102377,0.00687500000000005);
#21967=CIRCLE('',#102381,0.0125);
#21968=CIRCLE('',#102382,2.74633883476483);
#21969=CIRCLE('',#102383,0.0124999999999998);
#21970=CIRCLE('',#102384,0.0125);
#21971=CIRCLE('',#102386,0.0125);
#21972=CIRCLE('',#102387,0.0125000000000001);
#21973=CIRCLE('',#102388,0.0125000000000005);
#21974=CIRCLE('',#102389,0.0125000000000005);
#21975=CIRCLE('',#102390,0.0124999999999997);
#21976=CIRCLE('',#102391,0.0125);
#21977=CIRCLE('',#102393,0.0125);
#21978=CIRCLE('',#102400,0.0068749999999999);
#21979=CIRCLE('',#102404,0.0125000000000001);
#21980=CIRCLE('',#102405,2.74633883476483);
#21981=CIRCLE('',#102406,0.0124999999999998);
#21982=CIRCLE('',#102407,0.0125000000000001);
#21983=CIRCLE('',#102409,0.0125000000000001);
#21984=CIRCLE('',#102410,0.0124999999999999);
#21985=CIRCLE('',#102411,0.0125000000000004);
#21986=CIRCLE('',#102412,0.0125000000000004);
#21987=CIRCLE('',#102413,0.0124999999999998);
#21988=CIRCLE('',#102414,0.0125);
#21989=CIRCLE('',#102416,0.0125000000000001);
#21990=CIRCLE('',#102423,0.00687499999999987);
#21991=CIRCLE('',#102427,0.0125000000000001);
#21992=CIRCLE('',#102428,2.74633883476483);
#21993=CIRCLE('',#102429,0.0125);
#21994=CIRCLE('',#102430,0.0125);
#21995=CIRCLE('',#102432,0.0125);
#21996=CIRCLE('',#102433,0.0125);
#21997=CIRCLE('',#102434,0.0125000000000003);
#21998=CIRCLE('',#102435,0.0125000000000003);
#21999=CIRCLE('',#102436,0.0124999999999997);
#22000=CIRCLE('',#102437,0.0125);
#22001=CIRCLE('',#102439,0.0125000000000001);
#22002=CIRCLE('',#102446,0.0068749999999999);
#22003=CIRCLE('',#102450,0.0125000000000002);
#22004=CIRCLE('',#102451,2.74633883476483);
#22005=CIRCLE('',#102452,0.0125);
#22006=CIRCLE('',#102453,0.0124999999999999);
#22007=CIRCLE('',#102455,0.0124999999999999);
#22008=CIRCLE('',#102456,0.0124999999999999);
#22009=CIRCLE('',#102457,0.0125000000000005);
#22010=CIRCLE('',#102458,0.0125000000000005);
#22011=CIRCLE('',#102459,0.0124999999999998);
#22012=CIRCLE('',#102460,0.0124999999999999);
#22013=CIRCLE('',#102462,0.0125000000000001);
#22014=CIRCLE('',#102469,0.00687499999999986);
#22015=CIRCLE('',#102473,0.0125);
#22016=CIRCLE('',#102474,2.74633883476483);
#22017=CIRCLE('',#102475,0.0125);
#22018=CIRCLE('',#102476,0.0125000000000001);
#22019=CIRCLE('',#102478,0.0125000000000001);
#22020=CIRCLE('',#102479,0.0124999999999999);
#22021=CIRCLE('',#102480,0.0125000000000005);
#22022=CIRCLE('',#102481,0.0125000000000005);
#22023=CIRCLE('',#102482,0.0124999999999998);
#22024=CIRCLE('',#102483,0.0125000000000001);
#22025=CIRCLE('',#102485,0.0125);
#22026=CIRCLE('',#102492,0.00687499999999985);
#22027=CIRCLE('',#102496,0.0124999999999998);
#22028=CIRCLE('',#102497,2.74633883476483);
#22029=CIRCLE('',#102498,0.0124999999999999);
#22030=CIRCLE('',#102499,0.0125000000000001);
#22031=CIRCLE('',#102501,0.0125000000000001);
#22032=CIRCLE('',#102502,0.0125);
#22033=CIRCLE('',#102503,0.0125000000000004);
#22034=CIRCLE('',#102504,0.0125000000000004);
#22035=CIRCLE('',#102505,0.0124999999999999);
#22036=CIRCLE('',#102506,0.0125000000000001);
#22037=CIRCLE('',#102508,0.0124999999999999);
#22038=CIRCLE('',#102515,0.00687499999999996);
#22039=CIRCLE('',#102519,0.0125);
#22040=CIRCLE('',#102520,2.74633883476483);
#22041=CIRCLE('',#102521,0.0125000000000001);
#22042=CIRCLE('',#102522,0.0125000000000001);
#22043=CIRCLE('',#102524,0.0125000000000001);
#22044=CIRCLE('',#102525,0.0125000000000001);
#22045=CIRCLE('',#102526,0.0125000000000004);
#22046=CIRCLE('',#102527,0.0125000000000004);
#22047=CIRCLE('',#102528,0.0124999999999998);
#22048=CIRCLE('',#102529,0.0125000000000001);
#22049=CIRCLE('',#102531,0.0125);
#22050=CIRCLE('',#102538,0.00687499999999994);
#22051=CIRCLE('',#102542,0.0124999999999999);
#22052=CIRCLE('',#102543,2.74633883476483);
#22053=CIRCLE('',#102544,0.0124999999999999);
#22054=CIRCLE('',#102545,0.0125);
#22055=CIRCLE('',#102547,0.0125);
#22056=CIRCLE('',#102548,0.0125000000000001);
#22057=CIRCLE('',#102549,0.0125000000000003);
#22058=CIRCLE('',#102550,0.0125000000000003);
#22059=CIRCLE('',#102551,0.0124999999999998);
#22060=CIRCLE('',#102552,0.0125000000000001);
#22061=CIRCLE('',#102554,0.0125000000000001);
#22062=CIRCLE('',#102561,0.00687499999999994);
#22063=CIRCLE('',#102565,0.0125);
#22064=CIRCLE('',#102566,2.74633883476483);
#22065=CIRCLE('',#102567,0.0124999999999999);
#22066=CIRCLE('',#102568,0.0125);
#22067=CIRCLE('',#102570,0.0125);
#22068=CIRCLE('',#102571,0.0124999999999999);
#22069=CIRCLE('',#102572,0.0125000000000005);
#22070=CIRCLE('',#102573,0.0125000000000005);
#22071=CIRCLE('',#102574,0.0124999999999998);
#22072=CIRCLE('',#102575,0.0125);
#22073=CIRCLE('',#102577,0.0124999999999998);
#22074=CIRCLE('',#102584,0.00687499999999985);
#22075=CIRCLE('',#102588,0.0125000000000001);
#22076=CIRCLE('',#102589,2.74633883476483);
#22077=CIRCLE('',#102590,0.0125000000000001);
#22078=CIRCLE('',#102591,0.0125);
#22079=CIRCLE('',#102593,0.0125);
#22080=CIRCLE('',#102594,0.0125000000000001);
#22081=CIRCLE('',#102595,0.0125000000000004);
#22082=CIRCLE('',#102596,0.0125000000000004);
#22083=CIRCLE('',#102597,0.0124999999999997);
#22084=CIRCLE('',#102598,0.0125);
#22085=CIRCLE('',#102600,0.0125);
#22086=CIRCLE('',#102607,0.00687500000000006);
#22087=CIRCLE('',#102611,0.0125);
#22088=CIRCLE('',#102612,2.74633883476483);
#22089=CIRCLE('',#102613,0.0124999999999998);
#22090=CIRCLE('',#102614,0.0125);
#22091=CIRCLE('',#102616,0.0125);
#22092=CIRCLE('',#102617,0.0125000000000001);
#22093=CIRCLE('',#102618,0.0125000000000004);
#22094=CIRCLE('',#102619,0.0125000000000004);
#22095=CIRCLE('',#102620,0.0124999999999997);
#22096=CIRCLE('',#102621,0.0125);
#22097=CIRCLE('',#102623,0.0125);
#22098=CIRCLE('',#102630,0.00687500000000008);
#22099=CIRCLE('',#102634,0.0125000000000001);
#22100=CIRCLE('',#102635,2.74633883476483);
#22101=CIRCLE('',#102636,0.0124999999999999);
#22102=CIRCLE('',#102637,0.0124999999999999);
#22103=CIRCLE('',#102639,0.0124999999999999);
#22104=CIRCLE('',#102640,0.0125000000000001);
#22105=CIRCLE('',#102641,0.0125000000000004);
#22106=CIRCLE('',#102642,0.0125000000000004);
#22107=CIRCLE('',#102643,0.0124999999999998);
#22108=CIRCLE('',#102644,0.0124999999999999);
#22109=CIRCLE('',#102646,0.0124999999999998);
#24711=B_SPLINE_CURVE_WITH_KNOTS('',3,(#372462,#372463,#372464,#372465,
#372466,#372467,#372468,#372469,#372470,#372471,#372472,#372473,#372474,
#372475,#372476,#372477,#372478,#372479,#372480,#372481),.UNSPECIFIED.,
 .F.,.F.,(4,2,2,2,2,2,2,2,2,4),(-0.472681567119335,-0.442142555193499,-0.38234022419326,
-0.324797632394375,-0.265317638921683,-0.206291871345753,-0.149316840539157,
-0.0896533162312005,-0.0440651229089899,-9.99999998696488E-7),
 .UNSPECIFIED.);
#24712=B_SPLINE_CURVE_WITH_KNOTS('',3,(#372489,#372490,#372491,#372492,
#372493,#372494,#372495,#372496,#372497,#372498,#372499,#372500,#372501,
#372502,#372503,#372504),.UNSPECIFIED.,.F.,.F.,(4,2,2,2,2,2,2,4),(-26.8667509318511,
-26.824104786793,-26.7812253116685,-26.722294429582,-26.6622259040102,-26.6047498917014,
-26.5450263135477,-26.510596166175),.UNSPECIFIED.);
#24713=B_SPLINE_CURVE_WITH_KNOTS('',3,(#372509,#372510,#372511,#372512,
#372513,#372514,#372515,#372516,#372517,#372518,#372519,#372520,#372521,
#372522,#372523,#372524,#372525,#372526,#372527,#372528,#372529,#372530,
#372531,#372532,#372533,#372534,#372535,#372536,#372537,#372538,#372539,
#372540,#372541,#372542,#372543,#372544),.UNSPECIFIED.,.F.,.F.,(4,2,2,2,
2,2,2,2,2,2,2,2,2,2,2,2,2,4),(-1.41871218540484,-1.37878681735941,-1.31927200836046,
-1.26198522748958,-1.20229853529282,-1.14356070615823,-1.08648876969871,
-1.02678193345692,-0.968695892866923,-0.91068951354503,-0.851032976951095,
-0.793620463744822,-0.733538162871584,-0.674675729532023,-0.617695493756087,
-0.558023751508197,-0.499810626571642,-0.472681567119335),.UNSPECIFIED.);
#24714=B_SPLINE_CURVE_WITH_KNOTS('',3,(#372545,#372546,#372547,#372548,
#372549,#372550,#372551,#372552,#372553,#372554,#372555,#372556,#372557,
#372558,#372559,#372560,#372561,#372562,#372563,#372564,#372565,#372566,
#372567,#372568,#372569,#372570,#372571,#372572,#372573,#372574,#372575,
#372576,#372577,#372578,#372579,#372580),.UNSPECIFIED.,.F.,.F.,(4,2,2,2,
2,2,2,2,2,2,2,2,2,2,2,2,2,4),(-26.510596166175,-26.4870074929446,-26.4288576683979,
-26.3691024203233,-26.3119929596958,-26.2531910582434,-26.1934547120385,
-26.1361066574089,-26.0765272079356,-26.0180256611724,-25.9599965037028,
-25.899659107618,-25.8423746572756,-25.7836709165709,-25.7239000681539,
-25.6667235836525,-25.6073748228045,-25.5633168472621),.UNSPECIFIED.);
#24715=B_SPLINE_CURVE_WITH_KNOTS('',3,(#372585,#372586,#372587,#372588,
#372589,#372590,#372591,#372592,#372593,#372594,#372595,#372596,#372597,
#372598,#372599,#372600,#372601,#372602,#372603,#372604,#372605,#372606,
#372607,#372608,#372609,#372610,#372611,#372612,#372613,#372614,#372615,
#372616,#372617,#372618,#372619,#372620),.UNSPECIFIED.,.F.,.F.,(4,2,2,2,
2,2,2,2,2,2,2,2,2,2,2,2,2,4),(-2.36518766847454,-2.31596416709828,-2.25687811886001,
-2.1998608458798,-2.14015848136392,-2.08171970311433,-2.02430530224587,
-1.96425483793624,-1.90648696306987,-1.84756358898257,-1.78827674448427,
-1.73115470781314,-1.671427658721,-1.6127856936622,-1.55552841531158,-1.49525585707669,
-1.43728761568309,-1.41871218540484),.UNSPECIFIED.);
#24716=B_SPLINE_CURVE_WITH_KNOTS('',3,(#372621,#372622,#372623,#372624,
#372625,#372626,#372627,#372628,#372629,#372630,#372631,#372632,#372633,
#372634,#372635,#372636,#372637,#372638,#372639,#372640,#372641,#372642,
#372643,#372644,#372645,#372646,#372647,#372648,#372649,#372650,#372651,
#372652,#372653,#372654,#372655,#372656),.UNSPECIFIED.,.F.,.F.,(4,2,2,2,
2,2,2,2,2,2,2,2,2,2,2,2,2,4),(-25.5633168472621,-25.5484622494425,-25.4906365280881,
-25.4305245287703,-25.3730935305106,-25.3145962757104,-25.2548533628906,
-25.1977921450971,-25.1386474249518,-25.079220496869,-25.0215682750396,
-24.9616493129352,-24.9039748678532,-24.8456516573957,-24.7859071065283,
-24.7288626191054,-24.6698897716537,-24.6165058202546),.UNSPECIFIED.);
#24717=B_SPLINE_CURVE_WITH_KNOTS('',3,(#372661,#372662,#372663,#372664,
#372665,#372666,#372667,#372668,#372669,#372670,#372671,#372672,#372673,
#372674,#372675,#372676,#372677,#372678,#372679,#372680,#372681,#372682,
#372683,#372684,#372685,#372686,#372687,#372688,#372689,#372690,#372691,
#372692,#372693,#372694,#372695,#372696),.UNSPECIFIED.,.F.,.F.,(4,2,2,2,
2,2,2,2,2,2,2,2,2,2,2,2,2,4),(-3.31153449026076,-3.25341108907696,-3.19462285744369,
-3.13753038095501,-3.07779156837013,-3.01965519836493,-2.96165742705592,
-2.90194724384513,-2.84448427844684,-2.78444151548969,-2.72552350666032,
-2.66851289666458,-2.60880592198192,-2.55053735406635,-2.49287018538501,
-2.43300891651653,-2.37541100753461,-2.36518766847454),.UNSPECIFIED.);
#24718=B_SPLINE_CURVE_WITH_KNOTS('',3,(#372697,#372698,#372699,#372700,
#372701,#372702,#372703,#372704,#372705,#372706,#372707,#372708,#372709,
#372710,#372711,#372712,#372713,#372714,#372715,#372716,#372717,#372718,
#372719,#372720,#372721,#372722,#372723,#372724,#372725,#372726,#372727,
#372728,#372729,#372730,#372731,#372732,#372733,#372734),.UNSPECIFIED.,
 .F.,.F.,(4,2,2,2,2,2,2,2,2,2,2,2,2,2,2,2,2,2,4),(-24.6165058202546,-24.6098725741468,
-24.5523592800399,-24.4925957429875,-24.4345974342447,-24.3764107212499,
-24.316637102574,-24.2595192853478,-24.2006805602332,-24.1409243580283,
-24.0835417301909,-24.0239252260488,-23.9654580555157,-23.9073951002302,
-23.8470208311425,-23.789739831929,-23.7310017078749,-23.6712177426758,
-23.6690063317509),.UNSPECIFIED.);
#24719=B_SPLINE_CURVE_WITH_KNOTS('',3,(#372739,#372740,#372741,#372742,
#372743,#372744,#372745,#372746,#372747,#372748,#372749,#372750,#372751,
#372752,#372753,#372754,#372755,#372756,#372757,#372758,#372759,#372760,
#372761,#372762,#372763,#372764,#372765,#372766,#372767,#372768,#372769,
#372770,#372771,#372772,#372773,#372774,#372775,#372776),.UNSPECIFIED.,
 .F.,.F.,(4,2,2,2,2,2,2,2,2,2,2,2,2,2,2,2,2,2,4),(-4.25857656298863,-4.2514694638124,
-4.19174418285107,-4.13326131706642,-4.0758506244679,-4.01575319141907,
-3.95794168972433,-3.89905419814863,-3.83971964604971,-3.78255757670404,
-3.72280387132181,-3.66411410258304,-3.60684827544134,-3.54652503551378,
-3.48850971369039,-3.43003130272675,-3.37046574183593,-3.31313120077023,
-3.31153449026076),.UNSPECIFIED.);
#24720=B_SPLINE_CURVE_WITH_KNOTS('',3,(#372777,#372778,#372779,#372780,
#372781,#372782,#372783,#372784,#372785,#372786,#372787,#372788,#372789,
#372790,#372791,#372792,#372793,#372794,#372795,#372796,#372797,#372798,
#372799,#372800,#372801,#372802,#372803,#372804,#372805,#372806,#372807,
#372808,#372809,#372810,#372811,#372812),.UNSPECIFIED.,.F.,.F.,(4,2,2,2,
2,2,2,2,2,2,2,2,2,2,2,2,2,4),(-23.6690063317509,-23.6140133906547,-23.5546305007402,
-23.4957660462814,-23.4379098683801,-23.3777645802384,-23.320349365966,
-23.2618213189778,-23.2020690471691,-23.144991918597,-23.085816594075,-23.0264489632798,
-22.9687701730377,-22.9088221435739,-22.8511745951465,-22.792824818853,
-22.7330743558813,-22.7219983497172),.UNSPECIFIED.);
#24721=B_SPLINE_CURVE_WITH_KNOTS('',3,(#372817,#372818,#372819,#372820,
#372821,#372822,#372823,#372824,#372825,#372826,#372827,#372828,#372829,
#372830,#372831,#372832,#372833,#372834,#372835,#372836,#372837,#372838,
#372839,#372840,#372841,#372842,#372843,#372844,#372845,#372846,#372847,
#372848,#372849,#372850,#372851,#372852),.UNSPECIFIED.,.F.,.F.,(4,2,2,2,
2,2,2,2,2,2,2,2,2,2,2,2,2,4),(-5.2051363729884,-5.189395380046,-5.12964028728551,
-5.07146907437671,-5.01349379691273,-4.95374592874799,-4.89624787076232,
-4.83625851640013,-4.77730079908221,-4.72027382656529,-4.66054736488245,
-4.60223905529108,-4.54458645660951,-4.48468256608512,-4.427045030502,-4.36764481083087,
-4.30851470872145,-4.25857656298863),.UNSPECIFIED.);
#24722=B_SPLINE_CURVE_WITH_KNOTS('',3,(#372853,#372854,#372855,#372856,
#372857,#372858,#372859,#372860,#372861,#372862,#372863,#372864,#372865,
#372866,#372867,#372868,#372869,#372870,#372871,#372872,#372873,#372874,
#372875,#372876,#372877,#372878,#372879,#372880,#372881,#372882,#372883,
#372884,#372885,#372886,#372887,#372888),.UNSPECIFIED.,.F.,.F.,(4,2,2,2,
2,2,2,2,2,2,2,2,2,2,2,2,2,4),(-22.7219983497172,-22.676025638359,-22.6170264062843,
-22.5570758550377,-22.4995404278066,-22.4397526520792,-22.3817895352109,
-22.3235810572964,-22.2638047492202,-22.2066928005975,-22.1478325402814,
-22.0880720923164,-22.0306697641681,-21.9710316316543,-21.9126136704354,
-21.8545319204267,-21.7941363419943,-21.774643414205),.UNSPECIFIED.);
#24723=B_SPLINE_CURVE_WITH_KNOTS('',3,(#372893,#372894,#372895,#372896,
#372897,#372898,#372899,#372900,#372901,#372902,#372903,#372904,#372905,
#372906,#372907,#372908,#372909,#372910,#372911,#372912,#372913,#372914,
#372915,#372916,#372917,#372918,#372919,#372920,#372921,#372922,#372923,
#372924,#372925,#372926,#372927,#372928),.UNSPECIFIED.,.F.,.F.,(4,2,2,2,
2,2,2,2,2,2,2,2,2,2,2,2,2,4),(-6.1523798421435,-6.12797812550971,-6.0678494908681,
-6.01000954370658,-5.95117211963111,-5.89180550891634,-5.83461743202877,
-5.77485269586351,-5.71613058941083,-5.65887008025812,-5.59851207052264,
-5.54046497563872,-5.48202283843936,-5.4224223083538,-5.36505520297181,
-5.30531731824665,-5.24649433002998,-5.2051363729884),.UNSPECIFIED.);
#24724=B_SPLINE_CURVE_WITH_KNOTS('',3,(#372929,#372930,#372931,#372932,
#372933,#372934,#372935,#372936,#372937,#372938,#372939,#372940,#372941,
#372942,#372943,#372944,#372945,#372946,#372947,#372948,#372949,#372950,
#372951,#372952,#372953,#372954,#372955,#372956,#372957,#372958,#372959,
#372960,#372961,#372962,#372963,#372964),.UNSPECIFIED.,.F.,.F.,(4,2,2,2,
2,2,2,2,2,2,2,2,2,2,2,2,2,4),(-21.774643414205,-21.7368730308334,-21.6781156789626,
-21.6183343079821,-21.5611159054543,-21.5017142341325,-21.4429132756257,
-21.3850415803725,-21.3248784884646,-21.2674936111313,-21.2089498534046,
-21.149204030924,-21.092124905939,-21.0329342450041,-20.9736420131981,-20.9159515399632,
-20.8559898647572,-20.8275345885065),.UNSPECIFIED.);
#24725=B_SPLINE_CURVE_WITH_KNOTS('',3,(#372969,#372970,#372971,#372972,
#372973,#372974,#372975,#372976,#372977,#372978,#372979,#372980,#372981,
#372982,#372983,#372984,#372985,#372986,#372987,#372988,#372989,#372990,
#372991,#372992,#372993,#372994,#372995,#372996,#372997,#372998,#372999,
#373000,#373001,#373002,#373003,#373004),.UNSPECIFIED.,.F.,.F.,(4,2,2,2,
2,2,2,2,2,2,2,2,2,2,2,2,2,4),(-7.09901119411086,-7.06567228001258,-7.00590223384986,
-6.94838403007552,-6.88846344256541,-6.82948138012582,-6.77245205477943,
-6.71272178020251,-6.65438892106381,-6.59676515840048,-6.53683427285854,
-6.47917216681261,-6.41983327135308,-6.36067461928401,-6.30361531883792,
-6.24388277166941,-6.18537114395674,-6.1523798421435),.UNSPECIFIED.);
#24726=B_SPLINE_CURVE_WITH_KNOTS('',3,(#373005,#373006,#373007,#373008,
#373009,#373010,#373011,#373012,#373013,#373014,#373015,#373016,#373017,
#373018,#373019,#373020,#373021,#373022,#373023,#373024,#373025,#373026,
#373027,#373028,#373029,#373030,#373031,#373032,#373033,#373034,#373035,
#373036,#373037,#373038,#373039,#373040),.UNSPECIFIED.,.F.,.F.,(4,2,2,2,
2,2,2,2,2,2,2,2,2,2,2,2,2,4),(-20.8275345885065,-20.7983841401464,-20.7400228228779,
-20.680282347261,-20.6232436137976,-20.5642332011706,-20.5043661995887,
-20.4468234957869,-20.3870268705767,-20.3291145956587,-20.2708993561363,
-20.2111363425319,-20.154044915108,-20.0951782972609,-20.0354294865687,
-19.9780222496325,-19.9183778042751,-19.8805406314171),.UNSPECIFIED.);
#24727=B_SPLINE_CURVE_WITH_KNOTS('',3,(#373045,#373046,#373047,#373048,
#373049,#373050,#373051,#373052,#373053,#373054,#373055,#373056,#373057,
#373058,#373059,#373060,#373061,#373062,#373063,#373064,#373065,#373066,
#373067,#373068,#373069,#373070,#373071,#373072,#373073,#373074,#373075,
#373076,#373077,#373078,#373079,#373080),.UNSPECIFIED.,.F.,.F.,(4,2,2,2,
2,2,2,2,2,2,2,2,2,2,2,2,2,4),(-8.04621999375094,-8.00339153938214,-7.94400818753495,
-7.88680789834694,-7.82704787254924,-7.76830855204655,-7.71106766615472,
-7.65069041300283,-7.59262651715672,-7.53423564470816,-7.47461553332632,
-7.41723070274837,-7.35749066635497,-7.29864817158818,-7.24155700962402,
-7.18180133260471,-7.12361036089949,-7.09901119411086),.UNSPECIFIED.);
#24728=B_SPLINE_CURVE_WITH_KNOTS('',3,(#373081,#373082,#373083,#373084,
#373085,#373086,#373087,#373088,#373089,#373090,#373091,#373092,#373093,
#373094,#373095,#373096,#373097,#373098,#373099,#373100,#373101,#373102,
#373103,#373104,#373105,#373106,#373107,#373108,#373109,#373110,#373111,
#373112,#373113,#373114,#373115,#373116),.UNSPECIFIED.,.F.,.F.,(4,2,2,2,
2,2,2,2,2,2,2,2,2,2,2,2,2,4),(-19.8805406314171,-19.8600252528234,-19.8019396512075,
-19.7415382248585,-19.6843075087862,-19.6255460191888,-19.5657833749241,
-19.5085647062022,-19.4491595516306,-19.3904391548914,-19.3325668916662,
-19.2724014527642,-19.2150624092272,-19.156518030977,-19.0967949805335,
-19.0397279879862,-18.9805372818409,-18.9335464702939),.UNSPECIFIED.);
#24729=B_SPLINE_CURVE_WITH_KNOTS('',3,(#373121,#373122,#373123,#373124,
#373125,#373126,#373127,#373128,#373129,#373130,#373131,#373132,#373133,
#373134,#373135,#373136,#373137,#373138,#373139,#373140,#373141,#373142,
#373143,#373144,#373145,#373146,#373147,#373148,#373149,#373150,#373151,
#373152,#373153,#373154,#373155,#373156),.UNSPECIFIED.,.F.,.F.,(4,2,2,2,
2,2,2,2,2,2,2,2,2,2,2,2,2,4),(-8.99270588822923,-8.94052710995247,-8.88153589757056,
-8.82451847670245,-8.76480034119745,-8.70645794702851,-8.64887805663563,
-8.58893558193575,-8.53126377998128,-8.47200254273577,-8.41283058825612,
-8.35577115681652,-8.29604719351854,-8.23752186338507,-8.18016117488032,
-8.12001679633652,-8.06216332125115,-8.04621999375094),.UNSPECIFIED.);
#24730=B_SPLINE_CURVE_WITH_KNOTS('',3,(#373157,#373158,#373159,#373160,
#373161,#373162,#373163,#373164,#373165,#373166,#373167,#373168,#373169,
#373170,#373171,#373172,#373173,#373174,#373175,#373176,#373177,#373178,
#373179,#373180,#373181,#373182,#373183,#373184,#373185,#373186,#373187,
#373188,#373189,#373190,#373191,#373192),.UNSPECIFIED.,.F.,.F.,(4,2,2,2,
2,2,2,2,2,2,2,2,2,2,2,2,2,4),(-18.9335464702939,-18.9213385289384,-18.8636513496498,
-18.8036915093517,-18.7461437979602,-18.6877860607051,-18.6280720722102,
-18.571058014142,-18.5120517347588,-18.4522873912988,-18.3947524521812,
-18.3349625266769,-18.2771181850067,-18.2189113839145,-18.1591783284847,
-18.1021228024093,-18.0432652150961,-17.9871364878283),.UNSPECIFIED.);
#24731=B_SPLINE_CURVE_WITH_KNOTS('',3,(#373197,#373198,#373199,#373200,
#373201,#373202,#373203,#373204,#373205,#373206,#373207,#373208,#373209,
#373210,#373211,#373212,#373213,#373214,#373215,#373216,#373217,#373218,
#373219,#373220,#373221,#373222,#373223,#373224,#373225,#373226,#373227,
#373228,#373229,#373230,#373231,#373232,#373233,#373234),.UNSPECIFIED.,
 .F.,.F.,(4,2,2,2,2,2,2,2,2,2,2,2,2,2,2,2,2,2,4),(-9.93964057167184,-9.93859371440356,
-9.87885461052393,-9.82011317594689,-9.76290692726508,-9.70252589737089,
-9.64446015422855,-9.58613695209657,-9.52651257914626,-9.46912482257077,
-9.40939857554009,-9.35055175623928,-9.29348310865754,-9.23374289372987,
-9.17554716939251,-9.11766209798999,-9.05788526054439,-9.0003617689204,
-8.99270588822923),.UNSPECIFIED.);
#24732=B_SPLINE_CURVE_WITH_KNOTS('',3,(#373235,#373236,#373237,#373238,
#373239,#373240,#373241,#373242,#373243,#373244,#373245,#373246,#373247,
#373248,#373249,#373250,#373251,#373252,#373253,#373254,#373255,#373256,
#373257,#373258,#373259,#373260,#373261,#373262,#373263,#373264,#373265,
#373266,#373267,#373268,#373269,#373270,#373271,#373272),.UNSPECIFIED.,
 .F.,.F.,(4,2,2,2,2,2,2,2,2,2,2,2,2,2,2,2,2,2,4),(-17.9871364878283,-17.9835445667985,
-17.9261474434672,-17.8665122096331,-17.8082430505961,-17.7501687941794,
-17.6897771981761,-17.6325949724155,-17.573844684739,-17.5141177124938,
-17.4569127452413,-17.3975196787185,-17.3388990838463,-17.2810415304577,
-17.220889495943,-17.1636130941139,-17.1050835132873,-17.0454004826462,
-17.0404914447298),.UNSPECIFIED.);
#24733=B_SPLINE_CURVE_WITH_KNOTS('',3,(#373277,#373278,#373279,#373280,
#373281,#373282,#373283,#373284,#373285,#373286,#373287,#373288,#373289,
#373290,#373291,#373292,#373293,#373294,#373295,#373296,#373297,#373298,
#373299,#373300,#373301,#373302,#373303,#373304,#373305,#373306,#373307,
#373308,#373309,#373310,#373311,#373312),.UNSPECIFIED.,.F.,.F.,(4,2,2,2,
2,2,2,2,2,2,2,2,2,2,2,2,2,4),(-10.8858166820195,-10.8759296830837,-10.8162402914887,
-10.7579035150976,-10.700383897791,-10.6404453416983,-10.5827788519651,
-10.5236136488423,-10.4644437054219,-10.4073983139873,-10.3476993498427,
-10.2891754274228,-10.2318627119956,-10.1717180615585,-10.1138660280208,
-10.0551772063632,-9.99579242400764,-9.93964057167184),.UNSPECIFIED.);
#24734=B_SPLINE_CURVE_WITH_KNOTS('',3,(#373313,#373314,#373315,#373316,
#373317,#373318,#373319,#373320,#373321,#373322,#373323,#373324,#373325,
#373326,#373327,#373328,#373329,#373330,#373331,#373332,#373333,#373334,
#373335,#373336,#373337,#373338,#373339,#373340,#373341,#373342,#373343,
#373344,#373345,#373346,#373347,#373348),.UNSPECIFIED.,.F.,.F.,(4,2,2,2,
2,2,2,2,2,2,2,2,2,2,2,2,2,4),(-17.0404914447298,-16.9883602116983,-16.9291851008246,
-16.8701004552366,-16.812431962457,-16.7524898253569,-16.6950180268766,
-16.6366794116705,-16.5770094388777,-16.5200355200857,-16.4610491286714,
-16.4014094152831,-16.343897799262,-16.2841306201495,-16.2263732495688,
-16.1681906180146,-16.108505308808,-16.0948122175984),.UNSPECIFIED.);
#24735=B_SPLINE_CURVE_WITH_KNOTS('',3,(#373353,#373354,#373355,#373356,
#373357,#373358,#373359,#373360,#373361,#373362,#373363,#373364,#373365,
#373366,#373367,#373368,#373369,#373370,#373371,#373372,#373373,#373374,
#373375,#373376,#373377,#373378,#373379,#373380,#373381,#373382,#373383,
#373384,#373385,#373386,#373387,#373388),.UNSPECIFIED.,.F.,.F.,(4,2,2,2,
2,2,2,2,2,2,2,2,2,2,2,2,2,4),(-11.832087351168,-11.8138339556462,-11.7534648756654,
-11.6954125353176,-11.6371752570596,-11.5775621943317,-11.5201865842648,
-11.4604907625775,-11.4016550546539,-11.3446244188633,-11.284916446333,
-11.2267312150998,-11.16891646552,-11.1091484269857,-11.051634732786,-10.9919054425779,
-10.9329204280484,-10.8858166820195),.UNSPECIFIED.);
#24736=B_SPLINE_CURVE_WITH_KNOTS('',3,(#373389,#373390,#373391,#373392,
#373393,#373394,#373395,#373396,#373397,#373398,#373399,#373400,#373401,
#373402,#373403,#373404,#373405,#373406,#373407,#373408,#373409,#373410,
#373411,#373412,#373413,#373414,#373415,#373416,#373417,#373418,#373419,
#373420,#373421,#373422,#373423,#373424),.UNSPECIFIED.,.F.,.F.,(4,2,2,2,
2,2,2,2,2,2,2,2,2,2,2,2,2,4),(-16.0948122175984,-16.0515021496427,-15.9926695313415,
-15.9324153923589,-15.8750239845731,-15.8153918569545,-15.7572809932452,
-15.6992146839251,-15.6394874422163,-15.5823727082596,-15.5236537869628,
-15.463949466107,-15.4066780911298,-15.3471815689713,-15.2885473168338,
-15.2305919148884,-15.1703361945366,-15.1482252818032),.UNSPECIFIED.);
#24737=B_SPLINE_CURVE_WITH_KNOTS('',3,(#373429,#373430,#373431,#373432,
#373433,#373434,#373435,#373436,#373437,#373438,#373439,#373440,#373441,
#373442,#373443,#373444,#373445,#373446,#373447,#373448,#373449,#373450,
#373451,#373452,#373453,#373454,#373455,#373456,#373457,#373458,#373459,
#373460,#373461,#373462,#373463,#373464),.UNSPECIFIED.,.F.,.F.,(4,2,2,2,
2,2,2,2,2,2,2,2,2,2,2,2,2,4),(-12.7778456201867,-12.7507159363548,-12.6907972398182,
-12.63315153128,-12.5741033789915,-12.5149511544153,-12.457934468101,-12.3982779039036,
-12.3397708709816,-12.2825231389776,-12.2223940274391,-12.164558777205,
-12.1059724860861,-12.0466019010626,-11.9894187744342,-11.9297176737972,
-11.8709895175493,-11.832087351168),.UNSPECIFIED.);
#24738=B_SPLINE_CURVE_WITH_KNOTS('',3,(#373465,#373466,#373467,#373468,
#373469,#373470,#373471,#373472,#373473,#373474,#373475,#373476,#373477,
#373478,#373479,#373480,#373481,#373482,#373483,#373484,#373485,#373486,
#373487,#373488,#373489,#373490,#373491,#373492,#373493,#373494,#373495,
#373496,#373497,#373498,#373499,#373500),.UNSPECIFIED.,.F.,.F.,(4,2,2,2,
2,2,2,2,2,2,2,2,2,2,2,2,2,4),(-15.1482252818032,-15.113010827952,-15.0543821418657,
-14.9946236313547,-14.9374980414962,-14.87822340049,-14.8191393023084,-14.7593854651451,
-14.7011228135253,-14.6433226319139,-14.583472042581,-14.5258810193432,
-14.4662175738346,-14.4071474015193,-14.3501042723806,-14.2903635975994,
-14.2319417973738,-14.2013196209283),.UNSPECIFIED.);
#24739=B_SPLINE_CURVE_WITH_KNOTS('',3,(#373505,#373506,#373507,#373508,
#373509,#373510,#373511,#373512,#373513,#373514,#373515,#373516,#373517,
#373518,#373519,#373520,#373521,#373522,#373523,#373524,#373525,#373526,
#373527,#373528,#373529,#373530,#373531,#373532,#373533,#373534,#373535,
#373536,#373537,#373538,#373539,#373540),.UNSPECIFIED.,.F.,.F.,(4,2,2,2,
2,2,2,2,2,2,2,2,2,2,2,2,2,4),(-13.7232155909417,-13.6873757907163,-13.6277684747862,
-13.5704011152273,-13.5101862567796,-13.4513776947496,-13.3944017068863,
-13.3347439479979,-13.2765850339693,-13.2188599447086,-13.1591168402254,
-13.1016285928867,-13.0420270820403,-12.9830641004007,-12.926115617869,
-12.8664726675182,-12.8081571280792,-12.7778456201867),.UNSPECIFIED.);
#24740=B_SPLINE_CURVE_WITH_KNOTS('',3,(#373541,#373542,#373543,#373544,
#373545,#373546,#373547,#373548,#373549,#373550,#373551,#373552,#373553,
#373554,#373555,#373556,#373557,#373558,#373559,#373560,#373561,#373562,
#373563,#373564,#373565,#373566,#373567,#373568,#373569,#373570,#373571,
#373572,#373573,#373574,#373575,#373576),.UNSPECIFIED.,.F.,.F.,(4,2,2,2,
2,2,2,2,2,2,2,2,2,2,2,2,2,4),(-14.2013196209283,-14.1744209827898,-14.1143922449389,
-14.056641417422,-13.9975274962971,-13.9382658377259,-13.881148369121,-13.8213922549119,
-13.7627766957579,-13.7054437170459,-13.6452022732368,-13.5872597923407,
-13.5286021059723,-13.4691201312833,-13.4118301565226,-13.3520274598016,
-13.2931887753002,-13.2539690630572),.UNSPECIFIED.);
#24741=B_SPLINE_CURVE_WITH_KNOTS('',3,(#373581,#373582,#373583,#373584,
#373585,#373586,#373587,#373588,#373589,#373590,#373591,#373592,#373593,
#373594,#373595,#373596,#373597,#373598,#373599,#373600,#373601,#373602,
#373603,#373604,#373605,#373606,#373607,#373608,#373609,#373610,#373611,
#373612,#373613,#373614,#373615,#373616),.UNSPECIFIED.,.F.,.F.,(4,2,2,2,
2,2,2,2,2,2,2,2,2,2,2,2,2,4),(-14.6697112969214,-14.6241050026354,-14.5648559098276,
-14.5077561722265,-14.4480265312735,-14.3894230310587,-14.332128195858,
-14.2718981321671,-14.2139676440574,-14.1553691716209,-14.095897854982,
-14.038650897544,-13.9789744407945,-13.9202803244159,-13.8631942070711,
-13.8034950271421,-13.7454531716399,-13.7232155909417),.UNSPECIFIED.);
#24742=B_SPLINE_CURVE_WITH_KNOTS('',3,(#373617,#373618,#373619,#373620,
#373621,#373622,#373623,#373624,#373625,#373626,#373627,#373628,#373629,
#373630,#373631,#373632,#373633,#373634,#373635,#373636,#373637,#373638,
#373639,#373640,#373641,#373642,#373643,#373644,#373645,#373646,#373647,
#373648,#373649,#373650,#373651,#373652),.UNSPECIFIED.,.F.,.F.,(4,2,2,2,
2,2,2,2,2,2,2,2,2,2,2,2,2,4),(-13.2539690630572,-13.2359418394137,-13.176082960855,
-13.1178984829625,-13.0596379491205,-12.9998855188218,-12.9423777451317,
-12.8819525589879,-12.8230027330433,-12.765872417961,-12.7060572753572,
-12.6477589855018,-12.5898562582822,-12.5299712805315,-12.4723456099784,
-12.4125388540839,-12.3534374372755,-12.3060149682094),.UNSPECIFIED.);
#24743=B_SPLINE_CURVE_WITH_KNOTS('',3,(#373657,#373658,#373659,#373660,
#373661,#373662,#373663,#373664,#373665,#373666,#373667,#373668,#373669,
#373670,#373671,#373672,#373673,#373674,#373675,#373676,#373677,#373678,
#373679,#373680,#373681,#373682,#373683,#373684,#373685,#373686,#373687,
#373688,#373689,#373690,#373691,#373692),.UNSPECIFIED.,.F.,.F.,(4,2,2,2,
2,2,2,2,2,2,2,2,2,2,2,2,2,4),(-15.6160643869164,-15.5633841295623,-15.50414397945,
-15.4450746347767,-15.3873455777041,-15.3273390514912,-15.2698532500883,
-15.2114535121035,-15.1517412598184,-15.0947244496642,-15.0356767186234,
-14.9760606921884,-14.9184924702182,-14.8586652119684,-14.8009028783926,
-14.7408878749948,-14.6831512235933,-14.6697112969214),.UNSPECIFIED.);
#24744=B_SPLINE_CURVE_WITH_KNOTS('',3,(#373693,#373694,#373695,#373696,
#373697,#373698,#373699,#373700,#373701,#373702,#373703,#373704,#373705,
#373706,#373707,#373708,#373709,#373710,#373711,#373712,#373713,#373714,
#373715,#373716,#373717,#373718,#373719,#373720,#373721,#373722,#373723,
#373724,#373725,#373726,#373727,#373728),.UNSPECIFIED.,.F.,.F.,(4,2,2,2,
2,2,2,2,2,2,2,2,2,2,2,2,2,4),(-12.3060149682094,-12.2963423900386,-12.2365444281595,
-12.1780923177588,-12.1204810997582,-12.060423290409,-12.002642705299,-11.9433971991263,
-11.8841087980352,-11.8269538089724,-11.7671447134874,-11.7085033852916,
-11.6510943928729,-11.5908283874767,-11.5328603255245,-11.4740867043324,
-11.4145816503773,-11.3580906752407),.UNSPECIFIED.);
#24745=B_SPLINE_CURVE_WITH_KNOTS('',3,(#373733,#373734,#373735,#373736,
#373737,#373738,#373739,#373740,#373741,#373742,#373743,#373744,#373745,
#373746,#373747,#373748,#373749,#373750,#373751,#373752,#373753,#373754,
#373755,#373756,#373757,#373758,#373759,#373760,#373761,#373762,#373763,
#373764,#373765,#373766,#373767,#373768,#373769,#373770),.UNSPECIFIED.,
 .F.,.F.,(4,2,2,2,2,2,2,2,2,2,2,2,2,2,2,2,2,2,4),(-16.5634944095663,-16.558847104806,
-16.5013588527821,-16.4416263782018,-16.3834028937152,-16.3252384039002,
-16.2654055499546,-16.2081869526806,-16.1493686256731,-16.0895923551828,
-16.0323225157354,-15.9728613083516,-15.9142445390969,-15.8563229646398,
-15.7961028021386,-15.7388015559079,-15.6802071166945,-15.6204784650606,
-15.6160643869164),.UNSPECIFIED.);
#24746=B_SPLINE_CURVE_WITH_KNOTS('',3,(#373771,#373772,#373773,#373774,
#373775,#373776,#373777,#373778,#373779,#373780,#373781,#373782,#373783,
#373784,#373785,#373786,#373787,#373788,#373789,#373790,#373791,#373792,
#373793,#373794,#373795,#373796,#373797,#373798,#373799,#373800,#373801,
#373802,#373803,#373804,#373805,#373806,#373807,#373808),.UNSPECIFIED.,
 .F.,.F.,(4,2,2,2,2,2,2,2,2,2,2,2,2,2,2,2,2,2,4),(-11.3580906752407,-11.3572679784,
-11.2974169823782,-11.2385562886582,-11.1812485195102,-11.1207442499487,
-11.0625607234322,-11.0041471616058,-10.9444008964664,-10.8868963018946,
-10.8270552846813,-10.7680881341343,-10.7109133691843,-10.6510590470825,
-10.5927441318147,-10.5347636363483,-10.4748636050938,-10.4172220728686,
-10.4093537637416),.UNSPECIFIED.);
#24747=B_SPLINE_CURVE_WITH_KNOTS('',3,(#373813,#373814,#373815,#373816,
#373817,#373818,#373819,#373820,#373821,#373822,#373823,#373824,#373825,
#373826,#373827,#373828,#373829,#373830,#373831,#373832,#373833,#373834,
#373835,#373836,#373837,#373838,#373839,#373840,#373841,#373842,#373843,
#373844,#373845,#373846,#373847,#373848),.UNSPECIFIED.,.F.,.F.,(4,2,2,2,
2,2,2,2,2,2,2,2,2,2,2,2,2,4),(-17.5108474815656,-17.4981824073433,-17.4404188094185,
-17.3803782022338,-17.3227989832027,-17.264364113181,-17.2045902413959,
-17.1475176485416,-17.0884338098363,-17.0286723787512,-16.971064882126,
-16.9111983964038,-16.8533306609307,-16.7950509066526,-16.7352608424757,
-16.6781562232155,-16.6192252795436,-16.5634944095663),.UNSPECIFIED.);
#24748=B_SPLINE_CURVE_WITH_KNOTS('',3,(#373849,#373850,#373851,#373852,
#373853,#373854,#373855,#373856,#373857,#373858,#373859,#373860,#373861,
#373862,#373863,#373864,#373865,#373866,#373867,#373868,#373869,#373870,
#373871,#373872,#373873,#373874,#373875,#373876,#373877,#373878,#373879,
#373880,#373881,#373882,#373883,#373884),.UNSPECIFIED.,.F.,.F.,(4,2,2,2,
2,2,2,2,2,2,2,2,2,2,2,2,2,4),(-10.4093537637416,-10.357301350092,-10.2981875964388,
-10.2410598266438,-10.1812262852967,-10.1227625009788,-10.0650840056295,
-10.0050160951117,-9.94722420042477,-9.88787458177181,-9.8285780775151,
-9.77140334689103,-9.71156252645465,-9.65291378504466,-9.59545024275255,
-9.53517837450292,-9.47720292034625,-9.46102060630963),.UNSPECIFIED.);
#24749=B_SPLINE_CURVE_WITH_KNOTS('',3,(#373889,#373890,#373891,#373892,
#373893,#373894,#373895,#373896,#373897,#373898,#373899,#373900,#373901,
#373902,#373903,#373904,#373905,#373906,#373907,#373908,#373909,#373910,
#373911,#373912,#373913,#373914,#373915,#373916,#373917,#373918,#373919,
#373920,#373921,#373922,#373923,#373924),.UNSPECIFIED.,.F.,.F.,(4,2,2,2,
2,2,2,2,2,2,2,2,2,2,2,2,2,4),(-18.4588843632361,-18.4379249591453,-18.3797565748226,
-18.3192675325481,-18.2619844588132,-18.2031390102249,-18.1433099118157,
-18.08601177282,-18.0265223329137,-17.9677872345947,-17.9098351539592,-17.8495852647835,
-17.7922047206241,-17.7335795360629,-17.6737934777643,-17.6166574153344,
-17.5573855039092,-17.5108474815656),.UNSPECIFIED.);
#24750=B_SPLINE_CURVE_WITH_KNOTS('',3,(#373925,#373926,#373927,#373928,
#373929,#373930,#373931,#373932,#373933,#373934,#373935,#373936,#373937,
#373938,#373939,#373940,#373941,#373942,#373943,#373944,#373945,#373946,
#373947,#373948,#373949,#373950,#373951,#373952,#373953,#373954,#373955,
#373956,#373957,#373958,#373959,#373960),.UNSPECIFIED.,.F.,.F.,(4,2,2,2,
2,2,2,2,2,2,2,2,2,2,2,2,2,4),(-9.46102060630963,-9.41833880180209,-9.3588291150787,
-9.30150841089207,-9.24162988543094,-9.1827653326874,-9.12541671025634,
-9.06491011306255,-9.00672251636901,-8.94823424111932,-8.88848619394602,
-8.83097867682595,-8.77111742934779,-8.71214861344168,-8.65494532622163,
-8.59506904630521,-8.53675296718138,-8.51191438852878),.UNSPECIFIED.);
#24751=B_SPLINE_CURVE_WITH_KNOTS('',3,(#373965,#373966,#373967,#373968,
#373969,#373970,#373971,#373972,#373973,#373974,#373975,#373976,#373977,
#373978,#373979,#373980,#373981,#373982,#373983,#373984,#373985,#373986,
#373987,#373988,#373989,#373990,#373991,#373992,#373993,#373994,#373995,
#373996,#373997,#373998,#373999,#374000),.UNSPECIFIED.,.F.,.F.,(4,2,2,2,
2,2,2,2,2,2,2,2,2,2,2,2,2,4),(-19.4070183691008,-19.3774063864679,-19.3189557693523,
-19.2591417053657,-19.2020323274699,-19.1429320225021,-19.0830507906155,
-19.0254233516887,-18.965537605045,-18.9075870649366,-18.8492865591321,
-18.7894526316521,-18.7322992275162,-18.6733467783119,-18.6135256785197,
-18.5560357625839,-18.4963044063323,-18.4588843632361),.UNSPECIFIED.);
#24752=B_SPLINE_CURVE_WITH_KNOTS('',3,(#374001,#374002,#374003,#374004,
#374005,#374006,#374007,#374008,#374009,#374010,#374011,#374012,#374013,
#374014,#374015,#374016,#374017,#374018,#374019,#374020,#374021,#374022,
#374023,#374024,#374025,#374026,#374027,#374028,#374029,#374030,#374031,
#374032,#374033,#374034,#374035,#374036),.UNSPECIFIED.,.F.,.F.,(4,2,2,2,
2,2,2,2,2,2,2,2,2,2,2,2,2,4),(-8.51191438852878,-8.4787127733909,-8.41881348215695,
-8.36117138372012,-8.30115724125843,-8.24204667981905,-8.18490127059537,
-8.12504915972689,-8.06658902788,-8.00886034197012,-7.94879799919023,-7.89100997426156,
-7.83157560792974,-7.77228645996014,-7.71510635148775,-7.65525058713637,
-7.59660968033924,-7.56334284916346),.UNSPECIFIED.);
#24753=B_SPLINE_CURVE_WITH_KNOTS('',3,(#374041,#374042,#374043,#374044,
#374045,#374046,#374047,#374048,#374049,#374050,#374051,#374052,#374053,
#374054,#374055,#374056,#374057,#374058,#374059,#374060,#374061,#374062,
#374063,#374064,#374065,#374066,#374067,#374068,#374069,#374070,#374071,
#374072,#374073,#374074,#374075,#374076),.UNSPECIFIED.,.F.,.F.,(4,2,2,2,
2,2,2,2,2,2,2,2,2,2,2,2,2,4),(-20.3553623627869,-20.3171217343121,-20.2582684118752,
-20.1984073311347,-20.1410985076455,-20.0816003588123,-20.0227696675249,
-19.9648061934378,-19.9045463176452,-19.8471067919944,-19.7884701564408,
-19.7286478374059,-19.6714882098823,-19.6122040986311,-19.5528914181738,
-19.4951124766427,-19.4350576110104,-19.4070183691008),.UNSPECIFIED.);
#24754=B_SPLINE_CURVE_WITH_KNOTS('',3,(#374077,#374078,#374079,#374080,
#374081,#374082,#374083,#374084,#374085,#374086,#374087,#374088,#374089,
#374090,#374091,#374092,#374093,#374094,#374095,#374096,#374097,#374098,
#374099,#374100,#374101,#374102,#374103,#374104,#374105,#374106,#374107,
#374108,#374109,#374110,#374111,#374112),.UNSPECIFIED.,.F.,.F.,(4,2,2,2,
2,2,2,2,2,2,2,2,2,2,2,2,2,4),(-7.56334284916346,-7.53910774863586,-7.47884561490593,
-7.42087787571869,-7.3619414253141,-7.3024425331232,-7.2451286750284,-7.18523915485486,
-7.12638595068181,-7.06901188301772,-7.00851852031134,-6.95034191610438,
-6.89179603136193,-6.83206161385348,-6.77456607327972,-6.71470079446401,
-6.65574558736659,-6.61411156553163),.UNSPECIFIED.);
#24755=B_SPLINE_CURVE_WITH_KNOTS('',3,(#374117,#374118,#374119,#374120,
#374121,#374122,#374123,#374124,#374125,#374126,#374127,#374128,#374129,
#374130,#374131,#374132,#374133,#374134,#374135,#374136,#374137,#374138,
#374139,#374140,#374141,#374142,#374143,#374144,#374145,#374146,#374147,
#374148,#374149,#374150,#374151,#374152),.UNSPECIFIED.,.F.,.F.,(4,2,2,2,
2,2,2,2,2,2,2,2,2,2,2,2,2,4),(-21.3040471329169,-21.2575869056411,-21.1984857890134,
-21.1385060759405,-21.0808741357872,-21.020985062299,-20.9629703139414,
-20.9046646674613,-20.8448044072256,-20.7876184410835,-20.7286603001414,
-20.6688146325854,-20.6113178626411,-20.5515806625315,-20.4931217480668,
-20.4349453158928,-20.3744498438103,-20.3553623627869),.UNSPECIFIED.);
#24756=B_SPLINE_CURVE_WITH_KNOTS('',3,(#374153,#374154,#374155,#374156,
#374157,#374158,#374159,#374160,#374161,#374162,#374163,#374164,#374165,
#374166,#374167,#374168,#374169,#374170,#374171,#374172,#374173,#374174,
#374175,#374176,#374177,#374178,#374179,#374180,#374181,#374182,#374183,
#374184,#374185,#374186,#374187,#374188),.UNSPECIFIED.,.F.,.F.,(4,2,2,2,
2,2,2,2,2,2,2,2,2,2,2,2,2,4),(-6.61411156553163,-6.59852879776156,-6.53864687862724,
-6.48034472857874,-6.42226121693166,-6.36237812530755,-6.30475040045785,
-6.24466086149623,-6.18556874055552,-6.12842014710544,-6.06856566040906,
-6.0101242433252,-5.95236086994519,-5.89231953448862,-5.83455029960576,
-5.77504829554932,-5.71578177090393,-5.66552160898876),.UNSPECIFIED.);
#24757=B_SPLINE_CURVE_WITH_KNOTS('',3,(#374193,#374194,#374195,#374196,
#374197,#374198,#374199,#374200,#374201,#374202,#374203,#374204,#374205,
#374206,#374207,#374208,#374209,#374210,#374211,#374212,#374213,#374214,
#374215,#374216,#374217,#374218,#374219,#374220,#374221,#374222,#374223,
#374224,#374225,#374226,#374227,#374228),.UNSPECIFIED.,.F.,.F.,(4,2,2,2,
2,2,2,2,2,2,2,2,2,2,2,2,2,4),(-22.2524744631594,-22.1969643549059,-22.1374730057097,
-22.078565472214,-22.0206058074863,-21.9603516293046,-21.902869637356,-21.844236894089,
-21.7843953507018,-21.7272266490843,-21.6679458988016,-21.6085436857681,
-21.5507646986687,-21.4907113549369,-21.4330056552389,-21.3745547375389,
-21.3147177745165,-21.3040471329169),.UNSPECIFIED.);
#24758=B_SPLINE_CURVE_WITH_KNOTS('',3,(#374229,#374230,#374231,#374232,
#374233,#374234,#374235,#374236,#374237,#374238,#374239,#374240,#374241,
#374242,#374243,#374244,#374245,#374246,#374247,#374248,#374249,#374250,
#374251,#374252,#374253,#374254,#374255,#374256,#374257,#374258,#374259,
#374260,#374261,#374262,#374263,#374264,#374265,#374266),.UNSPECIFIED.,
 .F.,.F.,(4,2,2,2,2,2,2,2,2,2,2,2,2,2,2,2,2,2,4),(-5.66552160898876,-5.65861030605964,
-5.59875565665915,-5.54013765782867,-5.48261237053247,-5.42237542882488,
-5.36443033631434,-5.30543779450035,-5.24596500552574,-5.18867179004698,
-5.12878718949535,-5.06996044256316,-5.01257550757565,-4.95211087682467,
-4.89396022413654,-4.83537226336453,-4.77566683082353,-4.71819808424915,
-4.71640257571924),.UNSPECIFIED.);
#24759=B_SPLINE_CURVE_WITH_KNOTS('',3,(#374271,#374272,#374273,#374274,
#374275,#374276,#374277,#374278,#374279,#374280,#374281,#374282,#374283,
#374284,#374285,#374286,#374287,#374288,#374289,#374290,#374291,#374292,
#374293,#374294,#374295,#374296,#374297,#374298,#374299,#374300,#374301,
#374302,#374303,#374304,#374305,#374306,#374307,#374308),.UNSPECIFIED.,
 .F.,.F.,(4,2,2,2,2,2,2,2,2,2,2,2,2,2,2,2,2,2,4),(-23.2014899391179,-23.1944741493812,
-23.1368527057195,-23.0769758166295,-23.018913629611,-22.9606179964716,
-22.9007479118989,-22.8435446030669,-22.784596109354,-22.7247422526117,
-22.667253597635,-22.6075260296607,-22.5490052317576,-22.4908358902754,
-22.4303496168354,-22.3729921479549,-22.3141462340828,-22.2542699309318,
-22.2524744631594),.UNSPECIFIED.);
#24760=B_SPLINE_CURVE_WITH_KNOTS('',3,(#374309,#374310,#374311,#374312,
#374313,#374314,#374315,#374316,#374317,#374318,#374319,#374320,#374321,
#374322,#374323,#374324,#374325,#374326,#374327,#374328,#374329,#374330,
#374331,#374332,#374333,#374334,#374335,#374336,#374337,#374338,#374339,
#374340,#374341,#374342,#374343,#374344),.UNSPECIFIED.,.F.,.F.,(4,2,2,2,
2,2,2,2,2,2,2,2,2,2,2,2,2,4),(-4.71640257571924,-4.65834451124209,-4.59941813000702,
-4.54220227768689,-4.48233054243417,-4.42405736880598,-4.36594566804926,
-4.30609422957073,-4.24849578389153,-4.18834689967496,-4.1292885102004,
-4.07215083811356,-4.01230974894481,-3.95390216281254,-3.89611869200024,
-3.83611389751589,-3.77837843111154,-3.76793502765558),.UNSPECIFIED.);
#24761=B_SPLINE_CURVE_WITH_KNOTS('',3,(#374349,#374350,#374351,#374352,
#374353,#374354,#374355,#374356,#374357,#374358,#374359,#374360,#374361,
#374362,#374363,#374364,#374365,#374366,#374367,#374368,#374369,#374370,
#374371,#374372,#374373,#374374,#374375,#374376,#374377,#374378,#374379,
#374380,#374381,#374382,#374383,#374384),.UNSPECIFIED.,.F.,.F.,(4,2,2,2,
2,2,2,2,2,2,2,2,2,2,2,2,2,4),(-24.1499027888804,-24.1346238268317,-24.0766829154348,
-24.0164498947841,-23.9589407260275,-23.9003269603049,-23.8404823973082,
-23.7833187058296,-23.7240565994254,-23.6645824940566,-23.6068184151902,
-23.5467820581576,-23.4890377631433,-23.4306016418707,-23.3707581422136,
-23.3136203700441,-23.2545337284766,-23.2014899391179),.UNSPECIFIED.);
#24762=B_SPLINE_CURVE_WITH_KNOTS('',3,(#374385,#374386,#374387,#374388,
#374389,#374390,#374391,#374392,#374393,#374394,#374395,#374396,#374397,
#374398,#374399,#374400,#374401,#374402,#374403,#374404,#374405,#374406,
#374407,#374408,#374409,#374410,#374411,#374412,#374413,#374414,#374415,
#374416,#374417,#374418,#374419,#374420),.UNSPECIFIED.,.F.,.F.,(4,2,2,2,
2,2,2,2,2,2,2,2,2,2,2,2,2,4),(-3.76793502765558,-3.71882412297623,-3.65959561825608,
-3.60244671733181,-3.54260890239311,-3.48402902622074,-3.4264946173028,
-3.36629850670476,-3.30839113203855,-3.24935722391666,-3.18992604999305,
-3.1326674133047,-3.07280339483725,-3.01401842998219,-2.95663666569317,
-2.89621652056965,-2.83810698830649,-2.81929352507592),.UNSPECIFIED.);
#24763=B_SPLINE_CURVE_WITH_KNOTS('',3,(#374425,#374426,#374427,#374428,
#374429,#374430,#374431,#374432,#374433,#374434,#374435,#374436,#374437,
#374438,#374439,#374440,#374441,#374442,#374443,#374444,#374445,#374446,
#374447,#374448,#374449,#374450,#374451,#374452,#374453,#374454,#374455,
#374456,#374457,#374458,#374459,#374460),.UNSPECIFIED.,.F.,.F.,(4,2,2,2,
2,2,2,2,2,2,2,2,2,2,2,2,2,4),(-25.0988774139147,-25.0748748133069,-25.0166042193354,
-24.9567402234876,-24.8995341312701,-24.8406104828899,-24.7807642560441,
-24.723298521872,-24.6635959223151,-24.6050291412632,-24.546881843457,-24.4864202492779,
-24.4290481820111,-24.3702247779384,-24.3103492878962,-24.253060753562,
-24.193591509621,-24.1499027888804),.UNSPECIFIED.);
#24764=B_SPLINE_CURVE_WITH_KNOTS('',3,(#374461,#374462,#374463,#374464,
#374465,#374466,#374467,#374468,#374469,#374470,#374471,#374472,#374473,
#374474,#374475,#374476,#374477,#374478,#374479,#374480,#374481,#374482,
#374483,#374484,#374485,#374486,#374487,#374488,#374489,#374490,#374491,
#374492,#374493,#374494,#374495,#374496),.UNSPECIFIED.,.F.,.F.,(4,2,2,2,
2,2,2,2,2,2,2,2,2,2,2,2,2,4),(-2.81929352507592,-2.77949126923264,-2.71983044208255,
-2.66240353815619,-2.60257729967794,-2.54369522708906,-2.48649445360784,
-2.42664858989673,-2.36841971353789,-2.31029402853068,-2.25049001822912,
-2.19293604132315,-2.13274226536931,-2.07373326798044,-2.0166205280456,
-1.9568085453459,-1.8984502829867,-1.87105276048628),.UNSPECIFIED.);
#24765=B_SPLINE_CURVE_WITH_KNOTS('',3,(#374501,#374502,#374503,#374504,
#374505,#374506,#374507,#374508,#374509,#374510,#374511,#374512,#374513,
#374514,#374515,#374516,#374517,#374518,#374519,#374520,#374521,#374522,
#374523,#374524,#374525,#374526,#374527,#374528,#374529,#374530,#374531,
#374532,#374533,#374534,#374535,#374536),.UNSPECIFIED.,.F.,.F.,(4,2,2,2,
2,2,2,2,2,2,2,2,2,2,2,2,2,4),(-26.0471246382356,-26.014786013898,-25.9562063699669,
-25.8963745576448,-25.8392297972985,-25.780001663451,-25.7204714222612,
-25.6627371816127,-25.6027332862293,-25.5449651735138,-25.4865589174191,
-25.4267247255602,-25.3695942187353,-25.3105372981954,-25.2504143722874,
-25.1928183063652,-25.132969022655,-25.0988774139147),.UNSPECIFIED.);
#24766=B_SPLINE_CURVE_WITH_KNOTS('',3,(#374537,#374538,#374539,#374540,
#374541,#374542,#374543,#374544,#374545,#374546,#374547,#374548,#374549,
#374550,#374551,#374552,#374553,#374554,#374555,#374556,#374557,#374558,
#374559,#374560,#374561,#374562,#374563,#374564,#374565,#374566,#374567,
#374568,#374569,#374570,#374571,#374572),.UNSPECIFIED.,.F.,.F.,(4,2,2,2,
2,2,2,2,2,2,2,2,2,2,2,2,2,4),(-1.87105276048628,-1.84066057871695,-1.78070828476016,
-1.72302194556017,-1.66342921249075,-1.60425458530026,-1.54714230655092,
-1.4873370572563,-1.42881098805722,-1.3712811519465,-1.31114203082431,-1.25328791183393,
-1.19422612501562,-1.13485262074985,-1.07764287772901,-1.01781519741776,
-0.959087889976359,-0.923094486905693),.UNSPECIFIED.);
#24767=B_SPLINE_CURVE_WITH_KNOTS('',3,(#374577,#374578,#374579,#374580,
#374581,#374582,#374583,#374584,#374585,#374586,#374587,#374588,#374589,
#374590),.UNSPECIFIED.,.F.,.F.,(4,2,2,2,2,2,4),(-0.0885266411023889,-0.0801647036685068,
-0.0712344835087916,-0.0543173269975797,-0.031179370811489,-0.0186636990760277,
-9.9995278037468E-7),.UNSPECIFIED.);
#24768=B_SPLINE_CURVE_WITH_KNOTS('',3,(#374593,#374594,#374595,#374596,
#374597,#374598,#374599,#374600,#374601,#374602),.UNSPECIFIED.,.F.,.F.,
(4,2,2,2,4),(0.,0.0261902001057277,0.0515478142334988,0.0956791429839492,
0.112627808033314),.UNSPECIFIED.);
#24769=B_SPLINE_CURVE_WITH_KNOTS('',3,(#374607,#374608,#374609,#374610,
#374611,#374612,#374613,#374614,#374615,#374616,#374617,#374618,#374619,
#374620,#374621,#374622,#374623,#374624,#374625,#374626,#374627,#374628,
#374629,#374630,#374631,#374632,#374633,#374634),.UNSPECIFIED.,.F.,.F.,
(4,2,2,2,2,2,2,2,2,2,2,2,2,4),(-0.8274758898732,-0.742569538402508,-0.675901844511659,
-0.62317760234926,-0.574257833858176,-0.509286803493012,-0.421718441648047,
-0.331990489069755,-0.251855537588908,-0.165988637839021,-0.104830893630237,
-0.0601605470835078,-0.0309643052748887,0.),.UNSPECIFIED.);
#24770=B_SPLINE_CURVE_WITH_KNOTS('',3,(#374639,#374640,#374641,#374642,
#374643,#374644,#374645,#374646,#374647,#374648,#374649,#374650,#374651,
#374652),.UNSPECIFIED.,.F.,.F.,(4,2,2,2,2,2,4),(1.00000009773572E-6,0.0321609114607883,
0.0622225044979538,0.116840717683487,0.162125154778588,0.187837242944783,
0.212522064408195),.UNSPECIFIED.);
#24771=B_SPLINE_CURVE_WITH_KNOTS('',3,(#374655,#374656,#374657,#374658,
#374659,#374660,#374661,#374662,#374663,#374664,#374665,#374666,#374667,
#374668),.UNSPECIFIED.,.F.,.F.,(4,2,2,2,2,2,4),(-1.28815859321983,-1.20510585719494,
-1.12916275151302,-1.02246205795895,-0.923777683161166,-0.830690938202541,
-0.8274758898732),.UNSPECIFIED.);
#24772=B_SPLINE_CURVE_WITH_KNOTS('',3,(#374670,#374671,#374672,#374673,
#374674,#374675,#374676,#374677,#374678,#374679,#374680,#374681,#374682,
#374683,#374684,#374685,#374686,#374687,#374688,#374689,#374690,#374691,
#374692,#374693,#374694,#374695,#374696,#374697,#374698,#374699,#374700,
#374701),.UNSPECIFIED.,.F.,.F.,(4,2,2,2,2,2,2,2,2,2,2,2,2,2,2,4),(0.112627808033314,
0.149387855061838,0.209041889520592,0.264760139455438,0.319335059686991,
0.366312336217241,0.415214237389767,0.462499478525696,0.513472152163099,
0.578307516406786,0.666355563097664,0.758679715521255,0.848684132039911,
0.941858489596729,1.01877466686786,1.0988436208123),.UNSPECIFIED.);
#24773=B_SPLINE_CURVE_WITH_KNOTS('',3,(#374703,#374704,#374705,#374706,
#374707,#374708,#374709,#374710,#374711,#374712,#374713,#374714,#374715,
#374716,#374717,#374718,#374719,#374720,#374721,#374722,#374723,#374724,
#374725,#374726,#374727,#374728,#374729,#374730,#374731,#374732,#374733,
#374734,#374735,#374736,#374737,#374738),.UNSPECIFIED.,.F.,.F.,(4,2,2,2,
2,2,2,2,2,2,2,2,2,2,2,2,2,4),(-0.923094486905693,-0.901723063681326,-0.841363823302868,
-0.783311185390732,-0.724681122997764,-0.665081196534761,-0.607711810661505,
-0.547928834753099,-0.489107229536437,-0.431935698290824,-0.372131671145491,
-0.313963092952632,-0.255837015396937,-0.196096950836227,-0.138603322235919,
-0.078377809682703,-0.0389284678633673,-1.00000011094004E-6),
 .UNSPECIFIED.);
#24774=B_SPLINE_CURVE_WITH_KNOTS('',3,(#374739,#374740,#374741,#374742,
#374743,#374744,#374745,#374746,#374747,#374748,#374749,#374750,#374751,
#374752,#374753,#374754,#374755,#374756,#374757,#374758,#374759,#374760,
#374761,#374762,#374763,#374764,#374765,#374766,#374767,#374768,#374769,
#374770),.UNSPECIFIED.,.F.,.F.,(4,2,2,2,2,2,2,2,2,2,2,2,2,2,2,4),(-26.8550566050564,
-26.8176636569728,-26.7789214528464,-26.7192594122446,-26.6606613243223,
-26.6025512227894,-26.5421300349857,-26.4847575911641,-26.4259720044066,
-26.3661130930589,-26.3088555463882,-26.249423905818,-26.1904112321546,
-26.1325041472705,-26.072307916167,-26.0471246382356),.UNSPECIFIED.);
#24775=B_SPLINE_CURVE_WITH_KNOTS('',3,(#374816,#374817,#374818,#374819,
#374820,#374821,#374822),.UNSPECIFIED.,.F.,.F.,(4,3,4),(9.48676900924816E-20,
2.5000002149412E-5,9.54746331310774E-5),.UNSPECIFIED.);
#24776=B_SPLINE_CURVE_WITH_KNOTS('',3,(#374826,#374827,#374828,#374829,
#374830,#374831,#374832),.UNSPECIFIED.,.F.,.F.,(4,3,4),(0.,2.50000024491141E-5,
9.54746329568079E-5),.UNSPECIFIED.);
#24777=B_SPLINE_CURVE_WITH_KNOTS('',3,(#374836,#374837,#374838,#374839,
#374840,#374841,#374842),.UNSPECIFIED.,.F.,.F.,(4,3,4),(8.13151629364128E-20,
2.50000021494121E-5,9.54746331310775E-5),.UNSPECIFIED.);
#24778=B_SPLINE_CURVE_WITH_KNOTS('',3,(#374846,#374847,#374848,#374849,
#374850,#374851,#374852),.UNSPECIFIED.,.F.,.F.,(4,3,4),(0.,2.50000024491136E-5,
9.54746329568078E-5),.UNSPECIFIED.);
#24779=B_SPLINE_CURVE_WITH_KNOTS('',3,(#374856,#374857,#374858,#374859,
#374860,#374861,#374862),.UNSPECIFIED.,.F.,.F.,(4,3,4),(5.42101086242752E-20,
2.50000021494117E-5,9.5474633131077E-5),.UNSPECIFIED.);
#24780=B_SPLINE_CURVE_WITH_KNOTS('',3,(#374866,#374867,#374868,#374869,
#374870,#374871,#374872),.UNSPECIFIED.,.F.,.F.,(4,3,4),(0.,2.50000024491138E-5,
9.54746329568077E-5),.UNSPECIFIED.);
#24781=B_SPLINE_CURVE_WITH_KNOTS('',3,(#374876,#374877,#374878,#374879,
#374880,#374881,#374882),.UNSPECIFIED.,.F.,.F.,(4,3,4),(1.0842021724855E-19,
2.50000021494118E-5,9.54746331310773E-5),.UNSPECIFIED.);
#24782=B_SPLINE_CURVE_WITH_KNOTS('',3,(#374886,#374887,#374888,#374889,
#374890,#374891,#374892),.UNSPECIFIED.,.F.,.F.,(4,3,4),(0.,2.50000024491138E-5,
9.54746329568075E-5),.UNSPECIFIED.);
#24783=B_SPLINE_CURVE_WITH_KNOTS('',3,(#374896,#374897,#374898,#374899,
#374900,#374901,#374902),.UNSPECIFIED.,.F.,.F.,(4,3,4),(4.33680868994202E-19,
2.50000021494122E-5,9.54746331310774E-5),.UNSPECIFIED.);
#24784=B_SPLINE_CURVE_WITH_KNOTS('',3,(#374906,#374907,#374908,#374909,
#374910,#374911,#374912),.UNSPECIFIED.,.F.,.F.,(4,3,4),(0.,2.5000002449114E-5,
9.54746329568081E-5),.UNSPECIFIED.);
#24785=B_SPLINE_CURVE_WITH_KNOTS('',3,(#374916,#374917,#374918,#374919,
#374920,#374921,#374922),.UNSPECIFIED.,.F.,.F.,(4,3,4),(4.33680868994202E-19,
2.5000002149412E-5,9.54746331310775E-5),.UNSPECIFIED.);
#24786=B_SPLINE_CURVE_WITH_KNOTS('',3,(#374926,#374927,#374928,#374929,
#374930,#374931,#374932),.UNSPECIFIED.,.F.,.F.,(4,3,4),(0.,2.50000024491139E-5,
9.54746329568077E-5),.UNSPECIFIED.);
#24787=B_SPLINE_CURVE_WITH_KNOTS('',3,(#374936,#374937,#374938,#374939,
#374940,#374941,#374942),.UNSPECIFIED.,.F.,.F.,(4,3,4),(4.33680868994202E-19,
2.50000021494119E-5,9.54746331310775E-5),.UNSPECIFIED.);
#24788=B_SPLINE_CURVE_WITH_KNOTS('',3,(#374946,#374947,#374948,#374949,
#374950,#374951,#374952),.UNSPECIFIED.,.F.,.F.,(4,3,4),(0.,2.50000024491138E-5,
9.5474632956808E-5),.UNSPECIFIED.);
#24789=B_SPLINE_CURVE_WITH_KNOTS('',3,(#374956,#374957,#374958,#374959,
#374960,#374961,#374962),.UNSPECIFIED.,.F.,.F.,(4,3,4),(4.33680868994202E-19,
2.5000002149412E-5,9.54746331310776E-5),.UNSPECIFIED.);
#24790=B_SPLINE_CURVE_WITH_KNOTS('',3,(#374966,#374967,#374968,#374969,
#374970,#374971,#374972),.UNSPECIFIED.,.F.,.F.,(4,3,4),(0.,2.5000002449114E-5,
9.54746329568075E-5),.UNSPECIFIED.);
#24791=B_SPLINE_CURVE_WITH_KNOTS('',3,(#374976,#374977,#374978,#374979,
#374980,#374981,#374982),.UNSPECIFIED.,.F.,.F.,(4,3,4),(4.33680868994202E-19,
2.50000021494117E-5,9.54746331310776E-5),.UNSPECIFIED.);
#24792=B_SPLINE_CURVE_WITH_KNOTS('',3,(#374986,#374987,#374988,#374989,
#374990,#374991,#374992),.UNSPECIFIED.,.F.,.F.,(4,3,4),(0.,2.50000024491139E-5,
9.54746329568078E-5),.UNSPECIFIED.);
#24793=B_SPLINE_CURVE_WITH_KNOTS('',3,(#374996,#374997,#374998,#374999,
#375000,#375001,#375002),.UNSPECIFIED.,.F.,.F.,(4,3,4),(4.33680868994202E-19,
2.50000021494117E-5,9.54746331310774E-5),.UNSPECIFIED.);
#24794=B_SPLINE_CURVE_WITH_KNOTS('',3,(#375006,#375007,#375008,#375009,
#375010,#375011,#375012),.UNSPECIFIED.,.F.,.F.,(4,3,4),(0.,2.50000024491137E-5,
9.54746329568078E-5),.UNSPECIFIED.);
#24795=B_SPLINE_CURVE_WITH_KNOTS('',3,(#375016,#375017,#375018,#375019,
#375020,#375021,#375022),.UNSPECIFIED.,.F.,.F.,(4,3,4),(4.33680868994202E-19,
2.50000021494118E-5,9.54746331310774E-5),.UNSPECIFIED.);
#24796=B_SPLINE_CURVE_WITH_KNOTS('',3,(#375026,#375027,#375028,#375029,
#375030,#375031,#375032),.UNSPECIFIED.,.F.,.F.,(4,3,4),(0.,2.50000024491138E-5,
9.54746329568079E-5),.UNSPECIFIED.);
#24797=B_SPLINE_CURVE_WITH_KNOTS('',3,(#375036,#375037,#375038,#375039,
#375040,#375041,#375042),.UNSPECIFIED.,.F.,.F.,(4,3,4),(4.33680868994202E-19,
2.50000021494117E-5,9.54746331310776E-5),.UNSPECIFIED.);
#24798=B_SPLINE_CURVE_WITH_KNOTS('',3,(#375046,#375047,#375048,#375049,
#375050,#375051,#375052),.UNSPECIFIED.,.F.,.F.,(4,3,4),(0.,2.50000024491139E-5,
9.54746329568078E-5),.UNSPECIFIED.);
#24799=B_SPLINE_CURVE_WITH_KNOTS('',3,(#375056,#375057,#375058,#375059,
#375060,#375061,#375062),.UNSPECIFIED.,.F.,.F.,(4,3,4),(2.16840434497101E-19,
2.50000021494119E-5,9.54746331310775E-5),.UNSPECIFIED.);
#24800=B_SPLINE_CURVE_WITH_KNOTS('',3,(#375066,#375067,#375068,#375069,
#375070,#375071,#375072),.UNSPECIFIED.,.F.,.F.,(4,3,4),(0.,2.5000002449114E-5,
9.54746329568076E-5),.UNSPECIFIED.);
#24801=B_SPLINE_CURVE_WITH_KNOTS('',3,(#375076,#375077,#375078,#375079,
#375080,#375081,#375082),.UNSPECIFIED.,.F.,.F.,(4,3,4),(2.16840434497101E-19,
2.50000021494119E-5,9.54746331310775E-5),.UNSPECIFIED.);
#24802=B_SPLINE_CURVE_WITH_KNOTS('',3,(#375086,#375087,#375088,#375089,
#375090,#375091,#375092),.UNSPECIFIED.,.F.,.F.,(4,3,4),(0.,2.50000024491139E-5,
9.54746329568076E-5),.UNSPECIFIED.);
#24803=B_SPLINE_CURVE_WITH_KNOTS('',3,(#375096,#375097,#375098,#375099,
#375100,#375101,#375102),.UNSPECIFIED.,.F.,.F.,(4,3,4),(0.,2.5000002149412E-5,
9.54746331310776E-5),.UNSPECIFIED.);
#24804=B_SPLINE_CURVE_WITH_KNOTS('',3,(#375106,#375107,#375108,#375109,
#375110,#375111,#375112),.UNSPECIFIED.,.F.,.F.,(4,3,4),(0.,2.5000002449114E-5,
9.54746329568076E-5),.UNSPECIFIED.);
#24805=B_SPLINE_CURVE_WITH_KNOTS('',3,(#375116,#375117,#375118,#375119,
#375120,#375121,#375122),.UNSPECIFIED.,.F.,.F.,(4,3,4),(0.,2.50000021494119E-5,
9.54746331310776E-5),.UNSPECIFIED.);
#24806=B_SPLINE_CURVE_WITH_KNOTS('',3,(#375126,#375127,#375128,#375129,
#375130,#375131,#375132),.UNSPECIFIED.,.F.,.F.,(4,3,4),(0.,2.50000024491138E-5,
9.54746329568075E-5),.UNSPECIFIED.);
#24807=B_SPLINE_CURVE_WITH_KNOTS('',3,(#375136,#375137,#375138,#375139,
#375140,#375141,#375142),.UNSPECIFIED.,.F.,.F.,(4,3,4),(2.16840434497101E-19,
2.50000021494118E-5,9.54746331310777E-5),.UNSPECIFIED.);
#24808=B_SPLINE_CURVE_WITH_KNOTS('',3,(#375146,#375147,#375148,#375149,
#375150,#375151,#375152),.UNSPECIFIED.,.F.,.F.,(4,3,4),(0.,2.50000024491137E-5,
9.54746329568079E-5),.UNSPECIFIED.);
#24809=B_SPLINE_CURVE_WITH_KNOTS('',3,(#375156,#375157,#375158,#375159,
#375160,#375161,#375162),.UNSPECIFIED.,.F.,.F.,(4,3,4),(2.16840434497101E-19,
2.5000002149412E-5,9.54746331310779E-5),.UNSPECIFIED.);
#24810=B_SPLINE_CURVE_WITH_KNOTS('',3,(#375166,#375167,#375168,#375169,
#375170,#375171,#375172),.UNSPECIFIED.,.F.,.F.,(4,3,4),(0.,2.50000024491141E-5,
9.5474632956808E-5),.UNSPECIFIED.);
#24811=B_SPLINE_CURVE_WITH_KNOTS('',3,(#375176,#375177,#375178,#375179,
#375180,#375181,#375182),.UNSPECIFIED.,.F.,.F.,(4,3,4),(2.16840434497101E-19,
2.50000021494116E-5,9.54746331310775E-5),.UNSPECIFIED.);
#24812=B_SPLINE_CURVE_WITH_KNOTS('',3,(#375186,#375187,#375188,#375189,
#375190,#375191,#375192),.UNSPECIFIED.,.F.,.F.,(4,3,4),(0.,2.50000024491134E-5,
9.54746329568073E-5),.UNSPECIFIED.);
#24813=B_SPLINE_CURVE_WITH_KNOTS('',3,(#375196,#375197,#375198,#375199,
#375200,#375201,#375202),.UNSPECIFIED.,.F.,.F.,(4,3,4),(2.16840434497101E-19,
2.50000021494119E-5,9.54746331310774E-5),.UNSPECIFIED.);
#24814=B_SPLINE_CURVE_WITH_KNOTS('',3,(#375206,#375207,#375208,#375209,
#375210,#375211,#375212),.UNSPECIFIED.,.F.,.F.,(4,3,4),(0.,2.5000002449114E-5,
9.54746329568077E-5),.UNSPECIFIED.);
#24815=B_SPLINE_CURVE_WITH_KNOTS('',3,(#375216,#375217,#375218,#375219,
#375220,#375221,#375222),.UNSPECIFIED.,.F.,.F.,(4,3,4),(1.0842021724855E-19,
2.5000002149412E-5,9.54746331310776E-5),.UNSPECIFIED.);
#24816=B_SPLINE_CURVE_WITH_KNOTS('',3,(#375226,#375227,#375228,#375229,
#375230,#375231,#375232),.UNSPECIFIED.,.F.,.F.,(4,3,4),(0.,2.50000024491137E-5,
9.54746329568074E-5),.UNSPECIFIED.);
#24817=B_SPLINE_CURVE_WITH_KNOTS('',3,(#375236,#375237,#375238,#375239,
#375240,#375241,#375242),.UNSPECIFIED.,.F.,.F.,(4,3,4),(1.0842021724855E-19,
2.50000021494121E-5,9.54746331310777E-5),.UNSPECIFIED.);
#24818=B_SPLINE_CURVE_WITH_KNOTS('',3,(#375246,#375247,#375248,#375249,
#375250,#375251,#375252),.UNSPECIFIED.,.F.,.F.,(4,3,4),(0.,2.50000024491138E-5,
9.54746329568079E-5),.UNSPECIFIED.);
#24819=B_SPLINE_CURVE_WITH_KNOTS('',3,(#375256,#375257,#375258,#375259,
#375260,#375261,#375262),.UNSPECIFIED.,.F.,.F.,(4,3,4),(1.0842021724855E-19,
2.50000021494117E-5,9.54746331310775E-5),.UNSPECIFIED.);
#24820=B_SPLINE_CURVE_WITH_KNOTS('',3,(#375266,#375267,#375268,#375269,
#375270,#375271,#375272),.UNSPECIFIED.,.F.,.F.,(4,3,4),(0.,2.50000024491141E-5,
9.54746329568077E-5),.UNSPECIFIED.);
#24821=B_SPLINE_CURVE_WITH_KNOTS('',3,(#375276,#375277,#375278,#375279,
#375280,#375281,#375282),.UNSPECIFIED.,.F.,.F.,(4,3,4),(1.0842021724855E-19,
2.5000002149412E-5,9.54746331310775E-5),.UNSPECIFIED.);
#24822=B_SPLINE_CURVE_WITH_KNOTS('',3,(#375286,#375287,#375288,#375289,
#375290,#375291,#375292),.UNSPECIFIED.,.F.,.F.,(4,3,4),(0.,2.50000024491137E-5,
9.54746329568075E-5),.UNSPECIFIED.);
#24823=B_SPLINE_CURVE_WITH_KNOTS('',3,(#375296,#375297,#375298,#375299,
#375300,#375301,#375302),.UNSPECIFIED.,.F.,.F.,(4,3,4),(1.01643953670516E-19,
2.50000021494119E-5,9.54746331310775E-5),.UNSPECIFIED.);
#24824=B_SPLINE_CURVE_WITH_KNOTS('',3,(#375306,#375307,#375308,#375309,
#375310,#375311,#375312),.UNSPECIFIED.,.F.,.F.,(4,3,4),(0.,2.50000024491139E-5,
9.54746329568077E-5),.UNSPECIFIED.);
#24825=B_SPLINE_CURVE_WITH_KNOTS('',3,(#375316,#375317,#375318,#375319,
#375320,#375321,#375322),.UNSPECIFIED.,.F.,.F.,(4,3,4),(8.13151629364128E-20,
2.50000021494123E-5,9.54746331310776E-5),.UNSPECIFIED.);
#24826=B_SPLINE_CURVE_WITH_KNOTS('',3,(#375326,#375327,#375328,#375329,
#375330,#375331,#375332),.UNSPECIFIED.,.F.,.F.,(4,3,4),(0.,2.50000024491137E-5,
9.54746329568075E-5),.UNSPECIFIED.);
#24827=B_SPLINE_CURVE_WITH_KNOTS('',3,(#375336,#375337,#375338,#375339,
#375340,#375341,#375342),.UNSPECIFIED.,.F.,.F.,(4,3,4),(5.42101086242752E-20,
2.50000021494119E-5,9.54746331310775E-5),.UNSPECIFIED.);
#24828=B_SPLINE_CURVE_WITH_KNOTS('',3,(#375346,#375347,#375348,#375349,
#375350,#375351,#375352),.UNSPECIFIED.,.F.,.F.,(4,3,4),(0.,2.50000024491138E-5,
9.54746329568073E-5),.UNSPECIFIED.);
#24829=B_SPLINE_CURVE_WITH_KNOTS('',3,(#375356,#375357,#375358,#375359,
#375360,#375361,#375362),.UNSPECIFIED.,.F.,.F.,(4,3,4),(5.42101086242752E-20,
2.5000002149412E-5,9.54746331310778E-5),.UNSPECIFIED.);
#24830=B_SPLINE_CURVE_WITH_KNOTS('',3,(#375366,#375367,#375368,#375369,
#375370,#375371,#375372),.UNSPECIFIED.,.F.,.F.,(4,3,4),(0.,2.50000024491139E-5,
9.54746329568078E-5),.UNSPECIFIED.);
#24831=B_SPLINE_CURVE_WITH_KNOTS('',3,(#375376,#375377,#375378,#375379,
#375380,#375381,#375382),.UNSPECIFIED.,.F.,.F.,(4,3,4),(0.,2.50000021494121E-5,
9.54746331310777E-5),.UNSPECIFIED.);
#24832=B_SPLINE_CURVE_WITH_KNOTS('',3,(#375386,#375387,#375388,#375389,
#375390,#375391,#375392),.UNSPECIFIED.,.F.,.F.,(4,3,4),(0.,2.50000024491139E-5,
9.54746329568077E-5),.UNSPECIFIED.);
#24833=B_SPLINE_CURVE_WITH_KNOTS('',3,(#375396,#375397,#375398,#375399,
#375400,#375401,#375402),.UNSPECIFIED.,.F.,.F.,(4,3,4),(4.33680868994202E-19,
2.50000021494121E-5,9.54746331310774E-5),.UNSPECIFIED.);
#24834=B_SPLINE_CURVE_WITH_KNOTS('',3,(#375406,#375407,#375408,#375409,
#375410,#375411,#375412),.UNSPECIFIED.,.F.,.F.,(4,3,4),(0.,2.50000024491139E-5,
9.54746329568078E-5),.UNSPECIFIED.);
#24835=B_SPLINE_CURVE_WITH_KNOTS('',3,(#375416,#375417,#375418,#375419,
#375420,#375421,#375422),.UNSPECIFIED.,.F.,.F.,(4,3,4),(4.33680868994202E-19,
2.50000021494119E-5,9.54746331310773E-5),.UNSPECIFIED.);
#24836=B_SPLINE_CURVE_WITH_KNOTS('',3,(#375426,#375427,#375428,#375429,
#375430,#375431,#375432),.UNSPECIFIED.,.F.,.F.,(4,3,4),(0.,2.50000024491138E-5,
9.54746329568077E-5),.UNSPECIFIED.);
#24837=B_SPLINE_CURVE_WITH_KNOTS('',3,(#375436,#375437,#375438,#375439,
#375440,#375441,#375442),.UNSPECIFIED.,.F.,.F.,(4,3,4),(4.33680868994202E-19,
2.5000002149412E-5,9.54746331310777E-5),.UNSPECIFIED.);
#24838=B_SPLINE_CURVE_WITH_KNOTS('',3,(#375446,#375447,#375448,#375449,
#375450,#375451,#375452),.UNSPECIFIED.,.F.,.F.,(4,3,4),(0.,2.5000002449114E-5,
9.54746329568079E-5),.UNSPECIFIED.);
#24839=B_SPLINE_CURVE_WITH_KNOTS('',3,(#375456,#375457,#375458,#375459,
#375460,#375461,#375462),.UNSPECIFIED.,.F.,.F.,(4,3,4),(4.33680868994202E-19,
2.50000021494121E-5,9.54746331310776E-5),.UNSPECIFIED.);
#24840=B_SPLINE_CURVE_WITH_KNOTS('',3,(#375466,#375467,#375468,#375469,
#375470,#375471,#375472),.UNSPECIFIED.,.F.,.F.,(4,3,4),(0.,2.50000024491138E-5,
9.5474632956808E-5),.UNSPECIFIED.);
#24841=B_SPLINE_CURVE_WITH_KNOTS('',3,(#375476,#375477,#375478,#375479,
#375480,#375481,#375482),.UNSPECIFIED.,.F.,.F.,(4,3,4),(4.33680868994202E-19,
2.50000021494121E-5,9.54746331310774E-5),.UNSPECIFIED.);
#24842=B_SPLINE_CURVE_WITH_KNOTS('',3,(#375486,#375487,#375488,#375489,
#375490,#375491,#375492),.UNSPECIFIED.,.F.,.F.,(4,3,4),(0.,2.50000024491138E-5,
9.54746329568077E-5),.UNSPECIFIED.);
#24843=B_SPLINE_CURVE_WITH_KNOTS('',3,(#375496,#375497,#375498,#375499,
#375500,#375501,#375502),.UNSPECIFIED.,.F.,.F.,(4,3,4),(4.33680868994202E-19,
2.50000021494118E-5,9.54746331310775E-5),.UNSPECIFIED.);
#24844=B_SPLINE_CURVE_WITH_KNOTS('',3,(#375506,#375507,#375508,#375509,
#375510,#375511,#375512),.UNSPECIFIED.,.F.,.F.,(4,3,4),(0.,2.50000024491139E-5,
9.54746329568079E-5),.UNSPECIFIED.);
#24845=B_SPLINE_CURVE_WITH_KNOTS('',3,(#375516,#375517,#375518,#375519,
#375520,#375521,#375522),.UNSPECIFIED.,.F.,.F.,(4,3,4),(4.33680868994202E-19,
2.50000021494117E-5,9.54746331310775E-5),.UNSPECIFIED.);
#24846=B_SPLINE_CURVE_WITH_KNOTS('',3,(#375526,#375527,#375528,#375529,
#375530,#375531,#375532),.UNSPECIFIED.,.F.,.F.,(4,3,4),(0.,2.50000024491138E-5,
9.54746329568079E-5),.UNSPECIFIED.);
#24847=B_SPLINE_CURVE_WITH_KNOTS('',3,(#375536,#375537,#375538,#375539,
#375540,#375541,#375542),.UNSPECIFIED.,.F.,.F.,(4,3,4),(4.33680868994202E-19,
2.50000021494119E-5,9.54746331310774E-5),.UNSPECIFIED.);
#24848=B_SPLINE_CURVE_WITH_KNOTS('',3,(#375546,#375547,#375548,#375549,
#375550,#375551,#375552),.UNSPECIFIED.,.F.,.F.,(4,3,4),(0.,2.50000024491139E-5,
9.54746329568077E-5),.UNSPECIFIED.);
#24849=B_SPLINE_CURVE_WITH_KNOTS('',3,(#375556,#375557,#375558,#375559,
#375560,#375561,#375562),.UNSPECIFIED.,.F.,.F.,(4,3,4),(2.16840434497101E-19,
2.50000021494119E-5,9.54746331310775E-5),.UNSPECIFIED.);
#24850=B_SPLINE_CURVE_WITH_KNOTS('',3,(#375566,#375567,#375568,#375569,
#375570,#375571,#375572),.UNSPECIFIED.,.F.,.F.,(4,3,4),(0.,2.50000024491139E-5,
9.5474632956808E-5),.UNSPECIFIED.);
#24851=B_SPLINE_CURVE_WITH_KNOTS('',3,(#375576,#375577,#375578,#375579,
#375580,#375581,#375582),.UNSPECIFIED.,.F.,.F.,(4,3,4),(2.16840434497101E-19,
2.5000002149412E-5,9.54746331310775E-5),.UNSPECIFIED.);
#24852=B_SPLINE_CURVE_WITH_KNOTS('',3,(#375586,#375587,#375588,#375589,
#375590,#375591,#375592),.UNSPECIFIED.,.F.,.F.,(4,3,4),(0.,2.50000024491142E-5,
9.54746329568079E-5),.UNSPECIFIED.);
#24853=B_SPLINE_CURVE_WITH_KNOTS('',3,(#375596,#375597,#375598,#375599,
#375600,#375601,#375602),.UNSPECIFIED.,.F.,.F.,(4,3,4),(2.16840434497101E-19,
2.5000002149412E-5,9.54746331310776E-5),.UNSPECIFIED.);
#24854=B_SPLINE_CURVE_WITH_KNOTS('',3,(#375606,#375607,#375608,#375609,
#375610,#375611,#375612),.UNSPECIFIED.,.F.,.F.,(4,3,4),(0.,2.50000024491136E-5,
9.54746329568075E-5),.UNSPECIFIED.);
#24855=B_SPLINE_CURVE_WITH_KNOTS('',3,(#375616,#375617,#375618,#375619,
#375620,#375621,#375622),.UNSPECIFIED.,.F.,.F.,(4,3,4),(2.16840434497101E-19,
2.50000021494117E-5,9.54746331310776E-5),.UNSPECIFIED.);
#24856=B_SPLINE_CURVE_WITH_KNOTS('',3,(#375626,#375627,#375628,#375629,
#375630,#375631,#375632),.UNSPECIFIED.,.F.,.F.,(4,3,4),(0.,2.50000024491138E-5,
9.54746329568075E-5),.UNSPECIFIED.);
#24857=B_SPLINE_CURVE_WITH_KNOTS('',3,(#375636,#375637,#375638,#375639,
#375640,#375641,#375642),.UNSPECIFIED.,.F.,.F.,(4,3,4),(2.16840434497101E-19,
2.50000021494118E-5,9.54746331310776E-5),.UNSPECIFIED.);
#24858=B_SPLINE_CURVE_WITH_KNOTS('',3,(#375646,#375647,#375648,#375649,
#375650,#375651,#375652),.UNSPECIFIED.,.F.,.F.,(4,3,4),(0.,2.50000024491139E-5,
9.54746329568075E-5),.UNSPECIFIED.);
#24859=B_SPLINE_CURVE_WITH_KNOTS('',3,(#375656,#375657,#375658,#375659,
#375660,#375661,#375662),.UNSPECIFIED.,.F.,.F.,(4,3,4),(2.16840434497101E-19,
2.5000002149412E-5,9.54746331310774E-5),.UNSPECIFIED.);
#24860=B_SPLINE_CURVE_WITH_KNOTS('',3,(#375666,#375667,#375668,#375669,
#375670,#375671,#375672),.UNSPECIFIED.,.F.,.F.,(4,3,4),(0.,2.5000002449114E-5,
9.54746329568077E-5),.UNSPECIFIED.);
#24861=B_SPLINE_CURVE_WITH_KNOTS('',3,(#375676,#375677,#375678,#375679,
#375680,#375681,#375682),.UNSPECIFIED.,.F.,.F.,(4,3,4),(2.16840434497101E-19,
2.50000021494121E-5,9.54746331310778E-5),.UNSPECIFIED.);
#24862=B_SPLINE_CURVE_WITH_KNOTS('',3,(#375686,#375687,#375688,#375689,
#375690,#375691,#375692),.UNSPECIFIED.,.F.,.F.,(4,3,4),(0.,2.50000024491136E-5,
9.54746329568075E-5),.UNSPECIFIED.);
#24863=B_SPLINE_CURVE_WITH_KNOTS('',3,(#375696,#375697,#375698,#375699,
#375700,#375701,#375702),.UNSPECIFIED.,.F.,.F.,(4,3,4),(0.,2.5000002149412E-5,
9.54746331310776E-5),.UNSPECIFIED.);
#24864=B_SPLINE_CURVE_WITH_KNOTS('',3,(#375706,#375707,#375708,#375709,
#375710,#375711,#375712),.UNSPECIFIED.,.F.,.F.,(4,3,4),(0.,2.5000002449114E-5,
9.54746329568075E-5),.UNSPECIFIED.);
#24865=B_SPLINE_CURVE_WITH_KNOTS('',3,(#375716,#375717,#375718,#375719,
#375720,#375721,#375722),.UNSPECIFIED.,.F.,.F.,(4,3,4),(1.0842021724855E-19,
2.50000021494118E-5,9.54746331310777E-5),.UNSPECIFIED.);
#24866=B_SPLINE_CURVE_WITH_KNOTS('',3,(#375726,#375727,#375728,#375729,
#375730,#375731,#375732),.UNSPECIFIED.,.F.,.F.,(4,3,4),(0.,2.50000024491137E-5,
9.5474632956808E-5),.UNSPECIFIED.);
#24867=B_SPLINE_CURVE_WITH_KNOTS('',3,(#375736,#375737,#375738,#375739,
#375740,#375741,#375742),.UNSPECIFIED.,.F.,.F.,(4,3,4),(1.0842021724855E-19,
2.50000021494119E-5,9.54746331310774E-5),.UNSPECIFIED.);
#24868=B_SPLINE_CURVE_WITH_KNOTS('',3,(#375746,#375747,#375748,#375749,
#375750,#375751,#375752),.UNSPECIFIED.,.F.,.F.,(4,3,4),(0.,2.50000024491138E-5,
9.54746329568078E-5),.UNSPECIFIED.);
#24869=B_SPLINE_CURVE_WITH_KNOTS('',3,(#375756,#375757,#375758,#375759,
#375760,#375761,#375762),.UNSPECIFIED.,.F.,.F.,(4,3,4),(1.0842021724855E-19,
2.50000021494117E-5,9.54746331310775E-5),.UNSPECIFIED.);
#24870=B_SPLINE_CURVE_WITH_KNOTS('',3,(#375766,#375767,#375768,#375769,
#375770,#375771,#375772),.UNSPECIFIED.,.F.,.F.,(4,3,4),(0.,2.50000024491139E-5,
9.54746329568076E-5),.UNSPECIFIED.);
#24871=B_SPLINE_CURVE_WITH_KNOTS('',3,(#375776,#375777,#375778,#375779,
#375780,#375781,#375782),.UNSPECIFIED.,.F.,.F.,(4,3,4),(1.0842021724855E-19,
2.5000002149412E-5,9.54746331310773E-5),.UNSPECIFIED.);
#24872=B_SPLINE_CURVE_WITH_KNOTS('',3,(#375786,#375787,#375788,#375789,
#375790,#375791,#375792),.UNSPECIFIED.,.F.,.F.,(4,3,4),(0.,2.50000024491138E-5,
9.54746329568079E-5),.UNSPECIFIED.);
#24873=B_SPLINE_CURVE_WITH_KNOTS('',3,(#375803,#375804,#375805,#375806,
#375807,#375808,#375809),.UNSPECIFIED.,.F.,.F.,(4,3,4),(9.48676900924816E-20,
2.50000021494119E-5,9.54746331310775E-5),.UNSPECIFIED.);
#24874=B_SPLINE_CURVE_WITH_KNOTS('',3,(#375813,#375814,#375815,#375816,
#375817,#375818,#375819),.UNSPECIFIED.,.F.,.F.,(4,3,4),(0.,2.50000024491136E-5,
9.54746329568077E-5),.UNSPECIFIED.);
#24875=B_SPLINE_CURVE_WITH_KNOTS('',3,(#375823,#375824,#375825,#375826,
#375827,#375828,#375829),.UNSPECIFIED.,.F.,.F.,(4,3,4),(8.13151629364128E-20,
2.5000002149412E-5,9.54746331310776E-5),.UNSPECIFIED.);
#24876=B_SPLINE_CURVE_WITH_KNOTS('',3,(#375833,#375834,#375835,#375836,
#375837,#375838,#375839),.UNSPECIFIED.,.F.,.F.,(4,3,4),(0.,2.5000002449114E-5,
9.54746329568077E-5),.UNSPECIFIED.);
#24877=B_SPLINE_CURVE_WITH_KNOTS('',3,(#375843,#375844,#375845,#375846,
#375847,#375848,#375849),.UNSPECIFIED.,.F.,.F.,(4,3,4),(5.42101086242752E-20,
2.5000002149412E-5,9.54746331310776E-5),.UNSPECIFIED.);
#24878=B_SPLINE_CURVE_WITH_KNOTS('',3,(#375853,#375854,#375855,#375856,
#375857,#375858,#375859),.UNSPECIFIED.,.F.,.F.,(4,3,4),(0.,2.50000024491138E-5,
9.54746329568079E-5),.UNSPECIFIED.);
#24879=B_SPLINE_CURVE_WITH_KNOTS('',3,(#375863,#375864,#375865,#375866,
#375867,#375868,#375869),.UNSPECIFIED.,.F.,.F.,(4,3,4),(1.0842021724855E-19,
2.50000021494121E-5,9.54746331310775E-5),.UNSPECIFIED.);
#24880=B_SPLINE_CURVE_WITH_KNOTS('',3,(#375873,#375874,#375875,#375876,
#375877,#375878,#375879),.UNSPECIFIED.,.F.,.F.,(4,3,4),(0.,2.50000024491138E-5,
9.54746329568079E-5),.UNSPECIFIED.);
#24881=B_SPLINE_CURVE_WITH_KNOTS('',3,(#375883,#375884,#375885,#375886,
#375887,#375888,#375889),.UNSPECIFIED.,.F.,.F.,(4,3,4),(4.33680868994202E-19,
2.50000021494119E-5,9.54746331310774E-5),.UNSPECIFIED.);
#24882=B_SPLINE_CURVE_WITH_KNOTS('',3,(#375893,#375894,#375895,#375896,
#375897,#375898,#375899),.UNSPECIFIED.,.F.,.F.,(4,3,4),(0.,2.50000024491138E-5,
9.54746329568078E-5),.UNSPECIFIED.);
#24883=B_SPLINE_CURVE_WITH_KNOTS('',3,(#375903,#375904,#375905,#375906,
#375907,#375908,#375909),.UNSPECIFIED.,.F.,.F.,(4,3,4),(4.33680868994202E-19,
2.5000002149412E-5,9.54746331310775E-5),.UNSPECIFIED.);
#24884=B_SPLINE_CURVE_WITH_KNOTS('',3,(#375913,#375914,#375915,#375916,
#375917,#375918,#375919),.UNSPECIFIED.,.F.,.F.,(4,3,4),(0.,2.50000024491135E-5,
9.54746329568076E-5),.UNSPECIFIED.);
#24885=B_SPLINE_CURVE_WITH_KNOTS('',3,(#375923,#375924,#375925,#375926,
#375927,#375928,#375929),.UNSPECIFIED.,.F.,.F.,(4,3,4),(4.33680868994202E-19,
2.50000021494119E-5,9.54746331310774E-5),.UNSPECIFIED.);
#24886=B_SPLINE_CURVE_WITH_KNOTS('',3,(#375933,#375934,#375935,#375936,
#375937,#375938,#375939),.UNSPECIFIED.,.F.,.F.,(4,3,4),(0.,2.5000002449114E-5,
9.54746329568078E-5),.UNSPECIFIED.);
#24887=B_SPLINE_CURVE_WITH_KNOTS('',3,(#375943,#375944,#375945,#375946,
#375947,#375948,#375949),.UNSPECIFIED.,.F.,.F.,(4,3,4),(0.,2.5000002149412E-5,
9.54746331310773E-5),.UNSPECIFIED.);
#24888=B_SPLINE_CURVE_WITH_KNOTS('',3,(#375953,#375954,#375955,#375956,
#375957,#375958,#375959),.UNSPECIFIED.,.F.,.F.,(4,3,4),(0.,2.50000024491138E-5,
9.54746329568076E-5),.UNSPECIFIED.);
#24889=B_SPLINE_CURVE_WITH_KNOTS('',3,(#375963,#375964,#375965,#375966,
#375967,#375968,#375969),.UNSPECIFIED.,.F.,.F.,(4,3,4),(4.33680868994202E-19,
2.5000002149412E-5,9.54746331310777E-5),.UNSPECIFIED.);
#24890=B_SPLINE_CURVE_WITH_KNOTS('',3,(#375973,#375974,#375975,#375976,
#375977,#375978,#375979),.UNSPECIFIED.,.F.,.F.,(4,3,4),(0.,2.50000024491138E-5,
9.54746329568077E-5),.UNSPECIFIED.);
#24891=B_SPLINE_CURVE_WITH_KNOTS('',3,(#375983,#375984,#375985,#375986,
#375987,#375988,#375989),.UNSPECIFIED.,.F.,.F.,(4,3,4),(4.33680868994202E-19,
2.5000002149412E-5,9.54746331310777E-5),.UNSPECIFIED.);
#24892=B_SPLINE_CURVE_WITH_KNOTS('',3,(#375993,#375994,#375995,#375996,
#375997,#375998,#375999),.UNSPECIFIED.,.F.,.F.,(4,3,4),(0.,2.50000024491139E-5,
9.5474632956808E-5),.UNSPECIFIED.);
#24893=B_SPLINE_CURVE_WITH_KNOTS('',3,(#376003,#376004,#376005,#376006,
#376007,#376008,#376009),.UNSPECIFIED.,.F.,.F.,(4,3,4),(4.33680868994202E-19,
2.50000021494121E-5,9.54746331310776E-5),.UNSPECIFIED.);
#24894=B_SPLINE_CURVE_WITH_KNOTS('',3,(#376013,#376014,#376015,#376016,
#376017,#376018,#376019),.UNSPECIFIED.,.F.,.F.,(4,3,4),(0.,2.50000024491141E-5,
9.5474632956808E-5),.UNSPECIFIED.);
#24895=B_SPLINE_CURVE_WITH_KNOTS('',3,(#376023,#376024,#376025,#376026,
#376027,#376028,#376029),.UNSPECIFIED.,.F.,.F.,(4,3,4),(0.,2.50000021494123E-5,
9.54746331310777E-5),.UNSPECIFIED.);
#24896=B_SPLINE_CURVE_WITH_KNOTS('',3,(#376033,#376034,#376035,#376036,
#376037,#376038,#376039),.UNSPECIFIED.,.F.,.F.,(4,3,4),(0.,2.50000024491141E-5,
9.54746329568078E-5),.UNSPECIFIED.);
#24897=B_SPLINE_CURVE_WITH_KNOTS('',3,(#376043,#376044,#376045,#376046,
#376047,#376048,#376049),.UNSPECIFIED.,.F.,.F.,(4,3,4),(2.16840434497101E-19,
2.50000021494118E-5,9.54746331310777E-5),.UNSPECIFIED.);
#24898=B_SPLINE_CURVE_WITH_KNOTS('',3,(#376053,#376054,#376055,#376056,
#376057,#376058,#376059),.UNSPECIFIED.,.F.,.F.,(4,3,4),(0.,2.50000024491138E-5,
9.54746329568075E-5),.UNSPECIFIED.);
#24899=B_SPLINE_CURVE_WITH_KNOTS('',3,(#376063,#376064,#376065,#376066,
#376067,#376068,#376069),.UNSPECIFIED.,.F.,.F.,(4,3,4),(2.16840434497101E-19,
2.5000002149412E-5,9.54746331310779E-5),.UNSPECIFIED.);
#24900=B_SPLINE_CURVE_WITH_KNOTS('',3,(#376073,#376074,#376075,#376076,
#376077,#376078,#376079),.UNSPECIFIED.,.F.,.F.,(4,3,4),(0.,2.5000002449114E-5,
9.54746329568079E-5),.UNSPECIFIED.);
#24901=B_SPLINE_CURVE_WITH_KNOTS('',3,(#376083,#376084,#376085,#376086,
#376087,#376088,#376089),.UNSPECIFIED.,.F.,.F.,(4,3,4),(2.16840434497101E-19,
2.50000021494118E-5,9.54746331310775E-5),.UNSPECIFIED.);
#24902=B_SPLINE_CURVE_WITH_KNOTS('',3,(#376093,#376094,#376095,#376096,
#376097,#376098,#376099),.UNSPECIFIED.,.F.,.F.,(4,3,4),(0.,2.50000024491142E-5,
9.54746329568079E-5),.UNSPECIFIED.);
#24903=B_SPLINE_CURVE_WITH_KNOTS('',3,(#376103,#376104,#376105,#376106,
#376107,#376108,#376109),.UNSPECIFIED.,.F.,.F.,(4,3,4),(2.16840434497101E-19,
2.50000021494119E-5,9.54746331310776E-5),.UNSPECIFIED.);
#24904=B_SPLINE_CURVE_WITH_KNOTS('',3,(#376113,#376114,#376115,#376116,
#376117,#376118,#376119),.UNSPECIFIED.,.F.,.F.,(4,3,4),(0.,2.50000024491138E-5,
9.54746329568075E-5),.UNSPECIFIED.);
#24905=B_SPLINE_CURVE_WITH_KNOTS('',3,(#376123,#376124,#376125,#376126,
#376127,#376128,#376129),.UNSPECIFIED.,.F.,.F.,(4,3,4),(2.16840434497101E-19,
2.50000021494119E-5,9.54746331310776E-5),.UNSPECIFIED.);
#24906=B_SPLINE_CURVE_WITH_KNOTS('',3,(#376133,#376134,#376135,#376136,
#376137,#376138,#376139),.UNSPECIFIED.,.F.,.F.,(4,3,4),(0.,2.50000024491141E-5,
9.54746329568079E-5),.UNSPECIFIED.);
#24907=B_SPLINE_CURVE_WITH_KNOTS('',3,(#376143,#376144,#376145,#376146,
#376147,#376148,#376149),.UNSPECIFIED.,.F.,.F.,(4,3,4),(2.16840434497101E-19,
2.50000021494117E-5,9.54746331310775E-5),.UNSPECIFIED.);
#24908=B_SPLINE_CURVE_WITH_KNOTS('',3,(#376153,#376154,#376155,#376156,
#376157,#376158,#376159),.UNSPECIFIED.,.F.,.F.,(4,3,4),(0.,2.50000024491134E-5,
9.54746329568077E-5),.UNSPECIFIED.);
#24909=B_SPLINE_CURVE_WITH_KNOTS('',3,(#376163,#376164,#376165,#376166,
#376167,#376168,#376169),.UNSPECIFIED.,.F.,.F.,(4,3,4),(0.,2.5000002149412E-5,
9.54746331310777E-5),.UNSPECIFIED.);
#24910=B_SPLINE_CURVE_WITH_KNOTS('',3,(#376173,#376174,#376175,#376176,
#376177,#376178,#376179),.UNSPECIFIED.,.F.,.F.,(4,3,4),(0.,2.50000024491141E-5,
9.54746329568077E-5),.UNSPECIFIED.);
#24911=B_SPLINE_CURVE_WITH_KNOTS('',3,(#376183,#376184,#376185,#376186,
#376187,#376188,#376189),.UNSPECIFIED.,.F.,.F.,(4,3,4),(1.0842021724855E-19,
2.50000021494119E-5,9.54746331310777E-5),.UNSPECIFIED.);
#24912=B_SPLINE_CURVE_WITH_KNOTS('',3,(#376193,#376194,#376195,#376196,
#376197,#376198,#376199),.UNSPECIFIED.,.F.,.F.,(4,3,4),(0.,2.50000024491137E-5,
9.54746329568078E-5),.UNSPECIFIED.);
#24913=B_SPLINE_CURVE_WITH_KNOTS('',3,(#376203,#376204,#376205,#376206,
#376207,#376208,#376209),.UNSPECIFIED.,.F.,.F.,(4,3,4),(1.0842021724855E-19,
2.50000021494122E-5,9.54746331310776E-5),.UNSPECIFIED.);
#24914=B_SPLINE_CURVE_WITH_KNOTS('',3,(#376213,#376214,#376215,#376216,
#376217,#376218,#376219),.UNSPECIFIED.,.F.,.F.,(4,3,4),(0.,2.5000002449114E-5,
9.54746329568078E-5),.UNSPECIFIED.);
#24915=B_SPLINE_CURVE_WITH_KNOTS('',3,(#376223,#376224,#376225,#376226,
#376227,#376228,#376229),.UNSPECIFIED.,.F.,.F.,(4,3,4),(1.0842021724855E-19,
2.50000021494121E-5,9.54746331310776E-5),.UNSPECIFIED.);
#24916=B_SPLINE_CURVE_WITH_KNOTS('',3,(#376233,#376234,#376235,#376236,
#376237,#376238,#376239),.UNSPECIFIED.,.F.,.F.,(4,3,4),(0.,2.50000024491138E-5,
9.54746329568077E-5),.UNSPECIFIED.);
#24917=B_SPLINE_CURVE_WITH_KNOTS('',3,(#376243,#376244,#376245,#376246,
#376247,#376248,#376249),.UNSPECIFIED.,.F.,.F.,(4,3,4),(1.0842021724855E-19,
2.50000021494122E-5,9.54746331310776E-5),.UNSPECIFIED.);
#24918=B_SPLINE_CURVE_WITH_KNOTS('',3,(#376253,#376254,#376255,#376256,
#376257,#376258,#376259),.UNSPECIFIED.,.F.,.F.,(4,3,4),(0.,2.50000024491135E-5,
9.54746329568075E-5),.UNSPECIFIED.);
#24919=B_SPLINE_CURVE_WITH_KNOTS('',3,(#376263,#376264,#376265,#376266,
#376267,#376268,#376269),.UNSPECIFIED.,.F.,.F.,(4,3,4),(1.0842021724855E-19,
2.5000002149412E-5,9.54746331310773E-5),.UNSPECIFIED.);
#24920=B_SPLINE_CURVE_WITH_KNOTS('',3,(#376273,#376274,#376275,#376276,
#376277,#376278,#376279),.UNSPECIFIED.,.F.,.F.,(4,3,4),(0.,2.5000002449114E-5,
9.54746329568076E-5),.UNSPECIFIED.);
#24921=B_SPLINE_CURVE_WITH_KNOTS('',3,(#376283,#376284,#376285,#376286,
#376287,#376288,#376289),.UNSPECIFIED.,.F.,.F.,(4,3,4),(1.01643953670516E-19,
2.50000021494119E-5,9.54746331310775E-5),.UNSPECIFIED.);
#24922=B_SPLINE_CURVE_WITH_KNOTS('',3,(#376293,#376294,#376295,#376296,
#376297,#376298,#376299),.UNSPECIFIED.,.F.,.F.,(4,3,4),(0.,2.50000024491139E-5,
9.54746329568077E-5),.UNSPECIFIED.);
#24923=B_SPLINE_CURVE_WITH_KNOTS('',3,(#376303,#376304,#376305,#376306,
#376307,#376308,#376309),.UNSPECIFIED.,.F.,.F.,(4,3,4),(8.13151629364128E-20,
2.5000002149412E-5,9.54746331310775E-5),.UNSPECIFIED.);
#24924=B_SPLINE_CURVE_WITH_KNOTS('',3,(#376313,#376314,#376315,#376316,
#376317,#376318,#376319),.UNSPECIFIED.,.F.,.F.,(4,3,4),(0.,2.50000024491139E-5,
9.54746329568076E-5),.UNSPECIFIED.);
#24925=B_SPLINE_CURVE_WITH_KNOTS('',3,(#376323,#376324,#376325,#376326,
#376327,#376328,#376329),.UNSPECIFIED.,.F.,.F.,(4,3,4),(5.42101086242752E-20,
2.50000021494122E-5,9.54746331310777E-5),.UNSPECIFIED.);
#24926=B_SPLINE_CURVE_WITH_KNOTS('',3,(#376333,#376334,#376335,#376336,
#376337,#376338,#376339),.UNSPECIFIED.,.F.,.F.,(4,3,4),(0.,2.5000002449114E-5,
9.54746329568076E-5),.UNSPECIFIED.);
#24927=B_SPLINE_CURVE_WITH_KNOTS('',3,(#376343,#376344,#376345,#376346,
#376347,#376348,#376349),.UNSPECIFIED.,.F.,.F.,(4,3,4),(4.37055868292169E-19,
2.50000021494117E-5,9.54746331310773E-5),.UNSPECIFIED.);
#24928=B_SPLINE_CURVE_WITH_KNOTS('',3,(#376353,#376354,#376355,#376356,
#376357,#376358,#376359),.UNSPECIFIED.,.F.,.F.,(4,3,4),(0.,2.50000024491139E-5,
9.54746329568076E-5),.UNSPECIFIED.);
#24929=B_SPLINE_CURVE_WITH_KNOTS('',3,(#376363,#376364,#376365,#376366,
#376367,#376368,#376369),.UNSPECIFIED.,.F.,.F.,(4,3,4),(4.47028007668187E-19,
2.50000021494118E-5,9.54746331310774E-5),.UNSPECIFIED.);
#24930=B_SPLINE_CURVE_WITH_KNOTS('',3,(#376373,#376374,#376375,#376376,
#376377,#376378,#376379),.UNSPECIFIED.,.F.,.F.,(4,3,4),(0.,2.50000024491138E-5,
9.54746329568077E-5),.UNSPECIFIED.);
#24931=B_SPLINE_CURVE_WITH_KNOTS('',3,(#376383,#376384,#376385,#376386,
#376387,#376388,#376389),.UNSPECIFIED.,.F.,.F.,(4,3,4),(4.33680868994202E-19,
2.50000021494119E-5,9.54746331310775E-5),.UNSPECIFIED.);
#24932=B_SPLINE_CURVE_WITH_KNOTS('',3,(#376393,#376394,#376395,#376396,
#376397,#376398,#376399),.UNSPECIFIED.,.F.,.F.,(4,3,4),(0.,2.50000024491143E-5,
9.54746329568081E-5),.UNSPECIFIED.);
#24933=B_SPLINE_CURVE_WITH_KNOTS('',3,(#376403,#376404,#376405,#376406,
#376407,#376408,#376409),.UNSPECIFIED.,.F.,.F.,(4,3,4),(4.33680868994202E-19,
2.50000021494122E-5,9.54746331310777E-5),.UNSPECIFIED.);
#24934=B_SPLINE_CURVE_WITH_KNOTS('',3,(#376413,#376414,#376415,#376416,
#376417,#376418,#376419),.UNSPECIFIED.,.F.,.F.,(4,3,4),(0.,2.5000002449114E-5,
9.54746329568078E-5),.UNSPECIFIED.);
#24935=B_SPLINE_CURVE_WITH_KNOTS('',3,(#376423,#376424,#376425,#376426,
#376427,#376428,#376429),.UNSPECIFIED.,.F.,.F.,(4,3,4),(4.33680868994202E-19,
2.5000002149412E-5,9.54746331310774E-5),.UNSPECIFIED.);
#24936=B_SPLINE_CURVE_WITH_KNOTS('',3,(#376433,#376434,#376435,#376436,
#376437,#376438,#376439),.UNSPECIFIED.,.F.,.F.,(4,3,4),(0.,2.50000024491139E-5,
9.54746329568078E-5),.UNSPECIFIED.);
#24937=B_SPLINE_CURVE_WITH_KNOTS('',3,(#376443,#376444,#376445,#376446,
#376447,#376448,#376449),.UNSPECIFIED.,.F.,.F.,(4,3,4),(4.33680868994202E-19,
2.50000021494118E-5,9.54746331310773E-5),.UNSPECIFIED.);
#24938=B_SPLINE_CURVE_WITH_KNOTS('',3,(#376453,#376454,#376455,#376456,
#376457,#376458,#376459),.UNSPECIFIED.,.F.,.F.,(4,3,4),(0.,2.50000024491138E-5,
9.54746329568079E-5),.UNSPECIFIED.);
#24939=B_SPLINE_CURVE_WITH_KNOTS('',3,(#376463,#376464,#376465,#376466,
#376467,#376468,#376469),.UNSPECIFIED.,.F.,.F.,(4,3,4),(4.33680868994202E-19,
2.50000021494121E-5,9.54746331310776E-5),.UNSPECIFIED.);
#24940=B_SPLINE_CURVE_WITH_KNOTS('',3,(#376473,#376474,#376475,#376476,
#376477,#376478,#376479),.UNSPECIFIED.,.F.,.F.,(4,3,4),(0.,2.50000024491139E-5,
9.54746329568078E-5),.UNSPECIFIED.);
#24941=B_SPLINE_CURVE_WITH_KNOTS('',3,(#376483,#376484,#376485,#376486,
#376487,#376488,#376489),.UNSPECIFIED.,.F.,.F.,(4,3,4),(0.,2.50000021494121E-5,
9.54746331310774E-5),.UNSPECIFIED.);
#24942=B_SPLINE_CURVE_WITH_KNOTS('',3,(#376493,#376494,#376495,#376496,
#376497,#376498,#376499),.UNSPECIFIED.,.F.,.F.,(4,3,4),(0.,2.50000024491139E-5,
9.54746329568077E-5),.UNSPECIFIED.);
#24943=B_SPLINE_CURVE_WITH_KNOTS('',3,(#376503,#376504,#376505,#376506,
#376507,#376508,#376509),.UNSPECIFIED.,.F.,.F.,(4,3,4),(4.33680868994202E-19,
2.50000021494123E-5,9.54746331310777E-5),.UNSPECIFIED.);
#24944=B_SPLINE_CURVE_WITH_KNOTS('',3,(#376513,#376514,#376515,#376516,
#376517,#376518,#376519),.UNSPECIFIED.,.F.,.F.,(4,3,4),(0.,2.50000024491139E-5,
9.5474632956808E-5),.UNSPECIFIED.);
#24945=B_SPLINE_CURVE_WITH_KNOTS('',3,(#376523,#376524,#376525,#376526,
#376527,#376528,#376529),.UNSPECIFIED.,.F.,.F.,(4,3,4),(4.33680868994202E-19,
2.50000021494122E-5,9.54746331310776E-5),.UNSPECIFIED.);
#24946=B_SPLINE_CURVE_WITH_KNOTS('',3,(#376533,#376534,#376535,#376536,
#376537,#376538,#376539),.UNSPECIFIED.,.F.,.F.,(4,3,4),(0.,2.50000024491141E-5,
9.5474632956808E-5),.UNSPECIFIED.);
#24947=B_SPLINE_CURVE_WITH_KNOTS('',3,(#376543,#376544,#376545,#376546,
#376547,#376548,#376549),.UNSPECIFIED.,.F.,.F.,(4,3,4),(2.16840434497101E-19,
2.50000021494118E-5,9.54746331310776E-5),.UNSPECIFIED.);
#24948=B_SPLINE_CURVE_WITH_KNOTS('',3,(#376553,#376554,#376555,#376556,
#376557,#376558,#376559),.UNSPECIFIED.,.F.,.F.,(4,3,4),(0.,2.50000024491139E-5,
9.54746329568075E-5),.UNSPECIFIED.);
#24949=B_SPLINE_CURVE_WITH_KNOTS('',3,(#376563,#376564,#376565,#376566,
#376567,#376568,#376569),.UNSPECIFIED.,.F.,.F.,(4,3,4),(2.16840434497101E-19,
2.50000021494121E-5,9.54746331310777E-5),.UNSPECIFIED.);
#24950=B_SPLINE_CURVE_WITH_KNOTS('',3,(#376573,#376574,#376575,#376576,
#376577,#376578,#376579),.UNSPECIFIED.,.F.,.F.,(4,3,4),(0.,2.50000024491136E-5,
9.54746329568077E-5),.UNSPECIFIED.);
#24951=B_SPLINE_CURVE_WITH_KNOTS('',3,(#376583,#376584,#376585,#376586,
#376587,#376588,#376589),.UNSPECIFIED.,.F.,.F.,(4,3,4),(2.16840434497101E-19,
2.50000021494119E-5,9.54746331310775E-5),.UNSPECIFIED.);
#24952=B_SPLINE_CURVE_WITH_KNOTS('',3,(#376593,#376594,#376595,#376596,
#376597,#376598,#376599),.UNSPECIFIED.,.F.,.F.,(4,3,4),(0.,2.50000024491136E-5,
9.54746329568076E-5),.UNSPECIFIED.);
#24953=B_SPLINE_CURVE_WITH_KNOTS('',3,(#376603,#376604,#376605,#376606,
#376607,#376608,#376609),.UNSPECIFIED.,.F.,.F.,(4,3,4),(2.16840434497101E-19,
2.50000021494119E-5,9.54746331310777E-5),.UNSPECIFIED.);
#24954=B_SPLINE_CURVE_WITH_KNOTS('',3,(#376613,#376614,#376615,#376616,
#376617,#376618,#376619),.UNSPECIFIED.,.F.,.F.,(4,3,4),(0.,2.50000024491141E-5,
9.54746329568079E-5),.UNSPECIFIED.);
#24955=B_SPLINE_CURVE_WITH_KNOTS('',3,(#376623,#376624,#376625,#376626,
#376627,#376628,#376629),.UNSPECIFIED.,.F.,.F.,(4,3,4),(2.16840434497101E-19,
2.50000021494119E-5,9.54746331310777E-5),.UNSPECIFIED.);
#24956=B_SPLINE_CURVE_WITH_KNOTS('',3,(#376633,#376634,#376635,#376636,
#376637,#376638,#376639),.UNSPECIFIED.,.F.,.F.,(4,3,4),(0.,2.50000024491142E-5,
9.54746329568078E-5),.UNSPECIFIED.);
#24957=B_SPLINE_CURVE_WITH_KNOTS('',3,(#376643,#376644,#376645,#376646,
#376647,#376648,#376649),.UNSPECIFIED.,.F.,.F.,(4,3,4),(0.,2.50000021494122E-5,
9.54746331310779E-5),.UNSPECIFIED.);
#24958=B_SPLINE_CURVE_WITH_KNOTS('',3,(#376653,#376654,#376655,#376656,
#376657,#376658,#376659),.UNSPECIFIED.,.F.,.F.,(4,3,4),(0.,2.5000002449114E-5,
9.54746329568077E-5),.UNSPECIFIED.);
#24959=B_SPLINE_CURVE_WITH_KNOTS('',3,(#376663,#376664,#376665,#376666,
#376667,#376668,#376669),.UNSPECIFIED.,.F.,.F.,(4,3,4),(2.16840434497101E-19,
2.50000021494119E-5,9.54746331310779E-5),.UNSPECIFIED.);
#24960=B_SPLINE_CURVE_WITH_KNOTS('',3,(#376673,#376674,#376675,#376676,
#376677,#376678,#376679),.UNSPECIFIED.,.F.,.F.,(4,3,4),(0.,2.50000024491139E-5,
9.54746329568078E-5),.UNSPECIFIED.);
#24961=B_SPLINE_CURVE_WITH_KNOTS('',3,(#376683,#376684,#376685,#376686,
#376687,#376688,#376689),.UNSPECIFIED.,.F.,.F.,(4,3,4),(2.16840434497101E-19,
2.50000021494118E-5,9.54746331310776E-5),.UNSPECIFIED.);
#24962=B_SPLINE_CURVE_WITH_KNOTS('',3,(#376693,#376694,#376695,#376696,
#376697,#376698,#376699),.UNSPECIFIED.,.F.,.F.,(4,3,4),(0.,2.50000024491143E-5,
9.54746329568081E-5),.UNSPECIFIED.);
#24963=B_SPLINE_CURVE_WITH_KNOTS('',3,(#376703,#376704,#376705,#376706,
#376707,#376708,#376709),.UNSPECIFIED.,.F.,.F.,(4,3,4),(1.0842021724855E-19,
2.50000021494121E-5,9.54746331310775E-5),.UNSPECIFIED.);
#24964=B_SPLINE_CURVE_WITH_KNOTS('',3,(#376713,#376714,#376715,#376716,
#376717,#376718,#376719),.UNSPECIFIED.,.F.,.F.,(4,3,4),(0.,2.50000024491141E-5,
9.54746329568079E-5),.UNSPECIFIED.);
#24965=B_SPLINE_CURVE_WITH_KNOTS('',3,(#376723,#376724,#376725,#376726,
#376727,#376728,#376729),.UNSPECIFIED.,.F.,.F.,(4,3,4),(1.62630325872826E-19,
2.5000002149412E-5,9.54746331310773E-5),.UNSPECIFIED.);
#24966=B_SPLINE_CURVE_WITH_KNOTS('',3,(#376733,#376734,#376735,#376736,
#376737,#376738,#376739),.UNSPECIFIED.,.F.,.F.,(4,3,4),(0.,2.50000024491141E-5,
9.5474632956808E-5),.UNSPECIFIED.);
#24967=B_SPLINE_CURVE_WITH_KNOTS('',3,(#376743,#376744,#376745,#376746,
#376747,#376748,#376749),.UNSPECIFIED.,.F.,.F.,(4,3,4),(1.0842021724855E-19,
2.50000021494122E-5,9.54746331310777E-5),.UNSPECIFIED.);
#24968=B_SPLINE_CURVE_WITH_KNOTS('',3,(#376753,#376754,#376755,#376756,
#376757,#376758,#376759),.UNSPECIFIED.,.F.,.F.,(4,3,4),(0.,2.50000024491138E-5,
9.54746329568075E-5),.UNSPECIFIED.);
#24969=B_SPLINE_CURVE_WITH_KNOTS('',3,(#376763,#376764,#376765,#376766,
#376767,#376768,#376769),.UNSPECIFIED.,.F.,.F.,(4,3,4),(1.0842021724855E-19,
2.50000021494118E-5,9.54746331310775E-5),.UNSPECIFIED.);
#24970=B_SPLINE_CURVE_WITH_KNOTS('',3,(#376772,#376773,#376774,#376775,
#376776,#376777,#376778),.UNSPECIFIED.,.F.,.F.,(4,3,4),(0.,2.50000024491137E-5,
9.54746329568074E-5),.UNSPECIFIED.);
#24971=B_SPLINE_CURVE_WITH_KNOTS('',3,(#378259,#378260,#378261,#378262,
#378263,#378264,#378265,#378266,#378267,#378268,#378269,#378270,#378271,
#378272,#378273,#378274,#378275,#378276,#378277,#378278,#378279,#378280,
#378281,#378282,#378283,#378284,#378285,#378286,#378287,#378288,#378289,
#378290,#378291,#378292,#378293,#378294,#378295,#378296,#378297,#378298,
#378299,#378300,#378301,#378302,#378303,#378304,#378305,#378306,#378307),
 .UNSPECIFIED.,.F.,.F.,(4,3,3,3,3,3,3,3,3,3,3,3,3,3,3,3,4),(0.,1.53100299373414E-6,
4.52554775678511E-6,7.01151246291606E-6,9.267529338009E-6,1.03084066197173E-5,
1.17138990826862E-5,1.22284894984074E-5,1.30315035324817E-5,1.38363728497813E-5,
1.40464197777495E-5,1.5459774956464E-5,1.62073588704069E-5,1.92092968712803E-5,
1.95234416882555E-5,2.37637844577586E-5,2.61487188977262E-5),
 .UNSPECIFIED.);
#24972=B_SPLINE_CURVE_WITH_KNOTS('',3,(#378315,#378316,#378317,#378318),
 .UNSPECIFIED.,.F.,.F.,(4,4),(4.52388553334502E-19,9.54361881492177E-5),
 .UNSPECIFIED.);
#24973=B_SPLINE_CURVE_WITH_KNOTS('',3,(#378320,#378321,#378322,#378323,
#378324,#378325,#378326),.UNSPECIFIED.,.F.,.F.,(4,3,4),(8.470329472543E-22,
6.9863024419149E-5,0.000113969974038089),.UNSPECIFIED.);
#24974=B_SPLINE_CURVE_WITH_KNOTS('',3,(#378330,#378331,#378332,#378333),
 .UNSPECIFIED.,.F.,.F.,(4,4),(0.,9.54361881492174E-5),.UNSPECIFIED.);
#24975=B_SPLINE_CURVE_WITH_KNOTS('',3,(#378338,#378339,#378340,#378341,
#378342,#378343,#378344),.UNSPECIFIED.,.F.,.F.,(4,3,4),(0.,4.41069704323469E-5,
0.000113970027818833),.UNSPECIFIED.);
#24976=B_SPLINE_CURVE_WITH_KNOTS('',3,(#379924,#379925,#379926,#379927),
 .UNSPECIFIED.,.F.,.F.,(4,4),(4.78962492688793E-19,0.00010938435327491),
 .UNSPECIFIED.);
#24977=B_SPLINE_CURVE_WITH_KNOTS('',3,(#379929,#379930,#379931,#379932),
 .UNSPECIFIED.,.F.,.F.,(4,4),(0.,0.000109384345496908),.UNSPECIFIED.);
#24978=B_SPLINE_CURVE_WITH_KNOTS('',3,(#379946,#379947,#379948,#379949,
#379950,#379951,#379952,#379953,#379954,#379955,#379956,#379957,#379958,
#379959,#379960,#379961,#379962,#379963,#379964,#379965,#379966,#379967,
#379968,#379969,#379970,#379971,#379972,#379973,#379974,#379975,#379976),
 .UNSPECIFIED.,.F.,.F.,(4,3,3,3,3,3,3,3,3,3,4),(0.,3.95507910396971E-6,
7.53768426604197E-6,1.19904533335326E-5,1.40475043392548E-5,1.5145210427592E-5,
1.6786627281411E-5,1.69621513005302E-5,1.81338315460649E-5,1.98906334656487E-5,
2.06132424588165E-5),.UNSPECIFIED.);
#24979=B_SPLINE_CURVE_WITH_KNOTS('',3,(#380032,#380033,#380034,#380035,
#380036,#380037,#380038,#380039,#380040,#380041,#380042,#380043,#380044,
#380045,#380046,#380047,#380048,#380049,#380050,#380051,#380052,#380053,
#380054,#380055,#380056,#380057,#380058,#380059,#380060,#380061,#380062,
#380063,#380064,#380065),.UNSPECIFIED.,.F.,.F.,(4,3,3,3,3,3,3,3,3,3,3,4),
(1.35525271560688E-19,2.0962399272944E-6,3.17176647120221E-6,4.82636181944412E-6,
5.01000917339962E-6,6.13126454147496E-6,8.60486650288856E-6,9.21144281170493E-6,
1.24722301136011E-5,1.42666454787857E-5,2.04670653756765E-5,2.08026438176807E-5),
 .UNSPECIFIED.);
#24980=B_SPLINE_CURVE_WITH_KNOTS('',3,(#380139,#380140,#380141,#380142),
 .UNSPECIFIED.,.F.,.F.,(4,4),(0.,9.54361881492174E-5),.UNSPECIFIED.);
#24981=B_SPLINE_CURVE_WITH_KNOTS('',3,(#380147,#380148,#380149,#380150,
#380151,#380152,#380153),.UNSPECIFIED.,.F.,.F.,(4,3,4),(0.,4.41069704323468E-5,
0.000113970027818833),.UNSPECIFIED.);
#24982=B_SPLINE_CURVE_WITH_KNOTS('',3,(#380159,#380160,#380161,#380162),
 .UNSPECIFIED.,.F.,.F.,(4,4),(4.5436350575631E-19,9.54361881492177E-5),
 .UNSPECIFIED.);
#24983=B_SPLINE_CURVE_WITH_KNOTS('',3,(#380166,#380167,#380168,#380169,
#380170,#380171,#380172),.UNSPECIFIED.,.F.,.F.,(4,3,4),(0.,6.98630244191492E-5,
0.000113969974038089),.UNSPECIFIED.);
#24984=B_SPLINE_CURVE_WITH_KNOTS('',3,(#380175,#380176,#380177,#380178,
#380179,#380180,#380181,#380182,#380183,#380184,#380185,#380186,#380187,
#380188,#380189,#380190,#380191,#380192,#380193,#380194,#380195,#380196,
#380197,#380198,#380199,#380200,#380201,#380202,#380203,#380204,#380205,
#380206,#380207,#380208,#380209,#380210,#380211,#380212,#380213,#380214,
#380215,#380216,#380217,#380218,#380219,#380220,#380221,#380222,#380223),
 .UNSPECIFIED.,.F.,.F.,(4,3,3,3,3,3,3,3,3,3,3,3,3,3,3,3,4),(0.,1.53100299373415E-6,
4.52554775679471E-6,7.01151246291607E-6,9.26752933799583E-6,1.03084066197174E-5,
1.17138990826861E-5,1.22284894984074E-5,1.30315035324818E-5,1.38363728497812E-5,
1.40464197777495E-5,1.5459774956464E-5,1.62073588704069E-5,1.92092968712868E-5,
1.95234416882554E-5,2.37637844577581E-5,2.6148718897726E-5),
 .UNSPECIFIED.);
#24985=B_SPLINE_CURVE_WITH_KNOTS('',3,(#380238,#380239,#380240,#380241,
#380242,#380243,#380244,#380245,#380246,#380247,#380248,#380249,#380250,
#380251,#380252,#380253,#380254,#380255,#380256,#380257,#380258,#380259,
#380260,#380261,#380262,#380263,#380264,#380265,#380266,#380267,#380268),
 .UNSPECIFIED.,.F.,.F.,(4,3,3,3,3,3,3,3,3,3,4),(0.,3.955079103984E-6,7.53768426604202E-6,
1.19904533335351E-5,1.40475043392586E-5,1.51452104275965E-5,1.67866272814136E-5,
1.69621513005359E-5,1.81338315460712E-5,1.98906334656503E-5,2.06132424588245E-5),
 .UNSPECIFIED.);
#24986=B_SPLINE_CURVE_WITH_KNOTS('',3,(#380271,#380272,#380273,#380274),
 .UNSPECIFIED.,.F.,.F.,(4,4),(4.97582654080651E-19,0.00010938435327491),
 .UNSPECIFIED.);
#24987=B_SPLINE_CURVE_WITH_KNOTS('',3,(#380301,#380302,#380303,#380304,
#380305,#380306,#380307,#380308,#380309,#380310,#380311,#380312,#380313,
#380314,#380315,#380316,#380317,#380318,#380319,#380320,#380321,#380322,
#380323,#380324,#380325,#380326,#380327,#380328,#380329,#380330,#380331,
#380332,#380333,#380334),.UNSPECIFIED.,.F.,.F.,(4,3,3,3,3,3,3,3,3,3,3,4),
(1.35525271560688E-19,2.09623992729445E-6,3.17176647120226E-6,4.82636181942471E-6,
5.01000917339969E-6,6.13126454147507E-6,8.60486650288873E-6,9.21144281170513E-6,
1.24722301135971E-5,1.4266645478786E-5,2.04670653756875E-5,2.0802643817681E-5),
 .UNSPECIFIED.);
#24988=B_SPLINE_CURVE_WITH_KNOTS('',3,(#380335,#380336,#380337,#380338),
 .UNSPECIFIED.,.F.,.F.,(4,4),(0.,0.000109384345496908),.UNSPECIFIED.);
#24989=B_SPLINE_CURVE_WITH_KNOTS('',3,(#380443,#380444,#380445,#380446),
 .UNSPECIFIED.,.F.,.F.,(4,4),(0.,9.54361881492173E-5),.UNSPECIFIED.);
#24990=B_SPLINE_CURVE_WITH_KNOTS('',3,(#380451,#380452,#380453,#380454,
#380455,#380456,#380457),.UNSPECIFIED.,.F.,.F.,(4,3,4),(0.,4.41069704323468E-5,
0.000113970027818833),.UNSPECIFIED.);
#24991=B_SPLINE_CURVE_WITH_KNOTS('',3,(#380463,#380464,#380465,#380466),
 .UNSPECIFIED.,.F.,.F.,(4,4),(4.47028007668187E-19,9.54361881492177E-5),
 .UNSPECIFIED.);
#24992=B_SPLINE_CURVE_WITH_KNOTS('',3,(#380470,#380471,#380472,#380473,
#380474,#380475,#380476),.UNSPECIFIED.,.F.,.F.,(4,3,4),(0.,6.98630244191489E-5,
0.000113969974038089),.UNSPECIFIED.);
#24993=B_SPLINE_CURVE_WITH_KNOTS('',3,(#380479,#380480,#380481,#380482,
#380483,#380484,#380485,#380486,#380487,#380488,#380489,#380490,#380491,
#380492,#380493,#380494,#380495,#380496,#380497,#380498,#380499,#380500,
#380501,#380502,#380503,#380504,#380505,#380506,#380507,#380508,#380509,
#380510,#380511,#380512,#380513,#380514,#380515,#380516,#380517,#380518,
#380519,#380520,#380521,#380522,#380523,#380524,#380525,#380526,#380527),
 .UNSPECIFIED.,.F.,.F.,(4,3,3,3,3,3,3,3,3,3,3,3,3,3,3,3,4),(0.,1.53100299373405E-6,
4.52554775679585E-6,7.01151246291601E-6,9.26752933800506E-6,1.03084066197174E-5,
1.17138990826862E-5,1.22284894984075E-5,1.30315035324818E-5,1.38363728497813E-5,
1.40464197777496E-5,1.54597749564641E-5,1.62073588704069E-5,1.92092968712673E-5,
1.95234416882556E-5,2.37637844577608E-5,2.61487188977265E-5),
 .UNSPECIFIED.);
#24994=B_SPLINE_CURVE_WITH_KNOTS('',3,(#380542,#380543,#380544,#380545,
#380546,#380547,#380548,#380549,#380550,#380551,#380552,#380553,#380554,
#380555,#380556,#380557,#380558,#380559,#380560,#380561,#380562,#380563,
#380564,#380565,#380566,#380567,#380568,#380569,#380570,#380571,#380572),
 .UNSPECIFIED.,.F.,.F.,(4,3,3,3,3,3,3,3,3,3,4),(0.,3.95507910397942E-6,
7.53768426604206E-6,1.19904533335352E-5,1.40475043392586E-5,1.51452104275965E-5,
1.67866272814147E-5,1.69621513005359E-5,1.81338315460713E-5,1.9890633465653E-5,
2.06132424588247E-5),.UNSPECIFIED.);
#24995=B_SPLINE_CURVE_WITH_KNOTS('',3,(#380575,#380576,#380577,#380578),
 .UNSPECIFIED.,.F.,.F.,(4,4),(4.73369422993816E-19,0.00010938435327491),
 .UNSPECIFIED.);
#24996=B_SPLINE_CURVE_WITH_KNOTS('',3,(#380605,#380606,#380607,#380608,
#380609,#380610,#380611,#380612,#380613,#380614,#380615,#380616,#380617,
#380618,#380619,#380620,#380621,#380622,#380623,#380624,#380625,#380626,
#380627,#380628,#380629,#380630,#380631,#380632,#380633,#380634,#380635,
#380636,#380637,#380638),.UNSPECIFIED.,.F.,.F.,(4,3,3,3,3,3,3,3,3,3,3,4),
(1.35525271560688E-19,2.09623992729439E-6,3.17176647120221E-6,4.82636181945277E-6,
5.01000917339961E-6,6.13126454147493E-6,8.60486650288835E-6,9.21144281170465E-6,
1.24722301135837E-5,1.42666454787848E-5,2.04670653756579E-5,2.08026438176788E-5),
 .UNSPECIFIED.);
#24997=B_SPLINE_CURVE_WITH_KNOTS('',3,(#380639,#380640,#380641,#380642),
 .UNSPECIFIED.,.F.,.F.,(4,4),(0.,0.000109384345496908),.UNSPECIFIED.);
#24998=B_SPLINE_CURVE_WITH_KNOTS('',3,(#380747,#380748,#380749,#380750),
 .UNSPECIFIED.,.F.,.F.,(4,4),(0.,9.54361881492175E-5),.UNSPECIFIED.);
#24999=B_SPLINE_CURVE_WITH_KNOTS('',3,(#380755,#380756,#380757,#380758,
#380759,#380760,#380761),.UNSPECIFIED.,.F.,.F.,(4,3,4),(0.,4.41069704323466E-5,
0.000113970027818833),.UNSPECIFIED.);
#25000=B_SPLINE_CURVE_WITH_KNOTS('',3,(#380767,#380768,#380769,#380770),
 .UNSPECIFIED.,.F.,.F.,(4,4),(4.47028007668187E-19,9.5436188149218E-5),
 .UNSPECIFIED.);
#25001=B_SPLINE_CURVE_WITH_KNOTS('',3,(#380774,#380775,#380776,#380777,
#380778,#380779,#380780),.UNSPECIFIED.,.F.,.F.,(4,3,4),(0.,6.98630244191489E-5,
0.000113969974038089),.UNSPECIFIED.);
#25002=B_SPLINE_CURVE_WITH_KNOTS('',3,(#380783,#380784,#380785,#380786,
#380787,#380788,#380789,#380790,#380791,#380792,#380793,#380794,#380795,
#380796,#380797,#380798,#380799,#380800,#380801,#380802,#380803,#380804,
#380805,#380806,#380807,#380808,#380809,#380810,#380811,#380812,#380813,
#380814,#380815,#380816,#380817,#380818,#380819,#380820,#380821,#380822,
#380823,#380824,#380825,#380826,#380827,#380828,#380829,#380830,#380831),
 .UNSPECIFIED.,.F.,.F.,(4,3,3,3,3,3,3,3,3,3,3,3,3,3,3,3,4),(0.,1.53100299373417E-6,
4.52554775679147E-6,7.01151246291613E-6,9.26752933799189E-6,1.03084066197174E-5,
1.17138990826863E-5,1.22284894984075E-5,1.30315035324818E-5,1.38363728497813E-5,
1.40464197777496E-5,1.54597749564641E-5,1.6207358870407E-5,1.92092968713039E-5,
1.95234416882556E-5,2.37637844577595E-5,2.61487188977263E-5),
 .UNSPECIFIED.);
#25003=B_SPLINE_CURVE_WITH_KNOTS('',3,(#380846,#380847,#380848,#380849,
#380850,#380851,#380852,#380853,#380854,#380855,#380856,#380857,#380858,
#380859,#380860,#380861,#380862,#380863,#380864,#380865,#380866,#380867,
#380868,#380869,#380870,#380871,#380872,#380873,#380874,#380875,#380876),
 .UNSPECIFIED.,.F.,.F.,(4,3,3,3,3,3,3,3,3,3,4),(0.,3.95507910397588E-6,
7.53768426604194E-6,1.1990453333535E-5,1.40475043392586E-5,1.51452104275964E-5,
1.67866272814194E-5,1.69621513005358E-5,1.81338315460711E-5,1.9890633465654E-5,
2.06132424588243E-5),.UNSPECIFIED.);
#25004=B_SPLINE_CURVE_WITH_KNOTS('',3,(#380879,#380880,#380881,#380882),
 .UNSPECIFIED.,.F.,.F.,(4,4),(4.63171371119878E-19,0.00010938435327491),
 .UNSPECIFIED.);
#25005=B_SPLINE_CURVE_WITH_KNOTS('',3,(#380909,#380910,#380911,#380912,
#380913,#380914,#380915,#380916,#380917,#380918,#380919,#380920,#380921,
#380922,#380923,#380924,#380925,#380926,#380927,#380928,#380929,#380930,
#380931,#380932,#380933,#380934,#380935,#380936,#380937,#380938,#380939,
#380940,#380941,#380942),.UNSPECIFIED.,.F.,.F.,(4,3,3,3,3,3,3,3,3,3,3,4),
(1.62630325872826E-19,2.09623992729438E-6,3.17176647120217E-6,4.82636181944348E-6,
5.0100091733996E-6,6.13126454147498E-6,8.60486650288868E-6,9.21144281170502E-6,
1.24722301135972E-5,1.42666454787857E-5,2.04670653756983E-5,2.08026438176807E-5),
 .UNSPECIFIED.);
#25006=B_SPLINE_CURVE_WITH_KNOTS('',3,(#380943,#380944,#380945,#380946),
 .UNSPECIFIED.,.F.,.F.,(4,4),(0.,0.000109384345496908),.UNSPECIFIED.);
#25007=B_SPLINE_CURVE_WITH_KNOTS('',3,(#381051,#381052,#381053,#381054),
 .UNSPECIFIED.,.F.,.F.,(4,4),(0.,9.54361881492172E-5),.UNSPECIFIED.);
#25008=B_SPLINE_CURVE_WITH_KNOTS('',3,(#381059,#381060,#381061,#381062,
#381063,#381064,#381065),.UNSPECIFIED.,.F.,.F.,(4,3,4),(0.,4.41069704323472E-5,
0.000113970027818833),.UNSPECIFIED.);
#25009=B_SPLINE_CURVE_WITH_KNOTS('',3,(#381071,#381072,#381073,#381074),
 .UNSPECIFIED.,.F.,.F.,(4,4),(4.37055868292169E-19,9.54361881492179E-5),
 .UNSPECIFIED.);
#25010=B_SPLINE_CURVE_WITH_KNOTS('',3,(#381078,#381079,#381080,#381081,
#381082,#381083,#381084),.UNSPECIFIED.,.F.,.F.,(4,3,4),(0.,6.98630244191489E-5,
0.000113969974038089),.UNSPECIFIED.);
#25011=B_SPLINE_CURVE_WITH_KNOTS('',3,(#381087,#381088,#381089,#381090,
#381091,#381092,#381093,#381094,#381095,#381096,#381097,#381098,#381099,
#381100,#381101,#381102,#381103,#381104,#381105,#381106,#381107,#381108,
#381109,#381110,#381111,#381112,#381113,#381114,#381115,#381116,#381117,
#381118,#381119,#381120,#381121,#381122,#381123,#381124,#381125,#381126,
#381127,#381128,#381129,#381130,#381131,#381132,#381133,#381134,#381135),
 .UNSPECIFIED.,.F.,.F.,(4,3,3,3,3,3,3,3,3,3,3,3,3,3,3,3,4),(0.,1.53100299373414E-6,
4.52554775679612E-6,7.01151246291615E-6,9.26752933800107E-6,1.03084066197174E-5,
1.17138990826862E-5,1.22284894984074E-5,1.30315035324818E-5,1.38363728497813E-5,
1.40464197777496E-5,1.54597749564641E-5,1.6207358870407E-5,1.9209296871355E-5,
1.95234416882559E-5,2.37637844577606E-5,2.61487188977269E-5),
 .UNSPECIFIED.);
#25012=B_SPLINE_CURVE_WITH_KNOTS('',3,(#381150,#381151,#381152,#381153,
#381154,#381155,#381156,#381157,#381158,#381159,#381160,#381161,#381162,
#381163,#381164,#381165,#381166,#381167,#381168,#381169,#381170,#381171,
#381172,#381173,#381174,#381175,#381176,#381177,#381178,#381179,#381180),
 .UNSPECIFIED.,.F.,.F.,(4,3,3,3,3,3,3,3,3,3,4),(0.,3.9550791039771E-6,7.53768426604201E-6,
1.19904533335351E-5,1.40475043392586E-5,1.51452104275965E-5,1.67866272814208E-5,
1.69621513005358E-5,1.81338315460712E-5,1.9890633465655E-5,2.06132424588245E-5),
 .UNSPECIFIED.);
#25013=B_SPLINE_CURVE_WITH_KNOTS('',3,(#381183,#381184,#381185,#381186),
 .UNSPECIFIED.,.F.,.F.,(4,4),(4.47028007668187E-19,0.00010938435327491),
 .UNSPECIFIED.);
#25014=B_SPLINE_CURVE_WITH_KNOTS('',3,(#381213,#381214,#381215,#381216,
#381217,#381218,#381219,#381220,#381221,#381222,#381223,#381224,#381225,
#381226,#381227,#381228,#381229,#381230,#381231,#381232,#381233,#381234,
#381235,#381236,#381237,#381238,#381239,#381240,#381241,#381242,#381243,
#381244,#381245,#381246),.UNSPECIFIED.,.F.,.F.,(4,3,3,3,3,3,3,3,3,3,3,4),
(1.0842021724855E-19,2.09623992729441E-6,3.17176647120218E-6,4.82636181944089E-6,
5.01000917339966E-6,6.13126454147497E-6,8.60486650288866E-6,9.21144281170497E-6,
1.24722301135846E-5,1.42666454787859E-5,2.04670653756979E-5,2.08026438176808E-5),
 .UNSPECIFIED.);
#25015=B_SPLINE_CURVE_WITH_KNOTS('',3,(#381247,#381248,#381249,#381250),
 .UNSPECIFIED.,.F.,.F.,(4,4),(0.,0.000109384345496908),.UNSPECIFIED.);
#25016=B_SPLINE_CURVE_WITH_KNOTS('',3,(#381355,#381356,#381357,#381358),
 .UNSPECIFIED.,.F.,.F.,(4,4),(0.,9.54361881492173E-5),.UNSPECIFIED.);
#25017=B_SPLINE_CURVE_WITH_KNOTS('',3,(#381363,#381364,#381365,#381366,
#381367,#381368,#381369),.UNSPECIFIED.,.F.,.F.,(4,3,4),(0.,4.41069704323466E-5,
0.000113970027818833),.UNSPECIFIED.);
#25018=B_SPLINE_CURVE_WITH_KNOTS('',3,(#381375,#381376,#381377,#381378),
 .UNSPECIFIED.,.F.,.F.,(4,4),(4.47028007668187E-19,9.54361881492179E-5),
 .UNSPECIFIED.);
#25019=B_SPLINE_CURVE_WITH_KNOTS('',3,(#381382,#381383,#381384,#381385,
#381386,#381387,#381388),.UNSPECIFIED.,.F.,.F.,(4,3,4),(0.,6.98630244191492E-5,
0.000113969974038089),.UNSPECIFIED.);
#25020=B_SPLINE_CURVE_WITH_KNOTS('',3,(#381391,#381392,#381393,#381394,
#381395,#381396,#381397,#381398,#381399,#381400,#381401,#381402,#381403,
#381404,#381405,#381406,#381407,#381408,#381409,#381410,#381411,#381412,
#381413,#381414,#381415,#381416,#381417,#381418,#381419,#381420,#381421,
#381422,#381423,#381424,#381425,#381426,#381427,#381428,#381429,#381430,
#381431,#381432,#381433,#381434,#381435,#381436,#381437,#381438,#381439),
 .UNSPECIFIED.,.F.,.F.,(4,3,3,3,3,3,3,3,3,3,3,3,3,3,3,3,4),(0.,1.53100299373415E-6,
4.52554775679401E-6,7.01151246291589E-6,9.26752933799417E-6,1.03084066197173E-5,
1.1713899082686E-5,1.22284894984072E-5,1.30315035324816E-5,1.38363728497811E-5,
1.40464197777493E-5,1.54597749564639E-5,1.62073588704067E-5,1.92092968713137E-5,
1.95234416882553E-5,2.37637844577647E-5,2.61487188977258E-5),
 .UNSPECIFIED.);
#25021=B_SPLINE_CURVE_WITH_KNOTS('',3,(#381454,#381455,#381456,#381457,
#381458,#381459,#381460,#381461,#381462,#381463,#381464,#381465,#381466,
#381467,#381468,#381469,#381470,#381471,#381472,#381473,#381474,#381475,
#381476,#381477,#381478,#381479,#381480,#381481,#381482,#381483,#381484),
 .UNSPECIFIED.,.F.,.F.,(4,3,3,3,3,3,3,3,3,3,4),(0.,3.95507910398011E-6,
7.53768426604197E-6,1.1990453333535E-5,1.40475043392585E-5,1.51452104275964E-5,
1.67866272814066E-5,1.69621513005359E-5,1.81338315460713E-5,1.98906334656507E-5,
2.06132424588245E-5),.UNSPECIFIED.);
#25022=B_SPLINE_CURVE_WITH_KNOTS('',3,(#381487,#381488,#381489,#381490),
 .UNSPECIFIED.,.F.,.F.,(4,4),(4.47028007668187E-19,0.00010938435327491),
 .UNSPECIFIED.);
#25023=B_SPLINE_CURVE_WITH_KNOTS('',3,(#381517,#381518,#381519,#381520,
#381521,#381522,#381523,#381524,#381525,#381526,#381527,#381528,#381529,
#381530,#381531,#381532,#381533,#381534,#381535,#381536,#381537,#381538,
#381539,#381540,#381541,#381542,#381543,#381544,#381545,#381546,#381547,
#381548,#381549,#381550),.UNSPECIFIED.,.F.,.F.,(4,3,3,3,3,3,3,3,3,3,3,4),
(1.0842021724855E-19,2.09623992729435E-6,3.17176647120225E-6,4.82636181945333E-6,
5.01000917339964E-6,6.13126454147489E-6,8.60486650288845E-6,9.21144281170481E-6,
1.24722301136083E-5,1.42666454787854E-5,2.04670653756731E-5,2.08026438176802E-5),
 .UNSPECIFIED.);
#25024=B_SPLINE_CURVE_WITH_KNOTS('',3,(#381551,#381552,#381553,#381554),
 .UNSPECIFIED.,.F.,.F.,(4,4),(0.,0.000109384345496908),.UNSPECIFIED.);
#25025=B_SPLINE_CURVE_WITH_KNOTS('',3,(#381659,#381660,#381661,#381662),
 .UNSPECIFIED.,.F.,.F.,(4,4),(0.,9.54361881492174E-5),.UNSPECIFIED.);
#25026=B_SPLINE_CURVE_WITH_KNOTS('',3,(#381667,#381668,#381669,#381670,
#381671,#381672,#381673),.UNSPECIFIED.,.F.,.F.,(4,3,4),(0.,4.41069704323472E-5,
0.000113970027818833),.UNSPECIFIED.);
#25027=B_SPLINE_CURVE_WITH_KNOTS('',3,(#381679,#381680,#381681,#381682),
 .UNSPECIFIED.,.F.,.F.,(4,4),(4.47028007668187E-19,9.54361881492179E-5),
 .UNSPECIFIED.);
#25028=B_SPLINE_CURVE_WITH_KNOTS('',3,(#381686,#381687,#381688,#381689,
#381690,#381691,#381692),.UNSPECIFIED.,.F.,.F.,(4,3,4),(0.,6.98630244191489E-5,
0.000113969974038089),.UNSPECIFIED.);
#25029=B_SPLINE_CURVE_WITH_KNOTS('',3,(#381695,#381696,#381697,#381698,
#381699,#381700,#381701,#381702,#381703,#381704,#381705,#381706,#381707,
#381708,#381709,#381710,#381711,#381712,#381713,#381714,#381715,#381716,
#381717,#381718,#381719,#381720,#381721,#381722,#381723,#381724,#381725,
#381726,#381727,#381728,#381729,#381730,#381731,#381732,#381733,#381734,
#381735,#381736,#381737,#381738,#381739,#381740,#381741,#381742,#381743),
 .UNSPECIFIED.,.F.,.F.,(4,3,3,3,3,3,3,3,3,3,3,3,3,3,3,3,4),(0.,1.53100299373425E-6,
4.52554775679595E-6,7.01151246291619E-6,9.26752933800558E-6,1.03084066197173E-5,
1.17138990826862E-5,1.22284894984073E-5,1.30315035324817E-5,1.38363728497812E-5,
1.40464197777493E-5,1.54597749564638E-5,1.62073588704066E-5,1.92092968713467E-5,
1.95234416882551E-5,2.37637844577615E-5,2.61487188977252E-5),
 .UNSPECIFIED.);
#25030=B_SPLINE_CURVE_WITH_KNOTS('',3,(#381758,#381759,#381760,#381761,
#381762,#381763,#381764,#381765,#381766,#381767,#381768,#381769,#381770,
#381771,#381772,#381773,#381774,#381775,#381776,#381777,#381778,#381779,
#381780,#381781,#381782,#381783,#381784,#381785,#381786,#381787,#381788),
 .UNSPECIFIED.,.F.,.F.,(4,3,3,3,3,3,3,3,3,3,4),(0.,3.95507910398648E-6,
7.53768426604196E-6,1.19904533335351E-5,1.40475043392585E-5,1.51452104275965E-5,
1.67866272814172E-5,1.69621513005359E-5,1.81338315460713E-5,1.98906334656488E-5,
2.06132424588247E-5),.UNSPECIFIED.);
#25031=B_SPLINE_CURVE_WITH_KNOTS('',3,(#381791,#381792,#381793,#381794),
 .UNSPECIFIED.,.F.,.F.,(4,4),(4.47028007668187E-19,0.00010938435327491),
 .UNSPECIFIED.);
#25032=B_SPLINE_CURVE_WITH_KNOTS('',3,(#381821,#381822,#381823,#381824,
#381825,#381826,#381827,#381828,#381829,#381830,#381831,#381832,#381833,
#381834,#381835,#381836,#381837,#381838,#381839,#381840,#381841,#381842,
#381843,#381844,#381845,#381846,#381847,#381848,#381849,#381850,#381851,
#381852,#381853,#381854),.UNSPECIFIED.,.F.,.F.,(4,3,3,3,3,3,3,3,3,3,3,4),
(2.16840434497101E-19,2.09623992729427E-6,3.17176647120211E-6,4.82636181942053E-6,
5.01000917339956E-6,6.13126454147484E-6,8.60486650288841E-6,9.21144281170459E-6,
1.24722301135956E-5,1.4266645478785E-5,2.04670653756731E-5,2.08026438176793E-5),
 .UNSPECIFIED.);
#25033=B_SPLINE_CURVE_WITH_KNOTS('',3,(#381855,#381856,#381857,#381858),
 .UNSPECIFIED.,.F.,.F.,(4,4),(0.,0.000109384345496908),.UNSPECIFIED.);
#25034=B_SPLINE_CURVE_WITH_KNOTS('',3,(#381963,#381964,#381965,#381966),
 .UNSPECIFIED.,.F.,.F.,(4,4),(0.,9.54361881492177E-5),.UNSPECIFIED.);
#25035=B_SPLINE_CURVE_WITH_KNOTS('',3,(#381971,#381972,#381973,#381974,
#381975,#381976,#381977),.UNSPECIFIED.,.F.,.F.,(4,3,4),(0.,4.4106970432347E-5,
0.000113970027818833),.UNSPECIFIED.);
#25036=B_SPLINE_CURVE_WITH_KNOTS('',3,(#381983,#381984,#381985,#381986),
 .UNSPECIFIED.,.F.,.F.,(4,4),(0.,9.54361881492179E-5),.UNSPECIFIED.);
#25037=B_SPLINE_CURVE_WITH_KNOTS('',3,(#381990,#381991,#381992,#381993,
#381994,#381995,#381996),.UNSPECIFIED.,.F.,.F.,(4,3,4),(0.,6.98630244191492E-5,
0.000113969974038089),.UNSPECIFIED.);
#25038=B_SPLINE_CURVE_WITH_KNOTS('',3,(#381999,#382000,#382001,#382002,
#382003,#382004,#382005,#382006,#382007,#382008,#382009,#382010,#382011,
#382012,#382013,#382014,#382015,#382016,#382017,#382018,#382019,#382020,
#382021,#382022,#382023,#382024,#382025,#382026,#382027,#382028,#382029,
#382030,#382031,#382032,#382033,#382034,#382035,#382036,#382037,#382038,
#382039,#382040,#382041,#382042,#382043,#382044,#382045,#382046,#382047),
 .UNSPECIFIED.,.F.,.F.,(4,3,3,3,3,3,3,3,3,3,3,3,3,3,3,3,4),(0.,1.53100299373418E-6,
4.52554775680239E-6,7.01151246291602E-6,9.26752933798331E-6,1.03084066197173E-5,
1.17138990826861E-5,1.22284894984073E-5,1.30315035324816E-5,1.38363728497811E-5,
1.40464197777492E-5,1.54597749564639E-5,1.62073588704068E-5,1.92092968713089E-5,
1.95234416882554E-5,2.37637844577582E-5,2.61487188977262E-5),
 .UNSPECIFIED.);
#25039=B_SPLINE_CURVE_WITH_KNOTS('',3,(#382062,#382063,#382064,#382065,
#382066,#382067,#382068,#382069,#382070,#382071,#382072,#382073,#382074,
#382075,#382076,#382077,#382078,#382079,#382080,#382081,#382082,#382083,
#382084,#382085,#382086,#382087,#382088,#382089,#382090,#382091,#382092),
 .UNSPECIFIED.,.F.,.F.,(4,3,3,3,3,3,3,3,3,3,4),(0.,3.95507910398411E-6,
7.53768426604195E-6,1.19904533335351E-5,1.40475043392585E-5,1.51452104275965E-5,
1.6786627281414E-5,1.6962151300536E-5,1.81338315460712E-5,1.98906334656507E-5,
2.06132424588247E-5),.UNSPECIFIED.);
#25040=B_SPLINE_CURVE_WITH_KNOTS('',3,(#382095,#382096,#382097,#382098),
 .UNSPECIFIED.,.F.,.F.,(4,4),(4.33680868994202E-19,0.00010938435327491),
 .UNSPECIFIED.);
#25041=B_SPLINE_CURVE_WITH_KNOTS('',3,(#382125,#382126,#382127,#382128,
#382129,#382130,#382131,#382132,#382133,#382134,#382135,#382136,#382137,
#382138,#382139,#382140,#382141,#382142,#382143,#382144,#382145,#382146,
#382147,#382148,#382149,#382150,#382151,#382152,#382153,#382154,#382155,
#382156,#382157,#382158),.UNSPECIFIED.,.F.,.F.,(4,3,3,3,3,3,3,3,3,3,3,4),
(2.16840434497101E-19,2.09623992729466E-6,3.17176647120241E-6,4.82636181943524E-6,
5.01000917339945E-6,6.13126454147498E-6,8.60486650288857E-6,9.21144281170474E-6,
1.24722301135961E-5,1.42666454787854E-5,2.04670653756923E-5,2.08026438176799E-5),
 .UNSPECIFIED.);
#25042=B_SPLINE_CURVE_WITH_KNOTS('',3,(#382159,#382160,#382161,#382162),
 .UNSPECIFIED.,.F.,.F.,(4,4),(0.,0.000109384345496909),.UNSPECIFIED.);
#25043=B_SPLINE_CURVE_WITH_KNOTS('',3,(#382267,#382268,#382269,#382270),
 .UNSPECIFIED.,.F.,.F.,(4,4),(0.,9.54361881492174E-5),.UNSPECIFIED.);
#25044=B_SPLINE_CURVE_WITH_KNOTS('',3,(#382275,#382276,#382277,#382278,
#382279,#382280,#382281),.UNSPECIFIED.,.F.,.F.,(4,3,4),(0.,4.4106970432347E-5,
0.000113970027818833),.UNSPECIFIED.);
#25045=B_SPLINE_CURVE_WITH_KNOTS('',3,(#382287,#382288,#382289,#382290),
 .UNSPECIFIED.,.F.,.F.,(4,4),(4.33680868994202E-19,9.54361881492179E-5),
 .UNSPECIFIED.);
#25046=B_SPLINE_CURVE_WITH_KNOTS('',3,(#382294,#382295,#382296,#382297,
#382298,#382299,#382300),.UNSPECIFIED.,.F.,.F.,(4,3,4),(0.,6.98630244191489E-5,
0.000113969974038089),.UNSPECIFIED.);
#25047=B_SPLINE_CURVE_WITH_KNOTS('',3,(#382303,#382304,#382305,#382306,
#382307,#382308,#382309,#382310,#382311,#382312,#382313,#382314,#382315,
#382316,#382317,#382318,#382319,#382320,#382321,#382322,#382323,#382324,
#382325,#382326,#382327,#382328,#382329,#382330,#382331,#382332,#382333,
#382334,#382335,#382336,#382337,#382338,#382339,#382340,#382341,#382342,
#382343,#382344,#382345,#382346,#382347,#382348,#382349,#382350,#382351),
 .UNSPECIFIED.,.F.,.F.,(4,3,3,3,3,3,3,3,3,3,3,3,3,3,3,3,4),(0.,1.53100299373401E-6,
4.52554775679861E-6,7.01151246291619E-6,9.26752933802088E-6,1.03084066197173E-5,
1.1713899082686E-5,1.22284894984074E-5,1.30315035324816E-5,1.38363728497811E-5,
1.40464197777492E-5,1.5459774956464E-5,1.62073588704067E-5,1.92092968712723E-5,
1.95234416882556E-5,2.37637844577569E-5,2.61487188977263E-5),
 .UNSPECIFIED.);
#25048=B_SPLINE_CURVE_WITH_KNOTS('',3,(#382366,#382367,#382368,#382369,
#382370,#382371,#382372,#382373,#382374,#382375,#382376,#382377,#382378,
#382379,#382380,#382381,#382382,#382383,#382384,#382385,#382386,#382387,
#382388,#382389,#382390,#382391,#382392,#382393,#382394,#382395,#382396),
 .UNSPECIFIED.,.F.,.F.,(4,3,3,3,3,3,3,3,3,3,4),(0.,3.95507910396927E-6,
7.53768426604198E-6,1.1990453333535E-5,1.40475043392585E-5,1.51452104275963E-5,
1.67866272814057E-5,1.69621513005357E-5,1.8133831546071E-5,1.98906334656562E-5,
2.06132424588242E-5),.UNSPECIFIED.);
#25049=B_SPLINE_CURVE_WITH_KNOTS('',3,(#382399,#382400,#382401,#382402),
 .UNSPECIFIED.,.F.,.F.,(4,4),(4.33680868994202E-19,0.00010938435327491),
 .UNSPECIFIED.);
#25050=B_SPLINE_CURVE_WITH_KNOTS('',3,(#382429,#382430,#382431,#382432,
#382433,#382434,#382435,#382436,#382437,#382438,#382439,#382440,#382441,
#382442,#382443,#382444,#382445,#382446,#382447,#382448,#382449,#382450,
#382451,#382452,#382453,#382454,#382455,#382456,#382457,#382458,#382459,
#382460,#382461,#382462),.UNSPECIFIED.,.F.,.F.,(4,3,3,3,3,3,3,3,3,3,3,4),
(2.16840434497101E-19,2.09623992729424E-6,3.17176647120203E-6,4.82636181944634E-6,
5.01000917339943E-6,6.13126454147496E-6,8.60486650288851E-6,9.21144281170474E-6,
1.24722301136161E-5,1.42666454787853E-5,2.04670653756786E-5,2.08026438176797E-5),
 .UNSPECIFIED.);
#25051=B_SPLINE_CURVE_WITH_KNOTS('',3,(#382463,#382464,#382465,#382466),
 .UNSPECIFIED.,.F.,.F.,(4,4),(0.,0.000109384345496908),.UNSPECIFIED.);
#25052=B_SPLINE_CURVE_WITH_KNOTS('',3,(#382571,#382572,#382573,#382574),
 .UNSPECIFIED.,.F.,.F.,(4,4),(0.,9.54361881492174E-5),.UNSPECIFIED.);
#25053=B_SPLINE_CURVE_WITH_KNOTS('',3,(#382579,#382580,#382581,#382582,
#382583,#382584,#382585),.UNSPECIFIED.,.F.,.F.,(4,3,4),(0.,4.41069704323468E-5,
0.000113970027818833),.UNSPECIFIED.);
#25054=B_SPLINE_CURVE_WITH_KNOTS('',3,(#382591,#382592,#382593,#382594),
 .UNSPECIFIED.,.F.,.F.,(4,4),(4.33680868994202E-19,9.54361881492175E-5),
 .UNSPECIFIED.);
#25055=B_SPLINE_CURVE_WITH_KNOTS('',3,(#382598,#382599,#382600,#382601,
#382602,#382603,#382604),.UNSPECIFIED.,.F.,.F.,(4,3,4),(0.,6.9863024419149E-5,
0.000113969974038089),.UNSPECIFIED.);
#25056=B_SPLINE_CURVE_WITH_KNOTS('',3,(#382607,#382608,#382609,#382610,
#382611,#382612,#382613,#382614,#382615,#382616,#382617,#382618,#382619,
#382620,#382621,#382622,#382623,#382624,#382625,#382626,#382627,#382628,
#382629,#382630,#382631,#382632,#382633,#382634,#382635,#382636,#382637,
#382638,#382639,#382640,#382641,#382642,#382643,#382644,#382645,#382646,
#382647,#382648,#382649,#382650,#382651,#382652,#382653,#382654,#382655),
 .UNSPECIFIED.,.F.,.F.,(4,3,3,3,3,3,3,3,3,3,3,3,3,3,3,3,4),(0.,1.53100299373428E-6,
4.52554775679969E-6,7.01151246291618E-6,9.26752933799351E-6,1.03084066197174E-5,
1.17138990826862E-5,1.22284894984074E-5,1.30315035324818E-5,1.38363728497811E-5,
1.40464197777494E-5,1.54597749564639E-5,1.62073588704067E-5,1.92092968712941E-5,
1.95234416882553E-5,2.37637844577599E-5,2.61487188977258E-5),
 .UNSPECIFIED.);
#25057=B_SPLINE_CURVE_WITH_KNOTS('',3,(#382670,#382671,#382672,#382673,
#382674,#382675,#382676,#382677,#382678,#382679,#382680,#382681,#382682,
#382683,#382684,#382685,#382686,#382687,#382688,#382689,#382690,#382691,
#382692,#382693,#382694,#382695,#382696,#382697,#382698,#382699,#382700),
 .UNSPECIFIED.,.F.,.F.,(4,3,3,3,3,3,3,3,3,3,4),(0.,3.95507910398186E-6,
7.53768426604201E-6,1.19904533335352E-5,1.40475043392585E-5,1.51452104275964E-5,
1.67866272814194E-5,1.69621513005358E-5,1.81338315460712E-5,1.98906334656509E-5,
2.06132424588244E-5),.UNSPECIFIED.);
#25058=B_SPLINE_CURVE_WITH_KNOTS('',3,(#382703,#382704,#382705,#382706),
 .UNSPECIFIED.,.F.,.F.,(4,4),(9.69739903612216E-19,0.00010938435327491),
 .UNSPECIFIED.);
#25059=B_SPLINE_CURVE_WITH_KNOTS('',3,(#382733,#382734,#382735,#382736,
#382737,#382738,#382739,#382740,#382741,#382742,#382743,#382744,#382745,
#382746,#382747,#382748,#382749,#382750,#382751,#382752,#382753,#382754,
#382755,#382756,#382757,#382758,#382759,#382760,#382761,#382762,#382763,
#382764,#382765,#382766),.UNSPECIFIED.,.F.,.F.,(4,3,3,3,3,3,3,3,3,3,3,4),
(0.,2.09623992729434E-6,3.17176647120218E-6,4.82636181943681E-6,5.0100091733997E-6,
6.13126454147484E-6,8.60486650288858E-6,9.21144281170488E-6,1.24722301135974E-5,
1.42666454787854E-5,2.04670653756692E-5,2.08026438176798E-5),
 .UNSPECIFIED.);
#25060=B_SPLINE_CURVE_WITH_KNOTS('',3,(#382767,#382768,#382769,#382770),
 .UNSPECIFIED.,.F.,.F.,(4,4),(0.,0.000109384345496908),.UNSPECIFIED.);
#25061=B_SPLINE_CURVE_WITH_KNOTS('',3,(#382875,#382876,#382877,#382878),
 .UNSPECIFIED.,.F.,.F.,(4,4),(0.,9.54361881492176E-5),.UNSPECIFIED.);
#25062=B_SPLINE_CURVE_WITH_KNOTS('',3,(#382883,#382884,#382885,#382886,
#382887,#382888,#382889),.UNSPECIFIED.,.F.,.F.,(4,3,4),(0.,4.41069704323469E-5,
0.000113970027818833),.UNSPECIFIED.);
#25063=B_SPLINE_CURVE_WITH_KNOTS('',3,(#382895,#382896,#382897,#382898),
 .UNSPECIFIED.,.F.,.F.,(4,4),(4.33680868994202E-19,9.54361881492181E-5),
 .UNSPECIFIED.);
#25064=B_SPLINE_CURVE_WITH_KNOTS('',3,(#382902,#382903,#382904,#382905,
#382906,#382907,#382908),.UNSPECIFIED.,.F.,.F.,(4,3,4),(0.,6.98630244191488E-5,
0.000113969974038089),.UNSPECIFIED.);
#25065=B_SPLINE_CURVE_WITH_KNOTS('',3,(#382911,#382912,#382913,#382914,
#382915,#382916,#382917,#382918,#382919,#382920,#382921,#382922,#382923,
#382924,#382925,#382926,#382927,#382928,#382929,#382930,#382931,#382932,
#382933,#382934,#382935,#382936,#382937,#382938,#382939,#382940,#382941,
#382942,#382943,#382944,#382945,#382946,#382947,#382948,#382949,#382950,
#382951,#382952,#382953,#382954,#382955,#382956,#382957,#382958,#382959),
 .UNSPECIFIED.,.F.,.F.,(4,3,3,3,3,3,3,3,3,3,3,3,3,3,3,3,4),(0.,1.53100299373429E-6,
4.52554775678867E-6,7.01151246291612E-6,9.26752933799565E-6,1.03084066197174E-5,
1.1713899082686E-5,1.22284894984071E-5,1.30315035324816E-5,1.38363728497813E-5,
1.40464197777496E-5,1.5459774956464E-5,1.62073588704069E-5,1.9209296871261E-5,
1.95234416882556E-5,2.37637844577607E-5,2.61487188977264E-5),
 .UNSPECIFIED.);
#25066=B_SPLINE_CURVE_WITH_KNOTS('',3,(#382974,#382975,#382976,#382977,
#382978,#382979,#382980,#382981,#382982,#382983,#382984,#382985,#382986,
#382987,#382988,#382989,#382990,#382991,#382992,#382993,#382994,#382995,
#382996,#382997,#382998,#382999,#383000,#383001,#383002,#383003,#383004),
 .UNSPECIFIED.,.F.,.F.,(4,3,3,3,3,3,3,3,3,3,4),(0.,3.95507910397189E-6,
7.53768426604198E-6,1.19904533335351E-5,1.40475043392586E-5,1.51452104275963E-5,
1.67866272814151E-5,1.69621513005357E-5,1.8133831546071E-5,1.98906334656561E-5,
2.06132424588244E-5),.UNSPECIFIED.);
#25067=B_SPLINE_CURVE_WITH_KNOTS('',3,(#383007,#383008,#383009,#383010),
 .UNSPECIFIED.,.F.,.F.,(4,4),(4.33680868994202E-19,0.00010938435327491),
 .UNSPECIFIED.);
#25068=B_SPLINE_CURVE_WITH_KNOTS('',3,(#383037,#383038,#383039,#383040,
#383041,#383042,#383043,#383044,#383045,#383046,#383047,#383048,#383049,
#383050,#383051,#383052,#383053,#383054,#383055,#383056,#383057,#383058,
#383059,#383060,#383061,#383062,#383063,#383064,#383065,#383066,#383067,
#383068,#383069,#383070),.UNSPECIFIED.,.F.,.F.,(4,3,3,3,3,3,3,3,3,3,3,4),
(2.16840434497101E-19,2.09623992729412E-6,3.17176647120213E-6,4.82636181943927E-6,
5.01000917339946E-6,6.13126454147475E-6,8.60486650288808E-6,9.21144281170435E-6,
1.24722301135917E-5,1.42666454787843E-5,2.04670653757219E-5,2.08026438176781E-5),
 .UNSPECIFIED.);
#25069=B_SPLINE_CURVE_WITH_KNOTS('',3,(#383071,#383072,#383073,#383074),
 .UNSPECIFIED.,.F.,.F.,(4,4),(0.,0.000109384345496908),.UNSPECIFIED.);
#25070=B_SPLINE_CURVE_WITH_KNOTS('',3,(#383179,#383180,#383181,#383182),
 .UNSPECIFIED.,.F.,.F.,(4,4),(0.,9.54361881492176E-5),.UNSPECIFIED.);
#25071=B_SPLINE_CURVE_WITH_KNOTS('',3,(#383187,#383188,#383189,#383190,
#383191,#383192,#383193),.UNSPECIFIED.,.F.,.F.,(4,3,4),(0.,4.4106970432347E-5,
0.000113970027818833),.UNSPECIFIED.);
#25072=B_SPLINE_CURVE_WITH_KNOTS('',3,(#383199,#383200,#383201,#383202),
 .UNSPECIFIED.,.F.,.F.,(4,4),(4.33680868994202E-19,9.5436188149218E-5),
 .UNSPECIFIED.);
#25073=B_SPLINE_CURVE_WITH_KNOTS('',3,(#383206,#383207,#383208,#383209,
#383210,#383211,#383212),.UNSPECIFIED.,.F.,.F.,(4,3,4),(0.,6.98630244191492E-5,
0.000113969974038089),.UNSPECIFIED.);
#25074=B_SPLINE_CURVE_WITH_KNOTS('',3,(#383215,#383216,#383217,#383218,
#383219,#383220,#383221,#383222,#383223,#383224,#383225,#383226,#383227,
#383228,#383229,#383230,#383231,#383232,#383233,#383234,#383235,#383236,
#383237,#383238,#383239,#383240,#383241,#383242,#383243,#383244,#383245,
#383246,#383247,#383248,#383249,#383250,#383251,#383252,#383253,#383254,
#383255,#383256,#383257,#383258,#383259,#383260,#383261,#383262,#383263),
 .UNSPECIFIED.,.F.,.F.,(4,3,3,3,3,3,3,3,3,3,3,3,3,3,3,3,4),(0.,1.53100299373403E-6,
4.5255477567934E-6,7.01151246291602E-6,9.26752933800128E-6,1.03084066197172E-5,
1.17138990826861E-5,1.22284894984074E-5,1.30315035324817E-5,1.3836372849781E-5,
1.40464197777492E-5,1.54597749564639E-5,1.62073588704066E-5,1.92092968712801E-5,
1.95234416882552E-5,2.37637844577568E-5,2.61487188977257E-5),
 .UNSPECIFIED.);
#25075=B_SPLINE_CURVE_WITH_KNOTS('',3,(#383278,#383279,#383280,#383281,
#383282,#383283,#383284,#383285,#383286,#383287,#383288,#383289,#383290,
#383291,#383292,#383293,#383294,#383295,#383296,#383297,#383298,#383299,
#383300,#383301,#383302,#383303,#383304,#383305,#383306,#383307,#383308),
 .UNSPECIFIED.,.F.,.F.,(4,3,3,3,3,3,3,3,3,3,4),(0.,3.95507910397134E-6,
7.53768426604187E-6,1.19904533335349E-5,1.40475043392585E-5,1.51452104275965E-5,
1.67866272814129E-5,1.69621513005357E-5,1.81338315460711E-5,1.98906334656565E-5,
2.06132424588243E-5),.UNSPECIFIED.);
#25076=B_SPLINE_CURVE_WITH_KNOTS('',3,(#383311,#383312,#383313,#383314),
 .UNSPECIFIED.,.F.,.F.,(4,4),(9.69739903612216E-19,0.00010938435327491),
 .UNSPECIFIED.);
#25077=B_SPLINE_CURVE_WITH_KNOTS('',3,(#383341,#383342,#383343,#383344,
#383345,#383346,#383347,#383348,#383349,#383350,#383351,#383352,#383353,
#383354,#383355,#383356,#383357,#383358,#383359,#383360,#383361,#383362,
#383363,#383364,#383365,#383366,#383367,#383368,#383369,#383370,#383371,
#383372,#383373,#383374),.UNSPECIFIED.,.F.,.F.,(4,3,3,3,3,3,3,3,3,3,3,4),
(0.,2.09623992729436E-6,3.17176647120223E-6,4.82636181942795E-6,5.01000917339974E-6,
6.13126454147501E-6,8.60486650288861E-6,9.21144281170489E-6,1.24722301136162E-5,
1.42666454787854E-5,2.04670653756897E-5,2.08026438176798E-5),
 .UNSPECIFIED.);
#25078=B_SPLINE_CURVE_WITH_KNOTS('',3,(#383375,#383376,#383377,#383378),
 .UNSPECIFIED.,.F.,.F.,(4,4),(0.,0.000109384345496908),.UNSPECIFIED.);
#25079=B_SPLINE_CURVE_WITH_KNOTS('',3,(#383483,#383484,#383485,#383486),
 .UNSPECIFIED.,.F.,.F.,(4,4),(0.,9.54361881492176E-5),.UNSPECIFIED.);
#25080=B_SPLINE_CURVE_WITH_KNOTS('',3,(#383491,#383492,#383493,#383494,
#383495,#383496,#383497),.UNSPECIFIED.,.F.,.F.,(4,3,4),(0.,4.41069704323469E-5,
0.000113970027818833),.UNSPECIFIED.);
#25081=B_SPLINE_CURVE_WITH_KNOTS('',3,(#383503,#383504,#383505,#383506),
 .UNSPECIFIED.,.F.,.F.,(4,4),(4.33680868994202E-19,9.54361881492174E-5),
 .UNSPECIFIED.);
#25082=B_SPLINE_CURVE_WITH_KNOTS('',3,(#383510,#383511,#383512,#383513,
#383514,#383515,#383516),.UNSPECIFIED.,.F.,.F.,(4,3,4),(0.,6.98630244191489E-5,
0.000113969974038089),.UNSPECIFIED.);
#25083=B_SPLINE_CURVE_WITH_KNOTS('',3,(#383519,#383520,#383521,#383522,
#383523,#383524,#383525,#383526,#383527,#383528,#383529,#383530,#383531,
#383532,#383533,#383534,#383535,#383536,#383537,#383538,#383539,#383540,
#383541,#383542,#383543,#383544,#383545,#383546,#383547,#383548,#383549,
#383550,#383551,#383552,#383553,#383554,#383555,#383556,#383557,#383558,
#383559,#383560,#383561,#383562,#383563,#383564,#383565,#383566,#383567),
 .UNSPECIFIED.,.F.,.F.,(4,3,3,3,3,3,3,3,3,3,3,3,3,3,3,3,4),(0.,1.5310029937343E-6,
4.52554775679482E-6,7.01151246291627E-6,9.26752933801453E-6,1.03084066197174E-5,
1.17138990826864E-5,1.22284894984078E-5,1.30315035324817E-5,1.38363728497815E-5,
1.40464197777497E-5,1.5459774956464E-5,1.6207358870407E-5,1.92092968713133E-5,
1.95234416882558E-5,2.37637844577604E-5,2.61487188977267E-5),
 .UNSPECIFIED.);
#25084=B_SPLINE_CURVE_WITH_KNOTS('',3,(#383582,#383583,#383584,#383585,
#383586,#383587,#383588,#383589,#383590,#383591,#383592,#383593,#383594,
#383595,#383596,#383597,#383598,#383599,#383600,#383601,#383602,#383603,
#383604,#383605,#383606,#383607,#383608,#383609,#383610,#383611,#383612),
 .UNSPECIFIED.,.F.,.F.,(4,3,3,3,3,3,3,3,3,3,4),(0.,3.95507910397896E-6,
7.53768426604197E-6,1.1990453333535E-5,1.40475043392585E-5,1.51452104275964E-5,
1.67866272814317E-5,1.69621513005359E-5,1.81338315460711E-5,1.9890633465653E-5,
2.06132424588247E-5),.UNSPECIFIED.);
#25085=B_SPLINE_CURVE_WITH_KNOTS('',3,(#383615,#383616,#383617,#383618),
 .UNSPECIFIED.,.F.,.F.,(4,4),(4.33680868994202E-19,0.00010938435327491),
 .UNSPECIFIED.);
#25086=B_SPLINE_CURVE_WITH_KNOTS('',3,(#383645,#383646,#383647,#383648,
#383649,#383650,#383651,#383652,#383653,#383654,#383655,#383656,#383657,
#383658,#383659,#383660,#383661,#383662,#383663,#383664,#383665,#383666,
#383667,#383668,#383669,#383670,#383671,#383672,#383673,#383674,#383675,
#383676,#383677,#383678),.UNSPECIFIED.,.F.,.F.,(4,3,3,3,3,3,3,3,3,3,3,4),
(2.16840434497101E-19,2.09623992729433E-6,3.17176647120203E-6,4.8263618194373E-6,
5.01000917339969E-6,6.13126454147473E-6,8.60486650288812E-6,9.21144281170456E-6,
1.24722301136098E-5,1.42666454787845E-5,2.04670653756581E-5,2.08026438176784E-5),
 .UNSPECIFIED.);
#25087=B_SPLINE_CURVE_WITH_KNOTS('',3,(#383679,#383680,#383681,#383682),
 .UNSPECIFIED.,.F.,.F.,(4,4),(0.,0.000109384345496908),.UNSPECIFIED.);
#25088=B_SPLINE_CURVE_WITH_KNOTS('',3,(#383787,#383788,#383789,#383790),
 .UNSPECIFIED.,.F.,.F.,(4,4),(0.,9.54361881492175E-5),.UNSPECIFIED.);
#25089=B_SPLINE_CURVE_WITH_KNOTS('',3,(#383795,#383796,#383797,#383798,
#383799,#383800,#383801),.UNSPECIFIED.,.F.,.F.,(4,3,4),(0.,4.4106970432347E-5,
0.000113970027818833),.UNSPECIFIED.);
#25090=B_SPLINE_CURVE_WITH_KNOTS('',3,(#383807,#383808,#383809,#383810),
 .UNSPECIFIED.,.F.,.F.,(4,4),(4.33680868994202E-19,9.54361881492178E-5),
 .UNSPECIFIED.);
#25091=B_SPLINE_CURVE_WITH_KNOTS('',3,(#383814,#383815,#383816,#383817,
#383818,#383819,#383820),.UNSPECIFIED.,.F.,.F.,(4,3,4),(0.,6.98630244191491E-5,
0.000113969974038089),.UNSPECIFIED.);
#25092=B_SPLINE_CURVE_WITH_KNOTS('',3,(#383823,#383824,#383825,#383826,
#383827,#383828,#383829,#383830,#383831,#383832,#383833,#383834,#383835,
#383836,#383837,#383838,#383839,#383840,#383841,#383842,#383843,#383844,
#383845,#383846,#383847,#383848,#383849,#383850,#383851,#383852,#383853,
#383854,#383855,#383856,#383857,#383858,#383859,#383860,#383861,#383862,
#383863,#383864,#383865,#383866,#383867,#383868,#383869,#383870,#383871),
 .UNSPECIFIED.,.F.,.F.,(4,3,3,3,3,3,3,3,3,3,3,3,3,3,3,3,4),(0.,1.53100299373408E-6,
4.52554775679743E-6,7.01151246291611E-6,9.2675293380054E-6,1.03084066197173E-5,
1.17138990826862E-5,1.22284894984075E-5,1.30315035324818E-5,1.38363728497812E-5,
1.40464197777494E-5,1.54597749564639E-5,1.6207358870407E-5,1.92092968712166E-5,
1.95234416882556E-5,2.37637844577591E-5,2.61487188977264E-5),
 .UNSPECIFIED.);
#25093=B_SPLINE_CURVE_WITH_KNOTS('',3,(#383886,#383887,#383888,#383889,
#383890,#383891,#383892,#383893,#383894,#383895,#383896,#383897,#383898,
#383899,#383900,#383901,#383902,#383903,#383904,#383905,#383906,#383907,
#383908,#383909,#383910,#383911,#383912,#383913,#383914,#383915,#383916),
 .UNSPECIFIED.,.F.,.F.,(4,3,3,3,3,3,3,3,3,3,4),(0.,3.9550791039714E-6,7.53768426604213E-6,
1.19904533335353E-5,1.40475043392588E-5,1.51452104275968E-5,1.67866272814203E-5,
1.6962151300536E-5,1.81338315460714E-5,1.98906334656568E-5,2.06132424588248E-5),
 .UNSPECIFIED.);
#25094=B_SPLINE_CURVE_WITH_KNOTS('',3,(#383919,#383920,#383921,#383922),
 .UNSPECIFIED.,.F.,.F.,(4,4),(9.93687704810078E-19,0.00010938435327491),
 .UNSPECIFIED.);
#25095=B_SPLINE_CURVE_WITH_KNOTS('',3,(#383949,#383950,#383951,#383952,
#383953,#383954,#383955,#383956,#383957,#383958,#383959,#383960,#383961,
#383962,#383963,#383964,#383965,#383966,#383967,#383968,#383969,#383970,
#383971,#383972,#383973,#383974,#383975,#383976,#383977,#383978,#383979,
#383980,#383981,#383982),.UNSPECIFIED.,.F.,.F.,(4,3,3,3,3,3,3,3,3,3,3,4),
(2.16840434497101E-19,2.09623992729456E-6,3.17176647120225E-6,4.82636181944301E-6,
5.01000917339998E-6,6.13126454147519E-6,8.60486650288873E-6,9.21144281170526E-6,
1.24722301136018E-5,1.42666454787858E-5,2.04670653756884E-5,2.08026438176806E-5),
 .UNSPECIFIED.);
#25096=B_SPLINE_CURVE_WITH_KNOTS('',3,(#383983,#383984,#383985,#383986),
 .UNSPECIFIED.,.F.,.F.,(4,4),(0.,0.000109384345496908),.UNSPECIFIED.);
#25097=B_SPLINE_CURVE_WITH_KNOTS('',3,(#384091,#384092,#384093,#384094),
 .UNSPECIFIED.,.F.,.F.,(4,4),(0.,9.54361881492173E-5),.UNSPECIFIED.);
#25098=B_SPLINE_CURVE_WITH_KNOTS('',3,(#384099,#384100,#384101,#384102,
#384103,#384104,#384105),.UNSPECIFIED.,.F.,.F.,(4,3,4),(0.,4.41069704323469E-5,
0.000113970027818833),.UNSPECIFIED.);
#25099=B_SPLINE_CURVE_WITH_KNOTS('',3,(#384111,#384112,#384113,#384114),
 .UNSPECIFIED.,.F.,.F.,(4,4),(2.16840434497101E-19,9.54361881492178E-5),
 .UNSPECIFIED.);
#25100=B_SPLINE_CURVE_WITH_KNOTS('',3,(#384118,#384119,#384120,#384121,
#384122,#384123,#384124),.UNSPECIFIED.,.F.,.F.,(4,3,4),(0.,6.98630244191491E-5,
0.000113969974038089),.UNSPECIFIED.);
#25101=B_SPLINE_CURVE_WITH_KNOTS('',3,(#384127,#384128,#384129,#384130,
#384131,#384132,#384133,#384134,#384135,#384136,#384137,#384138,#384139,
#384140,#384141,#384142,#384143,#384144,#384145,#384146,#384147,#384148,
#384149,#384150,#384151,#384152,#384153,#384154,#384155,#384156,#384157,
#384158,#384159,#384160,#384161,#384162,#384163,#384164,#384165,#384166,
#384167,#384168,#384169,#384170,#384171,#384172,#384173,#384174,#384175),
 .UNSPECIFIED.,.F.,.F.,(4,3,3,3,3,3,3,3,3,3,3,3,3,3,3,3,4),(0.,1.5310029937342E-6,
4.52554775679593E-6,7.0115124629161E-6,9.26752933800773E-6,1.03084066197173E-5,
1.1713899082686E-5,1.22284894984073E-5,1.30315035324817E-5,1.38363728497814E-5,
1.40464197777494E-5,1.54597749564636E-5,1.62073588704066E-5,1.9209296871252E-5,
1.9523441688255E-5,2.37637844577529E-5,2.61487188977248E-5),
 .UNSPECIFIED.);
#25102=B_SPLINE_CURVE_WITH_KNOTS('',3,(#384190,#384191,#384192,#384193,
#384194,#384195,#384196,#384197,#384198,#384199,#384200,#384201,#384202,
#384203,#384204,#384205,#384206,#384207,#384208,#384209,#384210,#384211,
#384212,#384213,#384214,#384215,#384216,#384217,#384218,#384219,#384220),
 .UNSPECIFIED.,.F.,.F.,(4,3,3,3,3,3,3,3,3,3,4),(0.,3.95507910398813E-6,
7.5376842660421E-6,1.19904533335351E-5,1.40475043392585E-5,1.51452104275963E-5,
1.67866272814151E-5,1.69621513005358E-5,1.81338315460713E-5,1.98906334656507E-5,
2.06132424588243E-5),.UNSPECIFIED.);
#25103=B_SPLINE_CURVE_WITH_KNOTS('',3,(#384223,#384224,#384225,#384226),
 .UNSPECIFIED.,.F.,.F.,(4,4),(9.69739903612216E-19,0.00010938435327491),
 .UNSPECIFIED.);
#25104=B_SPLINE_CURVE_WITH_KNOTS('',3,(#384253,#384254,#384255,#384256,
#384257,#384258,#384259,#384260,#384261,#384262,#384263,#384264,#384265,
#384266,#384267,#384268,#384269,#384270,#384271,#384272,#384273,#384274,
#384275,#384276,#384277,#384278,#384279,#384280,#384281,#384282,#384283,
#384284,#384285,#384286),.UNSPECIFIED.,.F.,.F.,(4,3,3,3,3,3,3,3,3,3,3,4),
(2.16840434497101E-19,2.09623992729424E-6,3.17176647120173E-6,4.82636181943504E-6,
5.01000917339928E-6,6.13126454147462E-6,8.60486650288808E-6,9.2114428117044E-6,
1.24722301136036E-5,1.42666454787847E-5,2.0467065375693E-5,2.08026438176788E-5),
 .UNSPECIFIED.);
#25105=B_SPLINE_CURVE_WITH_KNOTS('',3,(#384287,#384288,#384289,#384290),
 .UNSPECIFIED.,.F.,.F.,(4,4),(0.,0.000109384345496909),.UNSPECIFIED.);
#25106=B_SPLINE_CURVE_WITH_KNOTS('',3,(#384395,#384396,#384397,#384398),
 .UNSPECIFIED.,.F.,.F.,(4,4),(0.,9.54361881492177E-5),.UNSPECIFIED.);
#25107=B_SPLINE_CURVE_WITH_KNOTS('',3,(#384403,#384404,#384405,#384406,
#384407,#384408,#384409),.UNSPECIFIED.,.F.,.F.,(4,3,4),(0.,4.4106970432347E-5,
0.000113970027818833),.UNSPECIFIED.);
#25108=B_SPLINE_CURVE_WITH_KNOTS('',3,(#384415,#384416,#384417,#384418),
 .UNSPECIFIED.,.F.,.F.,(4,4),(2.16840434497101E-19,9.54361881492179E-5),
 .UNSPECIFIED.);
#25109=B_SPLINE_CURVE_WITH_KNOTS('',3,(#384422,#384423,#384424,#384425,
#384426,#384427,#384428),.UNSPECIFIED.,.F.,.F.,(4,3,4),(0.,6.9863024419149E-5,
0.000113969974038089),.UNSPECIFIED.);
#25110=B_SPLINE_CURVE_WITH_KNOTS('',3,(#384431,#384432,#384433,#384434,
#384435,#384436,#384437,#384438,#384439,#384440,#384441,#384442,#384443,
#384444,#384445,#384446,#384447,#384448,#384449,#384450,#384451,#384452,
#384453,#384454,#384455,#384456,#384457,#384458,#384459,#384460,#384461,
#384462,#384463,#384464,#384465,#384466,#384467,#384468,#384469,#384470,
#384471,#384472,#384473,#384474,#384475,#384476,#384477,#384478,#384479),
 .UNSPECIFIED.,.F.,.F.,(4,3,3,3,3,3,3,3,3,3,3,3,3,3,3,3,4),(0.,1.53100299373407E-6,
4.52554775679964E-6,7.01151246291605E-6,9.26752933799828E-6,1.03084066197173E-5,
1.17138990826861E-5,1.22284894984075E-5,1.30315035324815E-5,1.38363728497813E-5,
1.40464197777497E-5,1.54597749564639E-5,1.62073588704066E-5,1.92092968712802E-5,
1.95234416882554E-5,2.37637844577551E-5,2.61487188977257E-5),
 .UNSPECIFIED.);
#25111=B_SPLINE_CURVE_WITH_KNOTS('',3,(#384494,#384495,#384496,#384497,
#384498,#384499,#384500,#384501,#384502,#384503,#384504,#384505,#384506,
#384507,#384508,#384509,#384510,#384511,#384512,#384513,#384514,#384515,
#384516,#384517,#384518,#384519,#384520,#384521,#384522,#384523,#384524),
 .UNSPECIFIED.,.F.,.F.,(4,3,3,3,3,3,3,3,3,3,4),(0.,3.95507910396865E-6,
7.53768426604195E-6,1.19904533335351E-5,1.40475043392586E-5,1.51452104275965E-5,
1.67866272814148E-5,1.6962151300536E-5,1.8133831546071E-5,1.98906334656545E-5,
2.06132424588246E-5),.UNSPECIFIED.);
#25112=B_SPLINE_CURVE_WITH_KNOTS('',3,(#384527,#384528,#384529,#384530),
 .UNSPECIFIED.,.F.,.F.,(4,4),(2.16840434497101E-19,0.00010938435327491),
 .UNSPECIFIED.);
#25113=B_SPLINE_CURVE_WITH_KNOTS('',3,(#384557,#384558,#384559,#384560,
#384561,#384562,#384563,#384564,#384565,#384566,#384567,#384568,#384569,
#384570,#384571,#384572,#384573,#384574,#384575,#384576,#384577,#384578,
#384579,#384580,#384581,#384582,#384583,#384584,#384585,#384586,#384587,
#384588,#384589,#384590),.UNSPECIFIED.,.F.,.F.,(4,3,3,3,3,3,3,3,3,3,3,4),
(0.,2.09623992729435E-6,3.17176647120248E-6,4.82636181943654E-6,5.01000917339974E-6,
6.131264541475E-6,8.60486650288874E-6,9.21144281170515E-6,1.24722301135883E-5,
1.4266645478786E-5,2.04670653756816E-5,2.0802643817681E-5),
 .UNSPECIFIED.);
#25114=B_SPLINE_CURVE_WITH_KNOTS('',3,(#384591,#384592,#384593,#384594),
 .UNSPECIFIED.,.F.,.F.,(4,4),(0.,0.000109384345496908),.UNSPECIFIED.);
#25115=B_SPLINE_CURVE_WITH_KNOTS('',3,(#384699,#384700,#384701,#384702),
 .UNSPECIFIED.,.F.,.F.,(4,4),(0.,9.54361881492176E-5),.UNSPECIFIED.);
#25116=B_SPLINE_CURVE_WITH_KNOTS('',3,(#384707,#384708,#384709,#384710,
#384711,#384712,#384713),.UNSPECIFIED.,.F.,.F.,(4,3,4),(0.,4.41069704323469E-5,
0.000113970027818834),.UNSPECIFIED.);
#25117=B_SPLINE_CURVE_WITH_KNOTS('',3,(#384719,#384720,#384721,#384722),
 .UNSPECIFIED.,.F.,.F.,(4,4),(2.16840434497101E-19,9.54361881492178E-5),
 .UNSPECIFIED.);
#25118=B_SPLINE_CURVE_WITH_KNOTS('',3,(#384726,#384727,#384728,#384729,
#384730,#384731,#384732),.UNSPECIFIED.,.F.,.F.,(4,3,4),(0.,6.9863024419149E-5,
0.000113969974038089),.UNSPECIFIED.);
#25119=B_SPLINE_CURVE_WITH_KNOTS('',3,(#384735,#384736,#384737,#384738,
#384739,#384740,#384741,#384742,#384743,#384744,#384745,#384746,#384747,
#384748,#384749,#384750,#384751,#384752,#384753,#384754,#384755,#384756,
#384757,#384758,#384759,#384760,#384761,#384762,#384763,#384764,#384765,
#384766,#384767,#384768,#384769,#384770,#384771,#384772,#384773,#384774,
#384775,#384776,#384777,#384778,#384779,#384780,#384781,#384782,#384783),
 .UNSPECIFIED.,.F.,.F.,(4,3,3,3,3,3,3,3,3,3,3,3,3,3,3,3,4),(0.,1.53100299373425E-6,
4.52554775679411E-6,7.01151246291613E-6,9.26752933801911E-6,1.03084066197173E-5,
1.17138990826863E-5,1.22284894984073E-5,1.30315035324819E-5,1.38363728497813E-5,
1.40464197777495E-5,1.54597749564641E-5,1.62073588704069E-5,1.920929687123E-5,
1.9523441688256E-5,2.3763784457758E-5,2.61487188977268E-5),
 .UNSPECIFIED.);
#25120=B_SPLINE_CURVE_WITH_KNOTS('',3,(#384798,#384799,#384800,#384801,
#384802,#384803,#384804,#384805,#384806,#384807,#384808,#384809,#384810,
#384811,#384812,#384813,#384814,#384815,#384816,#384817,#384818,#384819,
#384820,#384821,#384822,#384823,#384824,#384825,#384826,#384827,#384828),
 .UNSPECIFIED.,.F.,.F.,(4,3,3,3,3,3,3,3,3,3,4),(0.,3.95507910399092E-6,
7.53768426604211E-6,1.1990453333535E-5,1.40475043392589E-5,1.51452104275967E-5,
1.67866272814072E-5,1.6962151300536E-5,1.81338315460714E-5,1.98906334656527E-5,
2.06132424588247E-5),.UNSPECIFIED.);
#25121=B_SPLINE_CURVE_WITH_KNOTS('',3,(#384831,#384832,#384833,#384834),
 .UNSPECIFIED.,.F.,.F.,(4,4),(2.16840434497101E-19,0.00010938435327491),
 .UNSPECIFIED.);
#25122=B_SPLINE_CURVE_WITH_KNOTS('',3,(#384861,#384862,#384863,#384864,
#384865,#384866,#384867,#384868,#384869,#384870,#384871,#384872,#384873,
#384874,#384875,#384876,#384877,#384878,#384879,#384880,#384881,#384882,
#384883,#384884,#384885,#384886,#384887,#384888,#384889,#384890,#384891,
#384892,#384893,#384894),.UNSPECIFIED.,.F.,.F.,(4,3,3,3,3,3,3,3,3,3,3,4),
(0.,2.09623992729424E-6,3.171766471202E-6,4.82636181944403E-6,5.01000917339938E-6,
6.13126454147494E-6,8.60486650288832E-6,9.21144281170473E-6,1.24722301135726E-5,
1.42666454787854E-5,2.04670653757091E-5,2.08026438176801E-5),
 .UNSPECIFIED.);
#25123=B_SPLINE_CURVE_WITH_KNOTS('',3,(#384895,#384896,#384897,#384898),
 .UNSPECIFIED.,.F.,.F.,(4,4),(0.,0.000109384345496908),.UNSPECIFIED.);
#25124=B_SPLINE_CURVE_WITH_KNOTS('',3,(#385003,#385004,#385005,#385006),
 .UNSPECIFIED.,.F.,.F.,(4,4),(0.,9.54361881492174E-5),.UNSPECIFIED.);
#25125=B_SPLINE_CURVE_WITH_KNOTS('',3,(#385011,#385012,#385013,#385014,
#385015,#385016,#385017),.UNSPECIFIED.,.F.,.F.,(4,3,4),(0.,4.41069704323469E-5,
0.000113970027818833),.UNSPECIFIED.);
#25126=B_SPLINE_CURVE_WITH_KNOTS('',3,(#385023,#385024,#385025,#385026),
 .UNSPECIFIED.,.F.,.F.,(4,4),(2.16840434497101E-19,9.54361881492181E-5),
 .UNSPECIFIED.);
#25127=B_SPLINE_CURVE_WITH_KNOTS('',3,(#385030,#385031,#385032,#385033,
#385034,#385035,#385036),.UNSPECIFIED.,.F.,.F.,(4,3,4),(0.,6.98630244191489E-5,
0.000113969974038089),.UNSPECIFIED.);
#25128=B_SPLINE_CURVE_WITH_KNOTS('',3,(#385039,#385040,#385041,#385042,
#385043,#385044,#385045,#385046,#385047,#385048,#385049,#385050,#385051,
#385052,#385053,#385054,#385055,#385056,#385057,#385058,#385059,#385060,
#385061,#385062,#385063,#385064,#385065,#385066,#385067,#385068,#385069,
#385070,#385071,#385072,#385073,#385074,#385075,#385076,#385077,#385078,
#385079,#385080,#385081,#385082,#385083,#385084,#385085,#385086,#385087),
 .UNSPECIFIED.,.F.,.F.,(4,3,3,3,3,3,3,3,3,3,3,3,3,3,3,3,4),(0.,1.53100299373416E-6,
4.52554775679832E-6,7.01151246291608E-6,9.26752933799768E-6,1.03084066197173E-5,
1.1713899082686E-5,1.22284894984076E-5,1.30315035324819E-5,1.38363728497816E-5,
1.40464197777497E-5,1.54597749564643E-5,1.62073588704072E-5,1.9209296871267E-5,
1.95234416882563E-5,2.37637844577567E-5,2.61487188977274E-5),
 .UNSPECIFIED.);
#25129=B_SPLINE_CURVE_WITH_KNOTS('',3,(#385102,#385103,#385104,#385105,
#385106,#385107,#385108,#385109,#385110,#385111,#385112,#385113,#385114,
#385115,#385116,#385117,#385118,#385119,#385120,#385121,#385122,#385123,
#385124,#385125,#385126,#385127,#385128,#385129,#385130,#385131,#385132),
 .UNSPECIFIED.,.F.,.F.,(4,3,3,3,3,3,3,3,3,3,4),(0.,3.95507910397923E-6,
7.53768426604195E-6,1.19904533335349E-5,1.40475043392586E-5,1.51452104275964E-5,
1.67866272814122E-5,1.69621513005357E-5,1.81338315460711E-5,1.98906334656528E-5,
2.06132424588245E-5),.UNSPECIFIED.);
#25130=B_SPLINE_CURVE_WITH_KNOTS('',3,(#385135,#385136,#385137,#385138),
 .UNSPECIFIED.,.F.,.F.,(4,4),(1.06229684024259E-18,0.00010938435327491),
 .UNSPECIFIED.);
#25131=B_SPLINE_CURVE_WITH_KNOTS('',3,(#385165,#385166,#385167,#385168,
#385169,#385170,#385171,#385172,#385173,#385174,#385175,#385176,#385177,
#385178,#385179,#385180,#385181,#385182,#385183,#385184,#385185,#385186,
#385187,#385188,#385189,#385190,#385191,#385192,#385193,#385194,#385195,
#385196,#385197,#385198),.UNSPECIFIED.,.F.,.F.,(4,3,3,3,3,3,3,3,3,3,3,4),
(0.,2.09623992729422E-6,3.17176647120225E-6,4.82636181943692E-6,5.01000917339947E-6,
6.13126454147503E-6,8.6048665028885E-6,9.2114428117048E-6,1.24722301135852E-5,
1.42666454787854E-5,2.04670653756892E-5,2.080264381768E-5),
 .UNSPECIFIED.);
#25132=B_SPLINE_CURVE_WITH_KNOTS('',3,(#385199,#385200,#385201,#385202),
 .UNSPECIFIED.,.F.,.F.,(4,4),(0.,0.000109384345496908),.UNSPECIFIED.);
#25133=B_SPLINE_CURVE_WITH_KNOTS('',3,(#385307,#385308,#385309,#385310),
 .UNSPECIFIED.,.F.,.F.,(4,4),(0.,9.54361881492175E-5),.UNSPECIFIED.);
#25134=B_SPLINE_CURVE_WITH_KNOTS('',3,(#385315,#385316,#385317,#385318,
#385319,#385320,#385321),.UNSPECIFIED.,.F.,.F.,(4,3,4),(0.,4.41069704323467E-5,
0.000113970027818833),.UNSPECIFIED.);
#25135=B_SPLINE_CURVE_WITH_KNOTS('',3,(#385327,#385328,#385329,#385330),
 .UNSPECIFIED.,.F.,.F.,(4,4),(2.16840434497101E-19,9.54361881492181E-5),
 .UNSPECIFIED.);
#25136=B_SPLINE_CURVE_WITH_KNOTS('',3,(#385334,#385335,#385336,#385337,
#385338,#385339,#385340),.UNSPECIFIED.,.F.,.F.,(4,3,4),(0.,6.9863024419149E-5,
0.000113969974038089),.UNSPECIFIED.);
#25137=B_SPLINE_CURVE_WITH_KNOTS('',3,(#385343,#385344,#385345,#385346,
#385347,#385348,#385349,#385350,#385351,#385352,#385353,#385354,#385355,
#385356,#385357,#385358,#385359,#385360,#385361,#385362,#385363,#385364,
#385365,#385366,#385367,#385368,#385369,#385370,#385371,#385372,#385373,
#385374,#385375,#385376,#385377,#385378,#385379,#385380,#385381,#385382,
#385383,#385384,#385385,#385386,#385387,#385388,#385389,#385390,#385391),
 .UNSPECIFIED.,.F.,.F.,(4,3,3,3,3,3,3,3,3,3,3,3,3,3,3,3,4),(0.,1.53100299373411E-6,
4.52554775679572E-6,7.01151246291604E-6,9.26752933799538E-6,1.03084066197173E-5,
1.1713899082686E-5,1.22284894984074E-5,1.30315035324819E-5,1.3836372849781E-5,
1.40464197777494E-5,1.54597749564636E-5,1.62073588704066E-5,1.9209296871214E-5,
1.95234416882551E-5,2.37637844577601E-5,2.61487188977252E-5),
 .UNSPECIFIED.);
#25138=B_SPLINE_CURVE_WITH_KNOTS('',3,(#385406,#385407,#385408,#385409,
#385410,#385411,#385412,#385413,#385414,#385415,#385416,#385417,#385418,
#385419,#385420,#385421,#385422,#385423,#385424,#385425,#385426,#385427,
#385428,#385429,#385430,#385431,#385432,#385433,#385434,#385435,#385436),
 .UNSPECIFIED.,.F.,.F.,(4,3,3,3,3,3,3,3,3,3,4),(0.,3.95507910398871E-6,
7.53768426604198E-6,1.19904533335351E-5,1.40475043392587E-5,1.51452104275964E-5,
1.67866272814358E-5,1.6962151300536E-5,1.81338315460713E-5,1.98906334656512E-5,
2.06132424588245E-5),.UNSPECIFIED.);
#25139=B_SPLINE_CURVE_WITH_KNOTS('',3,(#385439,#385440,#385441,#385442),
 .UNSPECIFIED.,.F.,.F.,(4,4),(6.1331736667335E-19,0.00010938435327491),
 .UNSPECIFIED.);
#25140=B_SPLINE_CURVE_WITH_KNOTS('',3,(#385469,#385470,#385471,#385472,
#385473,#385474,#385475,#385476,#385477,#385478,#385479,#385480,#385481,
#385482,#385483,#385484,#385485,#385486,#385487,#385488,#385489,#385490,
#385491,#385492,#385493,#385494,#385495,#385496,#385497,#385498,#385499,
#385500,#385501,#385502),.UNSPECIFIED.,.F.,.F.,(4,3,3,3,3,3,3,3,3,3,3,4),
(2.16840434497101E-19,2.09623992729438E-6,3.17176647120237E-6,4.82636181943731E-6,
5.01000917339986E-6,6.13126454147497E-6,8.60486650288864E-6,9.21144281170504E-6,
1.24722301135917E-5,1.42666454787861E-5,2.04670653756963E-5,2.08026438176811E-5),
 .UNSPECIFIED.);
#25141=B_SPLINE_CURVE_WITH_KNOTS('',3,(#385503,#385504,#385505,#385506),
 .UNSPECIFIED.,.F.,.F.,(4,4),(0.,0.000109384345496908),.UNSPECIFIED.);
#25142=B_SPLINE_CURVE_WITH_KNOTS('',3,(#385611,#385612,#385613,#385614),
 .UNSPECIFIED.,.F.,.F.,(4,4),(0.,9.54361881492172E-5),.UNSPECIFIED.);
#25143=B_SPLINE_CURVE_WITH_KNOTS('',3,(#385619,#385620,#385621,#385622,
#385623,#385624,#385625),.UNSPECIFIED.,.F.,.F.,(4,3,4),(0.,4.41069704323469E-5,
0.000113970027818833),.UNSPECIFIED.);
#25144=B_SPLINE_CURVE_WITH_KNOTS('',3,(#385631,#385632,#385633,#385634),
 .UNSPECIFIED.,.F.,.F.,(4,4),(2.16840434497101E-19,9.54361881492179E-5),
 .UNSPECIFIED.);
#25145=B_SPLINE_CURVE_WITH_KNOTS('',3,(#385638,#385639,#385640,#385641,
#385642,#385643,#385644),.UNSPECIFIED.,.F.,.F.,(4,3,4),(0.,6.9863024419149E-5,
0.000113969974038089),.UNSPECIFIED.);
#25146=B_SPLINE_CURVE_WITH_KNOTS('',3,(#385647,#385648,#385649,#385650,
#385651,#385652,#385653,#385654,#385655,#385656,#385657,#385658,#385659,
#385660,#385661,#385662,#385663,#385664,#385665,#385666,#385667,#385668,
#385669,#385670,#385671,#385672,#385673,#385674,#385675,#385676,#385677,
#385678,#385679,#385680,#385681,#385682,#385683,#385684,#385685,#385686,
#385687,#385688,#385689,#385690,#385691,#385692,#385693,#385694,#385695),
 .UNSPECIFIED.,.F.,.F.,(4,3,3,3,3,3,3,3,3,3,3,3,3,3,3,3,4),(0.,1.53100299373413E-6,
4.52554775679023E-6,7.01151246291602E-6,9.26752933801105E-6,1.03084066197174E-5,
1.17138990826861E-5,1.22284894984072E-5,1.30315035324816E-5,1.38363728497811E-5,
1.40464197777495E-5,1.54597749564638E-5,1.62073588704065E-5,1.92092968712831E-5,
1.95234416882549E-5,2.37637844577551E-5,2.61487188977251E-5),
 .UNSPECIFIED.);
#25147=B_SPLINE_CURVE_WITH_KNOTS('',3,(#385710,#385711,#385712,#385713,
#385714,#385715,#385716,#385717,#385718,#385719,#385720,#385721,#385722,
#385723,#385724,#385725,#385726,#385727,#385728,#385729,#385730,#385731,
#385732,#385733,#385734,#385735,#385736,#385737,#385738,#385739,#385740),
 .UNSPECIFIED.,.F.,.F.,(4,3,3,3,3,3,3,3,3,3,4),(0.,3.95507910397591E-6,
7.53768426604203E-6,1.19904533335351E-5,1.40475043392586E-5,1.51452104275964E-5,
1.67866272814308E-5,1.69621513005358E-5,1.81338315460711E-5,1.98906334656559E-5,
2.06132424588246E-5),.UNSPECIFIED.);
#25148=B_SPLINE_CURVE_WITH_KNOTS('',3,(#385743,#385744,#385745,#385746),
 .UNSPECIFIED.,.F.,.F.,(4,4),(6.1331736667335E-19,0.00010938435327491),
 .UNSPECIFIED.);
#25149=B_SPLINE_CURVE_WITH_KNOTS('',3,(#385773,#385774,#385775,#385776,
#385777,#385778,#385779,#385780,#385781,#385782,#385783,#385784,#385785,
#385786,#385787,#385788,#385789,#385790,#385791,#385792,#385793,#385794,
#385795,#385796,#385797,#385798,#385799,#385800,#385801,#385802,#385803,
#385804,#385805,#385806),.UNSPECIFIED.,.F.,.F.,(4,3,3,3,3,3,3,3,3,3,3,4),
(0.,2.09623992729445E-6,3.17176647120217E-6,4.82636181944129E-6,5.01000917339974E-6,
6.13126454147491E-6,8.60486650288863E-6,9.21144281170486E-6,1.24722301136039E-5,
1.42666454787853E-5,2.0467065375687E-5,2.08026438176795E-5),
 .UNSPECIFIED.);
#25150=B_SPLINE_CURVE_WITH_KNOTS('',3,(#385807,#385808,#385809,#385810),
 .UNSPECIFIED.,.F.,.F.,(4,4),(0.,0.000109384345496908),.UNSPECIFIED.);
#25151=B_SPLINE_CURVE_WITH_KNOTS('',3,(#385915,#385916,#385917,#385918),
 .UNSPECIFIED.,.F.,.F.,(4,4),(0.,9.54361881492176E-5),.UNSPECIFIED.);
#25152=B_SPLINE_CURVE_WITH_KNOTS('',3,(#385923,#385924,#385925,#385926,
#385927,#385928,#385929),.UNSPECIFIED.,.F.,.F.,(4,3,4),(0.,4.41069704323467E-5,
0.000113970027818833),.UNSPECIFIED.);
#25153=B_SPLINE_CURVE_WITH_KNOTS('',3,(#385935,#385936,#385937,#385938),
 .UNSPECIFIED.,.F.,.F.,(4,4),(4.84869951806108E-19,9.54361881492178E-5),
 .UNSPECIFIED.);
#25154=B_SPLINE_CURVE_WITH_KNOTS('',3,(#385942,#385943,#385944,#385945,
#385946,#385947,#385948),.UNSPECIFIED.,.F.,.F.,(4,3,4),(0.,6.9863024419149E-5,
0.000113969974038089),.UNSPECIFIED.);
#25155=B_SPLINE_CURVE_WITH_KNOTS('',3,(#385951,#385952,#385953,#385954,
#385955,#385956,#385957,#385958,#385959,#385960,#385961,#385962,#385963,
#385964,#385965,#385966,#385967,#385968,#385969,#385970,#385971,#385972,
#385973,#385974,#385975,#385976,#385977,#385978,#385979,#385980,#385981,
#385982,#385983,#385984,#385985,#385986,#385987,#385988,#385989,#385990,
#385991,#385992,#385993,#385994,#385995,#385996,#385997,#385998,#385999),
 .UNSPECIFIED.,.F.,.F.,(4,3,3,3,3,3,3,3,3,3,3,3,3,3,3,3,4),(0.,1.53100299373415E-6,
4.52554775680005E-6,7.01151246291607E-6,9.26752933800049E-6,1.03084066197174E-5,
1.17138990826862E-5,1.22284894984074E-5,1.30315035324819E-5,1.38363728497813E-5,
1.40464197777493E-5,1.5459774956464E-5,1.6207358870407E-5,1.92092968712743E-5,
1.95234416882557E-5,2.3763784457763E-5,2.61487188977264E-5),
 .UNSPECIFIED.);
#25156=B_SPLINE_CURVE_WITH_KNOTS('',3,(#386014,#386015,#386016,#386017,
#386018,#386019,#386020,#386021,#386022,#386023,#386024,#386025,#386026,
#386027,#386028,#386029,#386030,#386031,#386032,#386033,#386034,#386035,
#386036,#386037,#386038,#386039,#386040,#386041,#386042,#386043,#386044),
 .UNSPECIFIED.,.F.,.F.,(4,3,3,3,3,3,3,3,3,3,4),(0.,3.95507910398088E-6,
7.53768426604196E-6,1.1990453333535E-5,1.40475043392586E-5,1.51452104275965E-5,
1.6786627281432E-5,1.69621513005358E-5,1.81338315460712E-5,1.98906334656528E-5,
2.06132424588243E-5),.UNSPECIFIED.);
#25157=B_SPLINE_CURVE_WITH_KNOTS('',3,(#386047,#386048,#386049,#386050),
 .UNSPECIFIED.,.F.,.F.,(4,4),(4.84869951806108E-19,0.00010938435327491),
 .UNSPECIFIED.);
#25158=B_SPLINE_CURVE_WITH_KNOTS('',3,(#386077,#386078,#386079,#386080,
#386081,#386082,#386083,#386084,#386085,#386086,#386087,#386088,#386089,
#386090,#386091,#386092,#386093,#386094,#386095,#386096,#386097,#386098,
#386099,#386100,#386101,#386102,#386103,#386104,#386105,#386106,#386107,
#386108,#386109,#386110),.UNSPECIFIED.,.F.,.F.,(4,3,3,3,3,3,3,3,3,3,3,4),
(1.0842021724855E-19,2.0962399272944E-6,3.17176647120221E-6,4.82636181943783E-6,
5.01000917339964E-6,6.13126454147497E-6,8.60486650288854E-6,9.2114428117049E-6,
1.24722301135937E-5,1.42666454787856E-5,2.046706537569E-5,2.08026438176804E-5),
 .UNSPECIFIED.);
#25159=B_SPLINE_CURVE_WITH_KNOTS('',3,(#386111,#386112,#386113,#386114),
 .UNSPECIFIED.,.F.,.F.,(4,4),(0.,0.000109384345496908),.UNSPECIFIED.);
#25160=B_SPLINE_CURVE_WITH_KNOTS('',3,(#386219,#386220,#386221,#386222),
 .UNSPECIFIED.,.F.,.F.,(4,4),(0.,9.54361881492172E-5),.UNSPECIFIED.);
#25161=B_SPLINE_CURVE_WITH_KNOTS('',3,(#386227,#386228,#386229,#386230,
#386231,#386232,#386233),.UNSPECIFIED.,.F.,.F.,(4,3,4),(0.,4.4106970432347E-5,
0.000113970027818833),.UNSPECIFIED.);
#25162=B_SPLINE_CURVE_WITH_KNOTS('',3,(#386239,#386240,#386241,#386242),
 .UNSPECIFIED.,.F.,.F.,(4,4),(2.16840434497101E-19,9.54361881492179E-5),
 .UNSPECIFIED.);
#25163=B_SPLINE_CURVE_WITH_KNOTS('',3,(#386246,#386247,#386248,#386249,
#386250,#386251,#386252),.UNSPECIFIED.,.F.,.F.,(4,3,4),(0.,6.98630244191491E-5,
0.000113969974038089),.UNSPECIFIED.);
#25164=B_SPLINE_CURVE_WITH_KNOTS('',3,(#386255,#386256,#386257,#386258,
#386259,#386260,#386261,#386262,#386263,#386264,#386265,#386266,#386267,
#386268,#386269,#386270,#386271,#386272,#386273,#386274,#386275,#386276,
#386277,#386278,#386279,#386280,#386281,#386282,#386283,#386284,#386285,
#386286,#386287,#386288,#386289,#386290,#386291,#386292,#386293,#386294,
#386295,#386296,#386297,#386298,#386299,#386300,#386301,#386302,#386303),
 .UNSPECIFIED.,.F.,.F.,(4,3,3,3,3,3,3,3,3,3,3,3,3,3,3,3,4),(0.,1.53100299373414E-6,
4.52554775678893E-6,7.01151246291594E-6,9.26752933800309E-6,1.03084066197173E-5,
1.17138990826862E-5,1.22284894984075E-5,1.30315035324817E-5,1.38363728497811E-5,
1.40464197777493E-5,1.54597749564637E-5,1.62073588704067E-5,1.92092968712795E-5,
1.95234416882552E-5,2.37637844577611E-5,2.61487188977259E-5),
 .UNSPECIFIED.);
#25165=B_SPLINE_CURVE_WITH_KNOTS('',3,(#386318,#386319,#386320,#386321,
#386322,#386323,#386324,#386325,#386326,#386327,#386328,#386329,#386330,
#386331,#386332,#386333,#386334,#386335,#386336,#386337,#386338,#386339,
#386340,#386341,#386342,#386343,#386344,#386345,#386346,#386347,#386348),
 .UNSPECIFIED.,.F.,.F.,(4,3,3,3,3,3,3,3,3,3,4),(0.,3.95507910398021E-6,
7.53768426604196E-6,1.1990453333535E-5,1.40475043392586E-5,1.51452104275966E-5,
1.67866272814092E-5,1.6962151300536E-5,1.81338315460713E-5,1.98906334656543E-5,
2.06132424588247E-5),.UNSPECIFIED.);
#25166=B_SPLINE_CURVE_WITH_KNOTS('',3,(#386351,#386352,#386353,#386354),
 .UNSPECIFIED.,.F.,.F.,(4,4),(5.42101086242752E-19,0.00010938435327491),
 .UNSPECIFIED.);
#25167=B_SPLINE_CURVE_WITH_KNOTS('',3,(#386381,#386382,#386383,#386384,
#386385,#386386,#386387,#386388,#386389,#386390,#386391,#386392,#386393,
#386394,#386395,#386396,#386397,#386398,#386399,#386400,#386401,#386402,
#386403,#386404,#386405,#386406,#386407,#386408,#386409,#386410,#386411,
#386412,#386413,#386414),.UNSPECIFIED.,.F.,.F.,(4,3,3,3,3,3,3,3,3,3,3,4),
(1.0842021724855E-19,2.09623992729453E-6,3.17176647120237E-6,4.82636181943783E-6,
5.0100091733997E-6,6.13126454147507E-6,8.60486650288873E-6,9.21144281170509E-6,
1.2472230113601E-5,1.42666454787859E-5,2.04670653757014E-5,2.08026438176806E-5),
 .UNSPECIFIED.);
#25168=B_SPLINE_CURVE_WITH_KNOTS('',3,(#386415,#386416,#386417,#386418),
 .UNSPECIFIED.,.F.,.F.,(4,4),(0.,0.000109384345496908),.UNSPECIFIED.);
#25169=B_SPLINE_CURVE_WITH_KNOTS('',3,(#386523,#386524,#386525,#386526),
 .UNSPECIFIED.,.F.,.F.,(4,4),(0.,9.54361881492174E-5),.UNSPECIFIED.);
#25170=B_SPLINE_CURVE_WITH_KNOTS('',3,(#386531,#386532,#386533,#386534,
#386535,#386536,#386537),.UNSPECIFIED.,.F.,.F.,(4,3,4),(0.,4.41069704323469E-5,
0.000113970027818833),.UNSPECIFIED.);
#25171=B_SPLINE_CURVE_WITH_KNOTS('',3,(#386543,#386544,#386545,#386546),
 .UNSPECIFIED.,.F.,.F.,(4,4),(4.84869951806108E-19,9.54361881492178E-5),
 .UNSPECIFIED.);
#25172=B_SPLINE_CURVE_WITH_KNOTS('',3,(#386550,#386551,#386552,#386553,
#386554,#386555,#386556),.UNSPECIFIED.,.F.,.F.,(4,3,4),(0.,6.98630244191491E-5,
0.000113969974038089),.UNSPECIFIED.);
#25173=B_SPLINE_CURVE_WITH_KNOTS('',3,(#386559,#386560,#386561,#386562,
#386563,#386564,#386565,#386566,#386567,#386568,#386569,#386570,#386571,
#386572,#386573,#386574,#386575,#386576,#386577,#386578,#386579,#386580,
#386581,#386582,#386583,#386584,#386585,#386586,#386587,#386588,#386589,
#386590,#386591,#386592,#386593,#386594,#386595,#386596,#386597,#386598,
#386599,#386600,#386601,#386602,#386603,#386604,#386605,#386606,#386607),
 .UNSPECIFIED.,.F.,.F.,(4,3,3,3,3,3,3,3,3,3,3,3,3,3,3,3,4),(0.,1.53100299373411E-6,
4.52554775679701E-6,7.01151246291601E-6,9.26752933800774E-6,1.03084066197173E-5,
1.17138990826861E-5,1.22284894984073E-5,1.30315035324816E-5,1.38363728497812E-5,
1.40464197777494E-5,1.54597749564639E-5,1.62073588704066E-5,1.9209296871257E-5,
1.9523441688255E-5,2.37637844577588E-5,2.61487188977256E-5),
 .UNSPECIFIED.);
#25174=B_SPLINE_CURVE_WITH_KNOTS('',3,(#386622,#386623,#386624,#386625,
#386626,#386627,#386628,#386629,#386630,#386631,#386632,#386633,#386634,
#386635,#386636,#386637,#386638,#386639,#386640,#386641,#386642,#386643,
#386644,#386645,#386646,#386647,#386648,#386649,#386650,#386651,#386652),
 .UNSPECIFIED.,.F.,.F.,(4,3,3,3,3,3,3,3,3,3,4),(0.,3.95507910398915E-6,
7.53768426604197E-6,1.1990453333535E-5,1.40475043392585E-5,1.51452104275964E-5,
1.67866272813909E-5,1.69621513005358E-5,1.81338315460713E-5,1.98906334656509E-5,
2.06132424588247E-5),.UNSPECIFIED.);
#25175=B_SPLINE_CURVE_WITH_KNOTS('',3,(#386655,#386656,#386657,#386658),
 .UNSPECIFIED.,.F.,.F.,(4,4),(5.42101086242752E-19,0.00010938435327491),
 .UNSPECIFIED.);
#25176=B_SPLINE_CURVE_WITH_KNOTS('',3,(#386685,#386686,#386687,#386688,
#386689,#386690,#386691,#386692,#386693,#386694,#386695,#386696,#386697,
#386698,#386699,#386700,#386701,#386702,#386703,#386704,#386705,#386706,
#386707,#386708,#386709,#386710,#386711,#386712,#386713,#386714,#386715,
#386716,#386717,#386718),.UNSPECIFIED.,.F.,.F.,(4,3,3,3,3,3,3,3,3,3,3,4),
(1.0842021724855E-19,2.09623992729424E-6,3.17176647120218E-6,4.82636181943516E-6,
5.01000917339966E-6,6.13126454147493E-6,8.60486650288855E-6,9.21144281170494E-6,
1.24722301135922E-5,1.42666454787859E-5,2.04670653757106E-5,2.08026438176806E-5),
 .UNSPECIFIED.);
#25177=B_SPLINE_CURVE_WITH_KNOTS('',3,(#386719,#386720,#386721,#386722),
 .UNSPECIFIED.,.F.,.F.,(4,4),(0.,0.000109384345496908),.UNSPECIFIED.);
#25178=B_SPLINE_CURVE_WITH_KNOTS('',3,(#386827,#386828,#386829,#386830),
 .UNSPECIFIED.,.F.,.F.,(4,4),(0.,9.54361881492175E-5),.UNSPECIFIED.);
#25179=B_SPLINE_CURVE_WITH_KNOTS('',3,(#386835,#386836,#386837,#386838,
#386839,#386840,#386841),.UNSPECIFIED.,.F.,.F.,(4,3,4),(0.,4.4106970432347E-5,
0.000113970027818833),.UNSPECIFIED.);
#25180=B_SPLINE_CURVE_WITH_KNOTS('',3,(#386847,#386848,#386849,#386850),
 .UNSPECIFIED.,.F.,.F.,(4,4),(5.42101086242752E-20,9.54361881492179E-5),
 .UNSPECIFIED.);
#25181=B_SPLINE_CURVE_WITH_KNOTS('',3,(#386854,#386855,#386856,#386857,
#386858,#386859,#386860),.UNSPECIFIED.,.F.,.F.,(4,3,4),(0.,6.9863024419149E-5,
0.00011396997403809),.UNSPECIFIED.);
#25182=B_SPLINE_CURVE_WITH_KNOTS('',3,(#386863,#386864,#386865,#386866,
#386867,#386868,#386869,#386870,#386871,#386872,#386873,#386874,#386875,
#386876,#386877,#386878,#386879,#386880,#386881,#386882,#386883,#386884,
#386885,#386886,#386887,#386888,#386889,#386890,#386891,#386892,#386893,
#386894,#386895,#386896,#386897,#386898,#386899,#386900,#386901,#386902,
#386903,#386904,#386905,#386906,#386907,#386908,#386909,#386910,#386911),
 .UNSPECIFIED.,.F.,.F.,(4,3,3,3,3,3,3,3,3,3,3,3,3,3,3,3,4),(0.,1.53100299373402E-6,
4.5255477568009E-6,7.01151246291603E-6,9.26752933799214E-6,1.03084066197173E-5,
1.17138990826862E-5,1.22284894984075E-5,1.30315035324817E-5,1.38363728497813E-5,
1.40464197777494E-5,1.5459774956464E-5,1.62073588704069E-5,1.92092968712782E-5,
1.95234416882555E-5,2.37637844577588E-5,2.61487188977261E-5),
 .UNSPECIFIED.);
#25183=B_SPLINE_CURVE_WITH_KNOTS('',3,(#386926,#386927,#386928,#386929,
#386930,#386931,#386932,#386933,#386934,#386935,#386936,#386937,#386938,
#386939,#386940,#386941,#386942,#386943,#386944,#386945,#386946,#386947,
#386948,#386949,#386950,#386951,#386952,#386953,#386954,#386955,#386956),
 .UNSPECIFIED.,.F.,.F.,(4,3,3,3,3,3,3,3,3,3,4),(0.,3.95507910398505E-6,
7.53768426604191E-6,1.19904533335349E-5,1.40475043392584E-5,1.51452104275963E-5,
1.67866272814112E-5,1.69621513005357E-5,1.81338315460712E-5,1.98906334656516E-5,
2.06132424588245E-5),.UNSPECIFIED.);
#25184=B_SPLINE_CURVE_WITH_KNOTS('',3,(#386959,#386960,#386961,#386962),
 .UNSPECIFIED.,.F.,.F.,(4,4),(5.11417141928151E-19,0.00010938435327491),
 .UNSPECIFIED.);
#25185=B_SPLINE_CURVE_WITH_KNOTS('',3,(#386989,#386990,#386991,#386992,
#386993,#386994,#386995,#386996,#386997,#386998,#386999,#387000,#387001,
#387002,#387003,#387004,#387005,#387006,#387007,#387008,#387009,#387010,
#387011,#387012,#387013,#387014,#387015,#387016,#387017,#387018,#387019,
#387020,#387021,#387022),.UNSPECIFIED.,.F.,.F.,(4,3,3,3,3,3,3,3,3,3,3,4),
(1.0842021724855E-19,2.09623992729433E-6,3.17176647120215E-6,4.82636181943702E-6,
5.01000917339958E-6,6.13126454147485E-6,8.60486650288838E-6,9.21144281170471E-6,
1.24722301135986E-5,1.42666454787852E-5,2.0467065375669E-5,2.08026438176793E-5),
 .UNSPECIFIED.);
#25186=B_SPLINE_CURVE_WITH_KNOTS('',3,(#387023,#387024,#387025,#387026),
 .UNSPECIFIED.,.F.,.F.,(4,4),(0.,0.000109384345496908),.UNSPECIFIED.);
#25187=B_SPLINE_CURVE_WITH_KNOTS('',3,(#387131,#387132,#387133,#387134),
 .UNSPECIFIED.,.F.,.F.,(4,4),(0.,9.54361881492177E-5),.UNSPECIFIED.);
#25188=B_SPLINE_CURVE_WITH_KNOTS('',3,(#387139,#387140,#387141,#387142,
#387143,#387144,#387145),.UNSPECIFIED.,.F.,.F.,(4,3,4),(0.,4.41069704323471E-5,
0.000113970027818834),.UNSPECIFIED.);
#25189=B_SPLINE_CURVE_WITH_KNOTS('',3,(#387151,#387152,#387153,#387154),
 .UNSPECIFIED.,.F.,.F.,(4,4),(4.63171371119878E-19,9.5436188149218E-5),
 .UNSPECIFIED.);
#25190=B_SPLINE_CURVE_WITH_KNOTS('',3,(#387158,#387159,#387160,#387161,
#387162,#387163,#387164),.UNSPECIFIED.,.F.,.F.,(4,3,4),(0.,6.98630244191489E-5,
0.000113969974038089),.UNSPECIFIED.);
#25191=B_SPLINE_CURVE_WITH_KNOTS('',3,(#387167,#387168,#387169,#387170,
#387171,#387172,#387173,#387174,#387175,#387176,#387177,#387178,#387179,
#387180,#387181,#387182,#387183,#387184,#387185,#387186,#387187,#387188,
#387189,#387190,#387191,#387192,#387193,#387194,#387195,#387196,#387197,
#387198,#387199,#387200,#387201,#387202,#387203,#387204,#387205,#387206,
#387207,#387208,#387209,#387210,#387211,#387212,#387213,#387214,#387215),
 .UNSPECIFIED.,.F.,.F.,(4,3,3,3,3,3,3,3,3,3,3,3,3,3,3,3,4),(0.,1.53100299373415E-6,
4.52554775679312E-6,7.01151246291606E-6,9.26752933799493E-6,1.03084066197173E-5,
1.17138990826862E-5,1.22284894984075E-5,1.30315035324818E-5,1.38363728497814E-5,
1.40464197777495E-5,1.54597749564641E-5,1.62073588704068E-5,1.9209296871244E-5,
1.95234416882555E-5,2.37637844577537E-5,2.61487188977259E-5),
 .UNSPECIFIED.);
#25192=B_SPLINE_CURVE_WITH_KNOTS('',3,(#387230,#387231,#387232,#387233,
#387234,#387235,#387236,#387237,#387238,#387239,#387240,#387241,#387242,
#387243,#387244,#387245,#387246,#387247,#387248,#387249,#387250,#387251,
#387252,#387253,#387254,#387255,#387256,#387257,#387258,#387259,#387260),
 .UNSPECIFIED.,.F.,.F.,(4,3,3,3,3,3,3,3,3,3,4),(0.,3.95507910398497E-6,
7.53768426604194E-6,1.1990453333535E-5,1.40475043392585E-5,1.51452104275964E-5,
1.67866272814021E-5,1.69621513005358E-5,1.81338315460712E-5,1.98906334656536E-5,
2.06132424588244E-5),.UNSPECIFIED.);
#25193=B_SPLINE_CURVE_WITH_KNOTS('',3,(#387263,#387264,#387265,#387266),
 .UNSPECIFIED.,.F.,.F.,(4,4),(4.84869951806108E-19,0.00010938435327491),
 .UNSPECIFIED.);
#25194=B_SPLINE_CURVE_WITH_KNOTS('',3,(#387293,#387294,#387295,#387296,
#387297,#387298,#387299,#387300,#387301,#387302,#387303,#387304,#387305,
#387306,#387307,#387308,#387309,#387310,#387311,#387312,#387313,#387314,
#387315,#387316,#387317,#387318,#387319,#387320,#387321,#387322,#387323,
#387324,#387325,#387326),.UNSPECIFIED.,.F.,.F.,(4,3,3,3,3,3,3,3,3,3,3,4),
(1.62630325872826E-19,2.09623992729446E-6,3.17176647120217E-6,4.8263618194318E-6,
5.01000917339966E-6,6.13126454147499E-6,8.60486650288858E-6,9.21144281170497E-6,
1.24722301136006E-5,1.42666454787858E-5,2.04670653756983E-5,2.08026438176805E-5),
 .UNSPECIFIED.);
#25195=B_SPLINE_CURVE_WITH_KNOTS('',3,(#387327,#387328,#387329,#387330),
 .UNSPECIFIED.,.F.,.F.,(4,4),(0.,0.000109384345496908),.UNSPECIFIED.);
#25196=B_SPLINE_CURVE_WITH_KNOTS('',3,(#387435,#387436,#387437,#387438),
 .UNSPECIFIED.,.F.,.F.,(4,4),(0.,9.54361881492175E-5),.UNSPECIFIED.);
#25197=B_SPLINE_CURVE_WITH_KNOTS('',3,(#387443,#387444,#387445,#387446,
#387447,#387448,#387449),.UNSPECIFIED.,.F.,.F.,(4,3,4),(0.,4.41069704323468E-5,
0.000113970027818834),.UNSPECIFIED.);
#25198=B_SPLINE_CURVE_WITH_KNOTS('',3,(#387455,#387456,#387457,#387458),
 .UNSPECIFIED.,.F.,.F.,(4,4),(4.5436350575631E-19,9.54361881492175E-5),
 .UNSPECIFIED.);
#25199=B_SPLINE_CURVE_WITH_KNOTS('',3,(#387462,#387463,#387464,#387465,
#387466,#387467,#387468),.UNSPECIFIED.,.F.,.F.,(4,3,4),(0.,6.98630244191489E-5,
0.000113969974038089),.UNSPECIFIED.);
#25200=B_SPLINE_CURVE_WITH_KNOTS('',3,(#387471,#387472,#387473,#387474,
#387475,#387476,#387477,#387478,#387479,#387480,#387481,#387482,#387483,
#387484,#387485,#387486,#387487,#387488,#387489,#387490,#387491,#387492,
#387493,#387494,#387495,#387496,#387497,#387498,#387499,#387500,#387501,
#387502,#387503,#387504,#387505,#387506,#387507,#387508,#387509,#387510,
#387511,#387512,#387513,#387514,#387515,#387516,#387517,#387518,#387519),
 .UNSPECIFIED.,.F.,.F.,(4,3,3,3,3,3,3,3,3,3,3,3,3,3,3,3,4),(0.,1.53100299373424E-6,
4.52554775679508E-6,7.01151246291611E-6,9.26752933800723E-6,1.03084066197174E-5,
1.17138990826861E-5,1.22284894984075E-5,1.30315035324817E-5,1.38363728497813E-5,
1.40464197777495E-5,1.5459774956464E-5,1.62073588704069E-5,1.9209296871253E-5,
1.95234416882555E-5,2.37637844577576E-5,2.61487188977262E-5),
 .UNSPECIFIED.);
#25201=B_SPLINE_CURVE_WITH_KNOTS('',3,(#387534,#387535,#387536,#387537,
#387538,#387539,#387540,#387541,#387542,#387543,#387544,#387545,#387546,
#387547,#387548,#387549,#387550,#387551,#387552,#387553,#387554,#387555,
#387556,#387557,#387558,#387559,#387560,#387561,#387562,#387563,#387564),
 .UNSPECIFIED.,.F.,.F.,(4,3,3,3,3,3,3,3,3,3,4),(0.,3.95507910397967E-6,
7.53768426604193E-6,1.19904533335349E-5,1.40475043392585E-5,1.51452104275964E-5,
1.67866272814196E-5,1.69621513005358E-5,1.81338315460712E-5,1.9890633465654E-5,
2.06132424588246E-5),.UNSPECIFIED.);
#25202=B_SPLINE_CURVE_WITH_KNOTS('',3,(#387567,#387568,#387569,#387570),
 .UNSPECIFIED.,.F.,.F.,(4,4),(4.84869951806108E-19,0.00010938435327491),
 .UNSPECIFIED.);
#25203=B_SPLINE_CURVE_WITH_KNOTS('',3,(#387597,#387598,#387599,#387600,
#387601,#387602,#387603,#387604,#387605,#387606,#387607,#387608,#387609,
#387610,#387611,#387612,#387613,#387614,#387615,#387616,#387617,#387618,
#387619,#387620,#387621,#387622,#387623,#387624,#387625,#387626,#387627,
#387628,#387629,#387630),.UNSPECIFIED.,.F.,.F.,(4,3,3,3,3,3,3,3,3,3,3,4),
(1.35525271560688E-19,2.0962399272944E-6,3.17176647120219E-6,4.82636181944153E-6,
5.01000917339958E-6,6.13126454147489E-6,8.60486650288847E-6,9.21144281170481E-6,
1.24722301136146E-5,1.42666454787853E-5,2.04670653756699E-5,2.08026438176797E-5),
 .UNSPECIFIED.);
#25204=B_SPLINE_CURVE_WITH_KNOTS('',3,(#387631,#387632,#387633,#387634),
 .UNSPECIFIED.,.F.,.F.,(4,4),(0.,0.000109384345496908),.UNSPECIFIED.);
#25205=B_SPLINE_CURVE_WITH_KNOTS('',3,(#387739,#387740,#387741,#387742),
 .UNSPECIFIED.,.F.,.F.,(4,4),(0.,9.54361881492175E-5),.UNSPECIFIED.);
#25206=B_SPLINE_CURVE_WITH_KNOTS('',3,(#387747,#387748,#387749,#387750,
#387751,#387752,#387753),.UNSPECIFIED.,.F.,.F.,(4,3,4),(0.,4.41069704323468E-5,
0.000113970027818833),.UNSPECIFIED.);
#25207=B_SPLINE_CURVE_WITH_KNOTS('',3,(#387759,#387760,#387761,#387762),
 .UNSPECIFIED.,.F.,.F.,(4,4),(4.48719651148014E-19,9.5436188149218E-5),
 .UNSPECIFIED.);
#25208=B_SPLINE_CURVE_WITH_KNOTS('',3,(#387766,#387767,#387768,#387769,
#387770,#387771,#387772),.UNSPECIFIED.,.F.,.F.,(4,3,4),(0.,6.98630244191489E-5,
0.000113969974038089),.UNSPECIFIED.);
#25209=B_SPLINE_CURVE_WITH_KNOTS('',3,(#387775,#387776,#387777,#387778,
#387779,#387780,#387781,#387782,#387783,#387784,#387785,#387786,#387787,
#387788,#387789,#387790,#387791,#387792,#387793,#387794,#387795,#387796,
#387797,#387798,#387799,#387800,#387801,#387802,#387803,#387804,#387805,
#387806,#387807,#387808,#387809,#387810,#387811,#387812,#387813,#387814,
#387815,#387816,#387817,#387818,#387819,#387820,#387821,#387822,#387823),
 .UNSPECIFIED.,.F.,.F.,(4,3,3,3,3,3,3,3,3,3,3,3,3,3,3,3,4),(0.,1.53100299373413E-6,
4.52554775679489E-6,7.01151246291594E-6,9.26752933800405E-6,1.03084066197173E-5,
1.17138990826861E-5,1.22284894984074E-5,1.30315035324817E-5,1.38363728497812E-5,
1.40464197777495E-5,1.54597749564639E-5,1.62073588704068E-5,1.92092968713333E-5,
1.95234416882555E-5,2.37637844577619E-5,2.61487188977262E-5),
 .UNSPECIFIED.);
#25210=B_SPLINE_CURVE_WITH_KNOTS('',3,(#387838,#387839,#387840,#387841,
#387842,#387843,#387844,#387845,#387846,#387847,#387848,#387849,#387850,
#387851,#387852,#387853,#387854,#387855,#387856,#387857,#387858,#387859,
#387860,#387861,#387862,#387863,#387864,#387865,#387866,#387867,#387868),
 .UNSPECIFIED.,.F.,.F.,(4,3,3,3,3,3,3,3,3,3,4),(0.,3.95507910398091E-6,
7.53768426604189E-6,1.1990453333535E-5,1.40475043392585E-5,1.51452104275964E-5,
1.67866272814286E-5,1.69621513005358E-5,1.81338315460712E-5,1.9890633465653E-5,
2.06132424588245E-5),.UNSPECIFIED.);
#25211=B_SPLINE_CURVE_WITH_KNOTS('',3,(#387871,#387872,#387873,#387874),
 .UNSPECIFIED.,.F.,.F.,(4,4),(4.73369422993816E-19,0.00010938435327491),
 .UNSPECIFIED.);
#25212=B_SPLINE_CURVE_WITH_KNOTS('',3,(#387901,#387902,#387903,#387904,
#387905,#387906,#387907,#387908,#387909,#387910,#387911,#387912,#387913,
#387914,#387915,#387916,#387917,#387918,#387919,#387920,#387921,#387922,
#387923,#387924,#387925,#387926,#387927,#387928,#387929,#387930,#387931,
#387932,#387933,#387934),.UNSPECIFIED.,.F.,.F.,(4,3,3,3,3,3,3,3,3,3,3,4),
(1.35525271560688E-19,2.09623992729438E-6,3.1717664712022E-6,4.82636181943525E-6,
5.0100091733996E-6,6.13126454147494E-6,8.6048665028885E-6,9.21144281170483E-6,
1.24722301136046E-5,1.42666454787854E-5,2.0467065375687E-5,2.08026438176799E-5),
 .UNSPECIFIED.);
#25213=B_SPLINE_CURVE_WITH_KNOTS('',3,(#387935,#387936,#387937,#387938),
 .UNSPECIFIED.,.F.,.F.,(4,4),(0.,0.000109384345496908),.UNSPECIFIED.);
#25214=B_SPLINE_CURVE_WITH_KNOTS('',3,(#388043,#388044,#388045,#388046),
 .UNSPECIFIED.,.F.,.F.,(4,4),(0.,9.5436188149217E-5),.UNSPECIFIED.);
#25215=B_SPLINE_CURVE_WITH_KNOTS('',3,(#388051,#388052,#388053,#388054,
#388055,#388056,#388057),.UNSPECIFIED.,.F.,.F.,(4,3,4),(0.,4.41069704323469E-5,
0.000113970027818833),.UNSPECIFIED.);
#25216=B_SPLINE_CURVE_WITH_KNOTS('',3,(#388063,#388064,#388065,#388066),
 .UNSPECIFIED.,.F.,.F.,(4,4),(4.47028007668187E-19,9.54361881492175E-5),
 .UNSPECIFIED.);
#25217=B_SPLINE_CURVE_WITH_KNOTS('',3,(#388070,#388071,#388072,#388073,
#388074,#388075,#388076),.UNSPECIFIED.,.F.,.F.,(4,3,4),(0.,6.9863024419149E-5,
0.000113969974038089),.UNSPECIFIED.);
#25218=B_SPLINE_CURVE_WITH_KNOTS('',3,(#388079,#388080,#388081,#388082,
#388083,#388084,#388085,#388086,#388087,#388088,#388089,#388090,#388091,
#388092,#388093,#388094,#388095,#388096,#388097,#388098,#388099,#388100,
#388101,#388102,#388103,#388104,#388105,#388106,#388107,#388108,#388109,
#388110,#388111,#388112,#388113,#388114,#388115,#388116,#388117,#388118,
#388119,#388120,#388121,#388122,#388123,#388124,#388125,#388126,#388127),
 .UNSPECIFIED.,.F.,.F.,(4,3,3,3,3,3,3,3,3,3,3,3,3,3,3,3,4),(0.,1.5310029937342E-6,
4.52554775679339E-6,7.01151246291608E-6,9.26752933799737E-6,1.03084066197173E-5,
1.17138990826863E-5,1.22284894984074E-5,1.30315035324817E-5,1.38363728497813E-5,
1.40464197777495E-5,1.54597749564639E-5,1.62073588704069E-5,1.92092968712856E-5,
1.95234416882552E-5,2.37637844577629E-5,2.61487188977258E-5),
 .UNSPECIFIED.);
#25219=B_SPLINE_CURVE_WITH_KNOTS('',3,(#388142,#388143,#388144,#388145,
#388146,#388147,#388148,#388149,#388150,#388151,#388152,#388153,#388154,
#388155,#388156,#388157,#388158,#388159,#388160,#388161,#388162,#388163,
#388164,#388165,#388166,#388167,#388168,#388169,#388170,#388171,#388172),
 .UNSPECIFIED.,.F.,.F.,(4,3,3,3,3,3,3,3,3,3,4),(0.,3.95507910398328E-6,
7.53768426604195E-6,1.19904533335349E-5,1.40475043392585E-5,1.51452104275964E-5,
1.67866272814049E-5,1.69621513005358E-5,1.81338315460712E-5,1.98906334656513E-5,
2.06132424588245E-5),.UNSPECIFIED.);
#25220=B_SPLINE_CURVE_WITH_KNOTS('',3,(#388175,#388176,#388177,#388178),
 .UNSPECIFIED.,.F.,.F.,(4,4),(4.63171371119878E-19,0.00010938435327491),
 .UNSPECIFIED.);
#25221=B_SPLINE_CURVE_WITH_KNOTS('',3,(#388205,#388206,#388207,#388208,
#388209,#388210,#388211,#388212,#388213,#388214,#388215,#388216,#388217,
#388218,#388219,#388220,#388221,#388222,#388223,#388224,#388225,#388226,
#388227,#388228,#388229,#388230,#388231,#388232,#388233,#388234,#388235,
#388236,#388237,#388238),.UNSPECIFIED.,.F.,.F.,(4,3,3,3,3,3,3,3,3,3,3,4),
(1.0842021724855E-19,2.09623992729441E-6,3.17176647120221E-6,4.82636181944583E-6,
5.0100091733996E-6,6.13126454147488E-6,8.60486650288823E-6,9.21144281170456E-6,
1.24722301136001E-5,1.42666454787847E-5,2.04670653757054E-5,2.08026438176787E-5),
 .UNSPECIFIED.);
#25222=B_SPLINE_CURVE_WITH_KNOTS('',3,(#388239,#388240,#388241,#388242),
 .UNSPECIFIED.,.F.,.F.,(4,4),(0.,0.000109384345496908),.UNSPECIFIED.);
#25223=B_SPLINE_CURVE_WITH_KNOTS('',3,(#388347,#388348,#388349,#388350),
 .UNSPECIFIED.,.F.,.F.,(4,4),(0.,9.54361881492172E-5),.UNSPECIFIED.);
#25224=B_SPLINE_CURVE_WITH_KNOTS('',3,(#388355,#388356,#388357,#388358,
#388359,#388360,#388361),.UNSPECIFIED.,.F.,.F.,(4,3,4),(0.,4.41069704323469E-5,
0.000113970027818833),.UNSPECIFIED.);
#25225=B_SPLINE_CURVE_WITH_KNOTS('',3,(#388367,#388368,#388369,#388370),
 .UNSPECIFIED.,.F.,.F.,(4,4),(4.47028007668187E-19,9.54361881492179E-5),
 .UNSPECIFIED.);
#25226=B_SPLINE_CURVE_WITH_KNOTS('',3,(#388374,#388375,#388376,#388377,
#388378,#388379,#388380),.UNSPECIFIED.,.F.,.F.,(4,3,4),(0.,6.98630244191492E-5,
0.000113969974038089),.UNSPECIFIED.);
#25227=B_SPLINE_CURVE_WITH_KNOTS('',3,(#388383,#388384,#388385,#388386,
#388387,#388388,#388389,#388390,#388391,#388392,#388393,#388394,#388395,
#388396,#388397,#388398,#388399,#388400,#388401,#388402,#388403,#388404,
#388405,#388406,#388407,#388408,#388409,#388410,#388411,#388412,#388413,
#388414,#388415,#388416,#388417,#388418,#388419,#388420,#388421,#388422,
#388423,#388424,#388425,#388426,#388427,#388428,#388429,#388430,#388431),
 .UNSPECIFIED.,.F.,.F.,(4,3,3,3,3,3,3,3,3,3,3,3,3,3,3,3,4),(0.,1.53100299373398E-6,
4.52554775679955E-6,7.01151246291586E-6,9.2675293380064E-6,1.03084066197173E-5,
1.17138990826862E-5,1.22284894984075E-5,1.30315035324817E-5,1.38363728497813E-5,
1.40464197777495E-5,1.54597749564641E-5,1.6207358870407E-5,1.92092968712452E-5,
1.95234416882558E-5,2.37637844577587E-5,2.61487188977266E-5),
 .UNSPECIFIED.);
#25228=B_SPLINE_CURVE_WITH_KNOTS('',3,(#388446,#388447,#388448,#388449,
#388450,#388451,#388452,#388453,#388454,#388455,#388456,#388457,#388458,
#388459,#388460,#388461,#388462,#388463,#388464,#388465,#388466,#388467,
#388468,#388469,#388470,#388471,#388472,#388473,#388474,#388475,#388476),
 .UNSPECIFIED.,.F.,.F.,(4,3,3,3,3,3,3,3,3,3,4),(0.,3.95507910397912E-6,
7.53768426604201E-6,1.1990453333535E-5,1.40475043392585E-5,1.51452104275963E-5,
1.6786627281435E-5,1.69621513005356E-5,1.81338315460709E-5,1.98906334656537E-5,
2.06132424588241E-5),.UNSPECIFIED.);
#25229=B_SPLINE_CURVE_WITH_KNOTS('',3,(#388479,#388480,#388481,#388482),
 .UNSPECIFIED.,.F.,.F.,(4,4),(4.63171371119878E-19,0.00010938435327491),
 .UNSPECIFIED.);
#25230=B_SPLINE_CURVE_WITH_KNOTS('',3,(#388509,#388510,#388511,#388512,
#388513,#388514,#388515,#388516,#388517,#388518,#388519,#388520,#388521,
#388522,#388523,#388524,#388525,#388526,#388527,#388528,#388529,#388530,
#388531,#388532,#388533,#388534,#388535,#388536,#388537,#388538,#388539,
#388540,#388541,#388542),.UNSPECIFIED.,.F.,.F.,(4,3,3,3,3,3,3,3,3,3,3,4),
(1.62630325872826E-19,2.0962399272944E-6,3.17176647120221E-6,4.82636181943954E-6,
5.01000917339966E-6,6.1312645414749E-6,8.60486650288846E-6,9.21144281170485E-6,
1.24722301136136E-5,1.42666454787854E-5,2.04670653756565E-5,2.080264381768E-5),
 .UNSPECIFIED.);
#25231=B_SPLINE_CURVE_WITH_KNOTS('',3,(#388543,#388544,#388545,#388546),
 .UNSPECIFIED.,.F.,.F.,(4,4),(0.,0.000109384345496908),.UNSPECIFIED.);
#25232=B_SPLINE_CURVE_WITH_KNOTS('',3,(#388651,#388652,#388653,#388654),
 .UNSPECIFIED.,.F.,.F.,(4,4),(0.,9.54361881492171E-5),.UNSPECIFIED.);
#25233=B_SPLINE_CURVE_WITH_KNOTS('',3,(#388659,#388660,#388661,#388662,
#388663,#388664,#388665),.UNSPECIFIED.,.F.,.F.,(4,3,4),(0.,4.41069704323471E-5,
0.000113970027818833),.UNSPECIFIED.);
#25234=B_SPLINE_CURVE_WITH_KNOTS('',3,(#388671,#388672,#388673,#388674),
 .UNSPECIFIED.,.F.,.F.,(4,4),(4.47028007668187E-19,9.54361881492177E-5),
 .UNSPECIFIED.);
#25235=B_SPLINE_CURVE_WITH_KNOTS('',3,(#388678,#388679,#388680,#388681,
#388682,#388683,#388684),.UNSPECIFIED.,.F.,.F.,(4,3,4),(0.,6.98630244191491E-5,
0.000113969974038089),.UNSPECIFIED.);
#25236=B_SPLINE_CURVE_WITH_KNOTS('',3,(#388687,#388688,#388689,#388690,
#388691,#388692,#388693,#388694,#388695,#388696,#388697,#388698,#388699,
#388700,#388701,#388702,#388703,#388704,#388705,#388706,#388707,#388708,
#388709,#388710,#388711,#388712,#388713,#388714,#388715,#388716,#388717,
#388718,#388719,#388720,#388721,#388722,#388723,#388724,#388725,#388726,
#388727,#388728,#388729,#388730,#388731,#388732,#388733,#388734,#388735),
 .UNSPECIFIED.,.F.,.F.,(4,3,3,3,3,3,3,3,3,3,3,3,3,3,3,3,4),(0.,1.53100299373411E-6,
4.52554775679518E-6,7.01151246291603E-6,9.26752933800355E-6,1.03084066197173E-5,
1.17138990826863E-5,1.22284894984076E-5,1.30315035324818E-5,1.38363728497813E-5,
1.40464197777496E-5,1.5459774956464E-5,1.62073588704068E-5,1.92092968713069E-5,
1.95234416882556E-5,2.37637844577537E-5,2.61487188977261E-5),
 .UNSPECIFIED.);
#25237=B_SPLINE_CURVE_WITH_KNOTS('',3,(#388750,#388751,#388752,#388753,
#388754,#388755,#388756,#388757,#388758,#388759,#388760,#388761,#388762,
#388763,#388764,#388765,#388766,#388767,#388768,#388769,#388770,#388771,
#388772,#388773,#388774,#388775,#388776,#388777,#388778,#388779,#388780),
 .UNSPECIFIED.,.F.,.F.,(4,3,3,3,3,3,3,3,3,3,4),(0.,3.95507910397527E-6,
7.53768426604199E-6,1.19904533335351E-5,1.40475043392585E-5,1.51452104275965E-5,
1.67866272814181E-5,1.69621513005357E-5,1.81338315460712E-5,1.98906334656553E-5,
2.06132424588244E-5),.UNSPECIFIED.);
#25238=B_SPLINE_CURVE_WITH_KNOTS('',3,(#388783,#388784,#388785,#388786),
 .UNSPECIFIED.,.F.,.F.,(4,4),(4.47028007668187E-19,0.00010938435327491),
 .UNSPECIFIED.);
#25239=B_SPLINE_CURVE_WITH_KNOTS('',3,(#388813,#388814,#388815,#388816,
#388817,#388818,#388819,#388820,#388821,#388822,#388823,#388824,#388825,
#388826,#388827,#388828,#388829,#388830,#388831,#388832,#388833,#388834,
#388835,#388836,#388837,#388838,#388839,#388840,#388841,#388842,#388843,
#388844,#388845,#388846),.UNSPECIFIED.,.F.,.F.,(4,3,3,3,3,3,3,3,3,3,3,4),
(1.0842021724855E-19,2.09623992729436E-6,3.17176647120224E-6,4.82636181944045E-6,
5.01000917339964E-6,6.13126454147505E-6,8.60486650288846E-6,9.21144281170488E-6,
1.24722301135973E-5,1.42666454787855E-5,2.04670653756798E-5,2.080264381768E-5),
 .UNSPECIFIED.);
#25240=B_SPLINE_CURVE_WITH_KNOTS('',3,(#388847,#388848,#388849,#388850),
 .UNSPECIFIED.,.F.,.F.,(4,4),(0.,0.000109384345496909),.UNSPECIFIED.);
#25241=B_SPLINE_CURVE_WITH_KNOTS('',3,(#388955,#388956,#388957,#388958),
 .UNSPECIFIED.,.F.,.F.,(4,4),(0.,9.54361881492175E-5),.UNSPECIFIED.);
#25242=B_SPLINE_CURVE_WITH_KNOTS('',3,(#388963,#388964,#388965,#388966,
#388967,#388968,#388969),.UNSPECIFIED.,.F.,.F.,(4,3,4),(0.,4.4106970432347E-5,
0.000113970027818833),.UNSPECIFIED.);
#25243=B_SPLINE_CURVE_WITH_KNOTS('',3,(#388975,#388976,#388977,#388978),
 .UNSPECIFIED.,.F.,.F.,(4,4),(4.33680868994202E-19,9.54361881492178E-5),
 .UNSPECIFIED.);
#25244=B_SPLINE_CURVE_WITH_KNOTS('',3,(#388982,#388983,#388984,#388985,
#388986,#388987,#388988),.UNSPECIFIED.,.F.,.F.,(4,3,4),(0.,6.98630244191489E-5,
0.000113969974038089),.UNSPECIFIED.);
#25245=B_SPLINE_CURVE_WITH_KNOTS('',3,(#388991,#388992,#388993,#388994,
#388995,#388996,#388997,#388998,#388999,#389000,#389001,#389002,#389003,
#389004,#389005,#389006,#389007,#389008,#389009,#389010,#389011,#389012,
#389013,#389014,#389015,#389016,#389017,#389018,#389019,#389020,#389021,
#389022,#389023,#389024,#389025,#389026,#389027,#389028,#389029,#389030,
#389031,#389032,#389033,#389034,#389035,#389036,#389037,#389038,#389039),
 .UNSPECIFIED.,.F.,.F.,(4,3,3,3,3,3,3,3,3,3,3,3,3,3,3,3,4),(0.,1.53100299373412E-6,
4.52554775679643E-6,7.01151246291612E-6,9.26752933801457E-6,1.03084066197173E-5,
1.17138990826862E-5,1.22284894984073E-5,1.30315035324817E-5,1.38363728497812E-5,
1.40464197777494E-5,1.54597749564638E-5,1.62073588704067E-5,1.92092968713275E-5,
1.95234416882553E-5,2.3763784457758E-5,2.61487188977258E-5),
 .UNSPECIFIED.);
#25246=B_SPLINE_CURVE_WITH_KNOTS('',3,(#389054,#389055,#389056,#389057,
#389058,#389059,#389060,#389061,#389062,#389063,#389064,#389065,#389066,
#389067,#389068,#389069,#389070,#389071,#389072,#389073,#389074,#389075,
#389076,#389077,#389078,#389079,#389080,#389081,#389082,#389083,#389084),
 .UNSPECIFIED.,.F.,.F.,(4,3,3,3,3,3,3,3,3,3,4),(0.,3.95507910397651E-6,
7.53768426604199E-6,1.1990453333535E-5,1.40475043392585E-5,1.51452104275963E-5,
1.67866272814247E-5,1.69621513005357E-5,1.81338315460712E-5,1.98906334656539E-5,
2.06132424588243E-5),.UNSPECIFIED.);
#25247=B_SPLINE_CURVE_WITH_KNOTS('',3,(#389087,#389088,#389089,#389090),
 .UNSPECIFIED.,.F.,.F.,(4,4),(4.47028007668187E-19,0.00010938435327491),
 .UNSPECIFIED.);
#25248=B_SPLINE_CURVE_WITH_KNOTS('',3,(#389117,#389118,#389119,#389120,
#389121,#389122,#389123,#389124,#389125,#389126,#389127,#389128,#389129,
#389130,#389131,#389132,#389133,#389134,#389135,#389136,#389137,#389138,
#389139,#389140,#389141,#389142,#389143,#389144,#389145,#389146,#389147,
#389148,#389149,#389150),.UNSPECIFIED.,.F.,.F.,(4,3,3,3,3,3,3,3,3,3,3,4),
(2.16840434497101E-19,2.09623992729447E-6,3.17176647120222E-6,4.82636181945244E-6,
5.01000917339954E-6,6.13126454147495E-6,8.60486650288834E-6,9.21144281170472E-6,
1.24722301135988E-5,1.42666454787852E-5,2.0467065375677E-5,2.08026438176796E-5),
 .UNSPECIFIED.);
#25249=B_SPLINE_CURVE_WITH_KNOTS('',3,(#389151,#389152,#389153,#389154),
 .UNSPECIFIED.,.F.,.F.,(4,4),(0.,0.000109384345496908),.UNSPECIFIED.);
#25250=B_SPLINE_CURVE_WITH_KNOTS('',3,(#389259,#389260,#389261,#389262),
 .UNSPECIFIED.,.F.,.F.,(4,4),(0.,9.54361881492176E-5),.UNSPECIFIED.);
#25251=B_SPLINE_CURVE_WITH_KNOTS('',3,(#389267,#389268,#389269,#389270,
#389271,#389272,#389273),.UNSPECIFIED.,.F.,.F.,(4,3,4),(0.,4.41069704323467E-5,
0.000113970027818833),.UNSPECIFIED.);
#25252=B_SPLINE_CURVE_WITH_KNOTS('',3,(#389279,#389280,#389281,#389282),
 .UNSPECIFIED.,.F.,.F.,(4,4),(0.,9.54361881492178E-5),.UNSPECIFIED.);
#25253=B_SPLINE_CURVE_WITH_KNOTS('',3,(#389286,#389287,#389288,#389289,
#389290,#389291,#389292),.UNSPECIFIED.,.F.,.F.,(4,3,4),(0.,6.98630244191494E-5,
0.000113969974038089),.UNSPECIFIED.);
#25254=B_SPLINE_CURVE_WITH_KNOTS('',3,(#389295,#389296,#389297,#389298,
#389299,#389300,#389301,#389302,#389303,#389304,#389305,#389306,#389307,
#389308,#389309,#389310,#389311,#389312,#389313,#389314,#389315,#389316,
#389317,#389318,#389319,#389320,#389321,#389322,#389323,#389324,#389325,
#389326,#389327,#389328,#389329,#389330,#389331,#389332,#389333,#389334,
#389335,#389336,#389337,#389338,#389339,#389340,#389341,#389342,#389343),
 .UNSPECIFIED.,.F.,.F.,(4,3,3,3,3,3,3,3,3,3,3,3,3,3,3,3,4),(0.,1.5310029937341E-6,
4.5255477567998E-6,7.01151246291602E-6,9.26752933800744E-6,1.03084066197172E-5,
1.17138990826861E-5,1.22284894984072E-5,1.30315035324817E-5,1.38363728497813E-5,
1.40464197777494E-5,1.5459774956464E-5,1.6207358870407E-5,1.92092968712811E-5,
1.95234416882557E-5,2.37637844577566E-5,2.61487188977266E-5),
 .UNSPECIFIED.);
#25255=B_SPLINE_CURVE_WITH_KNOTS('',3,(#389358,#389359,#389360,#389361,
#389362,#389363,#389364,#389365,#389366,#389367,#389368,#389369,#389370,
#389371,#389372,#389373,#389374,#389375,#389376,#389377,#389378,#389379,
#389380,#389381,#389382,#389383,#389384,#389385,#389386,#389387,#389388),
 .UNSPECIFIED.,.F.,.F.,(4,3,3,3,3,3,3,3,3,3,4),(0.,3.95507910397734E-6,
7.537684266042E-6,1.1990453333535E-5,1.40475043392585E-5,1.51452104275964E-5,
1.67866272814187E-5,1.69621513005358E-5,1.8133831546071E-5,1.98906334656531E-5,
2.06132424588243E-5),.UNSPECIFIED.);
#25256=B_SPLINE_CURVE_WITH_KNOTS('',3,(#389391,#389392,#389393,#389394),
 .UNSPECIFIED.,.F.,.F.,(4,4),(4.47028007668187E-19,0.00010938435327491),
 .UNSPECIFIED.);
#25257=B_SPLINE_CURVE_WITH_KNOTS('',3,(#389421,#389422,#389423,#389424,
#389425,#389426,#389427,#389428,#389429,#389430,#389431,#389432,#389433,
#389434,#389435,#389436,#389437,#389438,#389439,#389440,#389441,#389442,
#389443,#389444,#389445,#389446,#389447,#389448,#389449,#389450,#389451,
#389452,#389453,#389454),.UNSPECIFIED.,.F.,.F.,(4,3,3,3,3,3,3,3,3,3,3,4),
(2.16840434497101E-19,2.09623992729446E-6,3.17176647120221E-6,4.82636181944466E-6,
5.01000917339944E-6,6.13126454147503E-6,8.60486650288845E-6,9.21144281170482E-6,
1.24722301135897E-5,1.42666454787855E-5,2.04670653756925E-5,2.08026438176801E-5),
 .UNSPECIFIED.);
#25258=B_SPLINE_CURVE_WITH_KNOTS('',3,(#389455,#389456,#389457,#389458),
 .UNSPECIFIED.,.F.,.F.,(4,4),(0.,0.000109384345496908),.UNSPECIFIED.);
#25259=B_SPLINE_CURVE_WITH_KNOTS('',3,(#389563,#389564,#389565,#389566),
 .UNSPECIFIED.,.F.,.F.,(4,4),(0.,9.54361881492174E-5),.UNSPECIFIED.);
#25260=B_SPLINE_CURVE_WITH_KNOTS('',3,(#389571,#389572,#389573,#389574,
#389575,#389576,#389577),.UNSPECIFIED.,.F.,.F.,(4,3,4),(0.,4.41069704323472E-5,
0.000113970027818833),.UNSPECIFIED.);
#25261=B_SPLINE_CURVE_WITH_KNOTS('',3,(#389583,#389584,#389585,#389586),
 .UNSPECIFIED.,.F.,.F.,(4,4),(4.33680868994202E-19,9.54361881492176E-5),
 .UNSPECIFIED.);
#25262=B_SPLINE_CURVE_WITH_KNOTS('',3,(#389590,#389591,#389592,#389593,
#389594,#389595,#389596),.UNSPECIFIED.,.F.,.F.,(4,3,4),(0.,6.9863024419149E-5,
0.000113969974038089),.UNSPECIFIED.);
#25263=B_SPLINE_CURVE_WITH_KNOTS('',3,(#389599,#389600,#389601,#389602,
#389603,#389604,#389605,#389606,#389607,#389608,#389609,#389610,#389611,
#389612,#389613,#389614,#389615,#389616,#389617,#389618,#389619,#389620,
#389621,#389622,#389623,#389624,#389625,#389626,#389627,#389628,#389629,
#389630,#389631,#389632,#389633,#389634,#389635,#389636,#389637,#389638,
#389639,#389640,#389641,#389642,#389643,#389644,#389645,#389646,#389647),
 .UNSPECIFIED.,.F.,.F.,(4,3,3,3,3,3,3,3,3,3,3,3,3,3,3,3,4),(0.,1.53100299373409E-6,
4.52554775678909E-6,7.01151246291593E-6,9.26752933800868E-6,1.03084066197173E-5,
1.17138990826865E-5,1.22284894984075E-5,1.30315035324817E-5,1.38363728497814E-5,
1.40464197777496E-5,1.54597749564642E-5,1.62073588704071E-5,1.92092968712948E-5,
1.95234416882557E-5,2.37637844577641E-5,2.61487188977263E-5),
 .UNSPECIFIED.);
#25264=B_SPLINE_CURVE_WITH_KNOTS('',3,(#389662,#389663,#389664,#389665,
#389666,#389667,#389668,#389669,#389670,#389671,#389672,#389673,#389674,
#389675,#389676,#389677,#389678,#389679,#389680,#389681,#389682,#389683,
#389684,#389685,#389686,#389687,#389688,#389689,#389690,#389691,#389692),
 .UNSPECIFIED.,.F.,.F.,(4,3,3,3,3,3,3,3,3,3,4),(0.,3.95507910398428E-6,
7.53768426604197E-6,1.1990453333535E-5,1.40475043392584E-5,1.51452104275963E-5,
1.67866272814145E-5,1.6962151300536E-5,1.81338315460713E-5,1.9890633465654E-5,
2.06132424588247E-5),.UNSPECIFIED.);
#25265=B_SPLINE_CURVE_WITH_KNOTS('',3,(#389695,#389696,#389697,#389698),
 .UNSPECIFIED.,.F.,.F.,(4,4),(4.33680868994202E-19,0.00010938435327491),
 .UNSPECIFIED.);
#25266=B_SPLINE_CURVE_WITH_KNOTS('',3,(#389725,#389726,#389727,#389728,
#389729,#389730,#389731,#389732,#389733,#389734,#389735,#389736,#389737,
#389738,#389739,#389740,#389741,#389742,#389743,#389744,#389745,#389746,
#389747,#389748,#389749,#389750,#389751,#389752,#389753,#389754,#389755,
#389756,#389757,#389758),.UNSPECIFIED.,.F.,.F.,(4,3,3,3,3,3,3,3,3,3,3,4),
(0.,2.09623992729446E-6,3.1717664712022E-6,4.826361819433E-6,5.01000917339962E-6,
6.13126454147486E-6,8.60486650288814E-6,9.21144281170439E-6,1.24722301135902E-5,
1.42666454787843E-5,2.0467065375698E-5,2.08026438176779E-5),
 .UNSPECIFIED.);
#25267=B_SPLINE_CURVE_WITH_KNOTS('',3,(#389759,#389760,#389761,#389762),
 .UNSPECIFIED.,.F.,.F.,(4,4),(0.,0.000109384345496908),.UNSPECIFIED.);
#25268=B_SPLINE_CURVE_WITH_KNOTS('',3,(#389867,#389868,#389869,#389870),
 .UNSPECIFIED.,.F.,.F.,(4,4),(0.,9.54361881492177E-5),.UNSPECIFIED.);
#25269=B_SPLINE_CURVE_WITH_KNOTS('',3,(#389875,#389876,#389877,#389878,
#389879,#389880,#389881),.UNSPECIFIED.,.F.,.F.,(4,3,4),(0.,4.41069704323467E-5,
0.000113970027818833),.UNSPECIFIED.);
#25270=B_SPLINE_CURVE_WITH_KNOTS('',3,(#389887,#389888,#389889,#389890),
 .UNSPECIFIED.,.F.,.F.,(4,4),(4.33680868994202E-19,9.54361881492182E-5),
 .UNSPECIFIED.);
#25271=B_SPLINE_CURVE_WITH_KNOTS('',3,(#389894,#389895,#389896,#389897,
#389898,#389899,#389900),.UNSPECIFIED.,.F.,.F.,(4,3,4),(0.,6.9863024419149E-5,
0.000113969974038089),.UNSPECIFIED.);
#25272=B_SPLINE_CURVE_WITH_KNOTS('',3,(#389903,#389904,#389905,#389906,
#389907,#389908,#389909,#389910,#389911,#389912,#389913,#389914,#389915,
#389916,#389917,#389918,#389919,#389920,#389921,#389922,#389923,#389924,
#389925,#389926,#389927,#389928,#389929,#389930,#389931,#389932,#389933,
#389934,#389935,#389936,#389937,#389938,#389939,#389940,#389941,#389942,
#389943,#389944,#389945,#389946,#389947,#389948,#389949,#389950,#389951),
 .UNSPECIFIED.,.F.,.F.,(4,3,3,3,3,3,3,3,3,3,3,3,3,3,3,3,4),(0.,1.53100299373416E-6,
4.52554775679403E-6,7.01151246291602E-6,9.26752933799172E-6,1.03084066197174E-5,
1.17138990826862E-5,1.22284894984074E-5,1.30315035324817E-5,1.38363728497811E-5,
1.40464197777497E-5,1.54597749564639E-5,1.62073588704069E-5,1.92092968712594E-5,
1.95234416882556E-5,2.37637844577584E-5,2.61487188977261E-5),
 .UNSPECIFIED.);
#25273=B_SPLINE_CURVE_WITH_KNOTS('',3,(#389966,#389967,#389968,#389969,
#389970,#389971,#389972,#389973,#389974,#389975,#389976,#389977,#389978,
#389979,#389980,#389981,#389982,#389983,#389984,#389985,#389986,#389987,
#389988,#389989,#389990,#389991,#389992,#389993,#389994,#389995,#389996),
 .UNSPECIFIED.,.F.,.F.,(4,3,3,3,3,3,3,3,3,3,4),(0.,3.95507910398383E-6,
7.53768426604193E-6,1.1990453333535E-5,1.40475043392586E-5,1.51452104275962E-5,
1.67866272814302E-5,1.69621513005357E-5,1.81338315460711E-5,1.9890633465653E-5,
2.06132424588243E-5),.UNSPECIFIED.);
#25274=B_SPLINE_CURVE_WITH_KNOTS('',3,(#389999,#390000,#390001,#390002),
 .UNSPECIFIED.,.F.,.F.,(4,4),(4.33680868994202E-19,0.00010938435327491),
 .UNSPECIFIED.);
#25275=B_SPLINE_CURVE_WITH_KNOTS('',3,(#390029,#390030,#390031,#390032,
#390033,#390034,#390035,#390036,#390037,#390038,#390039,#390040,#390041,
#390042,#390043,#390044,#390045,#390046,#390047,#390048,#390049,#390050,
#390051,#390052,#390053,#390054,#390055,#390056,#390057,#390058,#390059,
#390060,#390061,#390062),.UNSPECIFIED.,.F.,.F.,(4,3,3,3,3,3,3,3,3,3,3,4),
(2.16840434497101E-19,2.09623992729435E-6,3.17176647120219E-6,4.82636181943341E-6,
5.01000917339972E-6,6.13126454147492E-6,8.60486650288852E-6,9.21144281170482E-6,
1.24722301135993E-5,1.42666454787856E-5,2.04670653756756E-5,2.08026438176803E-5),
 .UNSPECIFIED.);
#25276=B_SPLINE_CURVE_WITH_KNOTS('',3,(#390063,#390064,#390065,#390066),
 .UNSPECIFIED.,.F.,.F.,(4,4),(0.,0.000109384345496908),.UNSPECIFIED.);
#25277=B_SPLINE_CURVE_WITH_KNOTS('',3,(#390171,#390172,#390173,#390174),
 .UNSPECIFIED.,.F.,.F.,(4,4),(0.,9.54361881492174E-5),.UNSPECIFIED.);
#25278=B_SPLINE_CURVE_WITH_KNOTS('',3,(#390179,#390180,#390181,#390182,
#390183,#390184,#390185),.UNSPECIFIED.,.F.,.F.,(4,3,4),(0.,4.41069704323469E-5,
0.000113970027818833),.UNSPECIFIED.);
#25279=B_SPLINE_CURVE_WITH_KNOTS('',3,(#390191,#390192,#390193,#390194),
 .UNSPECIFIED.,.F.,.F.,(4,4),(4.63171371119878E-19,9.54361881492179E-5),
 .UNSPECIFIED.);
#25280=B_SPLINE_CURVE_WITH_KNOTS('',3,(#390198,#390199,#390200,#390201,
#390202,#390203,#390204),.UNSPECIFIED.,.F.,.F.,(4,3,4),(0.,6.98630244191489E-5,
0.000113969974038089),.UNSPECIFIED.);
#25281=B_SPLINE_CURVE_WITH_KNOTS('',3,(#390207,#390208,#390209,#390210,
#390211,#390212,#390213,#390214,#390215,#390216,#390217,#390218,#390219,
#390220,#390221,#390222,#390223,#390224,#390225,#390226,#390227,#390228,
#390229,#390230,#390231,#390232,#390233,#390234,#390235,#390236,#390237,
#390238,#390239,#390240,#390241,#390242,#390243,#390244,#390245,#390246,
#390247,#390248,#390249,#390250,#390251,#390252,#390253,#390254,#390255),
 .UNSPECIFIED.,.F.,.F.,(4,3,3,3,3,3,3,3,3,3,3,3,3,3,3,3,4),(0.,1.53100299373408E-6,
4.52554775679199E-6,7.01151246291604E-6,9.26752933800014E-6,1.03084066197173E-5,
1.17138990826862E-5,1.22284894984075E-5,1.30315035324817E-5,1.38363728497813E-5,
1.40464197777494E-5,1.5459774956464E-5,1.62073588704068E-5,1.92092968712309E-5,
1.95234416882555E-5,2.37637844577565E-5,2.61487188977261E-5),
 .UNSPECIFIED.);
#25282=B_SPLINE_CURVE_WITH_KNOTS('',3,(#390270,#390271,#390272,#390273,
#390274,#390275,#390276,#390277,#390278,#390279,#390280,#390281,#390282,
#390283,#390284,#390285,#390286,#390287,#390288,#390289,#390290,#390291,
#390292,#390293,#390294,#390295,#390296,#390297,#390298,#390299,#390300),
 .UNSPECIFIED.,.F.,.F.,(4,3,3,3,3,3,3,3,3,3,4),(0.,3.95507910399088E-6,
7.53768426604193E-6,1.19904533335349E-5,1.40475043392585E-5,1.51452104275963E-5,
1.67866272814177E-5,1.69621513005356E-5,1.8133831546071E-5,1.98906334656504E-5,
2.06132424588242E-5),.UNSPECIFIED.);
#25283=B_SPLINE_CURVE_WITH_KNOTS('',3,(#390303,#390304,#390305,#390306),
 .UNSPECIFIED.,.F.,.F.,(4,4),(5.11417141928151E-19,0.00010938435327491),
 .UNSPECIFIED.);
#25284=B_SPLINE_CURVE_WITH_KNOTS('',3,(#390333,#390334,#390335,#390336,
#390337,#390338,#390339,#390340,#390341,#390342,#390343,#390344,#390345,
#390346,#390347,#390348,#390349,#390350,#390351,#390352,#390353,#390354,
#390355,#390356,#390357,#390358,#390359,#390360,#390361,#390362,#390363,
#390364,#390365,#390366),.UNSPECIFIED.,.F.,.F.,(4,3,3,3,3,3,3,3,3,3,3,4),
(1.0842021724855E-19,2.09623992729441E-6,3.17176647120218E-6,4.82636181942557E-6,
5.01000917339962E-6,6.13126454147496E-6,8.60486650288856E-6,9.21144281170495E-6,
1.24722301135921E-5,1.42666454787855E-5,2.04670653756969E-5,2.08026438176802E-5),
 .UNSPECIFIED.);
#25285=B_SPLINE_CURVE_WITH_KNOTS('',3,(#390367,#390368,#390369,#390370),
 .UNSPECIFIED.,.F.,.F.,(4,4),(0.,0.000109384345496908),.UNSPECIFIED.);
#25286=B_SPLINE_CURVE_WITH_KNOTS('',3,(#390475,#390476,#390477,#390478),
 .UNSPECIFIED.,.F.,.F.,(4,4),(0.,9.54361881492174E-5),.UNSPECIFIED.);
#25287=B_SPLINE_CURVE_WITH_KNOTS('',3,(#390483,#390484,#390485,#390486,
#390487,#390488,#390489),.UNSPECIFIED.,.F.,.F.,(4,3,4),(0.,4.41069704323469E-5,
0.000113970027818833),.UNSPECIFIED.);
#25288=B_SPLINE_CURVE_WITH_KNOTS('',3,(#390495,#390496,#390497,#390498),
 .UNSPECIFIED.,.F.,.F.,(4,4),(2.16840434497101E-19,9.5436188149218E-5),
 .UNSPECIFIED.);
#25289=B_SPLINE_CURVE_WITH_KNOTS('',3,(#390502,#390503,#390504,#390505,
#390506,#390507,#390508),.UNSPECIFIED.,.F.,.F.,(4,3,4),(0.,6.98630244191491E-5,
0.000113969974038089),.UNSPECIFIED.);
#25290=B_SPLINE_CURVE_WITH_KNOTS('',3,(#390511,#390512,#390513,#390514,
#390515,#390516,#390517,#390518,#390519,#390520,#390521,#390522,#390523,
#390524,#390525,#390526,#390527,#390528,#390529,#390530,#390531,#390532,
#390533,#390534,#390535,#390536,#390537,#390538,#390539,#390540,#390541,
#390542,#390543,#390544,#390545,#390546,#390547,#390548,#390549,#390550,
#390551,#390552,#390553,#390554,#390555,#390556,#390557,#390558,#390559),
 .UNSPECIFIED.,.F.,.F.,(4,3,3,3,3,3,3,3,3,3,3,3,3,3,3,3,4),(0.,1.53100299373404E-6,
4.52554775679301E-6,7.01151246291608E-6,9.26752933800197E-6,1.03084066197173E-5,
1.17138990826862E-5,1.22284894984074E-5,1.30315035324818E-5,1.38363728497813E-5,
1.40464197777495E-5,1.54597749564641E-5,1.62073588704069E-5,1.92092968712377E-5,
1.95234416882556E-5,2.37637844577636E-5,2.61487188977264E-5),
 .UNSPECIFIED.);
#25291=B_SPLINE_CURVE_WITH_KNOTS('',3,(#390574,#390575,#390576,#390577,
#390578,#390579,#390580,#390581,#390582,#390583,#390584,#390585,#390586,
#390587,#390588,#390589,#390590,#390591,#390592,#390593,#390594,#390595,
#390596,#390597,#390598,#390599,#390600,#390601,#390602,#390603,#390604),
 .UNSPECIFIED.,.F.,.F.,(4,3,3,3,3,3,3,3,3,3,4),(0.,3.95507910397597E-6,
7.53768426604195E-6,1.19904533335351E-5,1.40475043392585E-5,1.51452104275964E-5,
1.67866272814042E-5,1.69621513005359E-5,1.81338315460713E-5,1.98906334656556E-5,
2.06132424588248E-5),.UNSPECIFIED.);
#25292=B_SPLINE_CURVE_WITH_KNOTS('',3,(#390607,#390608,#390609,#390610),
 .UNSPECIFIED.,.F.,.F.,(4,4),(4.84869951806108E-19,0.00010938435327491),
 .UNSPECIFIED.);
#25293=B_SPLINE_CURVE_WITH_KNOTS('',3,(#390637,#390638,#390639,#390640,
#390641,#390642,#390643,#390644,#390645,#390646,#390647,#390648,#390649,
#390650,#390651,#390652,#390653,#390654,#390655,#390656,#390657,#390658,
#390659,#390660,#390661,#390662,#390663,#390664,#390665,#390666,#390667,
#390668,#390669,#390670),.UNSPECIFIED.,.F.,.F.,(4,3,3,3,3,3,3,3,3,3,3,4),
(1.62630325872826E-19,2.09623992729434E-6,3.17176647120212E-6,4.82636181944639E-6,
5.01000917339947E-6,6.13126454147481E-6,8.60486650288819E-6,9.2114428117045E-6,
1.24722301136184E-5,1.42666454787845E-5,2.04670653756707E-5,2.08026438176783E-5),
 .UNSPECIFIED.);
#25294=B_SPLINE_CURVE_WITH_KNOTS('',3,(#390671,#390672,#390673,#390674),
 .UNSPECIFIED.,.F.,.F.,(4,4),(0.,0.000109384345496908),.UNSPECIFIED.);
#25295=B_SPLINE_CURVE_WITH_KNOTS('',3,(#390779,#390780,#390781,#390782),
 .UNSPECIFIED.,.F.,.F.,(4,4),(0.,9.54361881492171E-5),.UNSPECIFIED.);
#25296=B_SPLINE_CURVE_WITH_KNOTS('',3,(#390787,#390788,#390789,#390790,
#390791,#390792,#390793),.UNSPECIFIED.,.F.,.F.,(4,3,4),(0.,4.41069704323471E-5,
0.000113970027818833),.UNSPECIFIED.);
#25297=B_SPLINE_CURVE_WITH_KNOTS('',3,(#390799,#390800,#390801,#390802),
 .UNSPECIFIED.,.F.,.F.,(4,4),(4.84869951806108E-19,9.54361881492178E-5),
 .UNSPECIFIED.);
#25298=B_SPLINE_CURVE_WITH_KNOTS('',3,(#390806,#390807,#390808,#390809,
#390810,#390811,#390812),.UNSPECIFIED.,.F.,.F.,(4,3,4),(0.,6.98630244191492E-5,
0.000113969974038089),.UNSPECIFIED.);
#25299=B_SPLINE_CURVE_WITH_KNOTS('',3,(#390815,#390816,#390817,#390818,
#390819,#390820,#390821,#390822,#390823,#390824,#390825,#390826,#390827,
#390828,#390829,#390830,#390831,#390832,#390833,#390834,#390835,#390836,
#390837,#390838,#390839,#390840,#390841,#390842,#390843,#390844,#390845,
#390846,#390847,#390848,#390849,#390850,#390851,#390852,#390853,#390854,
#390855,#390856,#390857,#390858,#390859,#390860,#390861,#390862,#390863),
 .UNSPECIFIED.,.F.,.F.,(4,3,3,3,3,3,3,3,3,3,3,3,3,3,3,3,4),(0.,1.53100299373407E-6,
4.52554775679799E-6,7.01151246291605E-6,9.2675293380014E-6,1.03084066197173E-5,
1.17138990826862E-5,1.22284894984074E-5,1.30315035324817E-5,1.38363728497813E-5,
1.40464197777495E-5,1.54597749564641E-5,1.62073588704071E-5,1.92092968712794E-5,
1.95234416882559E-5,2.37637844577629E-5,2.61487188977271E-5),
 .UNSPECIFIED.);
#25300=B_SPLINE_CURVE_WITH_KNOTS('',3,(#390878,#390879,#390880,#390881,
#390882,#390883,#390884,#390885,#390886,#390887,#390888,#390889,#390890,
#390891,#390892,#390893,#390894,#390895,#390896,#390897,#390898,#390899,
#390900,#390901,#390902,#390903,#390904,#390905,#390906,#390907,#390908),
 .UNSPECIFIED.,.F.,.F.,(4,3,3,3,3,3,3,3,3,3,4),(0.,3.95507910396868E-6,
7.53768426604184E-6,1.19904533335349E-5,1.40475043392585E-5,1.51452104275964E-5,
1.67866272814194E-5,1.69621513005358E-5,1.8133831546071E-5,1.98906334656556E-5,
2.06132424588244E-5),.UNSPECIFIED.);
#25301=B_SPLINE_CURVE_WITH_KNOTS('',3,(#390911,#390912,#390913,#390914),
 .UNSPECIFIED.,.F.,.F.,(4,4),(5.42101086242752E-19,0.00010938435327491),
 .UNSPECIFIED.);
#25302=B_SPLINE_CURVE_WITH_KNOTS('',3,(#390941,#390942,#390943,#390944,
#390945,#390946,#390947,#390948,#390949,#390950,#390951,#390952,#390953,
#390954,#390955,#390956,#390957,#390958,#390959,#390960,#390961,#390962,
#390963,#390964,#390965,#390966,#390967,#390968,#390969,#390970,#390971,
#390972,#390973,#390974),.UNSPECIFIED.,.F.,.F.,(4,3,3,3,3,3,3,3,3,3,3,4),
(1.0842021724855E-19,2.09623992729447E-6,3.17176647120237E-6,4.82636181943974E-6,
5.01000917339962E-6,6.13126454147495E-6,8.60486650288846E-6,9.2114428117048E-6,
1.24722301136019E-5,1.4266645478785E-5,2.04670653756862E-5,2.08026438176791E-5),
 .UNSPECIFIED.);
#25303=B_SPLINE_CURVE_WITH_KNOTS('',3,(#390975,#390976,#390977,#390978),
 .UNSPECIFIED.,.F.,.F.,(4,4),(0.,0.000109384345496908),.UNSPECIFIED.);
#25304=B_SPLINE_CURVE_WITH_KNOTS('',3,(#391083,#391084,#391085,#391086),
 .UNSPECIFIED.,.F.,.F.,(4,4),(0.,9.54361881492177E-5),.UNSPECIFIED.);
#25305=B_SPLINE_CURVE_WITH_KNOTS('',3,(#391091,#391092,#391093,#391094,
#391095,#391096,#391097),.UNSPECIFIED.,.F.,.F.,(4,3,4),(0.,4.41069704323471E-5,
0.000113970027818833),.UNSPECIFIED.);
#25306=B_SPLINE_CURVE_WITH_KNOTS('',3,(#391103,#391104,#391105,#391106),
 .UNSPECIFIED.,.F.,.F.,(4,4),(1.0842021724855E-19,9.54361881492175E-5),
 .UNSPECIFIED.);
#25307=B_SPLINE_CURVE_WITH_KNOTS('',3,(#391110,#391111,#391112,#391113,
#391114,#391115,#391116),.UNSPECIFIED.,.F.,.F.,(4,3,4),(0.,6.98630244191488E-5,
0.000113969974038089),.UNSPECIFIED.);
#25308=B_SPLINE_CURVE_WITH_KNOTS('',3,(#391119,#391120,#391121,#391122,
#391123,#391124,#391125,#391126,#391127,#391128,#391129,#391130,#391131,
#391132,#391133,#391134,#391135,#391136,#391137,#391138,#391139,#391140,
#391141,#391142,#391143,#391144,#391145,#391146,#391147,#391148,#391149,
#391150,#391151,#391152,#391153,#391154,#391155,#391156,#391157,#391158,
#391159,#391160,#391161,#391162,#391163,#391164,#391165,#391166,#391167),
 .UNSPECIFIED.,.F.,.F.,(4,3,3,3,3,3,3,3,3,3,3,3,3,3,3,3,4),(0.,1.53100299373429E-6,
4.52554775679722E-6,7.01151246291618E-6,9.26752933798786E-6,1.03084066197175E-5,
1.17138990826863E-5,1.22284894984076E-5,1.3031503532482E-5,1.38363728497814E-5,
1.40464197777495E-5,1.54597749564641E-5,1.62073588704071E-5,1.92092968713176E-5,
1.95234416882558E-5,2.37637844577596E-5,2.61487188977265E-5),
 .UNSPECIFIED.);
#25309=B_SPLINE_CURVE_WITH_KNOTS('',3,(#391182,#391183,#391184,#391185,
#391186,#391187,#391188,#391189,#391190,#391191,#391192,#391193,#391194,
#391195,#391196,#391197,#391198,#391199,#391200,#391201,#391202,#391203,
#391204,#391205,#391206,#391207,#391208,#391209,#391210,#391211,#391212),
 .UNSPECIFIED.,.F.,.F.,(4,3,3,3,3,3,3,3,3,3,4),(0.,3.95507910397509E-6,
7.53768426604205E-6,1.19904533335352E-5,1.40475043392586E-5,1.51452104275965E-5,
1.67866272814222E-5,1.69621513005358E-5,1.81338315460713E-5,1.98906334656548E-5,
2.06132424588244E-5),.UNSPECIFIED.);
#25310=B_SPLINE_CURVE_WITH_KNOTS('',3,(#391215,#391216,#391217,#391218),
 .UNSPECIFIED.,.F.,.F.,(4,4),(2.16840434497101E-19,0.00010938435327491),
 .UNSPECIFIED.);
#25311=B_SPLINE_CURVE_WITH_KNOTS('',3,(#391245,#391246,#391247,#391248,
#391249,#391250,#391251,#391252,#391253,#391254,#391255,#391256,#391257,
#391258,#391259,#391260,#391261,#391262,#391263,#391264,#391265,#391266,
#391267,#391268,#391269,#391270,#391271,#391272,#391273,#391274,#391275,
#391276,#391277,#391278),.UNSPECIFIED.,.F.,.F.,(4,3,3,3,3,3,3,3,3,3,3,4),
(1.0842021724855E-19,2.0962399272944E-6,3.17176647120216E-6,4.8263618194377E-6,
5.01000917339973E-6,6.13126454147497E-6,8.60486650288862E-6,9.21144281170494E-6,
1.24722301135921E-5,1.42666454787858E-5,2.04670653756916E-5,2.08026438176805E-5),
 .UNSPECIFIED.);
#25312=B_SPLINE_CURVE_WITH_KNOTS('',3,(#391279,#391280,#391281,#391282),
 .UNSPECIFIED.,.F.,.F.,(4,4),(0.,0.000109384345496909),.UNSPECIFIED.);
#25313=B_SPLINE_CURVE_WITH_KNOTS('',3,(#391387,#391388,#391389,#391390),
 .UNSPECIFIED.,.F.,.F.,(4,4),(0.,9.54361881492175E-5),.UNSPECIFIED.);
#25314=B_SPLINE_CURVE_WITH_KNOTS('',3,(#391395,#391396,#391397,#391398,
#391399,#391400,#391401),.UNSPECIFIED.,.F.,.F.,(4,3,4),(0.,4.4106970432347E-5,
0.000113970027818833),.UNSPECIFIED.);
#25315=B_SPLINE_CURVE_WITH_KNOTS('',3,(#391407,#391408,#391409,#391410),
 .UNSPECIFIED.,.F.,.F.,(4,4),(2.16840434497101E-19,9.54361881492182E-5),
 .UNSPECIFIED.);
#25316=B_SPLINE_CURVE_WITH_KNOTS('',3,(#391414,#391415,#391416,#391417,
#391418,#391419,#391420),.UNSPECIFIED.,.F.,.F.,(4,3,4),(0.,6.98630244191491E-5,
0.000113969974038089),.UNSPECIFIED.);
#25317=B_SPLINE_CURVE_WITH_KNOTS('',3,(#391423,#391424,#391425,#391426,
#391427,#391428,#391429,#391430,#391431,#391432,#391433,#391434,#391435,
#391436,#391437,#391438,#391439,#391440,#391441,#391442,#391443,#391444,
#391445,#391446,#391447,#391448,#391449,#391450,#391451,#391452,#391453,
#391454,#391455,#391456,#391457,#391458,#391459,#391460,#391461,#391462,
#391463,#391464,#391465,#391466,#391467,#391468,#391469,#391470,#391471),
 .UNSPECIFIED.,.F.,.F.,(4,3,3,3,3,3,3,3,3,3,3,3,3,3,3,3,4),(0.,1.53100299373416E-6,
4.52554775679338E-6,7.01151246291604E-6,9.26752933799479E-6,1.03084066197174E-5,
1.1713899082686E-5,1.22284894984072E-5,1.30315035324815E-5,1.3836372849781E-5,
1.40464197777492E-5,1.54597749564636E-5,1.62073588704064E-5,1.92092968712892E-5,
1.95234416882548E-5,2.37637844577542E-5,2.61487188977248E-5),
 .UNSPECIFIED.);
#25318=B_SPLINE_CURVE_WITH_KNOTS('',3,(#391486,#391487,#391488,#391489,
#391490,#391491,#391492,#391493,#391494,#391495,#391496,#391497,#391498,
#391499,#391500,#391501,#391502,#391503,#391504,#391505,#391506,#391507,
#391508,#391509,#391510,#391511,#391512,#391513,#391514,#391515,#391516),
 .UNSPECIFIED.,.F.,.F.,(4,3,3,3,3,3,3,3,3,3,4),(0.,3.95507910398083E-6,
7.53768426604198E-6,1.19904533335351E-5,1.40475043392585E-5,1.51452104275965E-5,
1.67866272814139E-5,1.69621513005358E-5,1.81338315460711E-5,1.98906334656541E-5,
2.06132424588244E-5),.UNSPECIFIED.);
#25319=B_SPLINE_CURVE_WITH_KNOTS('',3,(#391519,#391520,#391521,#391522),
 .UNSPECIFIED.,.F.,.F.,(4,4),(4.84869951806108E-19,0.00010938435327491),
 .UNSPECIFIED.);
#25320=B_SPLINE_CURVE_WITH_KNOTS('',3,(#391549,#391550,#391551,#391552,
#391553,#391554,#391555,#391556,#391557,#391558,#391559,#391560,#391561,
#391562,#391563,#391564,#391565,#391566,#391567,#391568,#391569,#391570,
#391571,#391572,#391573,#391574,#391575,#391576,#391577,#391578,#391579,
#391580,#391581,#391582),.UNSPECIFIED.,.F.,.F.,(4,3,3,3,3,3,3,3,3,3,3,4),
(2.16840434497101E-19,2.0962399272943E-6,3.17176647120214E-6,4.82636181942743E-6,
5.01000917339943E-6,6.13126454147466E-6,8.60486650288832E-6,9.21144281170473E-6,
1.24722301136018E-5,1.42666454787853E-5,2.04670653757024E-5,2.08026438176798E-5),
 .UNSPECIFIED.);
#25321=B_SPLINE_CURVE_WITH_KNOTS('',3,(#391583,#391584,#391585,#391586),
 .UNSPECIFIED.,.F.,.F.,(4,4),(0.,0.000109384345496908),.UNSPECIFIED.);
#25322=B_SPLINE_CURVE_WITH_KNOTS('',3,(#391691,#391692,#391693,#391694),
 .UNSPECIFIED.,.F.,.F.,(4,4),(0.,9.54361881492178E-5),.UNSPECIFIED.);
#25323=B_SPLINE_CURVE_WITH_KNOTS('',3,(#391699,#391700,#391701,#391702,
#391703,#391704,#391705),.UNSPECIFIED.,.F.,.F.,(4,3,4),(0.,4.4106970432347E-5,
0.000113970027818834),.UNSPECIFIED.);
#25324=B_SPLINE_CURVE_WITH_KNOTS('',3,(#391711,#391712,#391713,#391714),
 .UNSPECIFIED.,.F.,.F.,(4,4),(2.16840434497101E-19,9.54361881492179E-5),
 .UNSPECIFIED.);
#25325=B_SPLINE_CURVE_WITH_KNOTS('',3,(#391718,#391719,#391720,#391721,
#391722,#391723,#391724),.UNSPECIFIED.,.F.,.F.,(4,3,4),(0.,6.98630244191491E-5,
0.000113969974038089),.UNSPECIFIED.);
#25326=B_SPLINE_CURVE_WITH_KNOTS('',3,(#391727,#391728,#391729,#391730,
#391731,#391732,#391733,#391734,#391735,#391736,#391737,#391738,#391739,
#391740,#391741,#391742,#391743,#391744,#391745,#391746,#391747,#391748,
#391749,#391750,#391751,#391752,#391753,#391754,#391755,#391756,#391757,
#391758,#391759,#391760,#391761,#391762,#391763,#391764,#391765,#391766,
#391767,#391768,#391769,#391770,#391771,#391772,#391773,#391774,#391775),
 .UNSPECIFIED.,.F.,.F.,(4,3,3,3,3,3,3,3,3,3,3,3,3,3,3,3,4),(0.,1.53100299373418E-6,
4.52554775679414E-6,7.01151246291608E-6,9.26752933800765E-6,1.03084066197173E-5,
1.1713899082686E-5,1.22284894984074E-5,1.30315035324818E-5,1.38363728497812E-5,
1.40464197777496E-5,1.54597749564643E-5,1.62073588704071E-5,1.92092968712819E-5,
1.95234416882561E-5,2.37637844577578E-5,2.61487188977273E-5),
 .UNSPECIFIED.);
#25327=B_SPLINE_CURVE_WITH_KNOTS('',3,(#391790,#391791,#391792,#391793,
#391794,#391795,#391796,#391797,#391798,#391799,#391800,#391801,#391802,
#391803,#391804,#391805,#391806,#391807,#391808,#391809,#391810,#391811,
#391812,#391813,#391814,#391815,#391816,#391817,#391818,#391819,#391820),
 .UNSPECIFIED.,.F.,.F.,(4,3,3,3,3,3,3,3,3,3,4),(0.,3.95507910397348E-6,
7.53768426604206E-6,1.19904533335352E-5,1.40475043392587E-5,1.51452104275967E-5,
1.67866272814203E-5,1.6962151300536E-5,1.81338315460713E-5,1.98906334656551E-5,
2.0613242458825E-5),.UNSPECIFIED.);
#25328=B_SPLINE_CURVE_WITH_KNOTS('',3,(#391823,#391824,#391825,#391826),
 .UNSPECIFIED.,.F.,.F.,(4,4),(4.84869951806108E-19,0.00010938435327491),
 .UNSPECIFIED.);
#25329=B_SPLINE_CURVE_WITH_KNOTS('',3,(#391853,#391854,#391855,#391856,
#391857,#391858,#391859,#391860,#391861,#391862,#391863,#391864,#391865,
#391866,#391867,#391868,#391869,#391870,#391871,#391872,#391873,#391874,
#391875,#391876,#391877,#391878,#391879,#391880,#391881,#391882,#391883,
#391884,#391885,#391886),.UNSPECIFIED.,.F.,.F.,(4,3,3,3,3,3,3,3,3,3,3,4),
(2.16840434497101E-19,2.0962399272944E-6,3.17176647120218E-6,4.82636181944615E-6,
5.01000917339954E-6,6.13126454147516E-6,8.6048665028885E-6,9.21144281170492E-6,
1.24722301135926E-5,1.42666454787855E-5,2.04670653756851E-5,2.08026438176801E-5),
 .UNSPECIFIED.);
#25330=B_SPLINE_CURVE_WITH_KNOTS('',3,(#391887,#391888,#391889,#391890),
 .UNSPECIFIED.,.F.,.F.,(4,4),(0.,0.000109384345496908),.UNSPECIFIED.);
#25331=B_SPLINE_CURVE_WITH_KNOTS('',3,(#391995,#391996,#391997,#391998),
 .UNSPECIFIED.,.F.,.F.,(4,4),(0.,9.54361881492175E-5),.UNSPECIFIED.);
#25332=B_SPLINE_CURVE_WITH_KNOTS('',3,(#392003,#392004,#392005,#392006,
#392007,#392008,#392009),.UNSPECIFIED.,.F.,.F.,(4,3,4),(0.,4.41069704323471E-5,
0.000113970027818833),.UNSPECIFIED.);
#25333=B_SPLINE_CURVE_WITH_KNOTS('',3,(#392015,#392016,#392017,#392018),
 .UNSPECIFIED.,.F.,.F.,(4,4),(2.16840434497101E-19,9.54361881492179E-5),
 .UNSPECIFIED.);
#25334=B_SPLINE_CURVE_WITH_KNOTS('',3,(#392022,#392023,#392024,#392025,
#392026,#392027,#392028),.UNSPECIFIED.,.F.,.F.,(4,3,4),(0.,6.98630244191488E-5,
0.000113969974038089),.UNSPECIFIED.);
#25335=B_SPLINE_CURVE_WITH_KNOTS('',3,(#392031,#392032,#392033,#392034,
#392035,#392036,#392037,#392038,#392039,#392040,#392041,#392042,#392043,
#392044,#392045,#392046,#392047,#392048,#392049,#392050,#392051,#392052,
#392053,#392054,#392055,#392056,#392057,#392058,#392059,#392060,#392061,
#392062,#392063,#392064,#392065,#392066,#392067,#392068,#392069,#392070,
#392071,#392072,#392073,#392074,#392075,#392076,#392077,#392078,#392079),
 .UNSPECIFIED.,.F.,.F.,(4,3,3,3,3,3,3,3,3,3,3,3,3,3,3,3,4),(0.,1.53100299373417E-6,
4.52554775678998E-6,7.01151246291595E-6,9.26752933800364E-6,1.03084066197173E-5,
1.1713899082686E-5,1.22284894984073E-5,1.30315035324817E-5,1.38363728497812E-5,
1.40464197777493E-5,1.54597749564639E-5,1.62073588704067E-5,1.92092968713107E-5,
1.95234416882552E-5,2.37637844577573E-5,2.61487188977257E-5),
 .UNSPECIFIED.);
#25336=B_SPLINE_CURVE_WITH_KNOTS('',3,(#392094,#392095,#392096,#392097,
#392098,#392099,#392100,#392101,#392102,#392103,#392104,#392105,#392106,
#392107,#392108,#392109,#392110,#392111,#392112,#392113,#392114,#392115,
#392116,#392117,#392118,#392119,#392120,#392121,#392122,#392123,#392124),
 .UNSPECIFIED.,.F.,.F.,(4,3,3,3,3,3,3,3,3,3,4),(0.,3.95507910397914E-6,
7.53768426604207E-6,1.19904533335351E-5,1.40475043392588E-5,1.51452104275968E-5,
1.67866272814232E-5,1.69621513005362E-5,1.81338315460716E-5,1.98906334656541E-5,
2.0613242458825E-5),.UNSPECIFIED.);
#25337=B_SPLINE_CURVE_WITH_KNOTS('',3,(#392127,#392128,#392129,#392130),
 .UNSPECIFIED.,.F.,.F.,(4,4),(2.16840434497101E-19,0.00010938435327491),
 .UNSPECIFIED.);
#25338=B_SPLINE_CURVE_WITH_KNOTS('',3,(#392157,#392158,#392159,#392160,
#392161,#392162,#392163,#392164,#392165,#392166,#392167,#392168,#392169,
#392170,#392171,#392172,#392173,#392174,#392175,#392176,#392177,#392178,
#392179,#392180,#392181,#392182,#392183,#392184,#392185,#392186,#392187,
#392188,#392189,#392190),.UNSPECIFIED.,.F.,.F.,(4,3,3,3,3,3,3,3,3,3,3,4),
(4.84869951806108E-19,2.0962399272945E-6,3.17176647120198E-6,4.82636181944282E-6,
5.01000917339938E-6,6.1312645414749E-6,8.60486650288829E-6,9.21144281170457E-6,
1.24722301135921E-5,1.42666454787849E-5,2.04670653756833E-5,2.08026438176789E-5),
 .UNSPECIFIED.);
#25339=B_SPLINE_CURVE_WITH_KNOTS('',3,(#392191,#392192,#392193,#392194),
 .UNSPECIFIED.,.F.,.F.,(4,4),(0.,0.000109384345496908),.UNSPECIFIED.);
#25340=B_SPLINE_CURVE_WITH_KNOTS('',3,(#392299,#392300,#392301,#392302),
 .UNSPECIFIED.,.F.,.F.,(4,4),(0.,9.54361881492172E-5),.UNSPECIFIED.);
#25341=B_SPLINE_CURVE_WITH_KNOTS('',3,(#392307,#392308,#392309,#392310,
#392311,#392312,#392313),.UNSPECIFIED.,.F.,.F.,(4,3,4),(0.,4.41069704323467E-5,
0.000113970027818833),.UNSPECIFIED.);
#25342=B_SPLINE_CURVE_WITH_KNOTS('',3,(#392319,#392320,#392321,#392322),
 .UNSPECIFIED.,.F.,.F.,(4,4),(2.16840434497101E-19,9.54361881492177E-5),
 .UNSPECIFIED.);
#25343=B_SPLINE_CURVE_WITH_KNOTS('',3,(#392326,#392327,#392328,#392329,
#392330,#392331,#392332),.UNSPECIFIED.,.F.,.F.,(4,3,4),(0.,6.9863024419149E-5,
0.000113969974038089),.UNSPECIFIED.);
#25344=B_SPLINE_CURVE_WITH_KNOTS('',3,(#392335,#392336,#392337,#392338,
#392339,#392340,#392341,#392342,#392343,#392344,#392345,#392346,#392347,
#392348,#392349,#392350,#392351,#392352,#392353,#392354,#392355,#392356,
#392357,#392358,#392359,#392360,#392361,#392362,#392363,#392364,#392365,
#392366,#392367,#392368,#392369,#392370,#392371,#392372,#392373,#392374,
#392375,#392376,#392377,#392378,#392379,#392380,#392381,#392382,#392383),
 .UNSPECIFIED.,.F.,.F.,(4,3,3,3,3,3,3,3,3,3,3,3,3,3,3,3,4),(0.,1.53100299373411E-6,
4.52554775678843E-6,7.01151246291605E-6,9.2675293380181E-6,1.03084066197174E-5,
1.17138990826862E-5,1.22284894984073E-5,1.30315035324817E-5,1.38363728497813E-5,
1.40464197777498E-5,1.5459774956464E-5,1.62073588704072E-5,1.92092968712942E-5,
1.9523441688256E-5,2.37637844577598E-5,2.61487188977274E-5),
 .UNSPECIFIED.);
#25345=B_SPLINE_CURVE_WITH_KNOTS('',3,(#392398,#392399,#392400,#392401,
#392402,#392403,#392404,#392405,#392406,#392407,#392408,#392409,#392410,
#392411,#392412,#392413,#392414,#392415,#392416,#392417,#392418,#392419,
#392420,#392421,#392422,#392423,#392424,#392425,#392426,#392427,#392428),
 .UNSPECIFIED.,.F.,.F.,(4,3,3,3,3,3,3,3,3,3,4),(0.,3.95507910397759E-6,
7.53768426604205E-6,1.19904533335349E-5,1.40475043392584E-5,1.51452104275962E-5,
1.67866272813981E-5,1.69621513005359E-5,1.81338315460713E-5,1.98906334656512E-5,
2.06132424588244E-5),.UNSPECIFIED.);
#25346=B_SPLINE_CURVE_WITH_KNOTS('',3,(#392431,#392432,#392433,#392434),
 .UNSPECIFIED.,.F.,.F.,(4,4),(4.33680868994202E-19,0.00010938435327491),
 .UNSPECIFIED.);
#25347=B_SPLINE_CURVE_WITH_KNOTS('',3,(#392461,#392462,#392463,#392464,
#392465,#392466,#392467,#392468,#392469,#392470,#392471,#392472,#392473,
#392474,#392475,#392476,#392477,#392478,#392479,#392480,#392481,#392482,
#392483,#392484,#392485,#392486,#392487,#392488,#392489,#392490,#392491,
#392492,#392493,#392494),.UNSPECIFIED.,.F.,.F.,(4,3,3,3,3,3,3,3,3,3,3,4),
(2.16840434497101E-19,2.09623992729441E-6,3.17176647120199E-6,4.82636181942181E-6,
5.01000917339924E-6,6.13126454147485E-6,8.60486650288836E-6,9.21144281170481E-6,
1.24722301135933E-5,1.42666454787854E-5,2.04670653757255E-5,2.08026438176801E-5),
 .UNSPECIFIED.);
#25348=B_SPLINE_CURVE_WITH_KNOTS('',3,(#392495,#392496,#392497,#392498),
 .UNSPECIFIED.,.F.,.F.,(4,4),(0.,0.000109384345496909),.UNSPECIFIED.);
#25349=B_SPLINE_CURVE_WITH_KNOTS('',3,(#392603,#392604,#392605,#392606),
 .UNSPECIFIED.,.F.,.F.,(4,4),(0.,9.54361881492178E-5),.UNSPECIFIED.);
#25350=B_SPLINE_CURVE_WITH_KNOTS('',3,(#392611,#392612,#392613,#392614,
#392615,#392616,#392617),.UNSPECIFIED.,.F.,.F.,(4,3,4),(0.,4.41069704323472E-5,
0.000113970027818834),.UNSPECIFIED.);
#25351=B_SPLINE_CURVE_WITH_KNOTS('',3,(#392623,#392624,#392625,#392626),
 .UNSPECIFIED.,.F.,.F.,(4,4),(2.16840434497101E-19,9.54361881492178E-5),
 .UNSPECIFIED.);
#25352=B_SPLINE_CURVE_WITH_KNOTS('',3,(#392630,#392631,#392632,#392633,
#392634,#392635,#392636),.UNSPECIFIED.,.F.,.F.,(4,3,4),(0.,6.98630244191492E-5,
0.000113969974038089),.UNSPECIFIED.);
#25353=B_SPLINE_CURVE_WITH_KNOTS('',3,(#392639,#392640,#392641,#392642,
#392643,#392644,#392645,#392646,#392647,#392648,#392649,#392650,#392651,
#392652,#392653,#392654,#392655,#392656,#392657,#392658,#392659,#392660,
#392661,#392662,#392663,#392664,#392665,#392666,#392667,#392668,#392669,
#392670,#392671,#392672,#392673,#392674,#392675,#392676,#392677,#392678,
#392679,#392680,#392681,#392682,#392683,#392684,#392685,#392686,#392687),
 .UNSPECIFIED.,.F.,.F.,(4,3,3,3,3,3,3,3,3,3,3,3,3,3,3,3,4),(0.,1.53100299373412E-6,
4.52554775679078E-6,7.011512462916E-6,9.26752933800588E-6,1.03084066197174E-5,
1.17138990826862E-5,1.22284894984074E-5,1.30315035324818E-5,1.38363728497811E-5,
1.40464197777491E-5,1.54597749564639E-5,1.62073588704066E-5,1.92092968713222E-5,
1.95234416882547E-5,2.37637844577591E-5,2.61487188977244E-5),
 .UNSPECIFIED.);
#25354=B_SPLINE_CURVE_WITH_KNOTS('',3,(#392702,#392703,#392704,#392705,
#392706,#392707,#392708,#392709,#392710,#392711,#392712,#392713,#392714,
#392715,#392716,#392717,#392718,#392719,#392720,#392721,#392722,#392723,
#392724,#392725,#392726,#392727,#392728,#392729,#392730,#392731,#392732),
 .UNSPECIFIED.,.F.,.F.,(4,3,3,3,3,3,3,3,3,3,4),(0.,3.95507910396997E-6,
7.53768426604195E-6,1.19904533335349E-5,1.40475043392585E-5,1.51452104275965E-5,
1.67866272814111E-5,1.69621513005356E-5,1.81338315460712E-5,1.98906334656546E-5,
2.06132424588245E-5),.UNSPECIFIED.);
#25355=B_SPLINE_CURVE_WITH_KNOTS('',3,(#392735,#392736,#392737,#392738),
 .UNSPECIFIED.,.F.,.F.,(4,4),(2.16840434497101E-19,0.00010938435327491),
 .UNSPECIFIED.);
#25356=B_SPLINE_CURVE_WITH_KNOTS('',3,(#392765,#392766,#392767,#392768,
#392769,#392770,#392771,#392772,#392773,#392774,#392775,#392776,#392777,
#392778,#392779,#392780,#392781,#392782,#392783,#392784,#392785,#392786,
#392787,#392788,#392789,#392790,#392791,#392792,#392793,#392794,#392795,
#392796,#392797,#392798),.UNSPECIFIED.,.F.,.F.,(4,3,3,3,3,3,3,3,3,3,3,4),
(0.,2.09623992729438E-6,3.17176647120216E-6,4.82636181943502E-6,5.01000917339982E-6,
6.13126454147495E-6,8.60486650288879E-6,9.21144281170511E-6,1.2472230113587E-5,
1.42666454787859E-5,2.04670653756995E-5,2.08026438176806E-5),
 .UNSPECIFIED.);
#25357=B_SPLINE_CURVE_WITH_KNOTS('',3,(#392799,#392800,#392801,#392802),
 .UNSPECIFIED.,.F.,.F.,(4,4),(0.,0.000109384345496908),.UNSPECIFIED.);
#25358=B_SPLINE_CURVE_WITH_KNOTS('',3,(#392907,#392908,#392909,#392910),
 .UNSPECIFIED.,.F.,.F.,(4,4),(0.,9.54361881492172E-5),.UNSPECIFIED.);
#25359=B_SPLINE_CURVE_WITH_KNOTS('',3,(#392915,#392916,#392917,#392918,
#392919,#392920,#392921),.UNSPECIFIED.,.F.,.F.,(4,3,4),(0.,4.41069704323469E-5,
0.000113970027818833),.UNSPECIFIED.);
#25360=B_SPLINE_CURVE_WITH_KNOTS('',3,(#392927,#392928,#392929,#392930),
 .UNSPECIFIED.,.F.,.F.,(4,4),(2.16840434497101E-19,9.5436188149218E-5),
 .UNSPECIFIED.);
#25361=B_SPLINE_CURVE_WITH_KNOTS('',3,(#392934,#392935,#392936,#392937,
#392938,#392939,#392940),.UNSPECIFIED.,.F.,.F.,(4,3,4),(0.,6.98630244191489E-5,
0.000113969974038089),.UNSPECIFIED.);
#25362=B_SPLINE_CURVE_WITH_KNOTS('',3,(#392943,#392944,#392945,#392946,
#392947,#392948,#392949,#392950,#392951,#392952,#392953,#392954,#392955,
#392956,#392957,#392958,#392959,#392960,#392961,#392962,#392963,#392964,
#392965,#392966,#392967,#392968,#392969,#392970,#392971,#392972,#392973,
#392974,#392975,#392976,#392977,#392978,#392979,#392980,#392981,#392982,
#392983,#392984,#392985,#392986,#392987,#392988,#392989,#392990,#392991),
 .UNSPECIFIED.,.F.,.F.,(4,3,3,3,3,3,3,3,3,3,3,3,3,3,3,3,4),(0.,1.53100299373414E-6,
4.52554775679806E-6,7.0115124629161E-6,9.26752933798902E-6,1.03084066197172E-5,
1.17138990826862E-5,1.22284894984076E-5,1.30315035324815E-5,1.38363728497814E-5,
1.40464197777496E-5,1.54597749564639E-5,1.62073588704069E-5,1.9209296871272E-5,
1.95234416882556E-5,2.37637844577596E-5,2.61487188977267E-5),
 .UNSPECIFIED.);
#25363=B_SPLINE_CURVE_WITH_KNOTS('',3,(#393006,#393007,#393008,#393009,
#393010,#393011,#393012,#393013,#393014,#393015,#393016,#393017,#393018,
#393019,#393020,#393021,#393022,#393023,#393024,#393025,#393026,#393027,
#393028,#393029,#393030,#393031,#393032,#393033,#393034,#393035,#393036),
 .UNSPECIFIED.,.F.,.F.,(4,3,3,3,3,3,3,3,3,3,4),(0.,3.95507910398563E-6,
7.53768426604196E-6,1.1990453333535E-5,1.40475043392585E-5,1.51452104275965E-5,
1.67866272814175E-5,1.69621513005359E-5,1.81338315460713E-5,1.98906334656545E-5,
2.06132424588247E-5),.UNSPECIFIED.);
#25364=B_SPLINE_CURVE_WITH_KNOTS('',3,(#393039,#393040,#393041,#393042),
 .UNSPECIFIED.,.F.,.F.,(4,4),(4.33680868994202E-19,0.00010938435327491),
 .UNSPECIFIED.);
#25365=B_SPLINE_CURVE_WITH_KNOTS('',3,(#393069,#393070,#393071,#393072,
#393073,#393074,#393075,#393076,#393077,#393078,#393079,#393080,#393081,
#393082,#393083,#393084,#393085,#393086,#393087,#393088,#393089,#393090,
#393091,#393092,#393093,#393094,#393095,#393096,#393097,#393098,#393099,
#393100,#393101,#393102),.UNSPECIFIED.,.F.,.F.,(4,3,3,3,3,3,3,3,3,3,3,4),
(0.,2.09623992729478E-6,3.17176647120224E-6,4.82636181942829E-6,5.01000917339992E-6,
6.13126454147526E-6,8.60486650288872E-6,9.21144281170506E-6,1.24722301135961E-5,
1.42666454787857E-5,2.0467065375705E-5,2.08026438176803E-5),
 .UNSPECIFIED.);
#25366=B_SPLINE_CURVE_WITH_KNOTS('',3,(#393103,#393104,#393105,#393106),
 .UNSPECIFIED.,.F.,.F.,(4,4),(0.,0.000109384345496908),.UNSPECIFIED.);
#25367=B_SPLINE_CURVE_WITH_KNOTS('',3,(#393211,#393212,#393213,#393214),
 .UNSPECIFIED.,.F.,.F.,(4,4),(0.,9.54361881492174E-5),.UNSPECIFIED.);
#25368=B_SPLINE_CURVE_WITH_KNOTS('',3,(#393219,#393220,#393221,#393222,
#393223,#393224,#393225),.UNSPECIFIED.,.F.,.F.,(4,3,4),(0.,4.41069704323471E-5,
0.000113970027818833),.UNSPECIFIED.);
#25369=B_SPLINE_CURVE_WITH_KNOTS('',3,(#393231,#393232,#393233,#393234),
 .UNSPECIFIED.,.F.,.F.,(4,4),(2.16840434497101E-19,9.54361881492179E-5),
 .UNSPECIFIED.);
#25370=B_SPLINE_CURVE_WITH_KNOTS('',3,(#393238,#393239,#393240,#393241,
#393242,#393243,#393244),.UNSPECIFIED.,.F.,.F.,(4,3,4),(0.,6.9863024419149E-5,
0.000113969974038089),.UNSPECIFIED.);
#25371=B_SPLINE_CURVE_WITH_KNOTS('',3,(#393247,#393248,#393249,#393250,
#393251,#393252,#393253,#393254,#393255,#393256,#393257,#393258,#393259,
#393260,#393261,#393262,#393263,#393264,#393265,#393266,#393267,#393268,
#393269,#393270,#393271,#393272,#393273,#393274,#393275,#393276,#393277,
#393278,#393279,#393280,#393281,#393282,#393283,#393284,#393285,#393286,
#393287,#393288,#393289,#393290,#393291,#393292,#393293,#393294,#393295),
 .UNSPECIFIED.,.F.,.F.,(4,3,3,3,3,3,3,3,3,3,3,3,3,3,3,3,4),(0.,1.53100299373417E-6,
4.525547756795E-6,7.011512462916E-6,9.26752933799827E-6,1.03084066197174E-5,
1.17138990826862E-5,1.22284894984076E-5,1.30315035324817E-5,1.38363728497811E-5,
1.40464197777495E-5,1.5459774956464E-5,1.62073588704069E-5,1.920929687129E-5,
1.95234416882555E-5,2.37637844577568E-5,2.61487188977261E-5),
 .UNSPECIFIED.);
#25372=B_SPLINE_CURVE_WITH_KNOTS('',3,(#393310,#393311,#393312,#393313,
#393314,#393315,#393316,#393317,#393318,#393319,#393320,#393321,#393322,
#393323,#393324,#393325,#393326,#393327,#393328,#393329,#393330,#393331,
#393332,#393333,#393334,#393335,#393336,#393337,#393338,#393339,#393340),
 .UNSPECIFIED.,.F.,.F.,(4,3,3,3,3,3,3,3,3,3,4),(0.,3.9550791039817E-6,7.537684266042E-6,
1.1990453333535E-5,1.40475043392584E-5,1.51452104275964E-5,1.67866272814146E-5,
1.69621513005355E-5,1.81338315460708E-5,1.98906334656541E-5,2.06132424588239E-5),
 .UNSPECIFIED.);
#25373=B_SPLINE_CURVE_WITH_KNOTS('',3,(#393343,#393344,#393345,#393346),
 .UNSPECIFIED.,.F.,.F.,(4,4),(9.93687704810078E-19,0.00010938435327491),
 .UNSPECIFIED.);
#25374=B_SPLINE_CURVE_WITH_KNOTS('',3,(#393373,#393374,#393375,#393376,
#393377,#393378,#393379,#393380,#393381,#393382,#393383,#393384,#393385,
#393386,#393387,#393388,#393389,#393390,#393391,#393392,#393393,#393394,
#393395,#393396,#393397,#393398,#393399,#393400,#393401,#393402,#393403,
#393404,#393405,#393406),.UNSPECIFIED.,.F.,.F.,(4,3,3,3,3,3,3,3,3,3,3,4),
(4.84869951806108E-19,2.09623992729445E-6,3.17176647120213E-6,4.82636181942555E-6,
5.01000917339949E-6,6.13126454147482E-6,8.6048665028884E-6,9.21144281170475E-6,
1.24722301135981E-5,1.42666454787855E-5,2.04670653756909E-5,2.08026438176802E-5),
 .UNSPECIFIED.);
#25375=B_SPLINE_CURVE_WITH_KNOTS('',3,(#393407,#393408,#393409,#393410),
 .UNSPECIFIED.,.F.,.F.,(4,4),(0.,0.000109384345496908),.UNSPECIFIED.);
#25376=B_SPLINE_CURVE_WITH_KNOTS('',3,(#393515,#393516,#393517,#393518),
 .UNSPECIFIED.,.F.,.F.,(4,4),(0.,9.54361881492174E-5),.UNSPECIFIED.);
#25377=B_SPLINE_CURVE_WITH_KNOTS('',3,(#393523,#393524,#393525,#393526,
#393527,#393528,#393529),.UNSPECIFIED.,.F.,.F.,(4,3,4),(0.,4.41069704323467E-5,
0.000113970027818833),.UNSPECIFIED.);
#25378=B_SPLINE_CURVE_WITH_KNOTS('',3,(#393535,#393536,#393537,#393538),
 .UNSPECIFIED.,.F.,.F.,(4,4),(4.84869951806108E-19,9.54361881492179E-5),
 .UNSPECIFIED.);
#25379=B_SPLINE_CURVE_WITH_KNOTS('',3,(#393542,#393543,#393544,#393545,
#393546,#393547,#393548),.UNSPECIFIED.,.F.,.F.,(4,3,4),(0.,6.98630244191489E-5,
0.000113969974038089),.UNSPECIFIED.);
#25380=B_SPLINE_CURVE_WITH_KNOTS('',3,(#393551,#393552,#393553,#393554,
#393555,#393556,#393557,#393558,#393559,#393560,#393561,#393562,#393563,
#393564,#393565,#393566,#393567,#393568,#393569,#393570,#393571,#393572,
#393573,#393574,#393575,#393576,#393577,#393578,#393579,#393580,#393581,
#393582,#393583,#393584,#393585,#393586,#393587,#393588,#393589,#393590,
#393591,#393592,#393593,#393594,#393595,#393596,#393597,#393598,#393599),
 .UNSPECIFIED.,.F.,.F.,(4,3,3,3,3,3,3,3,3,3,3,3,3,3,3,3,4),(0.,1.53100299373405E-6,
4.52554775679208E-6,7.01151246291602E-6,9.26752933800532E-6,1.03084066197175E-5,
1.17138990826864E-5,1.22284894984073E-5,1.30315035324821E-5,1.38363728497815E-5,
1.40464197777496E-5,1.54597749564641E-5,1.6207358870407E-5,1.9209296871288E-5,
1.95234416882559E-5,2.37637844577587E-5,2.61487188977268E-5),
 .UNSPECIFIED.);
#25381=B_SPLINE_CURVE_WITH_KNOTS('',3,(#393614,#393615,#393616,#393617,
#393618,#393619,#393620,#393621,#393622,#393623,#393624,#393625,#393626,
#393627,#393628,#393629,#393630,#393631,#393632,#393633,#393634,#393635,
#393636,#393637,#393638,#393639,#393640,#393641,#393642,#393643,#393644),
 .UNSPECIFIED.,.F.,.F.,(4,3,3,3,3,3,3,3,3,3,4),(0.,3.95507910397499E-6,
7.53768426604193E-6,1.1990453333535E-5,1.40475043392585E-5,1.51452104275963E-5,
1.67866272814283E-5,1.69621513005353E-5,1.81338315460707E-5,1.98906334656536E-5,
2.06132424588236E-5),.UNSPECIFIED.);
#25382=B_SPLINE_CURVE_WITH_KNOTS('',3,(#393647,#393648,#393649,#393650),
 .UNSPECIFIED.,.F.,.F.,(4,4),(4.33680868994202E-19,0.00010938435327491),
 .UNSPECIFIED.);
#25383=B_SPLINE_CURVE_WITH_KNOTS('',3,(#393677,#393678,#393679,#393680,
#393681,#393682,#393683,#393684,#393685,#393686,#393687,#393688,#393689,
#393690,#393691,#393692,#393693,#393694,#393695,#393696,#393697,#393698,
#393699,#393700,#393701,#393702,#393703,#393704,#393705,#393706,#393707,
#393708,#393709,#393710),.UNSPECIFIED.,.F.,.F.,(4,3,3,3,3,3,3,3,3,3,3,4),
(2.16840434497101E-19,2.09623992729444E-6,3.17176647120207E-6,4.8263618194376E-6,
5.01000917339953E-6,6.13126454147488E-6,8.60486650288845E-6,9.21144281170475E-6,
1.24722301135761E-5,1.42666454787854E-5,2.04670653756963E-5,2.08026438176801E-5),
 .UNSPECIFIED.);
#25384=B_SPLINE_CURVE_WITH_KNOTS('',3,(#393711,#393712,#393713,#393714),
 .UNSPECIFIED.,.F.,.F.,(4,4),(0.,0.000109384345496908),.UNSPECIFIED.);
#25385=B_SPLINE_CURVE_WITH_KNOTS('',3,(#393819,#393820,#393821,#393822),
 .UNSPECIFIED.,.F.,.F.,(4,4),(0.,9.54361881492176E-5),.UNSPECIFIED.);
#25386=B_SPLINE_CURVE_WITH_KNOTS('',3,(#393827,#393828,#393829,#393830,
#393831,#393832,#393833),.UNSPECIFIED.,.F.,.F.,(4,3,4),(0.,4.41069704323468E-5,
0.000113970027818833),.UNSPECIFIED.);
#25387=B_SPLINE_CURVE_WITH_KNOTS('',3,(#393839,#393840,#393841,#393842),
 .UNSPECIFIED.,.F.,.F.,(4,4),(0.,9.54361881492176E-5),.UNSPECIFIED.);
#25388=B_SPLINE_CURVE_WITH_KNOTS('',3,(#393846,#393847,#393848,#393849,
#393850,#393851,#393852),.UNSPECIFIED.,.F.,.F.,(4,3,4),(0.,6.98630244191492E-5,
0.00011396997403809),.UNSPECIFIED.);
#25389=B_SPLINE_CURVE_WITH_KNOTS('',3,(#393855,#393856,#393857,#393858,
#393859,#393860,#393861,#393862,#393863,#393864,#393865,#393866,#393867,
#393868,#393869,#393870,#393871,#393872,#393873,#393874,#393875,#393876,
#393877,#393878,#393879,#393880,#393881,#393882,#393883,#393884,#393885,
#393886,#393887,#393888,#393889,#393890,#393891,#393892,#393893,#393894,
#393895,#393896,#393897,#393898,#393899,#393900,#393901,#393902,#393903),
 .UNSPECIFIED.,.F.,.F.,(4,3,3,3,3,3,3,3,3,3,3,3,3,3,3,3,4),(0.,1.53100299373406E-6,
4.52554775679239E-6,7.01151246291597E-6,9.26752933799951E-6,1.03084066197172E-5,
1.17138990826861E-5,1.22284894984076E-5,1.30315035324813E-5,1.3836372849781E-5,
1.40464197777494E-5,1.54597749564638E-5,1.62073588704065E-5,1.92092968712532E-5,
1.9523441688255E-5,2.37637844577512E-5,2.61487188977251E-5),
 .UNSPECIFIED.);
#25390=B_SPLINE_CURVE_WITH_KNOTS('',3,(#393918,#393919,#393920,#393921,
#393922,#393923,#393924,#393925,#393926,#393927,#393928,#393929,#393930,
#393931,#393932,#393933,#393934,#393935,#393936,#393937,#393938,#393939,
#393940,#393941,#393942,#393943,#393944,#393945,#393946,#393947,#393948),
 .UNSPECIFIED.,.F.,.F.,(4,3,3,3,3,3,3,3,3,3,4),(0.,3.95507910398327E-6,
7.53768426604179E-6,1.19904533335349E-5,1.40475043392584E-5,1.51452104275965E-5,
1.67866272814327E-5,1.69621513005355E-5,1.8133831546071E-5,1.98906334656535E-5,
2.06132424588242E-5),.UNSPECIFIED.);
#25391=B_SPLINE_CURVE_WITH_KNOTS('',3,(#393951,#393952,#393953,#393954),
 .UNSPECIFIED.,.F.,.F.,(4,4),(4.33680868994202E-19,0.00010938435327491),
 .UNSPECIFIED.);
#25392=B_SPLINE_CURVE_WITH_KNOTS('',3,(#393981,#393982,#393983,#393984,
#393985,#393986,#393987,#393988,#393989,#393990,#393991,#393992,#393993,
#393994,#393995,#393996,#393997,#393998,#393999,#394000,#394001,#394002,
#394003,#394004,#394005,#394006,#394007,#394008,#394009,#394010,#394011,
#394012,#394013,#394014),.UNSPECIFIED.,.F.,.F.,(4,3,3,3,3,3,3,3,3,3,3,4),
(2.16840434497101E-19,2.09623992729472E-6,3.17176647120225E-6,4.82636181943107E-6,
5.01000917339993E-6,6.13126454147534E-6,8.6048665028888E-6,9.21144281170516E-6,
1.24722301135848E-5,1.42666454787862E-5,2.04670653757051E-5,2.08026438176813E-5),
 .UNSPECIFIED.);
#25393=B_SPLINE_CURVE_WITH_KNOTS('',3,(#394015,#394016,#394017,#394018),
 .UNSPECIFIED.,.F.,.F.,(4,4),(0.,0.000109384345496908),.UNSPECIFIED.);
#25394=B_SPLINE_CURVE_WITH_KNOTS('',3,(#394123,#394124,#394125,#394126),
 .UNSPECIFIED.,.F.,.F.,(4,4),(0.,9.54361881492176E-5),.UNSPECIFIED.);
#25395=B_SPLINE_CURVE_WITH_KNOTS('',3,(#394131,#394132,#394133,#394134,
#394135,#394136,#394137),.UNSPECIFIED.,.F.,.F.,(4,3,4),(0.,4.4106970432347E-5,
0.000113970027818834),.UNSPECIFIED.);
#25396=B_SPLINE_CURVE_WITH_KNOTS('',3,(#394143,#394144,#394145,#394146),
 .UNSPECIFIED.,.F.,.F.,(4,4),(0.,9.54361881492175E-5),.UNSPECIFIED.);
#25397=B_SPLINE_CURVE_WITH_KNOTS('',3,(#394150,#394151,#394152,#394153,
#394154,#394155,#394156),.UNSPECIFIED.,.F.,.F.,(4,3,4),(0.,6.9863024419149E-5,
0.000113969974038089),.UNSPECIFIED.);
#25398=B_SPLINE_CURVE_WITH_KNOTS('',3,(#394159,#394160,#394161,#394162,
#394163,#394164,#394165,#394166,#394167,#394168,#394169,#394170,#394171,
#394172,#394173,#394174,#394175,#394176,#394177,#394178,#394179,#394180,
#394181,#394182,#394183,#394184,#394185,#394186,#394187,#394188,#394189,
#394190,#394191,#394192,#394193,#394194,#394195,#394196,#394197,#394198,
#394199,#394200,#394201,#394202,#394203,#394204,#394205,#394206,#394207),
 .UNSPECIFIED.,.F.,.F.,(4,3,3,3,3,3,3,3,3,3,3,3,3,3,3,3,4),(0.,1.53100299373393E-6,
4.52554775679561E-6,7.01151246291605E-6,9.26752933800807E-6,1.03084066197171E-5,
1.17138990826863E-5,1.22284894984075E-5,1.30315035324816E-5,1.38363728497812E-5,
1.40464197777494E-5,1.54597749564639E-5,1.62073588704068E-5,1.92092968713281E-5,
1.95234416882556E-5,2.37637844577602E-5,2.61487188977265E-5),
 .UNSPECIFIED.);
#25399=B_SPLINE_CURVE_WITH_KNOTS('',3,(#394222,#394223,#394224,#394225,
#394226,#394227,#394228,#394229,#394230,#394231,#394232,#394233,#394234,
#394235,#394236,#394237,#394238,#394239,#394240,#394241,#394242,#394243,
#394244,#394245,#394246,#394247,#394248,#394249,#394250,#394251,#394252),
 .UNSPECIFIED.,.F.,.F.,(4,3,3,3,3,3,3,3,3,3,4),(0.,3.95507910397771E-6,
7.53768426604197E-6,1.19904533335349E-5,1.40475043392583E-5,1.51452104275962E-5,
1.67866272814353E-5,1.69621513005356E-5,1.81338315460708E-5,1.98906334656549E-5,
2.06132424588241E-5),.UNSPECIFIED.);
#25400=B_SPLINE_CURVE_WITH_KNOTS('',3,(#394255,#394256,#394257,#394258),
 .UNSPECIFIED.,.F.,.F.,(4,4),(9.69739903612216E-19,0.00010938435327491),
 .UNSPECIFIED.);
#25401=B_SPLINE_CURVE_WITH_KNOTS('',3,(#394285,#394286,#394287,#394288,
#394289,#394290,#394291,#394292,#394293,#394294,#394295,#394296,#394297,
#394298,#394299,#394300,#394301,#394302,#394303,#394304,#394305,#394306,
#394307,#394308,#394309,#394310,#394311,#394312,#394313,#394314,#394315,
#394316,#394317,#394318),.UNSPECIFIED.,.F.,.F.,(4,3,3,3,3,3,3,3,3,3,3,4),
(0.,2.09623992729454E-6,3.17176647120207E-6,4.82636181943974E-6,5.01000917339967E-6,
6.13126454147483E-6,8.60486650288849E-6,9.21144281170483E-6,1.24722301135987E-5,
1.42666454787853E-5,2.04670653757088E-5,2.080264381768E-5),
 .UNSPECIFIED.);
#25402=B_SPLINE_CURVE_WITH_KNOTS('',3,(#394319,#394320,#394321,#394322),
 .UNSPECIFIED.,.F.,.F.,(4,4),(0.,0.000109384345496908),.UNSPECIFIED.);
#25403=B_SPLINE_CURVE_WITH_KNOTS('',3,(#394427,#394428,#394429,#394430),
 .UNSPECIFIED.,.F.,.F.,(4,4),(0.,9.54361881492175E-5),.UNSPECIFIED.);
#25404=B_SPLINE_CURVE_WITH_KNOTS('',3,(#394435,#394436,#394437,#394438,
#394439,#394440,#394441),.UNSPECIFIED.,.F.,.F.,(4,3,4),(0.,4.4106970432347E-5,
0.000113970027818834),.UNSPECIFIED.);
#25405=B_SPLINE_CURVE_WITH_KNOTS('',3,(#394447,#394448,#394449,#394450),
 .UNSPECIFIED.,.F.,.F.,(4,4),(0.,9.54361881492177E-5),.UNSPECIFIED.);
#25406=B_SPLINE_CURVE_WITH_KNOTS('',3,(#394454,#394455,#394456,#394457,
#394458,#394459,#394460),.UNSPECIFIED.,.F.,.F.,(4,3,4),(0.,6.98630244191489E-5,
0.000113969974038089),.UNSPECIFIED.);
#25407=B_SPLINE_CURVE_WITH_KNOTS('',3,(#394463,#394464,#394465,#394466,
#394467,#394468,#394469,#394470,#394471,#394472,#394473,#394474,#394475,
#394476,#394477,#394478,#394479,#394480,#394481,#394482,#394483,#394484,
#394485,#394486,#394487,#394488,#394489,#394490,#394491,#394492,#394493,
#394494,#394495,#394496,#394497,#394498,#394499,#394500,#394501,#394502,
#394503,#394504,#394505,#394506,#394507,#394508,#394509,#394510,#394511),
 .UNSPECIFIED.,.F.,.F.,(4,3,3,3,3,3,3,3,3,3,3,3,3,3,3,3,4),(0.,1.53100299373408E-6,
4.52554775679461E-6,7.01151246291609E-6,9.26752933799773E-6,1.03084066197175E-5,
1.17138990826864E-5,1.22284894984077E-5,1.3031503532482E-5,1.38363728497815E-5,
1.40464197777496E-5,1.54597749564642E-5,1.62073588704071E-5,1.9209296871317E-5,
1.95234416882557E-5,2.37637844577593E-5,2.61487188977264E-5),
 .UNSPECIFIED.);
#25408=B_SPLINE_CURVE_WITH_KNOTS('',3,(#394526,#394527,#394528,#394529,
#394530,#394531,#394532,#394533,#394534,#394535,#394536,#394537,#394538,
#394539,#394540,#394541,#394542,#394543,#394544,#394545,#394546,#394547,
#394548,#394549,#394550,#394551,#394552,#394553,#394554,#394555,#394556),
 .UNSPECIFIED.,.F.,.F.,(4,3,3,3,3,3,3,3,3,3,4),(0.,3.95507910397035E-6,
7.53768426604196E-6,1.1990453333535E-5,1.40475043392584E-5,1.51452104275963E-5,
1.67866272814298E-5,1.69621513005357E-5,1.8133831546071E-5,1.98906334656556E-5,
2.06132424588243E-5),.UNSPECIFIED.);
#25409=B_SPLINE_CURVE_WITH_KNOTS('',3,(#394559,#394560,#394561,#394562),
 .UNSPECIFIED.,.F.,.F.,(4,4),(9.69739903612216E-19,0.00010938435327491),
 .UNSPECIFIED.);
#25410=B_SPLINE_CURVE_WITH_KNOTS('',3,(#394589,#394590,#394591,#394592,
#394593,#394594,#394595,#394596,#394597,#394598,#394599,#394600,#394601,
#394602,#394603,#394604,#394605,#394606,#394607,#394608,#394609,#394610,
#394611,#394612,#394613,#394614,#394615,#394616,#394617,#394618,#394619,
#394620,#394621,#394622),.UNSPECIFIED.,.F.,.F.,(4,3,3,3,3,3,3,3,3,3,3,4),
(0.,2.09623992729433E-6,3.17176647120226E-6,4.82636181944028E-6,5.01000917339988E-6,
6.1312645414751E-6,8.60486650288875E-6,9.21144281170504E-6,1.2472230113614E-5,
1.4266645478786E-5,2.04670653756726E-5,2.0802643817681E-5),
 .UNSPECIFIED.);
#25411=B_SPLINE_CURVE_WITH_KNOTS('',3,(#394623,#394624,#394625,#394626),
 .UNSPECIFIED.,.F.,.F.,(4,4),(0.,0.000109384345496908),.UNSPECIFIED.);
#25412=B_SPLINE_CURVE_WITH_KNOTS('',3,(#394731,#394732,#394733,#394734),
 .UNSPECIFIED.,.F.,.F.,(4,4),(0.,9.54361881492177E-5),.UNSPECIFIED.);
#25413=B_SPLINE_CURVE_WITH_KNOTS('',3,(#394739,#394740,#394741,#394742,
#394743,#394744,#394745),.UNSPECIFIED.,.F.,.F.,(4,3,4),(0.,4.4106970432347E-5,
0.000113970027818834),.UNSPECIFIED.);
#25414=B_SPLINE_CURVE_WITH_KNOTS('',3,(#394751,#394752,#394753,#394754),
 .UNSPECIFIED.,.F.,.F.,(4,4),(4.33680868994202E-19,9.54361881492179E-5),
 .UNSPECIFIED.);
#25415=B_SPLINE_CURVE_WITH_KNOTS('',3,(#394758,#394759,#394760,#394761,
#394762,#394763,#394764),.UNSPECIFIED.,.F.,.F.,(4,3,4),(0.,6.9863024419149E-5,
0.000113969974038089),.UNSPECIFIED.);
#25416=B_SPLINE_CURVE_WITH_KNOTS('',3,(#394767,#394768,#394769,#394770,
#394771,#394772,#394773,#394774,#394775,#394776,#394777,#394778,#394779,
#394780,#394781,#394782,#394783,#394784,#394785,#394786,#394787,#394788,
#394789,#394790,#394791,#394792,#394793,#394794,#394795,#394796,#394797,
#394798,#394799,#394800,#394801,#394802,#394803,#394804,#394805,#394806,
#394807,#394808,#394809,#394810,#394811,#394812,#394813,#394814,#394815),
 .UNSPECIFIED.,.F.,.F.,(4,3,3,3,3,3,3,3,3,3,3,3,3,3,3,3,4),(0.,1.53100299373416E-6,
4.52554775679475E-6,7.01151246291604E-6,9.26752933800239E-6,1.03084066197174E-5,
1.17138990826861E-5,1.22284894984075E-5,1.30315035324821E-5,1.38363728497814E-5,
1.40464197777497E-5,1.54597749564641E-5,1.62073588704072E-5,1.92092968713027E-5,
1.95234416882558E-5,2.37637844577584E-5,2.61487188977266E-5),
 .UNSPECIFIED.);
#25417=B_SPLINE_CURVE_WITH_KNOTS('',3,(#394830,#394831,#394832,#394833,
#394834,#394835,#394836,#394837,#394838,#394839,#394840,#394841,#394842,
#394843,#394844,#394845,#394846,#394847,#394848,#394849,#394850,#394851,
#394852,#394853,#394854,#394855,#394856,#394857,#394858,#394859,#394860),
 .UNSPECIFIED.,.F.,.F.,(4,3,3,3,3,3,3,3,3,3,4),(0.,3.95507910397657E-6,
7.53768426604195E-6,1.1990453333535E-5,1.40475043392586E-5,1.51452104275963E-5,
1.6786627281397E-5,1.69621513005358E-5,1.81338315460709E-5,1.98906334656537E-5,
2.06132424588241E-5),.UNSPECIFIED.);
#25418=B_SPLINE_CURVE_WITH_KNOTS('',3,(#394863,#394864,#394865,#394866),
 .UNSPECIFIED.,.F.,.F.,(4,4),(4.33680868994202E-19,0.00010938435327491),
 .UNSPECIFIED.);
#25419=B_SPLINE_CURVE_WITH_KNOTS('',3,(#394893,#394894,#394895,#394896,
#394897,#394898,#394899,#394900,#394901,#394902,#394903,#394904,#394905,
#394906,#394907,#394908,#394909,#394910,#394911,#394912,#394913,#394914,
#394915,#394916,#394917,#394918,#394919,#394920,#394921,#394922,#394923,
#394924,#394925,#394926),.UNSPECIFIED.,.F.,.F.,(4,3,3,3,3,3,3,3,3,3,3,4),
(2.16840434497101E-19,2.09623992729442E-6,3.17176647120239E-6,4.82636181941647E-6,
5.01000917339955E-6,6.13126454147491E-6,8.60486650288825E-6,9.21144281170468E-6,
1.2472230113594E-5,1.42666454787851E-5,2.0467065375728E-5,2.08026438176793E-5),
 .UNSPECIFIED.);
#25420=B_SPLINE_CURVE_WITH_KNOTS('',3,(#394927,#394928,#394929,#394930),
 .UNSPECIFIED.,.F.,.F.,(4,4),(0.,0.000109384345496908),.UNSPECIFIED.);
#25421=B_SPLINE_CURVE_WITH_KNOTS('',3,(#395035,#395036,#395037,#395038),
 .UNSPECIFIED.,.F.,.F.,(4,4),(0.,9.54361881492175E-5),.UNSPECIFIED.);
#25422=B_SPLINE_CURVE_WITH_KNOTS('',3,(#395043,#395044,#395045,#395046,
#395047,#395048,#395049),.UNSPECIFIED.,.F.,.F.,(4,3,4),(0.,4.4106970432347E-5,
0.000113970027818833),.UNSPECIFIED.);
#25423=B_SPLINE_CURVE_WITH_KNOTS('',3,(#395055,#395056,#395057,#395058),
 .UNSPECIFIED.,.F.,.F.,(4,4),(4.33680868994202E-19,9.54361881492179E-5),
 .UNSPECIFIED.);
#25424=B_SPLINE_CURVE_WITH_KNOTS('',3,(#395062,#395063,#395064,#395065,
#395066,#395067,#395068),.UNSPECIFIED.,.F.,.F.,(4,3,4),(0.,6.98630244191493E-5,
0.00011396997403809),.UNSPECIFIED.);
#25425=B_SPLINE_CURVE_WITH_KNOTS('',3,(#395071,#395072,#395073,#395074,
#395075,#395076,#395077,#395078,#395079,#395080,#395081,#395082,#395083,
#395084,#395085,#395086,#395087,#395088,#395089,#395090,#395091,#395092,
#395093,#395094,#395095,#395096,#395097,#395098,#395099,#395100,#395101,
#395102,#395103,#395104,#395105,#395106,#395107,#395108,#395109,#395110,
#395111,#395112,#395113,#395114,#395115,#395116,#395117,#395118,#395119),
 .UNSPECIFIED.,.F.,.F.,(4,3,3,3,3,3,3,3,3,3,3,3,3,3,3,3,4),(0.,1.53100299373408E-6,
4.52554775678945E-6,7.01151246291589E-6,9.26752933801257E-6,1.03084066197174E-5,
1.17138990826861E-5,1.22284894984071E-5,1.30315035324817E-5,1.3836372849781E-5,
1.40464197777495E-5,1.54597749564638E-5,1.62073588704067E-5,1.92092968712444E-5,
1.95234416882552E-5,2.37637844577596E-5,2.61487188977255E-5),
 .UNSPECIFIED.);
#25426=B_SPLINE_CURVE_WITH_KNOTS('',3,(#395134,#395135,#395136,#395137,
#395138,#395139,#395140,#395141,#395142,#395143,#395144,#395145,#395146,
#395147,#395148,#395149,#395150,#395151,#395152,#395153,#395154,#395155,
#395156,#395157,#395158,#395159,#395160,#395161,#395162,#395163,#395164),
 .UNSPECIFIED.,.F.,.F.,(4,3,3,3,3,3,3,3,3,3,4),(0.,3.95507910398509E-6,
7.53768426604194E-6,1.19904533335351E-5,1.40475043392585E-5,1.51452104275963E-5,
1.67866272814167E-5,1.69621513005357E-5,1.81338315460711E-5,1.98906334656521E-5,
2.06132424588243E-5),.UNSPECIFIED.);
#25427=B_SPLINE_CURVE_WITH_KNOTS('',3,(#395167,#395168,#395169,#395170),
 .UNSPECIFIED.,.F.,.F.,(4,4),(4.33680868994202E-19,0.00010938435327491),
 .UNSPECIFIED.);
#25428=B_SPLINE_CURVE_WITH_KNOTS('',3,(#395197,#395198,#395199,#395200,
#395201,#395202,#395203,#395204,#395205,#395206,#395207,#395208,#395209,
#395210,#395211,#395212,#395213,#395214,#395215,#395216,#395217,#395218,
#395219,#395220,#395221,#395222,#395223,#395224,#395225,#395226,#395227,
#395228,#395229,#395230),.UNSPECIFIED.,.F.,.F.,(4,3,3,3,3,3,3,3,3,3,3,4),
(2.16840434497101E-19,2.09623992729456E-6,3.17176647120226E-6,4.8263618194516E-6,
5.01000917339959E-6,6.13126454147491E-6,8.60486650288858E-6,9.21144281170482E-6,
1.24722301135962E-5,1.42666454787854E-5,2.04670653756933E-5,2.08026438176799E-5),
 .UNSPECIFIED.);
#25429=B_SPLINE_CURVE_WITH_KNOTS('',3,(#395231,#395232,#395233,#395234),
 .UNSPECIFIED.,.F.,.F.,(4,4),(0.,0.000109384345496908),.UNSPECIFIED.);
#25430=B_SPLINE_CURVE_WITH_KNOTS('',3,(#395339,#395340,#395341,#395342),
 .UNSPECIFIED.,.F.,.F.,(4,4),(0.,9.54361881492173E-5),.UNSPECIFIED.);
#25431=B_SPLINE_CURVE_WITH_KNOTS('',3,(#395347,#395348,#395349,#395350,
#395351,#395352,#395353),.UNSPECIFIED.,.F.,.F.,(4,3,4),(0.,4.41069704323469E-5,
0.000113970027818833),.UNSPECIFIED.);
#25432=B_SPLINE_CURVE_WITH_KNOTS('',3,(#395359,#395360,#395361,#395362),
 .UNSPECIFIED.,.F.,.F.,(4,4),(4.47028007668187E-19,9.54361881492177E-5),
 .UNSPECIFIED.);
#25433=B_SPLINE_CURVE_WITH_KNOTS('',3,(#395366,#395367,#395368,#395369,
#395370,#395371,#395372),.UNSPECIFIED.,.F.,.F.,(4,3,4),(0.,6.98630244191491E-5,
0.000113969974038089),.UNSPECIFIED.);
#25434=B_SPLINE_CURVE_WITH_KNOTS('',3,(#395375,#395376,#395377,#395378,
#395379,#395380,#395381,#395382,#395383,#395384,#395385,#395386,#395387,
#395388,#395389,#395390,#395391,#395392,#395393,#395394,#395395,#395396,
#395397,#395398,#395399,#395400,#395401,#395402,#395403,#395404,#395405,
#395406,#395407,#395408,#395409,#395410,#395411,#395412,#395413,#395414,
#395415,#395416,#395417,#395418,#395419,#395420,#395421,#395422,#395423),
 .UNSPECIFIED.,.F.,.F.,(4,3,3,3,3,3,3,3,3,3,3,3,3,3,3,3,4),(0.,1.5310029937341E-6,
4.52554775678762E-6,7.01151246291603E-6,9.26752933800599E-6,1.03084066197174E-5,
1.1713899082686E-5,1.22284894984073E-5,1.30315035324818E-5,1.38363728497812E-5,
1.40464197777493E-5,1.54597749564638E-5,1.62073588704067E-5,1.92092968712513E-5,
1.95234416882552E-5,2.37637844577644E-5,2.61487188977255E-5),
 .UNSPECIFIED.);
#25435=B_SPLINE_CURVE_WITH_KNOTS('',3,(#395438,#395439,#395440,#395441,
#395442,#395443,#395444,#395445,#395446,#395447,#395448,#395449,#395450,
#395451,#395452,#395453,#395454,#395455,#395456,#395457,#395458,#395459,
#395460,#395461,#395462,#395463,#395464,#395465,#395466,#395467,#395468),
 .UNSPECIFIED.,.F.,.F.,(4,3,3,3,3,3,3,3,3,3,4),(0.,3.95507910398144E-6,
7.53768426604199E-6,1.1990453333535E-5,1.40475043392586E-5,1.51452104275965E-5,
1.67866272814099E-5,1.69621513005358E-5,1.81338315460712E-5,1.98906334656528E-5,
2.06132424588245E-5),.UNSPECIFIED.);
#25436=B_SPLINE_CURVE_WITH_KNOTS('',3,(#395471,#395472,#395473,#395474),
 .UNSPECIFIED.,.F.,.F.,(4,4),(4.47028007668187E-19,0.00010938435327491),
 .UNSPECIFIED.);
#25437=B_SPLINE_CURVE_WITH_KNOTS('',3,(#395501,#395502,#395503,#395504,
#395505,#395506,#395507,#395508,#395509,#395510,#395511,#395512,#395513,
#395514,#395515,#395516,#395517,#395518,#395519,#395520,#395521,#395522,
#395523,#395524,#395525,#395526,#395527,#395528,#395529,#395530,#395531,
#395532,#395533,#395534),.UNSPECIFIED.,.F.,.F.,(4,3,3,3,3,3,3,3,3,3,3,4),
(0.,2.09623992729446E-6,3.17176647120222E-6,4.82636181943375E-6,5.0100091733998E-6,
6.13126454147495E-6,8.60486650288865E-6,9.21144281170494E-6,1.24722301135964E-5,
1.42666454787856E-5,2.04670653757012E-5,2.08026438176803E-5),
 .UNSPECIFIED.);
#25438=B_SPLINE_CURVE_WITH_KNOTS('',3,(#395535,#395536,#395537,#395538),
 .UNSPECIFIED.,.F.,.F.,(4,4),(0.,0.000109384345496908),.UNSPECIFIED.);
#25439=B_SPLINE_CURVE_WITH_KNOTS('',3,(#395643,#395644,#395645,#395646),
 .UNSPECIFIED.,.F.,.F.,(4,4),(0.,9.54361881492173E-5),.UNSPECIFIED.);
#25440=B_SPLINE_CURVE_WITH_KNOTS('',3,(#395651,#395652,#395653,#395654,
#395655,#395656,#395657),.UNSPECIFIED.,.F.,.F.,(4,3,4),(0.,4.41069704323467E-5,
0.000113970027818833),.UNSPECIFIED.);
#25441=B_SPLINE_CURVE_WITH_KNOTS('',3,(#395663,#395664,#395665,#395666),
 .UNSPECIFIED.,.F.,.F.,(4,4),(4.33680868994202E-19,9.5436188149218E-5),
 .UNSPECIFIED.);
#25442=B_SPLINE_CURVE_WITH_KNOTS('',3,(#395670,#395671,#395672,#395673,
#395674,#395675,#395676),.UNSPECIFIED.,.F.,.F.,(4,3,4),(0.,6.98630244191495E-5,
0.000113969974038089),.UNSPECIFIED.);
#25443=B_SPLINE_CURVE_WITH_KNOTS('',3,(#395679,#395680,#395681,#395682,
#395683,#395684,#395685,#395686,#395687,#395688,#395689,#395690,#395691,
#395692,#395693,#395694,#395695,#395696,#395697,#395698,#395699,#395700,
#395701,#395702,#395703,#395704,#395705,#395706,#395707,#395708,#395709,
#395710,#395711,#395712,#395713,#395714,#395715,#395716,#395717,#395718,
#395719,#395720,#395721,#395722,#395723,#395724,#395725,#395726,#395727),
 .UNSPECIFIED.,.F.,.F.,(4,3,3,3,3,3,3,3,3,3,3,3,3,3,3,3,4),(0.,1.53100299373412E-6,
4.52554775679016E-6,7.01151246291591E-6,9.26752933800179E-6,1.03084066197171E-5,
1.17138990826861E-5,1.22284894984074E-5,1.30315035324818E-5,1.38363728497813E-5,
1.40464197777495E-5,1.54597749564641E-5,1.62073588704071E-5,1.92092968712855E-5,
1.95234416882559E-5,2.37637844577606E-5,2.6148718897727E-5),
 .UNSPECIFIED.);
#25444=B_SPLINE_CURVE_WITH_KNOTS('',3,(#395742,#395743,#395744,#395745,
#395746,#395747,#395748,#395749,#395750,#395751,#395752,#395753,#395754,
#395755,#395756,#395757,#395758,#395759,#395760,#395761,#395762,#395763,
#395764,#395765,#395766,#395767,#395768,#395769,#395770,#395771,#395772),
 .UNSPECIFIED.,.F.,.F.,(4,3,3,3,3,3,3,3,3,3,4),(0.,3.95507910397768E-6,
7.53768426604198E-6,1.19904533335351E-5,1.40475043392586E-5,1.51452104275964E-5,
1.67866272814183E-5,1.69621513005358E-5,1.81338315460711E-5,1.98906334656542E-5,
2.06132424588245E-5),.UNSPECIFIED.);
#25445=B_SPLINE_CURVE_WITH_KNOTS('',3,(#395775,#395776,#395777,#395778),
 .UNSPECIFIED.,.F.,.F.,(4,4),(4.47028007668187E-19,0.00010938435327491),
 .UNSPECIFIED.);
#25446=B_SPLINE_CURVE_WITH_KNOTS('',3,(#395805,#395806,#395807,#395808,
#395809,#395810,#395811,#395812,#395813,#395814,#395815,#395816,#395817,
#395818,#395819,#395820,#395821,#395822,#395823,#395824,#395825,#395826,
#395827,#395828,#395829,#395830,#395831,#395832,#395833,#395834,#395835,
#395836,#395837,#395838),.UNSPECIFIED.,.F.,.F.,(4,3,3,3,3,3,3,3,3,3,3,4),
(1.0842021724855E-19,2.09623992729441E-6,3.17176647120226E-6,4.82636181944059E-6,
5.01000917339961E-6,6.13126454147497E-6,8.60486650288839E-6,9.21144281170474E-6,
1.24722301136207E-5,1.4266645478785E-5,2.04670653756626E-5,2.08026438176791E-5),
 .UNSPECIFIED.);
#25447=B_SPLINE_CURVE_WITH_KNOTS('',3,(#395839,#395840,#395841,#395842),
 .UNSPECIFIED.,.F.,.F.,(4,4),(0.,0.000109384345496908),.UNSPECIFIED.);
#25448=B_SPLINE_CURVE_WITH_KNOTS('',3,(#395947,#395948,#395949,#395950),
 .UNSPECIFIED.,.F.,.F.,(4,4),(0.,9.54361881492178E-5),.UNSPECIFIED.);
#25449=B_SPLINE_CURVE_WITH_KNOTS('',3,(#395955,#395956,#395957,#395958,
#395959,#395960,#395961),.UNSPECIFIED.,.F.,.F.,(4,3,4),(0.,4.41069704323469E-5,
0.000113970027818833),.UNSPECIFIED.);
#25450=B_SPLINE_CURVE_WITH_KNOTS('',3,(#395967,#395968,#395969,#395970),
 .UNSPECIFIED.,.F.,.F.,(4,4),(4.47028007668187E-19,9.54361881492176E-5),
 .UNSPECIFIED.);
#25451=B_SPLINE_CURVE_WITH_KNOTS('',3,(#395974,#395975,#395976,#395977,
#395978,#395979,#395980),.UNSPECIFIED.,.F.,.F.,(4,3,4),(0.,6.98630244191491E-5,
0.000113969974038089),.UNSPECIFIED.);
#25452=B_SPLINE_CURVE_WITH_KNOTS('',3,(#395983,#395984,#395985,#395986,
#395987,#395988,#395989,#395990,#395991,#395992,#395993,#395994,#395995,
#395996,#395997,#395998,#395999,#396000,#396001,#396002,#396003,#396004,
#396005,#396006,#396007,#396008,#396009,#396010,#396011,#396012,#396013,
#396014,#396015,#396016,#396017,#396018,#396019,#396020,#396021,#396022,
#396023,#396024,#396025,#396026,#396027,#396028,#396029,#396030,#396031),
 .UNSPECIFIED.,.F.,.F.,(4,3,3,3,3,3,3,3,3,3,3,3,3,3,3,3,4),(0.,1.53100299373409E-6,
4.52554775678942E-6,7.01151246291605E-6,9.26752933799663E-6,1.03084066197173E-5,
1.17138990826864E-5,1.22284894984076E-5,1.30315035324818E-5,1.38363728497813E-5,
1.40464197777496E-5,1.5459774956464E-5,1.62073588704069E-5,1.92092968712812E-5,
1.95234416882555E-5,2.3763784457762E-5,2.61487188977261E-5),
 .UNSPECIFIED.);
#25453=B_SPLINE_CURVE_WITH_KNOTS('',3,(#396046,#396047,#396048,#396049,
#396050,#396051,#396052,#396053,#396054,#396055,#396056,#396057,#396058,
#396059,#396060,#396061,#396062,#396063,#396064,#396065,#396066,#396067,
#396068,#396069,#396070,#396071,#396072,#396073,#396074,#396075,#396076),
 .UNSPECIFIED.,.F.,.F.,(4,3,3,3,3,3,3,3,3,3,4),(0.,3.95507910397385E-6,
7.53768426604199E-6,1.19904533335351E-5,1.40475043392587E-5,1.51452104275965E-5,
1.67866272814042E-5,1.69621513005359E-5,1.81338315460712E-5,1.98906334656544E-5,
2.06132424588247E-5),.UNSPECIFIED.);
#25454=B_SPLINE_CURVE_WITH_KNOTS('',3,(#396079,#396080,#396081,#396082),
 .UNSPECIFIED.,.F.,.F.,(4,4),(4.47028007668187E-19,0.00010938435327491),
 .UNSPECIFIED.);
#25455=B_SPLINE_CURVE_WITH_KNOTS('',3,(#396109,#396110,#396111,#396112,
#396113,#396114,#396115,#396116,#396117,#396118,#396119,#396120,#396121,
#396122,#396123,#396124,#396125,#396126,#396127,#396128,#396129,#396130,
#396131,#396132,#396133,#396134,#396135,#396136,#396137,#396138,#396139,
#396140,#396141,#396142),.UNSPECIFIED.,.F.,.F.,(4,3,3,3,3,3,3,3,3,3,3,4),
(1.0842021724855E-19,2.09623992729443E-6,3.17176647120216E-6,4.82636181943593E-6,
5.01000917339959E-6,6.13126454147479E-6,8.60486650288851E-6,9.21144281170492E-6,
1.24722301136026E-5,1.42666454787855E-5,2.04670653756902E-5,2.08026438176802E-5),
 .UNSPECIFIED.);
#25456=B_SPLINE_CURVE_WITH_KNOTS('',3,(#396143,#396144,#396145,#396146),
 .UNSPECIFIED.,.F.,.F.,(4,4),(0.,0.000109384345496908),.UNSPECIFIED.);
#25457=B_SPLINE_CURVE_WITH_KNOTS('',3,(#396251,#396252,#396253,#396254),
 .UNSPECIFIED.,.F.,.F.,(4,4),(0.,9.54361881492174E-5),.UNSPECIFIED.);
#25458=B_SPLINE_CURVE_WITH_KNOTS('',3,(#396259,#396260,#396261,#396262,
#396263,#396264,#396265),.UNSPECIFIED.,.F.,.F.,(4,3,4),(0.,4.41069704323467E-5,
0.000113970027818833),.UNSPECIFIED.);
#25459=B_SPLINE_CURVE_WITH_KNOTS('',3,(#396271,#396272,#396273,#396274),
 .UNSPECIFIED.,.F.,.F.,(4,4),(4.47028007668187E-19,9.54361881492181E-5),
 .UNSPECIFIED.);
#25460=B_SPLINE_CURVE_WITH_KNOTS('',3,(#396278,#396279,#396280,#396281,
#396282,#396283,#396284),.UNSPECIFIED.,.F.,.F.,(4,3,4),(0.,6.98630244191495E-5,
0.000113969974038089),.UNSPECIFIED.);
#25461=B_SPLINE_CURVE_WITH_KNOTS('',3,(#396287,#396288,#396289,#396290,
#396291,#396292,#396293,#396294,#396295,#396296,#396297,#396298,#396299,
#396300,#396301,#396302,#396303,#396304,#396305,#396306,#396307,#396308,
#396309,#396310,#396311,#396312,#396313,#396314,#396315,#396316,#396317,
#396318,#396319,#396320,#396321,#396322,#396323,#396324,#396325,#396326,
#396327,#396328,#396329,#396330,#396331,#396332,#396333,#396334,#396335),
 .UNSPECIFIED.,.F.,.F.,(4,3,3,3,3,3,3,3,3,3,3,3,3,3,3,3,4),(0.,1.53100299373397E-6,
4.52554775678549E-6,7.01151246291585E-6,9.26752933799876E-6,1.03084066197172E-5,
1.17138990826861E-5,1.22284894984074E-5,1.30315035324817E-5,1.38363728497813E-5,
1.40464197777495E-5,1.54597749564641E-5,1.6207358870407E-5,1.92092968712915E-5,
1.95234416882557E-5,2.37637844577633E-5,2.61487188977267E-5),
 .UNSPECIFIED.);
#25462=B_SPLINE_CURVE_WITH_KNOTS('',3,(#396350,#396351,#396352,#396353,
#396354,#396355,#396356,#396357,#396358,#396359,#396360,#396361,#396362,
#396363,#396364,#396365,#396366,#396367,#396368,#396369,#396370,#396371,
#396372,#396373,#396374,#396375,#396376,#396377,#396378,#396379,#396380),
 .UNSPECIFIED.,.F.,.F.,(4,3,3,3,3,3,3,3,3,3,4),(0.,3.95507910397337E-6,
7.53768426604201E-6,1.1990453333535E-5,1.40475043392586E-5,1.51452104275964E-5,
1.67866272814123E-5,1.69621513005357E-5,1.81338315460711E-5,1.98906334656556E-5,
2.06132424588244E-5),.UNSPECIFIED.);
#25463=B_SPLINE_CURVE_WITH_KNOTS('',3,(#396383,#396384,#396385,#396386),
 .UNSPECIFIED.,.F.,.F.,(4,4),(4.63171371119878E-19,0.00010938435327491),
 .UNSPECIFIED.);
#25464=B_SPLINE_CURVE_WITH_KNOTS('',3,(#396413,#396414,#396415,#396416,
#396417,#396418,#396419,#396420,#396421,#396422,#396423,#396424,#396425,
#396426,#396427,#396428,#396429,#396430,#396431,#396432,#396433,#396434,
#396435,#396436,#396437,#396438,#396439,#396440,#396441,#396442,#396443,
#396444,#396445,#396446),.UNSPECIFIED.,.F.,.F.,(4,3,3,3,3,3,3,3,3,3,3,4),
(1.62630325872826E-19,2.0962399272944E-6,3.17176647120221E-6,4.8263618194282E-6,
5.01000917339958E-6,6.1312645414749E-6,8.60486650288834E-6,9.21144281170484E-6,
1.24722301135973E-5,1.42666454787854E-5,2.04670653756913E-5,2.080264381768E-5),
 .UNSPECIFIED.);
#25465=B_SPLINE_CURVE_WITH_KNOTS('',3,(#396447,#396448,#396449,#396450),
 .UNSPECIFIED.,.F.,.F.,(4,4),(0.,0.000109384345496908),.UNSPECIFIED.);
#25466=B_SPLINE_CURVE_WITH_KNOTS('',3,(#396555,#396556,#396557,#396558),
 .UNSPECIFIED.,.F.,.F.,(4,4),(0.,9.54361881492176E-5),.UNSPECIFIED.);
#25467=B_SPLINE_CURVE_WITH_KNOTS('',3,(#396563,#396564,#396565,#396566,
#396567,#396568,#396569),.UNSPECIFIED.,.F.,.F.,(4,3,4),(0.,4.4106970432347E-5,
0.000113970027818834),.UNSPECIFIED.);
#25468=B_SPLINE_CURVE_WITH_KNOTS('',3,(#396575,#396576,#396577,#396578),
 .UNSPECIFIED.,.F.,.F.,(4,4),(4.47028007668187E-19,9.54361881492177E-5),
 .UNSPECIFIED.);
#25469=B_SPLINE_CURVE_WITH_KNOTS('',3,(#396582,#396583,#396584,#396585,
#396586,#396587,#396588),.UNSPECIFIED.,.F.,.F.,(4,3,4),(0.,6.98630244191489E-5,
0.000113969974038089),.UNSPECIFIED.);
#25470=B_SPLINE_CURVE_WITH_KNOTS('',3,(#396591,#396592,#396593,#396594,
#396595,#396596,#396597,#396598,#396599,#396600,#396601,#396602,#396603,
#396604,#396605,#396606,#396607,#396608,#396609,#396610,#396611,#396612,
#396613,#396614,#396615,#396616,#396617,#396618,#396619,#396620,#396621,
#396622,#396623,#396624,#396625,#396626,#396627,#396628,#396629,#396630,
#396631,#396632,#396633,#396634,#396635,#396636,#396637,#396638,#396639),
 .UNSPECIFIED.,.F.,.F.,(4,3,3,3,3,3,3,3,3,3,3,3,3,3,3,3,4),(0.,1.53100299373419E-6,
4.52554775679508E-6,7.01151246291607E-6,9.26752933799554E-6,1.03084066197173E-5,
1.17138990826862E-5,1.22284894984074E-5,1.30315035324817E-5,1.38363728497813E-5,
1.40464197777495E-5,1.54597749564641E-5,1.6207358870407E-5,1.92092968713182E-5,
1.95234416882557E-5,2.37637844577564E-5,2.61487188977266E-5),
 .UNSPECIFIED.);
#25471=B_SPLINE_CURVE_WITH_KNOTS('',3,(#396654,#396655,#396656,#396657,
#396658,#396659,#396660,#396661,#396662,#396663,#396664,#396665,#396666,
#396667,#396668,#396669,#396670,#396671,#396672,#396673,#396674,#396675,
#396676,#396677,#396678,#396679,#396680,#396681,#396682,#396683,#396684),
 .UNSPECIFIED.,.F.,.F.,(4,3,3,3,3,3,3,3,3,3,4),(0.,3.95507910399129E-6,
7.53768426604195E-6,1.19904533335351E-5,1.40475043392585E-5,1.51452104275963E-5,
1.67866272814177E-5,1.69621513005356E-5,1.81338315460709E-5,1.98906334656484E-5,
2.0613242458824E-5),.UNSPECIFIED.);
#25472=B_SPLINE_CURVE_WITH_KNOTS('',3,(#396687,#396688,#396689,#396690),
 .UNSPECIFIED.,.F.,.F.,(4,4),(4.63171371119878E-19,0.00010938435327491),
 .UNSPECIFIED.);
#25473=B_SPLINE_CURVE_WITH_KNOTS('',3,(#396717,#396718,#396719,#396720,
#396721,#396722,#396723,#396724,#396725,#396726,#396727,#396728,#396729,
#396730,#396731,#396732,#396733,#396734,#396735,#396736,#396737,#396738,
#396739,#396740,#396741,#396742,#396743,#396744,#396745,#396746,#396747,
#396748,#396749,#396750),.UNSPECIFIED.,.F.,.F.,(4,3,3,3,3,3,3,3,3,3,3,4),
(1.62630325872826E-19,2.09623992729438E-6,3.17176647120219E-6,4.82636181942821E-6,
5.01000917339952E-6,6.13126454147489E-6,8.6048665028884E-6,9.21144281170481E-6,
1.24722301135895E-5,1.42666454787855E-5,2.04670653756765E-5,2.080264381768E-5),
 .UNSPECIFIED.);
#25474=B_SPLINE_CURVE_WITH_KNOTS('',3,(#396751,#396752,#396753,#396754),
 .UNSPECIFIED.,.F.,.F.,(4,4),(0.,0.000109384345496908),.UNSPECIFIED.);
#25475=B_SPLINE_CURVE_WITH_KNOTS('',3,(#396859,#396860,#396861,#396862),
 .UNSPECIFIED.,.F.,.F.,(4,4),(0.,9.54361881492173E-5),.UNSPECIFIED.);
#25476=B_SPLINE_CURVE_WITH_KNOTS('',3,(#396867,#396868,#396869,#396870,
#396871,#396872,#396873),.UNSPECIFIED.,.F.,.F.,(4,3,4),(0.,4.41069704323472E-5,
0.000113970027818834),.UNSPECIFIED.);
#25477=B_SPLINE_CURVE_WITH_KNOTS('',3,(#396879,#396880,#396881,#396882),
 .UNSPECIFIED.,.F.,.F.,(4,4),(4.48719651148014E-19,9.54361881492176E-5),
 .UNSPECIFIED.);
#25478=B_SPLINE_CURVE_WITH_KNOTS('',3,(#396886,#396887,#396888,#396889,
#396890,#396891,#396892),.UNSPECIFIED.,.F.,.F.,(4,3,4),(0.,6.98630244191491E-5,
0.000113969974038089),.UNSPECIFIED.);
#25479=B_SPLINE_CURVE_WITH_KNOTS('',3,(#396895,#396896,#396897,#396898,
#396899,#396900,#396901,#396902,#396903,#396904,#396905,#396906,#396907,
#396908,#396909,#396910,#396911,#396912,#396913,#396914,#396915,#396916,
#396917,#396918,#396919,#396920,#396921,#396922,#396923,#396924,#396925,
#396926,#396927,#396928,#396929,#396930,#396931,#396932,#396933,#396934,
#396935,#396936,#396937,#396938,#396939,#396940,#396941,#396942,#396943),
 .UNSPECIFIED.,.F.,.F.,(4,3,3,3,3,3,3,3,3,3,3,3,3,3,3,3,4),(0.,1.53100299373413E-6,
4.52554775679464E-6,7.01151246291609E-6,9.26752933800805E-6,1.03084066197173E-5,
1.17138990826862E-5,1.22284894984074E-5,1.30315035324817E-5,1.38363728497812E-5,
1.40464197777494E-5,1.54597749564639E-5,1.62073588704068E-5,1.92092968713364E-5,
1.95234416882556E-5,2.37637844577523E-5,2.61487188977263E-5),
 .UNSPECIFIED.);
#25480=B_SPLINE_CURVE_WITH_KNOTS('',3,(#396958,#396959,#396960,#396961,
#396962,#396963,#396964,#396965,#396966,#396967,#396968,#396969,#396970,
#396971,#396972,#396973,#396974,#396975,#396976,#396977,#396978,#396979,
#396980,#396981,#396982,#396983,#396984,#396985,#396986,#396987,#396988),
 .UNSPECIFIED.,.F.,.F.,(4,3,3,3,3,3,3,3,3,3,4),(0.,3.95507910397758E-6,
7.53768426604201E-6,1.1990453333535E-5,1.40475043392586E-5,1.51452104275964E-5,
1.67866272814164E-5,1.69621513005358E-5,1.81338315460713E-5,1.98906334656549E-5,
2.06132424588247E-5),.UNSPECIFIED.);
#25481=B_SPLINE_CURVE_WITH_KNOTS('',3,(#396991,#396992,#396993,#396994),
 .UNSPECIFIED.,.F.,.F.,(4,4),(4.73369422993816E-19,0.00010938435327491),
 .UNSPECIFIED.);
#25482=B_SPLINE_CURVE_WITH_KNOTS('',3,(#397021,#397022,#397023,#397024,
#397025,#397026,#397027,#397028,#397029,#397030,#397031,#397032,#397033,
#397034,#397035,#397036,#397037,#397038,#397039,#397040,#397041,#397042,
#397043,#397044,#397045,#397046,#397047,#397048,#397049,#397050,#397051,
#397052,#397053,#397054),.UNSPECIFIED.,.F.,.F.,(4,3,3,3,3,3,3,3,3,3,3,4),
(1.62630325872826E-19,2.09623992729438E-6,3.1717664712022E-6,4.82636181943908E-6,
5.01000917339962E-6,6.13126454147497E-6,8.60486650288859E-6,9.21144281170501E-6,
1.24722301136026E-5,1.42666454787856E-5,2.04670653756757E-5,2.08026438176802E-5),
 .UNSPECIFIED.);
#25483=B_SPLINE_CURVE_WITH_KNOTS('',3,(#397055,#397056,#397057,#397058),
 .UNSPECIFIED.,.F.,.F.,(4,4),(0.,0.000109384345496908),.UNSPECIFIED.);
#25484=B_SPLINE_CURVE_WITH_KNOTS('',3,(#397163,#397164,#397165,#397166),
 .UNSPECIFIED.,.F.,.F.,(4,4),(0.,9.54361881492177E-5),.UNSPECIFIED.);
#25485=B_SPLINE_CURVE_WITH_KNOTS('',3,(#397171,#397172,#397173,#397174,
#397175,#397176,#397177),.UNSPECIFIED.,.F.,.F.,(4,3,4),(0.,4.41069704323469E-5,
0.000113970027818834),.UNSPECIFIED.);
#25486=B_SPLINE_CURVE_WITH_KNOTS('',3,(#397183,#397184,#397185,#397186),
 .UNSPECIFIED.,.F.,.F.,(4,4),(4.5436350575631E-19,9.54361881492179E-5),
 .UNSPECIFIED.);
#25487=B_SPLINE_CURVE_WITH_KNOTS('',3,(#397190,#397191,#397192,#397193,
#397194,#397195,#397196),.UNSPECIFIED.,.F.,.F.,(4,3,4),(0.,6.9863024419149E-5,
0.000113969974038089),.UNSPECIFIED.);
#25488=B_SPLINE_CURVE_WITH_KNOTS('',3,(#397199,#397200,#397201,#397202,
#397203,#397204,#397205,#397206,#397207,#397208,#397209,#397210,#397211,
#397212,#397213,#397214,#397215,#397216,#397217,#397218,#397219,#397220,
#397221,#397222,#397223,#397224,#397225,#397226,#397227,#397228,#397229,
#397230,#397231,#397232,#397233,#397234,#397235,#397236,#397237,#397238,
#397239,#397240,#397241,#397242,#397243,#397244,#397245,#397246,#397247),
 .UNSPECIFIED.,.F.,.F.,(4,3,3,3,3,3,3,3,3,3,3,3,3,3,3,3,4),(0.,1.5310029937341E-6,
4.52554775679536E-6,7.01151246291598E-6,9.26752933800322E-6,1.03084066197173E-5,
1.17138990826861E-5,1.22284894984075E-5,1.30315035324817E-5,1.38363728497813E-5,
1.40464197777495E-5,1.54597749564641E-5,1.62073588704069E-5,1.920929687127E-5,
1.95234416882555E-5,2.37637844577578E-5,2.61487188977261E-5),
 .UNSPECIFIED.);
#25489=B_SPLINE_CURVE_WITH_KNOTS('',3,(#397262,#397263,#397264,#397265,
#397266,#397267,#397268,#397269,#397270,#397271,#397272,#397273,#397274,
#397275,#397276,#397277,#397278,#397279,#397280,#397281,#397282,#397283,
#397284,#397285,#397286,#397287,#397288,#397289,#397290,#397291,#397292),
 .UNSPECIFIED.,.F.,.F.,(4,3,3,3,3,3,3,3,3,3,4),(0.,3.95507910396965E-6,
7.53768426604205E-6,1.1990453333535E-5,1.40475043392585E-5,1.51452104275965E-5,
1.6786627281402E-5,1.69621513005358E-5,1.81338315460712E-5,1.98906334656539E-5,
2.06132424588244E-5),.UNSPECIFIED.);
#25490=B_SPLINE_CURVE_WITH_KNOTS('',3,(#397295,#397296,#397297,#397298),
 .UNSPECIFIED.,.F.,.F.,(4,4),(4.84869951806108E-19,0.00010938435327491),
 .UNSPECIFIED.);
#25491=B_SPLINE_CURVE_WITH_KNOTS('',3,(#397325,#397326,#397327,#397328,
#397329,#397330,#397331,#397332,#397333,#397334,#397335,#397336,#397337,
#397338,#397339,#397340,#397341,#397342,#397343,#397344,#397345,#397346,
#397347,#397348,#397349,#397350,#397351,#397352,#397353,#397354,#397355,
#397356,#397357,#397358),.UNSPECIFIED.,.F.,.F.,(4,3,3,3,3,3,3,3,3,3,3,4),
(1.35525271560688E-19,2.09623992729433E-6,3.17176647120218E-6,4.82636181943005E-6,
5.01000917339954E-6,6.13126454147485E-6,8.60486650288841E-6,9.21144281170475E-6,
1.24722301135837E-5,1.42666454787852E-5,2.0467065375683E-5,2.08026438176799E-5),
 .UNSPECIFIED.);
#25492=B_SPLINE_CURVE_WITH_KNOTS('',3,(#397359,#397360,#397361,#397362),
 .UNSPECIFIED.,.F.,.F.,(4,4),(0.,0.000109384345496908),.UNSPECIFIED.);
#25493=B_SPLINE_CURVE_WITH_KNOTS('',3,(#397467,#397468,#397469,#397470),
 .UNSPECIFIED.,.F.,.F.,(4,4),(0.,9.54361881492175E-5),.UNSPECIFIED.);
#25494=B_SPLINE_CURVE_WITH_KNOTS('',3,(#397475,#397476,#397477,#397478,
#397479,#397480,#397481),.UNSPECIFIED.,.F.,.F.,(4,3,4),(0.,4.41069704323468E-5,
0.000113970027818833),.UNSPECIFIED.);
#25495=B_SPLINE_CURVE_WITH_KNOTS('',3,(#397487,#397488,#397489,#397490),
 .UNSPECIFIED.,.F.,.F.,(4,4),(4.63171371119878E-19,9.54361881492178E-5),
 .UNSPECIFIED.);
#25496=B_SPLINE_CURVE_WITH_KNOTS('',3,(#397494,#397495,#397496,#397497,
#397498,#397499,#397500),.UNSPECIFIED.,.F.,.F.,(4,3,4),(0.,6.9863024419149E-5,
0.000113969974038089),.UNSPECIFIED.);
#25497=B_SPLINE_CURVE_WITH_KNOTS('',3,(#397503,#397504,#397505,#397506,
#397507,#397508,#397509,#397510,#397511,#397512,#397513,#397514,#397515,
#397516,#397517,#397518,#397519,#397520,#397521,#397522,#397523,#397524,
#397525,#397526,#397527,#397528,#397529,#397530,#397531,#397532,#397533,
#397534,#397535,#397536,#397537,#397538,#397539,#397540,#397541,#397542,
#397543,#397544,#397545,#397546,#397547,#397548,#397549,#397550,#397551),
 .UNSPECIFIED.,.F.,.F.,(4,3,3,3,3,3,3,3,3,3,3,3,3,3,3,3,4),(0.,1.53100299373415E-6,
4.52554775679159E-6,7.01151246291606E-6,9.26752933801246E-6,1.03084066197173E-5,
1.17138990826861E-5,1.22284894984075E-5,1.30315035324817E-5,1.38363728497813E-5,
1.40464197777495E-5,1.54597749564642E-5,1.62073588704069E-5,1.9209296871264E-5,
1.95234416882557E-5,2.37637844577547E-5,2.61487188977263E-5),
 .UNSPECIFIED.);
#25498=B_SPLINE_CURVE_WITH_KNOTS('',3,(#397566,#397567,#397568,#397569,
#397570,#397571,#397572,#397573,#397574,#397575,#397576,#397577,#397578,
#397579,#397580,#397581,#397582,#397583,#397584,#397585,#397586,#397587,
#397588,#397589,#397590,#397591,#397592,#397593,#397594,#397595,#397596),
 .UNSPECIFIED.,.F.,.F.,(4,3,3,3,3,3,3,3,3,3,4),(0.,3.95507910398452E-6,
7.53768426604194E-6,1.1990453333535E-5,1.40475043392585E-5,1.51452104275964E-5,
1.67866272814187E-5,1.69621513005358E-5,1.81338315460712E-5,1.98906334656524E-5,
2.06132424588246E-5),.UNSPECIFIED.);
#25499=B_SPLINE_CURVE_WITH_KNOTS('',3,(#397599,#397600,#397601,#397602),
 .UNSPECIFIED.,.F.,.F.,(4,4),(5.11417141928151E-19,0.00010938435327491),
 .UNSPECIFIED.);
#25500=B_SPLINE_CURVE_WITH_KNOTS('',3,(#397629,#397630,#397631,#397632,
#397633,#397634,#397635,#397636,#397637,#397638,#397639,#397640,#397641,
#397642,#397643,#397644,#397645,#397646,#397647,#397648,#397649,#397650,
#397651,#397652,#397653,#397654,#397655,#397656,#397657,#397658,#397659,
#397660,#397661,#397662),.UNSPECIFIED.,.F.,.F.,(4,3,3,3,3,3,3,3,3,3,3,4),
(1.0842021724855E-19,2.09623992729446E-6,3.17176647120224E-6,4.8263618194523E-6,
5.01000917339966E-6,6.13126454147504E-6,8.60486650288861E-6,9.21144281170498E-6,
1.24722301135833E-5,1.42666454787858E-5,2.04670653756968E-5,2.08026438176805E-5),
 .UNSPECIFIED.);
#25501=B_SPLINE_CURVE_WITH_KNOTS('',3,(#397663,#397664,#397665,#397666),
 .UNSPECIFIED.,.F.,.F.,(4,4),(0.,0.000109384345496908),.UNSPECIFIED.);
#25502=B_SPLINE_CURVE_WITH_KNOTS('',3,(#397771,#397772,#397773,#397774),
 .UNSPECIFIED.,.F.,.F.,(4,4),(0.,9.54361881492173E-5),.UNSPECIFIED.);
#25503=B_SPLINE_CURVE_WITH_KNOTS('',3,(#397779,#397780,#397781,#397782,
#397783,#397784,#397785),.UNSPECIFIED.,.F.,.F.,(4,3,4),(0.,4.41069704323471E-5,
0.000113970027818833),.UNSPECIFIED.);
#25504=B_SPLINE_CURVE_WITH_KNOTS('',3,(#397791,#397792,#397793,#397794),
 .UNSPECIFIED.,.F.,.F.,(4,4),(4.63171371119878E-19,9.54361881492174E-5),
 .UNSPECIFIED.);
#25505=B_SPLINE_CURVE_WITH_KNOTS('',3,(#397798,#397799,#397800,#397801,
#397802,#397803,#397804),.UNSPECIFIED.,.F.,.F.,(4,3,4),(0.,6.98630244191489E-5,
0.000113969974038089),.UNSPECIFIED.);
#25506=B_SPLINE_CURVE_WITH_KNOTS('',3,(#397807,#397808,#397809,#397810,
#397811,#397812,#397813,#397814,#397815,#397816,#397817,#397818,#397819,
#397820,#397821,#397822,#397823,#397824,#397825,#397826,#397827,#397828,
#397829,#397830,#397831,#397832,#397833,#397834,#397835,#397836,#397837,
#397838,#397839,#397840,#397841,#397842,#397843,#397844,#397845,#397846,
#397847,#397848,#397849,#397850,#397851,#397852,#397853,#397854,#397855),
 .UNSPECIFIED.,.F.,.F.,(4,3,3,3,3,3,3,3,3,3,3,3,3,3,3,3,4),(0.,1.53100299373427E-6,
4.52554775679287E-6,7.01151246291616E-6,9.26752933799541E-6,1.03084066197174E-5,
1.17138990826863E-5,1.22284894984076E-5,1.30315035324818E-5,1.38363728497814E-5,
1.40464197777496E-5,1.54597749564642E-5,1.62073588704071E-5,1.92092968712996E-5,
1.95234416882555E-5,2.376378445776E-5,2.6148718897726E-5),.UNSPECIFIED.);
#25507=B_SPLINE_CURVE_WITH_KNOTS('',3,(#397870,#397871,#397872,#397873,
#397874,#397875,#397876,#397877,#397878,#397879,#397880,#397881,#397882,
#397883,#397884,#397885,#397886,#397887,#397888,#397889,#397890,#397891,
#397892,#397893,#397894,#397895,#397896,#397897,#397898,#397899,#397900),
 .UNSPECIFIED.,.F.,.F.,(4,3,3,3,3,3,3,3,3,3,4),(0.,3.95507910397904E-6,
7.53768426604202E-6,1.19904533335351E-5,1.40475043392587E-5,1.51452104275966E-5,
1.67866272814141E-5,1.6962151300536E-5,1.81338315460713E-5,1.98906334656548E-5,
2.06132424588246E-5),.UNSPECIFIED.);
#25508=B_SPLINE_CURVE_WITH_KNOTS('',3,(#397903,#397904,#397905,#397906),
 .UNSPECIFIED.,.F.,.F.,(4,4),(5.11417141928151E-19,0.00010938435327491),
 .UNSPECIFIED.);
#25509=B_SPLINE_CURVE_WITH_KNOTS('',3,(#397933,#397934,#397935,#397936,
#397937,#397938,#397939,#397940,#397941,#397942,#397943,#397944,#397945,
#397946,#397947,#397948,#397949,#397950,#397951,#397952,#397953,#397954,
#397955,#397956,#397957,#397958,#397959,#397960,#397961,#397962,#397963,
#397964,#397965,#397966),.UNSPECIFIED.,.F.,.F.,(4,3,3,3,3,3,3,3,3,3,3,4),
(1.62630325872826E-19,2.09623992729442E-6,3.17176647120233E-6,4.8263618194495E-6,
5.01000917339967E-6,6.13126454147504E-6,8.60486650288865E-6,9.21144281170504E-6,
1.24722301136077E-5,1.42666454787857E-5,2.04670653756745E-5,2.08026438176805E-5),
 .UNSPECIFIED.);
#25510=B_SPLINE_CURVE_WITH_KNOTS('',3,(#397967,#397968,#397969,#397970),
 .UNSPECIFIED.,.F.,.F.,(4,4),(0.,0.000109384345496908),.UNSPECIFIED.);
#25511=B_SPLINE_CURVE_WITH_KNOTS('',3,(#398075,#398076,#398077,#398078),
 .UNSPECIFIED.,.F.,.F.,(4,4),(0.,9.54361881492172E-5),.UNSPECIFIED.);
#25512=B_SPLINE_CURVE_WITH_KNOTS('',3,(#398083,#398084,#398085,#398086,
#398087,#398088,#398089),.UNSPECIFIED.,.F.,.F.,(4,3,4),(0.,4.4106970432347E-5,
0.000113970027818833),.UNSPECIFIED.);
#25513=B_SPLINE_CURVE_WITH_KNOTS('',3,(#398095,#398096,#398097,#398098),
 .UNSPECIFIED.,.F.,.F.,(4,4),(2.16840434497101E-19,9.54361881492181E-5),
 .UNSPECIFIED.);
#25514=B_SPLINE_CURVE_WITH_KNOTS('',3,(#398102,#398103,#398104,#398105,
#398106,#398107,#398108),.UNSPECIFIED.,.F.,.F.,(4,3,4),(0.,6.98630244191491E-5,
0.000113969974038089),.UNSPECIFIED.);
#25515=B_SPLINE_CURVE_WITH_KNOTS('',3,(#398111,#398112,#398113,#398114,
#398115,#398116,#398117,#398118,#398119,#398120,#398121,#398122,#398123,
#398124,#398125,#398126,#398127,#398128,#398129,#398130,#398131,#398132,
#398133,#398134,#398135,#398136,#398137,#398138,#398139,#398140,#398141,
#398142,#398143,#398144,#398145,#398146,#398147,#398148,#398149,#398150,
#398151,#398152,#398153,#398154,#398155,#398156,#398157,#398158,#398159),
 .UNSPECIFIED.,.F.,.F.,(4,3,3,3,3,3,3,3,3,3,3,3,3,3,3,3,4),(0.,1.53100299373411E-6,
4.52554775679125E-6,7.01151246291595E-6,9.26752933800362E-6,1.03084066197172E-5,
1.17138990826861E-5,1.22284894984074E-5,1.30315035324816E-5,1.3836372849781E-5,
1.40464197777493E-5,1.54597749564638E-5,1.62073588704067E-5,1.9209296871261E-5,
1.95234416882551E-5,2.37637844577578E-5,2.61487188977257E-5),
 .UNSPECIFIED.);
#25516=B_SPLINE_CURVE_WITH_KNOTS('',3,(#398174,#398175,#398176,#398177,
#398178,#398179,#398180,#398181,#398182,#398183,#398184,#398185,#398186,
#398187,#398188,#398189,#398190,#398191,#398192,#398193,#398194,#398195,
#398196,#398197,#398198,#398199,#398200,#398201,#398202,#398203,#398204),
 .UNSPECIFIED.,.F.,.F.,(4,3,3,3,3,3,3,3,3,3,4),(0.,3.95507910398269E-6,
7.53768426604198E-6,1.19904533335351E-5,1.40475043392586E-5,1.51452104275966E-5,
1.67866272814071E-5,1.69621513005359E-5,1.81338315460714E-5,1.98906334656536E-5,
2.06132424588246E-5),.UNSPECIFIED.);
#25517=B_SPLINE_CURVE_WITH_KNOTS('',3,(#398207,#398208,#398209,#398210),
 .UNSPECIFIED.,.F.,.F.,(4,4),(4.84869951806108E-19,0.00010938435327491),
 .UNSPECIFIED.);
#25518=B_SPLINE_CURVE_WITH_KNOTS('',3,(#398237,#398238,#398239,#398240,
#398241,#398242,#398243,#398244,#398245,#398246,#398247,#398248,#398249,
#398250,#398251,#398252,#398253,#398254,#398255,#398256,#398257,#398258,
#398259,#398260,#398261,#398262,#398263,#398264,#398265,#398266,#398267,
#398268,#398269,#398270),.UNSPECIFIED.,.F.,.F.,(4,3,3,3,3,3,3,3,3,3,3,4),
(2.16840434497101E-19,2.09623992729424E-6,3.17176647120196E-6,4.82636181943257E-6,
5.01000917339949E-6,6.1312645414749E-6,8.60486650288852E-6,9.2114428117048E-6,
1.2472230113601E-5,1.42666454787854E-5,2.04670653756909E-5,2.08026438176801E-5),
 .UNSPECIFIED.);
#25519=B_SPLINE_CURVE_WITH_KNOTS('',3,(#398271,#398272,#398273,#398274),
 .UNSPECIFIED.,.F.,.F.,(4,4),(0.,0.000109384345496908),.UNSPECIFIED.);
#25520=B_SPLINE_CURVE_WITH_KNOTS('',3,(#398379,#398380,#398381,#398382),
 .UNSPECIFIED.,.F.,.F.,(4,4),(0.,9.54361881492173E-5),.UNSPECIFIED.);
#25521=B_SPLINE_CURVE_WITH_KNOTS('',3,(#398387,#398388,#398389,#398390,
#398391,#398392,#398393),.UNSPECIFIED.,.F.,.F.,(4,3,4),(0.,4.4106970432347E-5,
0.000113970027818833),.UNSPECIFIED.);
#25522=B_SPLINE_CURVE_WITH_KNOTS('',3,(#398399,#398400,#398401,#398402),
 .UNSPECIFIED.,.F.,.F.,(4,4),(2.16840434497101E-19,9.54361881492179E-5),
 .UNSPECIFIED.);
#25523=B_SPLINE_CURVE_WITH_KNOTS('',3,(#398406,#398407,#398408,#398409,
#398410,#398411,#398412),.UNSPECIFIED.,.F.,.F.,(4,3,4),(0.,6.98630244191488E-5,
0.000113969974038089),.UNSPECIFIED.);
#25524=B_SPLINE_CURVE_WITH_KNOTS('',3,(#398415,#398416,#398417,#398418,
#398419,#398420,#398421,#398422,#398423,#398424,#398425,#398426,#398427,
#398428,#398429,#398430,#398431,#398432,#398433,#398434,#398435,#398436,
#398437,#398438,#398439,#398440,#398441,#398442,#398443,#398444,#398445,
#398446,#398447,#398448,#398449,#398450,#398451,#398452,#398453,#398454,
#398455,#398456,#398457,#398458,#398459,#398460,#398461,#398462,#398463),
 .UNSPECIFIED.,.F.,.F.,(4,3,3,3,3,3,3,3,3,3,3,3,3,3,3,3,4),(0.,1.53100299373426E-6,
4.52554775679122E-6,7.01151246291613E-6,9.26752933800967E-6,1.03084066197174E-5,
1.17138990826863E-5,1.22284894984075E-5,1.30315035324819E-5,1.38363728497814E-5,
1.40464197777496E-5,1.54597749564639E-5,1.62073588704069E-5,1.92092968712659E-5,
1.95234416882553E-5,2.37637844577623E-5,2.61487188977257E-5),
 .UNSPECIFIED.);
#25525=B_SPLINE_CURVE_WITH_KNOTS('',3,(#398478,#398479,#398480,#398481,
#398482,#398483,#398484,#398485,#398486,#398487,#398488,#398489,#398490,
#398491,#398492,#398493,#398494,#398495,#398496,#398497,#398498,#398499,
#398500,#398501,#398502,#398503,#398504,#398505,#398506,#398507,#398508),
 .UNSPECIFIED.,.F.,.F.,(4,3,3,3,3,3,3,3,3,3,4),(0.,3.95507910398825E-6,
7.53768426604196E-6,1.19904533335349E-5,1.40475043392586E-5,1.51452104275964E-5,
1.67866272814144E-5,1.69621513005358E-5,1.81338315460713E-5,1.98906334656502E-5,
2.06132424588246E-5),.UNSPECIFIED.);
#25526=B_SPLINE_CURVE_WITH_KNOTS('',3,(#398511,#398512,#398513,#398514),
 .UNSPECIFIED.,.F.,.F.,(4,4),(5.42101086242752E-19,0.00010938435327491),
 .UNSPECIFIED.);
#25527=B_SPLINE_CURVE_WITH_KNOTS('',3,(#398541,#398542,#398543,#398544,
#398545,#398546,#398547,#398548,#398549,#398550,#398551,#398552,#398553,
#398554,#398555,#398556,#398557,#398558,#398559,#398560,#398561,#398562,
#398563,#398564,#398565,#398566,#398567,#398568,#398569,#398570,#398571,
#398572,#398573,#398574),.UNSPECIFIED.,.F.,.F.,(4,3,3,3,3,3,3,3,3,3,3,4),
(1.0842021724855E-19,2.09623992729444E-6,3.17176647120229E-6,4.82636181943599E-6,
5.01000917339964E-6,6.13126454147494E-6,8.60486650288865E-6,9.21144281170499E-6,
1.24722301135751E-5,1.42666454787858E-5,2.04670653757029E-5,2.08026438176807E-5),
 .UNSPECIFIED.);
#25528=B_SPLINE_CURVE_WITH_KNOTS('',3,(#398575,#398576,#398577,#398578),
 .UNSPECIFIED.,.F.,.F.,(4,4),(0.,0.000109384345496909),.UNSPECIFIED.);
#25529=B_SPLINE_CURVE_WITH_KNOTS('',3,(#398683,#398684,#398685,#398686),
 .UNSPECIFIED.,.F.,.F.,(4,4),(0.,9.54361881492173E-5),.UNSPECIFIED.);
#25530=B_SPLINE_CURVE_WITH_KNOTS('',3,(#398691,#398692,#398693,#398694,
#398695,#398696,#398697),.UNSPECIFIED.,.F.,.F.,(4,3,4),(0.,4.41069704323471E-5,
0.000113970027818833),.UNSPECIFIED.);
#25531=B_SPLINE_CURVE_WITH_KNOTS('',3,(#398703,#398704,#398705,#398706),
 .UNSPECIFIED.,.F.,.F.,(4,4),(4.84869951806108E-19,9.54361881492178E-5),
 .UNSPECIFIED.);
#25532=B_SPLINE_CURVE_WITH_KNOTS('',3,(#398710,#398711,#398712,#398713,
#398714,#398715,#398716),.UNSPECIFIED.,.F.,.F.,(4,3,4),(0.,6.98630244191491E-5,
0.000113969974038089),.UNSPECIFIED.);
#25533=B_SPLINE_CURVE_WITH_KNOTS('',3,(#398719,#398720,#398721,#398722,
#398723,#398724,#398725,#398726,#398727,#398728,#398729,#398730,#398731,
#398732,#398733,#398734,#398735,#398736,#398737,#398738,#398739,#398740,
#398741,#398742,#398743,#398744,#398745,#398746,#398747,#398748,#398749,
#398750,#398751,#398752,#398753,#398754,#398755,#398756,#398757,#398758,
#398759,#398760,#398761,#398762,#398763,#398764,#398765,#398766,#398767),
 .UNSPECIFIED.,.F.,.F.,(4,3,3,3,3,3,3,3,3,3,3,3,3,3,3,3,4),(0.,1.53100299373415E-6,
4.52554775679612E-6,7.01151246291607E-6,9.26752933798826E-6,1.03084066197174E-5,
1.17138990826862E-5,1.22284894984074E-5,1.30315035324818E-5,1.38363728497812E-5,
1.40464197777495E-5,1.5459774956464E-5,1.6207358870407E-5,1.92092968712588E-5,
1.95234416882558E-5,2.37637844577578E-5,2.61487188977265E-5),
 .UNSPECIFIED.);
#25534=B_SPLINE_CURVE_WITH_KNOTS('',3,(#398782,#398783,#398784,#398785,
#398786,#398787,#398788,#398789,#398790,#398791,#398792,#398793,#398794,
#398795,#398796,#398797,#398798,#398799,#398800,#398801,#398802,#398803,
#398804,#398805,#398806,#398807,#398808,#398809,#398810,#398811,#398812),
 .UNSPECIFIED.,.F.,.F.,(4,3,3,3,3,3,3,3,3,3,4),(0.,3.95507910397645E-6,
7.53768426604196E-6,1.19904533335349E-5,1.40475043392584E-5,1.51452104275963E-5,
1.67866272814147E-5,1.69621513005358E-5,1.81338315460712E-5,1.98906334656532E-5,
2.06132424588247E-5),.UNSPECIFIED.);
#25535=B_SPLINE_CURVE_WITH_KNOTS('',3,(#398815,#398816,#398817,#398818),
 .UNSPECIFIED.,.F.,.F.,(4,4),(1.06229684024259E-18,0.00010938435327491),
 .UNSPECIFIED.);
#25536=B_SPLINE_CURVE_WITH_KNOTS('',3,(#398845,#398846,#398847,#398848,
#398849,#398850,#398851,#398852,#398853,#398854,#398855,#398856,#398857,
#398858,#398859,#398860,#398861,#398862,#398863,#398864,#398865,#398866,
#398867,#398868,#398869,#398870,#398871,#398872,#398873,#398874,#398875,
#398876,#398877,#398878),.UNSPECIFIED.,.F.,.F.,(4,3,3,3,3,3,3,3,3,3,3,4),
(1.0842021724855E-19,2.0962399272944E-6,3.17176647120221E-6,4.82636181942624E-6,
5.0100091733996E-6,6.13126454147486E-6,8.60486650288837E-6,9.21144281170471E-6,
1.24722301135842E-5,1.42666454787849E-5,2.04670653756911E-5,2.08026438176791E-5),
 .UNSPECIFIED.);
#25537=B_SPLINE_CURVE_WITH_KNOTS('',3,(#398879,#398880,#398881,#398882),
 .UNSPECIFIED.,.F.,.F.,(4,4),(0.,0.000109384345496908),.UNSPECIFIED.);
#25538=B_SPLINE_CURVE_WITH_KNOTS('',3,(#398987,#398988,#398989,#398990),
 .UNSPECIFIED.,.F.,.F.,(4,4),(0.,9.54361881492175E-5),.UNSPECIFIED.);
#25539=B_SPLINE_CURVE_WITH_KNOTS('',3,(#398995,#398996,#398997,#398998,
#398999,#399000,#399001),.UNSPECIFIED.,.F.,.F.,(4,3,4),(0.,4.41069704323469E-5,
0.000113970027818833),.UNSPECIFIED.);
#25540=B_SPLINE_CURVE_WITH_KNOTS('',3,(#399007,#399008,#399009,#399010),
 .UNSPECIFIED.,.F.,.F.,(4,4),(2.16840434497101E-19,9.54361881492181E-5),
 .UNSPECIFIED.);
#25541=B_SPLINE_CURVE_WITH_KNOTS('',3,(#399014,#399015,#399016,#399017,
#399018,#399019,#399020),.UNSPECIFIED.,.F.,.F.,(4,3,4),(0.,6.98630244191489E-5,
0.000113969974038089),.UNSPECIFIED.);
#25542=B_SPLINE_CURVE_WITH_KNOTS('',3,(#399023,#399024,#399025,#399026,
#399027,#399028,#399029,#399030,#399031,#399032,#399033,#399034,#399035,
#399036,#399037,#399038,#399039,#399040,#399041,#399042,#399043,#399044,
#399045,#399046,#399047,#399048,#399049,#399050,#399051,#399052,#399053,
#399054,#399055,#399056,#399057,#399058,#399059,#399060,#399061,#399062,
#399063,#399064,#399065,#399066,#399067,#399068,#399069,#399070,#399071),
 .UNSPECIFIED.,.F.,.F.,(4,3,3,3,3,3,3,3,3,3,3,3,3,3,3,3,4),(0.,1.53100299373423E-6,
4.52554775678839E-6,7.01151246291621E-6,9.2675293380022E-6,1.03084066197175E-5,
1.17138990826861E-5,1.22284894984073E-5,1.30315035324817E-5,1.3836372849781E-5,
1.40464197777494E-5,1.5459774956464E-5,1.62073588704068E-5,1.92092968713103E-5,
1.95234416882551E-5,2.37637844577638E-5,2.61487188977247E-5),
 .UNSPECIFIED.);
#25543=B_SPLINE_CURVE_WITH_KNOTS('',3,(#399086,#399087,#399088,#399089,
#399090,#399091,#399092,#399093,#399094,#399095,#399096,#399097,#399098,
#399099,#399100,#399101,#399102,#399103,#399104,#399105,#399106,#399107,
#399108,#399109,#399110,#399111,#399112,#399113,#399114,#399115,#399116),
 .UNSPECIFIED.,.F.,.F.,(4,3,3,3,3,3,3,3,3,3,4),(0.,3.95507910396983E-6,
7.53768426604189E-6,1.1990453333535E-5,1.40475043392585E-5,1.51452104275965E-5,
1.67866272814133E-5,1.6962151300536E-5,1.81338315460716E-5,1.98906334656569E-5,
2.06132424588254E-5),.UNSPECIFIED.);
#25544=B_SPLINE_CURVE_WITH_KNOTS('',3,(#399119,#399120,#399121,#399122),
 .UNSPECIFIED.,.F.,.F.,(4,4),(4.84869951806108E-19,0.00010938435327491),
 .UNSPECIFIED.);
#25545=B_SPLINE_CURVE_WITH_KNOTS('',3,(#399149,#399150,#399151,#399152,
#399153,#399154,#399155,#399156,#399157,#399158,#399159,#399160,#399161,
#399162,#399163,#399164,#399165,#399166,#399167,#399168,#399169,#399170,
#399171,#399172,#399173,#399174,#399175,#399176,#399177,#399178,#399179,
#399180,#399181,#399182),.UNSPECIFIED.,.F.,.F.,(4,3,3,3,3,3,3,3,3,3,3,4),
(2.16840434497101E-19,2.09623992729426E-6,3.17176647120219E-6,4.82636181942554E-6,
5.01000917339955E-6,6.13126454147493E-6,8.60486650288818E-6,9.21144281170458E-6,
1.24722301136027E-5,1.42666454787846E-5,2.04670653756731E-5,2.08026438176786E-5),
 .UNSPECIFIED.);
#25546=B_SPLINE_CURVE_WITH_KNOTS('',3,(#399183,#399184,#399185,#399186),
 .UNSPECIFIED.,.F.,.F.,(4,4),(0.,0.000109384345496908),.UNSPECIFIED.);
#25547=B_SPLINE_CURVE_WITH_KNOTS('',3,(#399291,#399292,#399293,#399294),
 .UNSPECIFIED.,.F.,.F.,(4,4),(0.,9.54361881492175E-5),.UNSPECIFIED.);
#25548=B_SPLINE_CURVE_WITH_KNOTS('',3,(#399299,#399300,#399301,#399302,
#399303,#399304,#399305),.UNSPECIFIED.,.F.,.F.,(4,3,4),(0.,4.41069704323471E-5,
0.000113970027818833),.UNSPECIFIED.);
#25549=B_SPLINE_CURVE_WITH_KNOTS('',3,(#399311,#399312,#399313,#399314),
 .UNSPECIFIED.,.F.,.F.,(4,4),(2.16840434497101E-19,9.54361881492182E-5),
 .UNSPECIFIED.);
#25550=B_SPLINE_CURVE_WITH_KNOTS('',3,(#399318,#399319,#399320,#399321,
#399322,#399323,#399324),.UNSPECIFIED.,.F.,.F.,(4,3,4),(0.,6.98630244191493E-5,
0.000113969974038089),.UNSPECIFIED.);
#25551=B_SPLINE_CURVE_WITH_KNOTS('',3,(#399327,#399328,#399329,#399330,
#399331,#399332,#399333,#399334,#399335,#399336,#399337,#399338,#399339,
#399340,#399341,#399342,#399343,#399344,#399345,#399346,#399347,#399348,
#399349,#399350,#399351,#399352,#399353,#399354,#399355,#399356,#399357,
#399358,#399359,#399360,#399361,#399362,#399363,#399364,#399365,#399366,
#399367,#399368,#399369,#399370,#399371,#399372,#399373,#399374,#399375),
 .UNSPECIFIED.,.F.,.F.,(4,3,3,3,3,3,3,3,3,3,3,3,3,3,3,3,4),(0.,1.53100299373411E-6,
4.52554775679371E-6,7.01151246291605E-6,9.26752933799832E-6,1.03084066197173E-5,
1.17138990826861E-5,1.22284894984075E-5,1.3031503532482E-5,1.38363728497812E-5,
1.40464197777496E-5,1.54597749564641E-5,1.6207358870407E-5,1.92092968713185E-5,
1.95234416882556E-5,2.37637844577594E-5,2.61487188977267E-5),
 .UNSPECIFIED.);
#25552=B_SPLINE_CURVE_WITH_KNOTS('',3,(#399390,#399391,#399392,#399393,
#399394,#399395,#399396,#399397,#399398,#399399,#399400,#399401,#399402,
#399403,#399404,#399405,#399406,#399407,#399408,#399409,#399410,#399411,
#399412,#399413,#399414,#399415,#399416,#399417,#399418,#399419,#399420),
 .UNSPECIFIED.,.F.,.F.,(4,3,3,3,3,3,3,3,3,3,4),(0.,3.9550791039821E-6,7.53768426604195E-6,
1.19904533335351E-5,1.40475043392586E-5,1.51452104275965E-5,1.67866272814213E-5,
1.69621513005356E-5,1.81338315460712E-5,1.98906334656531E-5,2.06132424588241E-5),
 .UNSPECIFIED.);
#25553=B_SPLINE_CURVE_WITH_KNOTS('',3,(#399423,#399424,#399425,#399426),
 .UNSPECIFIED.,.F.,.F.,(4,4),(6.1331736667335E-19,0.00010938435327491),
 .UNSPECIFIED.);
#25554=B_SPLINE_CURVE_WITH_KNOTS('',3,(#399453,#399454,#399455,#399456,
#399457,#399458,#399459,#399460,#399461,#399462,#399463,#399464,#399465,
#399466,#399467,#399468,#399469,#399470,#399471,#399472,#399473,#399474,
#399475,#399476,#399477,#399478,#399479,#399480,#399481,#399482,#399483,
#399484,#399485,#399486),.UNSPECIFIED.,.F.,.F.,(4,3,3,3,3,3,3,3,3,3,3,4),
(2.16840434497101E-19,2.09623992729438E-6,3.17176647120215E-6,4.82636181943272E-6,
5.01000917339969E-6,6.13126454147507E-6,8.60486650288861E-6,9.21144281170498E-6,
1.24722301135845E-5,1.42666454787857E-5,2.04670653757436E-5,2.08026438176804E-5),
 .UNSPECIFIED.);
#25555=B_SPLINE_CURVE_WITH_KNOTS('',3,(#399487,#399488,#399489,#399490),
 .UNSPECIFIED.,.F.,.F.,(4,4),(0.,0.000109384345496908),.UNSPECIFIED.);
#25556=B_SPLINE_CURVE_WITH_KNOTS('',3,(#399595,#399596,#399597,#399598),
 .UNSPECIFIED.,.F.,.F.,(4,4),(0.,9.54361881492177E-5),.UNSPECIFIED.);
#25557=B_SPLINE_CURVE_WITH_KNOTS('',3,(#399603,#399604,#399605,#399606,
#399607,#399608,#399609),.UNSPECIFIED.,.F.,.F.,(4,3,4),(0.,4.41069704323472E-5,
0.000113970027818834),.UNSPECIFIED.);
#25558=B_SPLINE_CURVE_WITH_KNOTS('',3,(#399615,#399616,#399617,#399618),
 .UNSPECIFIED.,.F.,.F.,(4,4),(2.16840434497101E-19,9.54361881492179E-5),
 .UNSPECIFIED.);
#25559=B_SPLINE_CURVE_WITH_KNOTS('',3,(#399622,#399623,#399624,#399625,
#399626,#399627,#399628),.UNSPECIFIED.,.F.,.F.,(4,3,4),(0.,6.98630244191492E-5,
0.000113969974038089),.UNSPECIFIED.);
#25560=B_SPLINE_CURVE_WITH_KNOTS('',3,(#399631,#399632,#399633,#399634,
#399635,#399636,#399637,#399638,#399639,#399640,#399641,#399642,#399643,
#399644,#399645,#399646,#399647,#399648,#399649,#399650,#399651,#399652,
#399653,#399654,#399655,#399656,#399657,#399658,#399659,#399660,#399661,
#399662,#399663,#399664,#399665,#399666,#399667,#399668,#399669,#399670,
#399671,#399672,#399673,#399674,#399675,#399676,#399677,#399678,#399679),
 .UNSPECIFIED.,.F.,.F.,(4,3,3,3,3,3,3,3,3,3,3,3,3,3,3,3,4),(0.,1.53100299373409E-6,
4.52554775679162E-6,7.0115124629161E-6,9.26752933800718E-6,1.03084066197173E-5,
1.17138990826861E-5,1.22284894984077E-5,1.30315035324817E-5,1.38363728497814E-5,
1.40464197777495E-5,1.54597749564643E-5,1.62073588704069E-5,1.92092968712789E-5,
1.95234416882557E-5,2.37637844577536E-5,2.61487188977265E-5),
 .UNSPECIFIED.);
#25561=B_SPLINE_CURVE_WITH_KNOTS('',3,(#399694,#399695,#399696,#399697,
#399698,#399699,#399700,#399701,#399702,#399703,#399704,#399705,#399706,
#399707,#399708,#399709,#399710,#399711,#399712,#399713,#399714,#399715,
#399716,#399717,#399718,#399719,#399720,#399721,#399722,#399723,#399724),
 .UNSPECIFIED.,.F.,.F.,(4,3,3,3,3,3,3,3,3,3,4),(0.,3.95507910396712E-6,
7.53768426604191E-6,1.1990453333535E-5,1.40475043392585E-5,1.51452104275962E-5,
1.67866272814315E-5,1.69621513005358E-5,1.81338315460713E-5,1.98906334656587E-5,
2.06132424588245E-5),.UNSPECIFIED.);
#25562=B_SPLINE_CURVE_WITH_KNOTS('',3,(#399727,#399728,#399729,#399730),
 .UNSPECIFIED.,.F.,.F.,(4,4),(6.1331736667335E-19,0.00010938435327491),
 .UNSPECIFIED.);
#25563=B_SPLINE_CURVE_WITH_KNOTS('',3,(#399757,#399758,#399759,#399760,
#399761,#399762,#399763,#399764,#399765,#399766,#399767,#399768,#399769,
#399770,#399771,#399772,#399773,#399774,#399775,#399776,#399777,#399778,
#399779,#399780,#399781,#399782,#399783,#399784,#399785,#399786,#399787,
#399788,#399789,#399790),.UNSPECIFIED.,.F.,.F.,(4,3,3,3,3,3,3,3,3,3,3,4),
(2.16840434497101E-19,2.09623992729449E-6,3.17176647120226E-6,4.82636181944115E-6,
5.01000917339949E-6,6.13126454147491E-6,8.60486650288856E-6,9.21144281170483E-6,
1.24722301135999E-5,1.42666454787852E-5,2.04670653756803E-5,2.08026438176794E-5),
 .UNSPECIFIED.);
#25564=B_SPLINE_CURVE_WITH_KNOTS('',3,(#399791,#399792,#399793,#399794),
 .UNSPECIFIED.,.F.,.F.,(4,4),(0.,0.000109384345496908),.UNSPECIFIED.);
#25565=B_SPLINE_CURVE_WITH_KNOTS('',3,(#399899,#399900,#399901,#399902),
 .UNSPECIFIED.,.F.,.F.,(4,4),(0.,9.54361881492176E-5),.UNSPECIFIED.);
#25566=B_SPLINE_CURVE_WITH_KNOTS('',3,(#399907,#399908,#399909,#399910,
#399911,#399912,#399913),.UNSPECIFIED.,.F.,.F.,(4,3,4),(0.,4.41069704323472E-5,
0.000113970027818833),.UNSPECIFIED.);
#25567=B_SPLINE_CURVE_WITH_KNOTS('',3,(#399919,#399920,#399921,#399922),
 .UNSPECIFIED.,.F.,.F.,(4,4),(2.16840434497101E-19,9.54361881492179E-5),
 .UNSPECIFIED.);
#25568=B_SPLINE_CURVE_WITH_KNOTS('',3,(#399926,#399927,#399928,#399929,
#399930,#399931,#399932),.UNSPECIFIED.,.F.,.F.,(4,3,4),(0.,6.9863024419149E-5,
0.000113969974038089),.UNSPECIFIED.);
#25569=B_SPLINE_CURVE_WITH_KNOTS('',3,(#399935,#399936,#399937,#399938,
#399939,#399940,#399941,#399942,#399943,#399944,#399945,#399946,#399947,
#399948,#399949,#399950,#399951,#399952,#399953,#399954,#399955,#399956,
#399957,#399958,#399959,#399960,#399961,#399962,#399963,#399964,#399965,
#399966,#399967,#399968,#399969,#399970,#399971,#399972,#399973,#399974,
#399975,#399976,#399977,#399978,#399979,#399980,#399981,#399982,#399983),
 .UNSPECIFIED.,.F.,.F.,(4,3,3,3,3,3,3,3,3,3,3,3,3,3,3,3,4),(0.,1.53100299373425E-6,
4.52554775679298E-6,7.01151246291614E-6,9.2675293379928E-6,1.03084066197173E-5,
1.17138990826863E-5,1.22284894984074E-5,1.3031503532482E-5,1.38363728497814E-5,
1.40464197777497E-5,1.54597749564644E-5,1.62073588704073E-5,1.92092968712382E-5,
1.95234416882566E-5,2.37637844577608E-5,2.61487188977282E-5),
 .UNSPECIFIED.);
#25570=B_SPLINE_CURVE_WITH_KNOTS('',3,(#399998,#399999,#400000,#400001,
#400002,#400003,#400004,#400005,#400006,#400007,#400008,#400009,#400010,
#400011,#400012,#400013,#400014,#400015,#400016,#400017,#400018,#400019,
#400020,#400021,#400022,#400023,#400024,#400025,#400026,#400027,#400028),
 .UNSPECIFIED.,.F.,.F.,(4,3,3,3,3,3,3,3,3,3,4),(0.,3.95507910398008E-6,
7.53768426604198E-6,1.1990453333535E-5,1.40475043392586E-5,1.51452104275965E-5,
1.67866272814163E-5,1.69621513005358E-5,1.81338315460713E-5,1.98906334656514E-5,
2.06132424588243E-5),.UNSPECIFIED.);
#25571=B_SPLINE_CURVE_WITH_KNOTS('',3,(#400031,#400032,#400033,#400034),
 .UNSPECIFIED.,.F.,.F.,(4,4),(4.33680868994202E-19,0.00010938435327491),
 .UNSPECIFIED.);
#25572=B_SPLINE_CURVE_WITH_KNOTS('',3,(#400061,#400062,#400063,#400064,
#400065,#400066,#400067,#400068,#400069,#400070,#400071,#400072,#400073,
#400074,#400075,#400076,#400077,#400078,#400079,#400080,#400081,#400082,
#400083,#400084,#400085,#400086,#400087,#400088,#400089,#400090,#400091,
#400092,#400093,#400094),.UNSPECIFIED.,.F.,.F.,(4,3,3,3,3,3,3,3,3,3,3,4),
(2.16840434497101E-19,2.0962399272944E-6,3.17176647120242E-6,4.82636181944529E-6,
5.01000917339975E-6,6.13126454147501E-6,8.6048665028885E-6,9.21144281170502E-6,
1.24722301136151E-5,1.42666454787858E-5,2.04670653756866E-5,2.08026438176806E-5),
 .UNSPECIFIED.);
#25573=B_SPLINE_CURVE_WITH_KNOTS('',3,(#400095,#400096,#400097,#400098),
 .UNSPECIFIED.,.F.,.F.,(4,4),(0.,0.000109384345496908),.UNSPECIFIED.);
#25574=B_SPLINE_CURVE_WITH_KNOTS('',3,(#400203,#400204,#400205,#400206),
 .UNSPECIFIED.,.F.,.F.,(4,4),(0.,9.54361881492176E-5),.UNSPECIFIED.);
#25575=B_SPLINE_CURVE_WITH_KNOTS('',3,(#400211,#400212,#400213,#400214,
#400215,#400216,#400217),.UNSPECIFIED.,.F.,.F.,(4,3,4),(0.,4.41069704323467E-5,
0.000113970027818833),.UNSPECIFIED.);
#25576=B_SPLINE_CURVE_WITH_KNOTS('',3,(#400223,#400224,#400225,#400226),
 .UNSPECIFIED.,.F.,.F.,(4,4),(2.16840434497101E-19,9.54361881492179E-5),
 .UNSPECIFIED.);
#25577=B_SPLINE_CURVE_WITH_KNOTS('',3,(#400230,#400231,#400232,#400233,
#400234,#400235,#400236),.UNSPECIFIED.,.F.,.F.,(4,3,4),(0.,6.98630244191488E-5,
0.000113969974038089),.UNSPECIFIED.);
#25578=B_SPLINE_CURVE_WITH_KNOTS('',3,(#400239,#400240,#400241,#400242,
#400243,#400244,#400245,#400246,#400247,#400248,#400249,#400250,#400251,
#400252,#400253,#400254,#400255,#400256,#400257,#400258,#400259,#400260,
#400261,#400262,#400263,#400264,#400265,#400266,#400267,#400268,#400269,
#400270,#400271,#400272,#400273,#400274,#400275,#400276,#400277,#400278,
#400279,#400280,#400281,#400282,#400283,#400284,#400285,#400286,#400287),
 .UNSPECIFIED.,.F.,.F.,(4,3,3,3,3,3,3,3,3,3,3,3,3,3,3,3,4),(0.,1.53100299373415E-6,
4.52554775679384E-6,7.01151246291613E-6,9.26752933801275E-6,1.03084066197174E-5,
1.17138990826863E-5,1.22284894984077E-5,1.30315035324817E-5,1.38363728497813E-5,
1.40464197777498E-5,1.5459774956464E-5,1.6207358870407E-5,1.92092968713218E-5,
1.95234416882559E-5,2.37637844577589E-5,2.61487188977269E-5),
 .UNSPECIFIED.);
#25579=B_SPLINE_CURVE_WITH_KNOTS('',3,(#400302,#400303,#400304,#400305,
#400306,#400307,#400308,#400309,#400310,#400311,#400312,#400313,#400314,
#400315,#400316,#400317,#400318,#400319,#400320,#400321,#400322,#400323,
#400324,#400325,#400326,#400327,#400328,#400329,#400330,#400331,#400332),
 .UNSPECIFIED.,.F.,.F.,(4,3,3,3,3,3,3,3,3,3,4),(0.,3.95507910398558E-6,
7.53768426604203E-6,1.19904533335348E-5,1.40475043392586E-5,1.51452104275963E-5,
1.67866272814335E-5,1.69621513005358E-5,1.81338315460711E-5,1.98906334656505E-5,
2.06132424588244E-5),.UNSPECIFIED.);
#25580=B_SPLINE_CURVE_WITH_KNOTS('',3,(#400335,#400336,#400337,#400338),
 .UNSPECIFIED.,.F.,.F.,(4,4),(2.16840434497101E-19,0.00010938435327491),
 .UNSPECIFIED.);
#25581=B_SPLINE_CURVE_WITH_KNOTS('',3,(#400365,#400366,#400367,#400368,
#400369,#400370,#400371,#400372,#400373,#400374,#400375,#400376,#400377,
#400378,#400379,#400380,#400381,#400382,#400383,#400384,#400385,#400386,
#400387,#400388,#400389,#400390,#400391,#400392,#400393,#400394,#400395,
#400396,#400397,#400398),.UNSPECIFIED.,.F.,.F.,(4,3,3,3,3,3,3,3,3,3,3,4),
(0.,2.09623992729418E-6,3.171766471202E-6,4.82636181943802E-6,5.01000917339955E-6,
6.13126454147495E-6,8.60486650288841E-6,9.21144281170478E-6,1.24722301136026E-5,
1.42666454787854E-5,2.04670653756955E-5,2.080264381768E-5),
 .UNSPECIFIED.);
#25582=B_SPLINE_CURVE_WITH_KNOTS('',3,(#400399,#400400,#400401,#400402),
 .UNSPECIFIED.,.F.,.F.,(4,4),(0.,0.000109384345496908),.UNSPECIFIED.);
#25583=B_SPLINE_CURVE_WITH_KNOTS('',3,(#400507,#400508,#400509,#400510),
 .UNSPECIFIED.,.F.,.F.,(4,4),(0.,9.54361881492176E-5),.UNSPECIFIED.);
#25584=B_SPLINE_CURVE_WITH_KNOTS('',3,(#400515,#400516,#400517,#400518,
#400519,#400520,#400521),.UNSPECIFIED.,.F.,.F.,(4,3,4),(0.,4.41069704323472E-5,
0.000113970027818833),.UNSPECIFIED.);
#25585=B_SPLINE_CURVE_WITH_KNOTS('',3,(#400527,#400528,#400529,#400530),
 .UNSPECIFIED.,.F.,.F.,(4,4),(2.16840434497101E-19,9.54361881492179E-5),
 .UNSPECIFIED.);
#25586=B_SPLINE_CURVE_WITH_KNOTS('',3,(#400534,#400535,#400536,#400537,
#400538,#400539,#400540),.UNSPECIFIED.,.F.,.F.,(4,3,4),(0.,6.98630244191491E-5,
0.000113969974038089),.UNSPECIFIED.);
#25587=B_SPLINE_CURVE_WITH_KNOTS('',3,(#400543,#400544,#400545,#400546,
#400547,#400548,#400549,#400550,#400551,#400552,#400553,#400554,#400555,
#400556,#400557,#400558,#400559,#400560,#400561,#400562,#400563,#400564,
#400565,#400566,#400567,#400568,#400569,#400570,#400571,#400572,#400573,
#400574,#400575,#400576,#400577,#400578,#400579,#400580,#400581,#400582,
#400583,#400584,#400585,#400586,#400587,#400588,#400589,#400590,#400591),
 .UNSPECIFIED.,.F.,.F.,(4,3,3,3,3,3,3,3,3,3,3,3,3,3,3,3,4),(0.,1.53100299373417E-6,
4.52554775679272E-6,7.01151246291594E-6,9.26752933800003E-6,1.03084066197173E-5,
1.17138990826861E-5,1.22284894984073E-5,1.30315035324815E-5,1.38363728497812E-5,
1.40464197777495E-5,1.54597749564639E-5,1.62073588704069E-5,1.92092968713092E-5,
1.95234416882555E-5,2.37637844577628E-5,2.61487188977262E-5),
 .UNSPECIFIED.);
#25588=B_SPLINE_CURVE_WITH_KNOTS('',3,(#400606,#400607,#400608,#400609,
#400610,#400611,#400612,#400613,#400614,#400615,#400616,#400617,#400618,
#400619,#400620,#400621,#400622,#400623,#400624,#400625,#400626,#400627,
#400628,#400629,#400630,#400631,#400632,#400633,#400634,#400635,#400636),
 .UNSPECIFIED.,.F.,.F.,(4,3,3,3,3,3,3,3,3,3,4),(0.,3.955079103977E-6,7.5376842660419E-6,
1.19904533335349E-5,1.40475043392587E-5,1.51452104275965E-5,1.67866272814353E-5,
1.69621513005359E-5,1.81338315460712E-5,1.9890633465657E-5,2.06132424588247E-5),
 .UNSPECIFIED.);
#25589=B_SPLINE_CURVE_WITH_KNOTS('',3,(#400639,#400640,#400641,#400642),
 .UNSPECIFIED.,.F.,.F.,(4,4),(2.16840434497101E-19,0.00010938435327491),
 .UNSPECIFIED.);
#25590=B_SPLINE_CURVE_WITH_KNOTS('',3,(#400669,#400670,#400671,#400672,
#400673,#400674,#400675,#400676,#400677,#400678,#400679,#400680,#400681,
#400682,#400683,#400684,#400685,#400686,#400687,#400688,#400689,#400690,
#400691,#400692,#400693,#400694,#400695,#400696,#400697,#400698,#400699,
#400700,#400701,#400702),.UNSPECIFIED.,.F.,.F.,(4,3,3,3,3,3,3,3,3,3,3,4),
(0.,2.09623992729445E-6,3.17176647120223E-6,4.82636181943907E-6,5.01000917339951E-6,
6.131264541475E-6,8.60486650288844E-6,9.21144281170483E-6,1.24722301135966E-5,
1.42666454787851E-5,2.0467065375686E-5,2.08026438176793E-5),
 .UNSPECIFIED.);
#25591=B_SPLINE_CURVE_WITH_KNOTS('',3,(#400703,#400704,#400705,#400706),
 .UNSPECIFIED.,.F.,.F.,(4,4),(0.,0.000109384345496908),.UNSPECIFIED.);
#25592=B_SPLINE_CURVE_WITH_KNOTS('',3,(#400811,#400812,#400813,#400814),
 .UNSPECIFIED.,.F.,.F.,(4,4),(0.,9.54361881492176E-5),.UNSPECIFIED.);
#25593=B_SPLINE_CURVE_WITH_KNOTS('',3,(#400819,#400820,#400821,#400822,
#400823,#400824,#400825),.UNSPECIFIED.,.F.,.F.,(4,3,4),(0.,4.41069704323469E-5,
0.000113970027818833),.UNSPECIFIED.);
#25594=B_SPLINE_CURVE_WITH_KNOTS('',3,(#400831,#400832,#400833,#400834),
 .UNSPECIFIED.,.F.,.F.,(4,4),(0.,9.54361881492176E-5),.UNSPECIFIED.);
#25595=B_SPLINE_CURVE_WITH_KNOTS('',3,(#400838,#400839,#400840,#400841,
#400842,#400843,#400844),.UNSPECIFIED.,.F.,.F.,(4,3,4),(0.,6.9863024419149E-5,
0.000113969974038089),.UNSPECIFIED.);
#25596=B_SPLINE_CURVE_WITH_KNOTS('',3,(#400847,#400848,#400849,#400850,
#400851,#400852,#400853,#400854,#400855,#400856,#400857,#400858,#400859,
#400860,#400861,#400862,#400863,#400864,#400865,#400866,#400867,#400868,
#400869,#400870,#400871,#400872,#400873,#400874,#400875,#400876,#400877,
#400878,#400879,#400880,#400881,#400882,#400883,#400884,#400885,#400886,
#400887,#400888,#400889,#400890,#400891,#400892,#400893,#400894,#400895),
 .UNSPECIFIED.,.F.,.F.,(4,3,3,3,3,3,3,3,3,3,3,3,3,3,3,3,4),(0.,1.53100299373414E-6,
4.52554775679455E-6,7.01151246291618E-6,9.26752933800158E-6,1.03084066197174E-5,
1.17138990826862E-5,1.22284894984075E-5,1.30315035324817E-5,1.38363728497811E-5,
1.40464197777495E-5,1.54597749564639E-5,1.62073588704068E-5,1.92092968712879E-5,
1.95234416882552E-5,2.3763784457757E-5,2.61487188977255E-5),
 .UNSPECIFIED.);
#25597=B_SPLINE_CURVE_WITH_KNOTS('',3,(#400910,#400911,#400912,#400913,
#400914,#400915,#400916,#400917,#400918,#400919,#400920,#400921,#400922,
#400923,#400924,#400925,#400926,#400927,#400928,#400929,#400930,#400931,
#400932,#400933,#400934,#400935,#400936,#400937,#400938,#400939,#400940),
 .UNSPECIFIED.,.F.,.F.,(4,3,3,3,3,3,3,3,3,3,4),(0.,3.95507910398038E-6,
7.53768426604196E-6,1.1990453333535E-5,1.40475043392586E-5,1.51452104275967E-5,
1.67866272814212E-5,1.69621513005361E-5,1.81338315460711E-5,1.98906334656552E-5,
2.06132424588246E-5),.UNSPECIFIED.);
#25598=B_SPLINE_CURVE_WITH_KNOTS('',3,(#400943,#400944,#400945,#400946),
 .UNSPECIFIED.,.F.,.F.,(4,4),(4.33680868994202E-19,0.00010938435327491),
 .UNSPECIFIED.);
#25599=B_SPLINE_CURVE_WITH_KNOTS('',3,(#400973,#400974,#400975,#400976,
#400977,#400978,#400979,#400980,#400981,#400982,#400983,#400984,#400985,
#400986,#400987,#400988,#400989,#400990,#400991,#400992,#400993,#400994,
#400995,#400996,#400997,#400998,#400999,#401000,#401001,#401002,#401003,
#401004,#401005,#401006),.UNSPECIFIED.,.F.,.F.,(4,3,3,3,3,3,3,3,3,3,3,4),
(3.06658683336675E-19,2.0962399272942E-6,3.17176647120205E-6,4.82636181942511E-6,
5.01000917339963E-6,6.13126454147484E-6,8.6048665028884E-6,9.21144281170476E-6,
1.24722301135868E-5,1.42666454787856E-5,2.0467065375687E-5,2.08026438176804E-5),
 .UNSPECIFIED.);
#25600=B_SPLINE_CURVE_WITH_KNOTS('',3,(#401007,#401008,#401009,#401010),
 .UNSPECIFIED.,.F.,.F.,(4,4),(0.,0.000109384345496908),.UNSPECIFIED.);
#25601=B_SPLINE_CURVE_WITH_KNOTS('',3,(#401115,#401116,#401117,#401118),
 .UNSPECIFIED.,.F.,.F.,(4,4),(0.,9.54361881492175E-5),.UNSPECIFIED.);
#25602=B_SPLINE_CURVE_WITH_KNOTS('',3,(#401123,#401124,#401125,#401126,
#401127,#401128,#401129),.UNSPECIFIED.,.F.,.F.,(4,3,4),(0.,4.41069704323469E-5,
0.000113970027818833),.UNSPECIFIED.);
#25603=B_SPLINE_CURVE_WITH_KNOTS('',3,(#401135,#401136,#401137,#401138),
 .UNSPECIFIED.,.F.,.F.,(4,4),(4.33680868994202E-19,9.54361881492178E-5),
 .UNSPECIFIED.);
#25604=B_SPLINE_CURVE_WITH_KNOTS('',3,(#401142,#401143,#401144,#401145,
#401146,#401147,#401148),.UNSPECIFIED.,.F.,.F.,(4,3,4),(0.,6.9863024419149E-5,
0.000113969974038089),.UNSPECIFIED.);
#25605=B_SPLINE_CURVE_WITH_KNOTS('',3,(#401151,#401152,#401153,#401154,
#401155,#401156,#401157,#401158,#401159,#401160,#401161,#401162,#401163,
#401164,#401165,#401166,#401167,#401168,#401169,#401170,#401171,#401172,
#401173,#401174,#401175,#401176,#401177,#401178,#401179,#401180,#401181,
#401182,#401183,#401184,#401185,#401186,#401187,#401188,#401189,#401190,
#401191,#401192,#401193,#401194,#401195,#401196,#401197,#401198,#401199),
 .UNSPECIFIED.,.F.,.F.,(4,3,3,3,3,3,3,3,3,3,3,3,3,3,3,3,4),(0.,1.53100299373413E-6,
4.52554775679261E-6,7.01151246291609E-6,9.26752933800109E-6,1.03084066197174E-5,
1.17138990826864E-5,1.22284894984075E-5,1.30315035324817E-5,1.38363728497814E-5,
1.40464197777494E-5,1.54597749564638E-5,1.62073588704068E-5,1.92092968712784E-5,
1.95234416882556E-5,2.37637844577558E-5,2.61487188977267E-5),
 .UNSPECIFIED.);
#25606=B_SPLINE_CURVE_WITH_KNOTS('',3,(#401214,#401215,#401216,#401217,
#401218,#401219,#401220,#401221,#401222,#401223,#401224,#401225,#401226,
#401227,#401228,#401229,#401230,#401231,#401232,#401233,#401234,#401235,
#401236,#401237,#401238,#401239,#401240,#401241,#401242,#401243,#401244),
 .UNSPECIFIED.,.F.,.F.,(4,3,3,3,3,3,3,3,3,3,4),(0.,3.95507910396964E-6,
7.53768426604187E-6,1.19904533335349E-5,1.40475043392586E-5,1.51452104275963E-5,
1.6786627281416E-5,1.69621513005355E-5,1.81338315460709E-5,1.98906334656525E-5,
2.0613242458824E-5),.UNSPECIFIED.);
#25607=B_SPLINE_CURVE_WITH_KNOTS('',3,(#401247,#401248,#401249,#401250),
 .UNSPECIFIED.,.F.,.F.,(4,4),(4.33680868994202E-19,0.00010938435327491),
 .UNSPECIFIED.);
#25608=B_SPLINE_CURVE_WITH_KNOTS('',3,(#401277,#401278,#401279,#401280,
#401281,#401282,#401283,#401284,#401285,#401286,#401287,#401288,#401289,
#401290,#401291,#401292,#401293,#401294,#401295,#401296,#401297,#401298,
#401299,#401300,#401301,#401302,#401303,#401304,#401305,#401306,#401307,
#401308,#401309,#401310),.UNSPECIFIED.,.F.,.F.,(4,3,3,3,3,3,3,3,3,3,3,4),
(2.16840434497101E-19,2.09623992729392E-6,3.17176647120205E-6,4.82636181942159E-6,
5.01000917339932E-6,6.13126454147464E-6,8.60486650288817E-6,9.2114428117045E-6,
1.24722301136082E-5,1.42666454787851E-5,2.04670653757038E-5,2.08026438176795E-5),
 .UNSPECIFIED.);
#25609=B_SPLINE_CURVE_WITH_KNOTS('',3,(#401311,#401312,#401313,#401314),
 .UNSPECIFIED.,.F.,.F.,(4,4),(0.,0.000109384345496908),.UNSPECIFIED.);
#25610=B_SPLINE_CURVE_WITH_KNOTS('',3,(#401419,#401420,#401421,#401422),
 .UNSPECIFIED.,.F.,.F.,(4,4),(0.,9.54361881492175E-5),.UNSPECIFIED.);
#25611=B_SPLINE_CURVE_WITH_KNOTS('',3,(#401427,#401428,#401429,#401430,
#401431,#401432,#401433),.UNSPECIFIED.,.F.,.F.,(4,3,4),(0.,4.41069704323469E-5,
0.000113970027818833),.UNSPECIFIED.);
#25612=B_SPLINE_CURVE_WITH_KNOTS('',3,(#401439,#401440,#401441,#401442),
 .UNSPECIFIED.,.F.,.F.,(4,4),(4.33680868994202E-19,9.54361881492177E-5),
 .UNSPECIFIED.);
#25613=B_SPLINE_CURVE_WITH_KNOTS('',3,(#401446,#401447,#401448,#401449,
#401450,#401451,#401452),.UNSPECIFIED.,.F.,.F.,(4,3,4),(0.,6.98630244191489E-5,
0.000113969974038089),.UNSPECIFIED.);
#25614=B_SPLINE_CURVE_WITH_KNOTS('',3,(#401455,#401456,#401457,#401458,
#401459,#401460,#401461,#401462,#401463,#401464,#401465,#401466,#401467,
#401468,#401469,#401470,#401471,#401472,#401473,#401474,#401475,#401476,
#401477,#401478,#401479,#401480,#401481,#401482,#401483,#401484,#401485,
#401486,#401487,#401488,#401489,#401490,#401491,#401492,#401493,#401494,
#401495,#401496,#401497,#401498,#401499,#401500,#401501,#401502,#401503),
 .UNSPECIFIED.,.F.,.F.,(4,3,3,3,3,3,3,3,3,3,3,3,3,3,3,3,4),(0.,1.53100299373419E-6,
4.52554775679468E-6,7.01151246291595E-6,9.26752933801825E-6,1.03084066197172E-5,
1.17138990826859E-5,1.22284894984072E-5,1.30315035324817E-5,1.38363728497812E-5,
1.40464197777492E-5,1.54597749564638E-5,1.62073588704066E-5,1.92092968712874E-5,
1.95234416882548E-5,2.37637844577601E-5,2.61487188977246E-5),
 .UNSPECIFIED.);
#25615=B_SPLINE_CURVE_WITH_KNOTS('',3,(#401518,#401519,#401520,#401521,
#401522,#401523,#401524,#401525,#401526,#401527,#401528,#401529,#401530,
#401531,#401532,#401533,#401534,#401535,#401536,#401537,#401538,#401539,
#401540,#401541,#401542,#401543,#401544,#401545,#401546,#401547,#401548),
 .UNSPECIFIED.,.F.,.F.,(4,3,3,3,3,3,3,3,3,3,4),(0.,3.95507910396898E-6,
7.537684266042E-6,1.1990453333535E-5,1.40475043392585E-5,1.51452104275964E-5,
1.67866272814168E-5,1.69621513005359E-5,1.81338315460712E-5,1.98906334656556E-5,
2.06132424588245E-5),.UNSPECIFIED.);
#25616=B_SPLINE_CURVE_WITH_KNOTS('',3,(#401551,#401552,#401553,#401554),
 .UNSPECIFIED.,.F.,.F.,(4,4),(4.33680868994202E-19,0.00010938435327491),
 .UNSPECIFIED.);
#25617=B_SPLINE_CURVE_WITH_KNOTS('',3,(#401581,#401582,#401583,#401584,
#401585,#401586,#401587,#401588,#401589,#401590,#401591,#401592,#401593,
#401594,#401595,#401596,#401597,#401598,#401599,#401600,#401601,#401602,
#401603,#401604,#401605,#401606,#401607,#401608,#401609,#401610,#401611,
#401612,#401613,#401614),.UNSPECIFIED.,.F.,.F.,(4,3,3,3,3,3,3,3,3,3,3,4),
(2.16840434497101E-19,2.09623992729436E-6,3.17176647120222E-6,4.82636181944612E-6,
5.01000917339947E-6,6.13126454147495E-6,8.60486650288831E-6,9.21144281170459E-6,
1.24722301136143E-5,1.42666454787854E-5,2.04670653756866E-5,2.08026438176799E-5),
 .UNSPECIFIED.);
#25618=B_SPLINE_CURVE_WITH_KNOTS('',3,(#401615,#401616,#401617,#401618),
 .UNSPECIFIED.,.F.,.F.,(4,4),(0.,0.000109384345496908),.UNSPECIFIED.);
#25619=B_SPLINE_CURVE_WITH_KNOTS('',3,(#401723,#401724,#401725,#401726),
 .UNSPECIFIED.,.F.,.F.,(4,4),(0.,9.54361881492177E-5),.UNSPECIFIED.);
#25620=B_SPLINE_CURVE_WITH_KNOTS('',3,(#401731,#401732,#401733,#401734,
#401735,#401736,#401737),.UNSPECIFIED.,.F.,.F.,(4,3,4),(0.,4.41069704323469E-5,
0.000113970027818833),.UNSPECIFIED.);
#25621=B_SPLINE_CURVE_WITH_KNOTS('',3,(#401743,#401744,#401745,#401746),
 .UNSPECIFIED.,.F.,.F.,(4,4),(4.33680868994202E-19,9.54361881492178E-5),
 .UNSPECIFIED.);
#25622=B_SPLINE_CURVE_WITH_KNOTS('',3,(#401750,#401751,#401752,#401753,
#401754,#401755,#401756),.UNSPECIFIED.,.F.,.F.,(4,3,4),(0.,6.98630244191488E-5,
0.000113969974038089),.UNSPECIFIED.);
#25623=B_SPLINE_CURVE_WITH_KNOTS('',3,(#401759,#401760,#401761,#401762,
#401763,#401764,#401765,#401766,#401767,#401768,#401769,#401770,#401771,
#401772,#401773,#401774,#401775,#401776,#401777,#401778,#401779,#401780,
#401781,#401782,#401783,#401784,#401785,#401786,#401787,#401788,#401789,
#401790,#401791,#401792,#401793,#401794,#401795,#401796,#401797,#401798,
#401799,#401800,#401801,#401802,#401803,#401804,#401805,#401806,#401807),
 .UNSPECIFIED.,.F.,.F.,(4,3,3,3,3,3,3,3,3,3,3,3,3,3,3,3,4),(0.,1.53100299373429E-6,
4.5255477568026E-6,7.01151246291634E-6,9.26752933801703E-6,1.03084066197173E-5,
1.17138990826863E-5,1.22284894984075E-5,1.3031503532482E-5,1.38363728497815E-5,
1.40464197777499E-5,1.54597749564644E-5,1.62073588704075E-5,1.92092968712479E-5,
1.95234416882565E-5,2.37637844577607E-5,2.61487188977278E-5),
 .UNSPECIFIED.);
#25624=B_SPLINE_CURVE_WITH_KNOTS('',3,(#401822,#401823,#401824,#401825,
#401826,#401827,#401828,#401829,#401830,#401831,#401832,#401833,#401834,
#401835,#401836,#401837,#401838,#401839,#401840,#401841,#401842,#401843,
#401844,#401845,#401846,#401847,#401848,#401849,#401850,#401851,#401852),
 .UNSPECIFIED.,.F.,.F.,(4,3,3,3,3,3,3,3,3,3,4),(0.,3.95507910398437E-6,
7.53768426604198E-6,1.1990453333535E-5,1.40475043392586E-5,1.51452104275963E-5,
1.67866272814243E-5,1.69621513005356E-5,1.81338315460712E-5,1.98906334656531E-5,
2.06132424588245E-5),.UNSPECIFIED.);
#25625=B_SPLINE_CURVE_WITH_KNOTS('',3,(#401855,#401856,#401857,#401858),
 .UNSPECIFIED.,.F.,.F.,(4,4),(4.33680868994202E-19,0.00010938435327491),
 .UNSPECIFIED.);
#25626=B_SPLINE_CURVE_WITH_KNOTS('',3,(#401885,#401886,#401887,#401888,
#401889,#401890,#401891,#401892,#401893,#401894,#401895,#401896,#401897,
#401898,#401899,#401900,#401901,#401902,#401903,#401904,#401905,#401906,
#401907,#401908,#401909,#401910,#401911,#401912,#401913,#401914,#401915,
#401916,#401917,#401918),.UNSPECIFIED.,.F.,.F.,(4,3,3,3,3,3,3,3,3,3,3,4),
(2.16840434497101E-19,2.09623992729449E-6,3.17176647120214E-6,4.82636181942187E-6,
5.01000917339954E-6,6.13126454147488E-6,8.60486650288861E-6,9.21144281170478E-6,
1.24722301135873E-5,1.42666454787854E-5,2.04670653756818E-5,2.08026438176801E-5),
 .UNSPECIFIED.);
#25627=B_SPLINE_CURVE_WITH_KNOTS('',3,(#401919,#401920,#401921,#401922),
 .UNSPECIFIED.,.F.,.F.,(4,4),(0.,0.000109384345496908),.UNSPECIFIED.);
#25628=B_SPLINE_CURVE_WITH_KNOTS('',3,(#402027,#402028,#402029,#402030),
 .UNSPECIFIED.,.F.,.F.,(4,4),(0.,9.54361881492177E-5),.UNSPECIFIED.);
#25629=B_SPLINE_CURVE_WITH_KNOTS('',3,(#402035,#402036,#402037,#402038,
#402039,#402040,#402041),.UNSPECIFIED.,.F.,.F.,(4,3,4),(0.,4.4106970432347E-5,
0.000113970027818834),.UNSPECIFIED.);
#25630=B_SPLINE_CURVE_WITH_KNOTS('',3,(#402047,#402048,#402049,#402050),
 .UNSPECIFIED.,.F.,.F.,(4,4),(4.33680868994202E-19,9.54361881492178E-5),
 .UNSPECIFIED.);
#25631=B_SPLINE_CURVE_WITH_KNOTS('',3,(#402054,#402055,#402056,#402057,
#402058,#402059,#402060),.UNSPECIFIED.,.F.,.F.,(4,3,4),(0.,6.9863024419149E-5,
0.000113969974038089),.UNSPECIFIED.);
#25632=B_SPLINE_CURVE_WITH_KNOTS('',3,(#402063,#402064,#402065,#402066,
#402067,#402068,#402069,#402070,#402071,#402072,#402073,#402074,#402075,
#402076,#402077,#402078,#402079,#402080,#402081,#402082,#402083,#402084,
#402085,#402086,#402087,#402088,#402089,#402090,#402091,#402092,#402093,
#402094,#402095,#402096,#402097,#402098,#402099,#402100,#402101,#402102,
#402103,#402104,#402105,#402106,#402107,#402108,#402109,#402110,#402111),
 .UNSPECIFIED.,.F.,.F.,(4,3,3,3,3,3,3,3,3,3,3,3,3,3,3,3,4),(0.,1.53100299373411E-6,
4.52554775679681E-6,7.01151246291603E-6,9.26752933799318E-6,1.03084066197172E-5,
1.1713899082686E-5,1.22284894984074E-5,1.30315035324816E-5,1.38363728497814E-5,
1.40464197777494E-5,1.54597749564641E-5,1.62073588704069E-5,1.920929687127E-5,
1.95234416882557E-5,2.37637844577625E-5,2.61487188977266E-5),
 .UNSPECIFIED.);
#25633=B_SPLINE_CURVE_WITH_KNOTS('',3,(#402126,#402127,#402128,#402129,
#402130,#402131,#402132,#402133,#402134,#402135,#402136,#402137,#402138,
#402139,#402140,#402141,#402142,#402143,#402144,#402145,#402146,#402147,
#402148,#402149,#402150,#402151,#402152,#402153,#402154,#402155,#402156),
 .UNSPECIFIED.,.F.,.F.,(4,3,3,3,3,3,3,3,3,3,4),(0.,3.95507910397755E-6,
7.53768426604204E-6,1.1990453333535E-5,1.40475043392587E-5,1.51452104275965E-5,
1.67866272814177E-5,1.69621513005359E-5,1.81338315460714E-5,1.98906334656546E-5,
2.0613242458825E-5),.UNSPECIFIED.);
#25634=B_SPLINE_CURVE_WITH_KNOTS('',3,(#402159,#402160,#402161,#402162),
 .UNSPECIFIED.,.F.,.F.,(4,4),(9.69739903612216E-19,0.000109384353274909),
 .UNSPECIFIED.);
#25635=B_SPLINE_CURVE_WITH_KNOTS('',3,(#402189,#402190,#402191,#402192,
#402193,#402194,#402195,#402196,#402197,#402198,#402199,#402200,#402201,
#402202,#402203,#402204,#402205,#402206,#402207,#402208,#402209,#402210,
#402211,#402212,#402213,#402214,#402215,#402216,#402217,#402218,#402219,
#402220,#402221,#402222),.UNSPECIFIED.,.F.,.F.,(4,3,3,3,3,3,3,3,3,3,3,4),
(0.,2.09623992729429E-6,3.17176647120231E-6,4.82636181944926E-6,5.01000917339935E-6,
6.13126454147493E-6,8.60486650288825E-6,9.21144281170447E-6,1.24722301135953E-5,
1.4266645478785E-5,2.04670653756821E-5,2.08026438176793E-5),
 .UNSPECIFIED.);
#25636=B_SPLINE_CURVE_WITH_KNOTS('',3,(#402223,#402224,#402225,#402226),
 .UNSPECIFIED.,.F.,.F.,(4,4),(0.,0.000109384345496908),.UNSPECIFIED.);
#25637=B_SPLINE_CURVE_WITH_KNOTS('',3,(#402331,#402332,#402333,#402334),
 .UNSPECIFIED.,.F.,.F.,(4,4),(0.,9.54361881492175E-5),.UNSPECIFIED.);
#25638=B_SPLINE_CURVE_WITH_KNOTS('',3,(#402339,#402340,#402341,#402342,
#402343,#402344,#402345),.UNSPECIFIED.,.F.,.F.,(4,3,4),(0.,4.4106970432347E-5,
0.000113970027818833),.UNSPECIFIED.);
#25639=B_SPLINE_CURVE_WITH_KNOTS('',3,(#402351,#402352,#402353,#402354),
 .UNSPECIFIED.,.F.,.F.,(4,4),(4.33680868994202E-19,9.54361881492175E-5),
 .UNSPECIFIED.);
#25640=B_SPLINE_CURVE_WITH_KNOTS('',3,(#402358,#402359,#402360,#402361,
#402362,#402363,#402364),.UNSPECIFIED.,.F.,.F.,(4,3,4),(0.,6.98630244191489E-5,
0.000113969974038089),.UNSPECIFIED.);
#25641=B_SPLINE_CURVE_WITH_KNOTS('',3,(#402367,#402368,#402369,#402370,
#402371,#402372,#402373,#402374,#402375,#402376,#402377,#402378,#402379,
#402380,#402381,#402382,#402383,#402384,#402385,#402386,#402387,#402388,
#402389,#402390,#402391,#402392,#402393,#402394,#402395,#402396,#402397,
#402398,#402399,#402400,#402401,#402402,#402403,#402404,#402405,#402406,
#402407,#402408,#402409,#402410,#402411,#402412,#402413,#402414,#402415),
 .UNSPECIFIED.,.F.,.F.,(4,3,3,3,3,3,3,3,3,3,3,3,3,3,3,3,4),(0.,1.53100299373417E-6,
4.52554775680002E-6,7.01151246291616E-6,9.26752933800212E-6,1.03084066197174E-5,
1.1713899082686E-5,1.22284894984073E-5,1.30315035324815E-5,1.38363728497811E-5,
1.40464197777491E-5,1.54597749564636E-5,1.62073588704065E-5,1.92092968712526E-5,
1.95234416882551E-5,2.37637844577574E-5,2.61487188977254E-5),
 .UNSPECIFIED.);
#25642=B_SPLINE_CURVE_WITH_KNOTS('',3,(#402430,#402431,#402432,#402433,
#402434,#402435,#402436,#402437,#402438,#402439,#402440,#402441,#402442,
#402443,#402444,#402445,#402446,#402447,#402448,#402449,#402450,#402451,
#402452,#402453,#402454,#402455,#402456,#402457,#402458,#402459,#402460),
 .UNSPECIFIED.,.F.,.F.,(4,3,3,3,3,3,3,3,3,3,4),(0.,3.9550791039745E-6,7.53768426604198E-6,
1.19904533335351E-5,1.40475043392586E-5,1.51452104275967E-5,1.67866272814068E-5,
1.69621513005358E-5,1.81338315460714E-5,1.98906334656572E-5,2.06132424588245E-5),
 .UNSPECIFIED.);
#25643=B_SPLINE_CURVE_WITH_KNOTS('',3,(#402463,#402464,#402465,#402466),
 .UNSPECIFIED.,.F.,.F.,(4,4),(4.33680868994202E-19,0.00010938435327491),
 .UNSPECIFIED.);
#25644=B_SPLINE_CURVE_WITH_KNOTS('',3,(#402493,#402494,#402495,#402496,
#402497,#402498,#402499,#402500,#402501,#402502,#402503,#402504,#402505,
#402506,#402507,#402508,#402509,#402510,#402511,#402512,#402513,#402514,
#402515,#402516,#402517,#402518,#402519,#402520,#402521,#402522,#402523,
#402524,#402525,#402526),.UNSPECIFIED.,.F.,.F.,(4,3,3,3,3,3,3,3,3,3,3,4),
(2.16840434497101E-19,2.09623992729457E-6,3.17176647120237E-6,4.8263618194444E-6,
5.01000917339961E-6,6.13126454147503E-6,8.6048665028887E-6,9.21144281170501E-6,
1.24722301135885E-5,1.42666454787857E-5,2.04670653756818E-5,2.08026438176804E-5),
 .UNSPECIFIED.);
#25645=B_SPLINE_CURVE_WITH_KNOTS('',3,(#402527,#402528,#402529,#402530),
 .UNSPECIFIED.,.F.,.F.,(4,4),(0.,0.000109384345496908),.UNSPECIFIED.);
#25646=B_SPLINE_CURVE_WITH_KNOTS('',3,(#402635,#402636,#402637,#402638),
 .UNSPECIFIED.,.F.,.F.,(4,4),(0.,9.54361881492175E-5),.UNSPECIFIED.);
#25647=B_SPLINE_CURVE_WITH_KNOTS('',3,(#402643,#402644,#402645,#402646,
#402647,#402648,#402649),.UNSPECIFIED.,.F.,.F.,(4,3,4),(0.,4.41069704323469E-5,
0.000113970027818833),.UNSPECIFIED.);
#25648=B_SPLINE_CURVE_WITH_KNOTS('',3,(#402655,#402656,#402657,#402658),
 .UNSPECIFIED.,.F.,.F.,(4,4),(4.33680868994202E-19,9.54361881492175E-5),
 .UNSPECIFIED.);
#25649=B_SPLINE_CURVE_WITH_KNOTS('',3,(#402662,#402663,#402664,#402665,
#402666,#402667,#402668),.UNSPECIFIED.,.F.,.F.,(4,3,4),(0.,6.98630244191489E-5,
0.000113969974038089),.UNSPECIFIED.);
#25650=B_SPLINE_CURVE_WITH_KNOTS('',3,(#402671,#402672,#402673,#402674,
#402675,#402676,#402677,#402678,#402679,#402680,#402681,#402682,#402683,
#402684,#402685,#402686,#402687,#402688,#402689,#402690,#402691,#402692,
#402693,#402694,#402695,#402696,#402697,#402698,#402699,#402700,#402701,
#402702,#402703,#402704,#402705,#402706,#402707,#402708,#402709,#402710,
#402711,#402712,#402713,#402714,#402715,#402716,#402717,#402718,#402719),
 .UNSPECIFIED.,.F.,.F.,(4,3,3,3,3,3,3,3,3,3,3,3,3,3,3,3,4),(0.,1.53100299373418E-6,
4.52554775679361E-6,7.01151246291622E-6,9.26752933800728E-6,1.03084066197175E-5,
1.17138990826863E-5,1.22284894984073E-5,1.30315035324818E-5,1.38363728497812E-5,
1.40464197777495E-5,1.54597749564641E-5,1.62073588704069E-5,1.92092968713019E-5,
1.95234416882557E-5,2.37637844577584E-5,2.61487188977265E-5),
 .UNSPECIFIED.);
#25651=B_SPLINE_CURVE_WITH_KNOTS('',3,(#402734,#402735,#402736,#402737,
#402738,#402739,#402740,#402741,#402742,#402743,#402744,#402745,#402746,
#402747,#402748,#402749,#402750,#402751,#402752,#402753,#402754,#402755,
#402756,#402757,#402758,#402759,#402760,#402761,#402762,#402763,#402764),
 .UNSPECIFIED.,.F.,.F.,(4,3,3,3,3,3,3,3,3,3,4),(0.,3.95507910398474E-6,
7.53768426604196E-6,1.1990453333535E-5,1.40475043392584E-5,1.51452104275962E-5,
1.67866272814233E-5,1.69621513005357E-5,1.8133831546071E-5,1.98906334656502E-5,
2.06132424588241E-5),.UNSPECIFIED.);
#25652=B_SPLINE_CURVE_WITH_KNOTS('',3,(#402767,#402768,#402769,#402770),
 .UNSPECIFIED.,.F.,.F.,(4,4),(4.33680868994202E-19,0.00010938435327491),
 .UNSPECIFIED.);
#25653=B_SPLINE_CURVE_WITH_KNOTS('',3,(#402797,#402798,#402799,#402800,
#402801,#402802,#402803,#402804,#402805,#402806,#402807,#402808,#402809,
#402810,#402811,#402812,#402813,#402814,#402815,#402816,#402817,#402818,
#402819,#402820,#402821,#402822,#402823,#402824,#402825,#402826,#402827,
#402828,#402829,#402830),.UNSPECIFIED.,.F.,.F.,(4,3,3,3,3,3,3,3,3,3,3,4),
(0.,2.09623992729435E-6,3.17176647120212E-6,4.82636181943321E-6,5.01000917339988E-6,
6.13126454147513E-6,8.60486650288861E-6,9.21144281170496E-6,1.24722301136148E-5,
1.4266645478786E-5,2.04670653756914E-5,2.08026438176811E-5),
 .UNSPECIFIED.);
#25654=B_SPLINE_CURVE_WITH_KNOTS('',3,(#402831,#402832,#402833,#402834),
 .UNSPECIFIED.,.F.,.F.,(4,4),(0.,0.000109384345496909),.UNSPECIFIED.);
#25655=B_SPLINE_CURVE_WITH_KNOTS('',3,(#402939,#402940,#402941,#402942),
 .UNSPECIFIED.,.F.,.F.,(4,4),(0.,9.54361881492174E-5),.UNSPECIFIED.);
#25656=B_SPLINE_CURVE_WITH_KNOTS('',3,(#402947,#402948,#402949,#402950,
#402951,#402952,#402953),.UNSPECIFIED.,.F.,.F.,(4,3,4),(0.,4.41069704323467E-5,
0.000113970027818833),.UNSPECIFIED.);
#25657=B_SPLINE_CURVE_WITH_KNOTS('',3,(#402959,#402960,#402961,#402962),
 .UNSPECIFIED.,.F.,.F.,(4,4),(4.33680868994202E-19,9.54361881492178E-5),
 .UNSPECIFIED.);
#25658=B_SPLINE_CURVE_WITH_KNOTS('',3,(#402966,#402967,#402968,#402969,
#402970,#402971,#402972),.UNSPECIFIED.,.F.,.F.,(4,3,4),(0.,6.98630244191492E-5,
0.000113969974038089),.UNSPECIFIED.);
#25659=B_SPLINE_CURVE_WITH_KNOTS('',3,(#402975,#402976,#402977,#402978,
#402979,#402980,#402981,#402982,#402983,#402984,#402985,#402986,#402987,
#402988,#402989,#402990,#402991,#402992,#402993,#402994,#402995,#402996,
#402997,#402998,#402999,#403000,#403001,#403002,#403003,#403004,#403005,
#403006,#403007,#403008,#403009,#403010,#403011,#403012,#403013,#403014,
#403015,#403016,#403017,#403018,#403019,#403020,#403021,#403022,#403023),
 .UNSPECIFIED.,.F.,.F.,(4,3,3,3,3,3,3,3,3,3,3,3,3,3,3,3,4),(0.,1.53100299373391E-6,
4.52554775679138E-6,7.01151246291585E-6,9.2675293380002E-6,1.03084066197173E-5,
1.17138990826862E-5,1.22284894984076E-5,1.30315035324817E-5,1.38363728497813E-5,
1.40464197777495E-5,1.54597749564641E-5,1.6207358870407E-5,1.92092968713447E-5,
1.95234416882558E-5,2.37637844577641E-5,2.61487188977268E-5),
 .UNSPECIFIED.);
#25660=B_SPLINE_CURVE_WITH_KNOTS('',3,(#403038,#403039,#403040,#403041,
#403042,#403043,#403044,#403045,#403046,#403047,#403048,#403049,#403050,
#403051,#403052,#403053,#403054,#403055,#403056,#403057,#403058,#403059,
#403060,#403061,#403062,#403063,#403064,#403065,#403066,#403067,#403068),
 .UNSPECIFIED.,.F.,.F.,(4,3,3,3,3,3,3,3,3,3,4),(0.,3.95507910399186E-6,
7.53768426604196E-6,1.1990453333535E-5,1.40475043392585E-5,1.51452104275965E-5,
1.67866272814145E-5,1.69621513005358E-5,1.81338315460712E-5,1.9890633465651E-5,
2.06132424588246E-5),.UNSPECIFIED.);
#25661=B_SPLINE_CURVE_WITH_KNOTS('',3,(#403071,#403072,#403073,#403074),
 .UNSPECIFIED.,.F.,.F.,(4,4),(4.47028007668187E-19,0.00010938435327491),
 .UNSPECIFIED.);
#25662=B_SPLINE_CURVE_WITH_KNOTS('',3,(#403101,#403102,#403103,#403104,
#403105,#403106,#403107,#403108,#403109,#403110,#403111,#403112,#403113,
#403114,#403115,#403116,#403117,#403118,#403119,#403120,#403121,#403122,
#403123,#403124,#403125,#403126,#403127,#403128,#403129,#403130,#403131,
#403132,#403133,#403134),.UNSPECIFIED.,.F.,.F.,(4,3,3,3,3,3,3,3,3,3,3,4),
(1.0842021724855E-19,2.09623992729434E-6,3.17176647120229E-6,4.82636181944625E-6,
5.01000917339952E-6,6.13126454147493E-6,8.6048665028886E-6,9.2114428117048E-6,
1.24722301135969E-5,1.42666454787854E-5,2.04670653756842E-5,2.08026438176801E-5),
 .UNSPECIFIED.);
#25663=B_SPLINE_CURVE_WITH_KNOTS('',3,(#403135,#403136,#403137,#403138),
 .UNSPECIFIED.,.F.,.F.,(4,4),(0.,0.000109384345496909),.UNSPECIFIED.);
#25664=B_SPLINE_CURVE_WITH_KNOTS('',3,(#403243,#403244,#403245,#403246),
 .UNSPECIFIED.,.F.,.F.,(4,4),(0.,9.54361881492175E-5),.UNSPECIFIED.);
#25665=B_SPLINE_CURVE_WITH_KNOTS('',3,(#403251,#403252,#403253,#403254,
#403255,#403256,#403257),.UNSPECIFIED.,.F.,.F.,(4,3,4),(0.,4.41069704323469E-5,
0.000113970027818833),.UNSPECIFIED.);
#25666=B_SPLINE_CURVE_WITH_KNOTS('',3,(#403263,#403264,#403265,#403266),
 .UNSPECIFIED.,.F.,.F.,(4,4),(4.47028007668187E-19,9.54361881492181E-5),
 .UNSPECIFIED.);
#25667=B_SPLINE_CURVE_WITH_KNOTS('',3,(#403270,#403271,#403272,#403273,
#403274,#403275,#403276),.UNSPECIFIED.,.F.,.F.,(4,3,4),(0.,6.98630244191488E-5,
0.000113969974038089),.UNSPECIFIED.);
#25668=B_SPLINE_CURVE_WITH_KNOTS('',3,(#403279,#403280,#403281,#403282,
#403283,#403284,#403285,#403286,#403287,#403288,#403289,#403290,#403291,
#403292,#403293,#403294,#403295,#403296,#403297,#403298,#403299,#403300,
#403301,#403302,#403303,#403304,#403305,#403306,#403307,#403308,#403309,
#403310,#403311,#403312,#403313,#403314,#403315,#403316,#403317,#403318,
#403319,#403320,#403321,#403322,#403323,#403324,#403325,#403326,#403327),
 .UNSPECIFIED.,.F.,.F.,(4,3,3,3,3,3,3,3,3,3,3,3,3,3,3,3,4),(0.,1.53100299373415E-6,
4.52554775679494E-6,7.01151246291608E-6,9.26752933799504E-6,1.03084066197173E-5,
1.17138990826863E-5,1.22284894984074E-5,1.30315035324818E-5,1.38363728497813E-5,
1.40464197777495E-5,1.5459774956464E-5,1.62073588704069E-5,1.92092968712925E-5,
1.95234416882555E-5,2.37637844577608E-5,2.61487188977261E-5),
 .UNSPECIFIED.);
#25669=B_SPLINE_CURVE_WITH_KNOTS('',3,(#403342,#403343,#403344,#403345,
#403346,#403347,#403348,#403349,#403350,#403351,#403352,#403353,#403354,
#403355,#403356,#403357,#403358,#403359,#403360,#403361,#403362,#403363,
#403364,#403365,#403366,#403367,#403368,#403369,#403370,#403371,#403372),
 .UNSPECIFIED.,.F.,.F.,(4,3,3,3,3,3,3,3,3,3,4),(0.,3.95507910398488E-6,
7.53768426604197E-6,1.19904533335349E-5,1.40475043392583E-5,1.51452104275962E-5,
1.67866272814071E-5,1.69621513005355E-5,1.81338315460707E-5,1.98906334656513E-5,
2.06132424588239E-5),.UNSPECIFIED.);
#25670=B_SPLINE_CURVE_WITH_KNOTS('',3,(#403375,#403376,#403377,#403378),
 .UNSPECIFIED.,.F.,.F.,(4,4),(4.47028007668187E-19,0.00010938435327491),
 .UNSPECIFIED.);
#25671=B_SPLINE_CURVE_WITH_KNOTS('',3,(#403405,#403406,#403407,#403408,
#403409,#403410,#403411,#403412,#403413,#403414,#403415,#403416,#403417,
#403418,#403419,#403420,#403421,#403422,#403423,#403424,#403425,#403426,
#403427,#403428,#403429,#403430,#403431,#403432,#403433,#403434,#403435,
#403436,#403437,#403438),.UNSPECIFIED.,.F.,.F.,(4,3,3,3,3,3,3,3,3,3,3,4),
(1.0842021724855E-19,2.09623992729452E-6,3.17176647120229E-6,4.82636181942986E-6,
5.01000917339994E-6,6.13126454147503E-6,8.60486650288877E-6,9.21144281170519E-6,
1.24722301135898E-5,1.4266645478786E-5,2.04670653756804E-5,2.08026438176811E-5),
 .UNSPECIFIED.);
#25672=B_SPLINE_CURVE_WITH_KNOTS('',3,(#403439,#403440,#403441,#403442),
 .UNSPECIFIED.,.F.,.F.,(4,4),(0.,0.000109384345496908),.UNSPECIFIED.);
#25673=B_SPLINE_CURVE_WITH_KNOTS('',3,(#403547,#403548,#403549,#403550),
 .UNSPECIFIED.,.F.,.F.,(4,4),(0.,9.54361881492177E-5),.UNSPECIFIED.);
#25674=B_SPLINE_CURVE_WITH_KNOTS('',3,(#403555,#403556,#403557,#403558,
#403559,#403560,#403561),.UNSPECIFIED.,.F.,.F.,(4,3,4),(0.,4.4106970432347E-5,
0.000113970027818834),.UNSPECIFIED.);
#25675=B_SPLINE_CURVE_WITH_KNOTS('',3,(#403567,#403568,#403569,#403570),
 .UNSPECIFIED.,.F.,.F.,(4,4),(4.37055868292169E-19,9.54361881492178E-5),
 .UNSPECIFIED.);
#25676=B_SPLINE_CURVE_WITH_KNOTS('',3,(#403574,#403575,#403576,#403577,
#403578,#403579,#403580),.UNSPECIFIED.,.F.,.F.,(4,3,4),(0.,6.98630244191491E-5,
0.000113969974038089),.UNSPECIFIED.);
#25677=B_SPLINE_CURVE_WITH_KNOTS('',3,(#403583,#403584,#403585,#403586,
#403587,#403588,#403589,#403590,#403591,#403592,#403593,#403594,#403595,
#403596,#403597,#403598,#403599,#403600,#403601,#403602,#403603,#403604,
#403605,#403606,#403607,#403608,#403609,#403610,#403611,#403612,#403613,
#403614,#403615,#403616,#403617,#403618,#403619,#403620,#403621,#403622,
#403623,#403624,#403625,#403626,#403627,#403628,#403629,#403630,#403631),
 .UNSPECIFIED.,.F.,.F.,(4,3,3,3,3,3,3,3,3,3,3,3,3,3,3,3,4),(0.,1.53100299373428E-6,
4.52554775678673E-6,7.01151246291611E-6,9.2675293380117E-6,1.03084066197174E-5,
1.17138990826861E-5,1.22284894984074E-5,1.30315035324817E-5,1.38363728497813E-5,
1.40464197777495E-5,1.54597749564639E-5,1.62073588704068E-5,1.92092968713227E-5,
1.95234416882553E-5,2.37637844577601E-5,2.61487188977258E-5),
 .UNSPECIFIED.);
#25678=B_SPLINE_CURVE_WITH_KNOTS('',3,(#403646,#403647,#403648,#403649,
#403650,#403651,#403652,#403653,#403654,#403655,#403656,#403657,#403658,
#403659,#403660,#403661,#403662,#403663,#403664,#403665,#403666,#403667,
#403668,#403669,#403670,#403671,#403672,#403673,#403674,#403675,#403676),
 .UNSPECIFIED.,.F.,.F.,(4,3,3,3,3,3,3,3,3,3,4),(0.,3.95507910397771E-6,
7.53768426604201E-6,1.1990453333535E-5,1.40475043392585E-5,1.51452104275964E-5,
1.67866272814242E-5,1.69621513005359E-5,1.81338315460713E-5,1.98906334656549E-5,
2.06132424588246E-5),.UNSPECIFIED.);
#25679=B_SPLINE_CURVE_WITH_KNOTS('',3,(#403679,#403680,#403681,#403682),
 .UNSPECIFIED.,.F.,.F.,(4,4),(4.47028007668187E-19,0.00010938435327491),
 .UNSPECIFIED.);
#25680=B_SPLINE_CURVE_WITH_KNOTS('',3,(#403709,#403710,#403711,#403712,
#403713,#403714,#403715,#403716,#403717,#403718,#403719,#403720,#403721,
#403722,#403723,#403724,#403725,#403726,#403727,#403728,#403729,#403730,
#403731,#403732,#403733,#403734,#403735,#403736,#403737,#403738,#403739,
#403740,#403741,#403742),.UNSPECIFIED.,.F.,.F.,(4,3,3,3,3,3,3,3,3,3,3,4),
(3.25260651745651E-19,2.09623992729428E-6,3.17176647120214E-6,4.82636181944364E-6,
5.01000917339949E-6,6.13126454147488E-6,8.60486650288841E-6,9.21144281170483E-6,
1.24722301135897E-5,1.42666454787855E-5,2.04670653756992E-5,2.08026438176802E-5),
 .UNSPECIFIED.);
#25681=B_SPLINE_CURVE_WITH_KNOTS('',3,(#403743,#403744,#403745,#403746),
 .UNSPECIFIED.,.F.,.F.,(4,4),(0.,0.000109384345496908),.UNSPECIFIED.);
#25682=B_SPLINE_CURVE_WITH_KNOTS('',3,(#403851,#403852,#403853,#403854),
 .UNSPECIFIED.,.F.,.F.,(4,4),(0.,9.54361881492177E-5),.UNSPECIFIED.);
#25683=B_SPLINE_CURVE_WITH_KNOTS('',3,(#403859,#403860,#403861,#403862,
#403863,#403864,#403865),.UNSPECIFIED.,.F.,.F.,(4,3,4),(0.,4.4106970432347E-5,
0.000113970027818834),.UNSPECIFIED.);
#25684=B_SPLINE_CURVE_WITH_KNOTS('',3,(#403871,#403872,#403873,#403874),
 .UNSPECIFIED.,.F.,.F.,(4,4),(4.47028007668187E-19,9.54361881492176E-5),
 .UNSPECIFIED.);
#25685=B_SPLINE_CURVE_WITH_KNOTS('',3,(#403878,#403879,#403880,#403881,
#403882,#403883,#403884),.UNSPECIFIED.,.F.,.F.,(4,3,4),(0.,6.98630244191491E-5,
0.000113969974038089),.UNSPECIFIED.);
#25686=B_SPLINE_CURVE_WITH_KNOTS('',3,(#403887,#403888,#403889,#403890,
#403891,#403892,#403893,#403894,#403895,#403896,#403897,#403898,#403899,
#403900,#403901,#403902,#403903,#403904,#403905,#403906,#403907,#403908,
#403909,#403910,#403911,#403912,#403913,#403914,#403915,#403916,#403917,
#403918,#403919,#403920,#403921,#403922,#403923,#403924,#403925,#403926,
#403927,#403928,#403929,#403930,#403931,#403932,#403933,#403934,#403935),
 .UNSPECIFIED.,.F.,.F.,(4,3,3,3,3,3,3,3,3,3,3,3,3,3,3,3,4),(0.,1.53100299373417E-6,
4.52554775678891E-6,7.01151246291613E-6,9.26752933800967E-6,1.03084066197174E-5,
1.17138990826861E-5,1.22284894984074E-5,1.30315035324817E-5,1.38363728497813E-5,
1.40464197777495E-5,1.54597749564641E-5,1.6207358870407E-5,1.92092968712626E-5,
1.95234416882557E-5,2.37637844577605E-5,2.61487188977263E-5),
 .UNSPECIFIED.);
#25687=B_SPLINE_CURVE_WITH_KNOTS('',3,(#403950,#403951,#403952,#403953,
#403954,#403955,#403956,#403957,#403958,#403959,#403960,#403961,#403962,
#403963,#403964,#403965,#403966,#403967,#403968,#403969,#403970,#403971,
#403972,#403973,#403974,#403975,#403976,#403977,#403978,#403979,#403980),
 .UNSPECIFIED.,.F.,.F.,(4,3,3,3,3,3,3,3,3,3,4),(0.,3.95507910397136E-6,
7.53768426604194E-6,1.1990453333535E-5,1.40475043392585E-5,1.51452104275964E-5,
1.67866272814088E-5,1.69621513005357E-5,1.81338315460711E-5,1.98906334656549E-5,
2.06132424588245E-5),.UNSPECIFIED.);
#25688=B_SPLINE_CURVE_WITH_KNOTS('',3,(#403983,#403984,#403985,#403986),
 .UNSPECIFIED.,.F.,.F.,(4,4),(4.63171371119878E-19,0.00010938435327491),
 .UNSPECIFIED.);
#25689=B_SPLINE_CURVE_WITH_KNOTS('',3,(#404013,#404014,#404015,#404016,
#404017,#404018,#404019,#404020,#404021,#404022,#404023,#404024,#404025,
#404026,#404027,#404028,#404029,#404030,#404031,#404032,#404033,#404034,
#404035,#404036,#404037,#404038,#404039,#404040,#404041,#404042,#404043,
#404044,#404045,#404046),.UNSPECIFIED.,.F.,.F.,(4,3,3,3,3,3,3,3,3,3,3,4),
(1.0842021724855E-19,2.09623992729439E-6,3.17176647120223E-6,4.82636181943523E-6,
5.01000917339971E-6,6.13126454147506E-6,8.60486650288868E-6,9.21144281170512E-6,
1.24722301135849E-5,1.42666454787859E-5,2.04670653756996E-5,2.08026438176807E-5),
 .UNSPECIFIED.);
#25690=B_SPLINE_CURVE_WITH_KNOTS('',3,(#404047,#404048,#404049,#404050),
 .UNSPECIFIED.,.F.,.F.,(4,4),(0.,0.000109384345496908),.UNSPECIFIED.);
#25691=B_SPLINE_CURVE_WITH_KNOTS('',3,(#404155,#404156,#404157,#404158),
 .UNSPECIFIED.,.F.,.F.,(4,4),(0.,9.54361881492175E-5),.UNSPECIFIED.);
#25692=B_SPLINE_CURVE_WITH_KNOTS('',3,(#404163,#404164,#404165,#404166,
#404167,#404168,#404169),.UNSPECIFIED.,.F.,.F.,(4,3,4),(0.,4.41069704323469E-5,
0.000113970027818833),.UNSPECIFIED.);
#25693=B_SPLINE_CURVE_WITH_KNOTS('',3,(#404175,#404176,#404177,#404178),
 .UNSPECIFIED.,.F.,.F.,(4,4),(4.47028007668187E-19,9.54361881492176E-5),
 .UNSPECIFIED.);
#25694=B_SPLINE_CURVE_WITH_KNOTS('',3,(#404182,#404183,#404184,#404185,
#404186,#404187,#404188),.UNSPECIFIED.,.F.,.F.,(4,3,4),(0.,6.98630244191494E-5,
0.000113969974038089),.UNSPECIFIED.);
#25695=B_SPLINE_CURVE_WITH_KNOTS('',3,(#404191,#404192,#404193,#404194,
#404195,#404196,#404197,#404198,#404199,#404200,#404201,#404202,#404203,
#404204,#404205,#404206,#404207,#404208,#404209,#404210,#404211,#404212,
#404213,#404214,#404215,#404216,#404217,#404218,#404219,#404220,#404221,
#404222,#404223,#404224,#404225,#404226,#404227,#404228,#404229,#404230,
#404231,#404232,#404233,#404234,#404235,#404236,#404237,#404238,#404239),
 .UNSPECIFIED.,.F.,.F.,(4,3,3,3,3,3,3,3,3,3,3,3,3,3,3,3,4),(0.,1.53100299373404E-6,
4.52554775679048E-6,7.01151246291601E-6,9.26752933800589E-6,1.03084066197173E-5,
1.17138990826862E-5,1.22284894984074E-5,1.30315035324817E-5,1.38363728497813E-5,
1.40464197777495E-5,1.5459774956464E-5,1.62073588704068E-5,1.92092968712522E-5,
1.95234416882554E-5,2.37637844577637E-5,2.61487188977262E-5),
 .UNSPECIFIED.);
#25696=B_SPLINE_CURVE_WITH_KNOTS('',3,(#404254,#404255,#404256,#404257,
#404258,#404259,#404260,#404261,#404262,#404263,#404264,#404265,#404266,
#404267,#404268,#404269,#404270,#404271,#404272,#404273,#404274,#404275,
#404276,#404277,#404278,#404279,#404280,#404281,#404282,#404283,#404284),
 .UNSPECIFIED.,.F.,.F.,(4,3,3,3,3,3,3,3,3,3,4),(0.,3.95507910397345E-6,
7.53768426604206E-6,1.19904533335351E-5,1.40475043392586E-5,1.51452104275965E-5,
1.67866272814209E-5,1.69621513005358E-5,1.81338315460712E-5,1.98906334656557E-5,
2.06132424588245E-5),.UNSPECIFIED.);
#25697=B_SPLINE_CURVE_WITH_KNOTS('',3,(#404287,#404288,#404289,#404290),
 .UNSPECIFIED.,.F.,.F.,(4,4),(4.73369422993816E-19,0.00010938435327491),
 .UNSPECIFIED.);
#25698=B_SPLINE_CURVE_WITH_KNOTS('',3,(#404317,#404318,#404319,#404320,
#404321,#404322,#404323,#404324,#404325,#404326,#404327,#404328,#404329,
#404330,#404331,#404332,#404333,#404334,#404335,#404336,#404337,#404338,
#404339,#404340,#404341,#404342,#404343,#404344,#404345,#404346,#404347,
#404348,#404349,#404350),.UNSPECIFIED.,.F.,.F.,(4,3,3,3,3,3,3,3,3,3,3,4),
(1.35525271560688E-19,2.09623992729445E-6,3.17176647120224E-6,4.82636181943226E-6,
5.01000917339961E-6,6.13126454147493E-6,8.6048665028883E-6,9.21144281170468E-6,
1.24722301135904E-5,1.42666454787847E-5,2.04670653757035E-5,2.08026438176787E-5),
 .UNSPECIFIED.);
#25699=B_SPLINE_CURVE_WITH_KNOTS('',3,(#404351,#404352,#404353,#404354),
 .UNSPECIFIED.,.F.,.F.,(4,4),(0.,0.000109384345496908),.UNSPECIFIED.);
#25700=B_SPLINE_CURVE_WITH_KNOTS('',3,(#404459,#404460,#404461,#404462),
 .UNSPECIFIED.,.F.,.F.,(4,4),(0.,9.54361881492174E-5),.UNSPECIFIED.);
#25701=B_SPLINE_CURVE_WITH_KNOTS('',3,(#404467,#404468,#404469,#404470,
#404471,#404472,#404473),.UNSPECIFIED.,.F.,.F.,(4,3,4),(0.,4.41069704323469E-5,
0.000113970027818833),.UNSPECIFIED.);
#25702=B_SPLINE_CURVE_WITH_KNOTS('',3,(#404479,#404480,#404481,#404482),
 .UNSPECIFIED.,.F.,.F.,(4,4),(4.52388553334502E-19,9.54361881492177E-5),
 .UNSPECIFIED.);
#25703=B_SPLINE_CURVE_WITH_KNOTS('',3,(#404486,#404487,#404488,#404489,
#404490,#404491,#404492),.UNSPECIFIED.,.F.,.F.,(4,3,4),(8.470329472543E-22,
6.9863024419149E-5,0.000113969974038089),.UNSPECIFIED.);
#25704=B_SPLINE_CURVE_WITH_KNOTS('',3,(#404495,#404496,#404497,#404498,
#404499,#404500,#404501,#404502,#404503,#404504,#404505,#404506,#404507,
#404508,#404509,#404510,#404511,#404512,#404513,#404514,#404515,#404516,
#404517,#404518,#404519,#404520,#404521,#404522,#404523,#404524,#404525,
#404526,#404527,#404528,#404529,#404530,#404531,#404532,#404533,#404534,
#404535,#404536,#404537,#404538,#404539,#404540,#404541,#404542,#404543),
 .UNSPECIFIED.,.F.,.F.,(4,3,3,3,3,3,3,3,3,3,3,3,3,3,3,3,4),(0.,1.53100299373414E-6,
4.52554775678511E-6,7.01151246291606E-6,9.267529338009E-6,1.03084066197173E-5,
1.17138990826862E-5,1.22284894984074E-5,1.30315035324817E-5,1.38363728497813E-5,
1.40464197777495E-5,1.5459774956464E-5,1.62073588704069E-5,1.92092968712803E-5,
1.95234416882555E-5,2.37637844577586E-5,2.61487188977262E-5),
 .UNSPECIFIED.);
#25705=B_SPLINE_CURVE_WITH_KNOTS('',3,(#404558,#404559,#404560,#404561,
#404562,#404563,#404564,#404565,#404566,#404567,#404568,#404569,#404570,
#404571,#404572,#404573,#404574,#404575,#404576,#404577,#404578,#404579,
#404580,#404581,#404582,#404583,#404584,#404585,#404586,#404587,#404588),
 .UNSPECIFIED.,.F.,.F.,(4,3,3,3,3,3,3,3,3,3,4),(0.,3.9550791039786E-6,7.53768426604197E-6,
1.1990453333535E-5,1.40475043392586E-5,1.51452104275964E-5,1.67866272814111E-5,
1.69621513005358E-5,1.81338315460712E-5,1.98906334656562E-5,2.06132424588244E-5),
 .UNSPECIFIED.);
#25706=B_SPLINE_CURVE_WITH_KNOTS('',3,(#404591,#404592,#404593,#404594),
 .UNSPECIFIED.,.F.,.F.,(4,4),(4.78962492688793E-19,0.00010938435327491),
 .UNSPECIFIED.);
#25707=B_SPLINE_CURVE_WITH_KNOTS('',3,(#404621,#404622,#404623,#404624,
#404625,#404626,#404627,#404628,#404629,#404630,#404631,#404632,#404633,
#404634,#404635,#404636,#404637,#404638,#404639,#404640,#404641,#404642,
#404643,#404644,#404645,#404646,#404647,#404648,#404649,#404650,#404651,
#404652,#404653,#404654),.UNSPECIFIED.,.F.,.F.,(4,3,3,3,3,3,3,3,3,3,3,4),
(1.35525271560688E-19,2.0962399272944E-6,3.17176647120221E-6,4.82636181943873E-6,
5.01000917339963E-6,6.13126454147497E-6,8.6048665028886E-6,9.21144281170497E-6,
1.24722301136065E-5,1.42666454787857E-5,2.04670653756822E-5,2.08026438176805E-5),
 .UNSPECIFIED.);
#25708=B_SPLINE_CURVE_WITH_KNOTS('',3,(#404655,#404656,#404657,#404658),
 .UNSPECIFIED.,.F.,.F.,(4,4),(0.,0.000109384345496908),.UNSPECIFIED.);
#25709=B_SPLINE_CURVE_WITH_KNOTS('',3,(#404763,#404764,#404765,#404766),
 .UNSPECIFIED.,.F.,.F.,(4,4),(0.,9.54361881492175E-5),.UNSPECIFIED.);
#25710=B_SPLINE_CURVE_WITH_KNOTS('',3,(#404771,#404772,#404773,#404774,
#404775,#404776,#404777),.UNSPECIFIED.,.F.,.F.,(4,3,4),(0.,4.41069704323468E-5,
0.000113970027818834),.UNSPECIFIED.);
#25711=B_SPLINE_CURVE_WITH_KNOTS('',3,(#404783,#404784,#404785,#404786),
 .UNSPECIFIED.,.F.,.F.,(4,4),(4.5436350575631E-19,9.54361881492176E-5),
 .UNSPECIFIED.);
#25712=B_SPLINE_CURVE_WITH_KNOTS('',3,(#404790,#404791,#404792,#404793,
#404794,#404795,#404796),.UNSPECIFIED.,.F.,.F.,(4,3,4),(0.,6.9863024419149E-5,
0.000113969974038089),.UNSPECIFIED.);
#25713=B_SPLINE_CURVE_WITH_KNOTS('',3,(#404799,#404800,#404801,#404802,
#404803,#404804,#404805,#404806,#404807,#404808,#404809,#404810,#404811,
#404812,#404813,#404814,#404815,#404816,#404817,#404818,#404819,#404820,
#404821,#404822,#404823,#404824,#404825,#404826,#404827,#404828,#404829,
#404830,#404831,#404832,#404833,#404834,#404835,#404836,#404837,#404838,
#404839,#404840,#404841,#404842,#404843,#404844,#404845,#404846,#404847),
 .UNSPECIFIED.,.F.,.F.,(4,3,3,3,3,3,3,3,3,3,3,3,3,3,3,3,4),(0.,1.53100299373415E-6,
4.52554775679134E-6,7.01151246291607E-6,9.26752933800752E-6,1.03084066197173E-5,
1.17138990826861E-5,1.22284894984074E-5,1.30315035324817E-5,1.38363728497812E-5,
1.40464197777495E-5,1.5459774956464E-5,1.62073588704068E-5,1.92092968713003E-5,
1.95234416882555E-5,2.37637844577607E-5,2.61487188977258E-5),
 .UNSPECIFIED.);
#25714=B_SPLINE_CURVE_WITH_KNOTS('',3,(#404862,#404863,#404864,#404865,
#404866,#404867,#404868,#404869,#404870,#404871,#404872,#404873,#404874,
#404875,#404876,#404877,#404878,#404879,#404880,#404881,#404882,#404883,
#404884,#404885,#404886,#404887,#404888,#404889,#404890,#404891,#404892),
 .UNSPECIFIED.,.F.,.F.,(4,3,3,3,3,3,3,3,3,3,4),(0.,3.95507910399298E-6,
7.53768426604202E-6,1.19904533335351E-5,1.40475043392586E-5,1.51452104275965E-5,
1.67866272814125E-5,1.69621513005359E-5,1.81338315460713E-5,1.9890633465649E-5,
2.06132424588247E-5),.UNSPECIFIED.);
#25715=B_SPLINE_CURVE_WITH_KNOTS('',3,(#404895,#404896,#404897,#404898),
 .UNSPECIFIED.,.F.,.F.,(4,4),(4.84869951806108E-19,0.00010938435327491),
 .UNSPECIFIED.);
#25716=B_SPLINE_CURVE_WITH_KNOTS('',3,(#404925,#404926,#404927,#404928,
#404929,#404930,#404931,#404932,#404933,#404934,#404935,#404936,#404937,
#404938,#404939,#404940,#404941,#404942,#404943,#404944,#404945,#404946,
#404947,#404948,#404949,#404950,#404951,#404952,#404953,#404954,#404955,
#404956,#404957,#404958),.UNSPECIFIED.,.F.,.F.,(4,3,3,3,3,3,3,3,3,3,3,4),
(1.35525271560688E-19,2.09623992729443E-6,3.17176647120225E-6,4.8263618194329E-6,
5.01000917339965E-6,6.13126454147501E-6,8.60486650288862E-6,9.21144281170501E-6,
1.24722301135748E-5,1.42666454787858E-5,2.04670653757036E-5,2.08026438176807E-5),
 .UNSPECIFIED.);
#25717=B_SPLINE_CURVE_WITH_KNOTS('',3,(#404959,#404960,#404961,#404962),
 .UNSPECIFIED.,.F.,.F.,(4,4),(0.,0.000109384345496908),.UNSPECIFIED.);
#25718=B_SPLINE_CURVE_WITH_KNOTS('',3,(#405067,#405068,#405069,#405070),
 .UNSPECIFIED.,.F.,.F.,(4,4),(0.,9.54361881492173E-5),.UNSPECIFIED.);
#25719=B_SPLINE_CURVE_WITH_KNOTS('',3,(#405075,#405076,#405077,#405078,
#405079,#405080,#405081),.UNSPECIFIED.,.F.,.F.,(4,3,4),(0.,4.41069704323472E-5,
0.000113970027818833),.UNSPECIFIED.);
#25720=B_SPLINE_CURVE_WITH_KNOTS('',3,(#405087,#405088,#405089,#405090),
 .UNSPECIFIED.,.F.,.F.,(4,4),(4.63171371119878E-19,9.54361881492176E-5),
 .UNSPECIFIED.);
#25721=B_SPLINE_CURVE_WITH_KNOTS('',3,(#405094,#405095,#405096,#405097,
#405098,#405099,#405100),.UNSPECIFIED.,.F.,.F.,(4,3,4),(0.,6.98630244191491E-5,
0.000113969974038089),.UNSPECIFIED.);
#25722=B_SPLINE_CURVE_WITH_KNOTS('',3,(#405103,#405104,#405105,#405106,
#405107,#405108,#405109,#405110,#405111,#405112,#405113,#405114,#405115,
#405116,#405117,#405118,#405119,#405120,#405121,#405122,#405123,#405124,
#405125,#405126,#405127,#405128,#405129,#405130,#405131,#405132,#405133,
#405134,#405135,#405136,#405137,#405138,#405139,#405140,#405141,#405142,
#405143,#405144,#405145,#405146,#405147,#405148,#405149,#405150,#405151),
 .UNSPECIFIED.,.F.,.F.,(4,3,3,3,3,3,3,3,3,3,3,3,3,3,3,3,4),(0.,1.53100299373408E-6,
4.52554775679546E-6,7.01151246291603E-6,9.26752933800014E-6,1.03084066197173E-5,
1.17138990826862E-5,1.22284894984074E-5,1.30315035324817E-5,1.38363728497812E-5,
1.40464197777494E-5,1.54597749564638E-5,1.62073588704067E-5,1.92092968712711E-5,
1.95234416882554E-5,2.37637844577557E-5,2.6148718897726E-5),
 .UNSPECIFIED.);
#25723=B_SPLINE_CURVE_WITH_KNOTS('',3,(#405166,#405167,#405168,#405169,
#405170,#405171,#405172,#405173,#405174,#405175,#405176,#405177,#405178,
#405179,#405180,#405181,#405182,#405183,#405184,#405185,#405186,#405187,
#405188,#405189,#405190,#405191,#405192,#405193,#405194,#405195,#405196),
 .UNSPECIFIED.,.F.,.F.,(4,3,3,3,3,3,3,3,3,3,4),(0.,3.95507910396783E-6,
7.53768426604193E-6,1.19904533335351E-5,1.40475043392585E-5,1.51452104275963E-5,
1.67866272814202E-5,1.69621513005356E-5,1.8133831546071E-5,1.98906334656567E-5,
2.06132424588241E-5),.UNSPECIFIED.);
#25724=B_SPLINE_CURVE_WITH_KNOTS('',3,(#405199,#405200,#405201,#405202),
 .UNSPECIFIED.,.F.,.F.,(4,4),(1.62630325872826E-19,0.00010938435327491),
 .UNSPECIFIED.);
#25725=B_SPLINE_CURVE_WITH_KNOTS('',3,(#405229,#405230,#405231,#405232,
#405233,#405234,#405235,#405236,#405237,#405238,#405239,#405240,#405241,
#405242,#405243,#405244,#405245,#405246,#405247,#405248,#405249,#405250,
#405251,#405252,#405253,#405254,#405255,#405256,#405257,#405258,#405259,
#405260,#405261,#405262),.UNSPECIFIED.,.F.,.F.,(4,3,3,3,3,3,3,3,3,3,3,4),
(5.42101086242752E-20,2.09623992729448E-6,3.17176647120223E-6,4.82636181942703E-6,
5.0100091733996E-6,6.13126454147494E-6,8.60486650288851E-6,9.21144281170486E-6,
1.24722301136045E-5,1.42666454787856E-5,2.04670653757033E-5,2.08026438176802E-5),
 .UNSPECIFIED.);
#25726=B_SPLINE_CURVE_WITH_KNOTS('',3,(#405263,#405264,#405265,#405266),
 .UNSPECIFIED.,.F.,.F.,(4,4),(0.,0.000109384345496908),.UNSPECIFIED.);
#25727=B_SPLINE_CURVE_WITH_KNOTS('',3,(#405371,#405372,#405373,#405374),
 .UNSPECIFIED.,.F.,.F.,(4,4),(0.,9.54361881492172E-5),.UNSPECIFIED.);
#25728=B_SPLINE_CURVE_WITH_KNOTS('',3,(#405379,#405380,#405381,#405382,
#405383,#405384,#405385),.UNSPECIFIED.,.F.,.F.,(4,3,4),(0.,4.41069704323469E-5,
0.000113970027818833),.UNSPECIFIED.);
#25729=B_SPLINE_CURVE_WITH_KNOTS('',3,(#405391,#405392,#405393,#405394),
 .UNSPECIFIED.,.F.,.F.,(4,4),(4.84869951806108E-19,9.54361881492178E-5),
 .UNSPECIFIED.);
#25730=B_SPLINE_CURVE_WITH_KNOTS('',3,(#405398,#405399,#405400,#405401,
#405402,#405403,#405404),.UNSPECIFIED.,.F.,.F.,(4,3,4),(0.,6.9863024419149E-5,
0.000113969974038089),.UNSPECIFIED.);
#25731=B_SPLINE_CURVE_WITH_KNOTS('',3,(#405407,#405408,#405409,#405410,
#405411,#405412,#405413,#405414,#405415,#405416,#405417,#405418,#405419,
#405420,#405421,#405422,#405423,#405424,#405425,#405426,#405427,#405428,
#405429,#405430,#405431,#405432,#405433,#405434,#405435,#405436,#405437,
#405438,#405439,#405440,#405441,#405442,#405443,#405444,#405445,#405446,
#405447,#405448,#405449,#405450,#405451,#405452,#405453,#405454,#405455),
 .UNSPECIFIED.,.F.,.F.,(4,3,3,3,3,3,3,3,3,3,3,3,3,3,3,3,4),(0.,1.53100299373416E-6,
4.52554775679585E-6,7.01151246291608E-6,9.26752933800778E-6,1.03084066197173E-5,
1.17138990826861E-5,1.22284894984073E-5,1.30315035324816E-5,1.38363728497814E-5,
1.40464197777495E-5,1.54597749564641E-5,1.62073588704069E-5,1.9209296871241E-5,
1.95234416882557E-5,2.37637844577615E-5,2.61487188977267E-5),
 .UNSPECIFIED.);
#25732=B_SPLINE_CURVE_WITH_KNOTS('',3,(#405470,#405471,#405472,#405473,
#405474,#405475,#405476,#405477,#405478,#405479,#405480,#405481,#405482,
#405483,#405484,#405485,#405486,#405487,#405488,#405489,#405490,#405491,
#405492,#405493,#405494,#405495,#405496,#405497,#405498,#405499,#405500),
 .UNSPECIFIED.,.F.,.F.,(4,3,3,3,3,3,3,3,3,3,4),(0.,3.95507910397426E-6,
7.53768426604206E-6,1.19904533335352E-5,1.40475043392587E-5,1.51452104275966E-5,
1.67866272814278E-5,1.6962151300536E-5,1.81338315460714E-5,1.98906334656544E-5,
2.06132424588248E-5),.UNSPECIFIED.);
#25733=B_SPLINE_CURVE_WITH_KNOTS('',3,(#405503,#405504,#405505,#405506),
 .UNSPECIFIED.,.F.,.F.,(4,4),(5.42101086242752E-19,0.00010938435327491),
 .UNSPECIFIED.);
#25734=B_SPLINE_CURVE_WITH_KNOTS('',3,(#405533,#405534,#405535,#405536,
#405537,#405538,#405539,#405540,#405541,#405542,#405543,#405544,#405545,
#405546,#405547,#405548,#405549,#405550,#405551,#405552,#405553,#405554,
#405555,#405556,#405557,#405558,#405559,#405560,#405561,#405562,#405563,
#405564,#405565,#405566),.UNSPECIFIED.,.F.,.F.,(4,3,3,3,3,3,3,3,3,3,3,4),
(1.0842021724855E-19,2.09623992729449E-6,3.17176647120226E-6,4.82636181944126E-6,
5.0100091733997E-6,6.13126454147493E-6,8.6048665028884E-6,9.21144281170475E-6,
1.24722301135929E-5,1.42666454787848E-5,2.04670653756726E-5,2.08026438176789E-5),
 .UNSPECIFIED.);
#25735=B_SPLINE_CURVE_WITH_KNOTS('',3,(#405567,#405568,#405569,#405570),
 .UNSPECIFIED.,.F.,.F.,(4,4),(0.,0.000109384345496908),.UNSPECIFIED.);
#25736=B_SPLINE_CURVE_WITH_KNOTS('',3,(#405675,#405676,#405677,#405678),
 .UNSPECIFIED.,.F.,.F.,(4,4),(0.,9.54361881492173E-5),.UNSPECIFIED.);
#25737=B_SPLINE_CURVE_WITH_KNOTS('',3,(#405683,#405684,#405685,#405686,
#405687,#405688,#405689),.UNSPECIFIED.,.F.,.F.,(4,3,4),(0.,4.41069704323467E-5,
0.000113970027818833),.UNSPECIFIED.);
#25738=B_SPLINE_CURVE_WITH_KNOTS('',3,(#405695,#405696,#405697,#405698),
 .UNSPECIFIED.,.F.,.F.,(4,4),(2.16840434497101E-19,9.54361881492178E-5),
 .UNSPECIFIED.);
#25739=B_SPLINE_CURVE_WITH_KNOTS('',3,(#405702,#405703,#405704,#405705,
#405706,#405707,#405708),.UNSPECIFIED.,.F.,.F.,(4,3,4),(0.,6.98630244191491E-5,
0.000113969974038089),.UNSPECIFIED.);
#25740=B_SPLINE_CURVE_WITH_KNOTS('',3,(#405711,#405712,#405713,#405714,
#405715,#405716,#405717,#405718,#405719,#405720,#405721,#405722,#405723,
#405724,#405725,#405726,#405727,#405728,#405729,#405730,#405731,#405732,
#405733,#405734,#405735,#405736,#405737,#405738,#405739,#405740,#405741,
#405742,#405743,#405744,#405745,#405746,#405747,#405748,#405749,#405750,
#405751,#405752,#405753,#405754,#405755,#405756,#405757,#405758,#405759),
 .UNSPECIFIED.,.F.,.F.,(4,3,3,3,3,3,3,3,3,3,3,3,3,3,3,3,4),(0.,1.53100299373419E-6,
4.52554775679209E-6,7.01151246291602E-6,9.26752933799641E-6,1.03084066197174E-5,
1.17138990826862E-5,1.22284894984075E-5,1.30315035324818E-5,1.38363728497813E-5,
1.40464197777496E-5,1.5459774956464E-5,1.62073588704068E-5,1.92092968712732E-5,
1.95234416882555E-5,2.3763784457757E-5,2.6148718897726E-5),
 .UNSPECIFIED.);
#25741=B_SPLINE_CURVE_WITH_KNOTS('',3,(#405774,#405775,#405776,#405777,
#405778,#405779,#405780,#405781,#405782,#405783,#405784,#405785,#405786,
#405787,#405788,#405789,#405790,#405791,#405792,#405793,#405794,#405795,
#405796,#405797,#405798,#405799,#405800,#405801,#405802,#405803,#405804),
 .UNSPECIFIED.,.F.,.F.,(4,3,3,3,3,3,3,3,3,3,4),(0.,3.95507910397029E-6,
7.53768426604194E-6,1.1990453333535E-5,1.40475043392585E-5,1.51452104275964E-5,
1.67866272814301E-5,1.69621513005357E-5,1.81338315460711E-5,1.98906334656535E-5,
2.06132424588243E-5),.UNSPECIFIED.);
#25742=B_SPLINE_CURVE_WITH_KNOTS('',3,(#405807,#405808,#405809,#405810),
 .UNSPECIFIED.,.F.,.F.,(4,4),(5.42101086242752E-19,0.00010938435327491),
 .UNSPECIFIED.);
#25743=B_SPLINE_CURVE_WITH_KNOTS('',3,(#405837,#405838,#405839,#405840,
#405841,#405842,#405843,#405844,#405845,#405846,#405847,#405848,#405849,
#405850,#405851,#405852,#405853,#405854,#405855,#405856,#405857,#405858,
#405859,#405860,#405861,#405862,#405863,#405864,#405865,#405866,#405867,
#405868,#405869,#405870),.UNSPECIFIED.,.F.,.F.,(4,3,3,3,3,3,3,3,3,3,3,4),
(1.0842021724855E-19,2.09623992729457E-6,3.17176647120225E-6,4.82636181943907E-6,
5.0100091733998E-6,6.13126454147517E-6,8.60486650288879E-6,9.21144281170528E-6,
1.24722301136079E-5,1.42666454787861E-5,2.04670653756915E-5,2.08026438176811E-5),
 .UNSPECIFIED.);
#25744=B_SPLINE_CURVE_WITH_KNOTS('',3,(#405871,#405872,#405873,#405874),
 .UNSPECIFIED.,.F.,.F.,(4,4),(0.,0.000109384345496908),.UNSPECIFIED.);
#25745=B_SPLINE_CURVE_WITH_KNOTS('',3,(#405979,#405980,#405981,#405982),
 .UNSPECIFIED.,.F.,.F.,(4,4),(0.,9.54361881492174E-5),.UNSPECIFIED.);
#25746=B_SPLINE_CURVE_WITH_KNOTS('',3,(#405987,#405988,#405989,#405990,
#405991,#405992,#405993),.UNSPECIFIED.,.F.,.F.,(4,3,4),(0.,4.41069704323467E-5,
0.000113970027818833),.UNSPECIFIED.);
#25747=B_SPLINE_CURVE_WITH_KNOTS('',3,(#405999,#406000,#406001,#406002),
 .UNSPECIFIED.,.F.,.F.,(4,4),(1.0842021724855E-19,9.5436188149218E-5),
 .UNSPECIFIED.);
#25748=B_SPLINE_CURVE_WITH_KNOTS('',3,(#406006,#406007,#406008,#406009,
#406010,#406011,#406012),.UNSPECIFIED.,.F.,.F.,(4,3,4),(0.,6.98630244191491E-5,
0.000113969974038089),.UNSPECIFIED.);
#25749=B_SPLINE_CURVE_WITH_KNOTS('',3,(#406015,#406016,#406017,#406018,
#406019,#406020,#406021,#406022,#406023,#406024,#406025,#406026,#406027,
#406028,#406029,#406030,#406031,#406032,#406033,#406034,#406035,#406036,
#406037,#406038,#406039,#406040,#406041,#406042,#406043,#406044,#406045,
#406046,#406047,#406048,#406049,#406050,#406051,#406052,#406053,#406054,
#406055,#406056,#406057,#406058,#406059,#406060,#406061,#406062,#406063),
 .UNSPECIFIED.,.F.,.F.,(4,3,3,3,3,3,3,3,3,3,3,3,3,3,3,3,4),(0.,1.53100299373407E-6,
4.52554775679091E-6,7.011512462916E-6,9.26752933799658E-6,1.03084066197173E-5,
1.17138990826861E-5,1.22284894984074E-5,1.30315035324817E-5,1.38363728497813E-5,
1.40464197777494E-5,1.54597749564637E-5,1.62073588704067E-5,1.92092968712989E-5,
1.95234416882551E-5,2.37637844577598E-5,2.61487188977256E-5),
 .UNSPECIFIED.);
#25750=B_SPLINE_CURVE_WITH_KNOTS('',3,(#406078,#406079,#406080,#406081,
#406082,#406083,#406084,#406085,#406086,#406087,#406088,#406089,#406090,
#406091,#406092,#406093,#406094,#406095,#406096,#406097,#406098,#406099,
#406100,#406101,#406102,#406103,#406104,#406105,#406106,#406107,#406108),
 .UNSPECIFIED.,.F.,.F.,(4,3,3,3,3,3,3,3,3,3,4),(0.,3.95507910398523E-6,
7.53768426604203E-6,1.1990453333535E-5,1.40475043392585E-5,1.51452104275962E-5,
1.67866272813973E-5,1.69621513005356E-5,1.8133831546071E-5,1.98906334656504E-5,
2.06132424588242E-5),.UNSPECIFIED.);
#25751=B_SPLINE_CURVE_WITH_KNOTS('',3,(#406111,#406112,#406113,#406114),
 .UNSPECIFIED.,.F.,.F.,(4,4),(5.42101086242752E-19,0.00010938435327491),
 .UNSPECIFIED.);
#25752=B_SPLINE_CURVE_WITH_KNOTS('',3,(#406141,#406142,#406143,#406144,
#406145,#406146,#406147,#406148,#406149,#406150,#406151,#406152,#406153,
#406154,#406155,#406156,#406157,#406158,#406159,#406160,#406161,#406162,
#406163,#406164,#406165,#406166,#406167,#406168,#406169,#406170,#406171,
#406172,#406173,#406174),.UNSPECIFIED.,.F.,.F.,(4,3,3,3,3,3,3,3,3,3,3,4),
(1.0842021724855E-19,2.09623992729449E-6,3.17176647120215E-6,4.82636181943874E-6,
5.01000917339961E-6,6.13126454147489E-6,8.60486650288858E-6,9.21144281170495E-6,
1.24722301136101E-5,1.42666454787857E-5,2.04670653756931E-5,2.08026438176806E-5),
 .UNSPECIFIED.);
#25753=B_SPLINE_CURVE_WITH_KNOTS('',3,(#406175,#406176,#406177,#406178),
 .UNSPECIFIED.,.F.,.F.,(4,4),(0.,0.000109384345496908),.UNSPECIFIED.);
#25754=B_SPLINE_CURVE_WITH_KNOTS('',3,(#406283,#406284,#406285,#406286),
 .UNSPECIFIED.,.F.,.F.,(4,4),(0.,9.54361881492175E-5),.UNSPECIFIED.);
#25755=B_SPLINE_CURVE_WITH_KNOTS('',3,(#406291,#406292,#406293,#406294,
#406295,#406296,#406297),.UNSPECIFIED.,.F.,.F.,(4,3,4),(0.,4.4106970432347E-5,
0.000113970027818833),.UNSPECIFIED.);
#25756=B_SPLINE_CURVE_WITH_KNOTS('',3,(#406303,#406304,#406305,#406306),
 .UNSPECIFIED.,.F.,.F.,(4,4),(2.16840434497101E-19,9.54361881492178E-5),
 .UNSPECIFIED.);
#25757=B_SPLINE_CURVE_WITH_KNOTS('',3,(#406310,#406311,#406312,#406313,
#406314,#406315,#406316),.UNSPECIFIED.,.F.,.F.,(4,3,4),(0.,6.9863024419149E-5,
0.000113969974038089),.UNSPECIFIED.);
#25758=B_SPLINE_CURVE_WITH_KNOTS('',3,(#406319,#406320,#406321,#406322,
#406323,#406324,#406325,#406326,#406327,#406328,#406329,#406330,#406331,
#406332,#406333,#406334,#406335,#406336,#406337,#406338,#406339,#406340,
#406341,#406342,#406343,#406344,#406345,#406346,#406347,#406348,#406349,
#406350,#406351,#406352,#406353,#406354,#406355,#406356,#406357,#406358,
#406359,#406360,#406361,#406362,#406363,#406364,#406365,#406366,#406367),
 .UNSPECIFIED.,.F.,.F.,(4,3,3,3,3,3,3,3,3,3,3,3,3,3,3,3,4),(0.,1.53100299373416E-6,
4.52554775679514E-6,7.0115124629161E-6,9.26752933799368E-6,1.03084066197174E-5,
1.17138990826862E-5,1.22284894984073E-5,1.30315035324817E-5,1.38363728497812E-5,
1.40464197777492E-5,1.5459774956464E-5,1.62073588704068E-5,1.92092968713296E-5,
1.95234416882555E-5,2.37637844577558E-5,2.6148718897726E-5),
 .UNSPECIFIED.);
#25759=B_SPLINE_CURVE_WITH_KNOTS('',3,(#406382,#406383,#406384,#406385,
#406386,#406387,#406388,#406389,#406390,#406391,#406392,#406393,#406394,
#406395,#406396,#406397,#406398,#406399,#406400,#406401,#406402,#406403,
#406404,#406405,#406406,#406407,#406408,#406409,#406410,#406411,#406412),
 .UNSPECIFIED.,.F.,.F.,(4,3,3,3,3,3,3,3,3,3,4),(0.,3.95507910397283E-6,
7.53768426604198E-6,1.19904533335351E-5,1.40475043392585E-5,1.51452104275962E-5,
1.67866272814064E-5,1.69621513005357E-5,1.81338315460709E-5,1.98906334656548E-5,
2.06132424588242E-5),.UNSPECIFIED.);
#25760=B_SPLINE_CURVE_WITH_KNOTS('',3,(#406415,#406416,#406417,#406418),
 .UNSPECIFIED.,.F.,.F.,(4,4),(1.06229684024259E-18,0.00010938435327491),
 .UNSPECIFIED.);
#25761=B_SPLINE_CURVE_WITH_KNOTS('',3,(#406445,#406446,#406447,#406448,
#406449,#406450,#406451,#406452,#406453,#406454,#406455,#406456,#406457,
#406458,#406459,#406460,#406461,#406462,#406463,#406464,#406465,#406466,
#406467,#406468,#406469,#406470,#406471,#406472,#406473,#406474,#406475,
#406476,#406477,#406478),.UNSPECIFIED.,.F.,.F.,(4,3,3,3,3,3,3,3,3,3,3,4),
(0.,2.0962399272943E-6,3.17176647120212E-6,4.82636181943056E-6,5.01000917339971E-6,
6.13126454147472E-6,8.60486650288839E-6,9.21144281170468E-6,1.24722301136024E-5,
1.42666454787851E-5,2.04670653756884E-5,2.08026438176793E-5),
 .UNSPECIFIED.);
#25762=B_SPLINE_CURVE_WITH_KNOTS('',3,(#406479,#406480,#406481,#406482),
 .UNSPECIFIED.,.F.,.F.,(4,4),(0.,0.000109384345496908),.UNSPECIFIED.);
#25763=B_SPLINE_CURVE_WITH_KNOTS('',3,(#406587,#406588,#406589,#406590),
 .UNSPECIFIED.,.F.,.F.,(4,4),(0.,9.54361881492172E-5),.UNSPECIFIED.);
#25764=B_SPLINE_CURVE_WITH_KNOTS('',3,(#406595,#406596,#406597,#406598,
#406599,#406600,#406601),.UNSPECIFIED.,.F.,.F.,(4,3,4),(0.,4.41069704323466E-5,
0.000113970027818833),.UNSPECIFIED.);
#25765=B_SPLINE_CURVE_WITH_KNOTS('',3,(#406607,#406608,#406609,#406610),
 .UNSPECIFIED.,.F.,.F.,(4,4),(2.16840434497101E-19,9.54361881492177E-5),
 .UNSPECIFIED.);
#25766=B_SPLINE_CURVE_WITH_KNOTS('',3,(#406614,#406615,#406616,#406617,
#406618,#406619,#406620),.UNSPECIFIED.,.F.,.F.,(4,3,4),(0.,6.98630244191489E-5,
0.000113969974038089),.UNSPECIFIED.);
#25767=B_SPLINE_CURVE_WITH_KNOTS('',3,(#406623,#406624,#406625,#406626,
#406627,#406628,#406629,#406630,#406631,#406632,#406633,#406634,#406635,
#406636,#406637,#406638,#406639,#406640,#406641,#406642,#406643,#406644,
#406645,#406646,#406647,#406648,#406649,#406650,#406651,#406652,#406653,
#406654,#406655,#406656,#406657,#406658,#406659,#406660,#406661,#406662,
#406663,#406664,#406665,#406666,#406667,#406668,#406669,#406670,#406671),
 .UNSPECIFIED.,.F.,.F.,(4,3,3,3,3,3,3,3,3,3,3,3,3,3,3,3,4),(0.,1.53100299373418E-6,
4.52554775678938E-6,7.01151246291608E-6,9.26752933799924E-6,1.03084066197175E-5,
1.17138990826861E-5,1.22284894984077E-5,1.30315035324817E-5,1.38363728497813E-5,
1.40464197777495E-5,1.54597749564642E-5,1.62073588704069E-5,1.9209296871297E-5,
1.95234416882558E-5,2.37637844577571E-5,2.61487188977267E-5),
 .UNSPECIFIED.);
#25768=B_SPLINE_CURVE_WITH_KNOTS('',3,(#406686,#406687,#406688,#406689,
#406690,#406691,#406692,#406693,#406694,#406695,#406696,#406697,#406698,
#406699,#406700,#406701,#406702,#406703,#406704,#406705,#406706,#406707,
#406708,#406709,#406710,#406711,#406712,#406713,#406714,#406715,#406716),
 .UNSPECIFIED.,.F.,.F.,(4,3,3,3,3,3,3,3,3,3,4),(0.,3.95507910397925E-6,
7.53768426604196E-6,1.19904533335351E-5,1.40475043392584E-5,1.51452104275962E-5,
1.67866272814223E-5,1.69621513005356E-5,1.8133831546071E-5,1.98906334656514E-5,
2.06132424588242E-5),.UNSPECIFIED.);
#25769=B_SPLINE_CURVE_WITH_KNOTS('',3,(#406719,#406720,#406721,#406722),
 .UNSPECIFIED.,.F.,.F.,(4,4),(4.84869951806108E-19,0.00010938435327491),
 .UNSPECIFIED.);
#25770=B_SPLINE_CURVE_WITH_KNOTS('',3,(#406749,#406750,#406751,#406752,
#406753,#406754,#406755,#406756,#406757,#406758,#406759,#406760,#406761,
#406762,#406763,#406764,#406765,#406766,#406767,#406768,#406769,#406770,
#406771,#406772,#406773,#406774,#406775,#406776,#406777,#406778,#406779,
#406780,#406781,#406782),.UNSPECIFIED.,.F.,.F.,(4,3,3,3,3,3,3,3,3,3,3,4),
(2.16840434497101E-19,2.0962399272944E-6,3.17176647120198E-6,4.82636181943813E-6,
5.0100091733995E-6,6.13126454147485E-6,8.60486650288839E-6,9.21144281170471E-6,
1.24722301135892E-5,1.42666454787855E-5,2.04670653756988E-5,2.08026438176803E-5),
 .UNSPECIFIED.);
#25771=B_SPLINE_CURVE_WITH_KNOTS('',3,(#406783,#406784,#406785,#406786),
 .UNSPECIFIED.,.F.,.F.,(4,4),(0.,0.000109384345496908),.UNSPECIFIED.);
#25772=B_SPLINE_CURVE_WITH_KNOTS('',3,(#406891,#406892,#406893,#406894),
 .UNSPECIFIED.,.F.,.F.,(4,4),(0.,9.54361881492175E-5),.UNSPECIFIED.);
#25773=B_SPLINE_CURVE_WITH_KNOTS('',3,(#406899,#406900,#406901,#406902,
#406903,#406904,#406905),.UNSPECIFIED.,.F.,.F.,(4,3,4),(0.,4.41069704323467E-5,
0.000113970027818833),.UNSPECIFIED.);
#25774=B_SPLINE_CURVE_WITH_KNOTS('',3,(#406911,#406912,#406913,#406914),
 .UNSPECIFIED.,.F.,.F.,(4,4),(2.16840434497101E-19,9.5436188149218E-5),
 .UNSPECIFIED.);
#25775=B_SPLINE_CURVE_WITH_KNOTS('',3,(#406918,#406919,#406920,#406921,
#406922,#406923,#406924),.UNSPECIFIED.,.F.,.F.,(4,3,4),(0.,6.9863024419149E-5,
0.000113969974038089),.UNSPECIFIED.);
#25776=B_SPLINE_CURVE_WITH_KNOTS('',3,(#406927,#406928,#406929,#406930,
#406931,#406932,#406933,#406934,#406935,#406936,#406937,#406938,#406939,
#406940,#406941,#406942,#406943,#406944,#406945,#406946,#406947,#406948,
#406949,#406950,#406951,#406952,#406953,#406954,#406955,#406956,#406957,
#406958,#406959,#406960,#406961,#406962,#406963,#406964,#406965,#406966,
#406967,#406968,#406969,#406970,#406971,#406972,#406973,#406974,#406975),
 .UNSPECIFIED.,.F.,.F.,(4,3,3,3,3,3,3,3,3,3,3,3,3,3,3,3,4),(0.,1.53100299373417E-6,
4.5255477567939E-6,7.01151246291599E-6,9.26752933800752E-6,1.03084066197173E-5,
1.1713899082686E-5,1.22284894984074E-5,1.30315035324818E-5,1.38363728497814E-5,
1.40464197777495E-5,1.54597749564642E-5,1.62073588704071E-5,1.92092968712427E-5,
1.95234416882558E-5,2.37637844577606E-5,2.61487188977267E-5),
 .UNSPECIFIED.);
#25777=B_SPLINE_CURVE_WITH_KNOTS('',3,(#406990,#406991,#406992,#406993,
#406994,#406995,#406996,#406997,#406998,#406999,#407000,#407001,#407002,
#407003,#407004,#407005,#407006,#407007,#407008,#407009,#407010,#407011,
#407012,#407013,#407014,#407015,#407016,#407017,#407018,#407019,#407020),
 .UNSPECIFIED.,.F.,.F.,(4,3,3,3,3,3,3,3,3,3,4),(0.,3.95507910397345E-6,
7.53768426604203E-6,1.19904533335351E-5,1.40475043392584E-5,1.51452104275961E-5,
1.67866272814359E-5,1.69621513005354E-5,1.81338315460706E-5,1.98906334656507E-5,
2.06132424588236E-5),.UNSPECIFIED.);
#25778=B_SPLINE_CURVE_WITH_KNOTS('',3,(#407023,#407024,#407025,#407026),
 .UNSPECIFIED.,.F.,.F.,(4,4),(6.1331736667335E-19,0.00010938435327491),
 .UNSPECIFIED.);
#25779=B_SPLINE_CURVE_WITH_KNOTS('',3,(#407053,#407054,#407055,#407056,
#407057,#407058,#407059,#407060,#407061,#407062,#407063,#407064,#407065,
#407066,#407067,#407068,#407069,#407070,#407071,#407072,#407073,#407074,
#407075,#407076,#407077,#407078,#407079,#407080,#407081,#407082,#407083,
#407084,#407085,#407086),.UNSPECIFIED.,.F.,.F.,(4,3,3,3,3,3,3,3,3,3,3,4),
(2.16840434497101E-19,2.09623992729424E-6,3.17176647120213E-6,4.82636181944472E-6,
5.01000917339969E-6,6.13126454147474E-6,8.6048665028883E-6,9.21144281170472E-6,
1.2472230113588E-5,1.42666454787853E-5,2.04670653757003E-5,2.08026438176799E-5),
 .UNSPECIFIED.);
#25780=B_SPLINE_CURVE_WITH_KNOTS('',3,(#407087,#407088,#407089,#407090),
 .UNSPECIFIED.,.F.,.F.,(4,4),(0.,0.000109384345496908),.UNSPECIFIED.);
#25781=B_SPLINE_CURVE_WITH_KNOTS('',3,(#407195,#407196,#407197,#407198),
 .UNSPECIFIED.,.F.,.F.,(4,4),(0.,9.54361881492175E-5),.UNSPECIFIED.);
#25782=B_SPLINE_CURVE_WITH_KNOTS('',3,(#407203,#407204,#407205,#407206,
#407207,#407208,#407209),.UNSPECIFIED.,.F.,.F.,(4,3,4),(0.,4.4106970432347E-5,
0.000113970027818833),.UNSPECIFIED.);
#25783=B_SPLINE_CURVE_WITH_KNOTS('',3,(#407215,#407216,#407217,#407218),
 .UNSPECIFIED.,.F.,.F.,(4,4),(2.16840434497101E-19,9.54361881492179E-5),
 .UNSPECIFIED.);
#25784=B_SPLINE_CURVE_WITH_KNOTS('',3,(#407222,#407223,#407224,#407225,
#407226,#407227,#407228),.UNSPECIFIED.,.F.,.F.,(4,3,4),(0.,6.98630244191489E-5,
0.000113969974038089),.UNSPECIFIED.);
#25785=B_SPLINE_CURVE_WITH_KNOTS('',3,(#407231,#407232,#407233,#407234,
#407235,#407236,#407237,#407238,#407239,#407240,#407241,#407242,#407243,
#407244,#407245,#407246,#407247,#407248,#407249,#407250,#407251,#407252,
#407253,#407254,#407255,#407256,#407257,#407258,#407259,#407260,#407261,
#407262,#407263,#407264,#407265,#407266,#407267,#407268,#407269,#407270,
#407271,#407272,#407273,#407274,#407275,#407276,#407277,#407278,#407279),
 .UNSPECIFIED.,.F.,.F.,(4,3,3,3,3,3,3,3,3,3,3,3,3,3,3,3,4),(0.,1.53100299373418E-6,
4.52554775679471E-6,7.0115124629162E-6,9.26752933799194E-6,1.03084066197174E-5,
1.17138990826862E-5,1.22284894984075E-5,1.30315035324818E-5,1.38363728497813E-5,
1.40464197777498E-5,1.54597749564643E-5,1.62073588704074E-5,1.92092968711982E-5,
1.95234416882562E-5,2.37637844577607E-5,2.6148718897727E-5),
 .UNSPECIFIED.);
#25786=B_SPLINE_CURVE_WITH_KNOTS('',3,(#407294,#407295,#407296,#407297,
#407298,#407299,#407300,#407301,#407302,#407303,#407304,#407305,#407306,
#407307,#407308,#407309,#407310,#407311,#407312,#407313,#407314,#407315,
#407316,#407317,#407318,#407319,#407320,#407321,#407322,#407323,#407324),
 .UNSPECIFIED.,.F.,.F.,(4,3,3,3,3,3,3,3,3,3,4),(0.,3.95507910397078E-6,
7.537684266042E-6,1.19904533335351E-5,1.40475043392585E-5,1.51452104275965E-5,
1.67866272814274E-5,1.69621513005358E-5,1.81338315460712E-5,1.98906334656593E-5,
2.06132424588248E-5),.UNSPECIFIED.);
#25787=B_SPLINE_CURVE_WITH_KNOTS('',3,(#407327,#407328,#407329,#407330),
 .UNSPECIFIED.,.F.,.F.,(4,4),(2.16840434497101E-19,0.00010938435327491),
 .UNSPECIFIED.);
#25788=B_SPLINE_CURVE_WITH_KNOTS('',3,(#407357,#407358,#407359,#407360,
#407361,#407362,#407363,#407364,#407365,#407366,#407367,#407368,#407369,
#407370,#407371,#407372,#407373,#407374,#407375,#407376,#407377,#407378,
#407379,#407380,#407381,#407382,#407383,#407384,#407385,#407386,#407387,
#407388,#407389,#407390),.UNSPECIFIED.,.F.,.F.,(4,3,3,3,3,3,3,3,3,3,3,4),
(0.,2.09623992729454E-6,3.17176647120236E-6,4.82636181944207E-6,5.01000917339988E-6,
6.13126454147488E-6,8.60486650288867E-6,9.21144281170499E-6,1.24722301136154E-5,
1.42666454787857E-5,2.04670653757237E-5,2.08026438176804E-5),
 .UNSPECIFIED.);
#25789=B_SPLINE_CURVE_WITH_KNOTS('',3,(#407391,#407392,#407393,#407394),
 .UNSPECIFIED.,.F.,.F.,(4,4),(0.,0.000109384345496908),.UNSPECIFIED.);
#25790=B_SPLINE_CURVE_WITH_KNOTS('',3,(#407499,#407500,#407501,#407502),
 .UNSPECIFIED.,.F.,.F.,(4,4),(0.,9.54361881492175E-5),.UNSPECIFIED.);
#25791=B_SPLINE_CURVE_WITH_KNOTS('',3,(#407507,#407508,#407509,#407510,
#407511,#407512,#407513),.UNSPECIFIED.,.F.,.F.,(4,3,4),(0.,4.41069704323469E-5,
0.000113970027818833),.UNSPECIFIED.);
#25792=B_SPLINE_CURVE_WITH_KNOTS('',3,(#407519,#407520,#407521,#407522),
 .UNSPECIFIED.,.F.,.F.,(4,4),(2.16840434497101E-19,9.54361881492178E-5),
 .UNSPECIFIED.);
#25793=B_SPLINE_CURVE_WITH_KNOTS('',3,(#407526,#407527,#407528,#407529,
#407530,#407531,#407532),.UNSPECIFIED.,.F.,.F.,(4,3,4),(0.,6.98630244191491E-5,
0.000113969974038089),.UNSPECIFIED.);
#25794=B_SPLINE_CURVE_WITH_KNOTS('',3,(#407535,#407536,#407537,#407538,
#407539,#407540,#407541,#407542,#407543,#407544,#407545,#407546,#407547,
#407548,#407549,#407550,#407551,#407552,#407553,#407554,#407555,#407556,
#407557,#407558,#407559,#407560,#407561,#407562,#407563,#407564,#407565,
#407566,#407567,#407568,#407569,#407570,#407571,#407572,#407573,#407574,
#407575,#407576,#407577,#407578,#407579,#407580,#407581,#407582,#407583),
 .UNSPECIFIED.,.F.,.F.,(4,3,3,3,3,3,3,3,3,3,3,3,3,3,3,3,4),(0.,1.53100299373406E-6,
4.52554775679257E-6,7.01151246291608E-6,9.26752933799928E-6,1.03084066197173E-5,
1.17138990826861E-5,1.22284894984075E-5,1.30315035324818E-5,1.38363728497812E-5,
1.40464197777496E-5,1.54597749564643E-5,1.62073588704074E-5,1.92092968712653E-5,
1.95234416882563E-5,2.37637844577625E-5,2.61487188977276E-5),
 .UNSPECIFIED.);
#25795=B_SPLINE_CURVE_WITH_KNOTS('',3,(#407598,#407599,#407600,#407601,
#407602,#407603,#407604,#407605,#407606,#407607,#407608,#407609,#407610,
#407611,#407612,#407613,#407614,#407615,#407616,#407617,#407618,#407619,
#407620,#407621,#407622,#407623,#407624,#407625,#407626,#407627,#407628),
 .UNSPECIFIED.,.F.,.F.,(4,3,3,3,3,3,3,3,3,3,4),(0.,3.9550791039781E-6,7.53768426604216E-6,
1.19904533335351E-5,1.40475043392587E-5,1.51452104275965E-5,1.67866272814076E-5,
1.69621513005362E-5,1.81338315460716E-5,1.98906334656553E-5,2.06132424588251E-5),
 .UNSPECIFIED.);
#25796=B_SPLINE_CURVE_WITH_KNOTS('',3,(#407631,#407632,#407633,#407634),
 .UNSPECIFIED.,.F.,.F.,(4,4),(4.33680868994202E-19,0.00010938435327491),
 .UNSPECIFIED.);
#25797=B_SPLINE_CURVE_WITH_KNOTS('',3,(#407661,#407662,#407663,#407664,
#407665,#407666,#407667,#407668,#407669,#407670,#407671,#407672,#407673,
#407674,#407675,#407676,#407677,#407678,#407679,#407680,#407681,#407682,
#407683,#407684,#407685,#407686,#407687,#407688,#407689,#407690,#407691,
#407692,#407693,#407694),.UNSPECIFIED.,.F.,.F.,(4,3,3,3,3,3,3,3,3,3,3,4),
(4.84869951806108E-19,2.09623992729453E-6,3.17176647120215E-6,4.8263618194302E-6,
5.01000917339957E-6,6.13126454147488E-6,8.60486650288844E-6,9.21144281170473E-6,
1.2472230113588E-5,1.4266645478785E-5,2.04670653756879E-5,2.08026438176792E-5),
 .UNSPECIFIED.);
#25798=B_SPLINE_CURVE_WITH_KNOTS('',3,(#407695,#407696,#407697,#407698),
 .UNSPECIFIED.,.F.,.F.,(4,4),(0.,0.000109384345496908),.UNSPECIFIED.);
#25799=B_SPLINE_CURVE_WITH_KNOTS('',3,(#407803,#407804,#407805,#407806),
 .UNSPECIFIED.,.F.,.F.,(4,4),(0.,9.54361881492177E-5),.UNSPECIFIED.);
#25800=B_SPLINE_CURVE_WITH_KNOTS('',3,(#407811,#407812,#407813,#407814,
#407815,#407816,#407817),.UNSPECIFIED.,.F.,.F.,(4,3,4),(0.,4.41069704323469E-5,
0.000113970027818833),.UNSPECIFIED.);
#25801=B_SPLINE_CURVE_WITH_KNOTS('',3,(#407823,#407824,#407825,#407826),
 .UNSPECIFIED.,.F.,.F.,(4,4),(2.16840434497101E-19,9.5436188149218E-5),
 .UNSPECIFIED.);
#25802=B_SPLINE_CURVE_WITH_KNOTS('',3,(#407830,#407831,#407832,#407833,
#407834,#407835,#407836),.UNSPECIFIED.,.F.,.F.,(4,3,4),(0.,6.98630244191492E-5,
0.000113969974038089),.UNSPECIFIED.);
#25803=B_SPLINE_CURVE_WITH_KNOTS('',3,(#407839,#407840,#407841,#407842,
#407843,#407844,#407845,#407846,#407847,#407848,#407849,#407850,#407851,
#407852,#407853,#407854,#407855,#407856,#407857,#407858,#407859,#407860,
#407861,#407862,#407863,#407864,#407865,#407866,#407867,#407868,#407869,
#407870,#407871,#407872,#407873,#407874,#407875,#407876,#407877,#407878,
#407879,#407880,#407881,#407882,#407883,#407884,#407885,#407886,#407887),
 .UNSPECIFIED.,.F.,.F.,(4,3,3,3,3,3,3,3,3,3,3,3,3,3,3,3,4),(0.,1.53100299373414E-6,
4.52554775679078E-6,7.01151246291599E-6,9.26752933800656E-6,1.03084066197172E-5,
1.17138990826861E-5,1.22284894984074E-5,1.30315035324815E-5,1.38363728497812E-5,
1.40464197777494E-5,1.54597749564641E-5,1.62073588704067E-5,1.92092968712602E-5,
1.95234416882553E-5,2.37637844577585E-5,2.61487188977259E-5),
 .UNSPECIFIED.);
#25804=B_SPLINE_CURVE_WITH_KNOTS('',3,(#407902,#407903,#407904,#407905,
#407906,#407907,#407908,#407909,#407910,#407911,#407912,#407913,#407914,
#407915,#407916,#407917,#407918,#407919,#407920,#407921,#407922,#407923,
#407924,#407925,#407926,#407927,#407928,#407929,#407930,#407931,#407932),
 .UNSPECIFIED.,.F.,.F.,(4,3,3,3,3,3,3,3,3,3,4),(0.,3.95507910397798E-6,
7.53768426604199E-6,1.19904533335349E-5,1.40475043392583E-5,1.51452104275965E-5,
1.67866272814203E-5,1.69621513005356E-5,1.81338315460712E-5,1.98906334656551E-5,
2.0613242458824E-5),.UNSPECIFIED.);
#25805=B_SPLINE_CURVE_WITH_KNOTS('',3,(#407935,#407936,#407937,#407938),
 .UNSPECIFIED.,.F.,.F.,(4,4),(4.33680868994202E-19,0.00010938435327491),
 .UNSPECIFIED.);
#25806=B_SPLINE_CURVE_WITH_KNOTS('',3,(#407965,#407966,#407967,#407968,
#407969,#407970,#407971,#407972,#407973,#407974,#407975,#407976,#407977,
#407978,#407979,#407980,#407981,#407982,#407983,#407984,#407985,#407986,
#407987,#407988,#407989,#407990,#407991,#407992,#407993,#407994,#407995,
#407996,#407997,#407998),.UNSPECIFIED.,.F.,.F.,(4,3,3,3,3,3,3,3,3,3,3,4),
(0.,2.0962399272946E-6,3.1717664712022E-6,4.8263618194285E-6,5.01000917339962E-6,
6.13126454147512E-6,8.60486650288865E-6,9.21144281170501E-6,1.24722301135971E-5,
1.42666454787856E-5,2.04670653756864E-5,2.08026438176801E-5),
 .UNSPECIFIED.);
#25807=B_SPLINE_CURVE_WITH_KNOTS('',3,(#407999,#408000,#408001,#408002),
 .UNSPECIFIED.,.F.,.F.,(4,4),(0.,0.000109384345496908),.UNSPECIFIED.);
#25808=B_SPLINE_CURVE_WITH_KNOTS('',3,(#408107,#408108,#408109,#408110),
 .UNSPECIFIED.,.F.,.F.,(4,4),(0.,9.54361881492175E-5),.UNSPECIFIED.);
#25809=B_SPLINE_CURVE_WITH_KNOTS('',3,(#408115,#408116,#408117,#408118,
#408119,#408120,#408121),.UNSPECIFIED.,.F.,.F.,(4,3,4),(0.,4.41069704323471E-5,
0.000113970027818833),.UNSPECIFIED.);
#25810=B_SPLINE_CURVE_WITH_KNOTS('',3,(#408127,#408128,#408129,#408130),
 .UNSPECIFIED.,.F.,.F.,(4,4),(0.,9.54361881492177E-5),.UNSPECIFIED.);
#25811=B_SPLINE_CURVE_WITH_KNOTS('',3,(#408134,#408135,#408136,#408137,
#408138,#408139,#408140),.UNSPECIFIED.,.F.,.F.,(4,3,4),(0.,6.9863024419149E-5,
0.000113969974038089),.UNSPECIFIED.);
#25812=B_SPLINE_CURVE_WITH_KNOTS('',3,(#408143,#408144,#408145,#408146,
#408147,#408148,#408149,#408150,#408151,#408152,#408153,#408154,#408155,
#408156,#408157,#408158,#408159,#408160,#408161,#408162,#408163,#408164,
#408165,#408166,#408167,#408168,#408169,#408170,#408171,#408172,#408173,
#408174,#408175,#408176,#408177,#408178,#408179,#408180,#408181,#408182,
#408183,#408184,#408185,#408186,#408187,#408188,#408189,#408190,#408191),
 .UNSPECIFIED.,.F.,.F.,(4,3,3,3,3,3,3,3,3,3,3,3,3,3,3,3,4),(0.,1.53100299373409E-6,
4.5255477567909E-6,7.01151246291603E-6,9.26752933800813E-6,1.03084066197175E-5,
1.17138990826863E-5,1.22284894984075E-5,1.30315035324818E-5,1.38363728497814E-5,
1.40464197777496E-5,1.5459774956464E-5,1.6207358870407E-5,1.92092968712736E-5,
1.9523441688256E-5,2.37637844577608E-5,2.61487188977272E-5),
 .UNSPECIFIED.);
#25813=B_SPLINE_CURVE_WITH_KNOTS('',3,(#408206,#408207,#408208,#408209,
#408210,#408211,#408212,#408213,#408214,#408215,#408216,#408217,#408218,
#408219,#408220,#408221,#408222,#408223,#408224,#408225,#408226,#408227,
#408228,#408229,#408230,#408231,#408232,#408233,#408234,#408235,#408236),
 .UNSPECIFIED.,.F.,.F.,(4,3,3,3,3,3,3,3,3,3,4),(0.,3.95507910397288E-6,
7.53768426604196E-6,1.1990453333535E-5,1.40475043392584E-5,1.51452104275964E-5,
1.67866272814138E-5,1.69621513005357E-5,1.8133831546071E-5,1.98906334656539E-5,
2.06132424588241E-5),.UNSPECIFIED.);
#25814=B_SPLINE_CURVE_WITH_KNOTS('',3,(#408239,#408240,#408241,#408242),
 .UNSPECIFIED.,.F.,.F.,(4,4),(4.84869951806108E-19,0.00010938435327491),
 .UNSPECIFIED.);
#25815=B_SPLINE_CURVE_WITH_KNOTS('',3,(#408269,#408270,#408271,#408272,
#408273,#408274,#408275,#408276,#408277,#408278,#408279,#408280,#408281,
#408282,#408283,#408284,#408285,#408286,#408287,#408288,#408289,#408290,
#408291,#408292,#408293,#408294,#408295,#408296,#408297,#408298,#408299,
#408300,#408301,#408302),.UNSPECIFIED.,.F.,.F.,(4,3,3,3,3,3,3,3,3,3,3,4),
(4.84869951806108E-19,2.09623992729411E-6,3.17176647120198E-6,4.82636181942691E-6,
5.01000917339932E-6,6.13126454147457E-6,8.60486650288819E-6,9.21144281170453E-6,
1.24722301135754E-5,1.42666454787853E-5,2.04670653757023E-5,2.080264381768E-5),
 .UNSPECIFIED.);
#25816=B_SPLINE_CURVE_WITH_KNOTS('',3,(#408303,#408304,#408305,#408306),
 .UNSPECIFIED.,.F.,.F.,(4,4),(0.,0.000109384345496908),.UNSPECIFIED.);
#25817=B_SPLINE_CURVE_WITH_KNOTS('',3,(#408411,#408412,#408413,#408414),
 .UNSPECIFIED.,.F.,.F.,(4,4),(0.,9.54361881492177E-5),.UNSPECIFIED.);
#25818=B_SPLINE_CURVE_WITH_KNOTS('',3,(#408419,#408420,#408421,#408422,
#408423,#408424,#408425),.UNSPECIFIED.,.F.,.F.,(4,3,4),(0.,4.4106970432347E-5,
0.000113970027818833),.UNSPECIFIED.);
#25819=B_SPLINE_CURVE_WITH_KNOTS('',3,(#408431,#408432,#408433,#408434),
 .UNSPECIFIED.,.F.,.F.,(4,4),(4.33680868994202E-19,9.54361881492178E-5),
 .UNSPECIFIED.);
#25820=B_SPLINE_CURVE_WITH_KNOTS('',3,(#408438,#408439,#408440,#408441,
#408442,#408443,#408444),.UNSPECIFIED.,.F.,.F.,(4,3,4),(0.,6.98630244191492E-5,
0.000113969974038089),.UNSPECIFIED.);
#25821=B_SPLINE_CURVE_WITH_KNOTS('',3,(#408447,#408448,#408449,#408450,
#408451,#408452,#408453,#408454,#408455,#408456,#408457,#408458,#408459,
#408460,#408461,#408462,#408463,#408464,#408465,#408466,#408467,#408468,
#408469,#408470,#408471,#408472,#408473,#408474,#408475,#408476,#408477,
#408478,#408479,#408480,#408481,#408482,#408483,#408484,#408485,#408486,
#408487,#408488,#408489,#408490,#408491,#408492,#408493,#408494,#408495),
 .UNSPECIFIED.,.F.,.F.,(4,3,3,3,3,3,3,3,3,3,3,3,3,3,3,3,4),(0.,1.53100299373405E-6,
4.52554775679714E-6,7.01151246291601E-6,9.26752933800423E-6,1.03084066197175E-5,
1.17138990826862E-5,1.22284894984072E-5,1.30315035324815E-5,1.3836372849781E-5,
1.40464197777492E-5,1.54597749564635E-5,1.62073588704063E-5,1.920929687128E-5,
1.95234416882546E-5,2.37637844577566E-5,2.61487188977245E-5),
 .UNSPECIFIED.);
#25822=B_SPLINE_CURVE_WITH_KNOTS('',3,(#408510,#408511,#408512,#408513,
#408514,#408515,#408516,#408517,#408518,#408519,#408520,#408521,#408522,
#408523,#408524,#408525,#408526,#408527,#408528,#408529,#408530,#408531,
#408532,#408533,#408534,#408535,#408536,#408537,#408538,#408539,#408540),
 .UNSPECIFIED.,.F.,.F.,(4,3,3,3,3,3,3,3,3,3,4),(0.,3.95507910397667E-6,
7.53768426604193E-6,1.1990453333535E-5,1.40475043392584E-5,1.51452104275964E-5,
1.6786627281433E-5,1.69621513005355E-5,1.81338315460713E-5,1.98906334656521E-5,
2.06132424588243E-5),.UNSPECIFIED.);
#25823=B_SPLINE_CURVE_WITH_KNOTS('',3,(#408543,#408544,#408545,#408546),
 .UNSPECIFIED.,.F.,.F.,(4,4),(4.33680868994202E-19,0.00010938435327491),
 .UNSPECIFIED.);
#25824=B_SPLINE_CURVE_WITH_KNOTS('',3,(#408573,#408574,#408575,#408576,
#408577,#408578,#408579,#408580,#408581,#408582,#408583,#408584,#408585,
#408586,#408587,#408588,#408589,#408590,#408591,#408592,#408593,#408594,
#408595,#408596,#408597,#408598,#408599,#408600,#408601,#408602,#408603,
#408604,#408605,#408606),.UNSPECIFIED.,.F.,.F.,(4,3,3,3,3,3,3,3,3,3,3,4),
(0.,2.09623992729444E-6,3.17176647120251E-6,4.82636181942884E-6,5.01000917339967E-6,
6.131264541475E-6,8.60486650288851E-6,9.21144281170478E-6,1.24722301135965E-5,
1.42666454787855E-5,2.04670653756859E-5,2.08026438176798E-5),
 .UNSPECIFIED.);
#25825=B_SPLINE_CURVE_WITH_KNOTS('',3,(#408607,#408608,#408609,#408610),
 .UNSPECIFIED.,.F.,.F.,(4,4),(0.,0.000109384345496908),.UNSPECIFIED.);
#25826=B_SPLINE_CURVE_WITH_KNOTS('',3,(#408715,#408716,#408717,#408718),
 .UNSPECIFIED.,.F.,.F.,(4,4),(0.,9.54361881492176E-5),.UNSPECIFIED.);
#25827=B_SPLINE_CURVE_WITH_KNOTS('',3,(#408723,#408724,#408725,#408726,
#408727,#408728,#408729),.UNSPECIFIED.,.F.,.F.,(4,3,4),(0.,4.41069704323469E-5,
0.000113970027818834),.UNSPECIFIED.);
#25828=B_SPLINE_CURVE_WITH_KNOTS('',3,(#408735,#408736,#408737,#408738),
 .UNSPECIFIED.,.F.,.F.,(4,4),(4.33680868994202E-19,9.54361881492182E-5),
 .UNSPECIFIED.);
#25829=B_SPLINE_CURVE_WITH_KNOTS('',3,(#408742,#408743,#408744,#408745,
#408746,#408747,#408748),.UNSPECIFIED.,.F.,.F.,(4,3,4),(0.,6.98630244191492E-5,
0.000113969974038089),.UNSPECIFIED.);
#25830=B_SPLINE_CURVE_WITH_KNOTS('',3,(#408751,#408752,#408753,#408754,
#408755,#408756,#408757,#408758,#408759,#408760,#408761,#408762,#408763,
#408764,#408765,#408766,#408767,#408768,#408769,#408770,#408771,#408772,
#408773,#408774,#408775,#408776,#408777,#408778,#408779,#408780,#408781,
#408782,#408783,#408784,#408785,#408786,#408787,#408788,#408789,#408790,
#408791,#408792,#408793,#408794,#408795,#408796,#408797,#408798,#408799),
 .UNSPECIFIED.,.F.,.F.,(4,3,3,3,3,3,3,3,3,3,3,3,3,3,3,3,4),(0.,1.53100299373406E-6,
4.52554775679991E-6,7.01151246291622E-6,9.26752933802365E-6,1.03084066197173E-5,
1.17138990826863E-5,1.22284894984077E-5,1.30315035324818E-5,1.38363728497814E-5,
1.40464197777498E-5,1.54597749564644E-5,1.62073588704074E-5,1.92092968713074E-5,
1.95234416882564E-5,2.37637844577626E-5,2.6148718897728E-5),
 .UNSPECIFIED.);
#25831=B_SPLINE_CURVE_WITH_KNOTS('',3,(#408814,#408815,#408816,#408817,
#408818,#408819,#408820,#408821,#408822,#408823,#408824,#408825,#408826,
#408827,#408828,#408829,#408830,#408831,#408832,#408833,#408834,#408835,
#408836,#408837,#408838,#408839,#408840,#408841,#408842,#408843,#408844),
 .UNSPECIFIED.,.F.,.F.,(4,3,3,3,3,3,3,3,3,3,4),(0.,3.95507910397371E-6,
7.537684266042E-6,1.1990453333535E-5,1.40475043392586E-5,1.51452104275965E-5,
1.67866272814201E-5,1.69621513005358E-5,1.8133831546071E-5,1.98906334656563E-5,
2.0613242458824E-5),.UNSPECIFIED.);
#25832=B_SPLINE_CURVE_WITH_KNOTS('',3,(#408847,#408848,#408849,#408850),
 .UNSPECIFIED.,.F.,.F.,(4,4),(9.69739903612216E-19,0.00010938435327491),
 .UNSPECIFIED.);
#25833=B_SPLINE_CURVE_WITH_KNOTS('',3,(#408877,#408878,#408879,#408880,
#408881,#408882,#408883,#408884,#408885,#408886,#408887,#408888,#408889,
#408890,#408891,#408892,#408893,#408894,#408895,#408896,#408897,#408898,
#408899,#408900,#408901,#408902,#408903,#408904,#408905,#408906,#408907,
#408908,#408909,#408910),.UNSPECIFIED.,.F.,.F.,(4,3,3,3,3,3,3,3,3,3,3,4),
(2.16840434497101E-19,2.09623992729432E-6,3.17176647120227E-6,4.82636181943918E-6,
5.01000917339956E-6,6.13126454147501E-6,8.60486650288879E-6,9.21144281170531E-6,
1.24722301135938E-5,1.4266645478786E-5,2.04670653756976E-5,2.08026438176811E-5),
 .UNSPECIFIED.);
#25834=B_SPLINE_CURVE_WITH_KNOTS('',3,(#408911,#408912,#408913,#408914),
 .UNSPECIFIED.,.F.,.F.,(4,4),(0.,0.000109384345496908),.UNSPECIFIED.);
#25835=B_SPLINE_CURVE_WITH_KNOTS('',3,(#409019,#409020,#409021,#409022),
 .UNSPECIFIED.,.F.,.F.,(4,4),(0.,9.54361881492175E-5),.UNSPECIFIED.);
#25836=B_SPLINE_CURVE_WITH_KNOTS('',3,(#409027,#409028,#409029,#409030,
#409031,#409032,#409033),.UNSPECIFIED.,.F.,.F.,(4,3,4),(0.,4.41069704323468E-5,
0.000113970027818833),.UNSPECIFIED.);
#25837=B_SPLINE_CURVE_WITH_KNOTS('',3,(#409039,#409040,#409041,#409042),
 .UNSPECIFIED.,.F.,.F.,(4,4),(0.,9.54361881492175E-5),.UNSPECIFIED.);
#25838=B_SPLINE_CURVE_WITH_KNOTS('',3,(#409046,#409047,#409048,#409049,
#409050,#409051,#409052),.UNSPECIFIED.,.F.,.F.,(4,3,4),(0.,6.9863024419149E-5,
0.000113969974038089),.UNSPECIFIED.);
#25839=B_SPLINE_CURVE_WITH_KNOTS('',3,(#409055,#409056,#409057,#409058,
#409059,#409060,#409061,#409062,#409063,#409064,#409065,#409066,#409067,
#409068,#409069,#409070,#409071,#409072,#409073,#409074,#409075,#409076,
#409077,#409078,#409079,#409080,#409081,#409082,#409083,#409084,#409085,
#409086,#409087,#409088,#409089,#409090,#409091,#409092,#409093,#409094,
#409095,#409096,#409097,#409098,#409099,#409100,#409101,#409102,#409103),
 .UNSPECIFIED.,.F.,.F.,(4,3,3,3,3,3,3,3,3,3,3,3,3,3,3,3,4),(0.,1.53100299373409E-6,
4.52554775679543E-6,7.0115124629162E-6,9.26752933800661E-6,1.03084066197173E-5,
1.17138990826866E-5,1.22284894984077E-5,1.30315035324818E-5,1.38363728497812E-5,
1.40464197777494E-5,1.54597749564641E-5,1.62073588704069E-5,1.92092968713103E-5,
1.95234416882556E-5,2.37637844577594E-5,2.61487188977262E-5),
 .UNSPECIFIED.);
#25840=B_SPLINE_CURVE_WITH_KNOTS('',3,(#409118,#409119,#409120,#409121,
#409122,#409123,#409124,#409125,#409126,#409127,#409128,#409129,#409130,
#409131,#409132,#409133,#409134,#409135,#409136,#409137,#409138,#409139,
#409140,#409141,#409142,#409143,#409144,#409145,#409146,#409147,#409148),
 .UNSPECIFIED.,.F.,.F.,(4,3,3,3,3,3,3,3,3,3,4),(0.,3.95507910398226E-6,
7.53768426604186E-6,1.19904533335351E-5,1.40475043392585E-5,1.51452104275963E-5,
1.67866272814373E-5,1.69621513005357E-5,1.81338315460711E-5,1.98906334656523E-5,
2.06132424588248E-5),.UNSPECIFIED.);
#25841=B_SPLINE_CURVE_WITH_KNOTS('',3,(#409151,#409152,#409153,#409154),
 .UNSPECIFIED.,.F.,.F.,(4,4),(9.69739903612216E-19,0.00010938435327491),
 .UNSPECIFIED.);
#25842=B_SPLINE_CURVE_WITH_KNOTS('',3,(#409181,#409182,#409183,#409184,
#409185,#409186,#409187,#409188,#409189,#409190,#409191,#409192,#409193,
#409194,#409195,#409196,#409197,#409198,#409199,#409200,#409201,#409202,
#409203,#409204,#409205,#409206,#409207,#409208,#409209,#409210,#409211,
#409212,#409213,#409214),.UNSPECIFIED.,.F.,.F.,(4,3,3,3,3,3,3,3,3,3,3,4),
(0.,2.09623992729454E-6,3.17176647120208E-6,4.82636181943714E-6,5.01000917339954E-6,
6.13126454147485E-6,8.6048665028884E-6,9.21144281170467E-6,1.24722301135978E-5,
1.42666454787854E-5,2.04670653756991E-5,2.08026438176802E-5),
 .UNSPECIFIED.);
#25843=B_SPLINE_CURVE_WITH_KNOTS('',3,(#409215,#409216,#409217,#409218),
 .UNSPECIFIED.,.F.,.F.,(4,4),(0.,0.000109384345496908),.UNSPECIFIED.);
#25844=B_SPLINE_CURVE_WITH_KNOTS('',3,(#409323,#409324,#409325,#409326),
 .UNSPECIFIED.,.F.,.F.,(4,4),(0.,9.54361881492177E-5),.UNSPECIFIED.);
#25845=B_SPLINE_CURVE_WITH_KNOTS('',3,(#409331,#409332,#409333,#409334,
#409335,#409336,#409337),.UNSPECIFIED.,.F.,.F.,(4,3,4),(0.,4.4106970432347E-5,
0.000113970027818833),.UNSPECIFIED.);
#25846=B_SPLINE_CURVE_WITH_KNOTS('',3,(#409343,#409344,#409345,#409346),
 .UNSPECIFIED.,.F.,.F.,(4,4),(4.33680868994202E-19,9.54361881492177E-5),
 .UNSPECIFIED.);
#25847=B_SPLINE_CURVE_WITH_KNOTS('',3,(#409350,#409351,#409352,#409353,
#409354,#409355,#409356),.UNSPECIFIED.,.F.,.F.,(4,3,4),(0.,6.98630244191492E-5,
0.000113969974038089),.UNSPECIFIED.);
#25848=B_SPLINE_CURVE_WITH_KNOTS('',3,(#409359,#409360,#409361,#409362,
#409363,#409364,#409365,#409366,#409367,#409368,#409369,#409370,#409371,
#409372,#409373,#409374,#409375,#409376,#409377,#409378,#409379,#409380,
#409381,#409382,#409383,#409384,#409385,#409386,#409387,#409388,#409389,
#409390,#409391,#409392,#409393,#409394,#409395,#409396,#409397,#409398,
#409399,#409400,#409401,#409402,#409403,#409404,#409405,#409406,#409407),
 .UNSPECIFIED.,.F.,.F.,(4,3,3,3,3,3,3,3,3,3,3,3,3,3,3,3,4),(0.,1.53100299373425E-6,
4.52554775679046E-6,7.01151246291605E-6,9.26752933801314E-6,1.03084066197174E-5,
1.17138990826863E-5,1.22284894984077E-5,1.30315035324819E-5,1.38363728497813E-5,
1.40464197777496E-5,1.54597749564642E-5,1.62073588704071E-5,1.92092968712869E-5,
1.95234416882558E-5,2.37637844577587E-5,2.61487188977268E-5),
 .UNSPECIFIED.);
#25849=B_SPLINE_CURVE_WITH_KNOTS('',3,(#409422,#409423,#409424,#409425,
#409426,#409427,#409428,#409429,#409430,#409431,#409432,#409433,#409434,
#409435,#409436,#409437,#409438,#409439,#409440,#409441,#409442,#409443,
#409444,#409445,#409446,#409447,#409448,#409449,#409450,#409451,#409452),
 .UNSPECIFIED.,.F.,.F.,(4,3,3,3,3,3,3,3,3,3,4),(0.,3.95507910398037E-6,
7.53768426604205E-6,1.1990453333535E-5,1.40475043392586E-5,1.51452104275966E-5,
1.67866272814047E-5,1.69621513005358E-5,1.81338315460714E-5,1.98906334656534E-5,
2.06132424588246E-5),.UNSPECIFIED.);
#25850=B_SPLINE_CURVE_WITH_KNOTS('',3,(#409455,#409456,#409457,#409458),
 .UNSPECIFIED.,.F.,.F.,(4,4),(9.69739903612216E-19,0.00010938435327491),
 .UNSPECIFIED.);
#25851=B_SPLINE_CURVE_WITH_KNOTS('',3,(#409485,#409486,#409487,#409488,
#409489,#409490,#409491,#409492,#409493,#409494,#409495,#409496,#409497,
#409498,#409499,#409500,#409501,#409502,#409503,#409504,#409505,#409506,
#409507,#409508,#409509,#409510,#409511,#409512,#409513,#409514,#409515,
#409516,#409517,#409518),.UNSPECIFIED.,.F.,.F.,(4,3,3,3,3,3,3,3,3,3,3,4),
(0.,2.09623992729449E-6,3.17176647120242E-6,4.8263618194437E-6,5.01000917339965E-6,
6.1312645414752E-6,8.60486650288857E-6,9.21144281170512E-6,1.24722301136084E-5,
1.42666454787857E-5,2.04670653757026E-5,2.08026438176804E-5),
 .UNSPECIFIED.);
#25852=B_SPLINE_CURVE_WITH_KNOTS('',3,(#409519,#409520,#409521,#409522),
 .UNSPECIFIED.,.F.,.F.,(4,4),(0.,0.000109384345496908),.UNSPECIFIED.);
#29078=LINE('',#371611,#32880);
#29079=LINE('',#371620,#32881);
#29080=LINE('',#371650,#32882);
#29081=LINE('',#371680,#32883);
#29082=LINE('',#371710,#32884);
#29083=LINE('',#371740,#32885);
#29084=LINE('',#371770,#32886);
#29085=LINE('',#371800,#32887);
#29086=LINE('',#371830,#32888);
#29087=LINE('',#371860,#32889);
#29088=LINE('',#371890,#32890);
#29089=LINE('',#371920,#32891);
#29090=LINE('',#371950,#32892);
#29091=LINE('',#371980,#32893);
#29092=LINE('',#372010,#32894);
#29093=LINE('',#372040,#32895);
#29094=LINE('',#372070,#32896);
#29095=LINE('',#372100,#32897);
#29096=LINE('',#372130,#32898);
#29097=LINE('',#372160,#32899);
#29098=LINE('',#372190,#32900);
#29099=LINE('',#372220,#32901);
#29100=LINE('',#372250,#32902);
#29101=LINE('',#372280,#32903);
#29102=LINE('',#372310,#32904);
#29103=LINE('',#372340,#32905);
#29104=LINE('',#372370,#32906);
#29105=LINE('',#372400,#32907);
#29106=LINE('',#372430,#32908);
#29107=LINE('',#372460,#32909);
#29108=LINE('',#372485,#32910);
#29109=LINE('',#372508,#32911);
#29110=LINE('',#372584,#32912);
#29111=LINE('',#372660,#32913);
#29112=LINE('',#372738,#32914);
#29113=LINE('',#372816,#32915);
#29114=LINE('',#372892,#32916);
#29115=LINE('',#372968,#32917);
#29116=LINE('',#373044,#32918);
#29117=LINE('',#373120,#32919);
#29118=LINE('',#373196,#32920);
#29119=LINE('',#373276,#32921);
#29120=LINE('',#373352,#32922);
#29121=LINE('',#373428,#32923);
#29122=LINE('',#373504,#32924);
#29123=LINE('',#373580,#32925);
#29124=LINE('',#373656,#32926);
#29125=LINE('',#373732,#32927);
#29126=LINE('',#373812,#32928);
#29127=LINE('',#373888,#32929);
#29128=LINE('',#373964,#32930);
#29129=LINE('',#374040,#32931);
#29130=LINE('',#374116,#32932);
#29131=LINE('',#374192,#32933);
#29132=LINE('',#374270,#32934);
#29133=LINE('',#374348,#32935);
#29134=LINE('',#374424,#32936);
#29135=LINE('',#374500,#32937);
#29136=LINE('',#374575,#32938);
#29137=LINE('',#374606,#32939);
#29138=LINE('',#374778,#32940);
#29139=LINE('',#374806,#32941);
#29140=LINE('',#375796,#32942);
#29141=LINE('',#376788,#32943);
#29142=LINE('',#376796,#32944);
#29143=LINE('',#376800,#32945);
#29144=LINE('',#376808,#32946);
#29145=LINE('',#376812,#32947);
#29146=LINE('',#376820,#32948);
#29147=LINE('',#376824,#32949);
#29148=LINE('',#376832,#32950);
#29149=LINE('',#376836,#32951);
#29150=LINE('',#376844,#32952);
#29151=LINE('',#376848,#32953);
#29152=LINE('',#376856,#32954);
#29153=LINE('',#376860,#32955);
#29154=LINE('',#376868,#32956);
#29155=LINE('',#376872,#32957);
#29156=LINE('',#376880,#32958);
#29157=LINE('',#376884,#32959);
#29158=LINE('',#376892,#32960);
#29159=LINE('',#376896,#32961);
#29160=LINE('',#376904,#32962);
#29161=LINE('',#376908,#32963);
#29162=LINE('',#376916,#32964);
#29163=LINE('',#376920,#32965);
#29164=LINE('',#376928,#32966);
#29165=LINE('',#376932,#32967);
#29166=LINE('',#376940,#32968);
#29167=LINE('',#376944,#32969);
#29168=LINE('',#376952,#32970);
#29169=LINE('',#376956,#32971);
#29170=LINE('',#376964,#32972);
#29171=LINE('',#376968,#32973);
#29172=LINE('',#376976,#32974);
#29173=LINE('',#376980,#32975);
#29174=LINE('',#376988,#32976);
#29175=LINE('',#376992,#32977);
#29176=LINE('',#377000,#32978);
#29177=LINE('',#377004,#32979);
#29178=LINE('',#377012,#32980);
#29179=LINE('',#377016,#32981);
#29180=LINE('',#377024,#32982);
#29181=LINE('',#377028,#32983);
#29182=LINE('',#377036,#32984);
#29183=LINE('',#377040,#32985);
#29184=LINE('',#377048,#32986);
#29185=LINE('',#377052,#32987);
#29186=LINE('',#377060,#32988);
#29187=LINE('',#377064,#32989);
#29188=LINE('',#377072,#32990);
#29189=LINE('',#377076,#32991);
#29190=LINE('',#377084,#32992);
#29191=LINE('',#377088,#32993);
#29192=LINE('',#377096,#32994);
#29193=LINE('',#377100,#32995);
#29194=LINE('',#377108,#32996);
#29195=LINE('',#377112,#32997);
#29196=LINE('',#377120,#32998);
#29197=LINE('',#377124,#32999);
#29198=LINE('',#377132,#33000);
#29199=LINE('',#377136,#33001);
#29200=LINE('',#377144,#33002);
#29201=LINE('',#377148,#33003);
#29202=LINE('',#377156,#33004);
#29203=LINE('',#377160,#33005);
#29204=LINE('',#377168,#33006);
#29205=LINE('',#377172,#33007);
#29206=LINE('',#377180,#33008);
#29207=LINE('',#377184,#33009);
#29208=LINE('',#377192,#33010);
#29209=LINE('',#377196,#33011);
#29210=LINE('',#377204,#33012);
#29211=LINE('',#377208,#33013);
#29212=LINE('',#377216,#33014);
#29213=LINE('',#377220,#33015);
#29214=LINE('',#377228,#33016);
#29215=LINE('',#377232,#33017);
#29216=LINE('',#377240,#33018);
#29217=LINE('',#377244,#33019);
#29218=LINE('',#377252,#33020);
#29219=LINE('',#377256,#33021);
#29220=LINE('',#377264,#33022);
#29221=LINE('',#377268,#33023);
#29222=LINE('',#377276,#33024);
#29223=LINE('',#377280,#33025);
#29224=LINE('',#377288,#33026);
#29225=LINE('',#377292,#33027);
#29226=LINE('',#377300,#33028);
#29227=LINE('',#377304,#33029);
#29228=LINE('',#377312,#33030);
#29229=LINE('',#377316,#33031);
#29230=LINE('',#377324,#33032);
#29231=LINE('',#377328,#33033);
#29232=LINE('',#377336,#33034);
#29233=LINE('',#377340,#33035);
#29234=LINE('',#377348,#33036);
#29235=LINE('',#377352,#33037);
#29236=LINE('',#377360,#33038);
#29237=LINE('',#377364,#33039);
#29238=LINE('',#377372,#33040);
#29239=LINE('',#377375,#33041);
#29240=LINE('',#377379,#33042);
#29241=LINE('',#377387,#33043);
#29242=LINE('',#377391,#33044);
#29243=LINE('',#377399,#33045);
#29244=LINE('',#377403,#33046);
#29245=LINE('',#377411,#33047);
#29246=LINE('',#377415,#33048);
#29247=LINE('',#377423,#33049);
#29248=LINE('',#377427,#33050);
#29249=LINE('',#377435,#33051);
#29250=LINE('',#377439,#33052);
#29251=LINE('',#377447,#33053);
#29252=LINE('',#377451,#33054);
#29253=LINE('',#377459,#33055);
#29254=LINE('',#377463,#33056);
#29255=LINE('',#377471,#33057);
#29256=LINE('',#377475,#33058);
#29257=LINE('',#377483,#33059);
#29258=LINE('',#377487,#33060);
#29259=LINE('',#377495,#33061);
#29260=LINE('',#377499,#33062);
#29261=LINE('',#377507,#33063);
#29262=LINE('',#377511,#33064);
#29263=LINE('',#377519,#33065);
#29264=LINE('',#377523,#33066);
#29265=LINE('',#377531,#33067);
#29266=LINE('',#377535,#33068);
#29267=LINE('',#377543,#33069);
#29268=LINE('',#377547,#33070);
#29269=LINE('',#377555,#33071);
#29270=LINE('',#377559,#33072);
#29271=LINE('',#377567,#33073);
#29272=LINE('',#377571,#33074);
#29273=LINE('',#377579,#33075);
#29274=LINE('',#377583,#33076);
#29275=LINE('',#377591,#33077);
#29276=LINE('',#377595,#33078);
#29277=LINE('',#377603,#33079);
#29278=LINE('',#377607,#33080);
#29279=LINE('',#377615,#33081);
#29280=LINE('',#377619,#33082);
#29281=LINE('',#377627,#33083);
#29282=LINE('',#377631,#33084);
#29283=LINE('',#377639,#33085);
#29284=LINE('',#377643,#33086);
#29285=LINE('',#377651,#33087);
#29286=LINE('',#377655,#33088);
#29287=LINE('',#377663,#33089);
#29288=LINE('',#377667,#33090);
#29289=LINE('',#377675,#33091);
#29290=LINE('',#377679,#33092);
#29291=LINE('',#377687,#33093);
#29292=LINE('',#377691,#33094);
#29293=LINE('',#377699,#33095);
#29294=LINE('',#377703,#33096);
#29295=LINE('',#377711,#33097);
#29296=LINE('',#377715,#33098);
#29297=LINE('',#377723,#33099);
#29298=LINE('',#377727,#33100);
#29299=LINE('',#377735,#33101);
#29300=LINE('',#377739,#33102);
#29301=LINE('',#377747,#33103);
#29302=LINE('',#377751,#33104);
#29303=LINE('',#377759,#33105);
#29304=LINE('',#377763,#33106);
#29305=LINE('',#377771,#33107);
#29306=LINE('',#377775,#33108);
#29307=LINE('',#377783,#33109);
#29308=LINE('',#377787,#33110);
#29309=LINE('',#377795,#33111);
#29310=LINE('',#377799,#33112);
#29311=LINE('',#377807,#33113);
#29312=LINE('',#377811,#33114);
#29313=LINE('',#377819,#33115);
#29314=LINE('',#377823,#33116);
#29315=LINE('',#377831,#33117);
#29316=LINE('',#377835,#33118);
#29317=LINE('',#377843,#33119);
#29318=LINE('',#377847,#33120);
#29319=LINE('',#377855,#33121);
#29320=LINE('',#377859,#33122);
#29321=LINE('',#377867,#33123);
#29322=LINE('',#377871,#33124);
#29323=LINE('',#377879,#33125);
#29324=LINE('',#377883,#33126);
#29325=LINE('',#377891,#33127);
#29326=LINE('',#377895,#33128);
#29327=LINE('',#377903,#33129);
#29328=LINE('',#377907,#33130);
#29329=LINE('',#377915,#33131);
#29330=LINE('',#377919,#33132);
#29331=LINE('',#377927,#33133);
#29332=LINE('',#377931,#33134);
#29333=LINE('',#377939,#33135);
#29334=LINE('',#377943,#33136);
#29335=LINE('',#377951,#33137);
#29336=LINE('',#377955,#33138);
#29337=LINE('',#377962,#33139);
#29338=LINE('',#378257,#33140);
#29339=LINE('',#378309,#33141);
#29340=LINE('',#378327,#33142);
#29341=LINE('',#378337,#33143);
#29342=LINE('',#378347,#33144);
#29343=LINE('',#378348,#33145);
#29344=LINE('',#378351,#33146);
#29345=LINE('',#378352,#33147);
#29346=LINE('',#378355,#33148);
#29347=LINE('',#378356,#33149);
#29348=LINE('',#378359,#33150);
#29349=LINE('',#378360,#33151);
#29350=LINE('',#378363,#33152);
#29351=LINE('',#378364,#33153);
#29352=LINE('',#378379,#33154);
#29353=LINE('',#378383,#33155);
#29354=LINE('',#378385,#33156);
#29355=LINE('',#378387,#33157);
#29356=LINE('',#378393,#33158);
#29357=LINE('',#378397,#33159);
#29358=LINE('',#378399,#33160);
#29359=LINE('',#378403,#33161);
#29360=LINE('',#380137,#33162);
#29361=LINE('',#380146,#33163);
#29362=LINE('',#380164,#33164);
#29363=LINE('',#380173,#33165);
#29364=LINE('',#380441,#33166);
#29365=LINE('',#380450,#33167);
#29366=LINE('',#380468,#33168);
#29367=LINE('',#380477,#33169);
#29368=LINE('',#380745,#33170);
#29369=LINE('',#380754,#33171);
#29370=LINE('',#380772,#33172);
#29371=LINE('',#380781,#33173);
#29372=LINE('',#381049,#33174);
#29373=LINE('',#381058,#33175);
#29374=LINE('',#381076,#33176);
#29375=LINE('',#381085,#33177);
#29376=LINE('',#381353,#33178);
#29377=LINE('',#381362,#33179);
#29378=LINE('',#381380,#33180);
#29379=LINE('',#381389,#33181);
#29380=LINE('',#381657,#33182);
#29381=LINE('',#381666,#33183);
#29382=LINE('',#381684,#33184);
#29383=LINE('',#381693,#33185);
#29384=LINE('',#381961,#33186);
#29385=LINE('',#381970,#33187);
#29386=LINE('',#381988,#33188);
#29387=LINE('',#381997,#33189);
#29388=LINE('',#382265,#33190);
#29389=LINE('',#382274,#33191);
#29390=LINE('',#382292,#33192);
#29391=LINE('',#382301,#33193);
#29392=LINE('',#382569,#33194);
#29393=LINE('',#382578,#33195);
#29394=LINE('',#382596,#33196);
#29395=LINE('',#382605,#33197);
#29396=LINE('',#382873,#33198);
#29397=LINE('',#382882,#33199);
#29398=LINE('',#382900,#33200);
#29399=LINE('',#382909,#33201);
#29400=LINE('',#383177,#33202);
#29401=LINE('',#383186,#33203);
#29402=LINE('',#383204,#33204);
#29403=LINE('',#383213,#33205);
#29404=LINE('',#383481,#33206);
#29405=LINE('',#383490,#33207);
#29406=LINE('',#383508,#33208);
#29407=LINE('',#383517,#33209);
#29408=LINE('',#383785,#33210);
#29409=LINE('',#383794,#33211);
#29410=LINE('',#383812,#33212);
#29411=LINE('',#383821,#33213);
#29412=LINE('',#384089,#33214);
#29413=LINE('',#384098,#33215);
#29414=LINE('',#384116,#33216);
#29415=LINE('',#384125,#33217);
#29416=LINE('',#384393,#33218);
#29417=LINE('',#384402,#33219);
#29418=LINE('',#384420,#33220);
#29419=LINE('',#384429,#33221);
#29420=LINE('',#384697,#33222);
#29421=LINE('',#384706,#33223);
#29422=LINE('',#384724,#33224);
#29423=LINE('',#384733,#33225);
#29424=LINE('',#385001,#33226);
#29425=LINE('',#385010,#33227);
#29426=LINE('',#385028,#33228);
#29427=LINE('',#385037,#33229);
#29428=LINE('',#385305,#33230);
#29429=LINE('',#385314,#33231);
#29430=LINE('',#385332,#33232);
#29431=LINE('',#385341,#33233);
#29432=LINE('',#385609,#33234);
#29433=LINE('',#385618,#33235);
#29434=LINE('',#385636,#33236);
#29435=LINE('',#385645,#33237);
#29436=LINE('',#385913,#33238);
#29437=LINE('',#385922,#33239);
#29438=LINE('',#385940,#33240);
#29439=LINE('',#385949,#33241);
#29440=LINE('',#386217,#33242);
#29441=LINE('',#386226,#33243);
#29442=LINE('',#386244,#33244);
#29443=LINE('',#386253,#33245);
#29444=LINE('',#386521,#33246);
#29445=LINE('',#386530,#33247);
#29446=LINE('',#386548,#33248);
#29447=LINE('',#386557,#33249);
#29448=LINE('',#386825,#33250);
#29449=LINE('',#386834,#33251);
#29450=LINE('',#386852,#33252);
#29451=LINE('',#386861,#33253);
#29452=LINE('',#387129,#33254);
#29453=LINE('',#387138,#33255);
#29454=LINE('',#387156,#33256);
#29455=LINE('',#387165,#33257);
#29456=LINE('',#387433,#33258);
#29457=LINE('',#387442,#33259);
#29458=LINE('',#387460,#33260);
#29459=LINE('',#387469,#33261);
#29460=LINE('',#387737,#33262);
#29461=LINE('',#387746,#33263);
#29462=LINE('',#387764,#33264);
#29463=LINE('',#387773,#33265);
#29464=LINE('',#388041,#33266);
#29465=LINE('',#388050,#33267);
#29466=LINE('',#388068,#33268);
#29467=LINE('',#388077,#33269);
#29468=LINE('',#388345,#33270);
#29469=LINE('',#388354,#33271);
#29470=LINE('',#388372,#33272);
#29471=LINE('',#388381,#33273);
#29472=LINE('',#388649,#33274);
#29473=LINE('',#388658,#33275);
#29474=LINE('',#388676,#33276);
#29475=LINE('',#388685,#33277);
#29476=LINE('',#388953,#33278);
#29477=LINE('',#388962,#33279);
#29478=LINE('',#388980,#33280);
#29479=LINE('',#388989,#33281);
#29480=LINE('',#389257,#33282);
#29481=LINE('',#389266,#33283);
#29482=LINE('',#389284,#33284);
#29483=LINE('',#389293,#33285);
#29484=LINE('',#389561,#33286);
#29485=LINE('',#389570,#33287);
#29486=LINE('',#389588,#33288);
#29487=LINE('',#389597,#33289);
#29488=LINE('',#389865,#33290);
#29489=LINE('',#389874,#33291);
#29490=LINE('',#389892,#33292);
#29491=LINE('',#389901,#33293);
#29492=LINE('',#390169,#33294);
#29493=LINE('',#390178,#33295);
#29494=LINE('',#390196,#33296);
#29495=LINE('',#390205,#33297);
#29496=LINE('',#390473,#33298);
#29497=LINE('',#390482,#33299);
#29498=LINE('',#390500,#33300);
#29499=LINE('',#390509,#33301);
#29500=LINE('',#390777,#33302);
#29501=LINE('',#390786,#33303);
#29502=LINE('',#390804,#33304);
#29503=LINE('',#390813,#33305);
#29504=LINE('',#391081,#33306);
#29505=LINE('',#391090,#33307);
#29506=LINE('',#391108,#33308);
#29507=LINE('',#391117,#33309);
#29508=LINE('',#391385,#33310);
#29509=LINE('',#391394,#33311);
#29510=LINE('',#391412,#33312);
#29511=LINE('',#391421,#33313);
#29512=LINE('',#391689,#33314);
#29513=LINE('',#391698,#33315);
#29514=LINE('',#391716,#33316);
#29515=LINE('',#391725,#33317);
#29516=LINE('',#391993,#33318);
#29517=LINE('',#392002,#33319);
#29518=LINE('',#392020,#33320);
#29519=LINE('',#392029,#33321);
#29520=LINE('',#392297,#33322);
#29521=LINE('',#392306,#33323);
#29522=LINE('',#392324,#33324);
#29523=LINE('',#392333,#33325);
#29524=LINE('',#392601,#33326);
#29525=LINE('',#392610,#33327);
#29526=LINE('',#392628,#33328);
#29527=LINE('',#392637,#33329);
#29528=LINE('',#392905,#33330);
#29529=LINE('',#392914,#33331);
#29530=LINE('',#392932,#33332);
#29531=LINE('',#392941,#33333);
#29532=LINE('',#393209,#33334);
#29533=LINE('',#393218,#33335);
#29534=LINE('',#393236,#33336);
#29535=LINE('',#393245,#33337);
#29536=LINE('',#393513,#33338);
#29537=LINE('',#393522,#33339);
#29538=LINE('',#393540,#33340);
#29539=LINE('',#393549,#33341);
#29540=LINE('',#393817,#33342);
#29541=LINE('',#393826,#33343);
#29542=LINE('',#393844,#33344);
#29543=LINE('',#393853,#33345);
#29544=LINE('',#394121,#33346);
#29545=LINE('',#394130,#33347);
#29546=LINE('',#394148,#33348);
#29547=LINE('',#394157,#33349);
#29548=LINE('',#394425,#33350);
#29549=LINE('',#394434,#33351);
#29550=LINE('',#394452,#33352);
#29551=LINE('',#394461,#33353);
#29552=LINE('',#394729,#33354);
#29553=LINE('',#394738,#33355);
#29554=LINE('',#394756,#33356);
#29555=LINE('',#394765,#33357);
#29556=LINE('',#395033,#33358);
#29557=LINE('',#395042,#33359);
#29558=LINE('',#395060,#33360);
#29559=LINE('',#395069,#33361);
#29560=LINE('',#395337,#33362);
#29561=LINE('',#395346,#33363);
#29562=LINE('',#395364,#33364);
#29563=LINE('',#395373,#33365);
#29564=LINE('',#395641,#33366);
#29565=LINE('',#395650,#33367);
#29566=LINE('',#395668,#33368);
#29567=LINE('',#395677,#33369);
#29568=LINE('',#395945,#33370);
#29569=LINE('',#395954,#33371);
#29570=LINE('',#395972,#33372);
#29571=LINE('',#395981,#33373);
#29572=LINE('',#396249,#33374);
#29573=LINE('',#396258,#33375);
#29574=LINE('',#396276,#33376);
#29575=LINE('',#396285,#33377);
#29576=LINE('',#396553,#33378);
#29577=LINE('',#396562,#33379);
#29578=LINE('',#396580,#33380);
#29579=LINE('',#396589,#33381);
#29580=LINE('',#396857,#33382);
#29581=LINE('',#396866,#33383);
#29582=LINE('',#396884,#33384);
#29583=LINE('',#396893,#33385);
#29584=LINE('',#397161,#33386);
#29585=LINE('',#397170,#33387);
#29586=LINE('',#397188,#33388);
#29587=LINE('',#397197,#33389);
#29588=LINE('',#397465,#33390);
#29589=LINE('',#397474,#33391);
#29590=LINE('',#397492,#33392);
#29591=LINE('',#397501,#33393);
#29592=LINE('',#397769,#33394);
#29593=LINE('',#397778,#33395);
#29594=LINE('',#397796,#33396);
#29595=LINE('',#397805,#33397);
#29596=LINE('',#398073,#33398);
#29597=LINE('',#398082,#33399);
#29598=LINE('',#398100,#33400);
#29599=LINE('',#398109,#33401);
#29600=LINE('',#398377,#33402);
#29601=LINE('',#398386,#33403);
#29602=LINE('',#398404,#33404);
#29603=LINE('',#398413,#33405);
#29604=LINE('',#398681,#33406);
#29605=LINE('',#398690,#33407);
#29606=LINE('',#398708,#33408);
#29607=LINE('',#398717,#33409);
#29608=LINE('',#398985,#33410);
#29609=LINE('',#398994,#33411);
#29610=LINE('',#399012,#33412);
#29611=LINE('',#399021,#33413);
#29612=LINE('',#399289,#33414);
#29613=LINE('',#399298,#33415);
#29614=LINE('',#399316,#33416);
#29615=LINE('',#399325,#33417);
#29616=LINE('',#399593,#33418);
#29617=LINE('',#399602,#33419);
#29618=LINE('',#399620,#33420);
#29619=LINE('',#399629,#33421);
#29620=LINE('',#399897,#33422);
#29621=LINE('',#399906,#33423);
#29622=LINE('',#399924,#33424);
#29623=LINE('',#399933,#33425);
#29624=LINE('',#400201,#33426);
#29625=LINE('',#400210,#33427);
#29626=LINE('',#400228,#33428);
#29627=LINE('',#400237,#33429);
#29628=LINE('',#400505,#33430);
#29629=LINE('',#400514,#33431);
#29630=LINE('',#400532,#33432);
#29631=LINE('',#400541,#33433);
#29632=LINE('',#400809,#33434);
#29633=LINE('',#400818,#33435);
#29634=LINE('',#400836,#33436);
#29635=LINE('',#400845,#33437);
#29636=LINE('',#401113,#33438);
#29637=LINE('',#401122,#33439);
#29638=LINE('',#401140,#33440);
#29639=LINE('',#401149,#33441);
#29640=LINE('',#401417,#33442);
#29641=LINE('',#401426,#33443);
#29642=LINE('',#401444,#33444);
#29643=LINE('',#401453,#33445);
#29644=LINE('',#401721,#33446);
#29645=LINE('',#401730,#33447);
#29646=LINE('',#401748,#33448);
#29647=LINE('',#401757,#33449);
#29648=LINE('',#402025,#33450);
#29649=LINE('',#402034,#33451);
#29650=LINE('',#402052,#33452);
#29651=LINE('',#402061,#33453);
#29652=LINE('',#402329,#33454);
#29653=LINE('',#402338,#33455);
#29654=LINE('',#402356,#33456);
#29655=LINE('',#402365,#33457);
#29656=LINE('',#402633,#33458);
#29657=LINE('',#402642,#33459);
#29658=LINE('',#402660,#33460);
#29659=LINE('',#402669,#33461);
#29660=LINE('',#402937,#33462);
#29661=LINE('',#402946,#33463);
#29662=LINE('',#402964,#33464);
#29663=LINE('',#402973,#33465);
#29664=LINE('',#403241,#33466);
#29665=LINE('',#403250,#33467);
#29666=LINE('',#403268,#33468);
#29667=LINE('',#403277,#33469);
#29668=LINE('',#403545,#33470);
#29669=LINE('',#403554,#33471);
#29670=LINE('',#403572,#33472);
#29671=LINE('',#403581,#33473);
#29672=LINE('',#403849,#33474);
#29673=LINE('',#403858,#33475);
#29674=LINE('',#403876,#33476);
#29675=LINE('',#403885,#33477);
#29676=LINE('',#404153,#33478);
#29677=LINE('',#404162,#33479);
#29678=LINE('',#404180,#33480);
#29679=LINE('',#404189,#33481);
#29680=LINE('',#404457,#33482);
#29681=LINE('',#404466,#33483);
#29682=LINE('',#404484,#33484);
#29683=LINE('',#404493,#33485);
#29684=LINE('',#404761,#33486);
#29685=LINE('',#404770,#33487);
#29686=LINE('',#404788,#33488);
#29687=LINE('',#404797,#33489);
#29688=LINE('',#405065,#33490);
#29689=LINE('',#405074,#33491);
#29690=LINE('',#405092,#33492);
#29691=LINE('',#405101,#33493);
#29692=LINE('',#405369,#33494);
#29693=LINE('',#405378,#33495);
#29694=LINE('',#405396,#33496);
#29695=LINE('',#405405,#33497);
#29696=LINE('',#405673,#33498);
#29697=LINE('',#405682,#33499);
#29698=LINE('',#405700,#33500);
#29699=LINE('',#405709,#33501);
#29700=LINE('',#405977,#33502);
#29701=LINE('',#405986,#33503);
#29702=LINE('',#406004,#33504);
#29703=LINE('',#406013,#33505);
#29704=LINE('',#406281,#33506);
#29705=LINE('',#406290,#33507);
#29706=LINE('',#406308,#33508);
#29707=LINE('',#406317,#33509);
#29708=LINE('',#406585,#33510);
#29709=LINE('',#406594,#33511);
#29710=LINE('',#406612,#33512);
#29711=LINE('',#406621,#33513);
#29712=LINE('',#406889,#33514);
#29713=LINE('',#406898,#33515);
#29714=LINE('',#406916,#33516);
#29715=LINE('',#406925,#33517);
#29716=LINE('',#407193,#33518);
#29717=LINE('',#407202,#33519);
#29718=LINE('',#407220,#33520);
#29719=LINE('',#407229,#33521);
#29720=LINE('',#407497,#33522);
#29721=LINE('',#407506,#33523);
#29722=LINE('',#407524,#33524);
#29723=LINE('',#407533,#33525);
#29724=LINE('',#407801,#33526);
#29725=LINE('',#407810,#33527);
#29726=LINE('',#407828,#33528);
#29727=LINE('',#407837,#33529);
#29728=LINE('',#408105,#33530);
#29729=LINE('',#408114,#33531);
#29730=LINE('',#408132,#33532);
#29731=LINE('',#408141,#33533);
#29732=LINE('',#408409,#33534);
#29733=LINE('',#408418,#33535);
#29734=LINE('',#408436,#33536);
#29735=LINE('',#408445,#33537);
#29736=LINE('',#408713,#33538);
#29737=LINE('',#408722,#33539);
#29738=LINE('',#408740,#33540);
#29739=LINE('',#408749,#33541);
#29740=LINE('',#409017,#33542);
#29741=LINE('',#409026,#33543);
#29742=LINE('',#409044,#33544);
#29743=LINE('',#409053,#33545);
#29744=LINE('',#409321,#33546);
#29745=LINE('',#409330,#33547);
#29746=LINE('',#409348,#33548);
#29747=LINE('',#409357,#33549);
#32880=VECTOR('',#116572,1.17524047358083);
#32881=VECTOR('',#116577,1.17524047358083);
#32882=VECTOR('',#116580,1.17524047358083);
#32883=VECTOR('',#116583,1.17524047358083);
#32884=VECTOR('',#116586,1.17524047358083);
#32885=VECTOR('',#116589,1.17524047358083);
#32886=VECTOR('',#116592,1.17524047358083);
#32887=VECTOR('',#116595,1.17524047358083);
#32888=VECTOR('',#116598,1.17524047358083);
#32889=VECTOR('',#116601,1.17524047358083);
#32890=VECTOR('',#116604,1.17524047358083);
#32891=VECTOR('',#116607,1.17524047358083);
#32892=VECTOR('',#116610,1.17524047358083);
#32893=VECTOR('',#116613,1.17524047358083);
#32894=VECTOR('',#116616,1.17524047358083);
#32895=VECTOR('',#116619,1.17524047358083);
#32896=VECTOR('',#116622,1.17524047358083);
#32897=VECTOR('',#116625,1.17524047358083);
#32898=VECTOR('',#116628,1.17524047358083);
#32899=VECTOR('',#116631,1.17524047358083);
#32900=VECTOR('',#116634,1.17524047358083);
#32901=VECTOR('',#116637,1.17524047358083);
#32902=VECTOR('',#116640,1.17524047358083);
#32903=VECTOR('',#116643,1.17524047358083);
#32904=VECTOR('',#116646,1.17524047358083);
#32905=VECTOR('',#116649,1.17524047358083);
#32906=VECTOR('',#116652,1.17524047358083);
#32907=VECTOR('',#116655,1.17524047358083);
#32908=VECTOR('',#116658,1.17524047358083);
#32909=VECTOR('',#116661,1.5);
#32910=VECTOR('',#116664,1.5);
#32911=VECTOR('',#116671,1.5);
#32912=VECTOR('',#116674,1.5);
#32913=VECTOR('',#116677,1.5);
#32914=VECTOR('',#116680,1.5);
#32915=VECTOR('',#116683,1.5);
#32916=VECTOR('',#116686,1.5);
#32917=VECTOR('',#116689,1.5);
#32918=VECTOR('',#116692,1.5);
#32919=VECTOR('',#116695,1.5);
#32920=VECTOR('',#116698,1.5);
#32921=VECTOR('',#116701,1.5);
#32922=VECTOR('',#116704,1.5);
#32923=VECTOR('',#116707,1.5);
#32924=VECTOR('',#116710,1.5);
#32925=VECTOR('',#116713,1.5);
#32926=VECTOR('',#116716,1.5);
#32927=VECTOR('',#116719,1.5);
#32928=VECTOR('',#116722,1.5);
#32929=VECTOR('',#116725,1.5);
#32930=VECTOR('',#116728,1.5);
#32931=VECTOR('',#116731,1.5);
#32932=VECTOR('',#116734,1.5);
#32933=VECTOR('',#116737,1.5);
#32934=VECTOR('',#116740,1.5);
#32935=VECTOR('',#116743,1.5);
#32936=VECTOR('',#116746,1.5);
#32937=VECTOR('',#116749,1.5);
#32938=VECTOR('',#116752,999.999999999989);
#32939=VECTOR('',#116757,1.17524047358083);
#32940=VECTOR('',#116778,1.25);
#32941=VECTOR('',#116807,2.54610912703474);
#32942=VECTOR('',#117014,2.73389087296526);
#32943=VECTOR('',#117225,1000.);
#32944=VECTOR('',#117232,1000.);
#32945=VECTOR('',#117235,1000.);
#32946=VECTOR('',#117242,1000.);
#32947=VECTOR('',#117245,1000.);
#32948=VECTOR('',#117252,1000.);
#32949=VECTOR('',#117255,1000.);
#32950=VECTOR('',#117262,1000.);
#32951=VECTOR('',#117265,1000.);
#32952=VECTOR('',#117272,1000.);
#32953=VECTOR('',#117275,1000.);
#32954=VECTOR('',#117282,1000.);
#32955=VECTOR('',#117285,1000.);
#32956=VECTOR('',#117292,1000.);
#32957=VECTOR('',#117295,1000.);
#32958=VECTOR('',#117302,1000.);
#32959=VECTOR('',#117305,1000.);
#32960=VECTOR('',#117312,1000.);
#32961=VECTOR('',#117315,1000.);
#32962=VECTOR('',#117322,1000.);
#32963=VECTOR('',#117325,1000.);
#32964=VECTOR('',#117332,1000.);
#32965=VECTOR('',#117335,1000.);
#32966=VECTOR('',#117342,1000.);
#32967=VECTOR('',#117345,1000.);
#32968=VECTOR('',#117352,1000.);
#32969=VECTOR('',#117355,1000.);
#32970=VECTOR('',#117362,1000.);
#32971=VECTOR('',#117365,1000.);
#32972=VECTOR('',#117372,1000.);
#32973=VECTOR('',#117375,1000.);
#32974=VECTOR('',#117382,1000.);
#32975=VECTOR('',#117385,1000.);
#32976=VECTOR('',#117392,1000.);
#32977=VECTOR('',#117395,1000.);
#32978=VECTOR('',#117402,1000.);
#32979=VECTOR('',#117405,1000.);
#32980=VECTOR('',#117412,1000.);
#32981=VECTOR('',#117415,1000.);
#32982=VECTOR('',#117422,1000.);
#32983=VECTOR('',#117425,1000.);
#32984=VECTOR('',#117432,1000.);
#32985=VECTOR('',#117435,1000.);
#32986=VECTOR('',#117442,1000.);
#32987=VECTOR('',#117445,1000.);
#32988=VECTOR('',#117452,1000.);
#32989=VECTOR('',#117455,1000.);
#32990=VECTOR('',#117462,1000.);
#32991=VECTOR('',#117465,1000.);
#32992=VECTOR('',#117472,1000.);
#32993=VECTOR('',#117475,1000.);
#32994=VECTOR('',#117482,1000.);
#32995=VECTOR('',#117485,1000.);
#32996=VECTOR('',#117492,1000.);
#32997=VECTOR('',#117495,1000.);
#32998=VECTOR('',#117502,1000.);
#32999=VECTOR('',#117505,1000.);
#33000=VECTOR('',#117512,1000.);
#33001=VECTOR('',#117515,1000.);
#33002=VECTOR('',#117522,1000.);
#33003=VECTOR('',#117525,1000.);
#33004=VECTOR('',#117532,1000.);
#33005=VECTOR('',#117535,1000.);
#33006=VECTOR('',#117542,1000.);
#33007=VECTOR('',#117545,1000.);
#33008=VECTOR('',#117552,1000.);
#33009=VECTOR('',#117555,1000.);
#33010=VECTOR('',#117562,1000.);
#33011=VECTOR('',#117565,1000.);
#33012=VECTOR('',#117572,1000.);
#33013=VECTOR('',#117575,1000.);
#33014=VECTOR('',#117582,1000.);
#33015=VECTOR('',#117585,1000.);
#33016=VECTOR('',#117592,1000.);
#33017=VECTOR('',#117595,1000.);
#33018=VECTOR('',#117602,1000.);
#33019=VECTOR('',#117605,1000.);
#33020=VECTOR('',#117612,1000.);
#33021=VECTOR('',#117615,1000.);
#33022=VECTOR('',#117622,1000.);
#33023=VECTOR('',#117625,1000.);
#33024=VECTOR('',#117632,1000.);
#33025=VECTOR('',#117635,1000.);
#33026=VECTOR('',#117642,1000.);
#33027=VECTOR('',#117645,1000.);
#33028=VECTOR('',#117652,1000.);
#33029=VECTOR('',#117655,1000.);
#33030=VECTOR('',#117662,1000.);
#33031=VECTOR('',#117665,1000.);
#33032=VECTOR('',#117672,1000.);
#33033=VECTOR('',#117675,1000.);
#33034=VECTOR('',#117682,1000.);
#33035=VECTOR('',#117685,1000.);
#33036=VECTOR('',#117692,1000.);
#33037=VECTOR('',#117695,1000.);
#33038=VECTOR('',#117702,1000.);
#33039=VECTOR('',#117705,1000.);
#33040=VECTOR('',#117712,1000.);
#33041=VECTOR('',#117715,2.75);
#33042=VECTOR('',#117718,1000.);
#33043=VECTOR('',#117725,1000.);
#33044=VECTOR('',#117728,1000.);
#33045=VECTOR('',#117735,1000.);
#33046=VECTOR('',#117738,1000.);
#33047=VECTOR('',#117745,1000.);
#33048=VECTOR('',#117748,1000.);
#33049=VECTOR('',#117755,1000.);
#33050=VECTOR('',#117758,1000.);
#33051=VECTOR('',#117765,1000.);
#33052=VECTOR('',#117768,1000.);
#33053=VECTOR('',#117775,1000.);
#33054=VECTOR('',#117778,1000.);
#33055=VECTOR('',#117785,1000.);
#33056=VECTOR('',#117788,1000.);
#33057=VECTOR('',#117795,1000.);
#33058=VECTOR('',#117798,1000.);
#33059=VECTOR('',#117805,1000.);
#33060=VECTOR('',#117808,1000.);
#33061=VECTOR('',#117815,1000.);
#33062=VECTOR('',#117818,1000.);
#33063=VECTOR('',#117825,1000.);
#33064=VECTOR('',#117828,1000.);
#33065=VECTOR('',#117835,1000.);
#33066=VECTOR('',#117838,1000.);
#33067=VECTOR('',#117845,1000.);
#33068=VECTOR('',#117848,1000.);
#33069=VECTOR('',#117855,1000.);
#33070=VECTOR('',#117858,1000.);
#33071=VECTOR('',#117865,1000.);
#33072=VECTOR('',#117868,1000.);
#33073=VECTOR('',#117875,1000.);
#33074=VECTOR('',#117878,1000.);
#33075=VECTOR('',#117885,1000.);
#33076=VECTOR('',#117888,1000.);
#33077=VECTOR('',#117895,1000.);
#33078=VECTOR('',#117898,1000.);
#33079=VECTOR('',#117905,1000.);
#33080=VECTOR('',#117908,1000.);
#33081=VECTOR('',#117915,1000.);
#33082=VECTOR('',#117918,1000.);
#33083=VECTOR('',#117925,1000.);
#33084=VECTOR('',#117928,1000.);
#33085=VECTOR('',#117935,1000.);
#33086=VECTOR('',#117938,1000.);
#33087=VECTOR('',#117945,1000.);
#33088=VECTOR('',#117948,1000.);
#33089=VECTOR('',#117955,1000.);
#33090=VECTOR('',#117958,1000.);
#33091=VECTOR('',#117965,1000.);
#33092=VECTOR('',#117968,1000.);
#33093=VECTOR('',#117975,1000.);
#33094=VECTOR('',#117978,1000.);
#33095=VECTOR('',#117985,1000.);
#33096=VECTOR('',#117988,1000.);
#33097=VECTOR('',#117995,1000.);
#33098=VECTOR('',#117998,1000.);
#33099=VECTOR('',#118005,1000.);
#33100=VECTOR('',#118008,1000.);
#33101=VECTOR('',#118015,1000.);
#33102=VECTOR('',#118018,1000.);
#33103=VECTOR('',#118025,1000.);
#33104=VECTOR('',#118028,1000.);
#33105=VECTOR('',#118035,1000.);
#33106=VECTOR('',#118038,1000.);
#33107=VECTOR('',#118045,1000.);
#33108=VECTOR('',#118048,1000.);
#33109=VECTOR('',#118055,1000.);
#33110=VECTOR('',#118058,1000.);
#33111=VECTOR('',#118065,1000.);
#33112=VECTOR('',#118068,1000.);
#33113=VECTOR('',#118075,1000.);
#33114=VECTOR('',#118078,1000.);
#33115=VECTOR('',#118085,1000.);
#33116=VECTOR('',#118088,1000.);
#33117=VECTOR('',#118095,1000.);
#33118=VECTOR('',#118098,1000.);
#33119=VECTOR('',#118105,1000.);
#33120=VECTOR('',#118108,1000.);
#33121=VECTOR('',#118115,1000.);
#33122=VECTOR('',#118118,1000.);
#33123=VECTOR('',#118125,1000.);
#33124=VECTOR('',#118128,1000.);
#33125=VECTOR('',#118135,1000.);
#33126=VECTOR('',#118138,1000.);
#33127=VECTOR('',#118145,1000.);
#33128=VECTOR('',#118148,1000.);
#33129=VECTOR('',#118155,1000.);
#33130=VECTOR('',#118158,1000.);
#33131=VECTOR('',#118165,1000.);
#33132=VECTOR('',#118168,1000.);
#33133=VECTOR('',#118175,1000.);
#33134=VECTOR('',#118178,1000.);
#33135=VECTOR('',#118185,1000.);
#33136=VECTOR('',#118188,1000.);
#33137=VECTOR('',#118195,1000.);
#33138=VECTOR('',#118198,1000.);
#33139=VECTOR('',#118205,1000.);
#33140=VECTOR('',#118790,1000.);
#33141=VECTOR('',#118791,1000.);
#33142=VECTOR('',#118798,1000.);
#33143=VECTOR('',#118803,1000.);
#33144=VECTOR('',#118806,1000.);
#33145=VECTOR('',#118807,1000.);
#33146=VECTOR('',#118810,1000.);
#33147=VECTOR('',#118811,1000.);
#33148=VECTOR('',#118814,1000.);
#33149=VECTOR('',#118815,1000.);
#33150=VECTOR('',#118818,1000.);
#33151=VECTOR('',#118819,1000.);
#33152=VECTOR('',#118822,1000.);
#33153=VECTOR('',#118823,1000.);
#33154=VECTOR('',#118844,1000.);
#33155=VECTOR('',#118845,1000.);
#33156=VECTOR('',#118848,1000.);
#33157=VECTOR('',#118851,1000.);
#33158=VECTOR('',#118854,1000.);
#33159=VECTOR('',#118855,1000.);
#33160=VECTOR('',#118858,1000.);
#33161=VECTOR('',#118859,1000.);
#33162=VECTOR('',#118916,1000.);
#33163=VECTOR('',#118919,1000.);
#33164=VECTOR('',#118924,1000.);
#33165=VECTOR('',#118925,1000.);
#33166=VECTOR('',#118966,1000.);
#33167=VECTOR('',#118969,1000.);
#33168=VECTOR('',#118974,1000.);
#33169=VECTOR('',#118975,1000.);
#33170=VECTOR('',#119016,1000.);
#33171=VECTOR('',#119019,1000.);
#33172=VECTOR('',#119024,1000.);
#33173=VECTOR('',#119025,1000.);
#33174=VECTOR('',#119066,1000.);
#33175=VECTOR('',#119069,1000.);
#33176=VECTOR('',#119074,1000.);
#33177=VECTOR('',#119075,1000.);
#33178=VECTOR('',#119116,1000.);
#33179=VECTOR('',#119119,1000.);
#33180=VECTOR('',#119124,1000.);
#33181=VECTOR('',#119125,1000.);
#33182=VECTOR('',#119166,1000.);
#33183=VECTOR('',#119169,1000.);
#33184=VECTOR('',#119174,1000.);
#33185=VECTOR('',#119175,1000.);
#33186=VECTOR('',#119216,1000.);
#33187=VECTOR('',#119219,1000.);
#33188=VECTOR('',#119224,1000.);
#33189=VECTOR('',#119225,1000.);
#33190=VECTOR('',#119266,1000.);
#33191=VECTOR('',#119269,1000.);
#33192=VECTOR('',#119274,1000.);
#33193=VECTOR('',#119275,1000.);
#33194=VECTOR('',#119316,1000.);
#33195=VECTOR('',#119319,1000.);
#33196=VECTOR('',#119324,1000.);
#33197=VECTOR('',#119325,1000.);
#33198=VECTOR('',#119366,1000.);
#33199=VECTOR('',#119369,1000.);
#33200=VECTOR('',#119374,1000.);
#33201=VECTOR('',#119375,1000.);
#33202=VECTOR('',#119416,1000.);
#33203=VECTOR('',#119419,1000.);
#33204=VECTOR('',#119424,1000.);
#33205=VECTOR('',#119425,1000.);
#33206=VECTOR('',#119466,1000.);
#33207=VECTOR('',#119469,1000.);
#33208=VECTOR('',#119474,1000.);
#33209=VECTOR('',#119475,1000.);
#33210=VECTOR('',#119516,1000.);
#33211=VECTOR('',#119519,1000.);
#33212=VECTOR('',#119524,1000.);
#33213=VECTOR('',#119525,1000.);
#33214=VECTOR('',#119566,1000.);
#33215=VECTOR('',#119569,1000.);
#33216=VECTOR('',#119574,1000.);
#33217=VECTOR('',#119575,1000.);
#33218=VECTOR('',#119616,1000.);
#33219=VECTOR('',#119619,1000.);
#33220=VECTOR('',#119624,1000.);
#33221=VECTOR('',#119625,1000.);
#33222=VECTOR('',#119666,1000.);
#33223=VECTOR('',#119669,1000.);
#33224=VECTOR('',#119674,1000.);
#33225=VECTOR('',#119675,1000.);
#33226=VECTOR('',#119716,1000.);
#33227=VECTOR('',#119719,1000.);
#33228=VECTOR('',#119724,1000.);
#33229=VECTOR('',#119725,1000.);
#33230=VECTOR('',#119766,1000.);
#33231=VECTOR('',#119769,1000.);
#33232=VECTOR('',#119774,1000.);
#33233=VECTOR('',#119775,1000.);
#33234=VECTOR('',#119816,1000.);
#33235=VECTOR('',#119819,1000.);
#33236=VECTOR('',#119824,1000.);
#33237=VECTOR('',#119825,1000.);
#33238=VECTOR('',#119866,1000.);
#33239=VECTOR('',#119869,1000.);
#33240=VECTOR('',#119874,1000.);
#33241=VECTOR('',#119875,1000.);
#33242=VECTOR('',#119916,1000.);
#33243=VECTOR('',#119919,1000.);
#33244=VECTOR('',#119924,1000.);
#33245=VECTOR('',#119925,1000.);
#33246=VECTOR('',#119966,1000.);
#33247=VECTOR('',#119969,1000.);
#33248=VECTOR('',#119974,1000.);
#33249=VECTOR('',#119975,1000.);
#33250=VECTOR('',#120016,1000.);
#33251=VECTOR('',#120019,1000.);
#33252=VECTOR('',#120024,1000.);
#33253=VECTOR('',#120025,1000.);
#33254=VECTOR('',#120066,1000.);
#33255=VECTOR('',#120069,1000.);
#33256=VECTOR('',#120074,1000.);
#33257=VECTOR('',#120075,1000.);
#33258=VECTOR('',#120116,1000.);
#33259=VECTOR('',#120119,1000.);
#33260=VECTOR('',#120124,1000.);
#33261=VECTOR('',#120125,1000.);
#33262=VECTOR('',#120166,1000.);
#33263=VECTOR('',#120169,1000.);
#33264=VECTOR('',#120174,1000.);
#33265=VECTOR('',#120175,1000.);
#33266=VECTOR('',#120216,1000.);
#33267=VECTOR('',#120219,1000.);
#33268=VECTOR('',#120224,1000.);
#33269=VECTOR('',#120225,1000.);
#33270=VECTOR('',#120266,1000.);
#33271=VECTOR('',#120269,1000.);
#33272=VECTOR('',#120274,1000.);
#33273=VECTOR('',#120275,1000.);
#33274=VECTOR('',#120316,1000.);
#33275=VECTOR('',#120319,1000.);
#33276=VECTOR('',#120324,1000.);
#33277=VECTOR('',#120325,1000.);
#33278=VECTOR('',#120366,1000.);
#33279=VECTOR('',#120369,1000.);
#33280=VECTOR('',#120374,1000.);
#33281=VECTOR('',#120375,1000.);
#33282=VECTOR('',#120416,1000.);
#33283=VECTOR('',#120419,1000.);
#33284=VECTOR('',#120424,1000.);
#33285=VECTOR('',#120425,1000.);
#33286=VECTOR('',#120466,1000.);
#33287=VECTOR('',#120469,1000.);
#33288=VECTOR('',#120474,1000.);
#33289=VECTOR('',#120475,1000.);
#33290=VECTOR('',#120516,1000.);
#33291=VECTOR('',#120519,1000.);
#33292=VECTOR('',#120524,1000.);
#33293=VECTOR('',#120525,1000.);
#33294=VECTOR('',#120566,1000.);
#33295=VECTOR('',#120569,1000.);
#33296=VECTOR('',#120574,1000.);
#33297=VECTOR('',#120575,1000.);
#33298=VECTOR('',#120616,1000.);
#33299=VECTOR('',#120619,1000.);
#33300=VECTOR('',#120624,1000.);
#33301=VECTOR('',#120625,1000.);
#33302=VECTOR('',#120666,1000.);
#33303=VECTOR('',#120669,1000.);
#33304=VECTOR('',#120674,1000.);
#33305=VECTOR('',#120675,1000.);
#33306=VECTOR('',#120716,1000.);
#33307=VECTOR('',#120719,1000.);
#33308=VECTOR('',#120724,1000.);
#33309=VECTOR('',#120725,1000.);
#33310=VECTOR('',#120766,1000.);
#33311=VECTOR('',#120769,1000.);
#33312=VECTOR('',#120774,1000.);
#33313=VECTOR('',#120775,1000.);
#33314=VECTOR('',#120816,1000.);
#33315=VECTOR('',#120819,1000.);
#33316=VECTOR('',#120824,1000.);
#33317=VECTOR('',#120825,1000.);
#33318=VECTOR('',#120866,1000.);
#33319=VECTOR('',#120869,1000.);
#33320=VECTOR('',#120874,1000.);
#33321=VECTOR('',#120875,1000.);
#33322=VECTOR('',#120916,1000.);
#33323=VECTOR('',#120919,1000.);
#33324=VECTOR('',#120924,1000.);
#33325=VECTOR('',#120925,1000.);
#33326=VECTOR('',#120966,1000.);
#33327=VECTOR('',#120969,1000.);
#33328=VECTOR('',#120974,1000.);
#33329=VECTOR('',#120975,1000.);
#33330=VECTOR('',#121016,1000.);
#33331=VECTOR('',#121019,1000.);
#33332=VECTOR('',#121024,1000.);
#33333=VECTOR('',#121025,1000.);
#33334=VECTOR('',#121066,1000.);
#33335=VECTOR('',#121069,1000.);
#33336=VECTOR('',#121074,1000.);
#33337=VECTOR('',#121075,1000.);
#33338=VECTOR('',#121116,1000.);
#33339=VECTOR('',#121119,1000.);
#33340=VECTOR('',#121124,1000.);
#33341=VECTOR('',#121125,1000.);
#33342=VECTOR('',#121166,1000.);
#33343=VECTOR('',#121169,1000.);
#33344=VECTOR('',#121174,1000.);
#33345=VECTOR('',#121175,1000.);
#33346=VECTOR('',#121216,1000.);
#33347=VECTOR('',#121219,1000.);
#33348=VECTOR('',#121224,1000.);
#33349=VECTOR('',#121225,1000.);
#33350=VECTOR('',#121266,1000.);
#33351=VECTOR('',#121269,1000.);
#33352=VECTOR('',#121274,1000.);
#33353=VECTOR('',#121275,1000.);
#33354=VECTOR('',#121316,1000.);
#33355=VECTOR('',#121319,1000.);
#33356=VECTOR('',#121324,1000.);
#33357=VECTOR('',#121325,1000.);
#33358=VECTOR('',#121366,1000.);
#33359=VECTOR('',#121369,1000.);
#33360=VECTOR('',#121374,1000.);
#33361=VECTOR('',#121375,1000.);
#33362=VECTOR('',#121416,1000.);
#33363=VECTOR('',#121419,1000.);
#33364=VECTOR('',#121424,1000.);
#33365=VECTOR('',#121425,1000.);
#33366=VECTOR('',#121466,1000.);
#33367=VECTOR('',#121469,1000.);
#33368=VECTOR('',#121474,1000.);
#33369=VECTOR('',#121475,1000.);
#33370=VECTOR('',#121516,1000.);
#33371=VECTOR('',#121519,1000.);
#33372=VECTOR('',#121524,1000.);
#33373=VECTOR('',#121525,1000.);
#33374=VECTOR('',#121566,1000.);
#33375=VECTOR('',#121569,1000.);
#33376=VECTOR('',#121574,1000.);
#33377=VECTOR('',#121575,1000.);
#33378=VECTOR('',#121616,1000.);
#33379=VECTOR('',#121619,1000.);
#33380=VECTOR('',#121624,1000.);
#33381=VECTOR('',#121625,1000.);
#33382=VECTOR('',#121666,1000.);
#33383=VECTOR('',#121669,1000.);
#33384=VECTOR('',#121674,1000.);
#33385=VECTOR('',#121675,1000.);
#33386=VECTOR('',#121716,1000.);
#33387=VECTOR('',#121719,1000.);
#33388=VECTOR('',#121724,1000.);
#33389=VECTOR('',#121725,1000.);
#33390=VECTOR('',#121766,1000.);
#33391=VECTOR('',#121769,1000.);
#33392=VECTOR('',#121774,1000.);
#33393=VECTOR('',#121775,1000.);
#33394=VECTOR('',#121816,1000.);
#33395=VECTOR('',#121819,1000.);
#33396=VECTOR('',#121824,1000.);
#33397=VECTOR('',#121825,1000.);
#33398=VECTOR('',#121866,1000.);
#33399=VECTOR('',#121869,1000.);
#33400=VECTOR('',#121874,1000.);
#33401=VECTOR('',#121875,1000.);
#33402=VECTOR('',#121916,1000.);
#33403=VECTOR('',#121919,1000.);
#33404=VECTOR('',#121924,1000.);
#33405=VECTOR('',#121925,1000.);
#33406=VECTOR('',#121966,1000.);
#33407=VECTOR('',#121969,1000.);
#33408=VECTOR('',#121974,1000.);
#33409=VECTOR('',#121975,1000.);
#33410=VECTOR('',#122016,1000.);
#33411=VECTOR('',#122019,1000.);
#33412=VECTOR('',#122024,1000.);
#33413=VECTOR('',#122025,1000.);
#33414=VECTOR('',#122066,1000.);
#33415=VECTOR('',#122069,1000.);
#33416=VECTOR('',#122074,1000.);
#33417=VECTOR('',#122075,1000.);
#33418=VECTOR('',#122116,1000.);
#33419=VECTOR('',#122119,1000.);
#33420=VECTOR('',#122124,1000.);
#33421=VECTOR('',#122125,1000.);
#33422=VECTOR('',#122166,1000.);
#33423=VECTOR('',#122169,1000.);
#33424=VECTOR('',#122174,1000.);
#33425=VECTOR('',#122175,1000.);
#33426=VECTOR('',#122216,1000.);
#33427=VECTOR('',#122219,1000.);
#33428=VECTOR('',#122224,1000.);
#33429=VECTOR('',#122225,1000.);
#33430=VECTOR('',#122266,1000.);
#33431=VECTOR('',#122269,1000.);
#33432=VECTOR('',#122274,1000.);
#33433=VECTOR('',#122275,1000.);
#33434=VECTOR('',#122316,1000.);
#33435=VECTOR('',#122319,1000.);
#33436=VECTOR('',#122324,1000.);
#33437=VECTOR('',#122325,1000.);
#33438=VECTOR('',#122366,1000.);
#33439=VECTOR('',#122369,1000.);
#33440=VECTOR('',#122374,1000.);
#33441=VECTOR('',#122375,1000.);
#33442=VECTOR('',#122416,1000.);
#33443=VECTOR('',#122419,1000.);
#33444=VECTOR('',#122424,1000.);
#33445=VECTOR('',#122425,1000.);
#33446=VECTOR('',#122466,1000.);
#33447=VECTOR('',#122469,1000.);
#33448=VECTOR('',#122474,1000.);
#33449=VECTOR('',#122475,1000.);
#33450=VECTOR('',#122516,1000.);
#33451=VECTOR('',#122519,1000.);
#33452=VECTOR('',#122524,1000.);
#33453=VECTOR('',#122525,1000.);
#33454=VECTOR('',#122566,1000.);
#33455=VECTOR('',#122569,1000.);
#33456=VECTOR('',#122574,1000.);
#33457=VECTOR('',#122575,1000.);
#33458=VECTOR('',#122616,1000.);
#33459=VECTOR('',#122619,1000.);
#33460=VECTOR('',#122624,1000.);
#33461=VECTOR('',#122625,1000.);
#33462=VECTOR('',#122666,1000.);
#33463=VECTOR('',#122669,1000.);
#33464=VECTOR('',#122674,1000.);
#33465=VECTOR('',#122675,1000.);
#33466=VECTOR('',#122716,1000.);
#33467=VECTOR('',#122719,1000.);
#33468=VECTOR('',#122724,1000.);
#33469=VECTOR('',#122725,1000.);
#33470=VECTOR('',#122766,1000.);
#33471=VECTOR('',#122769,1000.);
#33472=VECTOR('',#122774,1000.);
#33473=VECTOR('',#122775,1000.);
#33474=VECTOR('',#122816,1000.);
#33475=VECTOR('',#122819,1000.);
#33476=VECTOR('',#122824,1000.);
#33477=VECTOR('',#122825,1000.);
#33478=VECTOR('',#122866,1000.);
#33479=VECTOR('',#122869,1000.);
#33480=VECTOR('',#122874,1000.);
#33481=VECTOR('',#122875,1000.);
#33482=VECTOR('',#122916,1000.);
#33483=VECTOR('',#122919,1000.);
#33484=VECTOR('',#122924,1000.);
#33485=VECTOR('',#122925,1000.);
#33486=VECTOR('',#122966,1000.);
#33487=VECTOR('',#122969,1000.);
#33488=VECTOR('',#122974,1000.);
#33489=VECTOR('',#122975,1000.);
#33490=VECTOR('',#123016,1000.);
#33491=VECTOR('',#123019,1000.);
#33492=VECTOR('',#123024,1000.);
#33493=VECTOR('',#123025,1000.);
#33494=VECTOR('',#123066,1000.);
#33495=VECTOR('',#123069,1000.);
#33496=VECTOR('',#123074,1000.);
#33497=VECTOR('',#123075,1000.);
#33498=VECTOR('',#123116,1000.);
#33499=VECTOR('',#123119,1000.);
#33500=VECTOR('',#123124,1000.);
#33501=VECTOR('',#123125,1000.);
#33502=VECTOR('',#123166,1000.);
#33503=VECTOR('',#123169,1000.);
#33504=VECTOR('',#123174,1000.);
#33505=VECTOR('',#123175,1000.);
#33506=VECTOR('',#123216,1000.);
#33507=VECTOR('',#123219,1000.);
#33508=VECTOR('',#123224,1000.);
#33509=VECTOR('',#123225,1000.);
#33510=VECTOR('',#123266,1000.);
#33511=VECTOR('',#123269,1000.);
#33512=VECTOR('',#123274,1000.);
#33513=VECTOR('',#123275,1000.);
#33514=VECTOR('',#123316,1000.);
#33515=VECTOR('',#123319,1000.);
#33516=VECTOR('',#123324,1000.);
#33517=VECTOR('',#123325,1000.);
#33518=VECTOR('',#123366,1000.);
#33519=VECTOR('',#123369,1000.);
#33520=VECTOR('',#123374,1000.);
#33521=VECTOR('',#123375,1000.);
#33522=VECTOR('',#123416,1000.);
#33523=VECTOR('',#123419,1000.);
#33524=VECTOR('',#123424,1000.);
#33525=VECTOR('',#123425,1000.);
#33526=VECTOR('',#123466,1000.);
#33527=VECTOR('',#123469,1000.);
#33528=VECTOR('',#123474,1000.);
#33529=VECTOR('',#123475,1000.);
#33530=VECTOR('',#123516,1000.);
#33531=VECTOR('',#123519,1000.);
#33532=VECTOR('',#123524,1000.);
#33533=VECTOR('',#123525,1000.);
#33534=VECTOR('',#123566,1000.);
#33535=VECTOR('',#123569,1000.);
#33536=VECTOR('',#123574,1000.);
#33537=VECTOR('',#123575,1000.);
#33538=VECTOR('',#123616,1000.);
#33539=VECTOR('',#123619,1000.);
#33540=VECTOR('',#123624,1000.);
#33541=VECTOR('',#123625,1000.);
#33542=VECTOR('',#123666,1000.);
#33543=VECTOR('',#123669,1000.);
#33544=VECTOR('',#123674,1000.);
#33545=VECTOR('',#123675,1000.);
#33546=VECTOR('',#123716,1000.);
#33547=VECTOR('',#123719,1000.);
#33548=VECTOR('',#123724,1000.);
#33549=VECTOR('',#123725,1000.);
#38516=VERTEX_POINT('',#371609);
#38517=VERTEX_POINT('',#371610);
#38518=VERTEX_POINT('',#371612);
#38519=VERTEX_POINT('',#371618);
#38520=VERTEX_POINT('',#371619);
#38521=VERTEX_POINT('',#371648);
#38522=VERTEX_POINT('',#371649);
#38523=VERTEX_POINT('',#371678);
#38524=VERTEX_POINT('',#371679);
#38525=VERTEX_POINT('',#371708);
#38526=VERTEX_POINT('',#371709);
#38527=VERTEX_POINT('',#371738);
#38528=VERTEX_POINT('',#371739);
#38529=VERTEX_POINT('',#371768);
#38530=VERTEX_POINT('',#371769);
#38531=VERTEX_POINT('',#371798);
#38532=VERTEX_POINT('',#371799);
#38533=VERTEX_POINT('',#371828);
#38534=VERTEX_POINT('',#371829);
#38535=VERTEX_POINT('',#371858);
#38536=VERTEX_POINT('',#371859);
#38537=VERTEX_POINT('',#371888);
#38538=VERTEX_POINT('',#371889);
#38539=VERTEX_POINT('',#371918);
#38540=VERTEX_POINT('',#371919);
#38541=VERTEX_POINT('',#371948);
#38542=VERTEX_POINT('',#371949);
#38543=VERTEX_POINT('',#371978);
#38544=VERTEX_POINT('',#371979);
#38545=VERTEX_POINT('',#372008);
#38546=VERTEX_POINT('',#372009);
#38547=VERTEX_POINT('',#372038);
#38548=VERTEX_POINT('',#372039);
#38549=VERTEX_POINT('',#372068);
#38550=VERTEX_POINT('',#372069);
#38551=VERTEX_POINT('',#372098);
#38552=VERTEX_POINT('',#372099);
#38553=VERTEX_POINT('',#372128);
#38554=VERTEX_POINT('',#372129);
#38555=VERTEX_POINT('',#372158);
#38556=VERTEX_POINT('',#372159);
#38557=VERTEX_POINT('',#372188);
#38558=VERTEX_POINT('',#372189);
#38559=VERTEX_POINT('',#372218);
#38560=VERTEX_POINT('',#372219);
#38561=VERTEX_POINT('',#372248);
#38562=VERTEX_POINT('',#372249);
#38563=VERTEX_POINT('',#372278);
#38564=VERTEX_POINT('',#372279);
#38565=VERTEX_POINT('',#372308);
#38566=VERTEX_POINT('',#372309);
#38567=VERTEX_POINT('',#372338);
#38568=VERTEX_POINT('',#372339);
#38569=VERTEX_POINT('',#372368);
#38570=VERTEX_POINT('',#372369);
#38571=VERTEX_POINT('',#372398);
#38572=VERTEX_POINT('',#372399);
#38573=VERTEX_POINT('',#372428);
#38574=VERTEX_POINT('',#372429);
#38575=VERTEX_POINT('',#372458);
#38576=VERTEX_POINT('',#372459);
#38577=VERTEX_POINT('',#372461);
#38578=VERTEX_POINT('',#372482);
#38579=VERTEX_POINT('',#372484);
#38580=VERTEX_POINT('',#372487);
#38581=VERTEX_POINT('',#372506);
#38582=VERTEX_POINT('',#372507);
#38583=VERTEX_POINT('',#372582);
#38584=VERTEX_POINT('',#372583);
#38585=VERTEX_POINT('',#372658);
#38586=VERTEX_POINT('',#372659);
#38587=VERTEX_POINT('',#372736);
#38588=VERTEX_POINT('',#372737);
#38589=VERTEX_POINT('',#372814);
#38590=VERTEX_POINT('',#372815);
#38591=VERTEX_POINT('',#372890);
#38592=VERTEX_POINT('',#372891);
#38593=VERTEX_POINT('',#372966);
#38594=VERTEX_POINT('',#372967);
#38595=VERTEX_POINT('',#373042);
#38596=VERTEX_POINT('',#373043);
#38597=VERTEX_POINT('',#373118);
#38598=VERTEX_POINT('',#373119);
#38599=VERTEX_POINT('',#373194);
#38600=VERTEX_POINT('',#373195);
#38601=VERTEX_POINT('',#373274);
#38602=VERTEX_POINT('',#373275);
#38603=VERTEX_POINT('',#373350);
#38604=VERTEX_POINT('',#373351);
#38605=VERTEX_POINT('',#373426);
#38606=VERTEX_POINT('',#373427);
#38607=VERTEX_POINT('',#373502);
#38608=VERTEX_POINT('',#373503);
#38609=VERTEX_POINT('',#373578);
#38610=VERTEX_POINT('',#373579);
#38611=VERTEX_POINT('',#373654);
#38612=VERTEX_POINT('',#373655);
#38613=VERTEX_POINT('',#373730);
#38614=VERTEX_POINT('',#373731);
#38615=VERTEX_POINT('',#373810);
#38616=VERTEX_POINT('',#373811);
#38617=VERTEX_POINT('',#373886);
#38618=VERTEX_POINT('',#373887);
#38619=VERTEX_POINT('',#373962);
#38620=VERTEX_POINT('',#373963);
#38621=VERTEX_POINT('',#374038);
#38622=VERTEX_POINT('',#374039);
#38623=VERTEX_POINT('',#374114);
#38624=VERTEX_POINT('',#374115);
#38625=VERTEX_POINT('',#374190);
#38626=VERTEX_POINT('',#374191);
#38627=VERTEX_POINT('',#374268);
#38628=VERTEX_POINT('',#374269);
#38629=VERTEX_POINT('',#374346);
#38630=VERTEX_POINT('',#374347);
#38631=VERTEX_POINT('',#374422);
#38632=VERTEX_POINT('',#374423);
#38633=VERTEX_POINT('',#374498);
#38634=VERTEX_POINT('',#374499);
#38635=VERTEX_POINT('',#374574);
#38636=VERTEX_POINT('',#374576);
#38637=VERTEX_POINT('',#374591);
#38638=VERTEX_POINT('',#374604);
#38639=VERTEX_POINT('',#374605);
#38640=VERTEX_POINT('',#374638);
#38641=VERTEX_POINT('',#374653);
#38642=VERTEX_POINT('',#374772);
#38643=VERTEX_POINT('',#374776);
#38644=VERTEX_POINT('',#374777);
#38645=VERTEX_POINT('',#374779);
#38646=VERTEX_POINT('',#374781);
#38647=VERTEX_POINT('',#374783);
#38648=VERTEX_POINT('',#374785);
#38649=VERTEX_POINT('',#374787);
#38650=VERTEX_POINT('',#374791);
#38651=VERTEX_POINT('',#374792);
#38652=VERTEX_POINT('',#374798);
#38653=VERTEX_POINT('',#374800);
#38654=VERTEX_POINT('',#374804);
#38655=VERTEX_POINT('',#374808);
#38656=VERTEX_POINT('',#374812);
#38657=VERTEX_POINT('',#374813);
#38658=VERTEX_POINT('',#374815);
#38659=VERTEX_POINT('',#374823);
#38660=VERTEX_POINT('',#374825);
#38661=VERTEX_POINT('',#374833);
#38662=VERTEX_POINT('',#374835);
#38663=VERTEX_POINT('',#374843);
#38664=VERTEX_POINT('',#374845);
#38665=VERTEX_POINT('',#374853);
#38666=VERTEX_POINT('',#374855);
#38667=VERTEX_POINT('',#374863);
#38668=VERTEX_POINT('',#374865);
#38669=VERTEX_POINT('',#374873);
#38670=VERTEX_POINT('',#374875);
#38671=VERTEX_POINT('',#374883);
#38672=VERTEX_POINT('',#374885);
#38673=VERTEX_POINT('',#374893);
#38674=VERTEX_POINT('',#374895);
#38675=VERTEX_POINT('',#374903);
#38676=VERTEX_POINT('',#374905);
#38677=VERTEX_POINT('',#374913);
#38678=VERTEX_POINT('',#374915);
#38679=VERTEX_POINT('',#374923);
#38680=VERTEX_POINT('',#374925);
#38681=VERTEX_POINT('',#374933);
#38682=VERTEX_POINT('',#374935);
#38683=VERTEX_POINT('',#374943);
#38684=VERTEX_POINT('',#374945);
#38685=VERTEX_POINT('',#374953);
#38686=VERTEX_POINT('',#374955);
#38687=VERTEX_POINT('',#374963);
#38688=VERTEX_POINT('',#374965);
#38689=VERTEX_POINT('',#374973);
#38690=VERTEX_POINT('',#374975);
#38691=VERTEX_POINT('',#374983);
#38692=VERTEX_POINT('',#374985);
#38693=VERTEX_POINT('',#374993);
#38694=VERTEX_POINT('',#374995);
#38695=VERTEX_POINT('',#375003);
#38696=VERTEX_POINT('',#375005);
#38697=VERTEX_POINT('',#375013);
#38698=VERTEX_POINT('',#375015);
#38699=VERTEX_POINT('',#375023);
#38700=VERTEX_POINT('',#375025);
#38701=VERTEX_POINT('',#375033);
#38702=VERTEX_POINT('',#375035);
#38703=VERTEX_POINT('',#375043);
#38704=VERTEX_POINT('',#375045);
#38705=VERTEX_POINT('',#375053);
#38706=VERTEX_POINT('',#375055);
#38707=VERTEX_POINT('',#375063);
#38708=VERTEX_POINT('',#375065);
#38709=VERTEX_POINT('',#375073);
#38710=VERTEX_POINT('',#375075);
#38711=VERTEX_POINT('',#375083);
#38712=VERTEX_POINT('',#375085);
#38713=VERTEX_POINT('',#375093);
#38714=VERTEX_POINT('',#375095);
#38715=VERTEX_POINT('',#375103);
#38716=VERTEX_POINT('',#375105);
#38717=VERTEX_POINT('',#375113);
#38718=VERTEX_POINT('',#375115);
#38719=VERTEX_POINT('',#375123);
#38720=VERTEX_POINT('',#375125);
#38721=VERTEX_POINT('',#375133);
#38722=VERTEX_POINT('',#375135);
#38723=VERTEX_POINT('',#375143);
#38724=VERTEX_POINT('',#375145);
#38725=VERTEX_POINT('',#375153);
#38726=VERTEX_POINT('',#375155);
#38727=VERTEX_POINT('',#375163);
#38728=VERTEX_POINT('',#375165);
#38729=VERTEX_POINT('',#375173);
#38730=VERTEX_POINT('',#375175);
#38731=VERTEX_POINT('',#375183);
#38732=VERTEX_POINT('',#375185);
#38733=VERTEX_POINT('',#375193);
#38734=VERTEX_POINT('',#375195);
#38735=VERTEX_POINT('',#375203);
#38736=VERTEX_POINT('',#375205);
#38737=VERTEX_POINT('',#375213);
#38738=VERTEX_POINT('',#375215);
#38739=VERTEX_POINT('',#375223);
#38740=VERTEX_POINT('',#375225);
#38741=VERTEX_POINT('',#375233);
#38742=VERTEX_POINT('',#375235);
#38743=VERTEX_POINT('',#375243);
#38744=VERTEX_POINT('',#375245);
#38745=VERTEX_POINT('',#375253);
#38746=VERTEX_POINT('',#375255);
#38747=VERTEX_POINT('',#375263);
#38748=VERTEX_POINT('',#375265);
#38749=VERTEX_POINT('',#375273);
#38750=VERTEX_POINT('',#375275);
#38751=VERTEX_POINT('',#375283);
#38752=VERTEX_POINT('',#375285);
#38753=VERTEX_POINT('',#375293);
#38754=VERTEX_POINT('',#375295);
#38755=VERTEX_POINT('',#375303);
#38756=VERTEX_POINT('',#375305);
#38757=VERTEX_POINT('',#375313);
#38758=VERTEX_POINT('',#375315);
#38759=VERTEX_POINT('',#375323);
#38760=VERTEX_POINT('',#375325);
#38761=VERTEX_POINT('',#375333);
#38762=VERTEX_POINT('',#375335);
#38763=VERTEX_POINT('',#375343);
#38764=VERTEX_POINT('',#375345);
#38765=VERTEX_POINT('',#375353);
#38766=VERTEX_POINT('',#375355);
#38767=VERTEX_POINT('',#375363);
#38768=VERTEX_POINT('',#375365);
#38769=VERTEX_POINT('',#375373);
#38770=VERTEX_POINT('',#375375);
#38771=VERTEX_POINT('',#375383);
#38772=VERTEX_POINT('',#375385);
#38773=VERTEX_POINT('',#375393);
#38774=VERTEX_POINT('',#375395);
#38775=VERTEX_POINT('',#375403);
#38776=VERTEX_POINT('',#375405);
#38777=VERTEX_POINT('',#375413);
#38778=VERTEX_POINT('',#375415);
#38779=VERTEX_POINT('',#375423);
#38780=VERTEX_POINT('',#375425);
#38781=VERTEX_POINT('',#375433);
#38782=VERTEX_POINT('',#375435);
#38783=VERTEX_POINT('',#375443);
#38784=VERTEX_POINT('',#375445);
#38785=VERTEX_POINT('',#375453);
#38786=VERTEX_POINT('',#375455);
#38787=VERTEX_POINT('',#375463);
#38788=VERTEX_POINT('',#375465);
#38789=VERTEX_POINT('',#375473);
#38790=VERTEX_POINT('',#375475);
#38791=VERTEX_POINT('',#375483);
#38792=VERTEX_POINT('',#375485);
#38793=VERTEX_POINT('',#375493);
#38794=VERTEX_POINT('',#375495);
#38795=VERTEX_POINT('',#375503);
#38796=VERTEX_POINT('',#375505);
#38797=VERTEX_POINT('',#375513);
#38798=VERTEX_POINT('',#375515);
#38799=VERTEX_POINT('',#375523);
#38800=VERTEX_POINT('',#375525);
#38801=VERTEX_POINT('',#375533);
#38802=VERTEX_POINT('',#375535);
#38803=VERTEX_POINT('',#375543);
#38804=VERTEX_POINT('',#375545);
#38805=VERTEX_POINT('',#375553);
#38806=VERTEX_POINT('',#375555);
#38807=VERTEX_POINT('',#375563);
#38808=VERTEX_POINT('',#375565);
#38809=VERTEX_POINT('',#375573);
#38810=VERTEX_POINT('',#375575);
#38811=VERTEX_POINT('',#375583);
#38812=VERTEX_POINT('',#375585);
#38813=VERTEX_POINT('',#375593);
#38814=VERTEX_POINT('',#375595);
#38815=VERTEX_POINT('',#375603);
#38816=VERTEX_POINT('',#375605);
#38817=VERTEX_POINT('',#375613);
#38818=VERTEX_POINT('',#375615);
#38819=VERTEX_POINT('',#375623);
#38820=VERTEX_POINT('',#375625);
#38821=VERTEX_POINT('',#375633);
#38822=VERTEX_POINT('',#375635);
#38823=VERTEX_POINT('',#375643);
#38824=VERTEX_POINT('',#375645);
#38825=VERTEX_POINT('',#375653);
#38826=VERTEX_POINT('',#375655);
#38827=VERTEX_POINT('',#375663);
#38828=VERTEX_POINT('',#375665);
#38829=VERTEX_POINT('',#375673);
#38830=VERTEX_POINT('',#375675);
#38831=VERTEX_POINT('',#375683);
#38832=VERTEX_POINT('',#375685);
#38833=VERTEX_POINT('',#375693);
#38834=VERTEX_POINT('',#375695);
#38835=VERTEX_POINT('',#375703);
#38836=VERTEX_POINT('',#375705);
#38837=VERTEX_POINT('',#375713);
#38838=VERTEX_POINT('',#375715);
#38839=VERTEX_POINT('',#375723);
#38840=VERTEX_POINT('',#375725);
#38841=VERTEX_POINT('',#375733);
#38842=VERTEX_POINT('',#375735);
#38843=VERTEX_POINT('',#375743);
#38844=VERTEX_POINT('',#375745);
#38845=VERTEX_POINT('',#375753);
#38846=VERTEX_POINT('',#375755);
#38847=VERTEX_POINT('',#375763);
#38848=VERTEX_POINT('',#375765);
#38849=VERTEX_POINT('',#375773);
#38850=VERTEX_POINT('',#375775);
#38851=VERTEX_POINT('',#375783);
#38852=VERTEX_POINT('',#375785);
#38853=VERTEX_POINT('',#375793);
#38854=VERTEX_POINT('',#375795);
#38855=VERTEX_POINT('',#375797);
#38856=VERTEX_POINT('',#375800);
#38857=VERTEX_POINT('',#375802);
#38858=VERTEX_POINT('',#375810);
#38859=VERTEX_POINT('',#375812);
#38860=VERTEX_POINT('',#375820);
#38861=VERTEX_POINT('',#375822);
#38862=VERTEX_POINT('',#375830);
#38863=VERTEX_POINT('',#375832);
#38864=VERTEX_POINT('',#375840);
#38865=VERTEX_POINT('',#375842);
#38866=VERTEX_POINT('',#375850);
#38867=VERTEX_POINT('',#375852);
#38868=VERTEX_POINT('',#375860);
#38869=VERTEX_POINT('',#375862);
#38870=VERTEX_POINT('',#375870);
#38871=VERTEX_POINT('',#375872);
#38872=VERTEX_POINT('',#375880);
#38873=VERTEX_POINT('',#375882);
#38874=VERTEX_POINT('',#375890);
#38875=VERTEX_POINT('',#375892);
#38876=VERTEX_POINT('',#375900);
#38877=VERTEX_POINT('',#375902);
#38878=VERTEX_POINT('',#375910);
#38879=VERTEX_POINT('',#375912);
#38880=VERTEX_POINT('',#375920);
#38881=VERTEX_POINT('',#375922);
#38882=VERTEX_POINT('',#375930);
#38883=VERTEX_POINT('',#375932);
#38884=VERTEX_POINT('',#375940);
#38885=VERTEX_POINT('',#375942);
#38886=VERTEX_POINT('',#375950);
#38887=VERTEX_POINT('',#375952);
#38888=VERTEX_POINT('',#375960);
#38889=VERTEX_POINT('',#375962);
#38890=VERTEX_POINT('',#375970);
#38891=VERTEX_POINT('',#375972);
#38892=VERTEX_POINT('',#375980);
#38893=VERTEX_POINT('',#375982);
#38894=VERTEX_POINT('',#375990);
#38895=VERTEX_POINT('',#375992);
#38896=VERTEX_POINT('',#376000);
#38897=VERTEX_POINT('',#376002);
#38898=VERTEX_POINT('',#376010);
#38899=VERTEX_POINT('',#376012);
#38900=VERTEX_POINT('',#376020);
#38901=VERTEX_POINT('',#376022);
#38902=VERTEX_POINT('',#376030);
#38903=VERTEX_POINT('',#376032);
#38904=VERTEX_POINT('',#376040);
#38905=VERTEX_POINT('',#376042);
#38906=VERTEX_POINT('',#376050);
#38907=VERTEX_POINT('',#376052);
#38908=VERTEX_POINT('',#376060);
#38909=VERTEX_POINT('',#376062);
#38910=VERTEX_POINT('',#376070);
#38911=VERTEX_POINT('',#376072);
#38912=VERTEX_POINT('',#376080);
#38913=VERTEX_POINT('',#376082);
#38914=VERTEX_POINT('',#376090);
#38915=VERTEX_POINT('',#376092);
#38916=VERTEX_POINT('',#376100);
#38917=VERTEX_POINT('',#376102);
#38918=VERTEX_POINT('',#376110);
#38919=VERTEX_POINT('',#376112);
#38920=VERTEX_POINT('',#376120);
#38921=VERTEX_POINT('',#376122);
#38922=VERTEX_POINT('',#376130);
#38923=VERTEX_POINT('',#376132);
#38924=VERTEX_POINT('',#376140);
#38925=VERTEX_POINT('',#376142);
#38926=VERTEX_POINT('',#376150);
#38927=VERTEX_POINT('',#376152);
#38928=VERTEX_POINT('',#376160);
#38929=VERTEX_POINT('',#376162);
#38930=VERTEX_POINT('',#376170);
#38931=VERTEX_POINT('',#376172);
#38932=VERTEX_POINT('',#376180);
#38933=VERTEX_POINT('',#376182);
#38934=VERTEX_POINT('',#376190);
#38935=VERTEX_POINT('',#376192);
#38936=VERTEX_POINT('',#376200);
#38937=VERTEX_POINT('',#376202);
#38938=VERTEX_POINT('',#376210);
#38939=VERTEX_POINT('',#376212);
#38940=VERTEX_POINT('',#376220);
#38941=VERTEX_POINT('',#376222);
#38942=VERTEX_POINT('',#376230);
#38943=VERTEX_POINT('',#376232);
#38944=VERTEX_POINT('',#376240);
#38945=VERTEX_POINT('',#376242);
#38946=VERTEX_POINT('',#376250);
#38947=VERTEX_POINT('',#376252);
#38948=VERTEX_POINT('',#376260);
#38949=VERTEX_POINT('',#376262);
#38950=VERTEX_POINT('',#376270);
#38951=VERTEX_POINT('',#376272);
#38952=VERTEX_POINT('',#376280);
#38953=VERTEX_POINT('',#376282);
#38954=VERTEX_POINT('',#376290);
#38955=VERTEX_POINT('',#376292);
#38956=VERTEX_POINT('',#376300);
#38957=VERTEX_POINT('',#376302);
#38958=VERTEX_POINT('',#376310);
#38959=VERTEX_POINT('',#376312);
#38960=VERTEX_POINT('',#376320);
#38961=VERTEX_POINT('',#376322);
#38962=VERTEX_POINT('',#376330);
#38963=VERTEX_POINT('',#376332);
#38964=VERTEX_POINT('',#376340);
#38965=VERTEX_POINT('',#376342);
#38966=VERTEX_POINT('',#376350);
#38967=VERTEX_POINT('',#376352);
#38968=VERTEX_POINT('',#376360);
#38969=VERTEX_POINT('',#376362);
#38970=VERTEX_POINT('',#376370);
#38971=VERTEX_POINT('',#376372);
#38972=VERTEX_POINT('',#376380);
#38973=VERTEX_POINT('',#376382);
#38974=VERTEX_POINT('',#376390);
#38975=VERTEX_POINT('',#376392);
#38976=VERTEX_POINT('',#376400);
#38977=VERTEX_POINT('',#376402);
#38978=VERTEX_POINT('',#376410);
#38979=VERTEX_POINT('',#376412);
#38980=VERTEX_POINT('',#376420);
#38981=VERTEX_POINT('',#376422);
#38982=VERTEX_POINT('',#376430);
#38983=VERTEX_POINT('',#376432);
#38984=VERTEX_POINT('',#376440);
#38985=VERTEX_POINT('',#376442);
#38986=VERTEX_POINT('',#376450);
#38987=VERTEX_POINT('',#376452);
#38988=VERTEX_POINT('',#376460);
#38989=VERTEX_POINT('',#376462);
#38990=VERTEX_POINT('',#376470);
#38991=VERTEX_POINT('',#376472);
#38992=VERTEX_POINT('',#376480);
#38993=VERTEX_POINT('',#376482);
#38994=VERTEX_POINT('',#376490);
#38995=VERTEX_POINT('',#376492);
#38996=VERTEX_POINT('',#376500);
#38997=VERTEX_POINT('',#376502);
#38998=VERTEX_POINT('',#376510);
#38999=VERTEX_POINT('',#376512);
#39000=VERTEX_POINT('',#376520);
#39001=VERTEX_POINT('',#376522);
#39002=VERTEX_POINT('',#376530);
#39003=VERTEX_POINT('',#376532);
#39004=VERTEX_POINT('',#376540);
#39005=VERTEX_POINT('',#376542);
#39006=VERTEX_POINT('',#376550);
#39007=VERTEX_POINT('',#376552);
#39008=VERTEX_POINT('',#376560);
#39009=VERTEX_POINT('',#376562);
#39010=VERTEX_POINT('',#376570);
#39011=VERTEX_POINT('',#376572);
#39012=VERTEX_POINT('',#376580);
#39013=VERTEX_POINT('',#376582);
#39014=VERTEX_POINT('',#376590);
#39015=VERTEX_POINT('',#376592);
#39016=VERTEX_POINT('',#376600);
#39017=VERTEX_POINT('',#376602);
#39018=VERTEX_POINT('',#376610);
#39019=VERTEX_POINT('',#376612);
#39020=VERTEX_POINT('',#376620);
#39021=VERTEX_POINT('',#376622);
#39022=VERTEX_POINT('',#376630);
#39023=VERTEX_POINT('',#376632);
#39024=VERTEX_POINT('',#376640);
#39025=VERTEX_POINT('',#376642);
#39026=VERTEX_POINT('',#376650);
#39027=VERTEX_POINT('',#376652);
#39028=VERTEX_POINT('',#376660);
#39029=VERTEX_POINT('',#376662);
#39030=VERTEX_POINT('',#376670);
#39031=VERTEX_POINT('',#376672);
#39032=VERTEX_POINT('',#376680);
#39033=VERTEX_POINT('',#376682);
#39034=VERTEX_POINT('',#376690);
#39035=VERTEX_POINT('',#376692);
#39036=VERTEX_POINT('',#376700);
#39037=VERTEX_POINT('',#376702);
#39038=VERTEX_POINT('',#376710);
#39039=VERTEX_POINT('',#376712);
#39040=VERTEX_POINT('',#376720);
#39041=VERTEX_POINT('',#376722);
#39042=VERTEX_POINT('',#376730);
#39043=VERTEX_POINT('',#376732);
#39044=VERTEX_POINT('',#376740);
#39045=VERTEX_POINT('',#376742);
#39046=VERTEX_POINT('',#376750);
#39047=VERTEX_POINT('',#376752);
#39048=VERTEX_POINT('',#376760);
#39049=VERTEX_POINT('',#376762);
#39050=VERTEX_POINT('',#376770);
#39051=VERTEX_POINT('',#376780);
#39052=VERTEX_POINT('',#376784);
#39053=VERTEX_POINT('',#376785);
#39054=VERTEX_POINT('',#376787);
#39055=VERTEX_POINT('',#376789);
#39056=VERTEX_POINT('',#376791);
#39057=VERTEX_POINT('',#376793);
#39058=VERTEX_POINT('',#376795);
#39059=VERTEX_POINT('',#376797);
#39060=VERTEX_POINT('',#376799);
#39061=VERTEX_POINT('',#376801);
#39062=VERTEX_POINT('',#376803);
#39063=VERTEX_POINT('',#376805);
#39064=VERTEX_POINT('',#376807);
#39065=VERTEX_POINT('',#376809);
#39066=VERTEX_POINT('',#376811);
#39067=VERTEX_POINT('',#376813);
#39068=VERTEX_POINT('',#376815);
#39069=VERTEX_POINT('',#376817);
#39070=VERTEX_POINT('',#376819);
#39071=VERTEX_POINT('',#376821);
#39072=VERTEX_POINT('',#376823);
#39073=VERTEX_POINT('',#376825);
#39074=VERTEX_POINT('',#376827);
#39075=VERTEX_POINT('',#376829);
#39076=VERTEX_POINT('',#376831);
#39077=VERTEX_POINT('',#376833);
#39078=VERTEX_POINT('',#376835);
#39079=VERTEX_POINT('',#376837);
#39080=VERTEX_POINT('',#376839);
#39081=VERTEX_POINT('',#376841);
#39082=VERTEX_POINT('',#376843);
#39083=VERTEX_POINT('',#376845);
#39084=VERTEX_POINT('',#376847);
#39085=VERTEX_POINT('',#376849);
#39086=VERTEX_POINT('',#376851);
#39087=VERTEX_POINT('',#376853);
#39088=VERTEX_POINT('',#376855);
#39089=VERTEX_POINT('',#376857);
#39090=VERTEX_POINT('',#376859);
#39091=VERTEX_POINT('',#376861);
#39092=VERTEX_POINT('',#376863);
#39093=VERTEX_POINT('',#376865);
#39094=VERTEX_POINT('',#376867);
#39095=VERTEX_POINT('',#376869);
#39096=VERTEX_POINT('',#376871);
#39097=VERTEX_POINT('',#376873);
#39098=VERTEX_POINT('',#376875);
#39099=VERTEX_POINT('',#376877);
#39100=VERTEX_POINT('',#376879);
#39101=VERTEX_POINT('',#376881);
#39102=VERTEX_POINT('',#376883);
#39103=VERTEX_POINT('',#376885);
#39104=VERTEX_POINT('',#376887);
#39105=VERTEX_POINT('',#376889);
#39106=VERTEX_POINT('',#376891);
#39107=VERTEX_POINT('',#376893);
#39108=VERTEX_POINT('',#376895);
#39109=VERTEX_POINT('',#376897);
#39110=VERTEX_POINT('',#376899);
#39111=VERTEX_POINT('',#376901);
#39112=VERTEX_POINT('',#376903);
#39113=VERTEX_POINT('',#376905);
#39114=VERTEX_POINT('',#376907);
#39115=VERTEX_POINT('',#376909);
#39116=VERTEX_POINT('',#376911);
#39117=VERTEX_POINT('',#376913);
#39118=VERTEX_POINT('',#376915);
#39119=VERTEX_POINT('',#376917);
#39120=VERTEX_POINT('',#376919);
#39121=VERTEX_POINT('',#376921);
#39122=VERTEX_POINT('',#376923);
#39123=VERTEX_POINT('',#376925);
#39124=VERTEX_POINT('',#376927);
#39125=VERTEX_POINT('',#376929);
#39126=VERTEX_POINT('',#376931);
#39127=VERTEX_POINT('',#376933);
#39128=VERTEX_POINT('',#376935);
#39129=VERTEX_POINT('',#376937);
#39130=VERTEX_POINT('',#376939);
#39131=VERTEX_POINT('',#376941);
#39132=VERTEX_POINT('',#376943);
#39133=VERTEX_POINT('',#376945);
#39134=VERTEX_POINT('',#376947);
#39135=VERTEX_POINT('',#376949);
#39136=VERTEX_POINT('',#376951);
#39137=VERTEX_POINT('',#376953);
#39138=VERTEX_POINT('',#376955);
#39139=VERTEX_POINT('',#376957);
#39140=VERTEX_POINT('',#376959);
#39141=VERTEX_POINT('',#376961);
#39142=VERTEX_POINT('',#376963);
#39143=VERTEX_POINT('',#376965);
#39144=VERTEX_POINT('',#376967);
#39145=VERTEX_POINT('',#376969);
#39146=VERTEX_POINT('',#376971);
#39147=VERTEX_POINT('',#376973);
#39148=VERTEX_POINT('',#376975);
#39149=VERTEX_POINT('',#376977);
#39150=VERTEX_POINT('',#376979);
#39151=VERTEX_POINT('',#376981);
#39152=VERTEX_POINT('',#376983);
#39153=VERTEX_POINT('',#376985);
#39154=VERTEX_POINT('',#376987);
#39155=VERTEX_POINT('',#376989);
#39156=VERTEX_POINT('',#376991);
#39157=VERTEX_POINT('',#376993);
#39158=VERTEX_POINT('',#376995);
#39159=VERTEX_POINT('',#376997);
#39160=VERTEX_POINT('',#376999);
#39161=VERTEX_POINT('',#377001);
#39162=VERTEX_POINT('',#377003);
#39163=VERTEX_POINT('',#377005);
#39164=VERTEX_POINT('',#377007);
#39165=VERTEX_POINT('',#377009);
#39166=VERTEX_POINT('',#377011);
#39167=VERTEX_POINT('',#377013);
#39168=VERTEX_POINT('',#377015);
#39169=VERTEX_POINT('',#377017);
#39170=VERTEX_POINT('',#377019);
#39171=VERTEX_POINT('',#377021);
#39172=VERTEX_POINT('',#377023);
#39173=VERTEX_POINT('',#377025);
#39174=VERTEX_POINT('',#377027);
#39175=VERTEX_POINT('',#377029);
#39176=VERTEX_POINT('',#377031);
#39177=VERTEX_POINT('',#377033);
#39178=VERTEX_POINT('',#377035);
#39179=VERTEX_POINT('',#377037);
#39180=VERTEX_POINT('',#377039);
#39181=VERTEX_POINT('',#377041);
#39182=VERTEX_POINT('',#377043);
#39183=VERTEX_POINT('',#377045);
#39184=VERTEX_POINT('',#377047);
#39185=VERTEX_POINT('',#377049);
#39186=VERTEX_POINT('',#377051);
#39187=VERTEX_POINT('',#377053);
#39188=VERTEX_POINT('',#377055);
#39189=VERTEX_POINT('',#377057);
#39190=VERTEX_POINT('',#377059);
#39191=VERTEX_POINT('',#377061);
#39192=VERTEX_POINT('',#377063);
#39193=VERTEX_POINT('',#377065);
#39194=VERTEX_POINT('',#377067);
#39195=VERTEX_POINT('',#377069);
#39196=VERTEX_POINT('',#377071);
#39197=VERTEX_POINT('',#377073);
#39198=VERTEX_POINT('',#377075);
#39199=VERTEX_POINT('',#377077);
#39200=VERTEX_POINT('',#377079);
#39201=VERTEX_POINT('',#377081);
#39202=VERTEX_POINT('',#377083);
#39203=VERTEX_POINT('',#377085);
#39204=VERTEX_POINT('',#377087);
#39205=VERTEX_POINT('',#377089);
#39206=VERTEX_POINT('',#377091);
#39207=VERTEX_POINT('',#377093);
#39208=VERTEX_POINT('',#377095);
#39209=VERTEX_POINT('',#377097);
#39210=VERTEX_POINT('',#377099);
#39211=VERTEX_POINT('',#377101);
#39212=VERTEX_POINT('',#377103);
#39213=VERTEX_POINT('',#377105);
#39214=VERTEX_POINT('',#377107);
#39215=VERTEX_POINT('',#377109);
#39216=VERTEX_POINT('',#377111);
#39217=VERTEX_POINT('',#377113);
#39218=VERTEX_POINT('',#377115);
#39219=VERTEX_POINT('',#377117);
#39220=VERTEX_POINT('',#377119);
#39221=VERTEX_POINT('',#377121);
#39222=VERTEX_POINT('',#377123);
#39223=VERTEX_POINT('',#377125);
#39224=VERTEX_POINT('',#377127);
#39225=VERTEX_POINT('',#377129);
#39226=VERTEX_POINT('',#377131);
#39227=VERTEX_POINT('',#377133);
#39228=VERTEX_POINT('',#377135);
#39229=VERTEX_POINT('',#377137);
#39230=VERTEX_POINT('',#377139);
#39231=VERTEX_POINT('',#377141);
#39232=VERTEX_POINT('',#377143);
#39233=VERTEX_POINT('',#377145);
#39234=VERTEX_POINT('',#377147);
#39235=VERTEX_POINT('',#377149);
#39236=VERTEX_POINT('',#377151);
#39237=VERTEX_POINT('',#377153);
#39238=VERTEX_POINT('',#377155);
#39239=VERTEX_POINT('',#377157);
#39240=VERTEX_POINT('',#377159);
#39241=VERTEX_POINT('',#377161);
#39242=VERTEX_POINT('',#377163);
#39243=VERTEX_POINT('',#377165);
#39244=VERTEX_POINT('',#377167);
#39245=VERTEX_POINT('',#377169);
#39246=VERTEX_POINT('',#377171);
#39247=VERTEX_POINT('',#377173);
#39248=VERTEX_POINT('',#377175);
#39249=VERTEX_POINT('',#377177);
#39250=VERTEX_POINT('',#377179);
#39251=VERTEX_POINT('',#377181);
#39252=VERTEX_POINT('',#377183);
#39253=VERTEX_POINT('',#377185);
#39254=VERTEX_POINT('',#377187);
#39255=VERTEX_POINT('',#377189);
#39256=VERTEX_POINT('',#377191);
#39257=VERTEX_POINT('',#377193);
#39258=VERTEX_POINT('',#377195);
#39259=VERTEX_POINT('',#377197);
#39260=VERTEX_POINT('',#377199);
#39261=VERTEX_POINT('',#377201);
#39262=VERTEX_POINT('',#377203);
#39263=VERTEX_POINT('',#377205);
#39264=VERTEX_POINT('',#377207);
#39265=VERTEX_POINT('',#377209);
#39266=VERTEX_POINT('',#377211);
#39267=VERTEX_POINT('',#377213);
#39268=VERTEX_POINT('',#377215);
#39269=VERTEX_POINT('',#377217);
#39270=VERTEX_POINT('',#377219);
#39271=VERTEX_POINT('',#377221);
#39272=VERTEX_POINT('',#377223);
#39273=VERTEX_POINT('',#377225);
#39274=VERTEX_POINT('',#377227);
#39275=VERTEX_POINT('',#377229);
#39276=VERTEX_POINT('',#377231);
#39277=VERTEX_POINT('',#377233);
#39278=VERTEX_POINT('',#377235);
#39279=VERTEX_POINT('',#377237);
#39280=VERTEX_POINT('',#377239);
#39281=VERTEX_POINT('',#377241);
#39282=VERTEX_POINT('',#377243);
#39283=VERTEX_POINT('',#377245);
#39284=VERTEX_POINT('',#377247);
#39285=VERTEX_POINT('',#377249);
#39286=VERTEX_POINT('',#377251);
#39287=VERTEX_POINT('',#377253);
#39288=VERTEX_POINT('',#377255);
#39289=VERTEX_POINT('',#377257);
#39290=VERTEX_POINT('',#377259);
#39291=VERTEX_POINT('',#377261);
#39292=VERTEX_POINT('',#377263);
#39293=VERTEX_POINT('',#377265);
#39294=VERTEX_POINT('',#377267);
#39295=VERTEX_POINT('',#377269);
#39296=VERTEX_POINT('',#377271);
#39297=VERTEX_POINT('',#377273);
#39298=VERTEX_POINT('',#377275);
#39299=VERTEX_POINT('',#377277);
#39300=VERTEX_POINT('',#377279);
#39301=VERTEX_POINT('',#377281);
#39302=VERTEX_POINT('',#377283);
#39303=VERTEX_POINT('',#377285);
#39304=VERTEX_POINT('',#377287);
#39305=VERTEX_POINT('',#377289);
#39306=VERTEX_POINT('',#377291);
#39307=VERTEX_POINT('',#377293);
#39308=VERTEX_POINT('',#377295);
#39309=VERTEX_POINT('',#377297);
#39310=VERTEX_POINT('',#377299);
#39311=VERTEX_POINT('',#377301);
#39312=VERTEX_POINT('',#377303);
#39313=VERTEX_POINT('',#377305);
#39314=VERTEX_POINT('',#377307);
#39315=VERTEX_POINT('',#377309);
#39316=VERTEX_POINT('',#377311);
#39317=VERTEX_POINT('',#377313);
#39318=VERTEX_POINT('',#377315);
#39319=VERTEX_POINT('',#377317);
#39320=VERTEX_POINT('',#377319);
#39321=VERTEX_POINT('',#377321);
#39322=VERTEX_POINT('',#377323);
#39323=VERTEX_POINT('',#377325);
#39324=VERTEX_POINT('',#377327);
#39325=VERTEX_POINT('',#377329);
#39326=VERTEX_POINT('',#377331);
#39327=VERTEX_POINT('',#377333);
#39328=VERTEX_POINT('',#377335);
#39329=VERTEX_POINT('',#377337);
#39330=VERTEX_POINT('',#377339);
#39331=VERTEX_POINT('',#377341);
#39332=VERTEX_POINT('',#377343);
#39333=VERTEX_POINT('',#377345);
#39334=VERTEX_POINT('',#377347);
#39335=VERTEX_POINT('',#377349);
#39336=VERTEX_POINT('',#377351);
#39337=VERTEX_POINT('',#377353);
#39338=VERTEX_POINT('',#377355);
#39339=VERTEX_POINT('',#377357);
#39340=VERTEX_POINT('',#377359);
#39341=VERTEX_POINT('',#377361);
#39342=VERTEX_POINT('',#377363);
#39343=VERTEX_POINT('',#377365);
#39344=VERTEX_POINT('',#377367);
#39345=VERTEX_POINT('',#377369);
#39346=VERTEX_POINT('',#377371);
#39347=VERTEX_POINT('',#377373);
#39348=VERTEX_POINT('',#377376);
#39349=VERTEX_POINT('',#377378);
#39350=VERTEX_POINT('',#377380);
#39351=VERTEX_POINT('',#377382);
#39352=VERTEX_POINT('',#377384);
#39353=VERTEX_POINT('',#377386);
#39354=VERTEX_POINT('',#377388);
#39355=VERTEX_POINT('',#377390);
#39356=VERTEX_POINT('',#377392);
#39357=VERTEX_POINT('',#377394);
#39358=VERTEX_POINT('',#377396);
#39359=VERTEX_POINT('',#377398);
#39360=VERTEX_POINT('',#377400);
#39361=VERTEX_POINT('',#377402);
#39362=VERTEX_POINT('',#377404);
#39363=VERTEX_POINT('',#377406);
#39364=VERTEX_POINT('',#377408);
#39365=VERTEX_POINT('',#377410);
#39366=VERTEX_POINT('',#377412);
#39367=VERTEX_POINT('',#377414);
#39368=VERTEX_POINT('',#377416);
#39369=VERTEX_POINT('',#377418);
#39370=VERTEX_POINT('',#377420);
#39371=VERTEX_POINT('',#377422);
#39372=VERTEX_POINT('',#377424);
#39373=VERTEX_POINT('',#377426);
#39374=VERTEX_POINT('',#377428);
#39375=VERTEX_POINT('',#377430);
#39376=VERTEX_POINT('',#377432);
#39377=VERTEX_POINT('',#377434);
#39378=VERTEX_POINT('',#377436);
#39379=VERTEX_POINT('',#377438);
#39380=VERTEX_POINT('',#377440);
#39381=VERTEX_POINT('',#377442);
#39382=VERTEX_POINT('',#377444);
#39383=VERTEX_POINT('',#377446);
#39384=VERTEX_POINT('',#377448);
#39385=VERTEX_POINT('',#377450);
#39386=VERTEX_POINT('',#377452);
#39387=VERTEX_POINT('',#377454);
#39388=VERTEX_POINT('',#377456);
#39389=VERTEX_POINT('',#377458);
#39390=VERTEX_POINT('',#377460);
#39391=VERTEX_POINT('',#377462);
#39392=VERTEX_POINT('',#377464);
#39393=VERTEX_POINT('',#377466);
#39394=VERTEX_POINT('',#377468);
#39395=VERTEX_POINT('',#377470);
#39396=VERTEX_POINT('',#377472);
#39397=VERTEX_POINT('',#377474);
#39398=VERTEX_POINT('',#377476);
#39399=VERTEX_POINT('',#377478);
#39400=VERTEX_POINT('',#377480);
#39401=VERTEX_POINT('',#377482);
#39402=VERTEX_POINT('',#377484);
#39403=VERTEX_POINT('',#377486);
#39404=VERTEX_POINT('',#377488);
#39405=VERTEX_POINT('',#377490);
#39406=VERTEX_POINT('',#377492);
#39407=VERTEX_POINT('',#377494);
#39408=VERTEX_POINT('',#377496);
#39409=VERTEX_POINT('',#377498);
#39410=VERTEX_POINT('',#377500);
#39411=VERTEX_POINT('',#377502);
#39412=VERTEX_POINT('',#377504);
#39413=VERTEX_POINT('',#377506);
#39414=VERTEX_POINT('',#377508);
#39415=VERTEX_POINT('',#377510);
#39416=VERTEX_POINT('',#377512);
#39417=VERTEX_POINT('',#377514);
#39418=VERTEX_POINT('',#377516);
#39419=VERTEX_POINT('',#377518);
#39420=VERTEX_POINT('',#377520);
#39421=VERTEX_POINT('',#377522);
#39422=VERTEX_POINT('',#377524);
#39423=VERTEX_POINT('',#377526);
#39424=VERTEX_POINT('',#377528);
#39425=VERTEX_POINT('',#377530);
#39426=VERTEX_POINT('',#377532);
#39427=VERTEX_POINT('',#377534);
#39428=VERTEX_POINT('',#377536);
#39429=VERTEX_POINT('',#377538);
#39430=VERTEX_POINT('',#377540);
#39431=VERTEX_POINT('',#377542);
#39432=VERTEX_POINT('',#377544);
#39433=VERTEX_POINT('',#377546);
#39434=VERTEX_POINT('',#377548);
#39435=VERTEX_POINT('',#377550);
#39436=VERTEX_POINT('',#377552);
#39437=VERTEX_POINT('',#377554);
#39438=VERTEX_POINT('',#377556);
#39439=VERTEX_POINT('',#377558);
#39440=VERTEX_POINT('',#377560);
#39441=VERTEX_POINT('',#377562);
#39442=VERTEX_POINT('',#377564);
#39443=VERTEX_POINT('',#377566);
#39444=VERTEX_POINT('',#377568);
#39445=VERTEX_POINT('',#377570);
#39446=VERTEX_POINT('',#377572);
#39447=VERTEX_POINT('',#377574);
#39448=VERTEX_POINT('',#377576);
#39449=VERTEX_POINT('',#377578);
#39450=VERTEX_POINT('',#377580);
#39451=VERTEX_POINT('',#377582);
#39452=VERTEX_POINT('',#377584);
#39453=VERTEX_POINT('',#377586);
#39454=VERTEX_POINT('',#377588);
#39455=VERTEX_POINT('',#377590);
#39456=VERTEX_POINT('',#377592);
#39457=VERTEX_POINT('',#377594);
#39458=VERTEX_POINT('',#377596);
#39459=VERTEX_POINT('',#377598);
#39460=VERTEX_POINT('',#377600);
#39461=VERTEX_POINT('',#377602);
#39462=VERTEX_POINT('',#377604);
#39463=VERTEX_POINT('',#377606);
#39464=VERTEX_POINT('',#377608);
#39465=VERTEX_POINT('',#377610);
#39466=VERTEX_POINT('',#377612);
#39467=VERTEX_POINT('',#377614);
#39468=VERTEX_POINT('',#377616);
#39469=VERTEX_POINT('',#377618);
#39470=VERTEX_POINT('',#377620);
#39471=VERTEX_POINT('',#377622);
#39472=VERTEX_POINT('',#377624);
#39473=VERTEX_POINT('',#377626);
#39474=VERTEX_POINT('',#377628);
#39475=VERTEX_POINT('',#377630);
#39476=VERTEX_POINT('',#377632);
#39477=VERTEX_POINT('',#377634);
#39478=VERTEX_POINT('',#377636);
#39479=VERTEX_POINT('',#377638);
#39480=VERTEX_POINT('',#377640);
#39481=VERTEX_POINT('',#377642);
#39482=VERTEX_POINT('',#377644);
#39483=VERTEX_POINT('',#377646);
#39484=VERTEX_POINT('',#377648);
#39485=VERTEX_POINT('',#377650);
#39486=VERTEX_POINT('',#377652);
#39487=VERTEX_POINT('',#377654);
#39488=VERTEX_POINT('',#377656);
#39489=VERTEX_POINT('',#377658);
#39490=VERTEX_POINT('',#377660);
#39491=VERTEX_POINT('',#377662);
#39492=VERTEX_POINT('',#377664);
#39493=VERTEX_POINT('',#377666);
#39494=VERTEX_POINT('',#377668);
#39495=VERTEX_POINT('',#377670);
#39496=VERTEX_POINT('',#377672);
#39497=VERTEX_POINT('',#377674);
#39498=VERTEX_POINT('',#377676);
#39499=VERTEX_POINT('',#377678);
#39500=VERTEX_POINT('',#377680);
#39501=VERTEX_POINT('',#377682);
#39502=VERTEX_POINT('',#377684);
#39503=VERTEX_POINT('',#377686);
#39504=VERTEX_POINT('',#377688);
#39505=VERTEX_POINT('',#377690);
#39506=VERTEX_POINT('',#377692);
#39507=VERTEX_POINT('',#377694);
#39508=VERTEX_POINT('',#377696);
#39509=VERTEX_POINT('',#377698);
#39510=VERTEX_POINT('',#377700);
#39511=VERTEX_POINT('',#377702);
#39512=VERTEX_POINT('',#377704);
#39513=VERTEX_POINT('',#377706);
#39514=VERTEX_POINT('',#377708);
#39515=VERTEX_POINT('',#377710);
#39516=VERTEX_POINT('',#377712);
#39517=VERTEX_POINT('',#377714);
#39518=VERTEX_POINT('',#377716);
#39519=VERTEX_POINT('',#377718);
#39520=VERTEX_POINT('',#377720);
#39521=VERTEX_POINT('',#377722);
#39522=VERTEX_POINT('',#377724);
#39523=VERTEX_POINT('',#377726);
#39524=VERTEX_POINT('',#377728);
#39525=VERTEX_POINT('',#377730);
#39526=VERTEX_POINT('',#377732);
#39527=VERTEX_POINT('',#377734);
#39528=VERTEX_POINT('',#377736);
#39529=VERTEX_POINT('',#377738);
#39530=VERTEX_POINT('',#377740);
#39531=VERTEX_POINT('',#377742);
#39532=VERTEX_POINT('',#377744);
#39533=VERTEX_POINT('',#377746);
#39534=VERTEX_POINT('',#377748);
#39535=VERTEX_POINT('',#377750);
#39536=VERTEX_POINT('',#377752);
#39537=VERTEX_POINT('',#377754);
#39538=VERTEX_POINT('',#377756);
#39539=VERTEX_POINT('',#377758);
#39540=VERTEX_POINT('',#377760);
#39541=VERTEX_POINT('',#377762);
#39542=VERTEX_POINT('',#377764);
#39543=VERTEX_POINT('',#377766);
#39544=VERTEX_POINT('',#377768);
#39545=VERTEX_POINT('',#377770);
#39546=VERTEX_POINT('',#377772);
#39547=VERTEX_POINT('',#377774);
#39548=VERTEX_POINT('',#377776);
#39549=VERTEX_POINT('',#377778);
#39550=VERTEX_POINT('',#377780);
#39551=VERTEX_POINT('',#377782);
#39552=VERTEX_POINT('',#377784);
#39553=VERTEX_POINT('',#377786);
#39554=VERTEX_POINT('',#377788);
#39555=VERTEX_POINT('',#377790);
#39556=VERTEX_POINT('',#377792);
#39557=VERTEX_POINT('',#377794);
#39558=VERTEX_POINT('',#377796);
#39559=VERTEX_POINT('',#377798);
#39560=VERTEX_POINT('',#377800);
#39561=VERTEX_POINT('',#377802);
#39562=VERTEX_POINT('',#377804);
#39563=VERTEX_POINT('',#377806);
#39564=VERTEX_POINT('',#377808);
#39565=VERTEX_POINT('',#377810);
#39566=VERTEX_POINT('',#377812);
#39567=VERTEX_POINT('',#377814);
#39568=VERTEX_POINT('',#377816);
#39569=VERTEX_POINT('',#377818);
#39570=VERTEX_POINT('',#377820);
#39571=VERTEX_POINT('',#377822);
#39572=VERTEX_POINT('',#377824);
#39573=VERTEX_POINT('',#377826);
#39574=VERTEX_POINT('',#377828);
#39575=VERTEX_POINT('',#377830);
#39576=VERTEX_POINT('',#377832);
#39577=VERTEX_POINT('',#377834);
#39578=VERTEX_POINT('',#377836);
#39579=VERTEX_POINT('',#377838);
#39580=VERTEX_POINT('',#377840);
#39581=VERTEX_POINT('',#377842);
#39582=VERTEX_POINT('',#377844);
#39583=VERTEX_POINT('',#377846);
#39584=VERTEX_POINT('',#377848);
#39585=VERTEX_POINT('',#377850);
#39586=VERTEX_POINT('',#377852);
#39587=VERTEX_POINT('',#377854);
#39588=VERTEX_POINT('',#377856);
#39589=VERTEX_POINT('',#377858);
#39590=VERTEX_POINT('',#377860);
#39591=VERTEX_POINT('',#377862);
#39592=VERTEX_POINT('',#377864);
#39593=VERTEX_POINT('',#377866);
#39594=VERTEX_POINT('',#377868);
#39595=VERTEX_POINT('',#377870);
#39596=VERTEX_POINT('',#377872);
#39597=VERTEX_POINT('',#377874);
#39598=VERTEX_POINT('',#377876);
#39599=VERTEX_POINT('',#377878);
#39600=VERTEX_POINT('',#377880);
#39601=VERTEX_POINT('',#377882);
#39602=VERTEX_POINT('',#377884);
#39603=VERTEX_POINT('',#377886);
#39604=VERTEX_POINT('',#377888);
#39605=VERTEX_POINT('',#377890);
#39606=VERTEX_POINT('',#377892);
#39607=VERTEX_POINT('',#377894);
#39608=VERTEX_POINT('',#377896);
#39609=VERTEX_POINT('',#377898);
#39610=VERTEX_POINT('',#377900);
#39611=VERTEX_POINT('',#377902);
#39612=VERTEX_POINT('',#377904);
#39613=VERTEX_POINT('',#377906);
#39614=VERTEX_POINT('',#377908);
#39615=VERTEX_POINT('',#377910);
#39616=VERTEX_POINT('',#377912);
#39617=VERTEX_POINT('',#377914);
#39618=VERTEX_POINT('',#377916);
#39619=VERTEX_POINT('',#377918);
#39620=VERTEX_POINT('',#377920);
#39621=VERTEX_POINT('',#377922);
#39622=VERTEX_POINT('',#377924);
#39623=VERTEX_POINT('',#377926);
#39624=VERTEX_POINT('',#377928);
#39625=VERTEX_POINT('',#377930);
#39626=VERTEX_POINT('',#377932);
#39627=VERTEX_POINT('',#377934);
#39628=VERTEX_POINT('',#377936);
#39629=VERTEX_POINT('',#377938);
#39630=VERTEX_POINT('',#377940);
#39631=VERTEX_POINT('',#377942);
#39632=VERTEX_POINT('',#377944);
#39633=VERTEX_POINT('',#377946);
#39634=VERTEX_POINT('',#377948);
#39635=VERTEX_POINT('',#377950);
#39636=VERTEX_POINT('',#377952);
#39637=VERTEX_POINT('',#377954);
#39638=VERTEX_POINT('',#377956);
#39639=VERTEX_POINT('',#377958);
#39640=VERTEX_POINT('',#377960);
#39641=VERTEX_POINT('',#378255);
#39642=VERTEX_POINT('',#378256);
#39643=VERTEX_POINT('',#378258);
#39644=VERTEX_POINT('',#378308);
#39645=VERTEX_POINT('',#378312);
#39646=VERTEX_POINT('',#378313);
#39647=VERTEX_POINT('',#378319);
#39648=VERTEX_POINT('',#378329);
#39649=VERTEX_POINT('',#378334);
#39650=VERTEX_POINT('',#378336);
#39651=VERTEX_POINT('',#378346);
#39652=VERTEX_POINT('',#378350);
#39653=VERTEX_POINT('',#378354);
#39654=VERTEX_POINT('',#378358);
#39655=VERTEX_POINT('',#378362);
#39656=VERTEX_POINT('',#378366);
#39657=VERTEX_POINT('',#378367);
#39658=VERTEX_POINT('',#378370);
#39659=VERTEX_POINT('',#378372);
#39660=VERTEX_POINT('',#378392);
#39661=VERTEX_POINT('',#379922);
#39662=VERTEX_POINT('',#379923);
#39663=VERTEX_POINT('',#379928);
#39664=VERTEX_POINT('',#380135);
#39665=VERTEX_POINT('',#380136);
#39666=VERTEX_POINT('',#380138);
#39667=VERTEX_POINT('',#380143);
#39668=VERTEX_POINT('',#380145);
#39669=VERTEX_POINT('',#380155);
#39670=VERTEX_POINT('',#380156);
#39671=VERTEX_POINT('',#380158);
#39672=VERTEX_POINT('',#380163);
#39673=VERTEX_POINT('',#380165);
#39674=VERTEX_POINT('',#380237);
#39675=VERTEX_POINT('',#380269);
#39676=VERTEX_POINT('',#380300);
#39677=VERTEX_POINT('',#380439);
#39678=VERTEX_POINT('',#380440);
#39679=VERTEX_POINT('',#380442);
#39680=VERTEX_POINT('',#380447);
#39681=VERTEX_POINT('',#380449);
#39682=VERTEX_POINT('',#380459);
#39683=VERTEX_POINT('',#380460);
#39684=VERTEX_POINT('',#380462);
#39685=VERTEX_POINT('',#380467);
#39686=VERTEX_POINT('',#380469);
#39687=VERTEX_POINT('',#380541);
#39688=VERTEX_POINT('',#380573);
#39689=VERTEX_POINT('',#380604);
#39690=VERTEX_POINT('',#380743);
#39691=VERTEX_POINT('',#380744);
#39692=VERTEX_POINT('',#380746);
#39693=VERTEX_POINT('',#380751);
#39694=VERTEX_POINT('',#380753);
#39695=VERTEX_POINT('',#380763);
#39696=VERTEX_POINT('',#380764);
#39697=VERTEX_POINT('',#380766);
#39698=VERTEX_POINT('',#380771);
#39699=VERTEX_POINT('',#380773);
#39700=VERTEX_POINT('',#380845);
#39701=VERTEX_POINT('',#380877);
#39702=VERTEX_POINT('',#380908);
#39703=VERTEX_POINT('',#381047);
#39704=VERTEX_POINT('',#381048);
#39705=VERTEX_POINT('',#381050);
#39706=VERTEX_POINT('',#381055);
#39707=VERTEX_POINT('',#381057);
#39708=VERTEX_POINT('',#381067);
#39709=VERTEX_POINT('',#381068);
#39710=VERTEX_POINT('',#381070);
#39711=VERTEX_POINT('',#381075);
#39712=VERTEX_POINT('',#381077);
#39713=VERTEX_POINT('',#381149);
#39714=VERTEX_POINT('',#381181);
#39715=VERTEX_POINT('',#381212);
#39716=VERTEX_POINT('',#381351);
#39717=VERTEX_POINT('',#381352);
#39718=VERTEX_POINT('',#381354);
#39719=VERTEX_POINT('',#381359);
#39720=VERTEX_POINT('',#381361);
#39721=VERTEX_POINT('',#381371);
#39722=VERTEX_POINT('',#381372);
#39723=VERTEX_POINT('',#381374);
#39724=VERTEX_POINT('',#381379);
#39725=VERTEX_POINT('',#381381);
#39726=VERTEX_POINT('',#381453);
#39727=VERTEX_POINT('',#381485);
#39728=VERTEX_POINT('',#381516);
#39729=VERTEX_POINT('',#381655);
#39730=VERTEX_POINT('',#381656);
#39731=VERTEX_POINT('',#381658);
#39732=VERTEX_POINT('',#381663);
#39733=VERTEX_POINT('',#381665);
#39734=VERTEX_POINT('',#381675);
#39735=VERTEX_POINT('',#381676);
#39736=VERTEX_POINT('',#381678);
#39737=VERTEX_POINT('',#381683);
#39738=VERTEX_POINT('',#381685);
#39739=VERTEX_POINT('',#381757);
#39740=VERTEX_POINT('',#381789);
#39741=VERTEX_POINT('',#381820);
#39742=VERTEX_POINT('',#381959);
#39743=VERTEX_POINT('',#381960);
#39744=VERTEX_POINT('',#381962);
#39745=VERTEX_POINT('',#381967);
#39746=VERTEX_POINT('',#381969);
#39747=VERTEX_POINT('',#381979);
#39748=VERTEX_POINT('',#381980);
#39749=VERTEX_POINT('',#381982);
#39750=VERTEX_POINT('',#381987);
#39751=VERTEX_POINT('',#381989);
#39752=VERTEX_POINT('',#382061);
#39753=VERTEX_POINT('',#382093);
#39754=VERTEX_POINT('',#382124);
#39755=VERTEX_POINT('',#382263);
#39756=VERTEX_POINT('',#382264);
#39757=VERTEX_POINT('',#382266);
#39758=VERTEX_POINT('',#382271);
#39759=VERTEX_POINT('',#382273);
#39760=VERTEX_POINT('',#382283);
#39761=VERTEX_POINT('',#382284);
#39762=VERTEX_POINT('',#382286);
#39763=VERTEX_POINT('',#382291);
#39764=VERTEX_POINT('',#382293);
#39765=VERTEX_POINT('',#382365);
#39766=VERTEX_POINT('',#382397);
#39767=VERTEX_POINT('',#382428);
#39768=VERTEX_POINT('',#382567);
#39769=VERTEX_POINT('',#382568);
#39770=VERTEX_POINT('',#382570);
#39771=VERTEX_POINT('',#382575);
#39772=VERTEX_POINT('',#382577);
#39773=VERTEX_POINT('',#382587);
#39774=VERTEX_POINT('',#382588);
#39775=VERTEX_POINT('',#382590);
#39776=VERTEX_POINT('',#382595);
#39777=VERTEX_POINT('',#382597);
#39778=VERTEX_POINT('',#382669);
#39779=VERTEX_POINT('',#382701);
#39780=VERTEX_POINT('',#382732);
#39781=VERTEX_POINT('',#382871);
#39782=VERTEX_POINT('',#382872);
#39783=VERTEX_POINT('',#382874);
#39784=VERTEX_POINT('',#382879);
#39785=VERTEX_POINT('',#382881);
#39786=VERTEX_POINT('',#382891);
#39787=VERTEX_POINT('',#382892);
#39788=VERTEX_POINT('',#382894);
#39789=VERTEX_POINT('',#382899);
#39790=VERTEX_POINT('',#382901);
#39791=VERTEX_POINT('',#382973);
#39792=VERTEX_POINT('',#383005);
#39793=VERTEX_POINT('',#383036);
#39794=VERTEX_POINT('',#383175);
#39795=VERTEX_POINT('',#383176);
#39796=VERTEX_POINT('',#383178);
#39797=VERTEX_POINT('',#383183);
#39798=VERTEX_POINT('',#383185);
#39799=VERTEX_POINT('',#383195);
#39800=VERTEX_POINT('',#383196);
#39801=VERTEX_POINT('',#383198);
#39802=VERTEX_POINT('',#383203);
#39803=VERTEX_POINT('',#383205);
#39804=VERTEX_POINT('',#383277);
#39805=VERTEX_POINT('',#383309);
#39806=VERTEX_POINT('',#383340);
#39807=VERTEX_POINT('',#383479);
#39808=VERTEX_POINT('',#383480);
#39809=VERTEX_POINT('',#383482);
#39810=VERTEX_POINT('',#383487);
#39811=VERTEX_POINT('',#383489);
#39812=VERTEX_POINT('',#383499);
#39813=VERTEX_POINT('',#383500);
#39814=VERTEX_POINT('',#383502);
#39815=VERTEX_POINT('',#383507);
#39816=VERTEX_POINT('',#383509);
#39817=VERTEX_POINT('',#383581);
#39818=VERTEX_POINT('',#383613);
#39819=VERTEX_POINT('',#383644);
#39820=VERTEX_POINT('',#383783);
#39821=VERTEX_POINT('',#383784);
#39822=VERTEX_POINT('',#383786);
#39823=VERTEX_POINT('',#383791);
#39824=VERTEX_POINT('',#383793);
#39825=VERTEX_POINT('',#383803);
#39826=VERTEX_POINT('',#383804);
#39827=VERTEX_POINT('',#383806);
#39828=VERTEX_POINT('',#383811);
#39829=VERTEX_POINT('',#383813);
#39830=VERTEX_POINT('',#383885);
#39831=VERTEX_POINT('',#383917);
#39832=VERTEX_POINT('',#383948);
#39833=VERTEX_POINT('',#384087);
#39834=VERTEX_POINT('',#384088);
#39835=VERTEX_POINT('',#384090);
#39836=VERTEX_POINT('',#384095);
#39837=VERTEX_POINT('',#384097);
#39838=VERTEX_POINT('',#384107);
#39839=VERTEX_POINT('',#384108);
#39840=VERTEX_POINT('',#384110);
#39841=VERTEX_POINT('',#384115);
#39842=VERTEX_POINT('',#384117);
#39843=VERTEX_POINT('',#384189);
#39844=VERTEX_POINT('',#384221);
#39845=VERTEX_POINT('',#384252);
#39846=VERTEX_POINT('',#384391);
#39847=VERTEX_POINT('',#384392);
#39848=VERTEX_POINT('',#384394);
#39849=VERTEX_POINT('',#384399);
#39850=VERTEX_POINT('',#384401);
#39851=VERTEX_POINT('',#384411);
#39852=VERTEX_POINT('',#384412);
#39853=VERTEX_POINT('',#384414);
#39854=VERTEX_POINT('',#384419);
#39855=VERTEX_POINT('',#384421);
#39856=VERTEX_POINT('',#384493);
#39857=VERTEX_POINT('',#384525);
#39858=VERTEX_POINT('',#384556);
#39859=VERTEX_POINT('',#384695);
#39860=VERTEX_POINT('',#384696);
#39861=VERTEX_POINT('',#384698);
#39862=VERTEX_POINT('',#384703);
#39863=VERTEX_POINT('',#384705);
#39864=VERTEX_POINT('',#384715);
#39865=VERTEX_POINT('',#384716);
#39866=VERTEX_POINT('',#384718);
#39867=VERTEX_POINT('',#384723);
#39868=VERTEX_POINT('',#384725);
#39869=VERTEX_POINT('',#384797);
#39870=VERTEX_POINT('',#384829);
#39871=VERTEX_POINT('',#384860);
#39872=VERTEX_POINT('',#384999);
#39873=VERTEX_POINT('',#385000);
#39874=VERTEX_POINT('',#385002);
#39875=VERTEX_POINT('',#385007);
#39876=VERTEX_POINT('',#385009);
#39877=VERTEX_POINT('',#385019);
#39878=VERTEX_POINT('',#385020);
#39879=VERTEX_POINT('',#385022);
#39880=VERTEX_POINT('',#385027);
#39881=VERTEX_POINT('',#385029);
#39882=VERTEX_POINT('',#385101);
#39883=VERTEX_POINT('',#385133);
#39884=VERTEX_POINT('',#385164);
#39885=VERTEX_POINT('',#385303);
#39886=VERTEX_POINT('',#385304);
#39887=VERTEX_POINT('',#385306);
#39888=VERTEX_POINT('',#385311);
#39889=VERTEX_POINT('',#385313);
#39890=VERTEX_POINT('',#385323);
#39891=VERTEX_POINT('',#385324);
#39892=VERTEX_POINT('',#385326);
#39893=VERTEX_POINT('',#385331);
#39894=VERTEX_POINT('',#385333);
#39895=VERTEX_POINT('',#385405);
#39896=VERTEX_POINT('',#385437);
#39897=VERTEX_POINT('',#385468);
#39898=VERTEX_POINT('',#385607);
#39899=VERTEX_POINT('',#385608);
#39900=VERTEX_POINT('',#385610);
#39901=VERTEX_POINT('',#385615);
#39902=VERTEX_POINT('',#385617);
#39903=VERTEX_POINT('',#385627);
#39904=VERTEX_POINT('',#385628);
#39905=VERTEX_POINT('',#385630);
#39906=VERTEX_POINT('',#385635);
#39907=VERTEX_POINT('',#385637);
#39908=VERTEX_POINT('',#385709);
#39909=VERTEX_POINT('',#385741);
#39910=VERTEX_POINT('',#385772);
#39911=VERTEX_POINT('',#385911);
#39912=VERTEX_POINT('',#385912);
#39913=VERTEX_POINT('',#385914);
#39914=VERTEX_POINT('',#385919);
#39915=VERTEX_POINT('',#385921);
#39916=VERTEX_POINT('',#385931);
#39917=VERTEX_POINT('',#385932);
#39918=VERTEX_POINT('',#385934);
#39919=VERTEX_POINT('',#385939);
#39920=VERTEX_POINT('',#385941);
#39921=VERTEX_POINT('',#386013);
#39922=VERTEX_POINT('',#386045);
#39923=VERTEX_POINT('',#386076);
#39924=VERTEX_POINT('',#386215);
#39925=VERTEX_POINT('',#386216);
#39926=VERTEX_POINT('',#386218);
#39927=VERTEX_POINT('',#386223);
#39928=VERTEX_POINT('',#386225);
#39929=VERTEX_POINT('',#386235);
#39930=VERTEX_POINT('',#386236);
#39931=VERTEX_POINT('',#386238);
#39932=VERTEX_POINT('',#386243);
#39933=VERTEX_POINT('',#386245);
#39934=VERTEX_POINT('',#386317);
#39935=VERTEX_POINT('',#386349);
#39936=VERTEX_POINT('',#386380);
#39937=VERTEX_POINT('',#386519);
#39938=VERTEX_POINT('',#386520);
#39939=VERTEX_POINT('',#386522);
#39940=VERTEX_POINT('',#386527);
#39941=VERTEX_POINT('',#386529);
#39942=VERTEX_POINT('',#386539);
#39943=VERTEX_POINT('',#386540);
#39944=VERTEX_POINT('',#386542);
#39945=VERTEX_POINT('',#386547);
#39946=VERTEX_POINT('',#386549);
#39947=VERTEX_POINT('',#386621);
#39948=VERTEX_POINT('',#386653);
#39949=VERTEX_POINT('',#386684);
#39950=VERTEX_POINT('',#386823);
#39951=VERTEX_POINT('',#386824);
#39952=VERTEX_POINT('',#386826);
#39953=VERTEX_POINT('',#386831);
#39954=VERTEX_POINT('',#386833);
#39955=VERTEX_POINT('',#386843);
#39956=VERTEX_POINT('',#386844);
#39957=VERTEX_POINT('',#386846);
#39958=VERTEX_POINT('',#386851);
#39959=VERTEX_POINT('',#386853);
#39960=VERTEX_POINT('',#386925);
#39961=VERTEX_POINT('',#386957);
#39962=VERTEX_POINT('',#386988);
#39963=VERTEX_POINT('',#387127);
#39964=VERTEX_POINT('',#387128);
#39965=VERTEX_POINT('',#387130);
#39966=VERTEX_POINT('',#387135);
#39967=VERTEX_POINT('',#387137);
#39968=VERTEX_POINT('',#387147);
#39969=VERTEX_POINT('',#387148);
#39970=VERTEX_POINT('',#387150);
#39971=VERTEX_POINT('',#387155);
#39972=VERTEX_POINT('',#387157);
#39973=VERTEX_POINT('',#387229);
#39974=VERTEX_POINT('',#387261);
#39975=VERTEX_POINT('',#387292);
#39976=VERTEX_POINT('',#387431);
#39977=VERTEX_POINT('',#387432);
#39978=VERTEX_POINT('',#387434);
#39979=VERTEX_POINT('',#387439);
#39980=VERTEX_POINT('',#387441);
#39981=VERTEX_POINT('',#387451);
#39982=VERTEX_POINT('',#387452);
#39983=VERTEX_POINT('',#387454);
#39984=VERTEX_POINT('',#387459);
#39985=VERTEX_POINT('',#387461);
#39986=VERTEX_POINT('',#387533);
#39987=VERTEX_POINT('',#387565);
#39988=VERTEX_POINT('',#387596);
#39989=VERTEX_POINT('',#387735);
#39990=VERTEX_POINT('',#387736);
#39991=VERTEX_POINT('',#387738);
#39992=VERTEX_POINT('',#387743);
#39993=VERTEX_POINT('',#387745);
#39994=VERTEX_POINT('',#387755);
#39995=VERTEX_POINT('',#387756);
#39996=VERTEX_POINT('',#387758);
#39997=VERTEX_POINT('',#387763);
#39998=VERTEX_POINT('',#387765);
#39999=VERTEX_POINT('',#387837);
#40000=VERTEX_POINT('',#387869);
#40001=VERTEX_POINT('',#387900);
#40002=VERTEX_POINT('',#388039);
#40003=VERTEX_POINT('',#388040);
#40004=VERTEX_POINT('',#388042);
#40005=VERTEX_POINT('',#388047);
#40006=VERTEX_POINT('',#388049);
#40007=VERTEX_POINT('',#388059);
#40008=VERTEX_POINT('',#388060);
#40009=VERTEX_POINT('',#388062);
#40010=VERTEX_POINT('',#388067);
#40011=VERTEX_POINT('',#388069);
#40012=VERTEX_POINT('',#388141);
#40013=VERTEX_POINT('',#388173);
#40014=VERTEX_POINT('',#388204);
#40015=VERTEX_POINT('',#388343);
#40016=VERTEX_POINT('',#388344);
#40017=VERTEX_POINT('',#388346);
#40018=VERTEX_POINT('',#388351);
#40019=VERTEX_POINT('',#388353);
#40020=VERTEX_POINT('',#388363);
#40021=VERTEX_POINT('',#388364);
#40022=VERTEX_POINT('',#388366);
#40023=VERTEX_POINT('',#388371);
#40024=VERTEX_POINT('',#388373);
#40025=VERTEX_POINT('',#388445);
#40026=VERTEX_POINT('',#388477);
#40027=VERTEX_POINT('',#388508);
#40028=VERTEX_POINT('',#388647);
#40029=VERTEX_POINT('',#388648);
#40030=VERTEX_POINT('',#388650);
#40031=VERTEX_POINT('',#388655);
#40032=VERTEX_POINT('',#388657);
#40033=VERTEX_POINT('',#388667);
#40034=VERTEX_POINT('',#388668);
#40035=VERTEX_POINT('',#388670);
#40036=VERTEX_POINT('',#388675);
#40037=VERTEX_POINT('',#388677);
#40038=VERTEX_POINT('',#388749);
#40039=VERTEX_POINT('',#388781);
#40040=VERTEX_POINT('',#388812);
#40041=VERTEX_POINT('',#388951);
#40042=VERTEX_POINT('',#388952);
#40043=VERTEX_POINT('',#388954);
#40044=VERTEX_POINT('',#388959);
#40045=VERTEX_POINT('',#388961);
#40046=VERTEX_POINT('',#388971);
#40047=VERTEX_POINT('',#388972);
#40048=VERTEX_POINT('',#388974);
#40049=VERTEX_POINT('',#388979);
#40050=VERTEX_POINT('',#388981);
#40051=VERTEX_POINT('',#389053);
#40052=VERTEX_POINT('',#389085);
#40053=VERTEX_POINT('',#389116);
#40054=VERTEX_POINT('',#389255);
#40055=VERTEX_POINT('',#389256);
#40056=VERTEX_POINT('',#389258);
#40057=VERTEX_POINT('',#389263);
#40058=VERTEX_POINT('',#389265);
#40059=VERTEX_POINT('',#389275);
#40060=VERTEX_POINT('',#389276);
#40061=VERTEX_POINT('',#389278);
#40062=VERTEX_POINT('',#389283);
#40063=VERTEX_POINT('',#389285);
#40064=VERTEX_POINT('',#389357);
#40065=VERTEX_POINT('',#389389);
#40066=VERTEX_POINT('',#389420);
#40067=VERTEX_POINT('',#389559);
#40068=VERTEX_POINT('',#389560);
#40069=VERTEX_POINT('',#389562);
#40070=VERTEX_POINT('',#389567);
#40071=VERTEX_POINT('',#389569);
#40072=VERTEX_POINT('',#389579);
#40073=VERTEX_POINT('',#389580);
#40074=VERTEX_POINT('',#389582);
#40075=VERTEX_POINT('',#389587);
#40076=VERTEX_POINT('',#389589);
#40077=VERTEX_POINT('',#389661);
#40078=VERTEX_POINT('',#389693);
#40079=VERTEX_POINT('',#389724);
#40080=VERTEX_POINT('',#389863);
#40081=VERTEX_POINT('',#389864);
#40082=VERTEX_POINT('',#389866);
#40083=VERTEX_POINT('',#389871);
#40084=VERTEX_POINT('',#389873);
#40085=VERTEX_POINT('',#389883);
#40086=VERTEX_POINT('',#389884);
#40087=VERTEX_POINT('',#389886);
#40088=VERTEX_POINT('',#389891);
#40089=VERTEX_POINT('',#389893);
#40090=VERTEX_POINT('',#389965);
#40091=VERTEX_POINT('',#389997);
#40092=VERTEX_POINT('',#390028);
#40093=VERTEX_POINT('',#390167);
#40094=VERTEX_POINT('',#390168);
#40095=VERTEX_POINT('',#390170);
#40096=VERTEX_POINT('',#390175);
#40097=VERTEX_POINT('',#390177);
#40098=VERTEX_POINT('',#390187);
#40099=VERTEX_POINT('',#390188);
#40100=VERTEX_POINT('',#390190);
#40101=VERTEX_POINT('',#390195);
#40102=VERTEX_POINT('',#390197);
#40103=VERTEX_POINT('',#390269);
#40104=VERTEX_POINT('',#390301);
#40105=VERTEX_POINT('',#390332);
#40106=VERTEX_POINT('',#390471);
#40107=VERTEX_POINT('',#390472);
#40108=VERTEX_POINT('',#390474);
#40109=VERTEX_POINT('',#390479);
#40110=VERTEX_POINT('',#390481);
#40111=VERTEX_POINT('',#390491);
#40112=VERTEX_POINT('',#390492);
#40113=VERTEX_POINT('',#390494);
#40114=VERTEX_POINT('',#390499);
#40115=VERTEX_POINT('',#390501);
#40116=VERTEX_POINT('',#390573);
#40117=VERTEX_POINT('',#390605);
#40118=VERTEX_POINT('',#390636);
#40119=VERTEX_POINT('',#390775);
#40120=VERTEX_POINT('',#390776);
#40121=VERTEX_POINT('',#390778);
#40122=VERTEX_POINT('',#390783);
#40123=VERTEX_POINT('',#390785);
#40124=VERTEX_POINT('',#390795);
#40125=VERTEX_POINT('',#390796);
#40126=VERTEX_POINT('',#390798);
#40127=VERTEX_POINT('',#390803);
#40128=VERTEX_POINT('',#390805);
#40129=VERTEX_POINT('',#390877);
#40130=VERTEX_POINT('',#390909);
#40131=VERTEX_POINT('',#390940);
#40132=VERTEX_POINT('',#391079);
#40133=VERTEX_POINT('',#391080);
#40134=VERTEX_POINT('',#391082);
#40135=VERTEX_POINT('',#391087);
#40136=VERTEX_POINT('',#391089);
#40137=VERTEX_POINT('',#391099);
#40138=VERTEX_POINT('',#391100);
#40139=VERTEX_POINT('',#391102);
#40140=VERTEX_POINT('',#391107);
#40141=VERTEX_POINT('',#391109);
#40142=VERTEX_POINT('',#391181);
#40143=VERTEX_POINT('',#391213);
#40144=VERTEX_POINT('',#391244);
#40145=VERTEX_POINT('',#391383);
#40146=VERTEX_POINT('',#391384);
#40147=VERTEX_POINT('',#391386);
#40148=VERTEX_POINT('',#391391);
#40149=VERTEX_POINT('',#391393);
#40150=VERTEX_POINT('',#391403);
#40151=VERTEX_POINT('',#391404);
#40152=VERTEX_POINT('',#391406);
#40153=VERTEX_POINT('',#391411);
#40154=VERTEX_POINT('',#391413);
#40155=VERTEX_POINT('',#391485);
#40156=VERTEX_POINT('',#391517);
#40157=VERTEX_POINT('',#391548);
#40158=VERTEX_POINT('',#391687);
#40159=VERTEX_POINT('',#391688);
#40160=VERTEX_POINT('',#391690);
#40161=VERTEX_POINT('',#391695);
#40162=VERTEX_POINT('',#391697);
#40163=VERTEX_POINT('',#391707);
#40164=VERTEX_POINT('',#391708);
#40165=VERTEX_POINT('',#391710);
#40166=VERTEX_POINT('',#391715);
#40167=VERTEX_POINT('',#391717);
#40168=VERTEX_POINT('',#391789);
#40169=VERTEX_POINT('',#391821);
#40170=VERTEX_POINT('',#391852);
#40171=VERTEX_POINT('',#391991);
#40172=VERTEX_POINT('',#391992);
#40173=VERTEX_POINT('',#391994);
#40174=VERTEX_POINT('',#391999);
#40175=VERTEX_POINT('',#392001);
#40176=VERTEX_POINT('',#392011);
#40177=VERTEX_POINT('',#392012);
#40178=VERTEX_POINT('',#392014);
#40179=VERTEX_POINT('',#392019);
#40180=VERTEX_POINT('',#392021);
#40181=VERTEX_POINT('',#392093);
#40182=VERTEX_POINT('',#392125);
#40183=VERTEX_POINT('',#392156);
#40184=VERTEX_POINT('',#392295);
#40185=VERTEX_POINT('',#392296);
#40186=VERTEX_POINT('',#392298);
#40187=VERTEX_POINT('',#392303);
#40188=VERTEX_POINT('',#392305);
#40189=VERTEX_POINT('',#392315);
#40190=VERTEX_POINT('',#392316);
#40191=VERTEX_POINT('',#392318);
#40192=VERTEX_POINT('',#392323);
#40193=VERTEX_POINT('',#392325);
#40194=VERTEX_POINT('',#392397);
#40195=VERTEX_POINT('',#392429);
#40196=VERTEX_POINT('',#392460);
#40197=VERTEX_POINT('',#392599);
#40198=VERTEX_POINT('',#392600);
#40199=VERTEX_POINT('',#392602);
#40200=VERTEX_POINT('',#392607);
#40201=VERTEX_POINT('',#392609);
#40202=VERTEX_POINT('',#392619);
#40203=VERTEX_POINT('',#392620);
#40204=VERTEX_POINT('',#392622);
#40205=VERTEX_POINT('',#392627);
#40206=VERTEX_POINT('',#392629);
#40207=VERTEX_POINT('',#392701);
#40208=VERTEX_POINT('',#392733);
#40209=VERTEX_POINT('',#392764);
#40210=VERTEX_POINT('',#392903);
#40211=VERTEX_POINT('',#392904);
#40212=VERTEX_POINT('',#392906);
#40213=VERTEX_POINT('',#392911);
#40214=VERTEX_POINT('',#392913);
#40215=VERTEX_POINT('',#392923);
#40216=VERTEX_POINT('',#392924);
#40217=VERTEX_POINT('',#392926);
#40218=VERTEX_POINT('',#392931);
#40219=VERTEX_POINT('',#392933);
#40220=VERTEX_POINT('',#393005);
#40221=VERTEX_POINT('',#393037);
#40222=VERTEX_POINT('',#393068);
#40223=VERTEX_POINT('',#393207);
#40224=VERTEX_POINT('',#393208);
#40225=VERTEX_POINT('',#393210);
#40226=VERTEX_POINT('',#393215);
#40227=VERTEX_POINT('',#393217);
#40228=VERTEX_POINT('',#393227);
#40229=VERTEX_POINT('',#393228);
#40230=VERTEX_POINT('',#393230);
#40231=VERTEX_POINT('',#393235);
#40232=VERTEX_POINT('',#393237);
#40233=VERTEX_POINT('',#393309);
#40234=VERTEX_POINT('',#393341);
#40235=VERTEX_POINT('',#393372);
#40236=VERTEX_POINT('',#393511);
#40237=VERTEX_POINT('',#393512);
#40238=VERTEX_POINT('',#393514);
#40239=VERTEX_POINT('',#393519);
#40240=VERTEX_POINT('',#393521);
#40241=VERTEX_POINT('',#393531);
#40242=VERTEX_POINT('',#393532);
#40243=VERTEX_POINT('',#393534);
#40244=VERTEX_POINT('',#393539);
#40245=VERTEX_POINT('',#393541);
#40246=VERTEX_POINT('',#393613);
#40247=VERTEX_POINT('',#393645);
#40248=VERTEX_POINT('',#393676);
#40249=VERTEX_POINT('',#393815);
#40250=VERTEX_POINT('',#393816);
#40251=VERTEX_POINT('',#393818);
#40252=VERTEX_POINT('',#393823);
#40253=VERTEX_POINT('',#393825);
#40254=VERTEX_POINT('',#393835);
#40255=VERTEX_POINT('',#393836);
#40256=VERTEX_POINT('',#393838);
#40257=VERTEX_POINT('',#393843);
#40258=VERTEX_POINT('',#393845);
#40259=VERTEX_POINT('',#393917);
#40260=VERTEX_POINT('',#393949);
#40261=VERTEX_POINT('',#393980);
#40262=VERTEX_POINT('',#394119);
#40263=VERTEX_POINT('',#394120);
#40264=VERTEX_POINT('',#394122);
#40265=VERTEX_POINT('',#394127);
#40266=VERTEX_POINT('',#394129);
#40267=VERTEX_POINT('',#394139);
#40268=VERTEX_POINT('',#394140);
#40269=VERTEX_POINT('',#394142);
#40270=VERTEX_POINT('',#394147);
#40271=VERTEX_POINT('',#394149);
#40272=VERTEX_POINT('',#394221);
#40273=VERTEX_POINT('',#394253);
#40274=VERTEX_POINT('',#394284);
#40275=VERTEX_POINT('',#394423);
#40276=VERTEX_POINT('',#394424);
#40277=VERTEX_POINT('',#394426);
#40278=VERTEX_POINT('',#394431);
#40279=VERTEX_POINT('',#394433);
#40280=VERTEX_POINT('',#394443);
#40281=VERTEX_POINT('',#394444);
#40282=VERTEX_POINT('',#394446);
#40283=VERTEX_POINT('',#394451);
#40284=VERTEX_POINT('',#394453);
#40285=VERTEX_POINT('',#394525);
#40286=VERTEX_POINT('',#394557);
#40287=VERTEX_POINT('',#394588);
#40288=VERTEX_POINT('',#394727);
#40289=VERTEX_POINT('',#394728);
#40290=VERTEX_POINT('',#394730);
#40291=VERTEX_POINT('',#394735);
#40292=VERTEX_POINT('',#394737);
#40293=VERTEX_POINT('',#394747);
#40294=VERTEX_POINT('',#394748);
#40295=VERTEX_POINT('',#394750);
#40296=VERTEX_POINT('',#394755);
#40297=VERTEX_POINT('',#394757);
#40298=VERTEX_POINT('',#394829);
#40299=VERTEX_POINT('',#394861);
#40300=VERTEX_POINT('',#394892);
#40301=VERTEX_POINT('',#395031);
#40302=VERTEX_POINT('',#395032);
#40303=VERTEX_POINT('',#395034);
#40304=VERTEX_POINT('',#395039);
#40305=VERTEX_POINT('',#395041);
#40306=VERTEX_POINT('',#395051);
#40307=VERTEX_POINT('',#395052);
#40308=VERTEX_POINT('',#395054);
#40309=VERTEX_POINT('',#395059);
#40310=VERTEX_POINT('',#395061);
#40311=VERTEX_POINT('',#395133);
#40312=VERTEX_POINT('',#395165);
#40313=VERTEX_POINT('',#395196);
#40314=VERTEX_POINT('',#395335);
#40315=VERTEX_POINT('',#395336);
#40316=VERTEX_POINT('',#395338);
#40317=VERTEX_POINT('',#395343);
#40318=VERTEX_POINT('',#395345);
#40319=VERTEX_POINT('',#395355);
#40320=VERTEX_POINT('',#395356);
#40321=VERTEX_POINT('',#395358);
#40322=VERTEX_POINT('',#395363);
#40323=VERTEX_POINT('',#395365);
#40324=VERTEX_POINT('',#395437);
#40325=VERTEX_POINT('',#395469);
#40326=VERTEX_POINT('',#395500);
#40327=VERTEX_POINT('',#395639);
#40328=VERTEX_POINT('',#395640);
#40329=VERTEX_POINT('',#395642);
#40330=VERTEX_POINT('',#395647);
#40331=VERTEX_POINT('',#395649);
#40332=VERTEX_POINT('',#395659);
#40333=VERTEX_POINT('',#395660);
#40334=VERTEX_POINT('',#395662);
#40335=VERTEX_POINT('',#395667);
#40336=VERTEX_POINT('',#395669);
#40337=VERTEX_POINT('',#395741);
#40338=VERTEX_POINT('',#395773);
#40339=VERTEX_POINT('',#395804);
#40340=VERTEX_POINT('',#395943);
#40341=VERTEX_POINT('',#395944);
#40342=VERTEX_POINT('',#395946);
#40343=VERTEX_POINT('',#395951);
#40344=VERTEX_POINT('',#395953);
#40345=VERTEX_POINT('',#395963);
#40346=VERTEX_POINT('',#395964);
#40347=VERTEX_POINT('',#395966);
#40348=VERTEX_POINT('',#395971);
#40349=VERTEX_POINT('',#395973);
#40350=VERTEX_POINT('',#396045);
#40351=VERTEX_POINT('',#396077);
#40352=VERTEX_POINT('',#396108);
#40353=VERTEX_POINT('',#396247);
#40354=VERTEX_POINT('',#396248);
#40355=VERTEX_POINT('',#396250);
#40356=VERTEX_POINT('',#396255);
#40357=VERTEX_POINT('',#396257);
#40358=VERTEX_POINT('',#396267);
#40359=VERTEX_POINT('',#396268);
#40360=VERTEX_POINT('',#396270);
#40361=VERTEX_POINT('',#396275);
#40362=VERTEX_POINT('',#396277);
#40363=VERTEX_POINT('',#396349);
#40364=VERTEX_POINT('',#396381);
#40365=VERTEX_POINT('',#396412);
#40366=VERTEX_POINT('',#396551);
#40367=VERTEX_POINT('',#396552);
#40368=VERTEX_POINT('',#396554);
#40369=VERTEX_POINT('',#396559);
#40370=VERTEX_POINT('',#396561);
#40371=VERTEX_POINT('',#396571);
#40372=VERTEX_POINT('',#396572);
#40373=VERTEX_POINT('',#396574);
#40374=VERTEX_POINT('',#396579);
#40375=VERTEX_POINT('',#396581);
#40376=VERTEX_POINT('',#396653);
#40377=VERTEX_POINT('',#396685);
#40378=VERTEX_POINT('',#396716);
#40379=VERTEX_POINT('',#396855);
#40380=VERTEX_POINT('',#396856);
#40381=VERTEX_POINT('',#396858);
#40382=VERTEX_POINT('',#396863);
#40383=VERTEX_POINT('',#396865);
#40384=VERTEX_POINT('',#396875);
#40385=VERTEX_POINT('',#396876);
#40386=VERTEX_POINT('',#396878);
#40387=VERTEX_POINT('',#396883);
#40388=VERTEX_POINT('',#396885);
#40389=VERTEX_POINT('',#396957);
#40390=VERTEX_POINT('',#396989);
#40391=VERTEX_POINT('',#397020);
#40392=VERTEX_POINT('',#397159);
#40393=VERTEX_POINT('',#397160);
#40394=VERTEX_POINT('',#397162);
#40395=VERTEX_POINT('',#397167);
#40396=VERTEX_POINT('',#397169);
#40397=VERTEX_POINT('',#397179);
#40398=VERTEX_POINT('',#397180);
#40399=VERTEX_POINT('',#397182);
#40400=VERTEX_POINT('',#397187);
#40401=VERTEX_POINT('',#397189);
#40402=VERTEX_POINT('',#397261);
#40403=VERTEX_POINT('',#397293);
#40404=VERTEX_POINT('',#397324);
#40405=VERTEX_POINT('',#397463);
#40406=VERTEX_POINT('',#397464);
#40407=VERTEX_POINT('',#397466);
#40408=VERTEX_POINT('',#397471);
#40409=VERTEX_POINT('',#397473);
#40410=VERTEX_POINT('',#397483);
#40411=VERTEX_POINT('',#397484);
#40412=VERTEX_POINT('',#397486);
#40413=VERTEX_POINT('',#397491);
#40414=VERTEX_POINT('',#397493);
#40415=VERTEX_POINT('',#397565);
#40416=VERTEX_POINT('',#397597);
#40417=VERTEX_POINT('',#397628);
#40418=VERTEX_POINT('',#397767);
#40419=VERTEX_POINT('',#397768);
#40420=VERTEX_POINT('',#397770);
#40421=VERTEX_POINT('',#397775);
#40422=VERTEX_POINT('',#397777);
#40423=VERTEX_POINT('',#397787);
#40424=VERTEX_POINT('',#397788);
#40425=VERTEX_POINT('',#397790);
#40426=VERTEX_POINT('',#397795);
#40427=VERTEX_POINT('',#397797);
#40428=VERTEX_POINT('',#397869);
#40429=VERTEX_POINT('',#397901);
#40430=VERTEX_POINT('',#397932);
#40431=VERTEX_POINT('',#398071);
#40432=VERTEX_POINT('',#398072);
#40433=VERTEX_POINT('',#398074);
#40434=VERTEX_POINT('',#398079);
#40435=VERTEX_POINT('',#398081);
#40436=VERTEX_POINT('',#398091);
#40437=VERTEX_POINT('',#398092);
#40438=VERTEX_POINT('',#398094);
#40439=VERTEX_POINT('',#398099);
#40440=VERTEX_POINT('',#398101);
#40441=VERTEX_POINT('',#398173);
#40442=VERTEX_POINT('',#398205);
#40443=VERTEX_POINT('',#398236);
#40444=VERTEX_POINT('',#398375);
#40445=VERTEX_POINT('',#398376);
#40446=VERTEX_POINT('',#398378);
#40447=VERTEX_POINT('',#398383);
#40448=VERTEX_POINT('',#398385);
#40449=VERTEX_POINT('',#398395);
#40450=VERTEX_POINT('',#398396);
#40451=VERTEX_POINT('',#398398);
#40452=VERTEX_POINT('',#398403);
#40453=VERTEX_POINT('',#398405);
#40454=VERTEX_POINT('',#398477);
#40455=VERTEX_POINT('',#398509);
#40456=VERTEX_POINT('',#398540);
#40457=VERTEX_POINT('',#398679);
#40458=VERTEX_POINT('',#398680);
#40459=VERTEX_POINT('',#398682);
#40460=VERTEX_POINT('',#398687);
#40461=VERTEX_POINT('',#398689);
#40462=VERTEX_POINT('',#398699);
#40463=VERTEX_POINT('',#398700);
#40464=VERTEX_POINT('',#398702);
#40465=VERTEX_POINT('',#398707);
#40466=VERTEX_POINT('',#398709);
#40467=VERTEX_POINT('',#398781);
#40468=VERTEX_POINT('',#398813);
#40469=VERTEX_POINT('',#398844);
#40470=VERTEX_POINT('',#398983);
#40471=VERTEX_POINT('',#398984);
#40472=VERTEX_POINT('',#398986);
#40473=VERTEX_POINT('',#398991);
#40474=VERTEX_POINT('',#398993);
#40475=VERTEX_POINT('',#399003);
#40476=VERTEX_POINT('',#399004);
#40477=VERTEX_POINT('',#399006);
#40478=VERTEX_POINT('',#399011);
#40479=VERTEX_POINT('',#399013);
#40480=VERTEX_POINT('',#399085);
#40481=VERTEX_POINT('',#399117);
#40482=VERTEX_POINT('',#399148);
#40483=VERTEX_POINT('',#399287);
#40484=VERTEX_POINT('',#399288);
#40485=VERTEX_POINT('',#399290);
#40486=VERTEX_POINT('',#399295);
#40487=VERTEX_POINT('',#399297);
#40488=VERTEX_POINT('',#399307);
#40489=VERTEX_POINT('',#399308);
#40490=VERTEX_POINT('',#399310);
#40491=VERTEX_POINT('',#399315);
#40492=VERTEX_POINT('',#399317);
#40493=VERTEX_POINT('',#399389);
#40494=VERTEX_POINT('',#399421);
#40495=VERTEX_POINT('',#399452);
#40496=VERTEX_POINT('',#399591);
#40497=VERTEX_POINT('',#399592);
#40498=VERTEX_POINT('',#399594);
#40499=VERTEX_POINT('',#399599);
#40500=VERTEX_POINT('',#399601);
#40501=VERTEX_POINT('',#399611);
#40502=VERTEX_POINT('',#399612);
#40503=VERTEX_POINT('',#399614);
#40504=VERTEX_POINT('',#399619);
#40505=VERTEX_POINT('',#399621);
#40506=VERTEX_POINT('',#399693);
#40507=VERTEX_POINT('',#399725);
#40508=VERTEX_POINT('',#399756);
#40509=VERTEX_POINT('',#399895);
#40510=VERTEX_POINT('',#399896);
#40511=VERTEX_POINT('',#399898);
#40512=VERTEX_POINT('',#399903);
#40513=VERTEX_POINT('',#399905);
#40514=VERTEX_POINT('',#399915);
#40515=VERTEX_POINT('',#399916);
#40516=VERTEX_POINT('',#399918);
#40517=VERTEX_POINT('',#399923);
#40518=VERTEX_POINT('',#399925);
#40519=VERTEX_POINT('',#399997);
#40520=VERTEX_POINT('',#400029);
#40521=VERTEX_POINT('',#400060);
#40522=VERTEX_POINT('',#400199);
#40523=VERTEX_POINT('',#400200);
#40524=VERTEX_POINT('',#400202);
#40525=VERTEX_POINT('',#400207);
#40526=VERTEX_POINT('',#400209);
#40527=VERTEX_POINT('',#400219);
#40528=VERTEX_POINT('',#400220);
#40529=VERTEX_POINT('',#400222);
#40530=VERTEX_POINT('',#400227);
#40531=VERTEX_POINT('',#400229);
#40532=VERTEX_POINT('',#400301);
#40533=VERTEX_POINT('',#400333);
#40534=VERTEX_POINT('',#400364);
#40535=VERTEX_POINT('',#400503);
#40536=VERTEX_POINT('',#400504);
#40537=VERTEX_POINT('',#400506);
#40538=VERTEX_POINT('',#400511);
#40539=VERTEX_POINT('',#400513);
#40540=VERTEX_POINT('',#400523);
#40541=VERTEX_POINT('',#400524);
#40542=VERTEX_POINT('',#400526);
#40543=VERTEX_POINT('',#400531);
#40544=VERTEX_POINT('',#400533);
#40545=VERTEX_POINT('',#400605);
#40546=VERTEX_POINT('',#400637);
#40547=VERTEX_POINT('',#400668);
#40548=VERTEX_POINT('',#400807);
#40549=VERTEX_POINT('',#400808);
#40550=VERTEX_POINT('',#400810);
#40551=VERTEX_POINT('',#400815);
#40552=VERTEX_POINT('',#400817);
#40553=VERTEX_POINT('',#400827);
#40554=VERTEX_POINT('',#400828);
#40555=VERTEX_POINT('',#400830);
#40556=VERTEX_POINT('',#400835);
#40557=VERTEX_POINT('',#400837);
#40558=VERTEX_POINT('',#400909);
#40559=VERTEX_POINT('',#400941);
#40560=VERTEX_POINT('',#400972);
#40561=VERTEX_POINT('',#401111);
#40562=VERTEX_POINT('',#401112);
#40563=VERTEX_POINT('',#401114);
#40564=VERTEX_POINT('',#401119);
#40565=VERTEX_POINT('',#401121);
#40566=VERTEX_POINT('',#401131);
#40567=VERTEX_POINT('',#401132);
#40568=VERTEX_POINT('',#401134);
#40569=VERTEX_POINT('',#401139);
#40570=VERTEX_POINT('',#401141);
#40571=VERTEX_POINT('',#401213);
#40572=VERTEX_POINT('',#401245);
#40573=VERTEX_POINT('',#401276);
#40574=VERTEX_POINT('',#401415);
#40575=VERTEX_POINT('',#401416);
#40576=VERTEX_POINT('',#401418);
#40577=VERTEX_POINT('',#401423);
#40578=VERTEX_POINT('',#401425);
#40579=VERTEX_POINT('',#401435);
#40580=VERTEX_POINT('',#401436);
#40581=VERTEX_POINT('',#401438);
#40582=VERTEX_POINT('',#401443);
#40583=VERTEX_POINT('',#401445);
#40584=VERTEX_POINT('',#401517);
#40585=VERTEX_POINT('',#401549);
#40586=VERTEX_POINT('',#401580);
#40587=VERTEX_POINT('',#401719);
#40588=VERTEX_POINT('',#401720);
#40589=VERTEX_POINT('',#401722);
#40590=VERTEX_POINT('',#401727);
#40591=VERTEX_POINT('',#401729);
#40592=VERTEX_POINT('',#401739);
#40593=VERTEX_POINT('',#401740);
#40594=VERTEX_POINT('',#401742);
#40595=VERTEX_POINT('',#401747);
#40596=VERTEX_POINT('',#401749);
#40597=VERTEX_POINT('',#401821);
#40598=VERTEX_POINT('',#401853);
#40599=VERTEX_POINT('',#401884);
#40600=VERTEX_POINT('',#402023);
#40601=VERTEX_POINT('',#402024);
#40602=VERTEX_POINT('',#402026);
#40603=VERTEX_POINT('',#402031);
#40604=VERTEX_POINT('',#402033);
#40605=VERTEX_POINT('',#402043);
#40606=VERTEX_POINT('',#402044);
#40607=VERTEX_POINT('',#402046);
#40608=VERTEX_POINT('',#402051);
#40609=VERTEX_POINT('',#402053);
#40610=VERTEX_POINT('',#402125);
#40611=VERTEX_POINT('',#402157);
#40612=VERTEX_POINT('',#402188);
#40613=VERTEX_POINT('',#402327);
#40614=VERTEX_POINT('',#402328);
#40615=VERTEX_POINT('',#402330);
#40616=VERTEX_POINT('',#402335);
#40617=VERTEX_POINT('',#402337);
#40618=VERTEX_POINT('',#402347);
#40619=VERTEX_POINT('',#402348);
#40620=VERTEX_POINT('',#402350);
#40621=VERTEX_POINT('',#402355);
#40622=VERTEX_POINT('',#402357);
#40623=VERTEX_POINT('',#402429);
#40624=VERTEX_POINT('',#402461);
#40625=VERTEX_POINT('',#402492);
#40626=VERTEX_POINT('',#402631);
#40627=VERTEX_POINT('',#402632);
#40628=VERTEX_POINT('',#402634);
#40629=VERTEX_POINT('',#402639);
#40630=VERTEX_POINT('',#402641);
#40631=VERTEX_POINT('',#402651);
#40632=VERTEX_POINT('',#402652);
#40633=VERTEX_POINT('',#402654);
#40634=VERTEX_POINT('',#402659);
#40635=VERTEX_POINT('',#402661);
#40636=VERTEX_POINT('',#402733);
#40637=VERTEX_POINT('',#402765);
#40638=VERTEX_POINT('',#402796);
#40639=VERTEX_POINT('',#402935);
#40640=VERTEX_POINT('',#402936);
#40641=VERTEX_POINT('',#402938);
#40642=VERTEX_POINT('',#402943);
#40643=VERTEX_POINT('',#402945);
#40644=VERTEX_POINT('',#402955);
#40645=VERTEX_POINT('',#402956);
#40646=VERTEX_POINT('',#402958);
#40647=VERTEX_POINT('',#402963);
#40648=VERTEX_POINT('',#402965);
#40649=VERTEX_POINT('',#403037);
#40650=VERTEX_POINT('',#403069);
#40651=VERTEX_POINT('',#403100);
#40652=VERTEX_POINT('',#403239);
#40653=VERTEX_POINT('',#403240);
#40654=VERTEX_POINT('',#403242);
#40655=VERTEX_POINT('',#403247);
#40656=VERTEX_POINT('',#403249);
#40657=VERTEX_POINT('',#403259);
#40658=VERTEX_POINT('',#403260);
#40659=VERTEX_POINT('',#403262);
#40660=VERTEX_POINT('',#403267);
#40661=VERTEX_POINT('',#403269);
#40662=VERTEX_POINT('',#403341);
#40663=VERTEX_POINT('',#403373);
#40664=VERTEX_POINT('',#403404);
#40665=VERTEX_POINT('',#403543);
#40666=VERTEX_POINT('',#403544);
#40667=VERTEX_POINT('',#403546);
#40668=VERTEX_POINT('',#403551);
#40669=VERTEX_POINT('',#403553);
#40670=VERTEX_POINT('',#403563);
#40671=VERTEX_POINT('',#403564);
#40672=VERTEX_POINT('',#403566);
#40673=VERTEX_POINT('',#403571);
#40674=VERTEX_POINT('',#403573);
#40675=VERTEX_POINT('',#403645);
#40676=VERTEX_POINT('',#403677);
#40677=VERTEX_POINT('',#403708);
#40678=VERTEX_POINT('',#403847);
#40679=VERTEX_POINT('',#403848);
#40680=VERTEX_POINT('',#403850);
#40681=VERTEX_POINT('',#403855);
#40682=VERTEX_POINT('',#403857);
#40683=VERTEX_POINT('',#403867);
#40684=VERTEX_POINT('',#403868);
#40685=VERTEX_POINT('',#403870);
#40686=VERTEX_POINT('',#403875);
#40687=VERTEX_POINT('',#403877);
#40688=VERTEX_POINT('',#403949);
#40689=VERTEX_POINT('',#403981);
#40690=VERTEX_POINT('',#404012);
#40691=VERTEX_POINT('',#404151);
#40692=VERTEX_POINT('',#404152);
#40693=VERTEX_POINT('',#404154);
#40694=VERTEX_POINT('',#404159);
#40695=VERTEX_POINT('',#404161);
#40696=VERTEX_POINT('',#404171);
#40697=VERTEX_POINT('',#404172);
#40698=VERTEX_POINT('',#404174);
#40699=VERTEX_POINT('',#404179);
#40700=VERTEX_POINT('',#404181);
#40701=VERTEX_POINT('',#404253);
#40702=VERTEX_POINT('',#404285);
#40703=VERTEX_POINT('',#404316);
#40704=VERTEX_POINT('',#404455);
#40705=VERTEX_POINT('',#404456);
#40706=VERTEX_POINT('',#404458);
#40707=VERTEX_POINT('',#404463);
#40708=VERTEX_POINT('',#404465);
#40709=VERTEX_POINT('',#404475);
#40710=VERTEX_POINT('',#404476);
#40711=VERTEX_POINT('',#404478);
#40712=VERTEX_POINT('',#404483);
#40713=VERTEX_POINT('',#404485);
#40714=VERTEX_POINT('',#404557);
#40715=VERTEX_POINT('',#404589);
#40716=VERTEX_POINT('',#404620);
#40717=VERTEX_POINT('',#404759);
#40718=VERTEX_POINT('',#404760);
#40719=VERTEX_POINT('',#404762);
#40720=VERTEX_POINT('',#404767);
#40721=VERTEX_POINT('',#404769);
#40722=VERTEX_POINT('',#404779);
#40723=VERTEX_POINT('',#404780);
#40724=VERTEX_POINT('',#404782);
#40725=VERTEX_POINT('',#404787);
#40726=VERTEX_POINT('',#404789);
#40727=VERTEX_POINT('',#404861);
#40728=VERTEX_POINT('',#404893);
#40729=VERTEX_POINT('',#404924);
#40730=VERTEX_POINT('',#405063);
#40731=VERTEX_POINT('',#405064);
#40732=VERTEX_POINT('',#405066);
#40733=VERTEX_POINT('',#405071);
#40734=VERTEX_POINT('',#405073);
#40735=VERTEX_POINT('',#405083);
#40736=VERTEX_POINT('',#405084);
#40737=VERTEX_POINT('',#405086);
#40738=VERTEX_POINT('',#405091);
#40739=VERTEX_POINT('',#405093);
#40740=VERTEX_POINT('',#405165);
#40741=VERTEX_POINT('',#405197);
#40742=VERTEX_POINT('',#405228);
#40743=VERTEX_POINT('',#405367);
#40744=VERTEX_POINT('',#405368);
#40745=VERTEX_POINT('',#405370);
#40746=VERTEX_POINT('',#405375);
#40747=VERTEX_POINT('',#405377);
#40748=VERTEX_POINT('',#405387);
#40749=VERTEX_POINT('',#405388);
#40750=VERTEX_POINT('',#405390);
#40751=VERTEX_POINT('',#405395);
#40752=VERTEX_POINT('',#405397);
#40753=VERTEX_POINT('',#405469);
#40754=VERTEX_POINT('',#405501);
#40755=VERTEX_POINT('',#405532);
#40756=VERTEX_POINT('',#405671);
#40757=VERTEX_POINT('',#405672);
#40758=VERTEX_POINT('',#405674);
#40759=VERTEX_POINT('',#405679);
#40760=VERTEX_POINT('',#405681);
#40761=VERTEX_POINT('',#405691);
#40762=VERTEX_POINT('',#405692);
#40763=VERTEX_POINT('',#405694);
#40764=VERTEX_POINT('',#405699);
#40765=VERTEX_POINT('',#405701);
#40766=VERTEX_POINT('',#405773);
#40767=VERTEX_POINT('',#405805);
#40768=VERTEX_POINT('',#405836);
#40769=VERTEX_POINT('',#405975);
#40770=VERTEX_POINT('',#405976);
#40771=VERTEX_POINT('',#405978);
#40772=VERTEX_POINT('',#405983);
#40773=VERTEX_POINT('',#405985);
#40774=VERTEX_POINT('',#405995);
#40775=VERTEX_POINT('',#405996);
#40776=VERTEX_POINT('',#405998);
#40777=VERTEX_POINT('',#406003);
#40778=VERTEX_POINT('',#406005);
#40779=VERTEX_POINT('',#406077);
#40780=VERTEX_POINT('',#406109);
#40781=VERTEX_POINT('',#406140);
#40782=VERTEX_POINT('',#406279);
#40783=VERTEX_POINT('',#406280);
#40784=VERTEX_POINT('',#406282);
#40785=VERTEX_POINT('',#406287);
#40786=VERTEX_POINT('',#406289);
#40787=VERTEX_POINT('',#406299);
#40788=VERTEX_POINT('',#406300);
#40789=VERTEX_POINT('',#406302);
#40790=VERTEX_POINT('',#406307);
#40791=VERTEX_POINT('',#406309);
#40792=VERTEX_POINT('',#406381);
#40793=VERTEX_POINT('',#406413);
#40794=VERTEX_POINT('',#406444);
#40795=VERTEX_POINT('',#406583);
#40796=VERTEX_POINT('',#406584);
#40797=VERTEX_POINT('',#406586);
#40798=VERTEX_POINT('',#406591);
#40799=VERTEX_POINT('',#406593);
#40800=VERTEX_POINT('',#406603);
#40801=VERTEX_POINT('',#406604);
#40802=VERTEX_POINT('',#406606);
#40803=VERTEX_POINT('',#406611);
#40804=VERTEX_POINT('',#406613);
#40805=VERTEX_POINT('',#406685);
#40806=VERTEX_POINT('',#406717);
#40807=VERTEX_POINT('',#406748);
#40808=VERTEX_POINT('',#406887);
#40809=VERTEX_POINT('',#406888);
#40810=VERTEX_POINT('',#406890);
#40811=VERTEX_POINT('',#406895);
#40812=VERTEX_POINT('',#406897);
#40813=VERTEX_POINT('',#406907);
#40814=VERTEX_POINT('',#406908);
#40815=VERTEX_POINT('',#406910);
#40816=VERTEX_POINT('',#406915);
#40817=VERTEX_POINT('',#406917);
#40818=VERTEX_POINT('',#406989);
#40819=VERTEX_POINT('',#407021);
#40820=VERTEX_POINT('',#407052);
#40821=VERTEX_POINT('',#407191);
#40822=VERTEX_POINT('',#407192);
#40823=VERTEX_POINT('',#407194);
#40824=VERTEX_POINT('',#407199);
#40825=VERTEX_POINT('',#407201);
#40826=VERTEX_POINT('',#407211);
#40827=VERTEX_POINT('',#407212);
#40828=VERTEX_POINT('',#407214);
#40829=VERTEX_POINT('',#407219);
#40830=VERTEX_POINT('',#407221);
#40831=VERTEX_POINT('',#407293);
#40832=VERTEX_POINT('',#407325);
#40833=VERTEX_POINT('',#407356);
#40834=VERTEX_POINT('',#407495);
#40835=VERTEX_POINT('',#407496);
#40836=VERTEX_POINT('',#407498);
#40837=VERTEX_POINT('',#407503);
#40838=VERTEX_POINT('',#407505);
#40839=VERTEX_POINT('',#407515);
#40840=VERTEX_POINT('',#407516);
#40841=VERTEX_POINT('',#407518);
#40842=VERTEX_POINT('',#407523);
#40843=VERTEX_POINT('',#407525);
#40844=VERTEX_POINT('',#407597);
#40845=VERTEX_POINT('',#407629);
#40846=VERTEX_POINT('',#407660);
#40847=VERTEX_POINT('',#407799);
#40848=VERTEX_POINT('',#407800);
#40849=VERTEX_POINT('',#407802);
#40850=VERTEX_POINT('',#407807);
#40851=VERTEX_POINT('',#407809);
#40852=VERTEX_POINT('',#407819);
#40853=VERTEX_POINT('',#407820);
#40854=VERTEX_POINT('',#407822);
#40855=VERTEX_POINT('',#407827);
#40856=VERTEX_POINT('',#407829);
#40857=VERTEX_POINT('',#407901);
#40858=VERTEX_POINT('',#407933);
#40859=VERTEX_POINT('',#407964);
#40860=VERTEX_POINT('',#408103);
#40861=VERTEX_POINT('',#408104);
#40862=VERTEX_POINT('',#408106);
#40863=VERTEX_POINT('',#408111);
#40864=VERTEX_POINT('',#408113);
#40865=VERTEX_POINT('',#408123);
#40866=VERTEX_POINT('',#408124);
#40867=VERTEX_POINT('',#408126);
#40868=VERTEX_POINT('',#408131);
#40869=VERTEX_POINT('',#408133);
#40870=VERTEX_POINT('',#408205);
#40871=VERTEX_POINT('',#408237);
#40872=VERTEX_POINT('',#408268);
#40873=VERTEX_POINT('',#408407);
#40874=VERTEX_POINT('',#408408);
#40875=VERTEX_POINT('',#408410);
#40876=VERTEX_POINT('',#408415);
#40877=VERTEX_POINT('',#408417);
#40878=VERTEX_POINT('',#408427);
#40879=VERTEX_POINT('',#408428);
#40880=VERTEX_POINT('',#408430);
#40881=VERTEX_POINT('',#408435);
#40882=VERTEX_POINT('',#408437);
#40883=VERTEX_POINT('',#408509);
#40884=VERTEX_POINT('',#408541);
#40885=VERTEX_POINT('',#408572);
#40886=VERTEX_POINT('',#408711);
#40887=VERTEX_POINT('',#408712);
#40888=VERTEX_POINT('',#408714);
#40889=VERTEX_POINT('',#408719);
#40890=VERTEX_POINT('',#408721);
#40891=VERTEX_POINT('',#408731);
#40892=VERTEX_POINT('',#408732);
#40893=VERTEX_POINT('',#408734);
#40894=VERTEX_POINT('',#408739);
#40895=VERTEX_POINT('',#408741);
#40896=VERTEX_POINT('',#408813);
#40897=VERTEX_POINT('',#408845);
#40898=VERTEX_POINT('',#408876);
#40899=VERTEX_POINT('',#409015);
#40900=VERTEX_POINT('',#409016);
#40901=VERTEX_POINT('',#409018);
#40902=VERTEX_POINT('',#409023);
#40903=VERTEX_POINT('',#409025);
#40904=VERTEX_POINT('',#409035);
#40905=VERTEX_POINT('',#409036);
#40906=VERTEX_POINT('',#409038);
#40907=VERTEX_POINT('',#409043);
#40908=VERTEX_POINT('',#409045);
#40909=VERTEX_POINT('',#409117);
#40910=VERTEX_POINT('',#409149);
#40911=VERTEX_POINT('',#409180);
#40912=VERTEX_POINT('',#409319);
#40913=VERTEX_POINT('',#409320);
#40914=VERTEX_POINT('',#409322);
#40915=VERTEX_POINT('',#409327);
#40916=VERTEX_POINT('',#409329);
#40917=VERTEX_POINT('',#409339);
#40918=VERTEX_POINT('',#409340);
#40919=VERTEX_POINT('',#409342);
#40920=VERTEX_POINT('',#409347);
#40921=VERTEX_POINT('',#409349);
#40922=VERTEX_POINT('',#409421);
#40923=VERTEX_POINT('',#409453);
#40924=VERTEX_POINT('',#409484);
#49464=EDGE_CURVE('',#38516,#38517,#29078,.T.);
#49465=EDGE_CURVE('',#38518,#38516,#4261,.T.);
#49466=EDGE_CURVE('',#38518,#38517,#20606,.T.);
#49467=EDGE_CURVE('',#38519,#38520,#29079,.T.);
#49468=EDGE_CURVE('',#38516,#38519,#4262,.T.);
#49469=EDGE_CURVE('',#38517,#38520,#4263,.T.);
#49470=EDGE_CURVE('',#38521,#38522,#29080,.T.);
#49471=EDGE_CURVE('',#38519,#38521,#4264,.T.);
#49472=EDGE_CURVE('',#38520,#38522,#4265,.T.);
#49473=EDGE_CURVE('',#38523,#38524,#29081,.T.);
#49474=EDGE_CURVE('',#38521,#38523,#4266,.T.);
#49475=EDGE_CURVE('',#38522,#38524,#4267,.T.);
#49476=EDGE_CURVE('',#38525,#38526,#29082,.T.);
#49477=EDGE_CURVE('',#38523,#38525,#4268,.T.);
#49478=EDGE_CURVE('',#38524,#38526,#4269,.T.);
#49479=EDGE_CURVE('',#38527,#38528,#29083,.T.);
#49480=EDGE_CURVE('',#38525,#38527,#4270,.T.);
#49481=EDGE_CURVE('',#38526,#38528,#4271,.T.);
#49482=EDGE_CURVE('',#38529,#38530,#29084,.T.);
#49483=EDGE_CURVE('',#38527,#38529,#4272,.T.);
#49484=EDGE_CURVE('',#38528,#38530,#4273,.T.);
#49485=EDGE_CURVE('',#38531,#38532,#29085,.T.);
#49486=EDGE_CURVE('',#38529,#38531,#4274,.T.);
#49487=EDGE_CURVE('',#38530,#38532,#4275,.T.);
#49488=EDGE_CURVE('',#38533,#38534,#29086,.T.);
#49489=EDGE_CURVE('',#38531,#38533,#4276,.T.);
#49490=EDGE_CURVE('',#38532,#38534,#4277,.T.);
#49491=EDGE_CURVE('',#38535,#38536,#29087,.T.);
#49492=EDGE_CURVE('',#38533,#38535,#4278,.T.);
#49493=EDGE_CURVE('',#38534,#38536,#4279,.T.);
#49494=EDGE_CURVE('',#38537,#38538,#29088,.T.);
#49495=EDGE_CURVE('',#38535,#38537,#4280,.T.);
#49496=EDGE_CURVE('',#38536,#38538,#4281,.T.);
#49497=EDGE_CURVE('',#38539,#38540,#29089,.T.);
#49498=EDGE_CURVE('',#38537,#38539,#4282,.T.);
#49499=EDGE_CURVE('',#38538,#38540,#4283,.T.);
#49500=EDGE_CURVE('',#38541,#38542,#29090,.T.);
#49501=EDGE_CURVE('',#38539,#38541,#4284,.T.);
#49502=EDGE_CURVE('',#38540,#38542,#4285,.T.);
#49503=EDGE_CURVE('',#38543,#38544,#29091,.T.);
#49504=EDGE_CURVE('',#38541,#38543,#4286,.T.);
#49505=EDGE_CURVE('',#38542,#38544,#4287,.T.);
#49506=EDGE_CURVE('',#38545,#38546,#29092,.T.);
#49507=EDGE_CURVE('',#38543,#38545,#4288,.T.);
#49508=EDGE_CURVE('',#38544,#38546,#4289,.T.);
#49509=EDGE_CURVE('',#38547,#38548,#29093,.T.);
#49510=EDGE_CURVE('',#38545,#38547,#4290,.T.);
#49511=EDGE_CURVE('',#38546,#38548,#4291,.T.);
#49512=EDGE_CURVE('',#38549,#38550,#29094,.T.);
#49513=EDGE_CURVE('',#38547,#38549,#4292,.T.);
#49514=EDGE_CURVE('',#38548,#38550,#4293,.T.);
#49515=EDGE_CURVE('',#38551,#38552,#29095,.T.);
#49516=EDGE_CURVE('',#38549,#38551,#4294,.T.);
#49517=EDGE_CURVE('',#38550,#38552,#4295,.T.);
#49518=EDGE_CURVE('',#38553,#38554,#29096,.T.);
#49519=EDGE_CURVE('',#38551,#38553,#4296,.T.);
#49520=EDGE_CURVE('',#38552,#38554,#4297,.T.);
#49521=EDGE_CURVE('',#38555,#38556,#29097,.T.);
#49522=EDGE_CURVE('',#38553,#38555,#4298,.T.);
#49523=EDGE_CURVE('',#38554,#38556,#4299,.T.);
#49524=EDGE_CURVE('',#38557,#38558,#29098,.T.);
#49525=EDGE_CURVE('',#38555,#38557,#4300,.T.);
#49526=EDGE_CURVE('',#38556,#38558,#4301,.T.);
#49527=EDGE_CURVE('',#38559,#38560,#29099,.T.);
#49528=EDGE_CURVE('',#38557,#38559,#4302,.T.);
#49529=EDGE_CURVE('',#38558,#38560,#4303,.T.);
#49530=EDGE_CURVE('',#38561,#38562,#29100,.T.);
#49531=EDGE_CURVE('',#38559,#38561,#4304,.T.);
#49532=EDGE_CURVE('',#38560,#38562,#4305,.T.);
#49533=EDGE_CURVE('',#38563,#38564,#29101,.T.);
#49534=EDGE_CURVE('',#38561,#38563,#4306,.T.);
#49535=EDGE_CURVE('',#38562,#38564,#4307,.T.);
#49536=EDGE_CURVE('',#38565,#38566,#29102,.T.);
#49537=EDGE_CURVE('',#38563,#38565,#4308,.T.);
#49538=EDGE_CURVE('',#38564,#38566,#4309,.T.);
#49539=EDGE_CURVE('',#38567,#38568,#29103,.T.);
#49540=EDGE_CURVE('',#38565,#38567,#4310,.T.);
#49541=EDGE_CURVE('',#38566,#38568,#4311,.T.);
#49542=EDGE_CURVE('',#38569,#38570,#29104,.T.);
#49543=EDGE_CURVE('',#38567,#38569,#4312,.T.);
#49544=EDGE_CURVE('',#38568,#38570,#4313,.T.);
#49545=EDGE_CURVE('',#38571,#38572,#29105,.T.);
#49546=EDGE_CURVE('',#38569,#38571,#4314,.T.);
#49547=EDGE_CURVE('',#38570,#38572,#4315,.T.);
#49548=EDGE_CURVE('',#38573,#38574,#29106,.T.);
#49549=EDGE_CURVE('',#38571,#38573,#4316,.T.);
#49550=EDGE_CURVE('',#38572,#38574,#4317,.T.);
#49551=EDGE_CURVE('',#38575,#38576,#29107,.T.);
#49552=EDGE_CURVE('',#38575,#38577,#24711,.T.);
#49553=EDGE_CURVE('',#38578,#38577,#20607,.T.);
#49554=EDGE_CURVE('',#38578,#38579,#29108,.T.);
#49555=EDGE_CURVE('',#38579,#38579,#20608,.T.);
#49556=EDGE_CURVE('',#38580,#38578,#20609,.T.);
#49557=EDGE_CURVE('',#38580,#38576,#24712,.T.);
#49558=EDGE_CURVE('',#38581,#38582,#29109,.T.);
#49559=EDGE_CURVE('',#38581,#38575,#24713,.T.);
#49560=EDGE_CURVE('',#38576,#38582,#24714,.T.);
#49561=EDGE_CURVE('',#38583,#38584,#29110,.T.);
#49562=EDGE_CURVE('',#38583,#38581,#24715,.T.);
#49563=EDGE_CURVE('',#38582,#38584,#24716,.T.);
#49564=EDGE_CURVE('',#38585,#38586,#29111,.T.);
#49565=EDGE_CURVE('',#38585,#38583,#24717,.T.);
#49566=EDGE_CURVE('',#38584,#38586,#24718,.T.);
#49567=EDGE_CURVE('',#38587,#38588,#29112,.T.);
#49568=EDGE_CURVE('',#38587,#38585,#24719,.T.);
#49569=EDGE_CURVE('',#38586,#38588,#24720,.T.);
#49570=EDGE_CURVE('',#38589,#38590,#29113,.T.);
#49571=EDGE_CURVE('',#38589,#38587,#24721,.T.);
#49572=EDGE_CURVE('',#38588,#38590,#24722,.T.);
#49573=EDGE_CURVE('',#38591,#38592,#29114,.T.);
#49574=EDGE_CURVE('',#38591,#38589,#24723,.T.);
#49575=EDGE_CURVE('',#38590,#38592,#24724,.T.);
#49576=EDGE_CURVE('',#38593,#38594,#29115,.T.);
#49577=EDGE_CURVE('',#38593,#38591,#24725,.T.);
#49578=EDGE_CURVE('',#38592,#38594,#24726,.T.);
#49579=EDGE_CURVE('',#38595,#38596,#29116,.T.);
#49580=EDGE_CURVE('',#38595,#38593,#24727,.T.);
#49581=EDGE_CURVE('',#38594,#38596,#24728,.T.);
#49582=EDGE_CURVE('',#38597,#38598,#29117,.T.);
#49583=EDGE_CURVE('',#38597,#38595,#24729,.T.);
#49584=EDGE_CURVE('',#38596,#38598,#24730,.T.);
#49585=EDGE_CURVE('',#38599,#38600,#29118,.T.);
#49586=EDGE_CURVE('',#38599,#38597,#24731,.T.);
#49587=EDGE_CURVE('',#38598,#38600,#24732,.T.);
#49588=EDGE_CURVE('',#38601,#38602,#29119,.T.);
#49589=EDGE_CURVE('',#38601,#38599,#24733,.T.);
#49590=EDGE_CURVE('',#38600,#38602,#24734,.T.);
#49591=EDGE_CURVE('',#38603,#38604,#29120,.T.);
#49592=EDGE_CURVE('',#38603,#38601,#24735,.T.);
#49593=EDGE_CURVE('',#38602,#38604,#24736,.T.);
#49594=EDGE_CURVE('',#38605,#38606,#29121,.T.);
#49595=EDGE_CURVE('',#38605,#38603,#24737,.T.);
#49596=EDGE_CURVE('',#38604,#38606,#24738,.T.);
#49597=EDGE_CURVE('',#38607,#38608,#29122,.T.);
#49598=EDGE_CURVE('',#38607,#38605,#24739,.T.);
#49599=EDGE_CURVE('',#38606,#38608,#24740,.T.);
#49600=EDGE_CURVE('',#38609,#38610,#29123,.T.);
#49601=EDGE_CURVE('',#38609,#38607,#24741,.T.);
#49602=EDGE_CURVE('',#38608,#38610,#24742,.T.);
#49603=EDGE_CURVE('',#38611,#38612,#29124,.T.);
#49604=EDGE_CURVE('',#38611,#38609,#24743,.T.);
#49605=EDGE_CURVE('',#38610,#38612,#24744,.T.);
#49606=EDGE_CURVE('',#38613,#38614,#29125,.T.);
#49607=EDGE_CURVE('',#38613,#38611,#24745,.T.);
#49608=EDGE_CURVE('',#38612,#38614,#24746,.T.);
#49609=EDGE_CURVE('',#38615,#38616,#29126,.T.);
#49610=EDGE_CURVE('',#38615,#38613,#24747,.T.);
#49611=EDGE_CURVE('',#38614,#38616,#24748,.T.);
#49612=EDGE_CURVE('',#38617,#38618,#29127,.T.);
#49613=EDGE_CURVE('',#38617,#38615,#24749,.T.);
#49614=EDGE_CURVE('',#38616,#38618,#24750,.T.);
#49615=EDGE_CURVE('',#38619,#38620,#29128,.T.);
#49616=EDGE_CURVE('',#38619,#38617,#24751,.T.);
#49617=EDGE_CURVE('',#38618,#38620,#24752,.T.);
#49618=EDGE_CURVE('',#38621,#38622,#29129,.T.);
#49619=EDGE_CURVE('',#38621,#38619,#24753,.T.);
#49620=EDGE_CURVE('',#38620,#38622,#24754,.T.);
#49621=EDGE_CURVE('',#38623,#38624,#29130,.T.);
#49622=EDGE_CURVE('',#38623,#38621,#24755,.T.);
#49623=EDGE_CURVE('',#38622,#38624,#24756,.T.);
#49624=EDGE_CURVE('',#38625,#38626,#29131,.T.);
#49625=EDGE_CURVE('',#38625,#38623,#24757,.T.);
#49626=EDGE_CURVE('',#38624,#38626,#24758,.T.);
#49627=EDGE_CURVE('',#38627,#38628,#29132,.T.);
#49628=EDGE_CURVE('',#38627,#38625,#24759,.T.);
#49629=EDGE_CURVE('',#38626,#38628,#24760,.T.);
#49630=EDGE_CURVE('',#38629,#38630,#29133,.T.);
#49631=EDGE_CURVE('',#38629,#38627,#24761,.T.);
#49632=EDGE_CURVE('',#38628,#38630,#24762,.T.);
#49633=EDGE_CURVE('',#38631,#38632,#29134,.T.);
#49634=EDGE_CURVE('',#38631,#38629,#24763,.T.);
#49635=EDGE_CURVE('',#38630,#38632,#24764,.T.);
#49636=EDGE_CURVE('',#38633,#38634,#29135,.T.);
#49637=EDGE_CURVE('',#38633,#38631,#24765,.T.);
#49638=EDGE_CURVE('',#38632,#38634,#24766,.T.);
#49639=EDGE_CURVE('',#38577,#38635,#29136,.T.);
#49640=EDGE_CURVE('',#38636,#38577,#24767,.T.);
#49641=EDGE_CURVE('',#38637,#38636,#20610,.T.);
#49642=EDGE_CURVE('',#38635,#38637,#24768,.F.);
#49643=EDGE_CURVE('',#38638,#38639,#29137,.T.);
#49644=EDGE_CURVE('',#38517,#38638,#24769,.F.);
#49645=EDGE_CURVE('',#38517,#38639,#20611,.T.);
#49646=EDGE_CURVE('',#38639,#38518,#20612,.T.);
#49647=EDGE_CURVE('',#38640,#38518,#24770,.T.);
#49648=EDGE_CURVE('',#38641,#38640,#20613,.T.);
#49649=EDGE_CURVE('',#38638,#38641,#24771,.F.);
#49650=EDGE_CURVE('',#38580,#38635,#24772,.F.);
#49651=EDGE_CURVE('',#38634,#38641,#24773,.T.);
#49652=EDGE_CURVE('',#38640,#38633,#24774,.T.);
#49653=EDGE_CURVE('',#38579,#38642,#20614,.T.);
#49654=EDGE_CURVE('',#38642,#38642,#20615,.T.);
#49655=EDGE_CURVE('',#38643,#38644,#29138,.T.);
#49656=EDGE_CURVE('',#38645,#38644,#20616,.T.);
#49657=EDGE_CURVE('',#38646,#38645,#20617,.T.);
#49658=EDGE_CURVE('',#38647,#38646,#20618,.T.);
#49659=EDGE_CURVE('',#38647,#38648,#20619,.T.);
#49660=EDGE_CURVE('',#38649,#38648,#20620,.T.);
#49661=EDGE_CURVE('',#38644,#38649,#20621,.T.);
#49662=EDGE_CURVE('',#38650,#38651,#4318,.T.);
#49663=EDGE_CURVE('',#38651,#38650,#20622,.T.);
#49664=EDGE_CURVE('',#38652,#38652,#20623,.T.);
#49665=EDGE_CURVE('',#38652,#38653,#20624,.T.);
#49666=EDGE_CURVE('',#38653,#38653,#20625,.T.);
#49667=EDGE_CURVE('',#38654,#38654,#20626,.T.);
#49668=EDGE_CURVE('',#38654,#38652,#29139,.T.);
#49669=EDGE_CURVE('',#38655,#38655,#20627,.T.);
#49670=EDGE_CURVE('',#38655,#38654,#20628,.T.);
#49671=EDGE_CURVE('',#38656,#38657,#20629,.T.);
#49672=EDGE_CURVE('',#38657,#38658,#24775,.T.);
#49673=EDGE_CURVE('',#38658,#38659,#198,.T.);
#49674=EDGE_CURVE('',#38659,#38660,#24776,.T.);
#49675=EDGE_CURVE('',#38660,#38661,#20630,.T.);
#49676=EDGE_CURVE('',#38661,#38662,#24777,.T.);
#49677=EDGE_CURVE('',#38662,#38663,#199,.T.);
#49678=EDGE_CURVE('',#38663,#38664,#24778,.T.);
#49679=EDGE_CURVE('',#38664,#38665,#20631,.T.);
#49680=EDGE_CURVE('',#38665,#38666,#24779,.T.);
#49681=EDGE_CURVE('',#38666,#38667,#200,.T.);
#49682=EDGE_CURVE('',#38667,#38668,#24780,.T.);
#49683=EDGE_CURVE('',#38668,#38669,#20632,.T.);
#49684=EDGE_CURVE('',#38669,#38670,#24781,.T.);
#49685=EDGE_CURVE('',#38670,#38671,#201,.T.);
#49686=EDGE_CURVE('',#38671,#38672,#24782,.T.);
#49687=EDGE_CURVE('',#38672,#38673,#20633,.T.);
#49688=EDGE_CURVE('',#38673,#38674,#24783,.T.);
#49689=EDGE_CURVE('',#38674,#38675,#202,.T.);
#49690=EDGE_CURVE('',#38675,#38676,#24784,.T.);
#49691=EDGE_CURVE('',#38676,#38677,#20634,.T.);
#49692=EDGE_CURVE('',#38677,#38678,#24785,.T.);
#49693=EDGE_CURVE('',#38678,#38679,#203,.T.);
#49694=EDGE_CURVE('',#38679,#38680,#24786,.T.);
#49695=EDGE_CURVE('',#38680,#38681,#20635,.T.);
#49696=EDGE_CURVE('',#38681,#38682,#24787,.T.);
#49697=EDGE_CURVE('',#38682,#38683,#204,.T.);
#49698=EDGE_CURVE('',#38683,#38684,#24788,.T.);
#49699=EDGE_CURVE('',#38684,#38685,#20636,.T.);
#49700=EDGE_CURVE('',#38685,#38686,#24789,.T.);
#49701=EDGE_CURVE('',#38686,#38687,#205,.T.);
#49702=EDGE_CURVE('',#38687,#38688,#24790,.T.);
#49703=EDGE_CURVE('',#38688,#38689,#20637,.T.);
#49704=EDGE_CURVE('',#38689,#38690,#24791,.T.);
#49705=EDGE_CURVE('',#38690,#38691,#206,.T.);
#49706=EDGE_CURVE('',#38691,#38692,#24792,.T.);
#49707=EDGE_CURVE('',#38692,#38693,#20638,.T.);
#49708=EDGE_CURVE('',#38693,#38694,#24793,.T.);
#49709=EDGE_CURVE('',#38694,#38695,#207,.T.);
#49710=EDGE_CURVE('',#38695,#38696,#24794,.T.);
#49711=EDGE_CURVE('',#38696,#38697,#20639,.T.);
#49712=EDGE_CURVE('',#38697,#38698,#24795,.T.);
#49713=EDGE_CURVE('',#38698,#38699,#208,.T.);
#49714=EDGE_CURVE('',#38699,#38700,#24796,.T.);
#49715=EDGE_CURVE('',#38700,#38701,#20640,.T.);
#49716=EDGE_CURVE('',#38701,#38702,#24797,.T.);
#49717=EDGE_CURVE('',#38702,#38703,#209,.T.);
#49718=EDGE_CURVE('',#38703,#38704,#24798,.T.);
#49719=EDGE_CURVE('',#38704,#38705,#20641,.T.);
#49720=EDGE_CURVE('',#38705,#38706,#24799,.T.);
#49721=EDGE_CURVE('',#38706,#38707,#210,.T.);
#49722=EDGE_CURVE('',#38707,#38708,#24800,.T.);
#49723=EDGE_CURVE('',#38708,#38709,#20642,.T.);
#49724=EDGE_CURVE('',#38709,#38710,#24801,.T.);
#49725=EDGE_CURVE('',#38710,#38711,#211,.T.);
#49726=EDGE_CURVE('',#38711,#38712,#24802,.T.);
#49727=EDGE_CURVE('',#38712,#38713,#20643,.T.);
#49728=EDGE_CURVE('',#38713,#38714,#24803,.T.);
#49729=EDGE_CURVE('',#38714,#38715,#212,.T.);
#49730=EDGE_CURVE('',#38715,#38716,#24804,.T.);
#49731=EDGE_CURVE('',#38716,#38717,#20644,.T.);
#49732=EDGE_CURVE('',#38717,#38718,#24805,.T.);
#49733=EDGE_CURVE('',#38718,#38719,#213,.T.);
#49734=EDGE_CURVE('',#38719,#38720,#24806,.T.);
#49735=EDGE_CURVE('',#38720,#38721,#20645,.T.);
#49736=EDGE_CURVE('',#38721,#38722,#24807,.T.);
#49737=EDGE_CURVE('',#38722,#38723,#214,.T.);
#49738=EDGE_CURVE('',#38723,#38724,#24808,.T.);
#49739=EDGE_CURVE('',#38724,#38725,#20646,.T.);
#49740=EDGE_CURVE('',#38725,#38726,#24809,.T.);
#49741=EDGE_CURVE('',#38726,#38727,#215,.T.);
#49742=EDGE_CURVE('',#38727,#38728,#24810,.T.);
#49743=EDGE_CURVE('',#38728,#38729,#20647,.T.);
#49744=EDGE_CURVE('',#38729,#38730,#24811,.T.);
#49745=EDGE_CURVE('',#38730,#38731,#216,.T.);
#49746=EDGE_CURVE('',#38731,#38732,#24812,.T.);
#49747=EDGE_CURVE('',#38732,#38733,#20648,.T.);
#49748=EDGE_CURVE('',#38733,#38734,#24813,.T.);
#49749=EDGE_CURVE('',#38734,#38735,#217,.T.);
#49750=EDGE_CURVE('',#38735,#38736,#24814,.T.);
#49751=EDGE_CURVE('',#38736,#38737,#20649,.T.);
#49752=EDGE_CURVE('',#38737,#38738,#24815,.T.);
#49753=EDGE_CURVE('',#38738,#38739,#218,.T.);
#49754=EDGE_CURVE('',#38739,#38740,#24816,.T.);
#49755=EDGE_CURVE('',#38740,#38741,#20650,.T.);
#49756=EDGE_CURVE('',#38741,#38742,#24817,.T.);
#49757=EDGE_CURVE('',#38742,#38743,#219,.T.);
#49758=EDGE_CURVE('',#38743,#38744,#24818,.T.);
#49759=EDGE_CURVE('',#38744,#38745,#20651,.T.);
#49760=EDGE_CURVE('',#38745,#38746,#24819,.T.);
#49761=EDGE_CURVE('',#38746,#38747,#220,.T.);
#49762=EDGE_CURVE('',#38747,#38748,#24820,.T.);
#49763=EDGE_CURVE('',#38748,#38749,#20652,.T.);
#49764=EDGE_CURVE('',#38749,#38750,#24821,.T.);
#49765=EDGE_CURVE('',#38750,#38751,#221,.T.);
#49766=EDGE_CURVE('',#38751,#38752,#24822,.T.);
#49767=EDGE_CURVE('',#38752,#38753,#20653,.T.);
#49768=EDGE_CURVE('',#38753,#38754,#24823,.T.);
#49769=EDGE_CURVE('',#38754,#38755,#222,.T.);
#49770=EDGE_CURVE('',#38755,#38756,#24824,.T.);
#49771=EDGE_CURVE('',#38756,#38757,#20654,.T.);
#49772=EDGE_CURVE('',#38757,#38758,#24825,.T.);
#49773=EDGE_CURVE('',#38758,#38759,#223,.T.);
#49774=EDGE_CURVE('',#38759,#38760,#24826,.T.);
#49775=EDGE_CURVE('',#38760,#38761,#20655,.T.);
#49776=EDGE_CURVE('',#38761,#38762,#24827,.T.);
#49777=EDGE_CURVE('',#38762,#38763,#224,.T.);
#49778=EDGE_CURVE('',#38763,#38764,#24828,.T.);
#49779=EDGE_CURVE('',#38764,#38765,#20656,.T.);
#49780=EDGE_CURVE('',#38765,#38766,#24829,.T.);
#49781=EDGE_CURVE('',#38766,#38767,#225,.T.);
#49782=EDGE_CURVE('',#38767,#38768,#24830,.T.);
#49783=EDGE_CURVE('',#38768,#38769,#20657,.T.);
#49784=EDGE_CURVE('',#38769,#38770,#24831,.T.);
#49785=EDGE_CURVE('',#38770,#38771,#226,.T.);
#49786=EDGE_CURVE('',#38771,#38772,#24832,.T.);
#49787=EDGE_CURVE('',#38772,#38773,#20658,.T.);
#49788=EDGE_CURVE('',#38773,#38774,#24833,.T.);
#49789=EDGE_CURVE('',#38774,#38775,#227,.T.);
#49790=EDGE_CURVE('',#38775,#38776,#24834,.T.);
#49791=EDGE_CURVE('',#38776,#38777,#20659,.T.);
#49792=EDGE_CURVE('',#38777,#38778,#24835,.T.);
#49793=EDGE_CURVE('',#38778,#38779,#228,.T.);
#49794=EDGE_CURVE('',#38779,#38780,#24836,.T.);
#49795=EDGE_CURVE('',#38780,#38781,#20660,.T.);
#49796=EDGE_CURVE('',#38781,#38782,#24837,.T.);
#49797=EDGE_CURVE('',#38782,#38783,#229,.T.);
#49798=EDGE_CURVE('',#38783,#38784,#24838,.T.);
#49799=EDGE_CURVE('',#38784,#38785,#20661,.T.);
#49800=EDGE_CURVE('',#38785,#38786,#24839,.T.);
#49801=EDGE_CURVE('',#38786,#38787,#230,.T.);
#49802=EDGE_CURVE('',#38787,#38788,#24840,.T.);
#49803=EDGE_CURVE('',#38788,#38789,#20662,.T.);
#49804=EDGE_CURVE('',#38789,#38790,#24841,.T.);
#49805=EDGE_CURVE('',#38790,#38791,#231,.T.);
#49806=EDGE_CURVE('',#38791,#38792,#24842,.T.);
#49807=EDGE_CURVE('',#38792,#38793,#20663,.T.);
#49808=EDGE_CURVE('',#38793,#38794,#24843,.T.);
#49809=EDGE_CURVE('',#38794,#38795,#232,.T.);
#49810=EDGE_CURVE('',#38795,#38796,#24844,.T.);
#49811=EDGE_CURVE('',#38796,#38797,#20664,.T.);
#49812=EDGE_CURVE('',#38797,#38798,#24845,.T.);
#49813=EDGE_CURVE('',#38798,#38799,#233,.T.);
#49814=EDGE_CURVE('',#38799,#38800,#24846,.T.);
#49815=EDGE_CURVE('',#38800,#38801,#20665,.T.);
#49816=EDGE_CURVE('',#38801,#38802,#24847,.T.);
#49817=EDGE_CURVE('',#38802,#38803,#234,.T.);
#49818=EDGE_CURVE('',#38803,#38804,#24848,.T.);
#49819=EDGE_CURVE('',#38804,#38805,#20666,.T.);
#49820=EDGE_CURVE('',#38805,#38806,#24849,.T.);
#49821=EDGE_CURVE('',#38806,#38807,#235,.T.);
#49822=EDGE_CURVE('',#38807,#38808,#24850,.T.);
#49823=EDGE_CURVE('',#38808,#38809,#20667,.T.);
#49824=EDGE_CURVE('',#38809,#38810,#24851,.T.);
#49825=EDGE_CURVE('',#38810,#38811,#236,.T.);
#49826=EDGE_CURVE('',#38811,#38812,#24852,.T.);
#49827=EDGE_CURVE('',#38812,#38813,#20668,.T.);
#49828=EDGE_CURVE('',#38813,#38814,#24853,.T.);
#49829=EDGE_CURVE('',#38814,#38815,#237,.T.);
#49830=EDGE_CURVE('',#38815,#38816,#24854,.T.);
#49831=EDGE_CURVE('',#38816,#38817,#20669,.T.);
#49832=EDGE_CURVE('',#38817,#38818,#24855,.T.);
#49833=EDGE_CURVE('',#38818,#38819,#238,.T.);
#49834=EDGE_CURVE('',#38819,#38820,#24856,.T.);
#49835=EDGE_CURVE('',#38820,#38821,#20670,.T.);
#49836=EDGE_CURVE('',#38821,#38822,#24857,.T.);
#49837=EDGE_CURVE('',#38822,#38823,#239,.T.);
#49838=EDGE_CURVE('',#38823,#38824,#24858,.T.);
#49839=EDGE_CURVE('',#38824,#38825,#20671,.T.);
#49840=EDGE_CURVE('',#38825,#38826,#24859,.T.);
#49841=EDGE_CURVE('',#38826,#38827,#240,.T.);
#49842=EDGE_CURVE('',#38827,#38828,#24860,.T.);
#49843=EDGE_CURVE('',#38828,#38829,#20672,.T.);
#49844=EDGE_CURVE('',#38829,#38830,#24861,.T.);
#49845=EDGE_CURVE('',#38830,#38831,#241,.T.);
#49846=EDGE_CURVE('',#38831,#38832,#24862,.T.);
#49847=EDGE_CURVE('',#38832,#38833,#20673,.T.);
#49848=EDGE_CURVE('',#38833,#38834,#24863,.T.);
#49849=EDGE_CURVE('',#38834,#38835,#242,.T.);
#49850=EDGE_CURVE('',#38835,#38836,#24864,.T.);
#49851=EDGE_CURVE('',#38836,#38837,#20674,.T.);
#49852=EDGE_CURVE('',#38837,#38838,#24865,.T.);
#49853=EDGE_CURVE('',#38838,#38839,#243,.T.);
#49854=EDGE_CURVE('',#38839,#38840,#24866,.T.);
#49855=EDGE_CURVE('',#38840,#38841,#20675,.T.);
#49856=EDGE_CURVE('',#38841,#38842,#24867,.T.);
#49857=EDGE_CURVE('',#38842,#38843,#244,.T.);
#49858=EDGE_CURVE('',#38843,#38844,#24868,.T.);
#49859=EDGE_CURVE('',#38844,#38845,#20676,.T.);
#49860=EDGE_CURVE('',#38845,#38846,#24869,.T.);
#49861=EDGE_CURVE('',#38846,#38847,#245,.T.);
#49862=EDGE_CURVE('',#38847,#38848,#24870,.T.);
#49863=EDGE_CURVE('',#38848,#38849,#20677,.T.);
#49864=EDGE_CURVE('',#38849,#38850,#24871,.T.);
#49865=EDGE_CURVE('',#38850,#38851,#246,.T.);
#49866=EDGE_CURVE('',#38851,#38852,#24872,.T.);
#49867=EDGE_CURVE('',#38852,#38853,#20678,.T.);
#49868=EDGE_CURVE('',#38853,#38854,#29140,.T.);
#49869=EDGE_CURVE('',#38855,#38854,#20679,.T.);
#49870=EDGE_CURVE('',#38854,#38855,#20680,.T.);
#49871=EDGE_CURVE('',#38853,#38856,#20681,.T.);
#49872=EDGE_CURVE('',#38856,#38857,#24873,.T.);
#49873=EDGE_CURVE('',#38857,#38858,#247,.T.);
#49874=EDGE_CURVE('',#38858,#38859,#24874,.T.);
#49875=EDGE_CURVE('',#38859,#38860,#20682,.T.);
#49876=EDGE_CURVE('',#38860,#38861,#24875,.T.);
#49877=EDGE_CURVE('',#38861,#38862,#248,.T.);
#49878=EDGE_CURVE('',#38862,#38863,#24876,.T.);
#49879=EDGE_CURVE('',#38863,#38864,#20683,.T.);
#49880=EDGE_CURVE('',#38864,#38865,#24877,.T.);
#49881=EDGE_CURVE('',#38865,#38866,#249,.T.);
#49882=EDGE_CURVE('',#38866,#38867,#24878,.T.);
#49883=EDGE_CURVE('',#38867,#38868,#20684,.T.);
#49884=EDGE_CURVE('',#38868,#38869,#24879,.T.);
#49885=EDGE_CURVE('',#38869,#38870,#250,.T.);
#49886=EDGE_CURVE('',#38870,#38871,#24880,.T.);
#49887=EDGE_CURVE('',#38871,#38872,#20685,.T.);
#49888=EDGE_CURVE('',#38872,#38873,#24881,.T.);
#49889=EDGE_CURVE('',#38873,#38874,#251,.T.);
#49890=EDGE_CURVE('',#38874,#38875,#24882,.T.);
#49891=EDGE_CURVE('',#38875,#38876,#20686,.T.);
#49892=EDGE_CURVE('',#38876,#38877,#24883,.T.);
#49893=EDGE_CURVE('',#38877,#38878,#252,.T.);
#49894=EDGE_CURVE('',#38878,#38879,#24884,.T.);
#49895=EDGE_CURVE('',#38879,#38880,#20687,.T.);
#49896=EDGE_CURVE('',#38880,#38881,#24885,.T.);
#49897=EDGE_CURVE('',#38881,#38882,#253,.T.);
#49898=EDGE_CURVE('',#38882,#38883,#24886,.T.);
#49899=EDGE_CURVE('',#38883,#38884,#20688,.T.);
#49900=EDGE_CURVE('',#38884,#38885,#24887,.T.);
#49901=EDGE_CURVE('',#38885,#38886,#254,.T.);
#49902=EDGE_CURVE('',#38886,#38887,#24888,.T.);
#49903=EDGE_CURVE('',#38887,#38888,#20689,.T.);
#49904=EDGE_CURVE('',#38888,#38889,#24889,.T.);
#49905=EDGE_CURVE('',#38889,#38890,#255,.T.);
#49906=EDGE_CURVE('',#38890,#38891,#24890,.T.);
#49907=EDGE_CURVE('',#38891,#38892,#20690,.T.);
#49908=EDGE_CURVE('',#38892,#38893,#24891,.T.);
#49909=EDGE_CURVE('',#38893,#38894,#256,.T.);
#49910=EDGE_CURVE('',#38894,#38895,#24892,.T.);
#49911=EDGE_CURVE('',#38895,#38896,#20691,.T.);
#49912=EDGE_CURVE('',#38896,#38897,#24893,.T.);
#49913=EDGE_CURVE('',#38897,#38898,#257,.T.);
#49914=EDGE_CURVE('',#38898,#38899,#24894,.T.);
#49915=EDGE_CURVE('',#38899,#38900,#20692,.T.);
#49916=EDGE_CURVE('',#38900,#38901,#24895,.T.);
#49917=EDGE_CURVE('',#38901,#38902,#258,.T.);
#49918=EDGE_CURVE('',#38902,#38903,#24896,.T.);
#49919=EDGE_CURVE('',#38903,#38904,#20693,.T.);
#49920=EDGE_CURVE('',#38904,#38905,#24897,.T.);
#49921=EDGE_CURVE('',#38905,#38906,#259,.T.);
#49922=EDGE_CURVE('',#38906,#38907,#24898,.T.);
#49923=EDGE_CURVE('',#38907,#38908,#20694,.T.);
#49924=EDGE_CURVE('',#38908,#38909,#24899,.T.);
#49925=EDGE_CURVE('',#38909,#38910,#260,.T.);
#49926=EDGE_CURVE('',#38910,#38911,#24900,.T.);
#49927=EDGE_CURVE('',#38911,#38912,#20695,.T.);
#49928=EDGE_CURVE('',#38912,#38913,#24901,.T.);
#49929=EDGE_CURVE('',#38913,#38914,#261,.T.);
#49930=EDGE_CURVE('',#38914,#38915,#24902,.T.);
#49931=EDGE_CURVE('',#38915,#38916,#20696,.T.);
#49932=EDGE_CURVE('',#38916,#38917,#24903,.T.);
#49933=EDGE_CURVE('',#38917,#38918,#262,.T.);
#49934=EDGE_CURVE('',#38918,#38919,#24904,.T.);
#49935=EDGE_CURVE('',#38919,#38920,#20697,.T.);
#49936=EDGE_CURVE('',#38920,#38921,#24905,.T.);
#49937=EDGE_CURVE('',#38921,#38922,#263,.T.);
#49938=EDGE_CURVE('',#38922,#38923,#24906,.T.);
#49939=EDGE_CURVE('',#38923,#38924,#20698,.T.);
#49940=EDGE_CURVE('',#38924,#38925,#24907,.T.);
#49941=EDGE_CURVE('',#38925,#38926,#264,.T.);
#49942=EDGE_CURVE('',#38926,#38927,#24908,.T.);
#49943=EDGE_CURVE('',#38927,#38928,#20699,.T.);
#49944=EDGE_CURVE('',#38928,#38929,#24909,.T.);
#49945=EDGE_CURVE('',#38929,#38930,#265,.T.);
#49946=EDGE_CURVE('',#38930,#38931,#24910,.T.);
#49947=EDGE_CURVE('',#38931,#38932,#20700,.T.);
#49948=EDGE_CURVE('',#38932,#38933,#24911,.T.);
#49949=EDGE_CURVE('',#38933,#38934,#266,.T.);
#49950=EDGE_CURVE('',#38934,#38935,#24912,.T.);
#49951=EDGE_CURVE('',#38935,#38936,#20701,.T.);
#49952=EDGE_CURVE('',#38936,#38937,#24913,.T.);
#49953=EDGE_CURVE('',#38937,#38938,#267,.T.);
#49954=EDGE_CURVE('',#38938,#38939,#24914,.T.);
#49955=EDGE_CURVE('',#38939,#38940,#20702,.T.);
#49956=EDGE_CURVE('',#38940,#38941,#24915,.T.);
#49957=EDGE_CURVE('',#38941,#38942,#268,.T.);
#49958=EDGE_CURVE('',#38942,#38943,#24916,.T.);
#49959=EDGE_CURVE('',#38943,#38944,#20703,.T.);
#49960=EDGE_CURVE('',#38944,#38945,#24917,.T.);
#49961=EDGE_CURVE('',#38945,#38946,#269,.T.);
#49962=EDGE_CURVE('',#38946,#38947,#24918,.T.);
#49963=EDGE_CURVE('',#38947,#38948,#20704,.T.);
#49964=EDGE_CURVE('',#38948,#38949,#24919,.T.);
#49965=EDGE_CURVE('',#38949,#38950,#270,.T.);
#49966=EDGE_CURVE('',#38950,#38951,#24920,.T.);
#49967=EDGE_CURVE('',#38951,#38952,#20705,.T.);
#49968=EDGE_CURVE('',#38952,#38953,#24921,.T.);
#49969=EDGE_CURVE('',#38953,#38954,#271,.T.);
#49970=EDGE_CURVE('',#38954,#38955,#24922,.T.);
#49971=EDGE_CURVE('',#38955,#38956,#20706,.T.);
#49972=EDGE_CURVE('',#38956,#38957,#24923,.T.);
#49973=EDGE_CURVE('',#38957,#38958,#272,.T.);
#49974=EDGE_CURVE('',#38958,#38959,#24924,.T.);
#49975=EDGE_CURVE('',#38959,#38960,#20707,.T.);
#49976=EDGE_CURVE('',#38960,#38961,#24925,.T.);
#49977=EDGE_CURVE('',#38961,#38962,#273,.T.);
#49978=EDGE_CURVE('',#38962,#38963,#24926,.T.);
#49979=EDGE_CURVE('',#38963,#38964,#20708,.T.);
#49980=EDGE_CURVE('',#38964,#38965,#24927,.T.);
#49981=EDGE_CURVE('',#38965,#38966,#274,.T.);
#49982=EDGE_CURVE('',#38966,#38967,#24928,.T.);
#49983=EDGE_CURVE('',#38967,#38968,#20709,.T.);
#49984=EDGE_CURVE('',#38968,#38969,#24929,.T.);
#49985=EDGE_CURVE('',#38969,#38970,#275,.T.);
#49986=EDGE_CURVE('',#38970,#38971,#24930,.T.);
#49987=EDGE_CURVE('',#38971,#38972,#20710,.T.);
#49988=EDGE_CURVE('',#38972,#38973,#24931,.T.);
#49989=EDGE_CURVE('',#38973,#38974,#276,.T.);
#49990=EDGE_CURVE('',#38974,#38975,#24932,.T.);
#49991=EDGE_CURVE('',#38975,#38976,#20711,.T.);
#49992=EDGE_CURVE('',#38976,#38977,#24933,.T.);
#49993=EDGE_CURVE('',#38977,#38978,#277,.T.);
#49994=EDGE_CURVE('',#38978,#38979,#24934,.T.);
#49995=EDGE_CURVE('',#38979,#38980,#20712,.T.);
#49996=EDGE_CURVE('',#38980,#38981,#24935,.T.);
#49997=EDGE_CURVE('',#38981,#38982,#278,.T.);
#49998=EDGE_CURVE('',#38982,#38983,#24936,.T.);
#49999=EDGE_CURVE('',#38983,#38984,#20713,.T.);
#50000=EDGE_CURVE('',#38984,#38985,#24937,.T.);
#50001=EDGE_CURVE('',#38985,#38986,#279,.T.);
#50002=EDGE_CURVE('',#38986,#38987,#24938,.T.);
#50003=EDGE_CURVE('',#38987,#38988,#20714,.T.);
#50004=EDGE_CURVE('',#38988,#38989,#24939,.T.);
#50005=EDGE_CURVE('',#38989,#38990,#280,.T.);
#50006=EDGE_CURVE('',#38990,#38991,#24940,.T.);
#50007=EDGE_CURVE('',#38991,#38992,#20715,.T.);
#50008=EDGE_CURVE('',#38992,#38993,#24941,.T.);
#50009=EDGE_CURVE('',#38993,#38994,#281,.T.);
#50010=EDGE_CURVE('',#38994,#38995,#24942,.T.);
#50011=EDGE_CURVE('',#38995,#38996,#20716,.T.);
#50012=EDGE_CURVE('',#38996,#38997,#24943,.T.);
#50013=EDGE_CURVE('',#38997,#38998,#282,.T.);
#50014=EDGE_CURVE('',#38998,#38999,#24944,.T.);
#50015=EDGE_CURVE('',#38999,#39000,#20717,.T.);
#50016=EDGE_CURVE('',#39000,#39001,#24945,.T.);
#50017=EDGE_CURVE('',#39001,#39002,#283,.T.);
#50018=EDGE_CURVE('',#39002,#39003,#24946,.T.);
#50019=EDGE_CURVE('',#39003,#39004,#20718,.T.);
#50020=EDGE_CURVE('',#39004,#39005,#24947,.T.);
#50021=EDGE_CURVE('',#39005,#39006,#284,.T.);
#50022=EDGE_CURVE('',#39006,#39007,#24948,.T.);
#50023=EDGE_CURVE('',#39007,#39008,#20719,.T.);
#50024=EDGE_CURVE('',#39008,#39009,#24949,.T.);
#50025=EDGE_CURVE('',#39009,#39010,#285,.T.);
#50026=EDGE_CURVE('',#39010,#39011,#24950,.T.);
#50027=EDGE_CURVE('',#39011,#39012,#20720,.T.);
#50028=EDGE_CURVE('',#39012,#39013,#24951,.T.);
#50029=EDGE_CURVE('',#39013,#39014,#286,.T.);
#50030=EDGE_CURVE('',#39014,#39015,#24952,.T.);
#50031=EDGE_CURVE('',#39015,#39016,#20721,.T.);
#50032=EDGE_CURVE('',#39016,#39017,#24953,.T.);
#50033=EDGE_CURVE('',#39017,#39018,#287,.T.);
#50034=EDGE_CURVE('',#39018,#39019,#24954,.T.);
#50035=EDGE_CURVE('',#39019,#39020,#20722,.T.);
#50036=EDGE_CURVE('',#39020,#39021,#24955,.T.);
#50037=EDGE_CURVE('',#39021,#39022,#288,.T.);
#50038=EDGE_CURVE('',#39022,#39023,#24956,.T.);
#50039=EDGE_CURVE('',#39023,#39024,#20723,.T.);
#50040=EDGE_CURVE('',#39024,#39025,#24957,.T.);
#50041=EDGE_CURVE('',#39025,#39026,#289,.T.);
#50042=EDGE_CURVE('',#39026,#39027,#24958,.T.);
#50043=EDGE_CURVE('',#39027,#39028,#20724,.T.);
#50044=EDGE_CURVE('',#39028,#39029,#24959,.T.);
#50045=EDGE_CURVE('',#39029,#39030,#290,.T.);
#50046=EDGE_CURVE('',#39030,#39031,#24960,.T.);
#50047=EDGE_CURVE('',#39031,#39032,#20725,.T.);
#50048=EDGE_CURVE('',#39032,#39033,#24961,.T.);
#50049=EDGE_CURVE('',#39033,#39034,#291,.T.);
#50050=EDGE_CURVE('',#39034,#39035,#24962,.T.);
#50051=EDGE_CURVE('',#39035,#39036,#20726,.T.);
#50052=EDGE_CURVE('',#39036,#39037,#24963,.T.);
#50053=EDGE_CURVE('',#39037,#39038,#292,.T.);
#50054=EDGE_CURVE('',#39038,#39039,#24964,.T.);
#50055=EDGE_CURVE('',#39039,#39040,#20727,.T.);
#50056=EDGE_CURVE('',#39040,#39041,#24965,.T.);
#50057=EDGE_CURVE('',#39041,#39042,#293,.T.);
#50058=EDGE_CURVE('',#39042,#39043,#24966,.T.);
#50059=EDGE_CURVE('',#39043,#39044,#20728,.T.);
#50060=EDGE_CURVE('',#39044,#39045,#24967,.T.);
#50061=EDGE_CURVE('',#39045,#39046,#294,.T.);
#50062=EDGE_CURVE('',#39046,#39047,#24968,.T.);
#50063=EDGE_CURVE('',#39047,#39048,#20729,.T.);
#50064=EDGE_CURVE('',#39048,#39049,#24969,.T.);
#50065=EDGE_CURVE('',#39049,#39050,#295,.T.);
#50066=EDGE_CURVE('',#39050,#38656,#24970,.T.);
#50067=EDGE_CURVE('',#39051,#39051,#20730,.T.);
#50068=EDGE_CURVE('',#39051,#38855,#20731,.T.);
#50069=EDGE_CURVE('',#39052,#39053,#20732,.T.);
#50070=EDGE_CURVE('',#39052,#39054,#29141,.T.);
#50071=EDGE_CURVE('',#39055,#39054,#296,.T.);
#50072=EDGE_CURVE('',#39055,#39056,#20733,.T.);
#50073=EDGE_CURVE('',#39057,#39056,#297,.T.);
#50074=EDGE_CURVE('',#39057,#39058,#29142,.T.);
#50075=EDGE_CURVE('',#39059,#39058,#20734,.T.);
#50076=EDGE_CURVE('',#39059,#39060,#29143,.T.);
#50077=EDGE_CURVE('',#39061,#39060,#298,.T.);
#50078=EDGE_CURVE('',#39061,#39062,#20735,.T.);
#50079=EDGE_CURVE('',#39063,#39062,#299,.T.);
#50080=EDGE_CURVE('',#39063,#39064,#29144,.T.);
#50081=EDGE_CURVE('',#39065,#39064,#20736,.T.);
#50082=EDGE_CURVE('',#39065,#39066,#29145,.T.);
#50083=EDGE_CURVE('',#39067,#39066,#300,.T.);
#50084=EDGE_CURVE('',#39067,#39068,#20737,.T.);
#50085=EDGE_CURVE('',#39069,#39068,#301,.T.);
#50086=EDGE_CURVE('',#39069,#39070,#29146,.T.);
#50087=EDGE_CURVE('',#39071,#39070,#20738,.T.);
#50088=EDGE_CURVE('',#39071,#39072,#29147,.T.);
#50089=EDGE_CURVE('',#39073,#39072,#302,.T.);
#50090=EDGE_CURVE('',#39073,#39074,#20739,.T.);
#50091=EDGE_CURVE('',#39075,#39074,#303,.T.);
#50092=EDGE_CURVE('',#39075,#39076,#29148,.T.);
#50093=EDGE_CURVE('',#39077,#39076,#20740,.T.);
#50094=EDGE_CURVE('',#39077,#39078,#29149,.T.);
#50095=EDGE_CURVE('',#39079,#39078,#304,.T.);
#50096=EDGE_CURVE('',#39079,#39080,#20741,.T.);
#50097=EDGE_CURVE('',#39081,#39080,#305,.T.);
#50098=EDGE_CURVE('',#39081,#39082,#29150,.T.);
#50099=EDGE_CURVE('',#39083,#39082,#20742,.T.);
#50100=EDGE_CURVE('',#39083,#39084,#29151,.T.);
#50101=EDGE_CURVE('',#39085,#39084,#306,.T.);
#50102=EDGE_CURVE('',#39085,#39086,#20743,.T.);
#50103=EDGE_CURVE('',#39087,#39086,#307,.T.);
#50104=EDGE_CURVE('',#39087,#39088,#29152,.T.);
#50105=EDGE_CURVE('',#39089,#39088,#20744,.T.);
#50106=EDGE_CURVE('',#39089,#39090,#29153,.T.);
#50107=EDGE_CURVE('',#39091,#39090,#308,.T.);
#50108=EDGE_CURVE('',#39091,#39092,#20745,.T.);
#50109=EDGE_CURVE('',#39093,#39092,#309,.T.);
#50110=EDGE_CURVE('',#39093,#39094,#29154,.T.);
#50111=EDGE_CURVE('',#39095,#39094,#20746,.T.);
#50112=EDGE_CURVE('',#39095,#39096,#29155,.T.);
#50113=EDGE_CURVE('',#39097,#39096,#310,.T.);
#50114=EDGE_CURVE('',#39097,#39098,#20747,.T.);
#50115=EDGE_CURVE('',#39099,#39098,#311,.T.);
#50116=EDGE_CURVE('',#39099,#39100,#29156,.T.);
#50117=EDGE_CURVE('',#39101,#39100,#20748,.T.);
#50118=EDGE_CURVE('',#39101,#39102,#29157,.T.);
#50119=EDGE_CURVE('',#39103,#39102,#312,.T.);
#50120=EDGE_CURVE('',#39103,#39104,#20749,.T.);
#50121=EDGE_CURVE('',#39105,#39104,#313,.T.);
#50122=EDGE_CURVE('',#39105,#39106,#29158,.T.);
#50123=EDGE_CURVE('',#39107,#39106,#20750,.T.);
#50124=EDGE_CURVE('',#39107,#39108,#29159,.T.);
#50125=EDGE_CURVE('',#39109,#39108,#314,.T.);
#50126=EDGE_CURVE('',#39109,#39110,#20751,.T.);
#50127=EDGE_CURVE('',#39111,#39110,#315,.T.);
#50128=EDGE_CURVE('',#39111,#39112,#29160,.T.);
#50129=EDGE_CURVE('',#39113,#39112,#20752,.T.);
#50130=EDGE_CURVE('',#39113,#39114,#29161,.T.);
#50131=EDGE_CURVE('',#39115,#39114,#316,.T.);
#50132=EDGE_CURVE('',#39115,#39116,#20753,.T.);
#50133=EDGE_CURVE('',#39117,#39116,#317,.T.);
#50134=EDGE_CURVE('',#39117,#39118,#29162,.T.);
#50135=EDGE_CURVE('',#39119,#39118,#20754,.T.);
#50136=EDGE_CURVE('',#39119,#39120,#29163,.T.);
#50137=EDGE_CURVE('',#39121,#39120,#318,.T.);
#50138=EDGE_CURVE('',#39121,#39122,#20755,.T.);
#50139=EDGE_CURVE('',#39123,#39122,#319,.T.);
#50140=EDGE_CURVE('',#39123,#39124,#29164,.T.);
#50141=EDGE_CURVE('',#39125,#39124,#20756,.T.);
#50142=EDGE_CURVE('',#39125,#39126,#29165,.T.);
#50143=EDGE_CURVE('',#39127,#39126,#320,.T.);
#50144=EDGE_CURVE('',#39127,#39128,#20757,.T.);
#50145=EDGE_CURVE('',#39129,#39128,#321,.T.);
#50146=EDGE_CURVE('',#39129,#39130,#29166,.T.);
#50147=EDGE_CURVE('',#39131,#39130,#20758,.T.);
#50148=EDGE_CURVE('',#39131,#39132,#29167,.T.);
#50149=EDGE_CURVE('',#39133,#39132,#322,.T.);
#50150=EDGE_CURVE('',#39133,#39134,#20759,.T.);
#50151=EDGE_CURVE('',#39135,#39134,#323,.T.);
#50152=EDGE_CURVE('',#39135,#39136,#29168,.T.);
#50153=EDGE_CURVE('',#39137,#39136,#20760,.T.);
#50154=EDGE_CURVE('',#39137,#39138,#29169,.T.);
#50155=EDGE_CURVE('',#39139,#39138,#324,.T.);
#50156=EDGE_CURVE('',#39139,#39140,#20761,.T.);
#50157=EDGE_CURVE('',#39141,#39140,#325,.T.);
#50158=EDGE_CURVE('',#39141,#39142,#29170,.T.);
#50159=EDGE_CURVE('',#39143,#39142,#20762,.T.);
#50160=EDGE_CURVE('',#39143,#39144,#29171,.T.);
#50161=EDGE_CURVE('',#39145,#39144,#326,.T.);
#50162=EDGE_CURVE('',#39145,#39146,#20763,.T.);
#50163=EDGE_CURVE('',#39147,#39146,#327,.T.);
#50164=EDGE_CURVE('',#39147,#39148,#29172,.T.);
#50165=EDGE_CURVE('',#39149,#39148,#20764,.T.);
#50166=EDGE_CURVE('',#39149,#39150,#29173,.T.);
#50167=EDGE_CURVE('',#39151,#39150,#328,.T.);
#50168=EDGE_CURVE('',#39151,#39152,#20765,.T.);
#50169=EDGE_CURVE('',#39153,#39152,#329,.T.);
#50170=EDGE_CURVE('',#39153,#39154,#29174,.T.);
#50171=EDGE_CURVE('',#39155,#39154,#20766,.T.);
#50172=EDGE_CURVE('',#39155,#39156,#29175,.T.);
#50173=EDGE_CURVE('',#39157,#39156,#330,.T.);
#50174=EDGE_CURVE('',#39157,#39158,#20767,.T.);
#50175=EDGE_CURVE('',#39159,#39158,#331,.T.);
#50176=EDGE_CURVE('',#39159,#39160,#29176,.T.);
#50177=EDGE_CURVE('',#39161,#39160,#20768,.T.);
#50178=EDGE_CURVE('',#39161,#39162,#29177,.T.);
#50179=EDGE_CURVE('',#39163,#39162,#332,.T.);
#50180=EDGE_CURVE('',#39163,#39164,#20769,.T.);
#50181=EDGE_CURVE('',#39165,#39164,#333,.T.);
#50182=EDGE_CURVE('',#39165,#39166,#29178,.T.);
#50183=EDGE_CURVE('',#39167,#39166,#20770,.T.);
#50184=EDGE_CURVE('',#39167,#39168,#29179,.T.);
#50185=EDGE_CURVE('',#39169,#39168,#334,.T.);
#50186=EDGE_CURVE('',#39169,#39170,#20771,.T.);
#50187=EDGE_CURVE('',#39171,#39170,#335,.T.);
#50188=EDGE_CURVE('',#39171,#39172,#29180,.T.);
#50189=EDGE_CURVE('',#39173,#39172,#20772,.T.);
#50190=EDGE_CURVE('',#39173,#39174,#29181,.T.);
#50191=EDGE_CURVE('',#39175,#39174,#336,.T.);
#50192=EDGE_CURVE('',#39175,#39176,#20773,.T.);
#50193=EDGE_CURVE('',#39177,#39176,#337,.T.);
#50194=EDGE_CURVE('',#39177,#39178,#29182,.T.);
#50195=EDGE_CURVE('',#39179,#39178,#20774,.T.);
#50196=EDGE_CURVE('',#39179,#39180,#29183,.T.);
#50197=EDGE_CURVE('',#39181,#39180,#338,.T.);
#50198=EDGE_CURVE('',#39181,#39182,#20775,.T.);
#50199=EDGE_CURVE('',#39183,#39182,#339,.T.);
#50200=EDGE_CURVE('',#39183,#39184,#29184,.T.);
#50201=EDGE_CURVE('',#39185,#39184,#20776,.T.);
#50202=EDGE_CURVE('',#39185,#39186,#29185,.T.);
#50203=EDGE_CURVE('',#39187,#39186,#340,.T.);
#50204=EDGE_CURVE('',#39187,#39188,#20777,.T.);
#50205=EDGE_CURVE('',#39189,#39188,#341,.T.);
#50206=EDGE_CURVE('',#39189,#39190,#29186,.T.);
#50207=EDGE_CURVE('',#39191,#39190,#20778,.T.);
#50208=EDGE_CURVE('',#39191,#39192,#29187,.T.);
#50209=EDGE_CURVE('',#39193,#39192,#342,.T.);
#50210=EDGE_CURVE('',#39193,#39194,#20779,.T.);
#50211=EDGE_CURVE('',#39195,#39194,#343,.T.);
#50212=EDGE_CURVE('',#39195,#39196,#29188,.T.);
#50213=EDGE_CURVE('',#39197,#39196,#20780,.T.);
#50214=EDGE_CURVE('',#39197,#39198,#29189,.T.);
#50215=EDGE_CURVE('',#39199,#39198,#344,.T.);
#50216=EDGE_CURVE('',#39199,#39200,#20781,.T.);
#50217=EDGE_CURVE('',#39201,#39200,#345,.T.);
#50218=EDGE_CURVE('',#39201,#39202,#29190,.T.);
#50219=EDGE_CURVE('',#39203,#39202,#20782,.T.);
#50220=EDGE_CURVE('',#39203,#39204,#29191,.T.);
#50221=EDGE_CURVE('',#39205,#39204,#346,.T.);
#50222=EDGE_CURVE('',#39205,#39206,#20783,.T.);
#50223=EDGE_CURVE('',#39207,#39206,#347,.T.);
#50224=EDGE_CURVE('',#39207,#39208,#29192,.T.);
#50225=EDGE_CURVE('',#39209,#39208,#20784,.T.);
#50226=EDGE_CURVE('',#39209,#39210,#29193,.T.);
#50227=EDGE_CURVE('',#39211,#39210,#348,.T.);
#50228=EDGE_CURVE('',#39211,#39212,#20785,.T.);
#50229=EDGE_CURVE('',#39213,#39212,#349,.T.);
#50230=EDGE_CURVE('',#39213,#39214,#29194,.T.);
#50231=EDGE_CURVE('',#39215,#39214,#20786,.T.);
#50232=EDGE_CURVE('',#39215,#39216,#29195,.T.);
#50233=EDGE_CURVE('',#39217,#39216,#350,.T.);
#50234=EDGE_CURVE('',#39217,#39218,#20787,.T.);
#50235=EDGE_CURVE('',#39219,#39218,#351,.T.);
#50236=EDGE_CURVE('',#39219,#39220,#29196,.T.);
#50237=EDGE_CURVE('',#39221,#39220,#20788,.T.);
#50238=EDGE_CURVE('',#39221,#39222,#29197,.T.);
#50239=EDGE_CURVE('',#39223,#39222,#352,.T.);
#50240=EDGE_CURVE('',#39223,#39224,#20789,.T.);
#50241=EDGE_CURVE('',#39225,#39224,#353,.T.);
#50242=EDGE_CURVE('',#39225,#39226,#29198,.T.);
#50243=EDGE_CURVE('',#39227,#39226,#20790,.T.);
#50244=EDGE_CURVE('',#39227,#39228,#29199,.T.);
#50245=EDGE_CURVE('',#39229,#39228,#354,.T.);
#50246=EDGE_CURVE('',#39229,#39230,#20791,.T.);
#50247=EDGE_CURVE('',#39231,#39230,#355,.T.);
#50248=EDGE_CURVE('',#39231,#39232,#29200,.T.);
#50249=EDGE_CURVE('',#39233,#39232,#20792,.T.);
#50250=EDGE_CURVE('',#39233,#39234,#29201,.T.);
#50251=EDGE_CURVE('',#39235,#39234,#356,.T.);
#50252=EDGE_CURVE('',#39235,#39236,#20793,.T.);
#50253=EDGE_CURVE('',#39237,#39236,#357,.T.);
#50254=EDGE_CURVE('',#39237,#39238,#29202,.T.);
#50255=EDGE_CURVE('',#39239,#39238,#20794,.T.);
#50256=EDGE_CURVE('',#39239,#39240,#29203,.T.);
#50257=EDGE_CURVE('',#39241,#39240,#358,.T.);
#50258=EDGE_CURVE('',#39241,#39242,#20795,.T.);
#50259=EDGE_CURVE('',#39243,#39242,#359,.T.);
#50260=EDGE_CURVE('',#39243,#39244,#29204,.T.);
#50261=EDGE_CURVE('',#39245,#39244,#20796,.T.);
#50262=EDGE_CURVE('',#39245,#39246,#29205,.T.);
#50263=EDGE_CURVE('',#39247,#39246,#360,.T.);
#50264=EDGE_CURVE('',#39247,#39248,#20797,.T.);
#50265=EDGE_CURVE('',#39249,#39248,#361,.T.);
#50266=EDGE_CURVE('',#39249,#39250,#29206,.T.);
#50267=EDGE_CURVE('',#39251,#39250,#20798,.T.);
#50268=EDGE_CURVE('',#39251,#39252,#29207,.T.);
#50269=EDGE_CURVE('',#39253,#39252,#362,.T.);
#50270=EDGE_CURVE('',#39253,#39254,#20799,.T.);
#50271=EDGE_CURVE('',#39255,#39254,#363,.T.);
#50272=EDGE_CURVE('',#39255,#39256,#29208,.T.);
#50273=EDGE_CURVE('',#39257,#39256,#20800,.T.);
#50274=EDGE_CURVE('',#39257,#39258,#29209,.T.);
#50275=EDGE_CURVE('',#39259,#39258,#364,.T.);
#50276=EDGE_CURVE('',#39259,#39260,#20801,.T.);
#50277=EDGE_CURVE('',#39261,#39260,#365,.T.);
#50278=EDGE_CURVE('',#39261,#39262,#29210,.T.);
#50279=EDGE_CURVE('',#39263,#39262,#20802,.T.);
#50280=EDGE_CURVE('',#39263,#39264,#29211,.T.);
#50281=EDGE_CURVE('',#39265,#39264,#366,.T.);
#50282=EDGE_CURVE('',#39265,#39266,#20803,.T.);
#50283=EDGE_CURVE('',#39267,#39266,#367,.T.);
#50284=EDGE_CURVE('',#39267,#39268,#29212,.T.);
#50285=EDGE_CURVE('',#39269,#39268,#20804,.T.);
#50286=EDGE_CURVE('',#39269,#39270,#29213,.T.);
#50287=EDGE_CURVE('',#39271,#39270,#368,.T.);
#50288=EDGE_CURVE('',#39271,#39272,#20805,.T.);
#50289=EDGE_CURVE('',#39273,#39272,#369,.T.);
#50290=EDGE_CURVE('',#39273,#39274,#29214,.T.);
#50291=EDGE_CURVE('',#39275,#39274,#20806,.T.);
#50292=EDGE_CURVE('',#39275,#39276,#29215,.T.);
#50293=EDGE_CURVE('',#39277,#39276,#370,.T.);
#50294=EDGE_CURVE('',#39277,#39278,#20807,.T.);
#50295=EDGE_CURVE('',#39279,#39278,#371,.T.);
#50296=EDGE_CURVE('',#39279,#39280,#29216,.T.);
#50297=EDGE_CURVE('',#39281,#39280,#20808,.T.);
#50298=EDGE_CURVE('',#39281,#39282,#29217,.T.);
#50299=EDGE_CURVE('',#39283,#39282,#372,.T.);
#50300=EDGE_CURVE('',#39283,#39284,#20809,.T.);
#50301=EDGE_CURVE('',#39285,#39284,#373,.T.);
#50302=EDGE_CURVE('',#39285,#39286,#29218,.T.);
#50303=EDGE_CURVE('',#39287,#39286,#20810,.T.);
#50304=EDGE_CURVE('',#39287,#39288,#29219,.T.);
#50305=EDGE_CURVE('',#39289,#39288,#374,.T.);
#50306=EDGE_CURVE('',#39289,#39290,#20811,.T.);
#50307=EDGE_CURVE('',#39291,#39290,#375,.T.);
#50308=EDGE_CURVE('',#39291,#39292,#29220,.T.);
#50309=EDGE_CURVE('',#39293,#39292,#20812,.T.);
#50310=EDGE_CURVE('',#39293,#39294,#29221,.T.);
#50311=EDGE_CURVE('',#39295,#39294,#376,.T.);
#50312=EDGE_CURVE('',#39295,#39296,#20813,.T.);
#50313=EDGE_CURVE('',#39297,#39296,#377,.T.);
#50314=EDGE_CURVE('',#39297,#39298,#29222,.T.);
#50315=EDGE_CURVE('',#39299,#39298,#20814,.T.);
#50316=EDGE_CURVE('',#39299,#39300,#29223,.T.);
#50317=EDGE_CURVE('',#39301,#39300,#378,.T.);
#50318=EDGE_CURVE('',#39301,#39302,#20815,.T.);
#50319=EDGE_CURVE('',#39303,#39302,#379,.T.);
#50320=EDGE_CURVE('',#39303,#39304,#29224,.T.);
#50321=EDGE_CURVE('',#39305,#39304,#20816,.T.);
#50322=EDGE_CURVE('',#39305,#39306,#29225,.T.);
#50323=EDGE_CURVE('',#39307,#39306,#380,.T.);
#50324=EDGE_CURVE('',#39307,#39308,#20817,.T.);
#50325=EDGE_CURVE('',#39309,#39308,#381,.T.);
#50326=EDGE_CURVE('',#39309,#39310,#29226,.T.);
#50327=EDGE_CURVE('',#39311,#39310,#20818,.T.);
#50328=EDGE_CURVE('',#39311,#39312,#29227,.T.);
#50329=EDGE_CURVE('',#39313,#39312,#382,.T.);
#50330=EDGE_CURVE('',#39313,#39314,#20819,.T.);
#50331=EDGE_CURVE('',#39315,#39314,#383,.T.);
#50332=EDGE_CURVE('',#39315,#39316,#29228,.T.);
#50333=EDGE_CURVE('',#39317,#39316,#20820,.T.);
#50334=EDGE_CURVE('',#39317,#39318,#29229,.T.);
#50335=EDGE_CURVE('',#39319,#39318,#384,.T.);
#50336=EDGE_CURVE('',#39319,#39320,#20821,.T.);
#50337=EDGE_CURVE('',#39321,#39320,#385,.T.);
#50338=EDGE_CURVE('',#39321,#39322,#29230,.T.);
#50339=EDGE_CURVE('',#39323,#39322,#20822,.T.);
#50340=EDGE_CURVE('',#39323,#39324,#29231,.T.);
#50341=EDGE_CURVE('',#39325,#39324,#386,.T.);
#50342=EDGE_CURVE('',#39325,#39326,#20823,.T.);
#50343=EDGE_CURVE('',#39327,#39326,#387,.T.);
#50344=EDGE_CURVE('',#39327,#39328,#29232,.T.);
#50345=EDGE_CURVE('',#39329,#39328,#20824,.T.);
#50346=EDGE_CURVE('',#39329,#39330,#29233,.T.);
#50347=EDGE_CURVE('',#39331,#39330,#388,.T.);
#50348=EDGE_CURVE('',#39331,#39332,#20825,.T.);
#50349=EDGE_CURVE('',#39333,#39332,#389,.T.);
#50350=EDGE_CURVE('',#39333,#39334,#29234,.T.);
#50351=EDGE_CURVE('',#39335,#39334,#20826,.T.);
#50352=EDGE_CURVE('',#39335,#39336,#29235,.T.);
#50353=EDGE_CURVE('',#39337,#39336,#390,.T.);
#50354=EDGE_CURVE('',#39337,#39338,#20827,.T.);
#50355=EDGE_CURVE('',#39339,#39338,#391,.T.);
#50356=EDGE_CURVE('',#39339,#39340,#29236,.T.);
#50357=EDGE_CURVE('',#39341,#39340,#20828,.T.);
#50358=EDGE_CURVE('',#39341,#39342,#29237,.T.);
#50359=EDGE_CURVE('',#39343,#39342,#392,.T.);
#50360=EDGE_CURVE('',#39343,#39344,#20829,.T.);
#50361=EDGE_CURVE('',#39345,#39344,#393,.T.);
#50362=EDGE_CURVE('',#39345,#39346,#29238,.T.);
#50363=EDGE_CURVE('',#39347,#39346,#20830,.T.);
#50364=EDGE_CURVE('',#39347,#38655,#29239,.T.);
#50365=EDGE_CURVE('',#39348,#39347,#20831,.T.);
#50366=EDGE_CURVE('',#39348,#39349,#29240,.T.);
#50367=EDGE_CURVE('',#39350,#39349,#394,.T.);
#50368=EDGE_CURVE('',#39350,#39351,#20832,.T.);
#50369=EDGE_CURVE('',#39352,#39351,#395,.T.);
#50370=EDGE_CURVE('',#39352,#39353,#29241,.T.);
#50371=EDGE_CURVE('',#39354,#39353,#20833,.T.);
#50372=EDGE_CURVE('',#39354,#39355,#29242,.T.);
#50373=EDGE_CURVE('',#39356,#39355,#396,.T.);
#50374=EDGE_CURVE('',#39356,#39357,#20834,.T.);
#50375=EDGE_CURVE('',#39358,#39357,#397,.T.);
#50376=EDGE_CURVE('',#39358,#39359,#29243,.T.);
#50377=EDGE_CURVE('',#39360,#39359,#20835,.T.);
#50378=EDGE_CURVE('',#39360,#39361,#29244,.T.);
#50379=EDGE_CURVE('',#39362,#39361,#398,.T.);
#50380=EDGE_CURVE('',#39362,#39363,#20836,.T.);
#50381=EDGE_CURVE('',#39364,#39363,#399,.T.);
#50382=EDGE_CURVE('',#39364,#39365,#29245,.T.);
#50383=EDGE_CURVE('',#39366,#39365,#20837,.T.);
#50384=EDGE_CURVE('',#39366,#39367,#29246,.T.);
#50385=EDGE_CURVE('',#39368,#39367,#400,.T.);
#50386=EDGE_CURVE('',#39368,#39369,#20838,.T.);
#50387=EDGE_CURVE('',#39370,#39369,#401,.T.);
#50388=EDGE_CURVE('',#39370,#39371,#29247,.T.);
#50389=EDGE_CURVE('',#39372,#39371,#20839,.T.);
#50390=EDGE_CURVE('',#39372,#39373,#29248,.T.);
#50391=EDGE_CURVE('',#39374,#39373,#402,.T.);
#50392=EDGE_CURVE('',#39374,#39375,#20840,.T.);
#50393=EDGE_CURVE('',#39376,#39375,#403,.T.);
#50394=EDGE_CURVE('',#39376,#39377,#29249,.T.);
#50395=EDGE_CURVE('',#39378,#39377,#20841,.T.);
#50396=EDGE_CURVE('',#39378,#39379,#29250,.T.);
#50397=EDGE_CURVE('',#39380,#39379,#404,.T.);
#50398=EDGE_CURVE('',#39380,#39381,#20842,.T.);
#50399=EDGE_CURVE('',#39382,#39381,#405,.T.);
#50400=EDGE_CURVE('',#39382,#39383,#29251,.T.);
#50401=EDGE_CURVE('',#39384,#39383,#20843,.T.);
#50402=EDGE_CURVE('',#39384,#39385,#29252,.T.);
#50403=EDGE_CURVE('',#39386,#39385,#406,.T.);
#50404=EDGE_CURVE('',#39386,#39387,#20844,.T.);
#50405=EDGE_CURVE('',#39388,#39387,#407,.T.);
#50406=EDGE_CURVE('',#39388,#39389,#29253,.T.);
#50407=EDGE_CURVE('',#39390,#39389,#20845,.T.);
#50408=EDGE_CURVE('',#39390,#39391,#29254,.T.);
#50409=EDGE_CURVE('',#39392,#39391,#408,.T.);
#50410=EDGE_CURVE('',#39392,#39393,#20846,.T.);
#50411=EDGE_CURVE('',#39394,#39393,#409,.T.);
#50412=EDGE_CURVE('',#39394,#39395,#29255,.T.);
#50413=EDGE_CURVE('',#39396,#39395,#20847,.T.);
#50414=EDGE_CURVE('',#39396,#39397,#29256,.T.);
#50415=EDGE_CURVE('',#39398,#39397,#410,.T.);
#50416=EDGE_CURVE('',#39398,#39399,#20848,.T.);
#50417=EDGE_CURVE('',#39400,#39399,#411,.T.);
#50418=EDGE_CURVE('',#39400,#39401,#29257,.T.);
#50419=EDGE_CURVE('',#39402,#39401,#20849,.T.);
#50420=EDGE_CURVE('',#39402,#39403,#29258,.T.);
#50421=EDGE_CURVE('',#39404,#39403,#412,.T.);
#50422=EDGE_CURVE('',#39404,#39405,#20850,.T.);
#50423=EDGE_CURVE('',#39406,#39405,#413,.T.);
#50424=EDGE_CURVE('',#39406,#39407,#29259,.T.);
#50425=EDGE_CURVE('',#39408,#39407,#20851,.T.);
#50426=EDGE_CURVE('',#39408,#39409,#29260,.T.);
#50427=EDGE_CURVE('',#39410,#39409,#414,.T.);
#50428=EDGE_CURVE('',#39410,#39411,#20852,.T.);
#50429=EDGE_CURVE('',#39412,#39411,#415,.T.);
#50430=EDGE_CURVE('',#39412,#39413,#29261,.T.);
#50431=EDGE_CURVE('',#39414,#39413,#20853,.T.);
#50432=EDGE_CURVE('',#39414,#39415,#29262,.T.);
#50433=EDGE_CURVE('',#39416,#39415,#416,.T.);
#50434=EDGE_CURVE('',#39416,#39417,#20854,.T.);
#50435=EDGE_CURVE('',#39418,#39417,#417,.T.);
#50436=EDGE_CURVE('',#39418,#39419,#29263,.T.);
#50437=EDGE_CURVE('',#39420,#39419,#20855,.T.);
#50438=EDGE_CURVE('',#39420,#39421,#29264,.T.);
#50439=EDGE_CURVE('',#39422,#39421,#418,.T.);
#50440=EDGE_CURVE('',#39422,#39423,#20856,.T.);
#50441=EDGE_CURVE('',#39424,#39423,#419,.T.);
#50442=EDGE_CURVE('',#39424,#39425,#29265,.T.);
#50443=EDGE_CURVE('',#39426,#39425,#20857,.T.);
#50444=EDGE_CURVE('',#39426,#39427,#29266,.T.);
#50445=EDGE_CURVE('',#39428,#39427,#420,.T.);
#50446=EDGE_CURVE('',#39428,#39429,#20858,.T.);
#50447=EDGE_CURVE('',#39430,#39429,#421,.T.);
#50448=EDGE_CURVE('',#39430,#39431,#29267,.T.);
#50449=EDGE_CURVE('',#39432,#39431,#20859,.T.);
#50450=EDGE_CURVE('',#39432,#39433,#29268,.T.);
#50451=EDGE_CURVE('',#39434,#39433,#422,.T.);
#50452=EDGE_CURVE('',#39434,#39435,#20860,.T.);
#50453=EDGE_CURVE('',#39436,#39435,#423,.T.);
#50454=EDGE_CURVE('',#39436,#39437,#29269,.T.);
#50455=EDGE_CURVE('',#39438,#39437,#20861,.T.);
#50456=EDGE_CURVE('',#39438,#39439,#29270,.T.);
#50457=EDGE_CURVE('',#39440,#39439,#424,.T.);
#50458=EDGE_CURVE('',#39440,#39441,#20862,.T.);
#50459=EDGE_CURVE('',#39442,#39441,#425,.T.);
#50460=EDGE_CURVE('',#39442,#39443,#29271,.T.);
#50461=EDGE_CURVE('',#39444,#39443,#20863,.T.);
#50462=EDGE_CURVE('',#39444,#39445,#29272,.T.);
#50463=EDGE_CURVE('',#39446,#39445,#426,.T.);
#50464=EDGE_CURVE('',#39446,#39447,#20864,.T.);
#50465=EDGE_CURVE('',#39448,#39447,#427,.T.);
#50466=EDGE_CURVE('',#39448,#39449,#29273,.T.);
#50467=EDGE_CURVE('',#39450,#39449,#20865,.T.);
#50468=EDGE_CURVE('',#39450,#39451,#29274,.T.);
#50469=EDGE_CURVE('',#39452,#39451,#428,.T.);
#50470=EDGE_CURVE('',#39452,#39453,#20866,.T.);
#50471=EDGE_CURVE('',#39454,#39453,#429,.T.);
#50472=EDGE_CURVE('',#39454,#39455,#29275,.T.);
#50473=EDGE_CURVE('',#39456,#39455,#20867,.T.);
#50474=EDGE_CURVE('',#39456,#39457,#29276,.T.);
#50475=EDGE_CURVE('',#39458,#39457,#430,.T.);
#50476=EDGE_CURVE('',#39458,#39459,#20868,.T.);
#50477=EDGE_CURVE('',#39460,#39459,#431,.T.);
#50478=EDGE_CURVE('',#39460,#39461,#29277,.T.);
#50479=EDGE_CURVE('',#39462,#39461,#20869,.T.);
#50480=EDGE_CURVE('',#39462,#39463,#29278,.T.);
#50481=EDGE_CURVE('',#39464,#39463,#432,.T.);
#50482=EDGE_CURVE('',#39464,#39465,#20870,.T.);
#50483=EDGE_CURVE('',#39466,#39465,#433,.T.);
#50484=EDGE_CURVE('',#39466,#39467,#29279,.T.);
#50485=EDGE_CURVE('',#39468,#39467,#20871,.T.);
#50486=EDGE_CURVE('',#39468,#39469,#29280,.T.);
#50487=EDGE_CURVE('',#39470,#39469,#434,.T.);
#50488=EDGE_CURVE('',#39470,#39471,#20872,.T.);
#50489=EDGE_CURVE('',#39472,#39471,#435,.T.);
#50490=EDGE_CURVE('',#39472,#39473,#29281,.T.);
#50491=EDGE_CURVE('',#39474,#39473,#20873,.T.);
#50492=EDGE_CURVE('',#39474,#39475,#29282,.T.);
#50493=EDGE_CURVE('',#39476,#39475,#436,.T.);
#50494=EDGE_CURVE('',#39476,#39477,#20874,.T.);
#50495=EDGE_CURVE('',#39478,#39477,#437,.T.);
#50496=EDGE_CURVE('',#39478,#39479,#29283,.T.);
#50497=EDGE_CURVE('',#39480,#39479,#20875,.T.);
#50498=EDGE_CURVE('',#39480,#39481,#29284,.T.);
#50499=EDGE_CURVE('',#39482,#39481,#438,.T.);
#50500=EDGE_CURVE('',#39482,#39483,#20876,.T.);
#50501=EDGE_CURVE('',#39484,#39483,#439,.T.);
#50502=EDGE_CURVE('',#39484,#39485,#29285,.T.);
#50503=EDGE_CURVE('',#39486,#39485,#20877,.T.);
#50504=EDGE_CURVE('',#39486,#39487,#29286,.T.);
#50505=EDGE_CURVE('',#39488,#39487,#440,.T.);
#50506=EDGE_CURVE('',#39488,#39489,#20878,.T.);
#50507=EDGE_CURVE('',#39490,#39489,#441,.T.);
#50508=EDGE_CURVE('',#39490,#39491,#29287,.T.);
#50509=EDGE_CURVE('',#39492,#39491,#20879,.T.);
#50510=EDGE_CURVE('',#39492,#39493,#29288,.T.);
#50511=EDGE_CURVE('',#39494,#39493,#442,.T.);
#50512=EDGE_CURVE('',#39494,#39495,#20880,.T.);
#50513=EDGE_CURVE('',#39496,#39495,#443,.T.);
#50514=EDGE_CURVE('',#39496,#39497,#29289,.T.);
#50515=EDGE_CURVE('',#39498,#39497,#20881,.T.);
#50516=EDGE_CURVE('',#39498,#39499,#29290,.T.);
#50517=EDGE_CURVE('',#39500,#39499,#444,.T.);
#50518=EDGE_CURVE('',#39500,#39501,#20882,.T.);
#50519=EDGE_CURVE('',#39502,#39501,#445,.T.);
#50520=EDGE_CURVE('',#39502,#39503,#29291,.T.);
#50521=EDGE_CURVE('',#39504,#39503,#20883,.T.);
#50522=EDGE_CURVE('',#39504,#39505,#29292,.T.);
#50523=EDGE_CURVE('',#39506,#39505,#446,.T.);
#50524=EDGE_CURVE('',#39506,#39507,#20884,.T.);
#50525=EDGE_CURVE('',#39508,#39507,#447,.T.);
#50526=EDGE_CURVE('',#39508,#39509,#29293,.T.);
#50527=EDGE_CURVE('',#39510,#39509,#20885,.T.);
#50528=EDGE_CURVE('',#39510,#39511,#29294,.T.);
#50529=EDGE_CURVE('',#39512,#39511,#448,.T.);
#50530=EDGE_CURVE('',#39512,#39513,#20886,.T.);
#50531=EDGE_CURVE('',#39514,#39513,#449,.T.);
#50532=EDGE_CURVE('',#39514,#39515,#29295,.T.);
#50533=EDGE_CURVE('',#39516,#39515,#20887,.T.);
#50534=EDGE_CURVE('',#39516,#39517,#29296,.T.);
#50535=EDGE_CURVE('',#39518,#39517,#450,.T.);
#50536=EDGE_CURVE('',#39518,#39519,#20888,.T.);
#50537=EDGE_CURVE('',#39520,#39519,#451,.T.);
#50538=EDGE_CURVE('',#39520,#39521,#29297,.T.);
#50539=EDGE_CURVE('',#39522,#39521,#20889,.T.);
#50540=EDGE_CURVE('',#39522,#39523,#29298,.T.);
#50541=EDGE_CURVE('',#39524,#39523,#452,.T.);
#50542=EDGE_CURVE('',#39524,#39525,#20890,.T.);
#50543=EDGE_CURVE('',#39526,#39525,#453,.T.);
#50544=EDGE_CURVE('',#39526,#39527,#29299,.T.);
#50545=EDGE_CURVE('',#39528,#39527,#20891,.T.);
#50546=EDGE_CURVE('',#39528,#39529,#29300,.T.);
#50547=EDGE_CURVE('',#39530,#39529,#454,.T.);
#50548=EDGE_CURVE('',#39530,#39531,#20892,.T.);
#50549=EDGE_CURVE('',#39532,#39531,#455,.T.);
#50550=EDGE_CURVE('',#39532,#39533,#29301,.T.);
#50551=EDGE_CURVE('',#39534,#39533,#20893,.T.);
#50552=EDGE_CURVE('',#39534,#39535,#29302,.T.);
#50553=EDGE_CURVE('',#39536,#39535,#456,.T.);
#50554=EDGE_CURVE('',#39536,#39537,#20894,.T.);
#50555=EDGE_CURVE('',#39538,#39537,#457,.T.);
#50556=EDGE_CURVE('',#39538,#39539,#29303,.T.);
#50557=EDGE_CURVE('',#39540,#39539,#20895,.T.);
#50558=EDGE_CURVE('',#39540,#39541,#29304,.T.);
#50559=EDGE_CURVE('',#39542,#39541,#458,.T.);
#50560=EDGE_CURVE('',#39542,#39543,#20896,.T.);
#50561=EDGE_CURVE('',#39544,#39543,#459,.T.);
#50562=EDGE_CURVE('',#39544,#39545,#29305,.T.);
#50563=EDGE_CURVE('',#39546,#39545,#20897,.T.);
#50564=EDGE_CURVE('',#39546,#39547,#29306,.T.);
#50565=EDGE_CURVE('',#39548,#39547,#460,.T.);
#50566=EDGE_CURVE('',#39548,#39549,#20898,.T.);
#50567=EDGE_CURVE('',#39550,#39549,#461,.T.);
#50568=EDGE_CURVE('',#39550,#39551,#29307,.T.);
#50569=EDGE_CURVE('',#39552,#39551,#20899,.T.);
#50570=EDGE_CURVE('',#39552,#39553,#29308,.T.);
#50571=EDGE_CURVE('',#39554,#39553,#462,.T.);
#50572=EDGE_CURVE('',#39554,#39555,#20900,.T.);
#50573=EDGE_CURVE('',#39556,#39555,#463,.T.);
#50574=EDGE_CURVE('',#39556,#39557,#29309,.T.);
#50575=EDGE_CURVE('',#39558,#39557,#20901,.T.);
#50576=EDGE_CURVE('',#39558,#39559,#29310,.T.);
#50577=EDGE_CURVE('',#39560,#39559,#464,.T.);
#50578=EDGE_CURVE('',#39560,#39561,#20902,.T.);
#50579=EDGE_CURVE('',#39562,#39561,#465,.T.);
#50580=EDGE_CURVE('',#39562,#39563,#29311,.T.);
#50581=EDGE_CURVE('',#39564,#39563,#20903,.T.);
#50582=EDGE_CURVE('',#39564,#39565,#29312,.T.);
#50583=EDGE_CURVE('',#39566,#39565,#466,.T.);
#50584=EDGE_CURVE('',#39566,#39567,#20904,.T.);
#50585=EDGE_CURVE('',#39568,#39567,#467,.T.);
#50586=EDGE_CURVE('',#39568,#39569,#29313,.T.);
#50587=EDGE_CURVE('',#39570,#39569,#20905,.T.);
#50588=EDGE_CURVE('',#39570,#39571,#29314,.T.);
#50589=EDGE_CURVE('',#39572,#39571,#468,.T.);
#50590=EDGE_CURVE('',#39572,#39573,#20906,.T.);
#50591=EDGE_CURVE('',#39574,#39573,#469,.T.);
#50592=EDGE_CURVE('',#39574,#39575,#29315,.T.);
#50593=EDGE_CURVE('',#39576,#39575,#20907,.T.);
#50594=EDGE_CURVE('',#39576,#39577,#29316,.T.);
#50595=EDGE_CURVE('',#39578,#39577,#470,.T.);
#50596=EDGE_CURVE('',#39578,#39579,#20908,.T.);
#50597=EDGE_CURVE('',#39580,#39579,#471,.T.);
#50598=EDGE_CURVE('',#39580,#39581,#29317,.T.);
#50599=EDGE_CURVE('',#39582,#39581,#20909,.T.);
#50600=EDGE_CURVE('',#39582,#39583,#29318,.T.);
#50601=EDGE_CURVE('',#39584,#39583,#472,.T.);
#50602=EDGE_CURVE('',#39584,#39585,#20910,.T.);
#50603=EDGE_CURVE('',#39586,#39585,#473,.T.);
#50604=EDGE_CURVE('',#39586,#39587,#29319,.T.);
#50605=EDGE_CURVE('',#39588,#39587,#20911,.T.);
#50606=EDGE_CURVE('',#39588,#39589,#29320,.T.);
#50607=EDGE_CURVE('',#39590,#39589,#474,.T.);
#50608=EDGE_CURVE('',#39590,#39591,#20912,.T.);
#50609=EDGE_CURVE('',#39592,#39591,#475,.T.);
#50610=EDGE_CURVE('',#39592,#39593,#29321,.T.);
#50611=EDGE_CURVE('',#39594,#39593,#20913,.T.);
#50612=EDGE_CURVE('',#39594,#39595,#29322,.T.);
#50613=EDGE_CURVE('',#39596,#39595,#476,.T.);
#50614=EDGE_CURVE('',#39596,#39597,#20914,.T.);
#50615=EDGE_CURVE('',#39598,#39597,#477,.T.);
#50616=EDGE_CURVE('',#39598,#39599,#29323,.T.);
#50617=EDGE_CURVE('',#39600,#39599,#20915,.T.);
#50618=EDGE_CURVE('',#39600,#39601,#29324,.T.);
#50619=EDGE_CURVE('',#39602,#39601,#478,.T.);
#50620=EDGE_CURVE('',#39602,#39603,#20916,.T.);
#50621=EDGE_CURVE('',#39604,#39603,#479,.T.);
#50622=EDGE_CURVE('',#39604,#39605,#29325,.T.);
#50623=EDGE_CURVE('',#39606,#39605,#20917,.T.);
#50624=EDGE_CURVE('',#39606,#39607,#29326,.T.);
#50625=EDGE_CURVE('',#39608,#39607,#480,.T.);
#50626=EDGE_CURVE('',#39608,#39609,#20918,.T.);
#50627=EDGE_CURVE('',#39610,#39609,#481,.T.);
#50628=EDGE_CURVE('',#39610,#39611,#29327,.T.);
#50629=EDGE_CURVE('',#39612,#39611,#20919,.T.);
#50630=EDGE_CURVE('',#39612,#39613,#29328,.T.);
#50631=EDGE_CURVE('',#39614,#39613,#482,.T.);
#50632=EDGE_CURVE('',#39614,#39615,#20920,.T.);
#50633=EDGE_CURVE('',#39616,#39615,#483,.T.);
#50634=EDGE_CURVE('',#39616,#39617,#29329,.T.);
#50635=EDGE_CURVE('',#39618,#39617,#20921,.T.);
#50636=EDGE_CURVE('',#39618,#39619,#29330,.T.);
#50637=EDGE_CURVE('',#39620,#39619,#484,.T.);
#50638=EDGE_CURVE('',#39620,#39621,#20922,.T.);
#50639=EDGE_CURVE('',#39622,#39621,#485,.T.);
#50640=EDGE_CURVE('',#39622,#39623,#29331,.T.);
#50641=EDGE_CURVE('',#39624,#39623,#20923,.T.);
#50642=EDGE_CURVE('',#39624,#39625,#29332,.T.);
#50643=EDGE_CURVE('',#39626,#39625,#486,.T.);
#50644=EDGE_CURVE('',#39626,#39627,#20924,.T.);
#50645=EDGE_CURVE('',#39628,#39627,#487,.T.);
#50646=EDGE_CURVE('',#39628,#39629,#29333,.T.);
#50647=EDGE_CURVE('',#39630,#39629,#20925,.T.);
#50648=EDGE_CURVE('',#39630,#39631,#29334,.T.);
#50649=EDGE_CURVE('',#39632,#39631,#488,.T.);
#50650=EDGE_CURVE('',#39632,#39633,#20926,.T.);
#50651=EDGE_CURVE('',#39634,#39633,#489,.T.);
#50652=EDGE_CURVE('',#39634,#39635,#29335,.T.);
#50653=EDGE_CURVE('',#39636,#39635,#20927,.T.);
#50654=EDGE_CURVE('',#39636,#39637,#29336,.T.);
#50655=EDGE_CURVE('',#39638,#39637,#490,.T.);
#50656=EDGE_CURVE('',#39638,#39639,#20928,.T.);
#50657=EDGE_CURVE('',#39640,#39639,#491,.T.);
#50658=EDGE_CURVE('',#39640,#39053,#29337,.T.);
#50659=EDGE_CURVE('',#39053,#38856,#492,.T.);
#50660=EDGE_CURVE('',#38852,#39052,#493,.T.);
#50661=EDGE_CURVE('',#38820,#39101,#494,.T.);
#50662=EDGE_CURVE('',#39100,#38821,#495,.T.);
#50663=EDGE_CURVE('',#39106,#38817,#496,.T.);
#50664=EDGE_CURVE('',#38816,#39107,#497,.T.);
#50665=EDGE_CURVE('',#39112,#38813,#498,.T.);
#50666=EDGE_CURVE('',#38812,#39113,#499,.T.);
#50667=EDGE_CURVE('',#39118,#38809,#500,.T.);
#50668=EDGE_CURVE('',#38808,#39119,#501,.T.);
#50669=EDGE_CURVE('',#39124,#38805,#502,.T.);
#50670=EDGE_CURVE('',#38804,#39125,#503,.T.);
#50671=EDGE_CURVE('',#39130,#38801,#504,.T.);
#50672=EDGE_CURVE('',#38800,#39131,#505,.T.);
#50673=EDGE_CURVE('',#39136,#38797,#506,.T.);
#50674=EDGE_CURVE('',#38796,#39137,#507,.T.);
#50675=EDGE_CURVE('',#39142,#38793,#508,.T.);
#50676=EDGE_CURVE('',#38792,#39143,#509,.T.);
#50677=EDGE_CURVE('',#39148,#38789,#510,.T.);
#50678=EDGE_CURVE('',#38788,#39149,#511,.T.);
#50679=EDGE_CURVE('',#39154,#38785,#512,.T.);
#50680=EDGE_CURVE('',#38784,#39155,#513,.T.);
#50681=EDGE_CURVE('',#39160,#38781,#514,.T.);
#50682=EDGE_CURVE('',#38780,#39161,#515,.T.);
#50683=EDGE_CURVE('',#39166,#38777,#516,.T.);
#50684=EDGE_CURVE('',#38776,#39167,#517,.T.);
#50685=EDGE_CURVE('',#39172,#38773,#518,.T.);
#50686=EDGE_CURVE('',#38772,#39173,#519,.T.);
#50687=EDGE_CURVE('',#39178,#38769,#520,.T.);
#50688=EDGE_CURVE('',#38768,#39179,#521,.T.);
#50689=EDGE_CURVE('',#39184,#38765,#522,.T.);
#50690=EDGE_CURVE('',#38764,#39185,#523,.T.);
#50691=EDGE_CURVE('',#39190,#38761,#524,.T.);
#50692=EDGE_CURVE('',#38760,#39191,#525,.T.);
#50693=EDGE_CURVE('',#39196,#38757,#526,.T.);
#50694=EDGE_CURVE('',#38756,#39197,#527,.T.);
#50695=EDGE_CURVE('',#39202,#38753,#528,.T.);
#50696=EDGE_CURVE('',#38752,#39203,#529,.T.);
#50697=EDGE_CURVE('',#39208,#38749,#530,.T.);
#50698=EDGE_CURVE('',#38748,#39209,#531,.T.);
#50699=EDGE_CURVE('',#39214,#38745,#532,.T.);
#50700=EDGE_CURVE('',#38744,#39215,#533,.T.);
#50701=EDGE_CURVE('',#39220,#38741,#534,.T.);
#50702=EDGE_CURVE('',#38740,#39221,#535,.T.);
#50703=EDGE_CURVE('',#39226,#38737,#536,.T.);
#50704=EDGE_CURVE('',#38736,#39227,#537,.T.);
#50705=EDGE_CURVE('',#39232,#38733,#538,.T.);
#50706=EDGE_CURVE('',#38732,#39233,#539,.T.);
#50707=EDGE_CURVE('',#39238,#38729,#540,.T.);
#50708=EDGE_CURVE('',#38728,#39239,#541,.T.);
#50709=EDGE_CURVE('',#39244,#38725,#542,.T.);
#50710=EDGE_CURVE('',#38724,#39245,#543,.T.);
#50711=EDGE_CURVE('',#39250,#38721,#544,.T.);
#50712=EDGE_CURVE('',#38720,#39251,#545,.T.);
#50713=EDGE_CURVE('',#39256,#38717,#546,.T.);
#50714=EDGE_CURVE('',#38716,#39257,#547,.T.);
#50715=EDGE_CURVE('',#39262,#38713,#548,.T.);
#50716=EDGE_CURVE('',#38712,#39263,#549,.T.);
#50717=EDGE_CURVE('',#39268,#38709,#550,.T.);
#50718=EDGE_CURVE('',#38708,#39269,#551,.T.);
#50719=EDGE_CURVE('',#39274,#38705,#552,.T.);
#50720=EDGE_CURVE('',#38704,#39275,#553,.T.);
#50721=EDGE_CURVE('',#39280,#38701,#554,.T.);
#50722=EDGE_CURVE('',#38700,#39281,#555,.T.);
#50723=EDGE_CURVE('',#39286,#38697,#556,.T.);
#50724=EDGE_CURVE('',#38696,#39287,#557,.T.);
#50725=EDGE_CURVE('',#39292,#38693,#558,.T.);
#50726=EDGE_CURVE('',#38692,#39293,#559,.T.);
#50727=EDGE_CURVE('',#39298,#38689,#560,.T.);
#50728=EDGE_CURVE('',#38688,#39299,#561,.T.);
#50729=EDGE_CURVE('',#39304,#38685,#562,.T.);
#50730=EDGE_CURVE('',#38684,#39305,#563,.T.);
#50731=EDGE_CURVE('',#39310,#38681,#564,.T.);
#50732=EDGE_CURVE('',#38680,#39311,#565,.T.);
#50733=EDGE_CURVE('',#39316,#38677,#566,.T.);
#50734=EDGE_CURVE('',#38676,#39317,#567,.T.);
#50735=EDGE_CURVE('',#39322,#38673,#568,.T.);
#50736=EDGE_CURVE('',#38672,#39323,#569,.T.);
#50737=EDGE_CURVE('',#39328,#38669,#570,.T.);
#50738=EDGE_CURVE('',#38668,#39329,#571,.T.);
#50739=EDGE_CURVE('',#39334,#38665,#572,.T.);
#50740=EDGE_CURVE('',#38664,#39335,#573,.T.);
#50741=EDGE_CURVE('',#39340,#38661,#574,.T.);
#50742=EDGE_CURVE('',#38660,#39341,#575,.T.);
#50743=EDGE_CURVE('',#39346,#38657,#576,.T.);
#50744=EDGE_CURVE('',#38656,#39348,#577,.T.);
#50745=EDGE_CURVE('',#39353,#39048,#578,.T.);
#50746=EDGE_CURVE('',#39047,#39354,#579,.T.);
#50747=EDGE_CURVE('',#39359,#39044,#580,.T.);
#50748=EDGE_CURVE('',#39043,#39360,#581,.T.);
#50749=EDGE_CURVE('',#39365,#39040,#582,.T.);
#50750=EDGE_CURVE('',#39039,#39366,#583,.T.);
#50751=EDGE_CURVE('',#39371,#39036,#584,.T.);
#50752=EDGE_CURVE('',#39035,#39372,#585,.T.);
#50753=EDGE_CURVE('',#39377,#39032,#586,.T.);
#50754=EDGE_CURVE('',#39031,#39378,#587,.T.);
#50755=EDGE_CURVE('',#39383,#39028,#588,.T.);
#50756=EDGE_CURVE('',#39027,#39384,#589,.T.);
#50757=EDGE_CURVE('',#39389,#39024,#590,.T.);
#50758=EDGE_CURVE('',#39023,#39390,#591,.T.);
#50759=EDGE_CURVE('',#39395,#39020,#592,.T.);
#50760=EDGE_CURVE('',#39019,#39396,#593,.T.);
#50761=EDGE_CURVE('',#39401,#39016,#594,.T.);
#50762=EDGE_CURVE('',#39015,#39402,#595,.T.);
#50763=EDGE_CURVE('',#39407,#39012,#596,.T.);
#50764=EDGE_CURVE('',#39011,#39408,#597,.T.);
#50765=EDGE_CURVE('',#39413,#39008,#598,.T.);
#50766=EDGE_CURVE('',#39007,#39414,#599,.T.);
#50767=EDGE_CURVE('',#39419,#39004,#600,.T.);
#50768=EDGE_CURVE('',#39003,#39420,#601,.T.);
#50769=EDGE_CURVE('',#39425,#39000,#602,.T.);
#50770=EDGE_CURVE('',#38999,#39426,#603,.T.);
#50771=EDGE_CURVE('',#39431,#38996,#604,.T.);
#50772=EDGE_CURVE('',#38995,#39432,#605,.T.);
#50773=EDGE_CURVE('',#39437,#38992,#606,.T.);
#50774=EDGE_CURVE('',#38991,#39438,#607,.T.);
#50775=EDGE_CURVE('',#39443,#38988,#608,.T.);
#50776=EDGE_CURVE('',#38987,#39444,#609,.T.);
#50777=EDGE_CURVE('',#39449,#38984,#610,.T.);
#50778=EDGE_CURVE('',#38983,#39450,#611,.T.);
#50779=EDGE_CURVE('',#39455,#38980,#612,.T.);
#50780=EDGE_CURVE('',#38979,#39456,#613,.T.);
#50781=EDGE_CURVE('',#39461,#38976,#614,.T.);
#50782=EDGE_CURVE('',#38975,#39462,#615,.T.);
#50783=EDGE_CURVE('',#39467,#38972,#616,.T.);
#50784=EDGE_CURVE('',#38971,#39468,#617,.T.);
#50785=EDGE_CURVE('',#39473,#38968,#618,.T.);
#50786=EDGE_CURVE('',#38967,#39474,#619,.T.);
#50787=EDGE_CURVE('',#39479,#38964,#620,.T.);
#50788=EDGE_CURVE('',#38963,#39480,#621,.T.);
#50789=EDGE_CURVE('',#38824,#39095,#622,.T.);
#50790=EDGE_CURVE('',#39094,#38825,#623,.T.);
#50791=EDGE_CURVE('',#38828,#39089,#624,.T.);
#50792=EDGE_CURVE('',#39088,#38829,#625,.T.);
#50793=EDGE_CURVE('',#38832,#39083,#626,.T.);
#50794=EDGE_CURVE('',#39082,#38833,#627,.T.);
#50795=EDGE_CURVE('',#38836,#39077,#628,.T.);
#50796=EDGE_CURVE('',#39076,#38837,#629,.T.);
#50797=EDGE_CURVE('',#38840,#39071,#630,.T.);
#50798=EDGE_CURVE('',#39070,#38841,#631,.T.);
#50799=EDGE_CURVE('',#38844,#39065,#632,.T.);
#50800=EDGE_CURVE('',#39064,#38845,#633,.T.);
#50801=EDGE_CURVE('',#38848,#39059,#634,.T.);
#50802=EDGE_CURVE('',#39058,#38849,#635,.T.);
#50803=EDGE_CURVE('',#38859,#39636,#636,.T.);
#50804=EDGE_CURVE('',#39635,#38860,#637,.T.);
#50805=EDGE_CURVE('',#38863,#39630,#638,.T.);
#50806=EDGE_CURVE('',#39629,#38864,#639,.T.);
#50807=EDGE_CURVE('',#38867,#39624,#640,.T.);
#50808=EDGE_CURVE('',#39623,#38868,#641,.T.);
#50809=EDGE_CURVE('',#38871,#39618,#642,.T.);
#50810=EDGE_CURVE('',#39617,#38872,#643,.T.);
#50811=EDGE_CURVE('',#38875,#39612,#644,.T.);
#50812=EDGE_CURVE('',#39611,#38876,#645,.T.);
#50813=EDGE_CURVE('',#38879,#39606,#646,.T.);
#50814=EDGE_CURVE('',#39605,#38880,#647,.T.);
#50815=EDGE_CURVE('',#38883,#39600,#648,.T.);
#50816=EDGE_CURVE('',#39599,#38884,#649,.T.);
#50817=EDGE_CURVE('',#38887,#39594,#650,.T.);
#50818=EDGE_CURVE('',#39593,#38888,#651,.T.);
#50819=EDGE_CURVE('',#38891,#39588,#652,.T.);
#50820=EDGE_CURVE('',#39587,#38892,#653,.T.);
#50821=EDGE_CURVE('',#38895,#39582,#654,.T.);
#50822=EDGE_CURVE('',#39581,#38896,#655,.T.);
#50823=EDGE_CURVE('',#38899,#39576,#656,.T.);
#50824=EDGE_CURVE('',#39575,#38900,#657,.T.);
#50825=EDGE_CURVE('',#38903,#39570,#658,.T.);
#50826=EDGE_CURVE('',#39569,#38904,#659,.T.);
#50827=EDGE_CURVE('',#38907,#39564,#660,.T.);
#50828=EDGE_CURVE('',#39563,#38908,#661,.T.);
#50829=EDGE_CURVE('',#38911,#39558,#662,.T.);
#50830=EDGE_CURVE('',#39557,#38912,#663,.T.);
#50831=EDGE_CURVE('',#38915,#39552,#664,.T.);
#50832=EDGE_CURVE('',#39551,#38916,#665,.T.);
#50833=EDGE_CURVE('',#38919,#39546,#666,.T.);
#50834=EDGE_CURVE('',#39545,#38920,#667,.T.);
#50835=EDGE_CURVE('',#38923,#39540,#668,.T.);
#50836=EDGE_CURVE('',#39539,#38924,#669,.T.);
#50837=EDGE_CURVE('',#38927,#39534,#670,.T.);
#50838=EDGE_CURVE('',#39533,#38928,#671,.T.);
#50839=EDGE_CURVE('',#38931,#39528,#672,.T.);
#50840=EDGE_CURVE('',#39527,#38932,#673,.T.);
#50841=EDGE_CURVE('',#38935,#39522,#674,.T.);
#50842=EDGE_CURVE('',#39521,#38936,#675,.T.);
#50843=EDGE_CURVE('',#38939,#39516,#676,.T.);
#50844=EDGE_CURVE('',#39515,#38940,#677,.T.);
#50845=EDGE_CURVE('',#38943,#39510,#678,.T.);
#50846=EDGE_CURVE('',#39509,#38944,#679,.T.);
#50847=EDGE_CURVE('',#38947,#39504,#680,.T.);
#50848=EDGE_CURVE('',#39503,#38948,#681,.T.);
#50849=EDGE_CURVE('',#38951,#39498,#682,.T.);
#50850=EDGE_CURVE('',#39497,#38952,#683,.T.);
#50851=EDGE_CURVE('',#39485,#38960,#684,.T.);
#50852=EDGE_CURVE('',#38959,#39486,#685,.T.);
#50853=EDGE_CURVE('',#39641,#39642,#29338,.T.);
#50854=EDGE_CURVE('',#39642,#39643,#24971,.T.);
#50855=EDGE_CURVE('',#39644,#39643,#29339,.T.);
#50856=EDGE_CURVE('',#39644,#39641,#20929,.T.);
#50857=EDGE_CURVE('',#39645,#39646,#686,.T.);
#50858=EDGE_CURVE('',#39646,#39642,#24972,.T.);
#50859=EDGE_CURVE('',#39641,#39647,#24973,.T.);
#50860=EDGE_CURVE('',#39647,#39645,#29340,.T.);
#50861=EDGE_CURVE('',#39643,#39648,#24974,.T.);
#50862=EDGE_CURVE('',#39648,#39649,#687,.T.);
#50863=EDGE_CURVE('',#39649,#39650,#29341,.T.);
#50864=EDGE_CURVE('',#39650,#39644,#24975,.T.);
#50865=EDGE_CURVE('',#39651,#38644,#29342,.T.);
#50866=EDGE_CURVE('',#38649,#39651,#29343,.T.);
#50867=EDGE_CURVE('',#39652,#38649,#29344,.T.);
#50868=EDGE_CURVE('',#38648,#39652,#29345,.T.);
#50869=EDGE_CURVE('',#39653,#38648,#29346,.T.);
#50870=EDGE_CURVE('',#38647,#39653,#29347,.T.);
#50871=EDGE_CURVE('',#39654,#38647,#29348,.T.);
#50872=EDGE_CURVE('',#38646,#39654,#29349,.T.);
#50873=EDGE_CURVE('',#39655,#38646,#29350,.T.);
#50874=EDGE_CURVE('',#38645,#39655,#29351,.T.);
#50875=EDGE_CURVE('',#39656,#39657,#20930,.T.);
#50876=EDGE_CURVE('',#38650,#39656,#20931,.T.);
#50877=EDGE_CURVE('',#39658,#38651,#20932,.T.);
#50878=EDGE_CURVE('',#39659,#39658,#20933,.T.);
#50879=EDGE_CURVE('',#39657,#39659,#20934,.T.);
#50880=EDGE_CURVE('',#39491,#38956,#688,.T.);
#50881=EDGE_CURVE('',#38955,#39492,#689,.T.);
#50882=EDGE_CURVE('',#39653,#38650,#29352,.T.);
#50883=EDGE_CURVE('',#39656,#38650,#4319,.T.);
#50884=EDGE_CURVE('',#39652,#39656,#29353,.T.);
#50885=EDGE_CURVE('',#39654,#38651,#29354,.T.);
#50886=EDGE_CURVE('',#39655,#39658,#29355,.T.);
#50887=EDGE_CURVE('',#38651,#39658,#4320,.T.);
#50888=EDGE_CURVE('',#39660,#39659,#29356,.T.);
#50889=EDGE_CURVE('',#39658,#39659,#4321,.T.);
#50890=EDGE_CURVE('',#39660,#38645,#29357,.T.);
#50891=EDGE_CURVE('',#39651,#39657,#29358,.T.);
#50892=EDGE_CURVE('',#39659,#39657,#4322,.T.);
#50893=EDGE_CURVE('',#38644,#39660,#29359,.T.);
#50894=EDGE_CURVE('',#39657,#39656,#4323,.T.);
#50895=EDGE_CURVE('',#38574,#38637,#4324,.T.);
#50896=EDGE_CURVE('',#38573,#38636,#4325,.T.);
#50897=EDGE_CURVE('',#39661,#39662,#24976,.T.);
#50898=EDGE_CURVE('',#39662,#39663,#24977,.T.);
#50899=EDGE_CURVE('',#39663,#39661,#20935,.T.);
#50900=EDGE_CURVE('',#39647,#39661,#24978,.T.);
#50901=EDGE_CURVE('',#39662,#39641,#690,.T.);
#50902=EDGE_CURVE('',#39645,#39492,#20936,.T.);
#50903=EDGE_CURVE('',#39493,#39647,#20937,.T.);
#50904=EDGE_CURVE('',#39662,#39644,#691,.T.);
#50905=EDGE_CURVE('',#39494,#39661,#20938,.T.);
#50906=EDGE_CURVE('',#39646,#38955,#20939,.T.);
#50907=EDGE_CURVE('',#39663,#39650,#24979,.T.);
#50908=EDGE_CURVE('',#39495,#39663,#20940,.T.);
#50909=EDGE_CURVE('',#39642,#38954,#20941,.T.);
#50910=EDGE_CURVE('',#39496,#39650,#20942,.T.);
#50911=EDGE_CURVE('',#39643,#38953,#20943,.T.);
#50912=EDGE_CURVE('',#39497,#39649,#20944,.T.);
#50913=EDGE_CURVE('',#39648,#38952,#20945,.T.);
#50914=EDGE_CURVE('',#39664,#39665,#29360,.T.);
#50915=EDGE_CURVE('',#39665,#39666,#24980,.T.);
#50916=EDGE_CURVE('',#39666,#39667,#692,.T.);
#50917=EDGE_CURVE('',#39667,#39668,#29361,.T.);
#50918=EDGE_CURVE('',#39668,#39664,#24981,.T.);
#50919=EDGE_CURVE('',#39669,#39670,#693,.T.);
#50920=EDGE_CURVE('',#39670,#39671,#24982,.T.);
#50921=EDGE_CURVE('',#39672,#39671,#29362,.T.);
#50922=EDGE_CURVE('',#39672,#39673,#24983,.T.);
#50923=EDGE_CURVE('',#39673,#39669,#29363,.T.);
#50924=EDGE_CURVE('',#39671,#39665,#24984,.T.);
#50925=EDGE_CURVE('',#39664,#39672,#20946,.T.);
#50926=EDGE_CURVE('',#39673,#39674,#24985,.T.);
#50927=EDGE_CURVE('',#39675,#39672,#694,.T.);
#50928=EDGE_CURVE('',#39674,#39675,#24986,.T.);
#50929=EDGE_CURVE('',#39675,#39664,#695,.T.);
#50930=EDGE_CURVE('',#39676,#39668,#24987,.T.);
#50931=EDGE_CURVE('',#39675,#39676,#24988,.T.);
#50932=EDGE_CURVE('',#39488,#39674,#20947,.T.);
#50933=EDGE_CURVE('',#39676,#39674,#20948,.T.);
#50934=EDGE_CURVE('',#39489,#39676,#20949,.T.);
#50935=EDGE_CURVE('',#39487,#39673,#20950,.T.);
#50936=EDGE_CURVE('',#39669,#39486,#20951,.T.);
#50937=EDGE_CURVE('',#39670,#38959,#20952,.T.);
#50938=EDGE_CURVE('',#39671,#38958,#20953,.T.);
#50939=EDGE_CURVE('',#39665,#38957,#20954,.T.);
#50940=EDGE_CURVE('',#39666,#38956,#20955,.T.);
#50941=EDGE_CURVE('',#39491,#39667,#20956,.T.);
#50942=EDGE_CURVE('',#39490,#39668,#20957,.T.);
#50943=EDGE_CURVE('',#39677,#39678,#29364,.T.);
#50944=EDGE_CURVE('',#39678,#39679,#24989,.T.);
#50945=EDGE_CURVE('',#39679,#39680,#696,.T.);
#50946=EDGE_CURVE('',#39680,#39681,#29365,.T.);
#50947=EDGE_CURVE('',#39681,#39677,#24990,.T.);
#50948=EDGE_CURVE('',#39682,#39683,#697,.T.);
#50949=EDGE_CURVE('',#39683,#39684,#24991,.T.);
#50950=EDGE_CURVE('',#39685,#39684,#29366,.T.);
#50951=EDGE_CURVE('',#39685,#39686,#24992,.T.);
#50952=EDGE_CURVE('',#39686,#39682,#29367,.T.);
#50953=EDGE_CURVE('',#39684,#39678,#24993,.T.);
#50954=EDGE_CURVE('',#39677,#39685,#20958,.T.);
#50955=EDGE_CURVE('',#39686,#39687,#24994,.T.);
#50956=EDGE_CURVE('',#39688,#39685,#698,.T.);
#50957=EDGE_CURVE('',#39687,#39688,#24995,.T.);
#50958=EDGE_CURVE('',#39688,#39677,#699,.T.);
#50959=EDGE_CURVE('',#39689,#39681,#24996,.T.);
#50960=EDGE_CURVE('',#39688,#39689,#24997,.T.);
#50961=EDGE_CURVE('',#39500,#39687,#20959,.T.);
#50962=EDGE_CURVE('',#39689,#39687,#20960,.T.);
#50963=EDGE_CURVE('',#39501,#39689,#20961,.T.);
#50964=EDGE_CURVE('',#39499,#39686,#20962,.T.);
#50965=EDGE_CURVE('',#39682,#39498,#20963,.T.);
#50966=EDGE_CURVE('',#39683,#38951,#20964,.T.);
#50967=EDGE_CURVE('',#39684,#38950,#20965,.T.);
#50968=EDGE_CURVE('',#39678,#38949,#20966,.T.);
#50969=EDGE_CURVE('',#39679,#38948,#20967,.T.);
#50970=EDGE_CURVE('',#39503,#39680,#20968,.T.);
#50971=EDGE_CURVE('',#39502,#39681,#20969,.T.);
#50972=EDGE_CURVE('',#39690,#39691,#29368,.T.);
#50973=EDGE_CURVE('',#39691,#39692,#24998,.T.);
#50974=EDGE_CURVE('',#39692,#39693,#700,.T.);
#50975=EDGE_CURVE('',#39693,#39694,#29369,.T.);
#50976=EDGE_CURVE('',#39694,#39690,#24999,.T.);
#50977=EDGE_CURVE('',#39695,#39696,#701,.T.);
#50978=EDGE_CURVE('',#39696,#39697,#25000,.T.);
#50979=EDGE_CURVE('',#39698,#39697,#29370,.T.);
#50980=EDGE_CURVE('',#39698,#39699,#25001,.T.);
#50981=EDGE_CURVE('',#39699,#39695,#29371,.T.);
#50982=EDGE_CURVE('',#39697,#39691,#25002,.T.);
#50983=EDGE_CURVE('',#39690,#39698,#20970,.T.);
#50984=EDGE_CURVE('',#39699,#39700,#25003,.T.);
#50985=EDGE_CURVE('',#39701,#39698,#702,.T.);
#50986=EDGE_CURVE('',#39700,#39701,#25004,.T.);
#50987=EDGE_CURVE('',#39701,#39690,#703,.T.);
#50988=EDGE_CURVE('',#39702,#39694,#25005,.T.);
#50989=EDGE_CURVE('',#39701,#39702,#25006,.T.);
#50990=EDGE_CURVE('',#39506,#39700,#20971,.T.);
#50991=EDGE_CURVE('',#39702,#39700,#20972,.T.);
#50992=EDGE_CURVE('',#39507,#39702,#20973,.T.);
#50993=EDGE_CURVE('',#39505,#39699,#20974,.T.);
#50994=EDGE_CURVE('',#39695,#39504,#20975,.T.);
#50995=EDGE_CURVE('',#39696,#38947,#20976,.T.);
#50996=EDGE_CURVE('',#39697,#38946,#20977,.T.);
#50997=EDGE_CURVE('',#39691,#38945,#20978,.T.);
#50998=EDGE_CURVE('',#39692,#38944,#20979,.T.);
#50999=EDGE_CURVE('',#39509,#39693,#20980,.T.);
#51000=EDGE_CURVE('',#39508,#39694,#20981,.T.);
#51001=EDGE_CURVE('',#39703,#39704,#29372,.T.);
#51002=EDGE_CURVE('',#39704,#39705,#25007,.T.);
#51003=EDGE_CURVE('',#39705,#39706,#704,.T.);
#51004=EDGE_CURVE('',#39706,#39707,#29373,.T.);
#51005=EDGE_CURVE('',#39707,#39703,#25008,.T.);
#51006=EDGE_CURVE('',#39708,#39709,#705,.T.);
#51007=EDGE_CURVE('',#39709,#39710,#25009,.T.);
#51008=EDGE_CURVE('',#39711,#39710,#29374,.T.);
#51009=EDGE_CURVE('',#39711,#39712,#25010,.T.);
#51010=EDGE_CURVE('',#39712,#39708,#29375,.T.);
#51011=EDGE_CURVE('',#39710,#39704,#25011,.T.);
#51012=EDGE_CURVE('',#39703,#39711,#20982,.T.);
#51013=EDGE_CURVE('',#39712,#39713,#25012,.T.);
#51014=EDGE_CURVE('',#39714,#39711,#706,.T.);
#51015=EDGE_CURVE('',#39713,#39714,#25013,.T.);
#51016=EDGE_CURVE('',#39714,#39703,#707,.T.);
#51017=EDGE_CURVE('',#39715,#39707,#25014,.T.);
#51018=EDGE_CURVE('',#39714,#39715,#25015,.T.);
#51019=EDGE_CURVE('',#39512,#39713,#20983,.T.);
#51020=EDGE_CURVE('',#39715,#39713,#20984,.T.);
#51021=EDGE_CURVE('',#39513,#39715,#20985,.T.);
#51022=EDGE_CURVE('',#39511,#39712,#20986,.T.);
#51023=EDGE_CURVE('',#39708,#39510,#20987,.T.);
#51024=EDGE_CURVE('',#39709,#38943,#20988,.T.);
#51025=EDGE_CURVE('',#39710,#38942,#20989,.T.);
#51026=EDGE_CURVE('',#39704,#38941,#20990,.T.);
#51027=EDGE_CURVE('',#39705,#38940,#20991,.T.);
#51028=EDGE_CURVE('',#39515,#39706,#20992,.T.);
#51029=EDGE_CURVE('',#39514,#39707,#20993,.T.);
#51030=EDGE_CURVE('',#39716,#39717,#29376,.T.);
#51031=EDGE_CURVE('',#39717,#39718,#25016,.T.);
#51032=EDGE_CURVE('',#39718,#39719,#708,.T.);
#51033=EDGE_CURVE('',#39719,#39720,#29377,.T.);
#51034=EDGE_CURVE('',#39720,#39716,#25017,.T.);
#51035=EDGE_CURVE('',#39721,#39722,#709,.T.);
#51036=EDGE_CURVE('',#39722,#39723,#25018,.T.);
#51037=EDGE_CURVE('',#39724,#39723,#29378,.T.);
#51038=EDGE_CURVE('',#39724,#39725,#25019,.T.);
#51039=EDGE_CURVE('',#39725,#39721,#29379,.T.);
#51040=EDGE_CURVE('',#39723,#39717,#25020,.T.);
#51041=EDGE_CURVE('',#39716,#39724,#20994,.T.);
#51042=EDGE_CURVE('',#39725,#39726,#25021,.T.);
#51043=EDGE_CURVE('',#39727,#39724,#710,.T.);
#51044=EDGE_CURVE('',#39726,#39727,#25022,.T.);
#51045=EDGE_CURVE('',#39727,#39716,#711,.T.);
#51046=EDGE_CURVE('',#39728,#39720,#25023,.T.);
#51047=EDGE_CURVE('',#39727,#39728,#25024,.T.);
#51048=EDGE_CURVE('',#39518,#39726,#20995,.T.);
#51049=EDGE_CURVE('',#39728,#39726,#20996,.T.);
#51050=EDGE_CURVE('',#39519,#39728,#20997,.T.);
#51051=EDGE_CURVE('',#39517,#39725,#20998,.T.);
#51052=EDGE_CURVE('',#39721,#39516,#20999,.T.);
#51053=EDGE_CURVE('',#39722,#38939,#21000,.T.);
#51054=EDGE_CURVE('',#39723,#38938,#21001,.T.);
#51055=EDGE_CURVE('',#39717,#38937,#21002,.T.);
#51056=EDGE_CURVE('',#39718,#38936,#21003,.T.);
#51057=EDGE_CURVE('',#39521,#39719,#21004,.T.);
#51058=EDGE_CURVE('',#39520,#39720,#21005,.T.);
#51059=EDGE_CURVE('',#39729,#39730,#29380,.T.);
#51060=EDGE_CURVE('',#39730,#39731,#25025,.T.);
#51061=EDGE_CURVE('',#39731,#39732,#712,.T.);
#51062=EDGE_CURVE('',#39732,#39733,#29381,.T.);
#51063=EDGE_CURVE('',#39733,#39729,#25026,.T.);
#51064=EDGE_CURVE('',#39734,#39735,#713,.T.);
#51065=EDGE_CURVE('',#39735,#39736,#25027,.T.);
#51066=EDGE_CURVE('',#39737,#39736,#29382,.T.);
#51067=EDGE_CURVE('',#39737,#39738,#25028,.T.);
#51068=EDGE_CURVE('',#39738,#39734,#29383,.T.);
#51069=EDGE_CURVE('',#39736,#39730,#25029,.T.);
#51070=EDGE_CURVE('',#39729,#39737,#21006,.T.);
#51071=EDGE_CURVE('',#39738,#39739,#25030,.T.);
#51072=EDGE_CURVE('',#39740,#39737,#714,.T.);
#51073=EDGE_CURVE('',#39739,#39740,#25031,.T.);
#51074=EDGE_CURVE('',#39740,#39729,#715,.T.);
#51075=EDGE_CURVE('',#39741,#39733,#25032,.T.);
#51076=EDGE_CURVE('',#39740,#39741,#25033,.T.);
#51077=EDGE_CURVE('',#39524,#39739,#21007,.T.);
#51078=EDGE_CURVE('',#39741,#39739,#21008,.T.);
#51079=EDGE_CURVE('',#39525,#39741,#21009,.T.);
#51080=EDGE_CURVE('',#39523,#39738,#21010,.T.);
#51081=EDGE_CURVE('',#39734,#39522,#21011,.T.);
#51082=EDGE_CURVE('',#39735,#38935,#21012,.T.);
#51083=EDGE_CURVE('',#39736,#38934,#21013,.T.);
#51084=EDGE_CURVE('',#39730,#38933,#21014,.T.);
#51085=EDGE_CURVE('',#39731,#38932,#21015,.T.);
#51086=EDGE_CURVE('',#39527,#39732,#21016,.T.);
#51087=EDGE_CURVE('',#39526,#39733,#21017,.T.);
#51088=EDGE_CURVE('',#39742,#39743,#29384,.T.);
#51089=EDGE_CURVE('',#39743,#39744,#25034,.T.);
#51090=EDGE_CURVE('',#39744,#39745,#716,.T.);
#51091=EDGE_CURVE('',#39745,#39746,#29385,.T.);
#51092=EDGE_CURVE('',#39746,#39742,#25035,.T.);
#51093=EDGE_CURVE('',#39747,#39748,#717,.T.);
#51094=EDGE_CURVE('',#39748,#39749,#25036,.T.);
#51095=EDGE_CURVE('',#39750,#39749,#29386,.T.);
#51096=EDGE_CURVE('',#39750,#39751,#25037,.T.);
#51097=EDGE_CURVE('',#39751,#39747,#29387,.T.);
#51098=EDGE_CURVE('',#39749,#39743,#25038,.T.);
#51099=EDGE_CURVE('',#39742,#39750,#21018,.T.);
#51100=EDGE_CURVE('',#39751,#39752,#25039,.T.);
#51101=EDGE_CURVE('',#39753,#39750,#718,.T.);
#51102=EDGE_CURVE('',#39752,#39753,#25040,.T.);
#51103=EDGE_CURVE('',#39753,#39742,#719,.T.);
#51104=EDGE_CURVE('',#39754,#39746,#25041,.T.);
#51105=EDGE_CURVE('',#39753,#39754,#25042,.T.);
#51106=EDGE_CURVE('',#39530,#39752,#21019,.T.);
#51107=EDGE_CURVE('',#39754,#39752,#21020,.T.);
#51108=EDGE_CURVE('',#39531,#39754,#21021,.T.);
#51109=EDGE_CURVE('',#39529,#39751,#21022,.T.);
#51110=EDGE_CURVE('',#39747,#39528,#21023,.T.);
#51111=EDGE_CURVE('',#39748,#38931,#21024,.T.);
#51112=EDGE_CURVE('',#39749,#38930,#21025,.T.);
#51113=EDGE_CURVE('',#39743,#38929,#21026,.T.);
#51114=EDGE_CURVE('',#39744,#38928,#21027,.T.);
#51115=EDGE_CURVE('',#39533,#39745,#21028,.T.);
#51116=EDGE_CURVE('',#39532,#39746,#21029,.T.);
#51117=EDGE_CURVE('',#39755,#39756,#29388,.T.);
#51118=EDGE_CURVE('',#39756,#39757,#25043,.T.);
#51119=EDGE_CURVE('',#39757,#39758,#720,.T.);
#51120=EDGE_CURVE('',#39758,#39759,#29389,.T.);
#51121=EDGE_CURVE('',#39759,#39755,#25044,.T.);
#51122=EDGE_CURVE('',#39760,#39761,#721,.T.);
#51123=EDGE_CURVE('',#39761,#39762,#25045,.T.);
#51124=EDGE_CURVE('',#39763,#39762,#29390,.T.);
#51125=EDGE_CURVE('',#39763,#39764,#25046,.T.);
#51126=EDGE_CURVE('',#39764,#39760,#29391,.T.);
#51127=EDGE_CURVE('',#39762,#39756,#25047,.T.);
#51128=EDGE_CURVE('',#39755,#39763,#21030,.T.);
#51129=EDGE_CURVE('',#39764,#39765,#25048,.T.);
#51130=EDGE_CURVE('',#39766,#39763,#722,.T.);
#51131=EDGE_CURVE('',#39765,#39766,#25049,.T.);
#51132=EDGE_CURVE('',#39766,#39755,#723,.T.);
#51133=EDGE_CURVE('',#39767,#39759,#25050,.T.);
#51134=EDGE_CURVE('',#39766,#39767,#25051,.T.);
#51135=EDGE_CURVE('',#39536,#39765,#21031,.T.);
#51136=EDGE_CURVE('',#39767,#39765,#21032,.T.);
#51137=EDGE_CURVE('',#39537,#39767,#21033,.T.);
#51138=EDGE_CURVE('',#39535,#39764,#21034,.T.);
#51139=EDGE_CURVE('',#39760,#39534,#21035,.T.);
#51140=EDGE_CURVE('',#39761,#38927,#21036,.T.);
#51141=EDGE_CURVE('',#39762,#38926,#21037,.T.);
#51142=EDGE_CURVE('',#39756,#38925,#21038,.T.);
#51143=EDGE_CURVE('',#39757,#38924,#21039,.T.);
#51144=EDGE_CURVE('',#39539,#39758,#21040,.T.);
#51145=EDGE_CURVE('',#39538,#39759,#21041,.T.);
#51146=EDGE_CURVE('',#39768,#39769,#29392,.T.);
#51147=EDGE_CURVE('',#39769,#39770,#25052,.T.);
#51148=EDGE_CURVE('',#39770,#39771,#724,.T.);
#51149=EDGE_CURVE('',#39771,#39772,#29393,.T.);
#51150=EDGE_CURVE('',#39772,#39768,#25053,.T.);
#51151=EDGE_CURVE('',#39773,#39774,#725,.T.);
#51152=EDGE_CURVE('',#39774,#39775,#25054,.T.);
#51153=EDGE_CURVE('',#39776,#39775,#29394,.T.);
#51154=EDGE_CURVE('',#39776,#39777,#25055,.T.);
#51155=EDGE_CURVE('',#39777,#39773,#29395,.T.);
#51156=EDGE_CURVE('',#39775,#39769,#25056,.T.);
#51157=EDGE_CURVE('',#39768,#39776,#21042,.T.);
#51158=EDGE_CURVE('',#39777,#39778,#25057,.T.);
#51159=EDGE_CURVE('',#39779,#39776,#726,.T.);
#51160=EDGE_CURVE('',#39778,#39779,#25058,.T.);
#51161=EDGE_CURVE('',#39779,#39768,#727,.T.);
#51162=EDGE_CURVE('',#39780,#39772,#25059,.T.);
#51163=EDGE_CURVE('',#39779,#39780,#25060,.T.);
#51164=EDGE_CURVE('',#39542,#39778,#21043,.T.);
#51165=EDGE_CURVE('',#39780,#39778,#21044,.T.);
#51166=EDGE_CURVE('',#39543,#39780,#21045,.T.);
#51167=EDGE_CURVE('',#39541,#39777,#21046,.T.);
#51168=EDGE_CURVE('',#39773,#39540,#21047,.T.);
#51169=EDGE_CURVE('',#39774,#38923,#21048,.T.);
#51170=EDGE_CURVE('',#39775,#38922,#21049,.T.);
#51171=EDGE_CURVE('',#39769,#38921,#21050,.T.);
#51172=EDGE_CURVE('',#39770,#38920,#21051,.T.);
#51173=EDGE_CURVE('',#39545,#39771,#21052,.T.);
#51174=EDGE_CURVE('',#39544,#39772,#21053,.T.);
#51175=EDGE_CURVE('',#39781,#39782,#29396,.T.);
#51176=EDGE_CURVE('',#39782,#39783,#25061,.T.);
#51177=EDGE_CURVE('',#39783,#39784,#728,.T.);
#51178=EDGE_CURVE('',#39784,#39785,#29397,.T.);
#51179=EDGE_CURVE('',#39785,#39781,#25062,.T.);
#51180=EDGE_CURVE('',#39786,#39787,#729,.T.);
#51181=EDGE_CURVE('',#39787,#39788,#25063,.T.);
#51182=EDGE_CURVE('',#39789,#39788,#29398,.T.);
#51183=EDGE_CURVE('',#39789,#39790,#25064,.T.);
#51184=EDGE_CURVE('',#39790,#39786,#29399,.T.);
#51185=EDGE_CURVE('',#39788,#39782,#25065,.T.);
#51186=EDGE_CURVE('',#39781,#39789,#21054,.T.);
#51187=EDGE_CURVE('',#39790,#39791,#25066,.T.);
#51188=EDGE_CURVE('',#39792,#39789,#730,.T.);
#51189=EDGE_CURVE('',#39791,#39792,#25067,.T.);
#51190=EDGE_CURVE('',#39792,#39781,#731,.T.);
#51191=EDGE_CURVE('',#39793,#39785,#25068,.T.);
#51192=EDGE_CURVE('',#39792,#39793,#25069,.T.);
#51193=EDGE_CURVE('',#39548,#39791,#21055,.T.);
#51194=EDGE_CURVE('',#39793,#39791,#21056,.T.);
#51195=EDGE_CURVE('',#39549,#39793,#21057,.T.);
#51196=EDGE_CURVE('',#39547,#39790,#21058,.T.);
#51197=EDGE_CURVE('',#39786,#39546,#21059,.T.);
#51198=EDGE_CURVE('',#39787,#38919,#21060,.T.);
#51199=EDGE_CURVE('',#39788,#38918,#21061,.T.);
#51200=EDGE_CURVE('',#39782,#38917,#21062,.T.);
#51201=EDGE_CURVE('',#39783,#38916,#21063,.T.);
#51202=EDGE_CURVE('',#39551,#39784,#21064,.T.);
#51203=EDGE_CURVE('',#39550,#39785,#21065,.T.);
#51204=EDGE_CURVE('',#39794,#39795,#29400,.T.);
#51205=EDGE_CURVE('',#39795,#39796,#25070,.T.);
#51206=EDGE_CURVE('',#39796,#39797,#732,.T.);
#51207=EDGE_CURVE('',#39797,#39798,#29401,.T.);
#51208=EDGE_CURVE('',#39798,#39794,#25071,.T.);
#51209=EDGE_CURVE('',#39799,#39800,#733,.T.);
#51210=EDGE_CURVE('',#39800,#39801,#25072,.T.);
#51211=EDGE_CURVE('',#39802,#39801,#29402,.T.);
#51212=EDGE_CURVE('',#39802,#39803,#25073,.T.);
#51213=EDGE_CURVE('',#39803,#39799,#29403,.T.);
#51214=EDGE_CURVE('',#39801,#39795,#25074,.T.);
#51215=EDGE_CURVE('',#39794,#39802,#21066,.T.);
#51216=EDGE_CURVE('',#39803,#39804,#25075,.T.);
#51217=EDGE_CURVE('',#39805,#39802,#734,.T.);
#51218=EDGE_CURVE('',#39804,#39805,#25076,.T.);
#51219=EDGE_CURVE('',#39805,#39794,#735,.T.);
#51220=EDGE_CURVE('',#39806,#39798,#25077,.T.);
#51221=EDGE_CURVE('',#39805,#39806,#25078,.T.);
#51222=EDGE_CURVE('',#39554,#39804,#21067,.T.);
#51223=EDGE_CURVE('',#39806,#39804,#21068,.T.);
#51224=EDGE_CURVE('',#39555,#39806,#21069,.T.);
#51225=EDGE_CURVE('',#39553,#39803,#21070,.T.);
#51226=EDGE_CURVE('',#39799,#39552,#21071,.T.);
#51227=EDGE_CURVE('',#39800,#38915,#21072,.T.);
#51228=EDGE_CURVE('',#39801,#38914,#21073,.T.);
#51229=EDGE_CURVE('',#39795,#38913,#21074,.T.);
#51230=EDGE_CURVE('',#39796,#38912,#21075,.T.);
#51231=EDGE_CURVE('',#39557,#39797,#21076,.T.);
#51232=EDGE_CURVE('',#39556,#39798,#21077,.T.);
#51233=EDGE_CURVE('',#39807,#39808,#29404,.T.);
#51234=EDGE_CURVE('',#39808,#39809,#25079,.T.);
#51235=EDGE_CURVE('',#39809,#39810,#736,.T.);
#51236=EDGE_CURVE('',#39810,#39811,#29405,.T.);
#51237=EDGE_CURVE('',#39811,#39807,#25080,.T.);
#51238=EDGE_CURVE('',#39812,#39813,#737,.T.);
#51239=EDGE_CURVE('',#39813,#39814,#25081,.T.);
#51240=EDGE_CURVE('',#39815,#39814,#29406,.T.);
#51241=EDGE_CURVE('',#39815,#39816,#25082,.T.);
#51242=EDGE_CURVE('',#39816,#39812,#29407,.T.);
#51243=EDGE_CURVE('',#39814,#39808,#25083,.T.);
#51244=EDGE_CURVE('',#39807,#39815,#21078,.T.);
#51245=EDGE_CURVE('',#39816,#39817,#25084,.T.);
#51246=EDGE_CURVE('',#39818,#39815,#738,.T.);
#51247=EDGE_CURVE('',#39817,#39818,#25085,.T.);
#51248=EDGE_CURVE('',#39818,#39807,#739,.T.);
#51249=EDGE_CURVE('',#39819,#39811,#25086,.T.);
#51250=EDGE_CURVE('',#39818,#39819,#25087,.T.);
#51251=EDGE_CURVE('',#39560,#39817,#21079,.T.);
#51252=EDGE_CURVE('',#39819,#39817,#21080,.T.);
#51253=EDGE_CURVE('',#39561,#39819,#21081,.T.);
#51254=EDGE_CURVE('',#39559,#39816,#21082,.T.);
#51255=EDGE_CURVE('',#39812,#39558,#21083,.T.);
#51256=EDGE_CURVE('',#39813,#38911,#21084,.T.);
#51257=EDGE_CURVE('',#39814,#38910,#21085,.T.);
#51258=EDGE_CURVE('',#39808,#38909,#21086,.T.);
#51259=EDGE_CURVE('',#39809,#38908,#21087,.T.);
#51260=EDGE_CURVE('',#39563,#39810,#21088,.T.);
#51261=EDGE_CURVE('',#39562,#39811,#21089,.T.);
#51262=EDGE_CURVE('',#39820,#39821,#29408,.T.);
#51263=EDGE_CURVE('',#39821,#39822,#25088,.T.);
#51264=EDGE_CURVE('',#39822,#39823,#740,.T.);
#51265=EDGE_CURVE('',#39823,#39824,#29409,.T.);
#51266=EDGE_CURVE('',#39824,#39820,#25089,.T.);
#51267=EDGE_CURVE('',#39825,#39826,#741,.T.);
#51268=EDGE_CURVE('',#39826,#39827,#25090,.T.);
#51269=EDGE_CURVE('',#39828,#39827,#29410,.T.);
#51270=EDGE_CURVE('',#39828,#39829,#25091,.T.);
#51271=EDGE_CURVE('',#39829,#39825,#29411,.T.);
#51272=EDGE_CURVE('',#39827,#39821,#25092,.T.);
#51273=EDGE_CURVE('',#39820,#39828,#21090,.T.);
#51274=EDGE_CURVE('',#39829,#39830,#25093,.T.);
#51275=EDGE_CURVE('',#39831,#39828,#742,.T.);
#51276=EDGE_CURVE('',#39830,#39831,#25094,.T.);
#51277=EDGE_CURVE('',#39831,#39820,#743,.T.);
#51278=EDGE_CURVE('',#39832,#39824,#25095,.T.);
#51279=EDGE_CURVE('',#39831,#39832,#25096,.T.);
#51280=EDGE_CURVE('',#39566,#39830,#21091,.T.);
#51281=EDGE_CURVE('',#39832,#39830,#21092,.T.);
#51282=EDGE_CURVE('',#39567,#39832,#21093,.T.);
#51283=EDGE_CURVE('',#39565,#39829,#21094,.T.);
#51284=EDGE_CURVE('',#39825,#39564,#21095,.T.);
#51285=EDGE_CURVE('',#39826,#38907,#21096,.T.);
#51286=EDGE_CURVE('',#39827,#38906,#21097,.T.);
#51287=EDGE_CURVE('',#39821,#38905,#21098,.T.);
#51288=EDGE_CURVE('',#39822,#38904,#21099,.T.);
#51289=EDGE_CURVE('',#39569,#39823,#21100,.T.);
#51290=EDGE_CURVE('',#39568,#39824,#21101,.T.);
#51291=EDGE_CURVE('',#39833,#39834,#29412,.T.);
#51292=EDGE_CURVE('',#39834,#39835,#25097,.T.);
#51293=EDGE_CURVE('',#39835,#39836,#744,.T.);
#51294=EDGE_CURVE('',#39836,#39837,#29413,.T.);
#51295=EDGE_CURVE('',#39837,#39833,#25098,.T.);
#51296=EDGE_CURVE('',#39838,#39839,#745,.T.);
#51297=EDGE_CURVE('',#39839,#39840,#25099,.T.);
#51298=EDGE_CURVE('',#39841,#39840,#29414,.T.);
#51299=EDGE_CURVE('',#39841,#39842,#25100,.T.);
#51300=EDGE_CURVE('',#39842,#39838,#29415,.T.);
#51301=EDGE_CURVE('',#39840,#39834,#25101,.T.);
#51302=EDGE_CURVE('',#39833,#39841,#21102,.T.);
#51303=EDGE_CURVE('',#39842,#39843,#25102,.T.);
#51304=EDGE_CURVE('',#39844,#39841,#746,.T.);
#51305=EDGE_CURVE('',#39843,#39844,#25103,.T.);
#51306=EDGE_CURVE('',#39844,#39833,#747,.T.);
#51307=EDGE_CURVE('',#39845,#39837,#25104,.T.);
#51308=EDGE_CURVE('',#39844,#39845,#25105,.T.);
#51309=EDGE_CURVE('',#39572,#39843,#21103,.T.);
#51310=EDGE_CURVE('',#39845,#39843,#21104,.T.);
#51311=EDGE_CURVE('',#39573,#39845,#21105,.T.);
#51312=EDGE_CURVE('',#39571,#39842,#21106,.T.);
#51313=EDGE_CURVE('',#39838,#39570,#21107,.T.);
#51314=EDGE_CURVE('',#39839,#38903,#21108,.T.);
#51315=EDGE_CURVE('',#39840,#38902,#21109,.T.);
#51316=EDGE_CURVE('',#39834,#38901,#21110,.T.);
#51317=EDGE_CURVE('',#39835,#38900,#21111,.T.);
#51318=EDGE_CURVE('',#39575,#39836,#21112,.T.);
#51319=EDGE_CURVE('',#39574,#39837,#21113,.T.);
#51320=EDGE_CURVE('',#39846,#39847,#29416,.T.);
#51321=EDGE_CURVE('',#39847,#39848,#25106,.T.);
#51322=EDGE_CURVE('',#39848,#39849,#748,.T.);
#51323=EDGE_CURVE('',#39849,#39850,#29417,.T.);
#51324=EDGE_CURVE('',#39850,#39846,#25107,.T.);
#51325=EDGE_CURVE('',#39851,#39852,#749,.T.);
#51326=EDGE_CURVE('',#39852,#39853,#25108,.T.);
#51327=EDGE_CURVE('',#39854,#39853,#29418,.T.);
#51328=EDGE_CURVE('',#39854,#39855,#25109,.T.);
#51329=EDGE_CURVE('',#39855,#39851,#29419,.T.);
#51330=EDGE_CURVE('',#39853,#39847,#25110,.T.);
#51331=EDGE_CURVE('',#39846,#39854,#21114,.T.);
#51332=EDGE_CURVE('',#39855,#39856,#25111,.T.);
#51333=EDGE_CURVE('',#39857,#39854,#750,.T.);
#51334=EDGE_CURVE('',#39856,#39857,#25112,.T.);
#51335=EDGE_CURVE('',#39857,#39846,#751,.T.);
#51336=EDGE_CURVE('',#39858,#39850,#25113,.T.);
#51337=EDGE_CURVE('',#39857,#39858,#25114,.T.);
#51338=EDGE_CURVE('',#39578,#39856,#21115,.T.);
#51339=EDGE_CURVE('',#39858,#39856,#21116,.T.);
#51340=EDGE_CURVE('',#39579,#39858,#21117,.T.);
#51341=EDGE_CURVE('',#39577,#39855,#21118,.T.);
#51342=EDGE_CURVE('',#39851,#39576,#21119,.T.);
#51343=EDGE_CURVE('',#39852,#38899,#21120,.T.);
#51344=EDGE_CURVE('',#39853,#38898,#21121,.T.);
#51345=EDGE_CURVE('',#39847,#38897,#21122,.T.);
#51346=EDGE_CURVE('',#39848,#38896,#21123,.T.);
#51347=EDGE_CURVE('',#39581,#39849,#21124,.T.);
#51348=EDGE_CURVE('',#39580,#39850,#21125,.T.);
#51349=EDGE_CURVE('',#39859,#39860,#29420,.T.);
#51350=EDGE_CURVE('',#39860,#39861,#25115,.T.);
#51351=EDGE_CURVE('',#39861,#39862,#752,.T.);
#51352=EDGE_CURVE('',#39862,#39863,#29421,.T.);
#51353=EDGE_CURVE('',#39863,#39859,#25116,.T.);
#51354=EDGE_CURVE('',#39864,#39865,#753,.T.);
#51355=EDGE_CURVE('',#39865,#39866,#25117,.T.);
#51356=EDGE_CURVE('',#39867,#39866,#29422,.T.);
#51357=EDGE_CURVE('',#39867,#39868,#25118,.T.);
#51358=EDGE_CURVE('',#39868,#39864,#29423,.T.);
#51359=EDGE_CURVE('',#39866,#39860,#25119,.T.);
#51360=EDGE_CURVE('',#39859,#39867,#21126,.T.);
#51361=EDGE_CURVE('',#39868,#39869,#25120,.T.);
#51362=EDGE_CURVE('',#39870,#39867,#754,.T.);
#51363=EDGE_CURVE('',#39869,#39870,#25121,.T.);
#51364=EDGE_CURVE('',#39870,#39859,#755,.T.);
#51365=EDGE_CURVE('',#39871,#39863,#25122,.T.);
#51366=EDGE_CURVE('',#39870,#39871,#25123,.T.);
#51367=EDGE_CURVE('',#39584,#39869,#21127,.T.);
#51368=EDGE_CURVE('',#39871,#39869,#21128,.T.);
#51369=EDGE_CURVE('',#39585,#39871,#21129,.T.);
#51370=EDGE_CURVE('',#39583,#39868,#21130,.T.);
#51371=EDGE_CURVE('',#39864,#39582,#21131,.T.);
#51372=EDGE_CURVE('',#39865,#38895,#21132,.T.);
#51373=EDGE_CURVE('',#39866,#38894,#21133,.T.);
#51374=EDGE_CURVE('',#39860,#38893,#21134,.T.);
#51375=EDGE_CURVE('',#39861,#38892,#21135,.T.);
#51376=EDGE_CURVE('',#39587,#39862,#21136,.T.);
#51377=EDGE_CURVE('',#39586,#39863,#21137,.T.);
#51378=EDGE_CURVE('',#39872,#39873,#29424,.T.);
#51379=EDGE_CURVE('',#39873,#39874,#25124,.T.);
#51380=EDGE_CURVE('',#39874,#39875,#756,.T.);
#51381=EDGE_CURVE('',#39875,#39876,#29425,.T.);
#51382=EDGE_CURVE('',#39876,#39872,#25125,.T.);
#51383=EDGE_CURVE('',#39877,#39878,#757,.T.);
#51384=EDGE_CURVE('',#39878,#39879,#25126,.T.);
#51385=EDGE_CURVE('',#39880,#39879,#29426,.T.);
#51386=EDGE_CURVE('',#39880,#39881,#25127,.T.);
#51387=EDGE_CURVE('',#39881,#39877,#29427,.T.);
#51388=EDGE_CURVE('',#39879,#39873,#25128,.T.);
#51389=EDGE_CURVE('',#39872,#39880,#21138,.T.);
#51390=EDGE_CURVE('',#39881,#39882,#25129,.T.);
#51391=EDGE_CURVE('',#39883,#39880,#758,.T.);
#51392=EDGE_CURVE('',#39882,#39883,#25130,.T.);
#51393=EDGE_CURVE('',#39883,#39872,#759,.T.);
#51394=EDGE_CURVE('',#39884,#39876,#25131,.T.);
#51395=EDGE_CURVE('',#39883,#39884,#25132,.T.);
#51396=EDGE_CURVE('',#39590,#39882,#21139,.T.);
#51397=EDGE_CURVE('',#39884,#39882,#21140,.T.);
#51398=EDGE_CURVE('',#39591,#39884,#21141,.T.);
#51399=EDGE_CURVE('',#39589,#39881,#21142,.T.);
#51400=EDGE_CURVE('',#39877,#39588,#21143,.T.);
#51401=EDGE_CURVE('',#39878,#38891,#21144,.T.);
#51402=EDGE_CURVE('',#39879,#38890,#21145,.T.);
#51403=EDGE_CURVE('',#39873,#38889,#21146,.T.);
#51404=EDGE_CURVE('',#39874,#38888,#21147,.T.);
#51405=EDGE_CURVE('',#39593,#39875,#21148,.T.);
#51406=EDGE_CURVE('',#39592,#39876,#21149,.T.);
#51407=EDGE_CURVE('',#39885,#39886,#29428,.T.);
#51408=EDGE_CURVE('',#39886,#39887,#25133,.T.);
#51409=EDGE_CURVE('',#39887,#39888,#760,.T.);
#51410=EDGE_CURVE('',#39888,#39889,#29429,.T.);
#51411=EDGE_CURVE('',#39889,#39885,#25134,.T.);
#51412=EDGE_CURVE('',#39890,#39891,#761,.T.);
#51413=EDGE_CURVE('',#39891,#39892,#25135,.T.);
#51414=EDGE_CURVE('',#39893,#39892,#29430,.T.);
#51415=EDGE_CURVE('',#39893,#39894,#25136,.T.);
#51416=EDGE_CURVE('',#39894,#39890,#29431,.T.);
#51417=EDGE_CURVE('',#39892,#39886,#25137,.T.);
#51418=EDGE_CURVE('',#39885,#39893,#21150,.T.);
#51419=EDGE_CURVE('',#39894,#39895,#25138,.T.);
#51420=EDGE_CURVE('',#39896,#39893,#762,.T.);
#51421=EDGE_CURVE('',#39895,#39896,#25139,.T.);
#51422=EDGE_CURVE('',#39896,#39885,#763,.T.);
#51423=EDGE_CURVE('',#39897,#39889,#25140,.T.);
#51424=EDGE_CURVE('',#39896,#39897,#25141,.T.);
#51425=EDGE_CURVE('',#39596,#39895,#21151,.T.);
#51426=EDGE_CURVE('',#39897,#39895,#21152,.T.);
#51427=EDGE_CURVE('',#39597,#39897,#21153,.T.);
#51428=EDGE_CURVE('',#39595,#39894,#21154,.T.);
#51429=EDGE_CURVE('',#39890,#39594,#21155,.T.);
#51430=EDGE_CURVE('',#39891,#38887,#21156,.T.);
#51431=EDGE_CURVE('',#39892,#38886,#21157,.T.);
#51432=EDGE_CURVE('',#39886,#38885,#21158,.T.);
#51433=EDGE_CURVE('',#39887,#38884,#21159,.T.);
#51434=EDGE_CURVE('',#39599,#39888,#21160,.T.);
#51435=EDGE_CURVE('',#39598,#39889,#21161,.T.);
#51436=EDGE_CURVE('',#39898,#39899,#29432,.T.);
#51437=EDGE_CURVE('',#39899,#39900,#25142,.T.);
#51438=EDGE_CURVE('',#39900,#39901,#764,.T.);
#51439=EDGE_CURVE('',#39901,#39902,#29433,.T.);
#51440=EDGE_CURVE('',#39902,#39898,#25143,.T.);
#51441=EDGE_CURVE('',#39903,#39904,#765,.T.);
#51442=EDGE_CURVE('',#39904,#39905,#25144,.T.);
#51443=EDGE_CURVE('',#39906,#39905,#29434,.T.);
#51444=EDGE_CURVE('',#39906,#39907,#25145,.T.);
#51445=EDGE_CURVE('',#39907,#39903,#29435,.T.);
#51446=EDGE_CURVE('',#39905,#39899,#25146,.T.);
#51447=EDGE_CURVE('',#39898,#39906,#21162,.T.);
#51448=EDGE_CURVE('',#39907,#39908,#25147,.T.);
#51449=EDGE_CURVE('',#39909,#39906,#766,.T.);
#51450=EDGE_CURVE('',#39908,#39909,#25148,.T.);
#51451=EDGE_CURVE('',#39909,#39898,#767,.T.);
#51452=EDGE_CURVE('',#39910,#39902,#25149,.T.);
#51453=EDGE_CURVE('',#39909,#39910,#25150,.T.);
#51454=EDGE_CURVE('',#39602,#39908,#21163,.T.);
#51455=EDGE_CURVE('',#39910,#39908,#21164,.T.);
#51456=EDGE_CURVE('',#39603,#39910,#21165,.T.);
#51457=EDGE_CURVE('',#39601,#39907,#21166,.T.);
#51458=EDGE_CURVE('',#39903,#39600,#21167,.T.);
#51459=EDGE_CURVE('',#39904,#38883,#21168,.T.);
#51460=EDGE_CURVE('',#39905,#38882,#21169,.T.);
#51461=EDGE_CURVE('',#39899,#38881,#21170,.T.);
#51462=EDGE_CURVE('',#39900,#38880,#21171,.T.);
#51463=EDGE_CURVE('',#39605,#39901,#21172,.T.);
#51464=EDGE_CURVE('',#39604,#39902,#21173,.T.);
#51465=EDGE_CURVE('',#39911,#39912,#29436,.T.);
#51466=EDGE_CURVE('',#39912,#39913,#25151,.T.);
#51467=EDGE_CURVE('',#39913,#39914,#768,.T.);
#51468=EDGE_CURVE('',#39914,#39915,#29437,.T.);
#51469=EDGE_CURVE('',#39915,#39911,#25152,.T.);
#51470=EDGE_CURVE('',#39916,#39917,#769,.T.);
#51471=EDGE_CURVE('',#39917,#39918,#25153,.T.);
#51472=EDGE_CURVE('',#39919,#39918,#29438,.T.);
#51473=EDGE_CURVE('',#39919,#39920,#25154,.T.);
#51474=EDGE_CURVE('',#39920,#39916,#29439,.T.);
#51475=EDGE_CURVE('',#39918,#39912,#25155,.T.);
#51476=EDGE_CURVE('',#39911,#39919,#21174,.T.);
#51477=EDGE_CURVE('',#39920,#39921,#25156,.T.);
#51478=EDGE_CURVE('',#39922,#39919,#770,.T.);
#51479=EDGE_CURVE('',#39921,#39922,#25157,.T.);
#51480=EDGE_CURVE('',#39922,#39911,#771,.T.);
#51481=EDGE_CURVE('',#39923,#39915,#25158,.T.);
#51482=EDGE_CURVE('',#39922,#39923,#25159,.T.);
#51483=EDGE_CURVE('',#39608,#39921,#21175,.T.);
#51484=EDGE_CURVE('',#39923,#39921,#21176,.T.);
#51485=EDGE_CURVE('',#39609,#39923,#21177,.T.);
#51486=EDGE_CURVE('',#39607,#39920,#21178,.T.);
#51487=EDGE_CURVE('',#39916,#39606,#21179,.T.);
#51488=EDGE_CURVE('',#39917,#38879,#21180,.T.);
#51489=EDGE_CURVE('',#39918,#38878,#21181,.T.);
#51490=EDGE_CURVE('',#39912,#38877,#21182,.T.);
#51491=EDGE_CURVE('',#39913,#38876,#21183,.T.);
#51492=EDGE_CURVE('',#39611,#39914,#21184,.T.);
#51493=EDGE_CURVE('',#39610,#39915,#21185,.T.);
#51494=EDGE_CURVE('',#39924,#39925,#29440,.T.);
#51495=EDGE_CURVE('',#39925,#39926,#25160,.T.);
#51496=EDGE_CURVE('',#39926,#39927,#772,.T.);
#51497=EDGE_CURVE('',#39927,#39928,#29441,.T.);
#51498=EDGE_CURVE('',#39928,#39924,#25161,.T.);
#51499=EDGE_CURVE('',#39929,#39930,#773,.T.);
#51500=EDGE_CURVE('',#39930,#39931,#25162,.T.);
#51501=EDGE_CURVE('',#39932,#39931,#29442,.T.);
#51502=EDGE_CURVE('',#39932,#39933,#25163,.T.);
#51503=EDGE_CURVE('',#39933,#39929,#29443,.T.);
#51504=EDGE_CURVE('',#39931,#39925,#25164,.T.);
#51505=EDGE_CURVE('',#39924,#39932,#21186,.T.);
#51506=EDGE_CURVE('',#39933,#39934,#25165,.T.);
#51507=EDGE_CURVE('',#39935,#39932,#774,.T.);
#51508=EDGE_CURVE('',#39934,#39935,#25166,.T.);
#51509=EDGE_CURVE('',#39935,#39924,#775,.T.);
#51510=EDGE_CURVE('',#39936,#39928,#25167,.T.);
#51511=EDGE_CURVE('',#39935,#39936,#25168,.T.);
#51512=EDGE_CURVE('',#39614,#39934,#21187,.T.);
#51513=EDGE_CURVE('',#39936,#39934,#21188,.T.);
#51514=EDGE_CURVE('',#39615,#39936,#21189,.T.);
#51515=EDGE_CURVE('',#39613,#39933,#21190,.T.);
#51516=EDGE_CURVE('',#39929,#39612,#21191,.T.);
#51517=EDGE_CURVE('',#39930,#38875,#21192,.T.);
#51518=EDGE_CURVE('',#39931,#38874,#21193,.T.);
#51519=EDGE_CURVE('',#39925,#38873,#21194,.T.);
#51520=EDGE_CURVE('',#39926,#38872,#21195,.T.);
#51521=EDGE_CURVE('',#39617,#39927,#21196,.T.);
#51522=EDGE_CURVE('',#39616,#39928,#21197,.T.);
#51523=EDGE_CURVE('',#39937,#39938,#29444,.T.);
#51524=EDGE_CURVE('',#39938,#39939,#25169,.T.);
#51525=EDGE_CURVE('',#39939,#39940,#776,.T.);
#51526=EDGE_CURVE('',#39940,#39941,#29445,.T.);
#51527=EDGE_CURVE('',#39941,#39937,#25170,.T.);
#51528=EDGE_CURVE('',#39942,#39943,#777,.T.);
#51529=EDGE_CURVE('',#39943,#39944,#25171,.T.);
#51530=EDGE_CURVE('',#39945,#39944,#29446,.T.);
#51531=EDGE_CURVE('',#39945,#39946,#25172,.T.);
#51532=EDGE_CURVE('',#39946,#39942,#29447,.T.);
#51533=EDGE_CURVE('',#39944,#39938,#25173,.T.);
#51534=EDGE_CURVE('',#39937,#39945,#21198,.T.);
#51535=EDGE_CURVE('',#39946,#39947,#25174,.T.);
#51536=EDGE_CURVE('',#39948,#39945,#778,.T.);
#51537=EDGE_CURVE('',#39947,#39948,#25175,.T.);
#51538=EDGE_CURVE('',#39948,#39937,#779,.T.);
#51539=EDGE_CURVE('',#39949,#39941,#25176,.T.);
#51540=EDGE_CURVE('',#39948,#39949,#25177,.T.);
#51541=EDGE_CURVE('',#39620,#39947,#21199,.T.);
#51542=EDGE_CURVE('',#39949,#39947,#21200,.T.);
#51543=EDGE_CURVE('',#39621,#39949,#21201,.T.);
#51544=EDGE_CURVE('',#39619,#39946,#21202,.T.);
#51545=EDGE_CURVE('',#39942,#39618,#21203,.T.);
#51546=EDGE_CURVE('',#39943,#38871,#21204,.T.);
#51547=EDGE_CURVE('',#39944,#38870,#21205,.T.);
#51548=EDGE_CURVE('',#39938,#38869,#21206,.T.);
#51549=EDGE_CURVE('',#39939,#38868,#21207,.T.);
#51550=EDGE_CURVE('',#39623,#39940,#21208,.T.);
#51551=EDGE_CURVE('',#39622,#39941,#21209,.T.);
#51552=EDGE_CURVE('',#39950,#39951,#29448,.T.);
#51553=EDGE_CURVE('',#39951,#39952,#25178,.T.);
#51554=EDGE_CURVE('',#39952,#39953,#780,.T.);
#51555=EDGE_CURVE('',#39953,#39954,#29449,.T.);
#51556=EDGE_CURVE('',#39954,#39950,#25179,.T.);
#51557=EDGE_CURVE('',#39955,#39956,#781,.T.);
#51558=EDGE_CURVE('',#39956,#39957,#25180,.T.);
#51559=EDGE_CURVE('',#39958,#39957,#29450,.T.);
#51560=EDGE_CURVE('',#39958,#39959,#25181,.T.);
#51561=EDGE_CURVE('',#39959,#39955,#29451,.T.);
#51562=EDGE_CURVE('',#39957,#39951,#25182,.T.);
#51563=EDGE_CURVE('',#39950,#39958,#21210,.T.);
#51564=EDGE_CURVE('',#39959,#39960,#25183,.T.);
#51565=EDGE_CURVE('',#39961,#39958,#782,.T.);
#51566=EDGE_CURVE('',#39960,#39961,#25184,.T.);
#51567=EDGE_CURVE('',#39961,#39950,#783,.T.);
#51568=EDGE_CURVE('',#39962,#39954,#25185,.T.);
#51569=EDGE_CURVE('',#39961,#39962,#25186,.T.);
#51570=EDGE_CURVE('',#39626,#39960,#21211,.T.);
#51571=EDGE_CURVE('',#39962,#39960,#21212,.T.);
#51572=EDGE_CURVE('',#39627,#39962,#21213,.T.);
#51573=EDGE_CURVE('',#39625,#39959,#21214,.T.);
#51574=EDGE_CURVE('',#39955,#39624,#21215,.T.);
#51575=EDGE_CURVE('',#39956,#38867,#21216,.T.);
#51576=EDGE_CURVE('',#39957,#38866,#21217,.T.);
#51577=EDGE_CURVE('',#39951,#38865,#21218,.T.);
#51578=EDGE_CURVE('',#39952,#38864,#21219,.T.);
#51579=EDGE_CURVE('',#39629,#39953,#21220,.T.);
#51580=EDGE_CURVE('',#39628,#39954,#21221,.T.);
#51581=EDGE_CURVE('',#39963,#39964,#29452,.T.);
#51582=EDGE_CURVE('',#39964,#39965,#25187,.T.);
#51583=EDGE_CURVE('',#39965,#39966,#784,.T.);
#51584=EDGE_CURVE('',#39966,#39967,#29453,.T.);
#51585=EDGE_CURVE('',#39967,#39963,#25188,.T.);
#51586=EDGE_CURVE('',#39968,#39969,#785,.T.);
#51587=EDGE_CURVE('',#39969,#39970,#25189,.T.);
#51588=EDGE_CURVE('',#39971,#39970,#29454,.T.);
#51589=EDGE_CURVE('',#39971,#39972,#25190,.T.);
#51590=EDGE_CURVE('',#39972,#39968,#29455,.T.);
#51591=EDGE_CURVE('',#39970,#39964,#25191,.T.);
#51592=EDGE_CURVE('',#39963,#39971,#21222,.T.);
#51593=EDGE_CURVE('',#39972,#39973,#25192,.T.);
#51594=EDGE_CURVE('',#39974,#39971,#786,.T.);
#51595=EDGE_CURVE('',#39973,#39974,#25193,.T.);
#51596=EDGE_CURVE('',#39974,#39963,#787,.T.);
#51597=EDGE_CURVE('',#39975,#39967,#25194,.T.);
#51598=EDGE_CURVE('',#39974,#39975,#25195,.T.);
#51599=EDGE_CURVE('',#39632,#39973,#21223,.T.);
#51600=EDGE_CURVE('',#39975,#39973,#21224,.T.);
#51601=EDGE_CURVE('',#39633,#39975,#21225,.T.);
#51602=EDGE_CURVE('',#39631,#39972,#21226,.T.);
#51603=EDGE_CURVE('',#39968,#39630,#21227,.T.);
#51604=EDGE_CURVE('',#39969,#38863,#21228,.T.);
#51605=EDGE_CURVE('',#39970,#38862,#21229,.T.);
#51606=EDGE_CURVE('',#39964,#38861,#21230,.T.);
#51607=EDGE_CURVE('',#39965,#38860,#21231,.T.);
#51608=EDGE_CURVE('',#39635,#39966,#21232,.T.);
#51609=EDGE_CURVE('',#39634,#39967,#21233,.T.);
#51610=EDGE_CURVE('',#39976,#39977,#29456,.T.);
#51611=EDGE_CURVE('',#39977,#39978,#25196,.T.);
#51612=EDGE_CURVE('',#39978,#39979,#788,.T.);
#51613=EDGE_CURVE('',#39979,#39980,#29457,.T.);
#51614=EDGE_CURVE('',#39980,#39976,#25197,.T.);
#51615=EDGE_CURVE('',#39981,#39982,#789,.T.);
#51616=EDGE_CURVE('',#39982,#39983,#25198,.T.);
#51617=EDGE_CURVE('',#39984,#39983,#29458,.T.);
#51618=EDGE_CURVE('',#39984,#39985,#25199,.T.);
#51619=EDGE_CURVE('',#39985,#39981,#29459,.T.);
#51620=EDGE_CURVE('',#39983,#39977,#25200,.T.);
#51621=EDGE_CURVE('',#39976,#39984,#21234,.T.);
#51622=EDGE_CURVE('',#39985,#39986,#25201,.T.);
#51623=EDGE_CURVE('',#39987,#39984,#790,.T.);
#51624=EDGE_CURVE('',#39986,#39987,#25202,.T.);
#51625=EDGE_CURVE('',#39987,#39976,#791,.T.);
#51626=EDGE_CURVE('',#39988,#39980,#25203,.T.);
#51627=EDGE_CURVE('',#39987,#39988,#25204,.T.);
#51628=EDGE_CURVE('',#39638,#39986,#21235,.T.);
#51629=EDGE_CURVE('',#39988,#39986,#21236,.T.);
#51630=EDGE_CURVE('',#39639,#39988,#21237,.T.);
#51631=EDGE_CURVE('',#39637,#39985,#21238,.T.);
#51632=EDGE_CURVE('',#39981,#39636,#21239,.T.);
#51633=EDGE_CURVE('',#39982,#38859,#21240,.T.);
#51634=EDGE_CURVE('',#39983,#38858,#21241,.T.);
#51635=EDGE_CURVE('',#39977,#38857,#21242,.T.);
#51636=EDGE_CURVE('',#39978,#38856,#21243,.T.);
#51637=EDGE_CURVE('',#39053,#39979,#21244,.T.);
#51638=EDGE_CURVE('',#39640,#39980,#21245,.T.);
#51639=EDGE_CURVE('',#39989,#39990,#29460,.T.);
#51640=EDGE_CURVE('',#39990,#39991,#25205,.T.);
#51641=EDGE_CURVE('',#39991,#39992,#792,.T.);
#51642=EDGE_CURVE('',#39992,#39993,#29461,.T.);
#51643=EDGE_CURVE('',#39993,#39989,#25206,.T.);
#51644=EDGE_CURVE('',#39994,#39995,#793,.T.);
#51645=EDGE_CURVE('',#39995,#39996,#25207,.T.);
#51646=EDGE_CURVE('',#39997,#39996,#29462,.T.);
#51647=EDGE_CURVE('',#39997,#39998,#25208,.T.);
#51648=EDGE_CURVE('',#39998,#39994,#29463,.T.);
#51649=EDGE_CURVE('',#39996,#39990,#25209,.T.);
#51650=EDGE_CURVE('',#39989,#39997,#21246,.T.);
#51651=EDGE_CURVE('',#39998,#39999,#25210,.T.);
#51652=EDGE_CURVE('',#40000,#39997,#794,.T.);
#51653=EDGE_CURVE('',#39999,#40000,#25211,.T.);
#51654=EDGE_CURVE('',#40000,#39989,#795,.T.);
#51655=EDGE_CURVE('',#40001,#39993,#25212,.T.);
#51656=EDGE_CURVE('',#40000,#40001,#25213,.T.);
#51657=EDGE_CURVE('',#39055,#39999,#21247,.T.);
#51658=EDGE_CURVE('',#40001,#39999,#21248,.T.);
#51659=EDGE_CURVE('',#39056,#40001,#21249,.T.);
#51660=EDGE_CURVE('',#39054,#39998,#21250,.T.);
#51661=EDGE_CURVE('',#39994,#39052,#21251,.T.);
#51662=EDGE_CURVE('',#39995,#38852,#21252,.T.);
#51663=EDGE_CURVE('',#39996,#38851,#21253,.T.);
#51664=EDGE_CURVE('',#39990,#38850,#21254,.T.);
#51665=EDGE_CURVE('',#39991,#38849,#21255,.T.);
#51666=EDGE_CURVE('',#39058,#39992,#21256,.T.);
#51667=EDGE_CURVE('',#39057,#39993,#21257,.T.);
#51668=EDGE_CURVE('',#40002,#40003,#29464,.T.);
#51669=EDGE_CURVE('',#40003,#40004,#25214,.T.);
#51670=EDGE_CURVE('',#40004,#40005,#796,.T.);
#51671=EDGE_CURVE('',#40005,#40006,#29465,.T.);
#51672=EDGE_CURVE('',#40006,#40002,#25215,.T.);
#51673=EDGE_CURVE('',#40007,#40008,#797,.T.);
#51674=EDGE_CURVE('',#40008,#40009,#25216,.T.);
#51675=EDGE_CURVE('',#40010,#40009,#29466,.T.);
#51676=EDGE_CURVE('',#40010,#40011,#25217,.T.);
#51677=EDGE_CURVE('',#40011,#40007,#29467,.T.);
#51678=EDGE_CURVE('',#40009,#40003,#25218,.T.);
#51679=EDGE_CURVE('',#40002,#40010,#21258,.T.);
#51680=EDGE_CURVE('',#40011,#40012,#25219,.T.);
#51681=EDGE_CURVE('',#40013,#40010,#798,.T.);
#51682=EDGE_CURVE('',#40012,#40013,#25220,.T.);
#51683=EDGE_CURVE('',#40013,#40002,#799,.T.);
#51684=EDGE_CURVE('',#40014,#40006,#25221,.T.);
#51685=EDGE_CURVE('',#40013,#40014,#25222,.T.);
#51686=EDGE_CURVE('',#39061,#40012,#21259,.T.);
#51687=EDGE_CURVE('',#40014,#40012,#21260,.T.);
#51688=EDGE_CURVE('',#39062,#40014,#21261,.T.);
#51689=EDGE_CURVE('',#39060,#40011,#21262,.T.);
#51690=EDGE_CURVE('',#40007,#39059,#21263,.T.);
#51691=EDGE_CURVE('',#40008,#38848,#21264,.T.);
#51692=EDGE_CURVE('',#40009,#38847,#21265,.T.);
#51693=EDGE_CURVE('',#40003,#38846,#21266,.T.);
#51694=EDGE_CURVE('',#40004,#38845,#21267,.T.);
#51695=EDGE_CURVE('',#39064,#40005,#21268,.T.);
#51696=EDGE_CURVE('',#39063,#40006,#21269,.T.);
#51697=EDGE_CURVE('',#40015,#40016,#29468,.T.);
#51698=EDGE_CURVE('',#40016,#40017,#25223,.T.);
#51699=EDGE_CURVE('',#40017,#40018,#800,.T.);
#51700=EDGE_CURVE('',#40018,#40019,#29469,.T.);
#51701=EDGE_CURVE('',#40019,#40015,#25224,.T.);
#51702=EDGE_CURVE('',#40020,#40021,#801,.T.);
#51703=EDGE_CURVE('',#40021,#40022,#25225,.T.);
#51704=EDGE_CURVE('',#40023,#40022,#29470,.T.);
#51705=EDGE_CURVE('',#40023,#40024,#25226,.T.);
#51706=EDGE_CURVE('',#40024,#40020,#29471,.T.);
#51707=EDGE_CURVE('',#40022,#40016,#25227,.T.);
#51708=EDGE_CURVE('',#40015,#40023,#21270,.T.);
#51709=EDGE_CURVE('',#40024,#40025,#25228,.T.);
#51710=EDGE_CURVE('',#40026,#40023,#802,.T.);
#51711=EDGE_CURVE('',#40025,#40026,#25229,.T.);
#51712=EDGE_CURVE('',#40026,#40015,#803,.T.);
#51713=EDGE_CURVE('',#40027,#40019,#25230,.T.);
#51714=EDGE_CURVE('',#40026,#40027,#25231,.T.);
#51715=EDGE_CURVE('',#39067,#40025,#21271,.T.);
#51716=EDGE_CURVE('',#40027,#40025,#21272,.T.);
#51717=EDGE_CURVE('',#39068,#40027,#21273,.T.);
#51718=EDGE_CURVE('',#39066,#40024,#21274,.T.);
#51719=EDGE_CURVE('',#40020,#39065,#21275,.T.);
#51720=EDGE_CURVE('',#40021,#38844,#21276,.T.);
#51721=EDGE_CURVE('',#40022,#38843,#21277,.T.);
#51722=EDGE_CURVE('',#40016,#38842,#21278,.T.);
#51723=EDGE_CURVE('',#40017,#38841,#21279,.T.);
#51724=EDGE_CURVE('',#39070,#40018,#21280,.T.);
#51725=EDGE_CURVE('',#39069,#40019,#21281,.T.);
#51726=EDGE_CURVE('',#40028,#40029,#29472,.T.);
#51727=EDGE_CURVE('',#40029,#40030,#25232,.T.);
#51728=EDGE_CURVE('',#40030,#40031,#804,.T.);
#51729=EDGE_CURVE('',#40031,#40032,#29473,.T.);
#51730=EDGE_CURVE('',#40032,#40028,#25233,.T.);
#51731=EDGE_CURVE('',#40033,#40034,#805,.T.);
#51732=EDGE_CURVE('',#40034,#40035,#25234,.T.);
#51733=EDGE_CURVE('',#40036,#40035,#29474,.T.);
#51734=EDGE_CURVE('',#40036,#40037,#25235,.T.);
#51735=EDGE_CURVE('',#40037,#40033,#29475,.T.);
#51736=EDGE_CURVE('',#40035,#40029,#25236,.T.);
#51737=EDGE_CURVE('',#40028,#40036,#21282,.T.);
#51738=EDGE_CURVE('',#40037,#40038,#25237,.T.);
#51739=EDGE_CURVE('',#40039,#40036,#806,.T.);
#51740=EDGE_CURVE('',#40038,#40039,#25238,.T.);
#51741=EDGE_CURVE('',#40039,#40028,#807,.T.);
#51742=EDGE_CURVE('',#40040,#40032,#25239,.T.);
#51743=EDGE_CURVE('',#40039,#40040,#25240,.T.);
#51744=EDGE_CURVE('',#39073,#40038,#21283,.T.);
#51745=EDGE_CURVE('',#40040,#40038,#21284,.T.);
#51746=EDGE_CURVE('',#39074,#40040,#21285,.T.);
#51747=EDGE_CURVE('',#39072,#40037,#21286,.T.);
#51748=EDGE_CURVE('',#40033,#39071,#21287,.T.);
#51749=EDGE_CURVE('',#40034,#38840,#21288,.T.);
#51750=EDGE_CURVE('',#40035,#38839,#21289,.T.);
#51751=EDGE_CURVE('',#40029,#38838,#21290,.T.);
#51752=EDGE_CURVE('',#40030,#38837,#21291,.T.);
#51753=EDGE_CURVE('',#39076,#40031,#21292,.T.);
#51754=EDGE_CURVE('',#39075,#40032,#21293,.T.);
#51755=EDGE_CURVE('',#40041,#40042,#29476,.T.);
#51756=EDGE_CURVE('',#40042,#40043,#25241,.T.);
#51757=EDGE_CURVE('',#40043,#40044,#808,.T.);
#51758=EDGE_CURVE('',#40044,#40045,#29477,.T.);
#51759=EDGE_CURVE('',#40045,#40041,#25242,.T.);
#51760=EDGE_CURVE('',#40046,#40047,#809,.T.);
#51761=EDGE_CURVE('',#40047,#40048,#25243,.T.);
#51762=EDGE_CURVE('',#40049,#40048,#29478,.T.);
#51763=EDGE_CURVE('',#40049,#40050,#25244,.T.);
#51764=EDGE_CURVE('',#40050,#40046,#29479,.T.);
#51765=EDGE_CURVE('',#40048,#40042,#25245,.T.);
#51766=EDGE_CURVE('',#40041,#40049,#21294,.T.);
#51767=EDGE_CURVE('',#40050,#40051,#25246,.T.);
#51768=EDGE_CURVE('',#40052,#40049,#810,.T.);
#51769=EDGE_CURVE('',#40051,#40052,#25247,.T.);
#51770=EDGE_CURVE('',#40052,#40041,#811,.T.);
#51771=EDGE_CURVE('',#40053,#40045,#25248,.T.);
#51772=EDGE_CURVE('',#40052,#40053,#25249,.T.);
#51773=EDGE_CURVE('',#39079,#40051,#21295,.T.);
#51774=EDGE_CURVE('',#40053,#40051,#21296,.T.);
#51775=EDGE_CURVE('',#39080,#40053,#21297,.T.);
#51776=EDGE_CURVE('',#39078,#40050,#21298,.T.);
#51777=EDGE_CURVE('',#40046,#39077,#21299,.T.);
#51778=EDGE_CURVE('',#40047,#38836,#21300,.T.);
#51779=EDGE_CURVE('',#40048,#38835,#21301,.T.);
#51780=EDGE_CURVE('',#40042,#38834,#21302,.T.);
#51781=EDGE_CURVE('',#40043,#38833,#21303,.T.);
#51782=EDGE_CURVE('',#39082,#40044,#21304,.T.);
#51783=EDGE_CURVE('',#39081,#40045,#21305,.T.);
#51784=EDGE_CURVE('',#40054,#40055,#29480,.T.);
#51785=EDGE_CURVE('',#40055,#40056,#25250,.T.);
#51786=EDGE_CURVE('',#40056,#40057,#812,.T.);
#51787=EDGE_CURVE('',#40057,#40058,#29481,.T.);
#51788=EDGE_CURVE('',#40058,#40054,#25251,.T.);
#51789=EDGE_CURVE('',#40059,#40060,#813,.T.);
#51790=EDGE_CURVE('',#40060,#40061,#25252,.T.);
#51791=EDGE_CURVE('',#40062,#40061,#29482,.T.);
#51792=EDGE_CURVE('',#40062,#40063,#25253,.T.);
#51793=EDGE_CURVE('',#40063,#40059,#29483,.T.);
#51794=EDGE_CURVE('',#40061,#40055,#25254,.T.);
#51795=EDGE_CURVE('',#40054,#40062,#21306,.T.);
#51796=EDGE_CURVE('',#40063,#40064,#25255,.T.);
#51797=EDGE_CURVE('',#40065,#40062,#814,.T.);
#51798=EDGE_CURVE('',#40064,#40065,#25256,.T.);
#51799=EDGE_CURVE('',#40065,#40054,#815,.T.);
#51800=EDGE_CURVE('',#40066,#40058,#25257,.T.);
#51801=EDGE_CURVE('',#40065,#40066,#25258,.T.);
#51802=EDGE_CURVE('',#39085,#40064,#21307,.T.);
#51803=EDGE_CURVE('',#40066,#40064,#21308,.T.);
#51804=EDGE_CURVE('',#39086,#40066,#21309,.T.);
#51805=EDGE_CURVE('',#39084,#40063,#21310,.T.);
#51806=EDGE_CURVE('',#40059,#39083,#21311,.T.);
#51807=EDGE_CURVE('',#40060,#38832,#21312,.T.);
#51808=EDGE_CURVE('',#40061,#38831,#21313,.T.);
#51809=EDGE_CURVE('',#40055,#38830,#21314,.T.);
#51810=EDGE_CURVE('',#40056,#38829,#21315,.T.);
#51811=EDGE_CURVE('',#39088,#40057,#21316,.T.);
#51812=EDGE_CURVE('',#39087,#40058,#21317,.T.);
#51813=EDGE_CURVE('',#40067,#40068,#29484,.T.);
#51814=EDGE_CURVE('',#40068,#40069,#25259,.T.);
#51815=EDGE_CURVE('',#40069,#40070,#816,.T.);
#51816=EDGE_CURVE('',#40070,#40071,#29485,.T.);
#51817=EDGE_CURVE('',#40071,#40067,#25260,.T.);
#51818=EDGE_CURVE('',#40072,#40073,#817,.T.);
#51819=EDGE_CURVE('',#40073,#40074,#25261,.T.);
#51820=EDGE_CURVE('',#40075,#40074,#29486,.T.);
#51821=EDGE_CURVE('',#40075,#40076,#25262,.T.);
#51822=EDGE_CURVE('',#40076,#40072,#29487,.T.);
#51823=EDGE_CURVE('',#40074,#40068,#25263,.T.);
#51824=EDGE_CURVE('',#40067,#40075,#21318,.T.);
#51825=EDGE_CURVE('',#40076,#40077,#25264,.T.);
#51826=EDGE_CURVE('',#40078,#40075,#818,.T.);
#51827=EDGE_CURVE('',#40077,#40078,#25265,.T.);
#51828=EDGE_CURVE('',#40078,#40067,#819,.T.);
#51829=EDGE_CURVE('',#40079,#40071,#25266,.T.);
#51830=EDGE_CURVE('',#40078,#40079,#25267,.T.);
#51831=EDGE_CURVE('',#39091,#40077,#21319,.T.);
#51832=EDGE_CURVE('',#40079,#40077,#21320,.T.);
#51833=EDGE_CURVE('',#39092,#40079,#21321,.T.);
#51834=EDGE_CURVE('',#39090,#40076,#21322,.T.);
#51835=EDGE_CURVE('',#40072,#39089,#21323,.T.);
#51836=EDGE_CURVE('',#40073,#38828,#21324,.T.);
#51837=EDGE_CURVE('',#40074,#38827,#21325,.T.);
#51838=EDGE_CURVE('',#40068,#38826,#21326,.T.);
#51839=EDGE_CURVE('',#40069,#38825,#21327,.T.);
#51840=EDGE_CURVE('',#39094,#40070,#21328,.T.);
#51841=EDGE_CURVE('',#39093,#40071,#21329,.T.);
#51842=EDGE_CURVE('',#40080,#40081,#29488,.T.);
#51843=EDGE_CURVE('',#40081,#40082,#25268,.T.);
#51844=EDGE_CURVE('',#40082,#40083,#820,.T.);
#51845=EDGE_CURVE('',#40083,#40084,#29489,.T.);
#51846=EDGE_CURVE('',#40084,#40080,#25269,.T.);
#51847=EDGE_CURVE('',#40085,#40086,#821,.T.);
#51848=EDGE_CURVE('',#40086,#40087,#25270,.T.);
#51849=EDGE_CURVE('',#40088,#40087,#29490,.T.);
#51850=EDGE_CURVE('',#40088,#40089,#25271,.T.);
#51851=EDGE_CURVE('',#40089,#40085,#29491,.T.);
#51852=EDGE_CURVE('',#40087,#40081,#25272,.T.);
#51853=EDGE_CURVE('',#40080,#40088,#21330,.T.);
#51854=EDGE_CURVE('',#40089,#40090,#25273,.T.);
#51855=EDGE_CURVE('',#40091,#40088,#822,.T.);
#51856=EDGE_CURVE('',#40090,#40091,#25274,.T.);
#51857=EDGE_CURVE('',#40091,#40080,#823,.T.);
#51858=EDGE_CURVE('',#40092,#40084,#25275,.T.);
#51859=EDGE_CURVE('',#40091,#40092,#25276,.T.);
#51860=EDGE_CURVE('',#39097,#40090,#21331,.T.);
#51861=EDGE_CURVE('',#40092,#40090,#21332,.T.);
#51862=EDGE_CURVE('',#39098,#40092,#21333,.T.);
#51863=EDGE_CURVE('',#39096,#40089,#21334,.T.);
#51864=EDGE_CURVE('',#40085,#39095,#21335,.T.);
#51865=EDGE_CURVE('',#40086,#38824,#21336,.T.);
#51866=EDGE_CURVE('',#40087,#38823,#21337,.T.);
#51867=EDGE_CURVE('',#40081,#38822,#21338,.T.);
#51868=EDGE_CURVE('',#40082,#38821,#21339,.T.);
#51869=EDGE_CURVE('',#39100,#40083,#21340,.T.);
#51870=EDGE_CURVE('',#39099,#40084,#21341,.T.);
#51871=EDGE_CURVE('',#40093,#40094,#29492,.T.);
#51872=EDGE_CURVE('',#40094,#40095,#25277,.T.);
#51873=EDGE_CURVE('',#40095,#40096,#824,.T.);
#51874=EDGE_CURVE('',#40096,#40097,#29493,.T.);
#51875=EDGE_CURVE('',#40097,#40093,#25278,.T.);
#51876=EDGE_CURVE('',#40098,#40099,#825,.T.);
#51877=EDGE_CURVE('',#40099,#40100,#25279,.T.);
#51878=EDGE_CURVE('',#40101,#40100,#29494,.T.);
#51879=EDGE_CURVE('',#40101,#40102,#25280,.T.);
#51880=EDGE_CURVE('',#40102,#40098,#29495,.T.);
#51881=EDGE_CURVE('',#40100,#40094,#25281,.T.);
#51882=EDGE_CURVE('',#40093,#40101,#21342,.T.);
#51883=EDGE_CURVE('',#40102,#40103,#25282,.T.);
#51884=EDGE_CURVE('',#40104,#40101,#826,.T.);
#51885=EDGE_CURVE('',#40103,#40104,#25283,.T.);
#51886=EDGE_CURVE('',#40104,#40093,#827,.T.);
#51887=EDGE_CURVE('',#40105,#40097,#25284,.T.);
#51888=EDGE_CURVE('',#40104,#40105,#25285,.T.);
#51889=EDGE_CURVE('',#39482,#40103,#21343,.T.);
#51890=EDGE_CURVE('',#40105,#40103,#21344,.T.);
#51891=EDGE_CURVE('',#39483,#40105,#21345,.T.);
#51892=EDGE_CURVE('',#39481,#40102,#21346,.T.);
#51893=EDGE_CURVE('',#40098,#39480,#21347,.T.);
#51894=EDGE_CURVE('',#40099,#38963,#21348,.T.);
#51895=EDGE_CURVE('',#40100,#38962,#21349,.T.);
#51896=EDGE_CURVE('',#40094,#38961,#21350,.T.);
#51897=EDGE_CURVE('',#40095,#38960,#21351,.T.);
#51898=EDGE_CURVE('',#39485,#40096,#21352,.T.);
#51899=EDGE_CURVE('',#39484,#40097,#21353,.T.);
#51900=EDGE_CURVE('',#40106,#40107,#29496,.T.);
#51901=EDGE_CURVE('',#40107,#40108,#25286,.T.);
#51902=EDGE_CURVE('',#40108,#40109,#828,.T.);
#51903=EDGE_CURVE('',#40109,#40110,#29497,.T.);
#51904=EDGE_CURVE('',#40110,#40106,#25287,.T.);
#51905=EDGE_CURVE('',#40111,#40112,#829,.T.);
#51906=EDGE_CURVE('',#40112,#40113,#25288,.T.);
#51907=EDGE_CURVE('',#40114,#40113,#29498,.T.);
#51908=EDGE_CURVE('',#40114,#40115,#25289,.T.);
#51909=EDGE_CURVE('',#40115,#40111,#29499,.T.);
#51910=EDGE_CURVE('',#40113,#40107,#25290,.T.);
#51911=EDGE_CURVE('',#40106,#40114,#21354,.T.);
#51912=EDGE_CURVE('',#40115,#40116,#25291,.T.);
#51913=EDGE_CURVE('',#40117,#40114,#830,.T.);
#51914=EDGE_CURVE('',#40116,#40117,#25292,.T.);
#51915=EDGE_CURVE('',#40117,#40106,#831,.T.);
#51916=EDGE_CURVE('',#40118,#40110,#25293,.T.);
#51917=EDGE_CURVE('',#40117,#40118,#25294,.T.);
#51918=EDGE_CURVE('',#39476,#40116,#21355,.T.);
#51919=EDGE_CURVE('',#40118,#40116,#21356,.T.);
#51920=EDGE_CURVE('',#39477,#40118,#21357,.T.);
#51921=EDGE_CURVE('',#39475,#40115,#21358,.T.);
#51922=EDGE_CURVE('',#40111,#39474,#21359,.T.);
#51923=EDGE_CURVE('',#40112,#38967,#21360,.T.);
#51924=EDGE_CURVE('',#40113,#38966,#21361,.T.);
#51925=EDGE_CURVE('',#40107,#38965,#21362,.T.);
#51926=EDGE_CURVE('',#40108,#38964,#21363,.T.);
#51927=EDGE_CURVE('',#39479,#40109,#21364,.T.);
#51928=EDGE_CURVE('',#39478,#40110,#21365,.T.);
#51929=EDGE_CURVE('',#40119,#40120,#29500,.T.);
#51930=EDGE_CURVE('',#40120,#40121,#25295,.T.);
#51931=EDGE_CURVE('',#40121,#40122,#832,.T.);
#51932=EDGE_CURVE('',#40122,#40123,#29501,.T.);
#51933=EDGE_CURVE('',#40123,#40119,#25296,.T.);
#51934=EDGE_CURVE('',#40124,#40125,#833,.T.);
#51935=EDGE_CURVE('',#40125,#40126,#25297,.T.);
#51936=EDGE_CURVE('',#40127,#40126,#29502,.T.);
#51937=EDGE_CURVE('',#40127,#40128,#25298,.T.);
#51938=EDGE_CURVE('',#40128,#40124,#29503,.T.);
#51939=EDGE_CURVE('',#40126,#40120,#25299,.T.);
#51940=EDGE_CURVE('',#40119,#40127,#21366,.T.);
#51941=EDGE_CURVE('',#40128,#40129,#25300,.T.);
#51942=EDGE_CURVE('',#40130,#40127,#834,.T.);
#51943=EDGE_CURVE('',#40129,#40130,#25301,.T.);
#51944=EDGE_CURVE('',#40130,#40119,#835,.T.);
#51945=EDGE_CURVE('',#40131,#40123,#25302,.T.);
#51946=EDGE_CURVE('',#40130,#40131,#25303,.T.);
#51947=EDGE_CURVE('',#39470,#40129,#21367,.T.);
#51948=EDGE_CURVE('',#40131,#40129,#21368,.T.);
#51949=EDGE_CURVE('',#39471,#40131,#21369,.T.);
#51950=EDGE_CURVE('',#39469,#40128,#21370,.T.);
#51951=EDGE_CURVE('',#40124,#39468,#21371,.T.);
#51952=EDGE_CURVE('',#40125,#38971,#21372,.T.);
#51953=EDGE_CURVE('',#40126,#38970,#21373,.T.);
#51954=EDGE_CURVE('',#40120,#38969,#21374,.T.);
#51955=EDGE_CURVE('',#40121,#38968,#21375,.T.);
#51956=EDGE_CURVE('',#39473,#40122,#21376,.T.);
#51957=EDGE_CURVE('',#39472,#40123,#21377,.T.);
#51958=EDGE_CURVE('',#40132,#40133,#29504,.T.);
#51959=EDGE_CURVE('',#40133,#40134,#25304,.T.);
#51960=EDGE_CURVE('',#40134,#40135,#836,.T.);
#51961=EDGE_CURVE('',#40135,#40136,#29505,.T.);
#51962=EDGE_CURVE('',#40136,#40132,#25305,.T.);
#51963=EDGE_CURVE('',#40137,#40138,#837,.T.);
#51964=EDGE_CURVE('',#40138,#40139,#25306,.T.);
#51965=EDGE_CURVE('',#40140,#40139,#29506,.T.);
#51966=EDGE_CURVE('',#40140,#40141,#25307,.T.);
#51967=EDGE_CURVE('',#40141,#40137,#29507,.T.);
#51968=EDGE_CURVE('',#40139,#40133,#25308,.T.);
#51969=EDGE_CURVE('',#40132,#40140,#21378,.T.);
#51970=EDGE_CURVE('',#40141,#40142,#25309,.T.);
#51971=EDGE_CURVE('',#40143,#40140,#838,.T.);
#51972=EDGE_CURVE('',#40142,#40143,#25310,.T.);
#51973=EDGE_CURVE('',#40143,#40132,#839,.T.);
#51974=EDGE_CURVE('',#40144,#40136,#25311,.T.);
#51975=EDGE_CURVE('',#40143,#40144,#25312,.T.);
#51976=EDGE_CURVE('',#39464,#40142,#21379,.T.);
#51977=EDGE_CURVE('',#40144,#40142,#21380,.T.);
#51978=EDGE_CURVE('',#39465,#40144,#21381,.T.);
#51979=EDGE_CURVE('',#39463,#40141,#21382,.T.);
#51980=EDGE_CURVE('',#40137,#39462,#21383,.T.);
#51981=EDGE_CURVE('',#40138,#38975,#21384,.T.);
#51982=EDGE_CURVE('',#40139,#38974,#21385,.T.);
#51983=EDGE_CURVE('',#40133,#38973,#21386,.T.);
#51984=EDGE_CURVE('',#40134,#38972,#21387,.T.);
#51985=EDGE_CURVE('',#39467,#40135,#21388,.T.);
#51986=EDGE_CURVE('',#39466,#40136,#21389,.T.);
#51987=EDGE_CURVE('',#40145,#40146,#29508,.T.);
#51988=EDGE_CURVE('',#40146,#40147,#25313,.T.);
#51989=EDGE_CURVE('',#40147,#40148,#840,.T.);
#51990=EDGE_CURVE('',#40148,#40149,#29509,.T.);
#51991=EDGE_CURVE('',#40149,#40145,#25314,.T.);
#51992=EDGE_CURVE('',#40150,#40151,#841,.T.);
#51993=EDGE_CURVE('',#40151,#40152,#25315,.T.);
#51994=EDGE_CURVE('',#40153,#40152,#29510,.T.);
#51995=EDGE_CURVE('',#40153,#40154,#25316,.T.);
#51996=EDGE_CURVE('',#40154,#40150,#29511,.T.);
#51997=EDGE_CURVE('',#40152,#40146,#25317,.T.);
#51998=EDGE_CURVE('',#40145,#40153,#21390,.T.);
#51999=EDGE_CURVE('',#40154,#40155,#25318,.T.);
#52000=EDGE_CURVE('',#40156,#40153,#842,.T.);
#52001=EDGE_CURVE('',#40155,#40156,#25319,.T.);
#52002=EDGE_CURVE('',#40156,#40145,#843,.T.);
#52003=EDGE_CURVE('',#40157,#40149,#25320,.T.);
#52004=EDGE_CURVE('',#40156,#40157,#25321,.T.);
#52005=EDGE_CURVE('',#39458,#40155,#21391,.T.);
#52006=EDGE_CURVE('',#40157,#40155,#21392,.T.);
#52007=EDGE_CURVE('',#39459,#40157,#21393,.T.);
#52008=EDGE_CURVE('',#39457,#40154,#21394,.T.);
#52009=EDGE_CURVE('',#40150,#39456,#21395,.T.);
#52010=EDGE_CURVE('',#40151,#38979,#21396,.T.);
#52011=EDGE_CURVE('',#40152,#38978,#21397,.T.);
#52012=EDGE_CURVE('',#40146,#38977,#21398,.T.);
#52013=EDGE_CURVE('',#40147,#38976,#21399,.T.);
#52014=EDGE_CURVE('',#39461,#40148,#21400,.T.);
#52015=EDGE_CURVE('',#39460,#40149,#21401,.T.);
#52016=EDGE_CURVE('',#40158,#40159,#29512,.T.);
#52017=EDGE_CURVE('',#40159,#40160,#25322,.T.);
#52018=EDGE_CURVE('',#40160,#40161,#844,.T.);
#52019=EDGE_CURVE('',#40161,#40162,#29513,.T.);
#52020=EDGE_CURVE('',#40162,#40158,#25323,.T.);
#52021=EDGE_CURVE('',#40163,#40164,#845,.T.);
#52022=EDGE_CURVE('',#40164,#40165,#25324,.T.);
#52023=EDGE_CURVE('',#40166,#40165,#29514,.T.);
#52024=EDGE_CURVE('',#40166,#40167,#25325,.T.);
#52025=EDGE_CURVE('',#40167,#40163,#29515,.T.);
#52026=EDGE_CURVE('',#40165,#40159,#25326,.T.);
#52027=EDGE_CURVE('',#40158,#40166,#21402,.T.);
#52028=EDGE_CURVE('',#40167,#40168,#25327,.T.);
#52029=EDGE_CURVE('',#40169,#40166,#846,.T.);
#52030=EDGE_CURVE('',#40168,#40169,#25328,.T.);
#52031=EDGE_CURVE('',#40169,#40158,#847,.T.);
#52032=EDGE_CURVE('',#40170,#40162,#25329,.T.);
#52033=EDGE_CURVE('',#40169,#40170,#25330,.T.);
#52034=EDGE_CURVE('',#39452,#40168,#21403,.T.);
#52035=EDGE_CURVE('',#40170,#40168,#21404,.T.);
#52036=EDGE_CURVE('',#39453,#40170,#21405,.T.);
#52037=EDGE_CURVE('',#39451,#40167,#21406,.T.);
#52038=EDGE_CURVE('',#40163,#39450,#21407,.T.);
#52039=EDGE_CURVE('',#40164,#38983,#21408,.T.);
#52040=EDGE_CURVE('',#40165,#38982,#21409,.T.);
#52041=EDGE_CURVE('',#40159,#38981,#21410,.T.);
#52042=EDGE_CURVE('',#40160,#38980,#21411,.T.);
#52043=EDGE_CURVE('',#39455,#40161,#21412,.T.);
#52044=EDGE_CURVE('',#39454,#40162,#21413,.T.);
#52045=EDGE_CURVE('',#40171,#40172,#29516,.T.);
#52046=EDGE_CURVE('',#40172,#40173,#25331,.T.);
#52047=EDGE_CURVE('',#40173,#40174,#848,.T.);
#52048=EDGE_CURVE('',#40174,#40175,#29517,.T.);
#52049=EDGE_CURVE('',#40175,#40171,#25332,.T.);
#52050=EDGE_CURVE('',#40176,#40177,#849,.T.);
#52051=EDGE_CURVE('',#40177,#40178,#25333,.T.);
#52052=EDGE_CURVE('',#40179,#40178,#29518,.T.);
#52053=EDGE_CURVE('',#40179,#40180,#25334,.T.);
#52054=EDGE_CURVE('',#40180,#40176,#29519,.T.);
#52055=EDGE_CURVE('',#40178,#40172,#25335,.T.);
#52056=EDGE_CURVE('',#40171,#40179,#21414,.T.);
#52057=EDGE_CURVE('',#40180,#40181,#25336,.T.);
#52058=EDGE_CURVE('',#40182,#40179,#850,.T.);
#52059=EDGE_CURVE('',#40181,#40182,#25337,.T.);
#52060=EDGE_CURVE('',#40182,#40171,#851,.T.);
#52061=EDGE_CURVE('',#40183,#40175,#25338,.T.);
#52062=EDGE_CURVE('',#40182,#40183,#25339,.T.);
#52063=EDGE_CURVE('',#39446,#40181,#21415,.T.);
#52064=EDGE_CURVE('',#40183,#40181,#21416,.T.);
#52065=EDGE_CURVE('',#39447,#40183,#21417,.T.);
#52066=EDGE_CURVE('',#39445,#40180,#21418,.T.);
#52067=EDGE_CURVE('',#40176,#39444,#21419,.T.);
#52068=EDGE_CURVE('',#40177,#38987,#21420,.T.);
#52069=EDGE_CURVE('',#40178,#38986,#21421,.T.);
#52070=EDGE_CURVE('',#40172,#38985,#21422,.T.);
#52071=EDGE_CURVE('',#40173,#38984,#21423,.T.);
#52072=EDGE_CURVE('',#39449,#40174,#21424,.T.);
#52073=EDGE_CURVE('',#39448,#40175,#21425,.T.);
#52074=EDGE_CURVE('',#40184,#40185,#29520,.T.);
#52075=EDGE_CURVE('',#40185,#40186,#25340,.T.);
#52076=EDGE_CURVE('',#40186,#40187,#852,.T.);
#52077=EDGE_CURVE('',#40187,#40188,#29521,.T.);
#52078=EDGE_CURVE('',#40188,#40184,#25341,.T.);
#52079=EDGE_CURVE('',#40189,#40190,#853,.T.);
#52080=EDGE_CURVE('',#40190,#40191,#25342,.T.);
#52081=EDGE_CURVE('',#40192,#40191,#29522,.T.);
#52082=EDGE_CURVE('',#40192,#40193,#25343,.T.);
#52083=EDGE_CURVE('',#40193,#40189,#29523,.T.);
#52084=EDGE_CURVE('',#40191,#40185,#25344,.T.);
#52085=EDGE_CURVE('',#40184,#40192,#21426,.T.);
#52086=EDGE_CURVE('',#40193,#40194,#25345,.T.);
#52087=EDGE_CURVE('',#40195,#40192,#854,.T.);
#52088=EDGE_CURVE('',#40194,#40195,#25346,.T.);
#52089=EDGE_CURVE('',#40195,#40184,#855,.T.);
#52090=EDGE_CURVE('',#40196,#40188,#25347,.T.);
#52091=EDGE_CURVE('',#40195,#40196,#25348,.T.);
#52092=EDGE_CURVE('',#39440,#40194,#21427,.T.);
#52093=EDGE_CURVE('',#40196,#40194,#21428,.T.);
#52094=EDGE_CURVE('',#39441,#40196,#21429,.T.);
#52095=EDGE_CURVE('',#39439,#40193,#21430,.T.);
#52096=EDGE_CURVE('',#40189,#39438,#21431,.T.);
#52097=EDGE_CURVE('',#40190,#38991,#21432,.T.);
#52098=EDGE_CURVE('',#40191,#38990,#21433,.T.);
#52099=EDGE_CURVE('',#40185,#38989,#21434,.T.);
#52100=EDGE_CURVE('',#40186,#38988,#21435,.T.);
#52101=EDGE_CURVE('',#39443,#40187,#21436,.T.);
#52102=EDGE_CURVE('',#39442,#40188,#21437,.T.);
#52103=EDGE_CURVE('',#40197,#40198,#29524,.T.);
#52104=EDGE_CURVE('',#40198,#40199,#25349,.T.);
#52105=EDGE_CURVE('',#40199,#40200,#856,.T.);
#52106=EDGE_CURVE('',#40200,#40201,#29525,.T.);
#52107=EDGE_CURVE('',#40201,#40197,#25350,.T.);
#52108=EDGE_CURVE('',#40202,#40203,#857,.T.);
#52109=EDGE_CURVE('',#40203,#40204,#25351,.T.);
#52110=EDGE_CURVE('',#40205,#40204,#29526,.T.);
#52111=EDGE_CURVE('',#40205,#40206,#25352,.T.);
#52112=EDGE_CURVE('',#40206,#40202,#29527,.T.);
#52113=EDGE_CURVE('',#40204,#40198,#25353,.T.);
#52114=EDGE_CURVE('',#40197,#40205,#21438,.T.);
#52115=EDGE_CURVE('',#40206,#40207,#25354,.T.);
#52116=EDGE_CURVE('',#40208,#40205,#858,.T.);
#52117=EDGE_CURVE('',#40207,#40208,#25355,.T.);
#52118=EDGE_CURVE('',#40208,#40197,#859,.T.);
#52119=EDGE_CURVE('',#40209,#40201,#25356,.T.);
#52120=EDGE_CURVE('',#40208,#40209,#25357,.T.);
#52121=EDGE_CURVE('',#39434,#40207,#21439,.T.);
#52122=EDGE_CURVE('',#40209,#40207,#21440,.T.);
#52123=EDGE_CURVE('',#39435,#40209,#21441,.T.);
#52124=EDGE_CURVE('',#39433,#40206,#21442,.T.);
#52125=EDGE_CURVE('',#40202,#39432,#21443,.T.);
#52126=EDGE_CURVE('',#40203,#38995,#21444,.T.);
#52127=EDGE_CURVE('',#40204,#38994,#21445,.T.);
#52128=EDGE_CURVE('',#40198,#38993,#21446,.T.);
#52129=EDGE_CURVE('',#40199,#38992,#21447,.T.);
#52130=EDGE_CURVE('',#39437,#40200,#21448,.T.);
#52131=EDGE_CURVE('',#39436,#40201,#21449,.T.);
#52132=EDGE_CURVE('',#40210,#40211,#29528,.T.);
#52133=EDGE_CURVE('',#40211,#40212,#25358,.T.);
#52134=EDGE_CURVE('',#40212,#40213,#860,.T.);
#52135=EDGE_CURVE('',#40213,#40214,#29529,.T.);
#52136=EDGE_CURVE('',#40214,#40210,#25359,.T.);
#52137=EDGE_CURVE('',#40215,#40216,#861,.T.);
#52138=EDGE_CURVE('',#40216,#40217,#25360,.T.);
#52139=EDGE_CURVE('',#40218,#40217,#29530,.T.);
#52140=EDGE_CURVE('',#40218,#40219,#25361,.T.);
#52141=EDGE_CURVE('',#40219,#40215,#29531,.T.);
#52142=EDGE_CURVE('',#40217,#40211,#25362,.T.);
#52143=EDGE_CURVE('',#40210,#40218,#21450,.T.);
#52144=EDGE_CURVE('',#40219,#40220,#25363,.T.);
#52145=EDGE_CURVE('',#40221,#40218,#862,.T.);
#52146=EDGE_CURVE('',#40220,#40221,#25364,.T.);
#52147=EDGE_CURVE('',#40221,#40210,#863,.T.);
#52148=EDGE_CURVE('',#40222,#40214,#25365,.T.);
#52149=EDGE_CURVE('',#40221,#40222,#25366,.T.);
#52150=EDGE_CURVE('',#39428,#40220,#21451,.T.);
#52151=EDGE_CURVE('',#40222,#40220,#21452,.T.);
#52152=EDGE_CURVE('',#39429,#40222,#21453,.T.);
#52153=EDGE_CURVE('',#39427,#40219,#21454,.T.);
#52154=EDGE_CURVE('',#40215,#39426,#21455,.T.);
#52155=EDGE_CURVE('',#40216,#38999,#21456,.T.);
#52156=EDGE_CURVE('',#40217,#38998,#21457,.T.);
#52157=EDGE_CURVE('',#40211,#38997,#21458,.T.);
#52158=EDGE_CURVE('',#40212,#38996,#21459,.T.);
#52159=EDGE_CURVE('',#39431,#40213,#21460,.T.);
#52160=EDGE_CURVE('',#39430,#40214,#21461,.T.);
#52161=EDGE_CURVE('',#40223,#40224,#29532,.T.);
#52162=EDGE_CURVE('',#40224,#40225,#25367,.T.);
#52163=EDGE_CURVE('',#40225,#40226,#864,.T.);
#52164=EDGE_CURVE('',#40226,#40227,#29533,.T.);
#52165=EDGE_CURVE('',#40227,#40223,#25368,.T.);
#52166=EDGE_CURVE('',#40228,#40229,#865,.T.);
#52167=EDGE_CURVE('',#40229,#40230,#25369,.T.);
#52168=EDGE_CURVE('',#40231,#40230,#29534,.T.);
#52169=EDGE_CURVE('',#40231,#40232,#25370,.T.);
#52170=EDGE_CURVE('',#40232,#40228,#29535,.T.);
#52171=EDGE_CURVE('',#40230,#40224,#25371,.T.);
#52172=EDGE_CURVE('',#40223,#40231,#21462,.T.);
#52173=EDGE_CURVE('',#40232,#40233,#25372,.T.);
#52174=EDGE_CURVE('',#40234,#40231,#866,.T.);
#52175=EDGE_CURVE('',#40233,#40234,#25373,.T.);
#52176=EDGE_CURVE('',#40234,#40223,#867,.T.);
#52177=EDGE_CURVE('',#40235,#40227,#25374,.T.);
#52178=EDGE_CURVE('',#40234,#40235,#25375,.T.);
#52179=EDGE_CURVE('',#39422,#40233,#21463,.T.);
#52180=EDGE_CURVE('',#40235,#40233,#21464,.T.);
#52181=EDGE_CURVE('',#39423,#40235,#21465,.T.);
#52182=EDGE_CURVE('',#39421,#40232,#21466,.T.);
#52183=EDGE_CURVE('',#40228,#39420,#21467,.T.);
#52184=EDGE_CURVE('',#40229,#39003,#21468,.T.);
#52185=EDGE_CURVE('',#40230,#39002,#21469,.T.);
#52186=EDGE_CURVE('',#40224,#39001,#21470,.T.);
#52187=EDGE_CURVE('',#40225,#39000,#21471,.T.);
#52188=EDGE_CURVE('',#39425,#40226,#21472,.T.);
#52189=EDGE_CURVE('',#39424,#40227,#21473,.T.);
#52190=EDGE_CURVE('',#40236,#40237,#29536,.T.);
#52191=EDGE_CURVE('',#40237,#40238,#25376,.T.);
#52192=EDGE_CURVE('',#40238,#40239,#868,.T.);
#52193=EDGE_CURVE('',#40239,#40240,#29537,.T.);
#52194=EDGE_CURVE('',#40240,#40236,#25377,.T.);
#52195=EDGE_CURVE('',#40241,#40242,#869,.T.);
#52196=EDGE_CURVE('',#40242,#40243,#25378,.T.);
#52197=EDGE_CURVE('',#40244,#40243,#29538,.T.);
#52198=EDGE_CURVE('',#40244,#40245,#25379,.T.);
#52199=EDGE_CURVE('',#40245,#40241,#29539,.T.);
#52200=EDGE_CURVE('',#40243,#40237,#25380,.T.);
#52201=EDGE_CURVE('',#40236,#40244,#21474,.T.);
#52202=EDGE_CURVE('',#40245,#40246,#25381,.T.);
#52203=EDGE_CURVE('',#40247,#40244,#870,.T.);
#52204=EDGE_CURVE('',#40246,#40247,#25382,.T.);
#52205=EDGE_CURVE('',#40247,#40236,#871,.T.);
#52206=EDGE_CURVE('',#40248,#40240,#25383,.T.);
#52207=EDGE_CURVE('',#40247,#40248,#25384,.T.);
#52208=EDGE_CURVE('',#39416,#40246,#21475,.T.);
#52209=EDGE_CURVE('',#40248,#40246,#21476,.T.);
#52210=EDGE_CURVE('',#39417,#40248,#21477,.T.);
#52211=EDGE_CURVE('',#39415,#40245,#21478,.T.);
#52212=EDGE_CURVE('',#40241,#39414,#21479,.T.);
#52213=EDGE_CURVE('',#40242,#39007,#21480,.T.);
#52214=EDGE_CURVE('',#40243,#39006,#21481,.T.);
#52215=EDGE_CURVE('',#40237,#39005,#21482,.T.);
#52216=EDGE_CURVE('',#40238,#39004,#21483,.T.);
#52217=EDGE_CURVE('',#39419,#40239,#21484,.T.);
#52218=EDGE_CURVE('',#39418,#40240,#21485,.T.);
#52219=EDGE_CURVE('',#40249,#40250,#29540,.T.);
#52220=EDGE_CURVE('',#40250,#40251,#25385,.T.);
#52221=EDGE_CURVE('',#40251,#40252,#872,.T.);
#52222=EDGE_CURVE('',#40252,#40253,#29541,.T.);
#52223=EDGE_CURVE('',#40253,#40249,#25386,.T.);
#52224=EDGE_CURVE('',#40254,#40255,#873,.T.);
#52225=EDGE_CURVE('',#40255,#40256,#25387,.T.);
#52226=EDGE_CURVE('',#40257,#40256,#29542,.T.);
#52227=EDGE_CURVE('',#40257,#40258,#25388,.T.);
#52228=EDGE_CURVE('',#40258,#40254,#29543,.T.);
#52229=EDGE_CURVE('',#40256,#40250,#25389,.T.);
#52230=EDGE_CURVE('',#40249,#40257,#21486,.T.);
#52231=EDGE_CURVE('',#40258,#40259,#25390,.T.);
#52232=EDGE_CURVE('',#40260,#40257,#874,.T.);
#52233=EDGE_CURVE('',#40259,#40260,#25391,.T.);
#52234=EDGE_CURVE('',#40260,#40249,#875,.T.);
#52235=EDGE_CURVE('',#40261,#40253,#25392,.T.);
#52236=EDGE_CURVE('',#40260,#40261,#25393,.T.);
#52237=EDGE_CURVE('',#39410,#40259,#21487,.T.);
#52238=EDGE_CURVE('',#40261,#40259,#21488,.T.);
#52239=EDGE_CURVE('',#39411,#40261,#21489,.T.);
#52240=EDGE_CURVE('',#39409,#40258,#21490,.T.);
#52241=EDGE_CURVE('',#40254,#39408,#21491,.T.);
#52242=EDGE_CURVE('',#40255,#39011,#21492,.T.);
#52243=EDGE_CURVE('',#40256,#39010,#21493,.T.);
#52244=EDGE_CURVE('',#40250,#39009,#21494,.T.);
#52245=EDGE_CURVE('',#40251,#39008,#21495,.T.);
#52246=EDGE_CURVE('',#39413,#40252,#21496,.T.);
#52247=EDGE_CURVE('',#39412,#40253,#21497,.T.);
#52248=EDGE_CURVE('',#40262,#40263,#29544,.T.);
#52249=EDGE_CURVE('',#40263,#40264,#25394,.T.);
#52250=EDGE_CURVE('',#40264,#40265,#876,.T.);
#52251=EDGE_CURVE('',#40265,#40266,#29545,.T.);
#52252=EDGE_CURVE('',#40266,#40262,#25395,.T.);
#52253=EDGE_CURVE('',#40267,#40268,#877,.T.);
#52254=EDGE_CURVE('',#40268,#40269,#25396,.T.);
#52255=EDGE_CURVE('',#40270,#40269,#29546,.T.);
#52256=EDGE_CURVE('',#40270,#40271,#25397,.T.);
#52257=EDGE_CURVE('',#40271,#40267,#29547,.T.);
#52258=EDGE_CURVE('',#40269,#40263,#25398,.T.);
#52259=EDGE_CURVE('',#40262,#40270,#21498,.T.);
#52260=EDGE_CURVE('',#40271,#40272,#25399,.T.);
#52261=EDGE_CURVE('',#40273,#40270,#878,.T.);
#52262=EDGE_CURVE('',#40272,#40273,#25400,.T.);
#52263=EDGE_CURVE('',#40273,#40262,#879,.T.);
#52264=EDGE_CURVE('',#40274,#40266,#25401,.T.);
#52265=EDGE_CURVE('',#40273,#40274,#25402,.T.);
#52266=EDGE_CURVE('',#39404,#40272,#21499,.T.);
#52267=EDGE_CURVE('',#40274,#40272,#21500,.T.);
#52268=EDGE_CURVE('',#39405,#40274,#21501,.T.);
#52269=EDGE_CURVE('',#39403,#40271,#21502,.T.);
#52270=EDGE_CURVE('',#40267,#39402,#21503,.T.);
#52271=EDGE_CURVE('',#40268,#39015,#21504,.T.);
#52272=EDGE_CURVE('',#40269,#39014,#21505,.T.);
#52273=EDGE_CURVE('',#40263,#39013,#21506,.T.);
#52274=EDGE_CURVE('',#40264,#39012,#21507,.T.);
#52275=EDGE_CURVE('',#39407,#40265,#21508,.T.);
#52276=EDGE_CURVE('',#39406,#40266,#21509,.T.);
#52277=EDGE_CURVE('',#40275,#40276,#29548,.T.);
#52278=EDGE_CURVE('',#40276,#40277,#25403,.T.);
#52279=EDGE_CURVE('',#40277,#40278,#880,.T.);
#52280=EDGE_CURVE('',#40278,#40279,#29549,.T.);
#52281=EDGE_CURVE('',#40279,#40275,#25404,.T.);
#52282=EDGE_CURVE('',#40280,#40281,#881,.T.);
#52283=EDGE_CURVE('',#40281,#40282,#25405,.T.);
#52284=EDGE_CURVE('',#40283,#40282,#29550,.T.);
#52285=EDGE_CURVE('',#40283,#40284,#25406,.T.);
#52286=EDGE_CURVE('',#40284,#40280,#29551,.T.);
#52287=EDGE_CURVE('',#40282,#40276,#25407,.T.);
#52288=EDGE_CURVE('',#40275,#40283,#21510,.T.);
#52289=EDGE_CURVE('',#40284,#40285,#25408,.T.);
#52290=EDGE_CURVE('',#40286,#40283,#882,.T.);
#52291=EDGE_CURVE('',#40285,#40286,#25409,.T.);
#52292=EDGE_CURVE('',#40286,#40275,#883,.T.);
#52293=EDGE_CURVE('',#40287,#40279,#25410,.T.);
#52294=EDGE_CURVE('',#40286,#40287,#25411,.T.);
#52295=EDGE_CURVE('',#39398,#40285,#21511,.T.);
#52296=EDGE_CURVE('',#40287,#40285,#21512,.T.);
#52297=EDGE_CURVE('',#39399,#40287,#21513,.T.);
#52298=EDGE_CURVE('',#39397,#40284,#21514,.T.);
#52299=EDGE_CURVE('',#40280,#39396,#21515,.T.);
#52300=EDGE_CURVE('',#40281,#39019,#21516,.T.);
#52301=EDGE_CURVE('',#40282,#39018,#21517,.T.);
#52302=EDGE_CURVE('',#40276,#39017,#21518,.T.);
#52303=EDGE_CURVE('',#40277,#39016,#21519,.T.);
#52304=EDGE_CURVE('',#39401,#40278,#21520,.T.);
#52305=EDGE_CURVE('',#39400,#40279,#21521,.T.);
#52306=EDGE_CURVE('',#40288,#40289,#29552,.T.);
#52307=EDGE_CURVE('',#40289,#40290,#25412,.T.);
#52308=EDGE_CURVE('',#40290,#40291,#884,.T.);
#52309=EDGE_CURVE('',#40291,#40292,#29553,.T.);
#52310=EDGE_CURVE('',#40292,#40288,#25413,.T.);
#52311=EDGE_CURVE('',#40293,#40294,#885,.T.);
#52312=EDGE_CURVE('',#40294,#40295,#25414,.T.);
#52313=EDGE_CURVE('',#40296,#40295,#29554,.T.);
#52314=EDGE_CURVE('',#40296,#40297,#25415,.T.);
#52315=EDGE_CURVE('',#40297,#40293,#29555,.T.);
#52316=EDGE_CURVE('',#40295,#40289,#25416,.T.);
#52317=EDGE_CURVE('',#40288,#40296,#21522,.T.);
#52318=EDGE_CURVE('',#40297,#40298,#25417,.T.);
#52319=EDGE_CURVE('',#40299,#40296,#886,.T.);
#52320=EDGE_CURVE('',#40298,#40299,#25418,.T.);
#52321=EDGE_CURVE('',#40299,#40288,#887,.T.);
#52322=EDGE_CURVE('',#40300,#40292,#25419,.T.);
#52323=EDGE_CURVE('',#40299,#40300,#25420,.T.);
#52324=EDGE_CURVE('',#39392,#40298,#21523,.T.);
#52325=EDGE_CURVE('',#40300,#40298,#21524,.T.);
#52326=EDGE_CURVE('',#39393,#40300,#21525,.T.);
#52327=EDGE_CURVE('',#39391,#40297,#21526,.T.);
#52328=EDGE_CURVE('',#40293,#39390,#21527,.T.);
#52329=EDGE_CURVE('',#40294,#39023,#21528,.T.);
#52330=EDGE_CURVE('',#40295,#39022,#21529,.T.);
#52331=EDGE_CURVE('',#40289,#39021,#21530,.T.);
#52332=EDGE_CURVE('',#40290,#39020,#21531,.T.);
#52333=EDGE_CURVE('',#39395,#40291,#21532,.T.);
#52334=EDGE_CURVE('',#39394,#40292,#21533,.T.);
#52335=EDGE_CURVE('',#40301,#40302,#29556,.T.);
#52336=EDGE_CURVE('',#40302,#40303,#25421,.T.);
#52337=EDGE_CURVE('',#40303,#40304,#888,.T.);
#52338=EDGE_CURVE('',#40304,#40305,#29557,.T.);
#52339=EDGE_CURVE('',#40305,#40301,#25422,.T.);
#52340=EDGE_CURVE('',#40306,#40307,#889,.T.);
#52341=EDGE_CURVE('',#40307,#40308,#25423,.T.);
#52342=EDGE_CURVE('',#40309,#40308,#29558,.T.);
#52343=EDGE_CURVE('',#40309,#40310,#25424,.T.);
#52344=EDGE_CURVE('',#40310,#40306,#29559,.T.);
#52345=EDGE_CURVE('',#40308,#40302,#25425,.T.);
#52346=EDGE_CURVE('',#40301,#40309,#21534,.T.);
#52347=EDGE_CURVE('',#40310,#40311,#25426,.T.);
#52348=EDGE_CURVE('',#40312,#40309,#890,.T.);
#52349=EDGE_CURVE('',#40311,#40312,#25427,.T.);
#52350=EDGE_CURVE('',#40312,#40301,#891,.T.);
#52351=EDGE_CURVE('',#40313,#40305,#25428,.T.);
#52352=EDGE_CURVE('',#40312,#40313,#25429,.T.);
#52353=EDGE_CURVE('',#39386,#40311,#21535,.T.);
#52354=EDGE_CURVE('',#40313,#40311,#21536,.T.);
#52355=EDGE_CURVE('',#39387,#40313,#21537,.T.);
#52356=EDGE_CURVE('',#39385,#40310,#21538,.T.);
#52357=EDGE_CURVE('',#40306,#39384,#21539,.T.);
#52358=EDGE_CURVE('',#40307,#39027,#21540,.T.);
#52359=EDGE_CURVE('',#40308,#39026,#21541,.T.);
#52360=EDGE_CURVE('',#40302,#39025,#21542,.T.);
#52361=EDGE_CURVE('',#40303,#39024,#21543,.T.);
#52362=EDGE_CURVE('',#39389,#40304,#21544,.T.);
#52363=EDGE_CURVE('',#39388,#40305,#21545,.T.);
#52364=EDGE_CURVE('',#40314,#40315,#29560,.T.);
#52365=EDGE_CURVE('',#40315,#40316,#25430,.T.);
#52366=EDGE_CURVE('',#40316,#40317,#892,.T.);
#52367=EDGE_CURVE('',#40317,#40318,#29561,.T.);
#52368=EDGE_CURVE('',#40318,#40314,#25431,.T.);
#52369=EDGE_CURVE('',#40319,#40320,#893,.T.);
#52370=EDGE_CURVE('',#40320,#40321,#25432,.T.);
#52371=EDGE_CURVE('',#40322,#40321,#29562,.T.);
#52372=EDGE_CURVE('',#40322,#40323,#25433,.T.);
#52373=EDGE_CURVE('',#40323,#40319,#29563,.T.);
#52374=EDGE_CURVE('',#40321,#40315,#25434,.T.);
#52375=EDGE_CURVE('',#40314,#40322,#21546,.T.);
#52376=EDGE_CURVE('',#40323,#40324,#25435,.T.);
#52377=EDGE_CURVE('',#40325,#40322,#894,.T.);
#52378=EDGE_CURVE('',#40324,#40325,#25436,.T.);
#52379=EDGE_CURVE('',#40325,#40314,#895,.T.);
#52380=EDGE_CURVE('',#40326,#40318,#25437,.T.);
#52381=EDGE_CURVE('',#40325,#40326,#25438,.T.);
#52382=EDGE_CURVE('',#39380,#40324,#21547,.T.);
#52383=EDGE_CURVE('',#40326,#40324,#21548,.T.);
#52384=EDGE_CURVE('',#39381,#40326,#21549,.T.);
#52385=EDGE_CURVE('',#39379,#40323,#21550,.T.);
#52386=EDGE_CURVE('',#40319,#39378,#21551,.T.);
#52387=EDGE_CURVE('',#40320,#39031,#21552,.T.);
#52388=EDGE_CURVE('',#40321,#39030,#21553,.T.);
#52389=EDGE_CURVE('',#40315,#39029,#21554,.T.);
#52390=EDGE_CURVE('',#40316,#39028,#21555,.T.);
#52391=EDGE_CURVE('',#39383,#40317,#21556,.T.);
#52392=EDGE_CURVE('',#39382,#40318,#21557,.T.);
#52393=EDGE_CURVE('',#40327,#40328,#29564,.T.);
#52394=EDGE_CURVE('',#40328,#40329,#25439,.T.);
#52395=EDGE_CURVE('',#40329,#40330,#896,.T.);
#52396=EDGE_CURVE('',#40330,#40331,#29565,.T.);
#52397=EDGE_CURVE('',#40331,#40327,#25440,.T.);
#52398=EDGE_CURVE('',#40332,#40333,#897,.T.);
#52399=EDGE_CURVE('',#40333,#40334,#25441,.T.);
#52400=EDGE_CURVE('',#40335,#40334,#29566,.T.);
#52401=EDGE_CURVE('',#40335,#40336,#25442,.T.);
#52402=EDGE_CURVE('',#40336,#40332,#29567,.T.);
#52403=EDGE_CURVE('',#40334,#40328,#25443,.T.);
#52404=EDGE_CURVE('',#40327,#40335,#21558,.T.);
#52405=EDGE_CURVE('',#40336,#40337,#25444,.T.);
#52406=EDGE_CURVE('',#40338,#40335,#898,.T.);
#52407=EDGE_CURVE('',#40337,#40338,#25445,.T.);
#52408=EDGE_CURVE('',#40338,#40327,#899,.T.);
#52409=EDGE_CURVE('',#40339,#40331,#25446,.T.);
#52410=EDGE_CURVE('',#40338,#40339,#25447,.T.);
#52411=EDGE_CURVE('',#39374,#40337,#21559,.T.);
#52412=EDGE_CURVE('',#40339,#40337,#21560,.T.);
#52413=EDGE_CURVE('',#39375,#40339,#21561,.T.);
#52414=EDGE_CURVE('',#39373,#40336,#21562,.T.);
#52415=EDGE_CURVE('',#40332,#39372,#21563,.T.);
#52416=EDGE_CURVE('',#40333,#39035,#21564,.T.);
#52417=EDGE_CURVE('',#40334,#39034,#21565,.T.);
#52418=EDGE_CURVE('',#40328,#39033,#21566,.T.);
#52419=EDGE_CURVE('',#40329,#39032,#21567,.T.);
#52420=EDGE_CURVE('',#39377,#40330,#21568,.T.);
#52421=EDGE_CURVE('',#39376,#40331,#21569,.T.);
#52422=EDGE_CURVE('',#40340,#40341,#29568,.T.);
#52423=EDGE_CURVE('',#40341,#40342,#25448,.T.);
#52424=EDGE_CURVE('',#40342,#40343,#900,.T.);
#52425=EDGE_CURVE('',#40343,#40344,#29569,.T.);
#52426=EDGE_CURVE('',#40344,#40340,#25449,.T.);
#52427=EDGE_CURVE('',#40345,#40346,#901,.T.);
#52428=EDGE_CURVE('',#40346,#40347,#25450,.T.);
#52429=EDGE_CURVE('',#40348,#40347,#29570,.T.);
#52430=EDGE_CURVE('',#40348,#40349,#25451,.T.);
#52431=EDGE_CURVE('',#40349,#40345,#29571,.T.);
#52432=EDGE_CURVE('',#40347,#40341,#25452,.T.);
#52433=EDGE_CURVE('',#40340,#40348,#21570,.T.);
#52434=EDGE_CURVE('',#40349,#40350,#25453,.T.);
#52435=EDGE_CURVE('',#40351,#40348,#902,.T.);
#52436=EDGE_CURVE('',#40350,#40351,#25454,.T.);
#52437=EDGE_CURVE('',#40351,#40340,#903,.T.);
#52438=EDGE_CURVE('',#40352,#40344,#25455,.T.);
#52439=EDGE_CURVE('',#40351,#40352,#25456,.T.);
#52440=EDGE_CURVE('',#39368,#40350,#21571,.T.);
#52441=EDGE_CURVE('',#40352,#40350,#21572,.T.);
#52442=EDGE_CURVE('',#39369,#40352,#21573,.T.);
#52443=EDGE_CURVE('',#39367,#40349,#21574,.T.);
#52444=EDGE_CURVE('',#40345,#39366,#21575,.T.);
#52445=EDGE_CURVE('',#40346,#39039,#21576,.T.);
#52446=EDGE_CURVE('',#40347,#39038,#21577,.T.);
#52447=EDGE_CURVE('',#40341,#39037,#21578,.T.);
#52448=EDGE_CURVE('',#40342,#39036,#21579,.T.);
#52449=EDGE_CURVE('',#39371,#40343,#21580,.T.);
#52450=EDGE_CURVE('',#39370,#40344,#21581,.T.);
#52451=EDGE_CURVE('',#40353,#40354,#29572,.T.);
#52452=EDGE_CURVE('',#40354,#40355,#25457,.T.);
#52453=EDGE_CURVE('',#40355,#40356,#904,.T.);
#52454=EDGE_CURVE('',#40356,#40357,#29573,.T.);
#52455=EDGE_CURVE('',#40357,#40353,#25458,.T.);
#52456=EDGE_CURVE('',#40358,#40359,#905,.T.);
#52457=EDGE_CURVE('',#40359,#40360,#25459,.T.);
#52458=EDGE_CURVE('',#40361,#40360,#29574,.T.);
#52459=EDGE_CURVE('',#40361,#40362,#25460,.T.);
#52460=EDGE_CURVE('',#40362,#40358,#29575,.T.);
#52461=EDGE_CURVE('',#40360,#40354,#25461,.T.);
#52462=EDGE_CURVE('',#40353,#40361,#21582,.T.);
#52463=EDGE_CURVE('',#40362,#40363,#25462,.T.);
#52464=EDGE_CURVE('',#40364,#40361,#906,.T.);
#52465=EDGE_CURVE('',#40363,#40364,#25463,.T.);
#52466=EDGE_CURVE('',#40364,#40353,#907,.T.);
#52467=EDGE_CURVE('',#40365,#40357,#25464,.T.);
#52468=EDGE_CURVE('',#40364,#40365,#25465,.T.);
#52469=EDGE_CURVE('',#39362,#40363,#21583,.T.);
#52470=EDGE_CURVE('',#40365,#40363,#21584,.T.);
#52471=EDGE_CURVE('',#39363,#40365,#21585,.T.);
#52472=EDGE_CURVE('',#39361,#40362,#21586,.T.);
#52473=EDGE_CURVE('',#40358,#39360,#21587,.T.);
#52474=EDGE_CURVE('',#40359,#39043,#21588,.T.);
#52475=EDGE_CURVE('',#40360,#39042,#21589,.T.);
#52476=EDGE_CURVE('',#40354,#39041,#21590,.T.);
#52477=EDGE_CURVE('',#40355,#39040,#21591,.T.);
#52478=EDGE_CURVE('',#39365,#40356,#21592,.T.);
#52479=EDGE_CURVE('',#39364,#40357,#21593,.T.);
#52480=EDGE_CURVE('',#40366,#40367,#29576,.T.);
#52481=EDGE_CURVE('',#40367,#40368,#25466,.T.);
#52482=EDGE_CURVE('',#40368,#40369,#908,.T.);
#52483=EDGE_CURVE('',#40369,#40370,#29577,.T.);
#52484=EDGE_CURVE('',#40370,#40366,#25467,.T.);
#52485=EDGE_CURVE('',#40371,#40372,#909,.T.);
#52486=EDGE_CURVE('',#40372,#40373,#25468,.T.);
#52487=EDGE_CURVE('',#40374,#40373,#29578,.T.);
#52488=EDGE_CURVE('',#40374,#40375,#25469,.T.);
#52489=EDGE_CURVE('',#40375,#40371,#29579,.T.);
#52490=EDGE_CURVE('',#40373,#40367,#25470,.T.);
#52491=EDGE_CURVE('',#40366,#40374,#21594,.T.);
#52492=EDGE_CURVE('',#40375,#40376,#25471,.T.);
#52493=EDGE_CURVE('',#40377,#40374,#910,.T.);
#52494=EDGE_CURVE('',#40376,#40377,#25472,.T.);
#52495=EDGE_CURVE('',#40377,#40366,#911,.T.);
#52496=EDGE_CURVE('',#40378,#40370,#25473,.T.);
#52497=EDGE_CURVE('',#40377,#40378,#25474,.T.);
#52498=EDGE_CURVE('',#39356,#40376,#21595,.T.);
#52499=EDGE_CURVE('',#40378,#40376,#21596,.T.);
#52500=EDGE_CURVE('',#39357,#40378,#21597,.T.);
#52501=EDGE_CURVE('',#39355,#40375,#21598,.T.);
#52502=EDGE_CURVE('',#40371,#39354,#21599,.T.);
#52503=EDGE_CURVE('',#40372,#39047,#21600,.T.);
#52504=EDGE_CURVE('',#40373,#39046,#21601,.T.);
#52505=EDGE_CURVE('',#40367,#39045,#21602,.T.);
#52506=EDGE_CURVE('',#40368,#39044,#21603,.T.);
#52507=EDGE_CURVE('',#39359,#40369,#21604,.T.);
#52508=EDGE_CURVE('',#39358,#40370,#21605,.T.);
#52509=EDGE_CURVE('',#40379,#40380,#29580,.T.);
#52510=EDGE_CURVE('',#40380,#40381,#25475,.T.);
#52511=EDGE_CURVE('',#40381,#40382,#912,.T.);
#52512=EDGE_CURVE('',#40382,#40383,#29581,.T.);
#52513=EDGE_CURVE('',#40383,#40379,#25476,.T.);
#52514=EDGE_CURVE('',#40384,#40385,#913,.T.);
#52515=EDGE_CURVE('',#40385,#40386,#25477,.T.);
#52516=EDGE_CURVE('',#40387,#40386,#29582,.T.);
#52517=EDGE_CURVE('',#40387,#40388,#25478,.T.);
#52518=EDGE_CURVE('',#40388,#40384,#29583,.T.);
#52519=EDGE_CURVE('',#40386,#40380,#25479,.T.);
#52520=EDGE_CURVE('',#40379,#40387,#21606,.T.);
#52521=EDGE_CURVE('',#40388,#40389,#25480,.T.);
#52522=EDGE_CURVE('',#40390,#40387,#914,.T.);
#52523=EDGE_CURVE('',#40389,#40390,#25481,.T.);
#52524=EDGE_CURVE('',#40390,#40379,#915,.T.);
#52525=EDGE_CURVE('',#40391,#40383,#25482,.T.);
#52526=EDGE_CURVE('',#40390,#40391,#25483,.T.);
#52527=EDGE_CURVE('',#39350,#40389,#21607,.T.);
#52528=EDGE_CURVE('',#40391,#40389,#21608,.T.);
#52529=EDGE_CURVE('',#39351,#40391,#21609,.T.);
#52530=EDGE_CURVE('',#39349,#40388,#21610,.T.);
#52531=EDGE_CURVE('',#40384,#39348,#21611,.T.);
#52532=EDGE_CURVE('',#40385,#38656,#21612,.T.);
#52533=EDGE_CURVE('',#40386,#39050,#21613,.T.);
#52534=EDGE_CURVE('',#40380,#39049,#21614,.T.);
#52535=EDGE_CURVE('',#40381,#39048,#21615,.T.);
#52536=EDGE_CURVE('',#39353,#40382,#21616,.T.);
#52537=EDGE_CURVE('',#39352,#40383,#21617,.T.);
#52538=EDGE_CURVE('',#40392,#40393,#29584,.T.);
#52539=EDGE_CURVE('',#40393,#40394,#25484,.T.);
#52540=EDGE_CURVE('',#40394,#40395,#916,.T.);
#52541=EDGE_CURVE('',#40395,#40396,#29585,.T.);
#52542=EDGE_CURVE('',#40396,#40392,#25485,.T.);
#52543=EDGE_CURVE('',#40397,#40398,#917,.T.);
#52544=EDGE_CURVE('',#40398,#40399,#25486,.T.);
#52545=EDGE_CURVE('',#40400,#40399,#29586,.T.);
#52546=EDGE_CURVE('',#40400,#40401,#25487,.T.);
#52547=EDGE_CURVE('',#40401,#40397,#29587,.T.);
#52548=EDGE_CURVE('',#40399,#40393,#25488,.T.);
#52549=EDGE_CURVE('',#40392,#40400,#21618,.T.);
#52550=EDGE_CURVE('',#40401,#40402,#25489,.T.);
#52551=EDGE_CURVE('',#40403,#40400,#918,.T.);
#52552=EDGE_CURVE('',#40402,#40403,#25490,.T.);
#52553=EDGE_CURVE('',#40403,#40392,#919,.T.);
#52554=EDGE_CURVE('',#40404,#40396,#25491,.T.);
#52555=EDGE_CURVE('',#40403,#40404,#25492,.T.);
#52556=EDGE_CURVE('',#39343,#40402,#21619,.T.);
#52557=EDGE_CURVE('',#40404,#40402,#21620,.T.);
#52558=EDGE_CURVE('',#39344,#40404,#21621,.T.);
#52559=EDGE_CURVE('',#39342,#40401,#21622,.T.);
#52560=EDGE_CURVE('',#40397,#39341,#21623,.T.);
#52561=EDGE_CURVE('',#40398,#38660,#21624,.T.);
#52562=EDGE_CURVE('',#40399,#38659,#21625,.T.);
#52563=EDGE_CURVE('',#40393,#38658,#21626,.T.);
#52564=EDGE_CURVE('',#40394,#38657,#21627,.T.);
#52565=EDGE_CURVE('',#39346,#40395,#21628,.T.);
#52566=EDGE_CURVE('',#39345,#40396,#21629,.T.);
#52567=EDGE_CURVE('',#40405,#40406,#29588,.T.);
#52568=EDGE_CURVE('',#40406,#40407,#25493,.T.);
#52569=EDGE_CURVE('',#40407,#40408,#920,.T.);
#52570=EDGE_CURVE('',#40408,#40409,#29589,.T.);
#52571=EDGE_CURVE('',#40409,#40405,#25494,.T.);
#52572=EDGE_CURVE('',#40410,#40411,#921,.T.);
#52573=EDGE_CURVE('',#40411,#40412,#25495,.T.);
#52574=EDGE_CURVE('',#40413,#40412,#29590,.T.);
#52575=EDGE_CURVE('',#40413,#40414,#25496,.T.);
#52576=EDGE_CURVE('',#40414,#40410,#29591,.T.);
#52577=EDGE_CURVE('',#40412,#40406,#25497,.T.);
#52578=EDGE_CURVE('',#40405,#40413,#21630,.T.);
#52579=EDGE_CURVE('',#40414,#40415,#25498,.T.);
#52580=EDGE_CURVE('',#40416,#40413,#922,.T.);
#52581=EDGE_CURVE('',#40415,#40416,#25499,.T.);
#52582=EDGE_CURVE('',#40416,#40405,#923,.T.);
#52583=EDGE_CURVE('',#40417,#40409,#25500,.T.);
#52584=EDGE_CURVE('',#40416,#40417,#25501,.T.);
#52585=EDGE_CURVE('',#39337,#40415,#21631,.T.);
#52586=EDGE_CURVE('',#40417,#40415,#21632,.T.);
#52587=EDGE_CURVE('',#39338,#40417,#21633,.T.);
#52588=EDGE_CURVE('',#39336,#40414,#21634,.T.);
#52589=EDGE_CURVE('',#40410,#39335,#21635,.T.);
#52590=EDGE_CURVE('',#40411,#38664,#21636,.T.);
#52591=EDGE_CURVE('',#40412,#38663,#21637,.T.);
#52592=EDGE_CURVE('',#40406,#38662,#21638,.T.);
#52593=EDGE_CURVE('',#40407,#38661,#21639,.T.);
#52594=EDGE_CURVE('',#39340,#40408,#21640,.T.);
#52595=EDGE_CURVE('',#39339,#40409,#21641,.T.);
#52596=EDGE_CURVE('',#40418,#40419,#29592,.T.);
#52597=EDGE_CURVE('',#40419,#40420,#25502,.T.);
#52598=EDGE_CURVE('',#40420,#40421,#924,.T.);
#52599=EDGE_CURVE('',#40421,#40422,#29593,.T.);
#52600=EDGE_CURVE('',#40422,#40418,#25503,.T.);
#52601=EDGE_CURVE('',#40423,#40424,#925,.T.);
#52602=EDGE_CURVE('',#40424,#40425,#25504,.T.);
#52603=EDGE_CURVE('',#40426,#40425,#29594,.T.);
#52604=EDGE_CURVE('',#40426,#40427,#25505,.T.);
#52605=EDGE_CURVE('',#40427,#40423,#29595,.T.);
#52606=EDGE_CURVE('',#40425,#40419,#25506,.T.);
#52607=EDGE_CURVE('',#40418,#40426,#21642,.T.);
#52608=EDGE_CURVE('',#40427,#40428,#25507,.T.);
#52609=EDGE_CURVE('',#40429,#40426,#926,.T.);
#52610=EDGE_CURVE('',#40428,#40429,#25508,.T.);
#52611=EDGE_CURVE('',#40429,#40418,#927,.T.);
#52612=EDGE_CURVE('',#40430,#40422,#25509,.T.);
#52613=EDGE_CURVE('',#40429,#40430,#25510,.T.);
#52614=EDGE_CURVE('',#39331,#40428,#21643,.T.);
#52615=EDGE_CURVE('',#40430,#40428,#21644,.T.);
#52616=EDGE_CURVE('',#39332,#40430,#21645,.T.);
#52617=EDGE_CURVE('',#39330,#40427,#21646,.T.);
#52618=EDGE_CURVE('',#40423,#39329,#21647,.T.);
#52619=EDGE_CURVE('',#40424,#38668,#21648,.T.);
#52620=EDGE_CURVE('',#40425,#38667,#21649,.T.);
#52621=EDGE_CURVE('',#40419,#38666,#21650,.T.);
#52622=EDGE_CURVE('',#40420,#38665,#21651,.T.);
#52623=EDGE_CURVE('',#39334,#40421,#21652,.T.);
#52624=EDGE_CURVE('',#39333,#40422,#21653,.T.);
#52625=EDGE_CURVE('',#40431,#40432,#29596,.T.);
#52626=EDGE_CURVE('',#40432,#40433,#25511,.T.);
#52627=EDGE_CURVE('',#40433,#40434,#928,.T.);
#52628=EDGE_CURVE('',#40434,#40435,#29597,.T.);
#52629=EDGE_CURVE('',#40435,#40431,#25512,.T.);
#52630=EDGE_CURVE('',#40436,#40437,#929,.T.);
#52631=EDGE_CURVE('',#40437,#40438,#25513,.T.);
#52632=EDGE_CURVE('',#40439,#40438,#29598,.T.);
#52633=EDGE_CURVE('',#40439,#40440,#25514,.T.);
#52634=EDGE_CURVE('',#40440,#40436,#29599,.T.);
#52635=EDGE_CURVE('',#40438,#40432,#25515,.T.);
#52636=EDGE_CURVE('',#40431,#40439,#21654,.T.);
#52637=EDGE_CURVE('',#40440,#40441,#25516,.T.);
#52638=EDGE_CURVE('',#40442,#40439,#930,.T.);
#52639=EDGE_CURVE('',#40441,#40442,#25517,.T.);
#52640=EDGE_CURVE('',#40442,#40431,#931,.T.);
#52641=EDGE_CURVE('',#40443,#40435,#25518,.T.);
#52642=EDGE_CURVE('',#40442,#40443,#25519,.T.);
#52643=EDGE_CURVE('',#39325,#40441,#21655,.T.);
#52644=EDGE_CURVE('',#40443,#40441,#21656,.T.);
#52645=EDGE_CURVE('',#39326,#40443,#21657,.T.);
#52646=EDGE_CURVE('',#39324,#40440,#21658,.T.);
#52647=EDGE_CURVE('',#40436,#39323,#21659,.T.);
#52648=EDGE_CURVE('',#40437,#38672,#21660,.T.);
#52649=EDGE_CURVE('',#40438,#38671,#21661,.T.);
#52650=EDGE_CURVE('',#40432,#38670,#21662,.T.);
#52651=EDGE_CURVE('',#40433,#38669,#21663,.T.);
#52652=EDGE_CURVE('',#39328,#40434,#21664,.T.);
#52653=EDGE_CURVE('',#39327,#40435,#21665,.T.);
#52654=EDGE_CURVE('',#40444,#40445,#29600,.T.);
#52655=EDGE_CURVE('',#40445,#40446,#25520,.T.);
#52656=EDGE_CURVE('',#40446,#40447,#932,.T.);
#52657=EDGE_CURVE('',#40447,#40448,#29601,.T.);
#52658=EDGE_CURVE('',#40448,#40444,#25521,.T.);
#52659=EDGE_CURVE('',#40449,#40450,#933,.T.);
#52660=EDGE_CURVE('',#40450,#40451,#25522,.T.);
#52661=EDGE_CURVE('',#40452,#40451,#29602,.T.);
#52662=EDGE_CURVE('',#40452,#40453,#25523,.T.);
#52663=EDGE_CURVE('',#40453,#40449,#29603,.T.);
#52664=EDGE_CURVE('',#40451,#40445,#25524,.T.);
#52665=EDGE_CURVE('',#40444,#40452,#21666,.T.);
#52666=EDGE_CURVE('',#40453,#40454,#25525,.T.);
#52667=EDGE_CURVE('',#40455,#40452,#934,.T.);
#52668=EDGE_CURVE('',#40454,#40455,#25526,.T.);
#52669=EDGE_CURVE('',#40455,#40444,#935,.T.);
#52670=EDGE_CURVE('',#40456,#40448,#25527,.T.);
#52671=EDGE_CURVE('',#40455,#40456,#25528,.T.);
#52672=EDGE_CURVE('',#39319,#40454,#21667,.T.);
#52673=EDGE_CURVE('',#40456,#40454,#21668,.T.);
#52674=EDGE_CURVE('',#39320,#40456,#21669,.T.);
#52675=EDGE_CURVE('',#39318,#40453,#21670,.T.);
#52676=EDGE_CURVE('',#40449,#39317,#21671,.T.);
#52677=EDGE_CURVE('',#40450,#38676,#21672,.T.);
#52678=EDGE_CURVE('',#40451,#38675,#21673,.T.);
#52679=EDGE_CURVE('',#40445,#38674,#21674,.T.);
#52680=EDGE_CURVE('',#40446,#38673,#21675,.T.);
#52681=EDGE_CURVE('',#39322,#40447,#21676,.T.);
#52682=EDGE_CURVE('',#39321,#40448,#21677,.T.);
#52683=EDGE_CURVE('',#40457,#40458,#29604,.T.);
#52684=EDGE_CURVE('',#40458,#40459,#25529,.T.);
#52685=EDGE_CURVE('',#40459,#40460,#936,.T.);
#52686=EDGE_CURVE('',#40460,#40461,#29605,.T.);
#52687=EDGE_CURVE('',#40461,#40457,#25530,.T.);
#52688=EDGE_CURVE('',#40462,#40463,#937,.T.);
#52689=EDGE_CURVE('',#40463,#40464,#25531,.T.);
#52690=EDGE_CURVE('',#40465,#40464,#29606,.T.);
#52691=EDGE_CURVE('',#40465,#40466,#25532,.T.);
#52692=EDGE_CURVE('',#40466,#40462,#29607,.T.);
#52693=EDGE_CURVE('',#40464,#40458,#25533,.T.);
#52694=EDGE_CURVE('',#40457,#40465,#21678,.T.);
#52695=EDGE_CURVE('',#40466,#40467,#25534,.T.);
#52696=EDGE_CURVE('',#40468,#40465,#938,.T.);
#52697=EDGE_CURVE('',#40467,#40468,#25535,.T.);
#52698=EDGE_CURVE('',#40468,#40457,#939,.T.);
#52699=EDGE_CURVE('',#40469,#40461,#25536,.T.);
#52700=EDGE_CURVE('',#40468,#40469,#25537,.T.);
#52701=EDGE_CURVE('',#39313,#40467,#21679,.T.);
#52702=EDGE_CURVE('',#40469,#40467,#21680,.T.);
#52703=EDGE_CURVE('',#39314,#40469,#21681,.T.);
#52704=EDGE_CURVE('',#39312,#40466,#21682,.T.);
#52705=EDGE_CURVE('',#40462,#39311,#21683,.T.);
#52706=EDGE_CURVE('',#40463,#38680,#21684,.T.);
#52707=EDGE_CURVE('',#40464,#38679,#21685,.T.);
#52708=EDGE_CURVE('',#40458,#38678,#21686,.T.);
#52709=EDGE_CURVE('',#40459,#38677,#21687,.T.);
#52710=EDGE_CURVE('',#39316,#40460,#21688,.T.);
#52711=EDGE_CURVE('',#39315,#40461,#21689,.T.);
#52712=EDGE_CURVE('',#40470,#40471,#29608,.T.);
#52713=EDGE_CURVE('',#40471,#40472,#25538,.T.);
#52714=EDGE_CURVE('',#40472,#40473,#940,.T.);
#52715=EDGE_CURVE('',#40473,#40474,#29609,.T.);
#52716=EDGE_CURVE('',#40474,#40470,#25539,.T.);
#52717=EDGE_CURVE('',#40475,#40476,#941,.T.);
#52718=EDGE_CURVE('',#40476,#40477,#25540,.T.);
#52719=EDGE_CURVE('',#40478,#40477,#29610,.T.);
#52720=EDGE_CURVE('',#40478,#40479,#25541,.T.);
#52721=EDGE_CURVE('',#40479,#40475,#29611,.T.);
#52722=EDGE_CURVE('',#40477,#40471,#25542,.T.);
#52723=EDGE_CURVE('',#40470,#40478,#21690,.T.);
#52724=EDGE_CURVE('',#40479,#40480,#25543,.T.);
#52725=EDGE_CURVE('',#40481,#40478,#942,.T.);
#52726=EDGE_CURVE('',#40480,#40481,#25544,.T.);
#52727=EDGE_CURVE('',#40481,#40470,#943,.T.);
#52728=EDGE_CURVE('',#40482,#40474,#25545,.T.);
#52729=EDGE_CURVE('',#40481,#40482,#25546,.T.);
#52730=EDGE_CURVE('',#39307,#40480,#21691,.T.);
#52731=EDGE_CURVE('',#40482,#40480,#21692,.T.);
#52732=EDGE_CURVE('',#39308,#40482,#21693,.T.);
#52733=EDGE_CURVE('',#39306,#40479,#21694,.T.);
#52734=EDGE_CURVE('',#40475,#39305,#21695,.T.);
#52735=EDGE_CURVE('',#40476,#38684,#21696,.T.);
#52736=EDGE_CURVE('',#40477,#38683,#21697,.T.);
#52737=EDGE_CURVE('',#40471,#38682,#21698,.T.);
#52738=EDGE_CURVE('',#40472,#38681,#21699,.T.);
#52739=EDGE_CURVE('',#39310,#40473,#21700,.T.);
#52740=EDGE_CURVE('',#39309,#40474,#21701,.T.);
#52741=EDGE_CURVE('',#40483,#40484,#29612,.T.);
#52742=EDGE_CURVE('',#40484,#40485,#25547,.T.);
#52743=EDGE_CURVE('',#40485,#40486,#944,.T.);
#52744=EDGE_CURVE('',#40486,#40487,#29613,.T.);
#52745=EDGE_CURVE('',#40487,#40483,#25548,.T.);
#52746=EDGE_CURVE('',#40488,#40489,#945,.T.);
#52747=EDGE_CURVE('',#40489,#40490,#25549,.T.);
#52748=EDGE_CURVE('',#40491,#40490,#29614,.T.);
#52749=EDGE_CURVE('',#40491,#40492,#25550,.T.);
#52750=EDGE_CURVE('',#40492,#40488,#29615,.T.);
#52751=EDGE_CURVE('',#40490,#40484,#25551,.T.);
#52752=EDGE_CURVE('',#40483,#40491,#21702,.T.);
#52753=EDGE_CURVE('',#40492,#40493,#25552,.T.);
#52754=EDGE_CURVE('',#40494,#40491,#946,.T.);
#52755=EDGE_CURVE('',#40493,#40494,#25553,.T.);
#52756=EDGE_CURVE('',#40494,#40483,#947,.T.);
#52757=EDGE_CURVE('',#40495,#40487,#25554,.T.);
#52758=EDGE_CURVE('',#40494,#40495,#25555,.T.);
#52759=EDGE_CURVE('',#39301,#40493,#21703,.T.);
#52760=EDGE_CURVE('',#40495,#40493,#21704,.T.);
#52761=EDGE_CURVE('',#39302,#40495,#21705,.T.);
#52762=EDGE_CURVE('',#39300,#40492,#21706,.T.);
#52763=EDGE_CURVE('',#40488,#39299,#21707,.T.);
#52764=EDGE_CURVE('',#40489,#38688,#21708,.T.);
#52765=EDGE_CURVE('',#40490,#38687,#21709,.T.);
#52766=EDGE_CURVE('',#40484,#38686,#21710,.T.);
#52767=EDGE_CURVE('',#40485,#38685,#21711,.T.);
#52768=EDGE_CURVE('',#39304,#40486,#21712,.T.);
#52769=EDGE_CURVE('',#39303,#40487,#21713,.T.);
#52770=EDGE_CURVE('',#40496,#40497,#29616,.T.);
#52771=EDGE_CURVE('',#40497,#40498,#25556,.T.);
#52772=EDGE_CURVE('',#40498,#40499,#948,.T.);
#52773=EDGE_CURVE('',#40499,#40500,#29617,.T.);
#52774=EDGE_CURVE('',#40500,#40496,#25557,.T.);
#52775=EDGE_CURVE('',#40501,#40502,#949,.T.);
#52776=EDGE_CURVE('',#40502,#40503,#25558,.T.);
#52777=EDGE_CURVE('',#40504,#40503,#29618,.T.);
#52778=EDGE_CURVE('',#40504,#40505,#25559,.T.);
#52779=EDGE_CURVE('',#40505,#40501,#29619,.T.);
#52780=EDGE_CURVE('',#40503,#40497,#25560,.T.);
#52781=EDGE_CURVE('',#40496,#40504,#21714,.T.);
#52782=EDGE_CURVE('',#40505,#40506,#25561,.T.);
#52783=EDGE_CURVE('',#40507,#40504,#950,.T.);
#52784=EDGE_CURVE('',#40506,#40507,#25562,.T.);
#52785=EDGE_CURVE('',#40507,#40496,#951,.T.);
#52786=EDGE_CURVE('',#40508,#40500,#25563,.T.);
#52787=EDGE_CURVE('',#40507,#40508,#25564,.T.);
#52788=EDGE_CURVE('',#39295,#40506,#21715,.T.);
#52789=EDGE_CURVE('',#40508,#40506,#21716,.T.);
#52790=EDGE_CURVE('',#39296,#40508,#21717,.T.);
#52791=EDGE_CURVE('',#39294,#40505,#21718,.T.);
#52792=EDGE_CURVE('',#40501,#39293,#21719,.T.);
#52793=EDGE_CURVE('',#40502,#38692,#21720,.T.);
#52794=EDGE_CURVE('',#40503,#38691,#21721,.T.);
#52795=EDGE_CURVE('',#40497,#38690,#21722,.T.);
#52796=EDGE_CURVE('',#40498,#38689,#21723,.T.);
#52797=EDGE_CURVE('',#39298,#40499,#21724,.T.);
#52798=EDGE_CURVE('',#39297,#40500,#21725,.T.);
#52799=EDGE_CURVE('',#40509,#40510,#29620,.T.);
#52800=EDGE_CURVE('',#40510,#40511,#25565,.T.);
#52801=EDGE_CURVE('',#40511,#40512,#952,.T.);
#52802=EDGE_CURVE('',#40512,#40513,#29621,.T.);
#52803=EDGE_CURVE('',#40513,#40509,#25566,.T.);
#52804=EDGE_CURVE('',#40514,#40515,#953,.T.);
#52805=EDGE_CURVE('',#40515,#40516,#25567,.T.);
#52806=EDGE_CURVE('',#40517,#40516,#29622,.T.);
#52807=EDGE_CURVE('',#40517,#40518,#25568,.T.);
#52808=EDGE_CURVE('',#40518,#40514,#29623,.T.);
#52809=EDGE_CURVE('',#40516,#40510,#25569,.T.);
#52810=EDGE_CURVE('',#40509,#40517,#21726,.T.);
#52811=EDGE_CURVE('',#40518,#40519,#25570,.T.);
#52812=EDGE_CURVE('',#40520,#40517,#954,.T.);
#52813=EDGE_CURVE('',#40519,#40520,#25571,.T.);
#52814=EDGE_CURVE('',#40520,#40509,#955,.T.);
#52815=EDGE_CURVE('',#40521,#40513,#25572,.T.);
#52816=EDGE_CURVE('',#40520,#40521,#25573,.T.);
#52817=EDGE_CURVE('',#39289,#40519,#21727,.T.);
#52818=EDGE_CURVE('',#40521,#40519,#21728,.T.);
#52819=EDGE_CURVE('',#39290,#40521,#21729,.T.);
#52820=EDGE_CURVE('',#39288,#40518,#21730,.T.);
#52821=EDGE_CURVE('',#40514,#39287,#21731,.T.);
#52822=EDGE_CURVE('',#40515,#38696,#21732,.T.);
#52823=EDGE_CURVE('',#40516,#38695,#21733,.T.);
#52824=EDGE_CURVE('',#40510,#38694,#21734,.T.);
#52825=EDGE_CURVE('',#40511,#38693,#21735,.T.);
#52826=EDGE_CURVE('',#39292,#40512,#21736,.T.);
#52827=EDGE_CURVE('',#39291,#40513,#21737,.T.);
#52828=EDGE_CURVE('',#40522,#40523,#29624,.T.);
#52829=EDGE_CURVE('',#40523,#40524,#25574,.T.);
#52830=EDGE_CURVE('',#40524,#40525,#956,.T.);
#52831=EDGE_CURVE('',#40525,#40526,#29625,.T.);
#52832=EDGE_CURVE('',#40526,#40522,#25575,.T.);
#52833=EDGE_CURVE('',#40527,#40528,#957,.T.);
#52834=EDGE_CURVE('',#40528,#40529,#25576,.T.);
#52835=EDGE_CURVE('',#40530,#40529,#29626,.T.);
#52836=EDGE_CURVE('',#40530,#40531,#25577,.T.);
#52837=EDGE_CURVE('',#40531,#40527,#29627,.T.);
#52838=EDGE_CURVE('',#40529,#40523,#25578,.T.);
#52839=EDGE_CURVE('',#40522,#40530,#21738,.T.);
#52840=EDGE_CURVE('',#40531,#40532,#25579,.T.);
#52841=EDGE_CURVE('',#40533,#40530,#958,.T.);
#52842=EDGE_CURVE('',#40532,#40533,#25580,.T.);
#52843=EDGE_CURVE('',#40533,#40522,#959,.T.);
#52844=EDGE_CURVE('',#40534,#40526,#25581,.T.);
#52845=EDGE_CURVE('',#40533,#40534,#25582,.T.);
#52846=EDGE_CURVE('',#39283,#40532,#21739,.T.);
#52847=EDGE_CURVE('',#40534,#40532,#21740,.T.);
#52848=EDGE_CURVE('',#39284,#40534,#21741,.T.);
#52849=EDGE_CURVE('',#39282,#40531,#21742,.T.);
#52850=EDGE_CURVE('',#40527,#39281,#21743,.T.);
#52851=EDGE_CURVE('',#40528,#38700,#21744,.T.);
#52852=EDGE_CURVE('',#40529,#38699,#21745,.T.);
#52853=EDGE_CURVE('',#40523,#38698,#21746,.T.);
#52854=EDGE_CURVE('',#40524,#38697,#21747,.T.);
#52855=EDGE_CURVE('',#39286,#40525,#21748,.T.);
#52856=EDGE_CURVE('',#39285,#40526,#21749,.T.);
#52857=EDGE_CURVE('',#40535,#40536,#29628,.T.);
#52858=EDGE_CURVE('',#40536,#40537,#25583,.T.);
#52859=EDGE_CURVE('',#40537,#40538,#960,.T.);
#52860=EDGE_CURVE('',#40538,#40539,#29629,.T.);
#52861=EDGE_CURVE('',#40539,#40535,#25584,.T.);
#52862=EDGE_CURVE('',#40540,#40541,#961,.T.);
#52863=EDGE_CURVE('',#40541,#40542,#25585,.T.);
#52864=EDGE_CURVE('',#40543,#40542,#29630,.T.);
#52865=EDGE_CURVE('',#40543,#40544,#25586,.T.);
#52866=EDGE_CURVE('',#40544,#40540,#29631,.T.);
#52867=EDGE_CURVE('',#40542,#40536,#25587,.T.);
#52868=EDGE_CURVE('',#40535,#40543,#21750,.T.);
#52869=EDGE_CURVE('',#40544,#40545,#25588,.T.);
#52870=EDGE_CURVE('',#40546,#40543,#962,.T.);
#52871=EDGE_CURVE('',#40545,#40546,#25589,.T.);
#52872=EDGE_CURVE('',#40546,#40535,#963,.T.);
#52873=EDGE_CURVE('',#40547,#40539,#25590,.T.);
#52874=EDGE_CURVE('',#40546,#40547,#25591,.T.);
#52875=EDGE_CURVE('',#39277,#40545,#21751,.T.);
#52876=EDGE_CURVE('',#40547,#40545,#21752,.T.);
#52877=EDGE_CURVE('',#39278,#40547,#21753,.T.);
#52878=EDGE_CURVE('',#39276,#40544,#21754,.T.);
#52879=EDGE_CURVE('',#40540,#39275,#21755,.T.);
#52880=EDGE_CURVE('',#40541,#38704,#21756,.T.);
#52881=EDGE_CURVE('',#40542,#38703,#21757,.T.);
#52882=EDGE_CURVE('',#40536,#38702,#21758,.T.);
#52883=EDGE_CURVE('',#40537,#38701,#21759,.T.);
#52884=EDGE_CURVE('',#39280,#40538,#21760,.T.);
#52885=EDGE_CURVE('',#39279,#40539,#21761,.T.);
#52886=EDGE_CURVE('',#40548,#40549,#29632,.T.);
#52887=EDGE_CURVE('',#40549,#40550,#25592,.T.);
#52888=EDGE_CURVE('',#40550,#40551,#964,.T.);
#52889=EDGE_CURVE('',#40551,#40552,#29633,.T.);
#52890=EDGE_CURVE('',#40552,#40548,#25593,.T.);
#52891=EDGE_CURVE('',#40553,#40554,#965,.T.);
#52892=EDGE_CURVE('',#40554,#40555,#25594,.T.);
#52893=EDGE_CURVE('',#40556,#40555,#29634,.T.);
#52894=EDGE_CURVE('',#40556,#40557,#25595,.T.);
#52895=EDGE_CURVE('',#40557,#40553,#29635,.T.);
#52896=EDGE_CURVE('',#40555,#40549,#25596,.T.);
#52897=EDGE_CURVE('',#40548,#40556,#21762,.T.);
#52898=EDGE_CURVE('',#40557,#40558,#25597,.T.);
#52899=EDGE_CURVE('',#40559,#40556,#966,.T.);
#52900=EDGE_CURVE('',#40558,#40559,#25598,.T.);
#52901=EDGE_CURVE('',#40559,#40548,#967,.T.);
#52902=EDGE_CURVE('',#40560,#40552,#25599,.T.);
#52903=EDGE_CURVE('',#40559,#40560,#25600,.T.);
#52904=EDGE_CURVE('',#39271,#40558,#21763,.T.);
#52905=EDGE_CURVE('',#40560,#40558,#21764,.T.);
#52906=EDGE_CURVE('',#39272,#40560,#21765,.T.);
#52907=EDGE_CURVE('',#39270,#40557,#21766,.T.);
#52908=EDGE_CURVE('',#40553,#39269,#21767,.T.);
#52909=EDGE_CURVE('',#40554,#38708,#21768,.T.);
#52910=EDGE_CURVE('',#40555,#38707,#21769,.T.);
#52911=EDGE_CURVE('',#40549,#38706,#21770,.T.);
#52912=EDGE_CURVE('',#40550,#38705,#21771,.T.);
#52913=EDGE_CURVE('',#39274,#40551,#21772,.T.);
#52914=EDGE_CURVE('',#39273,#40552,#21773,.T.);
#52915=EDGE_CURVE('',#40561,#40562,#29636,.T.);
#52916=EDGE_CURVE('',#40562,#40563,#25601,.T.);
#52917=EDGE_CURVE('',#40563,#40564,#968,.T.);
#52918=EDGE_CURVE('',#40564,#40565,#29637,.T.);
#52919=EDGE_CURVE('',#40565,#40561,#25602,.T.);
#52920=EDGE_CURVE('',#40566,#40567,#969,.T.);
#52921=EDGE_CURVE('',#40567,#40568,#25603,.T.);
#52922=EDGE_CURVE('',#40569,#40568,#29638,.T.);
#52923=EDGE_CURVE('',#40569,#40570,#25604,.T.);
#52924=EDGE_CURVE('',#40570,#40566,#29639,.T.);
#52925=EDGE_CURVE('',#40568,#40562,#25605,.T.);
#52926=EDGE_CURVE('',#40561,#40569,#21774,.T.);
#52927=EDGE_CURVE('',#40570,#40571,#25606,.T.);
#52928=EDGE_CURVE('',#40572,#40569,#970,.T.);
#52929=EDGE_CURVE('',#40571,#40572,#25607,.T.);
#52930=EDGE_CURVE('',#40572,#40561,#971,.T.);
#52931=EDGE_CURVE('',#40573,#40565,#25608,.T.);
#52932=EDGE_CURVE('',#40572,#40573,#25609,.T.);
#52933=EDGE_CURVE('',#39265,#40571,#21775,.T.);
#52934=EDGE_CURVE('',#40573,#40571,#21776,.T.);
#52935=EDGE_CURVE('',#39266,#40573,#21777,.T.);
#52936=EDGE_CURVE('',#39264,#40570,#21778,.T.);
#52937=EDGE_CURVE('',#40566,#39263,#21779,.T.);
#52938=EDGE_CURVE('',#40567,#38712,#21780,.T.);
#52939=EDGE_CURVE('',#40568,#38711,#21781,.T.);
#52940=EDGE_CURVE('',#40562,#38710,#21782,.T.);
#52941=EDGE_CURVE('',#40563,#38709,#21783,.T.);
#52942=EDGE_CURVE('',#39268,#40564,#21784,.T.);
#52943=EDGE_CURVE('',#39267,#40565,#21785,.T.);
#52944=EDGE_CURVE('',#40574,#40575,#29640,.T.);
#52945=EDGE_CURVE('',#40575,#40576,#25610,.T.);
#52946=EDGE_CURVE('',#40576,#40577,#972,.T.);
#52947=EDGE_CURVE('',#40577,#40578,#29641,.T.);
#52948=EDGE_CURVE('',#40578,#40574,#25611,.T.);
#52949=EDGE_CURVE('',#40579,#40580,#973,.T.);
#52950=EDGE_CURVE('',#40580,#40581,#25612,.T.);
#52951=EDGE_CURVE('',#40582,#40581,#29642,.T.);
#52952=EDGE_CURVE('',#40582,#40583,#25613,.T.);
#52953=EDGE_CURVE('',#40583,#40579,#29643,.T.);
#52954=EDGE_CURVE('',#40581,#40575,#25614,.T.);
#52955=EDGE_CURVE('',#40574,#40582,#21786,.T.);
#52956=EDGE_CURVE('',#40583,#40584,#25615,.T.);
#52957=EDGE_CURVE('',#40585,#40582,#974,.T.);
#52958=EDGE_CURVE('',#40584,#40585,#25616,.T.);
#52959=EDGE_CURVE('',#40585,#40574,#975,.T.);
#52960=EDGE_CURVE('',#40586,#40578,#25617,.T.);
#52961=EDGE_CURVE('',#40585,#40586,#25618,.T.);
#52962=EDGE_CURVE('',#39259,#40584,#21787,.T.);
#52963=EDGE_CURVE('',#40586,#40584,#21788,.T.);
#52964=EDGE_CURVE('',#39260,#40586,#21789,.T.);
#52965=EDGE_CURVE('',#39258,#40583,#21790,.T.);
#52966=EDGE_CURVE('',#40579,#39257,#21791,.T.);
#52967=EDGE_CURVE('',#40580,#38716,#21792,.T.);
#52968=EDGE_CURVE('',#40581,#38715,#21793,.T.);
#52969=EDGE_CURVE('',#40575,#38714,#21794,.T.);
#52970=EDGE_CURVE('',#40576,#38713,#21795,.T.);
#52971=EDGE_CURVE('',#39262,#40577,#21796,.T.);
#52972=EDGE_CURVE('',#39261,#40578,#21797,.T.);
#52973=EDGE_CURVE('',#40587,#40588,#29644,.T.);
#52974=EDGE_CURVE('',#40588,#40589,#25619,.T.);
#52975=EDGE_CURVE('',#40589,#40590,#976,.T.);
#52976=EDGE_CURVE('',#40590,#40591,#29645,.T.);
#52977=EDGE_CURVE('',#40591,#40587,#25620,.T.);
#52978=EDGE_CURVE('',#40592,#40593,#977,.T.);
#52979=EDGE_CURVE('',#40593,#40594,#25621,.T.);
#52980=EDGE_CURVE('',#40595,#40594,#29646,.T.);
#52981=EDGE_CURVE('',#40595,#40596,#25622,.T.);
#52982=EDGE_CURVE('',#40596,#40592,#29647,.T.);
#52983=EDGE_CURVE('',#40594,#40588,#25623,.T.);
#52984=EDGE_CURVE('',#40587,#40595,#21798,.T.);
#52985=EDGE_CURVE('',#40596,#40597,#25624,.T.);
#52986=EDGE_CURVE('',#40598,#40595,#978,.T.);
#52987=EDGE_CURVE('',#40597,#40598,#25625,.T.);
#52988=EDGE_CURVE('',#40598,#40587,#979,.T.);
#52989=EDGE_CURVE('',#40599,#40591,#25626,.T.);
#52990=EDGE_CURVE('',#40598,#40599,#25627,.T.);
#52991=EDGE_CURVE('',#39253,#40597,#21799,.T.);
#52992=EDGE_CURVE('',#40599,#40597,#21800,.T.);
#52993=EDGE_CURVE('',#39254,#40599,#21801,.T.);
#52994=EDGE_CURVE('',#39252,#40596,#21802,.T.);
#52995=EDGE_CURVE('',#40592,#39251,#21803,.T.);
#52996=EDGE_CURVE('',#40593,#38720,#21804,.T.);
#52997=EDGE_CURVE('',#40594,#38719,#21805,.T.);
#52998=EDGE_CURVE('',#40588,#38718,#21806,.T.);
#52999=EDGE_CURVE('',#40589,#38717,#21807,.T.);
#53000=EDGE_CURVE('',#39256,#40590,#21808,.T.);
#53001=EDGE_CURVE('',#39255,#40591,#21809,.T.);
#53002=EDGE_CURVE('',#40600,#40601,#29648,.T.);
#53003=EDGE_CURVE('',#40601,#40602,#25628,.T.);
#53004=EDGE_CURVE('',#40602,#40603,#980,.T.);
#53005=EDGE_CURVE('',#40603,#40604,#29649,.T.);
#53006=EDGE_CURVE('',#40604,#40600,#25629,.T.);
#53007=EDGE_CURVE('',#40605,#40606,#981,.T.);
#53008=EDGE_CURVE('',#40606,#40607,#25630,.T.);
#53009=EDGE_CURVE('',#40608,#40607,#29650,.T.);
#53010=EDGE_CURVE('',#40608,#40609,#25631,.T.);
#53011=EDGE_CURVE('',#40609,#40605,#29651,.T.);
#53012=EDGE_CURVE('',#40607,#40601,#25632,.T.);
#53013=EDGE_CURVE('',#40600,#40608,#21810,.T.);
#53014=EDGE_CURVE('',#40609,#40610,#25633,.T.);
#53015=EDGE_CURVE('',#40611,#40608,#982,.T.);
#53016=EDGE_CURVE('',#40610,#40611,#25634,.T.);
#53017=EDGE_CURVE('',#40611,#40600,#983,.T.);
#53018=EDGE_CURVE('',#40612,#40604,#25635,.T.);
#53019=EDGE_CURVE('',#40611,#40612,#25636,.T.);
#53020=EDGE_CURVE('',#39247,#40610,#21811,.T.);
#53021=EDGE_CURVE('',#40612,#40610,#21812,.T.);
#53022=EDGE_CURVE('',#39248,#40612,#21813,.T.);
#53023=EDGE_CURVE('',#39246,#40609,#21814,.T.);
#53024=EDGE_CURVE('',#40605,#39245,#21815,.T.);
#53025=EDGE_CURVE('',#40606,#38724,#21816,.T.);
#53026=EDGE_CURVE('',#40607,#38723,#21817,.T.);
#53027=EDGE_CURVE('',#40601,#38722,#21818,.T.);
#53028=EDGE_CURVE('',#40602,#38721,#21819,.T.);
#53029=EDGE_CURVE('',#39250,#40603,#21820,.T.);
#53030=EDGE_CURVE('',#39249,#40604,#21821,.T.);
#53031=EDGE_CURVE('',#40613,#40614,#29652,.T.);
#53032=EDGE_CURVE('',#40614,#40615,#25637,.T.);
#53033=EDGE_CURVE('',#40615,#40616,#984,.T.);
#53034=EDGE_CURVE('',#40616,#40617,#29653,.T.);
#53035=EDGE_CURVE('',#40617,#40613,#25638,.T.);
#53036=EDGE_CURVE('',#40618,#40619,#985,.T.);
#53037=EDGE_CURVE('',#40619,#40620,#25639,.T.);
#53038=EDGE_CURVE('',#40621,#40620,#29654,.T.);
#53039=EDGE_CURVE('',#40621,#40622,#25640,.T.);
#53040=EDGE_CURVE('',#40622,#40618,#29655,.T.);
#53041=EDGE_CURVE('',#40620,#40614,#25641,.T.);
#53042=EDGE_CURVE('',#40613,#40621,#21822,.T.);
#53043=EDGE_CURVE('',#40622,#40623,#25642,.T.);
#53044=EDGE_CURVE('',#40624,#40621,#986,.T.);
#53045=EDGE_CURVE('',#40623,#40624,#25643,.T.);
#53046=EDGE_CURVE('',#40624,#40613,#987,.T.);
#53047=EDGE_CURVE('',#40625,#40617,#25644,.T.);
#53048=EDGE_CURVE('',#40624,#40625,#25645,.T.);
#53049=EDGE_CURVE('',#39241,#40623,#21823,.T.);
#53050=EDGE_CURVE('',#40625,#40623,#21824,.T.);
#53051=EDGE_CURVE('',#39242,#40625,#21825,.T.);
#53052=EDGE_CURVE('',#39240,#40622,#21826,.T.);
#53053=EDGE_CURVE('',#40618,#39239,#21827,.T.);
#53054=EDGE_CURVE('',#40619,#38728,#21828,.T.);
#53055=EDGE_CURVE('',#40620,#38727,#21829,.T.);
#53056=EDGE_CURVE('',#40614,#38726,#21830,.T.);
#53057=EDGE_CURVE('',#40615,#38725,#21831,.T.);
#53058=EDGE_CURVE('',#39244,#40616,#21832,.T.);
#53059=EDGE_CURVE('',#39243,#40617,#21833,.T.);
#53060=EDGE_CURVE('',#40626,#40627,#29656,.T.);
#53061=EDGE_CURVE('',#40627,#40628,#25646,.T.);
#53062=EDGE_CURVE('',#40628,#40629,#988,.T.);
#53063=EDGE_CURVE('',#40629,#40630,#29657,.T.);
#53064=EDGE_CURVE('',#40630,#40626,#25647,.T.);
#53065=EDGE_CURVE('',#40631,#40632,#989,.T.);
#53066=EDGE_CURVE('',#40632,#40633,#25648,.T.);
#53067=EDGE_CURVE('',#40634,#40633,#29658,.T.);
#53068=EDGE_CURVE('',#40634,#40635,#25649,.T.);
#53069=EDGE_CURVE('',#40635,#40631,#29659,.T.);
#53070=EDGE_CURVE('',#40633,#40627,#25650,.T.);
#53071=EDGE_CURVE('',#40626,#40634,#21834,.T.);
#53072=EDGE_CURVE('',#40635,#40636,#25651,.T.);
#53073=EDGE_CURVE('',#40637,#40634,#990,.T.);
#53074=EDGE_CURVE('',#40636,#40637,#25652,.T.);
#53075=EDGE_CURVE('',#40637,#40626,#991,.T.);
#53076=EDGE_CURVE('',#40638,#40630,#25653,.T.);
#53077=EDGE_CURVE('',#40637,#40638,#25654,.T.);
#53078=EDGE_CURVE('',#39235,#40636,#21835,.T.);
#53079=EDGE_CURVE('',#40638,#40636,#21836,.T.);
#53080=EDGE_CURVE('',#39236,#40638,#21837,.T.);
#53081=EDGE_CURVE('',#39234,#40635,#21838,.T.);
#53082=EDGE_CURVE('',#40631,#39233,#21839,.T.);
#53083=EDGE_CURVE('',#40632,#38732,#21840,.T.);
#53084=EDGE_CURVE('',#40633,#38731,#21841,.T.);
#53085=EDGE_CURVE('',#40627,#38730,#21842,.T.);
#53086=EDGE_CURVE('',#40628,#38729,#21843,.T.);
#53087=EDGE_CURVE('',#39238,#40629,#21844,.T.);
#53088=EDGE_CURVE('',#39237,#40630,#21845,.T.);
#53089=EDGE_CURVE('',#40639,#40640,#29660,.T.);
#53090=EDGE_CURVE('',#40640,#40641,#25655,.T.);
#53091=EDGE_CURVE('',#40641,#40642,#992,.T.);
#53092=EDGE_CURVE('',#40642,#40643,#29661,.T.);
#53093=EDGE_CURVE('',#40643,#40639,#25656,.T.);
#53094=EDGE_CURVE('',#40644,#40645,#993,.T.);
#53095=EDGE_CURVE('',#40645,#40646,#25657,.T.);
#53096=EDGE_CURVE('',#40647,#40646,#29662,.T.);
#53097=EDGE_CURVE('',#40647,#40648,#25658,.T.);
#53098=EDGE_CURVE('',#40648,#40644,#29663,.T.);
#53099=EDGE_CURVE('',#40646,#40640,#25659,.T.);
#53100=EDGE_CURVE('',#40639,#40647,#21846,.T.);
#53101=EDGE_CURVE('',#40648,#40649,#25660,.T.);
#53102=EDGE_CURVE('',#40650,#40647,#994,.T.);
#53103=EDGE_CURVE('',#40649,#40650,#25661,.T.);
#53104=EDGE_CURVE('',#40650,#40639,#995,.T.);
#53105=EDGE_CURVE('',#40651,#40643,#25662,.T.);
#53106=EDGE_CURVE('',#40650,#40651,#25663,.T.);
#53107=EDGE_CURVE('',#39229,#40649,#21847,.T.);
#53108=EDGE_CURVE('',#40651,#40649,#21848,.T.);
#53109=EDGE_CURVE('',#39230,#40651,#21849,.T.);
#53110=EDGE_CURVE('',#39228,#40648,#21850,.T.);
#53111=EDGE_CURVE('',#40644,#39227,#21851,.T.);
#53112=EDGE_CURVE('',#40645,#38736,#21852,.T.);
#53113=EDGE_CURVE('',#40646,#38735,#21853,.T.);
#53114=EDGE_CURVE('',#40640,#38734,#21854,.T.);
#53115=EDGE_CURVE('',#40641,#38733,#21855,.T.);
#53116=EDGE_CURVE('',#39232,#40642,#21856,.T.);
#53117=EDGE_CURVE('',#39231,#40643,#21857,.T.);
#53118=EDGE_CURVE('',#40652,#40653,#29664,.T.);
#53119=EDGE_CURVE('',#40653,#40654,#25664,.T.);
#53120=EDGE_CURVE('',#40654,#40655,#996,.T.);
#53121=EDGE_CURVE('',#40655,#40656,#29665,.T.);
#53122=EDGE_CURVE('',#40656,#40652,#25665,.T.);
#53123=EDGE_CURVE('',#40657,#40658,#997,.T.);
#53124=EDGE_CURVE('',#40658,#40659,#25666,.T.);
#53125=EDGE_CURVE('',#40660,#40659,#29666,.T.);
#53126=EDGE_CURVE('',#40660,#40661,#25667,.T.);
#53127=EDGE_CURVE('',#40661,#40657,#29667,.T.);
#53128=EDGE_CURVE('',#40659,#40653,#25668,.T.);
#53129=EDGE_CURVE('',#40652,#40660,#21858,.T.);
#53130=EDGE_CURVE('',#40661,#40662,#25669,.T.);
#53131=EDGE_CURVE('',#40663,#40660,#998,.T.);
#53132=EDGE_CURVE('',#40662,#40663,#25670,.T.);
#53133=EDGE_CURVE('',#40663,#40652,#999,.T.);
#53134=EDGE_CURVE('',#40664,#40656,#25671,.T.);
#53135=EDGE_CURVE('',#40663,#40664,#25672,.T.);
#53136=EDGE_CURVE('',#39223,#40662,#21859,.T.);
#53137=EDGE_CURVE('',#40664,#40662,#21860,.T.);
#53138=EDGE_CURVE('',#39224,#40664,#21861,.T.);
#53139=EDGE_CURVE('',#39222,#40661,#21862,.T.);
#53140=EDGE_CURVE('',#40657,#39221,#21863,.T.);
#53141=EDGE_CURVE('',#40658,#38740,#21864,.T.);
#53142=EDGE_CURVE('',#40659,#38739,#21865,.T.);
#53143=EDGE_CURVE('',#40653,#38738,#21866,.T.);
#53144=EDGE_CURVE('',#40654,#38737,#21867,.T.);
#53145=EDGE_CURVE('',#39226,#40655,#21868,.T.);
#53146=EDGE_CURVE('',#39225,#40656,#21869,.T.);
#53147=EDGE_CURVE('',#40665,#40666,#29668,.T.);
#53148=EDGE_CURVE('',#40666,#40667,#25673,.T.);
#53149=EDGE_CURVE('',#40667,#40668,#1000,.T.);
#53150=EDGE_CURVE('',#40668,#40669,#29669,.T.);
#53151=EDGE_CURVE('',#40669,#40665,#25674,.T.);
#53152=EDGE_CURVE('',#40670,#40671,#1001,.T.);
#53153=EDGE_CURVE('',#40671,#40672,#25675,.T.);
#53154=EDGE_CURVE('',#40673,#40672,#29670,.T.);
#53155=EDGE_CURVE('',#40673,#40674,#25676,.T.);
#53156=EDGE_CURVE('',#40674,#40670,#29671,.T.);
#53157=EDGE_CURVE('',#40672,#40666,#25677,.T.);
#53158=EDGE_CURVE('',#40665,#40673,#21870,.T.);
#53159=EDGE_CURVE('',#40674,#40675,#25678,.T.);
#53160=EDGE_CURVE('',#40676,#40673,#1002,.T.);
#53161=EDGE_CURVE('',#40675,#40676,#25679,.T.);
#53162=EDGE_CURVE('',#40676,#40665,#1003,.T.);
#53163=EDGE_CURVE('',#40677,#40669,#25680,.T.);
#53164=EDGE_CURVE('',#40676,#40677,#25681,.T.);
#53165=EDGE_CURVE('',#39217,#40675,#21871,.T.);
#53166=EDGE_CURVE('',#40677,#40675,#21872,.T.);
#53167=EDGE_CURVE('',#39218,#40677,#21873,.T.);
#53168=EDGE_CURVE('',#39216,#40674,#21874,.T.);
#53169=EDGE_CURVE('',#40670,#39215,#21875,.T.);
#53170=EDGE_CURVE('',#40671,#38744,#21876,.T.);
#53171=EDGE_CURVE('',#40672,#38743,#21877,.T.);
#53172=EDGE_CURVE('',#40666,#38742,#21878,.T.);
#53173=EDGE_CURVE('',#40667,#38741,#21879,.T.);
#53174=EDGE_CURVE('',#39220,#40668,#21880,.T.);
#53175=EDGE_CURVE('',#39219,#40669,#21881,.T.);
#53176=EDGE_CURVE('',#40678,#40679,#29672,.T.);
#53177=EDGE_CURVE('',#40679,#40680,#25682,.T.);
#53178=EDGE_CURVE('',#40680,#40681,#1004,.T.);
#53179=EDGE_CURVE('',#40681,#40682,#29673,.T.);
#53180=EDGE_CURVE('',#40682,#40678,#25683,.T.);
#53181=EDGE_CURVE('',#40683,#40684,#1005,.T.);
#53182=EDGE_CURVE('',#40684,#40685,#25684,.T.);
#53183=EDGE_CURVE('',#40686,#40685,#29674,.T.);
#53184=EDGE_CURVE('',#40686,#40687,#25685,.T.);
#53185=EDGE_CURVE('',#40687,#40683,#29675,.T.);
#53186=EDGE_CURVE('',#40685,#40679,#25686,.T.);
#53187=EDGE_CURVE('',#40678,#40686,#21882,.T.);
#53188=EDGE_CURVE('',#40687,#40688,#25687,.T.);
#53189=EDGE_CURVE('',#40689,#40686,#1006,.T.);
#53190=EDGE_CURVE('',#40688,#40689,#25688,.T.);
#53191=EDGE_CURVE('',#40689,#40678,#1007,.T.);
#53192=EDGE_CURVE('',#40690,#40682,#25689,.T.);
#53193=EDGE_CURVE('',#40689,#40690,#25690,.T.);
#53194=EDGE_CURVE('',#39211,#40688,#21883,.T.);
#53195=EDGE_CURVE('',#40690,#40688,#21884,.T.);
#53196=EDGE_CURVE('',#39212,#40690,#21885,.T.);
#53197=EDGE_CURVE('',#39210,#40687,#21886,.T.);
#53198=EDGE_CURVE('',#40683,#39209,#21887,.T.);
#53199=EDGE_CURVE('',#40684,#38748,#21888,.T.);
#53200=EDGE_CURVE('',#40685,#38747,#21889,.T.);
#53201=EDGE_CURVE('',#40679,#38746,#21890,.T.);
#53202=EDGE_CURVE('',#40680,#38745,#21891,.T.);
#53203=EDGE_CURVE('',#39214,#40681,#21892,.T.);
#53204=EDGE_CURVE('',#39213,#40682,#21893,.T.);
#53205=EDGE_CURVE('',#40691,#40692,#29676,.T.);
#53206=EDGE_CURVE('',#40692,#40693,#25691,.T.);
#53207=EDGE_CURVE('',#40693,#40694,#1008,.T.);
#53208=EDGE_CURVE('',#40694,#40695,#29677,.T.);
#53209=EDGE_CURVE('',#40695,#40691,#25692,.T.);
#53210=EDGE_CURVE('',#40696,#40697,#1009,.T.);
#53211=EDGE_CURVE('',#40697,#40698,#25693,.T.);
#53212=EDGE_CURVE('',#40699,#40698,#29678,.T.);
#53213=EDGE_CURVE('',#40699,#40700,#25694,.T.);
#53214=EDGE_CURVE('',#40700,#40696,#29679,.T.);
#53215=EDGE_CURVE('',#40698,#40692,#25695,.T.);
#53216=EDGE_CURVE('',#40691,#40699,#21894,.T.);
#53217=EDGE_CURVE('',#40700,#40701,#25696,.T.);
#53218=EDGE_CURVE('',#40702,#40699,#1010,.T.);
#53219=EDGE_CURVE('',#40701,#40702,#25697,.T.);
#53220=EDGE_CURVE('',#40702,#40691,#1011,.T.);
#53221=EDGE_CURVE('',#40703,#40695,#25698,.T.);
#53222=EDGE_CURVE('',#40702,#40703,#25699,.T.);
#53223=EDGE_CURVE('',#39205,#40701,#21895,.T.);
#53224=EDGE_CURVE('',#40703,#40701,#21896,.T.);
#53225=EDGE_CURVE('',#39206,#40703,#21897,.T.);
#53226=EDGE_CURVE('',#39204,#40700,#21898,.T.);
#53227=EDGE_CURVE('',#40696,#39203,#21899,.T.);
#53228=EDGE_CURVE('',#40697,#38752,#21900,.T.);
#53229=EDGE_CURVE('',#40698,#38751,#21901,.T.);
#53230=EDGE_CURVE('',#40692,#38750,#21902,.T.);
#53231=EDGE_CURVE('',#40693,#38749,#21903,.T.);
#53232=EDGE_CURVE('',#39208,#40694,#21904,.T.);
#53233=EDGE_CURVE('',#39207,#40695,#21905,.T.);
#53234=EDGE_CURVE('',#40704,#40705,#29680,.T.);
#53235=EDGE_CURVE('',#40705,#40706,#25700,.T.);
#53236=EDGE_CURVE('',#40706,#40707,#1012,.T.);
#53237=EDGE_CURVE('',#40707,#40708,#29681,.T.);
#53238=EDGE_CURVE('',#40708,#40704,#25701,.T.);
#53239=EDGE_CURVE('',#40709,#40710,#1013,.T.);
#53240=EDGE_CURVE('',#40710,#40711,#25702,.T.);
#53241=EDGE_CURVE('',#40712,#40711,#29682,.T.);
#53242=EDGE_CURVE('',#40712,#40713,#25703,.T.);
#53243=EDGE_CURVE('',#40713,#40709,#29683,.T.);
#53244=EDGE_CURVE('',#40711,#40705,#25704,.T.);
#53245=EDGE_CURVE('',#40704,#40712,#21906,.T.);
#53246=EDGE_CURVE('',#40713,#40714,#25705,.T.);
#53247=EDGE_CURVE('',#40715,#40712,#1014,.T.);
#53248=EDGE_CURVE('',#40714,#40715,#25706,.T.);
#53249=EDGE_CURVE('',#40715,#40704,#1015,.T.);
#53250=EDGE_CURVE('',#40716,#40708,#25707,.T.);
#53251=EDGE_CURVE('',#40715,#40716,#25708,.T.);
#53252=EDGE_CURVE('',#39199,#40714,#21907,.T.);
#53253=EDGE_CURVE('',#40716,#40714,#21908,.T.);
#53254=EDGE_CURVE('',#39200,#40716,#21909,.T.);
#53255=EDGE_CURVE('',#39198,#40713,#21910,.T.);
#53256=EDGE_CURVE('',#40709,#39197,#21911,.T.);
#53257=EDGE_CURVE('',#40710,#38756,#21912,.T.);
#53258=EDGE_CURVE('',#40711,#38755,#21913,.T.);
#53259=EDGE_CURVE('',#40705,#38754,#21914,.T.);
#53260=EDGE_CURVE('',#40706,#38753,#21915,.T.);
#53261=EDGE_CURVE('',#39202,#40707,#21916,.T.);
#53262=EDGE_CURVE('',#39201,#40708,#21917,.T.);
#53263=EDGE_CURVE('',#40717,#40718,#29684,.T.);
#53264=EDGE_CURVE('',#40718,#40719,#25709,.T.);
#53265=EDGE_CURVE('',#40719,#40720,#1016,.T.);
#53266=EDGE_CURVE('',#40720,#40721,#29685,.T.);
#53267=EDGE_CURVE('',#40721,#40717,#25710,.T.);
#53268=EDGE_CURVE('',#40722,#40723,#1017,.T.);
#53269=EDGE_CURVE('',#40723,#40724,#25711,.T.);
#53270=EDGE_CURVE('',#40725,#40724,#29686,.T.);
#53271=EDGE_CURVE('',#40725,#40726,#25712,.T.);
#53272=EDGE_CURVE('',#40726,#40722,#29687,.T.);
#53273=EDGE_CURVE('',#40724,#40718,#25713,.T.);
#53274=EDGE_CURVE('',#40717,#40725,#21918,.T.);
#53275=EDGE_CURVE('',#40726,#40727,#25714,.T.);
#53276=EDGE_CURVE('',#40728,#40725,#1018,.T.);
#53277=EDGE_CURVE('',#40727,#40728,#25715,.T.);
#53278=EDGE_CURVE('',#40728,#40717,#1019,.T.);
#53279=EDGE_CURVE('',#40729,#40721,#25716,.T.);
#53280=EDGE_CURVE('',#40728,#40729,#25717,.T.);
#53281=EDGE_CURVE('',#39193,#40727,#21919,.T.);
#53282=EDGE_CURVE('',#40729,#40727,#21920,.T.);
#53283=EDGE_CURVE('',#39194,#40729,#21921,.T.);
#53284=EDGE_CURVE('',#39192,#40726,#21922,.T.);
#53285=EDGE_CURVE('',#40722,#39191,#21923,.T.);
#53286=EDGE_CURVE('',#40723,#38760,#21924,.T.);
#53287=EDGE_CURVE('',#40724,#38759,#21925,.T.);
#53288=EDGE_CURVE('',#40718,#38758,#21926,.T.);
#53289=EDGE_CURVE('',#40719,#38757,#21927,.T.);
#53290=EDGE_CURVE('',#39196,#40720,#21928,.T.);
#53291=EDGE_CURVE('',#39195,#40721,#21929,.T.);
#53292=EDGE_CURVE('',#40730,#40731,#29688,.T.);
#53293=EDGE_CURVE('',#40731,#40732,#25718,.T.);
#53294=EDGE_CURVE('',#40732,#40733,#1020,.T.);
#53295=EDGE_CURVE('',#40733,#40734,#29689,.T.);
#53296=EDGE_CURVE('',#40734,#40730,#25719,.T.);
#53297=EDGE_CURVE('',#40735,#40736,#1021,.T.);
#53298=EDGE_CURVE('',#40736,#40737,#25720,.T.);
#53299=EDGE_CURVE('',#40738,#40737,#29690,.T.);
#53300=EDGE_CURVE('',#40738,#40739,#25721,.T.);
#53301=EDGE_CURVE('',#40739,#40735,#29691,.T.);
#53302=EDGE_CURVE('',#40737,#40731,#25722,.T.);
#53303=EDGE_CURVE('',#40730,#40738,#21930,.T.);
#53304=EDGE_CURVE('',#40739,#40740,#25723,.T.);
#53305=EDGE_CURVE('',#40741,#40738,#1022,.T.);
#53306=EDGE_CURVE('',#40740,#40741,#25724,.T.);
#53307=EDGE_CURVE('',#40741,#40730,#1023,.T.);
#53308=EDGE_CURVE('',#40742,#40734,#25725,.T.);
#53309=EDGE_CURVE('',#40741,#40742,#25726,.T.);
#53310=EDGE_CURVE('',#39187,#40740,#21931,.T.);
#53311=EDGE_CURVE('',#40742,#40740,#21932,.T.);
#53312=EDGE_CURVE('',#39188,#40742,#21933,.T.);
#53313=EDGE_CURVE('',#39186,#40739,#21934,.T.);
#53314=EDGE_CURVE('',#40735,#39185,#21935,.T.);
#53315=EDGE_CURVE('',#40736,#38764,#21936,.T.);
#53316=EDGE_CURVE('',#40737,#38763,#21937,.T.);
#53317=EDGE_CURVE('',#40731,#38762,#21938,.T.);
#53318=EDGE_CURVE('',#40732,#38761,#21939,.T.);
#53319=EDGE_CURVE('',#39190,#40733,#21940,.T.);
#53320=EDGE_CURVE('',#39189,#40734,#21941,.T.);
#53321=EDGE_CURVE('',#40743,#40744,#29692,.T.);
#53322=EDGE_CURVE('',#40744,#40745,#25727,.T.);
#53323=EDGE_CURVE('',#40745,#40746,#1024,.T.);
#53324=EDGE_CURVE('',#40746,#40747,#29693,.T.);
#53325=EDGE_CURVE('',#40747,#40743,#25728,.T.);
#53326=EDGE_CURVE('',#40748,#40749,#1025,.T.);
#53327=EDGE_CURVE('',#40749,#40750,#25729,.T.);
#53328=EDGE_CURVE('',#40751,#40750,#29694,.T.);
#53329=EDGE_CURVE('',#40751,#40752,#25730,.T.);
#53330=EDGE_CURVE('',#40752,#40748,#29695,.T.);
#53331=EDGE_CURVE('',#40750,#40744,#25731,.T.);
#53332=EDGE_CURVE('',#40743,#40751,#21942,.T.);
#53333=EDGE_CURVE('',#40752,#40753,#25732,.T.);
#53334=EDGE_CURVE('',#40754,#40751,#1026,.T.);
#53335=EDGE_CURVE('',#40753,#40754,#25733,.T.);
#53336=EDGE_CURVE('',#40754,#40743,#1027,.T.);
#53337=EDGE_CURVE('',#40755,#40747,#25734,.T.);
#53338=EDGE_CURVE('',#40754,#40755,#25735,.T.);
#53339=EDGE_CURVE('',#39181,#40753,#21943,.T.);
#53340=EDGE_CURVE('',#40755,#40753,#21944,.T.);
#53341=EDGE_CURVE('',#39182,#40755,#21945,.T.);
#53342=EDGE_CURVE('',#39180,#40752,#21946,.T.);
#53343=EDGE_CURVE('',#40748,#39179,#21947,.T.);
#53344=EDGE_CURVE('',#40749,#38768,#21948,.T.);
#53345=EDGE_CURVE('',#40750,#38767,#21949,.T.);
#53346=EDGE_CURVE('',#40744,#38766,#21950,.T.);
#53347=EDGE_CURVE('',#40745,#38765,#21951,.T.);
#53348=EDGE_CURVE('',#39184,#40746,#21952,.T.);
#53349=EDGE_CURVE('',#39183,#40747,#21953,.T.);
#53350=EDGE_CURVE('',#40756,#40757,#29696,.T.);
#53351=EDGE_CURVE('',#40757,#40758,#25736,.T.);
#53352=EDGE_CURVE('',#40758,#40759,#1028,.T.);
#53353=EDGE_CURVE('',#40759,#40760,#29697,.T.);
#53354=EDGE_CURVE('',#40760,#40756,#25737,.T.);
#53355=EDGE_CURVE('',#40761,#40762,#1029,.T.);
#53356=EDGE_CURVE('',#40762,#40763,#25738,.T.);
#53357=EDGE_CURVE('',#40764,#40763,#29698,.T.);
#53358=EDGE_CURVE('',#40764,#40765,#25739,.T.);
#53359=EDGE_CURVE('',#40765,#40761,#29699,.T.);
#53360=EDGE_CURVE('',#40763,#40757,#25740,.T.);
#53361=EDGE_CURVE('',#40756,#40764,#21954,.T.);
#53362=EDGE_CURVE('',#40765,#40766,#25741,.T.);
#53363=EDGE_CURVE('',#40767,#40764,#1030,.T.);
#53364=EDGE_CURVE('',#40766,#40767,#25742,.T.);
#53365=EDGE_CURVE('',#40767,#40756,#1031,.T.);
#53366=EDGE_CURVE('',#40768,#40760,#25743,.T.);
#53367=EDGE_CURVE('',#40767,#40768,#25744,.T.);
#53368=EDGE_CURVE('',#39175,#40766,#21955,.T.);
#53369=EDGE_CURVE('',#40768,#40766,#21956,.T.);
#53370=EDGE_CURVE('',#39176,#40768,#21957,.T.);
#53371=EDGE_CURVE('',#39174,#40765,#21958,.T.);
#53372=EDGE_CURVE('',#40761,#39173,#21959,.T.);
#53373=EDGE_CURVE('',#40762,#38772,#21960,.T.);
#53374=EDGE_CURVE('',#40763,#38771,#21961,.T.);
#53375=EDGE_CURVE('',#40757,#38770,#21962,.T.);
#53376=EDGE_CURVE('',#40758,#38769,#21963,.T.);
#53377=EDGE_CURVE('',#39178,#40759,#21964,.T.);
#53378=EDGE_CURVE('',#39177,#40760,#21965,.T.);
#53379=EDGE_CURVE('',#40769,#40770,#29700,.T.);
#53380=EDGE_CURVE('',#40770,#40771,#25745,.T.);
#53381=EDGE_CURVE('',#40771,#40772,#1032,.T.);
#53382=EDGE_CURVE('',#40772,#40773,#29701,.T.);
#53383=EDGE_CURVE('',#40773,#40769,#25746,.T.);
#53384=EDGE_CURVE('',#40774,#40775,#1033,.T.);
#53385=EDGE_CURVE('',#40775,#40776,#25747,.T.);
#53386=EDGE_CURVE('',#40777,#40776,#29702,.T.);
#53387=EDGE_CURVE('',#40777,#40778,#25748,.T.);
#53388=EDGE_CURVE('',#40778,#40774,#29703,.T.);
#53389=EDGE_CURVE('',#40776,#40770,#25749,.T.);
#53390=EDGE_CURVE('',#40769,#40777,#21966,.T.);
#53391=EDGE_CURVE('',#40778,#40779,#25750,.T.);
#53392=EDGE_CURVE('',#40780,#40777,#1034,.T.);
#53393=EDGE_CURVE('',#40779,#40780,#25751,.T.);
#53394=EDGE_CURVE('',#40780,#40769,#1035,.T.);
#53395=EDGE_CURVE('',#40781,#40773,#25752,.T.);
#53396=EDGE_CURVE('',#40780,#40781,#25753,.T.);
#53397=EDGE_CURVE('',#39169,#40779,#21967,.T.);
#53398=EDGE_CURVE('',#40781,#40779,#21968,.T.);
#53399=EDGE_CURVE('',#39170,#40781,#21969,.T.);
#53400=EDGE_CURVE('',#39168,#40778,#21970,.T.);
#53401=EDGE_CURVE('',#40774,#39167,#21971,.T.);
#53402=EDGE_CURVE('',#40775,#38776,#21972,.T.);
#53403=EDGE_CURVE('',#40776,#38775,#21973,.T.);
#53404=EDGE_CURVE('',#40770,#38774,#21974,.T.);
#53405=EDGE_CURVE('',#40771,#38773,#21975,.T.);
#53406=EDGE_CURVE('',#39172,#40772,#21976,.T.);
#53407=EDGE_CURVE('',#39171,#40773,#21977,.T.);
#53408=EDGE_CURVE('',#40782,#40783,#29704,.T.);
#53409=EDGE_CURVE('',#40783,#40784,#25754,.T.);
#53410=EDGE_CURVE('',#40784,#40785,#1036,.T.);
#53411=EDGE_CURVE('',#40785,#40786,#29705,.T.);
#53412=EDGE_CURVE('',#40786,#40782,#25755,.T.);
#53413=EDGE_CURVE('',#40787,#40788,#1037,.T.);
#53414=EDGE_CURVE('',#40788,#40789,#25756,.T.);
#53415=EDGE_CURVE('',#40790,#40789,#29706,.T.);
#53416=EDGE_CURVE('',#40790,#40791,#25757,.T.);
#53417=EDGE_CURVE('',#40791,#40787,#29707,.T.);
#53418=EDGE_CURVE('',#40789,#40783,#25758,.T.);
#53419=EDGE_CURVE('',#40782,#40790,#21978,.T.);
#53420=EDGE_CURVE('',#40791,#40792,#25759,.T.);
#53421=EDGE_CURVE('',#40793,#40790,#1038,.T.);
#53422=EDGE_CURVE('',#40792,#40793,#25760,.T.);
#53423=EDGE_CURVE('',#40793,#40782,#1039,.T.);
#53424=EDGE_CURVE('',#40794,#40786,#25761,.T.);
#53425=EDGE_CURVE('',#40793,#40794,#25762,.T.);
#53426=EDGE_CURVE('',#39163,#40792,#21979,.T.);
#53427=EDGE_CURVE('',#40794,#40792,#21980,.T.);
#53428=EDGE_CURVE('',#39164,#40794,#21981,.T.);
#53429=EDGE_CURVE('',#39162,#40791,#21982,.T.);
#53430=EDGE_CURVE('',#40787,#39161,#21983,.T.);
#53431=EDGE_CURVE('',#40788,#38780,#21984,.T.);
#53432=EDGE_CURVE('',#40789,#38779,#21985,.T.);
#53433=EDGE_CURVE('',#40783,#38778,#21986,.T.);
#53434=EDGE_CURVE('',#40784,#38777,#21987,.T.);
#53435=EDGE_CURVE('',#39166,#40785,#21988,.T.);
#53436=EDGE_CURVE('',#39165,#40786,#21989,.T.);
#53437=EDGE_CURVE('',#40795,#40796,#29708,.T.);
#53438=EDGE_CURVE('',#40796,#40797,#25763,.T.);
#53439=EDGE_CURVE('',#40797,#40798,#1040,.T.);
#53440=EDGE_CURVE('',#40798,#40799,#29709,.T.);
#53441=EDGE_CURVE('',#40799,#40795,#25764,.T.);
#53442=EDGE_CURVE('',#40800,#40801,#1041,.T.);
#53443=EDGE_CURVE('',#40801,#40802,#25765,.T.);
#53444=EDGE_CURVE('',#40803,#40802,#29710,.T.);
#53445=EDGE_CURVE('',#40803,#40804,#25766,.T.);
#53446=EDGE_CURVE('',#40804,#40800,#29711,.T.);
#53447=EDGE_CURVE('',#40802,#40796,#25767,.T.);
#53448=EDGE_CURVE('',#40795,#40803,#21990,.T.);
#53449=EDGE_CURVE('',#40804,#40805,#25768,.T.);
#53450=EDGE_CURVE('',#40806,#40803,#1042,.T.);
#53451=EDGE_CURVE('',#40805,#40806,#25769,.T.);
#53452=EDGE_CURVE('',#40806,#40795,#1043,.T.);
#53453=EDGE_CURVE('',#40807,#40799,#25770,.T.);
#53454=EDGE_CURVE('',#40806,#40807,#25771,.T.);
#53455=EDGE_CURVE('',#39157,#40805,#21991,.T.);
#53456=EDGE_CURVE('',#40807,#40805,#21992,.T.);
#53457=EDGE_CURVE('',#39158,#40807,#21993,.T.);
#53458=EDGE_CURVE('',#39156,#40804,#21994,.T.);
#53459=EDGE_CURVE('',#40800,#39155,#21995,.T.);
#53460=EDGE_CURVE('',#40801,#38784,#21996,.T.);
#53461=EDGE_CURVE('',#40802,#38783,#21997,.T.);
#53462=EDGE_CURVE('',#40796,#38782,#21998,.T.);
#53463=EDGE_CURVE('',#40797,#38781,#21999,.T.);
#53464=EDGE_CURVE('',#39160,#40798,#22000,.T.);
#53465=EDGE_CURVE('',#39159,#40799,#22001,.T.);
#53466=EDGE_CURVE('',#40808,#40809,#29712,.T.);
#53467=EDGE_CURVE('',#40809,#40810,#25772,.T.);
#53468=EDGE_CURVE('',#40810,#40811,#1044,.T.);
#53469=EDGE_CURVE('',#40811,#40812,#29713,.T.);
#53470=EDGE_CURVE('',#40812,#40808,#25773,.T.);
#53471=EDGE_CURVE('',#40813,#40814,#1045,.T.);
#53472=EDGE_CURVE('',#40814,#40815,#25774,.T.);
#53473=EDGE_CURVE('',#40816,#40815,#29714,.T.);
#53474=EDGE_CURVE('',#40816,#40817,#25775,.T.);
#53475=EDGE_CURVE('',#40817,#40813,#29715,.T.);
#53476=EDGE_CURVE('',#40815,#40809,#25776,.T.);
#53477=EDGE_CURVE('',#40808,#40816,#22002,.T.);
#53478=EDGE_CURVE('',#40817,#40818,#25777,.T.);
#53479=EDGE_CURVE('',#40819,#40816,#1046,.T.);
#53480=EDGE_CURVE('',#40818,#40819,#25778,.T.);
#53481=EDGE_CURVE('',#40819,#40808,#1047,.T.);
#53482=EDGE_CURVE('',#40820,#40812,#25779,.T.);
#53483=EDGE_CURVE('',#40819,#40820,#25780,.T.);
#53484=EDGE_CURVE('',#39151,#40818,#22003,.T.);
#53485=EDGE_CURVE('',#40820,#40818,#22004,.T.);
#53486=EDGE_CURVE('',#39152,#40820,#22005,.T.);
#53487=EDGE_CURVE('',#39150,#40817,#22006,.T.);
#53488=EDGE_CURVE('',#40813,#39149,#22007,.T.);
#53489=EDGE_CURVE('',#40814,#38788,#22008,.T.);
#53490=EDGE_CURVE('',#40815,#38787,#22009,.T.);
#53491=EDGE_CURVE('',#40809,#38786,#22010,.T.);
#53492=EDGE_CURVE('',#40810,#38785,#22011,.T.);
#53493=EDGE_CURVE('',#39154,#40811,#22012,.T.);
#53494=EDGE_CURVE('',#39153,#40812,#22013,.T.);
#53495=EDGE_CURVE('',#40821,#40822,#29716,.T.);
#53496=EDGE_CURVE('',#40822,#40823,#25781,.T.);
#53497=EDGE_CURVE('',#40823,#40824,#1048,.T.);
#53498=EDGE_CURVE('',#40824,#40825,#29717,.T.);
#53499=EDGE_CURVE('',#40825,#40821,#25782,.T.);
#53500=EDGE_CURVE('',#40826,#40827,#1049,.T.);
#53501=EDGE_CURVE('',#40827,#40828,#25783,.T.);
#53502=EDGE_CURVE('',#40829,#40828,#29718,.T.);
#53503=EDGE_CURVE('',#40829,#40830,#25784,.T.);
#53504=EDGE_CURVE('',#40830,#40826,#29719,.T.);
#53505=EDGE_CURVE('',#40828,#40822,#25785,.T.);
#53506=EDGE_CURVE('',#40821,#40829,#22014,.T.);
#53507=EDGE_CURVE('',#40830,#40831,#25786,.T.);
#53508=EDGE_CURVE('',#40832,#40829,#1050,.T.);
#53509=EDGE_CURVE('',#40831,#40832,#25787,.T.);
#53510=EDGE_CURVE('',#40832,#40821,#1051,.T.);
#53511=EDGE_CURVE('',#40833,#40825,#25788,.T.);
#53512=EDGE_CURVE('',#40832,#40833,#25789,.T.);
#53513=EDGE_CURVE('',#39145,#40831,#22015,.T.);
#53514=EDGE_CURVE('',#40833,#40831,#22016,.T.);
#53515=EDGE_CURVE('',#39146,#40833,#22017,.T.);
#53516=EDGE_CURVE('',#39144,#40830,#22018,.T.);
#53517=EDGE_CURVE('',#40826,#39143,#22019,.T.);
#53518=EDGE_CURVE('',#40827,#38792,#22020,.T.);
#53519=EDGE_CURVE('',#40828,#38791,#22021,.T.);
#53520=EDGE_CURVE('',#40822,#38790,#22022,.T.);
#53521=EDGE_CURVE('',#40823,#38789,#22023,.T.);
#53522=EDGE_CURVE('',#39148,#40824,#22024,.T.);
#53523=EDGE_CURVE('',#39147,#40825,#22025,.T.);
#53524=EDGE_CURVE('',#40834,#40835,#29720,.T.);
#53525=EDGE_CURVE('',#40835,#40836,#25790,.T.);
#53526=EDGE_CURVE('',#40836,#40837,#1052,.T.);
#53527=EDGE_CURVE('',#40837,#40838,#29721,.T.);
#53528=EDGE_CURVE('',#40838,#40834,#25791,.T.);
#53529=EDGE_CURVE('',#40839,#40840,#1053,.T.);
#53530=EDGE_CURVE('',#40840,#40841,#25792,.T.);
#53531=EDGE_CURVE('',#40842,#40841,#29722,.T.);
#53532=EDGE_CURVE('',#40842,#40843,#25793,.T.);
#53533=EDGE_CURVE('',#40843,#40839,#29723,.T.);
#53534=EDGE_CURVE('',#40841,#40835,#25794,.T.);
#53535=EDGE_CURVE('',#40834,#40842,#22026,.T.);
#53536=EDGE_CURVE('',#40843,#40844,#25795,.T.);
#53537=EDGE_CURVE('',#40845,#40842,#1054,.T.);
#53538=EDGE_CURVE('',#40844,#40845,#25796,.T.);
#53539=EDGE_CURVE('',#40845,#40834,#1055,.T.);
#53540=EDGE_CURVE('',#40846,#40838,#25797,.T.);
#53541=EDGE_CURVE('',#40845,#40846,#25798,.T.);
#53542=EDGE_CURVE('',#39139,#40844,#22027,.T.);
#53543=EDGE_CURVE('',#40846,#40844,#22028,.T.);
#53544=EDGE_CURVE('',#39140,#40846,#22029,.T.);
#53545=EDGE_CURVE('',#39138,#40843,#22030,.T.);
#53546=EDGE_CURVE('',#40839,#39137,#22031,.T.);
#53547=EDGE_CURVE('',#40840,#38796,#22032,.T.);
#53548=EDGE_CURVE('',#40841,#38795,#22033,.T.);
#53549=EDGE_CURVE('',#40835,#38794,#22034,.T.);
#53550=EDGE_CURVE('',#40836,#38793,#22035,.T.);
#53551=EDGE_CURVE('',#39142,#40837,#22036,.T.);
#53552=EDGE_CURVE('',#39141,#40838,#22037,.T.);
#53553=EDGE_CURVE('',#40847,#40848,#29724,.T.);
#53554=EDGE_CURVE('',#40848,#40849,#25799,.T.);
#53555=EDGE_CURVE('',#40849,#40850,#1056,.T.);
#53556=EDGE_CURVE('',#40850,#40851,#29725,.T.);
#53557=EDGE_CURVE('',#40851,#40847,#25800,.T.);
#53558=EDGE_CURVE('',#40852,#40853,#1057,.T.);
#53559=EDGE_CURVE('',#40853,#40854,#25801,.T.);
#53560=EDGE_CURVE('',#40855,#40854,#29726,.T.);
#53561=EDGE_CURVE('',#40855,#40856,#25802,.T.);
#53562=EDGE_CURVE('',#40856,#40852,#29727,.T.);
#53563=EDGE_CURVE('',#40854,#40848,#25803,.T.);
#53564=EDGE_CURVE('',#40847,#40855,#22038,.T.);
#53565=EDGE_CURVE('',#40856,#40857,#25804,.T.);
#53566=EDGE_CURVE('',#40858,#40855,#1058,.T.);
#53567=EDGE_CURVE('',#40857,#40858,#25805,.T.);
#53568=EDGE_CURVE('',#40858,#40847,#1059,.T.);
#53569=EDGE_CURVE('',#40859,#40851,#25806,.T.);
#53570=EDGE_CURVE('',#40858,#40859,#25807,.T.);
#53571=EDGE_CURVE('',#39133,#40857,#22039,.T.);
#53572=EDGE_CURVE('',#40859,#40857,#22040,.T.);
#53573=EDGE_CURVE('',#39134,#40859,#22041,.T.);
#53574=EDGE_CURVE('',#39132,#40856,#22042,.T.);
#53575=EDGE_CURVE('',#40852,#39131,#22043,.T.);
#53576=EDGE_CURVE('',#40853,#38800,#22044,.T.);
#53577=EDGE_CURVE('',#40854,#38799,#22045,.T.);
#53578=EDGE_CURVE('',#40848,#38798,#22046,.T.);
#53579=EDGE_CURVE('',#40849,#38797,#22047,.T.);
#53580=EDGE_CURVE('',#39136,#40850,#22048,.T.);
#53581=EDGE_CURVE('',#39135,#40851,#22049,.T.);
#53582=EDGE_CURVE('',#40860,#40861,#29728,.T.);
#53583=EDGE_CURVE('',#40861,#40862,#25808,.T.);
#53584=EDGE_CURVE('',#40862,#40863,#1060,.T.);
#53585=EDGE_CURVE('',#40863,#40864,#29729,.T.);
#53586=EDGE_CURVE('',#40864,#40860,#25809,.T.);
#53587=EDGE_CURVE('',#40865,#40866,#1061,.T.);
#53588=EDGE_CURVE('',#40866,#40867,#25810,.T.);
#53589=EDGE_CURVE('',#40868,#40867,#29730,.T.);
#53590=EDGE_CURVE('',#40868,#40869,#25811,.T.);
#53591=EDGE_CURVE('',#40869,#40865,#29731,.T.);
#53592=EDGE_CURVE('',#40867,#40861,#25812,.T.);
#53593=EDGE_CURVE('',#40860,#40868,#22050,.T.);
#53594=EDGE_CURVE('',#40869,#40870,#25813,.T.);
#53595=EDGE_CURVE('',#40871,#40868,#1062,.T.);
#53596=EDGE_CURVE('',#40870,#40871,#25814,.T.);
#53597=EDGE_CURVE('',#40871,#40860,#1063,.T.);
#53598=EDGE_CURVE('',#40872,#40864,#25815,.T.);
#53599=EDGE_CURVE('',#40871,#40872,#25816,.T.);
#53600=EDGE_CURVE('',#39127,#40870,#22051,.T.);
#53601=EDGE_CURVE('',#40872,#40870,#22052,.T.);
#53602=EDGE_CURVE('',#39128,#40872,#22053,.T.);
#53603=EDGE_CURVE('',#39126,#40869,#22054,.T.);
#53604=EDGE_CURVE('',#40865,#39125,#22055,.T.);
#53605=EDGE_CURVE('',#40866,#38804,#22056,.T.);
#53606=EDGE_CURVE('',#40867,#38803,#22057,.T.);
#53607=EDGE_CURVE('',#40861,#38802,#22058,.T.);
#53608=EDGE_CURVE('',#40862,#38801,#22059,.T.);
#53609=EDGE_CURVE('',#39130,#40863,#22060,.T.);
#53610=EDGE_CURVE('',#39129,#40864,#22061,.T.);
#53611=EDGE_CURVE('',#40873,#40874,#29732,.T.);
#53612=EDGE_CURVE('',#40874,#40875,#25817,.T.);
#53613=EDGE_CURVE('',#40875,#40876,#1064,.T.);
#53614=EDGE_CURVE('',#40876,#40877,#29733,.T.);
#53615=EDGE_CURVE('',#40877,#40873,#25818,.T.);
#53616=EDGE_CURVE('',#40878,#40879,#1065,.T.);
#53617=EDGE_CURVE('',#40879,#40880,#25819,.T.);
#53618=EDGE_CURVE('',#40881,#40880,#29734,.T.);
#53619=EDGE_CURVE('',#40881,#40882,#25820,.T.);
#53620=EDGE_CURVE('',#40882,#40878,#29735,.T.);
#53621=EDGE_CURVE('',#40880,#40874,#25821,.T.);
#53622=EDGE_CURVE('',#40873,#40881,#22062,.T.);
#53623=EDGE_CURVE('',#40882,#40883,#25822,.T.);
#53624=EDGE_CURVE('',#40884,#40881,#1066,.T.);
#53625=EDGE_CURVE('',#40883,#40884,#25823,.T.);
#53626=EDGE_CURVE('',#40884,#40873,#1067,.T.);
#53627=EDGE_CURVE('',#40885,#40877,#25824,.T.);
#53628=EDGE_CURVE('',#40884,#40885,#25825,.T.);
#53629=EDGE_CURVE('',#39121,#40883,#22063,.T.);
#53630=EDGE_CURVE('',#40885,#40883,#22064,.T.);
#53631=EDGE_CURVE('',#39122,#40885,#22065,.T.);
#53632=EDGE_CURVE('',#39120,#40882,#22066,.T.);
#53633=EDGE_CURVE('',#40878,#39119,#22067,.T.);
#53634=EDGE_CURVE('',#40879,#38808,#22068,.T.);
#53635=EDGE_CURVE('',#40880,#38807,#22069,.T.);
#53636=EDGE_CURVE('',#40874,#38806,#22070,.T.);
#53637=EDGE_CURVE('',#40875,#38805,#22071,.T.);
#53638=EDGE_CURVE('',#39124,#40876,#22072,.T.);
#53639=EDGE_CURVE('',#39123,#40877,#22073,.T.);
#53640=EDGE_CURVE('',#40886,#40887,#29736,.T.);
#53641=EDGE_CURVE('',#40887,#40888,#25826,.T.);
#53642=EDGE_CURVE('',#40888,#40889,#1068,.T.);
#53643=EDGE_CURVE('',#40889,#40890,#29737,.T.);
#53644=EDGE_CURVE('',#40890,#40886,#25827,.T.);
#53645=EDGE_CURVE('',#40891,#40892,#1069,.T.);
#53646=EDGE_CURVE('',#40892,#40893,#25828,.T.);
#53647=EDGE_CURVE('',#40894,#40893,#29738,.T.);
#53648=EDGE_CURVE('',#40894,#40895,#25829,.T.);
#53649=EDGE_CURVE('',#40895,#40891,#29739,.T.);
#53650=EDGE_CURVE('',#40893,#40887,#25830,.T.);
#53651=EDGE_CURVE('',#40886,#40894,#22074,.T.);
#53652=EDGE_CURVE('',#40895,#40896,#25831,.T.);
#53653=EDGE_CURVE('',#40897,#40894,#1070,.T.);
#53654=EDGE_CURVE('',#40896,#40897,#25832,.T.);
#53655=EDGE_CURVE('',#40897,#40886,#1071,.T.);
#53656=EDGE_CURVE('',#40898,#40890,#25833,.T.);
#53657=EDGE_CURVE('',#40897,#40898,#25834,.T.);
#53658=EDGE_CURVE('',#39115,#40896,#22075,.T.);
#53659=EDGE_CURVE('',#40898,#40896,#22076,.T.);
#53660=EDGE_CURVE('',#39116,#40898,#22077,.T.);
#53661=EDGE_CURVE('',#39114,#40895,#22078,.T.);
#53662=EDGE_CURVE('',#40891,#39113,#22079,.T.);
#53663=EDGE_CURVE('',#40892,#38812,#22080,.T.);
#53664=EDGE_CURVE('',#40893,#38811,#22081,.T.);
#53665=EDGE_CURVE('',#40887,#38810,#22082,.T.);
#53666=EDGE_CURVE('',#40888,#38809,#22083,.T.);
#53667=EDGE_CURVE('',#39118,#40889,#22084,.T.);
#53668=EDGE_CURVE('',#39117,#40890,#22085,.T.);
#53669=EDGE_CURVE('',#40899,#40900,#29740,.T.);
#53670=EDGE_CURVE('',#40900,#40901,#25835,.T.);
#53671=EDGE_CURVE('',#40901,#40902,#1072,.T.);
#53672=EDGE_CURVE('',#40902,#40903,#29741,.T.);
#53673=EDGE_CURVE('',#40903,#40899,#25836,.T.);
#53674=EDGE_CURVE('',#40904,#40905,#1073,.T.);
#53675=EDGE_CURVE('',#40905,#40906,#25837,.T.);
#53676=EDGE_CURVE('',#40907,#40906,#29742,.T.);
#53677=EDGE_CURVE('',#40907,#40908,#25838,.T.);
#53678=EDGE_CURVE('',#40908,#40904,#29743,.T.);
#53679=EDGE_CURVE('',#40906,#40900,#25839,.T.);
#53680=EDGE_CURVE('',#40899,#40907,#22086,.T.);
#53681=EDGE_CURVE('',#40908,#40909,#25840,.T.);
#53682=EDGE_CURVE('',#40910,#40907,#1074,.T.);
#53683=EDGE_CURVE('',#40909,#40910,#25841,.T.);
#53684=EDGE_CURVE('',#40910,#40899,#1075,.T.);
#53685=EDGE_CURVE('',#40911,#40903,#25842,.T.);
#53686=EDGE_CURVE('',#40910,#40911,#25843,.T.);
#53687=EDGE_CURVE('',#39109,#40909,#22087,.T.);
#53688=EDGE_CURVE('',#40911,#40909,#22088,.T.);
#53689=EDGE_CURVE('',#39110,#40911,#22089,.T.);
#53690=EDGE_CURVE('',#39108,#40908,#22090,.T.);
#53691=EDGE_CURVE('',#40904,#39107,#22091,.T.);
#53692=EDGE_CURVE('',#40905,#38816,#22092,.T.);
#53693=EDGE_CURVE('',#40906,#38815,#22093,.T.);
#53694=EDGE_CURVE('',#40900,#38814,#22094,.T.);
#53695=EDGE_CURVE('',#40901,#38813,#22095,.T.);
#53696=EDGE_CURVE('',#39112,#40902,#22096,.T.);
#53697=EDGE_CURVE('',#39111,#40903,#22097,.T.);
#53698=EDGE_CURVE('',#40912,#40913,#29744,.T.);
#53699=EDGE_CURVE('',#40913,#40914,#25844,.T.);
#53700=EDGE_CURVE('',#40914,#40915,#1076,.T.);
#53701=EDGE_CURVE('',#40915,#40916,#29745,.T.);
#53702=EDGE_CURVE('',#40916,#40912,#25845,.T.);
#53703=EDGE_CURVE('',#40917,#40918,#1077,.T.);
#53704=EDGE_CURVE('',#40918,#40919,#25846,.T.);
#53705=EDGE_CURVE('',#40920,#40919,#29746,.T.);
#53706=EDGE_CURVE('',#40920,#40921,#25847,.T.);
#53707=EDGE_CURVE('',#40921,#40917,#29747,.T.);
#53708=EDGE_CURVE('',#40919,#40913,#25848,.T.);
#53709=EDGE_CURVE('',#40912,#40920,#22098,.T.);
#53710=EDGE_CURVE('',#40921,#40922,#25849,.T.);
#53711=EDGE_CURVE('',#40923,#40920,#1078,.T.);
#53712=EDGE_CURVE('',#40922,#40923,#25850,.T.);
#53713=EDGE_CURVE('',#40923,#40912,#1079,.T.);
#53714=EDGE_CURVE('',#40924,#40916,#25851,.T.);
#53715=EDGE_CURVE('',#40923,#40924,#25852,.T.);
#53716=EDGE_CURVE('',#39103,#40922,#22099,.T.);
#53717=EDGE_CURVE('',#40924,#40922,#22100,.T.);
#53718=EDGE_CURVE('',#39104,#40924,#22101,.T.);
#53719=EDGE_CURVE('',#39102,#40921,#22102,.T.);
#53720=EDGE_CURVE('',#40917,#39101,#22103,.T.);
#53721=EDGE_CURVE('',#40918,#38820,#22104,.T.);
#53722=EDGE_CURVE('',#40919,#38819,#22105,.T.);
#53723=EDGE_CURVE('',#40913,#38818,#22106,.T.);
#53724=EDGE_CURVE('',#40914,#38817,#22107,.T.);
#53725=EDGE_CURVE('',#39106,#40915,#22108,.T.);
#53726=EDGE_CURVE('',#39105,#40916,#22109,.T.);
#69924=ORIENTED_EDGE('',*,*,#49464,.F.);
#69925=ORIENTED_EDGE('',*,*,#49465,.F.);
#69926=ORIENTED_EDGE('',*,*,#49466,.T.);
#69927=ORIENTED_EDGE('',*,*,#49467,.F.);
#69928=ORIENTED_EDGE('',*,*,#49468,.F.);
#69929=ORIENTED_EDGE('',*,*,#49464,.T.);
#69930=ORIENTED_EDGE('',*,*,#49469,.T.);
#69931=ORIENTED_EDGE('',*,*,#49470,.F.);
#69932=ORIENTED_EDGE('',*,*,#49471,.F.);
#69933=ORIENTED_EDGE('',*,*,#49467,.T.);
#69934=ORIENTED_EDGE('',*,*,#49472,.T.);
#69935=ORIENTED_EDGE('',*,*,#49473,.F.);
#69936=ORIENTED_EDGE('',*,*,#49474,.F.);
#69937=ORIENTED_EDGE('',*,*,#49470,.T.);
#69938=ORIENTED_EDGE('',*,*,#49475,.T.);
#69939=ORIENTED_EDGE('',*,*,#49476,.F.);
#69940=ORIENTED_EDGE('',*,*,#49477,.F.);
#69941=ORIENTED_EDGE('',*,*,#49473,.T.);
#69942=ORIENTED_EDGE('',*,*,#49478,.T.);
#69943=ORIENTED_EDGE('',*,*,#49479,.F.);
#69944=ORIENTED_EDGE('',*,*,#49480,.F.);
#69945=ORIENTED_EDGE('',*,*,#49476,.T.);
#69946=ORIENTED_EDGE('',*,*,#49481,.T.);
#69947=ORIENTED_EDGE('',*,*,#49482,.F.);
#69948=ORIENTED_EDGE('',*,*,#49483,.F.);
#69949=ORIENTED_EDGE('',*,*,#49479,.T.);
#69950=ORIENTED_EDGE('',*,*,#49484,.T.);
#69951=ORIENTED_EDGE('',*,*,#49485,.F.);
#69952=ORIENTED_EDGE('',*,*,#49486,.F.);
#69953=ORIENTED_EDGE('',*,*,#49482,.T.);
#69954=ORIENTED_EDGE('',*,*,#49487,.T.);
#69955=ORIENTED_EDGE('',*,*,#49488,.F.);
#69956=ORIENTED_EDGE('',*,*,#49489,.F.);
#69957=ORIENTED_EDGE('',*,*,#49485,.T.);
#69958=ORIENTED_EDGE('',*,*,#49490,.T.);
#69959=ORIENTED_EDGE('',*,*,#49491,.F.);
#69960=ORIENTED_EDGE('',*,*,#49492,.F.);
#69961=ORIENTED_EDGE('',*,*,#49488,.T.);
#69962=ORIENTED_EDGE('',*,*,#49493,.T.);
#69963=ORIENTED_EDGE('',*,*,#49494,.F.);
#69964=ORIENTED_EDGE('',*,*,#49495,.F.);
#69965=ORIENTED_EDGE('',*,*,#49491,.T.);
#69966=ORIENTED_EDGE('',*,*,#49496,.T.);
#69967=ORIENTED_EDGE('',*,*,#49497,.F.);
#69968=ORIENTED_EDGE('',*,*,#49498,.F.);
#69969=ORIENTED_EDGE('',*,*,#49494,.T.);
#69970=ORIENTED_EDGE('',*,*,#49499,.T.);
#69971=ORIENTED_EDGE('',*,*,#49500,.F.);
#69972=ORIENTED_EDGE('',*,*,#49501,.F.);
#69973=ORIENTED_EDGE('',*,*,#49497,.T.);
#69974=ORIENTED_EDGE('',*,*,#49502,.T.);
#69975=ORIENTED_EDGE('',*,*,#49503,.F.);
#69976=ORIENTED_EDGE('',*,*,#49504,.F.);
#69977=ORIENTED_EDGE('',*,*,#49500,.T.);
#69978=ORIENTED_EDGE('',*,*,#49505,.T.);
#69979=ORIENTED_EDGE('',*,*,#49506,.F.);
#69980=ORIENTED_EDGE('',*,*,#49507,.F.);
#69981=ORIENTED_EDGE('',*,*,#49503,.T.);
#69982=ORIENTED_EDGE('',*,*,#49508,.T.);
#69983=ORIENTED_EDGE('',*,*,#49509,.F.);
#69984=ORIENTED_EDGE('',*,*,#49510,.F.);
#69985=ORIENTED_EDGE('',*,*,#49506,.T.);
#69986=ORIENTED_EDGE('',*,*,#49511,.T.);
#69987=ORIENTED_EDGE('',*,*,#49512,.F.);
#69988=ORIENTED_EDGE('',*,*,#49513,.F.);
#69989=ORIENTED_EDGE('',*,*,#49509,.T.);
#69990=ORIENTED_EDGE('',*,*,#49514,.T.);
#69991=ORIENTED_EDGE('',*,*,#49515,.F.);
#69992=ORIENTED_EDGE('',*,*,#49516,.F.);
#69993=ORIENTED_EDGE('',*,*,#49512,.T.);
#69994=ORIENTED_EDGE('',*,*,#49517,.T.);
#69995=ORIENTED_EDGE('',*,*,#49518,.F.);
#69996=ORIENTED_EDGE('',*,*,#49519,.F.);
#69997=ORIENTED_EDGE('',*,*,#49515,.T.);
#69998=ORIENTED_EDGE('',*,*,#49520,.T.);
#69999=ORIENTED_EDGE('',*,*,#49521,.F.);
#70000=ORIENTED_EDGE('',*,*,#49522,.F.);
#70001=ORIENTED_EDGE('',*,*,#49518,.T.);
#70002=ORIENTED_EDGE('',*,*,#49523,.T.);
#70003=ORIENTED_EDGE('',*,*,#49524,.F.);
#70004=ORIENTED_EDGE('',*,*,#49525,.F.);
#70005=ORIENTED_EDGE('',*,*,#49521,.T.);
#70006=ORIENTED_EDGE('',*,*,#49526,.T.);
#70007=ORIENTED_EDGE('',*,*,#49527,.F.);
#70008=ORIENTED_EDGE('',*,*,#49528,.F.);
#70009=ORIENTED_EDGE('',*,*,#49524,.T.);
#70010=ORIENTED_EDGE('',*,*,#49529,.T.);
#70011=ORIENTED_EDGE('',*,*,#49530,.F.);
#70012=ORIENTED_EDGE('',*,*,#49531,.F.);
#70013=ORIENTED_EDGE('',*,*,#49527,.T.);
#70014=ORIENTED_EDGE('',*,*,#49532,.T.);
#70015=ORIENTED_EDGE('',*,*,#49533,.F.);
#70016=ORIENTED_EDGE('',*,*,#49534,.F.);
#70017=ORIENTED_EDGE('',*,*,#49530,.T.);
#70018=ORIENTED_EDGE('',*,*,#49535,.T.);
#70019=ORIENTED_EDGE('',*,*,#49536,.F.);
#70020=ORIENTED_EDGE('',*,*,#49537,.F.);
#70021=ORIENTED_EDGE('',*,*,#49533,.T.);
#70022=ORIENTED_EDGE('',*,*,#49538,.T.);
#70023=ORIENTED_EDGE('',*,*,#49539,.F.);
#70024=ORIENTED_EDGE('',*,*,#49540,.F.);
#70025=ORIENTED_EDGE('',*,*,#49536,.T.);
#70026=ORIENTED_EDGE('',*,*,#49541,.T.);
#70027=ORIENTED_EDGE('',*,*,#49542,.F.);
#70028=ORIENTED_EDGE('',*,*,#49543,.F.);
#70029=ORIENTED_EDGE('',*,*,#49539,.T.);
#70030=ORIENTED_EDGE('',*,*,#49544,.T.);
#70031=ORIENTED_EDGE('',*,*,#49545,.F.);
#70032=ORIENTED_EDGE('',*,*,#49546,.F.);
#70033=ORIENTED_EDGE('',*,*,#49542,.T.);
#70034=ORIENTED_EDGE('',*,*,#49547,.T.);
#70035=ORIENTED_EDGE('',*,*,#49548,.F.);
#70036=ORIENTED_EDGE('',*,*,#49549,.F.);
#70037=ORIENTED_EDGE('',*,*,#49545,.T.);
#70038=ORIENTED_EDGE('',*,*,#49550,.T.);
#70039=ORIENTED_EDGE('',*,*,#49551,.F.);
#70040=ORIENTED_EDGE('',*,*,#49552,.T.);
#70041=ORIENTED_EDGE('',*,*,#49553,.F.);
#70042=ORIENTED_EDGE('',*,*,#49554,.T.);
#70043=ORIENTED_EDGE('',*,*,#49555,.T.);
#70044=ORIENTED_EDGE('',*,*,#49554,.F.);
#70045=ORIENTED_EDGE('',*,*,#49556,.F.);
#70046=ORIENTED_EDGE('',*,*,#49557,.T.);
#70047=ORIENTED_EDGE('',*,*,#49558,.F.);
#70048=ORIENTED_EDGE('',*,*,#49559,.T.);
#70049=ORIENTED_EDGE('',*,*,#49551,.T.);
#70050=ORIENTED_EDGE('',*,*,#49560,.T.);
#70051=ORIENTED_EDGE('',*,*,#49561,.F.);
#70052=ORIENTED_EDGE('',*,*,#49562,.T.);
#70053=ORIENTED_EDGE('',*,*,#49558,.T.);
#70054=ORIENTED_EDGE('',*,*,#49563,.T.);
#70055=ORIENTED_EDGE('',*,*,#49564,.F.);
#70056=ORIENTED_EDGE('',*,*,#49565,.T.);
#70057=ORIENTED_EDGE('',*,*,#49561,.T.);
#70058=ORIENTED_EDGE('',*,*,#49566,.T.);
#70059=ORIENTED_EDGE('',*,*,#49567,.F.);
#70060=ORIENTED_EDGE('',*,*,#49568,.T.);
#70061=ORIENTED_EDGE('',*,*,#49564,.T.);
#70062=ORIENTED_EDGE('',*,*,#49569,.T.);
#70063=ORIENTED_EDGE('',*,*,#49570,.F.);
#70064=ORIENTED_EDGE('',*,*,#49571,.T.);
#70065=ORIENTED_EDGE('',*,*,#49567,.T.);
#70066=ORIENTED_EDGE('',*,*,#49572,.T.);
#70067=ORIENTED_EDGE('',*,*,#49573,.F.);
#70068=ORIENTED_EDGE('',*,*,#49574,.T.);
#70069=ORIENTED_EDGE('',*,*,#49570,.T.);
#70070=ORIENTED_EDGE('',*,*,#49575,.T.);
#70071=ORIENTED_EDGE('',*,*,#49576,.F.);
#70072=ORIENTED_EDGE('',*,*,#49577,.T.);
#70073=ORIENTED_EDGE('',*,*,#49573,.T.);
#70074=ORIENTED_EDGE('',*,*,#49578,.T.);
#70075=ORIENTED_EDGE('',*,*,#49579,.F.);
#70076=ORIENTED_EDGE('',*,*,#49580,.T.);
#70077=ORIENTED_EDGE('',*,*,#49576,.T.);
#70078=ORIENTED_EDGE('',*,*,#49581,.T.);
#70079=ORIENTED_EDGE('',*,*,#49582,.F.);
#70080=ORIENTED_EDGE('',*,*,#49583,.T.);
#70081=ORIENTED_EDGE('',*,*,#49579,.T.);
#70082=ORIENTED_EDGE('',*,*,#49584,.T.);
#70083=ORIENTED_EDGE('',*,*,#49585,.F.);
#70084=ORIENTED_EDGE('',*,*,#49586,.T.);
#70085=ORIENTED_EDGE('',*,*,#49582,.T.);
#70086=ORIENTED_EDGE('',*,*,#49587,.T.);
#70087=ORIENTED_EDGE('',*,*,#49588,.F.);
#70088=ORIENTED_EDGE('',*,*,#49589,.T.);
#70089=ORIENTED_EDGE('',*,*,#49585,.T.);
#70090=ORIENTED_EDGE('',*,*,#49590,.T.);
#70091=ORIENTED_EDGE('',*,*,#49591,.F.);
#70092=ORIENTED_EDGE('',*,*,#49592,.T.);
#70093=ORIENTED_EDGE('',*,*,#49588,.T.);
#70094=ORIENTED_EDGE('',*,*,#49593,.T.);
#70095=ORIENTED_EDGE('',*,*,#49594,.F.);
#70096=ORIENTED_EDGE('',*,*,#49595,.T.);
#70097=ORIENTED_EDGE('',*,*,#49591,.T.);
#70098=ORIENTED_EDGE('',*,*,#49596,.T.);
#70099=ORIENTED_EDGE('',*,*,#49597,.F.);
#70100=ORIENTED_EDGE('',*,*,#49598,.T.);
#70101=ORIENTED_EDGE('',*,*,#49594,.T.);
#70102=ORIENTED_EDGE('',*,*,#49599,.T.);
#70103=ORIENTED_EDGE('',*,*,#49600,.F.);
#70104=ORIENTED_EDGE('',*,*,#49601,.T.);
#70105=ORIENTED_EDGE('',*,*,#49597,.T.);
#70106=ORIENTED_EDGE('',*,*,#49602,.T.);
#70107=ORIENTED_EDGE('',*,*,#49603,.F.);
#70108=ORIENTED_EDGE('',*,*,#49604,.T.);
#70109=ORIENTED_EDGE('',*,*,#49600,.T.);
#70110=ORIENTED_EDGE('',*,*,#49605,.T.);
#70111=ORIENTED_EDGE('',*,*,#49606,.F.);
#70112=ORIENTED_EDGE('',*,*,#49607,.T.);
#70113=ORIENTED_EDGE('',*,*,#49603,.T.);
#70114=ORIENTED_EDGE('',*,*,#49608,.T.);
#70115=ORIENTED_EDGE('',*,*,#49609,.F.);
#70116=ORIENTED_EDGE('',*,*,#49610,.T.);
#70117=ORIENTED_EDGE('',*,*,#49606,.T.);
#70118=ORIENTED_EDGE('',*,*,#49611,.T.);
#70119=ORIENTED_EDGE('',*,*,#49612,.F.);
#70120=ORIENTED_EDGE('',*,*,#49613,.T.);
#70121=ORIENTED_EDGE('',*,*,#49609,.T.);
#70122=ORIENTED_EDGE('',*,*,#49614,.T.);
#70123=ORIENTED_EDGE('',*,*,#49615,.F.);
#70124=ORIENTED_EDGE('',*,*,#49616,.T.);
#70125=ORIENTED_EDGE('',*,*,#49612,.T.);
#70126=ORIENTED_EDGE('',*,*,#49617,.T.);
#70127=ORIENTED_EDGE('',*,*,#49618,.F.);
#70128=ORIENTED_EDGE('',*,*,#49619,.T.);
#70129=ORIENTED_EDGE('',*,*,#49615,.T.);
#70130=ORIENTED_EDGE('',*,*,#49620,.T.);
#70131=ORIENTED_EDGE('',*,*,#49621,.F.);
#70132=ORIENTED_EDGE('',*,*,#49622,.T.);
#70133=ORIENTED_EDGE('',*,*,#49618,.T.);
#70134=ORIENTED_EDGE('',*,*,#49623,.T.);
#70135=ORIENTED_EDGE('',*,*,#49624,.F.);
#70136=ORIENTED_EDGE('',*,*,#49625,.T.);
#70137=ORIENTED_EDGE('',*,*,#49621,.T.);
#70138=ORIENTED_EDGE('',*,*,#49626,.T.);
#70139=ORIENTED_EDGE('',*,*,#49627,.F.);
#70140=ORIENTED_EDGE('',*,*,#49628,.T.);
#70141=ORIENTED_EDGE('',*,*,#49624,.T.);
#70142=ORIENTED_EDGE('',*,*,#49629,.T.);
#70143=ORIENTED_EDGE('',*,*,#49630,.F.);
#70144=ORIENTED_EDGE('',*,*,#49631,.T.);
#70145=ORIENTED_EDGE('',*,*,#49627,.T.);
#70146=ORIENTED_EDGE('',*,*,#49632,.T.);
#70147=ORIENTED_EDGE('',*,*,#49633,.F.);
#70148=ORIENTED_EDGE('',*,*,#49634,.T.);
#70149=ORIENTED_EDGE('',*,*,#49630,.T.);
#70150=ORIENTED_EDGE('',*,*,#49635,.T.);
#70151=ORIENTED_EDGE('',*,*,#49636,.F.);
#70152=ORIENTED_EDGE('',*,*,#49637,.T.);
#70153=ORIENTED_EDGE('',*,*,#49633,.T.);
#70154=ORIENTED_EDGE('',*,*,#49638,.T.);
#70155=ORIENTED_EDGE('',*,*,#49639,.F.);
#70156=ORIENTED_EDGE('',*,*,#49640,.F.);
#70157=ORIENTED_EDGE('',*,*,#49641,.F.);
#70158=ORIENTED_EDGE('',*,*,#49642,.F.);
#70159=ORIENTED_EDGE('',*,*,#49643,.F.);
#70160=ORIENTED_EDGE('',*,*,#49644,.F.);
#70161=ORIENTED_EDGE('',*,*,#49645,.T.);
#70162=ORIENTED_EDGE('',*,*,#49643,.T.);
#70163=ORIENTED_EDGE('',*,*,#49646,.T.);
#70164=ORIENTED_EDGE('',*,*,#49647,.F.);
#70165=ORIENTED_EDGE('',*,*,#49648,.F.);
#70166=ORIENTED_EDGE('',*,*,#49649,.F.);
#70167=ORIENTED_EDGE('',*,*,#49639,.T.);
#70168=ORIENTED_EDGE('',*,*,#49650,.F.);
#70169=ORIENTED_EDGE('',*,*,#49556,.T.);
#70170=ORIENTED_EDGE('',*,*,#49553,.T.);
#70171=ORIENTED_EDGE('',*,*,#49636,.T.);
#70172=ORIENTED_EDGE('',*,*,#49651,.T.);
#70173=ORIENTED_EDGE('',*,*,#49648,.T.);
#70174=ORIENTED_EDGE('',*,*,#49652,.T.);
#70175=ORIENTED_EDGE('',*,*,#49555,.F.);
#70176=ORIENTED_EDGE('',*,*,#49653,.T.);
#70177=ORIENTED_EDGE('',*,*,#49654,.T.);
#70178=ORIENTED_EDGE('',*,*,#49653,.F.);
#70179=ORIENTED_EDGE('',*,*,#49655,.T.);
#70180=ORIENTED_EDGE('',*,*,#49656,.F.);
#70181=ORIENTED_EDGE('',*,*,#49657,.F.);
#70182=ORIENTED_EDGE('',*,*,#49658,.F.);
#70183=ORIENTED_EDGE('',*,*,#49659,.T.);
#70184=ORIENTED_EDGE('',*,*,#49660,.F.);
#70185=ORIENTED_EDGE('',*,*,#49661,.F.);
#70186=ORIENTED_EDGE('',*,*,#49655,.F.);
#70187=ORIENTED_EDGE('',*,*,#49662,.T.);
#70188=ORIENTED_EDGE('',*,*,#49663,.T.);
#70189=ORIENTED_EDGE('',*,*,#49664,.F.);
#70190=ORIENTED_EDGE('',*,*,#49665,.T.);
#70191=ORIENTED_EDGE('',*,*,#49666,.T.);
#70192=ORIENTED_EDGE('',*,*,#49665,.F.);
#70193=ORIENTED_EDGE('',*,*,#49667,.F.);
#70194=ORIENTED_EDGE('',*,*,#49668,.T.);
#70195=ORIENTED_EDGE('',*,*,#49664,.T.);
#70196=ORIENTED_EDGE('',*,*,#49668,.F.);
#70197=ORIENTED_EDGE('',*,*,#49669,.F.);
#70198=ORIENTED_EDGE('',*,*,#49670,.T.);
#70199=ORIENTED_EDGE('',*,*,#49667,.T.);
#70200=ORIENTED_EDGE('',*,*,#49670,.F.);
#70201=ORIENTED_EDGE('',*,*,#49671,.T.);
#70202=ORIENTED_EDGE('',*,*,#49672,.T.);
#70203=ORIENTED_EDGE('',*,*,#49673,.T.);
#70204=ORIENTED_EDGE('',*,*,#49674,.T.);
#70205=ORIENTED_EDGE('',*,*,#49675,.T.);
#70206=ORIENTED_EDGE('',*,*,#49676,.T.);
#70207=ORIENTED_EDGE('',*,*,#49677,.T.);
#70208=ORIENTED_EDGE('',*,*,#49678,.T.);
#70209=ORIENTED_EDGE('',*,*,#49679,.T.);
#70210=ORIENTED_EDGE('',*,*,#49680,.T.);
#70211=ORIENTED_EDGE('',*,*,#49681,.T.);
#70212=ORIENTED_EDGE('',*,*,#49682,.T.);
#70213=ORIENTED_EDGE('',*,*,#49683,.T.);
#70214=ORIENTED_EDGE('',*,*,#49684,.T.);
#70215=ORIENTED_EDGE('',*,*,#49685,.T.);
#70216=ORIENTED_EDGE('',*,*,#49686,.T.);
#70217=ORIENTED_EDGE('',*,*,#49687,.T.);
#70218=ORIENTED_EDGE('',*,*,#49688,.T.);
#70219=ORIENTED_EDGE('',*,*,#49689,.T.);
#70220=ORIENTED_EDGE('',*,*,#49690,.T.);
#70221=ORIENTED_EDGE('',*,*,#49691,.T.);
#70222=ORIENTED_EDGE('',*,*,#49692,.T.);
#70223=ORIENTED_EDGE('',*,*,#49693,.T.);
#70224=ORIENTED_EDGE('',*,*,#49694,.T.);
#70225=ORIENTED_EDGE('',*,*,#49695,.T.);
#70226=ORIENTED_EDGE('',*,*,#49696,.T.);
#70227=ORIENTED_EDGE('',*,*,#49697,.T.);
#70228=ORIENTED_EDGE('',*,*,#49698,.T.);
#70229=ORIENTED_EDGE('',*,*,#49699,.T.);
#70230=ORIENTED_EDGE('',*,*,#49700,.T.);
#70231=ORIENTED_EDGE('',*,*,#49701,.T.);
#70232=ORIENTED_EDGE('',*,*,#49702,.T.);
#70233=ORIENTED_EDGE('',*,*,#49703,.T.);
#70234=ORIENTED_EDGE('',*,*,#49704,.T.);
#70235=ORIENTED_EDGE('',*,*,#49705,.T.);
#70236=ORIENTED_EDGE('',*,*,#49706,.T.);
#70237=ORIENTED_EDGE('',*,*,#49707,.T.);
#70238=ORIENTED_EDGE('',*,*,#49708,.T.);
#70239=ORIENTED_EDGE('',*,*,#49709,.T.);
#70240=ORIENTED_EDGE('',*,*,#49710,.T.);
#70241=ORIENTED_EDGE('',*,*,#49711,.T.);
#70242=ORIENTED_EDGE('',*,*,#49712,.T.);
#70243=ORIENTED_EDGE('',*,*,#49713,.T.);
#70244=ORIENTED_EDGE('',*,*,#49714,.T.);
#70245=ORIENTED_EDGE('',*,*,#49715,.T.);
#70246=ORIENTED_EDGE('',*,*,#49716,.T.);
#70247=ORIENTED_EDGE('',*,*,#49717,.T.);
#70248=ORIENTED_EDGE('',*,*,#49718,.T.);
#70249=ORIENTED_EDGE('',*,*,#49719,.T.);
#70250=ORIENTED_EDGE('',*,*,#49720,.T.);
#70251=ORIENTED_EDGE('',*,*,#49721,.T.);
#70252=ORIENTED_EDGE('',*,*,#49722,.T.);
#70253=ORIENTED_EDGE('',*,*,#49723,.T.);
#70254=ORIENTED_EDGE('',*,*,#49724,.T.);
#70255=ORIENTED_EDGE('',*,*,#49725,.T.);
#70256=ORIENTED_EDGE('',*,*,#49726,.T.);
#70257=ORIENTED_EDGE('',*,*,#49727,.T.);
#70258=ORIENTED_EDGE('',*,*,#49728,.T.);
#70259=ORIENTED_EDGE('',*,*,#49729,.T.);
#70260=ORIENTED_EDGE('',*,*,#49730,.T.);
#70261=ORIENTED_EDGE('',*,*,#49731,.T.);
#70262=ORIENTED_EDGE('',*,*,#49732,.T.);
#70263=ORIENTED_EDGE('',*,*,#49733,.T.);
#70264=ORIENTED_EDGE('',*,*,#49734,.T.);
#70265=ORIENTED_EDGE('',*,*,#49735,.T.);
#70266=ORIENTED_EDGE('',*,*,#49736,.T.);
#70267=ORIENTED_EDGE('',*,*,#49737,.T.);
#70268=ORIENTED_EDGE('',*,*,#49738,.T.);
#70269=ORIENTED_EDGE('',*,*,#49739,.T.);
#70270=ORIENTED_EDGE('',*,*,#49740,.T.);
#70271=ORIENTED_EDGE('',*,*,#49741,.T.);
#70272=ORIENTED_EDGE('',*,*,#49742,.T.);
#70273=ORIENTED_EDGE('',*,*,#49743,.T.);
#70274=ORIENTED_EDGE('',*,*,#49744,.T.);
#70275=ORIENTED_EDGE('',*,*,#49745,.T.);
#70276=ORIENTED_EDGE('',*,*,#49746,.T.);
#70277=ORIENTED_EDGE('',*,*,#49747,.T.);
#70278=ORIENTED_EDGE('',*,*,#49748,.T.);
#70279=ORIENTED_EDGE('',*,*,#49749,.T.);
#70280=ORIENTED_EDGE('',*,*,#49750,.T.);
#70281=ORIENTED_EDGE('',*,*,#49751,.T.);
#70282=ORIENTED_EDGE('',*,*,#49752,.T.);
#70283=ORIENTED_EDGE('',*,*,#49753,.T.);
#70284=ORIENTED_EDGE('',*,*,#49754,.T.);
#70285=ORIENTED_EDGE('',*,*,#49755,.T.);
#70286=ORIENTED_EDGE('',*,*,#49756,.T.);
#70287=ORIENTED_EDGE('',*,*,#49757,.T.);
#70288=ORIENTED_EDGE('',*,*,#49758,.T.);
#70289=ORIENTED_EDGE('',*,*,#49759,.T.);
#70290=ORIENTED_EDGE('',*,*,#49760,.T.);
#70291=ORIENTED_EDGE('',*,*,#49761,.T.);
#70292=ORIENTED_EDGE('',*,*,#49762,.T.);
#70293=ORIENTED_EDGE('',*,*,#49763,.T.);
#70294=ORIENTED_EDGE('',*,*,#49764,.T.);
#70295=ORIENTED_EDGE('',*,*,#49765,.T.);
#70296=ORIENTED_EDGE('',*,*,#49766,.T.);
#70297=ORIENTED_EDGE('',*,*,#49767,.T.);
#70298=ORIENTED_EDGE('',*,*,#49768,.T.);
#70299=ORIENTED_EDGE('',*,*,#49769,.T.);
#70300=ORIENTED_EDGE('',*,*,#49770,.T.);
#70301=ORIENTED_EDGE('',*,*,#49771,.T.);
#70302=ORIENTED_EDGE('',*,*,#49772,.T.);
#70303=ORIENTED_EDGE('',*,*,#49773,.T.);
#70304=ORIENTED_EDGE('',*,*,#49774,.T.);
#70305=ORIENTED_EDGE('',*,*,#49775,.T.);
#70306=ORIENTED_EDGE('',*,*,#49776,.T.);
#70307=ORIENTED_EDGE('',*,*,#49777,.T.);
#70308=ORIENTED_EDGE('',*,*,#49778,.T.);
#70309=ORIENTED_EDGE('',*,*,#49779,.T.);
#70310=ORIENTED_EDGE('',*,*,#49780,.T.);
#70311=ORIENTED_EDGE('',*,*,#49781,.T.);
#70312=ORIENTED_EDGE('',*,*,#49782,.T.);
#70313=ORIENTED_EDGE('',*,*,#49783,.T.);
#70314=ORIENTED_EDGE('',*,*,#49784,.T.);
#70315=ORIENTED_EDGE('',*,*,#49785,.T.);
#70316=ORIENTED_EDGE('',*,*,#49786,.T.);
#70317=ORIENTED_EDGE('',*,*,#49787,.T.);
#70318=ORIENTED_EDGE('',*,*,#49788,.T.);
#70319=ORIENTED_EDGE('',*,*,#49789,.T.);
#70320=ORIENTED_EDGE('',*,*,#49790,.T.);
#70321=ORIENTED_EDGE('',*,*,#49791,.T.);
#70322=ORIENTED_EDGE('',*,*,#49792,.T.);
#70323=ORIENTED_EDGE('',*,*,#49793,.T.);
#70324=ORIENTED_EDGE('',*,*,#49794,.T.);
#70325=ORIENTED_EDGE('',*,*,#49795,.T.);
#70326=ORIENTED_EDGE('',*,*,#49796,.T.);
#70327=ORIENTED_EDGE('',*,*,#49797,.T.);
#70328=ORIENTED_EDGE('',*,*,#49798,.T.);
#70329=ORIENTED_EDGE('',*,*,#49799,.T.);
#70330=ORIENTED_EDGE('',*,*,#49800,.T.);
#70331=ORIENTED_EDGE('',*,*,#49801,.T.);
#70332=ORIENTED_EDGE('',*,*,#49802,.T.);
#70333=ORIENTED_EDGE('',*,*,#49803,.T.);
#70334=ORIENTED_EDGE('',*,*,#49804,.T.);
#70335=ORIENTED_EDGE('',*,*,#49805,.T.);
#70336=ORIENTED_EDGE('',*,*,#49806,.T.);
#70337=ORIENTED_EDGE('',*,*,#49807,.T.);
#70338=ORIENTED_EDGE('',*,*,#49808,.T.);
#70339=ORIENTED_EDGE('',*,*,#49809,.T.);
#70340=ORIENTED_EDGE('',*,*,#49810,.T.);
#70341=ORIENTED_EDGE('',*,*,#49811,.T.);
#70342=ORIENTED_EDGE('',*,*,#49812,.T.);
#70343=ORIENTED_EDGE('',*,*,#49813,.T.);
#70344=ORIENTED_EDGE('',*,*,#49814,.T.);
#70345=ORIENTED_EDGE('',*,*,#49815,.T.);
#70346=ORIENTED_EDGE('',*,*,#49816,.T.);
#70347=ORIENTED_EDGE('',*,*,#49817,.T.);
#70348=ORIENTED_EDGE('',*,*,#49818,.T.);
#70349=ORIENTED_EDGE('',*,*,#49819,.T.);
#70350=ORIENTED_EDGE('',*,*,#49820,.T.);
#70351=ORIENTED_EDGE('',*,*,#49821,.T.);
#70352=ORIENTED_EDGE('',*,*,#49822,.T.);
#70353=ORIENTED_EDGE('',*,*,#49823,.T.);
#70354=ORIENTED_EDGE('',*,*,#49824,.T.);
#70355=ORIENTED_EDGE('',*,*,#49825,.T.);
#70356=ORIENTED_EDGE('',*,*,#49826,.T.);
#70357=ORIENTED_EDGE('',*,*,#49827,.T.);
#70358=ORIENTED_EDGE('',*,*,#49828,.T.);
#70359=ORIENTED_EDGE('',*,*,#49829,.T.);
#70360=ORIENTED_EDGE('',*,*,#49830,.T.);
#70361=ORIENTED_EDGE('',*,*,#49831,.T.);
#70362=ORIENTED_EDGE('',*,*,#49832,.T.);
#70363=ORIENTED_EDGE('',*,*,#49833,.T.);
#70364=ORIENTED_EDGE('',*,*,#49834,.T.);
#70365=ORIENTED_EDGE('',*,*,#49835,.T.);
#70366=ORIENTED_EDGE('',*,*,#49836,.T.);
#70367=ORIENTED_EDGE('',*,*,#49837,.T.);
#70368=ORIENTED_EDGE('',*,*,#49838,.T.);
#70369=ORIENTED_EDGE('',*,*,#49839,.T.);
#70370=ORIENTED_EDGE('',*,*,#49840,.T.);
#70371=ORIENTED_EDGE('',*,*,#49841,.T.);
#70372=ORIENTED_EDGE('',*,*,#49842,.T.);
#70373=ORIENTED_EDGE('',*,*,#49843,.T.);
#70374=ORIENTED_EDGE('',*,*,#49844,.T.);
#70375=ORIENTED_EDGE('',*,*,#49845,.T.);
#70376=ORIENTED_EDGE('',*,*,#49846,.T.);
#70377=ORIENTED_EDGE('',*,*,#49847,.T.);
#70378=ORIENTED_EDGE('',*,*,#49848,.T.);
#70379=ORIENTED_EDGE('',*,*,#49849,.T.);
#70380=ORIENTED_EDGE('',*,*,#49850,.T.);
#70381=ORIENTED_EDGE('',*,*,#49851,.T.);
#70382=ORIENTED_EDGE('',*,*,#49852,.T.);
#70383=ORIENTED_EDGE('',*,*,#49853,.T.);
#70384=ORIENTED_EDGE('',*,*,#49854,.T.);
#70385=ORIENTED_EDGE('',*,*,#49855,.T.);
#70386=ORIENTED_EDGE('',*,*,#49856,.T.);
#70387=ORIENTED_EDGE('',*,*,#49857,.T.);
#70388=ORIENTED_EDGE('',*,*,#49858,.T.);
#70389=ORIENTED_EDGE('',*,*,#49859,.T.);
#70390=ORIENTED_EDGE('',*,*,#49860,.T.);
#70391=ORIENTED_EDGE('',*,*,#49861,.T.);
#70392=ORIENTED_EDGE('',*,*,#49862,.T.);
#70393=ORIENTED_EDGE('',*,*,#49863,.T.);
#70394=ORIENTED_EDGE('',*,*,#49864,.T.);
#70395=ORIENTED_EDGE('',*,*,#49865,.T.);
#70396=ORIENTED_EDGE('',*,*,#49866,.T.);
#70397=ORIENTED_EDGE('',*,*,#49867,.T.);
#70398=ORIENTED_EDGE('',*,*,#49868,.T.);
#70399=ORIENTED_EDGE('',*,*,#49869,.F.);
#70400=ORIENTED_EDGE('',*,*,#49870,.F.);
#70401=ORIENTED_EDGE('',*,*,#49868,.F.);
#70402=ORIENTED_EDGE('',*,*,#49871,.T.);
#70403=ORIENTED_EDGE('',*,*,#49872,.T.);
#70404=ORIENTED_EDGE('',*,*,#49873,.T.);
#70405=ORIENTED_EDGE('',*,*,#49874,.T.);
#70406=ORIENTED_EDGE('',*,*,#49875,.T.);
#70407=ORIENTED_EDGE('',*,*,#49876,.T.);
#70408=ORIENTED_EDGE('',*,*,#49877,.T.);
#70409=ORIENTED_EDGE('',*,*,#49878,.T.);
#70410=ORIENTED_EDGE('',*,*,#49879,.T.);
#70411=ORIENTED_EDGE('',*,*,#49880,.T.);
#70412=ORIENTED_EDGE('',*,*,#49881,.T.);
#70413=ORIENTED_EDGE('',*,*,#49882,.T.);
#70414=ORIENTED_EDGE('',*,*,#49883,.T.);
#70415=ORIENTED_EDGE('',*,*,#49884,.T.);
#70416=ORIENTED_EDGE('',*,*,#49885,.T.);
#70417=ORIENTED_EDGE('',*,*,#49886,.T.);
#70418=ORIENTED_EDGE('',*,*,#49887,.T.);
#70419=ORIENTED_EDGE('',*,*,#49888,.T.);
#70420=ORIENTED_EDGE('',*,*,#49889,.T.);
#70421=ORIENTED_EDGE('',*,*,#49890,.T.);
#70422=ORIENTED_EDGE('',*,*,#49891,.T.);
#70423=ORIENTED_EDGE('',*,*,#49892,.T.);
#70424=ORIENTED_EDGE('',*,*,#49893,.T.);
#70425=ORIENTED_EDGE('',*,*,#49894,.T.);
#70426=ORIENTED_EDGE('',*,*,#49895,.T.);
#70427=ORIENTED_EDGE('',*,*,#49896,.T.);
#70428=ORIENTED_EDGE('',*,*,#49897,.T.);
#70429=ORIENTED_EDGE('',*,*,#49898,.T.);
#70430=ORIENTED_EDGE('',*,*,#49899,.T.);
#70431=ORIENTED_EDGE('',*,*,#49900,.T.);
#70432=ORIENTED_EDGE('',*,*,#49901,.T.);
#70433=ORIENTED_EDGE('',*,*,#49902,.T.);
#70434=ORIENTED_EDGE('',*,*,#49903,.T.);
#70435=ORIENTED_EDGE('',*,*,#49904,.T.);
#70436=ORIENTED_EDGE('',*,*,#49905,.T.);
#70437=ORIENTED_EDGE('',*,*,#49906,.T.);
#70438=ORIENTED_EDGE('',*,*,#49907,.T.);
#70439=ORIENTED_EDGE('',*,*,#49908,.T.);
#70440=ORIENTED_EDGE('',*,*,#49909,.T.);
#70441=ORIENTED_EDGE('',*,*,#49910,.T.);
#70442=ORIENTED_EDGE('',*,*,#49911,.T.);
#70443=ORIENTED_EDGE('',*,*,#49912,.T.);
#70444=ORIENTED_EDGE('',*,*,#49913,.T.);
#70445=ORIENTED_EDGE('',*,*,#49914,.T.);
#70446=ORIENTED_EDGE('',*,*,#49915,.T.);
#70447=ORIENTED_EDGE('',*,*,#49916,.T.);
#70448=ORIENTED_EDGE('',*,*,#49917,.T.);
#70449=ORIENTED_EDGE('',*,*,#49918,.T.);
#70450=ORIENTED_EDGE('',*,*,#49919,.T.);
#70451=ORIENTED_EDGE('',*,*,#49920,.T.);
#70452=ORIENTED_EDGE('',*,*,#49921,.T.);
#70453=ORIENTED_EDGE('',*,*,#49922,.T.);
#70454=ORIENTED_EDGE('',*,*,#49923,.T.);
#70455=ORIENTED_EDGE('',*,*,#49924,.T.);
#70456=ORIENTED_EDGE('',*,*,#49925,.T.);
#70457=ORIENTED_EDGE('',*,*,#49926,.T.);
#70458=ORIENTED_EDGE('',*,*,#49927,.T.);
#70459=ORIENTED_EDGE('',*,*,#49928,.T.);
#70460=ORIENTED_EDGE('',*,*,#49929,.T.);
#70461=ORIENTED_EDGE('',*,*,#49930,.T.);
#70462=ORIENTED_EDGE('',*,*,#49931,.T.);
#70463=ORIENTED_EDGE('',*,*,#49932,.T.);
#70464=ORIENTED_EDGE('',*,*,#49933,.T.);
#70465=ORIENTED_EDGE('',*,*,#49934,.T.);
#70466=ORIENTED_EDGE('',*,*,#49935,.T.);
#70467=ORIENTED_EDGE('',*,*,#49936,.T.);
#70468=ORIENTED_EDGE('',*,*,#49937,.T.);
#70469=ORIENTED_EDGE('',*,*,#49938,.T.);
#70470=ORIENTED_EDGE('',*,*,#49939,.T.);
#70471=ORIENTED_EDGE('',*,*,#49940,.T.);
#70472=ORIENTED_EDGE('',*,*,#49941,.T.);
#70473=ORIENTED_EDGE('',*,*,#49942,.T.);
#70474=ORIENTED_EDGE('',*,*,#49943,.T.);
#70475=ORIENTED_EDGE('',*,*,#49944,.T.);
#70476=ORIENTED_EDGE('',*,*,#49945,.T.);
#70477=ORIENTED_EDGE('',*,*,#49946,.T.);
#70478=ORIENTED_EDGE('',*,*,#49947,.T.);
#70479=ORIENTED_EDGE('',*,*,#49948,.T.);
#70480=ORIENTED_EDGE('',*,*,#49949,.T.);
#70481=ORIENTED_EDGE('',*,*,#49950,.T.);
#70482=ORIENTED_EDGE('',*,*,#49951,.T.);
#70483=ORIENTED_EDGE('',*,*,#49952,.T.);
#70484=ORIENTED_EDGE('',*,*,#49953,.T.);
#70485=ORIENTED_EDGE('',*,*,#49954,.T.);
#70486=ORIENTED_EDGE('',*,*,#49955,.T.);
#70487=ORIENTED_EDGE('',*,*,#49956,.T.);
#70488=ORIENTED_EDGE('',*,*,#49957,.T.);
#70489=ORIENTED_EDGE('',*,*,#49958,.T.);
#70490=ORIENTED_EDGE('',*,*,#49959,.T.);
#70491=ORIENTED_EDGE('',*,*,#49960,.T.);
#70492=ORIENTED_EDGE('',*,*,#49961,.T.);
#70493=ORIENTED_EDGE('',*,*,#49962,.T.);
#70494=ORIENTED_EDGE('',*,*,#49963,.T.);
#70495=ORIENTED_EDGE('',*,*,#49964,.T.);
#70496=ORIENTED_EDGE('',*,*,#49965,.T.);
#70497=ORIENTED_EDGE('',*,*,#49966,.T.);
#70498=ORIENTED_EDGE('',*,*,#49967,.T.);
#70499=ORIENTED_EDGE('',*,*,#49968,.T.);
#70500=ORIENTED_EDGE('',*,*,#49969,.T.);
#70501=ORIENTED_EDGE('',*,*,#49970,.T.);
#70502=ORIENTED_EDGE('',*,*,#49971,.T.);
#70503=ORIENTED_EDGE('',*,*,#49972,.T.);
#70504=ORIENTED_EDGE('',*,*,#49973,.T.);
#70505=ORIENTED_EDGE('',*,*,#49974,.T.);
#70506=ORIENTED_EDGE('',*,*,#49975,.T.);
#70507=ORIENTED_EDGE('',*,*,#49976,.T.);
#70508=ORIENTED_EDGE('',*,*,#49977,.T.);
#70509=ORIENTED_EDGE('',*,*,#49978,.T.);
#70510=ORIENTED_EDGE('',*,*,#49979,.T.);
#70511=ORIENTED_EDGE('',*,*,#49980,.T.);
#70512=ORIENTED_EDGE('',*,*,#49981,.T.);
#70513=ORIENTED_EDGE('',*,*,#49982,.T.);
#70514=ORIENTED_EDGE('',*,*,#49983,.T.);
#70515=ORIENTED_EDGE('',*,*,#49984,.T.);
#70516=ORIENTED_EDGE('',*,*,#49985,.T.);
#70517=ORIENTED_EDGE('',*,*,#49986,.T.);
#70518=ORIENTED_EDGE('',*,*,#49987,.T.);
#70519=ORIENTED_EDGE('',*,*,#49988,.T.);
#70520=ORIENTED_EDGE('',*,*,#49989,.T.);
#70521=ORIENTED_EDGE('',*,*,#49990,.T.);
#70522=ORIENTED_EDGE('',*,*,#49991,.T.);
#70523=ORIENTED_EDGE('',*,*,#49992,.T.);
#70524=ORIENTED_EDGE('',*,*,#49993,.T.);
#70525=ORIENTED_EDGE('',*,*,#49994,.T.);
#70526=ORIENTED_EDGE('',*,*,#49995,.T.);
#70527=ORIENTED_EDGE('',*,*,#49996,.T.);
#70528=ORIENTED_EDGE('',*,*,#49997,.T.);
#70529=ORIENTED_EDGE('',*,*,#49998,.T.);
#70530=ORIENTED_EDGE('',*,*,#49999,.T.);
#70531=ORIENTED_EDGE('',*,*,#50000,.T.);
#70532=ORIENTED_EDGE('',*,*,#50001,.T.);
#70533=ORIENTED_EDGE('',*,*,#50002,.T.);
#70534=ORIENTED_EDGE('',*,*,#50003,.T.);
#70535=ORIENTED_EDGE('',*,*,#50004,.T.);
#70536=ORIENTED_EDGE('',*,*,#50005,.T.);
#70537=ORIENTED_EDGE('',*,*,#50006,.T.);
#70538=ORIENTED_EDGE('',*,*,#50007,.T.);
#70539=ORIENTED_EDGE('',*,*,#50008,.T.);
#70540=ORIENTED_EDGE('',*,*,#50009,.T.);
#70541=ORIENTED_EDGE('',*,*,#50010,.T.);
#70542=ORIENTED_EDGE('',*,*,#50011,.T.);
#70543=ORIENTED_EDGE('',*,*,#50012,.T.);
#70544=ORIENTED_EDGE('',*,*,#50013,.T.);
#70545=ORIENTED_EDGE('',*,*,#50014,.T.);
#70546=ORIENTED_EDGE('',*,*,#50015,.T.);
#70547=ORIENTED_EDGE('',*,*,#50016,.T.);
#70548=ORIENTED_EDGE('',*,*,#50017,.T.);
#70549=ORIENTED_EDGE('',*,*,#50018,.T.);
#70550=ORIENTED_EDGE('',*,*,#50019,.T.);
#70551=ORIENTED_EDGE('',*,*,#50020,.T.);
#70552=ORIENTED_EDGE('',*,*,#50021,.T.);
#70553=ORIENTED_EDGE('',*,*,#50022,.T.);
#70554=ORIENTED_EDGE('',*,*,#50023,.T.);
#70555=ORIENTED_EDGE('',*,*,#50024,.T.);
#70556=ORIENTED_EDGE('',*,*,#50025,.T.);
#70557=ORIENTED_EDGE('',*,*,#50026,.T.);
#70558=ORIENTED_EDGE('',*,*,#50027,.T.);
#70559=ORIENTED_EDGE('',*,*,#50028,.T.);
#70560=ORIENTED_EDGE('',*,*,#50029,.T.);
#70561=ORIENTED_EDGE('',*,*,#50030,.T.);
#70562=ORIENTED_EDGE('',*,*,#50031,.T.);
#70563=ORIENTED_EDGE('',*,*,#50032,.T.);
#70564=ORIENTED_EDGE('',*,*,#50033,.T.);
#70565=ORIENTED_EDGE('',*,*,#50034,.T.);
#70566=ORIENTED_EDGE('',*,*,#50035,.T.);
#70567=ORIENTED_EDGE('',*,*,#50036,.T.);
#70568=ORIENTED_EDGE('',*,*,#50037,.T.);
#70569=ORIENTED_EDGE('',*,*,#50038,.T.);
#70570=ORIENTED_EDGE('',*,*,#50039,.T.);
#70571=ORIENTED_EDGE('',*,*,#50040,.T.);
#70572=ORIENTED_EDGE('',*,*,#50041,.T.);
#70573=ORIENTED_EDGE('',*,*,#50042,.T.);
#70574=ORIENTED_EDGE('',*,*,#50043,.T.);
#70575=ORIENTED_EDGE('',*,*,#50044,.T.);
#70576=ORIENTED_EDGE('',*,*,#50045,.T.);
#70577=ORIENTED_EDGE('',*,*,#50046,.T.);
#70578=ORIENTED_EDGE('',*,*,#50047,.T.);
#70579=ORIENTED_EDGE('',*,*,#50048,.T.);
#70580=ORIENTED_EDGE('',*,*,#50049,.T.);
#70581=ORIENTED_EDGE('',*,*,#50050,.T.);
#70582=ORIENTED_EDGE('',*,*,#50051,.T.);
#70583=ORIENTED_EDGE('',*,*,#50052,.T.);
#70584=ORIENTED_EDGE('',*,*,#50053,.T.);
#70585=ORIENTED_EDGE('',*,*,#50054,.T.);
#70586=ORIENTED_EDGE('',*,*,#50055,.T.);
#70587=ORIENTED_EDGE('',*,*,#50056,.T.);
#70588=ORIENTED_EDGE('',*,*,#50057,.T.);
#70589=ORIENTED_EDGE('',*,*,#50058,.T.);
#70590=ORIENTED_EDGE('',*,*,#50059,.T.);
#70591=ORIENTED_EDGE('',*,*,#50060,.T.);
#70592=ORIENTED_EDGE('',*,*,#50061,.T.);
#70593=ORIENTED_EDGE('',*,*,#50062,.T.);
#70594=ORIENTED_EDGE('',*,*,#50063,.T.);
#70595=ORIENTED_EDGE('',*,*,#50064,.T.);
#70596=ORIENTED_EDGE('',*,*,#50065,.T.);
#70597=ORIENTED_EDGE('',*,*,#50066,.T.);
#70598=ORIENTED_EDGE('',*,*,#50067,.F.);
#70599=ORIENTED_EDGE('',*,*,#50068,.T.);
#70600=ORIENTED_EDGE('',*,*,#49869,.T.);
#70601=ORIENTED_EDGE('',*,*,#49870,.T.);
#70602=ORIENTED_EDGE('',*,*,#50068,.F.);
#70603=ORIENTED_EDGE('',*,*,#50069,.F.);
#70604=ORIENTED_EDGE('',*,*,#50070,.T.);
#70605=ORIENTED_EDGE('',*,*,#50071,.F.);
#70606=ORIENTED_EDGE('',*,*,#50072,.T.);
#70607=ORIENTED_EDGE('',*,*,#50073,.F.);
#70608=ORIENTED_EDGE('',*,*,#50074,.T.);
#70609=ORIENTED_EDGE('',*,*,#50075,.F.);
#70610=ORIENTED_EDGE('',*,*,#50076,.T.);
#70611=ORIENTED_EDGE('',*,*,#50077,.F.);
#70612=ORIENTED_EDGE('',*,*,#50078,.T.);
#70613=ORIENTED_EDGE('',*,*,#50079,.F.);
#70614=ORIENTED_EDGE('',*,*,#50080,.T.);
#70615=ORIENTED_EDGE('',*,*,#50081,.F.);
#70616=ORIENTED_EDGE('',*,*,#50082,.T.);
#70617=ORIENTED_EDGE('',*,*,#50083,.F.);
#70618=ORIENTED_EDGE('',*,*,#50084,.T.);
#70619=ORIENTED_EDGE('',*,*,#50085,.F.);
#70620=ORIENTED_EDGE('',*,*,#50086,.T.);
#70621=ORIENTED_EDGE('',*,*,#50087,.F.);
#70622=ORIENTED_EDGE('',*,*,#50088,.T.);
#70623=ORIENTED_EDGE('',*,*,#50089,.F.);
#70624=ORIENTED_EDGE('',*,*,#50090,.T.);
#70625=ORIENTED_EDGE('',*,*,#50091,.F.);
#70626=ORIENTED_EDGE('',*,*,#50092,.T.);
#70627=ORIENTED_EDGE('',*,*,#50093,.F.);
#70628=ORIENTED_EDGE('',*,*,#50094,.T.);
#70629=ORIENTED_EDGE('',*,*,#50095,.F.);
#70630=ORIENTED_EDGE('',*,*,#50096,.T.);
#70631=ORIENTED_EDGE('',*,*,#50097,.F.);
#70632=ORIENTED_EDGE('',*,*,#50098,.T.);
#70633=ORIENTED_EDGE('',*,*,#50099,.F.);
#70634=ORIENTED_EDGE('',*,*,#50100,.T.);
#70635=ORIENTED_EDGE('',*,*,#50101,.F.);
#70636=ORIENTED_EDGE('',*,*,#50102,.T.);
#70637=ORIENTED_EDGE('',*,*,#50103,.F.);
#70638=ORIENTED_EDGE('',*,*,#50104,.T.);
#70639=ORIENTED_EDGE('',*,*,#50105,.F.);
#70640=ORIENTED_EDGE('',*,*,#50106,.T.);
#70641=ORIENTED_EDGE('',*,*,#50107,.F.);
#70642=ORIENTED_EDGE('',*,*,#50108,.T.);
#70643=ORIENTED_EDGE('',*,*,#50109,.F.);
#70644=ORIENTED_EDGE('',*,*,#50110,.T.);
#70645=ORIENTED_EDGE('',*,*,#50111,.F.);
#70646=ORIENTED_EDGE('',*,*,#50112,.T.);
#70647=ORIENTED_EDGE('',*,*,#50113,.F.);
#70648=ORIENTED_EDGE('',*,*,#50114,.T.);
#70649=ORIENTED_EDGE('',*,*,#50115,.F.);
#70650=ORIENTED_EDGE('',*,*,#50116,.T.);
#70651=ORIENTED_EDGE('',*,*,#50117,.F.);
#70652=ORIENTED_EDGE('',*,*,#50118,.T.);
#70653=ORIENTED_EDGE('',*,*,#50119,.F.);
#70654=ORIENTED_EDGE('',*,*,#50120,.T.);
#70655=ORIENTED_EDGE('',*,*,#50121,.F.);
#70656=ORIENTED_EDGE('',*,*,#50122,.T.);
#70657=ORIENTED_EDGE('',*,*,#50123,.F.);
#70658=ORIENTED_EDGE('',*,*,#50124,.T.);
#70659=ORIENTED_EDGE('',*,*,#50125,.F.);
#70660=ORIENTED_EDGE('',*,*,#50126,.T.);
#70661=ORIENTED_EDGE('',*,*,#50127,.F.);
#70662=ORIENTED_EDGE('',*,*,#50128,.T.);
#70663=ORIENTED_EDGE('',*,*,#50129,.F.);
#70664=ORIENTED_EDGE('',*,*,#50130,.T.);
#70665=ORIENTED_EDGE('',*,*,#50131,.F.);
#70666=ORIENTED_EDGE('',*,*,#50132,.T.);
#70667=ORIENTED_EDGE('',*,*,#50133,.F.);
#70668=ORIENTED_EDGE('',*,*,#50134,.T.);
#70669=ORIENTED_EDGE('',*,*,#50135,.F.);
#70670=ORIENTED_EDGE('',*,*,#50136,.T.);
#70671=ORIENTED_EDGE('',*,*,#50137,.F.);
#70672=ORIENTED_EDGE('',*,*,#50138,.T.);
#70673=ORIENTED_EDGE('',*,*,#50139,.F.);
#70674=ORIENTED_EDGE('',*,*,#50140,.T.);
#70675=ORIENTED_EDGE('',*,*,#50141,.F.);
#70676=ORIENTED_EDGE('',*,*,#50142,.T.);
#70677=ORIENTED_EDGE('',*,*,#50143,.F.);
#70678=ORIENTED_EDGE('',*,*,#50144,.T.);
#70679=ORIENTED_EDGE('',*,*,#50145,.F.);
#70680=ORIENTED_EDGE('',*,*,#50146,.T.);
#70681=ORIENTED_EDGE('',*,*,#50147,.F.);
#70682=ORIENTED_EDGE('',*,*,#50148,.T.);
#70683=ORIENTED_EDGE('',*,*,#50149,.F.);
#70684=ORIENTED_EDGE('',*,*,#50150,.T.);
#70685=ORIENTED_EDGE('',*,*,#50151,.F.);
#70686=ORIENTED_EDGE('',*,*,#50152,.T.);
#70687=ORIENTED_EDGE('',*,*,#50153,.F.);
#70688=ORIENTED_EDGE('',*,*,#50154,.T.);
#70689=ORIENTED_EDGE('',*,*,#50155,.F.);
#70690=ORIENTED_EDGE('',*,*,#50156,.T.);
#70691=ORIENTED_EDGE('',*,*,#50157,.F.);
#70692=ORIENTED_EDGE('',*,*,#50158,.T.);
#70693=ORIENTED_EDGE('',*,*,#50159,.F.);
#70694=ORIENTED_EDGE('',*,*,#50160,.T.);
#70695=ORIENTED_EDGE('',*,*,#50161,.F.);
#70696=ORIENTED_EDGE('',*,*,#50162,.T.);
#70697=ORIENTED_EDGE('',*,*,#50163,.F.);
#70698=ORIENTED_EDGE('',*,*,#50164,.T.);
#70699=ORIENTED_EDGE('',*,*,#50165,.F.);
#70700=ORIENTED_EDGE('',*,*,#50166,.T.);
#70701=ORIENTED_EDGE('',*,*,#50167,.F.);
#70702=ORIENTED_EDGE('',*,*,#50168,.T.);
#70703=ORIENTED_EDGE('',*,*,#50169,.F.);
#70704=ORIENTED_EDGE('',*,*,#50170,.T.);
#70705=ORIENTED_EDGE('',*,*,#50171,.F.);
#70706=ORIENTED_EDGE('',*,*,#50172,.T.);
#70707=ORIENTED_EDGE('',*,*,#50173,.F.);
#70708=ORIENTED_EDGE('',*,*,#50174,.T.);
#70709=ORIENTED_EDGE('',*,*,#50175,.F.);
#70710=ORIENTED_EDGE('',*,*,#50176,.T.);
#70711=ORIENTED_EDGE('',*,*,#50177,.F.);
#70712=ORIENTED_EDGE('',*,*,#50178,.T.);
#70713=ORIENTED_EDGE('',*,*,#50179,.F.);
#70714=ORIENTED_EDGE('',*,*,#50180,.T.);
#70715=ORIENTED_EDGE('',*,*,#50181,.F.);
#70716=ORIENTED_EDGE('',*,*,#50182,.T.);
#70717=ORIENTED_EDGE('',*,*,#50183,.F.);
#70718=ORIENTED_EDGE('',*,*,#50184,.T.);
#70719=ORIENTED_EDGE('',*,*,#50185,.F.);
#70720=ORIENTED_EDGE('',*,*,#50186,.T.);
#70721=ORIENTED_EDGE('',*,*,#50187,.F.);
#70722=ORIENTED_EDGE('',*,*,#50188,.T.);
#70723=ORIENTED_EDGE('',*,*,#50189,.F.);
#70724=ORIENTED_EDGE('',*,*,#50190,.T.);
#70725=ORIENTED_EDGE('',*,*,#50191,.F.);
#70726=ORIENTED_EDGE('',*,*,#50192,.T.);
#70727=ORIENTED_EDGE('',*,*,#50193,.F.);
#70728=ORIENTED_EDGE('',*,*,#50194,.T.);
#70729=ORIENTED_EDGE('',*,*,#50195,.F.);
#70730=ORIENTED_EDGE('',*,*,#50196,.T.);
#70731=ORIENTED_EDGE('',*,*,#50197,.F.);
#70732=ORIENTED_EDGE('',*,*,#50198,.T.);
#70733=ORIENTED_EDGE('',*,*,#50199,.F.);
#70734=ORIENTED_EDGE('',*,*,#50200,.T.);
#70735=ORIENTED_EDGE('',*,*,#50201,.F.);
#70736=ORIENTED_EDGE('',*,*,#50202,.T.);
#70737=ORIENTED_EDGE('',*,*,#50203,.F.);
#70738=ORIENTED_EDGE('',*,*,#50204,.T.);
#70739=ORIENTED_EDGE('',*,*,#50205,.F.);
#70740=ORIENTED_EDGE('',*,*,#50206,.T.);
#70741=ORIENTED_EDGE('',*,*,#50207,.F.);
#70742=ORIENTED_EDGE('',*,*,#50208,.T.);
#70743=ORIENTED_EDGE('',*,*,#50209,.F.);
#70744=ORIENTED_EDGE('',*,*,#50210,.T.);
#70745=ORIENTED_EDGE('',*,*,#50211,.F.);
#70746=ORIENTED_EDGE('',*,*,#50212,.T.);
#70747=ORIENTED_EDGE('',*,*,#50213,.F.);
#70748=ORIENTED_EDGE('',*,*,#50214,.T.);
#70749=ORIENTED_EDGE('',*,*,#50215,.F.);
#70750=ORIENTED_EDGE('',*,*,#50216,.T.);
#70751=ORIENTED_EDGE('',*,*,#50217,.F.);
#70752=ORIENTED_EDGE('',*,*,#50218,.T.);
#70753=ORIENTED_EDGE('',*,*,#50219,.F.);
#70754=ORIENTED_EDGE('',*,*,#50220,.T.);
#70755=ORIENTED_EDGE('',*,*,#50221,.F.);
#70756=ORIENTED_EDGE('',*,*,#50222,.T.);
#70757=ORIENTED_EDGE('',*,*,#50223,.F.);
#70758=ORIENTED_EDGE('',*,*,#50224,.T.);
#70759=ORIENTED_EDGE('',*,*,#50225,.F.);
#70760=ORIENTED_EDGE('',*,*,#50226,.T.);
#70761=ORIENTED_EDGE('',*,*,#50227,.F.);
#70762=ORIENTED_EDGE('',*,*,#50228,.T.);
#70763=ORIENTED_EDGE('',*,*,#50229,.F.);
#70764=ORIENTED_EDGE('',*,*,#50230,.T.);
#70765=ORIENTED_EDGE('',*,*,#50231,.F.);
#70766=ORIENTED_EDGE('',*,*,#50232,.T.);
#70767=ORIENTED_EDGE('',*,*,#50233,.F.);
#70768=ORIENTED_EDGE('',*,*,#50234,.T.);
#70769=ORIENTED_EDGE('',*,*,#50235,.F.);
#70770=ORIENTED_EDGE('',*,*,#50236,.T.);
#70771=ORIENTED_EDGE('',*,*,#50237,.F.);
#70772=ORIENTED_EDGE('',*,*,#50238,.T.);
#70773=ORIENTED_EDGE('',*,*,#50239,.F.);
#70774=ORIENTED_EDGE('',*,*,#50240,.T.);
#70775=ORIENTED_EDGE('',*,*,#50241,.F.);
#70776=ORIENTED_EDGE('',*,*,#50242,.T.);
#70777=ORIENTED_EDGE('',*,*,#50243,.F.);
#70778=ORIENTED_EDGE('',*,*,#50244,.T.);
#70779=ORIENTED_EDGE('',*,*,#50245,.F.);
#70780=ORIENTED_EDGE('',*,*,#50246,.T.);
#70781=ORIENTED_EDGE('',*,*,#50247,.F.);
#70782=ORIENTED_EDGE('',*,*,#50248,.T.);
#70783=ORIENTED_EDGE('',*,*,#50249,.F.);
#70784=ORIENTED_EDGE('',*,*,#50250,.T.);
#70785=ORIENTED_EDGE('',*,*,#50251,.F.);
#70786=ORIENTED_EDGE('',*,*,#50252,.T.);
#70787=ORIENTED_EDGE('',*,*,#50253,.F.);
#70788=ORIENTED_EDGE('',*,*,#50254,.T.);
#70789=ORIENTED_EDGE('',*,*,#50255,.F.);
#70790=ORIENTED_EDGE('',*,*,#50256,.T.);
#70791=ORIENTED_EDGE('',*,*,#50257,.F.);
#70792=ORIENTED_EDGE('',*,*,#50258,.T.);
#70793=ORIENTED_EDGE('',*,*,#50259,.F.);
#70794=ORIENTED_EDGE('',*,*,#50260,.T.);
#70795=ORIENTED_EDGE('',*,*,#50261,.F.);
#70796=ORIENTED_EDGE('',*,*,#50262,.T.);
#70797=ORIENTED_EDGE('',*,*,#50263,.F.);
#70798=ORIENTED_EDGE('',*,*,#50264,.T.);
#70799=ORIENTED_EDGE('',*,*,#50265,.F.);
#70800=ORIENTED_EDGE('',*,*,#50266,.T.);
#70801=ORIENTED_EDGE('',*,*,#50267,.F.);
#70802=ORIENTED_EDGE('',*,*,#50268,.T.);
#70803=ORIENTED_EDGE('',*,*,#50269,.F.);
#70804=ORIENTED_EDGE('',*,*,#50270,.T.);
#70805=ORIENTED_EDGE('',*,*,#50271,.F.);
#70806=ORIENTED_EDGE('',*,*,#50272,.T.);
#70807=ORIENTED_EDGE('',*,*,#50273,.F.);
#70808=ORIENTED_EDGE('',*,*,#50274,.T.);
#70809=ORIENTED_EDGE('',*,*,#50275,.F.);
#70810=ORIENTED_EDGE('',*,*,#50276,.T.);
#70811=ORIENTED_EDGE('',*,*,#50277,.F.);
#70812=ORIENTED_EDGE('',*,*,#50278,.T.);
#70813=ORIENTED_EDGE('',*,*,#50279,.F.);
#70814=ORIENTED_EDGE('',*,*,#50280,.T.);
#70815=ORIENTED_EDGE('',*,*,#50281,.F.);
#70816=ORIENTED_EDGE('',*,*,#50282,.T.);
#70817=ORIENTED_EDGE('',*,*,#50283,.F.);
#70818=ORIENTED_EDGE('',*,*,#50284,.T.);
#70819=ORIENTED_EDGE('',*,*,#50285,.F.);
#70820=ORIENTED_EDGE('',*,*,#50286,.T.);
#70821=ORIENTED_EDGE('',*,*,#50287,.F.);
#70822=ORIENTED_EDGE('',*,*,#50288,.T.);
#70823=ORIENTED_EDGE('',*,*,#50289,.F.);
#70824=ORIENTED_EDGE('',*,*,#50290,.T.);
#70825=ORIENTED_EDGE('',*,*,#50291,.F.);
#70826=ORIENTED_EDGE('',*,*,#50292,.T.);
#70827=ORIENTED_EDGE('',*,*,#50293,.F.);
#70828=ORIENTED_EDGE('',*,*,#50294,.T.);
#70829=ORIENTED_EDGE('',*,*,#50295,.F.);
#70830=ORIENTED_EDGE('',*,*,#50296,.T.);
#70831=ORIENTED_EDGE('',*,*,#50297,.F.);
#70832=ORIENTED_EDGE('',*,*,#50298,.T.);
#70833=ORIENTED_EDGE('',*,*,#50299,.F.);
#70834=ORIENTED_EDGE('',*,*,#50300,.T.);
#70835=ORIENTED_EDGE('',*,*,#50301,.F.);
#70836=ORIENTED_EDGE('',*,*,#50302,.T.);
#70837=ORIENTED_EDGE('',*,*,#50303,.F.);
#70838=ORIENTED_EDGE('',*,*,#50304,.T.);
#70839=ORIENTED_EDGE('',*,*,#50305,.F.);
#70840=ORIENTED_EDGE('',*,*,#50306,.T.);
#70841=ORIENTED_EDGE('',*,*,#50307,.F.);
#70842=ORIENTED_EDGE('',*,*,#50308,.T.);
#70843=ORIENTED_EDGE('',*,*,#50309,.F.);
#70844=ORIENTED_EDGE('',*,*,#50310,.T.);
#70845=ORIENTED_EDGE('',*,*,#50311,.F.);
#70846=ORIENTED_EDGE('',*,*,#50312,.T.);
#70847=ORIENTED_EDGE('',*,*,#50313,.F.);
#70848=ORIENTED_EDGE('',*,*,#50314,.T.);
#70849=ORIENTED_EDGE('',*,*,#50315,.F.);
#70850=ORIENTED_EDGE('',*,*,#50316,.T.);
#70851=ORIENTED_EDGE('',*,*,#50317,.F.);
#70852=ORIENTED_EDGE('',*,*,#50318,.T.);
#70853=ORIENTED_EDGE('',*,*,#50319,.F.);
#70854=ORIENTED_EDGE('',*,*,#50320,.T.);
#70855=ORIENTED_EDGE('',*,*,#50321,.F.);
#70856=ORIENTED_EDGE('',*,*,#50322,.T.);
#70857=ORIENTED_EDGE('',*,*,#50323,.F.);
#70858=ORIENTED_EDGE('',*,*,#50324,.T.);
#70859=ORIENTED_EDGE('',*,*,#50325,.F.);
#70860=ORIENTED_EDGE('',*,*,#50326,.T.);
#70861=ORIENTED_EDGE('',*,*,#50327,.F.);
#70862=ORIENTED_EDGE('',*,*,#50328,.T.);
#70863=ORIENTED_EDGE('',*,*,#50329,.F.);
#70864=ORIENTED_EDGE('',*,*,#50330,.T.);
#70865=ORIENTED_EDGE('',*,*,#50331,.F.);
#70866=ORIENTED_EDGE('',*,*,#50332,.T.);
#70867=ORIENTED_EDGE('',*,*,#50333,.F.);
#70868=ORIENTED_EDGE('',*,*,#50334,.T.);
#70869=ORIENTED_EDGE('',*,*,#50335,.F.);
#70870=ORIENTED_EDGE('',*,*,#50336,.T.);
#70871=ORIENTED_EDGE('',*,*,#50337,.F.);
#70872=ORIENTED_EDGE('',*,*,#50338,.T.);
#70873=ORIENTED_EDGE('',*,*,#50339,.F.);
#70874=ORIENTED_EDGE('',*,*,#50340,.T.);
#70875=ORIENTED_EDGE('',*,*,#50341,.F.);
#70876=ORIENTED_EDGE('',*,*,#50342,.T.);
#70877=ORIENTED_EDGE('',*,*,#50343,.F.);
#70878=ORIENTED_EDGE('',*,*,#50344,.T.);
#70879=ORIENTED_EDGE('',*,*,#50345,.F.);
#70880=ORIENTED_EDGE('',*,*,#50346,.T.);
#70881=ORIENTED_EDGE('',*,*,#50347,.F.);
#70882=ORIENTED_EDGE('',*,*,#50348,.T.);
#70883=ORIENTED_EDGE('',*,*,#50349,.F.);
#70884=ORIENTED_EDGE('',*,*,#50350,.T.);
#70885=ORIENTED_EDGE('',*,*,#50351,.F.);
#70886=ORIENTED_EDGE('',*,*,#50352,.T.);
#70887=ORIENTED_EDGE('',*,*,#50353,.F.);
#70888=ORIENTED_EDGE('',*,*,#50354,.T.);
#70889=ORIENTED_EDGE('',*,*,#50355,.F.);
#70890=ORIENTED_EDGE('',*,*,#50356,.T.);
#70891=ORIENTED_EDGE('',*,*,#50357,.F.);
#70892=ORIENTED_EDGE('',*,*,#50358,.T.);
#70893=ORIENTED_EDGE('',*,*,#50359,.F.);
#70894=ORIENTED_EDGE('',*,*,#50360,.T.);
#70895=ORIENTED_EDGE('',*,*,#50361,.F.);
#70896=ORIENTED_EDGE('',*,*,#50362,.T.);
#70897=ORIENTED_EDGE('',*,*,#50363,.F.);
#70898=ORIENTED_EDGE('',*,*,#50364,.T.);
#70899=ORIENTED_EDGE('',*,*,#49669,.T.);
#70900=ORIENTED_EDGE('',*,*,#50364,.F.);
#70901=ORIENTED_EDGE('',*,*,#50365,.F.);
#70902=ORIENTED_EDGE('',*,*,#50366,.T.);
#70903=ORIENTED_EDGE('',*,*,#50367,.F.);
#70904=ORIENTED_EDGE('',*,*,#50368,.T.);
#70905=ORIENTED_EDGE('',*,*,#50369,.F.);
#70906=ORIENTED_EDGE('',*,*,#50370,.T.);
#70907=ORIENTED_EDGE('',*,*,#50371,.F.);
#70908=ORIENTED_EDGE('',*,*,#50372,.T.);
#70909=ORIENTED_EDGE('',*,*,#50373,.F.);
#70910=ORIENTED_EDGE('',*,*,#50374,.T.);
#70911=ORIENTED_EDGE('',*,*,#50375,.F.);
#70912=ORIENTED_EDGE('',*,*,#50376,.T.);
#70913=ORIENTED_EDGE('',*,*,#50377,.F.);
#70914=ORIENTED_EDGE('',*,*,#50378,.T.);
#70915=ORIENTED_EDGE('',*,*,#50379,.F.);
#70916=ORIENTED_EDGE('',*,*,#50380,.T.);
#70917=ORIENTED_EDGE('',*,*,#50381,.F.);
#70918=ORIENTED_EDGE('',*,*,#50382,.T.);
#70919=ORIENTED_EDGE('',*,*,#50383,.F.);
#70920=ORIENTED_EDGE('',*,*,#50384,.T.);
#70921=ORIENTED_EDGE('',*,*,#50385,.F.);
#70922=ORIENTED_EDGE('',*,*,#50386,.T.);
#70923=ORIENTED_EDGE('',*,*,#50387,.F.);
#70924=ORIENTED_EDGE('',*,*,#50388,.T.);
#70925=ORIENTED_EDGE('',*,*,#50389,.F.);
#70926=ORIENTED_EDGE('',*,*,#50390,.T.);
#70927=ORIENTED_EDGE('',*,*,#50391,.F.);
#70928=ORIENTED_EDGE('',*,*,#50392,.T.);
#70929=ORIENTED_EDGE('',*,*,#50393,.F.);
#70930=ORIENTED_EDGE('',*,*,#50394,.T.);
#70931=ORIENTED_EDGE('',*,*,#50395,.F.);
#70932=ORIENTED_EDGE('',*,*,#50396,.T.);
#70933=ORIENTED_EDGE('',*,*,#50397,.F.);
#70934=ORIENTED_EDGE('',*,*,#50398,.T.);
#70935=ORIENTED_EDGE('',*,*,#50399,.F.);
#70936=ORIENTED_EDGE('',*,*,#50400,.T.);
#70937=ORIENTED_EDGE('',*,*,#50401,.F.);
#70938=ORIENTED_EDGE('',*,*,#50402,.T.);
#70939=ORIENTED_EDGE('',*,*,#50403,.F.);
#70940=ORIENTED_EDGE('',*,*,#50404,.T.);
#70941=ORIENTED_EDGE('',*,*,#50405,.F.);
#70942=ORIENTED_EDGE('',*,*,#50406,.T.);
#70943=ORIENTED_EDGE('',*,*,#50407,.F.);
#70944=ORIENTED_EDGE('',*,*,#50408,.T.);
#70945=ORIENTED_EDGE('',*,*,#50409,.F.);
#70946=ORIENTED_EDGE('',*,*,#50410,.T.);
#70947=ORIENTED_EDGE('',*,*,#50411,.F.);
#70948=ORIENTED_EDGE('',*,*,#50412,.T.);
#70949=ORIENTED_EDGE('',*,*,#50413,.F.);
#70950=ORIENTED_EDGE('',*,*,#50414,.T.);
#70951=ORIENTED_EDGE('',*,*,#50415,.F.);
#70952=ORIENTED_EDGE('',*,*,#50416,.T.);
#70953=ORIENTED_EDGE('',*,*,#50417,.F.);
#70954=ORIENTED_EDGE('',*,*,#50418,.T.);
#70955=ORIENTED_EDGE('',*,*,#50419,.F.);
#70956=ORIENTED_EDGE('',*,*,#50420,.T.);
#70957=ORIENTED_EDGE('',*,*,#50421,.F.);
#70958=ORIENTED_EDGE('',*,*,#50422,.T.);
#70959=ORIENTED_EDGE('',*,*,#50423,.F.);
#70960=ORIENTED_EDGE('',*,*,#50424,.T.);
#70961=ORIENTED_EDGE('',*,*,#50425,.F.);
#70962=ORIENTED_EDGE('',*,*,#50426,.T.);
#70963=ORIENTED_EDGE('',*,*,#50427,.F.);
#70964=ORIENTED_EDGE('',*,*,#50428,.T.);
#70965=ORIENTED_EDGE('',*,*,#50429,.F.);
#70966=ORIENTED_EDGE('',*,*,#50430,.T.);
#70967=ORIENTED_EDGE('',*,*,#50431,.F.);
#70968=ORIENTED_EDGE('',*,*,#50432,.T.);
#70969=ORIENTED_EDGE('',*,*,#50433,.F.);
#70970=ORIENTED_EDGE('',*,*,#50434,.T.);
#70971=ORIENTED_EDGE('',*,*,#50435,.F.);
#70972=ORIENTED_EDGE('',*,*,#50436,.T.);
#70973=ORIENTED_EDGE('',*,*,#50437,.F.);
#70974=ORIENTED_EDGE('',*,*,#50438,.T.);
#70975=ORIENTED_EDGE('',*,*,#50439,.F.);
#70976=ORIENTED_EDGE('',*,*,#50440,.T.);
#70977=ORIENTED_EDGE('',*,*,#50441,.F.);
#70978=ORIENTED_EDGE('',*,*,#50442,.T.);
#70979=ORIENTED_EDGE('',*,*,#50443,.F.);
#70980=ORIENTED_EDGE('',*,*,#50444,.T.);
#70981=ORIENTED_EDGE('',*,*,#50445,.F.);
#70982=ORIENTED_EDGE('',*,*,#50446,.T.);
#70983=ORIENTED_EDGE('',*,*,#50447,.F.);
#70984=ORIENTED_EDGE('',*,*,#50448,.T.);
#70985=ORIENTED_EDGE('',*,*,#50449,.F.);
#70986=ORIENTED_EDGE('',*,*,#50450,.T.);
#70987=ORIENTED_EDGE('',*,*,#50451,.F.);
#70988=ORIENTED_EDGE('',*,*,#50452,.T.);
#70989=ORIENTED_EDGE('',*,*,#50453,.F.);
#70990=ORIENTED_EDGE('',*,*,#50454,.T.);
#70991=ORIENTED_EDGE('',*,*,#50455,.F.);
#70992=ORIENTED_EDGE('',*,*,#50456,.T.);
#70993=ORIENTED_EDGE('',*,*,#50457,.F.);
#70994=ORIENTED_EDGE('',*,*,#50458,.T.);
#70995=ORIENTED_EDGE('',*,*,#50459,.F.);
#70996=ORIENTED_EDGE('',*,*,#50460,.T.);
#70997=ORIENTED_EDGE('',*,*,#50461,.F.);
#70998=ORIENTED_EDGE('',*,*,#50462,.T.);
#70999=ORIENTED_EDGE('',*,*,#50463,.F.);
#71000=ORIENTED_EDGE('',*,*,#50464,.T.);
#71001=ORIENTED_EDGE('',*,*,#50465,.F.);
#71002=ORIENTED_EDGE('',*,*,#50466,.T.);
#71003=ORIENTED_EDGE('',*,*,#50467,.F.);
#71004=ORIENTED_EDGE('',*,*,#50468,.T.);
#71005=ORIENTED_EDGE('',*,*,#50469,.F.);
#71006=ORIENTED_EDGE('',*,*,#50470,.T.);
#71007=ORIENTED_EDGE('',*,*,#50471,.F.);
#71008=ORIENTED_EDGE('',*,*,#50472,.T.);
#71009=ORIENTED_EDGE('',*,*,#50473,.F.);
#71010=ORIENTED_EDGE('',*,*,#50474,.T.);
#71011=ORIENTED_EDGE('',*,*,#50475,.F.);
#71012=ORIENTED_EDGE('',*,*,#50476,.T.);
#71013=ORIENTED_EDGE('',*,*,#50477,.F.);
#71014=ORIENTED_EDGE('',*,*,#50478,.T.);
#71015=ORIENTED_EDGE('',*,*,#50479,.F.);
#71016=ORIENTED_EDGE('',*,*,#50480,.T.);
#71017=ORIENTED_EDGE('',*,*,#50481,.F.);
#71018=ORIENTED_EDGE('',*,*,#50482,.T.);
#71019=ORIENTED_EDGE('',*,*,#50483,.F.);
#71020=ORIENTED_EDGE('',*,*,#50484,.T.);
#71021=ORIENTED_EDGE('',*,*,#50485,.F.);
#71022=ORIENTED_EDGE('',*,*,#50486,.T.);
#71023=ORIENTED_EDGE('',*,*,#50487,.F.);
#71024=ORIENTED_EDGE('',*,*,#50488,.T.);
#71025=ORIENTED_EDGE('',*,*,#50489,.F.);
#71026=ORIENTED_EDGE('',*,*,#50490,.T.);
#71027=ORIENTED_EDGE('',*,*,#50491,.F.);
#71028=ORIENTED_EDGE('',*,*,#50492,.T.);
#71029=ORIENTED_EDGE('',*,*,#50493,.F.);
#71030=ORIENTED_EDGE('',*,*,#50494,.T.);
#71031=ORIENTED_EDGE('',*,*,#50495,.F.);
#71032=ORIENTED_EDGE('',*,*,#50496,.T.);
#71033=ORIENTED_EDGE('',*,*,#50497,.F.);
#71034=ORIENTED_EDGE('',*,*,#50498,.T.);
#71035=ORIENTED_EDGE('',*,*,#50499,.F.);
#71036=ORIENTED_EDGE('',*,*,#50500,.T.);
#71037=ORIENTED_EDGE('',*,*,#50501,.F.);
#71038=ORIENTED_EDGE('',*,*,#50502,.T.);
#71039=ORIENTED_EDGE('',*,*,#50503,.F.);
#71040=ORIENTED_EDGE('',*,*,#50504,.T.);
#71041=ORIENTED_EDGE('',*,*,#50505,.F.);
#71042=ORIENTED_EDGE('',*,*,#50506,.T.);
#71043=ORIENTED_EDGE('',*,*,#50507,.F.);
#71044=ORIENTED_EDGE('',*,*,#50508,.T.);
#71045=ORIENTED_EDGE('',*,*,#50509,.F.);
#71046=ORIENTED_EDGE('',*,*,#50510,.T.);
#71047=ORIENTED_EDGE('',*,*,#50511,.F.);
#71048=ORIENTED_EDGE('',*,*,#50512,.T.);
#71049=ORIENTED_EDGE('',*,*,#50513,.F.);
#71050=ORIENTED_EDGE('',*,*,#50514,.T.);
#71051=ORIENTED_EDGE('',*,*,#50515,.F.);
#71052=ORIENTED_EDGE('',*,*,#50516,.T.);
#71053=ORIENTED_EDGE('',*,*,#50517,.F.);
#71054=ORIENTED_EDGE('',*,*,#50518,.T.);
#71055=ORIENTED_EDGE('',*,*,#50519,.F.);
#71056=ORIENTED_EDGE('',*,*,#50520,.T.);
#71057=ORIENTED_EDGE('',*,*,#50521,.F.);
#71058=ORIENTED_EDGE('',*,*,#50522,.T.);
#71059=ORIENTED_EDGE('',*,*,#50523,.F.);
#71060=ORIENTED_EDGE('',*,*,#50524,.T.);
#71061=ORIENTED_EDGE('',*,*,#50525,.F.);
#71062=ORIENTED_EDGE('',*,*,#50526,.T.);
#71063=ORIENTED_EDGE('',*,*,#50527,.F.);
#71064=ORIENTED_EDGE('',*,*,#50528,.T.);
#71065=ORIENTED_EDGE('',*,*,#50529,.F.);
#71066=ORIENTED_EDGE('',*,*,#50530,.T.);
#71067=ORIENTED_EDGE('',*,*,#50531,.F.);
#71068=ORIENTED_EDGE('',*,*,#50532,.T.);
#71069=ORIENTED_EDGE('',*,*,#50533,.F.);
#71070=ORIENTED_EDGE('',*,*,#50534,.T.);
#71071=ORIENTED_EDGE('',*,*,#50535,.F.);
#71072=ORIENTED_EDGE('',*,*,#50536,.T.);
#71073=ORIENTED_EDGE('',*,*,#50537,.F.);
#71074=ORIENTED_EDGE('',*,*,#50538,.T.);
#71075=ORIENTED_EDGE('',*,*,#50539,.F.);
#71076=ORIENTED_EDGE('',*,*,#50540,.T.);
#71077=ORIENTED_EDGE('',*,*,#50541,.F.);
#71078=ORIENTED_EDGE('',*,*,#50542,.T.);
#71079=ORIENTED_EDGE('',*,*,#50543,.F.);
#71080=ORIENTED_EDGE('',*,*,#50544,.T.);
#71081=ORIENTED_EDGE('',*,*,#50545,.F.);
#71082=ORIENTED_EDGE('',*,*,#50546,.T.);
#71083=ORIENTED_EDGE('',*,*,#50547,.F.);
#71084=ORIENTED_EDGE('',*,*,#50548,.T.);
#71085=ORIENTED_EDGE('',*,*,#50549,.F.);
#71086=ORIENTED_EDGE('',*,*,#50550,.T.);
#71087=ORIENTED_EDGE('',*,*,#50551,.F.);
#71088=ORIENTED_EDGE('',*,*,#50552,.T.);
#71089=ORIENTED_EDGE('',*,*,#50553,.F.);
#71090=ORIENTED_EDGE('',*,*,#50554,.T.);
#71091=ORIENTED_EDGE('',*,*,#50555,.F.);
#71092=ORIENTED_EDGE('',*,*,#50556,.T.);
#71093=ORIENTED_EDGE('',*,*,#50557,.F.);
#71094=ORIENTED_EDGE('',*,*,#50558,.T.);
#71095=ORIENTED_EDGE('',*,*,#50559,.F.);
#71096=ORIENTED_EDGE('',*,*,#50560,.T.);
#71097=ORIENTED_EDGE('',*,*,#50561,.F.);
#71098=ORIENTED_EDGE('',*,*,#50562,.T.);
#71099=ORIENTED_EDGE('',*,*,#50563,.F.);
#71100=ORIENTED_EDGE('',*,*,#50564,.T.);
#71101=ORIENTED_EDGE('',*,*,#50565,.F.);
#71102=ORIENTED_EDGE('',*,*,#50566,.T.);
#71103=ORIENTED_EDGE('',*,*,#50567,.F.);
#71104=ORIENTED_EDGE('',*,*,#50568,.T.);
#71105=ORIENTED_EDGE('',*,*,#50569,.F.);
#71106=ORIENTED_EDGE('',*,*,#50570,.T.);
#71107=ORIENTED_EDGE('',*,*,#50571,.F.);
#71108=ORIENTED_EDGE('',*,*,#50572,.T.);
#71109=ORIENTED_EDGE('',*,*,#50573,.F.);
#71110=ORIENTED_EDGE('',*,*,#50574,.T.);
#71111=ORIENTED_EDGE('',*,*,#50575,.F.);
#71112=ORIENTED_EDGE('',*,*,#50576,.T.);
#71113=ORIENTED_EDGE('',*,*,#50577,.F.);
#71114=ORIENTED_EDGE('',*,*,#50578,.T.);
#71115=ORIENTED_EDGE('',*,*,#50579,.F.);
#71116=ORIENTED_EDGE('',*,*,#50580,.T.);
#71117=ORIENTED_EDGE('',*,*,#50581,.F.);
#71118=ORIENTED_EDGE('',*,*,#50582,.T.);
#71119=ORIENTED_EDGE('',*,*,#50583,.F.);
#71120=ORIENTED_EDGE('',*,*,#50584,.T.);
#71121=ORIENTED_EDGE('',*,*,#50585,.F.);
#71122=ORIENTED_EDGE('',*,*,#50586,.T.);
#71123=ORIENTED_EDGE('',*,*,#50587,.F.);
#71124=ORIENTED_EDGE('',*,*,#50588,.T.);
#71125=ORIENTED_EDGE('',*,*,#50589,.F.);
#71126=ORIENTED_EDGE('',*,*,#50590,.T.);
#71127=ORIENTED_EDGE('',*,*,#50591,.F.);
#71128=ORIENTED_EDGE('',*,*,#50592,.T.);
#71129=ORIENTED_EDGE('',*,*,#50593,.F.);
#71130=ORIENTED_EDGE('',*,*,#50594,.T.);
#71131=ORIENTED_EDGE('',*,*,#50595,.F.);
#71132=ORIENTED_EDGE('',*,*,#50596,.T.);
#71133=ORIENTED_EDGE('',*,*,#50597,.F.);
#71134=ORIENTED_EDGE('',*,*,#50598,.T.);
#71135=ORIENTED_EDGE('',*,*,#50599,.F.);
#71136=ORIENTED_EDGE('',*,*,#50600,.T.);
#71137=ORIENTED_EDGE('',*,*,#50601,.F.);
#71138=ORIENTED_EDGE('',*,*,#50602,.T.);
#71139=ORIENTED_EDGE('',*,*,#50603,.F.);
#71140=ORIENTED_EDGE('',*,*,#50604,.T.);
#71141=ORIENTED_EDGE('',*,*,#50605,.F.);
#71142=ORIENTED_EDGE('',*,*,#50606,.T.);
#71143=ORIENTED_EDGE('',*,*,#50607,.F.);
#71144=ORIENTED_EDGE('',*,*,#50608,.T.);
#71145=ORIENTED_EDGE('',*,*,#50609,.F.);
#71146=ORIENTED_EDGE('',*,*,#50610,.T.);
#71147=ORIENTED_EDGE('',*,*,#50611,.F.);
#71148=ORIENTED_EDGE('',*,*,#50612,.T.);
#71149=ORIENTED_EDGE('',*,*,#50613,.F.);
#71150=ORIENTED_EDGE('',*,*,#50614,.T.);
#71151=ORIENTED_EDGE('',*,*,#50615,.F.);
#71152=ORIENTED_EDGE('',*,*,#50616,.T.);
#71153=ORIENTED_EDGE('',*,*,#50617,.F.);
#71154=ORIENTED_EDGE('',*,*,#50618,.T.);
#71155=ORIENTED_EDGE('',*,*,#50619,.F.);
#71156=ORIENTED_EDGE('',*,*,#50620,.T.);
#71157=ORIENTED_EDGE('',*,*,#50621,.F.);
#71158=ORIENTED_EDGE('',*,*,#50622,.T.);
#71159=ORIENTED_EDGE('',*,*,#50623,.F.);
#71160=ORIENTED_EDGE('',*,*,#50624,.T.);
#71161=ORIENTED_EDGE('',*,*,#50625,.F.);
#71162=ORIENTED_EDGE('',*,*,#50626,.T.);
#71163=ORIENTED_EDGE('',*,*,#50627,.F.);
#71164=ORIENTED_EDGE('',*,*,#50628,.T.);
#71165=ORIENTED_EDGE('',*,*,#50629,.F.);
#71166=ORIENTED_EDGE('',*,*,#50630,.T.);
#71167=ORIENTED_EDGE('',*,*,#50631,.F.);
#71168=ORIENTED_EDGE('',*,*,#50632,.T.);
#71169=ORIENTED_EDGE('',*,*,#50633,.F.);
#71170=ORIENTED_EDGE('',*,*,#50634,.T.);
#71171=ORIENTED_EDGE('',*,*,#50635,.F.);
#71172=ORIENTED_EDGE('',*,*,#50636,.T.);
#71173=ORIENTED_EDGE('',*,*,#50637,.F.);
#71174=ORIENTED_EDGE('',*,*,#50638,.T.);
#71175=ORIENTED_EDGE('',*,*,#50639,.F.);
#71176=ORIENTED_EDGE('',*,*,#50640,.T.);
#71177=ORIENTED_EDGE('',*,*,#50641,.F.);
#71178=ORIENTED_EDGE('',*,*,#50642,.T.);
#71179=ORIENTED_EDGE('',*,*,#50643,.F.);
#71180=ORIENTED_EDGE('',*,*,#50644,.T.);
#71181=ORIENTED_EDGE('',*,*,#50645,.F.);
#71182=ORIENTED_EDGE('',*,*,#50646,.T.);
#71183=ORIENTED_EDGE('',*,*,#50647,.F.);
#71184=ORIENTED_EDGE('',*,*,#50648,.T.);
#71185=ORIENTED_EDGE('',*,*,#50649,.F.);
#71186=ORIENTED_EDGE('',*,*,#50650,.T.);
#71187=ORIENTED_EDGE('',*,*,#50651,.F.);
#71188=ORIENTED_EDGE('',*,*,#50652,.T.);
#71189=ORIENTED_EDGE('',*,*,#50653,.F.);
#71190=ORIENTED_EDGE('',*,*,#50654,.T.);
#71191=ORIENTED_EDGE('',*,*,#50655,.F.);
#71192=ORIENTED_EDGE('',*,*,#50656,.T.);
#71193=ORIENTED_EDGE('',*,*,#50657,.F.);
#71194=ORIENTED_EDGE('',*,*,#50658,.T.);
#71195=ORIENTED_EDGE('',*,*,#50069,.T.);
#71196=ORIENTED_EDGE('',*,*,#50659,.T.);
#71197=ORIENTED_EDGE('',*,*,#49871,.F.);
#71198=ORIENTED_EDGE('',*,*,#49867,.F.);
#71199=ORIENTED_EDGE('',*,*,#50660,.T.);
#71200=ORIENTED_EDGE('',*,*,#49835,.F.);
#71201=ORIENTED_EDGE('',*,*,#50661,.T.);
#71202=ORIENTED_EDGE('',*,*,#50117,.T.);
#71203=ORIENTED_EDGE('',*,*,#50662,.T.);
#71204=ORIENTED_EDGE('',*,*,#50123,.T.);
#71205=ORIENTED_EDGE('',*,*,#50663,.T.);
#71206=ORIENTED_EDGE('',*,*,#49831,.F.);
#71207=ORIENTED_EDGE('',*,*,#50664,.T.);
#71208=ORIENTED_EDGE('',*,*,#50129,.T.);
#71209=ORIENTED_EDGE('',*,*,#50665,.T.);
#71210=ORIENTED_EDGE('',*,*,#49827,.F.);
#71211=ORIENTED_EDGE('',*,*,#50666,.T.);
#71212=ORIENTED_EDGE('',*,*,#50135,.T.);
#71213=ORIENTED_EDGE('',*,*,#50667,.T.);
#71214=ORIENTED_EDGE('',*,*,#49823,.F.);
#71215=ORIENTED_EDGE('',*,*,#50668,.T.);
#71216=ORIENTED_EDGE('',*,*,#50141,.T.);
#71217=ORIENTED_EDGE('',*,*,#50669,.T.);
#71218=ORIENTED_EDGE('',*,*,#49819,.F.);
#71219=ORIENTED_EDGE('',*,*,#50670,.T.);
#71220=ORIENTED_EDGE('',*,*,#50147,.T.);
#71221=ORIENTED_EDGE('',*,*,#50671,.T.);
#71222=ORIENTED_EDGE('',*,*,#49815,.F.);
#71223=ORIENTED_EDGE('',*,*,#50672,.T.);
#71224=ORIENTED_EDGE('',*,*,#50153,.T.);
#71225=ORIENTED_EDGE('',*,*,#50673,.T.);
#71226=ORIENTED_EDGE('',*,*,#49811,.F.);
#71227=ORIENTED_EDGE('',*,*,#50674,.T.);
#71228=ORIENTED_EDGE('',*,*,#50159,.T.);
#71229=ORIENTED_EDGE('',*,*,#50675,.T.);
#71230=ORIENTED_EDGE('',*,*,#49807,.F.);
#71231=ORIENTED_EDGE('',*,*,#50676,.T.);
#71232=ORIENTED_EDGE('',*,*,#50165,.T.);
#71233=ORIENTED_EDGE('',*,*,#50677,.T.);
#71234=ORIENTED_EDGE('',*,*,#49803,.F.);
#71235=ORIENTED_EDGE('',*,*,#50678,.T.);
#71236=ORIENTED_EDGE('',*,*,#50171,.T.);
#71237=ORIENTED_EDGE('',*,*,#50679,.T.);
#71238=ORIENTED_EDGE('',*,*,#49799,.F.);
#71239=ORIENTED_EDGE('',*,*,#50680,.T.);
#71240=ORIENTED_EDGE('',*,*,#50177,.T.);
#71241=ORIENTED_EDGE('',*,*,#50681,.T.);
#71242=ORIENTED_EDGE('',*,*,#49795,.F.);
#71243=ORIENTED_EDGE('',*,*,#50682,.T.);
#71244=ORIENTED_EDGE('',*,*,#50183,.T.);
#71245=ORIENTED_EDGE('',*,*,#50683,.T.);
#71246=ORIENTED_EDGE('',*,*,#49791,.F.);
#71247=ORIENTED_EDGE('',*,*,#50684,.T.);
#71248=ORIENTED_EDGE('',*,*,#50189,.T.);
#71249=ORIENTED_EDGE('',*,*,#50685,.T.);
#71250=ORIENTED_EDGE('',*,*,#49787,.F.);
#71251=ORIENTED_EDGE('',*,*,#50686,.T.);
#71252=ORIENTED_EDGE('',*,*,#50195,.T.);
#71253=ORIENTED_EDGE('',*,*,#50687,.T.);
#71254=ORIENTED_EDGE('',*,*,#49783,.F.);
#71255=ORIENTED_EDGE('',*,*,#50688,.T.);
#71256=ORIENTED_EDGE('',*,*,#50201,.T.);
#71257=ORIENTED_EDGE('',*,*,#50689,.T.);
#71258=ORIENTED_EDGE('',*,*,#49779,.F.);
#71259=ORIENTED_EDGE('',*,*,#50690,.T.);
#71260=ORIENTED_EDGE('',*,*,#50207,.T.);
#71261=ORIENTED_EDGE('',*,*,#50691,.T.);
#71262=ORIENTED_EDGE('',*,*,#49775,.F.);
#71263=ORIENTED_EDGE('',*,*,#50692,.T.);
#71264=ORIENTED_EDGE('',*,*,#50213,.T.);
#71265=ORIENTED_EDGE('',*,*,#50693,.T.);
#71266=ORIENTED_EDGE('',*,*,#49771,.F.);
#71267=ORIENTED_EDGE('',*,*,#50694,.T.);
#71268=ORIENTED_EDGE('',*,*,#50219,.T.);
#71269=ORIENTED_EDGE('',*,*,#50695,.T.);
#71270=ORIENTED_EDGE('',*,*,#49767,.F.);
#71271=ORIENTED_EDGE('',*,*,#50696,.T.);
#71272=ORIENTED_EDGE('',*,*,#50225,.T.);
#71273=ORIENTED_EDGE('',*,*,#50697,.T.);
#71274=ORIENTED_EDGE('',*,*,#49763,.F.);
#71275=ORIENTED_EDGE('',*,*,#50698,.T.);
#71276=ORIENTED_EDGE('',*,*,#50231,.T.);
#71277=ORIENTED_EDGE('',*,*,#50699,.T.);
#71278=ORIENTED_EDGE('',*,*,#49759,.F.);
#71279=ORIENTED_EDGE('',*,*,#50700,.T.);
#71280=ORIENTED_EDGE('',*,*,#50237,.T.);
#71281=ORIENTED_EDGE('',*,*,#50701,.T.);
#71282=ORIENTED_EDGE('',*,*,#49755,.F.);
#71283=ORIENTED_EDGE('',*,*,#50702,.T.);
#71284=ORIENTED_EDGE('',*,*,#50243,.T.);
#71285=ORIENTED_EDGE('',*,*,#50703,.T.);
#71286=ORIENTED_EDGE('',*,*,#49751,.F.);
#71287=ORIENTED_EDGE('',*,*,#50704,.T.);
#71288=ORIENTED_EDGE('',*,*,#50249,.T.);
#71289=ORIENTED_EDGE('',*,*,#50705,.T.);
#71290=ORIENTED_EDGE('',*,*,#49747,.F.);
#71291=ORIENTED_EDGE('',*,*,#50706,.T.);
#71292=ORIENTED_EDGE('',*,*,#50255,.T.);
#71293=ORIENTED_EDGE('',*,*,#50707,.T.);
#71294=ORIENTED_EDGE('',*,*,#49743,.F.);
#71295=ORIENTED_EDGE('',*,*,#50708,.T.);
#71296=ORIENTED_EDGE('',*,*,#50261,.T.);
#71297=ORIENTED_EDGE('',*,*,#50709,.T.);
#71298=ORIENTED_EDGE('',*,*,#49739,.F.);
#71299=ORIENTED_EDGE('',*,*,#50710,.T.);
#71300=ORIENTED_EDGE('',*,*,#50267,.T.);
#71301=ORIENTED_EDGE('',*,*,#50711,.T.);
#71302=ORIENTED_EDGE('',*,*,#49735,.F.);
#71303=ORIENTED_EDGE('',*,*,#50712,.T.);
#71304=ORIENTED_EDGE('',*,*,#50273,.T.);
#71305=ORIENTED_EDGE('',*,*,#50713,.T.);
#71306=ORIENTED_EDGE('',*,*,#49731,.F.);
#71307=ORIENTED_EDGE('',*,*,#50714,.T.);
#71308=ORIENTED_EDGE('',*,*,#50279,.T.);
#71309=ORIENTED_EDGE('',*,*,#50715,.T.);
#71310=ORIENTED_EDGE('',*,*,#49727,.F.);
#71311=ORIENTED_EDGE('',*,*,#50716,.T.);
#71312=ORIENTED_EDGE('',*,*,#50285,.T.);
#71313=ORIENTED_EDGE('',*,*,#50717,.T.);
#71314=ORIENTED_EDGE('',*,*,#49723,.F.);
#71315=ORIENTED_EDGE('',*,*,#50718,.T.);
#71316=ORIENTED_EDGE('',*,*,#50291,.T.);
#71317=ORIENTED_EDGE('',*,*,#50719,.T.);
#71318=ORIENTED_EDGE('',*,*,#49719,.F.);
#71319=ORIENTED_EDGE('',*,*,#50720,.T.);
#71320=ORIENTED_EDGE('',*,*,#50297,.T.);
#71321=ORIENTED_EDGE('',*,*,#50721,.T.);
#71322=ORIENTED_EDGE('',*,*,#49715,.F.);
#71323=ORIENTED_EDGE('',*,*,#50722,.T.);
#71324=ORIENTED_EDGE('',*,*,#50303,.T.);
#71325=ORIENTED_EDGE('',*,*,#50723,.T.);
#71326=ORIENTED_EDGE('',*,*,#49711,.F.);
#71327=ORIENTED_EDGE('',*,*,#50724,.T.);
#71328=ORIENTED_EDGE('',*,*,#50309,.T.);
#71329=ORIENTED_EDGE('',*,*,#50725,.T.);
#71330=ORIENTED_EDGE('',*,*,#49707,.F.);
#71331=ORIENTED_EDGE('',*,*,#50726,.T.);
#71332=ORIENTED_EDGE('',*,*,#50315,.T.);
#71333=ORIENTED_EDGE('',*,*,#50727,.T.);
#71334=ORIENTED_EDGE('',*,*,#49703,.F.);
#71335=ORIENTED_EDGE('',*,*,#50728,.T.);
#71336=ORIENTED_EDGE('',*,*,#50321,.T.);
#71337=ORIENTED_EDGE('',*,*,#50729,.T.);
#71338=ORIENTED_EDGE('',*,*,#49699,.F.);
#71339=ORIENTED_EDGE('',*,*,#50730,.T.);
#71340=ORIENTED_EDGE('',*,*,#50327,.T.);
#71341=ORIENTED_EDGE('',*,*,#50731,.T.);
#71342=ORIENTED_EDGE('',*,*,#49695,.F.);
#71343=ORIENTED_EDGE('',*,*,#50732,.T.);
#71344=ORIENTED_EDGE('',*,*,#50333,.T.);
#71345=ORIENTED_EDGE('',*,*,#50733,.T.);
#71346=ORIENTED_EDGE('',*,*,#49691,.F.);
#71347=ORIENTED_EDGE('',*,*,#50734,.T.);
#71348=ORIENTED_EDGE('',*,*,#50339,.T.);
#71349=ORIENTED_EDGE('',*,*,#50735,.T.);
#71350=ORIENTED_EDGE('',*,*,#49687,.F.);
#71351=ORIENTED_EDGE('',*,*,#50736,.T.);
#71352=ORIENTED_EDGE('',*,*,#50345,.T.);
#71353=ORIENTED_EDGE('',*,*,#50737,.T.);
#71354=ORIENTED_EDGE('',*,*,#49683,.F.);
#71355=ORIENTED_EDGE('',*,*,#50738,.T.);
#71356=ORIENTED_EDGE('',*,*,#50351,.T.);
#71357=ORIENTED_EDGE('',*,*,#50739,.T.);
#71358=ORIENTED_EDGE('',*,*,#49679,.F.);
#71359=ORIENTED_EDGE('',*,*,#50740,.T.);
#71360=ORIENTED_EDGE('',*,*,#50357,.T.);
#71361=ORIENTED_EDGE('',*,*,#50741,.T.);
#71362=ORIENTED_EDGE('',*,*,#49675,.F.);
#71363=ORIENTED_EDGE('',*,*,#50742,.T.);
#71364=ORIENTED_EDGE('',*,*,#50365,.T.);
#71365=ORIENTED_EDGE('',*,*,#50363,.T.);
#71366=ORIENTED_EDGE('',*,*,#50743,.T.);
#71367=ORIENTED_EDGE('',*,*,#49671,.F.);
#71368=ORIENTED_EDGE('',*,*,#50744,.T.);
#71369=ORIENTED_EDGE('',*,*,#50371,.T.);
#71370=ORIENTED_EDGE('',*,*,#50745,.T.);
#71371=ORIENTED_EDGE('',*,*,#50063,.F.);
#71372=ORIENTED_EDGE('',*,*,#50746,.T.);
#71373=ORIENTED_EDGE('',*,*,#50377,.T.);
#71374=ORIENTED_EDGE('',*,*,#50747,.T.);
#71375=ORIENTED_EDGE('',*,*,#50059,.F.);
#71376=ORIENTED_EDGE('',*,*,#50748,.T.);
#71377=ORIENTED_EDGE('',*,*,#50383,.T.);
#71378=ORIENTED_EDGE('',*,*,#50749,.T.);
#71379=ORIENTED_EDGE('',*,*,#50055,.F.);
#71380=ORIENTED_EDGE('',*,*,#50750,.T.);
#71381=ORIENTED_EDGE('',*,*,#50389,.T.);
#71382=ORIENTED_EDGE('',*,*,#50751,.T.);
#71383=ORIENTED_EDGE('',*,*,#50051,.F.);
#71384=ORIENTED_EDGE('',*,*,#50752,.T.);
#71385=ORIENTED_EDGE('',*,*,#50395,.T.);
#71386=ORIENTED_EDGE('',*,*,#50753,.T.);
#71387=ORIENTED_EDGE('',*,*,#50047,.F.);
#71388=ORIENTED_EDGE('',*,*,#50754,.T.);
#71389=ORIENTED_EDGE('',*,*,#50401,.T.);
#71390=ORIENTED_EDGE('',*,*,#50755,.T.);
#71391=ORIENTED_EDGE('',*,*,#50043,.F.);
#71392=ORIENTED_EDGE('',*,*,#50756,.T.);
#71393=ORIENTED_EDGE('',*,*,#50407,.T.);
#71394=ORIENTED_EDGE('',*,*,#50757,.T.);
#71395=ORIENTED_EDGE('',*,*,#50039,.F.);
#71396=ORIENTED_EDGE('',*,*,#50758,.T.);
#71397=ORIENTED_EDGE('',*,*,#50413,.T.);
#71398=ORIENTED_EDGE('',*,*,#50759,.T.);
#71399=ORIENTED_EDGE('',*,*,#50035,.F.);
#71400=ORIENTED_EDGE('',*,*,#50760,.T.);
#71401=ORIENTED_EDGE('',*,*,#50419,.T.);
#71402=ORIENTED_EDGE('',*,*,#50761,.T.);
#71403=ORIENTED_EDGE('',*,*,#50031,.F.);
#71404=ORIENTED_EDGE('',*,*,#50762,.T.);
#71405=ORIENTED_EDGE('',*,*,#50425,.T.);
#71406=ORIENTED_EDGE('',*,*,#50763,.T.);
#71407=ORIENTED_EDGE('',*,*,#50027,.F.);
#71408=ORIENTED_EDGE('',*,*,#50764,.T.);
#71409=ORIENTED_EDGE('',*,*,#50431,.T.);
#71410=ORIENTED_EDGE('',*,*,#50765,.T.);
#71411=ORIENTED_EDGE('',*,*,#50023,.F.);
#71412=ORIENTED_EDGE('',*,*,#50766,.T.);
#71413=ORIENTED_EDGE('',*,*,#50437,.T.);
#71414=ORIENTED_EDGE('',*,*,#50767,.T.);
#71415=ORIENTED_EDGE('',*,*,#50019,.F.);
#71416=ORIENTED_EDGE('',*,*,#50768,.T.);
#71417=ORIENTED_EDGE('',*,*,#50443,.T.);
#71418=ORIENTED_EDGE('',*,*,#50769,.T.);
#71419=ORIENTED_EDGE('',*,*,#50015,.F.);
#71420=ORIENTED_EDGE('',*,*,#50770,.T.);
#71421=ORIENTED_EDGE('',*,*,#50449,.T.);
#71422=ORIENTED_EDGE('',*,*,#50771,.T.);
#71423=ORIENTED_EDGE('',*,*,#50011,.F.);
#71424=ORIENTED_EDGE('',*,*,#50772,.T.);
#71425=ORIENTED_EDGE('',*,*,#50455,.T.);
#71426=ORIENTED_EDGE('',*,*,#50773,.T.);
#71427=ORIENTED_EDGE('',*,*,#50007,.F.);
#71428=ORIENTED_EDGE('',*,*,#50774,.T.);
#71429=ORIENTED_EDGE('',*,*,#50461,.T.);
#71430=ORIENTED_EDGE('',*,*,#50775,.T.);
#71431=ORIENTED_EDGE('',*,*,#50003,.F.);
#71432=ORIENTED_EDGE('',*,*,#50776,.T.);
#71433=ORIENTED_EDGE('',*,*,#50467,.T.);
#71434=ORIENTED_EDGE('',*,*,#50777,.T.);
#71435=ORIENTED_EDGE('',*,*,#49999,.F.);
#71436=ORIENTED_EDGE('',*,*,#50778,.T.);
#71437=ORIENTED_EDGE('',*,*,#50473,.T.);
#71438=ORIENTED_EDGE('',*,*,#50779,.T.);
#71439=ORIENTED_EDGE('',*,*,#49995,.F.);
#71440=ORIENTED_EDGE('',*,*,#50780,.T.);
#71441=ORIENTED_EDGE('',*,*,#50479,.T.);
#71442=ORIENTED_EDGE('',*,*,#50781,.T.);
#71443=ORIENTED_EDGE('',*,*,#49991,.F.);
#71444=ORIENTED_EDGE('',*,*,#50782,.T.);
#71445=ORIENTED_EDGE('',*,*,#50485,.T.);
#71446=ORIENTED_EDGE('',*,*,#50783,.T.);
#71447=ORIENTED_EDGE('',*,*,#49987,.F.);
#71448=ORIENTED_EDGE('',*,*,#50784,.T.);
#71449=ORIENTED_EDGE('',*,*,#50491,.T.);
#71450=ORIENTED_EDGE('',*,*,#50785,.T.);
#71451=ORIENTED_EDGE('',*,*,#49983,.F.);
#71452=ORIENTED_EDGE('',*,*,#50786,.T.);
#71453=ORIENTED_EDGE('',*,*,#50497,.T.);
#71454=ORIENTED_EDGE('',*,*,#50787,.T.);
#71455=ORIENTED_EDGE('',*,*,#49979,.F.);
#71456=ORIENTED_EDGE('',*,*,#50788,.T.);
#71457=ORIENTED_EDGE('',*,*,#49839,.F.);
#71458=ORIENTED_EDGE('',*,*,#50789,.T.);
#71459=ORIENTED_EDGE('',*,*,#50111,.T.);
#71460=ORIENTED_EDGE('',*,*,#50790,.T.);
#71461=ORIENTED_EDGE('',*,*,#49843,.F.);
#71462=ORIENTED_EDGE('',*,*,#50791,.T.);
#71463=ORIENTED_EDGE('',*,*,#50105,.T.);
#71464=ORIENTED_EDGE('',*,*,#50792,.T.);
#71465=ORIENTED_EDGE('',*,*,#49847,.F.);
#71466=ORIENTED_EDGE('',*,*,#50793,.T.);
#71467=ORIENTED_EDGE('',*,*,#50099,.T.);
#71468=ORIENTED_EDGE('',*,*,#50794,.T.);
#71469=ORIENTED_EDGE('',*,*,#49851,.F.);
#71470=ORIENTED_EDGE('',*,*,#50795,.T.);
#71471=ORIENTED_EDGE('',*,*,#50093,.T.);
#71472=ORIENTED_EDGE('',*,*,#50796,.T.);
#71473=ORIENTED_EDGE('',*,*,#49855,.F.);
#71474=ORIENTED_EDGE('',*,*,#50797,.T.);
#71475=ORIENTED_EDGE('',*,*,#50087,.T.);
#71476=ORIENTED_EDGE('',*,*,#50798,.T.);
#71477=ORIENTED_EDGE('',*,*,#49859,.F.);
#71478=ORIENTED_EDGE('',*,*,#50799,.T.);
#71479=ORIENTED_EDGE('',*,*,#50081,.T.);
#71480=ORIENTED_EDGE('',*,*,#50800,.T.);
#71481=ORIENTED_EDGE('',*,*,#49863,.F.);
#71482=ORIENTED_EDGE('',*,*,#50801,.T.);
#71483=ORIENTED_EDGE('',*,*,#50075,.T.);
#71484=ORIENTED_EDGE('',*,*,#50802,.T.);
#71485=ORIENTED_EDGE('',*,*,#49875,.F.);
#71486=ORIENTED_EDGE('',*,*,#50803,.T.);
#71487=ORIENTED_EDGE('',*,*,#50653,.T.);
#71488=ORIENTED_EDGE('',*,*,#50804,.T.);
#71489=ORIENTED_EDGE('',*,*,#49879,.F.);
#71490=ORIENTED_EDGE('',*,*,#50805,.T.);
#71491=ORIENTED_EDGE('',*,*,#50647,.T.);
#71492=ORIENTED_EDGE('',*,*,#50806,.T.);
#71493=ORIENTED_EDGE('',*,*,#49883,.F.);
#71494=ORIENTED_EDGE('',*,*,#50807,.T.);
#71495=ORIENTED_EDGE('',*,*,#50641,.T.);
#71496=ORIENTED_EDGE('',*,*,#50808,.T.);
#71497=ORIENTED_EDGE('',*,*,#49887,.F.);
#71498=ORIENTED_EDGE('',*,*,#50809,.T.);
#71499=ORIENTED_EDGE('',*,*,#50635,.T.);
#71500=ORIENTED_EDGE('',*,*,#50810,.T.);
#71501=ORIENTED_EDGE('',*,*,#49891,.F.);
#71502=ORIENTED_EDGE('',*,*,#50811,.T.);
#71503=ORIENTED_EDGE('',*,*,#50629,.T.);
#71504=ORIENTED_EDGE('',*,*,#50812,.T.);
#71505=ORIENTED_EDGE('',*,*,#49895,.F.);
#71506=ORIENTED_EDGE('',*,*,#50813,.T.);
#71507=ORIENTED_EDGE('',*,*,#50623,.T.);
#71508=ORIENTED_EDGE('',*,*,#50814,.T.);
#71509=ORIENTED_EDGE('',*,*,#49899,.F.);
#71510=ORIENTED_EDGE('',*,*,#50815,.T.);
#71511=ORIENTED_EDGE('',*,*,#50617,.T.);
#71512=ORIENTED_EDGE('',*,*,#50816,.T.);
#71513=ORIENTED_EDGE('',*,*,#49903,.F.);
#71514=ORIENTED_EDGE('',*,*,#50817,.T.);
#71515=ORIENTED_EDGE('',*,*,#50611,.T.);
#71516=ORIENTED_EDGE('',*,*,#50818,.T.);
#71517=ORIENTED_EDGE('',*,*,#49907,.F.);
#71518=ORIENTED_EDGE('',*,*,#50819,.T.);
#71519=ORIENTED_EDGE('',*,*,#50605,.T.);
#71520=ORIENTED_EDGE('',*,*,#50820,.T.);
#71521=ORIENTED_EDGE('',*,*,#49911,.F.);
#71522=ORIENTED_EDGE('',*,*,#50821,.T.);
#71523=ORIENTED_EDGE('',*,*,#50599,.T.);
#71524=ORIENTED_EDGE('',*,*,#50822,.T.);
#71525=ORIENTED_EDGE('',*,*,#49915,.F.);
#71526=ORIENTED_EDGE('',*,*,#50823,.T.);
#71527=ORIENTED_EDGE('',*,*,#50593,.T.);
#71528=ORIENTED_EDGE('',*,*,#50824,.T.);
#71529=ORIENTED_EDGE('',*,*,#49919,.F.);
#71530=ORIENTED_EDGE('',*,*,#50825,.T.);
#71531=ORIENTED_EDGE('',*,*,#50587,.T.);
#71532=ORIENTED_EDGE('',*,*,#50826,.T.);
#71533=ORIENTED_EDGE('',*,*,#49923,.F.);
#71534=ORIENTED_EDGE('',*,*,#50827,.T.);
#71535=ORIENTED_EDGE('',*,*,#50581,.T.);
#71536=ORIENTED_EDGE('',*,*,#50828,.T.);
#71537=ORIENTED_EDGE('',*,*,#49927,.F.);
#71538=ORIENTED_EDGE('',*,*,#50829,.T.);
#71539=ORIENTED_EDGE('',*,*,#50575,.T.);
#71540=ORIENTED_EDGE('',*,*,#50830,.T.);
#71541=ORIENTED_EDGE('',*,*,#49931,.F.);
#71542=ORIENTED_EDGE('',*,*,#50831,.T.);
#71543=ORIENTED_EDGE('',*,*,#50569,.T.);
#71544=ORIENTED_EDGE('',*,*,#50832,.T.);
#71545=ORIENTED_EDGE('',*,*,#49935,.F.);
#71546=ORIENTED_EDGE('',*,*,#50833,.T.);
#71547=ORIENTED_EDGE('',*,*,#50563,.T.);
#71548=ORIENTED_EDGE('',*,*,#50834,.T.);
#71549=ORIENTED_EDGE('',*,*,#49939,.F.);
#71550=ORIENTED_EDGE('',*,*,#50835,.T.);
#71551=ORIENTED_EDGE('',*,*,#50557,.T.);
#71552=ORIENTED_EDGE('',*,*,#50836,.T.);
#71553=ORIENTED_EDGE('',*,*,#49943,.F.);
#71554=ORIENTED_EDGE('',*,*,#50837,.T.);
#71555=ORIENTED_EDGE('',*,*,#50551,.T.);
#71556=ORIENTED_EDGE('',*,*,#50838,.T.);
#71557=ORIENTED_EDGE('',*,*,#49947,.F.);
#71558=ORIENTED_EDGE('',*,*,#50839,.T.);
#71559=ORIENTED_EDGE('',*,*,#50545,.T.);
#71560=ORIENTED_EDGE('',*,*,#50840,.T.);
#71561=ORIENTED_EDGE('',*,*,#49951,.F.);
#71562=ORIENTED_EDGE('',*,*,#50841,.T.);
#71563=ORIENTED_EDGE('',*,*,#50539,.T.);
#71564=ORIENTED_EDGE('',*,*,#50842,.T.);
#71565=ORIENTED_EDGE('',*,*,#49955,.F.);
#71566=ORIENTED_EDGE('',*,*,#50843,.T.);
#71567=ORIENTED_EDGE('',*,*,#50533,.T.);
#71568=ORIENTED_EDGE('',*,*,#50844,.T.);
#71569=ORIENTED_EDGE('',*,*,#49959,.F.);
#71570=ORIENTED_EDGE('',*,*,#50845,.T.);
#71571=ORIENTED_EDGE('',*,*,#50527,.T.);
#71572=ORIENTED_EDGE('',*,*,#50846,.T.);
#71573=ORIENTED_EDGE('',*,*,#49963,.F.);
#71574=ORIENTED_EDGE('',*,*,#50847,.T.);
#71575=ORIENTED_EDGE('',*,*,#50521,.T.);
#71576=ORIENTED_EDGE('',*,*,#50848,.T.);
#71577=ORIENTED_EDGE('',*,*,#49967,.F.);
#71578=ORIENTED_EDGE('',*,*,#50849,.T.);
#71579=ORIENTED_EDGE('',*,*,#50515,.T.);
#71580=ORIENTED_EDGE('',*,*,#50850,.T.);
#71581=ORIENTED_EDGE('',*,*,#50503,.T.);
#71582=ORIENTED_EDGE('',*,*,#50851,.T.);
#71583=ORIENTED_EDGE('',*,*,#49975,.F.);
#71584=ORIENTED_EDGE('',*,*,#50852,.T.);
#71585=ORIENTED_EDGE('',*,*,#50853,.T.);
#71586=ORIENTED_EDGE('',*,*,#50854,.T.);
#71587=ORIENTED_EDGE('',*,*,#50855,.F.);
#71588=ORIENTED_EDGE('',*,*,#50856,.T.);
#71589=ORIENTED_EDGE('',*,*,#50857,.T.);
#71590=ORIENTED_EDGE('',*,*,#50858,.T.);
#71591=ORIENTED_EDGE('',*,*,#50853,.F.);
#71592=ORIENTED_EDGE('',*,*,#50859,.T.);
#71593=ORIENTED_EDGE('',*,*,#50860,.T.);
#71594=ORIENTED_EDGE('',*,*,#50855,.T.);
#71595=ORIENTED_EDGE('',*,*,#50861,.T.);
#71596=ORIENTED_EDGE('',*,*,#50862,.T.);
#71597=ORIENTED_EDGE('',*,*,#50863,.T.);
#71598=ORIENTED_EDGE('',*,*,#50864,.T.);
#71599=ORIENTED_EDGE('',*,*,#50865,.T.);
#71600=ORIENTED_EDGE('',*,*,#49661,.T.);
#71601=ORIENTED_EDGE('',*,*,#50866,.T.);
#71602=ORIENTED_EDGE('',*,*,#50867,.T.);
#71603=ORIENTED_EDGE('',*,*,#49660,.T.);
#71604=ORIENTED_EDGE('',*,*,#50868,.T.);
#71605=ORIENTED_EDGE('',*,*,#50869,.T.);
#71606=ORIENTED_EDGE('',*,*,#49659,.F.);
#71607=ORIENTED_EDGE('',*,*,#50870,.T.);
#71608=ORIENTED_EDGE('',*,*,#50871,.T.);
#71609=ORIENTED_EDGE('',*,*,#49658,.T.);
#71610=ORIENTED_EDGE('',*,*,#50872,.T.);
#71611=ORIENTED_EDGE('',*,*,#50873,.T.);
#71612=ORIENTED_EDGE('',*,*,#49657,.T.);
#71613=ORIENTED_EDGE('',*,*,#50874,.T.);
#71614=ORIENTED_EDGE('',*,*,#50067,.T.);
#71615=ORIENTED_EDGE('',*,*,#50875,.F.);
#71616=ORIENTED_EDGE('',*,*,#50876,.F.);
#71617=ORIENTED_EDGE('',*,*,#49663,.F.);
#71618=ORIENTED_EDGE('',*,*,#50877,.F.);
#71619=ORIENTED_EDGE('',*,*,#50878,.F.);
#71620=ORIENTED_EDGE('',*,*,#50879,.F.);
#71621=ORIENTED_EDGE('',*,*,#50509,.T.);
#71622=ORIENTED_EDGE('',*,*,#50880,.T.);
#71623=ORIENTED_EDGE('',*,*,#49971,.F.);
#71624=ORIENTED_EDGE('',*,*,#50881,.T.);
#71625=ORIENTED_EDGE('',*,*,#50882,.T.);
#71626=ORIENTED_EDGE('',*,*,#50883,.F.);
#71627=ORIENTED_EDGE('',*,*,#50884,.F.);
#71628=ORIENTED_EDGE('',*,*,#50868,.F.);
#71629=ORIENTED_EDGE('',*,*,#50869,.F.);
#71630=ORIENTED_EDGE('',*,*,#50885,.T.);
#71631=ORIENTED_EDGE('',*,*,#49662,.F.);
#71632=ORIENTED_EDGE('',*,*,#50882,.F.);
#71633=ORIENTED_EDGE('',*,*,#50870,.F.);
#71634=ORIENTED_EDGE('',*,*,#50871,.F.);
#71635=ORIENTED_EDGE('',*,*,#50886,.T.);
#71636=ORIENTED_EDGE('',*,*,#50887,.F.);
#71637=ORIENTED_EDGE('',*,*,#50885,.F.);
#71638=ORIENTED_EDGE('',*,*,#50872,.F.);
#71639=ORIENTED_EDGE('',*,*,#50873,.F.);
#71640=ORIENTED_EDGE('',*,*,#50888,.T.);
#71641=ORIENTED_EDGE('',*,*,#50889,.F.);
#71642=ORIENTED_EDGE('',*,*,#50886,.F.);
#71643=ORIENTED_EDGE('',*,*,#50874,.F.);
#71644=ORIENTED_EDGE('',*,*,#50890,.F.);
#71645=ORIENTED_EDGE('',*,*,#50891,.T.);
#71646=ORIENTED_EDGE('',*,*,#50892,.F.);
#71647=ORIENTED_EDGE('',*,*,#50888,.F.);
#71648=ORIENTED_EDGE('',*,*,#50893,.F.);
#71649=ORIENTED_EDGE('',*,*,#50865,.F.);
#71650=ORIENTED_EDGE('',*,*,#50884,.T.);
#71651=ORIENTED_EDGE('',*,*,#50894,.F.);
#71652=ORIENTED_EDGE('',*,*,#50891,.F.);
#71653=ORIENTED_EDGE('',*,*,#50866,.F.);
#71654=ORIENTED_EDGE('',*,*,#50867,.F.);
#71655=ORIENTED_EDGE('',*,*,#50890,.T.);
#71656=ORIENTED_EDGE('',*,*,#49656,.T.);
#71657=ORIENTED_EDGE('',*,*,#50893,.T.);
#71658=ORIENTED_EDGE('',*,*,#50894,.T.);
#71659=ORIENTED_EDGE('',*,*,#50875,.T.);
#71660=ORIENTED_EDGE('',*,*,#50889,.T.);
#71661=ORIENTED_EDGE('',*,*,#50878,.T.);
#71662=ORIENTED_EDGE('',*,*,#50887,.T.);
#71663=ORIENTED_EDGE('',*,*,#50877,.T.);
#71664=ORIENTED_EDGE('',*,*,#50892,.T.);
#71665=ORIENTED_EDGE('',*,*,#50879,.T.);
#71666=ORIENTED_EDGE('',*,*,#50883,.T.);
#71667=ORIENTED_EDGE('',*,*,#50876,.T.);
#71668=ORIENTED_EDGE('',*,*,#49666,.F.);
#71669=ORIENTED_EDGE('',*,*,#49654,.F.);
#71670=ORIENTED_EDGE('',*,*,#49466,.F.);
#71671=ORIENTED_EDGE('',*,*,#49646,.F.);
#71672=ORIENTED_EDGE('',*,*,#49645,.F.);
#71673=ORIENTED_EDGE('',*,*,#49548,.T.);
#71674=ORIENTED_EDGE('',*,*,#50895,.T.);
#71675=ORIENTED_EDGE('',*,*,#49641,.T.);
#71676=ORIENTED_EDGE('',*,*,#50896,.F.);
#71677=ORIENTED_EDGE('',*,*,#49557,.F.);
#71678=ORIENTED_EDGE('',*,*,#49650,.T.);
#71679=ORIENTED_EDGE('',*,*,#49642,.T.);
#71680=ORIENTED_EDGE('',*,*,#50895,.F.);
#71681=ORIENTED_EDGE('',*,*,#49550,.F.);
#71682=ORIENTED_EDGE('',*,*,#49547,.F.);
#71683=ORIENTED_EDGE('',*,*,#49544,.F.);
#71684=ORIENTED_EDGE('',*,*,#49541,.F.);
#71685=ORIENTED_EDGE('',*,*,#49538,.F.);
#71686=ORIENTED_EDGE('',*,*,#49535,.F.);
#71687=ORIENTED_EDGE('',*,*,#49532,.F.);
#71688=ORIENTED_EDGE('',*,*,#49529,.F.);
#71689=ORIENTED_EDGE('',*,*,#49526,.F.);
#71690=ORIENTED_EDGE('',*,*,#49523,.F.);
#71691=ORIENTED_EDGE('',*,*,#49520,.F.);
#71692=ORIENTED_EDGE('',*,*,#49517,.F.);
#71693=ORIENTED_EDGE('',*,*,#49514,.F.);
#71694=ORIENTED_EDGE('',*,*,#49511,.F.);
#71695=ORIENTED_EDGE('',*,*,#49508,.F.);
#71696=ORIENTED_EDGE('',*,*,#49505,.F.);
#71697=ORIENTED_EDGE('',*,*,#49502,.F.);
#71698=ORIENTED_EDGE('',*,*,#49499,.F.);
#71699=ORIENTED_EDGE('',*,*,#49496,.F.);
#71700=ORIENTED_EDGE('',*,*,#49493,.F.);
#71701=ORIENTED_EDGE('',*,*,#49490,.F.);
#71702=ORIENTED_EDGE('',*,*,#49487,.F.);
#71703=ORIENTED_EDGE('',*,*,#49484,.F.);
#71704=ORIENTED_EDGE('',*,*,#49481,.F.);
#71705=ORIENTED_EDGE('',*,*,#49478,.F.);
#71706=ORIENTED_EDGE('',*,*,#49475,.F.);
#71707=ORIENTED_EDGE('',*,*,#49472,.F.);
#71708=ORIENTED_EDGE('',*,*,#49469,.F.);
#71709=ORIENTED_EDGE('',*,*,#49644,.T.);
#71710=ORIENTED_EDGE('',*,*,#49649,.T.);
#71711=ORIENTED_EDGE('',*,*,#49651,.F.);
#71712=ORIENTED_EDGE('',*,*,#49638,.F.);
#71713=ORIENTED_EDGE('',*,*,#49635,.F.);
#71714=ORIENTED_EDGE('',*,*,#49632,.F.);
#71715=ORIENTED_EDGE('',*,*,#49629,.F.);
#71716=ORIENTED_EDGE('',*,*,#49626,.F.);
#71717=ORIENTED_EDGE('',*,*,#49623,.F.);
#71718=ORIENTED_EDGE('',*,*,#49620,.F.);
#71719=ORIENTED_EDGE('',*,*,#49617,.F.);
#71720=ORIENTED_EDGE('',*,*,#49614,.F.);
#71721=ORIENTED_EDGE('',*,*,#49611,.F.);
#71722=ORIENTED_EDGE('',*,*,#49608,.F.);
#71723=ORIENTED_EDGE('',*,*,#49605,.F.);
#71724=ORIENTED_EDGE('',*,*,#49602,.F.);
#71725=ORIENTED_EDGE('',*,*,#49599,.F.);
#71726=ORIENTED_EDGE('',*,*,#49596,.F.);
#71727=ORIENTED_EDGE('',*,*,#49593,.F.);
#71728=ORIENTED_EDGE('',*,*,#49590,.F.);
#71729=ORIENTED_EDGE('',*,*,#49587,.F.);
#71730=ORIENTED_EDGE('',*,*,#49584,.F.);
#71731=ORIENTED_EDGE('',*,*,#49581,.F.);
#71732=ORIENTED_EDGE('',*,*,#49578,.F.);
#71733=ORIENTED_EDGE('',*,*,#49575,.F.);
#71734=ORIENTED_EDGE('',*,*,#49572,.F.);
#71735=ORIENTED_EDGE('',*,*,#49569,.F.);
#71736=ORIENTED_EDGE('',*,*,#49566,.F.);
#71737=ORIENTED_EDGE('',*,*,#49563,.F.);
#71738=ORIENTED_EDGE('',*,*,#49560,.F.);
#71739=ORIENTED_EDGE('',*,*,#49465,.T.);
#71740=ORIENTED_EDGE('',*,*,#49468,.T.);
#71741=ORIENTED_EDGE('',*,*,#49471,.T.);
#71742=ORIENTED_EDGE('',*,*,#49474,.T.);
#71743=ORIENTED_EDGE('',*,*,#49477,.T.);
#71744=ORIENTED_EDGE('',*,*,#49480,.T.);
#71745=ORIENTED_EDGE('',*,*,#49483,.T.);
#71746=ORIENTED_EDGE('',*,*,#49486,.T.);
#71747=ORIENTED_EDGE('',*,*,#49489,.T.);
#71748=ORIENTED_EDGE('',*,*,#49492,.T.);
#71749=ORIENTED_EDGE('',*,*,#49495,.T.);
#71750=ORIENTED_EDGE('',*,*,#49498,.T.);
#71751=ORIENTED_EDGE('',*,*,#49501,.T.);
#71752=ORIENTED_EDGE('',*,*,#49504,.T.);
#71753=ORIENTED_EDGE('',*,*,#49507,.T.);
#71754=ORIENTED_EDGE('',*,*,#49510,.T.);
#71755=ORIENTED_EDGE('',*,*,#49513,.T.);
#71756=ORIENTED_EDGE('',*,*,#49516,.T.);
#71757=ORIENTED_EDGE('',*,*,#49519,.T.);
#71758=ORIENTED_EDGE('',*,*,#49522,.T.);
#71759=ORIENTED_EDGE('',*,*,#49525,.T.);
#71760=ORIENTED_EDGE('',*,*,#49528,.T.);
#71761=ORIENTED_EDGE('',*,*,#49531,.T.);
#71762=ORIENTED_EDGE('',*,*,#49534,.T.);
#71763=ORIENTED_EDGE('',*,*,#49537,.T.);
#71764=ORIENTED_EDGE('',*,*,#49540,.T.);
#71765=ORIENTED_EDGE('',*,*,#49543,.T.);
#71766=ORIENTED_EDGE('',*,*,#49546,.T.);
#71767=ORIENTED_EDGE('',*,*,#49549,.T.);
#71768=ORIENTED_EDGE('',*,*,#50896,.T.);
#71769=ORIENTED_EDGE('',*,*,#49640,.T.);
#71770=ORIENTED_EDGE('',*,*,#49552,.F.);
#71771=ORIENTED_EDGE('',*,*,#49559,.F.);
#71772=ORIENTED_EDGE('',*,*,#49562,.F.);
#71773=ORIENTED_EDGE('',*,*,#49565,.F.);
#71774=ORIENTED_EDGE('',*,*,#49568,.F.);
#71775=ORIENTED_EDGE('',*,*,#49571,.F.);
#71776=ORIENTED_EDGE('',*,*,#49574,.F.);
#71777=ORIENTED_EDGE('',*,*,#49577,.F.);
#71778=ORIENTED_EDGE('',*,*,#49580,.F.);
#71779=ORIENTED_EDGE('',*,*,#49583,.F.);
#71780=ORIENTED_EDGE('',*,*,#49586,.F.);
#71781=ORIENTED_EDGE('',*,*,#49589,.F.);
#71782=ORIENTED_EDGE('',*,*,#49592,.F.);
#71783=ORIENTED_EDGE('',*,*,#49595,.F.);
#71784=ORIENTED_EDGE('',*,*,#49598,.F.);
#71785=ORIENTED_EDGE('',*,*,#49601,.F.);
#71786=ORIENTED_EDGE('',*,*,#49604,.F.);
#71787=ORIENTED_EDGE('',*,*,#49607,.F.);
#71788=ORIENTED_EDGE('',*,*,#49610,.F.);
#71789=ORIENTED_EDGE('',*,*,#49613,.F.);
#71790=ORIENTED_EDGE('',*,*,#49616,.F.);
#71791=ORIENTED_EDGE('',*,*,#49619,.F.);
#71792=ORIENTED_EDGE('',*,*,#49622,.F.);
#71793=ORIENTED_EDGE('',*,*,#49625,.F.);
#71794=ORIENTED_EDGE('',*,*,#49628,.F.);
#71795=ORIENTED_EDGE('',*,*,#49631,.F.);
#71796=ORIENTED_EDGE('',*,*,#49634,.F.);
#71797=ORIENTED_EDGE('',*,*,#49637,.F.);
#71798=ORIENTED_EDGE('',*,*,#49652,.F.);
#71799=ORIENTED_EDGE('',*,*,#49647,.T.);
#71800=ORIENTED_EDGE('',*,*,#50897,.T.);
#71801=ORIENTED_EDGE('',*,*,#50898,.T.);
#71802=ORIENTED_EDGE('',*,*,#50899,.T.);
#71803=ORIENTED_EDGE('',*,*,#50900,.F.);
#71804=ORIENTED_EDGE('',*,*,#50859,.F.);
#71805=ORIENTED_EDGE('',*,*,#50901,.F.);
#71806=ORIENTED_EDGE('',*,*,#50897,.F.);
#71807=ORIENTED_EDGE('',*,*,#50902,.F.);
#71808=ORIENTED_EDGE('',*,*,#50860,.F.);
#71809=ORIENTED_EDGE('',*,*,#50903,.F.);
#71810=ORIENTED_EDGE('',*,*,#50510,.F.);
#71811=ORIENTED_EDGE('',*,*,#50901,.T.);
#71812=ORIENTED_EDGE('',*,*,#50856,.F.);
#71813=ORIENTED_EDGE('',*,*,#50904,.F.);
#71814=ORIENTED_EDGE('',*,*,#50903,.T.);
#71815=ORIENTED_EDGE('',*,*,#50900,.T.);
#71816=ORIENTED_EDGE('',*,*,#50905,.F.);
#71817=ORIENTED_EDGE('',*,*,#50511,.T.);
#71818=ORIENTED_EDGE('',*,*,#50902,.T.);
#71819=ORIENTED_EDGE('',*,*,#50881,.F.);
#71820=ORIENTED_EDGE('',*,*,#50906,.F.);
#71821=ORIENTED_EDGE('',*,*,#50857,.F.);
#71822=ORIENTED_EDGE('',*,*,#50904,.T.);
#71823=ORIENTED_EDGE('',*,*,#50864,.F.);
#71824=ORIENTED_EDGE('',*,*,#50907,.F.);
#71825=ORIENTED_EDGE('',*,*,#50898,.F.);
#71826=ORIENTED_EDGE('',*,*,#50905,.T.);
#71827=ORIENTED_EDGE('',*,*,#50899,.F.);
#71828=ORIENTED_EDGE('',*,*,#50908,.F.);
#71829=ORIENTED_EDGE('',*,*,#50512,.F.);
#71830=ORIENTED_EDGE('',*,*,#50906,.T.);
#71831=ORIENTED_EDGE('',*,*,#49970,.F.);
#71832=ORIENTED_EDGE('',*,*,#50909,.F.);
#71833=ORIENTED_EDGE('',*,*,#50858,.F.);
#71834=ORIENTED_EDGE('',*,*,#50908,.T.);
#71835=ORIENTED_EDGE('',*,*,#50907,.T.);
#71836=ORIENTED_EDGE('',*,*,#50910,.F.);
#71837=ORIENTED_EDGE('',*,*,#50513,.T.);
#71838=ORIENTED_EDGE('',*,*,#50909,.T.);
#71839=ORIENTED_EDGE('',*,*,#49969,.F.);
#71840=ORIENTED_EDGE('',*,*,#50911,.F.);
#71841=ORIENTED_EDGE('',*,*,#50854,.F.);
#71842=ORIENTED_EDGE('',*,*,#50910,.T.);
#71843=ORIENTED_EDGE('',*,*,#50863,.F.);
#71844=ORIENTED_EDGE('',*,*,#50912,.F.);
#71845=ORIENTED_EDGE('',*,*,#50514,.F.);
#71846=ORIENTED_EDGE('',*,*,#50911,.T.);
#71847=ORIENTED_EDGE('',*,*,#49968,.F.);
#71848=ORIENTED_EDGE('',*,*,#50913,.F.);
#71849=ORIENTED_EDGE('',*,*,#50861,.F.);
#71850=ORIENTED_EDGE('',*,*,#50912,.T.);
#71851=ORIENTED_EDGE('',*,*,#50862,.F.);
#71852=ORIENTED_EDGE('',*,*,#50913,.T.);
#71853=ORIENTED_EDGE('',*,*,#50850,.F.);
#71854=ORIENTED_EDGE('',*,*,#50914,.T.);
#71855=ORIENTED_EDGE('',*,*,#50915,.T.);
#71856=ORIENTED_EDGE('',*,*,#50916,.T.);
#71857=ORIENTED_EDGE('',*,*,#50917,.T.);
#71858=ORIENTED_EDGE('',*,*,#50918,.T.);
#71859=ORIENTED_EDGE('',*,*,#50919,.T.);
#71860=ORIENTED_EDGE('',*,*,#50920,.T.);
#71861=ORIENTED_EDGE('',*,*,#50921,.F.);
#71862=ORIENTED_EDGE('',*,*,#50922,.T.);
#71863=ORIENTED_EDGE('',*,*,#50923,.T.);
#71864=ORIENTED_EDGE('',*,*,#50921,.T.);
#71865=ORIENTED_EDGE('',*,*,#50924,.T.);
#71866=ORIENTED_EDGE('',*,*,#50914,.F.);
#71867=ORIENTED_EDGE('',*,*,#50925,.T.);
#71868=ORIENTED_EDGE('',*,*,#50926,.F.);
#71869=ORIENTED_EDGE('',*,*,#50922,.F.);
#71870=ORIENTED_EDGE('',*,*,#50927,.F.);
#71871=ORIENTED_EDGE('',*,*,#50928,.F.);
#71872=ORIENTED_EDGE('',*,*,#50927,.T.);
#71873=ORIENTED_EDGE('',*,*,#50925,.F.);
#71874=ORIENTED_EDGE('',*,*,#50929,.F.);
#71875=ORIENTED_EDGE('',*,*,#50929,.T.);
#71876=ORIENTED_EDGE('',*,*,#50918,.F.);
#71877=ORIENTED_EDGE('',*,*,#50930,.F.);
#71878=ORIENTED_EDGE('',*,*,#50931,.F.);
#71879=ORIENTED_EDGE('',*,*,#50932,.T.);
#71880=ORIENTED_EDGE('',*,*,#50933,.F.);
#71881=ORIENTED_EDGE('',*,*,#50934,.F.);
#71882=ORIENTED_EDGE('',*,*,#50506,.F.);
#71883=ORIENTED_EDGE('',*,*,#50935,.T.);
#71884=ORIENTED_EDGE('',*,*,#50926,.T.);
#71885=ORIENTED_EDGE('',*,*,#50932,.F.);
#71886=ORIENTED_EDGE('',*,*,#50505,.T.);
#71887=ORIENTED_EDGE('',*,*,#50936,.F.);
#71888=ORIENTED_EDGE('',*,*,#50923,.F.);
#71889=ORIENTED_EDGE('',*,*,#50935,.F.);
#71890=ORIENTED_EDGE('',*,*,#50504,.F.);
#71891=ORIENTED_EDGE('',*,*,#50936,.T.);
#71892=ORIENTED_EDGE('',*,*,#50852,.F.);
#71893=ORIENTED_EDGE('',*,*,#50937,.F.);
#71894=ORIENTED_EDGE('',*,*,#50919,.F.);
#71895=ORIENTED_EDGE('',*,*,#50937,.T.);
#71896=ORIENTED_EDGE('',*,*,#49974,.F.);
#71897=ORIENTED_EDGE('',*,*,#50938,.F.);
#71898=ORIENTED_EDGE('',*,*,#50920,.F.);
#71899=ORIENTED_EDGE('',*,*,#50938,.T.);
#71900=ORIENTED_EDGE('',*,*,#49973,.F.);
#71901=ORIENTED_EDGE('',*,*,#50939,.F.);
#71902=ORIENTED_EDGE('',*,*,#50924,.F.);
#71903=ORIENTED_EDGE('',*,*,#50939,.T.);
#71904=ORIENTED_EDGE('',*,*,#49972,.F.);
#71905=ORIENTED_EDGE('',*,*,#50940,.F.);
#71906=ORIENTED_EDGE('',*,*,#50915,.F.);
#71907=ORIENTED_EDGE('',*,*,#50941,.T.);
#71908=ORIENTED_EDGE('',*,*,#50916,.F.);
#71909=ORIENTED_EDGE('',*,*,#50940,.T.);
#71910=ORIENTED_EDGE('',*,*,#50880,.F.);
#71911=ORIENTED_EDGE('',*,*,#50942,.T.);
#71912=ORIENTED_EDGE('',*,*,#50917,.F.);
#71913=ORIENTED_EDGE('',*,*,#50941,.F.);
#71914=ORIENTED_EDGE('',*,*,#50508,.F.);
#71915=ORIENTED_EDGE('',*,*,#50934,.T.);
#71916=ORIENTED_EDGE('',*,*,#50930,.T.);
#71917=ORIENTED_EDGE('',*,*,#50942,.F.);
#71918=ORIENTED_EDGE('',*,*,#50507,.T.);
#71919=ORIENTED_EDGE('',*,*,#50928,.T.);
#71920=ORIENTED_EDGE('',*,*,#50931,.T.);
#71921=ORIENTED_EDGE('',*,*,#50933,.T.);
#71922=ORIENTED_EDGE('',*,*,#50943,.T.);
#71923=ORIENTED_EDGE('',*,*,#50944,.T.);
#71924=ORIENTED_EDGE('',*,*,#50945,.T.);
#71925=ORIENTED_EDGE('',*,*,#50946,.T.);
#71926=ORIENTED_EDGE('',*,*,#50947,.T.);
#71927=ORIENTED_EDGE('',*,*,#50948,.T.);
#71928=ORIENTED_EDGE('',*,*,#50949,.T.);
#71929=ORIENTED_EDGE('',*,*,#50950,.F.);
#71930=ORIENTED_EDGE('',*,*,#50951,.T.);
#71931=ORIENTED_EDGE('',*,*,#50952,.T.);
#71932=ORIENTED_EDGE('',*,*,#50950,.T.);
#71933=ORIENTED_EDGE('',*,*,#50953,.T.);
#71934=ORIENTED_EDGE('',*,*,#50943,.F.);
#71935=ORIENTED_EDGE('',*,*,#50954,.T.);
#71936=ORIENTED_EDGE('',*,*,#50955,.F.);
#71937=ORIENTED_EDGE('',*,*,#50951,.F.);
#71938=ORIENTED_EDGE('',*,*,#50956,.F.);
#71939=ORIENTED_EDGE('',*,*,#50957,.F.);
#71940=ORIENTED_EDGE('',*,*,#50956,.T.);
#71941=ORIENTED_EDGE('',*,*,#50954,.F.);
#71942=ORIENTED_EDGE('',*,*,#50958,.F.);
#71943=ORIENTED_EDGE('',*,*,#50958,.T.);
#71944=ORIENTED_EDGE('',*,*,#50947,.F.);
#71945=ORIENTED_EDGE('',*,*,#50959,.F.);
#71946=ORIENTED_EDGE('',*,*,#50960,.F.);
#71947=ORIENTED_EDGE('',*,*,#50961,.T.);
#71948=ORIENTED_EDGE('',*,*,#50962,.F.);
#71949=ORIENTED_EDGE('',*,*,#50963,.F.);
#71950=ORIENTED_EDGE('',*,*,#50518,.F.);
#71951=ORIENTED_EDGE('',*,*,#50964,.T.);
#71952=ORIENTED_EDGE('',*,*,#50955,.T.);
#71953=ORIENTED_EDGE('',*,*,#50961,.F.);
#71954=ORIENTED_EDGE('',*,*,#50517,.T.);
#71955=ORIENTED_EDGE('',*,*,#50965,.F.);
#71956=ORIENTED_EDGE('',*,*,#50952,.F.);
#71957=ORIENTED_EDGE('',*,*,#50964,.F.);
#71958=ORIENTED_EDGE('',*,*,#50516,.F.);
#71959=ORIENTED_EDGE('',*,*,#50965,.T.);
#71960=ORIENTED_EDGE('',*,*,#50849,.F.);
#71961=ORIENTED_EDGE('',*,*,#50966,.F.);
#71962=ORIENTED_EDGE('',*,*,#50948,.F.);
#71963=ORIENTED_EDGE('',*,*,#50966,.T.);
#71964=ORIENTED_EDGE('',*,*,#49966,.F.);
#71965=ORIENTED_EDGE('',*,*,#50967,.F.);
#71966=ORIENTED_EDGE('',*,*,#50949,.F.);
#71967=ORIENTED_EDGE('',*,*,#50967,.T.);
#71968=ORIENTED_EDGE('',*,*,#49965,.F.);
#71969=ORIENTED_EDGE('',*,*,#50968,.F.);
#71970=ORIENTED_EDGE('',*,*,#50953,.F.);
#71971=ORIENTED_EDGE('',*,*,#50968,.T.);
#71972=ORIENTED_EDGE('',*,*,#49964,.F.);
#71973=ORIENTED_EDGE('',*,*,#50969,.F.);
#71974=ORIENTED_EDGE('',*,*,#50944,.F.);
#71975=ORIENTED_EDGE('',*,*,#50970,.T.);
#71976=ORIENTED_EDGE('',*,*,#50945,.F.);
#71977=ORIENTED_EDGE('',*,*,#50969,.T.);
#71978=ORIENTED_EDGE('',*,*,#50848,.F.);
#71979=ORIENTED_EDGE('',*,*,#50971,.T.);
#71980=ORIENTED_EDGE('',*,*,#50946,.F.);
#71981=ORIENTED_EDGE('',*,*,#50970,.F.);
#71982=ORIENTED_EDGE('',*,*,#50520,.F.);
#71983=ORIENTED_EDGE('',*,*,#50963,.T.);
#71984=ORIENTED_EDGE('',*,*,#50959,.T.);
#71985=ORIENTED_EDGE('',*,*,#50971,.F.);
#71986=ORIENTED_EDGE('',*,*,#50519,.T.);
#71987=ORIENTED_EDGE('',*,*,#50957,.T.);
#71988=ORIENTED_EDGE('',*,*,#50960,.T.);
#71989=ORIENTED_EDGE('',*,*,#50962,.T.);
#71990=ORIENTED_EDGE('',*,*,#50972,.T.);
#71991=ORIENTED_EDGE('',*,*,#50973,.T.);
#71992=ORIENTED_EDGE('',*,*,#50974,.T.);
#71993=ORIENTED_EDGE('',*,*,#50975,.T.);
#71994=ORIENTED_EDGE('',*,*,#50976,.T.);
#71995=ORIENTED_EDGE('',*,*,#50977,.T.);
#71996=ORIENTED_EDGE('',*,*,#50978,.T.);
#71997=ORIENTED_EDGE('',*,*,#50979,.F.);
#71998=ORIENTED_EDGE('',*,*,#50980,.T.);
#71999=ORIENTED_EDGE('',*,*,#50981,.T.);
#72000=ORIENTED_EDGE('',*,*,#50979,.T.);
#72001=ORIENTED_EDGE('',*,*,#50982,.T.);
#72002=ORIENTED_EDGE('',*,*,#50972,.F.);
#72003=ORIENTED_EDGE('',*,*,#50983,.T.);
#72004=ORIENTED_EDGE('',*,*,#50984,.F.);
#72005=ORIENTED_EDGE('',*,*,#50980,.F.);
#72006=ORIENTED_EDGE('',*,*,#50985,.F.);
#72007=ORIENTED_EDGE('',*,*,#50986,.F.);
#72008=ORIENTED_EDGE('',*,*,#50985,.T.);
#72009=ORIENTED_EDGE('',*,*,#50983,.F.);
#72010=ORIENTED_EDGE('',*,*,#50987,.F.);
#72011=ORIENTED_EDGE('',*,*,#50987,.T.);
#72012=ORIENTED_EDGE('',*,*,#50976,.F.);
#72013=ORIENTED_EDGE('',*,*,#50988,.F.);
#72014=ORIENTED_EDGE('',*,*,#50989,.F.);
#72015=ORIENTED_EDGE('',*,*,#50990,.T.);
#72016=ORIENTED_EDGE('',*,*,#50991,.F.);
#72017=ORIENTED_EDGE('',*,*,#50992,.F.);
#72018=ORIENTED_EDGE('',*,*,#50524,.F.);
#72019=ORIENTED_EDGE('',*,*,#50993,.T.);
#72020=ORIENTED_EDGE('',*,*,#50984,.T.);
#72021=ORIENTED_EDGE('',*,*,#50990,.F.);
#72022=ORIENTED_EDGE('',*,*,#50523,.T.);
#72023=ORIENTED_EDGE('',*,*,#50994,.F.);
#72024=ORIENTED_EDGE('',*,*,#50981,.F.);
#72025=ORIENTED_EDGE('',*,*,#50993,.F.);
#72026=ORIENTED_EDGE('',*,*,#50522,.F.);
#72027=ORIENTED_EDGE('',*,*,#50994,.T.);
#72028=ORIENTED_EDGE('',*,*,#50847,.F.);
#72029=ORIENTED_EDGE('',*,*,#50995,.F.);
#72030=ORIENTED_EDGE('',*,*,#50977,.F.);
#72031=ORIENTED_EDGE('',*,*,#50995,.T.);
#72032=ORIENTED_EDGE('',*,*,#49962,.F.);
#72033=ORIENTED_EDGE('',*,*,#50996,.F.);
#72034=ORIENTED_EDGE('',*,*,#50978,.F.);
#72035=ORIENTED_EDGE('',*,*,#50996,.T.);
#72036=ORIENTED_EDGE('',*,*,#49961,.F.);
#72037=ORIENTED_EDGE('',*,*,#50997,.F.);
#72038=ORIENTED_EDGE('',*,*,#50982,.F.);
#72039=ORIENTED_EDGE('',*,*,#50997,.T.);
#72040=ORIENTED_EDGE('',*,*,#49960,.F.);
#72041=ORIENTED_EDGE('',*,*,#50998,.F.);
#72042=ORIENTED_EDGE('',*,*,#50973,.F.);
#72043=ORIENTED_EDGE('',*,*,#50999,.T.);
#72044=ORIENTED_EDGE('',*,*,#50974,.F.);
#72045=ORIENTED_EDGE('',*,*,#50998,.T.);
#72046=ORIENTED_EDGE('',*,*,#50846,.F.);
#72047=ORIENTED_EDGE('',*,*,#51000,.T.);
#72048=ORIENTED_EDGE('',*,*,#50975,.F.);
#72049=ORIENTED_EDGE('',*,*,#50999,.F.);
#72050=ORIENTED_EDGE('',*,*,#50526,.F.);
#72051=ORIENTED_EDGE('',*,*,#50992,.T.);
#72052=ORIENTED_EDGE('',*,*,#50988,.T.);
#72053=ORIENTED_EDGE('',*,*,#51000,.F.);
#72054=ORIENTED_EDGE('',*,*,#50525,.T.);
#72055=ORIENTED_EDGE('',*,*,#50986,.T.);
#72056=ORIENTED_EDGE('',*,*,#50989,.T.);
#72057=ORIENTED_EDGE('',*,*,#50991,.T.);
#72058=ORIENTED_EDGE('',*,*,#51001,.T.);
#72059=ORIENTED_EDGE('',*,*,#51002,.T.);
#72060=ORIENTED_EDGE('',*,*,#51003,.T.);
#72061=ORIENTED_EDGE('',*,*,#51004,.T.);
#72062=ORIENTED_EDGE('',*,*,#51005,.T.);
#72063=ORIENTED_EDGE('',*,*,#51006,.T.);
#72064=ORIENTED_EDGE('',*,*,#51007,.T.);
#72065=ORIENTED_EDGE('',*,*,#51008,.F.);
#72066=ORIENTED_EDGE('',*,*,#51009,.T.);
#72067=ORIENTED_EDGE('',*,*,#51010,.T.);
#72068=ORIENTED_EDGE('',*,*,#51008,.T.);
#72069=ORIENTED_EDGE('',*,*,#51011,.T.);
#72070=ORIENTED_EDGE('',*,*,#51001,.F.);
#72071=ORIENTED_EDGE('',*,*,#51012,.T.);
#72072=ORIENTED_EDGE('',*,*,#51013,.F.);
#72073=ORIENTED_EDGE('',*,*,#51009,.F.);
#72074=ORIENTED_EDGE('',*,*,#51014,.F.);
#72075=ORIENTED_EDGE('',*,*,#51015,.F.);
#72076=ORIENTED_EDGE('',*,*,#51014,.T.);
#72077=ORIENTED_EDGE('',*,*,#51012,.F.);
#72078=ORIENTED_EDGE('',*,*,#51016,.F.);
#72079=ORIENTED_EDGE('',*,*,#51016,.T.);
#72080=ORIENTED_EDGE('',*,*,#51005,.F.);
#72081=ORIENTED_EDGE('',*,*,#51017,.F.);
#72082=ORIENTED_EDGE('',*,*,#51018,.F.);
#72083=ORIENTED_EDGE('',*,*,#51019,.T.);
#72084=ORIENTED_EDGE('',*,*,#51020,.F.);
#72085=ORIENTED_EDGE('',*,*,#51021,.F.);
#72086=ORIENTED_EDGE('',*,*,#50530,.F.);
#72087=ORIENTED_EDGE('',*,*,#51022,.T.);
#72088=ORIENTED_EDGE('',*,*,#51013,.T.);
#72089=ORIENTED_EDGE('',*,*,#51019,.F.);
#72090=ORIENTED_EDGE('',*,*,#50529,.T.);
#72091=ORIENTED_EDGE('',*,*,#51023,.F.);
#72092=ORIENTED_EDGE('',*,*,#51010,.F.);
#72093=ORIENTED_EDGE('',*,*,#51022,.F.);
#72094=ORIENTED_EDGE('',*,*,#50528,.F.);
#72095=ORIENTED_EDGE('',*,*,#51023,.T.);
#72096=ORIENTED_EDGE('',*,*,#50845,.F.);
#72097=ORIENTED_EDGE('',*,*,#51024,.F.);
#72098=ORIENTED_EDGE('',*,*,#51006,.F.);
#72099=ORIENTED_EDGE('',*,*,#51024,.T.);
#72100=ORIENTED_EDGE('',*,*,#49958,.F.);
#72101=ORIENTED_EDGE('',*,*,#51025,.F.);
#72102=ORIENTED_EDGE('',*,*,#51007,.F.);
#72103=ORIENTED_EDGE('',*,*,#51025,.T.);
#72104=ORIENTED_EDGE('',*,*,#49957,.F.);
#72105=ORIENTED_EDGE('',*,*,#51026,.F.);
#72106=ORIENTED_EDGE('',*,*,#51011,.F.);
#72107=ORIENTED_EDGE('',*,*,#51026,.T.);
#72108=ORIENTED_EDGE('',*,*,#49956,.F.);
#72109=ORIENTED_EDGE('',*,*,#51027,.F.);
#72110=ORIENTED_EDGE('',*,*,#51002,.F.);
#72111=ORIENTED_EDGE('',*,*,#51028,.T.);
#72112=ORIENTED_EDGE('',*,*,#51003,.F.);
#72113=ORIENTED_EDGE('',*,*,#51027,.T.);
#72114=ORIENTED_EDGE('',*,*,#50844,.F.);
#72115=ORIENTED_EDGE('',*,*,#51029,.T.);
#72116=ORIENTED_EDGE('',*,*,#51004,.F.);
#72117=ORIENTED_EDGE('',*,*,#51028,.F.);
#72118=ORIENTED_EDGE('',*,*,#50532,.F.);
#72119=ORIENTED_EDGE('',*,*,#51021,.T.);
#72120=ORIENTED_EDGE('',*,*,#51017,.T.);
#72121=ORIENTED_EDGE('',*,*,#51029,.F.);
#72122=ORIENTED_EDGE('',*,*,#50531,.T.);
#72123=ORIENTED_EDGE('',*,*,#51015,.T.);
#72124=ORIENTED_EDGE('',*,*,#51018,.T.);
#72125=ORIENTED_EDGE('',*,*,#51020,.T.);
#72126=ORIENTED_EDGE('',*,*,#51030,.T.);
#72127=ORIENTED_EDGE('',*,*,#51031,.T.);
#72128=ORIENTED_EDGE('',*,*,#51032,.T.);
#72129=ORIENTED_EDGE('',*,*,#51033,.T.);
#72130=ORIENTED_EDGE('',*,*,#51034,.T.);
#72131=ORIENTED_EDGE('',*,*,#51035,.T.);
#72132=ORIENTED_EDGE('',*,*,#51036,.T.);
#72133=ORIENTED_EDGE('',*,*,#51037,.F.);
#72134=ORIENTED_EDGE('',*,*,#51038,.T.);
#72135=ORIENTED_EDGE('',*,*,#51039,.T.);
#72136=ORIENTED_EDGE('',*,*,#51037,.T.);
#72137=ORIENTED_EDGE('',*,*,#51040,.T.);
#72138=ORIENTED_EDGE('',*,*,#51030,.F.);
#72139=ORIENTED_EDGE('',*,*,#51041,.T.);
#72140=ORIENTED_EDGE('',*,*,#51042,.F.);
#72141=ORIENTED_EDGE('',*,*,#51038,.F.);
#72142=ORIENTED_EDGE('',*,*,#51043,.F.);
#72143=ORIENTED_EDGE('',*,*,#51044,.F.);
#72144=ORIENTED_EDGE('',*,*,#51043,.T.);
#72145=ORIENTED_EDGE('',*,*,#51041,.F.);
#72146=ORIENTED_EDGE('',*,*,#51045,.F.);
#72147=ORIENTED_EDGE('',*,*,#51045,.T.);
#72148=ORIENTED_EDGE('',*,*,#51034,.F.);
#72149=ORIENTED_EDGE('',*,*,#51046,.F.);
#72150=ORIENTED_EDGE('',*,*,#51047,.F.);
#72151=ORIENTED_EDGE('',*,*,#51048,.T.);
#72152=ORIENTED_EDGE('',*,*,#51049,.F.);
#72153=ORIENTED_EDGE('',*,*,#51050,.F.);
#72154=ORIENTED_EDGE('',*,*,#50536,.F.);
#72155=ORIENTED_EDGE('',*,*,#51051,.T.);
#72156=ORIENTED_EDGE('',*,*,#51042,.T.);
#72157=ORIENTED_EDGE('',*,*,#51048,.F.);
#72158=ORIENTED_EDGE('',*,*,#50535,.T.);
#72159=ORIENTED_EDGE('',*,*,#51052,.F.);
#72160=ORIENTED_EDGE('',*,*,#51039,.F.);
#72161=ORIENTED_EDGE('',*,*,#51051,.F.);
#72162=ORIENTED_EDGE('',*,*,#50534,.F.);
#72163=ORIENTED_EDGE('',*,*,#51052,.T.);
#72164=ORIENTED_EDGE('',*,*,#50843,.F.);
#72165=ORIENTED_EDGE('',*,*,#51053,.F.);
#72166=ORIENTED_EDGE('',*,*,#51035,.F.);
#72167=ORIENTED_EDGE('',*,*,#51053,.T.);
#72168=ORIENTED_EDGE('',*,*,#49954,.F.);
#72169=ORIENTED_EDGE('',*,*,#51054,.F.);
#72170=ORIENTED_EDGE('',*,*,#51036,.F.);
#72171=ORIENTED_EDGE('',*,*,#51054,.T.);
#72172=ORIENTED_EDGE('',*,*,#49953,.F.);
#72173=ORIENTED_EDGE('',*,*,#51055,.F.);
#72174=ORIENTED_EDGE('',*,*,#51040,.F.);
#72175=ORIENTED_EDGE('',*,*,#51055,.T.);
#72176=ORIENTED_EDGE('',*,*,#49952,.F.);
#72177=ORIENTED_EDGE('',*,*,#51056,.F.);
#72178=ORIENTED_EDGE('',*,*,#51031,.F.);
#72179=ORIENTED_EDGE('',*,*,#51057,.T.);
#72180=ORIENTED_EDGE('',*,*,#51032,.F.);
#72181=ORIENTED_EDGE('',*,*,#51056,.T.);
#72182=ORIENTED_EDGE('',*,*,#50842,.F.);
#72183=ORIENTED_EDGE('',*,*,#51058,.T.);
#72184=ORIENTED_EDGE('',*,*,#51033,.F.);
#72185=ORIENTED_EDGE('',*,*,#51057,.F.);
#72186=ORIENTED_EDGE('',*,*,#50538,.F.);
#72187=ORIENTED_EDGE('',*,*,#51050,.T.);
#72188=ORIENTED_EDGE('',*,*,#51046,.T.);
#72189=ORIENTED_EDGE('',*,*,#51058,.F.);
#72190=ORIENTED_EDGE('',*,*,#50537,.T.);
#72191=ORIENTED_EDGE('',*,*,#51044,.T.);
#72192=ORIENTED_EDGE('',*,*,#51047,.T.);
#72193=ORIENTED_EDGE('',*,*,#51049,.T.);
#72194=ORIENTED_EDGE('',*,*,#51059,.T.);
#72195=ORIENTED_EDGE('',*,*,#51060,.T.);
#72196=ORIENTED_EDGE('',*,*,#51061,.T.);
#72197=ORIENTED_EDGE('',*,*,#51062,.T.);
#72198=ORIENTED_EDGE('',*,*,#51063,.T.);
#72199=ORIENTED_EDGE('',*,*,#51064,.T.);
#72200=ORIENTED_EDGE('',*,*,#51065,.T.);
#72201=ORIENTED_EDGE('',*,*,#51066,.F.);
#72202=ORIENTED_EDGE('',*,*,#51067,.T.);
#72203=ORIENTED_EDGE('',*,*,#51068,.T.);
#72204=ORIENTED_EDGE('',*,*,#51066,.T.);
#72205=ORIENTED_EDGE('',*,*,#51069,.T.);
#72206=ORIENTED_EDGE('',*,*,#51059,.F.);
#72207=ORIENTED_EDGE('',*,*,#51070,.T.);
#72208=ORIENTED_EDGE('',*,*,#51071,.F.);
#72209=ORIENTED_EDGE('',*,*,#51067,.F.);
#72210=ORIENTED_EDGE('',*,*,#51072,.F.);
#72211=ORIENTED_EDGE('',*,*,#51073,.F.);
#72212=ORIENTED_EDGE('',*,*,#51072,.T.);
#72213=ORIENTED_EDGE('',*,*,#51070,.F.);
#72214=ORIENTED_EDGE('',*,*,#51074,.F.);
#72215=ORIENTED_EDGE('',*,*,#51074,.T.);
#72216=ORIENTED_EDGE('',*,*,#51063,.F.);
#72217=ORIENTED_EDGE('',*,*,#51075,.F.);
#72218=ORIENTED_EDGE('',*,*,#51076,.F.);
#72219=ORIENTED_EDGE('',*,*,#51077,.T.);
#72220=ORIENTED_EDGE('',*,*,#51078,.F.);
#72221=ORIENTED_EDGE('',*,*,#51079,.F.);
#72222=ORIENTED_EDGE('',*,*,#50542,.F.);
#72223=ORIENTED_EDGE('',*,*,#51080,.T.);
#72224=ORIENTED_EDGE('',*,*,#51071,.T.);
#72225=ORIENTED_EDGE('',*,*,#51077,.F.);
#72226=ORIENTED_EDGE('',*,*,#50541,.T.);
#72227=ORIENTED_EDGE('',*,*,#51081,.F.);
#72228=ORIENTED_EDGE('',*,*,#51068,.F.);
#72229=ORIENTED_EDGE('',*,*,#51080,.F.);
#72230=ORIENTED_EDGE('',*,*,#50540,.F.);
#72231=ORIENTED_EDGE('',*,*,#51081,.T.);
#72232=ORIENTED_EDGE('',*,*,#50841,.F.);
#72233=ORIENTED_EDGE('',*,*,#51082,.F.);
#72234=ORIENTED_EDGE('',*,*,#51064,.F.);
#72235=ORIENTED_EDGE('',*,*,#51082,.T.);
#72236=ORIENTED_EDGE('',*,*,#49950,.F.);
#72237=ORIENTED_EDGE('',*,*,#51083,.F.);
#72238=ORIENTED_EDGE('',*,*,#51065,.F.);
#72239=ORIENTED_EDGE('',*,*,#51083,.T.);
#72240=ORIENTED_EDGE('',*,*,#49949,.F.);
#72241=ORIENTED_EDGE('',*,*,#51084,.F.);
#72242=ORIENTED_EDGE('',*,*,#51069,.F.);
#72243=ORIENTED_EDGE('',*,*,#51084,.T.);
#72244=ORIENTED_EDGE('',*,*,#49948,.F.);
#72245=ORIENTED_EDGE('',*,*,#51085,.F.);
#72246=ORIENTED_EDGE('',*,*,#51060,.F.);
#72247=ORIENTED_EDGE('',*,*,#51086,.T.);
#72248=ORIENTED_EDGE('',*,*,#51061,.F.);
#72249=ORIENTED_EDGE('',*,*,#51085,.T.);
#72250=ORIENTED_EDGE('',*,*,#50840,.F.);
#72251=ORIENTED_EDGE('',*,*,#51087,.T.);
#72252=ORIENTED_EDGE('',*,*,#51062,.F.);
#72253=ORIENTED_EDGE('',*,*,#51086,.F.);
#72254=ORIENTED_EDGE('',*,*,#50544,.F.);
#72255=ORIENTED_EDGE('',*,*,#51079,.T.);
#72256=ORIENTED_EDGE('',*,*,#51075,.T.);
#72257=ORIENTED_EDGE('',*,*,#51087,.F.);
#72258=ORIENTED_EDGE('',*,*,#50543,.T.);
#72259=ORIENTED_EDGE('',*,*,#51073,.T.);
#72260=ORIENTED_EDGE('',*,*,#51076,.T.);
#72261=ORIENTED_EDGE('',*,*,#51078,.T.);
#72262=ORIENTED_EDGE('',*,*,#51088,.T.);
#72263=ORIENTED_EDGE('',*,*,#51089,.T.);
#72264=ORIENTED_EDGE('',*,*,#51090,.T.);
#72265=ORIENTED_EDGE('',*,*,#51091,.T.);
#72266=ORIENTED_EDGE('',*,*,#51092,.T.);
#72267=ORIENTED_EDGE('',*,*,#51093,.T.);
#72268=ORIENTED_EDGE('',*,*,#51094,.T.);
#72269=ORIENTED_EDGE('',*,*,#51095,.F.);
#72270=ORIENTED_EDGE('',*,*,#51096,.T.);
#72271=ORIENTED_EDGE('',*,*,#51097,.T.);
#72272=ORIENTED_EDGE('',*,*,#51095,.T.);
#72273=ORIENTED_EDGE('',*,*,#51098,.T.);
#72274=ORIENTED_EDGE('',*,*,#51088,.F.);
#72275=ORIENTED_EDGE('',*,*,#51099,.T.);
#72276=ORIENTED_EDGE('',*,*,#51100,.F.);
#72277=ORIENTED_EDGE('',*,*,#51096,.F.);
#72278=ORIENTED_EDGE('',*,*,#51101,.F.);
#72279=ORIENTED_EDGE('',*,*,#51102,.F.);
#72280=ORIENTED_EDGE('',*,*,#51101,.T.);
#72281=ORIENTED_EDGE('',*,*,#51099,.F.);
#72282=ORIENTED_EDGE('',*,*,#51103,.F.);
#72283=ORIENTED_EDGE('',*,*,#51103,.T.);
#72284=ORIENTED_EDGE('',*,*,#51092,.F.);
#72285=ORIENTED_EDGE('',*,*,#51104,.F.);
#72286=ORIENTED_EDGE('',*,*,#51105,.F.);
#72287=ORIENTED_EDGE('',*,*,#51106,.T.);
#72288=ORIENTED_EDGE('',*,*,#51107,.F.);
#72289=ORIENTED_EDGE('',*,*,#51108,.F.);
#72290=ORIENTED_EDGE('',*,*,#50548,.F.);
#72291=ORIENTED_EDGE('',*,*,#51109,.T.);
#72292=ORIENTED_EDGE('',*,*,#51100,.T.);
#72293=ORIENTED_EDGE('',*,*,#51106,.F.);
#72294=ORIENTED_EDGE('',*,*,#50547,.T.);
#72295=ORIENTED_EDGE('',*,*,#51110,.F.);
#72296=ORIENTED_EDGE('',*,*,#51097,.F.);
#72297=ORIENTED_EDGE('',*,*,#51109,.F.);
#72298=ORIENTED_EDGE('',*,*,#50546,.F.);
#72299=ORIENTED_EDGE('',*,*,#51110,.T.);
#72300=ORIENTED_EDGE('',*,*,#50839,.F.);
#72301=ORIENTED_EDGE('',*,*,#51111,.F.);
#72302=ORIENTED_EDGE('',*,*,#51093,.F.);
#72303=ORIENTED_EDGE('',*,*,#51111,.T.);
#72304=ORIENTED_EDGE('',*,*,#49946,.F.);
#72305=ORIENTED_EDGE('',*,*,#51112,.F.);
#72306=ORIENTED_EDGE('',*,*,#51094,.F.);
#72307=ORIENTED_EDGE('',*,*,#51112,.T.);
#72308=ORIENTED_EDGE('',*,*,#49945,.F.);
#72309=ORIENTED_EDGE('',*,*,#51113,.F.);
#72310=ORIENTED_EDGE('',*,*,#51098,.F.);
#72311=ORIENTED_EDGE('',*,*,#51113,.T.);
#72312=ORIENTED_EDGE('',*,*,#49944,.F.);
#72313=ORIENTED_EDGE('',*,*,#51114,.F.);
#72314=ORIENTED_EDGE('',*,*,#51089,.F.);
#72315=ORIENTED_EDGE('',*,*,#51115,.T.);
#72316=ORIENTED_EDGE('',*,*,#51090,.F.);
#72317=ORIENTED_EDGE('',*,*,#51114,.T.);
#72318=ORIENTED_EDGE('',*,*,#50838,.F.);
#72319=ORIENTED_EDGE('',*,*,#51116,.T.);
#72320=ORIENTED_EDGE('',*,*,#51091,.F.);
#72321=ORIENTED_EDGE('',*,*,#51115,.F.);
#72322=ORIENTED_EDGE('',*,*,#50550,.F.);
#72323=ORIENTED_EDGE('',*,*,#51108,.T.);
#72324=ORIENTED_EDGE('',*,*,#51104,.T.);
#72325=ORIENTED_EDGE('',*,*,#51116,.F.);
#72326=ORIENTED_EDGE('',*,*,#50549,.T.);
#72327=ORIENTED_EDGE('',*,*,#51102,.T.);
#72328=ORIENTED_EDGE('',*,*,#51105,.T.);
#72329=ORIENTED_EDGE('',*,*,#51107,.T.);
#72330=ORIENTED_EDGE('',*,*,#51117,.T.);
#72331=ORIENTED_EDGE('',*,*,#51118,.T.);
#72332=ORIENTED_EDGE('',*,*,#51119,.T.);
#72333=ORIENTED_EDGE('',*,*,#51120,.T.);
#72334=ORIENTED_EDGE('',*,*,#51121,.T.);
#72335=ORIENTED_EDGE('',*,*,#51122,.T.);
#72336=ORIENTED_EDGE('',*,*,#51123,.T.);
#72337=ORIENTED_EDGE('',*,*,#51124,.F.);
#72338=ORIENTED_EDGE('',*,*,#51125,.T.);
#72339=ORIENTED_EDGE('',*,*,#51126,.T.);
#72340=ORIENTED_EDGE('',*,*,#51124,.T.);
#72341=ORIENTED_EDGE('',*,*,#51127,.T.);
#72342=ORIENTED_EDGE('',*,*,#51117,.F.);
#72343=ORIENTED_EDGE('',*,*,#51128,.T.);
#72344=ORIENTED_EDGE('',*,*,#51129,.F.);
#72345=ORIENTED_EDGE('',*,*,#51125,.F.);
#72346=ORIENTED_EDGE('',*,*,#51130,.F.);
#72347=ORIENTED_EDGE('',*,*,#51131,.F.);
#72348=ORIENTED_EDGE('',*,*,#51130,.T.);
#72349=ORIENTED_EDGE('',*,*,#51128,.F.);
#72350=ORIENTED_EDGE('',*,*,#51132,.F.);
#72351=ORIENTED_EDGE('',*,*,#51132,.T.);
#72352=ORIENTED_EDGE('',*,*,#51121,.F.);
#72353=ORIENTED_EDGE('',*,*,#51133,.F.);
#72354=ORIENTED_EDGE('',*,*,#51134,.F.);
#72355=ORIENTED_EDGE('',*,*,#51135,.T.);
#72356=ORIENTED_EDGE('',*,*,#51136,.F.);
#72357=ORIENTED_EDGE('',*,*,#51137,.F.);
#72358=ORIENTED_EDGE('',*,*,#50554,.F.);
#72359=ORIENTED_EDGE('',*,*,#51138,.T.);
#72360=ORIENTED_EDGE('',*,*,#51129,.T.);
#72361=ORIENTED_EDGE('',*,*,#51135,.F.);
#72362=ORIENTED_EDGE('',*,*,#50553,.T.);
#72363=ORIENTED_EDGE('',*,*,#51139,.F.);
#72364=ORIENTED_EDGE('',*,*,#51126,.F.);
#72365=ORIENTED_EDGE('',*,*,#51138,.F.);
#72366=ORIENTED_EDGE('',*,*,#50552,.F.);
#72367=ORIENTED_EDGE('',*,*,#51139,.T.);
#72368=ORIENTED_EDGE('',*,*,#50837,.F.);
#72369=ORIENTED_EDGE('',*,*,#51140,.F.);
#72370=ORIENTED_EDGE('',*,*,#51122,.F.);
#72371=ORIENTED_EDGE('',*,*,#51140,.T.);
#72372=ORIENTED_EDGE('',*,*,#49942,.F.);
#72373=ORIENTED_EDGE('',*,*,#51141,.F.);
#72374=ORIENTED_EDGE('',*,*,#51123,.F.);
#72375=ORIENTED_EDGE('',*,*,#51141,.T.);
#72376=ORIENTED_EDGE('',*,*,#49941,.F.);
#72377=ORIENTED_EDGE('',*,*,#51142,.F.);
#72378=ORIENTED_EDGE('',*,*,#51127,.F.);
#72379=ORIENTED_EDGE('',*,*,#51142,.T.);
#72380=ORIENTED_EDGE('',*,*,#49940,.F.);
#72381=ORIENTED_EDGE('',*,*,#51143,.F.);
#72382=ORIENTED_EDGE('',*,*,#51118,.F.);
#72383=ORIENTED_EDGE('',*,*,#51144,.T.);
#72384=ORIENTED_EDGE('',*,*,#51119,.F.);
#72385=ORIENTED_EDGE('',*,*,#51143,.T.);
#72386=ORIENTED_EDGE('',*,*,#50836,.F.);
#72387=ORIENTED_EDGE('',*,*,#51145,.T.);
#72388=ORIENTED_EDGE('',*,*,#51120,.F.);
#72389=ORIENTED_EDGE('',*,*,#51144,.F.);
#72390=ORIENTED_EDGE('',*,*,#50556,.F.);
#72391=ORIENTED_EDGE('',*,*,#51137,.T.);
#72392=ORIENTED_EDGE('',*,*,#51133,.T.);
#72393=ORIENTED_EDGE('',*,*,#51145,.F.);
#72394=ORIENTED_EDGE('',*,*,#50555,.T.);
#72395=ORIENTED_EDGE('',*,*,#51131,.T.);
#72396=ORIENTED_EDGE('',*,*,#51134,.T.);
#72397=ORIENTED_EDGE('',*,*,#51136,.T.);
#72398=ORIENTED_EDGE('',*,*,#51146,.T.);
#72399=ORIENTED_EDGE('',*,*,#51147,.T.);
#72400=ORIENTED_EDGE('',*,*,#51148,.T.);
#72401=ORIENTED_EDGE('',*,*,#51149,.T.);
#72402=ORIENTED_EDGE('',*,*,#51150,.T.);
#72403=ORIENTED_EDGE('',*,*,#51151,.T.);
#72404=ORIENTED_EDGE('',*,*,#51152,.T.);
#72405=ORIENTED_EDGE('',*,*,#51153,.F.);
#72406=ORIENTED_EDGE('',*,*,#51154,.T.);
#72407=ORIENTED_EDGE('',*,*,#51155,.T.);
#72408=ORIENTED_EDGE('',*,*,#51153,.T.);
#72409=ORIENTED_EDGE('',*,*,#51156,.T.);
#72410=ORIENTED_EDGE('',*,*,#51146,.F.);
#72411=ORIENTED_EDGE('',*,*,#51157,.T.);
#72412=ORIENTED_EDGE('',*,*,#51158,.F.);
#72413=ORIENTED_EDGE('',*,*,#51154,.F.);
#72414=ORIENTED_EDGE('',*,*,#51159,.F.);
#72415=ORIENTED_EDGE('',*,*,#51160,.F.);
#72416=ORIENTED_EDGE('',*,*,#51159,.T.);
#72417=ORIENTED_EDGE('',*,*,#51157,.F.);
#72418=ORIENTED_EDGE('',*,*,#51161,.F.);
#72419=ORIENTED_EDGE('',*,*,#51161,.T.);
#72420=ORIENTED_EDGE('',*,*,#51150,.F.);
#72421=ORIENTED_EDGE('',*,*,#51162,.F.);
#72422=ORIENTED_EDGE('',*,*,#51163,.F.);
#72423=ORIENTED_EDGE('',*,*,#51164,.T.);
#72424=ORIENTED_EDGE('',*,*,#51165,.F.);
#72425=ORIENTED_EDGE('',*,*,#51166,.F.);
#72426=ORIENTED_EDGE('',*,*,#50560,.F.);
#72427=ORIENTED_EDGE('',*,*,#51167,.T.);
#72428=ORIENTED_EDGE('',*,*,#51158,.T.);
#72429=ORIENTED_EDGE('',*,*,#51164,.F.);
#72430=ORIENTED_EDGE('',*,*,#50559,.T.);
#72431=ORIENTED_EDGE('',*,*,#51168,.F.);
#72432=ORIENTED_EDGE('',*,*,#51155,.F.);
#72433=ORIENTED_EDGE('',*,*,#51167,.F.);
#72434=ORIENTED_EDGE('',*,*,#50558,.F.);
#72435=ORIENTED_EDGE('',*,*,#51168,.T.);
#72436=ORIENTED_EDGE('',*,*,#50835,.F.);
#72437=ORIENTED_EDGE('',*,*,#51169,.F.);
#72438=ORIENTED_EDGE('',*,*,#51151,.F.);
#72439=ORIENTED_EDGE('',*,*,#51169,.T.);
#72440=ORIENTED_EDGE('',*,*,#49938,.F.);
#72441=ORIENTED_EDGE('',*,*,#51170,.F.);
#72442=ORIENTED_EDGE('',*,*,#51152,.F.);
#72443=ORIENTED_EDGE('',*,*,#51170,.T.);
#72444=ORIENTED_EDGE('',*,*,#49937,.F.);
#72445=ORIENTED_EDGE('',*,*,#51171,.F.);
#72446=ORIENTED_EDGE('',*,*,#51156,.F.);
#72447=ORIENTED_EDGE('',*,*,#51171,.T.);
#72448=ORIENTED_EDGE('',*,*,#49936,.F.);
#72449=ORIENTED_EDGE('',*,*,#51172,.F.);
#72450=ORIENTED_EDGE('',*,*,#51147,.F.);
#72451=ORIENTED_EDGE('',*,*,#51173,.T.);
#72452=ORIENTED_EDGE('',*,*,#51148,.F.);
#72453=ORIENTED_EDGE('',*,*,#51172,.T.);
#72454=ORIENTED_EDGE('',*,*,#50834,.F.);
#72455=ORIENTED_EDGE('',*,*,#51174,.T.);
#72456=ORIENTED_EDGE('',*,*,#51149,.F.);
#72457=ORIENTED_EDGE('',*,*,#51173,.F.);
#72458=ORIENTED_EDGE('',*,*,#50562,.F.);
#72459=ORIENTED_EDGE('',*,*,#51166,.T.);
#72460=ORIENTED_EDGE('',*,*,#51162,.T.);
#72461=ORIENTED_EDGE('',*,*,#51174,.F.);
#72462=ORIENTED_EDGE('',*,*,#50561,.T.);
#72463=ORIENTED_EDGE('',*,*,#51160,.T.);
#72464=ORIENTED_EDGE('',*,*,#51163,.T.);
#72465=ORIENTED_EDGE('',*,*,#51165,.T.);
#72466=ORIENTED_EDGE('',*,*,#51175,.T.);
#72467=ORIENTED_EDGE('',*,*,#51176,.T.);
#72468=ORIENTED_EDGE('',*,*,#51177,.T.);
#72469=ORIENTED_EDGE('',*,*,#51178,.T.);
#72470=ORIENTED_EDGE('',*,*,#51179,.T.);
#72471=ORIENTED_EDGE('',*,*,#51180,.T.);
#72472=ORIENTED_EDGE('',*,*,#51181,.T.);
#72473=ORIENTED_EDGE('',*,*,#51182,.F.);
#72474=ORIENTED_EDGE('',*,*,#51183,.T.);
#72475=ORIENTED_EDGE('',*,*,#51184,.T.);
#72476=ORIENTED_EDGE('',*,*,#51182,.T.);
#72477=ORIENTED_EDGE('',*,*,#51185,.T.);
#72478=ORIENTED_EDGE('',*,*,#51175,.F.);
#72479=ORIENTED_EDGE('',*,*,#51186,.T.);
#72480=ORIENTED_EDGE('',*,*,#51187,.F.);
#72481=ORIENTED_EDGE('',*,*,#51183,.F.);
#72482=ORIENTED_EDGE('',*,*,#51188,.F.);
#72483=ORIENTED_EDGE('',*,*,#51189,.F.);
#72484=ORIENTED_EDGE('',*,*,#51188,.T.);
#72485=ORIENTED_EDGE('',*,*,#51186,.F.);
#72486=ORIENTED_EDGE('',*,*,#51190,.F.);
#72487=ORIENTED_EDGE('',*,*,#51190,.T.);
#72488=ORIENTED_EDGE('',*,*,#51179,.F.);
#72489=ORIENTED_EDGE('',*,*,#51191,.F.);
#72490=ORIENTED_EDGE('',*,*,#51192,.F.);
#72491=ORIENTED_EDGE('',*,*,#51193,.T.);
#72492=ORIENTED_EDGE('',*,*,#51194,.F.);
#72493=ORIENTED_EDGE('',*,*,#51195,.F.);
#72494=ORIENTED_EDGE('',*,*,#50566,.F.);
#72495=ORIENTED_EDGE('',*,*,#51196,.T.);
#72496=ORIENTED_EDGE('',*,*,#51187,.T.);
#72497=ORIENTED_EDGE('',*,*,#51193,.F.);
#72498=ORIENTED_EDGE('',*,*,#50565,.T.);
#72499=ORIENTED_EDGE('',*,*,#51197,.F.);
#72500=ORIENTED_EDGE('',*,*,#51184,.F.);
#72501=ORIENTED_EDGE('',*,*,#51196,.F.);
#72502=ORIENTED_EDGE('',*,*,#50564,.F.);
#72503=ORIENTED_EDGE('',*,*,#51197,.T.);
#72504=ORIENTED_EDGE('',*,*,#50833,.F.);
#72505=ORIENTED_EDGE('',*,*,#51198,.F.);
#72506=ORIENTED_EDGE('',*,*,#51180,.F.);
#72507=ORIENTED_EDGE('',*,*,#51198,.T.);
#72508=ORIENTED_EDGE('',*,*,#49934,.F.);
#72509=ORIENTED_EDGE('',*,*,#51199,.F.);
#72510=ORIENTED_EDGE('',*,*,#51181,.F.);
#72511=ORIENTED_EDGE('',*,*,#51199,.T.);
#72512=ORIENTED_EDGE('',*,*,#49933,.F.);
#72513=ORIENTED_EDGE('',*,*,#51200,.F.);
#72514=ORIENTED_EDGE('',*,*,#51185,.F.);
#72515=ORIENTED_EDGE('',*,*,#51200,.T.);
#72516=ORIENTED_EDGE('',*,*,#49932,.F.);
#72517=ORIENTED_EDGE('',*,*,#51201,.F.);
#72518=ORIENTED_EDGE('',*,*,#51176,.F.);
#72519=ORIENTED_EDGE('',*,*,#51202,.T.);
#72520=ORIENTED_EDGE('',*,*,#51177,.F.);
#72521=ORIENTED_EDGE('',*,*,#51201,.T.);
#72522=ORIENTED_EDGE('',*,*,#50832,.F.);
#72523=ORIENTED_EDGE('',*,*,#51203,.T.);
#72524=ORIENTED_EDGE('',*,*,#51178,.F.);
#72525=ORIENTED_EDGE('',*,*,#51202,.F.);
#72526=ORIENTED_EDGE('',*,*,#50568,.F.);
#72527=ORIENTED_EDGE('',*,*,#51195,.T.);
#72528=ORIENTED_EDGE('',*,*,#51191,.T.);
#72529=ORIENTED_EDGE('',*,*,#51203,.F.);
#72530=ORIENTED_EDGE('',*,*,#50567,.T.);
#72531=ORIENTED_EDGE('',*,*,#51189,.T.);
#72532=ORIENTED_EDGE('',*,*,#51192,.T.);
#72533=ORIENTED_EDGE('',*,*,#51194,.T.);
#72534=ORIENTED_EDGE('',*,*,#51204,.T.);
#72535=ORIENTED_EDGE('',*,*,#51205,.T.);
#72536=ORIENTED_EDGE('',*,*,#51206,.T.);
#72537=ORIENTED_EDGE('',*,*,#51207,.T.);
#72538=ORIENTED_EDGE('',*,*,#51208,.T.);
#72539=ORIENTED_EDGE('',*,*,#51209,.T.);
#72540=ORIENTED_EDGE('',*,*,#51210,.T.);
#72541=ORIENTED_EDGE('',*,*,#51211,.F.);
#72542=ORIENTED_EDGE('',*,*,#51212,.T.);
#72543=ORIENTED_EDGE('',*,*,#51213,.T.);
#72544=ORIENTED_EDGE('',*,*,#51211,.T.);
#72545=ORIENTED_EDGE('',*,*,#51214,.T.);
#72546=ORIENTED_EDGE('',*,*,#51204,.F.);
#72547=ORIENTED_EDGE('',*,*,#51215,.T.);
#72548=ORIENTED_EDGE('',*,*,#51216,.F.);
#72549=ORIENTED_EDGE('',*,*,#51212,.F.);
#72550=ORIENTED_EDGE('',*,*,#51217,.F.);
#72551=ORIENTED_EDGE('',*,*,#51218,.F.);
#72552=ORIENTED_EDGE('',*,*,#51217,.T.);
#72553=ORIENTED_EDGE('',*,*,#51215,.F.);
#72554=ORIENTED_EDGE('',*,*,#51219,.F.);
#72555=ORIENTED_EDGE('',*,*,#51219,.T.);
#72556=ORIENTED_EDGE('',*,*,#51208,.F.);
#72557=ORIENTED_EDGE('',*,*,#51220,.F.);
#72558=ORIENTED_EDGE('',*,*,#51221,.F.);
#72559=ORIENTED_EDGE('',*,*,#51222,.T.);
#72560=ORIENTED_EDGE('',*,*,#51223,.F.);
#72561=ORIENTED_EDGE('',*,*,#51224,.F.);
#72562=ORIENTED_EDGE('',*,*,#50572,.F.);
#72563=ORIENTED_EDGE('',*,*,#51225,.T.);
#72564=ORIENTED_EDGE('',*,*,#51216,.T.);
#72565=ORIENTED_EDGE('',*,*,#51222,.F.);
#72566=ORIENTED_EDGE('',*,*,#50571,.T.);
#72567=ORIENTED_EDGE('',*,*,#51226,.F.);
#72568=ORIENTED_EDGE('',*,*,#51213,.F.);
#72569=ORIENTED_EDGE('',*,*,#51225,.F.);
#72570=ORIENTED_EDGE('',*,*,#50570,.F.);
#72571=ORIENTED_EDGE('',*,*,#51226,.T.);
#72572=ORIENTED_EDGE('',*,*,#50831,.F.);
#72573=ORIENTED_EDGE('',*,*,#51227,.F.);
#72574=ORIENTED_EDGE('',*,*,#51209,.F.);
#72575=ORIENTED_EDGE('',*,*,#51227,.T.);
#72576=ORIENTED_EDGE('',*,*,#49930,.F.);
#72577=ORIENTED_EDGE('',*,*,#51228,.F.);
#72578=ORIENTED_EDGE('',*,*,#51210,.F.);
#72579=ORIENTED_EDGE('',*,*,#51228,.T.);
#72580=ORIENTED_EDGE('',*,*,#49929,.F.);
#72581=ORIENTED_EDGE('',*,*,#51229,.F.);
#72582=ORIENTED_EDGE('',*,*,#51214,.F.);
#72583=ORIENTED_EDGE('',*,*,#51229,.T.);
#72584=ORIENTED_EDGE('',*,*,#49928,.F.);
#72585=ORIENTED_EDGE('',*,*,#51230,.F.);
#72586=ORIENTED_EDGE('',*,*,#51205,.F.);
#72587=ORIENTED_EDGE('',*,*,#51231,.T.);
#72588=ORIENTED_EDGE('',*,*,#51206,.F.);
#72589=ORIENTED_EDGE('',*,*,#51230,.T.);
#72590=ORIENTED_EDGE('',*,*,#50830,.F.);
#72591=ORIENTED_EDGE('',*,*,#51232,.T.);
#72592=ORIENTED_EDGE('',*,*,#51207,.F.);
#72593=ORIENTED_EDGE('',*,*,#51231,.F.);
#72594=ORIENTED_EDGE('',*,*,#50574,.F.);
#72595=ORIENTED_EDGE('',*,*,#51224,.T.);
#72596=ORIENTED_EDGE('',*,*,#51220,.T.);
#72597=ORIENTED_EDGE('',*,*,#51232,.F.);
#72598=ORIENTED_EDGE('',*,*,#50573,.T.);
#72599=ORIENTED_EDGE('',*,*,#51218,.T.);
#72600=ORIENTED_EDGE('',*,*,#51221,.T.);
#72601=ORIENTED_EDGE('',*,*,#51223,.T.);
#72602=ORIENTED_EDGE('',*,*,#51233,.T.);
#72603=ORIENTED_EDGE('',*,*,#51234,.T.);
#72604=ORIENTED_EDGE('',*,*,#51235,.T.);
#72605=ORIENTED_EDGE('',*,*,#51236,.T.);
#72606=ORIENTED_EDGE('',*,*,#51237,.T.);
#72607=ORIENTED_EDGE('',*,*,#51238,.T.);
#72608=ORIENTED_EDGE('',*,*,#51239,.T.);
#72609=ORIENTED_EDGE('',*,*,#51240,.F.);
#72610=ORIENTED_EDGE('',*,*,#51241,.T.);
#72611=ORIENTED_EDGE('',*,*,#51242,.T.);
#72612=ORIENTED_EDGE('',*,*,#51240,.T.);
#72613=ORIENTED_EDGE('',*,*,#51243,.T.);
#72614=ORIENTED_EDGE('',*,*,#51233,.F.);
#72615=ORIENTED_EDGE('',*,*,#51244,.T.);
#72616=ORIENTED_EDGE('',*,*,#51245,.F.);
#72617=ORIENTED_EDGE('',*,*,#51241,.F.);
#72618=ORIENTED_EDGE('',*,*,#51246,.F.);
#72619=ORIENTED_EDGE('',*,*,#51247,.F.);
#72620=ORIENTED_EDGE('',*,*,#51246,.T.);
#72621=ORIENTED_EDGE('',*,*,#51244,.F.);
#72622=ORIENTED_EDGE('',*,*,#51248,.F.);
#72623=ORIENTED_EDGE('',*,*,#51248,.T.);
#72624=ORIENTED_EDGE('',*,*,#51237,.F.);
#72625=ORIENTED_EDGE('',*,*,#51249,.F.);
#72626=ORIENTED_EDGE('',*,*,#51250,.F.);
#72627=ORIENTED_EDGE('',*,*,#51251,.T.);
#72628=ORIENTED_EDGE('',*,*,#51252,.F.);
#72629=ORIENTED_EDGE('',*,*,#51253,.F.);
#72630=ORIENTED_EDGE('',*,*,#50578,.F.);
#72631=ORIENTED_EDGE('',*,*,#51254,.T.);
#72632=ORIENTED_EDGE('',*,*,#51245,.T.);
#72633=ORIENTED_EDGE('',*,*,#51251,.F.);
#72634=ORIENTED_EDGE('',*,*,#50577,.T.);
#72635=ORIENTED_EDGE('',*,*,#51255,.F.);
#72636=ORIENTED_EDGE('',*,*,#51242,.F.);
#72637=ORIENTED_EDGE('',*,*,#51254,.F.);
#72638=ORIENTED_EDGE('',*,*,#50576,.F.);
#72639=ORIENTED_EDGE('',*,*,#51255,.T.);
#72640=ORIENTED_EDGE('',*,*,#50829,.F.);
#72641=ORIENTED_EDGE('',*,*,#51256,.F.);
#72642=ORIENTED_EDGE('',*,*,#51238,.F.);
#72643=ORIENTED_EDGE('',*,*,#51256,.T.);
#72644=ORIENTED_EDGE('',*,*,#49926,.F.);
#72645=ORIENTED_EDGE('',*,*,#51257,.F.);
#72646=ORIENTED_EDGE('',*,*,#51239,.F.);
#72647=ORIENTED_EDGE('',*,*,#51257,.T.);
#72648=ORIENTED_EDGE('',*,*,#49925,.F.);
#72649=ORIENTED_EDGE('',*,*,#51258,.F.);
#72650=ORIENTED_EDGE('',*,*,#51243,.F.);
#72651=ORIENTED_EDGE('',*,*,#51258,.T.);
#72652=ORIENTED_EDGE('',*,*,#49924,.F.);
#72653=ORIENTED_EDGE('',*,*,#51259,.F.);
#72654=ORIENTED_EDGE('',*,*,#51234,.F.);
#72655=ORIENTED_EDGE('',*,*,#51260,.T.);
#72656=ORIENTED_EDGE('',*,*,#51235,.F.);
#72657=ORIENTED_EDGE('',*,*,#51259,.T.);
#72658=ORIENTED_EDGE('',*,*,#50828,.F.);
#72659=ORIENTED_EDGE('',*,*,#51261,.T.);
#72660=ORIENTED_EDGE('',*,*,#51236,.F.);
#72661=ORIENTED_EDGE('',*,*,#51260,.F.);
#72662=ORIENTED_EDGE('',*,*,#50580,.F.);
#72663=ORIENTED_EDGE('',*,*,#51253,.T.);
#72664=ORIENTED_EDGE('',*,*,#51249,.T.);
#72665=ORIENTED_EDGE('',*,*,#51261,.F.);
#72666=ORIENTED_EDGE('',*,*,#50579,.T.);
#72667=ORIENTED_EDGE('',*,*,#51247,.T.);
#72668=ORIENTED_EDGE('',*,*,#51250,.T.);
#72669=ORIENTED_EDGE('',*,*,#51252,.T.);
#72670=ORIENTED_EDGE('',*,*,#51262,.T.);
#72671=ORIENTED_EDGE('',*,*,#51263,.T.);
#72672=ORIENTED_EDGE('',*,*,#51264,.T.);
#72673=ORIENTED_EDGE('',*,*,#51265,.T.);
#72674=ORIENTED_EDGE('',*,*,#51266,.T.);
#72675=ORIENTED_EDGE('',*,*,#51267,.T.);
#72676=ORIENTED_EDGE('',*,*,#51268,.T.);
#72677=ORIENTED_EDGE('',*,*,#51269,.F.);
#72678=ORIENTED_EDGE('',*,*,#51270,.T.);
#72679=ORIENTED_EDGE('',*,*,#51271,.T.);
#72680=ORIENTED_EDGE('',*,*,#51269,.T.);
#72681=ORIENTED_EDGE('',*,*,#51272,.T.);
#72682=ORIENTED_EDGE('',*,*,#51262,.F.);
#72683=ORIENTED_EDGE('',*,*,#51273,.T.);
#72684=ORIENTED_EDGE('',*,*,#51274,.F.);
#72685=ORIENTED_EDGE('',*,*,#51270,.F.);
#72686=ORIENTED_EDGE('',*,*,#51275,.F.);
#72687=ORIENTED_EDGE('',*,*,#51276,.F.);
#72688=ORIENTED_EDGE('',*,*,#51275,.T.);
#72689=ORIENTED_EDGE('',*,*,#51273,.F.);
#72690=ORIENTED_EDGE('',*,*,#51277,.F.);
#72691=ORIENTED_EDGE('',*,*,#51277,.T.);
#72692=ORIENTED_EDGE('',*,*,#51266,.F.);
#72693=ORIENTED_EDGE('',*,*,#51278,.F.);
#72694=ORIENTED_EDGE('',*,*,#51279,.F.);
#72695=ORIENTED_EDGE('',*,*,#51280,.T.);
#72696=ORIENTED_EDGE('',*,*,#51281,.F.);
#72697=ORIENTED_EDGE('',*,*,#51282,.F.);
#72698=ORIENTED_EDGE('',*,*,#50584,.F.);
#72699=ORIENTED_EDGE('',*,*,#51283,.T.);
#72700=ORIENTED_EDGE('',*,*,#51274,.T.);
#72701=ORIENTED_EDGE('',*,*,#51280,.F.);
#72702=ORIENTED_EDGE('',*,*,#50583,.T.);
#72703=ORIENTED_EDGE('',*,*,#51284,.F.);
#72704=ORIENTED_EDGE('',*,*,#51271,.F.);
#72705=ORIENTED_EDGE('',*,*,#51283,.F.);
#72706=ORIENTED_EDGE('',*,*,#50582,.F.);
#72707=ORIENTED_EDGE('',*,*,#51284,.T.);
#72708=ORIENTED_EDGE('',*,*,#50827,.F.);
#72709=ORIENTED_EDGE('',*,*,#51285,.F.);
#72710=ORIENTED_EDGE('',*,*,#51267,.F.);
#72711=ORIENTED_EDGE('',*,*,#51285,.T.);
#72712=ORIENTED_EDGE('',*,*,#49922,.F.);
#72713=ORIENTED_EDGE('',*,*,#51286,.F.);
#72714=ORIENTED_EDGE('',*,*,#51268,.F.);
#72715=ORIENTED_EDGE('',*,*,#51286,.T.);
#72716=ORIENTED_EDGE('',*,*,#49921,.F.);
#72717=ORIENTED_EDGE('',*,*,#51287,.F.);
#72718=ORIENTED_EDGE('',*,*,#51272,.F.);
#72719=ORIENTED_EDGE('',*,*,#51287,.T.);
#72720=ORIENTED_EDGE('',*,*,#49920,.F.);
#72721=ORIENTED_EDGE('',*,*,#51288,.F.);
#72722=ORIENTED_EDGE('',*,*,#51263,.F.);
#72723=ORIENTED_EDGE('',*,*,#51289,.T.);
#72724=ORIENTED_EDGE('',*,*,#51264,.F.);
#72725=ORIENTED_EDGE('',*,*,#51288,.T.);
#72726=ORIENTED_EDGE('',*,*,#50826,.F.);
#72727=ORIENTED_EDGE('',*,*,#51290,.T.);
#72728=ORIENTED_EDGE('',*,*,#51265,.F.);
#72729=ORIENTED_EDGE('',*,*,#51289,.F.);
#72730=ORIENTED_EDGE('',*,*,#50586,.F.);
#72731=ORIENTED_EDGE('',*,*,#51282,.T.);
#72732=ORIENTED_EDGE('',*,*,#51278,.T.);
#72733=ORIENTED_EDGE('',*,*,#51290,.F.);
#72734=ORIENTED_EDGE('',*,*,#50585,.T.);
#72735=ORIENTED_EDGE('',*,*,#51276,.T.);
#72736=ORIENTED_EDGE('',*,*,#51279,.T.);
#72737=ORIENTED_EDGE('',*,*,#51281,.T.);
#72738=ORIENTED_EDGE('',*,*,#51291,.T.);
#72739=ORIENTED_EDGE('',*,*,#51292,.T.);
#72740=ORIENTED_EDGE('',*,*,#51293,.T.);
#72741=ORIENTED_EDGE('',*,*,#51294,.T.);
#72742=ORIENTED_EDGE('',*,*,#51295,.T.);
#72743=ORIENTED_EDGE('',*,*,#51296,.T.);
#72744=ORIENTED_EDGE('',*,*,#51297,.T.);
#72745=ORIENTED_EDGE('',*,*,#51298,.F.);
#72746=ORIENTED_EDGE('',*,*,#51299,.T.);
#72747=ORIENTED_EDGE('',*,*,#51300,.T.);
#72748=ORIENTED_EDGE('',*,*,#51298,.T.);
#72749=ORIENTED_EDGE('',*,*,#51301,.T.);
#72750=ORIENTED_EDGE('',*,*,#51291,.F.);
#72751=ORIENTED_EDGE('',*,*,#51302,.T.);
#72752=ORIENTED_EDGE('',*,*,#51303,.F.);
#72753=ORIENTED_EDGE('',*,*,#51299,.F.);
#72754=ORIENTED_EDGE('',*,*,#51304,.F.);
#72755=ORIENTED_EDGE('',*,*,#51305,.F.);
#72756=ORIENTED_EDGE('',*,*,#51304,.T.);
#72757=ORIENTED_EDGE('',*,*,#51302,.F.);
#72758=ORIENTED_EDGE('',*,*,#51306,.F.);
#72759=ORIENTED_EDGE('',*,*,#51306,.T.);
#72760=ORIENTED_EDGE('',*,*,#51295,.F.);
#72761=ORIENTED_EDGE('',*,*,#51307,.F.);
#72762=ORIENTED_EDGE('',*,*,#51308,.F.);
#72763=ORIENTED_EDGE('',*,*,#51309,.T.);
#72764=ORIENTED_EDGE('',*,*,#51310,.F.);
#72765=ORIENTED_EDGE('',*,*,#51311,.F.);
#72766=ORIENTED_EDGE('',*,*,#50590,.F.);
#72767=ORIENTED_EDGE('',*,*,#51312,.T.);
#72768=ORIENTED_EDGE('',*,*,#51303,.T.);
#72769=ORIENTED_EDGE('',*,*,#51309,.F.);
#72770=ORIENTED_EDGE('',*,*,#50589,.T.);
#72771=ORIENTED_EDGE('',*,*,#51313,.F.);
#72772=ORIENTED_EDGE('',*,*,#51300,.F.);
#72773=ORIENTED_EDGE('',*,*,#51312,.F.);
#72774=ORIENTED_EDGE('',*,*,#50588,.F.);
#72775=ORIENTED_EDGE('',*,*,#51313,.T.);
#72776=ORIENTED_EDGE('',*,*,#50825,.F.);
#72777=ORIENTED_EDGE('',*,*,#51314,.F.);
#72778=ORIENTED_EDGE('',*,*,#51296,.F.);
#72779=ORIENTED_EDGE('',*,*,#51314,.T.);
#72780=ORIENTED_EDGE('',*,*,#49918,.F.);
#72781=ORIENTED_EDGE('',*,*,#51315,.F.);
#72782=ORIENTED_EDGE('',*,*,#51297,.F.);
#72783=ORIENTED_EDGE('',*,*,#51315,.T.);
#72784=ORIENTED_EDGE('',*,*,#49917,.F.);
#72785=ORIENTED_EDGE('',*,*,#51316,.F.);
#72786=ORIENTED_EDGE('',*,*,#51301,.F.);
#72787=ORIENTED_EDGE('',*,*,#51316,.T.);
#72788=ORIENTED_EDGE('',*,*,#49916,.F.);
#72789=ORIENTED_EDGE('',*,*,#51317,.F.);
#72790=ORIENTED_EDGE('',*,*,#51292,.F.);
#72791=ORIENTED_EDGE('',*,*,#51318,.T.);
#72792=ORIENTED_EDGE('',*,*,#51293,.F.);
#72793=ORIENTED_EDGE('',*,*,#51317,.T.);
#72794=ORIENTED_EDGE('',*,*,#50824,.F.);
#72795=ORIENTED_EDGE('',*,*,#51319,.T.);
#72796=ORIENTED_EDGE('',*,*,#51294,.F.);
#72797=ORIENTED_EDGE('',*,*,#51318,.F.);
#72798=ORIENTED_EDGE('',*,*,#50592,.F.);
#72799=ORIENTED_EDGE('',*,*,#51311,.T.);
#72800=ORIENTED_EDGE('',*,*,#51307,.T.);
#72801=ORIENTED_EDGE('',*,*,#51319,.F.);
#72802=ORIENTED_EDGE('',*,*,#50591,.T.);
#72803=ORIENTED_EDGE('',*,*,#51305,.T.);
#72804=ORIENTED_EDGE('',*,*,#51308,.T.);
#72805=ORIENTED_EDGE('',*,*,#51310,.T.);
#72806=ORIENTED_EDGE('',*,*,#51320,.T.);
#72807=ORIENTED_EDGE('',*,*,#51321,.T.);
#72808=ORIENTED_EDGE('',*,*,#51322,.T.);
#72809=ORIENTED_EDGE('',*,*,#51323,.T.);
#72810=ORIENTED_EDGE('',*,*,#51324,.T.);
#72811=ORIENTED_EDGE('',*,*,#51325,.T.);
#72812=ORIENTED_EDGE('',*,*,#51326,.T.);
#72813=ORIENTED_EDGE('',*,*,#51327,.F.);
#72814=ORIENTED_EDGE('',*,*,#51328,.T.);
#72815=ORIENTED_EDGE('',*,*,#51329,.T.);
#72816=ORIENTED_EDGE('',*,*,#51327,.T.);
#72817=ORIENTED_EDGE('',*,*,#51330,.T.);
#72818=ORIENTED_EDGE('',*,*,#51320,.F.);
#72819=ORIENTED_EDGE('',*,*,#51331,.T.);
#72820=ORIENTED_EDGE('',*,*,#51332,.F.);
#72821=ORIENTED_EDGE('',*,*,#51328,.F.);
#72822=ORIENTED_EDGE('',*,*,#51333,.F.);
#72823=ORIENTED_EDGE('',*,*,#51334,.F.);
#72824=ORIENTED_EDGE('',*,*,#51333,.T.);
#72825=ORIENTED_EDGE('',*,*,#51331,.F.);
#72826=ORIENTED_EDGE('',*,*,#51335,.F.);
#72827=ORIENTED_EDGE('',*,*,#51335,.T.);
#72828=ORIENTED_EDGE('',*,*,#51324,.F.);
#72829=ORIENTED_EDGE('',*,*,#51336,.F.);
#72830=ORIENTED_EDGE('',*,*,#51337,.F.);
#72831=ORIENTED_EDGE('',*,*,#51338,.T.);
#72832=ORIENTED_EDGE('',*,*,#51339,.F.);
#72833=ORIENTED_EDGE('',*,*,#51340,.F.);
#72834=ORIENTED_EDGE('',*,*,#50596,.F.);
#72835=ORIENTED_EDGE('',*,*,#51341,.T.);
#72836=ORIENTED_EDGE('',*,*,#51332,.T.);
#72837=ORIENTED_EDGE('',*,*,#51338,.F.);
#72838=ORIENTED_EDGE('',*,*,#50595,.T.);
#72839=ORIENTED_EDGE('',*,*,#51342,.F.);
#72840=ORIENTED_EDGE('',*,*,#51329,.F.);
#72841=ORIENTED_EDGE('',*,*,#51341,.F.);
#72842=ORIENTED_EDGE('',*,*,#50594,.F.);
#72843=ORIENTED_EDGE('',*,*,#51342,.T.);
#72844=ORIENTED_EDGE('',*,*,#50823,.F.);
#72845=ORIENTED_EDGE('',*,*,#51343,.F.);
#72846=ORIENTED_EDGE('',*,*,#51325,.F.);
#72847=ORIENTED_EDGE('',*,*,#51343,.T.);
#72848=ORIENTED_EDGE('',*,*,#49914,.F.);
#72849=ORIENTED_EDGE('',*,*,#51344,.F.);
#72850=ORIENTED_EDGE('',*,*,#51326,.F.);
#72851=ORIENTED_EDGE('',*,*,#51344,.T.);
#72852=ORIENTED_EDGE('',*,*,#49913,.F.);
#72853=ORIENTED_EDGE('',*,*,#51345,.F.);
#72854=ORIENTED_EDGE('',*,*,#51330,.F.);
#72855=ORIENTED_EDGE('',*,*,#51345,.T.);
#72856=ORIENTED_EDGE('',*,*,#49912,.F.);
#72857=ORIENTED_EDGE('',*,*,#51346,.F.);
#72858=ORIENTED_EDGE('',*,*,#51321,.F.);
#72859=ORIENTED_EDGE('',*,*,#51347,.T.);
#72860=ORIENTED_EDGE('',*,*,#51322,.F.);
#72861=ORIENTED_EDGE('',*,*,#51346,.T.);
#72862=ORIENTED_EDGE('',*,*,#50822,.F.);
#72863=ORIENTED_EDGE('',*,*,#51348,.T.);
#72864=ORIENTED_EDGE('',*,*,#51323,.F.);
#72865=ORIENTED_EDGE('',*,*,#51347,.F.);
#72866=ORIENTED_EDGE('',*,*,#50598,.F.);
#72867=ORIENTED_EDGE('',*,*,#51340,.T.);
#72868=ORIENTED_EDGE('',*,*,#51336,.T.);
#72869=ORIENTED_EDGE('',*,*,#51348,.F.);
#72870=ORIENTED_EDGE('',*,*,#50597,.T.);
#72871=ORIENTED_EDGE('',*,*,#51334,.T.);
#72872=ORIENTED_EDGE('',*,*,#51337,.T.);
#72873=ORIENTED_EDGE('',*,*,#51339,.T.);
#72874=ORIENTED_EDGE('',*,*,#51349,.T.);
#72875=ORIENTED_EDGE('',*,*,#51350,.T.);
#72876=ORIENTED_EDGE('',*,*,#51351,.T.);
#72877=ORIENTED_EDGE('',*,*,#51352,.T.);
#72878=ORIENTED_EDGE('',*,*,#51353,.T.);
#72879=ORIENTED_EDGE('',*,*,#51354,.T.);
#72880=ORIENTED_EDGE('',*,*,#51355,.T.);
#72881=ORIENTED_EDGE('',*,*,#51356,.F.);
#72882=ORIENTED_EDGE('',*,*,#51357,.T.);
#72883=ORIENTED_EDGE('',*,*,#51358,.T.);
#72884=ORIENTED_EDGE('',*,*,#51356,.T.);
#72885=ORIENTED_EDGE('',*,*,#51359,.T.);
#72886=ORIENTED_EDGE('',*,*,#51349,.F.);
#72887=ORIENTED_EDGE('',*,*,#51360,.T.);
#72888=ORIENTED_EDGE('',*,*,#51361,.F.);
#72889=ORIENTED_EDGE('',*,*,#51357,.F.);
#72890=ORIENTED_EDGE('',*,*,#51362,.F.);
#72891=ORIENTED_EDGE('',*,*,#51363,.F.);
#72892=ORIENTED_EDGE('',*,*,#51362,.T.);
#72893=ORIENTED_EDGE('',*,*,#51360,.F.);
#72894=ORIENTED_EDGE('',*,*,#51364,.F.);
#72895=ORIENTED_EDGE('',*,*,#51364,.T.);
#72896=ORIENTED_EDGE('',*,*,#51353,.F.);
#72897=ORIENTED_EDGE('',*,*,#51365,.F.);
#72898=ORIENTED_EDGE('',*,*,#51366,.F.);
#72899=ORIENTED_EDGE('',*,*,#51367,.T.);
#72900=ORIENTED_EDGE('',*,*,#51368,.F.);
#72901=ORIENTED_EDGE('',*,*,#51369,.F.);
#72902=ORIENTED_EDGE('',*,*,#50602,.F.);
#72903=ORIENTED_EDGE('',*,*,#51370,.T.);
#72904=ORIENTED_EDGE('',*,*,#51361,.T.);
#72905=ORIENTED_EDGE('',*,*,#51367,.F.);
#72906=ORIENTED_EDGE('',*,*,#50601,.T.);
#72907=ORIENTED_EDGE('',*,*,#51371,.F.);
#72908=ORIENTED_EDGE('',*,*,#51358,.F.);
#72909=ORIENTED_EDGE('',*,*,#51370,.F.);
#72910=ORIENTED_EDGE('',*,*,#50600,.F.);
#72911=ORIENTED_EDGE('',*,*,#51371,.T.);
#72912=ORIENTED_EDGE('',*,*,#50821,.F.);
#72913=ORIENTED_EDGE('',*,*,#51372,.F.);
#72914=ORIENTED_EDGE('',*,*,#51354,.F.);
#72915=ORIENTED_EDGE('',*,*,#51372,.T.);
#72916=ORIENTED_EDGE('',*,*,#49910,.F.);
#72917=ORIENTED_EDGE('',*,*,#51373,.F.);
#72918=ORIENTED_EDGE('',*,*,#51355,.F.);
#72919=ORIENTED_EDGE('',*,*,#51373,.T.);
#72920=ORIENTED_EDGE('',*,*,#49909,.F.);
#72921=ORIENTED_EDGE('',*,*,#51374,.F.);
#72922=ORIENTED_EDGE('',*,*,#51359,.F.);
#72923=ORIENTED_EDGE('',*,*,#51374,.T.);
#72924=ORIENTED_EDGE('',*,*,#49908,.F.);
#72925=ORIENTED_EDGE('',*,*,#51375,.F.);
#72926=ORIENTED_EDGE('',*,*,#51350,.F.);
#72927=ORIENTED_EDGE('',*,*,#51376,.T.);
#72928=ORIENTED_EDGE('',*,*,#51351,.F.);
#72929=ORIENTED_EDGE('',*,*,#51375,.T.);
#72930=ORIENTED_EDGE('',*,*,#50820,.F.);
#72931=ORIENTED_EDGE('',*,*,#51377,.T.);
#72932=ORIENTED_EDGE('',*,*,#51352,.F.);
#72933=ORIENTED_EDGE('',*,*,#51376,.F.);
#72934=ORIENTED_EDGE('',*,*,#50604,.F.);
#72935=ORIENTED_EDGE('',*,*,#51369,.T.);
#72936=ORIENTED_EDGE('',*,*,#51365,.T.);
#72937=ORIENTED_EDGE('',*,*,#51377,.F.);
#72938=ORIENTED_EDGE('',*,*,#50603,.T.);
#72939=ORIENTED_EDGE('',*,*,#51363,.T.);
#72940=ORIENTED_EDGE('',*,*,#51366,.T.);
#72941=ORIENTED_EDGE('',*,*,#51368,.T.);
#72942=ORIENTED_EDGE('',*,*,#51378,.T.);
#72943=ORIENTED_EDGE('',*,*,#51379,.T.);
#72944=ORIENTED_EDGE('',*,*,#51380,.T.);
#72945=ORIENTED_EDGE('',*,*,#51381,.T.);
#72946=ORIENTED_EDGE('',*,*,#51382,.T.);
#72947=ORIENTED_EDGE('',*,*,#51383,.T.);
#72948=ORIENTED_EDGE('',*,*,#51384,.T.);
#72949=ORIENTED_EDGE('',*,*,#51385,.F.);
#72950=ORIENTED_EDGE('',*,*,#51386,.T.);
#72951=ORIENTED_EDGE('',*,*,#51387,.T.);
#72952=ORIENTED_EDGE('',*,*,#51385,.T.);
#72953=ORIENTED_EDGE('',*,*,#51388,.T.);
#72954=ORIENTED_EDGE('',*,*,#51378,.F.);
#72955=ORIENTED_EDGE('',*,*,#51389,.T.);
#72956=ORIENTED_EDGE('',*,*,#51390,.F.);
#72957=ORIENTED_EDGE('',*,*,#51386,.F.);
#72958=ORIENTED_EDGE('',*,*,#51391,.F.);
#72959=ORIENTED_EDGE('',*,*,#51392,.F.);
#72960=ORIENTED_EDGE('',*,*,#51391,.T.);
#72961=ORIENTED_EDGE('',*,*,#51389,.F.);
#72962=ORIENTED_EDGE('',*,*,#51393,.F.);
#72963=ORIENTED_EDGE('',*,*,#51393,.T.);
#72964=ORIENTED_EDGE('',*,*,#51382,.F.);
#72965=ORIENTED_EDGE('',*,*,#51394,.F.);
#72966=ORIENTED_EDGE('',*,*,#51395,.F.);
#72967=ORIENTED_EDGE('',*,*,#51396,.T.);
#72968=ORIENTED_EDGE('',*,*,#51397,.F.);
#72969=ORIENTED_EDGE('',*,*,#51398,.F.);
#72970=ORIENTED_EDGE('',*,*,#50608,.F.);
#72971=ORIENTED_EDGE('',*,*,#51399,.T.);
#72972=ORIENTED_EDGE('',*,*,#51390,.T.);
#72973=ORIENTED_EDGE('',*,*,#51396,.F.);
#72974=ORIENTED_EDGE('',*,*,#50607,.T.);
#72975=ORIENTED_EDGE('',*,*,#51400,.F.);
#72976=ORIENTED_EDGE('',*,*,#51387,.F.);
#72977=ORIENTED_EDGE('',*,*,#51399,.F.);
#72978=ORIENTED_EDGE('',*,*,#50606,.F.);
#72979=ORIENTED_EDGE('',*,*,#51400,.T.);
#72980=ORIENTED_EDGE('',*,*,#50819,.F.);
#72981=ORIENTED_EDGE('',*,*,#51401,.F.);
#72982=ORIENTED_EDGE('',*,*,#51383,.F.);
#72983=ORIENTED_EDGE('',*,*,#51401,.T.);
#72984=ORIENTED_EDGE('',*,*,#49906,.F.);
#72985=ORIENTED_EDGE('',*,*,#51402,.F.);
#72986=ORIENTED_EDGE('',*,*,#51384,.F.);
#72987=ORIENTED_EDGE('',*,*,#51402,.T.);
#72988=ORIENTED_EDGE('',*,*,#49905,.F.);
#72989=ORIENTED_EDGE('',*,*,#51403,.F.);
#72990=ORIENTED_EDGE('',*,*,#51388,.F.);
#72991=ORIENTED_EDGE('',*,*,#51403,.T.);
#72992=ORIENTED_EDGE('',*,*,#49904,.F.);
#72993=ORIENTED_EDGE('',*,*,#51404,.F.);
#72994=ORIENTED_EDGE('',*,*,#51379,.F.);
#72995=ORIENTED_EDGE('',*,*,#51405,.T.);
#72996=ORIENTED_EDGE('',*,*,#51380,.F.);
#72997=ORIENTED_EDGE('',*,*,#51404,.T.);
#72998=ORIENTED_EDGE('',*,*,#50818,.F.);
#72999=ORIENTED_EDGE('',*,*,#51406,.T.);
#73000=ORIENTED_EDGE('',*,*,#51381,.F.);
#73001=ORIENTED_EDGE('',*,*,#51405,.F.);
#73002=ORIENTED_EDGE('',*,*,#50610,.F.);
#73003=ORIENTED_EDGE('',*,*,#51398,.T.);
#73004=ORIENTED_EDGE('',*,*,#51394,.T.);
#73005=ORIENTED_EDGE('',*,*,#51406,.F.);
#73006=ORIENTED_EDGE('',*,*,#50609,.T.);
#73007=ORIENTED_EDGE('',*,*,#51392,.T.);
#73008=ORIENTED_EDGE('',*,*,#51395,.T.);
#73009=ORIENTED_EDGE('',*,*,#51397,.T.);
#73010=ORIENTED_EDGE('',*,*,#51407,.T.);
#73011=ORIENTED_EDGE('',*,*,#51408,.T.);
#73012=ORIENTED_EDGE('',*,*,#51409,.T.);
#73013=ORIENTED_EDGE('',*,*,#51410,.T.);
#73014=ORIENTED_EDGE('',*,*,#51411,.T.);
#73015=ORIENTED_EDGE('',*,*,#51412,.T.);
#73016=ORIENTED_EDGE('',*,*,#51413,.T.);
#73017=ORIENTED_EDGE('',*,*,#51414,.F.);
#73018=ORIENTED_EDGE('',*,*,#51415,.T.);
#73019=ORIENTED_EDGE('',*,*,#51416,.T.);
#73020=ORIENTED_EDGE('',*,*,#51414,.T.);
#73021=ORIENTED_EDGE('',*,*,#51417,.T.);
#73022=ORIENTED_EDGE('',*,*,#51407,.F.);
#73023=ORIENTED_EDGE('',*,*,#51418,.T.);
#73024=ORIENTED_EDGE('',*,*,#51419,.F.);
#73025=ORIENTED_EDGE('',*,*,#51415,.F.);
#73026=ORIENTED_EDGE('',*,*,#51420,.F.);
#73027=ORIENTED_EDGE('',*,*,#51421,.F.);
#73028=ORIENTED_EDGE('',*,*,#51420,.T.);
#73029=ORIENTED_EDGE('',*,*,#51418,.F.);
#73030=ORIENTED_EDGE('',*,*,#51422,.F.);
#73031=ORIENTED_EDGE('',*,*,#51422,.T.);
#73032=ORIENTED_EDGE('',*,*,#51411,.F.);
#73033=ORIENTED_EDGE('',*,*,#51423,.F.);
#73034=ORIENTED_EDGE('',*,*,#51424,.F.);
#73035=ORIENTED_EDGE('',*,*,#51425,.T.);
#73036=ORIENTED_EDGE('',*,*,#51426,.F.);
#73037=ORIENTED_EDGE('',*,*,#51427,.F.);
#73038=ORIENTED_EDGE('',*,*,#50614,.F.);
#73039=ORIENTED_EDGE('',*,*,#51428,.T.);
#73040=ORIENTED_EDGE('',*,*,#51419,.T.);
#73041=ORIENTED_EDGE('',*,*,#51425,.F.);
#73042=ORIENTED_EDGE('',*,*,#50613,.T.);
#73043=ORIENTED_EDGE('',*,*,#51429,.F.);
#73044=ORIENTED_EDGE('',*,*,#51416,.F.);
#73045=ORIENTED_EDGE('',*,*,#51428,.F.);
#73046=ORIENTED_EDGE('',*,*,#50612,.F.);
#73047=ORIENTED_EDGE('',*,*,#51429,.T.);
#73048=ORIENTED_EDGE('',*,*,#50817,.F.);
#73049=ORIENTED_EDGE('',*,*,#51430,.F.);
#73050=ORIENTED_EDGE('',*,*,#51412,.F.);
#73051=ORIENTED_EDGE('',*,*,#51430,.T.);
#73052=ORIENTED_EDGE('',*,*,#49902,.F.);
#73053=ORIENTED_EDGE('',*,*,#51431,.F.);
#73054=ORIENTED_EDGE('',*,*,#51413,.F.);
#73055=ORIENTED_EDGE('',*,*,#51431,.T.);
#73056=ORIENTED_EDGE('',*,*,#49901,.F.);
#73057=ORIENTED_EDGE('',*,*,#51432,.F.);
#73058=ORIENTED_EDGE('',*,*,#51417,.F.);
#73059=ORIENTED_EDGE('',*,*,#51432,.T.);
#73060=ORIENTED_EDGE('',*,*,#49900,.F.);
#73061=ORIENTED_EDGE('',*,*,#51433,.F.);
#73062=ORIENTED_EDGE('',*,*,#51408,.F.);
#73063=ORIENTED_EDGE('',*,*,#51434,.T.);
#73064=ORIENTED_EDGE('',*,*,#51409,.F.);
#73065=ORIENTED_EDGE('',*,*,#51433,.T.);
#73066=ORIENTED_EDGE('',*,*,#50816,.F.);
#73067=ORIENTED_EDGE('',*,*,#51435,.T.);
#73068=ORIENTED_EDGE('',*,*,#51410,.F.);
#73069=ORIENTED_EDGE('',*,*,#51434,.F.);
#73070=ORIENTED_EDGE('',*,*,#50616,.F.);
#73071=ORIENTED_EDGE('',*,*,#51427,.T.);
#73072=ORIENTED_EDGE('',*,*,#51423,.T.);
#73073=ORIENTED_EDGE('',*,*,#51435,.F.);
#73074=ORIENTED_EDGE('',*,*,#50615,.T.);
#73075=ORIENTED_EDGE('',*,*,#51421,.T.);
#73076=ORIENTED_EDGE('',*,*,#51424,.T.);
#73077=ORIENTED_EDGE('',*,*,#51426,.T.);
#73078=ORIENTED_EDGE('',*,*,#51436,.T.);
#73079=ORIENTED_EDGE('',*,*,#51437,.T.);
#73080=ORIENTED_EDGE('',*,*,#51438,.T.);
#73081=ORIENTED_EDGE('',*,*,#51439,.T.);
#73082=ORIENTED_EDGE('',*,*,#51440,.T.);
#73083=ORIENTED_EDGE('',*,*,#51441,.T.);
#73084=ORIENTED_EDGE('',*,*,#51442,.T.);
#73085=ORIENTED_EDGE('',*,*,#51443,.F.);
#73086=ORIENTED_EDGE('',*,*,#51444,.T.);
#73087=ORIENTED_EDGE('',*,*,#51445,.T.);
#73088=ORIENTED_EDGE('',*,*,#51443,.T.);
#73089=ORIENTED_EDGE('',*,*,#51446,.T.);
#73090=ORIENTED_EDGE('',*,*,#51436,.F.);
#73091=ORIENTED_EDGE('',*,*,#51447,.T.);
#73092=ORIENTED_EDGE('',*,*,#51448,.F.);
#73093=ORIENTED_EDGE('',*,*,#51444,.F.);
#73094=ORIENTED_EDGE('',*,*,#51449,.F.);
#73095=ORIENTED_EDGE('',*,*,#51450,.F.);
#73096=ORIENTED_EDGE('',*,*,#51449,.T.);
#73097=ORIENTED_EDGE('',*,*,#51447,.F.);
#73098=ORIENTED_EDGE('',*,*,#51451,.F.);
#73099=ORIENTED_EDGE('',*,*,#51451,.T.);
#73100=ORIENTED_EDGE('',*,*,#51440,.F.);
#73101=ORIENTED_EDGE('',*,*,#51452,.F.);
#73102=ORIENTED_EDGE('',*,*,#51453,.F.);
#73103=ORIENTED_EDGE('',*,*,#51454,.T.);
#73104=ORIENTED_EDGE('',*,*,#51455,.F.);
#73105=ORIENTED_EDGE('',*,*,#51456,.F.);
#73106=ORIENTED_EDGE('',*,*,#50620,.F.);
#73107=ORIENTED_EDGE('',*,*,#51457,.T.);
#73108=ORIENTED_EDGE('',*,*,#51448,.T.);
#73109=ORIENTED_EDGE('',*,*,#51454,.F.);
#73110=ORIENTED_EDGE('',*,*,#50619,.T.);
#73111=ORIENTED_EDGE('',*,*,#51458,.F.);
#73112=ORIENTED_EDGE('',*,*,#51445,.F.);
#73113=ORIENTED_EDGE('',*,*,#51457,.F.);
#73114=ORIENTED_EDGE('',*,*,#50618,.F.);
#73115=ORIENTED_EDGE('',*,*,#51458,.T.);
#73116=ORIENTED_EDGE('',*,*,#50815,.F.);
#73117=ORIENTED_EDGE('',*,*,#51459,.F.);
#73118=ORIENTED_EDGE('',*,*,#51441,.F.);
#73119=ORIENTED_EDGE('',*,*,#51459,.T.);
#73120=ORIENTED_EDGE('',*,*,#49898,.F.);
#73121=ORIENTED_EDGE('',*,*,#51460,.F.);
#73122=ORIENTED_EDGE('',*,*,#51442,.F.);
#73123=ORIENTED_EDGE('',*,*,#51460,.T.);
#73124=ORIENTED_EDGE('',*,*,#49897,.F.);
#73125=ORIENTED_EDGE('',*,*,#51461,.F.);
#73126=ORIENTED_EDGE('',*,*,#51446,.F.);
#73127=ORIENTED_EDGE('',*,*,#51461,.T.);
#73128=ORIENTED_EDGE('',*,*,#49896,.F.);
#73129=ORIENTED_EDGE('',*,*,#51462,.F.);
#73130=ORIENTED_EDGE('',*,*,#51437,.F.);
#73131=ORIENTED_EDGE('',*,*,#51463,.T.);
#73132=ORIENTED_EDGE('',*,*,#51438,.F.);
#73133=ORIENTED_EDGE('',*,*,#51462,.T.);
#73134=ORIENTED_EDGE('',*,*,#50814,.F.);
#73135=ORIENTED_EDGE('',*,*,#51464,.T.);
#73136=ORIENTED_EDGE('',*,*,#51439,.F.);
#73137=ORIENTED_EDGE('',*,*,#51463,.F.);
#73138=ORIENTED_EDGE('',*,*,#50622,.F.);
#73139=ORIENTED_EDGE('',*,*,#51456,.T.);
#73140=ORIENTED_EDGE('',*,*,#51452,.T.);
#73141=ORIENTED_EDGE('',*,*,#51464,.F.);
#73142=ORIENTED_EDGE('',*,*,#50621,.T.);
#73143=ORIENTED_EDGE('',*,*,#51450,.T.);
#73144=ORIENTED_EDGE('',*,*,#51453,.T.);
#73145=ORIENTED_EDGE('',*,*,#51455,.T.);
#73146=ORIENTED_EDGE('',*,*,#51465,.T.);
#73147=ORIENTED_EDGE('',*,*,#51466,.T.);
#73148=ORIENTED_EDGE('',*,*,#51467,.T.);
#73149=ORIENTED_EDGE('',*,*,#51468,.T.);
#73150=ORIENTED_EDGE('',*,*,#51469,.T.);
#73151=ORIENTED_EDGE('',*,*,#51470,.T.);
#73152=ORIENTED_EDGE('',*,*,#51471,.T.);
#73153=ORIENTED_EDGE('',*,*,#51472,.F.);
#73154=ORIENTED_EDGE('',*,*,#51473,.T.);
#73155=ORIENTED_EDGE('',*,*,#51474,.T.);
#73156=ORIENTED_EDGE('',*,*,#51472,.T.);
#73157=ORIENTED_EDGE('',*,*,#51475,.T.);
#73158=ORIENTED_EDGE('',*,*,#51465,.F.);
#73159=ORIENTED_EDGE('',*,*,#51476,.T.);
#73160=ORIENTED_EDGE('',*,*,#51477,.F.);
#73161=ORIENTED_EDGE('',*,*,#51473,.F.);
#73162=ORIENTED_EDGE('',*,*,#51478,.F.);
#73163=ORIENTED_EDGE('',*,*,#51479,.F.);
#73164=ORIENTED_EDGE('',*,*,#51478,.T.);
#73165=ORIENTED_EDGE('',*,*,#51476,.F.);
#73166=ORIENTED_EDGE('',*,*,#51480,.F.);
#73167=ORIENTED_EDGE('',*,*,#51480,.T.);
#73168=ORIENTED_EDGE('',*,*,#51469,.F.);
#73169=ORIENTED_EDGE('',*,*,#51481,.F.);
#73170=ORIENTED_EDGE('',*,*,#51482,.F.);
#73171=ORIENTED_EDGE('',*,*,#51483,.T.);
#73172=ORIENTED_EDGE('',*,*,#51484,.F.);
#73173=ORIENTED_EDGE('',*,*,#51485,.F.);
#73174=ORIENTED_EDGE('',*,*,#50626,.F.);
#73175=ORIENTED_EDGE('',*,*,#51486,.T.);
#73176=ORIENTED_EDGE('',*,*,#51477,.T.);
#73177=ORIENTED_EDGE('',*,*,#51483,.F.);
#73178=ORIENTED_EDGE('',*,*,#50625,.T.);
#73179=ORIENTED_EDGE('',*,*,#51487,.F.);
#73180=ORIENTED_EDGE('',*,*,#51474,.F.);
#73181=ORIENTED_EDGE('',*,*,#51486,.F.);
#73182=ORIENTED_EDGE('',*,*,#50624,.F.);
#73183=ORIENTED_EDGE('',*,*,#51487,.T.);
#73184=ORIENTED_EDGE('',*,*,#50813,.F.);
#73185=ORIENTED_EDGE('',*,*,#51488,.F.);
#73186=ORIENTED_EDGE('',*,*,#51470,.F.);
#73187=ORIENTED_EDGE('',*,*,#51488,.T.);
#73188=ORIENTED_EDGE('',*,*,#49894,.F.);
#73189=ORIENTED_EDGE('',*,*,#51489,.F.);
#73190=ORIENTED_EDGE('',*,*,#51471,.F.);
#73191=ORIENTED_EDGE('',*,*,#51489,.T.);
#73192=ORIENTED_EDGE('',*,*,#49893,.F.);
#73193=ORIENTED_EDGE('',*,*,#51490,.F.);
#73194=ORIENTED_EDGE('',*,*,#51475,.F.);
#73195=ORIENTED_EDGE('',*,*,#51490,.T.);
#73196=ORIENTED_EDGE('',*,*,#49892,.F.);
#73197=ORIENTED_EDGE('',*,*,#51491,.F.);
#73198=ORIENTED_EDGE('',*,*,#51466,.F.);
#73199=ORIENTED_EDGE('',*,*,#51492,.T.);
#73200=ORIENTED_EDGE('',*,*,#51467,.F.);
#73201=ORIENTED_EDGE('',*,*,#51491,.T.);
#73202=ORIENTED_EDGE('',*,*,#50812,.F.);
#73203=ORIENTED_EDGE('',*,*,#51493,.T.);
#73204=ORIENTED_EDGE('',*,*,#51468,.F.);
#73205=ORIENTED_EDGE('',*,*,#51492,.F.);
#73206=ORIENTED_EDGE('',*,*,#50628,.F.);
#73207=ORIENTED_EDGE('',*,*,#51485,.T.);
#73208=ORIENTED_EDGE('',*,*,#51481,.T.);
#73209=ORIENTED_EDGE('',*,*,#51493,.F.);
#73210=ORIENTED_EDGE('',*,*,#50627,.T.);
#73211=ORIENTED_EDGE('',*,*,#51479,.T.);
#73212=ORIENTED_EDGE('',*,*,#51482,.T.);
#73213=ORIENTED_EDGE('',*,*,#51484,.T.);
#73214=ORIENTED_EDGE('',*,*,#51494,.T.);
#73215=ORIENTED_EDGE('',*,*,#51495,.T.);
#73216=ORIENTED_EDGE('',*,*,#51496,.T.);
#73217=ORIENTED_EDGE('',*,*,#51497,.T.);
#73218=ORIENTED_EDGE('',*,*,#51498,.T.);
#73219=ORIENTED_EDGE('',*,*,#51499,.T.);
#73220=ORIENTED_EDGE('',*,*,#51500,.T.);
#73221=ORIENTED_EDGE('',*,*,#51501,.F.);
#73222=ORIENTED_EDGE('',*,*,#51502,.T.);
#73223=ORIENTED_EDGE('',*,*,#51503,.T.);
#73224=ORIENTED_EDGE('',*,*,#51501,.T.);
#73225=ORIENTED_EDGE('',*,*,#51504,.T.);
#73226=ORIENTED_EDGE('',*,*,#51494,.F.);
#73227=ORIENTED_EDGE('',*,*,#51505,.T.);
#73228=ORIENTED_EDGE('',*,*,#51506,.F.);
#73229=ORIENTED_EDGE('',*,*,#51502,.F.);
#73230=ORIENTED_EDGE('',*,*,#51507,.F.);
#73231=ORIENTED_EDGE('',*,*,#51508,.F.);
#73232=ORIENTED_EDGE('',*,*,#51507,.T.);
#73233=ORIENTED_EDGE('',*,*,#51505,.F.);
#73234=ORIENTED_EDGE('',*,*,#51509,.F.);
#73235=ORIENTED_EDGE('',*,*,#51509,.T.);
#73236=ORIENTED_EDGE('',*,*,#51498,.F.);
#73237=ORIENTED_EDGE('',*,*,#51510,.F.);
#73238=ORIENTED_EDGE('',*,*,#51511,.F.);
#73239=ORIENTED_EDGE('',*,*,#51512,.T.);
#73240=ORIENTED_EDGE('',*,*,#51513,.F.);
#73241=ORIENTED_EDGE('',*,*,#51514,.F.);
#73242=ORIENTED_EDGE('',*,*,#50632,.F.);
#73243=ORIENTED_EDGE('',*,*,#51515,.T.);
#73244=ORIENTED_EDGE('',*,*,#51506,.T.);
#73245=ORIENTED_EDGE('',*,*,#51512,.F.);
#73246=ORIENTED_EDGE('',*,*,#50631,.T.);
#73247=ORIENTED_EDGE('',*,*,#51516,.F.);
#73248=ORIENTED_EDGE('',*,*,#51503,.F.);
#73249=ORIENTED_EDGE('',*,*,#51515,.F.);
#73250=ORIENTED_EDGE('',*,*,#50630,.F.);
#73251=ORIENTED_EDGE('',*,*,#51516,.T.);
#73252=ORIENTED_EDGE('',*,*,#50811,.F.);
#73253=ORIENTED_EDGE('',*,*,#51517,.F.);
#73254=ORIENTED_EDGE('',*,*,#51499,.F.);
#73255=ORIENTED_EDGE('',*,*,#51517,.T.);
#73256=ORIENTED_EDGE('',*,*,#49890,.F.);
#73257=ORIENTED_EDGE('',*,*,#51518,.F.);
#73258=ORIENTED_EDGE('',*,*,#51500,.F.);
#73259=ORIENTED_EDGE('',*,*,#51518,.T.);
#73260=ORIENTED_EDGE('',*,*,#49889,.F.);
#73261=ORIENTED_EDGE('',*,*,#51519,.F.);
#73262=ORIENTED_EDGE('',*,*,#51504,.F.);
#73263=ORIENTED_EDGE('',*,*,#51519,.T.);
#73264=ORIENTED_EDGE('',*,*,#49888,.F.);
#73265=ORIENTED_EDGE('',*,*,#51520,.F.);
#73266=ORIENTED_EDGE('',*,*,#51495,.F.);
#73267=ORIENTED_EDGE('',*,*,#51521,.T.);
#73268=ORIENTED_EDGE('',*,*,#51496,.F.);
#73269=ORIENTED_EDGE('',*,*,#51520,.T.);
#73270=ORIENTED_EDGE('',*,*,#50810,.F.);
#73271=ORIENTED_EDGE('',*,*,#51522,.T.);
#73272=ORIENTED_EDGE('',*,*,#51497,.F.);
#73273=ORIENTED_EDGE('',*,*,#51521,.F.);
#73274=ORIENTED_EDGE('',*,*,#50634,.F.);
#73275=ORIENTED_EDGE('',*,*,#51514,.T.);
#73276=ORIENTED_EDGE('',*,*,#51510,.T.);
#73277=ORIENTED_EDGE('',*,*,#51522,.F.);
#73278=ORIENTED_EDGE('',*,*,#50633,.T.);
#73279=ORIENTED_EDGE('',*,*,#51508,.T.);
#73280=ORIENTED_EDGE('',*,*,#51511,.T.);
#73281=ORIENTED_EDGE('',*,*,#51513,.T.);
#73282=ORIENTED_EDGE('',*,*,#51523,.T.);
#73283=ORIENTED_EDGE('',*,*,#51524,.T.);
#73284=ORIENTED_EDGE('',*,*,#51525,.T.);
#73285=ORIENTED_EDGE('',*,*,#51526,.T.);
#73286=ORIENTED_EDGE('',*,*,#51527,.T.);
#73287=ORIENTED_EDGE('',*,*,#51528,.T.);
#73288=ORIENTED_EDGE('',*,*,#51529,.T.);
#73289=ORIENTED_EDGE('',*,*,#51530,.F.);
#73290=ORIENTED_EDGE('',*,*,#51531,.T.);
#73291=ORIENTED_EDGE('',*,*,#51532,.T.);
#73292=ORIENTED_EDGE('',*,*,#51530,.T.);
#73293=ORIENTED_EDGE('',*,*,#51533,.T.);
#73294=ORIENTED_EDGE('',*,*,#51523,.F.);
#73295=ORIENTED_EDGE('',*,*,#51534,.T.);
#73296=ORIENTED_EDGE('',*,*,#51535,.F.);
#73297=ORIENTED_EDGE('',*,*,#51531,.F.);
#73298=ORIENTED_EDGE('',*,*,#51536,.F.);
#73299=ORIENTED_EDGE('',*,*,#51537,.F.);
#73300=ORIENTED_EDGE('',*,*,#51536,.T.);
#73301=ORIENTED_EDGE('',*,*,#51534,.F.);
#73302=ORIENTED_EDGE('',*,*,#51538,.F.);
#73303=ORIENTED_EDGE('',*,*,#51538,.T.);
#73304=ORIENTED_EDGE('',*,*,#51527,.F.);
#73305=ORIENTED_EDGE('',*,*,#51539,.F.);
#73306=ORIENTED_EDGE('',*,*,#51540,.F.);
#73307=ORIENTED_EDGE('',*,*,#51541,.T.);
#73308=ORIENTED_EDGE('',*,*,#51542,.F.);
#73309=ORIENTED_EDGE('',*,*,#51543,.F.);
#73310=ORIENTED_EDGE('',*,*,#50638,.F.);
#73311=ORIENTED_EDGE('',*,*,#51544,.T.);
#73312=ORIENTED_EDGE('',*,*,#51535,.T.);
#73313=ORIENTED_EDGE('',*,*,#51541,.F.);
#73314=ORIENTED_EDGE('',*,*,#50637,.T.);
#73315=ORIENTED_EDGE('',*,*,#51545,.F.);
#73316=ORIENTED_EDGE('',*,*,#51532,.F.);
#73317=ORIENTED_EDGE('',*,*,#51544,.F.);
#73318=ORIENTED_EDGE('',*,*,#50636,.F.);
#73319=ORIENTED_EDGE('',*,*,#51545,.T.);
#73320=ORIENTED_EDGE('',*,*,#50809,.F.);
#73321=ORIENTED_EDGE('',*,*,#51546,.F.);
#73322=ORIENTED_EDGE('',*,*,#51528,.F.);
#73323=ORIENTED_EDGE('',*,*,#51546,.T.);
#73324=ORIENTED_EDGE('',*,*,#49886,.F.);
#73325=ORIENTED_EDGE('',*,*,#51547,.F.);
#73326=ORIENTED_EDGE('',*,*,#51529,.F.);
#73327=ORIENTED_EDGE('',*,*,#51547,.T.);
#73328=ORIENTED_EDGE('',*,*,#49885,.F.);
#73329=ORIENTED_EDGE('',*,*,#51548,.F.);
#73330=ORIENTED_EDGE('',*,*,#51533,.F.);
#73331=ORIENTED_EDGE('',*,*,#51548,.T.);
#73332=ORIENTED_EDGE('',*,*,#49884,.F.);
#73333=ORIENTED_EDGE('',*,*,#51549,.F.);
#73334=ORIENTED_EDGE('',*,*,#51524,.F.);
#73335=ORIENTED_EDGE('',*,*,#51550,.T.);
#73336=ORIENTED_EDGE('',*,*,#51525,.F.);
#73337=ORIENTED_EDGE('',*,*,#51549,.T.);
#73338=ORIENTED_EDGE('',*,*,#50808,.F.);
#73339=ORIENTED_EDGE('',*,*,#51551,.T.);
#73340=ORIENTED_EDGE('',*,*,#51526,.F.);
#73341=ORIENTED_EDGE('',*,*,#51550,.F.);
#73342=ORIENTED_EDGE('',*,*,#50640,.F.);
#73343=ORIENTED_EDGE('',*,*,#51543,.T.);
#73344=ORIENTED_EDGE('',*,*,#51539,.T.);
#73345=ORIENTED_EDGE('',*,*,#51551,.F.);
#73346=ORIENTED_EDGE('',*,*,#50639,.T.);
#73347=ORIENTED_EDGE('',*,*,#51537,.T.);
#73348=ORIENTED_EDGE('',*,*,#51540,.T.);
#73349=ORIENTED_EDGE('',*,*,#51542,.T.);
#73350=ORIENTED_EDGE('',*,*,#51552,.T.);
#73351=ORIENTED_EDGE('',*,*,#51553,.T.);
#73352=ORIENTED_EDGE('',*,*,#51554,.T.);
#73353=ORIENTED_EDGE('',*,*,#51555,.T.);
#73354=ORIENTED_EDGE('',*,*,#51556,.T.);
#73355=ORIENTED_EDGE('',*,*,#51557,.T.);
#73356=ORIENTED_EDGE('',*,*,#51558,.T.);
#73357=ORIENTED_EDGE('',*,*,#51559,.F.);
#73358=ORIENTED_EDGE('',*,*,#51560,.T.);
#73359=ORIENTED_EDGE('',*,*,#51561,.T.);
#73360=ORIENTED_EDGE('',*,*,#51559,.T.);
#73361=ORIENTED_EDGE('',*,*,#51562,.T.);
#73362=ORIENTED_EDGE('',*,*,#51552,.F.);
#73363=ORIENTED_EDGE('',*,*,#51563,.T.);
#73364=ORIENTED_EDGE('',*,*,#51564,.F.);
#73365=ORIENTED_EDGE('',*,*,#51560,.F.);
#73366=ORIENTED_EDGE('',*,*,#51565,.F.);
#73367=ORIENTED_EDGE('',*,*,#51566,.F.);
#73368=ORIENTED_EDGE('',*,*,#51565,.T.);
#73369=ORIENTED_EDGE('',*,*,#51563,.F.);
#73370=ORIENTED_EDGE('',*,*,#51567,.F.);
#73371=ORIENTED_EDGE('',*,*,#51567,.T.);
#73372=ORIENTED_EDGE('',*,*,#51556,.F.);
#73373=ORIENTED_EDGE('',*,*,#51568,.F.);
#73374=ORIENTED_EDGE('',*,*,#51569,.F.);
#73375=ORIENTED_EDGE('',*,*,#51570,.T.);
#73376=ORIENTED_EDGE('',*,*,#51571,.F.);
#73377=ORIENTED_EDGE('',*,*,#51572,.F.);
#73378=ORIENTED_EDGE('',*,*,#50644,.F.);
#73379=ORIENTED_EDGE('',*,*,#51573,.T.);
#73380=ORIENTED_EDGE('',*,*,#51564,.T.);
#73381=ORIENTED_EDGE('',*,*,#51570,.F.);
#73382=ORIENTED_EDGE('',*,*,#50643,.T.);
#73383=ORIENTED_EDGE('',*,*,#51574,.F.);
#73384=ORIENTED_EDGE('',*,*,#51561,.F.);
#73385=ORIENTED_EDGE('',*,*,#51573,.F.);
#73386=ORIENTED_EDGE('',*,*,#50642,.F.);
#73387=ORIENTED_EDGE('',*,*,#51574,.T.);
#73388=ORIENTED_EDGE('',*,*,#50807,.F.);
#73389=ORIENTED_EDGE('',*,*,#51575,.F.);
#73390=ORIENTED_EDGE('',*,*,#51557,.F.);
#73391=ORIENTED_EDGE('',*,*,#51575,.T.);
#73392=ORIENTED_EDGE('',*,*,#49882,.F.);
#73393=ORIENTED_EDGE('',*,*,#51576,.F.);
#73394=ORIENTED_EDGE('',*,*,#51558,.F.);
#73395=ORIENTED_EDGE('',*,*,#51576,.T.);
#73396=ORIENTED_EDGE('',*,*,#49881,.F.);
#73397=ORIENTED_EDGE('',*,*,#51577,.F.);
#73398=ORIENTED_EDGE('',*,*,#51562,.F.);
#73399=ORIENTED_EDGE('',*,*,#51577,.T.);
#73400=ORIENTED_EDGE('',*,*,#49880,.F.);
#73401=ORIENTED_EDGE('',*,*,#51578,.F.);
#73402=ORIENTED_EDGE('',*,*,#51553,.F.);
#73403=ORIENTED_EDGE('',*,*,#51579,.T.);
#73404=ORIENTED_EDGE('',*,*,#51554,.F.);
#73405=ORIENTED_EDGE('',*,*,#51578,.T.);
#73406=ORIENTED_EDGE('',*,*,#50806,.F.);
#73407=ORIENTED_EDGE('',*,*,#51580,.T.);
#73408=ORIENTED_EDGE('',*,*,#51555,.F.);
#73409=ORIENTED_EDGE('',*,*,#51579,.F.);
#73410=ORIENTED_EDGE('',*,*,#50646,.F.);
#73411=ORIENTED_EDGE('',*,*,#51572,.T.);
#73412=ORIENTED_EDGE('',*,*,#51568,.T.);
#73413=ORIENTED_EDGE('',*,*,#51580,.F.);
#73414=ORIENTED_EDGE('',*,*,#50645,.T.);
#73415=ORIENTED_EDGE('',*,*,#51566,.T.);
#73416=ORIENTED_EDGE('',*,*,#51569,.T.);
#73417=ORIENTED_EDGE('',*,*,#51571,.T.);
#73418=ORIENTED_EDGE('',*,*,#51581,.T.);
#73419=ORIENTED_EDGE('',*,*,#51582,.T.);
#73420=ORIENTED_EDGE('',*,*,#51583,.T.);
#73421=ORIENTED_EDGE('',*,*,#51584,.T.);
#73422=ORIENTED_EDGE('',*,*,#51585,.T.);
#73423=ORIENTED_EDGE('',*,*,#51586,.T.);
#73424=ORIENTED_EDGE('',*,*,#51587,.T.);
#73425=ORIENTED_EDGE('',*,*,#51588,.F.);
#73426=ORIENTED_EDGE('',*,*,#51589,.T.);
#73427=ORIENTED_EDGE('',*,*,#51590,.T.);
#73428=ORIENTED_EDGE('',*,*,#51588,.T.);
#73429=ORIENTED_EDGE('',*,*,#51591,.T.);
#73430=ORIENTED_EDGE('',*,*,#51581,.F.);
#73431=ORIENTED_EDGE('',*,*,#51592,.T.);
#73432=ORIENTED_EDGE('',*,*,#51593,.F.);
#73433=ORIENTED_EDGE('',*,*,#51589,.F.);
#73434=ORIENTED_EDGE('',*,*,#51594,.F.);
#73435=ORIENTED_EDGE('',*,*,#51595,.F.);
#73436=ORIENTED_EDGE('',*,*,#51594,.T.);
#73437=ORIENTED_EDGE('',*,*,#51592,.F.);
#73438=ORIENTED_EDGE('',*,*,#51596,.F.);
#73439=ORIENTED_EDGE('',*,*,#51596,.T.);
#73440=ORIENTED_EDGE('',*,*,#51585,.F.);
#73441=ORIENTED_EDGE('',*,*,#51597,.F.);
#73442=ORIENTED_EDGE('',*,*,#51598,.F.);
#73443=ORIENTED_EDGE('',*,*,#51599,.T.);
#73444=ORIENTED_EDGE('',*,*,#51600,.F.);
#73445=ORIENTED_EDGE('',*,*,#51601,.F.);
#73446=ORIENTED_EDGE('',*,*,#50650,.F.);
#73447=ORIENTED_EDGE('',*,*,#51602,.T.);
#73448=ORIENTED_EDGE('',*,*,#51593,.T.);
#73449=ORIENTED_EDGE('',*,*,#51599,.F.);
#73450=ORIENTED_EDGE('',*,*,#50649,.T.);
#73451=ORIENTED_EDGE('',*,*,#51603,.F.);
#73452=ORIENTED_EDGE('',*,*,#51590,.F.);
#73453=ORIENTED_EDGE('',*,*,#51602,.F.);
#73454=ORIENTED_EDGE('',*,*,#50648,.F.);
#73455=ORIENTED_EDGE('',*,*,#51603,.T.);
#73456=ORIENTED_EDGE('',*,*,#50805,.F.);
#73457=ORIENTED_EDGE('',*,*,#51604,.F.);
#73458=ORIENTED_EDGE('',*,*,#51586,.F.);
#73459=ORIENTED_EDGE('',*,*,#51604,.T.);
#73460=ORIENTED_EDGE('',*,*,#49878,.F.);
#73461=ORIENTED_EDGE('',*,*,#51605,.F.);
#73462=ORIENTED_EDGE('',*,*,#51587,.F.);
#73463=ORIENTED_EDGE('',*,*,#51605,.T.);
#73464=ORIENTED_EDGE('',*,*,#49877,.F.);
#73465=ORIENTED_EDGE('',*,*,#51606,.F.);
#73466=ORIENTED_EDGE('',*,*,#51591,.F.);
#73467=ORIENTED_EDGE('',*,*,#51606,.T.);
#73468=ORIENTED_EDGE('',*,*,#49876,.F.);
#73469=ORIENTED_EDGE('',*,*,#51607,.F.);
#73470=ORIENTED_EDGE('',*,*,#51582,.F.);
#73471=ORIENTED_EDGE('',*,*,#51608,.T.);
#73472=ORIENTED_EDGE('',*,*,#51583,.F.);
#73473=ORIENTED_EDGE('',*,*,#51607,.T.);
#73474=ORIENTED_EDGE('',*,*,#50804,.F.);
#73475=ORIENTED_EDGE('',*,*,#51609,.T.);
#73476=ORIENTED_EDGE('',*,*,#51584,.F.);
#73477=ORIENTED_EDGE('',*,*,#51608,.F.);
#73478=ORIENTED_EDGE('',*,*,#50652,.F.);
#73479=ORIENTED_EDGE('',*,*,#51601,.T.);
#73480=ORIENTED_EDGE('',*,*,#51597,.T.);
#73481=ORIENTED_EDGE('',*,*,#51609,.F.);
#73482=ORIENTED_EDGE('',*,*,#50651,.T.);
#73483=ORIENTED_EDGE('',*,*,#51595,.T.);
#73484=ORIENTED_EDGE('',*,*,#51598,.T.);
#73485=ORIENTED_EDGE('',*,*,#51600,.T.);
#73486=ORIENTED_EDGE('',*,*,#51610,.T.);
#73487=ORIENTED_EDGE('',*,*,#51611,.T.);
#73488=ORIENTED_EDGE('',*,*,#51612,.T.);
#73489=ORIENTED_EDGE('',*,*,#51613,.T.);
#73490=ORIENTED_EDGE('',*,*,#51614,.T.);
#73491=ORIENTED_EDGE('',*,*,#51615,.T.);
#73492=ORIENTED_EDGE('',*,*,#51616,.T.);
#73493=ORIENTED_EDGE('',*,*,#51617,.F.);
#73494=ORIENTED_EDGE('',*,*,#51618,.T.);
#73495=ORIENTED_EDGE('',*,*,#51619,.T.);
#73496=ORIENTED_EDGE('',*,*,#51617,.T.);
#73497=ORIENTED_EDGE('',*,*,#51620,.T.);
#73498=ORIENTED_EDGE('',*,*,#51610,.F.);
#73499=ORIENTED_EDGE('',*,*,#51621,.T.);
#73500=ORIENTED_EDGE('',*,*,#51622,.F.);
#73501=ORIENTED_EDGE('',*,*,#51618,.F.);
#73502=ORIENTED_EDGE('',*,*,#51623,.F.);
#73503=ORIENTED_EDGE('',*,*,#51624,.F.);
#73504=ORIENTED_EDGE('',*,*,#51623,.T.);
#73505=ORIENTED_EDGE('',*,*,#51621,.F.);
#73506=ORIENTED_EDGE('',*,*,#51625,.F.);
#73507=ORIENTED_EDGE('',*,*,#51625,.T.);
#73508=ORIENTED_EDGE('',*,*,#51614,.F.);
#73509=ORIENTED_EDGE('',*,*,#51626,.F.);
#73510=ORIENTED_EDGE('',*,*,#51627,.F.);
#73511=ORIENTED_EDGE('',*,*,#51628,.T.);
#73512=ORIENTED_EDGE('',*,*,#51629,.F.);
#73513=ORIENTED_EDGE('',*,*,#51630,.F.);
#73514=ORIENTED_EDGE('',*,*,#50656,.F.);
#73515=ORIENTED_EDGE('',*,*,#51631,.T.);
#73516=ORIENTED_EDGE('',*,*,#51622,.T.);
#73517=ORIENTED_EDGE('',*,*,#51628,.F.);
#73518=ORIENTED_EDGE('',*,*,#50655,.T.);
#73519=ORIENTED_EDGE('',*,*,#51632,.F.);
#73520=ORIENTED_EDGE('',*,*,#51619,.F.);
#73521=ORIENTED_EDGE('',*,*,#51631,.F.);
#73522=ORIENTED_EDGE('',*,*,#50654,.F.);
#73523=ORIENTED_EDGE('',*,*,#51632,.T.);
#73524=ORIENTED_EDGE('',*,*,#50803,.F.);
#73525=ORIENTED_EDGE('',*,*,#51633,.F.);
#73526=ORIENTED_EDGE('',*,*,#51615,.F.);
#73527=ORIENTED_EDGE('',*,*,#51633,.T.);
#73528=ORIENTED_EDGE('',*,*,#49874,.F.);
#73529=ORIENTED_EDGE('',*,*,#51634,.F.);
#73530=ORIENTED_EDGE('',*,*,#51616,.F.);
#73531=ORIENTED_EDGE('',*,*,#51634,.T.);
#73532=ORIENTED_EDGE('',*,*,#49873,.F.);
#73533=ORIENTED_EDGE('',*,*,#51635,.F.);
#73534=ORIENTED_EDGE('',*,*,#51620,.F.);
#73535=ORIENTED_EDGE('',*,*,#51635,.T.);
#73536=ORIENTED_EDGE('',*,*,#49872,.F.);
#73537=ORIENTED_EDGE('',*,*,#51636,.F.);
#73538=ORIENTED_EDGE('',*,*,#51611,.F.);
#73539=ORIENTED_EDGE('',*,*,#51637,.T.);
#73540=ORIENTED_EDGE('',*,*,#51612,.F.);
#73541=ORIENTED_EDGE('',*,*,#51636,.T.);
#73542=ORIENTED_EDGE('',*,*,#50659,.F.);
#73543=ORIENTED_EDGE('',*,*,#51638,.T.);
#73544=ORIENTED_EDGE('',*,*,#51613,.F.);
#73545=ORIENTED_EDGE('',*,*,#51637,.F.);
#73546=ORIENTED_EDGE('',*,*,#50658,.F.);
#73547=ORIENTED_EDGE('',*,*,#51630,.T.);
#73548=ORIENTED_EDGE('',*,*,#51626,.T.);
#73549=ORIENTED_EDGE('',*,*,#51638,.F.);
#73550=ORIENTED_EDGE('',*,*,#50657,.T.);
#73551=ORIENTED_EDGE('',*,*,#51624,.T.);
#73552=ORIENTED_EDGE('',*,*,#51627,.T.);
#73553=ORIENTED_EDGE('',*,*,#51629,.T.);
#73554=ORIENTED_EDGE('',*,*,#51639,.T.);
#73555=ORIENTED_EDGE('',*,*,#51640,.T.);
#73556=ORIENTED_EDGE('',*,*,#51641,.T.);
#73557=ORIENTED_EDGE('',*,*,#51642,.T.);
#73558=ORIENTED_EDGE('',*,*,#51643,.T.);
#73559=ORIENTED_EDGE('',*,*,#51644,.T.);
#73560=ORIENTED_EDGE('',*,*,#51645,.T.);
#73561=ORIENTED_EDGE('',*,*,#51646,.F.);
#73562=ORIENTED_EDGE('',*,*,#51647,.T.);
#73563=ORIENTED_EDGE('',*,*,#51648,.T.);
#73564=ORIENTED_EDGE('',*,*,#51646,.T.);
#73565=ORIENTED_EDGE('',*,*,#51649,.T.);
#73566=ORIENTED_EDGE('',*,*,#51639,.F.);
#73567=ORIENTED_EDGE('',*,*,#51650,.T.);
#73568=ORIENTED_EDGE('',*,*,#51651,.F.);
#73569=ORIENTED_EDGE('',*,*,#51647,.F.);
#73570=ORIENTED_EDGE('',*,*,#51652,.F.);
#73571=ORIENTED_EDGE('',*,*,#51653,.F.);
#73572=ORIENTED_EDGE('',*,*,#51652,.T.);
#73573=ORIENTED_EDGE('',*,*,#51650,.F.);
#73574=ORIENTED_EDGE('',*,*,#51654,.F.);
#73575=ORIENTED_EDGE('',*,*,#51654,.T.);
#73576=ORIENTED_EDGE('',*,*,#51643,.F.);
#73577=ORIENTED_EDGE('',*,*,#51655,.F.);
#73578=ORIENTED_EDGE('',*,*,#51656,.F.);
#73579=ORIENTED_EDGE('',*,*,#51657,.T.);
#73580=ORIENTED_EDGE('',*,*,#51658,.F.);
#73581=ORIENTED_EDGE('',*,*,#51659,.F.);
#73582=ORIENTED_EDGE('',*,*,#50072,.F.);
#73583=ORIENTED_EDGE('',*,*,#51660,.T.);
#73584=ORIENTED_EDGE('',*,*,#51651,.T.);
#73585=ORIENTED_EDGE('',*,*,#51657,.F.);
#73586=ORIENTED_EDGE('',*,*,#50071,.T.);
#73587=ORIENTED_EDGE('',*,*,#51661,.F.);
#73588=ORIENTED_EDGE('',*,*,#51648,.F.);
#73589=ORIENTED_EDGE('',*,*,#51660,.F.);
#73590=ORIENTED_EDGE('',*,*,#50070,.F.);
#73591=ORIENTED_EDGE('',*,*,#51661,.T.);
#73592=ORIENTED_EDGE('',*,*,#50660,.F.);
#73593=ORIENTED_EDGE('',*,*,#51662,.F.);
#73594=ORIENTED_EDGE('',*,*,#51644,.F.);
#73595=ORIENTED_EDGE('',*,*,#51662,.T.);
#73596=ORIENTED_EDGE('',*,*,#49866,.F.);
#73597=ORIENTED_EDGE('',*,*,#51663,.F.);
#73598=ORIENTED_EDGE('',*,*,#51645,.F.);
#73599=ORIENTED_EDGE('',*,*,#51663,.T.);
#73600=ORIENTED_EDGE('',*,*,#49865,.F.);
#73601=ORIENTED_EDGE('',*,*,#51664,.F.);
#73602=ORIENTED_EDGE('',*,*,#51649,.F.);
#73603=ORIENTED_EDGE('',*,*,#51664,.T.);
#73604=ORIENTED_EDGE('',*,*,#49864,.F.);
#73605=ORIENTED_EDGE('',*,*,#51665,.F.);
#73606=ORIENTED_EDGE('',*,*,#51640,.F.);
#73607=ORIENTED_EDGE('',*,*,#51666,.T.);
#73608=ORIENTED_EDGE('',*,*,#51641,.F.);
#73609=ORIENTED_EDGE('',*,*,#51665,.T.);
#73610=ORIENTED_EDGE('',*,*,#50802,.F.);
#73611=ORIENTED_EDGE('',*,*,#51667,.T.);
#73612=ORIENTED_EDGE('',*,*,#51642,.F.);
#73613=ORIENTED_EDGE('',*,*,#51666,.F.);
#73614=ORIENTED_EDGE('',*,*,#50074,.F.);
#73615=ORIENTED_EDGE('',*,*,#51659,.T.);
#73616=ORIENTED_EDGE('',*,*,#51655,.T.);
#73617=ORIENTED_EDGE('',*,*,#51667,.F.);
#73618=ORIENTED_EDGE('',*,*,#50073,.T.);
#73619=ORIENTED_EDGE('',*,*,#51653,.T.);
#73620=ORIENTED_EDGE('',*,*,#51656,.T.);
#73621=ORIENTED_EDGE('',*,*,#51658,.T.);
#73622=ORIENTED_EDGE('',*,*,#51668,.T.);
#73623=ORIENTED_EDGE('',*,*,#51669,.T.);
#73624=ORIENTED_EDGE('',*,*,#51670,.T.);
#73625=ORIENTED_EDGE('',*,*,#51671,.T.);
#73626=ORIENTED_EDGE('',*,*,#51672,.T.);
#73627=ORIENTED_EDGE('',*,*,#51673,.T.);
#73628=ORIENTED_EDGE('',*,*,#51674,.T.);
#73629=ORIENTED_EDGE('',*,*,#51675,.F.);
#73630=ORIENTED_EDGE('',*,*,#51676,.T.);
#73631=ORIENTED_EDGE('',*,*,#51677,.T.);
#73632=ORIENTED_EDGE('',*,*,#51675,.T.);
#73633=ORIENTED_EDGE('',*,*,#51678,.T.);
#73634=ORIENTED_EDGE('',*,*,#51668,.F.);
#73635=ORIENTED_EDGE('',*,*,#51679,.T.);
#73636=ORIENTED_EDGE('',*,*,#51680,.F.);
#73637=ORIENTED_EDGE('',*,*,#51676,.F.);
#73638=ORIENTED_EDGE('',*,*,#51681,.F.);
#73639=ORIENTED_EDGE('',*,*,#51682,.F.);
#73640=ORIENTED_EDGE('',*,*,#51681,.T.);
#73641=ORIENTED_EDGE('',*,*,#51679,.F.);
#73642=ORIENTED_EDGE('',*,*,#51683,.F.);
#73643=ORIENTED_EDGE('',*,*,#51683,.T.);
#73644=ORIENTED_EDGE('',*,*,#51672,.F.);
#73645=ORIENTED_EDGE('',*,*,#51684,.F.);
#73646=ORIENTED_EDGE('',*,*,#51685,.F.);
#73647=ORIENTED_EDGE('',*,*,#51686,.T.);
#73648=ORIENTED_EDGE('',*,*,#51687,.F.);
#73649=ORIENTED_EDGE('',*,*,#51688,.F.);
#73650=ORIENTED_EDGE('',*,*,#50078,.F.);
#73651=ORIENTED_EDGE('',*,*,#51689,.T.);
#73652=ORIENTED_EDGE('',*,*,#51680,.T.);
#73653=ORIENTED_EDGE('',*,*,#51686,.F.);
#73654=ORIENTED_EDGE('',*,*,#50077,.T.);
#73655=ORIENTED_EDGE('',*,*,#51690,.F.);
#73656=ORIENTED_EDGE('',*,*,#51677,.F.);
#73657=ORIENTED_EDGE('',*,*,#51689,.F.);
#73658=ORIENTED_EDGE('',*,*,#50076,.F.);
#73659=ORIENTED_EDGE('',*,*,#51690,.T.);
#73660=ORIENTED_EDGE('',*,*,#50801,.F.);
#73661=ORIENTED_EDGE('',*,*,#51691,.F.);
#73662=ORIENTED_EDGE('',*,*,#51673,.F.);
#73663=ORIENTED_EDGE('',*,*,#51691,.T.);
#73664=ORIENTED_EDGE('',*,*,#49862,.F.);
#73665=ORIENTED_EDGE('',*,*,#51692,.F.);
#73666=ORIENTED_EDGE('',*,*,#51674,.F.);
#73667=ORIENTED_EDGE('',*,*,#51692,.T.);
#73668=ORIENTED_EDGE('',*,*,#49861,.F.);
#73669=ORIENTED_EDGE('',*,*,#51693,.F.);
#73670=ORIENTED_EDGE('',*,*,#51678,.F.);
#73671=ORIENTED_EDGE('',*,*,#51693,.T.);
#73672=ORIENTED_EDGE('',*,*,#49860,.F.);
#73673=ORIENTED_EDGE('',*,*,#51694,.F.);
#73674=ORIENTED_EDGE('',*,*,#51669,.F.);
#73675=ORIENTED_EDGE('',*,*,#51695,.T.);
#73676=ORIENTED_EDGE('',*,*,#51670,.F.);
#73677=ORIENTED_EDGE('',*,*,#51694,.T.);
#73678=ORIENTED_EDGE('',*,*,#50800,.F.);
#73679=ORIENTED_EDGE('',*,*,#51696,.T.);
#73680=ORIENTED_EDGE('',*,*,#51671,.F.);
#73681=ORIENTED_EDGE('',*,*,#51695,.F.);
#73682=ORIENTED_EDGE('',*,*,#50080,.F.);
#73683=ORIENTED_EDGE('',*,*,#51688,.T.);
#73684=ORIENTED_EDGE('',*,*,#51684,.T.);
#73685=ORIENTED_EDGE('',*,*,#51696,.F.);
#73686=ORIENTED_EDGE('',*,*,#50079,.T.);
#73687=ORIENTED_EDGE('',*,*,#51682,.T.);
#73688=ORIENTED_EDGE('',*,*,#51685,.T.);
#73689=ORIENTED_EDGE('',*,*,#51687,.T.);
#73690=ORIENTED_EDGE('',*,*,#51697,.T.);
#73691=ORIENTED_EDGE('',*,*,#51698,.T.);
#73692=ORIENTED_EDGE('',*,*,#51699,.T.);
#73693=ORIENTED_EDGE('',*,*,#51700,.T.);
#73694=ORIENTED_EDGE('',*,*,#51701,.T.);
#73695=ORIENTED_EDGE('',*,*,#51702,.T.);
#73696=ORIENTED_EDGE('',*,*,#51703,.T.);
#73697=ORIENTED_EDGE('',*,*,#51704,.F.);
#73698=ORIENTED_EDGE('',*,*,#51705,.T.);
#73699=ORIENTED_EDGE('',*,*,#51706,.T.);
#73700=ORIENTED_EDGE('',*,*,#51704,.T.);
#73701=ORIENTED_EDGE('',*,*,#51707,.T.);
#73702=ORIENTED_EDGE('',*,*,#51697,.F.);
#73703=ORIENTED_EDGE('',*,*,#51708,.T.);
#73704=ORIENTED_EDGE('',*,*,#51709,.F.);
#73705=ORIENTED_EDGE('',*,*,#51705,.F.);
#73706=ORIENTED_EDGE('',*,*,#51710,.F.);
#73707=ORIENTED_EDGE('',*,*,#51711,.F.);
#73708=ORIENTED_EDGE('',*,*,#51710,.T.);
#73709=ORIENTED_EDGE('',*,*,#51708,.F.);
#73710=ORIENTED_EDGE('',*,*,#51712,.F.);
#73711=ORIENTED_EDGE('',*,*,#51712,.T.);
#73712=ORIENTED_EDGE('',*,*,#51701,.F.);
#73713=ORIENTED_EDGE('',*,*,#51713,.F.);
#73714=ORIENTED_EDGE('',*,*,#51714,.F.);
#73715=ORIENTED_EDGE('',*,*,#51715,.T.);
#73716=ORIENTED_EDGE('',*,*,#51716,.F.);
#73717=ORIENTED_EDGE('',*,*,#51717,.F.);
#73718=ORIENTED_EDGE('',*,*,#50084,.F.);
#73719=ORIENTED_EDGE('',*,*,#51718,.T.);
#73720=ORIENTED_EDGE('',*,*,#51709,.T.);
#73721=ORIENTED_EDGE('',*,*,#51715,.F.);
#73722=ORIENTED_EDGE('',*,*,#50083,.T.);
#73723=ORIENTED_EDGE('',*,*,#51719,.F.);
#73724=ORIENTED_EDGE('',*,*,#51706,.F.);
#73725=ORIENTED_EDGE('',*,*,#51718,.F.);
#73726=ORIENTED_EDGE('',*,*,#50082,.F.);
#73727=ORIENTED_EDGE('',*,*,#51719,.T.);
#73728=ORIENTED_EDGE('',*,*,#50799,.F.);
#73729=ORIENTED_EDGE('',*,*,#51720,.F.);
#73730=ORIENTED_EDGE('',*,*,#51702,.F.);
#73731=ORIENTED_EDGE('',*,*,#51720,.T.);
#73732=ORIENTED_EDGE('',*,*,#49858,.F.);
#73733=ORIENTED_EDGE('',*,*,#51721,.F.);
#73734=ORIENTED_EDGE('',*,*,#51703,.F.);
#73735=ORIENTED_EDGE('',*,*,#51721,.T.);
#73736=ORIENTED_EDGE('',*,*,#49857,.F.);
#73737=ORIENTED_EDGE('',*,*,#51722,.F.);
#73738=ORIENTED_EDGE('',*,*,#51707,.F.);
#73739=ORIENTED_EDGE('',*,*,#51722,.T.);
#73740=ORIENTED_EDGE('',*,*,#49856,.F.);
#73741=ORIENTED_EDGE('',*,*,#51723,.F.);
#73742=ORIENTED_EDGE('',*,*,#51698,.F.);
#73743=ORIENTED_EDGE('',*,*,#51724,.T.);
#73744=ORIENTED_EDGE('',*,*,#51699,.F.);
#73745=ORIENTED_EDGE('',*,*,#51723,.T.);
#73746=ORIENTED_EDGE('',*,*,#50798,.F.);
#73747=ORIENTED_EDGE('',*,*,#51725,.T.);
#73748=ORIENTED_EDGE('',*,*,#51700,.F.);
#73749=ORIENTED_EDGE('',*,*,#51724,.F.);
#73750=ORIENTED_EDGE('',*,*,#50086,.F.);
#73751=ORIENTED_EDGE('',*,*,#51717,.T.);
#73752=ORIENTED_EDGE('',*,*,#51713,.T.);
#73753=ORIENTED_EDGE('',*,*,#51725,.F.);
#73754=ORIENTED_EDGE('',*,*,#50085,.T.);
#73755=ORIENTED_EDGE('',*,*,#51711,.T.);
#73756=ORIENTED_EDGE('',*,*,#51714,.T.);
#73757=ORIENTED_EDGE('',*,*,#51716,.T.);
#73758=ORIENTED_EDGE('',*,*,#51726,.T.);
#73759=ORIENTED_EDGE('',*,*,#51727,.T.);
#73760=ORIENTED_EDGE('',*,*,#51728,.T.);
#73761=ORIENTED_EDGE('',*,*,#51729,.T.);
#73762=ORIENTED_EDGE('',*,*,#51730,.T.);
#73763=ORIENTED_EDGE('',*,*,#51731,.T.);
#73764=ORIENTED_EDGE('',*,*,#51732,.T.);
#73765=ORIENTED_EDGE('',*,*,#51733,.F.);
#73766=ORIENTED_EDGE('',*,*,#51734,.T.);
#73767=ORIENTED_EDGE('',*,*,#51735,.T.);
#73768=ORIENTED_EDGE('',*,*,#51733,.T.);
#73769=ORIENTED_EDGE('',*,*,#51736,.T.);
#73770=ORIENTED_EDGE('',*,*,#51726,.F.);
#73771=ORIENTED_EDGE('',*,*,#51737,.T.);
#73772=ORIENTED_EDGE('',*,*,#51738,.F.);
#73773=ORIENTED_EDGE('',*,*,#51734,.F.);
#73774=ORIENTED_EDGE('',*,*,#51739,.F.);
#73775=ORIENTED_EDGE('',*,*,#51740,.F.);
#73776=ORIENTED_EDGE('',*,*,#51739,.T.);
#73777=ORIENTED_EDGE('',*,*,#51737,.F.);
#73778=ORIENTED_EDGE('',*,*,#51741,.F.);
#73779=ORIENTED_EDGE('',*,*,#51741,.T.);
#73780=ORIENTED_EDGE('',*,*,#51730,.F.);
#73781=ORIENTED_EDGE('',*,*,#51742,.F.);
#73782=ORIENTED_EDGE('',*,*,#51743,.F.);
#73783=ORIENTED_EDGE('',*,*,#51744,.T.);
#73784=ORIENTED_EDGE('',*,*,#51745,.F.);
#73785=ORIENTED_EDGE('',*,*,#51746,.F.);
#73786=ORIENTED_EDGE('',*,*,#50090,.F.);
#73787=ORIENTED_EDGE('',*,*,#51747,.T.);
#73788=ORIENTED_EDGE('',*,*,#51738,.T.);
#73789=ORIENTED_EDGE('',*,*,#51744,.F.);
#73790=ORIENTED_EDGE('',*,*,#50089,.T.);
#73791=ORIENTED_EDGE('',*,*,#51748,.F.);
#73792=ORIENTED_EDGE('',*,*,#51735,.F.);
#73793=ORIENTED_EDGE('',*,*,#51747,.F.);
#73794=ORIENTED_EDGE('',*,*,#50088,.F.);
#73795=ORIENTED_EDGE('',*,*,#51748,.T.);
#73796=ORIENTED_EDGE('',*,*,#50797,.F.);
#73797=ORIENTED_EDGE('',*,*,#51749,.F.);
#73798=ORIENTED_EDGE('',*,*,#51731,.F.);
#73799=ORIENTED_EDGE('',*,*,#51749,.T.);
#73800=ORIENTED_EDGE('',*,*,#49854,.F.);
#73801=ORIENTED_EDGE('',*,*,#51750,.F.);
#73802=ORIENTED_EDGE('',*,*,#51732,.F.);
#73803=ORIENTED_EDGE('',*,*,#51750,.T.);
#73804=ORIENTED_EDGE('',*,*,#49853,.F.);
#73805=ORIENTED_EDGE('',*,*,#51751,.F.);
#73806=ORIENTED_EDGE('',*,*,#51736,.F.);
#73807=ORIENTED_EDGE('',*,*,#51751,.T.);
#73808=ORIENTED_EDGE('',*,*,#49852,.F.);
#73809=ORIENTED_EDGE('',*,*,#51752,.F.);
#73810=ORIENTED_EDGE('',*,*,#51727,.F.);
#73811=ORIENTED_EDGE('',*,*,#51753,.T.);
#73812=ORIENTED_EDGE('',*,*,#51728,.F.);
#73813=ORIENTED_EDGE('',*,*,#51752,.T.);
#73814=ORIENTED_EDGE('',*,*,#50796,.F.);
#73815=ORIENTED_EDGE('',*,*,#51754,.T.);
#73816=ORIENTED_EDGE('',*,*,#51729,.F.);
#73817=ORIENTED_EDGE('',*,*,#51753,.F.);
#73818=ORIENTED_EDGE('',*,*,#50092,.F.);
#73819=ORIENTED_EDGE('',*,*,#51746,.T.);
#73820=ORIENTED_EDGE('',*,*,#51742,.T.);
#73821=ORIENTED_EDGE('',*,*,#51754,.F.);
#73822=ORIENTED_EDGE('',*,*,#50091,.T.);
#73823=ORIENTED_EDGE('',*,*,#51740,.T.);
#73824=ORIENTED_EDGE('',*,*,#51743,.T.);
#73825=ORIENTED_EDGE('',*,*,#51745,.T.);
#73826=ORIENTED_EDGE('',*,*,#51755,.T.);
#73827=ORIENTED_EDGE('',*,*,#51756,.T.);
#73828=ORIENTED_EDGE('',*,*,#51757,.T.);
#73829=ORIENTED_EDGE('',*,*,#51758,.T.);
#73830=ORIENTED_EDGE('',*,*,#51759,.T.);
#73831=ORIENTED_EDGE('',*,*,#51760,.T.);
#73832=ORIENTED_EDGE('',*,*,#51761,.T.);
#73833=ORIENTED_EDGE('',*,*,#51762,.F.);
#73834=ORIENTED_EDGE('',*,*,#51763,.T.);
#73835=ORIENTED_EDGE('',*,*,#51764,.T.);
#73836=ORIENTED_EDGE('',*,*,#51762,.T.);
#73837=ORIENTED_EDGE('',*,*,#51765,.T.);
#73838=ORIENTED_EDGE('',*,*,#51755,.F.);
#73839=ORIENTED_EDGE('',*,*,#51766,.T.);
#73840=ORIENTED_EDGE('',*,*,#51767,.F.);
#73841=ORIENTED_EDGE('',*,*,#51763,.F.);
#73842=ORIENTED_EDGE('',*,*,#51768,.F.);
#73843=ORIENTED_EDGE('',*,*,#51769,.F.);
#73844=ORIENTED_EDGE('',*,*,#51768,.T.);
#73845=ORIENTED_EDGE('',*,*,#51766,.F.);
#73846=ORIENTED_EDGE('',*,*,#51770,.F.);
#73847=ORIENTED_EDGE('',*,*,#51770,.T.);
#73848=ORIENTED_EDGE('',*,*,#51759,.F.);
#73849=ORIENTED_EDGE('',*,*,#51771,.F.);
#73850=ORIENTED_EDGE('',*,*,#51772,.F.);
#73851=ORIENTED_EDGE('',*,*,#51773,.T.);
#73852=ORIENTED_EDGE('',*,*,#51774,.F.);
#73853=ORIENTED_EDGE('',*,*,#51775,.F.);
#73854=ORIENTED_EDGE('',*,*,#50096,.F.);
#73855=ORIENTED_EDGE('',*,*,#51776,.T.);
#73856=ORIENTED_EDGE('',*,*,#51767,.T.);
#73857=ORIENTED_EDGE('',*,*,#51773,.F.);
#73858=ORIENTED_EDGE('',*,*,#50095,.T.);
#73859=ORIENTED_EDGE('',*,*,#51777,.F.);
#73860=ORIENTED_EDGE('',*,*,#51764,.F.);
#73861=ORIENTED_EDGE('',*,*,#51776,.F.);
#73862=ORIENTED_EDGE('',*,*,#50094,.F.);
#73863=ORIENTED_EDGE('',*,*,#51777,.T.);
#73864=ORIENTED_EDGE('',*,*,#50795,.F.);
#73865=ORIENTED_EDGE('',*,*,#51778,.F.);
#73866=ORIENTED_EDGE('',*,*,#51760,.F.);
#73867=ORIENTED_EDGE('',*,*,#51778,.T.);
#73868=ORIENTED_EDGE('',*,*,#49850,.F.);
#73869=ORIENTED_EDGE('',*,*,#51779,.F.);
#73870=ORIENTED_EDGE('',*,*,#51761,.F.);
#73871=ORIENTED_EDGE('',*,*,#51779,.T.);
#73872=ORIENTED_EDGE('',*,*,#49849,.F.);
#73873=ORIENTED_EDGE('',*,*,#51780,.F.);
#73874=ORIENTED_EDGE('',*,*,#51765,.F.);
#73875=ORIENTED_EDGE('',*,*,#51780,.T.);
#73876=ORIENTED_EDGE('',*,*,#49848,.F.);
#73877=ORIENTED_EDGE('',*,*,#51781,.F.);
#73878=ORIENTED_EDGE('',*,*,#51756,.F.);
#73879=ORIENTED_EDGE('',*,*,#51782,.T.);
#73880=ORIENTED_EDGE('',*,*,#51757,.F.);
#73881=ORIENTED_EDGE('',*,*,#51781,.T.);
#73882=ORIENTED_EDGE('',*,*,#50794,.F.);
#73883=ORIENTED_EDGE('',*,*,#51783,.T.);
#73884=ORIENTED_EDGE('',*,*,#51758,.F.);
#73885=ORIENTED_EDGE('',*,*,#51782,.F.);
#73886=ORIENTED_EDGE('',*,*,#50098,.F.);
#73887=ORIENTED_EDGE('',*,*,#51775,.T.);
#73888=ORIENTED_EDGE('',*,*,#51771,.T.);
#73889=ORIENTED_EDGE('',*,*,#51783,.F.);
#73890=ORIENTED_EDGE('',*,*,#50097,.T.);
#73891=ORIENTED_EDGE('',*,*,#51769,.T.);
#73892=ORIENTED_EDGE('',*,*,#51772,.T.);
#73893=ORIENTED_EDGE('',*,*,#51774,.T.);
#73894=ORIENTED_EDGE('',*,*,#51784,.T.);
#73895=ORIENTED_EDGE('',*,*,#51785,.T.);
#73896=ORIENTED_EDGE('',*,*,#51786,.T.);
#73897=ORIENTED_EDGE('',*,*,#51787,.T.);
#73898=ORIENTED_EDGE('',*,*,#51788,.T.);
#73899=ORIENTED_EDGE('',*,*,#51789,.T.);
#73900=ORIENTED_EDGE('',*,*,#51790,.T.);
#73901=ORIENTED_EDGE('',*,*,#51791,.F.);
#73902=ORIENTED_EDGE('',*,*,#51792,.T.);
#73903=ORIENTED_EDGE('',*,*,#51793,.T.);
#73904=ORIENTED_EDGE('',*,*,#51791,.T.);
#73905=ORIENTED_EDGE('',*,*,#51794,.T.);
#73906=ORIENTED_EDGE('',*,*,#51784,.F.);
#73907=ORIENTED_EDGE('',*,*,#51795,.T.);
#73908=ORIENTED_EDGE('',*,*,#51796,.F.);
#73909=ORIENTED_EDGE('',*,*,#51792,.F.);
#73910=ORIENTED_EDGE('',*,*,#51797,.F.);
#73911=ORIENTED_EDGE('',*,*,#51798,.F.);
#73912=ORIENTED_EDGE('',*,*,#51797,.T.);
#73913=ORIENTED_EDGE('',*,*,#51795,.F.);
#73914=ORIENTED_EDGE('',*,*,#51799,.F.);
#73915=ORIENTED_EDGE('',*,*,#51799,.T.);
#73916=ORIENTED_EDGE('',*,*,#51788,.F.);
#73917=ORIENTED_EDGE('',*,*,#51800,.F.);
#73918=ORIENTED_EDGE('',*,*,#51801,.F.);
#73919=ORIENTED_EDGE('',*,*,#51802,.T.);
#73920=ORIENTED_EDGE('',*,*,#51803,.F.);
#73921=ORIENTED_EDGE('',*,*,#51804,.F.);
#73922=ORIENTED_EDGE('',*,*,#50102,.F.);
#73923=ORIENTED_EDGE('',*,*,#51805,.T.);
#73924=ORIENTED_EDGE('',*,*,#51796,.T.);
#73925=ORIENTED_EDGE('',*,*,#51802,.F.);
#73926=ORIENTED_EDGE('',*,*,#50101,.T.);
#73927=ORIENTED_EDGE('',*,*,#51806,.F.);
#73928=ORIENTED_EDGE('',*,*,#51793,.F.);
#73929=ORIENTED_EDGE('',*,*,#51805,.F.);
#73930=ORIENTED_EDGE('',*,*,#50100,.F.);
#73931=ORIENTED_EDGE('',*,*,#51806,.T.);
#73932=ORIENTED_EDGE('',*,*,#50793,.F.);
#73933=ORIENTED_EDGE('',*,*,#51807,.F.);
#73934=ORIENTED_EDGE('',*,*,#51789,.F.);
#73935=ORIENTED_EDGE('',*,*,#51807,.T.);
#73936=ORIENTED_EDGE('',*,*,#49846,.F.);
#73937=ORIENTED_EDGE('',*,*,#51808,.F.);
#73938=ORIENTED_EDGE('',*,*,#51790,.F.);
#73939=ORIENTED_EDGE('',*,*,#51808,.T.);
#73940=ORIENTED_EDGE('',*,*,#49845,.F.);
#73941=ORIENTED_EDGE('',*,*,#51809,.F.);
#73942=ORIENTED_EDGE('',*,*,#51794,.F.);
#73943=ORIENTED_EDGE('',*,*,#51809,.T.);
#73944=ORIENTED_EDGE('',*,*,#49844,.F.);
#73945=ORIENTED_EDGE('',*,*,#51810,.F.);
#73946=ORIENTED_EDGE('',*,*,#51785,.F.);
#73947=ORIENTED_EDGE('',*,*,#51811,.T.);
#73948=ORIENTED_EDGE('',*,*,#51786,.F.);
#73949=ORIENTED_EDGE('',*,*,#51810,.T.);
#73950=ORIENTED_EDGE('',*,*,#50792,.F.);
#73951=ORIENTED_EDGE('',*,*,#51812,.T.);
#73952=ORIENTED_EDGE('',*,*,#51787,.F.);
#73953=ORIENTED_EDGE('',*,*,#51811,.F.);
#73954=ORIENTED_EDGE('',*,*,#50104,.F.);
#73955=ORIENTED_EDGE('',*,*,#51804,.T.);
#73956=ORIENTED_EDGE('',*,*,#51800,.T.);
#73957=ORIENTED_EDGE('',*,*,#51812,.F.);
#73958=ORIENTED_EDGE('',*,*,#50103,.T.);
#73959=ORIENTED_EDGE('',*,*,#51798,.T.);
#73960=ORIENTED_EDGE('',*,*,#51801,.T.);
#73961=ORIENTED_EDGE('',*,*,#51803,.T.);
#73962=ORIENTED_EDGE('',*,*,#51813,.T.);
#73963=ORIENTED_EDGE('',*,*,#51814,.T.);
#73964=ORIENTED_EDGE('',*,*,#51815,.T.);
#73965=ORIENTED_EDGE('',*,*,#51816,.T.);
#73966=ORIENTED_EDGE('',*,*,#51817,.T.);
#73967=ORIENTED_EDGE('',*,*,#51818,.T.);
#73968=ORIENTED_EDGE('',*,*,#51819,.T.);
#73969=ORIENTED_EDGE('',*,*,#51820,.F.);
#73970=ORIENTED_EDGE('',*,*,#51821,.T.);
#73971=ORIENTED_EDGE('',*,*,#51822,.T.);
#73972=ORIENTED_EDGE('',*,*,#51820,.T.);
#73973=ORIENTED_EDGE('',*,*,#51823,.T.);
#73974=ORIENTED_EDGE('',*,*,#51813,.F.);
#73975=ORIENTED_EDGE('',*,*,#51824,.T.);
#73976=ORIENTED_EDGE('',*,*,#51825,.F.);
#73977=ORIENTED_EDGE('',*,*,#51821,.F.);
#73978=ORIENTED_EDGE('',*,*,#51826,.F.);
#73979=ORIENTED_EDGE('',*,*,#51827,.F.);
#73980=ORIENTED_EDGE('',*,*,#51826,.T.);
#73981=ORIENTED_EDGE('',*,*,#51824,.F.);
#73982=ORIENTED_EDGE('',*,*,#51828,.F.);
#73983=ORIENTED_EDGE('',*,*,#51828,.T.);
#73984=ORIENTED_EDGE('',*,*,#51817,.F.);
#73985=ORIENTED_EDGE('',*,*,#51829,.F.);
#73986=ORIENTED_EDGE('',*,*,#51830,.F.);
#73987=ORIENTED_EDGE('',*,*,#51831,.T.);
#73988=ORIENTED_EDGE('',*,*,#51832,.F.);
#73989=ORIENTED_EDGE('',*,*,#51833,.F.);
#73990=ORIENTED_EDGE('',*,*,#50108,.F.);
#73991=ORIENTED_EDGE('',*,*,#51834,.T.);
#73992=ORIENTED_EDGE('',*,*,#51825,.T.);
#73993=ORIENTED_EDGE('',*,*,#51831,.F.);
#73994=ORIENTED_EDGE('',*,*,#50107,.T.);
#73995=ORIENTED_EDGE('',*,*,#51835,.F.);
#73996=ORIENTED_EDGE('',*,*,#51822,.F.);
#73997=ORIENTED_EDGE('',*,*,#51834,.F.);
#73998=ORIENTED_EDGE('',*,*,#50106,.F.);
#73999=ORIENTED_EDGE('',*,*,#51835,.T.);
#74000=ORIENTED_EDGE('',*,*,#50791,.F.);
#74001=ORIENTED_EDGE('',*,*,#51836,.F.);
#74002=ORIENTED_EDGE('',*,*,#51818,.F.);
#74003=ORIENTED_EDGE('',*,*,#51836,.T.);
#74004=ORIENTED_EDGE('',*,*,#49842,.F.);
#74005=ORIENTED_EDGE('',*,*,#51837,.F.);
#74006=ORIENTED_EDGE('',*,*,#51819,.F.);
#74007=ORIENTED_EDGE('',*,*,#51837,.T.);
#74008=ORIENTED_EDGE('',*,*,#49841,.F.);
#74009=ORIENTED_EDGE('',*,*,#51838,.F.);
#74010=ORIENTED_EDGE('',*,*,#51823,.F.);
#74011=ORIENTED_EDGE('',*,*,#51838,.T.);
#74012=ORIENTED_EDGE('',*,*,#49840,.F.);
#74013=ORIENTED_EDGE('',*,*,#51839,.F.);
#74014=ORIENTED_EDGE('',*,*,#51814,.F.);
#74015=ORIENTED_EDGE('',*,*,#51840,.T.);
#74016=ORIENTED_EDGE('',*,*,#51815,.F.);
#74017=ORIENTED_EDGE('',*,*,#51839,.T.);
#74018=ORIENTED_EDGE('',*,*,#50790,.F.);
#74019=ORIENTED_EDGE('',*,*,#51841,.T.);
#74020=ORIENTED_EDGE('',*,*,#51816,.F.);
#74021=ORIENTED_EDGE('',*,*,#51840,.F.);
#74022=ORIENTED_EDGE('',*,*,#50110,.F.);
#74023=ORIENTED_EDGE('',*,*,#51833,.T.);
#74024=ORIENTED_EDGE('',*,*,#51829,.T.);
#74025=ORIENTED_EDGE('',*,*,#51841,.F.);
#74026=ORIENTED_EDGE('',*,*,#50109,.T.);
#74027=ORIENTED_EDGE('',*,*,#51827,.T.);
#74028=ORIENTED_EDGE('',*,*,#51830,.T.);
#74029=ORIENTED_EDGE('',*,*,#51832,.T.);
#74030=ORIENTED_EDGE('',*,*,#51842,.T.);
#74031=ORIENTED_EDGE('',*,*,#51843,.T.);
#74032=ORIENTED_EDGE('',*,*,#51844,.T.);
#74033=ORIENTED_EDGE('',*,*,#51845,.T.);
#74034=ORIENTED_EDGE('',*,*,#51846,.T.);
#74035=ORIENTED_EDGE('',*,*,#51847,.T.);
#74036=ORIENTED_EDGE('',*,*,#51848,.T.);
#74037=ORIENTED_EDGE('',*,*,#51849,.F.);
#74038=ORIENTED_EDGE('',*,*,#51850,.T.);
#74039=ORIENTED_EDGE('',*,*,#51851,.T.);
#74040=ORIENTED_EDGE('',*,*,#51849,.T.);
#74041=ORIENTED_EDGE('',*,*,#51852,.T.);
#74042=ORIENTED_EDGE('',*,*,#51842,.F.);
#74043=ORIENTED_EDGE('',*,*,#51853,.T.);
#74044=ORIENTED_EDGE('',*,*,#51854,.F.);
#74045=ORIENTED_EDGE('',*,*,#51850,.F.);
#74046=ORIENTED_EDGE('',*,*,#51855,.F.);
#74047=ORIENTED_EDGE('',*,*,#51856,.F.);
#74048=ORIENTED_EDGE('',*,*,#51855,.T.);
#74049=ORIENTED_EDGE('',*,*,#51853,.F.);
#74050=ORIENTED_EDGE('',*,*,#51857,.F.);
#74051=ORIENTED_EDGE('',*,*,#51857,.T.);
#74052=ORIENTED_EDGE('',*,*,#51846,.F.);
#74053=ORIENTED_EDGE('',*,*,#51858,.F.);
#74054=ORIENTED_EDGE('',*,*,#51859,.F.);
#74055=ORIENTED_EDGE('',*,*,#51860,.T.);
#74056=ORIENTED_EDGE('',*,*,#51861,.F.);
#74057=ORIENTED_EDGE('',*,*,#51862,.F.);
#74058=ORIENTED_EDGE('',*,*,#50114,.F.);
#74059=ORIENTED_EDGE('',*,*,#51863,.T.);
#74060=ORIENTED_EDGE('',*,*,#51854,.T.);
#74061=ORIENTED_EDGE('',*,*,#51860,.F.);
#74062=ORIENTED_EDGE('',*,*,#50113,.T.);
#74063=ORIENTED_EDGE('',*,*,#51864,.F.);
#74064=ORIENTED_EDGE('',*,*,#51851,.F.);
#74065=ORIENTED_EDGE('',*,*,#51863,.F.);
#74066=ORIENTED_EDGE('',*,*,#50112,.F.);
#74067=ORIENTED_EDGE('',*,*,#51864,.T.);
#74068=ORIENTED_EDGE('',*,*,#50789,.F.);
#74069=ORIENTED_EDGE('',*,*,#51865,.F.);
#74070=ORIENTED_EDGE('',*,*,#51847,.F.);
#74071=ORIENTED_EDGE('',*,*,#51865,.T.);
#74072=ORIENTED_EDGE('',*,*,#49838,.F.);
#74073=ORIENTED_EDGE('',*,*,#51866,.F.);
#74074=ORIENTED_EDGE('',*,*,#51848,.F.);
#74075=ORIENTED_EDGE('',*,*,#51866,.T.);
#74076=ORIENTED_EDGE('',*,*,#49837,.F.);
#74077=ORIENTED_EDGE('',*,*,#51867,.F.);
#74078=ORIENTED_EDGE('',*,*,#51852,.F.);
#74079=ORIENTED_EDGE('',*,*,#51867,.T.);
#74080=ORIENTED_EDGE('',*,*,#49836,.F.);
#74081=ORIENTED_EDGE('',*,*,#51868,.F.);
#74082=ORIENTED_EDGE('',*,*,#51843,.F.);
#74083=ORIENTED_EDGE('',*,*,#51869,.T.);
#74084=ORIENTED_EDGE('',*,*,#51844,.F.);
#74085=ORIENTED_EDGE('',*,*,#51868,.T.);
#74086=ORIENTED_EDGE('',*,*,#50662,.F.);
#74087=ORIENTED_EDGE('',*,*,#51870,.T.);
#74088=ORIENTED_EDGE('',*,*,#51845,.F.);
#74089=ORIENTED_EDGE('',*,*,#51869,.F.);
#74090=ORIENTED_EDGE('',*,*,#50116,.F.);
#74091=ORIENTED_EDGE('',*,*,#51862,.T.);
#74092=ORIENTED_EDGE('',*,*,#51858,.T.);
#74093=ORIENTED_EDGE('',*,*,#51870,.F.);
#74094=ORIENTED_EDGE('',*,*,#50115,.T.);
#74095=ORIENTED_EDGE('',*,*,#51856,.T.);
#74096=ORIENTED_EDGE('',*,*,#51859,.T.);
#74097=ORIENTED_EDGE('',*,*,#51861,.T.);
#74098=ORIENTED_EDGE('',*,*,#51871,.T.);
#74099=ORIENTED_EDGE('',*,*,#51872,.T.);
#74100=ORIENTED_EDGE('',*,*,#51873,.T.);
#74101=ORIENTED_EDGE('',*,*,#51874,.T.);
#74102=ORIENTED_EDGE('',*,*,#51875,.T.);
#74103=ORIENTED_EDGE('',*,*,#51876,.T.);
#74104=ORIENTED_EDGE('',*,*,#51877,.T.);
#74105=ORIENTED_EDGE('',*,*,#51878,.F.);
#74106=ORIENTED_EDGE('',*,*,#51879,.T.);
#74107=ORIENTED_EDGE('',*,*,#51880,.T.);
#74108=ORIENTED_EDGE('',*,*,#51878,.T.);
#74109=ORIENTED_EDGE('',*,*,#51881,.T.);
#74110=ORIENTED_EDGE('',*,*,#51871,.F.);
#74111=ORIENTED_EDGE('',*,*,#51882,.T.);
#74112=ORIENTED_EDGE('',*,*,#51883,.F.);
#74113=ORIENTED_EDGE('',*,*,#51879,.F.);
#74114=ORIENTED_EDGE('',*,*,#51884,.F.);
#74115=ORIENTED_EDGE('',*,*,#51885,.F.);
#74116=ORIENTED_EDGE('',*,*,#51884,.T.);
#74117=ORIENTED_EDGE('',*,*,#51882,.F.);
#74118=ORIENTED_EDGE('',*,*,#51886,.F.);
#74119=ORIENTED_EDGE('',*,*,#51886,.T.);
#74120=ORIENTED_EDGE('',*,*,#51875,.F.);
#74121=ORIENTED_EDGE('',*,*,#51887,.F.);
#74122=ORIENTED_EDGE('',*,*,#51888,.F.);
#74123=ORIENTED_EDGE('',*,*,#51889,.T.);
#74124=ORIENTED_EDGE('',*,*,#51890,.F.);
#74125=ORIENTED_EDGE('',*,*,#51891,.F.);
#74126=ORIENTED_EDGE('',*,*,#50500,.F.);
#74127=ORIENTED_EDGE('',*,*,#51892,.T.);
#74128=ORIENTED_EDGE('',*,*,#51883,.T.);
#74129=ORIENTED_EDGE('',*,*,#51889,.F.);
#74130=ORIENTED_EDGE('',*,*,#50499,.T.);
#74131=ORIENTED_EDGE('',*,*,#51893,.F.);
#74132=ORIENTED_EDGE('',*,*,#51880,.F.);
#74133=ORIENTED_EDGE('',*,*,#51892,.F.);
#74134=ORIENTED_EDGE('',*,*,#50498,.F.);
#74135=ORIENTED_EDGE('',*,*,#51893,.T.);
#74136=ORIENTED_EDGE('',*,*,#50788,.F.);
#74137=ORIENTED_EDGE('',*,*,#51894,.F.);
#74138=ORIENTED_EDGE('',*,*,#51876,.F.);
#74139=ORIENTED_EDGE('',*,*,#51894,.T.);
#74140=ORIENTED_EDGE('',*,*,#49978,.F.);
#74141=ORIENTED_EDGE('',*,*,#51895,.F.);
#74142=ORIENTED_EDGE('',*,*,#51877,.F.);
#74143=ORIENTED_EDGE('',*,*,#51895,.T.);
#74144=ORIENTED_EDGE('',*,*,#49977,.F.);
#74145=ORIENTED_EDGE('',*,*,#51896,.F.);
#74146=ORIENTED_EDGE('',*,*,#51881,.F.);
#74147=ORIENTED_EDGE('',*,*,#51896,.T.);
#74148=ORIENTED_EDGE('',*,*,#49976,.F.);
#74149=ORIENTED_EDGE('',*,*,#51897,.F.);
#74150=ORIENTED_EDGE('',*,*,#51872,.F.);
#74151=ORIENTED_EDGE('',*,*,#51898,.T.);
#74152=ORIENTED_EDGE('',*,*,#51873,.F.);
#74153=ORIENTED_EDGE('',*,*,#51897,.T.);
#74154=ORIENTED_EDGE('',*,*,#50851,.F.);
#74155=ORIENTED_EDGE('',*,*,#51899,.T.);
#74156=ORIENTED_EDGE('',*,*,#51874,.F.);
#74157=ORIENTED_EDGE('',*,*,#51898,.F.);
#74158=ORIENTED_EDGE('',*,*,#50502,.F.);
#74159=ORIENTED_EDGE('',*,*,#51891,.T.);
#74160=ORIENTED_EDGE('',*,*,#51887,.T.);
#74161=ORIENTED_EDGE('',*,*,#51899,.F.);
#74162=ORIENTED_EDGE('',*,*,#50501,.T.);
#74163=ORIENTED_EDGE('',*,*,#51885,.T.);
#74164=ORIENTED_EDGE('',*,*,#51888,.T.);
#74165=ORIENTED_EDGE('',*,*,#51890,.T.);
#74166=ORIENTED_EDGE('',*,*,#51900,.T.);
#74167=ORIENTED_EDGE('',*,*,#51901,.T.);
#74168=ORIENTED_EDGE('',*,*,#51902,.T.);
#74169=ORIENTED_EDGE('',*,*,#51903,.T.);
#74170=ORIENTED_EDGE('',*,*,#51904,.T.);
#74171=ORIENTED_EDGE('',*,*,#51905,.T.);
#74172=ORIENTED_EDGE('',*,*,#51906,.T.);
#74173=ORIENTED_EDGE('',*,*,#51907,.F.);
#74174=ORIENTED_EDGE('',*,*,#51908,.T.);
#74175=ORIENTED_EDGE('',*,*,#51909,.T.);
#74176=ORIENTED_EDGE('',*,*,#51907,.T.);
#74177=ORIENTED_EDGE('',*,*,#51910,.T.);
#74178=ORIENTED_EDGE('',*,*,#51900,.F.);
#74179=ORIENTED_EDGE('',*,*,#51911,.T.);
#74180=ORIENTED_EDGE('',*,*,#51912,.F.);
#74181=ORIENTED_EDGE('',*,*,#51908,.F.);
#74182=ORIENTED_EDGE('',*,*,#51913,.F.);
#74183=ORIENTED_EDGE('',*,*,#51914,.F.);
#74184=ORIENTED_EDGE('',*,*,#51913,.T.);
#74185=ORIENTED_EDGE('',*,*,#51911,.F.);
#74186=ORIENTED_EDGE('',*,*,#51915,.F.);
#74187=ORIENTED_EDGE('',*,*,#51915,.T.);
#74188=ORIENTED_EDGE('',*,*,#51904,.F.);
#74189=ORIENTED_EDGE('',*,*,#51916,.F.);
#74190=ORIENTED_EDGE('',*,*,#51917,.F.);
#74191=ORIENTED_EDGE('',*,*,#51918,.T.);
#74192=ORIENTED_EDGE('',*,*,#51919,.F.);
#74193=ORIENTED_EDGE('',*,*,#51920,.F.);
#74194=ORIENTED_EDGE('',*,*,#50494,.F.);
#74195=ORIENTED_EDGE('',*,*,#51921,.T.);
#74196=ORIENTED_EDGE('',*,*,#51912,.T.);
#74197=ORIENTED_EDGE('',*,*,#51918,.F.);
#74198=ORIENTED_EDGE('',*,*,#50493,.T.);
#74199=ORIENTED_EDGE('',*,*,#51922,.F.);
#74200=ORIENTED_EDGE('',*,*,#51909,.F.);
#74201=ORIENTED_EDGE('',*,*,#51921,.F.);
#74202=ORIENTED_EDGE('',*,*,#50492,.F.);
#74203=ORIENTED_EDGE('',*,*,#51922,.T.);
#74204=ORIENTED_EDGE('',*,*,#50786,.F.);
#74205=ORIENTED_EDGE('',*,*,#51923,.F.);
#74206=ORIENTED_EDGE('',*,*,#51905,.F.);
#74207=ORIENTED_EDGE('',*,*,#51923,.T.);
#74208=ORIENTED_EDGE('',*,*,#49982,.F.);
#74209=ORIENTED_EDGE('',*,*,#51924,.F.);
#74210=ORIENTED_EDGE('',*,*,#51906,.F.);
#74211=ORIENTED_EDGE('',*,*,#51924,.T.);
#74212=ORIENTED_EDGE('',*,*,#49981,.F.);
#74213=ORIENTED_EDGE('',*,*,#51925,.F.);
#74214=ORIENTED_EDGE('',*,*,#51910,.F.);
#74215=ORIENTED_EDGE('',*,*,#51925,.T.);
#74216=ORIENTED_EDGE('',*,*,#49980,.F.);
#74217=ORIENTED_EDGE('',*,*,#51926,.F.);
#74218=ORIENTED_EDGE('',*,*,#51901,.F.);
#74219=ORIENTED_EDGE('',*,*,#51927,.T.);
#74220=ORIENTED_EDGE('',*,*,#51902,.F.);
#74221=ORIENTED_EDGE('',*,*,#51926,.T.);
#74222=ORIENTED_EDGE('',*,*,#50787,.F.);
#74223=ORIENTED_EDGE('',*,*,#51928,.T.);
#74224=ORIENTED_EDGE('',*,*,#51903,.F.);
#74225=ORIENTED_EDGE('',*,*,#51927,.F.);
#74226=ORIENTED_EDGE('',*,*,#50496,.F.);
#74227=ORIENTED_EDGE('',*,*,#51920,.T.);
#74228=ORIENTED_EDGE('',*,*,#51916,.T.);
#74229=ORIENTED_EDGE('',*,*,#51928,.F.);
#74230=ORIENTED_EDGE('',*,*,#50495,.T.);
#74231=ORIENTED_EDGE('',*,*,#51914,.T.);
#74232=ORIENTED_EDGE('',*,*,#51917,.T.);
#74233=ORIENTED_EDGE('',*,*,#51919,.T.);
#74234=ORIENTED_EDGE('',*,*,#51929,.T.);
#74235=ORIENTED_EDGE('',*,*,#51930,.T.);
#74236=ORIENTED_EDGE('',*,*,#51931,.T.);
#74237=ORIENTED_EDGE('',*,*,#51932,.T.);
#74238=ORIENTED_EDGE('',*,*,#51933,.T.);
#74239=ORIENTED_EDGE('',*,*,#51934,.T.);
#74240=ORIENTED_EDGE('',*,*,#51935,.T.);
#74241=ORIENTED_EDGE('',*,*,#51936,.F.);
#74242=ORIENTED_EDGE('',*,*,#51937,.T.);
#74243=ORIENTED_EDGE('',*,*,#51938,.T.);
#74244=ORIENTED_EDGE('',*,*,#51936,.T.);
#74245=ORIENTED_EDGE('',*,*,#51939,.T.);
#74246=ORIENTED_EDGE('',*,*,#51929,.F.);
#74247=ORIENTED_EDGE('',*,*,#51940,.T.);
#74248=ORIENTED_EDGE('',*,*,#51941,.F.);
#74249=ORIENTED_EDGE('',*,*,#51937,.F.);
#74250=ORIENTED_EDGE('',*,*,#51942,.F.);
#74251=ORIENTED_EDGE('',*,*,#51943,.F.);
#74252=ORIENTED_EDGE('',*,*,#51942,.T.);
#74253=ORIENTED_EDGE('',*,*,#51940,.F.);
#74254=ORIENTED_EDGE('',*,*,#51944,.F.);
#74255=ORIENTED_EDGE('',*,*,#51944,.T.);
#74256=ORIENTED_EDGE('',*,*,#51933,.F.);
#74257=ORIENTED_EDGE('',*,*,#51945,.F.);
#74258=ORIENTED_EDGE('',*,*,#51946,.F.);
#74259=ORIENTED_EDGE('',*,*,#51947,.T.);
#74260=ORIENTED_EDGE('',*,*,#51948,.F.);
#74261=ORIENTED_EDGE('',*,*,#51949,.F.);
#74262=ORIENTED_EDGE('',*,*,#50488,.F.);
#74263=ORIENTED_EDGE('',*,*,#51950,.T.);
#74264=ORIENTED_EDGE('',*,*,#51941,.T.);
#74265=ORIENTED_EDGE('',*,*,#51947,.F.);
#74266=ORIENTED_EDGE('',*,*,#50487,.T.);
#74267=ORIENTED_EDGE('',*,*,#51951,.F.);
#74268=ORIENTED_EDGE('',*,*,#51938,.F.);
#74269=ORIENTED_EDGE('',*,*,#51950,.F.);
#74270=ORIENTED_EDGE('',*,*,#50486,.F.);
#74271=ORIENTED_EDGE('',*,*,#51951,.T.);
#74272=ORIENTED_EDGE('',*,*,#50784,.F.);
#74273=ORIENTED_EDGE('',*,*,#51952,.F.);
#74274=ORIENTED_EDGE('',*,*,#51934,.F.);
#74275=ORIENTED_EDGE('',*,*,#51952,.T.);
#74276=ORIENTED_EDGE('',*,*,#49986,.F.);
#74277=ORIENTED_EDGE('',*,*,#51953,.F.);
#74278=ORIENTED_EDGE('',*,*,#51935,.F.);
#74279=ORIENTED_EDGE('',*,*,#51953,.T.);
#74280=ORIENTED_EDGE('',*,*,#49985,.F.);
#74281=ORIENTED_EDGE('',*,*,#51954,.F.);
#74282=ORIENTED_EDGE('',*,*,#51939,.F.);
#74283=ORIENTED_EDGE('',*,*,#51954,.T.);
#74284=ORIENTED_EDGE('',*,*,#49984,.F.);
#74285=ORIENTED_EDGE('',*,*,#51955,.F.);
#74286=ORIENTED_EDGE('',*,*,#51930,.F.);
#74287=ORIENTED_EDGE('',*,*,#51956,.T.);
#74288=ORIENTED_EDGE('',*,*,#51931,.F.);
#74289=ORIENTED_EDGE('',*,*,#51955,.T.);
#74290=ORIENTED_EDGE('',*,*,#50785,.F.);
#74291=ORIENTED_EDGE('',*,*,#51957,.T.);
#74292=ORIENTED_EDGE('',*,*,#51932,.F.);
#74293=ORIENTED_EDGE('',*,*,#51956,.F.);
#74294=ORIENTED_EDGE('',*,*,#50490,.F.);
#74295=ORIENTED_EDGE('',*,*,#51949,.T.);
#74296=ORIENTED_EDGE('',*,*,#51945,.T.);
#74297=ORIENTED_EDGE('',*,*,#51957,.F.);
#74298=ORIENTED_EDGE('',*,*,#50489,.T.);
#74299=ORIENTED_EDGE('',*,*,#51943,.T.);
#74300=ORIENTED_EDGE('',*,*,#51946,.T.);
#74301=ORIENTED_EDGE('',*,*,#51948,.T.);
#74302=ORIENTED_EDGE('',*,*,#51958,.T.);
#74303=ORIENTED_EDGE('',*,*,#51959,.T.);
#74304=ORIENTED_EDGE('',*,*,#51960,.T.);
#74305=ORIENTED_EDGE('',*,*,#51961,.T.);
#74306=ORIENTED_EDGE('',*,*,#51962,.T.);
#74307=ORIENTED_EDGE('',*,*,#51963,.T.);
#74308=ORIENTED_EDGE('',*,*,#51964,.T.);
#74309=ORIENTED_EDGE('',*,*,#51965,.F.);
#74310=ORIENTED_EDGE('',*,*,#51966,.T.);
#74311=ORIENTED_EDGE('',*,*,#51967,.T.);
#74312=ORIENTED_EDGE('',*,*,#51965,.T.);
#74313=ORIENTED_EDGE('',*,*,#51968,.T.);
#74314=ORIENTED_EDGE('',*,*,#51958,.F.);
#74315=ORIENTED_EDGE('',*,*,#51969,.T.);
#74316=ORIENTED_EDGE('',*,*,#51970,.F.);
#74317=ORIENTED_EDGE('',*,*,#51966,.F.);
#74318=ORIENTED_EDGE('',*,*,#51971,.F.);
#74319=ORIENTED_EDGE('',*,*,#51972,.F.);
#74320=ORIENTED_EDGE('',*,*,#51971,.T.);
#74321=ORIENTED_EDGE('',*,*,#51969,.F.);
#74322=ORIENTED_EDGE('',*,*,#51973,.F.);
#74323=ORIENTED_EDGE('',*,*,#51973,.T.);
#74324=ORIENTED_EDGE('',*,*,#51962,.F.);
#74325=ORIENTED_EDGE('',*,*,#51974,.F.);
#74326=ORIENTED_EDGE('',*,*,#51975,.F.);
#74327=ORIENTED_EDGE('',*,*,#51976,.T.);
#74328=ORIENTED_EDGE('',*,*,#51977,.F.);
#74329=ORIENTED_EDGE('',*,*,#51978,.F.);
#74330=ORIENTED_EDGE('',*,*,#50482,.F.);
#74331=ORIENTED_EDGE('',*,*,#51979,.T.);
#74332=ORIENTED_EDGE('',*,*,#51970,.T.);
#74333=ORIENTED_EDGE('',*,*,#51976,.F.);
#74334=ORIENTED_EDGE('',*,*,#50481,.T.);
#74335=ORIENTED_EDGE('',*,*,#51980,.F.);
#74336=ORIENTED_EDGE('',*,*,#51967,.F.);
#74337=ORIENTED_EDGE('',*,*,#51979,.F.);
#74338=ORIENTED_EDGE('',*,*,#50480,.F.);
#74339=ORIENTED_EDGE('',*,*,#51980,.T.);
#74340=ORIENTED_EDGE('',*,*,#50782,.F.);
#74341=ORIENTED_EDGE('',*,*,#51981,.F.);
#74342=ORIENTED_EDGE('',*,*,#51963,.F.);
#74343=ORIENTED_EDGE('',*,*,#51981,.T.);
#74344=ORIENTED_EDGE('',*,*,#49990,.F.);
#74345=ORIENTED_EDGE('',*,*,#51982,.F.);
#74346=ORIENTED_EDGE('',*,*,#51964,.F.);
#74347=ORIENTED_EDGE('',*,*,#51982,.T.);
#74348=ORIENTED_EDGE('',*,*,#49989,.F.);
#74349=ORIENTED_EDGE('',*,*,#51983,.F.);
#74350=ORIENTED_EDGE('',*,*,#51968,.F.);
#74351=ORIENTED_EDGE('',*,*,#51983,.T.);
#74352=ORIENTED_EDGE('',*,*,#49988,.F.);
#74353=ORIENTED_EDGE('',*,*,#51984,.F.);
#74354=ORIENTED_EDGE('',*,*,#51959,.F.);
#74355=ORIENTED_EDGE('',*,*,#51985,.T.);
#74356=ORIENTED_EDGE('',*,*,#51960,.F.);
#74357=ORIENTED_EDGE('',*,*,#51984,.T.);
#74358=ORIENTED_EDGE('',*,*,#50783,.F.);
#74359=ORIENTED_EDGE('',*,*,#51986,.T.);
#74360=ORIENTED_EDGE('',*,*,#51961,.F.);
#74361=ORIENTED_EDGE('',*,*,#51985,.F.);
#74362=ORIENTED_EDGE('',*,*,#50484,.F.);
#74363=ORIENTED_EDGE('',*,*,#51978,.T.);
#74364=ORIENTED_EDGE('',*,*,#51974,.T.);
#74365=ORIENTED_EDGE('',*,*,#51986,.F.);
#74366=ORIENTED_EDGE('',*,*,#50483,.T.);
#74367=ORIENTED_EDGE('',*,*,#51972,.T.);
#74368=ORIENTED_EDGE('',*,*,#51975,.T.);
#74369=ORIENTED_EDGE('',*,*,#51977,.T.);
#74370=ORIENTED_EDGE('',*,*,#51987,.T.);
#74371=ORIENTED_EDGE('',*,*,#51988,.T.);
#74372=ORIENTED_EDGE('',*,*,#51989,.T.);
#74373=ORIENTED_EDGE('',*,*,#51990,.T.);
#74374=ORIENTED_EDGE('',*,*,#51991,.T.);
#74375=ORIENTED_EDGE('',*,*,#51992,.T.);
#74376=ORIENTED_EDGE('',*,*,#51993,.T.);
#74377=ORIENTED_EDGE('',*,*,#51994,.F.);
#74378=ORIENTED_EDGE('',*,*,#51995,.T.);
#74379=ORIENTED_EDGE('',*,*,#51996,.T.);
#74380=ORIENTED_EDGE('',*,*,#51994,.T.);
#74381=ORIENTED_EDGE('',*,*,#51997,.T.);
#74382=ORIENTED_EDGE('',*,*,#51987,.F.);
#74383=ORIENTED_EDGE('',*,*,#51998,.T.);
#74384=ORIENTED_EDGE('',*,*,#51999,.F.);
#74385=ORIENTED_EDGE('',*,*,#51995,.F.);
#74386=ORIENTED_EDGE('',*,*,#52000,.F.);
#74387=ORIENTED_EDGE('',*,*,#52001,.F.);
#74388=ORIENTED_EDGE('',*,*,#52000,.T.);
#74389=ORIENTED_EDGE('',*,*,#51998,.F.);
#74390=ORIENTED_EDGE('',*,*,#52002,.F.);
#74391=ORIENTED_EDGE('',*,*,#52002,.T.);
#74392=ORIENTED_EDGE('',*,*,#51991,.F.);
#74393=ORIENTED_EDGE('',*,*,#52003,.F.);
#74394=ORIENTED_EDGE('',*,*,#52004,.F.);
#74395=ORIENTED_EDGE('',*,*,#52005,.T.);
#74396=ORIENTED_EDGE('',*,*,#52006,.F.);
#74397=ORIENTED_EDGE('',*,*,#52007,.F.);
#74398=ORIENTED_EDGE('',*,*,#50476,.F.);
#74399=ORIENTED_EDGE('',*,*,#52008,.T.);
#74400=ORIENTED_EDGE('',*,*,#51999,.T.);
#74401=ORIENTED_EDGE('',*,*,#52005,.F.);
#74402=ORIENTED_EDGE('',*,*,#50475,.T.);
#74403=ORIENTED_EDGE('',*,*,#52009,.F.);
#74404=ORIENTED_EDGE('',*,*,#51996,.F.);
#74405=ORIENTED_EDGE('',*,*,#52008,.F.);
#74406=ORIENTED_EDGE('',*,*,#50474,.F.);
#74407=ORIENTED_EDGE('',*,*,#52009,.T.);
#74408=ORIENTED_EDGE('',*,*,#50780,.F.);
#74409=ORIENTED_EDGE('',*,*,#52010,.F.);
#74410=ORIENTED_EDGE('',*,*,#51992,.F.);
#74411=ORIENTED_EDGE('',*,*,#52010,.T.);
#74412=ORIENTED_EDGE('',*,*,#49994,.F.);
#74413=ORIENTED_EDGE('',*,*,#52011,.F.);
#74414=ORIENTED_EDGE('',*,*,#51993,.F.);
#74415=ORIENTED_EDGE('',*,*,#52011,.T.);
#74416=ORIENTED_EDGE('',*,*,#49993,.F.);
#74417=ORIENTED_EDGE('',*,*,#52012,.F.);
#74418=ORIENTED_EDGE('',*,*,#51997,.F.);
#74419=ORIENTED_EDGE('',*,*,#52012,.T.);
#74420=ORIENTED_EDGE('',*,*,#49992,.F.);
#74421=ORIENTED_EDGE('',*,*,#52013,.F.);
#74422=ORIENTED_EDGE('',*,*,#51988,.F.);
#74423=ORIENTED_EDGE('',*,*,#52014,.T.);
#74424=ORIENTED_EDGE('',*,*,#51989,.F.);
#74425=ORIENTED_EDGE('',*,*,#52013,.T.);
#74426=ORIENTED_EDGE('',*,*,#50781,.F.);
#74427=ORIENTED_EDGE('',*,*,#52015,.T.);
#74428=ORIENTED_EDGE('',*,*,#51990,.F.);
#74429=ORIENTED_EDGE('',*,*,#52014,.F.);
#74430=ORIENTED_EDGE('',*,*,#50478,.F.);
#74431=ORIENTED_EDGE('',*,*,#52007,.T.);
#74432=ORIENTED_EDGE('',*,*,#52003,.T.);
#74433=ORIENTED_EDGE('',*,*,#52015,.F.);
#74434=ORIENTED_EDGE('',*,*,#50477,.T.);
#74435=ORIENTED_EDGE('',*,*,#52001,.T.);
#74436=ORIENTED_EDGE('',*,*,#52004,.T.);
#74437=ORIENTED_EDGE('',*,*,#52006,.T.);
#74438=ORIENTED_EDGE('',*,*,#52016,.T.);
#74439=ORIENTED_EDGE('',*,*,#52017,.T.);
#74440=ORIENTED_EDGE('',*,*,#52018,.T.);
#74441=ORIENTED_EDGE('',*,*,#52019,.T.);
#74442=ORIENTED_EDGE('',*,*,#52020,.T.);
#74443=ORIENTED_EDGE('',*,*,#52021,.T.);
#74444=ORIENTED_EDGE('',*,*,#52022,.T.);
#74445=ORIENTED_EDGE('',*,*,#52023,.F.);
#74446=ORIENTED_EDGE('',*,*,#52024,.T.);
#74447=ORIENTED_EDGE('',*,*,#52025,.T.);
#74448=ORIENTED_EDGE('',*,*,#52023,.T.);
#74449=ORIENTED_EDGE('',*,*,#52026,.T.);
#74450=ORIENTED_EDGE('',*,*,#52016,.F.);
#74451=ORIENTED_EDGE('',*,*,#52027,.T.);
#74452=ORIENTED_EDGE('',*,*,#52028,.F.);
#74453=ORIENTED_EDGE('',*,*,#52024,.F.);
#74454=ORIENTED_EDGE('',*,*,#52029,.F.);
#74455=ORIENTED_EDGE('',*,*,#52030,.F.);
#74456=ORIENTED_EDGE('',*,*,#52029,.T.);
#74457=ORIENTED_EDGE('',*,*,#52027,.F.);
#74458=ORIENTED_EDGE('',*,*,#52031,.F.);
#74459=ORIENTED_EDGE('',*,*,#52031,.T.);
#74460=ORIENTED_EDGE('',*,*,#52020,.F.);
#74461=ORIENTED_EDGE('',*,*,#52032,.F.);
#74462=ORIENTED_EDGE('',*,*,#52033,.F.);
#74463=ORIENTED_EDGE('',*,*,#52034,.T.);
#74464=ORIENTED_EDGE('',*,*,#52035,.F.);
#74465=ORIENTED_EDGE('',*,*,#52036,.F.);
#74466=ORIENTED_EDGE('',*,*,#50470,.F.);
#74467=ORIENTED_EDGE('',*,*,#52037,.T.);
#74468=ORIENTED_EDGE('',*,*,#52028,.T.);
#74469=ORIENTED_EDGE('',*,*,#52034,.F.);
#74470=ORIENTED_EDGE('',*,*,#50469,.T.);
#74471=ORIENTED_EDGE('',*,*,#52038,.F.);
#74472=ORIENTED_EDGE('',*,*,#52025,.F.);
#74473=ORIENTED_EDGE('',*,*,#52037,.F.);
#74474=ORIENTED_EDGE('',*,*,#50468,.F.);
#74475=ORIENTED_EDGE('',*,*,#52038,.T.);
#74476=ORIENTED_EDGE('',*,*,#50778,.F.);
#74477=ORIENTED_EDGE('',*,*,#52039,.F.);
#74478=ORIENTED_EDGE('',*,*,#52021,.F.);
#74479=ORIENTED_EDGE('',*,*,#52039,.T.);
#74480=ORIENTED_EDGE('',*,*,#49998,.F.);
#74481=ORIENTED_EDGE('',*,*,#52040,.F.);
#74482=ORIENTED_EDGE('',*,*,#52022,.F.);
#74483=ORIENTED_EDGE('',*,*,#52040,.T.);
#74484=ORIENTED_EDGE('',*,*,#49997,.F.);
#74485=ORIENTED_EDGE('',*,*,#52041,.F.);
#74486=ORIENTED_EDGE('',*,*,#52026,.F.);
#74487=ORIENTED_EDGE('',*,*,#52041,.T.);
#74488=ORIENTED_EDGE('',*,*,#49996,.F.);
#74489=ORIENTED_EDGE('',*,*,#52042,.F.);
#74490=ORIENTED_EDGE('',*,*,#52017,.F.);
#74491=ORIENTED_EDGE('',*,*,#52043,.T.);
#74492=ORIENTED_EDGE('',*,*,#52018,.F.);
#74493=ORIENTED_EDGE('',*,*,#52042,.T.);
#74494=ORIENTED_EDGE('',*,*,#50779,.F.);
#74495=ORIENTED_EDGE('',*,*,#52044,.T.);
#74496=ORIENTED_EDGE('',*,*,#52019,.F.);
#74497=ORIENTED_EDGE('',*,*,#52043,.F.);
#74498=ORIENTED_EDGE('',*,*,#50472,.F.);
#74499=ORIENTED_EDGE('',*,*,#52036,.T.);
#74500=ORIENTED_EDGE('',*,*,#52032,.T.);
#74501=ORIENTED_EDGE('',*,*,#52044,.F.);
#74502=ORIENTED_EDGE('',*,*,#50471,.T.);
#74503=ORIENTED_EDGE('',*,*,#52030,.T.);
#74504=ORIENTED_EDGE('',*,*,#52033,.T.);
#74505=ORIENTED_EDGE('',*,*,#52035,.T.);
#74506=ORIENTED_EDGE('',*,*,#52045,.T.);
#74507=ORIENTED_EDGE('',*,*,#52046,.T.);
#74508=ORIENTED_EDGE('',*,*,#52047,.T.);
#74509=ORIENTED_EDGE('',*,*,#52048,.T.);
#74510=ORIENTED_EDGE('',*,*,#52049,.T.);
#74511=ORIENTED_EDGE('',*,*,#52050,.T.);
#74512=ORIENTED_EDGE('',*,*,#52051,.T.);
#74513=ORIENTED_EDGE('',*,*,#52052,.F.);
#74514=ORIENTED_EDGE('',*,*,#52053,.T.);
#74515=ORIENTED_EDGE('',*,*,#52054,.T.);
#74516=ORIENTED_EDGE('',*,*,#52052,.T.);
#74517=ORIENTED_EDGE('',*,*,#52055,.T.);
#74518=ORIENTED_EDGE('',*,*,#52045,.F.);
#74519=ORIENTED_EDGE('',*,*,#52056,.T.);
#74520=ORIENTED_EDGE('',*,*,#52057,.F.);
#74521=ORIENTED_EDGE('',*,*,#52053,.F.);
#74522=ORIENTED_EDGE('',*,*,#52058,.F.);
#74523=ORIENTED_EDGE('',*,*,#52059,.F.);
#74524=ORIENTED_EDGE('',*,*,#52058,.T.);
#74525=ORIENTED_EDGE('',*,*,#52056,.F.);
#74526=ORIENTED_EDGE('',*,*,#52060,.F.);
#74527=ORIENTED_EDGE('',*,*,#52060,.T.);
#74528=ORIENTED_EDGE('',*,*,#52049,.F.);
#74529=ORIENTED_EDGE('',*,*,#52061,.F.);
#74530=ORIENTED_EDGE('',*,*,#52062,.F.);
#74531=ORIENTED_EDGE('',*,*,#52063,.T.);
#74532=ORIENTED_EDGE('',*,*,#52064,.F.);
#74533=ORIENTED_EDGE('',*,*,#52065,.F.);
#74534=ORIENTED_EDGE('',*,*,#50464,.F.);
#74535=ORIENTED_EDGE('',*,*,#52066,.T.);
#74536=ORIENTED_EDGE('',*,*,#52057,.T.);
#74537=ORIENTED_EDGE('',*,*,#52063,.F.);
#74538=ORIENTED_EDGE('',*,*,#50463,.T.);
#74539=ORIENTED_EDGE('',*,*,#52067,.F.);
#74540=ORIENTED_EDGE('',*,*,#52054,.F.);
#74541=ORIENTED_EDGE('',*,*,#52066,.F.);
#74542=ORIENTED_EDGE('',*,*,#50462,.F.);
#74543=ORIENTED_EDGE('',*,*,#52067,.T.);
#74544=ORIENTED_EDGE('',*,*,#50776,.F.);
#74545=ORIENTED_EDGE('',*,*,#52068,.F.);
#74546=ORIENTED_EDGE('',*,*,#52050,.F.);
#74547=ORIENTED_EDGE('',*,*,#52068,.T.);
#74548=ORIENTED_EDGE('',*,*,#50002,.F.);
#74549=ORIENTED_EDGE('',*,*,#52069,.F.);
#74550=ORIENTED_EDGE('',*,*,#52051,.F.);
#74551=ORIENTED_EDGE('',*,*,#52069,.T.);
#74552=ORIENTED_EDGE('',*,*,#50001,.F.);
#74553=ORIENTED_EDGE('',*,*,#52070,.F.);
#74554=ORIENTED_EDGE('',*,*,#52055,.F.);
#74555=ORIENTED_EDGE('',*,*,#52070,.T.);
#74556=ORIENTED_EDGE('',*,*,#50000,.F.);
#74557=ORIENTED_EDGE('',*,*,#52071,.F.);
#74558=ORIENTED_EDGE('',*,*,#52046,.F.);
#74559=ORIENTED_EDGE('',*,*,#52072,.T.);
#74560=ORIENTED_EDGE('',*,*,#52047,.F.);
#74561=ORIENTED_EDGE('',*,*,#52071,.T.);
#74562=ORIENTED_EDGE('',*,*,#50777,.F.);
#74563=ORIENTED_EDGE('',*,*,#52073,.T.);
#74564=ORIENTED_EDGE('',*,*,#52048,.F.);
#74565=ORIENTED_EDGE('',*,*,#52072,.F.);
#74566=ORIENTED_EDGE('',*,*,#50466,.F.);
#74567=ORIENTED_EDGE('',*,*,#52065,.T.);
#74568=ORIENTED_EDGE('',*,*,#52061,.T.);
#74569=ORIENTED_EDGE('',*,*,#52073,.F.);
#74570=ORIENTED_EDGE('',*,*,#50465,.T.);
#74571=ORIENTED_EDGE('',*,*,#52059,.T.);
#74572=ORIENTED_EDGE('',*,*,#52062,.T.);
#74573=ORIENTED_EDGE('',*,*,#52064,.T.);
#74574=ORIENTED_EDGE('',*,*,#52074,.T.);
#74575=ORIENTED_EDGE('',*,*,#52075,.T.);
#74576=ORIENTED_EDGE('',*,*,#52076,.T.);
#74577=ORIENTED_EDGE('',*,*,#52077,.T.);
#74578=ORIENTED_EDGE('',*,*,#52078,.T.);
#74579=ORIENTED_EDGE('',*,*,#52079,.T.);
#74580=ORIENTED_EDGE('',*,*,#52080,.T.);
#74581=ORIENTED_EDGE('',*,*,#52081,.F.);
#74582=ORIENTED_EDGE('',*,*,#52082,.T.);
#74583=ORIENTED_EDGE('',*,*,#52083,.T.);
#74584=ORIENTED_EDGE('',*,*,#52081,.T.);
#74585=ORIENTED_EDGE('',*,*,#52084,.T.);
#74586=ORIENTED_EDGE('',*,*,#52074,.F.);
#74587=ORIENTED_EDGE('',*,*,#52085,.T.);
#74588=ORIENTED_EDGE('',*,*,#52086,.F.);
#74589=ORIENTED_EDGE('',*,*,#52082,.F.);
#74590=ORIENTED_EDGE('',*,*,#52087,.F.);
#74591=ORIENTED_EDGE('',*,*,#52088,.F.);
#74592=ORIENTED_EDGE('',*,*,#52087,.T.);
#74593=ORIENTED_EDGE('',*,*,#52085,.F.);
#74594=ORIENTED_EDGE('',*,*,#52089,.F.);
#74595=ORIENTED_EDGE('',*,*,#52089,.T.);
#74596=ORIENTED_EDGE('',*,*,#52078,.F.);
#74597=ORIENTED_EDGE('',*,*,#52090,.F.);
#74598=ORIENTED_EDGE('',*,*,#52091,.F.);
#74599=ORIENTED_EDGE('',*,*,#52092,.T.);
#74600=ORIENTED_EDGE('',*,*,#52093,.F.);
#74601=ORIENTED_EDGE('',*,*,#52094,.F.);
#74602=ORIENTED_EDGE('',*,*,#50458,.F.);
#74603=ORIENTED_EDGE('',*,*,#52095,.T.);
#74604=ORIENTED_EDGE('',*,*,#52086,.T.);
#74605=ORIENTED_EDGE('',*,*,#52092,.F.);
#74606=ORIENTED_EDGE('',*,*,#50457,.T.);
#74607=ORIENTED_EDGE('',*,*,#52096,.F.);
#74608=ORIENTED_EDGE('',*,*,#52083,.F.);
#74609=ORIENTED_EDGE('',*,*,#52095,.F.);
#74610=ORIENTED_EDGE('',*,*,#50456,.F.);
#74611=ORIENTED_EDGE('',*,*,#52096,.T.);
#74612=ORIENTED_EDGE('',*,*,#50774,.F.);
#74613=ORIENTED_EDGE('',*,*,#52097,.F.);
#74614=ORIENTED_EDGE('',*,*,#52079,.F.);
#74615=ORIENTED_EDGE('',*,*,#52097,.T.);
#74616=ORIENTED_EDGE('',*,*,#50006,.F.);
#74617=ORIENTED_EDGE('',*,*,#52098,.F.);
#74618=ORIENTED_EDGE('',*,*,#52080,.F.);
#74619=ORIENTED_EDGE('',*,*,#52098,.T.);
#74620=ORIENTED_EDGE('',*,*,#50005,.F.);
#74621=ORIENTED_EDGE('',*,*,#52099,.F.);
#74622=ORIENTED_EDGE('',*,*,#52084,.F.);
#74623=ORIENTED_EDGE('',*,*,#52099,.T.);
#74624=ORIENTED_EDGE('',*,*,#50004,.F.);
#74625=ORIENTED_EDGE('',*,*,#52100,.F.);
#74626=ORIENTED_EDGE('',*,*,#52075,.F.);
#74627=ORIENTED_EDGE('',*,*,#52101,.T.);
#74628=ORIENTED_EDGE('',*,*,#52076,.F.);
#74629=ORIENTED_EDGE('',*,*,#52100,.T.);
#74630=ORIENTED_EDGE('',*,*,#50775,.F.);
#74631=ORIENTED_EDGE('',*,*,#52102,.T.);
#74632=ORIENTED_EDGE('',*,*,#52077,.F.);
#74633=ORIENTED_EDGE('',*,*,#52101,.F.);
#74634=ORIENTED_EDGE('',*,*,#50460,.F.);
#74635=ORIENTED_EDGE('',*,*,#52094,.T.);
#74636=ORIENTED_EDGE('',*,*,#52090,.T.);
#74637=ORIENTED_EDGE('',*,*,#52102,.F.);
#74638=ORIENTED_EDGE('',*,*,#50459,.T.);
#74639=ORIENTED_EDGE('',*,*,#52088,.T.);
#74640=ORIENTED_EDGE('',*,*,#52091,.T.);
#74641=ORIENTED_EDGE('',*,*,#52093,.T.);
#74642=ORIENTED_EDGE('',*,*,#52103,.T.);
#74643=ORIENTED_EDGE('',*,*,#52104,.T.);
#74644=ORIENTED_EDGE('',*,*,#52105,.T.);
#74645=ORIENTED_EDGE('',*,*,#52106,.T.);
#74646=ORIENTED_EDGE('',*,*,#52107,.T.);
#74647=ORIENTED_EDGE('',*,*,#52108,.T.);
#74648=ORIENTED_EDGE('',*,*,#52109,.T.);
#74649=ORIENTED_EDGE('',*,*,#52110,.F.);
#74650=ORIENTED_EDGE('',*,*,#52111,.T.);
#74651=ORIENTED_EDGE('',*,*,#52112,.T.);
#74652=ORIENTED_EDGE('',*,*,#52110,.T.);
#74653=ORIENTED_EDGE('',*,*,#52113,.T.);
#74654=ORIENTED_EDGE('',*,*,#52103,.F.);
#74655=ORIENTED_EDGE('',*,*,#52114,.T.);
#74656=ORIENTED_EDGE('',*,*,#52115,.F.);
#74657=ORIENTED_EDGE('',*,*,#52111,.F.);
#74658=ORIENTED_EDGE('',*,*,#52116,.F.);
#74659=ORIENTED_EDGE('',*,*,#52117,.F.);
#74660=ORIENTED_EDGE('',*,*,#52116,.T.);
#74661=ORIENTED_EDGE('',*,*,#52114,.F.);
#74662=ORIENTED_EDGE('',*,*,#52118,.F.);
#74663=ORIENTED_EDGE('',*,*,#52118,.T.);
#74664=ORIENTED_EDGE('',*,*,#52107,.F.);
#74665=ORIENTED_EDGE('',*,*,#52119,.F.);
#74666=ORIENTED_EDGE('',*,*,#52120,.F.);
#74667=ORIENTED_EDGE('',*,*,#52121,.T.);
#74668=ORIENTED_EDGE('',*,*,#52122,.F.);
#74669=ORIENTED_EDGE('',*,*,#52123,.F.);
#74670=ORIENTED_EDGE('',*,*,#50452,.F.);
#74671=ORIENTED_EDGE('',*,*,#52124,.T.);
#74672=ORIENTED_EDGE('',*,*,#52115,.T.);
#74673=ORIENTED_EDGE('',*,*,#52121,.F.);
#74674=ORIENTED_EDGE('',*,*,#50451,.T.);
#74675=ORIENTED_EDGE('',*,*,#52125,.F.);
#74676=ORIENTED_EDGE('',*,*,#52112,.F.);
#74677=ORIENTED_EDGE('',*,*,#52124,.F.);
#74678=ORIENTED_EDGE('',*,*,#50450,.F.);
#74679=ORIENTED_EDGE('',*,*,#52125,.T.);
#74680=ORIENTED_EDGE('',*,*,#50772,.F.);
#74681=ORIENTED_EDGE('',*,*,#52126,.F.);
#74682=ORIENTED_EDGE('',*,*,#52108,.F.);
#74683=ORIENTED_EDGE('',*,*,#52126,.T.);
#74684=ORIENTED_EDGE('',*,*,#50010,.F.);
#74685=ORIENTED_EDGE('',*,*,#52127,.F.);
#74686=ORIENTED_EDGE('',*,*,#52109,.F.);
#74687=ORIENTED_EDGE('',*,*,#52127,.T.);
#74688=ORIENTED_EDGE('',*,*,#50009,.F.);
#74689=ORIENTED_EDGE('',*,*,#52128,.F.);
#74690=ORIENTED_EDGE('',*,*,#52113,.F.);
#74691=ORIENTED_EDGE('',*,*,#52128,.T.);
#74692=ORIENTED_EDGE('',*,*,#50008,.F.);
#74693=ORIENTED_EDGE('',*,*,#52129,.F.);
#74694=ORIENTED_EDGE('',*,*,#52104,.F.);
#74695=ORIENTED_EDGE('',*,*,#52130,.T.);
#74696=ORIENTED_EDGE('',*,*,#52105,.F.);
#74697=ORIENTED_EDGE('',*,*,#52129,.T.);
#74698=ORIENTED_EDGE('',*,*,#50773,.F.);
#74699=ORIENTED_EDGE('',*,*,#52131,.T.);
#74700=ORIENTED_EDGE('',*,*,#52106,.F.);
#74701=ORIENTED_EDGE('',*,*,#52130,.F.);
#74702=ORIENTED_EDGE('',*,*,#50454,.F.);
#74703=ORIENTED_EDGE('',*,*,#52123,.T.);
#74704=ORIENTED_EDGE('',*,*,#52119,.T.);
#74705=ORIENTED_EDGE('',*,*,#52131,.F.);
#74706=ORIENTED_EDGE('',*,*,#50453,.T.);
#74707=ORIENTED_EDGE('',*,*,#52117,.T.);
#74708=ORIENTED_EDGE('',*,*,#52120,.T.);
#74709=ORIENTED_EDGE('',*,*,#52122,.T.);
#74710=ORIENTED_EDGE('',*,*,#52132,.T.);
#74711=ORIENTED_EDGE('',*,*,#52133,.T.);
#74712=ORIENTED_EDGE('',*,*,#52134,.T.);
#74713=ORIENTED_EDGE('',*,*,#52135,.T.);
#74714=ORIENTED_EDGE('',*,*,#52136,.T.);
#74715=ORIENTED_EDGE('',*,*,#52137,.T.);
#74716=ORIENTED_EDGE('',*,*,#52138,.T.);
#74717=ORIENTED_EDGE('',*,*,#52139,.F.);
#74718=ORIENTED_EDGE('',*,*,#52140,.T.);
#74719=ORIENTED_EDGE('',*,*,#52141,.T.);
#74720=ORIENTED_EDGE('',*,*,#52139,.T.);
#74721=ORIENTED_EDGE('',*,*,#52142,.T.);
#74722=ORIENTED_EDGE('',*,*,#52132,.F.);
#74723=ORIENTED_EDGE('',*,*,#52143,.T.);
#74724=ORIENTED_EDGE('',*,*,#52144,.F.);
#74725=ORIENTED_EDGE('',*,*,#52140,.F.);
#74726=ORIENTED_EDGE('',*,*,#52145,.F.);
#74727=ORIENTED_EDGE('',*,*,#52146,.F.);
#74728=ORIENTED_EDGE('',*,*,#52145,.T.);
#74729=ORIENTED_EDGE('',*,*,#52143,.F.);
#74730=ORIENTED_EDGE('',*,*,#52147,.F.);
#74731=ORIENTED_EDGE('',*,*,#52147,.T.);
#74732=ORIENTED_EDGE('',*,*,#52136,.F.);
#74733=ORIENTED_EDGE('',*,*,#52148,.F.);
#74734=ORIENTED_EDGE('',*,*,#52149,.F.);
#74735=ORIENTED_EDGE('',*,*,#52150,.T.);
#74736=ORIENTED_EDGE('',*,*,#52151,.F.);
#74737=ORIENTED_EDGE('',*,*,#52152,.F.);
#74738=ORIENTED_EDGE('',*,*,#50446,.F.);
#74739=ORIENTED_EDGE('',*,*,#52153,.T.);
#74740=ORIENTED_EDGE('',*,*,#52144,.T.);
#74741=ORIENTED_EDGE('',*,*,#52150,.F.);
#74742=ORIENTED_EDGE('',*,*,#50445,.T.);
#74743=ORIENTED_EDGE('',*,*,#52154,.F.);
#74744=ORIENTED_EDGE('',*,*,#52141,.F.);
#74745=ORIENTED_EDGE('',*,*,#52153,.F.);
#74746=ORIENTED_EDGE('',*,*,#50444,.F.);
#74747=ORIENTED_EDGE('',*,*,#52154,.T.);
#74748=ORIENTED_EDGE('',*,*,#50770,.F.);
#74749=ORIENTED_EDGE('',*,*,#52155,.F.);
#74750=ORIENTED_EDGE('',*,*,#52137,.F.);
#74751=ORIENTED_EDGE('',*,*,#52155,.T.);
#74752=ORIENTED_EDGE('',*,*,#50014,.F.);
#74753=ORIENTED_EDGE('',*,*,#52156,.F.);
#74754=ORIENTED_EDGE('',*,*,#52138,.F.);
#74755=ORIENTED_EDGE('',*,*,#52156,.T.);
#74756=ORIENTED_EDGE('',*,*,#50013,.F.);
#74757=ORIENTED_EDGE('',*,*,#52157,.F.);
#74758=ORIENTED_EDGE('',*,*,#52142,.F.);
#74759=ORIENTED_EDGE('',*,*,#52157,.T.);
#74760=ORIENTED_EDGE('',*,*,#50012,.F.);
#74761=ORIENTED_EDGE('',*,*,#52158,.F.);
#74762=ORIENTED_EDGE('',*,*,#52133,.F.);
#74763=ORIENTED_EDGE('',*,*,#52159,.T.);
#74764=ORIENTED_EDGE('',*,*,#52134,.F.);
#74765=ORIENTED_EDGE('',*,*,#52158,.T.);
#74766=ORIENTED_EDGE('',*,*,#50771,.F.);
#74767=ORIENTED_EDGE('',*,*,#52160,.T.);
#74768=ORIENTED_EDGE('',*,*,#52135,.F.);
#74769=ORIENTED_EDGE('',*,*,#52159,.F.);
#74770=ORIENTED_EDGE('',*,*,#50448,.F.);
#74771=ORIENTED_EDGE('',*,*,#52152,.T.);
#74772=ORIENTED_EDGE('',*,*,#52148,.T.);
#74773=ORIENTED_EDGE('',*,*,#52160,.F.);
#74774=ORIENTED_EDGE('',*,*,#50447,.T.);
#74775=ORIENTED_EDGE('',*,*,#52146,.T.);
#74776=ORIENTED_EDGE('',*,*,#52149,.T.);
#74777=ORIENTED_EDGE('',*,*,#52151,.T.);
#74778=ORIENTED_EDGE('',*,*,#52161,.T.);
#74779=ORIENTED_EDGE('',*,*,#52162,.T.);
#74780=ORIENTED_EDGE('',*,*,#52163,.T.);
#74781=ORIENTED_EDGE('',*,*,#52164,.T.);
#74782=ORIENTED_EDGE('',*,*,#52165,.T.);
#74783=ORIENTED_EDGE('',*,*,#52166,.T.);
#74784=ORIENTED_EDGE('',*,*,#52167,.T.);
#74785=ORIENTED_EDGE('',*,*,#52168,.F.);
#74786=ORIENTED_EDGE('',*,*,#52169,.T.);
#74787=ORIENTED_EDGE('',*,*,#52170,.T.);
#74788=ORIENTED_EDGE('',*,*,#52168,.T.);
#74789=ORIENTED_EDGE('',*,*,#52171,.T.);
#74790=ORIENTED_EDGE('',*,*,#52161,.F.);
#74791=ORIENTED_EDGE('',*,*,#52172,.T.);
#74792=ORIENTED_EDGE('',*,*,#52173,.F.);
#74793=ORIENTED_EDGE('',*,*,#52169,.F.);
#74794=ORIENTED_EDGE('',*,*,#52174,.F.);
#74795=ORIENTED_EDGE('',*,*,#52175,.F.);
#74796=ORIENTED_EDGE('',*,*,#52174,.T.);
#74797=ORIENTED_EDGE('',*,*,#52172,.F.);
#74798=ORIENTED_EDGE('',*,*,#52176,.F.);
#74799=ORIENTED_EDGE('',*,*,#52176,.T.);
#74800=ORIENTED_EDGE('',*,*,#52165,.F.);
#74801=ORIENTED_EDGE('',*,*,#52177,.F.);
#74802=ORIENTED_EDGE('',*,*,#52178,.F.);
#74803=ORIENTED_EDGE('',*,*,#52179,.T.);
#74804=ORIENTED_EDGE('',*,*,#52180,.F.);
#74805=ORIENTED_EDGE('',*,*,#52181,.F.);
#74806=ORIENTED_EDGE('',*,*,#50440,.F.);
#74807=ORIENTED_EDGE('',*,*,#52182,.T.);
#74808=ORIENTED_EDGE('',*,*,#52173,.T.);
#74809=ORIENTED_EDGE('',*,*,#52179,.F.);
#74810=ORIENTED_EDGE('',*,*,#50439,.T.);
#74811=ORIENTED_EDGE('',*,*,#52183,.F.);
#74812=ORIENTED_EDGE('',*,*,#52170,.F.);
#74813=ORIENTED_EDGE('',*,*,#52182,.F.);
#74814=ORIENTED_EDGE('',*,*,#50438,.F.);
#74815=ORIENTED_EDGE('',*,*,#52183,.T.);
#74816=ORIENTED_EDGE('',*,*,#50768,.F.);
#74817=ORIENTED_EDGE('',*,*,#52184,.F.);
#74818=ORIENTED_EDGE('',*,*,#52166,.F.);
#74819=ORIENTED_EDGE('',*,*,#52184,.T.);
#74820=ORIENTED_EDGE('',*,*,#50018,.F.);
#74821=ORIENTED_EDGE('',*,*,#52185,.F.);
#74822=ORIENTED_EDGE('',*,*,#52167,.F.);
#74823=ORIENTED_EDGE('',*,*,#52185,.T.);
#74824=ORIENTED_EDGE('',*,*,#50017,.F.);
#74825=ORIENTED_EDGE('',*,*,#52186,.F.);
#74826=ORIENTED_EDGE('',*,*,#52171,.F.);
#74827=ORIENTED_EDGE('',*,*,#52186,.T.);
#74828=ORIENTED_EDGE('',*,*,#50016,.F.);
#74829=ORIENTED_EDGE('',*,*,#52187,.F.);
#74830=ORIENTED_EDGE('',*,*,#52162,.F.);
#74831=ORIENTED_EDGE('',*,*,#52188,.T.);
#74832=ORIENTED_EDGE('',*,*,#52163,.F.);
#74833=ORIENTED_EDGE('',*,*,#52187,.T.);
#74834=ORIENTED_EDGE('',*,*,#50769,.F.);
#74835=ORIENTED_EDGE('',*,*,#52189,.T.);
#74836=ORIENTED_EDGE('',*,*,#52164,.F.);
#74837=ORIENTED_EDGE('',*,*,#52188,.F.);
#74838=ORIENTED_EDGE('',*,*,#50442,.F.);
#74839=ORIENTED_EDGE('',*,*,#52181,.T.);
#74840=ORIENTED_EDGE('',*,*,#52177,.T.);
#74841=ORIENTED_EDGE('',*,*,#52189,.F.);
#74842=ORIENTED_EDGE('',*,*,#50441,.T.);
#74843=ORIENTED_EDGE('',*,*,#52175,.T.);
#74844=ORIENTED_EDGE('',*,*,#52178,.T.);
#74845=ORIENTED_EDGE('',*,*,#52180,.T.);
#74846=ORIENTED_EDGE('',*,*,#52190,.T.);
#74847=ORIENTED_EDGE('',*,*,#52191,.T.);
#74848=ORIENTED_EDGE('',*,*,#52192,.T.);
#74849=ORIENTED_EDGE('',*,*,#52193,.T.);
#74850=ORIENTED_EDGE('',*,*,#52194,.T.);
#74851=ORIENTED_EDGE('',*,*,#52195,.T.);
#74852=ORIENTED_EDGE('',*,*,#52196,.T.);
#74853=ORIENTED_EDGE('',*,*,#52197,.F.);
#74854=ORIENTED_EDGE('',*,*,#52198,.T.);
#74855=ORIENTED_EDGE('',*,*,#52199,.T.);
#74856=ORIENTED_EDGE('',*,*,#52197,.T.);
#74857=ORIENTED_EDGE('',*,*,#52200,.T.);
#74858=ORIENTED_EDGE('',*,*,#52190,.F.);
#74859=ORIENTED_EDGE('',*,*,#52201,.T.);
#74860=ORIENTED_EDGE('',*,*,#52202,.F.);
#74861=ORIENTED_EDGE('',*,*,#52198,.F.);
#74862=ORIENTED_EDGE('',*,*,#52203,.F.);
#74863=ORIENTED_EDGE('',*,*,#52204,.F.);
#74864=ORIENTED_EDGE('',*,*,#52203,.T.);
#74865=ORIENTED_EDGE('',*,*,#52201,.F.);
#74866=ORIENTED_EDGE('',*,*,#52205,.F.);
#74867=ORIENTED_EDGE('',*,*,#52205,.T.);
#74868=ORIENTED_EDGE('',*,*,#52194,.F.);
#74869=ORIENTED_EDGE('',*,*,#52206,.F.);
#74870=ORIENTED_EDGE('',*,*,#52207,.F.);
#74871=ORIENTED_EDGE('',*,*,#52208,.T.);
#74872=ORIENTED_EDGE('',*,*,#52209,.F.);
#74873=ORIENTED_EDGE('',*,*,#52210,.F.);
#74874=ORIENTED_EDGE('',*,*,#50434,.F.);
#74875=ORIENTED_EDGE('',*,*,#52211,.T.);
#74876=ORIENTED_EDGE('',*,*,#52202,.T.);
#74877=ORIENTED_EDGE('',*,*,#52208,.F.);
#74878=ORIENTED_EDGE('',*,*,#50433,.T.);
#74879=ORIENTED_EDGE('',*,*,#52212,.F.);
#74880=ORIENTED_EDGE('',*,*,#52199,.F.);
#74881=ORIENTED_EDGE('',*,*,#52211,.F.);
#74882=ORIENTED_EDGE('',*,*,#50432,.F.);
#74883=ORIENTED_EDGE('',*,*,#52212,.T.);
#74884=ORIENTED_EDGE('',*,*,#50766,.F.);
#74885=ORIENTED_EDGE('',*,*,#52213,.F.);
#74886=ORIENTED_EDGE('',*,*,#52195,.F.);
#74887=ORIENTED_EDGE('',*,*,#52213,.T.);
#74888=ORIENTED_EDGE('',*,*,#50022,.F.);
#74889=ORIENTED_EDGE('',*,*,#52214,.F.);
#74890=ORIENTED_EDGE('',*,*,#52196,.F.);
#74891=ORIENTED_EDGE('',*,*,#52214,.T.);
#74892=ORIENTED_EDGE('',*,*,#50021,.F.);
#74893=ORIENTED_EDGE('',*,*,#52215,.F.);
#74894=ORIENTED_EDGE('',*,*,#52200,.F.);
#74895=ORIENTED_EDGE('',*,*,#52215,.T.);
#74896=ORIENTED_EDGE('',*,*,#50020,.F.);
#74897=ORIENTED_EDGE('',*,*,#52216,.F.);
#74898=ORIENTED_EDGE('',*,*,#52191,.F.);
#74899=ORIENTED_EDGE('',*,*,#52217,.T.);
#74900=ORIENTED_EDGE('',*,*,#52192,.F.);
#74901=ORIENTED_EDGE('',*,*,#52216,.T.);
#74902=ORIENTED_EDGE('',*,*,#50767,.F.);
#74903=ORIENTED_EDGE('',*,*,#52218,.T.);
#74904=ORIENTED_EDGE('',*,*,#52193,.F.);
#74905=ORIENTED_EDGE('',*,*,#52217,.F.);
#74906=ORIENTED_EDGE('',*,*,#50436,.F.);
#74907=ORIENTED_EDGE('',*,*,#52210,.T.);
#74908=ORIENTED_EDGE('',*,*,#52206,.T.);
#74909=ORIENTED_EDGE('',*,*,#52218,.F.);
#74910=ORIENTED_EDGE('',*,*,#50435,.T.);
#74911=ORIENTED_EDGE('',*,*,#52204,.T.);
#74912=ORIENTED_EDGE('',*,*,#52207,.T.);
#74913=ORIENTED_EDGE('',*,*,#52209,.T.);
#74914=ORIENTED_EDGE('',*,*,#52219,.T.);
#74915=ORIENTED_EDGE('',*,*,#52220,.T.);
#74916=ORIENTED_EDGE('',*,*,#52221,.T.);
#74917=ORIENTED_EDGE('',*,*,#52222,.T.);
#74918=ORIENTED_EDGE('',*,*,#52223,.T.);
#74919=ORIENTED_EDGE('',*,*,#52224,.T.);
#74920=ORIENTED_EDGE('',*,*,#52225,.T.);
#74921=ORIENTED_EDGE('',*,*,#52226,.F.);
#74922=ORIENTED_EDGE('',*,*,#52227,.T.);
#74923=ORIENTED_EDGE('',*,*,#52228,.T.);
#74924=ORIENTED_EDGE('',*,*,#52226,.T.);
#74925=ORIENTED_EDGE('',*,*,#52229,.T.);
#74926=ORIENTED_EDGE('',*,*,#52219,.F.);
#74927=ORIENTED_EDGE('',*,*,#52230,.T.);
#74928=ORIENTED_EDGE('',*,*,#52231,.F.);
#74929=ORIENTED_EDGE('',*,*,#52227,.F.);
#74930=ORIENTED_EDGE('',*,*,#52232,.F.);
#74931=ORIENTED_EDGE('',*,*,#52233,.F.);
#74932=ORIENTED_EDGE('',*,*,#52232,.T.);
#74933=ORIENTED_EDGE('',*,*,#52230,.F.);
#74934=ORIENTED_EDGE('',*,*,#52234,.F.);
#74935=ORIENTED_EDGE('',*,*,#52234,.T.);
#74936=ORIENTED_EDGE('',*,*,#52223,.F.);
#74937=ORIENTED_EDGE('',*,*,#52235,.F.);
#74938=ORIENTED_EDGE('',*,*,#52236,.F.);
#74939=ORIENTED_EDGE('',*,*,#52237,.T.);
#74940=ORIENTED_EDGE('',*,*,#52238,.F.);
#74941=ORIENTED_EDGE('',*,*,#52239,.F.);
#74942=ORIENTED_EDGE('',*,*,#50428,.F.);
#74943=ORIENTED_EDGE('',*,*,#52240,.T.);
#74944=ORIENTED_EDGE('',*,*,#52231,.T.);
#74945=ORIENTED_EDGE('',*,*,#52237,.F.);
#74946=ORIENTED_EDGE('',*,*,#50427,.T.);
#74947=ORIENTED_EDGE('',*,*,#52241,.F.);
#74948=ORIENTED_EDGE('',*,*,#52228,.F.);
#74949=ORIENTED_EDGE('',*,*,#52240,.F.);
#74950=ORIENTED_EDGE('',*,*,#50426,.F.);
#74951=ORIENTED_EDGE('',*,*,#52241,.T.);
#74952=ORIENTED_EDGE('',*,*,#50764,.F.);
#74953=ORIENTED_EDGE('',*,*,#52242,.F.);
#74954=ORIENTED_EDGE('',*,*,#52224,.F.);
#74955=ORIENTED_EDGE('',*,*,#52242,.T.);
#74956=ORIENTED_EDGE('',*,*,#50026,.F.);
#74957=ORIENTED_EDGE('',*,*,#52243,.F.);
#74958=ORIENTED_EDGE('',*,*,#52225,.F.);
#74959=ORIENTED_EDGE('',*,*,#52243,.T.);
#74960=ORIENTED_EDGE('',*,*,#50025,.F.);
#74961=ORIENTED_EDGE('',*,*,#52244,.F.);
#74962=ORIENTED_EDGE('',*,*,#52229,.F.);
#74963=ORIENTED_EDGE('',*,*,#52244,.T.);
#74964=ORIENTED_EDGE('',*,*,#50024,.F.);
#74965=ORIENTED_EDGE('',*,*,#52245,.F.);
#74966=ORIENTED_EDGE('',*,*,#52220,.F.);
#74967=ORIENTED_EDGE('',*,*,#52246,.T.);
#74968=ORIENTED_EDGE('',*,*,#52221,.F.);
#74969=ORIENTED_EDGE('',*,*,#52245,.T.);
#74970=ORIENTED_EDGE('',*,*,#50765,.F.);
#74971=ORIENTED_EDGE('',*,*,#52247,.T.);
#74972=ORIENTED_EDGE('',*,*,#52222,.F.);
#74973=ORIENTED_EDGE('',*,*,#52246,.F.);
#74974=ORIENTED_EDGE('',*,*,#50430,.F.);
#74975=ORIENTED_EDGE('',*,*,#52239,.T.);
#74976=ORIENTED_EDGE('',*,*,#52235,.T.);
#74977=ORIENTED_EDGE('',*,*,#52247,.F.);
#74978=ORIENTED_EDGE('',*,*,#50429,.T.);
#74979=ORIENTED_EDGE('',*,*,#52233,.T.);
#74980=ORIENTED_EDGE('',*,*,#52236,.T.);
#74981=ORIENTED_EDGE('',*,*,#52238,.T.);
#74982=ORIENTED_EDGE('',*,*,#52248,.T.);
#74983=ORIENTED_EDGE('',*,*,#52249,.T.);
#74984=ORIENTED_EDGE('',*,*,#52250,.T.);
#74985=ORIENTED_EDGE('',*,*,#52251,.T.);
#74986=ORIENTED_EDGE('',*,*,#52252,.T.);
#74987=ORIENTED_EDGE('',*,*,#52253,.T.);
#74988=ORIENTED_EDGE('',*,*,#52254,.T.);
#74989=ORIENTED_EDGE('',*,*,#52255,.F.);
#74990=ORIENTED_EDGE('',*,*,#52256,.T.);
#74991=ORIENTED_EDGE('',*,*,#52257,.T.);
#74992=ORIENTED_EDGE('',*,*,#52255,.T.);
#74993=ORIENTED_EDGE('',*,*,#52258,.T.);
#74994=ORIENTED_EDGE('',*,*,#52248,.F.);
#74995=ORIENTED_EDGE('',*,*,#52259,.T.);
#74996=ORIENTED_EDGE('',*,*,#52260,.F.);
#74997=ORIENTED_EDGE('',*,*,#52256,.F.);
#74998=ORIENTED_EDGE('',*,*,#52261,.F.);
#74999=ORIENTED_EDGE('',*,*,#52262,.F.);
#75000=ORIENTED_EDGE('',*,*,#52261,.T.);
#75001=ORIENTED_EDGE('',*,*,#52259,.F.);
#75002=ORIENTED_EDGE('',*,*,#52263,.F.);
#75003=ORIENTED_EDGE('',*,*,#52263,.T.);
#75004=ORIENTED_EDGE('',*,*,#52252,.F.);
#75005=ORIENTED_EDGE('',*,*,#52264,.F.);
#75006=ORIENTED_EDGE('',*,*,#52265,.F.);
#75007=ORIENTED_EDGE('',*,*,#52266,.T.);
#75008=ORIENTED_EDGE('',*,*,#52267,.F.);
#75009=ORIENTED_EDGE('',*,*,#52268,.F.);
#75010=ORIENTED_EDGE('',*,*,#50422,.F.);
#75011=ORIENTED_EDGE('',*,*,#52269,.T.);
#75012=ORIENTED_EDGE('',*,*,#52260,.T.);
#75013=ORIENTED_EDGE('',*,*,#52266,.F.);
#75014=ORIENTED_EDGE('',*,*,#50421,.T.);
#75015=ORIENTED_EDGE('',*,*,#52270,.F.);
#75016=ORIENTED_EDGE('',*,*,#52257,.F.);
#75017=ORIENTED_EDGE('',*,*,#52269,.F.);
#75018=ORIENTED_EDGE('',*,*,#50420,.F.);
#75019=ORIENTED_EDGE('',*,*,#52270,.T.);
#75020=ORIENTED_EDGE('',*,*,#50762,.F.);
#75021=ORIENTED_EDGE('',*,*,#52271,.F.);
#75022=ORIENTED_EDGE('',*,*,#52253,.F.);
#75023=ORIENTED_EDGE('',*,*,#52271,.T.);
#75024=ORIENTED_EDGE('',*,*,#50030,.F.);
#75025=ORIENTED_EDGE('',*,*,#52272,.F.);
#75026=ORIENTED_EDGE('',*,*,#52254,.F.);
#75027=ORIENTED_EDGE('',*,*,#52272,.T.);
#75028=ORIENTED_EDGE('',*,*,#50029,.F.);
#75029=ORIENTED_EDGE('',*,*,#52273,.F.);
#75030=ORIENTED_EDGE('',*,*,#52258,.F.);
#75031=ORIENTED_EDGE('',*,*,#52273,.T.);
#75032=ORIENTED_EDGE('',*,*,#50028,.F.);
#75033=ORIENTED_EDGE('',*,*,#52274,.F.);
#75034=ORIENTED_EDGE('',*,*,#52249,.F.);
#75035=ORIENTED_EDGE('',*,*,#52275,.T.);
#75036=ORIENTED_EDGE('',*,*,#52250,.F.);
#75037=ORIENTED_EDGE('',*,*,#52274,.T.);
#75038=ORIENTED_EDGE('',*,*,#50763,.F.);
#75039=ORIENTED_EDGE('',*,*,#52276,.T.);
#75040=ORIENTED_EDGE('',*,*,#52251,.F.);
#75041=ORIENTED_EDGE('',*,*,#52275,.F.);
#75042=ORIENTED_EDGE('',*,*,#50424,.F.);
#75043=ORIENTED_EDGE('',*,*,#52268,.T.);
#75044=ORIENTED_EDGE('',*,*,#52264,.T.);
#75045=ORIENTED_EDGE('',*,*,#52276,.F.);
#75046=ORIENTED_EDGE('',*,*,#50423,.T.);
#75047=ORIENTED_EDGE('',*,*,#52262,.T.);
#75048=ORIENTED_EDGE('',*,*,#52265,.T.);
#75049=ORIENTED_EDGE('',*,*,#52267,.T.);
#75050=ORIENTED_EDGE('',*,*,#52277,.T.);
#75051=ORIENTED_EDGE('',*,*,#52278,.T.);
#75052=ORIENTED_EDGE('',*,*,#52279,.T.);
#75053=ORIENTED_EDGE('',*,*,#52280,.T.);
#75054=ORIENTED_EDGE('',*,*,#52281,.T.);
#75055=ORIENTED_EDGE('',*,*,#52282,.T.);
#75056=ORIENTED_EDGE('',*,*,#52283,.T.);
#75057=ORIENTED_EDGE('',*,*,#52284,.F.);
#75058=ORIENTED_EDGE('',*,*,#52285,.T.);
#75059=ORIENTED_EDGE('',*,*,#52286,.T.);
#75060=ORIENTED_EDGE('',*,*,#52284,.T.);
#75061=ORIENTED_EDGE('',*,*,#52287,.T.);
#75062=ORIENTED_EDGE('',*,*,#52277,.F.);
#75063=ORIENTED_EDGE('',*,*,#52288,.T.);
#75064=ORIENTED_EDGE('',*,*,#52289,.F.);
#75065=ORIENTED_EDGE('',*,*,#52285,.F.);
#75066=ORIENTED_EDGE('',*,*,#52290,.F.);
#75067=ORIENTED_EDGE('',*,*,#52291,.F.);
#75068=ORIENTED_EDGE('',*,*,#52290,.T.);
#75069=ORIENTED_EDGE('',*,*,#52288,.F.);
#75070=ORIENTED_EDGE('',*,*,#52292,.F.);
#75071=ORIENTED_EDGE('',*,*,#52292,.T.);
#75072=ORIENTED_EDGE('',*,*,#52281,.F.);
#75073=ORIENTED_EDGE('',*,*,#52293,.F.);
#75074=ORIENTED_EDGE('',*,*,#52294,.F.);
#75075=ORIENTED_EDGE('',*,*,#52295,.T.);
#75076=ORIENTED_EDGE('',*,*,#52296,.F.);
#75077=ORIENTED_EDGE('',*,*,#52297,.F.);
#75078=ORIENTED_EDGE('',*,*,#50416,.F.);
#75079=ORIENTED_EDGE('',*,*,#52298,.T.);
#75080=ORIENTED_EDGE('',*,*,#52289,.T.);
#75081=ORIENTED_EDGE('',*,*,#52295,.F.);
#75082=ORIENTED_EDGE('',*,*,#50415,.T.);
#75083=ORIENTED_EDGE('',*,*,#52299,.F.);
#75084=ORIENTED_EDGE('',*,*,#52286,.F.);
#75085=ORIENTED_EDGE('',*,*,#52298,.F.);
#75086=ORIENTED_EDGE('',*,*,#50414,.F.);
#75087=ORIENTED_EDGE('',*,*,#52299,.T.);
#75088=ORIENTED_EDGE('',*,*,#50760,.F.);
#75089=ORIENTED_EDGE('',*,*,#52300,.F.);
#75090=ORIENTED_EDGE('',*,*,#52282,.F.);
#75091=ORIENTED_EDGE('',*,*,#52300,.T.);
#75092=ORIENTED_EDGE('',*,*,#50034,.F.);
#75093=ORIENTED_EDGE('',*,*,#52301,.F.);
#75094=ORIENTED_EDGE('',*,*,#52283,.F.);
#75095=ORIENTED_EDGE('',*,*,#52301,.T.);
#75096=ORIENTED_EDGE('',*,*,#50033,.F.);
#75097=ORIENTED_EDGE('',*,*,#52302,.F.);
#75098=ORIENTED_EDGE('',*,*,#52287,.F.);
#75099=ORIENTED_EDGE('',*,*,#52302,.T.);
#75100=ORIENTED_EDGE('',*,*,#50032,.F.);
#75101=ORIENTED_EDGE('',*,*,#52303,.F.);
#75102=ORIENTED_EDGE('',*,*,#52278,.F.);
#75103=ORIENTED_EDGE('',*,*,#52304,.T.);
#75104=ORIENTED_EDGE('',*,*,#52279,.F.);
#75105=ORIENTED_EDGE('',*,*,#52303,.T.);
#75106=ORIENTED_EDGE('',*,*,#50761,.F.);
#75107=ORIENTED_EDGE('',*,*,#52305,.T.);
#75108=ORIENTED_EDGE('',*,*,#52280,.F.);
#75109=ORIENTED_EDGE('',*,*,#52304,.F.);
#75110=ORIENTED_EDGE('',*,*,#50418,.F.);
#75111=ORIENTED_EDGE('',*,*,#52297,.T.);
#75112=ORIENTED_EDGE('',*,*,#52293,.T.);
#75113=ORIENTED_EDGE('',*,*,#52305,.F.);
#75114=ORIENTED_EDGE('',*,*,#50417,.T.);
#75115=ORIENTED_EDGE('',*,*,#52291,.T.);
#75116=ORIENTED_EDGE('',*,*,#52294,.T.);
#75117=ORIENTED_EDGE('',*,*,#52296,.T.);
#75118=ORIENTED_EDGE('',*,*,#52306,.T.);
#75119=ORIENTED_EDGE('',*,*,#52307,.T.);
#75120=ORIENTED_EDGE('',*,*,#52308,.T.);
#75121=ORIENTED_EDGE('',*,*,#52309,.T.);
#75122=ORIENTED_EDGE('',*,*,#52310,.T.);
#75123=ORIENTED_EDGE('',*,*,#52311,.T.);
#75124=ORIENTED_EDGE('',*,*,#52312,.T.);
#75125=ORIENTED_EDGE('',*,*,#52313,.F.);
#75126=ORIENTED_EDGE('',*,*,#52314,.T.);
#75127=ORIENTED_EDGE('',*,*,#52315,.T.);
#75128=ORIENTED_EDGE('',*,*,#52313,.T.);
#75129=ORIENTED_EDGE('',*,*,#52316,.T.);
#75130=ORIENTED_EDGE('',*,*,#52306,.F.);
#75131=ORIENTED_EDGE('',*,*,#52317,.T.);
#75132=ORIENTED_EDGE('',*,*,#52318,.F.);
#75133=ORIENTED_EDGE('',*,*,#52314,.F.);
#75134=ORIENTED_EDGE('',*,*,#52319,.F.);
#75135=ORIENTED_EDGE('',*,*,#52320,.F.);
#75136=ORIENTED_EDGE('',*,*,#52319,.T.);
#75137=ORIENTED_EDGE('',*,*,#52317,.F.);
#75138=ORIENTED_EDGE('',*,*,#52321,.F.);
#75139=ORIENTED_EDGE('',*,*,#52321,.T.);
#75140=ORIENTED_EDGE('',*,*,#52310,.F.);
#75141=ORIENTED_EDGE('',*,*,#52322,.F.);
#75142=ORIENTED_EDGE('',*,*,#52323,.F.);
#75143=ORIENTED_EDGE('',*,*,#52324,.T.);
#75144=ORIENTED_EDGE('',*,*,#52325,.F.);
#75145=ORIENTED_EDGE('',*,*,#52326,.F.);
#75146=ORIENTED_EDGE('',*,*,#50410,.F.);
#75147=ORIENTED_EDGE('',*,*,#52327,.T.);
#75148=ORIENTED_EDGE('',*,*,#52318,.T.);
#75149=ORIENTED_EDGE('',*,*,#52324,.F.);
#75150=ORIENTED_EDGE('',*,*,#50409,.T.);
#75151=ORIENTED_EDGE('',*,*,#52328,.F.);
#75152=ORIENTED_EDGE('',*,*,#52315,.F.);
#75153=ORIENTED_EDGE('',*,*,#52327,.F.);
#75154=ORIENTED_EDGE('',*,*,#50408,.F.);
#75155=ORIENTED_EDGE('',*,*,#52328,.T.);
#75156=ORIENTED_EDGE('',*,*,#50758,.F.);
#75157=ORIENTED_EDGE('',*,*,#52329,.F.);
#75158=ORIENTED_EDGE('',*,*,#52311,.F.);
#75159=ORIENTED_EDGE('',*,*,#52329,.T.);
#75160=ORIENTED_EDGE('',*,*,#50038,.F.);
#75161=ORIENTED_EDGE('',*,*,#52330,.F.);
#75162=ORIENTED_EDGE('',*,*,#52312,.F.);
#75163=ORIENTED_EDGE('',*,*,#52330,.T.);
#75164=ORIENTED_EDGE('',*,*,#50037,.F.);
#75165=ORIENTED_EDGE('',*,*,#52331,.F.);
#75166=ORIENTED_EDGE('',*,*,#52316,.F.);
#75167=ORIENTED_EDGE('',*,*,#52331,.T.);
#75168=ORIENTED_EDGE('',*,*,#50036,.F.);
#75169=ORIENTED_EDGE('',*,*,#52332,.F.);
#75170=ORIENTED_EDGE('',*,*,#52307,.F.);
#75171=ORIENTED_EDGE('',*,*,#52333,.T.);
#75172=ORIENTED_EDGE('',*,*,#52308,.F.);
#75173=ORIENTED_EDGE('',*,*,#52332,.T.);
#75174=ORIENTED_EDGE('',*,*,#50759,.F.);
#75175=ORIENTED_EDGE('',*,*,#52334,.T.);
#75176=ORIENTED_EDGE('',*,*,#52309,.F.);
#75177=ORIENTED_EDGE('',*,*,#52333,.F.);
#75178=ORIENTED_EDGE('',*,*,#50412,.F.);
#75179=ORIENTED_EDGE('',*,*,#52326,.T.);
#75180=ORIENTED_EDGE('',*,*,#52322,.T.);
#75181=ORIENTED_EDGE('',*,*,#52334,.F.);
#75182=ORIENTED_EDGE('',*,*,#50411,.T.);
#75183=ORIENTED_EDGE('',*,*,#52320,.T.);
#75184=ORIENTED_EDGE('',*,*,#52323,.T.);
#75185=ORIENTED_EDGE('',*,*,#52325,.T.);
#75186=ORIENTED_EDGE('',*,*,#52335,.T.);
#75187=ORIENTED_EDGE('',*,*,#52336,.T.);
#75188=ORIENTED_EDGE('',*,*,#52337,.T.);
#75189=ORIENTED_EDGE('',*,*,#52338,.T.);
#75190=ORIENTED_EDGE('',*,*,#52339,.T.);
#75191=ORIENTED_EDGE('',*,*,#52340,.T.);
#75192=ORIENTED_EDGE('',*,*,#52341,.T.);
#75193=ORIENTED_EDGE('',*,*,#52342,.F.);
#75194=ORIENTED_EDGE('',*,*,#52343,.T.);
#75195=ORIENTED_EDGE('',*,*,#52344,.T.);
#75196=ORIENTED_EDGE('',*,*,#52342,.T.);
#75197=ORIENTED_EDGE('',*,*,#52345,.T.);
#75198=ORIENTED_EDGE('',*,*,#52335,.F.);
#75199=ORIENTED_EDGE('',*,*,#52346,.T.);
#75200=ORIENTED_EDGE('',*,*,#52347,.F.);
#75201=ORIENTED_EDGE('',*,*,#52343,.F.);
#75202=ORIENTED_EDGE('',*,*,#52348,.F.);
#75203=ORIENTED_EDGE('',*,*,#52349,.F.);
#75204=ORIENTED_EDGE('',*,*,#52348,.T.);
#75205=ORIENTED_EDGE('',*,*,#52346,.F.);
#75206=ORIENTED_EDGE('',*,*,#52350,.F.);
#75207=ORIENTED_EDGE('',*,*,#52350,.T.);
#75208=ORIENTED_EDGE('',*,*,#52339,.F.);
#75209=ORIENTED_EDGE('',*,*,#52351,.F.);
#75210=ORIENTED_EDGE('',*,*,#52352,.F.);
#75211=ORIENTED_EDGE('',*,*,#52353,.T.);
#75212=ORIENTED_EDGE('',*,*,#52354,.F.);
#75213=ORIENTED_EDGE('',*,*,#52355,.F.);
#75214=ORIENTED_EDGE('',*,*,#50404,.F.);
#75215=ORIENTED_EDGE('',*,*,#52356,.T.);
#75216=ORIENTED_EDGE('',*,*,#52347,.T.);
#75217=ORIENTED_EDGE('',*,*,#52353,.F.);
#75218=ORIENTED_EDGE('',*,*,#50403,.T.);
#75219=ORIENTED_EDGE('',*,*,#52357,.F.);
#75220=ORIENTED_EDGE('',*,*,#52344,.F.);
#75221=ORIENTED_EDGE('',*,*,#52356,.F.);
#75222=ORIENTED_EDGE('',*,*,#50402,.F.);
#75223=ORIENTED_EDGE('',*,*,#52357,.T.);
#75224=ORIENTED_EDGE('',*,*,#50756,.F.);
#75225=ORIENTED_EDGE('',*,*,#52358,.F.);
#75226=ORIENTED_EDGE('',*,*,#52340,.F.);
#75227=ORIENTED_EDGE('',*,*,#52358,.T.);
#75228=ORIENTED_EDGE('',*,*,#50042,.F.);
#75229=ORIENTED_EDGE('',*,*,#52359,.F.);
#75230=ORIENTED_EDGE('',*,*,#52341,.F.);
#75231=ORIENTED_EDGE('',*,*,#52359,.T.);
#75232=ORIENTED_EDGE('',*,*,#50041,.F.);
#75233=ORIENTED_EDGE('',*,*,#52360,.F.);
#75234=ORIENTED_EDGE('',*,*,#52345,.F.);
#75235=ORIENTED_EDGE('',*,*,#52360,.T.);
#75236=ORIENTED_EDGE('',*,*,#50040,.F.);
#75237=ORIENTED_EDGE('',*,*,#52361,.F.);
#75238=ORIENTED_EDGE('',*,*,#52336,.F.);
#75239=ORIENTED_EDGE('',*,*,#52362,.T.);
#75240=ORIENTED_EDGE('',*,*,#52337,.F.);
#75241=ORIENTED_EDGE('',*,*,#52361,.T.);
#75242=ORIENTED_EDGE('',*,*,#50757,.F.);
#75243=ORIENTED_EDGE('',*,*,#52363,.T.);
#75244=ORIENTED_EDGE('',*,*,#52338,.F.);
#75245=ORIENTED_EDGE('',*,*,#52362,.F.);
#75246=ORIENTED_EDGE('',*,*,#50406,.F.);
#75247=ORIENTED_EDGE('',*,*,#52355,.T.);
#75248=ORIENTED_EDGE('',*,*,#52351,.T.);
#75249=ORIENTED_EDGE('',*,*,#52363,.F.);
#75250=ORIENTED_EDGE('',*,*,#50405,.T.);
#75251=ORIENTED_EDGE('',*,*,#52349,.T.);
#75252=ORIENTED_EDGE('',*,*,#52352,.T.);
#75253=ORIENTED_EDGE('',*,*,#52354,.T.);
#75254=ORIENTED_EDGE('',*,*,#52364,.T.);
#75255=ORIENTED_EDGE('',*,*,#52365,.T.);
#75256=ORIENTED_EDGE('',*,*,#52366,.T.);
#75257=ORIENTED_EDGE('',*,*,#52367,.T.);
#75258=ORIENTED_EDGE('',*,*,#52368,.T.);
#75259=ORIENTED_EDGE('',*,*,#52369,.T.);
#75260=ORIENTED_EDGE('',*,*,#52370,.T.);
#75261=ORIENTED_EDGE('',*,*,#52371,.F.);
#75262=ORIENTED_EDGE('',*,*,#52372,.T.);
#75263=ORIENTED_EDGE('',*,*,#52373,.T.);
#75264=ORIENTED_EDGE('',*,*,#52371,.T.);
#75265=ORIENTED_EDGE('',*,*,#52374,.T.);
#75266=ORIENTED_EDGE('',*,*,#52364,.F.);
#75267=ORIENTED_EDGE('',*,*,#52375,.T.);
#75268=ORIENTED_EDGE('',*,*,#52376,.F.);
#75269=ORIENTED_EDGE('',*,*,#52372,.F.);
#75270=ORIENTED_EDGE('',*,*,#52377,.F.);
#75271=ORIENTED_EDGE('',*,*,#52378,.F.);
#75272=ORIENTED_EDGE('',*,*,#52377,.T.);
#75273=ORIENTED_EDGE('',*,*,#52375,.F.);
#75274=ORIENTED_EDGE('',*,*,#52379,.F.);
#75275=ORIENTED_EDGE('',*,*,#52379,.T.);
#75276=ORIENTED_EDGE('',*,*,#52368,.F.);
#75277=ORIENTED_EDGE('',*,*,#52380,.F.);
#75278=ORIENTED_EDGE('',*,*,#52381,.F.);
#75279=ORIENTED_EDGE('',*,*,#52382,.T.);
#75280=ORIENTED_EDGE('',*,*,#52383,.F.);
#75281=ORIENTED_EDGE('',*,*,#52384,.F.);
#75282=ORIENTED_EDGE('',*,*,#50398,.F.);
#75283=ORIENTED_EDGE('',*,*,#52385,.T.);
#75284=ORIENTED_EDGE('',*,*,#52376,.T.);
#75285=ORIENTED_EDGE('',*,*,#52382,.F.);
#75286=ORIENTED_EDGE('',*,*,#50397,.T.);
#75287=ORIENTED_EDGE('',*,*,#52386,.F.);
#75288=ORIENTED_EDGE('',*,*,#52373,.F.);
#75289=ORIENTED_EDGE('',*,*,#52385,.F.);
#75290=ORIENTED_EDGE('',*,*,#50396,.F.);
#75291=ORIENTED_EDGE('',*,*,#52386,.T.);
#75292=ORIENTED_EDGE('',*,*,#50754,.F.);
#75293=ORIENTED_EDGE('',*,*,#52387,.F.);
#75294=ORIENTED_EDGE('',*,*,#52369,.F.);
#75295=ORIENTED_EDGE('',*,*,#52387,.T.);
#75296=ORIENTED_EDGE('',*,*,#50046,.F.);
#75297=ORIENTED_EDGE('',*,*,#52388,.F.);
#75298=ORIENTED_EDGE('',*,*,#52370,.F.);
#75299=ORIENTED_EDGE('',*,*,#52388,.T.);
#75300=ORIENTED_EDGE('',*,*,#50045,.F.);
#75301=ORIENTED_EDGE('',*,*,#52389,.F.);
#75302=ORIENTED_EDGE('',*,*,#52374,.F.);
#75303=ORIENTED_EDGE('',*,*,#52389,.T.);
#75304=ORIENTED_EDGE('',*,*,#50044,.F.);
#75305=ORIENTED_EDGE('',*,*,#52390,.F.);
#75306=ORIENTED_EDGE('',*,*,#52365,.F.);
#75307=ORIENTED_EDGE('',*,*,#52391,.T.);
#75308=ORIENTED_EDGE('',*,*,#52366,.F.);
#75309=ORIENTED_EDGE('',*,*,#52390,.T.);
#75310=ORIENTED_EDGE('',*,*,#50755,.F.);
#75311=ORIENTED_EDGE('',*,*,#52392,.T.);
#75312=ORIENTED_EDGE('',*,*,#52367,.F.);
#75313=ORIENTED_EDGE('',*,*,#52391,.F.);
#75314=ORIENTED_EDGE('',*,*,#50400,.F.);
#75315=ORIENTED_EDGE('',*,*,#52384,.T.);
#75316=ORIENTED_EDGE('',*,*,#52380,.T.);
#75317=ORIENTED_EDGE('',*,*,#52392,.F.);
#75318=ORIENTED_EDGE('',*,*,#50399,.T.);
#75319=ORIENTED_EDGE('',*,*,#52378,.T.);
#75320=ORIENTED_EDGE('',*,*,#52381,.T.);
#75321=ORIENTED_EDGE('',*,*,#52383,.T.);
#75322=ORIENTED_EDGE('',*,*,#52393,.T.);
#75323=ORIENTED_EDGE('',*,*,#52394,.T.);
#75324=ORIENTED_EDGE('',*,*,#52395,.T.);
#75325=ORIENTED_EDGE('',*,*,#52396,.T.);
#75326=ORIENTED_EDGE('',*,*,#52397,.T.);
#75327=ORIENTED_EDGE('',*,*,#52398,.T.);
#75328=ORIENTED_EDGE('',*,*,#52399,.T.);
#75329=ORIENTED_EDGE('',*,*,#52400,.F.);
#75330=ORIENTED_EDGE('',*,*,#52401,.T.);
#75331=ORIENTED_EDGE('',*,*,#52402,.T.);
#75332=ORIENTED_EDGE('',*,*,#52400,.T.);
#75333=ORIENTED_EDGE('',*,*,#52403,.T.);
#75334=ORIENTED_EDGE('',*,*,#52393,.F.);
#75335=ORIENTED_EDGE('',*,*,#52404,.T.);
#75336=ORIENTED_EDGE('',*,*,#52405,.F.);
#75337=ORIENTED_EDGE('',*,*,#52401,.F.);
#75338=ORIENTED_EDGE('',*,*,#52406,.F.);
#75339=ORIENTED_EDGE('',*,*,#52407,.F.);
#75340=ORIENTED_EDGE('',*,*,#52406,.T.);
#75341=ORIENTED_EDGE('',*,*,#52404,.F.);
#75342=ORIENTED_EDGE('',*,*,#52408,.F.);
#75343=ORIENTED_EDGE('',*,*,#52408,.T.);
#75344=ORIENTED_EDGE('',*,*,#52397,.F.);
#75345=ORIENTED_EDGE('',*,*,#52409,.F.);
#75346=ORIENTED_EDGE('',*,*,#52410,.F.);
#75347=ORIENTED_EDGE('',*,*,#52411,.T.);
#75348=ORIENTED_EDGE('',*,*,#52412,.F.);
#75349=ORIENTED_EDGE('',*,*,#52413,.F.);
#75350=ORIENTED_EDGE('',*,*,#50392,.F.);
#75351=ORIENTED_EDGE('',*,*,#52414,.T.);
#75352=ORIENTED_EDGE('',*,*,#52405,.T.);
#75353=ORIENTED_EDGE('',*,*,#52411,.F.);
#75354=ORIENTED_EDGE('',*,*,#50391,.T.);
#75355=ORIENTED_EDGE('',*,*,#52415,.F.);
#75356=ORIENTED_EDGE('',*,*,#52402,.F.);
#75357=ORIENTED_EDGE('',*,*,#52414,.F.);
#75358=ORIENTED_EDGE('',*,*,#50390,.F.);
#75359=ORIENTED_EDGE('',*,*,#52415,.T.);
#75360=ORIENTED_EDGE('',*,*,#50752,.F.);
#75361=ORIENTED_EDGE('',*,*,#52416,.F.);
#75362=ORIENTED_EDGE('',*,*,#52398,.F.);
#75363=ORIENTED_EDGE('',*,*,#52416,.T.);
#75364=ORIENTED_EDGE('',*,*,#50050,.F.);
#75365=ORIENTED_EDGE('',*,*,#52417,.F.);
#75366=ORIENTED_EDGE('',*,*,#52399,.F.);
#75367=ORIENTED_EDGE('',*,*,#52417,.T.);
#75368=ORIENTED_EDGE('',*,*,#50049,.F.);
#75369=ORIENTED_EDGE('',*,*,#52418,.F.);
#75370=ORIENTED_EDGE('',*,*,#52403,.F.);
#75371=ORIENTED_EDGE('',*,*,#52418,.T.);
#75372=ORIENTED_EDGE('',*,*,#50048,.F.);
#75373=ORIENTED_EDGE('',*,*,#52419,.F.);
#75374=ORIENTED_EDGE('',*,*,#52394,.F.);
#75375=ORIENTED_EDGE('',*,*,#52420,.T.);
#75376=ORIENTED_EDGE('',*,*,#52395,.F.);
#75377=ORIENTED_EDGE('',*,*,#52419,.T.);
#75378=ORIENTED_EDGE('',*,*,#50753,.F.);
#75379=ORIENTED_EDGE('',*,*,#52421,.T.);
#75380=ORIENTED_EDGE('',*,*,#52396,.F.);
#75381=ORIENTED_EDGE('',*,*,#52420,.F.);
#75382=ORIENTED_EDGE('',*,*,#50394,.F.);
#75383=ORIENTED_EDGE('',*,*,#52413,.T.);
#75384=ORIENTED_EDGE('',*,*,#52409,.T.);
#75385=ORIENTED_EDGE('',*,*,#52421,.F.);
#75386=ORIENTED_EDGE('',*,*,#50393,.T.);
#75387=ORIENTED_EDGE('',*,*,#52407,.T.);
#75388=ORIENTED_EDGE('',*,*,#52410,.T.);
#75389=ORIENTED_EDGE('',*,*,#52412,.T.);
#75390=ORIENTED_EDGE('',*,*,#52422,.T.);
#75391=ORIENTED_EDGE('',*,*,#52423,.T.);
#75392=ORIENTED_EDGE('',*,*,#52424,.T.);
#75393=ORIENTED_EDGE('',*,*,#52425,.T.);
#75394=ORIENTED_EDGE('',*,*,#52426,.T.);
#75395=ORIENTED_EDGE('',*,*,#52427,.T.);
#75396=ORIENTED_EDGE('',*,*,#52428,.T.);
#75397=ORIENTED_EDGE('',*,*,#52429,.F.);
#75398=ORIENTED_EDGE('',*,*,#52430,.T.);
#75399=ORIENTED_EDGE('',*,*,#52431,.T.);
#75400=ORIENTED_EDGE('',*,*,#52429,.T.);
#75401=ORIENTED_EDGE('',*,*,#52432,.T.);
#75402=ORIENTED_EDGE('',*,*,#52422,.F.);
#75403=ORIENTED_EDGE('',*,*,#52433,.T.);
#75404=ORIENTED_EDGE('',*,*,#52434,.F.);
#75405=ORIENTED_EDGE('',*,*,#52430,.F.);
#75406=ORIENTED_EDGE('',*,*,#52435,.F.);
#75407=ORIENTED_EDGE('',*,*,#52436,.F.);
#75408=ORIENTED_EDGE('',*,*,#52435,.T.);
#75409=ORIENTED_EDGE('',*,*,#52433,.F.);
#75410=ORIENTED_EDGE('',*,*,#52437,.F.);
#75411=ORIENTED_EDGE('',*,*,#52437,.T.);
#75412=ORIENTED_EDGE('',*,*,#52426,.F.);
#75413=ORIENTED_EDGE('',*,*,#52438,.F.);
#75414=ORIENTED_EDGE('',*,*,#52439,.F.);
#75415=ORIENTED_EDGE('',*,*,#52440,.T.);
#75416=ORIENTED_EDGE('',*,*,#52441,.F.);
#75417=ORIENTED_EDGE('',*,*,#52442,.F.);
#75418=ORIENTED_EDGE('',*,*,#50386,.F.);
#75419=ORIENTED_EDGE('',*,*,#52443,.T.);
#75420=ORIENTED_EDGE('',*,*,#52434,.T.);
#75421=ORIENTED_EDGE('',*,*,#52440,.F.);
#75422=ORIENTED_EDGE('',*,*,#50385,.T.);
#75423=ORIENTED_EDGE('',*,*,#52444,.F.);
#75424=ORIENTED_EDGE('',*,*,#52431,.F.);
#75425=ORIENTED_EDGE('',*,*,#52443,.F.);
#75426=ORIENTED_EDGE('',*,*,#50384,.F.);
#75427=ORIENTED_EDGE('',*,*,#52444,.T.);
#75428=ORIENTED_EDGE('',*,*,#50750,.F.);
#75429=ORIENTED_EDGE('',*,*,#52445,.F.);
#75430=ORIENTED_EDGE('',*,*,#52427,.F.);
#75431=ORIENTED_EDGE('',*,*,#52445,.T.);
#75432=ORIENTED_EDGE('',*,*,#50054,.F.);
#75433=ORIENTED_EDGE('',*,*,#52446,.F.);
#75434=ORIENTED_EDGE('',*,*,#52428,.F.);
#75435=ORIENTED_EDGE('',*,*,#52446,.T.);
#75436=ORIENTED_EDGE('',*,*,#50053,.F.);
#75437=ORIENTED_EDGE('',*,*,#52447,.F.);
#75438=ORIENTED_EDGE('',*,*,#52432,.F.);
#75439=ORIENTED_EDGE('',*,*,#52447,.T.);
#75440=ORIENTED_EDGE('',*,*,#50052,.F.);
#75441=ORIENTED_EDGE('',*,*,#52448,.F.);
#75442=ORIENTED_EDGE('',*,*,#52423,.F.);
#75443=ORIENTED_EDGE('',*,*,#52449,.T.);
#75444=ORIENTED_EDGE('',*,*,#52424,.F.);
#75445=ORIENTED_EDGE('',*,*,#52448,.T.);
#75446=ORIENTED_EDGE('',*,*,#50751,.F.);
#75447=ORIENTED_EDGE('',*,*,#52450,.T.);
#75448=ORIENTED_EDGE('',*,*,#52425,.F.);
#75449=ORIENTED_EDGE('',*,*,#52449,.F.);
#75450=ORIENTED_EDGE('',*,*,#50388,.F.);
#75451=ORIENTED_EDGE('',*,*,#52442,.T.);
#75452=ORIENTED_EDGE('',*,*,#52438,.T.);
#75453=ORIENTED_EDGE('',*,*,#52450,.F.);
#75454=ORIENTED_EDGE('',*,*,#50387,.T.);
#75455=ORIENTED_EDGE('',*,*,#52436,.T.);
#75456=ORIENTED_EDGE('',*,*,#52439,.T.);
#75457=ORIENTED_EDGE('',*,*,#52441,.T.);
#75458=ORIENTED_EDGE('',*,*,#52451,.T.);
#75459=ORIENTED_EDGE('',*,*,#52452,.T.);
#75460=ORIENTED_EDGE('',*,*,#52453,.T.);
#75461=ORIENTED_EDGE('',*,*,#52454,.T.);
#75462=ORIENTED_EDGE('',*,*,#52455,.T.);
#75463=ORIENTED_EDGE('',*,*,#52456,.T.);
#75464=ORIENTED_EDGE('',*,*,#52457,.T.);
#75465=ORIENTED_EDGE('',*,*,#52458,.F.);
#75466=ORIENTED_EDGE('',*,*,#52459,.T.);
#75467=ORIENTED_EDGE('',*,*,#52460,.T.);
#75468=ORIENTED_EDGE('',*,*,#52458,.T.);
#75469=ORIENTED_EDGE('',*,*,#52461,.T.);
#75470=ORIENTED_EDGE('',*,*,#52451,.F.);
#75471=ORIENTED_EDGE('',*,*,#52462,.T.);
#75472=ORIENTED_EDGE('',*,*,#52463,.F.);
#75473=ORIENTED_EDGE('',*,*,#52459,.F.);
#75474=ORIENTED_EDGE('',*,*,#52464,.F.);
#75475=ORIENTED_EDGE('',*,*,#52465,.F.);
#75476=ORIENTED_EDGE('',*,*,#52464,.T.);
#75477=ORIENTED_EDGE('',*,*,#52462,.F.);
#75478=ORIENTED_EDGE('',*,*,#52466,.F.);
#75479=ORIENTED_EDGE('',*,*,#52466,.T.);
#75480=ORIENTED_EDGE('',*,*,#52455,.F.);
#75481=ORIENTED_EDGE('',*,*,#52467,.F.);
#75482=ORIENTED_EDGE('',*,*,#52468,.F.);
#75483=ORIENTED_EDGE('',*,*,#52469,.T.);
#75484=ORIENTED_EDGE('',*,*,#52470,.F.);
#75485=ORIENTED_EDGE('',*,*,#52471,.F.);
#75486=ORIENTED_EDGE('',*,*,#50380,.F.);
#75487=ORIENTED_EDGE('',*,*,#52472,.T.);
#75488=ORIENTED_EDGE('',*,*,#52463,.T.);
#75489=ORIENTED_EDGE('',*,*,#52469,.F.);
#75490=ORIENTED_EDGE('',*,*,#50379,.T.);
#75491=ORIENTED_EDGE('',*,*,#52473,.F.);
#75492=ORIENTED_EDGE('',*,*,#52460,.F.);
#75493=ORIENTED_EDGE('',*,*,#52472,.F.);
#75494=ORIENTED_EDGE('',*,*,#50378,.F.);
#75495=ORIENTED_EDGE('',*,*,#52473,.T.);
#75496=ORIENTED_EDGE('',*,*,#50748,.F.);
#75497=ORIENTED_EDGE('',*,*,#52474,.F.);
#75498=ORIENTED_EDGE('',*,*,#52456,.F.);
#75499=ORIENTED_EDGE('',*,*,#52474,.T.);
#75500=ORIENTED_EDGE('',*,*,#50058,.F.);
#75501=ORIENTED_EDGE('',*,*,#52475,.F.);
#75502=ORIENTED_EDGE('',*,*,#52457,.F.);
#75503=ORIENTED_EDGE('',*,*,#52475,.T.);
#75504=ORIENTED_EDGE('',*,*,#50057,.F.);
#75505=ORIENTED_EDGE('',*,*,#52476,.F.);
#75506=ORIENTED_EDGE('',*,*,#52461,.F.);
#75507=ORIENTED_EDGE('',*,*,#52476,.T.);
#75508=ORIENTED_EDGE('',*,*,#50056,.F.);
#75509=ORIENTED_EDGE('',*,*,#52477,.F.);
#75510=ORIENTED_EDGE('',*,*,#52452,.F.);
#75511=ORIENTED_EDGE('',*,*,#52478,.T.);
#75512=ORIENTED_EDGE('',*,*,#52453,.F.);
#75513=ORIENTED_EDGE('',*,*,#52477,.T.);
#75514=ORIENTED_EDGE('',*,*,#50749,.F.);
#75515=ORIENTED_EDGE('',*,*,#52479,.T.);
#75516=ORIENTED_EDGE('',*,*,#52454,.F.);
#75517=ORIENTED_EDGE('',*,*,#52478,.F.);
#75518=ORIENTED_EDGE('',*,*,#50382,.F.);
#75519=ORIENTED_EDGE('',*,*,#52471,.T.);
#75520=ORIENTED_EDGE('',*,*,#52467,.T.);
#75521=ORIENTED_EDGE('',*,*,#52479,.F.);
#75522=ORIENTED_EDGE('',*,*,#50381,.T.);
#75523=ORIENTED_EDGE('',*,*,#52465,.T.);
#75524=ORIENTED_EDGE('',*,*,#52468,.T.);
#75525=ORIENTED_EDGE('',*,*,#52470,.T.);
#75526=ORIENTED_EDGE('',*,*,#52480,.T.);
#75527=ORIENTED_EDGE('',*,*,#52481,.T.);
#75528=ORIENTED_EDGE('',*,*,#52482,.T.);
#75529=ORIENTED_EDGE('',*,*,#52483,.T.);
#75530=ORIENTED_EDGE('',*,*,#52484,.T.);
#75531=ORIENTED_EDGE('',*,*,#52485,.T.);
#75532=ORIENTED_EDGE('',*,*,#52486,.T.);
#75533=ORIENTED_EDGE('',*,*,#52487,.F.);
#75534=ORIENTED_EDGE('',*,*,#52488,.T.);
#75535=ORIENTED_EDGE('',*,*,#52489,.T.);
#75536=ORIENTED_EDGE('',*,*,#52487,.T.);
#75537=ORIENTED_EDGE('',*,*,#52490,.T.);
#75538=ORIENTED_EDGE('',*,*,#52480,.F.);
#75539=ORIENTED_EDGE('',*,*,#52491,.T.);
#75540=ORIENTED_EDGE('',*,*,#52492,.F.);
#75541=ORIENTED_EDGE('',*,*,#52488,.F.);
#75542=ORIENTED_EDGE('',*,*,#52493,.F.);
#75543=ORIENTED_EDGE('',*,*,#52494,.F.);
#75544=ORIENTED_EDGE('',*,*,#52493,.T.);
#75545=ORIENTED_EDGE('',*,*,#52491,.F.);
#75546=ORIENTED_EDGE('',*,*,#52495,.F.);
#75547=ORIENTED_EDGE('',*,*,#52495,.T.);
#75548=ORIENTED_EDGE('',*,*,#52484,.F.);
#75549=ORIENTED_EDGE('',*,*,#52496,.F.);
#75550=ORIENTED_EDGE('',*,*,#52497,.F.);
#75551=ORIENTED_EDGE('',*,*,#52498,.T.);
#75552=ORIENTED_EDGE('',*,*,#52499,.F.);
#75553=ORIENTED_EDGE('',*,*,#52500,.F.);
#75554=ORIENTED_EDGE('',*,*,#50374,.F.);
#75555=ORIENTED_EDGE('',*,*,#52501,.T.);
#75556=ORIENTED_EDGE('',*,*,#52492,.T.);
#75557=ORIENTED_EDGE('',*,*,#52498,.F.);
#75558=ORIENTED_EDGE('',*,*,#50373,.T.);
#75559=ORIENTED_EDGE('',*,*,#52502,.F.);
#75560=ORIENTED_EDGE('',*,*,#52489,.F.);
#75561=ORIENTED_EDGE('',*,*,#52501,.F.);
#75562=ORIENTED_EDGE('',*,*,#50372,.F.);
#75563=ORIENTED_EDGE('',*,*,#52502,.T.);
#75564=ORIENTED_EDGE('',*,*,#50746,.F.);
#75565=ORIENTED_EDGE('',*,*,#52503,.F.);
#75566=ORIENTED_EDGE('',*,*,#52485,.F.);
#75567=ORIENTED_EDGE('',*,*,#52503,.T.);
#75568=ORIENTED_EDGE('',*,*,#50062,.F.);
#75569=ORIENTED_EDGE('',*,*,#52504,.F.);
#75570=ORIENTED_EDGE('',*,*,#52486,.F.);
#75571=ORIENTED_EDGE('',*,*,#52504,.T.);
#75572=ORIENTED_EDGE('',*,*,#50061,.F.);
#75573=ORIENTED_EDGE('',*,*,#52505,.F.);
#75574=ORIENTED_EDGE('',*,*,#52490,.F.);
#75575=ORIENTED_EDGE('',*,*,#52505,.T.);
#75576=ORIENTED_EDGE('',*,*,#50060,.F.);
#75577=ORIENTED_EDGE('',*,*,#52506,.F.);
#75578=ORIENTED_EDGE('',*,*,#52481,.F.);
#75579=ORIENTED_EDGE('',*,*,#52507,.T.);
#75580=ORIENTED_EDGE('',*,*,#52482,.F.);
#75581=ORIENTED_EDGE('',*,*,#52506,.T.);
#75582=ORIENTED_EDGE('',*,*,#50747,.F.);
#75583=ORIENTED_EDGE('',*,*,#52508,.T.);
#75584=ORIENTED_EDGE('',*,*,#52483,.F.);
#75585=ORIENTED_EDGE('',*,*,#52507,.F.);
#75586=ORIENTED_EDGE('',*,*,#50376,.F.);
#75587=ORIENTED_EDGE('',*,*,#52500,.T.);
#75588=ORIENTED_EDGE('',*,*,#52496,.T.);
#75589=ORIENTED_EDGE('',*,*,#52508,.F.);
#75590=ORIENTED_EDGE('',*,*,#50375,.T.);
#75591=ORIENTED_EDGE('',*,*,#52494,.T.);
#75592=ORIENTED_EDGE('',*,*,#52497,.T.);
#75593=ORIENTED_EDGE('',*,*,#52499,.T.);
#75594=ORIENTED_EDGE('',*,*,#52509,.T.);
#75595=ORIENTED_EDGE('',*,*,#52510,.T.);
#75596=ORIENTED_EDGE('',*,*,#52511,.T.);
#75597=ORIENTED_EDGE('',*,*,#52512,.T.);
#75598=ORIENTED_EDGE('',*,*,#52513,.T.);
#75599=ORIENTED_EDGE('',*,*,#52514,.T.);
#75600=ORIENTED_EDGE('',*,*,#52515,.T.);
#75601=ORIENTED_EDGE('',*,*,#52516,.F.);
#75602=ORIENTED_EDGE('',*,*,#52517,.T.);
#75603=ORIENTED_EDGE('',*,*,#52518,.T.);
#75604=ORIENTED_EDGE('',*,*,#52516,.T.);
#75605=ORIENTED_EDGE('',*,*,#52519,.T.);
#75606=ORIENTED_EDGE('',*,*,#52509,.F.);
#75607=ORIENTED_EDGE('',*,*,#52520,.T.);
#75608=ORIENTED_EDGE('',*,*,#52521,.F.);
#75609=ORIENTED_EDGE('',*,*,#52517,.F.);
#75610=ORIENTED_EDGE('',*,*,#52522,.F.);
#75611=ORIENTED_EDGE('',*,*,#52523,.F.);
#75612=ORIENTED_EDGE('',*,*,#52522,.T.);
#75613=ORIENTED_EDGE('',*,*,#52520,.F.);
#75614=ORIENTED_EDGE('',*,*,#52524,.F.);
#75615=ORIENTED_EDGE('',*,*,#52524,.T.);
#75616=ORIENTED_EDGE('',*,*,#52513,.F.);
#75617=ORIENTED_EDGE('',*,*,#52525,.F.);
#75618=ORIENTED_EDGE('',*,*,#52526,.F.);
#75619=ORIENTED_EDGE('',*,*,#52527,.T.);
#75620=ORIENTED_EDGE('',*,*,#52528,.F.);
#75621=ORIENTED_EDGE('',*,*,#52529,.F.);
#75622=ORIENTED_EDGE('',*,*,#50368,.F.);
#75623=ORIENTED_EDGE('',*,*,#52530,.T.);
#75624=ORIENTED_EDGE('',*,*,#52521,.T.);
#75625=ORIENTED_EDGE('',*,*,#52527,.F.);
#75626=ORIENTED_EDGE('',*,*,#50367,.T.);
#75627=ORIENTED_EDGE('',*,*,#52531,.F.);
#75628=ORIENTED_EDGE('',*,*,#52518,.F.);
#75629=ORIENTED_EDGE('',*,*,#52530,.F.);
#75630=ORIENTED_EDGE('',*,*,#50366,.F.);
#75631=ORIENTED_EDGE('',*,*,#52531,.T.);
#75632=ORIENTED_EDGE('',*,*,#50744,.F.);
#75633=ORIENTED_EDGE('',*,*,#52532,.F.);
#75634=ORIENTED_EDGE('',*,*,#52514,.F.);
#75635=ORIENTED_EDGE('',*,*,#52532,.T.);
#75636=ORIENTED_EDGE('',*,*,#50066,.F.);
#75637=ORIENTED_EDGE('',*,*,#52533,.F.);
#75638=ORIENTED_EDGE('',*,*,#52515,.F.);
#75639=ORIENTED_EDGE('',*,*,#52533,.T.);
#75640=ORIENTED_EDGE('',*,*,#50065,.F.);
#75641=ORIENTED_EDGE('',*,*,#52534,.F.);
#75642=ORIENTED_EDGE('',*,*,#52519,.F.);
#75643=ORIENTED_EDGE('',*,*,#52534,.T.);
#75644=ORIENTED_EDGE('',*,*,#50064,.F.);
#75645=ORIENTED_EDGE('',*,*,#52535,.F.);
#75646=ORIENTED_EDGE('',*,*,#52510,.F.);
#75647=ORIENTED_EDGE('',*,*,#52536,.T.);
#75648=ORIENTED_EDGE('',*,*,#52511,.F.);
#75649=ORIENTED_EDGE('',*,*,#52535,.T.);
#75650=ORIENTED_EDGE('',*,*,#50745,.F.);
#75651=ORIENTED_EDGE('',*,*,#52537,.T.);
#75652=ORIENTED_EDGE('',*,*,#52512,.F.);
#75653=ORIENTED_EDGE('',*,*,#52536,.F.);
#75654=ORIENTED_EDGE('',*,*,#50370,.F.);
#75655=ORIENTED_EDGE('',*,*,#52529,.T.);
#75656=ORIENTED_EDGE('',*,*,#52525,.T.);
#75657=ORIENTED_EDGE('',*,*,#52537,.F.);
#75658=ORIENTED_EDGE('',*,*,#50369,.T.);
#75659=ORIENTED_EDGE('',*,*,#52523,.T.);
#75660=ORIENTED_EDGE('',*,*,#52526,.T.);
#75661=ORIENTED_EDGE('',*,*,#52528,.T.);
#75662=ORIENTED_EDGE('',*,*,#52538,.T.);
#75663=ORIENTED_EDGE('',*,*,#52539,.T.);
#75664=ORIENTED_EDGE('',*,*,#52540,.T.);
#75665=ORIENTED_EDGE('',*,*,#52541,.T.);
#75666=ORIENTED_EDGE('',*,*,#52542,.T.);
#75667=ORIENTED_EDGE('',*,*,#52543,.T.);
#75668=ORIENTED_EDGE('',*,*,#52544,.T.);
#75669=ORIENTED_EDGE('',*,*,#52545,.F.);
#75670=ORIENTED_EDGE('',*,*,#52546,.T.);
#75671=ORIENTED_EDGE('',*,*,#52547,.T.);
#75672=ORIENTED_EDGE('',*,*,#52545,.T.);
#75673=ORIENTED_EDGE('',*,*,#52548,.T.);
#75674=ORIENTED_EDGE('',*,*,#52538,.F.);
#75675=ORIENTED_EDGE('',*,*,#52549,.T.);
#75676=ORIENTED_EDGE('',*,*,#52550,.F.);
#75677=ORIENTED_EDGE('',*,*,#52546,.F.);
#75678=ORIENTED_EDGE('',*,*,#52551,.F.);
#75679=ORIENTED_EDGE('',*,*,#52552,.F.);
#75680=ORIENTED_EDGE('',*,*,#52551,.T.);
#75681=ORIENTED_EDGE('',*,*,#52549,.F.);
#75682=ORIENTED_EDGE('',*,*,#52553,.F.);
#75683=ORIENTED_EDGE('',*,*,#52553,.T.);
#75684=ORIENTED_EDGE('',*,*,#52542,.F.);
#75685=ORIENTED_EDGE('',*,*,#52554,.F.);
#75686=ORIENTED_EDGE('',*,*,#52555,.F.);
#75687=ORIENTED_EDGE('',*,*,#52556,.T.);
#75688=ORIENTED_EDGE('',*,*,#52557,.F.);
#75689=ORIENTED_EDGE('',*,*,#52558,.F.);
#75690=ORIENTED_EDGE('',*,*,#50360,.F.);
#75691=ORIENTED_EDGE('',*,*,#52559,.T.);
#75692=ORIENTED_EDGE('',*,*,#52550,.T.);
#75693=ORIENTED_EDGE('',*,*,#52556,.F.);
#75694=ORIENTED_EDGE('',*,*,#50359,.T.);
#75695=ORIENTED_EDGE('',*,*,#52560,.F.);
#75696=ORIENTED_EDGE('',*,*,#52547,.F.);
#75697=ORIENTED_EDGE('',*,*,#52559,.F.);
#75698=ORIENTED_EDGE('',*,*,#50358,.F.);
#75699=ORIENTED_EDGE('',*,*,#52560,.T.);
#75700=ORIENTED_EDGE('',*,*,#50742,.F.);
#75701=ORIENTED_EDGE('',*,*,#52561,.F.);
#75702=ORIENTED_EDGE('',*,*,#52543,.F.);
#75703=ORIENTED_EDGE('',*,*,#52561,.T.);
#75704=ORIENTED_EDGE('',*,*,#49674,.F.);
#75705=ORIENTED_EDGE('',*,*,#52562,.F.);
#75706=ORIENTED_EDGE('',*,*,#52544,.F.);
#75707=ORIENTED_EDGE('',*,*,#52562,.T.);
#75708=ORIENTED_EDGE('',*,*,#49673,.F.);
#75709=ORIENTED_EDGE('',*,*,#52563,.F.);
#75710=ORIENTED_EDGE('',*,*,#52548,.F.);
#75711=ORIENTED_EDGE('',*,*,#52563,.T.);
#75712=ORIENTED_EDGE('',*,*,#49672,.F.);
#75713=ORIENTED_EDGE('',*,*,#52564,.F.);
#75714=ORIENTED_EDGE('',*,*,#52539,.F.);
#75715=ORIENTED_EDGE('',*,*,#52565,.T.);
#75716=ORIENTED_EDGE('',*,*,#52540,.F.);
#75717=ORIENTED_EDGE('',*,*,#52564,.T.);
#75718=ORIENTED_EDGE('',*,*,#50743,.F.);
#75719=ORIENTED_EDGE('',*,*,#52566,.T.);
#75720=ORIENTED_EDGE('',*,*,#52541,.F.);
#75721=ORIENTED_EDGE('',*,*,#52565,.F.);
#75722=ORIENTED_EDGE('',*,*,#50362,.F.);
#75723=ORIENTED_EDGE('',*,*,#52558,.T.);
#75724=ORIENTED_EDGE('',*,*,#52554,.T.);
#75725=ORIENTED_EDGE('',*,*,#52566,.F.);
#75726=ORIENTED_EDGE('',*,*,#50361,.T.);
#75727=ORIENTED_EDGE('',*,*,#52552,.T.);
#75728=ORIENTED_EDGE('',*,*,#52555,.T.);
#75729=ORIENTED_EDGE('',*,*,#52557,.T.);
#75730=ORIENTED_EDGE('',*,*,#52567,.T.);
#75731=ORIENTED_EDGE('',*,*,#52568,.T.);
#75732=ORIENTED_EDGE('',*,*,#52569,.T.);
#75733=ORIENTED_EDGE('',*,*,#52570,.T.);
#75734=ORIENTED_EDGE('',*,*,#52571,.T.);
#75735=ORIENTED_EDGE('',*,*,#52572,.T.);
#75736=ORIENTED_EDGE('',*,*,#52573,.T.);
#75737=ORIENTED_EDGE('',*,*,#52574,.F.);
#75738=ORIENTED_EDGE('',*,*,#52575,.T.);
#75739=ORIENTED_EDGE('',*,*,#52576,.T.);
#75740=ORIENTED_EDGE('',*,*,#52574,.T.);
#75741=ORIENTED_EDGE('',*,*,#52577,.T.);
#75742=ORIENTED_EDGE('',*,*,#52567,.F.);
#75743=ORIENTED_EDGE('',*,*,#52578,.T.);
#75744=ORIENTED_EDGE('',*,*,#52579,.F.);
#75745=ORIENTED_EDGE('',*,*,#52575,.F.);
#75746=ORIENTED_EDGE('',*,*,#52580,.F.);
#75747=ORIENTED_EDGE('',*,*,#52581,.F.);
#75748=ORIENTED_EDGE('',*,*,#52580,.T.);
#75749=ORIENTED_EDGE('',*,*,#52578,.F.);
#75750=ORIENTED_EDGE('',*,*,#52582,.F.);
#75751=ORIENTED_EDGE('',*,*,#52582,.T.);
#75752=ORIENTED_EDGE('',*,*,#52571,.F.);
#75753=ORIENTED_EDGE('',*,*,#52583,.F.);
#75754=ORIENTED_EDGE('',*,*,#52584,.F.);
#75755=ORIENTED_EDGE('',*,*,#52585,.T.);
#75756=ORIENTED_EDGE('',*,*,#52586,.F.);
#75757=ORIENTED_EDGE('',*,*,#52587,.F.);
#75758=ORIENTED_EDGE('',*,*,#50354,.F.);
#75759=ORIENTED_EDGE('',*,*,#52588,.T.);
#75760=ORIENTED_EDGE('',*,*,#52579,.T.);
#75761=ORIENTED_EDGE('',*,*,#52585,.F.);
#75762=ORIENTED_EDGE('',*,*,#50353,.T.);
#75763=ORIENTED_EDGE('',*,*,#52589,.F.);
#75764=ORIENTED_EDGE('',*,*,#52576,.F.);
#75765=ORIENTED_EDGE('',*,*,#52588,.F.);
#75766=ORIENTED_EDGE('',*,*,#50352,.F.);
#75767=ORIENTED_EDGE('',*,*,#52589,.T.);
#75768=ORIENTED_EDGE('',*,*,#50740,.F.);
#75769=ORIENTED_EDGE('',*,*,#52590,.F.);
#75770=ORIENTED_EDGE('',*,*,#52572,.F.);
#75771=ORIENTED_EDGE('',*,*,#52590,.T.);
#75772=ORIENTED_EDGE('',*,*,#49678,.F.);
#75773=ORIENTED_EDGE('',*,*,#52591,.F.);
#75774=ORIENTED_EDGE('',*,*,#52573,.F.);
#75775=ORIENTED_EDGE('',*,*,#52591,.T.);
#75776=ORIENTED_EDGE('',*,*,#49677,.F.);
#75777=ORIENTED_EDGE('',*,*,#52592,.F.);
#75778=ORIENTED_EDGE('',*,*,#52577,.F.);
#75779=ORIENTED_EDGE('',*,*,#52592,.T.);
#75780=ORIENTED_EDGE('',*,*,#49676,.F.);
#75781=ORIENTED_EDGE('',*,*,#52593,.F.);
#75782=ORIENTED_EDGE('',*,*,#52568,.F.);
#75783=ORIENTED_EDGE('',*,*,#52594,.T.);
#75784=ORIENTED_EDGE('',*,*,#52569,.F.);
#75785=ORIENTED_EDGE('',*,*,#52593,.T.);
#75786=ORIENTED_EDGE('',*,*,#50741,.F.);
#75787=ORIENTED_EDGE('',*,*,#52595,.T.);
#75788=ORIENTED_EDGE('',*,*,#52570,.F.);
#75789=ORIENTED_EDGE('',*,*,#52594,.F.);
#75790=ORIENTED_EDGE('',*,*,#50356,.F.);
#75791=ORIENTED_EDGE('',*,*,#52587,.T.);
#75792=ORIENTED_EDGE('',*,*,#52583,.T.);
#75793=ORIENTED_EDGE('',*,*,#52595,.F.);
#75794=ORIENTED_EDGE('',*,*,#50355,.T.);
#75795=ORIENTED_EDGE('',*,*,#52581,.T.);
#75796=ORIENTED_EDGE('',*,*,#52584,.T.);
#75797=ORIENTED_EDGE('',*,*,#52586,.T.);
#75798=ORIENTED_EDGE('',*,*,#52596,.T.);
#75799=ORIENTED_EDGE('',*,*,#52597,.T.);
#75800=ORIENTED_EDGE('',*,*,#52598,.T.);
#75801=ORIENTED_EDGE('',*,*,#52599,.T.);
#75802=ORIENTED_EDGE('',*,*,#52600,.T.);
#75803=ORIENTED_EDGE('',*,*,#52601,.T.);
#75804=ORIENTED_EDGE('',*,*,#52602,.T.);
#75805=ORIENTED_EDGE('',*,*,#52603,.F.);
#75806=ORIENTED_EDGE('',*,*,#52604,.T.);
#75807=ORIENTED_EDGE('',*,*,#52605,.T.);
#75808=ORIENTED_EDGE('',*,*,#52603,.T.);
#75809=ORIENTED_EDGE('',*,*,#52606,.T.);
#75810=ORIENTED_EDGE('',*,*,#52596,.F.);
#75811=ORIENTED_EDGE('',*,*,#52607,.T.);
#75812=ORIENTED_EDGE('',*,*,#52608,.F.);
#75813=ORIENTED_EDGE('',*,*,#52604,.F.);
#75814=ORIENTED_EDGE('',*,*,#52609,.F.);
#75815=ORIENTED_EDGE('',*,*,#52610,.F.);
#75816=ORIENTED_EDGE('',*,*,#52609,.T.);
#75817=ORIENTED_EDGE('',*,*,#52607,.F.);
#75818=ORIENTED_EDGE('',*,*,#52611,.F.);
#75819=ORIENTED_EDGE('',*,*,#52611,.T.);
#75820=ORIENTED_EDGE('',*,*,#52600,.F.);
#75821=ORIENTED_EDGE('',*,*,#52612,.F.);
#75822=ORIENTED_EDGE('',*,*,#52613,.F.);
#75823=ORIENTED_EDGE('',*,*,#52614,.T.);
#75824=ORIENTED_EDGE('',*,*,#52615,.F.);
#75825=ORIENTED_EDGE('',*,*,#52616,.F.);
#75826=ORIENTED_EDGE('',*,*,#50348,.F.);
#75827=ORIENTED_EDGE('',*,*,#52617,.T.);
#75828=ORIENTED_EDGE('',*,*,#52608,.T.);
#75829=ORIENTED_EDGE('',*,*,#52614,.F.);
#75830=ORIENTED_EDGE('',*,*,#50347,.T.);
#75831=ORIENTED_EDGE('',*,*,#52618,.F.);
#75832=ORIENTED_EDGE('',*,*,#52605,.F.);
#75833=ORIENTED_EDGE('',*,*,#52617,.F.);
#75834=ORIENTED_EDGE('',*,*,#50346,.F.);
#75835=ORIENTED_EDGE('',*,*,#52618,.T.);
#75836=ORIENTED_EDGE('',*,*,#50738,.F.);
#75837=ORIENTED_EDGE('',*,*,#52619,.F.);
#75838=ORIENTED_EDGE('',*,*,#52601,.F.);
#75839=ORIENTED_EDGE('',*,*,#52619,.T.);
#75840=ORIENTED_EDGE('',*,*,#49682,.F.);
#75841=ORIENTED_EDGE('',*,*,#52620,.F.);
#75842=ORIENTED_EDGE('',*,*,#52602,.F.);
#75843=ORIENTED_EDGE('',*,*,#52620,.T.);
#75844=ORIENTED_EDGE('',*,*,#49681,.F.);
#75845=ORIENTED_EDGE('',*,*,#52621,.F.);
#75846=ORIENTED_EDGE('',*,*,#52606,.F.);
#75847=ORIENTED_EDGE('',*,*,#52621,.T.);
#75848=ORIENTED_EDGE('',*,*,#49680,.F.);
#75849=ORIENTED_EDGE('',*,*,#52622,.F.);
#75850=ORIENTED_EDGE('',*,*,#52597,.F.);
#75851=ORIENTED_EDGE('',*,*,#52623,.T.);
#75852=ORIENTED_EDGE('',*,*,#52598,.F.);
#75853=ORIENTED_EDGE('',*,*,#52622,.T.);
#75854=ORIENTED_EDGE('',*,*,#50739,.F.);
#75855=ORIENTED_EDGE('',*,*,#52624,.T.);
#75856=ORIENTED_EDGE('',*,*,#52599,.F.);
#75857=ORIENTED_EDGE('',*,*,#52623,.F.);
#75858=ORIENTED_EDGE('',*,*,#50350,.F.);
#75859=ORIENTED_EDGE('',*,*,#52616,.T.);
#75860=ORIENTED_EDGE('',*,*,#52612,.T.);
#75861=ORIENTED_EDGE('',*,*,#52624,.F.);
#75862=ORIENTED_EDGE('',*,*,#50349,.T.);
#75863=ORIENTED_EDGE('',*,*,#52610,.T.);
#75864=ORIENTED_EDGE('',*,*,#52613,.T.);
#75865=ORIENTED_EDGE('',*,*,#52615,.T.);
#75866=ORIENTED_EDGE('',*,*,#52625,.T.);
#75867=ORIENTED_EDGE('',*,*,#52626,.T.);
#75868=ORIENTED_EDGE('',*,*,#52627,.T.);
#75869=ORIENTED_EDGE('',*,*,#52628,.T.);
#75870=ORIENTED_EDGE('',*,*,#52629,.T.);
#75871=ORIENTED_EDGE('',*,*,#52630,.T.);
#75872=ORIENTED_EDGE('',*,*,#52631,.T.);
#75873=ORIENTED_EDGE('',*,*,#52632,.F.);
#75874=ORIENTED_EDGE('',*,*,#52633,.T.);
#75875=ORIENTED_EDGE('',*,*,#52634,.T.);
#75876=ORIENTED_EDGE('',*,*,#52632,.T.);
#75877=ORIENTED_EDGE('',*,*,#52635,.T.);
#75878=ORIENTED_EDGE('',*,*,#52625,.F.);
#75879=ORIENTED_EDGE('',*,*,#52636,.T.);
#75880=ORIENTED_EDGE('',*,*,#52637,.F.);
#75881=ORIENTED_EDGE('',*,*,#52633,.F.);
#75882=ORIENTED_EDGE('',*,*,#52638,.F.);
#75883=ORIENTED_EDGE('',*,*,#52639,.F.);
#75884=ORIENTED_EDGE('',*,*,#52638,.T.);
#75885=ORIENTED_EDGE('',*,*,#52636,.F.);
#75886=ORIENTED_EDGE('',*,*,#52640,.F.);
#75887=ORIENTED_EDGE('',*,*,#52640,.T.);
#75888=ORIENTED_EDGE('',*,*,#52629,.F.);
#75889=ORIENTED_EDGE('',*,*,#52641,.F.);
#75890=ORIENTED_EDGE('',*,*,#52642,.F.);
#75891=ORIENTED_EDGE('',*,*,#52643,.T.);
#75892=ORIENTED_EDGE('',*,*,#52644,.F.);
#75893=ORIENTED_EDGE('',*,*,#52645,.F.);
#75894=ORIENTED_EDGE('',*,*,#50342,.F.);
#75895=ORIENTED_EDGE('',*,*,#52646,.T.);
#75896=ORIENTED_EDGE('',*,*,#52637,.T.);
#75897=ORIENTED_EDGE('',*,*,#52643,.F.);
#75898=ORIENTED_EDGE('',*,*,#50341,.T.);
#75899=ORIENTED_EDGE('',*,*,#52647,.F.);
#75900=ORIENTED_EDGE('',*,*,#52634,.F.);
#75901=ORIENTED_EDGE('',*,*,#52646,.F.);
#75902=ORIENTED_EDGE('',*,*,#50340,.F.);
#75903=ORIENTED_EDGE('',*,*,#52647,.T.);
#75904=ORIENTED_EDGE('',*,*,#50736,.F.);
#75905=ORIENTED_EDGE('',*,*,#52648,.F.);
#75906=ORIENTED_EDGE('',*,*,#52630,.F.);
#75907=ORIENTED_EDGE('',*,*,#52648,.T.);
#75908=ORIENTED_EDGE('',*,*,#49686,.F.);
#75909=ORIENTED_EDGE('',*,*,#52649,.F.);
#75910=ORIENTED_EDGE('',*,*,#52631,.F.);
#75911=ORIENTED_EDGE('',*,*,#52649,.T.);
#75912=ORIENTED_EDGE('',*,*,#49685,.F.);
#75913=ORIENTED_EDGE('',*,*,#52650,.F.);
#75914=ORIENTED_EDGE('',*,*,#52635,.F.);
#75915=ORIENTED_EDGE('',*,*,#52650,.T.);
#75916=ORIENTED_EDGE('',*,*,#49684,.F.);
#75917=ORIENTED_EDGE('',*,*,#52651,.F.);
#75918=ORIENTED_EDGE('',*,*,#52626,.F.);
#75919=ORIENTED_EDGE('',*,*,#52652,.T.);
#75920=ORIENTED_EDGE('',*,*,#52627,.F.);
#75921=ORIENTED_EDGE('',*,*,#52651,.T.);
#75922=ORIENTED_EDGE('',*,*,#50737,.F.);
#75923=ORIENTED_EDGE('',*,*,#52653,.T.);
#75924=ORIENTED_EDGE('',*,*,#52628,.F.);
#75925=ORIENTED_EDGE('',*,*,#52652,.F.);
#75926=ORIENTED_EDGE('',*,*,#50344,.F.);
#75927=ORIENTED_EDGE('',*,*,#52645,.T.);
#75928=ORIENTED_EDGE('',*,*,#52641,.T.);
#75929=ORIENTED_EDGE('',*,*,#52653,.F.);
#75930=ORIENTED_EDGE('',*,*,#50343,.T.);
#75931=ORIENTED_EDGE('',*,*,#52639,.T.);
#75932=ORIENTED_EDGE('',*,*,#52642,.T.);
#75933=ORIENTED_EDGE('',*,*,#52644,.T.);
#75934=ORIENTED_EDGE('',*,*,#52654,.T.);
#75935=ORIENTED_EDGE('',*,*,#52655,.T.);
#75936=ORIENTED_EDGE('',*,*,#52656,.T.);
#75937=ORIENTED_EDGE('',*,*,#52657,.T.);
#75938=ORIENTED_EDGE('',*,*,#52658,.T.);
#75939=ORIENTED_EDGE('',*,*,#52659,.T.);
#75940=ORIENTED_EDGE('',*,*,#52660,.T.);
#75941=ORIENTED_EDGE('',*,*,#52661,.F.);
#75942=ORIENTED_EDGE('',*,*,#52662,.T.);
#75943=ORIENTED_EDGE('',*,*,#52663,.T.);
#75944=ORIENTED_EDGE('',*,*,#52661,.T.);
#75945=ORIENTED_EDGE('',*,*,#52664,.T.);
#75946=ORIENTED_EDGE('',*,*,#52654,.F.);
#75947=ORIENTED_EDGE('',*,*,#52665,.T.);
#75948=ORIENTED_EDGE('',*,*,#52666,.F.);
#75949=ORIENTED_EDGE('',*,*,#52662,.F.);
#75950=ORIENTED_EDGE('',*,*,#52667,.F.);
#75951=ORIENTED_EDGE('',*,*,#52668,.F.);
#75952=ORIENTED_EDGE('',*,*,#52667,.T.);
#75953=ORIENTED_EDGE('',*,*,#52665,.F.);
#75954=ORIENTED_EDGE('',*,*,#52669,.F.);
#75955=ORIENTED_EDGE('',*,*,#52669,.T.);
#75956=ORIENTED_EDGE('',*,*,#52658,.F.);
#75957=ORIENTED_EDGE('',*,*,#52670,.F.);
#75958=ORIENTED_EDGE('',*,*,#52671,.F.);
#75959=ORIENTED_EDGE('',*,*,#52672,.T.);
#75960=ORIENTED_EDGE('',*,*,#52673,.F.);
#75961=ORIENTED_EDGE('',*,*,#52674,.F.);
#75962=ORIENTED_EDGE('',*,*,#50336,.F.);
#75963=ORIENTED_EDGE('',*,*,#52675,.T.);
#75964=ORIENTED_EDGE('',*,*,#52666,.T.);
#75965=ORIENTED_EDGE('',*,*,#52672,.F.);
#75966=ORIENTED_EDGE('',*,*,#50335,.T.);
#75967=ORIENTED_EDGE('',*,*,#52676,.F.);
#75968=ORIENTED_EDGE('',*,*,#52663,.F.);
#75969=ORIENTED_EDGE('',*,*,#52675,.F.);
#75970=ORIENTED_EDGE('',*,*,#50334,.F.);
#75971=ORIENTED_EDGE('',*,*,#52676,.T.);
#75972=ORIENTED_EDGE('',*,*,#50734,.F.);
#75973=ORIENTED_EDGE('',*,*,#52677,.F.);
#75974=ORIENTED_EDGE('',*,*,#52659,.F.);
#75975=ORIENTED_EDGE('',*,*,#52677,.T.);
#75976=ORIENTED_EDGE('',*,*,#49690,.F.);
#75977=ORIENTED_EDGE('',*,*,#52678,.F.);
#75978=ORIENTED_EDGE('',*,*,#52660,.F.);
#75979=ORIENTED_EDGE('',*,*,#52678,.T.);
#75980=ORIENTED_EDGE('',*,*,#49689,.F.);
#75981=ORIENTED_EDGE('',*,*,#52679,.F.);
#75982=ORIENTED_EDGE('',*,*,#52664,.F.);
#75983=ORIENTED_EDGE('',*,*,#52679,.T.);
#75984=ORIENTED_EDGE('',*,*,#49688,.F.);
#75985=ORIENTED_EDGE('',*,*,#52680,.F.);
#75986=ORIENTED_EDGE('',*,*,#52655,.F.);
#75987=ORIENTED_EDGE('',*,*,#52681,.T.);
#75988=ORIENTED_EDGE('',*,*,#52656,.F.);
#75989=ORIENTED_EDGE('',*,*,#52680,.T.);
#75990=ORIENTED_EDGE('',*,*,#50735,.F.);
#75991=ORIENTED_EDGE('',*,*,#52682,.T.);
#75992=ORIENTED_EDGE('',*,*,#52657,.F.);
#75993=ORIENTED_EDGE('',*,*,#52681,.F.);
#75994=ORIENTED_EDGE('',*,*,#50338,.F.);
#75995=ORIENTED_EDGE('',*,*,#52674,.T.);
#75996=ORIENTED_EDGE('',*,*,#52670,.T.);
#75997=ORIENTED_EDGE('',*,*,#52682,.F.);
#75998=ORIENTED_EDGE('',*,*,#50337,.T.);
#75999=ORIENTED_EDGE('',*,*,#52668,.T.);
#76000=ORIENTED_EDGE('',*,*,#52671,.T.);
#76001=ORIENTED_EDGE('',*,*,#52673,.T.);
#76002=ORIENTED_EDGE('',*,*,#52683,.T.);
#76003=ORIENTED_EDGE('',*,*,#52684,.T.);
#76004=ORIENTED_EDGE('',*,*,#52685,.T.);
#76005=ORIENTED_EDGE('',*,*,#52686,.T.);
#76006=ORIENTED_EDGE('',*,*,#52687,.T.);
#76007=ORIENTED_EDGE('',*,*,#52688,.T.);
#76008=ORIENTED_EDGE('',*,*,#52689,.T.);
#76009=ORIENTED_EDGE('',*,*,#52690,.F.);
#76010=ORIENTED_EDGE('',*,*,#52691,.T.);
#76011=ORIENTED_EDGE('',*,*,#52692,.T.);
#76012=ORIENTED_EDGE('',*,*,#52690,.T.);
#76013=ORIENTED_EDGE('',*,*,#52693,.T.);
#76014=ORIENTED_EDGE('',*,*,#52683,.F.);
#76015=ORIENTED_EDGE('',*,*,#52694,.T.);
#76016=ORIENTED_EDGE('',*,*,#52695,.F.);
#76017=ORIENTED_EDGE('',*,*,#52691,.F.);
#76018=ORIENTED_EDGE('',*,*,#52696,.F.);
#76019=ORIENTED_EDGE('',*,*,#52697,.F.);
#76020=ORIENTED_EDGE('',*,*,#52696,.T.);
#76021=ORIENTED_EDGE('',*,*,#52694,.F.);
#76022=ORIENTED_EDGE('',*,*,#52698,.F.);
#76023=ORIENTED_EDGE('',*,*,#52698,.T.);
#76024=ORIENTED_EDGE('',*,*,#52687,.F.);
#76025=ORIENTED_EDGE('',*,*,#52699,.F.);
#76026=ORIENTED_EDGE('',*,*,#52700,.F.);
#76027=ORIENTED_EDGE('',*,*,#52701,.T.);
#76028=ORIENTED_EDGE('',*,*,#52702,.F.);
#76029=ORIENTED_EDGE('',*,*,#52703,.F.);
#76030=ORIENTED_EDGE('',*,*,#50330,.F.);
#76031=ORIENTED_EDGE('',*,*,#52704,.T.);
#76032=ORIENTED_EDGE('',*,*,#52695,.T.);
#76033=ORIENTED_EDGE('',*,*,#52701,.F.);
#76034=ORIENTED_EDGE('',*,*,#50329,.T.);
#76035=ORIENTED_EDGE('',*,*,#52705,.F.);
#76036=ORIENTED_EDGE('',*,*,#52692,.F.);
#76037=ORIENTED_EDGE('',*,*,#52704,.F.);
#76038=ORIENTED_EDGE('',*,*,#50328,.F.);
#76039=ORIENTED_EDGE('',*,*,#52705,.T.);
#76040=ORIENTED_EDGE('',*,*,#50732,.F.);
#76041=ORIENTED_EDGE('',*,*,#52706,.F.);
#76042=ORIENTED_EDGE('',*,*,#52688,.F.);
#76043=ORIENTED_EDGE('',*,*,#52706,.T.);
#76044=ORIENTED_EDGE('',*,*,#49694,.F.);
#76045=ORIENTED_EDGE('',*,*,#52707,.F.);
#76046=ORIENTED_EDGE('',*,*,#52689,.F.);
#76047=ORIENTED_EDGE('',*,*,#52707,.T.);
#76048=ORIENTED_EDGE('',*,*,#49693,.F.);
#76049=ORIENTED_EDGE('',*,*,#52708,.F.);
#76050=ORIENTED_EDGE('',*,*,#52693,.F.);
#76051=ORIENTED_EDGE('',*,*,#52708,.T.);
#76052=ORIENTED_EDGE('',*,*,#49692,.F.);
#76053=ORIENTED_EDGE('',*,*,#52709,.F.);
#76054=ORIENTED_EDGE('',*,*,#52684,.F.);
#76055=ORIENTED_EDGE('',*,*,#52710,.T.);
#76056=ORIENTED_EDGE('',*,*,#52685,.F.);
#76057=ORIENTED_EDGE('',*,*,#52709,.T.);
#76058=ORIENTED_EDGE('',*,*,#50733,.F.);
#76059=ORIENTED_EDGE('',*,*,#52711,.T.);
#76060=ORIENTED_EDGE('',*,*,#52686,.F.);
#76061=ORIENTED_EDGE('',*,*,#52710,.F.);
#76062=ORIENTED_EDGE('',*,*,#50332,.F.);
#76063=ORIENTED_EDGE('',*,*,#52703,.T.);
#76064=ORIENTED_EDGE('',*,*,#52699,.T.);
#76065=ORIENTED_EDGE('',*,*,#52711,.F.);
#76066=ORIENTED_EDGE('',*,*,#50331,.T.);
#76067=ORIENTED_EDGE('',*,*,#52697,.T.);
#76068=ORIENTED_EDGE('',*,*,#52700,.T.);
#76069=ORIENTED_EDGE('',*,*,#52702,.T.);
#76070=ORIENTED_EDGE('',*,*,#52712,.T.);
#76071=ORIENTED_EDGE('',*,*,#52713,.T.);
#76072=ORIENTED_EDGE('',*,*,#52714,.T.);
#76073=ORIENTED_EDGE('',*,*,#52715,.T.);
#76074=ORIENTED_EDGE('',*,*,#52716,.T.);
#76075=ORIENTED_EDGE('',*,*,#52717,.T.);
#76076=ORIENTED_EDGE('',*,*,#52718,.T.);
#76077=ORIENTED_EDGE('',*,*,#52719,.F.);
#76078=ORIENTED_EDGE('',*,*,#52720,.T.);
#76079=ORIENTED_EDGE('',*,*,#52721,.T.);
#76080=ORIENTED_EDGE('',*,*,#52719,.T.);
#76081=ORIENTED_EDGE('',*,*,#52722,.T.);
#76082=ORIENTED_EDGE('',*,*,#52712,.F.);
#76083=ORIENTED_EDGE('',*,*,#52723,.T.);
#76084=ORIENTED_EDGE('',*,*,#52724,.F.);
#76085=ORIENTED_EDGE('',*,*,#52720,.F.);
#76086=ORIENTED_EDGE('',*,*,#52725,.F.);
#76087=ORIENTED_EDGE('',*,*,#52726,.F.);
#76088=ORIENTED_EDGE('',*,*,#52725,.T.);
#76089=ORIENTED_EDGE('',*,*,#52723,.F.);
#76090=ORIENTED_EDGE('',*,*,#52727,.F.);
#76091=ORIENTED_EDGE('',*,*,#52727,.T.);
#76092=ORIENTED_EDGE('',*,*,#52716,.F.);
#76093=ORIENTED_EDGE('',*,*,#52728,.F.);
#76094=ORIENTED_EDGE('',*,*,#52729,.F.);
#76095=ORIENTED_EDGE('',*,*,#52730,.T.);
#76096=ORIENTED_EDGE('',*,*,#52731,.F.);
#76097=ORIENTED_EDGE('',*,*,#52732,.F.);
#76098=ORIENTED_EDGE('',*,*,#50324,.F.);
#76099=ORIENTED_EDGE('',*,*,#52733,.T.);
#76100=ORIENTED_EDGE('',*,*,#52724,.T.);
#76101=ORIENTED_EDGE('',*,*,#52730,.F.);
#76102=ORIENTED_EDGE('',*,*,#50323,.T.);
#76103=ORIENTED_EDGE('',*,*,#52734,.F.);
#76104=ORIENTED_EDGE('',*,*,#52721,.F.);
#76105=ORIENTED_EDGE('',*,*,#52733,.F.);
#76106=ORIENTED_EDGE('',*,*,#50322,.F.);
#76107=ORIENTED_EDGE('',*,*,#52734,.T.);
#76108=ORIENTED_EDGE('',*,*,#50730,.F.);
#76109=ORIENTED_EDGE('',*,*,#52735,.F.);
#76110=ORIENTED_EDGE('',*,*,#52717,.F.);
#76111=ORIENTED_EDGE('',*,*,#52735,.T.);
#76112=ORIENTED_EDGE('',*,*,#49698,.F.);
#76113=ORIENTED_EDGE('',*,*,#52736,.F.);
#76114=ORIENTED_EDGE('',*,*,#52718,.F.);
#76115=ORIENTED_EDGE('',*,*,#52736,.T.);
#76116=ORIENTED_EDGE('',*,*,#49697,.F.);
#76117=ORIENTED_EDGE('',*,*,#52737,.F.);
#76118=ORIENTED_EDGE('',*,*,#52722,.F.);
#76119=ORIENTED_EDGE('',*,*,#52737,.T.);
#76120=ORIENTED_EDGE('',*,*,#49696,.F.);
#76121=ORIENTED_EDGE('',*,*,#52738,.F.);
#76122=ORIENTED_EDGE('',*,*,#52713,.F.);
#76123=ORIENTED_EDGE('',*,*,#52739,.T.);
#76124=ORIENTED_EDGE('',*,*,#52714,.F.);
#76125=ORIENTED_EDGE('',*,*,#52738,.T.);
#76126=ORIENTED_EDGE('',*,*,#50731,.F.);
#76127=ORIENTED_EDGE('',*,*,#52740,.T.);
#76128=ORIENTED_EDGE('',*,*,#52715,.F.);
#76129=ORIENTED_EDGE('',*,*,#52739,.F.);
#76130=ORIENTED_EDGE('',*,*,#50326,.F.);
#76131=ORIENTED_EDGE('',*,*,#52732,.T.);
#76132=ORIENTED_EDGE('',*,*,#52728,.T.);
#76133=ORIENTED_EDGE('',*,*,#52740,.F.);
#76134=ORIENTED_EDGE('',*,*,#50325,.T.);
#76135=ORIENTED_EDGE('',*,*,#52726,.T.);
#76136=ORIENTED_EDGE('',*,*,#52729,.T.);
#76137=ORIENTED_EDGE('',*,*,#52731,.T.);
#76138=ORIENTED_EDGE('',*,*,#52741,.T.);
#76139=ORIENTED_EDGE('',*,*,#52742,.T.);
#76140=ORIENTED_EDGE('',*,*,#52743,.T.);
#76141=ORIENTED_EDGE('',*,*,#52744,.T.);
#76142=ORIENTED_EDGE('',*,*,#52745,.T.);
#76143=ORIENTED_EDGE('',*,*,#52746,.T.);
#76144=ORIENTED_EDGE('',*,*,#52747,.T.);
#76145=ORIENTED_EDGE('',*,*,#52748,.F.);
#76146=ORIENTED_EDGE('',*,*,#52749,.T.);
#76147=ORIENTED_EDGE('',*,*,#52750,.T.);
#76148=ORIENTED_EDGE('',*,*,#52748,.T.);
#76149=ORIENTED_EDGE('',*,*,#52751,.T.);
#76150=ORIENTED_EDGE('',*,*,#52741,.F.);
#76151=ORIENTED_EDGE('',*,*,#52752,.T.);
#76152=ORIENTED_EDGE('',*,*,#52753,.F.);
#76153=ORIENTED_EDGE('',*,*,#52749,.F.);
#76154=ORIENTED_EDGE('',*,*,#52754,.F.);
#76155=ORIENTED_EDGE('',*,*,#52755,.F.);
#76156=ORIENTED_EDGE('',*,*,#52754,.T.);
#76157=ORIENTED_EDGE('',*,*,#52752,.F.);
#76158=ORIENTED_EDGE('',*,*,#52756,.F.);
#76159=ORIENTED_EDGE('',*,*,#52756,.T.);
#76160=ORIENTED_EDGE('',*,*,#52745,.F.);
#76161=ORIENTED_EDGE('',*,*,#52757,.F.);
#76162=ORIENTED_EDGE('',*,*,#52758,.F.);
#76163=ORIENTED_EDGE('',*,*,#52759,.T.);
#76164=ORIENTED_EDGE('',*,*,#52760,.F.);
#76165=ORIENTED_EDGE('',*,*,#52761,.F.);
#76166=ORIENTED_EDGE('',*,*,#50318,.F.);
#76167=ORIENTED_EDGE('',*,*,#52762,.T.);
#76168=ORIENTED_EDGE('',*,*,#52753,.T.);
#76169=ORIENTED_EDGE('',*,*,#52759,.F.);
#76170=ORIENTED_EDGE('',*,*,#50317,.T.);
#76171=ORIENTED_EDGE('',*,*,#52763,.F.);
#76172=ORIENTED_EDGE('',*,*,#52750,.F.);
#76173=ORIENTED_EDGE('',*,*,#52762,.F.);
#76174=ORIENTED_EDGE('',*,*,#50316,.F.);
#76175=ORIENTED_EDGE('',*,*,#52763,.T.);
#76176=ORIENTED_EDGE('',*,*,#50728,.F.);
#76177=ORIENTED_EDGE('',*,*,#52764,.F.);
#76178=ORIENTED_EDGE('',*,*,#52746,.F.);
#76179=ORIENTED_EDGE('',*,*,#52764,.T.);
#76180=ORIENTED_EDGE('',*,*,#49702,.F.);
#76181=ORIENTED_EDGE('',*,*,#52765,.F.);
#76182=ORIENTED_EDGE('',*,*,#52747,.F.);
#76183=ORIENTED_EDGE('',*,*,#52765,.T.);
#76184=ORIENTED_EDGE('',*,*,#49701,.F.);
#76185=ORIENTED_EDGE('',*,*,#52766,.F.);
#76186=ORIENTED_EDGE('',*,*,#52751,.F.);
#76187=ORIENTED_EDGE('',*,*,#52766,.T.);
#76188=ORIENTED_EDGE('',*,*,#49700,.F.);
#76189=ORIENTED_EDGE('',*,*,#52767,.F.);
#76190=ORIENTED_EDGE('',*,*,#52742,.F.);
#76191=ORIENTED_EDGE('',*,*,#52768,.T.);
#76192=ORIENTED_EDGE('',*,*,#52743,.F.);
#76193=ORIENTED_EDGE('',*,*,#52767,.T.);
#76194=ORIENTED_EDGE('',*,*,#50729,.F.);
#76195=ORIENTED_EDGE('',*,*,#52769,.T.);
#76196=ORIENTED_EDGE('',*,*,#52744,.F.);
#76197=ORIENTED_EDGE('',*,*,#52768,.F.);
#76198=ORIENTED_EDGE('',*,*,#50320,.F.);
#76199=ORIENTED_EDGE('',*,*,#52761,.T.);
#76200=ORIENTED_EDGE('',*,*,#52757,.T.);
#76201=ORIENTED_EDGE('',*,*,#52769,.F.);
#76202=ORIENTED_EDGE('',*,*,#50319,.T.);
#76203=ORIENTED_EDGE('',*,*,#52755,.T.);
#76204=ORIENTED_EDGE('',*,*,#52758,.T.);
#76205=ORIENTED_EDGE('',*,*,#52760,.T.);
#76206=ORIENTED_EDGE('',*,*,#52770,.T.);
#76207=ORIENTED_EDGE('',*,*,#52771,.T.);
#76208=ORIENTED_EDGE('',*,*,#52772,.T.);
#76209=ORIENTED_EDGE('',*,*,#52773,.T.);
#76210=ORIENTED_EDGE('',*,*,#52774,.T.);
#76211=ORIENTED_EDGE('',*,*,#52775,.T.);
#76212=ORIENTED_EDGE('',*,*,#52776,.T.);
#76213=ORIENTED_EDGE('',*,*,#52777,.F.);
#76214=ORIENTED_EDGE('',*,*,#52778,.T.);
#76215=ORIENTED_EDGE('',*,*,#52779,.T.);
#76216=ORIENTED_EDGE('',*,*,#52777,.T.);
#76217=ORIENTED_EDGE('',*,*,#52780,.T.);
#76218=ORIENTED_EDGE('',*,*,#52770,.F.);
#76219=ORIENTED_EDGE('',*,*,#52781,.T.);
#76220=ORIENTED_EDGE('',*,*,#52782,.F.);
#76221=ORIENTED_EDGE('',*,*,#52778,.F.);
#76222=ORIENTED_EDGE('',*,*,#52783,.F.);
#76223=ORIENTED_EDGE('',*,*,#52784,.F.);
#76224=ORIENTED_EDGE('',*,*,#52783,.T.);
#76225=ORIENTED_EDGE('',*,*,#52781,.F.);
#76226=ORIENTED_EDGE('',*,*,#52785,.F.);
#76227=ORIENTED_EDGE('',*,*,#52785,.T.);
#76228=ORIENTED_EDGE('',*,*,#52774,.F.);
#76229=ORIENTED_EDGE('',*,*,#52786,.F.);
#76230=ORIENTED_EDGE('',*,*,#52787,.F.);
#76231=ORIENTED_EDGE('',*,*,#52788,.T.);
#76232=ORIENTED_EDGE('',*,*,#52789,.F.);
#76233=ORIENTED_EDGE('',*,*,#52790,.F.);
#76234=ORIENTED_EDGE('',*,*,#50312,.F.);
#76235=ORIENTED_EDGE('',*,*,#52791,.T.);
#76236=ORIENTED_EDGE('',*,*,#52782,.T.);
#76237=ORIENTED_EDGE('',*,*,#52788,.F.);
#76238=ORIENTED_EDGE('',*,*,#50311,.T.);
#76239=ORIENTED_EDGE('',*,*,#52792,.F.);
#76240=ORIENTED_EDGE('',*,*,#52779,.F.);
#76241=ORIENTED_EDGE('',*,*,#52791,.F.);
#76242=ORIENTED_EDGE('',*,*,#50310,.F.);
#76243=ORIENTED_EDGE('',*,*,#52792,.T.);
#76244=ORIENTED_EDGE('',*,*,#50726,.F.);
#76245=ORIENTED_EDGE('',*,*,#52793,.F.);
#76246=ORIENTED_EDGE('',*,*,#52775,.F.);
#76247=ORIENTED_EDGE('',*,*,#52793,.T.);
#76248=ORIENTED_EDGE('',*,*,#49706,.F.);
#76249=ORIENTED_EDGE('',*,*,#52794,.F.);
#76250=ORIENTED_EDGE('',*,*,#52776,.F.);
#76251=ORIENTED_EDGE('',*,*,#52794,.T.);
#76252=ORIENTED_EDGE('',*,*,#49705,.F.);
#76253=ORIENTED_EDGE('',*,*,#52795,.F.);
#76254=ORIENTED_EDGE('',*,*,#52780,.F.);
#76255=ORIENTED_EDGE('',*,*,#52795,.T.);
#76256=ORIENTED_EDGE('',*,*,#49704,.F.);
#76257=ORIENTED_EDGE('',*,*,#52796,.F.);
#76258=ORIENTED_EDGE('',*,*,#52771,.F.);
#76259=ORIENTED_EDGE('',*,*,#52797,.T.);
#76260=ORIENTED_EDGE('',*,*,#52772,.F.);
#76261=ORIENTED_EDGE('',*,*,#52796,.T.);
#76262=ORIENTED_EDGE('',*,*,#50727,.F.);
#76263=ORIENTED_EDGE('',*,*,#52798,.T.);
#76264=ORIENTED_EDGE('',*,*,#52773,.F.);
#76265=ORIENTED_EDGE('',*,*,#52797,.F.);
#76266=ORIENTED_EDGE('',*,*,#50314,.F.);
#76267=ORIENTED_EDGE('',*,*,#52790,.T.);
#76268=ORIENTED_EDGE('',*,*,#52786,.T.);
#76269=ORIENTED_EDGE('',*,*,#52798,.F.);
#76270=ORIENTED_EDGE('',*,*,#50313,.T.);
#76271=ORIENTED_EDGE('',*,*,#52784,.T.);
#76272=ORIENTED_EDGE('',*,*,#52787,.T.);
#76273=ORIENTED_EDGE('',*,*,#52789,.T.);
#76274=ORIENTED_EDGE('',*,*,#52799,.T.);
#76275=ORIENTED_EDGE('',*,*,#52800,.T.);
#76276=ORIENTED_EDGE('',*,*,#52801,.T.);
#76277=ORIENTED_EDGE('',*,*,#52802,.T.);
#76278=ORIENTED_EDGE('',*,*,#52803,.T.);
#76279=ORIENTED_EDGE('',*,*,#52804,.T.);
#76280=ORIENTED_EDGE('',*,*,#52805,.T.);
#76281=ORIENTED_EDGE('',*,*,#52806,.F.);
#76282=ORIENTED_EDGE('',*,*,#52807,.T.);
#76283=ORIENTED_EDGE('',*,*,#52808,.T.);
#76284=ORIENTED_EDGE('',*,*,#52806,.T.);
#76285=ORIENTED_EDGE('',*,*,#52809,.T.);
#76286=ORIENTED_EDGE('',*,*,#52799,.F.);
#76287=ORIENTED_EDGE('',*,*,#52810,.T.);
#76288=ORIENTED_EDGE('',*,*,#52811,.F.);
#76289=ORIENTED_EDGE('',*,*,#52807,.F.);
#76290=ORIENTED_EDGE('',*,*,#52812,.F.);
#76291=ORIENTED_EDGE('',*,*,#52813,.F.);
#76292=ORIENTED_EDGE('',*,*,#52812,.T.);
#76293=ORIENTED_EDGE('',*,*,#52810,.F.);
#76294=ORIENTED_EDGE('',*,*,#52814,.F.);
#76295=ORIENTED_EDGE('',*,*,#52814,.T.);
#76296=ORIENTED_EDGE('',*,*,#52803,.F.);
#76297=ORIENTED_EDGE('',*,*,#52815,.F.);
#76298=ORIENTED_EDGE('',*,*,#52816,.F.);
#76299=ORIENTED_EDGE('',*,*,#52817,.T.);
#76300=ORIENTED_EDGE('',*,*,#52818,.F.);
#76301=ORIENTED_EDGE('',*,*,#52819,.F.);
#76302=ORIENTED_EDGE('',*,*,#50306,.F.);
#76303=ORIENTED_EDGE('',*,*,#52820,.T.);
#76304=ORIENTED_EDGE('',*,*,#52811,.T.);
#76305=ORIENTED_EDGE('',*,*,#52817,.F.);
#76306=ORIENTED_EDGE('',*,*,#50305,.T.);
#76307=ORIENTED_EDGE('',*,*,#52821,.F.);
#76308=ORIENTED_EDGE('',*,*,#52808,.F.);
#76309=ORIENTED_EDGE('',*,*,#52820,.F.);
#76310=ORIENTED_EDGE('',*,*,#50304,.F.);
#76311=ORIENTED_EDGE('',*,*,#52821,.T.);
#76312=ORIENTED_EDGE('',*,*,#50724,.F.);
#76313=ORIENTED_EDGE('',*,*,#52822,.F.);
#76314=ORIENTED_EDGE('',*,*,#52804,.F.);
#76315=ORIENTED_EDGE('',*,*,#52822,.T.);
#76316=ORIENTED_EDGE('',*,*,#49710,.F.);
#76317=ORIENTED_EDGE('',*,*,#52823,.F.);
#76318=ORIENTED_EDGE('',*,*,#52805,.F.);
#76319=ORIENTED_EDGE('',*,*,#52823,.T.);
#76320=ORIENTED_EDGE('',*,*,#49709,.F.);
#76321=ORIENTED_EDGE('',*,*,#52824,.F.);
#76322=ORIENTED_EDGE('',*,*,#52809,.F.);
#76323=ORIENTED_EDGE('',*,*,#52824,.T.);
#76324=ORIENTED_EDGE('',*,*,#49708,.F.);
#76325=ORIENTED_EDGE('',*,*,#52825,.F.);
#76326=ORIENTED_EDGE('',*,*,#52800,.F.);
#76327=ORIENTED_EDGE('',*,*,#52826,.T.);
#76328=ORIENTED_EDGE('',*,*,#52801,.F.);
#76329=ORIENTED_EDGE('',*,*,#52825,.T.);
#76330=ORIENTED_EDGE('',*,*,#50725,.F.);
#76331=ORIENTED_EDGE('',*,*,#52827,.T.);
#76332=ORIENTED_EDGE('',*,*,#52802,.F.);
#76333=ORIENTED_EDGE('',*,*,#52826,.F.);
#76334=ORIENTED_EDGE('',*,*,#50308,.F.);
#76335=ORIENTED_EDGE('',*,*,#52819,.T.);
#76336=ORIENTED_EDGE('',*,*,#52815,.T.);
#76337=ORIENTED_EDGE('',*,*,#52827,.F.);
#76338=ORIENTED_EDGE('',*,*,#50307,.T.);
#76339=ORIENTED_EDGE('',*,*,#52813,.T.);
#76340=ORIENTED_EDGE('',*,*,#52816,.T.);
#76341=ORIENTED_EDGE('',*,*,#52818,.T.);
#76342=ORIENTED_EDGE('',*,*,#52828,.T.);
#76343=ORIENTED_EDGE('',*,*,#52829,.T.);
#76344=ORIENTED_EDGE('',*,*,#52830,.T.);
#76345=ORIENTED_EDGE('',*,*,#52831,.T.);
#76346=ORIENTED_EDGE('',*,*,#52832,.T.);
#76347=ORIENTED_EDGE('',*,*,#52833,.T.);
#76348=ORIENTED_EDGE('',*,*,#52834,.T.);
#76349=ORIENTED_EDGE('',*,*,#52835,.F.);
#76350=ORIENTED_EDGE('',*,*,#52836,.T.);
#76351=ORIENTED_EDGE('',*,*,#52837,.T.);
#76352=ORIENTED_EDGE('',*,*,#52835,.T.);
#76353=ORIENTED_EDGE('',*,*,#52838,.T.);
#76354=ORIENTED_EDGE('',*,*,#52828,.F.);
#76355=ORIENTED_EDGE('',*,*,#52839,.T.);
#76356=ORIENTED_EDGE('',*,*,#52840,.F.);
#76357=ORIENTED_EDGE('',*,*,#52836,.F.);
#76358=ORIENTED_EDGE('',*,*,#52841,.F.);
#76359=ORIENTED_EDGE('',*,*,#52842,.F.);
#76360=ORIENTED_EDGE('',*,*,#52841,.T.);
#76361=ORIENTED_EDGE('',*,*,#52839,.F.);
#76362=ORIENTED_EDGE('',*,*,#52843,.F.);
#76363=ORIENTED_EDGE('',*,*,#52843,.T.);
#76364=ORIENTED_EDGE('',*,*,#52832,.F.);
#76365=ORIENTED_EDGE('',*,*,#52844,.F.);
#76366=ORIENTED_EDGE('',*,*,#52845,.F.);
#76367=ORIENTED_EDGE('',*,*,#52846,.T.);
#76368=ORIENTED_EDGE('',*,*,#52847,.F.);
#76369=ORIENTED_EDGE('',*,*,#52848,.F.);
#76370=ORIENTED_EDGE('',*,*,#50300,.F.);
#76371=ORIENTED_EDGE('',*,*,#52849,.T.);
#76372=ORIENTED_EDGE('',*,*,#52840,.T.);
#76373=ORIENTED_EDGE('',*,*,#52846,.F.);
#76374=ORIENTED_EDGE('',*,*,#50299,.T.);
#76375=ORIENTED_EDGE('',*,*,#52850,.F.);
#76376=ORIENTED_EDGE('',*,*,#52837,.F.);
#76377=ORIENTED_EDGE('',*,*,#52849,.F.);
#76378=ORIENTED_EDGE('',*,*,#50298,.F.);
#76379=ORIENTED_EDGE('',*,*,#52850,.T.);
#76380=ORIENTED_EDGE('',*,*,#50722,.F.);
#76381=ORIENTED_EDGE('',*,*,#52851,.F.);
#76382=ORIENTED_EDGE('',*,*,#52833,.F.);
#76383=ORIENTED_EDGE('',*,*,#52851,.T.);
#76384=ORIENTED_EDGE('',*,*,#49714,.F.);
#76385=ORIENTED_EDGE('',*,*,#52852,.F.);
#76386=ORIENTED_EDGE('',*,*,#52834,.F.);
#76387=ORIENTED_EDGE('',*,*,#52852,.T.);
#76388=ORIENTED_EDGE('',*,*,#49713,.F.);
#76389=ORIENTED_EDGE('',*,*,#52853,.F.);
#76390=ORIENTED_EDGE('',*,*,#52838,.F.);
#76391=ORIENTED_EDGE('',*,*,#52853,.T.);
#76392=ORIENTED_EDGE('',*,*,#49712,.F.);
#76393=ORIENTED_EDGE('',*,*,#52854,.F.);
#76394=ORIENTED_EDGE('',*,*,#52829,.F.);
#76395=ORIENTED_EDGE('',*,*,#52855,.T.);
#76396=ORIENTED_EDGE('',*,*,#52830,.F.);
#76397=ORIENTED_EDGE('',*,*,#52854,.T.);
#76398=ORIENTED_EDGE('',*,*,#50723,.F.);
#76399=ORIENTED_EDGE('',*,*,#52856,.T.);
#76400=ORIENTED_EDGE('',*,*,#52831,.F.);
#76401=ORIENTED_EDGE('',*,*,#52855,.F.);
#76402=ORIENTED_EDGE('',*,*,#50302,.F.);
#76403=ORIENTED_EDGE('',*,*,#52848,.T.);
#76404=ORIENTED_EDGE('',*,*,#52844,.T.);
#76405=ORIENTED_EDGE('',*,*,#52856,.F.);
#76406=ORIENTED_EDGE('',*,*,#50301,.T.);
#76407=ORIENTED_EDGE('',*,*,#52842,.T.);
#76408=ORIENTED_EDGE('',*,*,#52845,.T.);
#76409=ORIENTED_EDGE('',*,*,#52847,.T.);
#76410=ORIENTED_EDGE('',*,*,#52857,.T.);
#76411=ORIENTED_EDGE('',*,*,#52858,.T.);
#76412=ORIENTED_EDGE('',*,*,#52859,.T.);
#76413=ORIENTED_EDGE('',*,*,#52860,.T.);
#76414=ORIENTED_EDGE('',*,*,#52861,.T.);
#76415=ORIENTED_EDGE('',*,*,#52862,.T.);
#76416=ORIENTED_EDGE('',*,*,#52863,.T.);
#76417=ORIENTED_EDGE('',*,*,#52864,.F.);
#76418=ORIENTED_EDGE('',*,*,#52865,.T.);
#76419=ORIENTED_EDGE('',*,*,#52866,.T.);
#76420=ORIENTED_EDGE('',*,*,#52864,.T.);
#76421=ORIENTED_EDGE('',*,*,#52867,.T.);
#76422=ORIENTED_EDGE('',*,*,#52857,.F.);
#76423=ORIENTED_EDGE('',*,*,#52868,.T.);
#76424=ORIENTED_EDGE('',*,*,#52869,.F.);
#76425=ORIENTED_EDGE('',*,*,#52865,.F.);
#76426=ORIENTED_EDGE('',*,*,#52870,.F.);
#76427=ORIENTED_EDGE('',*,*,#52871,.F.);
#76428=ORIENTED_EDGE('',*,*,#52870,.T.);
#76429=ORIENTED_EDGE('',*,*,#52868,.F.);
#76430=ORIENTED_EDGE('',*,*,#52872,.F.);
#76431=ORIENTED_EDGE('',*,*,#52872,.T.);
#76432=ORIENTED_EDGE('',*,*,#52861,.F.);
#76433=ORIENTED_EDGE('',*,*,#52873,.F.);
#76434=ORIENTED_EDGE('',*,*,#52874,.F.);
#76435=ORIENTED_EDGE('',*,*,#52875,.T.);
#76436=ORIENTED_EDGE('',*,*,#52876,.F.);
#76437=ORIENTED_EDGE('',*,*,#52877,.F.);
#76438=ORIENTED_EDGE('',*,*,#50294,.F.);
#76439=ORIENTED_EDGE('',*,*,#52878,.T.);
#76440=ORIENTED_EDGE('',*,*,#52869,.T.);
#76441=ORIENTED_EDGE('',*,*,#52875,.F.);
#76442=ORIENTED_EDGE('',*,*,#50293,.T.);
#76443=ORIENTED_EDGE('',*,*,#52879,.F.);
#76444=ORIENTED_EDGE('',*,*,#52866,.F.);
#76445=ORIENTED_EDGE('',*,*,#52878,.F.);
#76446=ORIENTED_EDGE('',*,*,#50292,.F.);
#76447=ORIENTED_EDGE('',*,*,#52879,.T.);
#76448=ORIENTED_EDGE('',*,*,#50720,.F.);
#76449=ORIENTED_EDGE('',*,*,#52880,.F.);
#76450=ORIENTED_EDGE('',*,*,#52862,.F.);
#76451=ORIENTED_EDGE('',*,*,#52880,.T.);
#76452=ORIENTED_EDGE('',*,*,#49718,.F.);
#76453=ORIENTED_EDGE('',*,*,#52881,.F.);
#76454=ORIENTED_EDGE('',*,*,#52863,.F.);
#76455=ORIENTED_EDGE('',*,*,#52881,.T.);
#76456=ORIENTED_EDGE('',*,*,#49717,.F.);
#76457=ORIENTED_EDGE('',*,*,#52882,.F.);
#76458=ORIENTED_EDGE('',*,*,#52867,.F.);
#76459=ORIENTED_EDGE('',*,*,#52882,.T.);
#76460=ORIENTED_EDGE('',*,*,#49716,.F.);
#76461=ORIENTED_EDGE('',*,*,#52883,.F.);
#76462=ORIENTED_EDGE('',*,*,#52858,.F.);
#76463=ORIENTED_EDGE('',*,*,#52884,.T.);
#76464=ORIENTED_EDGE('',*,*,#52859,.F.);
#76465=ORIENTED_EDGE('',*,*,#52883,.T.);
#76466=ORIENTED_EDGE('',*,*,#50721,.F.);
#76467=ORIENTED_EDGE('',*,*,#52885,.T.);
#76468=ORIENTED_EDGE('',*,*,#52860,.F.);
#76469=ORIENTED_EDGE('',*,*,#52884,.F.);
#76470=ORIENTED_EDGE('',*,*,#50296,.F.);
#76471=ORIENTED_EDGE('',*,*,#52877,.T.);
#76472=ORIENTED_EDGE('',*,*,#52873,.T.);
#76473=ORIENTED_EDGE('',*,*,#52885,.F.);
#76474=ORIENTED_EDGE('',*,*,#50295,.T.);
#76475=ORIENTED_EDGE('',*,*,#52871,.T.);
#76476=ORIENTED_EDGE('',*,*,#52874,.T.);
#76477=ORIENTED_EDGE('',*,*,#52876,.T.);
#76478=ORIENTED_EDGE('',*,*,#52886,.T.);
#76479=ORIENTED_EDGE('',*,*,#52887,.T.);
#76480=ORIENTED_EDGE('',*,*,#52888,.T.);
#76481=ORIENTED_EDGE('',*,*,#52889,.T.);
#76482=ORIENTED_EDGE('',*,*,#52890,.T.);
#76483=ORIENTED_EDGE('',*,*,#52891,.T.);
#76484=ORIENTED_EDGE('',*,*,#52892,.T.);
#76485=ORIENTED_EDGE('',*,*,#52893,.F.);
#76486=ORIENTED_EDGE('',*,*,#52894,.T.);
#76487=ORIENTED_EDGE('',*,*,#52895,.T.);
#76488=ORIENTED_EDGE('',*,*,#52893,.T.);
#76489=ORIENTED_EDGE('',*,*,#52896,.T.);
#76490=ORIENTED_EDGE('',*,*,#52886,.F.);
#76491=ORIENTED_EDGE('',*,*,#52897,.T.);
#76492=ORIENTED_EDGE('',*,*,#52898,.F.);
#76493=ORIENTED_EDGE('',*,*,#52894,.F.);
#76494=ORIENTED_EDGE('',*,*,#52899,.F.);
#76495=ORIENTED_EDGE('',*,*,#52900,.F.);
#76496=ORIENTED_EDGE('',*,*,#52899,.T.);
#76497=ORIENTED_EDGE('',*,*,#52897,.F.);
#76498=ORIENTED_EDGE('',*,*,#52901,.F.);
#76499=ORIENTED_EDGE('',*,*,#52901,.T.);
#76500=ORIENTED_EDGE('',*,*,#52890,.F.);
#76501=ORIENTED_EDGE('',*,*,#52902,.F.);
#76502=ORIENTED_EDGE('',*,*,#52903,.F.);
#76503=ORIENTED_EDGE('',*,*,#52904,.T.);
#76504=ORIENTED_EDGE('',*,*,#52905,.F.);
#76505=ORIENTED_EDGE('',*,*,#52906,.F.);
#76506=ORIENTED_EDGE('',*,*,#50288,.F.);
#76507=ORIENTED_EDGE('',*,*,#52907,.T.);
#76508=ORIENTED_EDGE('',*,*,#52898,.T.);
#76509=ORIENTED_EDGE('',*,*,#52904,.F.);
#76510=ORIENTED_EDGE('',*,*,#50287,.T.);
#76511=ORIENTED_EDGE('',*,*,#52908,.F.);
#76512=ORIENTED_EDGE('',*,*,#52895,.F.);
#76513=ORIENTED_EDGE('',*,*,#52907,.F.);
#76514=ORIENTED_EDGE('',*,*,#50286,.F.);
#76515=ORIENTED_EDGE('',*,*,#52908,.T.);
#76516=ORIENTED_EDGE('',*,*,#50718,.F.);
#76517=ORIENTED_EDGE('',*,*,#52909,.F.);
#76518=ORIENTED_EDGE('',*,*,#52891,.F.);
#76519=ORIENTED_EDGE('',*,*,#52909,.T.);
#76520=ORIENTED_EDGE('',*,*,#49722,.F.);
#76521=ORIENTED_EDGE('',*,*,#52910,.F.);
#76522=ORIENTED_EDGE('',*,*,#52892,.F.);
#76523=ORIENTED_EDGE('',*,*,#52910,.T.);
#76524=ORIENTED_EDGE('',*,*,#49721,.F.);
#76525=ORIENTED_EDGE('',*,*,#52911,.F.);
#76526=ORIENTED_EDGE('',*,*,#52896,.F.);
#76527=ORIENTED_EDGE('',*,*,#52911,.T.);
#76528=ORIENTED_EDGE('',*,*,#49720,.F.);
#76529=ORIENTED_EDGE('',*,*,#52912,.F.);
#76530=ORIENTED_EDGE('',*,*,#52887,.F.);
#76531=ORIENTED_EDGE('',*,*,#52913,.T.);
#76532=ORIENTED_EDGE('',*,*,#52888,.F.);
#76533=ORIENTED_EDGE('',*,*,#52912,.T.);
#76534=ORIENTED_EDGE('',*,*,#50719,.F.);
#76535=ORIENTED_EDGE('',*,*,#52914,.T.);
#76536=ORIENTED_EDGE('',*,*,#52889,.F.);
#76537=ORIENTED_EDGE('',*,*,#52913,.F.);
#76538=ORIENTED_EDGE('',*,*,#50290,.F.);
#76539=ORIENTED_EDGE('',*,*,#52906,.T.);
#76540=ORIENTED_EDGE('',*,*,#52902,.T.);
#76541=ORIENTED_EDGE('',*,*,#52914,.F.);
#76542=ORIENTED_EDGE('',*,*,#50289,.T.);
#76543=ORIENTED_EDGE('',*,*,#52900,.T.);
#76544=ORIENTED_EDGE('',*,*,#52903,.T.);
#76545=ORIENTED_EDGE('',*,*,#52905,.T.);
#76546=ORIENTED_EDGE('',*,*,#52915,.T.);
#76547=ORIENTED_EDGE('',*,*,#52916,.T.);
#76548=ORIENTED_EDGE('',*,*,#52917,.T.);
#76549=ORIENTED_EDGE('',*,*,#52918,.T.);
#76550=ORIENTED_EDGE('',*,*,#52919,.T.);
#76551=ORIENTED_EDGE('',*,*,#52920,.T.);
#76552=ORIENTED_EDGE('',*,*,#52921,.T.);
#76553=ORIENTED_EDGE('',*,*,#52922,.F.);
#76554=ORIENTED_EDGE('',*,*,#52923,.T.);
#76555=ORIENTED_EDGE('',*,*,#52924,.T.);
#76556=ORIENTED_EDGE('',*,*,#52922,.T.);
#76557=ORIENTED_EDGE('',*,*,#52925,.T.);
#76558=ORIENTED_EDGE('',*,*,#52915,.F.);
#76559=ORIENTED_EDGE('',*,*,#52926,.T.);
#76560=ORIENTED_EDGE('',*,*,#52927,.F.);
#76561=ORIENTED_EDGE('',*,*,#52923,.F.);
#76562=ORIENTED_EDGE('',*,*,#52928,.F.);
#76563=ORIENTED_EDGE('',*,*,#52929,.F.);
#76564=ORIENTED_EDGE('',*,*,#52928,.T.);
#76565=ORIENTED_EDGE('',*,*,#52926,.F.);
#76566=ORIENTED_EDGE('',*,*,#52930,.F.);
#76567=ORIENTED_EDGE('',*,*,#52930,.T.);
#76568=ORIENTED_EDGE('',*,*,#52919,.F.);
#76569=ORIENTED_EDGE('',*,*,#52931,.F.);
#76570=ORIENTED_EDGE('',*,*,#52932,.F.);
#76571=ORIENTED_EDGE('',*,*,#52933,.T.);
#76572=ORIENTED_EDGE('',*,*,#52934,.F.);
#76573=ORIENTED_EDGE('',*,*,#52935,.F.);
#76574=ORIENTED_EDGE('',*,*,#50282,.F.);
#76575=ORIENTED_EDGE('',*,*,#52936,.T.);
#76576=ORIENTED_EDGE('',*,*,#52927,.T.);
#76577=ORIENTED_EDGE('',*,*,#52933,.F.);
#76578=ORIENTED_EDGE('',*,*,#50281,.T.);
#76579=ORIENTED_EDGE('',*,*,#52937,.F.);
#76580=ORIENTED_EDGE('',*,*,#52924,.F.);
#76581=ORIENTED_EDGE('',*,*,#52936,.F.);
#76582=ORIENTED_EDGE('',*,*,#50280,.F.);
#76583=ORIENTED_EDGE('',*,*,#52937,.T.);
#76584=ORIENTED_EDGE('',*,*,#50716,.F.);
#76585=ORIENTED_EDGE('',*,*,#52938,.F.);
#76586=ORIENTED_EDGE('',*,*,#52920,.F.);
#76587=ORIENTED_EDGE('',*,*,#52938,.T.);
#76588=ORIENTED_EDGE('',*,*,#49726,.F.);
#76589=ORIENTED_EDGE('',*,*,#52939,.F.);
#76590=ORIENTED_EDGE('',*,*,#52921,.F.);
#76591=ORIENTED_EDGE('',*,*,#52939,.T.);
#76592=ORIENTED_EDGE('',*,*,#49725,.F.);
#76593=ORIENTED_EDGE('',*,*,#52940,.F.);
#76594=ORIENTED_EDGE('',*,*,#52925,.F.);
#76595=ORIENTED_EDGE('',*,*,#52940,.T.);
#76596=ORIENTED_EDGE('',*,*,#49724,.F.);
#76597=ORIENTED_EDGE('',*,*,#52941,.F.);
#76598=ORIENTED_EDGE('',*,*,#52916,.F.);
#76599=ORIENTED_EDGE('',*,*,#52942,.T.);
#76600=ORIENTED_EDGE('',*,*,#52917,.F.);
#76601=ORIENTED_EDGE('',*,*,#52941,.T.);
#76602=ORIENTED_EDGE('',*,*,#50717,.F.);
#76603=ORIENTED_EDGE('',*,*,#52943,.T.);
#76604=ORIENTED_EDGE('',*,*,#52918,.F.);
#76605=ORIENTED_EDGE('',*,*,#52942,.F.);
#76606=ORIENTED_EDGE('',*,*,#50284,.F.);
#76607=ORIENTED_EDGE('',*,*,#52935,.T.);
#76608=ORIENTED_EDGE('',*,*,#52931,.T.);
#76609=ORIENTED_EDGE('',*,*,#52943,.F.);
#76610=ORIENTED_EDGE('',*,*,#50283,.T.);
#76611=ORIENTED_EDGE('',*,*,#52929,.T.);
#76612=ORIENTED_EDGE('',*,*,#52932,.T.);
#76613=ORIENTED_EDGE('',*,*,#52934,.T.);
#76614=ORIENTED_EDGE('',*,*,#52944,.T.);
#76615=ORIENTED_EDGE('',*,*,#52945,.T.);
#76616=ORIENTED_EDGE('',*,*,#52946,.T.);
#76617=ORIENTED_EDGE('',*,*,#52947,.T.);
#76618=ORIENTED_EDGE('',*,*,#52948,.T.);
#76619=ORIENTED_EDGE('',*,*,#52949,.T.);
#76620=ORIENTED_EDGE('',*,*,#52950,.T.);
#76621=ORIENTED_EDGE('',*,*,#52951,.F.);
#76622=ORIENTED_EDGE('',*,*,#52952,.T.);
#76623=ORIENTED_EDGE('',*,*,#52953,.T.);
#76624=ORIENTED_EDGE('',*,*,#52951,.T.);
#76625=ORIENTED_EDGE('',*,*,#52954,.T.);
#76626=ORIENTED_EDGE('',*,*,#52944,.F.);
#76627=ORIENTED_EDGE('',*,*,#52955,.T.);
#76628=ORIENTED_EDGE('',*,*,#52956,.F.);
#76629=ORIENTED_EDGE('',*,*,#52952,.F.);
#76630=ORIENTED_EDGE('',*,*,#52957,.F.);
#76631=ORIENTED_EDGE('',*,*,#52958,.F.);
#76632=ORIENTED_EDGE('',*,*,#52957,.T.);
#76633=ORIENTED_EDGE('',*,*,#52955,.F.);
#76634=ORIENTED_EDGE('',*,*,#52959,.F.);
#76635=ORIENTED_EDGE('',*,*,#52959,.T.);
#76636=ORIENTED_EDGE('',*,*,#52948,.F.);
#76637=ORIENTED_EDGE('',*,*,#52960,.F.);
#76638=ORIENTED_EDGE('',*,*,#52961,.F.);
#76639=ORIENTED_EDGE('',*,*,#52962,.T.);
#76640=ORIENTED_EDGE('',*,*,#52963,.F.);
#76641=ORIENTED_EDGE('',*,*,#52964,.F.);
#76642=ORIENTED_EDGE('',*,*,#50276,.F.);
#76643=ORIENTED_EDGE('',*,*,#52965,.T.);
#76644=ORIENTED_EDGE('',*,*,#52956,.T.);
#76645=ORIENTED_EDGE('',*,*,#52962,.F.);
#76646=ORIENTED_EDGE('',*,*,#50275,.T.);
#76647=ORIENTED_EDGE('',*,*,#52966,.F.);
#76648=ORIENTED_EDGE('',*,*,#52953,.F.);
#76649=ORIENTED_EDGE('',*,*,#52965,.F.);
#76650=ORIENTED_EDGE('',*,*,#50274,.F.);
#76651=ORIENTED_EDGE('',*,*,#52966,.T.);
#76652=ORIENTED_EDGE('',*,*,#50714,.F.);
#76653=ORIENTED_EDGE('',*,*,#52967,.F.);
#76654=ORIENTED_EDGE('',*,*,#52949,.F.);
#76655=ORIENTED_EDGE('',*,*,#52967,.T.);
#76656=ORIENTED_EDGE('',*,*,#49730,.F.);
#76657=ORIENTED_EDGE('',*,*,#52968,.F.);
#76658=ORIENTED_EDGE('',*,*,#52950,.F.);
#76659=ORIENTED_EDGE('',*,*,#52968,.T.);
#76660=ORIENTED_EDGE('',*,*,#49729,.F.);
#76661=ORIENTED_EDGE('',*,*,#52969,.F.);
#76662=ORIENTED_EDGE('',*,*,#52954,.F.);
#76663=ORIENTED_EDGE('',*,*,#52969,.T.);
#76664=ORIENTED_EDGE('',*,*,#49728,.F.);
#76665=ORIENTED_EDGE('',*,*,#52970,.F.);
#76666=ORIENTED_EDGE('',*,*,#52945,.F.);
#76667=ORIENTED_EDGE('',*,*,#52971,.T.);
#76668=ORIENTED_EDGE('',*,*,#52946,.F.);
#76669=ORIENTED_EDGE('',*,*,#52970,.T.);
#76670=ORIENTED_EDGE('',*,*,#50715,.F.);
#76671=ORIENTED_EDGE('',*,*,#52972,.T.);
#76672=ORIENTED_EDGE('',*,*,#52947,.F.);
#76673=ORIENTED_EDGE('',*,*,#52971,.F.);
#76674=ORIENTED_EDGE('',*,*,#50278,.F.);
#76675=ORIENTED_EDGE('',*,*,#52964,.T.);
#76676=ORIENTED_EDGE('',*,*,#52960,.T.);
#76677=ORIENTED_EDGE('',*,*,#52972,.F.);
#76678=ORIENTED_EDGE('',*,*,#50277,.T.);
#76679=ORIENTED_EDGE('',*,*,#52958,.T.);
#76680=ORIENTED_EDGE('',*,*,#52961,.T.);
#76681=ORIENTED_EDGE('',*,*,#52963,.T.);
#76682=ORIENTED_EDGE('',*,*,#52973,.T.);
#76683=ORIENTED_EDGE('',*,*,#52974,.T.);
#76684=ORIENTED_EDGE('',*,*,#52975,.T.);
#76685=ORIENTED_EDGE('',*,*,#52976,.T.);
#76686=ORIENTED_EDGE('',*,*,#52977,.T.);
#76687=ORIENTED_EDGE('',*,*,#52978,.T.);
#76688=ORIENTED_EDGE('',*,*,#52979,.T.);
#76689=ORIENTED_EDGE('',*,*,#52980,.F.);
#76690=ORIENTED_EDGE('',*,*,#52981,.T.);
#76691=ORIENTED_EDGE('',*,*,#52982,.T.);
#76692=ORIENTED_EDGE('',*,*,#52980,.T.);
#76693=ORIENTED_EDGE('',*,*,#52983,.T.);
#76694=ORIENTED_EDGE('',*,*,#52973,.F.);
#76695=ORIENTED_EDGE('',*,*,#52984,.T.);
#76696=ORIENTED_EDGE('',*,*,#52985,.F.);
#76697=ORIENTED_EDGE('',*,*,#52981,.F.);
#76698=ORIENTED_EDGE('',*,*,#52986,.F.);
#76699=ORIENTED_EDGE('',*,*,#52987,.F.);
#76700=ORIENTED_EDGE('',*,*,#52986,.T.);
#76701=ORIENTED_EDGE('',*,*,#52984,.F.);
#76702=ORIENTED_EDGE('',*,*,#52988,.F.);
#76703=ORIENTED_EDGE('',*,*,#52988,.T.);
#76704=ORIENTED_EDGE('',*,*,#52977,.F.);
#76705=ORIENTED_EDGE('',*,*,#52989,.F.);
#76706=ORIENTED_EDGE('',*,*,#52990,.F.);
#76707=ORIENTED_EDGE('',*,*,#52991,.T.);
#76708=ORIENTED_EDGE('',*,*,#52992,.F.);
#76709=ORIENTED_EDGE('',*,*,#52993,.F.);
#76710=ORIENTED_EDGE('',*,*,#50270,.F.);
#76711=ORIENTED_EDGE('',*,*,#52994,.T.);
#76712=ORIENTED_EDGE('',*,*,#52985,.T.);
#76713=ORIENTED_EDGE('',*,*,#52991,.F.);
#76714=ORIENTED_EDGE('',*,*,#50269,.T.);
#76715=ORIENTED_EDGE('',*,*,#52995,.F.);
#76716=ORIENTED_EDGE('',*,*,#52982,.F.);
#76717=ORIENTED_EDGE('',*,*,#52994,.F.);
#76718=ORIENTED_EDGE('',*,*,#50268,.F.);
#76719=ORIENTED_EDGE('',*,*,#52995,.T.);
#76720=ORIENTED_EDGE('',*,*,#50712,.F.);
#76721=ORIENTED_EDGE('',*,*,#52996,.F.);
#76722=ORIENTED_EDGE('',*,*,#52978,.F.);
#76723=ORIENTED_EDGE('',*,*,#52996,.T.);
#76724=ORIENTED_EDGE('',*,*,#49734,.F.);
#76725=ORIENTED_EDGE('',*,*,#52997,.F.);
#76726=ORIENTED_EDGE('',*,*,#52979,.F.);
#76727=ORIENTED_EDGE('',*,*,#52997,.T.);
#76728=ORIENTED_EDGE('',*,*,#49733,.F.);
#76729=ORIENTED_EDGE('',*,*,#52998,.F.);
#76730=ORIENTED_EDGE('',*,*,#52983,.F.);
#76731=ORIENTED_EDGE('',*,*,#52998,.T.);
#76732=ORIENTED_EDGE('',*,*,#49732,.F.);
#76733=ORIENTED_EDGE('',*,*,#52999,.F.);
#76734=ORIENTED_EDGE('',*,*,#52974,.F.);
#76735=ORIENTED_EDGE('',*,*,#53000,.T.);
#76736=ORIENTED_EDGE('',*,*,#52975,.F.);
#76737=ORIENTED_EDGE('',*,*,#52999,.T.);
#76738=ORIENTED_EDGE('',*,*,#50713,.F.);
#76739=ORIENTED_EDGE('',*,*,#53001,.T.);
#76740=ORIENTED_EDGE('',*,*,#52976,.F.);
#76741=ORIENTED_EDGE('',*,*,#53000,.F.);
#76742=ORIENTED_EDGE('',*,*,#50272,.F.);
#76743=ORIENTED_EDGE('',*,*,#52993,.T.);
#76744=ORIENTED_EDGE('',*,*,#52989,.T.);
#76745=ORIENTED_EDGE('',*,*,#53001,.F.);
#76746=ORIENTED_EDGE('',*,*,#50271,.T.);
#76747=ORIENTED_EDGE('',*,*,#52987,.T.);
#76748=ORIENTED_EDGE('',*,*,#52990,.T.);
#76749=ORIENTED_EDGE('',*,*,#52992,.T.);
#76750=ORIENTED_EDGE('',*,*,#53002,.T.);
#76751=ORIENTED_EDGE('',*,*,#53003,.T.);
#76752=ORIENTED_EDGE('',*,*,#53004,.T.);
#76753=ORIENTED_EDGE('',*,*,#53005,.T.);
#76754=ORIENTED_EDGE('',*,*,#53006,.T.);
#76755=ORIENTED_EDGE('',*,*,#53007,.T.);
#76756=ORIENTED_EDGE('',*,*,#53008,.T.);
#76757=ORIENTED_EDGE('',*,*,#53009,.F.);
#76758=ORIENTED_EDGE('',*,*,#53010,.T.);
#76759=ORIENTED_EDGE('',*,*,#53011,.T.);
#76760=ORIENTED_EDGE('',*,*,#53009,.T.);
#76761=ORIENTED_EDGE('',*,*,#53012,.T.);
#76762=ORIENTED_EDGE('',*,*,#53002,.F.);
#76763=ORIENTED_EDGE('',*,*,#53013,.T.);
#76764=ORIENTED_EDGE('',*,*,#53014,.F.);
#76765=ORIENTED_EDGE('',*,*,#53010,.F.);
#76766=ORIENTED_EDGE('',*,*,#53015,.F.);
#76767=ORIENTED_EDGE('',*,*,#53016,.F.);
#76768=ORIENTED_EDGE('',*,*,#53015,.T.);
#76769=ORIENTED_EDGE('',*,*,#53013,.F.);
#76770=ORIENTED_EDGE('',*,*,#53017,.F.);
#76771=ORIENTED_EDGE('',*,*,#53017,.T.);
#76772=ORIENTED_EDGE('',*,*,#53006,.F.);
#76773=ORIENTED_EDGE('',*,*,#53018,.F.);
#76774=ORIENTED_EDGE('',*,*,#53019,.F.);
#76775=ORIENTED_EDGE('',*,*,#53020,.T.);
#76776=ORIENTED_EDGE('',*,*,#53021,.F.);
#76777=ORIENTED_EDGE('',*,*,#53022,.F.);
#76778=ORIENTED_EDGE('',*,*,#50264,.F.);
#76779=ORIENTED_EDGE('',*,*,#53023,.T.);
#76780=ORIENTED_EDGE('',*,*,#53014,.T.);
#76781=ORIENTED_EDGE('',*,*,#53020,.F.);
#76782=ORIENTED_EDGE('',*,*,#50263,.T.);
#76783=ORIENTED_EDGE('',*,*,#53024,.F.);
#76784=ORIENTED_EDGE('',*,*,#53011,.F.);
#76785=ORIENTED_EDGE('',*,*,#53023,.F.);
#76786=ORIENTED_EDGE('',*,*,#50262,.F.);
#76787=ORIENTED_EDGE('',*,*,#53024,.T.);
#76788=ORIENTED_EDGE('',*,*,#50710,.F.);
#76789=ORIENTED_EDGE('',*,*,#53025,.F.);
#76790=ORIENTED_EDGE('',*,*,#53007,.F.);
#76791=ORIENTED_EDGE('',*,*,#53025,.T.);
#76792=ORIENTED_EDGE('',*,*,#49738,.F.);
#76793=ORIENTED_EDGE('',*,*,#53026,.F.);
#76794=ORIENTED_EDGE('',*,*,#53008,.F.);
#76795=ORIENTED_EDGE('',*,*,#53026,.T.);
#76796=ORIENTED_EDGE('',*,*,#49737,.F.);
#76797=ORIENTED_EDGE('',*,*,#53027,.F.);
#76798=ORIENTED_EDGE('',*,*,#53012,.F.);
#76799=ORIENTED_EDGE('',*,*,#53027,.T.);
#76800=ORIENTED_EDGE('',*,*,#49736,.F.);
#76801=ORIENTED_EDGE('',*,*,#53028,.F.);
#76802=ORIENTED_EDGE('',*,*,#53003,.F.);
#76803=ORIENTED_EDGE('',*,*,#53029,.T.);
#76804=ORIENTED_EDGE('',*,*,#53004,.F.);
#76805=ORIENTED_EDGE('',*,*,#53028,.T.);
#76806=ORIENTED_EDGE('',*,*,#50711,.F.);
#76807=ORIENTED_EDGE('',*,*,#53030,.T.);
#76808=ORIENTED_EDGE('',*,*,#53005,.F.);
#76809=ORIENTED_EDGE('',*,*,#53029,.F.);
#76810=ORIENTED_EDGE('',*,*,#50266,.F.);
#76811=ORIENTED_EDGE('',*,*,#53022,.T.);
#76812=ORIENTED_EDGE('',*,*,#53018,.T.);
#76813=ORIENTED_EDGE('',*,*,#53030,.F.);
#76814=ORIENTED_EDGE('',*,*,#50265,.T.);
#76815=ORIENTED_EDGE('',*,*,#53016,.T.);
#76816=ORIENTED_EDGE('',*,*,#53019,.T.);
#76817=ORIENTED_EDGE('',*,*,#53021,.T.);
#76818=ORIENTED_EDGE('',*,*,#53031,.T.);
#76819=ORIENTED_EDGE('',*,*,#53032,.T.);
#76820=ORIENTED_EDGE('',*,*,#53033,.T.);
#76821=ORIENTED_EDGE('',*,*,#53034,.T.);
#76822=ORIENTED_EDGE('',*,*,#53035,.T.);
#76823=ORIENTED_EDGE('',*,*,#53036,.T.);
#76824=ORIENTED_EDGE('',*,*,#53037,.T.);
#76825=ORIENTED_EDGE('',*,*,#53038,.F.);
#76826=ORIENTED_EDGE('',*,*,#53039,.T.);
#76827=ORIENTED_EDGE('',*,*,#53040,.T.);
#76828=ORIENTED_EDGE('',*,*,#53038,.T.);
#76829=ORIENTED_EDGE('',*,*,#53041,.T.);
#76830=ORIENTED_EDGE('',*,*,#53031,.F.);
#76831=ORIENTED_EDGE('',*,*,#53042,.T.);
#76832=ORIENTED_EDGE('',*,*,#53043,.F.);
#76833=ORIENTED_EDGE('',*,*,#53039,.F.);
#76834=ORIENTED_EDGE('',*,*,#53044,.F.);
#76835=ORIENTED_EDGE('',*,*,#53045,.F.);
#76836=ORIENTED_EDGE('',*,*,#53044,.T.);
#76837=ORIENTED_EDGE('',*,*,#53042,.F.);
#76838=ORIENTED_EDGE('',*,*,#53046,.F.);
#76839=ORIENTED_EDGE('',*,*,#53046,.T.);
#76840=ORIENTED_EDGE('',*,*,#53035,.F.);
#76841=ORIENTED_EDGE('',*,*,#53047,.F.);
#76842=ORIENTED_EDGE('',*,*,#53048,.F.);
#76843=ORIENTED_EDGE('',*,*,#53049,.T.);
#76844=ORIENTED_EDGE('',*,*,#53050,.F.);
#76845=ORIENTED_EDGE('',*,*,#53051,.F.);
#76846=ORIENTED_EDGE('',*,*,#50258,.F.);
#76847=ORIENTED_EDGE('',*,*,#53052,.T.);
#76848=ORIENTED_EDGE('',*,*,#53043,.T.);
#76849=ORIENTED_EDGE('',*,*,#53049,.F.);
#76850=ORIENTED_EDGE('',*,*,#50257,.T.);
#76851=ORIENTED_EDGE('',*,*,#53053,.F.);
#76852=ORIENTED_EDGE('',*,*,#53040,.F.);
#76853=ORIENTED_EDGE('',*,*,#53052,.F.);
#76854=ORIENTED_EDGE('',*,*,#50256,.F.);
#76855=ORIENTED_EDGE('',*,*,#53053,.T.);
#76856=ORIENTED_EDGE('',*,*,#50708,.F.);
#76857=ORIENTED_EDGE('',*,*,#53054,.F.);
#76858=ORIENTED_EDGE('',*,*,#53036,.F.);
#76859=ORIENTED_EDGE('',*,*,#53054,.T.);
#76860=ORIENTED_EDGE('',*,*,#49742,.F.);
#76861=ORIENTED_EDGE('',*,*,#53055,.F.);
#76862=ORIENTED_EDGE('',*,*,#53037,.F.);
#76863=ORIENTED_EDGE('',*,*,#53055,.T.);
#76864=ORIENTED_EDGE('',*,*,#49741,.F.);
#76865=ORIENTED_EDGE('',*,*,#53056,.F.);
#76866=ORIENTED_EDGE('',*,*,#53041,.F.);
#76867=ORIENTED_EDGE('',*,*,#53056,.T.);
#76868=ORIENTED_EDGE('',*,*,#49740,.F.);
#76869=ORIENTED_EDGE('',*,*,#53057,.F.);
#76870=ORIENTED_EDGE('',*,*,#53032,.F.);
#76871=ORIENTED_EDGE('',*,*,#53058,.T.);
#76872=ORIENTED_EDGE('',*,*,#53033,.F.);
#76873=ORIENTED_EDGE('',*,*,#53057,.T.);
#76874=ORIENTED_EDGE('',*,*,#50709,.F.);
#76875=ORIENTED_EDGE('',*,*,#53059,.T.);
#76876=ORIENTED_EDGE('',*,*,#53034,.F.);
#76877=ORIENTED_EDGE('',*,*,#53058,.F.);
#76878=ORIENTED_EDGE('',*,*,#50260,.F.);
#76879=ORIENTED_EDGE('',*,*,#53051,.T.);
#76880=ORIENTED_EDGE('',*,*,#53047,.T.);
#76881=ORIENTED_EDGE('',*,*,#53059,.F.);
#76882=ORIENTED_EDGE('',*,*,#50259,.T.);
#76883=ORIENTED_EDGE('',*,*,#53045,.T.);
#76884=ORIENTED_EDGE('',*,*,#53048,.T.);
#76885=ORIENTED_EDGE('',*,*,#53050,.T.);
#76886=ORIENTED_EDGE('',*,*,#53060,.T.);
#76887=ORIENTED_EDGE('',*,*,#53061,.T.);
#76888=ORIENTED_EDGE('',*,*,#53062,.T.);
#76889=ORIENTED_EDGE('',*,*,#53063,.T.);
#76890=ORIENTED_EDGE('',*,*,#53064,.T.);
#76891=ORIENTED_EDGE('',*,*,#53065,.T.);
#76892=ORIENTED_EDGE('',*,*,#53066,.T.);
#76893=ORIENTED_EDGE('',*,*,#53067,.F.);
#76894=ORIENTED_EDGE('',*,*,#53068,.T.);
#76895=ORIENTED_EDGE('',*,*,#53069,.T.);
#76896=ORIENTED_EDGE('',*,*,#53067,.T.);
#76897=ORIENTED_EDGE('',*,*,#53070,.T.);
#76898=ORIENTED_EDGE('',*,*,#53060,.F.);
#76899=ORIENTED_EDGE('',*,*,#53071,.T.);
#76900=ORIENTED_EDGE('',*,*,#53072,.F.);
#76901=ORIENTED_EDGE('',*,*,#53068,.F.);
#76902=ORIENTED_EDGE('',*,*,#53073,.F.);
#76903=ORIENTED_EDGE('',*,*,#53074,.F.);
#76904=ORIENTED_EDGE('',*,*,#53073,.T.);
#76905=ORIENTED_EDGE('',*,*,#53071,.F.);
#76906=ORIENTED_EDGE('',*,*,#53075,.F.);
#76907=ORIENTED_EDGE('',*,*,#53075,.T.);
#76908=ORIENTED_EDGE('',*,*,#53064,.F.);
#76909=ORIENTED_EDGE('',*,*,#53076,.F.);
#76910=ORIENTED_EDGE('',*,*,#53077,.F.);
#76911=ORIENTED_EDGE('',*,*,#53078,.T.);
#76912=ORIENTED_EDGE('',*,*,#53079,.F.);
#76913=ORIENTED_EDGE('',*,*,#53080,.F.);
#76914=ORIENTED_EDGE('',*,*,#50252,.F.);
#76915=ORIENTED_EDGE('',*,*,#53081,.T.);
#76916=ORIENTED_EDGE('',*,*,#53072,.T.);
#76917=ORIENTED_EDGE('',*,*,#53078,.F.);
#76918=ORIENTED_EDGE('',*,*,#50251,.T.);
#76919=ORIENTED_EDGE('',*,*,#53082,.F.);
#76920=ORIENTED_EDGE('',*,*,#53069,.F.);
#76921=ORIENTED_EDGE('',*,*,#53081,.F.);
#76922=ORIENTED_EDGE('',*,*,#50250,.F.);
#76923=ORIENTED_EDGE('',*,*,#53082,.T.);
#76924=ORIENTED_EDGE('',*,*,#50706,.F.);
#76925=ORIENTED_EDGE('',*,*,#53083,.F.);
#76926=ORIENTED_EDGE('',*,*,#53065,.F.);
#76927=ORIENTED_EDGE('',*,*,#53083,.T.);
#76928=ORIENTED_EDGE('',*,*,#49746,.F.);
#76929=ORIENTED_EDGE('',*,*,#53084,.F.);
#76930=ORIENTED_EDGE('',*,*,#53066,.F.);
#76931=ORIENTED_EDGE('',*,*,#53084,.T.);
#76932=ORIENTED_EDGE('',*,*,#49745,.F.);
#76933=ORIENTED_EDGE('',*,*,#53085,.F.);
#76934=ORIENTED_EDGE('',*,*,#53070,.F.);
#76935=ORIENTED_EDGE('',*,*,#53085,.T.);
#76936=ORIENTED_EDGE('',*,*,#49744,.F.);
#76937=ORIENTED_EDGE('',*,*,#53086,.F.);
#76938=ORIENTED_EDGE('',*,*,#53061,.F.);
#76939=ORIENTED_EDGE('',*,*,#53087,.T.);
#76940=ORIENTED_EDGE('',*,*,#53062,.F.);
#76941=ORIENTED_EDGE('',*,*,#53086,.T.);
#76942=ORIENTED_EDGE('',*,*,#50707,.F.);
#76943=ORIENTED_EDGE('',*,*,#53088,.T.);
#76944=ORIENTED_EDGE('',*,*,#53063,.F.);
#76945=ORIENTED_EDGE('',*,*,#53087,.F.);
#76946=ORIENTED_EDGE('',*,*,#50254,.F.);
#76947=ORIENTED_EDGE('',*,*,#53080,.T.);
#76948=ORIENTED_EDGE('',*,*,#53076,.T.);
#76949=ORIENTED_EDGE('',*,*,#53088,.F.);
#76950=ORIENTED_EDGE('',*,*,#50253,.T.);
#76951=ORIENTED_EDGE('',*,*,#53074,.T.);
#76952=ORIENTED_EDGE('',*,*,#53077,.T.);
#76953=ORIENTED_EDGE('',*,*,#53079,.T.);
#76954=ORIENTED_EDGE('',*,*,#53089,.T.);
#76955=ORIENTED_EDGE('',*,*,#53090,.T.);
#76956=ORIENTED_EDGE('',*,*,#53091,.T.);
#76957=ORIENTED_EDGE('',*,*,#53092,.T.);
#76958=ORIENTED_EDGE('',*,*,#53093,.T.);
#76959=ORIENTED_EDGE('',*,*,#53094,.T.);
#76960=ORIENTED_EDGE('',*,*,#53095,.T.);
#76961=ORIENTED_EDGE('',*,*,#53096,.F.);
#76962=ORIENTED_EDGE('',*,*,#53097,.T.);
#76963=ORIENTED_EDGE('',*,*,#53098,.T.);
#76964=ORIENTED_EDGE('',*,*,#53096,.T.);
#76965=ORIENTED_EDGE('',*,*,#53099,.T.);
#76966=ORIENTED_EDGE('',*,*,#53089,.F.);
#76967=ORIENTED_EDGE('',*,*,#53100,.T.);
#76968=ORIENTED_EDGE('',*,*,#53101,.F.);
#76969=ORIENTED_EDGE('',*,*,#53097,.F.);
#76970=ORIENTED_EDGE('',*,*,#53102,.F.);
#76971=ORIENTED_EDGE('',*,*,#53103,.F.);
#76972=ORIENTED_EDGE('',*,*,#53102,.T.);
#76973=ORIENTED_EDGE('',*,*,#53100,.F.);
#76974=ORIENTED_EDGE('',*,*,#53104,.F.);
#76975=ORIENTED_EDGE('',*,*,#53104,.T.);
#76976=ORIENTED_EDGE('',*,*,#53093,.F.);
#76977=ORIENTED_EDGE('',*,*,#53105,.F.);
#76978=ORIENTED_EDGE('',*,*,#53106,.F.);
#76979=ORIENTED_EDGE('',*,*,#53107,.T.);
#76980=ORIENTED_EDGE('',*,*,#53108,.F.);
#76981=ORIENTED_EDGE('',*,*,#53109,.F.);
#76982=ORIENTED_EDGE('',*,*,#50246,.F.);
#76983=ORIENTED_EDGE('',*,*,#53110,.T.);
#76984=ORIENTED_EDGE('',*,*,#53101,.T.);
#76985=ORIENTED_EDGE('',*,*,#53107,.F.);
#76986=ORIENTED_EDGE('',*,*,#50245,.T.);
#76987=ORIENTED_EDGE('',*,*,#53111,.F.);
#76988=ORIENTED_EDGE('',*,*,#53098,.F.);
#76989=ORIENTED_EDGE('',*,*,#53110,.F.);
#76990=ORIENTED_EDGE('',*,*,#50244,.F.);
#76991=ORIENTED_EDGE('',*,*,#53111,.T.);
#76992=ORIENTED_EDGE('',*,*,#50704,.F.);
#76993=ORIENTED_EDGE('',*,*,#53112,.F.);
#76994=ORIENTED_EDGE('',*,*,#53094,.F.);
#76995=ORIENTED_EDGE('',*,*,#53112,.T.);
#76996=ORIENTED_EDGE('',*,*,#49750,.F.);
#76997=ORIENTED_EDGE('',*,*,#53113,.F.);
#76998=ORIENTED_EDGE('',*,*,#53095,.F.);
#76999=ORIENTED_EDGE('',*,*,#53113,.T.);
#77000=ORIENTED_EDGE('',*,*,#49749,.F.);
#77001=ORIENTED_EDGE('',*,*,#53114,.F.);
#77002=ORIENTED_EDGE('',*,*,#53099,.F.);
#77003=ORIENTED_EDGE('',*,*,#53114,.T.);
#77004=ORIENTED_EDGE('',*,*,#49748,.F.);
#77005=ORIENTED_EDGE('',*,*,#53115,.F.);
#77006=ORIENTED_EDGE('',*,*,#53090,.F.);
#77007=ORIENTED_EDGE('',*,*,#53116,.T.);
#77008=ORIENTED_EDGE('',*,*,#53091,.F.);
#77009=ORIENTED_EDGE('',*,*,#53115,.T.);
#77010=ORIENTED_EDGE('',*,*,#50705,.F.);
#77011=ORIENTED_EDGE('',*,*,#53117,.T.);
#77012=ORIENTED_EDGE('',*,*,#53092,.F.);
#77013=ORIENTED_EDGE('',*,*,#53116,.F.);
#77014=ORIENTED_EDGE('',*,*,#50248,.F.);
#77015=ORIENTED_EDGE('',*,*,#53109,.T.);
#77016=ORIENTED_EDGE('',*,*,#53105,.T.);
#77017=ORIENTED_EDGE('',*,*,#53117,.F.);
#77018=ORIENTED_EDGE('',*,*,#50247,.T.);
#77019=ORIENTED_EDGE('',*,*,#53103,.T.);
#77020=ORIENTED_EDGE('',*,*,#53106,.T.);
#77021=ORIENTED_EDGE('',*,*,#53108,.T.);
#77022=ORIENTED_EDGE('',*,*,#53118,.T.);
#77023=ORIENTED_EDGE('',*,*,#53119,.T.);
#77024=ORIENTED_EDGE('',*,*,#53120,.T.);
#77025=ORIENTED_EDGE('',*,*,#53121,.T.);
#77026=ORIENTED_EDGE('',*,*,#53122,.T.);
#77027=ORIENTED_EDGE('',*,*,#53123,.T.);
#77028=ORIENTED_EDGE('',*,*,#53124,.T.);
#77029=ORIENTED_EDGE('',*,*,#53125,.F.);
#77030=ORIENTED_EDGE('',*,*,#53126,.T.);
#77031=ORIENTED_EDGE('',*,*,#53127,.T.);
#77032=ORIENTED_EDGE('',*,*,#53125,.T.);
#77033=ORIENTED_EDGE('',*,*,#53128,.T.);
#77034=ORIENTED_EDGE('',*,*,#53118,.F.);
#77035=ORIENTED_EDGE('',*,*,#53129,.T.);
#77036=ORIENTED_EDGE('',*,*,#53130,.F.);
#77037=ORIENTED_EDGE('',*,*,#53126,.F.);
#77038=ORIENTED_EDGE('',*,*,#53131,.F.);
#77039=ORIENTED_EDGE('',*,*,#53132,.F.);
#77040=ORIENTED_EDGE('',*,*,#53131,.T.);
#77041=ORIENTED_EDGE('',*,*,#53129,.F.);
#77042=ORIENTED_EDGE('',*,*,#53133,.F.);
#77043=ORIENTED_EDGE('',*,*,#53133,.T.);
#77044=ORIENTED_EDGE('',*,*,#53122,.F.);
#77045=ORIENTED_EDGE('',*,*,#53134,.F.);
#77046=ORIENTED_EDGE('',*,*,#53135,.F.);
#77047=ORIENTED_EDGE('',*,*,#53136,.T.);
#77048=ORIENTED_EDGE('',*,*,#53137,.F.);
#77049=ORIENTED_EDGE('',*,*,#53138,.F.);
#77050=ORIENTED_EDGE('',*,*,#50240,.F.);
#77051=ORIENTED_EDGE('',*,*,#53139,.T.);
#77052=ORIENTED_EDGE('',*,*,#53130,.T.);
#77053=ORIENTED_EDGE('',*,*,#53136,.F.);
#77054=ORIENTED_EDGE('',*,*,#50239,.T.);
#77055=ORIENTED_EDGE('',*,*,#53140,.F.);
#77056=ORIENTED_EDGE('',*,*,#53127,.F.);
#77057=ORIENTED_EDGE('',*,*,#53139,.F.);
#77058=ORIENTED_EDGE('',*,*,#50238,.F.);
#77059=ORIENTED_EDGE('',*,*,#53140,.T.);
#77060=ORIENTED_EDGE('',*,*,#50702,.F.);
#77061=ORIENTED_EDGE('',*,*,#53141,.F.);
#77062=ORIENTED_EDGE('',*,*,#53123,.F.);
#77063=ORIENTED_EDGE('',*,*,#53141,.T.);
#77064=ORIENTED_EDGE('',*,*,#49754,.F.);
#77065=ORIENTED_EDGE('',*,*,#53142,.F.);
#77066=ORIENTED_EDGE('',*,*,#53124,.F.);
#77067=ORIENTED_EDGE('',*,*,#53142,.T.);
#77068=ORIENTED_EDGE('',*,*,#49753,.F.);
#77069=ORIENTED_EDGE('',*,*,#53143,.F.);
#77070=ORIENTED_EDGE('',*,*,#53128,.F.);
#77071=ORIENTED_EDGE('',*,*,#53143,.T.);
#77072=ORIENTED_EDGE('',*,*,#49752,.F.);
#77073=ORIENTED_EDGE('',*,*,#53144,.F.);
#77074=ORIENTED_EDGE('',*,*,#53119,.F.);
#77075=ORIENTED_EDGE('',*,*,#53145,.T.);
#77076=ORIENTED_EDGE('',*,*,#53120,.F.);
#77077=ORIENTED_EDGE('',*,*,#53144,.T.);
#77078=ORIENTED_EDGE('',*,*,#50703,.F.);
#77079=ORIENTED_EDGE('',*,*,#53146,.T.);
#77080=ORIENTED_EDGE('',*,*,#53121,.F.);
#77081=ORIENTED_EDGE('',*,*,#53145,.F.);
#77082=ORIENTED_EDGE('',*,*,#50242,.F.);
#77083=ORIENTED_EDGE('',*,*,#53138,.T.);
#77084=ORIENTED_EDGE('',*,*,#53134,.T.);
#77085=ORIENTED_EDGE('',*,*,#53146,.F.);
#77086=ORIENTED_EDGE('',*,*,#50241,.T.);
#77087=ORIENTED_EDGE('',*,*,#53132,.T.);
#77088=ORIENTED_EDGE('',*,*,#53135,.T.);
#77089=ORIENTED_EDGE('',*,*,#53137,.T.);
#77090=ORIENTED_EDGE('',*,*,#53147,.T.);
#77091=ORIENTED_EDGE('',*,*,#53148,.T.);
#77092=ORIENTED_EDGE('',*,*,#53149,.T.);
#77093=ORIENTED_EDGE('',*,*,#53150,.T.);
#77094=ORIENTED_EDGE('',*,*,#53151,.T.);
#77095=ORIENTED_EDGE('',*,*,#53152,.T.);
#77096=ORIENTED_EDGE('',*,*,#53153,.T.);
#77097=ORIENTED_EDGE('',*,*,#53154,.F.);
#77098=ORIENTED_EDGE('',*,*,#53155,.T.);
#77099=ORIENTED_EDGE('',*,*,#53156,.T.);
#77100=ORIENTED_EDGE('',*,*,#53154,.T.);
#77101=ORIENTED_EDGE('',*,*,#53157,.T.);
#77102=ORIENTED_EDGE('',*,*,#53147,.F.);
#77103=ORIENTED_EDGE('',*,*,#53158,.T.);
#77104=ORIENTED_EDGE('',*,*,#53159,.F.);
#77105=ORIENTED_EDGE('',*,*,#53155,.F.);
#77106=ORIENTED_EDGE('',*,*,#53160,.F.);
#77107=ORIENTED_EDGE('',*,*,#53161,.F.);
#77108=ORIENTED_EDGE('',*,*,#53160,.T.);
#77109=ORIENTED_EDGE('',*,*,#53158,.F.);
#77110=ORIENTED_EDGE('',*,*,#53162,.F.);
#77111=ORIENTED_EDGE('',*,*,#53162,.T.);
#77112=ORIENTED_EDGE('',*,*,#53151,.F.);
#77113=ORIENTED_EDGE('',*,*,#53163,.F.);
#77114=ORIENTED_EDGE('',*,*,#53164,.F.);
#77115=ORIENTED_EDGE('',*,*,#53165,.T.);
#77116=ORIENTED_EDGE('',*,*,#53166,.F.);
#77117=ORIENTED_EDGE('',*,*,#53167,.F.);
#77118=ORIENTED_EDGE('',*,*,#50234,.F.);
#77119=ORIENTED_EDGE('',*,*,#53168,.T.);
#77120=ORIENTED_EDGE('',*,*,#53159,.T.);
#77121=ORIENTED_EDGE('',*,*,#53165,.F.);
#77122=ORIENTED_EDGE('',*,*,#50233,.T.);
#77123=ORIENTED_EDGE('',*,*,#53169,.F.);
#77124=ORIENTED_EDGE('',*,*,#53156,.F.);
#77125=ORIENTED_EDGE('',*,*,#53168,.F.);
#77126=ORIENTED_EDGE('',*,*,#50232,.F.);
#77127=ORIENTED_EDGE('',*,*,#53169,.T.);
#77128=ORIENTED_EDGE('',*,*,#50700,.F.);
#77129=ORIENTED_EDGE('',*,*,#53170,.F.);
#77130=ORIENTED_EDGE('',*,*,#53152,.F.);
#77131=ORIENTED_EDGE('',*,*,#53170,.T.);
#77132=ORIENTED_EDGE('',*,*,#49758,.F.);
#77133=ORIENTED_EDGE('',*,*,#53171,.F.);
#77134=ORIENTED_EDGE('',*,*,#53153,.F.);
#77135=ORIENTED_EDGE('',*,*,#53171,.T.);
#77136=ORIENTED_EDGE('',*,*,#49757,.F.);
#77137=ORIENTED_EDGE('',*,*,#53172,.F.);
#77138=ORIENTED_EDGE('',*,*,#53157,.F.);
#77139=ORIENTED_EDGE('',*,*,#53172,.T.);
#77140=ORIENTED_EDGE('',*,*,#49756,.F.);
#77141=ORIENTED_EDGE('',*,*,#53173,.F.);
#77142=ORIENTED_EDGE('',*,*,#53148,.F.);
#77143=ORIENTED_EDGE('',*,*,#53174,.T.);
#77144=ORIENTED_EDGE('',*,*,#53149,.F.);
#77145=ORIENTED_EDGE('',*,*,#53173,.T.);
#77146=ORIENTED_EDGE('',*,*,#50701,.F.);
#77147=ORIENTED_EDGE('',*,*,#53175,.T.);
#77148=ORIENTED_EDGE('',*,*,#53150,.F.);
#77149=ORIENTED_EDGE('',*,*,#53174,.F.);
#77150=ORIENTED_EDGE('',*,*,#50236,.F.);
#77151=ORIENTED_EDGE('',*,*,#53167,.T.);
#77152=ORIENTED_EDGE('',*,*,#53163,.T.);
#77153=ORIENTED_EDGE('',*,*,#53175,.F.);
#77154=ORIENTED_EDGE('',*,*,#50235,.T.);
#77155=ORIENTED_EDGE('',*,*,#53161,.T.);
#77156=ORIENTED_EDGE('',*,*,#53164,.T.);
#77157=ORIENTED_EDGE('',*,*,#53166,.T.);
#77158=ORIENTED_EDGE('',*,*,#53176,.T.);
#77159=ORIENTED_EDGE('',*,*,#53177,.T.);
#77160=ORIENTED_EDGE('',*,*,#53178,.T.);
#77161=ORIENTED_EDGE('',*,*,#53179,.T.);
#77162=ORIENTED_EDGE('',*,*,#53180,.T.);
#77163=ORIENTED_EDGE('',*,*,#53181,.T.);
#77164=ORIENTED_EDGE('',*,*,#53182,.T.);
#77165=ORIENTED_EDGE('',*,*,#53183,.F.);
#77166=ORIENTED_EDGE('',*,*,#53184,.T.);
#77167=ORIENTED_EDGE('',*,*,#53185,.T.);
#77168=ORIENTED_EDGE('',*,*,#53183,.T.);
#77169=ORIENTED_EDGE('',*,*,#53186,.T.);
#77170=ORIENTED_EDGE('',*,*,#53176,.F.);
#77171=ORIENTED_EDGE('',*,*,#53187,.T.);
#77172=ORIENTED_EDGE('',*,*,#53188,.F.);
#77173=ORIENTED_EDGE('',*,*,#53184,.F.);
#77174=ORIENTED_EDGE('',*,*,#53189,.F.);
#77175=ORIENTED_EDGE('',*,*,#53190,.F.);
#77176=ORIENTED_EDGE('',*,*,#53189,.T.);
#77177=ORIENTED_EDGE('',*,*,#53187,.F.);
#77178=ORIENTED_EDGE('',*,*,#53191,.F.);
#77179=ORIENTED_EDGE('',*,*,#53191,.T.);
#77180=ORIENTED_EDGE('',*,*,#53180,.F.);
#77181=ORIENTED_EDGE('',*,*,#53192,.F.);
#77182=ORIENTED_EDGE('',*,*,#53193,.F.);
#77183=ORIENTED_EDGE('',*,*,#53194,.T.);
#77184=ORIENTED_EDGE('',*,*,#53195,.F.);
#77185=ORIENTED_EDGE('',*,*,#53196,.F.);
#77186=ORIENTED_EDGE('',*,*,#50228,.F.);
#77187=ORIENTED_EDGE('',*,*,#53197,.T.);
#77188=ORIENTED_EDGE('',*,*,#53188,.T.);
#77189=ORIENTED_EDGE('',*,*,#53194,.F.);
#77190=ORIENTED_EDGE('',*,*,#50227,.T.);
#77191=ORIENTED_EDGE('',*,*,#53198,.F.);
#77192=ORIENTED_EDGE('',*,*,#53185,.F.);
#77193=ORIENTED_EDGE('',*,*,#53197,.F.);
#77194=ORIENTED_EDGE('',*,*,#50226,.F.);
#77195=ORIENTED_EDGE('',*,*,#53198,.T.);
#77196=ORIENTED_EDGE('',*,*,#50698,.F.);
#77197=ORIENTED_EDGE('',*,*,#53199,.F.);
#77198=ORIENTED_EDGE('',*,*,#53181,.F.);
#77199=ORIENTED_EDGE('',*,*,#53199,.T.);
#77200=ORIENTED_EDGE('',*,*,#49762,.F.);
#77201=ORIENTED_EDGE('',*,*,#53200,.F.);
#77202=ORIENTED_EDGE('',*,*,#53182,.F.);
#77203=ORIENTED_EDGE('',*,*,#53200,.T.);
#77204=ORIENTED_EDGE('',*,*,#49761,.F.);
#77205=ORIENTED_EDGE('',*,*,#53201,.F.);
#77206=ORIENTED_EDGE('',*,*,#53186,.F.);
#77207=ORIENTED_EDGE('',*,*,#53201,.T.);
#77208=ORIENTED_EDGE('',*,*,#49760,.F.);
#77209=ORIENTED_EDGE('',*,*,#53202,.F.);
#77210=ORIENTED_EDGE('',*,*,#53177,.F.);
#77211=ORIENTED_EDGE('',*,*,#53203,.T.);
#77212=ORIENTED_EDGE('',*,*,#53178,.F.);
#77213=ORIENTED_EDGE('',*,*,#53202,.T.);
#77214=ORIENTED_EDGE('',*,*,#50699,.F.);
#77215=ORIENTED_EDGE('',*,*,#53204,.T.);
#77216=ORIENTED_EDGE('',*,*,#53179,.F.);
#77217=ORIENTED_EDGE('',*,*,#53203,.F.);
#77218=ORIENTED_EDGE('',*,*,#50230,.F.);
#77219=ORIENTED_EDGE('',*,*,#53196,.T.);
#77220=ORIENTED_EDGE('',*,*,#53192,.T.);
#77221=ORIENTED_EDGE('',*,*,#53204,.F.);
#77222=ORIENTED_EDGE('',*,*,#50229,.T.);
#77223=ORIENTED_EDGE('',*,*,#53190,.T.);
#77224=ORIENTED_EDGE('',*,*,#53193,.T.);
#77225=ORIENTED_EDGE('',*,*,#53195,.T.);
#77226=ORIENTED_EDGE('',*,*,#53205,.T.);
#77227=ORIENTED_EDGE('',*,*,#53206,.T.);
#77228=ORIENTED_EDGE('',*,*,#53207,.T.);
#77229=ORIENTED_EDGE('',*,*,#53208,.T.);
#77230=ORIENTED_EDGE('',*,*,#53209,.T.);
#77231=ORIENTED_EDGE('',*,*,#53210,.T.);
#77232=ORIENTED_EDGE('',*,*,#53211,.T.);
#77233=ORIENTED_EDGE('',*,*,#53212,.F.);
#77234=ORIENTED_EDGE('',*,*,#53213,.T.);
#77235=ORIENTED_EDGE('',*,*,#53214,.T.);
#77236=ORIENTED_EDGE('',*,*,#53212,.T.);
#77237=ORIENTED_EDGE('',*,*,#53215,.T.);
#77238=ORIENTED_EDGE('',*,*,#53205,.F.);
#77239=ORIENTED_EDGE('',*,*,#53216,.T.);
#77240=ORIENTED_EDGE('',*,*,#53217,.F.);
#77241=ORIENTED_EDGE('',*,*,#53213,.F.);
#77242=ORIENTED_EDGE('',*,*,#53218,.F.);
#77243=ORIENTED_EDGE('',*,*,#53219,.F.);
#77244=ORIENTED_EDGE('',*,*,#53218,.T.);
#77245=ORIENTED_EDGE('',*,*,#53216,.F.);
#77246=ORIENTED_EDGE('',*,*,#53220,.F.);
#77247=ORIENTED_EDGE('',*,*,#53220,.T.);
#77248=ORIENTED_EDGE('',*,*,#53209,.F.);
#77249=ORIENTED_EDGE('',*,*,#53221,.F.);
#77250=ORIENTED_EDGE('',*,*,#53222,.F.);
#77251=ORIENTED_EDGE('',*,*,#53223,.T.);
#77252=ORIENTED_EDGE('',*,*,#53224,.F.);
#77253=ORIENTED_EDGE('',*,*,#53225,.F.);
#77254=ORIENTED_EDGE('',*,*,#50222,.F.);
#77255=ORIENTED_EDGE('',*,*,#53226,.T.);
#77256=ORIENTED_EDGE('',*,*,#53217,.T.);
#77257=ORIENTED_EDGE('',*,*,#53223,.F.);
#77258=ORIENTED_EDGE('',*,*,#50221,.T.);
#77259=ORIENTED_EDGE('',*,*,#53227,.F.);
#77260=ORIENTED_EDGE('',*,*,#53214,.F.);
#77261=ORIENTED_EDGE('',*,*,#53226,.F.);
#77262=ORIENTED_EDGE('',*,*,#50220,.F.);
#77263=ORIENTED_EDGE('',*,*,#53227,.T.);
#77264=ORIENTED_EDGE('',*,*,#50696,.F.);
#77265=ORIENTED_EDGE('',*,*,#53228,.F.);
#77266=ORIENTED_EDGE('',*,*,#53210,.F.);
#77267=ORIENTED_EDGE('',*,*,#53228,.T.);
#77268=ORIENTED_EDGE('',*,*,#49766,.F.);
#77269=ORIENTED_EDGE('',*,*,#53229,.F.);
#77270=ORIENTED_EDGE('',*,*,#53211,.F.);
#77271=ORIENTED_EDGE('',*,*,#53229,.T.);
#77272=ORIENTED_EDGE('',*,*,#49765,.F.);
#77273=ORIENTED_EDGE('',*,*,#53230,.F.);
#77274=ORIENTED_EDGE('',*,*,#53215,.F.);
#77275=ORIENTED_EDGE('',*,*,#53230,.T.);
#77276=ORIENTED_EDGE('',*,*,#49764,.F.);
#77277=ORIENTED_EDGE('',*,*,#53231,.F.);
#77278=ORIENTED_EDGE('',*,*,#53206,.F.);
#77279=ORIENTED_EDGE('',*,*,#53232,.T.);
#77280=ORIENTED_EDGE('',*,*,#53207,.F.);
#77281=ORIENTED_EDGE('',*,*,#53231,.T.);
#77282=ORIENTED_EDGE('',*,*,#50697,.F.);
#77283=ORIENTED_EDGE('',*,*,#53233,.T.);
#77284=ORIENTED_EDGE('',*,*,#53208,.F.);
#77285=ORIENTED_EDGE('',*,*,#53232,.F.);
#77286=ORIENTED_EDGE('',*,*,#50224,.F.);
#77287=ORIENTED_EDGE('',*,*,#53225,.T.);
#77288=ORIENTED_EDGE('',*,*,#53221,.T.);
#77289=ORIENTED_EDGE('',*,*,#53233,.F.);
#77290=ORIENTED_EDGE('',*,*,#50223,.T.);
#77291=ORIENTED_EDGE('',*,*,#53219,.T.);
#77292=ORIENTED_EDGE('',*,*,#53222,.T.);
#77293=ORIENTED_EDGE('',*,*,#53224,.T.);
#77294=ORIENTED_EDGE('',*,*,#53234,.T.);
#77295=ORIENTED_EDGE('',*,*,#53235,.T.);
#77296=ORIENTED_EDGE('',*,*,#53236,.T.);
#77297=ORIENTED_EDGE('',*,*,#53237,.T.);
#77298=ORIENTED_EDGE('',*,*,#53238,.T.);
#77299=ORIENTED_EDGE('',*,*,#53239,.T.);
#77300=ORIENTED_EDGE('',*,*,#53240,.T.);
#77301=ORIENTED_EDGE('',*,*,#53241,.F.);
#77302=ORIENTED_EDGE('',*,*,#53242,.T.);
#77303=ORIENTED_EDGE('',*,*,#53243,.T.);
#77304=ORIENTED_EDGE('',*,*,#53241,.T.);
#77305=ORIENTED_EDGE('',*,*,#53244,.T.);
#77306=ORIENTED_EDGE('',*,*,#53234,.F.);
#77307=ORIENTED_EDGE('',*,*,#53245,.T.);
#77308=ORIENTED_EDGE('',*,*,#53246,.F.);
#77309=ORIENTED_EDGE('',*,*,#53242,.F.);
#77310=ORIENTED_EDGE('',*,*,#53247,.F.);
#77311=ORIENTED_EDGE('',*,*,#53248,.F.);
#77312=ORIENTED_EDGE('',*,*,#53247,.T.);
#77313=ORIENTED_EDGE('',*,*,#53245,.F.);
#77314=ORIENTED_EDGE('',*,*,#53249,.F.);
#77315=ORIENTED_EDGE('',*,*,#53249,.T.);
#77316=ORIENTED_EDGE('',*,*,#53238,.F.);
#77317=ORIENTED_EDGE('',*,*,#53250,.F.);
#77318=ORIENTED_EDGE('',*,*,#53251,.F.);
#77319=ORIENTED_EDGE('',*,*,#53252,.T.);
#77320=ORIENTED_EDGE('',*,*,#53253,.F.);
#77321=ORIENTED_EDGE('',*,*,#53254,.F.);
#77322=ORIENTED_EDGE('',*,*,#50216,.F.);
#77323=ORIENTED_EDGE('',*,*,#53255,.T.);
#77324=ORIENTED_EDGE('',*,*,#53246,.T.);
#77325=ORIENTED_EDGE('',*,*,#53252,.F.);
#77326=ORIENTED_EDGE('',*,*,#50215,.T.);
#77327=ORIENTED_EDGE('',*,*,#53256,.F.);
#77328=ORIENTED_EDGE('',*,*,#53243,.F.);
#77329=ORIENTED_EDGE('',*,*,#53255,.F.);
#77330=ORIENTED_EDGE('',*,*,#50214,.F.);
#77331=ORIENTED_EDGE('',*,*,#53256,.T.);
#77332=ORIENTED_EDGE('',*,*,#50694,.F.);
#77333=ORIENTED_EDGE('',*,*,#53257,.F.);
#77334=ORIENTED_EDGE('',*,*,#53239,.F.);
#77335=ORIENTED_EDGE('',*,*,#53257,.T.);
#77336=ORIENTED_EDGE('',*,*,#49770,.F.);
#77337=ORIENTED_EDGE('',*,*,#53258,.F.);
#77338=ORIENTED_EDGE('',*,*,#53240,.F.);
#77339=ORIENTED_EDGE('',*,*,#53258,.T.);
#77340=ORIENTED_EDGE('',*,*,#49769,.F.);
#77341=ORIENTED_EDGE('',*,*,#53259,.F.);
#77342=ORIENTED_EDGE('',*,*,#53244,.F.);
#77343=ORIENTED_EDGE('',*,*,#53259,.T.);
#77344=ORIENTED_EDGE('',*,*,#49768,.F.);
#77345=ORIENTED_EDGE('',*,*,#53260,.F.);
#77346=ORIENTED_EDGE('',*,*,#53235,.F.);
#77347=ORIENTED_EDGE('',*,*,#53261,.T.);
#77348=ORIENTED_EDGE('',*,*,#53236,.F.);
#77349=ORIENTED_EDGE('',*,*,#53260,.T.);
#77350=ORIENTED_EDGE('',*,*,#50695,.F.);
#77351=ORIENTED_EDGE('',*,*,#53262,.T.);
#77352=ORIENTED_EDGE('',*,*,#53237,.F.);
#77353=ORIENTED_EDGE('',*,*,#53261,.F.);
#77354=ORIENTED_EDGE('',*,*,#50218,.F.);
#77355=ORIENTED_EDGE('',*,*,#53254,.T.);
#77356=ORIENTED_EDGE('',*,*,#53250,.T.);
#77357=ORIENTED_EDGE('',*,*,#53262,.F.);
#77358=ORIENTED_EDGE('',*,*,#50217,.T.);
#77359=ORIENTED_EDGE('',*,*,#53248,.T.);
#77360=ORIENTED_EDGE('',*,*,#53251,.T.);
#77361=ORIENTED_EDGE('',*,*,#53253,.T.);
#77362=ORIENTED_EDGE('',*,*,#53263,.T.);
#77363=ORIENTED_EDGE('',*,*,#53264,.T.);
#77364=ORIENTED_EDGE('',*,*,#53265,.T.);
#77365=ORIENTED_EDGE('',*,*,#53266,.T.);
#77366=ORIENTED_EDGE('',*,*,#53267,.T.);
#77367=ORIENTED_EDGE('',*,*,#53268,.T.);
#77368=ORIENTED_EDGE('',*,*,#53269,.T.);
#77369=ORIENTED_EDGE('',*,*,#53270,.F.);
#77370=ORIENTED_EDGE('',*,*,#53271,.T.);
#77371=ORIENTED_EDGE('',*,*,#53272,.T.);
#77372=ORIENTED_EDGE('',*,*,#53270,.T.);
#77373=ORIENTED_EDGE('',*,*,#53273,.T.);
#77374=ORIENTED_EDGE('',*,*,#53263,.F.);
#77375=ORIENTED_EDGE('',*,*,#53274,.T.);
#77376=ORIENTED_EDGE('',*,*,#53275,.F.);
#77377=ORIENTED_EDGE('',*,*,#53271,.F.);
#77378=ORIENTED_EDGE('',*,*,#53276,.F.);
#77379=ORIENTED_EDGE('',*,*,#53277,.F.);
#77380=ORIENTED_EDGE('',*,*,#53276,.T.);
#77381=ORIENTED_EDGE('',*,*,#53274,.F.);
#77382=ORIENTED_EDGE('',*,*,#53278,.F.);
#77383=ORIENTED_EDGE('',*,*,#53278,.T.);
#77384=ORIENTED_EDGE('',*,*,#53267,.F.);
#77385=ORIENTED_EDGE('',*,*,#53279,.F.);
#77386=ORIENTED_EDGE('',*,*,#53280,.F.);
#77387=ORIENTED_EDGE('',*,*,#53281,.T.);
#77388=ORIENTED_EDGE('',*,*,#53282,.F.);
#77389=ORIENTED_EDGE('',*,*,#53283,.F.);
#77390=ORIENTED_EDGE('',*,*,#50210,.F.);
#77391=ORIENTED_EDGE('',*,*,#53284,.T.);
#77392=ORIENTED_EDGE('',*,*,#53275,.T.);
#77393=ORIENTED_EDGE('',*,*,#53281,.F.);
#77394=ORIENTED_EDGE('',*,*,#50209,.T.);
#77395=ORIENTED_EDGE('',*,*,#53285,.F.);
#77396=ORIENTED_EDGE('',*,*,#53272,.F.);
#77397=ORIENTED_EDGE('',*,*,#53284,.F.);
#77398=ORIENTED_EDGE('',*,*,#50208,.F.);
#77399=ORIENTED_EDGE('',*,*,#53285,.T.);
#77400=ORIENTED_EDGE('',*,*,#50692,.F.);
#77401=ORIENTED_EDGE('',*,*,#53286,.F.);
#77402=ORIENTED_EDGE('',*,*,#53268,.F.);
#77403=ORIENTED_EDGE('',*,*,#53286,.T.);
#77404=ORIENTED_EDGE('',*,*,#49774,.F.);
#77405=ORIENTED_EDGE('',*,*,#53287,.F.);
#77406=ORIENTED_EDGE('',*,*,#53269,.F.);
#77407=ORIENTED_EDGE('',*,*,#53287,.T.);
#77408=ORIENTED_EDGE('',*,*,#49773,.F.);
#77409=ORIENTED_EDGE('',*,*,#53288,.F.);
#77410=ORIENTED_EDGE('',*,*,#53273,.F.);
#77411=ORIENTED_EDGE('',*,*,#53288,.T.);
#77412=ORIENTED_EDGE('',*,*,#49772,.F.);
#77413=ORIENTED_EDGE('',*,*,#53289,.F.);
#77414=ORIENTED_EDGE('',*,*,#53264,.F.);
#77415=ORIENTED_EDGE('',*,*,#53290,.T.);
#77416=ORIENTED_EDGE('',*,*,#53265,.F.);
#77417=ORIENTED_EDGE('',*,*,#53289,.T.);
#77418=ORIENTED_EDGE('',*,*,#50693,.F.);
#77419=ORIENTED_EDGE('',*,*,#53291,.T.);
#77420=ORIENTED_EDGE('',*,*,#53266,.F.);
#77421=ORIENTED_EDGE('',*,*,#53290,.F.);
#77422=ORIENTED_EDGE('',*,*,#50212,.F.);
#77423=ORIENTED_EDGE('',*,*,#53283,.T.);
#77424=ORIENTED_EDGE('',*,*,#53279,.T.);
#77425=ORIENTED_EDGE('',*,*,#53291,.F.);
#77426=ORIENTED_EDGE('',*,*,#50211,.T.);
#77427=ORIENTED_EDGE('',*,*,#53277,.T.);
#77428=ORIENTED_EDGE('',*,*,#53280,.T.);
#77429=ORIENTED_EDGE('',*,*,#53282,.T.);
#77430=ORIENTED_EDGE('',*,*,#53292,.T.);
#77431=ORIENTED_EDGE('',*,*,#53293,.T.);
#77432=ORIENTED_EDGE('',*,*,#53294,.T.);
#77433=ORIENTED_EDGE('',*,*,#53295,.T.);
#77434=ORIENTED_EDGE('',*,*,#53296,.T.);
#77435=ORIENTED_EDGE('',*,*,#53297,.T.);
#77436=ORIENTED_EDGE('',*,*,#53298,.T.);
#77437=ORIENTED_EDGE('',*,*,#53299,.F.);
#77438=ORIENTED_EDGE('',*,*,#53300,.T.);
#77439=ORIENTED_EDGE('',*,*,#53301,.T.);
#77440=ORIENTED_EDGE('',*,*,#53299,.T.);
#77441=ORIENTED_EDGE('',*,*,#53302,.T.);
#77442=ORIENTED_EDGE('',*,*,#53292,.F.);
#77443=ORIENTED_EDGE('',*,*,#53303,.T.);
#77444=ORIENTED_EDGE('',*,*,#53304,.F.);
#77445=ORIENTED_EDGE('',*,*,#53300,.F.);
#77446=ORIENTED_EDGE('',*,*,#53305,.F.);
#77447=ORIENTED_EDGE('',*,*,#53306,.F.);
#77448=ORIENTED_EDGE('',*,*,#53305,.T.);
#77449=ORIENTED_EDGE('',*,*,#53303,.F.);
#77450=ORIENTED_EDGE('',*,*,#53307,.F.);
#77451=ORIENTED_EDGE('',*,*,#53307,.T.);
#77452=ORIENTED_EDGE('',*,*,#53296,.F.);
#77453=ORIENTED_EDGE('',*,*,#53308,.F.);
#77454=ORIENTED_EDGE('',*,*,#53309,.F.);
#77455=ORIENTED_EDGE('',*,*,#53310,.T.);
#77456=ORIENTED_EDGE('',*,*,#53311,.F.);
#77457=ORIENTED_EDGE('',*,*,#53312,.F.);
#77458=ORIENTED_EDGE('',*,*,#50204,.F.);
#77459=ORIENTED_EDGE('',*,*,#53313,.T.);
#77460=ORIENTED_EDGE('',*,*,#53304,.T.);
#77461=ORIENTED_EDGE('',*,*,#53310,.F.);
#77462=ORIENTED_EDGE('',*,*,#50203,.T.);
#77463=ORIENTED_EDGE('',*,*,#53314,.F.);
#77464=ORIENTED_EDGE('',*,*,#53301,.F.);
#77465=ORIENTED_EDGE('',*,*,#53313,.F.);
#77466=ORIENTED_EDGE('',*,*,#50202,.F.);
#77467=ORIENTED_EDGE('',*,*,#53314,.T.);
#77468=ORIENTED_EDGE('',*,*,#50690,.F.);
#77469=ORIENTED_EDGE('',*,*,#53315,.F.);
#77470=ORIENTED_EDGE('',*,*,#53297,.F.);
#77471=ORIENTED_EDGE('',*,*,#53315,.T.);
#77472=ORIENTED_EDGE('',*,*,#49778,.F.);
#77473=ORIENTED_EDGE('',*,*,#53316,.F.);
#77474=ORIENTED_EDGE('',*,*,#53298,.F.);
#77475=ORIENTED_EDGE('',*,*,#53316,.T.);
#77476=ORIENTED_EDGE('',*,*,#49777,.F.);
#77477=ORIENTED_EDGE('',*,*,#53317,.F.);
#77478=ORIENTED_EDGE('',*,*,#53302,.F.);
#77479=ORIENTED_EDGE('',*,*,#53317,.T.);
#77480=ORIENTED_EDGE('',*,*,#49776,.F.);
#77481=ORIENTED_EDGE('',*,*,#53318,.F.);
#77482=ORIENTED_EDGE('',*,*,#53293,.F.);
#77483=ORIENTED_EDGE('',*,*,#53319,.T.);
#77484=ORIENTED_EDGE('',*,*,#53294,.F.);
#77485=ORIENTED_EDGE('',*,*,#53318,.T.);
#77486=ORIENTED_EDGE('',*,*,#50691,.F.);
#77487=ORIENTED_EDGE('',*,*,#53320,.T.);
#77488=ORIENTED_EDGE('',*,*,#53295,.F.);
#77489=ORIENTED_EDGE('',*,*,#53319,.F.);
#77490=ORIENTED_EDGE('',*,*,#50206,.F.);
#77491=ORIENTED_EDGE('',*,*,#53312,.T.);
#77492=ORIENTED_EDGE('',*,*,#53308,.T.);
#77493=ORIENTED_EDGE('',*,*,#53320,.F.);
#77494=ORIENTED_EDGE('',*,*,#50205,.T.);
#77495=ORIENTED_EDGE('',*,*,#53306,.T.);
#77496=ORIENTED_EDGE('',*,*,#53309,.T.);
#77497=ORIENTED_EDGE('',*,*,#53311,.T.);
#77498=ORIENTED_EDGE('',*,*,#53321,.T.);
#77499=ORIENTED_EDGE('',*,*,#53322,.T.);
#77500=ORIENTED_EDGE('',*,*,#53323,.T.);
#77501=ORIENTED_EDGE('',*,*,#53324,.T.);
#77502=ORIENTED_EDGE('',*,*,#53325,.T.);
#77503=ORIENTED_EDGE('',*,*,#53326,.T.);
#77504=ORIENTED_EDGE('',*,*,#53327,.T.);
#77505=ORIENTED_EDGE('',*,*,#53328,.F.);
#77506=ORIENTED_EDGE('',*,*,#53329,.T.);
#77507=ORIENTED_EDGE('',*,*,#53330,.T.);
#77508=ORIENTED_EDGE('',*,*,#53328,.T.);
#77509=ORIENTED_EDGE('',*,*,#53331,.T.);
#77510=ORIENTED_EDGE('',*,*,#53321,.F.);
#77511=ORIENTED_EDGE('',*,*,#53332,.T.);
#77512=ORIENTED_EDGE('',*,*,#53333,.F.);
#77513=ORIENTED_EDGE('',*,*,#53329,.F.);
#77514=ORIENTED_EDGE('',*,*,#53334,.F.);
#77515=ORIENTED_EDGE('',*,*,#53335,.F.);
#77516=ORIENTED_EDGE('',*,*,#53334,.T.);
#77517=ORIENTED_EDGE('',*,*,#53332,.F.);
#77518=ORIENTED_EDGE('',*,*,#53336,.F.);
#77519=ORIENTED_EDGE('',*,*,#53336,.T.);
#77520=ORIENTED_EDGE('',*,*,#53325,.F.);
#77521=ORIENTED_EDGE('',*,*,#53337,.F.);
#77522=ORIENTED_EDGE('',*,*,#53338,.F.);
#77523=ORIENTED_EDGE('',*,*,#53339,.T.);
#77524=ORIENTED_EDGE('',*,*,#53340,.F.);
#77525=ORIENTED_EDGE('',*,*,#53341,.F.);
#77526=ORIENTED_EDGE('',*,*,#50198,.F.);
#77527=ORIENTED_EDGE('',*,*,#53342,.T.);
#77528=ORIENTED_EDGE('',*,*,#53333,.T.);
#77529=ORIENTED_EDGE('',*,*,#53339,.F.);
#77530=ORIENTED_EDGE('',*,*,#50197,.T.);
#77531=ORIENTED_EDGE('',*,*,#53343,.F.);
#77532=ORIENTED_EDGE('',*,*,#53330,.F.);
#77533=ORIENTED_EDGE('',*,*,#53342,.F.);
#77534=ORIENTED_EDGE('',*,*,#50196,.F.);
#77535=ORIENTED_EDGE('',*,*,#53343,.T.);
#77536=ORIENTED_EDGE('',*,*,#50688,.F.);
#77537=ORIENTED_EDGE('',*,*,#53344,.F.);
#77538=ORIENTED_EDGE('',*,*,#53326,.F.);
#77539=ORIENTED_EDGE('',*,*,#53344,.T.);
#77540=ORIENTED_EDGE('',*,*,#49782,.F.);
#77541=ORIENTED_EDGE('',*,*,#53345,.F.);
#77542=ORIENTED_EDGE('',*,*,#53327,.F.);
#77543=ORIENTED_EDGE('',*,*,#53345,.T.);
#77544=ORIENTED_EDGE('',*,*,#49781,.F.);
#77545=ORIENTED_EDGE('',*,*,#53346,.F.);
#77546=ORIENTED_EDGE('',*,*,#53331,.F.);
#77547=ORIENTED_EDGE('',*,*,#53346,.T.);
#77548=ORIENTED_EDGE('',*,*,#49780,.F.);
#77549=ORIENTED_EDGE('',*,*,#53347,.F.);
#77550=ORIENTED_EDGE('',*,*,#53322,.F.);
#77551=ORIENTED_EDGE('',*,*,#53348,.T.);
#77552=ORIENTED_EDGE('',*,*,#53323,.F.);
#77553=ORIENTED_EDGE('',*,*,#53347,.T.);
#77554=ORIENTED_EDGE('',*,*,#50689,.F.);
#77555=ORIENTED_EDGE('',*,*,#53349,.T.);
#77556=ORIENTED_EDGE('',*,*,#53324,.F.);
#77557=ORIENTED_EDGE('',*,*,#53348,.F.);
#77558=ORIENTED_EDGE('',*,*,#50200,.F.);
#77559=ORIENTED_EDGE('',*,*,#53341,.T.);
#77560=ORIENTED_EDGE('',*,*,#53337,.T.);
#77561=ORIENTED_EDGE('',*,*,#53349,.F.);
#77562=ORIENTED_EDGE('',*,*,#50199,.T.);
#77563=ORIENTED_EDGE('',*,*,#53335,.T.);
#77564=ORIENTED_EDGE('',*,*,#53338,.T.);
#77565=ORIENTED_EDGE('',*,*,#53340,.T.);
#77566=ORIENTED_EDGE('',*,*,#53350,.T.);
#77567=ORIENTED_EDGE('',*,*,#53351,.T.);
#77568=ORIENTED_EDGE('',*,*,#53352,.T.);
#77569=ORIENTED_EDGE('',*,*,#53353,.T.);
#77570=ORIENTED_EDGE('',*,*,#53354,.T.);
#77571=ORIENTED_EDGE('',*,*,#53355,.T.);
#77572=ORIENTED_EDGE('',*,*,#53356,.T.);
#77573=ORIENTED_EDGE('',*,*,#53357,.F.);
#77574=ORIENTED_EDGE('',*,*,#53358,.T.);
#77575=ORIENTED_EDGE('',*,*,#53359,.T.);
#77576=ORIENTED_EDGE('',*,*,#53357,.T.);
#77577=ORIENTED_EDGE('',*,*,#53360,.T.);
#77578=ORIENTED_EDGE('',*,*,#53350,.F.);
#77579=ORIENTED_EDGE('',*,*,#53361,.T.);
#77580=ORIENTED_EDGE('',*,*,#53362,.F.);
#77581=ORIENTED_EDGE('',*,*,#53358,.F.);
#77582=ORIENTED_EDGE('',*,*,#53363,.F.);
#77583=ORIENTED_EDGE('',*,*,#53364,.F.);
#77584=ORIENTED_EDGE('',*,*,#53363,.T.);
#77585=ORIENTED_EDGE('',*,*,#53361,.F.);
#77586=ORIENTED_EDGE('',*,*,#53365,.F.);
#77587=ORIENTED_EDGE('',*,*,#53365,.T.);
#77588=ORIENTED_EDGE('',*,*,#53354,.F.);
#77589=ORIENTED_EDGE('',*,*,#53366,.F.);
#77590=ORIENTED_EDGE('',*,*,#53367,.F.);
#77591=ORIENTED_EDGE('',*,*,#53368,.T.);
#77592=ORIENTED_EDGE('',*,*,#53369,.F.);
#77593=ORIENTED_EDGE('',*,*,#53370,.F.);
#77594=ORIENTED_EDGE('',*,*,#50192,.F.);
#77595=ORIENTED_EDGE('',*,*,#53371,.T.);
#77596=ORIENTED_EDGE('',*,*,#53362,.T.);
#77597=ORIENTED_EDGE('',*,*,#53368,.F.);
#77598=ORIENTED_EDGE('',*,*,#50191,.T.);
#77599=ORIENTED_EDGE('',*,*,#53372,.F.);
#77600=ORIENTED_EDGE('',*,*,#53359,.F.);
#77601=ORIENTED_EDGE('',*,*,#53371,.F.);
#77602=ORIENTED_EDGE('',*,*,#50190,.F.);
#77603=ORIENTED_EDGE('',*,*,#53372,.T.);
#77604=ORIENTED_EDGE('',*,*,#50686,.F.);
#77605=ORIENTED_EDGE('',*,*,#53373,.F.);
#77606=ORIENTED_EDGE('',*,*,#53355,.F.);
#77607=ORIENTED_EDGE('',*,*,#53373,.T.);
#77608=ORIENTED_EDGE('',*,*,#49786,.F.);
#77609=ORIENTED_EDGE('',*,*,#53374,.F.);
#77610=ORIENTED_EDGE('',*,*,#53356,.F.);
#77611=ORIENTED_EDGE('',*,*,#53374,.T.);
#77612=ORIENTED_EDGE('',*,*,#49785,.F.);
#77613=ORIENTED_EDGE('',*,*,#53375,.F.);
#77614=ORIENTED_EDGE('',*,*,#53360,.F.);
#77615=ORIENTED_EDGE('',*,*,#53375,.T.);
#77616=ORIENTED_EDGE('',*,*,#49784,.F.);
#77617=ORIENTED_EDGE('',*,*,#53376,.F.);
#77618=ORIENTED_EDGE('',*,*,#53351,.F.);
#77619=ORIENTED_EDGE('',*,*,#53377,.T.);
#77620=ORIENTED_EDGE('',*,*,#53352,.F.);
#77621=ORIENTED_EDGE('',*,*,#53376,.T.);
#77622=ORIENTED_EDGE('',*,*,#50687,.F.);
#77623=ORIENTED_EDGE('',*,*,#53378,.T.);
#77624=ORIENTED_EDGE('',*,*,#53353,.F.);
#77625=ORIENTED_EDGE('',*,*,#53377,.F.);
#77626=ORIENTED_EDGE('',*,*,#50194,.F.);
#77627=ORIENTED_EDGE('',*,*,#53370,.T.);
#77628=ORIENTED_EDGE('',*,*,#53366,.T.);
#77629=ORIENTED_EDGE('',*,*,#53378,.F.);
#77630=ORIENTED_EDGE('',*,*,#50193,.T.);
#77631=ORIENTED_EDGE('',*,*,#53364,.T.);
#77632=ORIENTED_EDGE('',*,*,#53367,.T.);
#77633=ORIENTED_EDGE('',*,*,#53369,.T.);
#77634=ORIENTED_EDGE('',*,*,#53379,.T.);
#77635=ORIENTED_EDGE('',*,*,#53380,.T.);
#77636=ORIENTED_EDGE('',*,*,#53381,.T.);
#77637=ORIENTED_EDGE('',*,*,#53382,.T.);
#77638=ORIENTED_EDGE('',*,*,#53383,.T.);
#77639=ORIENTED_EDGE('',*,*,#53384,.T.);
#77640=ORIENTED_EDGE('',*,*,#53385,.T.);
#77641=ORIENTED_EDGE('',*,*,#53386,.F.);
#77642=ORIENTED_EDGE('',*,*,#53387,.T.);
#77643=ORIENTED_EDGE('',*,*,#53388,.T.);
#77644=ORIENTED_EDGE('',*,*,#53386,.T.);
#77645=ORIENTED_EDGE('',*,*,#53389,.T.);
#77646=ORIENTED_EDGE('',*,*,#53379,.F.);
#77647=ORIENTED_EDGE('',*,*,#53390,.T.);
#77648=ORIENTED_EDGE('',*,*,#53391,.F.);
#77649=ORIENTED_EDGE('',*,*,#53387,.F.);
#77650=ORIENTED_EDGE('',*,*,#53392,.F.);
#77651=ORIENTED_EDGE('',*,*,#53393,.F.);
#77652=ORIENTED_EDGE('',*,*,#53392,.T.);
#77653=ORIENTED_EDGE('',*,*,#53390,.F.);
#77654=ORIENTED_EDGE('',*,*,#53394,.F.);
#77655=ORIENTED_EDGE('',*,*,#53394,.T.);
#77656=ORIENTED_EDGE('',*,*,#53383,.F.);
#77657=ORIENTED_EDGE('',*,*,#53395,.F.);
#77658=ORIENTED_EDGE('',*,*,#53396,.F.);
#77659=ORIENTED_EDGE('',*,*,#53397,.T.);
#77660=ORIENTED_EDGE('',*,*,#53398,.F.);
#77661=ORIENTED_EDGE('',*,*,#53399,.F.);
#77662=ORIENTED_EDGE('',*,*,#50186,.F.);
#77663=ORIENTED_EDGE('',*,*,#53400,.T.);
#77664=ORIENTED_EDGE('',*,*,#53391,.T.);
#77665=ORIENTED_EDGE('',*,*,#53397,.F.);
#77666=ORIENTED_EDGE('',*,*,#50185,.T.);
#77667=ORIENTED_EDGE('',*,*,#53401,.F.);
#77668=ORIENTED_EDGE('',*,*,#53388,.F.);
#77669=ORIENTED_EDGE('',*,*,#53400,.F.);
#77670=ORIENTED_EDGE('',*,*,#50184,.F.);
#77671=ORIENTED_EDGE('',*,*,#53401,.T.);
#77672=ORIENTED_EDGE('',*,*,#50684,.F.);
#77673=ORIENTED_EDGE('',*,*,#53402,.F.);
#77674=ORIENTED_EDGE('',*,*,#53384,.F.);
#77675=ORIENTED_EDGE('',*,*,#53402,.T.);
#77676=ORIENTED_EDGE('',*,*,#49790,.F.);
#77677=ORIENTED_EDGE('',*,*,#53403,.F.);
#77678=ORIENTED_EDGE('',*,*,#53385,.F.);
#77679=ORIENTED_EDGE('',*,*,#53403,.T.);
#77680=ORIENTED_EDGE('',*,*,#49789,.F.);
#77681=ORIENTED_EDGE('',*,*,#53404,.F.);
#77682=ORIENTED_EDGE('',*,*,#53389,.F.);
#77683=ORIENTED_EDGE('',*,*,#53404,.T.);
#77684=ORIENTED_EDGE('',*,*,#49788,.F.);
#77685=ORIENTED_EDGE('',*,*,#53405,.F.);
#77686=ORIENTED_EDGE('',*,*,#53380,.F.);
#77687=ORIENTED_EDGE('',*,*,#53406,.T.);
#77688=ORIENTED_EDGE('',*,*,#53381,.F.);
#77689=ORIENTED_EDGE('',*,*,#53405,.T.);
#77690=ORIENTED_EDGE('',*,*,#50685,.F.);
#77691=ORIENTED_EDGE('',*,*,#53407,.T.);
#77692=ORIENTED_EDGE('',*,*,#53382,.F.);
#77693=ORIENTED_EDGE('',*,*,#53406,.F.);
#77694=ORIENTED_EDGE('',*,*,#50188,.F.);
#77695=ORIENTED_EDGE('',*,*,#53399,.T.);
#77696=ORIENTED_EDGE('',*,*,#53395,.T.);
#77697=ORIENTED_EDGE('',*,*,#53407,.F.);
#77698=ORIENTED_EDGE('',*,*,#50187,.T.);
#77699=ORIENTED_EDGE('',*,*,#53393,.T.);
#77700=ORIENTED_EDGE('',*,*,#53396,.T.);
#77701=ORIENTED_EDGE('',*,*,#53398,.T.);
#77702=ORIENTED_EDGE('',*,*,#53408,.T.);
#77703=ORIENTED_EDGE('',*,*,#53409,.T.);
#77704=ORIENTED_EDGE('',*,*,#53410,.T.);
#77705=ORIENTED_EDGE('',*,*,#53411,.T.);
#77706=ORIENTED_EDGE('',*,*,#53412,.T.);
#77707=ORIENTED_EDGE('',*,*,#53413,.T.);
#77708=ORIENTED_EDGE('',*,*,#53414,.T.);
#77709=ORIENTED_EDGE('',*,*,#53415,.F.);
#77710=ORIENTED_EDGE('',*,*,#53416,.T.);
#77711=ORIENTED_EDGE('',*,*,#53417,.T.);
#77712=ORIENTED_EDGE('',*,*,#53415,.T.);
#77713=ORIENTED_EDGE('',*,*,#53418,.T.);
#77714=ORIENTED_EDGE('',*,*,#53408,.F.);
#77715=ORIENTED_EDGE('',*,*,#53419,.T.);
#77716=ORIENTED_EDGE('',*,*,#53420,.F.);
#77717=ORIENTED_EDGE('',*,*,#53416,.F.);
#77718=ORIENTED_EDGE('',*,*,#53421,.F.);
#77719=ORIENTED_EDGE('',*,*,#53422,.F.);
#77720=ORIENTED_EDGE('',*,*,#53421,.T.);
#77721=ORIENTED_EDGE('',*,*,#53419,.F.);
#77722=ORIENTED_EDGE('',*,*,#53423,.F.);
#77723=ORIENTED_EDGE('',*,*,#53423,.T.);
#77724=ORIENTED_EDGE('',*,*,#53412,.F.);
#77725=ORIENTED_EDGE('',*,*,#53424,.F.);
#77726=ORIENTED_EDGE('',*,*,#53425,.F.);
#77727=ORIENTED_EDGE('',*,*,#53426,.T.);
#77728=ORIENTED_EDGE('',*,*,#53427,.F.);
#77729=ORIENTED_EDGE('',*,*,#53428,.F.);
#77730=ORIENTED_EDGE('',*,*,#50180,.F.);
#77731=ORIENTED_EDGE('',*,*,#53429,.T.);
#77732=ORIENTED_EDGE('',*,*,#53420,.T.);
#77733=ORIENTED_EDGE('',*,*,#53426,.F.);
#77734=ORIENTED_EDGE('',*,*,#50179,.T.);
#77735=ORIENTED_EDGE('',*,*,#53430,.F.);
#77736=ORIENTED_EDGE('',*,*,#53417,.F.);
#77737=ORIENTED_EDGE('',*,*,#53429,.F.);
#77738=ORIENTED_EDGE('',*,*,#50178,.F.);
#77739=ORIENTED_EDGE('',*,*,#53430,.T.);
#77740=ORIENTED_EDGE('',*,*,#50682,.F.);
#77741=ORIENTED_EDGE('',*,*,#53431,.F.);
#77742=ORIENTED_EDGE('',*,*,#53413,.F.);
#77743=ORIENTED_EDGE('',*,*,#53431,.T.);
#77744=ORIENTED_EDGE('',*,*,#49794,.F.);
#77745=ORIENTED_EDGE('',*,*,#53432,.F.);
#77746=ORIENTED_EDGE('',*,*,#53414,.F.);
#77747=ORIENTED_EDGE('',*,*,#53432,.T.);
#77748=ORIENTED_EDGE('',*,*,#49793,.F.);
#77749=ORIENTED_EDGE('',*,*,#53433,.F.);
#77750=ORIENTED_EDGE('',*,*,#53418,.F.);
#77751=ORIENTED_EDGE('',*,*,#53433,.T.);
#77752=ORIENTED_EDGE('',*,*,#49792,.F.);
#77753=ORIENTED_EDGE('',*,*,#53434,.F.);
#77754=ORIENTED_EDGE('',*,*,#53409,.F.);
#77755=ORIENTED_EDGE('',*,*,#53435,.T.);
#77756=ORIENTED_EDGE('',*,*,#53410,.F.);
#77757=ORIENTED_EDGE('',*,*,#53434,.T.);
#77758=ORIENTED_EDGE('',*,*,#50683,.F.);
#77759=ORIENTED_EDGE('',*,*,#53436,.T.);
#77760=ORIENTED_EDGE('',*,*,#53411,.F.);
#77761=ORIENTED_EDGE('',*,*,#53435,.F.);
#77762=ORIENTED_EDGE('',*,*,#50182,.F.);
#77763=ORIENTED_EDGE('',*,*,#53428,.T.);
#77764=ORIENTED_EDGE('',*,*,#53424,.T.);
#77765=ORIENTED_EDGE('',*,*,#53436,.F.);
#77766=ORIENTED_EDGE('',*,*,#50181,.T.);
#77767=ORIENTED_EDGE('',*,*,#53422,.T.);
#77768=ORIENTED_EDGE('',*,*,#53425,.T.);
#77769=ORIENTED_EDGE('',*,*,#53427,.T.);
#77770=ORIENTED_EDGE('',*,*,#53437,.T.);
#77771=ORIENTED_EDGE('',*,*,#53438,.T.);
#77772=ORIENTED_EDGE('',*,*,#53439,.T.);
#77773=ORIENTED_EDGE('',*,*,#53440,.T.);
#77774=ORIENTED_EDGE('',*,*,#53441,.T.);
#77775=ORIENTED_EDGE('',*,*,#53442,.T.);
#77776=ORIENTED_EDGE('',*,*,#53443,.T.);
#77777=ORIENTED_EDGE('',*,*,#53444,.F.);
#77778=ORIENTED_EDGE('',*,*,#53445,.T.);
#77779=ORIENTED_EDGE('',*,*,#53446,.T.);
#77780=ORIENTED_EDGE('',*,*,#53444,.T.);
#77781=ORIENTED_EDGE('',*,*,#53447,.T.);
#77782=ORIENTED_EDGE('',*,*,#53437,.F.);
#77783=ORIENTED_EDGE('',*,*,#53448,.T.);
#77784=ORIENTED_EDGE('',*,*,#53449,.F.);
#77785=ORIENTED_EDGE('',*,*,#53445,.F.);
#77786=ORIENTED_EDGE('',*,*,#53450,.F.);
#77787=ORIENTED_EDGE('',*,*,#53451,.F.);
#77788=ORIENTED_EDGE('',*,*,#53450,.T.);
#77789=ORIENTED_EDGE('',*,*,#53448,.F.);
#77790=ORIENTED_EDGE('',*,*,#53452,.F.);
#77791=ORIENTED_EDGE('',*,*,#53452,.T.);
#77792=ORIENTED_EDGE('',*,*,#53441,.F.);
#77793=ORIENTED_EDGE('',*,*,#53453,.F.);
#77794=ORIENTED_EDGE('',*,*,#53454,.F.);
#77795=ORIENTED_EDGE('',*,*,#53455,.T.);
#77796=ORIENTED_EDGE('',*,*,#53456,.F.);
#77797=ORIENTED_EDGE('',*,*,#53457,.F.);
#77798=ORIENTED_EDGE('',*,*,#50174,.F.);
#77799=ORIENTED_EDGE('',*,*,#53458,.T.);
#77800=ORIENTED_EDGE('',*,*,#53449,.T.);
#77801=ORIENTED_EDGE('',*,*,#53455,.F.);
#77802=ORIENTED_EDGE('',*,*,#50173,.T.);
#77803=ORIENTED_EDGE('',*,*,#53459,.F.);
#77804=ORIENTED_EDGE('',*,*,#53446,.F.);
#77805=ORIENTED_EDGE('',*,*,#53458,.F.);
#77806=ORIENTED_EDGE('',*,*,#50172,.F.);
#77807=ORIENTED_EDGE('',*,*,#53459,.T.);
#77808=ORIENTED_EDGE('',*,*,#50680,.F.);
#77809=ORIENTED_EDGE('',*,*,#53460,.F.);
#77810=ORIENTED_EDGE('',*,*,#53442,.F.);
#77811=ORIENTED_EDGE('',*,*,#53460,.T.);
#77812=ORIENTED_EDGE('',*,*,#49798,.F.);
#77813=ORIENTED_EDGE('',*,*,#53461,.F.);
#77814=ORIENTED_EDGE('',*,*,#53443,.F.);
#77815=ORIENTED_EDGE('',*,*,#53461,.T.);
#77816=ORIENTED_EDGE('',*,*,#49797,.F.);
#77817=ORIENTED_EDGE('',*,*,#53462,.F.);
#77818=ORIENTED_EDGE('',*,*,#53447,.F.);
#77819=ORIENTED_EDGE('',*,*,#53462,.T.);
#77820=ORIENTED_EDGE('',*,*,#49796,.F.);
#77821=ORIENTED_EDGE('',*,*,#53463,.F.);
#77822=ORIENTED_EDGE('',*,*,#53438,.F.);
#77823=ORIENTED_EDGE('',*,*,#53464,.T.);
#77824=ORIENTED_EDGE('',*,*,#53439,.F.);
#77825=ORIENTED_EDGE('',*,*,#53463,.T.);
#77826=ORIENTED_EDGE('',*,*,#50681,.F.);
#77827=ORIENTED_EDGE('',*,*,#53465,.T.);
#77828=ORIENTED_EDGE('',*,*,#53440,.F.);
#77829=ORIENTED_EDGE('',*,*,#53464,.F.);
#77830=ORIENTED_EDGE('',*,*,#50176,.F.);
#77831=ORIENTED_EDGE('',*,*,#53457,.T.);
#77832=ORIENTED_EDGE('',*,*,#53453,.T.);
#77833=ORIENTED_EDGE('',*,*,#53465,.F.);
#77834=ORIENTED_EDGE('',*,*,#50175,.T.);
#77835=ORIENTED_EDGE('',*,*,#53451,.T.);
#77836=ORIENTED_EDGE('',*,*,#53454,.T.);
#77837=ORIENTED_EDGE('',*,*,#53456,.T.);
#77838=ORIENTED_EDGE('',*,*,#53466,.T.);
#77839=ORIENTED_EDGE('',*,*,#53467,.T.);
#77840=ORIENTED_EDGE('',*,*,#53468,.T.);
#77841=ORIENTED_EDGE('',*,*,#53469,.T.);
#77842=ORIENTED_EDGE('',*,*,#53470,.T.);
#77843=ORIENTED_EDGE('',*,*,#53471,.T.);
#77844=ORIENTED_EDGE('',*,*,#53472,.T.);
#77845=ORIENTED_EDGE('',*,*,#53473,.F.);
#77846=ORIENTED_EDGE('',*,*,#53474,.T.);
#77847=ORIENTED_EDGE('',*,*,#53475,.T.);
#77848=ORIENTED_EDGE('',*,*,#53473,.T.);
#77849=ORIENTED_EDGE('',*,*,#53476,.T.);
#77850=ORIENTED_EDGE('',*,*,#53466,.F.);
#77851=ORIENTED_EDGE('',*,*,#53477,.T.);
#77852=ORIENTED_EDGE('',*,*,#53478,.F.);
#77853=ORIENTED_EDGE('',*,*,#53474,.F.);
#77854=ORIENTED_EDGE('',*,*,#53479,.F.);
#77855=ORIENTED_EDGE('',*,*,#53480,.F.);
#77856=ORIENTED_EDGE('',*,*,#53479,.T.);
#77857=ORIENTED_EDGE('',*,*,#53477,.F.);
#77858=ORIENTED_EDGE('',*,*,#53481,.F.);
#77859=ORIENTED_EDGE('',*,*,#53481,.T.);
#77860=ORIENTED_EDGE('',*,*,#53470,.F.);
#77861=ORIENTED_EDGE('',*,*,#53482,.F.);
#77862=ORIENTED_EDGE('',*,*,#53483,.F.);
#77863=ORIENTED_EDGE('',*,*,#53484,.T.);
#77864=ORIENTED_EDGE('',*,*,#53485,.F.);
#77865=ORIENTED_EDGE('',*,*,#53486,.F.);
#77866=ORIENTED_EDGE('',*,*,#50168,.F.);
#77867=ORIENTED_EDGE('',*,*,#53487,.T.);
#77868=ORIENTED_EDGE('',*,*,#53478,.T.);
#77869=ORIENTED_EDGE('',*,*,#53484,.F.);
#77870=ORIENTED_EDGE('',*,*,#50167,.T.);
#77871=ORIENTED_EDGE('',*,*,#53488,.F.);
#77872=ORIENTED_EDGE('',*,*,#53475,.F.);
#77873=ORIENTED_EDGE('',*,*,#53487,.F.);
#77874=ORIENTED_EDGE('',*,*,#50166,.F.);
#77875=ORIENTED_EDGE('',*,*,#53488,.T.);
#77876=ORIENTED_EDGE('',*,*,#50678,.F.);
#77877=ORIENTED_EDGE('',*,*,#53489,.F.);
#77878=ORIENTED_EDGE('',*,*,#53471,.F.);
#77879=ORIENTED_EDGE('',*,*,#53489,.T.);
#77880=ORIENTED_EDGE('',*,*,#49802,.F.);
#77881=ORIENTED_EDGE('',*,*,#53490,.F.);
#77882=ORIENTED_EDGE('',*,*,#53472,.F.);
#77883=ORIENTED_EDGE('',*,*,#53490,.T.);
#77884=ORIENTED_EDGE('',*,*,#49801,.F.);
#77885=ORIENTED_EDGE('',*,*,#53491,.F.);
#77886=ORIENTED_EDGE('',*,*,#53476,.F.);
#77887=ORIENTED_EDGE('',*,*,#53491,.T.);
#77888=ORIENTED_EDGE('',*,*,#49800,.F.);
#77889=ORIENTED_EDGE('',*,*,#53492,.F.);
#77890=ORIENTED_EDGE('',*,*,#53467,.F.);
#77891=ORIENTED_EDGE('',*,*,#53493,.T.);
#77892=ORIENTED_EDGE('',*,*,#53468,.F.);
#77893=ORIENTED_EDGE('',*,*,#53492,.T.);
#77894=ORIENTED_EDGE('',*,*,#50679,.F.);
#77895=ORIENTED_EDGE('',*,*,#53494,.T.);
#77896=ORIENTED_EDGE('',*,*,#53469,.F.);
#77897=ORIENTED_EDGE('',*,*,#53493,.F.);
#77898=ORIENTED_EDGE('',*,*,#50170,.F.);
#77899=ORIENTED_EDGE('',*,*,#53486,.T.);
#77900=ORIENTED_EDGE('',*,*,#53482,.T.);
#77901=ORIENTED_EDGE('',*,*,#53494,.F.);
#77902=ORIENTED_EDGE('',*,*,#50169,.T.);
#77903=ORIENTED_EDGE('',*,*,#53480,.T.);
#77904=ORIENTED_EDGE('',*,*,#53483,.T.);
#77905=ORIENTED_EDGE('',*,*,#53485,.T.);
#77906=ORIENTED_EDGE('',*,*,#53495,.T.);
#77907=ORIENTED_EDGE('',*,*,#53496,.T.);
#77908=ORIENTED_EDGE('',*,*,#53497,.T.);
#77909=ORIENTED_EDGE('',*,*,#53498,.T.);
#77910=ORIENTED_EDGE('',*,*,#53499,.T.);
#77911=ORIENTED_EDGE('',*,*,#53500,.T.);
#77912=ORIENTED_EDGE('',*,*,#53501,.T.);
#77913=ORIENTED_EDGE('',*,*,#53502,.F.);
#77914=ORIENTED_EDGE('',*,*,#53503,.T.);
#77915=ORIENTED_EDGE('',*,*,#53504,.T.);
#77916=ORIENTED_EDGE('',*,*,#53502,.T.);
#77917=ORIENTED_EDGE('',*,*,#53505,.T.);
#77918=ORIENTED_EDGE('',*,*,#53495,.F.);
#77919=ORIENTED_EDGE('',*,*,#53506,.T.);
#77920=ORIENTED_EDGE('',*,*,#53507,.F.);
#77921=ORIENTED_EDGE('',*,*,#53503,.F.);
#77922=ORIENTED_EDGE('',*,*,#53508,.F.);
#77923=ORIENTED_EDGE('',*,*,#53509,.F.);
#77924=ORIENTED_EDGE('',*,*,#53508,.T.);
#77925=ORIENTED_EDGE('',*,*,#53506,.F.);
#77926=ORIENTED_EDGE('',*,*,#53510,.F.);
#77927=ORIENTED_EDGE('',*,*,#53510,.T.);
#77928=ORIENTED_EDGE('',*,*,#53499,.F.);
#77929=ORIENTED_EDGE('',*,*,#53511,.F.);
#77930=ORIENTED_EDGE('',*,*,#53512,.F.);
#77931=ORIENTED_EDGE('',*,*,#53513,.T.);
#77932=ORIENTED_EDGE('',*,*,#53514,.F.);
#77933=ORIENTED_EDGE('',*,*,#53515,.F.);
#77934=ORIENTED_EDGE('',*,*,#50162,.F.);
#77935=ORIENTED_EDGE('',*,*,#53516,.T.);
#77936=ORIENTED_EDGE('',*,*,#53507,.T.);
#77937=ORIENTED_EDGE('',*,*,#53513,.F.);
#77938=ORIENTED_EDGE('',*,*,#50161,.T.);
#77939=ORIENTED_EDGE('',*,*,#53517,.F.);
#77940=ORIENTED_EDGE('',*,*,#53504,.F.);
#77941=ORIENTED_EDGE('',*,*,#53516,.F.);
#77942=ORIENTED_EDGE('',*,*,#50160,.F.);
#77943=ORIENTED_EDGE('',*,*,#53517,.T.);
#77944=ORIENTED_EDGE('',*,*,#50676,.F.);
#77945=ORIENTED_EDGE('',*,*,#53518,.F.);
#77946=ORIENTED_EDGE('',*,*,#53500,.F.);
#77947=ORIENTED_EDGE('',*,*,#53518,.T.);
#77948=ORIENTED_EDGE('',*,*,#49806,.F.);
#77949=ORIENTED_EDGE('',*,*,#53519,.F.);
#77950=ORIENTED_EDGE('',*,*,#53501,.F.);
#77951=ORIENTED_EDGE('',*,*,#53519,.T.);
#77952=ORIENTED_EDGE('',*,*,#49805,.F.);
#77953=ORIENTED_EDGE('',*,*,#53520,.F.);
#77954=ORIENTED_EDGE('',*,*,#53505,.F.);
#77955=ORIENTED_EDGE('',*,*,#53520,.T.);
#77956=ORIENTED_EDGE('',*,*,#49804,.F.);
#77957=ORIENTED_EDGE('',*,*,#53521,.F.);
#77958=ORIENTED_EDGE('',*,*,#53496,.F.);
#77959=ORIENTED_EDGE('',*,*,#53522,.T.);
#77960=ORIENTED_EDGE('',*,*,#53497,.F.);
#77961=ORIENTED_EDGE('',*,*,#53521,.T.);
#77962=ORIENTED_EDGE('',*,*,#50677,.F.);
#77963=ORIENTED_EDGE('',*,*,#53523,.T.);
#77964=ORIENTED_EDGE('',*,*,#53498,.F.);
#77965=ORIENTED_EDGE('',*,*,#53522,.F.);
#77966=ORIENTED_EDGE('',*,*,#50164,.F.);
#77967=ORIENTED_EDGE('',*,*,#53515,.T.);
#77968=ORIENTED_EDGE('',*,*,#53511,.T.);
#77969=ORIENTED_EDGE('',*,*,#53523,.F.);
#77970=ORIENTED_EDGE('',*,*,#50163,.T.);
#77971=ORIENTED_EDGE('',*,*,#53509,.T.);
#77972=ORIENTED_EDGE('',*,*,#53512,.T.);
#77973=ORIENTED_EDGE('',*,*,#53514,.T.);
#77974=ORIENTED_EDGE('',*,*,#53524,.T.);
#77975=ORIENTED_EDGE('',*,*,#53525,.T.);
#77976=ORIENTED_EDGE('',*,*,#53526,.T.);
#77977=ORIENTED_EDGE('',*,*,#53527,.T.);
#77978=ORIENTED_EDGE('',*,*,#53528,.T.);
#77979=ORIENTED_EDGE('',*,*,#53529,.T.);
#77980=ORIENTED_EDGE('',*,*,#53530,.T.);
#77981=ORIENTED_EDGE('',*,*,#53531,.F.);
#77982=ORIENTED_EDGE('',*,*,#53532,.T.);
#77983=ORIENTED_EDGE('',*,*,#53533,.T.);
#77984=ORIENTED_EDGE('',*,*,#53531,.T.);
#77985=ORIENTED_EDGE('',*,*,#53534,.T.);
#77986=ORIENTED_EDGE('',*,*,#53524,.F.);
#77987=ORIENTED_EDGE('',*,*,#53535,.T.);
#77988=ORIENTED_EDGE('',*,*,#53536,.F.);
#77989=ORIENTED_EDGE('',*,*,#53532,.F.);
#77990=ORIENTED_EDGE('',*,*,#53537,.F.);
#77991=ORIENTED_EDGE('',*,*,#53538,.F.);
#77992=ORIENTED_EDGE('',*,*,#53537,.T.);
#77993=ORIENTED_EDGE('',*,*,#53535,.F.);
#77994=ORIENTED_EDGE('',*,*,#53539,.F.);
#77995=ORIENTED_EDGE('',*,*,#53539,.T.);
#77996=ORIENTED_EDGE('',*,*,#53528,.F.);
#77997=ORIENTED_EDGE('',*,*,#53540,.F.);
#77998=ORIENTED_EDGE('',*,*,#53541,.F.);
#77999=ORIENTED_EDGE('',*,*,#53542,.T.);
#78000=ORIENTED_EDGE('',*,*,#53543,.F.);
#78001=ORIENTED_EDGE('',*,*,#53544,.F.);
#78002=ORIENTED_EDGE('',*,*,#50156,.F.);
#78003=ORIENTED_EDGE('',*,*,#53545,.T.);
#78004=ORIENTED_EDGE('',*,*,#53536,.T.);
#78005=ORIENTED_EDGE('',*,*,#53542,.F.);
#78006=ORIENTED_EDGE('',*,*,#50155,.T.);
#78007=ORIENTED_EDGE('',*,*,#53546,.F.);
#78008=ORIENTED_EDGE('',*,*,#53533,.F.);
#78009=ORIENTED_EDGE('',*,*,#53545,.F.);
#78010=ORIENTED_EDGE('',*,*,#50154,.F.);
#78011=ORIENTED_EDGE('',*,*,#53546,.T.);
#78012=ORIENTED_EDGE('',*,*,#50674,.F.);
#78013=ORIENTED_EDGE('',*,*,#53547,.F.);
#78014=ORIENTED_EDGE('',*,*,#53529,.F.);
#78015=ORIENTED_EDGE('',*,*,#53547,.T.);
#78016=ORIENTED_EDGE('',*,*,#49810,.F.);
#78017=ORIENTED_EDGE('',*,*,#53548,.F.);
#78018=ORIENTED_EDGE('',*,*,#53530,.F.);
#78019=ORIENTED_EDGE('',*,*,#53548,.T.);
#78020=ORIENTED_EDGE('',*,*,#49809,.F.);
#78021=ORIENTED_EDGE('',*,*,#53549,.F.);
#78022=ORIENTED_EDGE('',*,*,#53534,.F.);
#78023=ORIENTED_EDGE('',*,*,#53549,.T.);
#78024=ORIENTED_EDGE('',*,*,#49808,.F.);
#78025=ORIENTED_EDGE('',*,*,#53550,.F.);
#78026=ORIENTED_EDGE('',*,*,#53525,.F.);
#78027=ORIENTED_EDGE('',*,*,#53551,.T.);
#78028=ORIENTED_EDGE('',*,*,#53526,.F.);
#78029=ORIENTED_EDGE('',*,*,#53550,.T.);
#78030=ORIENTED_EDGE('',*,*,#50675,.F.);
#78031=ORIENTED_EDGE('',*,*,#53552,.T.);
#78032=ORIENTED_EDGE('',*,*,#53527,.F.);
#78033=ORIENTED_EDGE('',*,*,#53551,.F.);
#78034=ORIENTED_EDGE('',*,*,#50158,.F.);
#78035=ORIENTED_EDGE('',*,*,#53544,.T.);
#78036=ORIENTED_EDGE('',*,*,#53540,.T.);
#78037=ORIENTED_EDGE('',*,*,#53552,.F.);
#78038=ORIENTED_EDGE('',*,*,#50157,.T.);
#78039=ORIENTED_EDGE('',*,*,#53538,.T.);
#78040=ORIENTED_EDGE('',*,*,#53541,.T.);
#78041=ORIENTED_EDGE('',*,*,#53543,.T.);
#78042=ORIENTED_EDGE('',*,*,#53553,.T.);
#78043=ORIENTED_EDGE('',*,*,#53554,.T.);
#78044=ORIENTED_EDGE('',*,*,#53555,.T.);
#78045=ORIENTED_EDGE('',*,*,#53556,.T.);
#78046=ORIENTED_EDGE('',*,*,#53557,.T.);
#78047=ORIENTED_EDGE('',*,*,#53558,.T.);
#78048=ORIENTED_EDGE('',*,*,#53559,.T.);
#78049=ORIENTED_EDGE('',*,*,#53560,.F.);
#78050=ORIENTED_EDGE('',*,*,#53561,.T.);
#78051=ORIENTED_EDGE('',*,*,#53562,.T.);
#78052=ORIENTED_EDGE('',*,*,#53560,.T.);
#78053=ORIENTED_EDGE('',*,*,#53563,.T.);
#78054=ORIENTED_EDGE('',*,*,#53553,.F.);
#78055=ORIENTED_EDGE('',*,*,#53564,.T.);
#78056=ORIENTED_EDGE('',*,*,#53565,.F.);
#78057=ORIENTED_EDGE('',*,*,#53561,.F.);
#78058=ORIENTED_EDGE('',*,*,#53566,.F.);
#78059=ORIENTED_EDGE('',*,*,#53567,.F.);
#78060=ORIENTED_EDGE('',*,*,#53566,.T.);
#78061=ORIENTED_EDGE('',*,*,#53564,.F.);
#78062=ORIENTED_EDGE('',*,*,#53568,.F.);
#78063=ORIENTED_EDGE('',*,*,#53568,.T.);
#78064=ORIENTED_EDGE('',*,*,#53557,.F.);
#78065=ORIENTED_EDGE('',*,*,#53569,.F.);
#78066=ORIENTED_EDGE('',*,*,#53570,.F.);
#78067=ORIENTED_EDGE('',*,*,#53571,.T.);
#78068=ORIENTED_EDGE('',*,*,#53572,.F.);
#78069=ORIENTED_EDGE('',*,*,#53573,.F.);
#78070=ORIENTED_EDGE('',*,*,#50150,.F.);
#78071=ORIENTED_EDGE('',*,*,#53574,.T.);
#78072=ORIENTED_EDGE('',*,*,#53565,.T.);
#78073=ORIENTED_EDGE('',*,*,#53571,.F.);
#78074=ORIENTED_EDGE('',*,*,#50149,.T.);
#78075=ORIENTED_EDGE('',*,*,#53575,.F.);
#78076=ORIENTED_EDGE('',*,*,#53562,.F.);
#78077=ORIENTED_EDGE('',*,*,#53574,.F.);
#78078=ORIENTED_EDGE('',*,*,#50148,.F.);
#78079=ORIENTED_EDGE('',*,*,#53575,.T.);
#78080=ORIENTED_EDGE('',*,*,#50672,.F.);
#78081=ORIENTED_EDGE('',*,*,#53576,.F.);
#78082=ORIENTED_EDGE('',*,*,#53558,.F.);
#78083=ORIENTED_EDGE('',*,*,#53576,.T.);
#78084=ORIENTED_EDGE('',*,*,#49814,.F.);
#78085=ORIENTED_EDGE('',*,*,#53577,.F.);
#78086=ORIENTED_EDGE('',*,*,#53559,.F.);
#78087=ORIENTED_EDGE('',*,*,#53577,.T.);
#78088=ORIENTED_EDGE('',*,*,#49813,.F.);
#78089=ORIENTED_EDGE('',*,*,#53578,.F.);
#78090=ORIENTED_EDGE('',*,*,#53563,.F.);
#78091=ORIENTED_EDGE('',*,*,#53578,.T.);
#78092=ORIENTED_EDGE('',*,*,#49812,.F.);
#78093=ORIENTED_EDGE('',*,*,#53579,.F.);
#78094=ORIENTED_EDGE('',*,*,#53554,.F.);
#78095=ORIENTED_EDGE('',*,*,#53580,.T.);
#78096=ORIENTED_EDGE('',*,*,#53555,.F.);
#78097=ORIENTED_EDGE('',*,*,#53579,.T.);
#78098=ORIENTED_EDGE('',*,*,#50673,.F.);
#78099=ORIENTED_EDGE('',*,*,#53581,.T.);
#78100=ORIENTED_EDGE('',*,*,#53556,.F.);
#78101=ORIENTED_EDGE('',*,*,#53580,.F.);
#78102=ORIENTED_EDGE('',*,*,#50152,.F.);
#78103=ORIENTED_EDGE('',*,*,#53573,.T.);
#78104=ORIENTED_EDGE('',*,*,#53569,.T.);
#78105=ORIENTED_EDGE('',*,*,#53581,.F.);
#78106=ORIENTED_EDGE('',*,*,#50151,.T.);
#78107=ORIENTED_EDGE('',*,*,#53567,.T.);
#78108=ORIENTED_EDGE('',*,*,#53570,.T.);
#78109=ORIENTED_EDGE('',*,*,#53572,.T.);
#78110=ORIENTED_EDGE('',*,*,#53582,.T.);
#78111=ORIENTED_EDGE('',*,*,#53583,.T.);
#78112=ORIENTED_EDGE('',*,*,#53584,.T.);
#78113=ORIENTED_EDGE('',*,*,#53585,.T.);
#78114=ORIENTED_EDGE('',*,*,#53586,.T.);
#78115=ORIENTED_EDGE('',*,*,#53587,.T.);
#78116=ORIENTED_EDGE('',*,*,#53588,.T.);
#78117=ORIENTED_EDGE('',*,*,#53589,.F.);
#78118=ORIENTED_EDGE('',*,*,#53590,.T.);
#78119=ORIENTED_EDGE('',*,*,#53591,.T.);
#78120=ORIENTED_EDGE('',*,*,#53589,.T.);
#78121=ORIENTED_EDGE('',*,*,#53592,.T.);
#78122=ORIENTED_EDGE('',*,*,#53582,.F.);
#78123=ORIENTED_EDGE('',*,*,#53593,.T.);
#78124=ORIENTED_EDGE('',*,*,#53594,.F.);
#78125=ORIENTED_EDGE('',*,*,#53590,.F.);
#78126=ORIENTED_EDGE('',*,*,#53595,.F.);
#78127=ORIENTED_EDGE('',*,*,#53596,.F.);
#78128=ORIENTED_EDGE('',*,*,#53595,.T.);
#78129=ORIENTED_EDGE('',*,*,#53593,.F.);
#78130=ORIENTED_EDGE('',*,*,#53597,.F.);
#78131=ORIENTED_EDGE('',*,*,#53597,.T.);
#78132=ORIENTED_EDGE('',*,*,#53586,.F.);
#78133=ORIENTED_EDGE('',*,*,#53598,.F.);
#78134=ORIENTED_EDGE('',*,*,#53599,.F.);
#78135=ORIENTED_EDGE('',*,*,#53600,.T.);
#78136=ORIENTED_EDGE('',*,*,#53601,.F.);
#78137=ORIENTED_EDGE('',*,*,#53602,.F.);
#78138=ORIENTED_EDGE('',*,*,#50144,.F.);
#78139=ORIENTED_EDGE('',*,*,#53603,.T.);
#78140=ORIENTED_EDGE('',*,*,#53594,.T.);
#78141=ORIENTED_EDGE('',*,*,#53600,.F.);
#78142=ORIENTED_EDGE('',*,*,#50143,.T.);
#78143=ORIENTED_EDGE('',*,*,#53604,.F.);
#78144=ORIENTED_EDGE('',*,*,#53591,.F.);
#78145=ORIENTED_EDGE('',*,*,#53603,.F.);
#78146=ORIENTED_EDGE('',*,*,#50142,.F.);
#78147=ORIENTED_EDGE('',*,*,#53604,.T.);
#78148=ORIENTED_EDGE('',*,*,#50670,.F.);
#78149=ORIENTED_EDGE('',*,*,#53605,.F.);
#78150=ORIENTED_EDGE('',*,*,#53587,.F.);
#78151=ORIENTED_EDGE('',*,*,#53605,.T.);
#78152=ORIENTED_EDGE('',*,*,#49818,.F.);
#78153=ORIENTED_EDGE('',*,*,#53606,.F.);
#78154=ORIENTED_EDGE('',*,*,#53588,.F.);
#78155=ORIENTED_EDGE('',*,*,#53606,.T.);
#78156=ORIENTED_EDGE('',*,*,#49817,.F.);
#78157=ORIENTED_EDGE('',*,*,#53607,.F.);
#78158=ORIENTED_EDGE('',*,*,#53592,.F.);
#78159=ORIENTED_EDGE('',*,*,#53607,.T.);
#78160=ORIENTED_EDGE('',*,*,#49816,.F.);
#78161=ORIENTED_EDGE('',*,*,#53608,.F.);
#78162=ORIENTED_EDGE('',*,*,#53583,.F.);
#78163=ORIENTED_EDGE('',*,*,#53609,.T.);
#78164=ORIENTED_EDGE('',*,*,#53584,.F.);
#78165=ORIENTED_EDGE('',*,*,#53608,.T.);
#78166=ORIENTED_EDGE('',*,*,#50671,.F.);
#78167=ORIENTED_EDGE('',*,*,#53610,.T.);
#78168=ORIENTED_EDGE('',*,*,#53585,.F.);
#78169=ORIENTED_EDGE('',*,*,#53609,.F.);
#78170=ORIENTED_EDGE('',*,*,#50146,.F.);
#78171=ORIENTED_EDGE('',*,*,#53602,.T.);
#78172=ORIENTED_EDGE('',*,*,#53598,.T.);
#78173=ORIENTED_EDGE('',*,*,#53610,.F.);
#78174=ORIENTED_EDGE('',*,*,#50145,.T.);
#78175=ORIENTED_EDGE('',*,*,#53596,.T.);
#78176=ORIENTED_EDGE('',*,*,#53599,.T.);
#78177=ORIENTED_EDGE('',*,*,#53601,.T.);
#78178=ORIENTED_EDGE('',*,*,#53611,.T.);
#78179=ORIENTED_EDGE('',*,*,#53612,.T.);
#78180=ORIENTED_EDGE('',*,*,#53613,.T.);
#78181=ORIENTED_EDGE('',*,*,#53614,.T.);
#78182=ORIENTED_EDGE('',*,*,#53615,.T.);
#78183=ORIENTED_EDGE('',*,*,#53616,.T.);
#78184=ORIENTED_EDGE('',*,*,#53617,.T.);
#78185=ORIENTED_EDGE('',*,*,#53618,.F.);
#78186=ORIENTED_EDGE('',*,*,#53619,.T.);
#78187=ORIENTED_EDGE('',*,*,#53620,.T.);
#78188=ORIENTED_EDGE('',*,*,#53618,.T.);
#78189=ORIENTED_EDGE('',*,*,#53621,.T.);
#78190=ORIENTED_EDGE('',*,*,#53611,.F.);
#78191=ORIENTED_EDGE('',*,*,#53622,.T.);
#78192=ORIENTED_EDGE('',*,*,#53623,.F.);
#78193=ORIENTED_EDGE('',*,*,#53619,.F.);
#78194=ORIENTED_EDGE('',*,*,#53624,.F.);
#78195=ORIENTED_EDGE('',*,*,#53625,.F.);
#78196=ORIENTED_EDGE('',*,*,#53624,.T.);
#78197=ORIENTED_EDGE('',*,*,#53622,.F.);
#78198=ORIENTED_EDGE('',*,*,#53626,.F.);
#78199=ORIENTED_EDGE('',*,*,#53626,.T.);
#78200=ORIENTED_EDGE('',*,*,#53615,.F.);
#78201=ORIENTED_EDGE('',*,*,#53627,.F.);
#78202=ORIENTED_EDGE('',*,*,#53628,.F.);
#78203=ORIENTED_EDGE('',*,*,#53629,.T.);
#78204=ORIENTED_EDGE('',*,*,#53630,.F.);
#78205=ORIENTED_EDGE('',*,*,#53631,.F.);
#78206=ORIENTED_EDGE('',*,*,#50138,.F.);
#78207=ORIENTED_EDGE('',*,*,#53632,.T.);
#78208=ORIENTED_EDGE('',*,*,#53623,.T.);
#78209=ORIENTED_EDGE('',*,*,#53629,.F.);
#78210=ORIENTED_EDGE('',*,*,#50137,.T.);
#78211=ORIENTED_EDGE('',*,*,#53633,.F.);
#78212=ORIENTED_EDGE('',*,*,#53620,.F.);
#78213=ORIENTED_EDGE('',*,*,#53632,.F.);
#78214=ORIENTED_EDGE('',*,*,#50136,.F.);
#78215=ORIENTED_EDGE('',*,*,#53633,.T.);
#78216=ORIENTED_EDGE('',*,*,#50668,.F.);
#78217=ORIENTED_EDGE('',*,*,#53634,.F.);
#78218=ORIENTED_EDGE('',*,*,#53616,.F.);
#78219=ORIENTED_EDGE('',*,*,#53634,.T.);
#78220=ORIENTED_EDGE('',*,*,#49822,.F.);
#78221=ORIENTED_EDGE('',*,*,#53635,.F.);
#78222=ORIENTED_EDGE('',*,*,#53617,.F.);
#78223=ORIENTED_EDGE('',*,*,#53635,.T.);
#78224=ORIENTED_EDGE('',*,*,#49821,.F.);
#78225=ORIENTED_EDGE('',*,*,#53636,.F.);
#78226=ORIENTED_EDGE('',*,*,#53621,.F.);
#78227=ORIENTED_EDGE('',*,*,#53636,.T.);
#78228=ORIENTED_EDGE('',*,*,#49820,.F.);
#78229=ORIENTED_EDGE('',*,*,#53637,.F.);
#78230=ORIENTED_EDGE('',*,*,#53612,.F.);
#78231=ORIENTED_EDGE('',*,*,#53638,.T.);
#78232=ORIENTED_EDGE('',*,*,#53613,.F.);
#78233=ORIENTED_EDGE('',*,*,#53637,.T.);
#78234=ORIENTED_EDGE('',*,*,#50669,.F.);
#78235=ORIENTED_EDGE('',*,*,#53639,.T.);
#78236=ORIENTED_EDGE('',*,*,#53614,.F.);
#78237=ORIENTED_EDGE('',*,*,#53638,.F.);
#78238=ORIENTED_EDGE('',*,*,#50140,.F.);
#78239=ORIENTED_EDGE('',*,*,#53631,.T.);
#78240=ORIENTED_EDGE('',*,*,#53627,.T.);
#78241=ORIENTED_EDGE('',*,*,#53639,.F.);
#78242=ORIENTED_EDGE('',*,*,#50139,.T.);
#78243=ORIENTED_EDGE('',*,*,#53625,.T.);
#78244=ORIENTED_EDGE('',*,*,#53628,.T.);
#78245=ORIENTED_EDGE('',*,*,#53630,.T.);
#78246=ORIENTED_EDGE('',*,*,#53640,.T.);
#78247=ORIENTED_EDGE('',*,*,#53641,.T.);
#78248=ORIENTED_EDGE('',*,*,#53642,.T.);
#78249=ORIENTED_EDGE('',*,*,#53643,.T.);
#78250=ORIENTED_EDGE('',*,*,#53644,.T.);
#78251=ORIENTED_EDGE('',*,*,#53645,.T.);
#78252=ORIENTED_EDGE('',*,*,#53646,.T.);
#78253=ORIENTED_EDGE('',*,*,#53647,.F.);
#78254=ORIENTED_EDGE('',*,*,#53648,.T.);
#78255=ORIENTED_EDGE('',*,*,#53649,.T.);
#78256=ORIENTED_EDGE('',*,*,#53647,.T.);
#78257=ORIENTED_EDGE('',*,*,#53650,.T.);
#78258=ORIENTED_EDGE('',*,*,#53640,.F.);
#78259=ORIENTED_EDGE('',*,*,#53651,.T.);
#78260=ORIENTED_EDGE('',*,*,#53652,.F.);
#78261=ORIENTED_EDGE('',*,*,#53648,.F.);
#78262=ORIENTED_EDGE('',*,*,#53653,.F.);
#78263=ORIENTED_EDGE('',*,*,#53654,.F.);
#78264=ORIENTED_EDGE('',*,*,#53653,.T.);
#78265=ORIENTED_EDGE('',*,*,#53651,.F.);
#78266=ORIENTED_EDGE('',*,*,#53655,.F.);
#78267=ORIENTED_EDGE('',*,*,#53655,.T.);
#78268=ORIENTED_EDGE('',*,*,#53644,.F.);
#78269=ORIENTED_EDGE('',*,*,#53656,.F.);
#78270=ORIENTED_EDGE('',*,*,#53657,.F.);
#78271=ORIENTED_EDGE('',*,*,#53658,.T.);
#78272=ORIENTED_EDGE('',*,*,#53659,.F.);
#78273=ORIENTED_EDGE('',*,*,#53660,.F.);
#78274=ORIENTED_EDGE('',*,*,#50132,.F.);
#78275=ORIENTED_EDGE('',*,*,#53661,.T.);
#78276=ORIENTED_EDGE('',*,*,#53652,.T.);
#78277=ORIENTED_EDGE('',*,*,#53658,.F.);
#78278=ORIENTED_EDGE('',*,*,#50131,.T.);
#78279=ORIENTED_EDGE('',*,*,#53662,.F.);
#78280=ORIENTED_EDGE('',*,*,#53649,.F.);
#78281=ORIENTED_EDGE('',*,*,#53661,.F.);
#78282=ORIENTED_EDGE('',*,*,#50130,.F.);
#78283=ORIENTED_EDGE('',*,*,#53662,.T.);
#78284=ORIENTED_EDGE('',*,*,#50666,.F.);
#78285=ORIENTED_EDGE('',*,*,#53663,.F.);
#78286=ORIENTED_EDGE('',*,*,#53645,.F.);
#78287=ORIENTED_EDGE('',*,*,#53663,.T.);
#78288=ORIENTED_EDGE('',*,*,#49826,.F.);
#78289=ORIENTED_EDGE('',*,*,#53664,.F.);
#78290=ORIENTED_EDGE('',*,*,#53646,.F.);
#78291=ORIENTED_EDGE('',*,*,#53664,.T.);
#78292=ORIENTED_EDGE('',*,*,#49825,.F.);
#78293=ORIENTED_EDGE('',*,*,#53665,.F.);
#78294=ORIENTED_EDGE('',*,*,#53650,.F.);
#78295=ORIENTED_EDGE('',*,*,#53665,.T.);
#78296=ORIENTED_EDGE('',*,*,#49824,.F.);
#78297=ORIENTED_EDGE('',*,*,#53666,.F.);
#78298=ORIENTED_EDGE('',*,*,#53641,.F.);
#78299=ORIENTED_EDGE('',*,*,#53667,.T.);
#78300=ORIENTED_EDGE('',*,*,#53642,.F.);
#78301=ORIENTED_EDGE('',*,*,#53666,.T.);
#78302=ORIENTED_EDGE('',*,*,#50667,.F.);
#78303=ORIENTED_EDGE('',*,*,#53668,.T.);
#78304=ORIENTED_EDGE('',*,*,#53643,.F.);
#78305=ORIENTED_EDGE('',*,*,#53667,.F.);
#78306=ORIENTED_EDGE('',*,*,#50134,.F.);
#78307=ORIENTED_EDGE('',*,*,#53660,.T.);
#78308=ORIENTED_EDGE('',*,*,#53656,.T.);
#78309=ORIENTED_EDGE('',*,*,#53668,.F.);
#78310=ORIENTED_EDGE('',*,*,#50133,.T.);
#78311=ORIENTED_EDGE('',*,*,#53654,.T.);
#78312=ORIENTED_EDGE('',*,*,#53657,.T.);
#78313=ORIENTED_EDGE('',*,*,#53659,.T.);
#78314=ORIENTED_EDGE('',*,*,#53669,.T.);
#78315=ORIENTED_EDGE('',*,*,#53670,.T.);
#78316=ORIENTED_EDGE('',*,*,#53671,.T.);
#78317=ORIENTED_EDGE('',*,*,#53672,.T.);
#78318=ORIENTED_EDGE('',*,*,#53673,.T.);
#78319=ORIENTED_EDGE('',*,*,#53674,.T.);
#78320=ORIENTED_EDGE('',*,*,#53675,.T.);
#78321=ORIENTED_EDGE('',*,*,#53676,.F.);
#78322=ORIENTED_EDGE('',*,*,#53677,.T.);
#78323=ORIENTED_EDGE('',*,*,#53678,.T.);
#78324=ORIENTED_EDGE('',*,*,#53676,.T.);
#78325=ORIENTED_EDGE('',*,*,#53679,.T.);
#78326=ORIENTED_EDGE('',*,*,#53669,.F.);
#78327=ORIENTED_EDGE('',*,*,#53680,.T.);
#78328=ORIENTED_EDGE('',*,*,#53681,.F.);
#78329=ORIENTED_EDGE('',*,*,#53677,.F.);
#78330=ORIENTED_EDGE('',*,*,#53682,.F.);
#78331=ORIENTED_EDGE('',*,*,#53683,.F.);
#78332=ORIENTED_EDGE('',*,*,#53682,.T.);
#78333=ORIENTED_EDGE('',*,*,#53680,.F.);
#78334=ORIENTED_EDGE('',*,*,#53684,.F.);
#78335=ORIENTED_EDGE('',*,*,#53684,.T.);
#78336=ORIENTED_EDGE('',*,*,#53673,.F.);
#78337=ORIENTED_EDGE('',*,*,#53685,.F.);
#78338=ORIENTED_EDGE('',*,*,#53686,.F.);
#78339=ORIENTED_EDGE('',*,*,#53687,.T.);
#78340=ORIENTED_EDGE('',*,*,#53688,.F.);
#78341=ORIENTED_EDGE('',*,*,#53689,.F.);
#78342=ORIENTED_EDGE('',*,*,#50126,.F.);
#78343=ORIENTED_EDGE('',*,*,#53690,.T.);
#78344=ORIENTED_EDGE('',*,*,#53681,.T.);
#78345=ORIENTED_EDGE('',*,*,#53687,.F.);
#78346=ORIENTED_EDGE('',*,*,#50125,.T.);
#78347=ORIENTED_EDGE('',*,*,#53691,.F.);
#78348=ORIENTED_EDGE('',*,*,#53678,.F.);
#78349=ORIENTED_EDGE('',*,*,#53690,.F.);
#78350=ORIENTED_EDGE('',*,*,#50124,.F.);
#78351=ORIENTED_EDGE('',*,*,#53691,.T.);
#78352=ORIENTED_EDGE('',*,*,#50664,.F.);
#78353=ORIENTED_EDGE('',*,*,#53692,.F.);
#78354=ORIENTED_EDGE('',*,*,#53674,.F.);
#78355=ORIENTED_EDGE('',*,*,#53692,.T.);
#78356=ORIENTED_EDGE('',*,*,#49830,.F.);
#78357=ORIENTED_EDGE('',*,*,#53693,.F.);
#78358=ORIENTED_EDGE('',*,*,#53675,.F.);
#78359=ORIENTED_EDGE('',*,*,#53693,.T.);
#78360=ORIENTED_EDGE('',*,*,#49829,.F.);
#78361=ORIENTED_EDGE('',*,*,#53694,.F.);
#78362=ORIENTED_EDGE('',*,*,#53679,.F.);
#78363=ORIENTED_EDGE('',*,*,#53694,.T.);
#78364=ORIENTED_EDGE('',*,*,#49828,.F.);
#78365=ORIENTED_EDGE('',*,*,#53695,.F.);
#78366=ORIENTED_EDGE('',*,*,#53670,.F.);
#78367=ORIENTED_EDGE('',*,*,#53696,.T.);
#78368=ORIENTED_EDGE('',*,*,#53671,.F.);
#78369=ORIENTED_EDGE('',*,*,#53695,.T.);
#78370=ORIENTED_EDGE('',*,*,#50665,.F.);
#78371=ORIENTED_EDGE('',*,*,#53697,.T.);
#78372=ORIENTED_EDGE('',*,*,#53672,.F.);
#78373=ORIENTED_EDGE('',*,*,#53696,.F.);
#78374=ORIENTED_EDGE('',*,*,#50128,.F.);
#78375=ORIENTED_EDGE('',*,*,#53689,.T.);
#78376=ORIENTED_EDGE('',*,*,#53685,.T.);
#78377=ORIENTED_EDGE('',*,*,#53697,.F.);
#78378=ORIENTED_EDGE('',*,*,#50127,.T.);
#78379=ORIENTED_EDGE('',*,*,#53683,.T.);
#78380=ORIENTED_EDGE('',*,*,#53686,.T.);
#78381=ORIENTED_EDGE('',*,*,#53688,.T.);
#78382=ORIENTED_EDGE('',*,*,#53698,.T.);
#78383=ORIENTED_EDGE('',*,*,#53699,.T.);
#78384=ORIENTED_EDGE('',*,*,#53700,.T.);
#78385=ORIENTED_EDGE('',*,*,#53701,.T.);
#78386=ORIENTED_EDGE('',*,*,#53702,.T.);
#78387=ORIENTED_EDGE('',*,*,#53703,.T.);
#78388=ORIENTED_EDGE('',*,*,#53704,.T.);
#78389=ORIENTED_EDGE('',*,*,#53705,.F.);
#78390=ORIENTED_EDGE('',*,*,#53706,.T.);
#78391=ORIENTED_EDGE('',*,*,#53707,.T.);
#78392=ORIENTED_EDGE('',*,*,#53705,.T.);
#78393=ORIENTED_EDGE('',*,*,#53708,.T.);
#78394=ORIENTED_EDGE('',*,*,#53698,.F.);
#78395=ORIENTED_EDGE('',*,*,#53709,.T.);
#78396=ORIENTED_EDGE('',*,*,#53710,.F.);
#78397=ORIENTED_EDGE('',*,*,#53706,.F.);
#78398=ORIENTED_EDGE('',*,*,#53711,.F.);
#78399=ORIENTED_EDGE('',*,*,#53712,.F.);
#78400=ORIENTED_EDGE('',*,*,#53711,.T.);
#78401=ORIENTED_EDGE('',*,*,#53709,.F.);
#78402=ORIENTED_EDGE('',*,*,#53713,.F.);
#78403=ORIENTED_EDGE('',*,*,#53713,.T.);
#78404=ORIENTED_EDGE('',*,*,#53702,.F.);
#78405=ORIENTED_EDGE('',*,*,#53714,.F.);
#78406=ORIENTED_EDGE('',*,*,#53715,.F.);
#78407=ORIENTED_EDGE('',*,*,#53716,.T.);
#78408=ORIENTED_EDGE('',*,*,#53717,.F.);
#78409=ORIENTED_EDGE('',*,*,#53718,.F.);
#78410=ORIENTED_EDGE('',*,*,#50120,.F.);
#78411=ORIENTED_EDGE('',*,*,#53719,.T.);
#78412=ORIENTED_EDGE('',*,*,#53710,.T.);
#78413=ORIENTED_EDGE('',*,*,#53716,.F.);
#78414=ORIENTED_EDGE('',*,*,#50119,.T.);
#78415=ORIENTED_EDGE('',*,*,#53720,.F.);
#78416=ORIENTED_EDGE('',*,*,#53707,.F.);
#78417=ORIENTED_EDGE('',*,*,#53719,.F.);
#78418=ORIENTED_EDGE('',*,*,#50118,.F.);
#78419=ORIENTED_EDGE('',*,*,#53720,.T.);
#78420=ORIENTED_EDGE('',*,*,#50661,.F.);
#78421=ORIENTED_EDGE('',*,*,#53721,.F.);
#78422=ORIENTED_EDGE('',*,*,#53703,.F.);
#78423=ORIENTED_EDGE('',*,*,#53721,.T.);
#78424=ORIENTED_EDGE('',*,*,#49834,.F.);
#78425=ORIENTED_EDGE('',*,*,#53722,.F.);
#78426=ORIENTED_EDGE('',*,*,#53704,.F.);
#78427=ORIENTED_EDGE('',*,*,#53722,.T.);
#78428=ORIENTED_EDGE('',*,*,#49833,.F.);
#78429=ORIENTED_EDGE('',*,*,#53723,.F.);
#78430=ORIENTED_EDGE('',*,*,#53708,.F.);
#78431=ORIENTED_EDGE('',*,*,#53723,.T.);
#78432=ORIENTED_EDGE('',*,*,#49832,.F.);
#78433=ORIENTED_EDGE('',*,*,#53724,.F.);
#78434=ORIENTED_EDGE('',*,*,#53699,.F.);
#78435=ORIENTED_EDGE('',*,*,#53725,.T.);
#78436=ORIENTED_EDGE('',*,*,#53700,.F.);
#78437=ORIENTED_EDGE('',*,*,#53724,.T.);
#78438=ORIENTED_EDGE('',*,*,#50663,.F.);
#78439=ORIENTED_EDGE('',*,*,#53726,.T.);
#78440=ORIENTED_EDGE('',*,*,#53701,.F.);
#78441=ORIENTED_EDGE('',*,*,#53725,.F.);
#78442=ORIENTED_EDGE('',*,*,#50122,.F.);
#78443=ORIENTED_EDGE('',*,*,#53718,.T.);
#78444=ORIENTED_EDGE('',*,*,#53714,.T.);
#78445=ORIENTED_EDGE('',*,*,#53726,.F.);
#78446=ORIENTED_EDGE('',*,*,#50121,.T.);
#78447=ORIENTED_EDGE('',*,*,#53712,.T.);
#78448=ORIENTED_EDGE('',*,*,#53715,.T.);
#78449=ORIENTED_EDGE('',*,*,#53717,.T.);
#87997=CYLINDRICAL_SURFACE('',#99386,1.17524047358083);
#87998=CYLINDRICAL_SURFACE('',#99388,1.17524047358083);
#87999=CYLINDRICAL_SURFACE('',#99389,1.17524047358083);
#88000=CYLINDRICAL_SURFACE('',#99390,1.17524047358083);
#88001=CYLINDRICAL_SURFACE('',#99391,1.17524047358083);
#88002=CYLINDRICAL_SURFACE('',#99392,1.17524047358083);
#88003=CYLINDRICAL_SURFACE('',#99393,1.17524047358083);
#88004=CYLINDRICAL_SURFACE('',#99394,1.17524047358083);
#88005=CYLINDRICAL_SURFACE('',#99395,1.17524047358083);
#88006=CYLINDRICAL_SURFACE('',#99396,1.17524047358083);
#88007=CYLINDRICAL_SURFACE('',#99397,1.17524047358083);
#88008=CYLINDRICAL_SURFACE('',#99398,1.17524047358083);
#88009=CYLINDRICAL_SURFACE('',#99399,1.17524047358083);
#88010=CYLINDRICAL_SURFACE('',#99400,1.17524047358083);
#88011=CYLINDRICAL_SURFACE('',#99401,1.17524047358083);
#88012=CYLINDRICAL_SURFACE('',#99402,1.17524047358083);
#88013=CYLINDRICAL_SURFACE('',#99403,1.17524047358083);
#88014=CYLINDRICAL_SURFACE('',#99404,1.17524047358083);
#88015=CYLINDRICAL_SURFACE('',#99405,1.17524047358083);
#88016=CYLINDRICAL_SURFACE('',#99406,1.17524047358083);
#88017=CYLINDRICAL_SURFACE('',#99407,1.17524047358083);
#88018=CYLINDRICAL_SURFACE('',#99408,1.17524047358083);
#88019=CYLINDRICAL_SURFACE('',#99409,1.17524047358083);
#88020=CYLINDRICAL_SURFACE('',#99410,1.17524047358083);
#88021=CYLINDRICAL_SURFACE('',#99411,1.17524047358083);
#88022=CYLINDRICAL_SURFACE('',#99412,1.17524047358083);
#88023=CYLINDRICAL_SURFACE('',#99413,1.17524047358083);
#88024=CYLINDRICAL_SURFACE('',#99414,1.17524047358083);
#88025=CYLINDRICAL_SURFACE('',#99415,1.17524047358083);
#88026=CYLINDRICAL_SURFACE('',#99416,1.5);
#88027=CYLINDRICAL_SURFACE('',#99420,1.5);
#88028=CYLINDRICAL_SURFACE('',#99421,1.5);
#88029=CYLINDRICAL_SURFACE('',#99422,1.5);
#88030=CYLINDRICAL_SURFACE('',#99423,1.5);
#88031=CYLINDRICAL_SURFACE('',#99424,1.5);
#88032=CYLINDRICAL_SURFACE('',#99425,1.5);
#88033=CYLINDRICAL_SURFACE('',#99426,1.5);
#88034=CYLINDRICAL_SURFACE('',#99427,1.5);
#88035=CYLINDRICAL_SURFACE('',#99428,1.5);
#88036=CYLINDRICAL_SURFACE('',#99429,1.5);
#88037=CYLINDRICAL_SURFACE('',#99430,1.5);
#88038=CYLINDRICAL_SURFACE('',#99431,1.5);
#88039=CYLINDRICAL_SURFACE('',#99432,1.5);
#88040=CYLINDRICAL_SURFACE('',#99433,1.5);
#88041=CYLINDRICAL_SURFACE('',#99434,1.5);
#88042=CYLINDRICAL_SURFACE('',#99435,1.5);
#88043=CYLINDRICAL_SURFACE('',#99436,1.5);
#88044=CYLINDRICAL_SURFACE('',#99437,1.5);
#88045=CYLINDRICAL_SURFACE('',#99438,1.5);
#88046=CYLINDRICAL_SURFACE('',#99439,1.5);
#88047=CYLINDRICAL_SURFACE('',#99440,1.5);
#88048=CYLINDRICAL_SURFACE('',#99441,1.5);
#88049=CYLINDRICAL_SURFACE('',#99442,1.5);
#88050=CYLINDRICAL_SURFACE('',#99443,1.5);
#88051=CYLINDRICAL_SURFACE('',#99444,1.5);
#88052=CYLINDRICAL_SURFACE('',#99445,1.5);
#88053=CYLINDRICAL_SURFACE('',#99446,1.5);
#88054=CYLINDRICAL_SURFACE('',#99455,1.5);
#88055=CYLINDRICAL_SURFACE('',#99680,2.75);
#88056=CYLINDRICAL_SURFACE('',#100365,0.00687499999999997);
#88057=CYLINDRICAL_SURFACE('',#100399,1.17524047358083);
#88058=CYLINDRICAL_SURFACE('',#100403,0.0125);
#88059=CYLINDRICAL_SURFACE('',#100414,0.0125);
#88060=CYLINDRICAL_SURFACE('',#100421,0.00687499999999996);
#88061=CYLINDRICAL_SURFACE('',#100430,0.0125);
#88062=CYLINDRICAL_SURFACE('',#100437,0.0125);
#88063=CYLINDRICAL_SURFACE('',#100444,0.00687499999999999);
#88064=CYLINDRICAL_SURFACE('',#100453,0.0125);
#88065=CYLINDRICAL_SURFACE('',#100460,0.0125);
#88066=CYLINDRICAL_SURFACE('',#100467,0.00687499999999993);
#88067=CYLINDRICAL_SURFACE('',#100476,0.0125);
#88068=CYLINDRICAL_SURFACE('',#100483,0.0125);
#88069=CYLINDRICAL_SURFACE('',#100490,0.00687499999999995);
#88070=CYLINDRICAL_SURFACE('',#100499,0.0125);
#88071=CYLINDRICAL_SURFACE('',#100506,0.0125);
#88072=CYLINDRICAL_SURFACE('',#100513,0.00687499999999998);
#88073=CYLINDRICAL_SURFACE('',#100522,0.0125000000000001);
#88074=CYLINDRICAL_SURFACE('',#100529,0.0125000000000001);
#88075=CYLINDRICAL_SURFACE('',#100536,0.00687499999999991);
#88076=CYLINDRICAL_SURFACE('',#100545,0.0125);
#88077=CYLINDRICAL_SURFACE('',#100552,0.0125);
#88078=CYLINDRICAL_SURFACE('',#100559,0.00687500000000009);
#88079=CYLINDRICAL_SURFACE('',#100568,0.0125);
#88080=CYLINDRICAL_SURFACE('',#100575,0.0124999999999999);
#88081=CYLINDRICAL_SURFACE('',#100582,0.00687500000000007);
#88082=CYLINDRICAL_SURFACE('',#100591,0.0125000000000001);
#88083=CYLINDRICAL_SURFACE('',#100598,0.0125000000000001);
#88084=CYLINDRICAL_SURFACE('',#100605,0.00687500000000009);
#88085=CYLINDRICAL_SURFACE('',#100614,0.0125000000000001);
#88086=CYLINDRICAL_SURFACE('',#100621,0.0125000000000001);
#88087=CYLINDRICAL_SURFACE('',#100628,0.00687500000000004);
#88088=CYLINDRICAL_SURFACE('',#100637,0.0125000000000001);
#88089=CYLINDRICAL_SURFACE('',#100644,0.0125000000000001);
#88090=CYLINDRICAL_SURFACE('',#100651,0.00687500000000003);
#88091=CYLINDRICAL_SURFACE('',#100660,0.0125);
#88092=CYLINDRICAL_SURFACE('',#100667,0.0125);
#88093=CYLINDRICAL_SURFACE('',#100674,0.00687499999999996);
#88094=CYLINDRICAL_SURFACE('',#100683,0.0125);
#88095=CYLINDRICAL_SURFACE('',#100690,0.0125);
#88096=CYLINDRICAL_SURFACE('',#100697,0.00687499999999994);
#88097=CYLINDRICAL_SURFACE('',#100706,0.0125);
#88098=CYLINDRICAL_SURFACE('',#100713,0.0125000000000001);
#88099=CYLINDRICAL_SURFACE('',#100720,0.00687499999999994);
#88100=CYLINDRICAL_SURFACE('',#100729,0.0124999999999999);
#88101=CYLINDRICAL_SURFACE('',#100736,0.0124999999999999);
#88102=CYLINDRICAL_SURFACE('',#100743,0.00687500000000012);
#88103=CYLINDRICAL_SURFACE('',#100752,0.0125);
#88104=CYLINDRICAL_SURFACE('',#100759,0.0125);
#88105=CYLINDRICAL_SURFACE('',#100766,0.00687499999999988);
#88106=CYLINDRICAL_SURFACE('',#100775,0.0125);
#88107=CYLINDRICAL_SURFACE('',#100782,0.0125);
#88108=CYLINDRICAL_SURFACE('',#100789,0.00687500000000008);
#88109=CYLINDRICAL_SURFACE('',#100798,0.0125000000000001);
#88110=CYLINDRICAL_SURFACE('',#100805,0.0125000000000001);
#88111=CYLINDRICAL_SURFACE('',#100812,0.00687500000000005);
#88112=CYLINDRICAL_SURFACE('',#100821,0.0125);
#88113=CYLINDRICAL_SURFACE('',#100828,0.0125);
#88114=CYLINDRICAL_SURFACE('',#100835,0.00687499999999988);
#88115=CYLINDRICAL_SURFACE('',#100844,0.0125);
#88116=CYLINDRICAL_SURFACE('',#100851,0.0125);
#88117=CYLINDRICAL_SURFACE('',#100858,0.00687499999999997);
#88118=CYLINDRICAL_SURFACE('',#100867,0.0125);
#88119=CYLINDRICAL_SURFACE('',#100874,0.0125);
#88120=CYLINDRICAL_SURFACE('',#100881,0.00687499999999996);
#88121=CYLINDRICAL_SURFACE('',#100890,0.0125);
#88122=CYLINDRICAL_SURFACE('',#100897,0.0125);
#88123=CYLINDRICAL_SURFACE('',#100904,0.00687499999999993);
#88124=CYLINDRICAL_SURFACE('',#100913,0.0125);
#88125=CYLINDRICAL_SURFACE('',#100920,0.0125);
#88126=CYLINDRICAL_SURFACE('',#100927,0.00687500000000001);
#88127=CYLINDRICAL_SURFACE('',#100936,0.0125);
#88128=CYLINDRICAL_SURFACE('',#100943,0.0125);
#88129=CYLINDRICAL_SURFACE('',#100950,0.00687499999999995);
#88130=CYLINDRICAL_SURFACE('',#100959,0.0125);
#88131=CYLINDRICAL_SURFACE('',#100966,0.0125);
#88132=CYLINDRICAL_SURFACE('',#100973,0.00687499999999997);
#88133=CYLINDRICAL_SURFACE('',#100982,0.0125);
#88134=CYLINDRICAL_SURFACE('',#100989,0.0125);
#88135=CYLINDRICAL_SURFACE('',#100996,0.00687499999999996);
#88136=CYLINDRICAL_SURFACE('',#101005,0.0125);
#88137=CYLINDRICAL_SURFACE('',#101012,0.0125);
#88138=CYLINDRICAL_SURFACE('',#101019,0.00687500000000001);
#88139=CYLINDRICAL_SURFACE('',#101028,0.0125);
#88140=CYLINDRICAL_SURFACE('',#101035,0.0125);
#88141=CYLINDRICAL_SURFACE('',#101042,0.00687499999999995);
#88142=CYLINDRICAL_SURFACE('',#101051,0.0125);
#88143=CYLINDRICAL_SURFACE('',#101058,0.0125);
#88144=CYLINDRICAL_SURFACE('',#101065,0.00687499999999993);
#88145=CYLINDRICAL_SURFACE('',#101074,0.0125);
#88146=CYLINDRICAL_SURFACE('',#101081,0.0125);
#88147=CYLINDRICAL_SURFACE('',#101088,0.00687499999999996);
#88148=CYLINDRICAL_SURFACE('',#101097,0.0125000000000001);
#88149=CYLINDRICAL_SURFACE('',#101104,0.0125000000000001);
#88150=CYLINDRICAL_SURFACE('',#101111,0.00687499999999997);
#88151=CYLINDRICAL_SURFACE('',#101120,0.0125000000000001);
#88152=CYLINDRICAL_SURFACE('',#101127,0.0125);
#88153=CYLINDRICAL_SURFACE('',#101134,0.00687499999999988);
#88154=CYLINDRICAL_SURFACE('',#101143,0.0124999999999999);
#88155=CYLINDRICAL_SURFACE('',#101150,0.0124999999999999);
#88156=CYLINDRICAL_SURFACE('',#101157,0.00687500000000005);
#88157=CYLINDRICAL_SURFACE('',#101166,0.0125);
#88158=CYLINDRICAL_SURFACE('',#101173,0.0125);
#88159=CYLINDRICAL_SURFACE('',#101180,0.00687499999999999);
#88160=CYLINDRICAL_SURFACE('',#101189,0.0125);
#88161=CYLINDRICAL_SURFACE('',#101196,0.0125);
#88162=CYLINDRICAL_SURFACE('',#101203,0.00687499999999995);
#88163=CYLINDRICAL_SURFACE('',#101212,0.0125);
#88164=CYLINDRICAL_SURFACE('',#101219,0.0125);
#88165=CYLINDRICAL_SURFACE('',#101226,0.00687499999999988);
#88166=CYLINDRICAL_SURFACE('',#101235,0.0124999999999999);
#88167=CYLINDRICAL_SURFACE('',#101242,0.0124999999999999);
#88168=CYLINDRICAL_SURFACE('',#101249,0.00687499999999991);
#88169=CYLINDRICAL_SURFACE('',#101258,0.0125);
#88170=CYLINDRICAL_SURFACE('',#101265,0.0125);
#88171=CYLINDRICAL_SURFACE('',#101272,0.0068749999999999);
#88172=CYLINDRICAL_SURFACE('',#101281,0.0125000000000001);
#88173=CYLINDRICAL_SURFACE('',#101288,0.0125);
#88174=CYLINDRICAL_SURFACE('',#101295,0.00687499999999987);
#88175=CYLINDRICAL_SURFACE('',#101304,0.0125);
#88176=CYLINDRICAL_SURFACE('',#101311,0.0125);
#88177=CYLINDRICAL_SURFACE('',#101318,0.00687500000000009);
#88178=CYLINDRICAL_SURFACE('',#101327,0.0124999999999999);
#88179=CYLINDRICAL_SURFACE('',#101334,0.0124999999999999);
#88180=CYLINDRICAL_SURFACE('',#101341,0.00687499999999986);
#88181=CYLINDRICAL_SURFACE('',#101350,0.0124999999999999);
#88182=CYLINDRICAL_SURFACE('',#101357,0.0124999999999999);
#88183=CYLINDRICAL_SURFACE('',#101364,0.00687500000000003);
#88184=CYLINDRICAL_SURFACE('',#101373,0.0124999999999999);
#88185=CYLINDRICAL_SURFACE('',#101380,0.0124999999999999);
#88186=CYLINDRICAL_SURFACE('',#101387,0.00687499999999996);
#88187=CYLINDRICAL_SURFACE('',#101396,0.0124999999999998);
#88188=CYLINDRICAL_SURFACE('',#101403,0.0124999999999998);
#88189=CYLINDRICAL_SURFACE('',#101410,0.00687499999999994);
#88190=CYLINDRICAL_SURFACE('',#101419,0.0125);
#88191=CYLINDRICAL_SURFACE('',#101426,0.0125000000000001);
#88192=CYLINDRICAL_SURFACE('',#101433,0.00687499999999994);
#88193=CYLINDRICAL_SURFACE('',#101442,0.0125);
#88194=CYLINDRICAL_SURFACE('',#101449,0.0125);
#88195=CYLINDRICAL_SURFACE('',#101456,0.00687499999999985);
#88196=CYLINDRICAL_SURFACE('',#101465,0.0125);
#88197=CYLINDRICAL_SURFACE('',#101472,0.0125);
#88198=CYLINDRICAL_SURFACE('',#101479,0.00687500000000006);
#88199=CYLINDRICAL_SURFACE('',#101488,0.0125);
#88200=CYLINDRICAL_SURFACE('',#101495,0.0125);
#88201=CYLINDRICAL_SURFACE('',#101502,0.00687500000000008);
#88202=CYLINDRICAL_SURFACE('',#101511,0.0124999999999999);
#88203=CYLINDRICAL_SURFACE('',#101518,0.0124999999999999);
#88204=CYLINDRICAL_SURFACE('',#101525,0.00687500000000005);
#88205=CYLINDRICAL_SURFACE('',#101534,0.0124999999999998);
#88206=CYLINDRICAL_SURFACE('',#101541,0.0124999999999998);
#88207=CYLINDRICAL_SURFACE('',#101548,0.00687499999999988);
#88208=CYLINDRICAL_SURFACE('',#101557,0.0124999999999999);
#88209=CYLINDRICAL_SURFACE('',#101564,0.0124999999999999);
#88210=CYLINDRICAL_SURFACE('',#101571,0.00687499999999997);
#88211=CYLINDRICAL_SURFACE('',#101580,0.0125);
#88212=CYLINDRICAL_SURFACE('',#101587,0.0125);
#88213=CYLINDRICAL_SURFACE('',#101594,0.00687499999999996);
#88214=CYLINDRICAL_SURFACE('',#101603,0.0125);
#88215=CYLINDRICAL_SURFACE('',#101610,0.0125);
#88216=CYLINDRICAL_SURFACE('',#101617,0.00687499999999993);
#88217=CYLINDRICAL_SURFACE('',#101626,0.0125);
#88218=CYLINDRICAL_SURFACE('',#101633,0.0125);
#88219=CYLINDRICAL_SURFACE('',#101640,0.00687499999999995);
#88220=CYLINDRICAL_SURFACE('',#101649,0.0125);
#88221=CYLINDRICAL_SURFACE('',#101656,0.0125);
#88222=CYLINDRICAL_SURFACE('',#101663,0.00687499999999995);
#88223=CYLINDRICAL_SURFACE('',#101672,0.0125);
#88224=CYLINDRICAL_SURFACE('',#101679,0.0125);
#88225=CYLINDRICAL_SURFACE('',#101686,0.00687499999999996);
#88226=CYLINDRICAL_SURFACE('',#101695,0.0125);
#88227=CYLINDRICAL_SURFACE('',#101702,0.0125);
#88228=CYLINDRICAL_SURFACE('',#101709,0.00687499999999996);
#88229=CYLINDRICAL_SURFACE('',#101718,0.0125);
#88230=CYLINDRICAL_SURFACE('',#101725,0.0125);
#88231=CYLINDRICAL_SURFACE('',#101732,0.00687499999999995);
#88232=CYLINDRICAL_SURFACE('',#101741,0.0125);
#88233=CYLINDRICAL_SURFACE('',#101748,0.0125);
#88234=CYLINDRICAL_SURFACE('',#101755,0.00687500000000001);
#88235=CYLINDRICAL_SURFACE('',#101764,0.0125000000000001);
#88236=CYLINDRICAL_SURFACE('',#101771,0.0125000000000001);
#88237=CYLINDRICAL_SURFACE('',#101778,0.00687499999999993);
#88238=CYLINDRICAL_SURFACE('',#101787,0.0125);
#88239=CYLINDRICAL_SURFACE('',#101794,0.0125);
#88240=CYLINDRICAL_SURFACE('',#101801,0.00687499999999996);
#88241=CYLINDRICAL_SURFACE('',#101810,0.0125);
#88242=CYLINDRICAL_SURFACE('',#101817,0.0125);
#88243=CYLINDRICAL_SURFACE('',#101824,0.00687499999999997);
#88244=CYLINDRICAL_SURFACE('',#101833,0.0125);
#88245=CYLINDRICAL_SURFACE('',#101840,0.0125);
#88246=CYLINDRICAL_SURFACE('',#101847,0.00687499999999988);
#88247=CYLINDRICAL_SURFACE('',#101856,0.0125);
#88248=CYLINDRICAL_SURFACE('',#101863,0.0125);
#88249=CYLINDRICAL_SURFACE('',#101870,0.00687500000000005);
#88250=CYLINDRICAL_SURFACE('',#101879,0.0125);
#88251=CYLINDRICAL_SURFACE('',#101886,0.0125);
#88252=CYLINDRICAL_SURFACE('',#101893,0.00687500000000008);
#88253=CYLINDRICAL_SURFACE('',#101902,0.0125000000000001);
#88254=CYLINDRICAL_SURFACE('',#101909,0.0125000000000001);
#88255=CYLINDRICAL_SURFACE('',#101916,0.00687499999999988);
#88256=CYLINDRICAL_SURFACE('',#101925,0.0125);
#88257=CYLINDRICAL_SURFACE('',#101932,0.0125);
#88258=CYLINDRICAL_SURFACE('',#101939,0.00687499999999985);
#88259=CYLINDRICAL_SURFACE('',#101948,0.0125);
#88260=CYLINDRICAL_SURFACE('',#101955,0.0125);
#88261=CYLINDRICAL_SURFACE('',#101962,0.00687499999999994);
#88262=CYLINDRICAL_SURFACE('',#101971,0.0125);
#88263=CYLINDRICAL_SURFACE('',#101978,0.0125);
#88264=CYLINDRICAL_SURFACE('',#101985,0.00687500000000009);
#88265=CYLINDRICAL_SURFACE('',#101994,0.0124999999999998);
#88266=CYLINDRICAL_SURFACE('',#102001,0.0125);
#88267=CYLINDRICAL_SURFACE('',#102008,0.00687499999999996);
#88268=CYLINDRICAL_SURFACE('',#102017,0.0124999999999998);
#88269=CYLINDRICAL_SURFACE('',#102024,0.0124999999999998);
#88270=CYLINDRICAL_SURFACE('',#102031,0.00687500000000003);
#88271=CYLINDRICAL_SURFACE('',#102040,0.0125);
#88272=CYLINDRICAL_SURFACE('',#102047,0.0125);
#88273=CYLINDRICAL_SURFACE('',#102054,0.00687500000000004);
#88274=CYLINDRICAL_SURFACE('',#102063,0.0124999999999999);
#88275=CYLINDRICAL_SURFACE('',#102070,0.0124999999999999);
#88276=CYLINDRICAL_SURFACE('',#102077,0.00687500000000009);
#88277=CYLINDRICAL_SURFACE('',#102086,0.0124999999999999);
#88278=CYLINDRICAL_SURFACE('',#102093,0.0124999999999999);
#88279=CYLINDRICAL_SURFACE('',#102100,0.00687500000000007);
#88280=CYLINDRICAL_SURFACE('',#102109,0.0124999999999999);
#88281=CYLINDRICAL_SURFACE('',#102116,0.0124999999999999);
#88282=CYLINDRICAL_SURFACE('',#102123,0.00687500000000009);
#88283=CYLINDRICAL_SURFACE('',#102132,0.0125);
#88284=CYLINDRICAL_SURFACE('',#102139,0.0125000000000001);
#88285=CYLINDRICAL_SURFACE('',#102146,0.00687499999999991);
#88286=CYLINDRICAL_SURFACE('',#102155,0.0125);
#88287=CYLINDRICAL_SURFACE('',#102162,0.0125);
#88288=CYLINDRICAL_SURFACE('',#102169,0.00687499999999998);
#88289=CYLINDRICAL_SURFACE('',#102178,0.0124999999999999);
#88290=CYLINDRICAL_SURFACE('',#102185,0.0124999999999999);
#88291=CYLINDRICAL_SURFACE('',#102192,0.00687499999999995);
#88292=CYLINDRICAL_SURFACE('',#102201,0.0125);
#88293=CYLINDRICAL_SURFACE('',#102208,0.0125);
#88294=CYLINDRICAL_SURFACE('',#102215,0.00687499999999993);
#88295=CYLINDRICAL_SURFACE('',#102224,0.0125);
#88296=CYLINDRICAL_SURFACE('',#102231,0.0125);
#88297=CYLINDRICAL_SURFACE('',#102238,0.00687499999999999);
#88298=CYLINDRICAL_SURFACE('',#102247,0.0125);
#88299=CYLINDRICAL_SURFACE('',#102254,0.0125);
#88300=CYLINDRICAL_SURFACE('',#102261,0.00687499999999997);
#88301=CYLINDRICAL_SURFACE('',#102270,0.0125);
#88302=CYLINDRICAL_SURFACE('',#102277,0.0125);
#88303=CYLINDRICAL_SURFACE('',#102284,0.00687499999999996);
#88304=CYLINDRICAL_SURFACE('',#102293,0.0125);
#88305=CYLINDRICAL_SURFACE('',#102300,0.0125);
#88306=CYLINDRICAL_SURFACE('',#102307,0.00687499999999999);
#88307=CYLINDRICAL_SURFACE('',#102316,0.0125);
#88308=CYLINDRICAL_SURFACE('',#102323,0.0125);
#88309=CYLINDRICAL_SURFACE('',#102330,0.00687499999999995);
#88310=CYLINDRICAL_SURFACE('',#102339,0.0125);
#88311=CYLINDRICAL_SURFACE('',#102346,0.0125);
#88312=CYLINDRICAL_SURFACE('',#102353,0.00687499999999988);
#88313=CYLINDRICAL_SURFACE('',#102362,0.0125000000000001);
#88314=CYLINDRICAL_SURFACE('',#102369,0.0125000000000001);
#88315=CYLINDRICAL_SURFACE('',#102376,0.00687500000000005);
#88316=CYLINDRICAL_SURFACE('',#102385,0.0125);
#88317=CYLINDRICAL_SURFACE('',#102392,0.0125);
#88318=CYLINDRICAL_SURFACE('',#102399,0.0068749999999999);
#88319=CYLINDRICAL_SURFACE('',#102408,0.0125000000000001);
#88320=CYLINDRICAL_SURFACE('',#102415,0.0125);
#88321=CYLINDRICAL_SURFACE('',#102422,0.00687499999999987);
#88322=CYLINDRICAL_SURFACE('',#102431,0.0125);
#88323=CYLINDRICAL_SURFACE('',#102438,0.0125);
#88324=CYLINDRICAL_SURFACE('',#102445,0.0068749999999999);
#88325=CYLINDRICAL_SURFACE('',#102454,0.0124999999999999);
#88326=CYLINDRICAL_SURFACE('',#102461,0.0124999999999999);
#88327=CYLINDRICAL_SURFACE('',#102468,0.00687499999999986);
#88328=CYLINDRICAL_SURFACE('',#102477,0.0125000000000001);
#88329=CYLINDRICAL_SURFACE('',#102484,0.0125000000000001);
#88330=CYLINDRICAL_SURFACE('',#102491,0.00687499999999985);
#88331=CYLINDRICAL_SURFACE('',#102500,0.0125000000000001);
#88332=CYLINDRICAL_SURFACE('',#102507,0.0125000000000001);
#88333=CYLINDRICAL_SURFACE('',#102514,0.00687499999999996);
#88334=CYLINDRICAL_SURFACE('',#102523,0.0125000000000001);
#88335=CYLINDRICAL_SURFACE('',#102530,0.0125000000000001);
#88336=CYLINDRICAL_SURFACE('',#102537,0.00687499999999994);
#88337=CYLINDRICAL_SURFACE('',#102546,0.0125);
#88338=CYLINDRICAL_SURFACE('',#102553,0.0125000000000001);
#88339=CYLINDRICAL_SURFACE('',#102560,0.00687499999999994);
#88340=CYLINDRICAL_SURFACE('',#102569,0.0125);
#88341=CYLINDRICAL_SURFACE('',#102576,0.0125);
#88342=CYLINDRICAL_SURFACE('',#102583,0.00687499999999985);
#88343=CYLINDRICAL_SURFACE('',#102592,0.0125);
#88344=CYLINDRICAL_SURFACE('',#102599,0.0125);
#88345=CYLINDRICAL_SURFACE('',#102606,0.00687500000000006);
#88346=CYLINDRICAL_SURFACE('',#102615,0.0125);
#88347=CYLINDRICAL_SURFACE('',#102622,0.0125);
#88348=CYLINDRICAL_SURFACE('',#102629,0.00687500000000008);
#88349=CYLINDRICAL_SURFACE('',#102638,0.0124999999999999);
#88350=CYLINDRICAL_SURFACE('',#102645,0.0124999999999999);
#91015=ADVANCED_FACE('',(#8551),#87997,.T.);
#91016=ADVANCED_FACE('',(#8552),#87998,.T.);
#91017=ADVANCED_FACE('',(#8553),#87999,.T.);
#91018=ADVANCED_FACE('',(#8554),#88000,.T.);
#91019=ADVANCED_FACE('',(#8555),#88001,.T.);
#91020=ADVANCED_FACE('',(#8556),#88002,.T.);
#91021=ADVANCED_FACE('',(#8557),#88003,.T.);
#91022=ADVANCED_FACE('',(#8558),#88004,.T.);
#91023=ADVANCED_FACE('',(#8559),#88005,.T.);
#91024=ADVANCED_FACE('',(#8560),#88006,.T.);
#91025=ADVANCED_FACE('',(#8561),#88007,.T.);
#91026=ADVANCED_FACE('',(#8562),#88008,.T.);
#91027=ADVANCED_FACE('',(#8563),#88009,.T.);
#91028=ADVANCED_FACE('',(#8564),#88010,.T.);
#91029=ADVANCED_FACE('',(#8565),#88011,.T.);
#91030=ADVANCED_FACE('',(#8566),#88012,.T.);
#91031=ADVANCED_FACE('',(#8567),#88013,.T.);
#91032=ADVANCED_FACE('',(#8568),#88014,.T.);
#91033=ADVANCED_FACE('',(#8569),#88015,.T.);
#91034=ADVANCED_FACE('',(#8570),#88016,.T.);
#91035=ADVANCED_FACE('',(#8571),#88017,.T.);
#91036=ADVANCED_FACE('',(#8572),#88018,.T.);
#91037=ADVANCED_FACE('',(#8573),#88019,.T.);
#91038=ADVANCED_FACE('',(#8574),#88020,.T.);
#91039=ADVANCED_FACE('',(#8575),#88021,.T.);
#91040=ADVANCED_FACE('',(#8576),#88022,.T.);
#91041=ADVANCED_FACE('',(#8577),#88023,.T.);
#91042=ADVANCED_FACE('',(#8578),#88024,.T.);
#91043=ADVANCED_FACE('',(#8579),#88025,.T.);
#91044=ADVANCED_FACE('',(#8580),#88026,.T.);
#91045=ADVANCED_FACE('',(#8581),#88027,.T.);
#91046=ADVANCED_FACE('',(#8582),#88028,.T.);
#91047=ADVANCED_FACE('',(#8583),#88029,.T.);
#91048=ADVANCED_FACE('',(#8584),#88030,.T.);
#91049=ADVANCED_FACE('',(#8585),#88031,.T.);
#91050=ADVANCED_FACE('',(#8586),#88032,.T.);
#91051=ADVANCED_FACE('',(#8587),#88033,.T.);
#91052=ADVANCED_FACE('',(#8588),#88034,.T.);
#91053=ADVANCED_FACE('',(#8589),#88035,.T.);
#91054=ADVANCED_FACE('',(#8590),#88036,.T.);
#91055=ADVANCED_FACE('',(#8591),#88037,.T.);
#91056=ADVANCED_FACE('',(#8592),#88038,.T.);
#91057=ADVANCED_FACE('',(#8593),#88039,.T.);
#91058=ADVANCED_FACE('',(#8594),#88040,.T.);
#91059=ADVANCED_FACE('',(#8595),#88041,.T.);
#91060=ADVANCED_FACE('',(#8596),#88042,.T.);
#91061=ADVANCED_FACE('',(#8597),#88043,.T.);
#91062=ADVANCED_FACE('',(#8598),#88044,.T.);
#91063=ADVANCED_FACE('',(#8599),#88045,.T.);
#91064=ADVANCED_FACE('',(#8600),#88046,.T.);
#91065=ADVANCED_FACE('',(#8601),#88047,.T.);
#91066=ADVANCED_FACE('',(#8602),#88048,.T.);
#91067=ADVANCED_FACE('',(#8603),#88049,.T.);
#91068=ADVANCED_FACE('',(#8604),#88050,.T.);
#91069=ADVANCED_FACE('',(#8605),#88051,.T.);
#91070=ADVANCED_FACE('',(#8606),#88052,.T.);
#91071=ADVANCED_FACE('',(#8607),#88053,.T.);
#91072=ADVANCED_FACE('',(#8608),#4903,.T.);
#91073=ADVANCED_FACE('',(#8609),#4904,.T.);
#91074=ADVANCED_FACE('',(#8610),#4905,.T.);
#91075=ADVANCED_FACE('',(#8611),#4906,.T.);
#91076=ADVANCED_FACE('',(#8612),#88054,.T.);
#91077=ADVANCED_FACE('',(#8613),#1864,.F.);
#91078=ADVANCED_FACE('',(#8614),#4907,.F.);
#91079=ADVANCED_FACE('',(#8615),#4908,.F.);
#91080=ADVANCED_FACE('',(#8616),#1865,.T.);
#91081=ADVANCED_FACE('',(#8617),#4909,.T.);
#91082=ADVANCED_FACE('',(#8618),#1866,.T.);
#91083=ADVANCED_FACE('',(#8619),#4910,.T.);
#91084=ADVANCED_FACE('',(#8620),#1867,.T.);
#91085=ADVANCED_FACE('',(#8621),#88055,.T.);
#91086=ADVANCED_FACE('',(#8622),#1868,.T.);
#91087=ADVANCED_FACE('',(#8623),#1869,.T.);
#91088=ADVANCED_FACE('',(#8624),#1870,.T.);
#91089=ADVANCED_FACE('',(#8625),#1871,.T.);
#91090=ADVANCED_FACE('',(#8626),#1872,.T.);
#91091=ADVANCED_FACE('',(#8627),#1873,.T.);
#91092=ADVANCED_FACE('',(#8628),#1874,.T.);
#91093=ADVANCED_FACE('',(#8629),#1875,.T.);
#91094=ADVANCED_FACE('',(#8630),#1876,.T.);
#91095=ADVANCED_FACE('',(#8631),#1877,.T.);
#91096=ADVANCED_FACE('',(#8632),#1878,.T.);
#91097=ADVANCED_FACE('',(#8633),#1879,.T.);
#91098=ADVANCED_FACE('',(#8634),#1880,.T.);
#91099=ADVANCED_FACE('',(#8635),#1881,.T.);
#91100=ADVANCED_FACE('',(#8636),#1882,.T.);
#91101=ADVANCED_FACE('',(#8637),#1883,.T.);
#91102=ADVANCED_FACE('',(#8638),#1884,.T.);
#91103=ADVANCED_FACE('',(#8639),#1885,.T.);
#91104=ADVANCED_FACE('',(#8640),#1886,.T.);
#91105=ADVANCED_FACE('',(#8641),#1887,.T.);
#91106=ADVANCED_FACE('',(#8642),#1888,.T.);
#91107=ADVANCED_FACE('',(#8643),#1889,.T.);
#91108=ADVANCED_FACE('',(#8644),#1890,.T.);
#91109=ADVANCED_FACE('',(#8645),#1891,.T.);
#91110=ADVANCED_FACE('',(#8646),#1892,.T.);
#91111=ADVANCED_FACE('',(#8647),#1893,.T.);
#91112=ADVANCED_FACE('',(#8648),#1894,.T.);
#91113=ADVANCED_FACE('',(#8649),#1895,.T.);
#91114=ADVANCED_FACE('',(#8650),#1896,.T.);
#91115=ADVANCED_FACE('',(#8651),#1897,.T.);
#91116=ADVANCED_FACE('',(#8652),#1898,.T.);
#91117=ADVANCED_FACE('',(#8653),#1899,.T.);
#91118=ADVANCED_FACE('',(#8654),#1900,.T.);
#91119=ADVANCED_FACE('',(#8655),#1901,.T.);
#91120=ADVANCED_FACE('',(#8656),#1902,.T.);
#91121=ADVANCED_FACE('',(#8657),#1903,.T.);
#91122=ADVANCED_FACE('',(#8658),#1904,.T.);
#91123=ADVANCED_FACE('',(#8659),#1905,.T.);
#91124=ADVANCED_FACE('',(#8660),#1906,.T.);
#91125=ADVANCED_FACE('',(#8661),#1907,.T.);
#91126=ADVANCED_FACE('',(#8662),#1908,.T.);
#91127=ADVANCED_FACE('',(#8663),#1909,.T.);
#91128=ADVANCED_FACE('',(#8664),#1910,.T.);
#91129=ADVANCED_FACE('',(#8665),#1911,.T.);
#91130=ADVANCED_FACE('',(#8666),#1912,.T.);
#91131=ADVANCED_FACE('',(#8667),#1913,.T.);
#91132=ADVANCED_FACE('',(#8668),#1914,.T.);
#91133=ADVANCED_FACE('',(#8669),#1915,.T.);
#91134=ADVANCED_FACE('',(#8670),#1916,.T.);
#91135=ADVANCED_FACE('',(#8671),#1917,.T.);
#91136=ADVANCED_FACE('',(#8672),#1918,.T.);
#91137=ADVANCED_FACE('',(#8673),#1919,.T.);
#91138=ADVANCED_FACE('',(#8674),#1920,.T.);
#91139=ADVANCED_FACE('',(#8675),#1921,.T.);
#91140=ADVANCED_FACE('',(#8676),#1922,.T.);
#91141=ADVANCED_FACE('',(#8677),#1923,.T.);
#91142=ADVANCED_FACE('',(#8678),#1924,.T.);
#91143=ADVANCED_FACE('',(#8679),#1925,.T.);
#91144=ADVANCED_FACE('',(#8680),#1926,.T.);
#91145=ADVANCED_FACE('',(#8681),#1927,.T.);
#91146=ADVANCED_FACE('',(#8682),#1928,.T.);
#91147=ADVANCED_FACE('',(#8683),#1929,.T.);
#91148=ADVANCED_FACE('',(#8684),#1930,.T.);
#91149=ADVANCED_FACE('',(#8685),#1931,.T.);
#91150=ADVANCED_FACE('',(#8686),#1932,.T.);
#91151=ADVANCED_FACE('',(#8687),#1933,.T.);
#91152=ADVANCED_FACE('',(#8688),#1934,.T.);
#91153=ADVANCED_FACE('',(#8689),#1935,.T.);
#91154=ADVANCED_FACE('',(#8690),#1936,.T.);
#91155=ADVANCED_FACE('',(#8691),#1937,.T.);
#91156=ADVANCED_FACE('',(#8692),#1938,.T.);
#91157=ADVANCED_FACE('',(#8693),#1939,.T.);
#91158=ADVANCED_FACE('',(#8694),#1940,.T.);
#91159=ADVANCED_FACE('',(#8695),#1941,.T.);
#91160=ADVANCED_FACE('',(#8696),#1942,.T.);
#91161=ADVANCED_FACE('',(#8697),#1943,.T.);
#91162=ADVANCED_FACE('',(#8698),#1944,.T.);
#91163=ADVANCED_FACE('',(#8699),#1945,.T.);
#91164=ADVANCED_FACE('',(#8700),#1946,.T.);
#91165=ADVANCED_FACE('',(#8701),#1947,.T.);
#91166=ADVANCED_FACE('',(#8702),#1948,.T.);
#91167=ADVANCED_FACE('',(#8703),#1949,.T.);
#91168=ADVANCED_FACE('',(#8704),#1950,.T.);
#91169=ADVANCED_FACE('',(#8705),#1951,.T.);
#91170=ADVANCED_FACE('',(#8706),#1952,.T.);
#91171=ADVANCED_FACE('',(#8707),#1953,.T.);
#91172=ADVANCED_FACE('',(#8708),#1954,.T.);
#91173=ADVANCED_FACE('',(#8709),#1955,.T.);
#91174=ADVANCED_FACE('',(#8710),#1956,.T.);
#91175=ADVANCED_FACE('',(#8711),#1957,.T.);
#91176=ADVANCED_FACE('',(#8712),#1958,.T.);
#91177=ADVANCED_FACE('',(#8713),#1959,.T.);
#91178=ADVANCED_FACE('',(#8714),#1960,.T.);
#91179=ADVANCED_FACE('',(#8715),#1961,.T.);
#91180=ADVANCED_FACE('',(#8716),#1962,.T.);
#91181=ADVANCED_FACE('',(#8717),#1963,.T.);
#91182=ADVANCED_FACE('',(#8718),#1964,.T.);
#91183=ADVANCED_FACE('',(#8719),#88056,.F.);
#91184=ADVANCED_FACE('',(#8720),#5726,.F.);
#91185=ADVANCED_FACE('',(#8721),#5727,.F.);
#91186=ADVANCED_FACE('',(#8722),#5728,.F.);
#91187=ADVANCED_FACE('',(#8723),#5729,.F.);
#91188=ADVANCED_FACE('',(#8724),#5730,.F.);
#91189=ADVANCED_FACE('',(#8725),#5731,.F.);
#91190=ADVANCED_FACE('',(#8726),#5732,.F.);
#91191=ADVANCED_FACE('',(#8727,#5226),#5733,.F.);
#91192=ADVANCED_FACE('',(#8728),#1965,.T.);
#91193=ADVANCED_FACE('',(#8729),#5734,.F.);
#91194=ADVANCED_FACE('',(#8730),#5735,.F.);
#91195=ADVANCED_FACE('',(#8731),#5736,.F.);
#91196=ADVANCED_FACE('',(#8732),#5737,.F.);
#91197=ADVANCED_FACE('',(#8733),#5738,.F.);
#91198=ADVANCED_FACE('',(#8734),#5739,.F.);
#91199=ADVANCED_FACE('',(#8735),#5740,.F.);
#91200=ADVANCED_FACE('',(#8736),#4911,.F.);
#91201=ADVANCED_FACE('',(#8737),#4912,.F.);
#91202=ADVANCED_FACE('',(#8738),#4913,.F.);
#91203=ADVANCED_FACE('',(#8739),#4914,.F.);
#91204=ADVANCED_FACE('',(#8740),#4915,.F.);
#91205=ADVANCED_FACE('',(#8741,#5227),#5741,.T.);
#91206=ADVANCED_FACE('',(#8742),#5742,.F.);
#91207=ADVANCED_FACE('',(#8743),#88057,.T.);
#91208=ADVANCED_FACE('',(#8744),#2319,.T.);
#91209=ADVANCED_FACE('',(#8745),#2320,.T.);
#91210=ADVANCED_FACE('',(#8746),#4916,.T.);
#91211=ADVANCED_FACE('',(#8747),#2321,.F.);
#91212=ADVANCED_FACE('',(#8748),#88058,.T.);
#91213=ADVANCED_FACE('',(#8749),#2322,.F.);
#91214=ADVANCED_FACE('',(#8750),#2323,.T.);
#91215=ADVANCED_FACE('',(#8751),#2324,.T.);
#91216=ADVANCED_FACE('',(#8752),#2325,.F.);
#91217=ADVANCED_FACE('',(#8753),#1966,.T.);
#91218=ADVANCED_FACE('',(#8754),#2326,.T.);
#91219=ADVANCED_FACE('',(#8755),#2327,.T.);
#91220=ADVANCED_FACE('',(#8756),#2328,.T.);
#91221=ADVANCED_FACE('',(#8757),#88059,.T.);
#91222=ADVANCED_FACE('',(#8758),#2329,.T.);
#91223=ADVANCED_FACE('',(#8759),#2330,.T.);
#91224=ADVANCED_FACE('',(#8760),#5743,.F.);
#91225=ADVANCED_FACE('',(#8761),#5744,.F.);
#91226=ADVANCED_FACE('',(#8762),#88060,.F.);
#91227=ADVANCED_FACE('',(#8763),#2331,.F.);
#91228=ADVANCED_FACE('',(#8764),#2332,.F.);
#91229=ADVANCED_FACE('',(#8765),#2333,.F.);
#91230=ADVANCED_FACE('',(#8766),#1967,.T.);
#91231=ADVANCED_FACE('',(#8767),#2334,.T.);
#91232=ADVANCED_FACE('',(#8768),#88061,.T.);
#91233=ADVANCED_FACE('',(#8769),#2335,.T.);
#91234=ADVANCED_FACE('',(#8770),#2336,.T.);
#91235=ADVANCED_FACE('',(#8771),#2337,.T.);
#91236=ADVANCED_FACE('',(#8772),#2338,.T.);
#91237=ADVANCED_FACE('',(#8773),#2339,.T.);
#91238=ADVANCED_FACE('',(#8774),#88062,.T.);
#91239=ADVANCED_FACE('',(#8775),#2340,.T.);
#91240=ADVANCED_FACE('',(#8776),#4917,.T.);
#91241=ADVANCED_FACE('',(#8777),#5745,.F.);
#91242=ADVANCED_FACE('',(#8778),#5746,.F.);
#91243=ADVANCED_FACE('',(#8779),#88063,.F.);
#91244=ADVANCED_FACE('',(#8780),#2341,.F.);
#91245=ADVANCED_FACE('',(#8781),#2342,.F.);
#91246=ADVANCED_FACE('',(#8782),#2343,.F.);
#91247=ADVANCED_FACE('',(#8783),#1968,.T.);
#91248=ADVANCED_FACE('',(#8784),#2344,.T.);
#91249=ADVANCED_FACE('',(#8785),#88064,.T.);
#91250=ADVANCED_FACE('',(#8786),#2345,.T.);
#91251=ADVANCED_FACE('',(#8787),#2346,.T.);
#91252=ADVANCED_FACE('',(#8788),#2347,.T.);
#91253=ADVANCED_FACE('',(#8789),#2348,.T.);
#91254=ADVANCED_FACE('',(#8790),#2349,.T.);
#91255=ADVANCED_FACE('',(#8791),#88065,.T.);
#91256=ADVANCED_FACE('',(#8792),#2350,.T.);
#91257=ADVANCED_FACE('',(#8793),#4918,.T.);
#91258=ADVANCED_FACE('',(#8794),#5747,.F.);
#91259=ADVANCED_FACE('',(#8795),#5748,.F.);
#91260=ADVANCED_FACE('',(#8796),#88066,.F.);
#91261=ADVANCED_FACE('',(#8797),#2351,.F.);
#91262=ADVANCED_FACE('',(#8798),#2352,.F.);
#91263=ADVANCED_FACE('',(#8799),#2353,.F.);
#91264=ADVANCED_FACE('',(#8800),#1969,.T.);
#91265=ADVANCED_FACE('',(#8801),#2354,.T.);
#91266=ADVANCED_FACE('',(#8802),#88067,.T.);
#91267=ADVANCED_FACE('',(#8803),#2355,.T.);
#91268=ADVANCED_FACE('',(#8804),#2356,.T.);
#91269=ADVANCED_FACE('',(#8805),#2357,.T.);
#91270=ADVANCED_FACE('',(#8806),#2358,.T.);
#91271=ADVANCED_FACE('',(#8807),#2359,.T.);
#91272=ADVANCED_FACE('',(#8808),#88068,.T.);
#91273=ADVANCED_FACE('',(#8809),#2360,.T.);
#91274=ADVANCED_FACE('',(#8810),#4919,.T.);
#91275=ADVANCED_FACE('',(#8811),#5749,.F.);
#91276=ADVANCED_FACE('',(#8812),#5750,.F.);
#91277=ADVANCED_FACE('',(#8813),#88069,.F.);
#91278=ADVANCED_FACE('',(#8814),#2361,.F.);
#91279=ADVANCED_FACE('',(#8815),#2362,.F.);
#91280=ADVANCED_FACE('',(#8816),#2363,.F.);
#91281=ADVANCED_FACE('',(#8817),#1970,.T.);
#91282=ADVANCED_FACE('',(#8818),#2364,.T.);
#91283=ADVANCED_FACE('',(#8819),#88070,.T.);
#91284=ADVANCED_FACE('',(#8820),#2365,.T.);
#91285=ADVANCED_FACE('',(#8821),#2366,.T.);
#91286=ADVANCED_FACE('',(#8822),#2367,.T.);
#91287=ADVANCED_FACE('',(#8823),#2368,.T.);
#91288=ADVANCED_FACE('',(#8824),#2369,.T.);
#91289=ADVANCED_FACE('',(#8825),#88071,.T.);
#91290=ADVANCED_FACE('',(#8826),#2370,.T.);
#91291=ADVANCED_FACE('',(#8827),#4920,.T.);
#91292=ADVANCED_FACE('',(#8828),#5751,.F.);
#91293=ADVANCED_FACE('',(#8829),#5752,.F.);
#91294=ADVANCED_FACE('',(#8830),#88072,.F.);
#91295=ADVANCED_FACE('',(#8831),#2371,.F.);
#91296=ADVANCED_FACE('',(#8832),#2372,.F.);
#91297=ADVANCED_FACE('',(#8833),#2373,.F.);
#91298=ADVANCED_FACE('',(#8834),#1971,.T.);
#91299=ADVANCED_FACE('',(#8835),#2374,.T.);
#91300=ADVANCED_FACE('',(#8836),#88073,.T.);
#91301=ADVANCED_FACE('',(#8837),#2375,.T.);
#91302=ADVANCED_FACE('',(#8838),#2376,.T.);
#91303=ADVANCED_FACE('',(#8839),#2377,.T.);
#91304=ADVANCED_FACE('',(#8840),#2378,.T.);
#91305=ADVANCED_FACE('',(#8841),#2379,.T.);
#91306=ADVANCED_FACE('',(#8842),#88074,.T.);
#91307=ADVANCED_FACE('',(#8843),#2380,.T.);
#91308=ADVANCED_FACE('',(#8844),#4921,.T.);
#91309=ADVANCED_FACE('',(#8845),#5753,.F.);
#91310=ADVANCED_FACE('',(#8846),#5754,.F.);
#91311=ADVANCED_FACE('',(#8847),#88075,.F.);
#91312=ADVANCED_FACE('',(#8848),#2381,.F.);
#91313=ADVANCED_FACE('',(#8849),#2382,.F.);
#91314=ADVANCED_FACE('',(#8850),#2383,.F.);
#91315=ADVANCED_FACE('',(#8851),#1972,.T.);
#91316=ADVANCED_FACE('',(#8852),#2384,.T.);
#91317=ADVANCED_FACE('',(#8853),#88076,.T.);
#91318=ADVANCED_FACE('',(#8854),#2385,.T.);
#91319=ADVANCED_FACE('',(#8855),#2386,.T.);
#91320=ADVANCED_FACE('',(#8856),#2387,.T.);
#91321=ADVANCED_FACE('',(#8857),#2388,.T.);
#91322=ADVANCED_FACE('',(#8858),#2389,.T.);
#91323=ADVANCED_FACE('',(#8859),#88077,.T.);
#91324=ADVANCED_FACE('',(#8860),#2390,.T.);
#91325=ADVANCED_FACE('',(#8861),#4922,.T.);
#91326=ADVANCED_FACE('',(#8862),#5755,.F.);
#91327=ADVANCED_FACE('',(#8863),#5756,.F.);
#91328=ADVANCED_FACE('',(#8864),#88078,.F.);
#91329=ADVANCED_FACE('',(#8865),#2391,.F.);
#91330=ADVANCED_FACE('',(#8866),#2392,.F.);
#91331=ADVANCED_FACE('',(#8867),#2393,.F.);
#91332=ADVANCED_FACE('',(#8868),#1973,.T.);
#91333=ADVANCED_FACE('',(#8869),#2394,.T.);
#91334=ADVANCED_FACE('',(#8870),#88079,.T.);
#91335=ADVANCED_FACE('',(#8871),#2395,.T.);
#91336=ADVANCED_FACE('',(#8872),#2396,.T.);
#91337=ADVANCED_FACE('',(#8873),#2397,.T.);
#91338=ADVANCED_FACE('',(#8874),#2398,.T.);
#91339=ADVANCED_FACE('',(#8875),#2399,.T.);
#91340=ADVANCED_FACE('',(#8876),#88080,.T.);
#91341=ADVANCED_FACE('',(#8877),#2400,.T.);
#91342=ADVANCED_FACE('',(#8878),#4923,.T.);
#91343=ADVANCED_FACE('',(#8879),#5757,.F.);
#91344=ADVANCED_FACE('',(#8880),#5758,.F.);
#91345=ADVANCED_FACE('',(#8881),#88081,.F.);
#91346=ADVANCED_FACE('',(#8882),#2401,.F.);
#91347=ADVANCED_FACE('',(#8883),#2402,.F.);
#91348=ADVANCED_FACE('',(#8884),#2403,.F.);
#91349=ADVANCED_FACE('',(#8885),#1974,.T.);
#91350=ADVANCED_FACE('',(#8886),#2404,.T.);
#91351=ADVANCED_FACE('',(#8887),#88082,.T.);
#91352=ADVANCED_FACE('',(#8888),#2405,.T.);
#91353=ADVANCED_FACE('',(#8889),#2406,.T.);
#91354=ADVANCED_FACE('',(#8890),#2407,.T.);
#91355=ADVANCED_FACE('',(#8891),#2408,.T.);
#91356=ADVANCED_FACE('',(#8892),#2409,.T.);
#91357=ADVANCED_FACE('',(#8893),#88083,.T.);
#91358=ADVANCED_FACE('',(#8894),#2410,.T.);
#91359=ADVANCED_FACE('',(#8895),#4924,.T.);
#91360=ADVANCED_FACE('',(#8896),#5759,.F.);
#91361=ADVANCED_FACE('',(#8897),#5760,.F.);
#91362=ADVANCED_FACE('',(#8898),#88084,.F.);
#91363=ADVANCED_FACE('',(#8899),#2411,.F.);
#91364=ADVANCED_FACE('',(#8900),#2412,.F.);
#91365=ADVANCED_FACE('',(#8901),#2413,.F.);
#91366=ADVANCED_FACE('',(#8902),#1975,.T.);
#91367=ADVANCED_FACE('',(#8903),#2414,.T.);
#91368=ADVANCED_FACE('',(#8904),#88085,.T.);
#91369=ADVANCED_FACE('',(#8905),#2415,.T.);
#91370=ADVANCED_FACE('',(#8906),#2416,.T.);
#91371=ADVANCED_FACE('',(#8907),#2417,.T.);
#91372=ADVANCED_FACE('',(#8908),#2418,.T.);
#91373=ADVANCED_FACE('',(#8909),#2419,.T.);
#91374=ADVANCED_FACE('',(#8910),#88086,.T.);
#91375=ADVANCED_FACE('',(#8911),#2420,.T.);
#91376=ADVANCED_FACE('',(#8912),#4925,.T.);
#91377=ADVANCED_FACE('',(#8913),#5761,.F.);
#91378=ADVANCED_FACE('',(#8914),#5762,.F.);
#91379=ADVANCED_FACE('',(#8915),#88087,.F.);
#91380=ADVANCED_FACE('',(#8916),#2421,.F.);
#91381=ADVANCED_FACE('',(#8917),#2422,.F.);
#91382=ADVANCED_FACE('',(#8918),#2423,.F.);
#91383=ADVANCED_FACE('',(#8919),#1976,.T.);
#91384=ADVANCED_FACE('',(#8920),#2424,.T.);
#91385=ADVANCED_FACE('',(#8921),#88088,.T.);
#91386=ADVANCED_FACE('',(#8922),#2425,.T.);
#91387=ADVANCED_FACE('',(#8923),#2426,.T.);
#91388=ADVANCED_FACE('',(#8924),#2427,.T.);
#91389=ADVANCED_FACE('',(#8925),#2428,.T.);
#91390=ADVANCED_FACE('',(#8926),#2429,.T.);
#91391=ADVANCED_FACE('',(#8927),#88089,.T.);
#91392=ADVANCED_FACE('',(#8928),#2430,.T.);
#91393=ADVANCED_FACE('',(#8929),#4926,.T.);
#91394=ADVANCED_FACE('',(#8930),#5763,.F.);
#91395=ADVANCED_FACE('',(#8931),#5764,.F.);
#91396=ADVANCED_FACE('',(#8932),#88090,.F.);
#91397=ADVANCED_FACE('',(#8933),#2431,.F.);
#91398=ADVANCED_FACE('',(#8934),#2432,.F.);
#91399=ADVANCED_FACE('',(#8935),#2433,.F.);
#91400=ADVANCED_FACE('',(#8936),#1977,.T.);
#91401=ADVANCED_FACE('',(#8937),#2434,.T.);
#91402=ADVANCED_FACE('',(#8938),#88091,.T.);
#91403=ADVANCED_FACE('',(#8939),#2435,.T.);
#91404=ADVANCED_FACE('',(#8940),#2436,.T.);
#91405=ADVANCED_FACE('',(#8941),#2437,.T.);
#91406=ADVANCED_FACE('',(#8942),#2438,.T.);
#91407=ADVANCED_FACE('',(#8943),#2439,.T.);
#91408=ADVANCED_FACE('',(#8944),#88092,.T.);
#91409=ADVANCED_FACE('',(#8945),#2440,.T.);
#91410=ADVANCED_FACE('',(#8946),#4927,.T.);
#91411=ADVANCED_FACE('',(#8947),#5765,.F.);
#91412=ADVANCED_FACE('',(#8948),#5766,.F.);
#91413=ADVANCED_FACE('',(#8949),#88093,.F.);
#91414=ADVANCED_FACE('',(#8950),#2441,.F.);
#91415=ADVANCED_FACE('',(#8951),#2442,.F.);
#91416=ADVANCED_FACE('',(#8952),#2443,.F.);
#91417=ADVANCED_FACE('',(#8953),#1978,.T.);
#91418=ADVANCED_FACE('',(#8954),#2444,.T.);
#91419=ADVANCED_FACE('',(#8955),#88094,.T.);
#91420=ADVANCED_FACE('',(#8956),#2445,.T.);
#91421=ADVANCED_FACE('',(#8957),#2446,.T.);
#91422=ADVANCED_FACE('',(#8958),#2447,.T.);
#91423=ADVANCED_FACE('',(#8959),#2448,.T.);
#91424=ADVANCED_FACE('',(#8960),#2449,.T.);
#91425=ADVANCED_FACE('',(#8961),#88095,.T.);
#91426=ADVANCED_FACE('',(#8962),#2450,.T.);
#91427=ADVANCED_FACE('',(#8963),#4928,.T.);
#91428=ADVANCED_FACE('',(#8964),#5767,.F.);
#91429=ADVANCED_FACE('',(#8965),#5768,.F.);
#91430=ADVANCED_FACE('',(#8966),#88096,.F.);
#91431=ADVANCED_FACE('',(#8967),#2451,.F.);
#91432=ADVANCED_FACE('',(#8968),#2452,.F.);
#91433=ADVANCED_FACE('',(#8969),#2453,.F.);
#91434=ADVANCED_FACE('',(#8970),#1979,.T.);
#91435=ADVANCED_FACE('',(#8971),#2454,.T.);
#91436=ADVANCED_FACE('',(#8972),#88097,.T.);
#91437=ADVANCED_FACE('',(#8973),#2455,.T.);
#91438=ADVANCED_FACE('',(#8974),#2456,.T.);
#91439=ADVANCED_FACE('',(#8975),#2457,.T.);
#91440=ADVANCED_FACE('',(#8976),#2458,.T.);
#91441=ADVANCED_FACE('',(#8977),#2459,.T.);
#91442=ADVANCED_FACE('',(#8978),#88098,.T.);
#91443=ADVANCED_FACE('',(#8979),#2460,.T.);
#91444=ADVANCED_FACE('',(#8980),#4929,.T.);
#91445=ADVANCED_FACE('',(#8981),#5769,.F.);
#91446=ADVANCED_FACE('',(#8982),#5770,.F.);
#91447=ADVANCED_FACE('',(#8983),#88099,.F.);
#91448=ADVANCED_FACE('',(#8984),#2461,.F.);
#91449=ADVANCED_FACE('',(#8985),#2462,.F.);
#91450=ADVANCED_FACE('',(#8986),#2463,.F.);
#91451=ADVANCED_FACE('',(#8987),#1980,.T.);
#91452=ADVANCED_FACE('',(#8988),#2464,.T.);
#91453=ADVANCED_FACE('',(#8989),#88100,.T.);
#91454=ADVANCED_FACE('',(#8990),#2465,.T.);
#91455=ADVANCED_FACE('',(#8991),#2466,.T.);
#91456=ADVANCED_FACE('',(#8992),#2467,.T.);
#91457=ADVANCED_FACE('',(#8993),#2468,.T.);
#91458=ADVANCED_FACE('',(#8994),#2469,.T.);
#91459=ADVANCED_FACE('',(#8995),#88101,.T.);
#91460=ADVANCED_FACE('',(#8996),#2470,.T.);
#91461=ADVANCED_FACE('',(#8997),#4930,.T.);
#91462=ADVANCED_FACE('',(#8998),#5771,.F.);
#91463=ADVANCED_FACE('',(#8999),#5772,.F.);
#91464=ADVANCED_FACE('',(#9000),#88102,.F.);
#91465=ADVANCED_FACE('',(#9001),#2471,.F.);
#91466=ADVANCED_FACE('',(#9002),#2472,.F.);
#91467=ADVANCED_FACE('',(#9003),#2473,.F.);
#91468=ADVANCED_FACE('',(#9004),#1981,.T.);
#91469=ADVANCED_FACE('',(#9005),#2474,.T.);
#91470=ADVANCED_FACE('',(#9006),#88103,.T.);
#91471=ADVANCED_FACE('',(#9007),#2475,.T.);
#91472=ADVANCED_FACE('',(#9008),#2476,.T.);
#91473=ADVANCED_FACE('',(#9009),#2477,.T.);
#91474=ADVANCED_FACE('',(#9010),#2478,.T.);
#91475=ADVANCED_FACE('',(#9011),#2479,.T.);
#91476=ADVANCED_FACE('',(#9012),#88104,.T.);
#91477=ADVANCED_FACE('',(#9013),#2480,.T.);
#91478=ADVANCED_FACE('',(#9014),#4931,.T.);
#91479=ADVANCED_FACE('',(#9015),#5773,.F.);
#91480=ADVANCED_FACE('',(#9016),#5774,.F.);
#91481=ADVANCED_FACE('',(#9017),#88105,.F.);
#91482=ADVANCED_FACE('',(#9018),#2481,.F.);
#91483=ADVANCED_FACE('',(#9019),#2482,.F.);
#91484=ADVANCED_FACE('',(#9020),#2483,.F.);
#91485=ADVANCED_FACE('',(#9021),#1982,.T.);
#91486=ADVANCED_FACE('',(#9022),#2484,.T.);
#91487=ADVANCED_FACE('',(#9023),#88106,.T.);
#91488=ADVANCED_FACE('',(#9024),#2485,.T.);
#91489=ADVANCED_FACE('',(#9025),#2486,.T.);
#91490=ADVANCED_FACE('',(#9026),#2487,.T.);
#91491=ADVANCED_FACE('',(#9027),#2488,.T.);
#91492=ADVANCED_FACE('',(#9028),#2489,.T.);
#91493=ADVANCED_FACE('',(#9029),#88107,.T.);
#91494=ADVANCED_FACE('',(#9030),#2490,.T.);
#91495=ADVANCED_FACE('',(#9031),#4932,.T.);
#91496=ADVANCED_FACE('',(#9032),#5775,.F.);
#91497=ADVANCED_FACE('',(#9033),#5776,.F.);
#91498=ADVANCED_FACE('',(#9034),#88108,.F.);
#91499=ADVANCED_FACE('',(#9035),#2491,.F.);
#91500=ADVANCED_FACE('',(#9036),#2492,.F.);
#91501=ADVANCED_FACE('',(#9037),#2493,.F.);
#91502=ADVANCED_FACE('',(#9038),#1983,.T.);
#91503=ADVANCED_FACE('',(#9039),#2494,.T.);
#91504=ADVANCED_FACE('',(#9040),#88109,.T.);
#91505=ADVANCED_FACE('',(#9041),#2495,.T.);
#91506=ADVANCED_FACE('',(#9042),#2496,.T.);
#91507=ADVANCED_FACE('',(#9043),#2497,.T.);
#91508=ADVANCED_FACE('',(#9044),#2498,.T.);
#91509=ADVANCED_FACE('',(#9045),#2499,.T.);
#91510=ADVANCED_FACE('',(#9046),#88110,.T.);
#91511=ADVANCED_FACE('',(#9047),#2500,.T.);
#91512=ADVANCED_FACE('',(#9048),#4933,.T.);
#91513=ADVANCED_FACE('',(#9049),#5777,.F.);
#91514=ADVANCED_FACE('',(#9050),#5778,.F.);
#91515=ADVANCED_FACE('',(#9051),#88111,.F.);
#91516=ADVANCED_FACE('',(#9052),#2501,.F.);
#91517=ADVANCED_FACE('',(#9053),#2502,.F.);
#91518=ADVANCED_FACE('',(#9054),#2503,.F.);
#91519=ADVANCED_FACE('',(#9055),#1984,.T.);
#91520=ADVANCED_FACE('',(#9056),#2504,.T.);
#91521=ADVANCED_FACE('',(#9057),#88112,.T.);
#91522=ADVANCED_FACE('',(#9058),#2505,.T.);
#91523=ADVANCED_FACE('',(#9059),#2506,.T.);
#91524=ADVANCED_FACE('',(#9060),#2507,.T.);
#91525=ADVANCED_FACE('',(#9061),#2508,.T.);
#91526=ADVANCED_FACE('',(#9062),#2509,.T.);
#91527=ADVANCED_FACE('',(#9063),#88113,.T.);
#91528=ADVANCED_FACE('',(#9064),#2510,.T.);
#91529=ADVANCED_FACE('',(#9065),#4934,.T.);
#91530=ADVANCED_FACE('',(#9066),#5779,.F.);
#91531=ADVANCED_FACE('',(#9067),#5780,.F.);
#91532=ADVANCED_FACE('',(#9068),#88114,.F.);
#91533=ADVANCED_FACE('',(#9069),#2511,.F.);
#91534=ADVANCED_FACE('',(#9070),#2512,.F.);
#91535=ADVANCED_FACE('',(#9071),#2513,.F.);
#91536=ADVANCED_FACE('',(#9072),#1985,.T.);
#91537=ADVANCED_FACE('',(#9073),#2514,.T.);
#91538=ADVANCED_FACE('',(#9074),#88115,.T.);
#91539=ADVANCED_FACE('',(#9075),#2515,.T.);
#91540=ADVANCED_FACE('',(#9076),#2516,.T.);
#91541=ADVANCED_FACE('',(#9077),#2517,.T.);
#91542=ADVANCED_FACE('',(#9078),#2518,.T.);
#91543=ADVANCED_FACE('',(#9079),#2519,.T.);
#91544=ADVANCED_FACE('',(#9080),#88116,.T.);
#91545=ADVANCED_FACE('',(#9081),#2520,.T.);
#91546=ADVANCED_FACE('',(#9082),#4935,.T.);
#91547=ADVANCED_FACE('',(#9083),#5781,.F.);
#91548=ADVANCED_FACE('',(#9084),#5782,.F.);
#91549=ADVANCED_FACE('',(#9085),#88117,.F.);
#91550=ADVANCED_FACE('',(#9086),#2521,.F.);
#91551=ADVANCED_FACE('',(#9087),#2522,.F.);
#91552=ADVANCED_FACE('',(#9088),#2523,.F.);
#91553=ADVANCED_FACE('',(#9089),#1986,.T.);
#91554=ADVANCED_FACE('',(#9090),#2524,.T.);
#91555=ADVANCED_FACE('',(#9091),#88118,.T.);
#91556=ADVANCED_FACE('',(#9092),#2525,.T.);
#91557=ADVANCED_FACE('',(#9093),#2526,.T.);
#91558=ADVANCED_FACE('',(#9094),#2527,.T.);
#91559=ADVANCED_FACE('',(#9095),#2528,.T.);
#91560=ADVANCED_FACE('',(#9096),#2529,.T.);
#91561=ADVANCED_FACE('',(#9097),#88119,.T.);
#91562=ADVANCED_FACE('',(#9098),#2530,.T.);
#91563=ADVANCED_FACE('',(#9099),#4936,.T.);
#91564=ADVANCED_FACE('',(#9100),#5783,.F.);
#91565=ADVANCED_FACE('',(#9101),#5784,.F.);
#91566=ADVANCED_FACE('',(#9102),#88120,.F.);
#91567=ADVANCED_FACE('',(#9103),#2531,.F.);
#91568=ADVANCED_FACE('',(#9104),#2532,.F.);
#91569=ADVANCED_FACE('',(#9105),#2533,.F.);
#91570=ADVANCED_FACE('',(#9106),#1987,.T.);
#91571=ADVANCED_FACE('',(#9107),#2534,.T.);
#91572=ADVANCED_FACE('',(#9108),#88121,.T.);
#91573=ADVANCED_FACE('',(#9109),#2535,.T.);
#91574=ADVANCED_FACE('',(#9110),#2536,.T.);
#91575=ADVANCED_FACE('',(#9111),#2537,.T.);
#91576=ADVANCED_FACE('',(#9112),#2538,.T.);
#91577=ADVANCED_FACE('',(#9113),#2539,.T.);
#91578=ADVANCED_FACE('',(#9114),#88122,.T.);
#91579=ADVANCED_FACE('',(#9115),#2540,.T.);
#91580=ADVANCED_FACE('',(#9116),#4937,.T.);
#91581=ADVANCED_FACE('',(#9117),#5785,.F.);
#91582=ADVANCED_FACE('',(#9118),#5786,.F.);
#91583=ADVANCED_FACE('',(#9119),#88123,.F.);
#91584=ADVANCED_FACE('',(#9120),#2541,.F.);
#91585=ADVANCED_FACE('',(#9121),#2542,.F.);
#91586=ADVANCED_FACE('',(#9122),#2543,.F.);
#91587=ADVANCED_FACE('',(#9123),#1988,.T.);
#91588=ADVANCED_FACE('',(#9124),#2544,.T.);
#91589=ADVANCED_FACE('',(#9125),#88124,.T.);
#91590=ADVANCED_FACE('',(#9126),#2545,.T.);
#91591=ADVANCED_FACE('',(#9127),#2546,.T.);
#91592=ADVANCED_FACE('',(#9128),#2547,.T.);
#91593=ADVANCED_FACE('',(#9129),#2548,.T.);
#91594=ADVANCED_FACE('',(#9130),#2549,.T.);
#91595=ADVANCED_FACE('',(#9131),#88125,.T.);
#91596=ADVANCED_FACE('',(#9132),#2550,.T.);
#91597=ADVANCED_FACE('',(#9133),#4938,.T.);
#91598=ADVANCED_FACE('',(#9134),#5787,.F.);
#91599=ADVANCED_FACE('',(#9135),#5788,.F.);
#91600=ADVANCED_FACE('',(#9136),#88126,.F.);
#91601=ADVANCED_FACE('',(#9137),#2551,.F.);
#91602=ADVANCED_FACE('',(#9138),#2552,.F.);
#91603=ADVANCED_FACE('',(#9139),#2553,.F.);
#91604=ADVANCED_FACE('',(#9140),#1989,.T.);
#91605=ADVANCED_FACE('',(#9141),#2554,.T.);
#91606=ADVANCED_FACE('',(#9142),#88127,.T.);
#91607=ADVANCED_FACE('',(#9143),#2555,.T.);
#91608=ADVANCED_FACE('',(#9144),#2556,.T.);
#91609=ADVANCED_FACE('',(#9145),#2557,.T.);
#91610=ADVANCED_FACE('',(#9146),#2558,.T.);
#91611=ADVANCED_FACE('',(#9147),#2559,.T.);
#91612=ADVANCED_FACE('',(#9148),#88128,.T.);
#91613=ADVANCED_FACE('',(#9149),#2560,.T.);
#91614=ADVANCED_FACE('',(#9150),#4939,.T.);
#91615=ADVANCED_FACE('',(#9151),#5789,.F.);
#91616=ADVANCED_FACE('',(#9152),#5790,.F.);
#91617=ADVANCED_FACE('',(#9153),#88129,.F.);
#91618=ADVANCED_FACE('',(#9154),#2561,.F.);
#91619=ADVANCED_FACE('',(#9155),#2562,.F.);
#91620=ADVANCED_FACE('',(#9156),#2563,.F.);
#91621=ADVANCED_FACE('',(#9157),#1990,.T.);
#91622=ADVANCED_FACE('',(#9158),#2564,.T.);
#91623=ADVANCED_FACE('',(#9159),#88130,.T.);
#91624=ADVANCED_FACE('',(#9160),#2565,.T.);
#91625=ADVANCED_FACE('',(#9161),#2566,.T.);
#91626=ADVANCED_FACE('',(#9162),#2567,.T.);
#91627=ADVANCED_FACE('',(#9163),#2568,.T.);
#91628=ADVANCED_FACE('',(#9164),#2569,.T.);
#91629=ADVANCED_FACE('',(#9165),#88131,.T.);
#91630=ADVANCED_FACE('',(#9166),#2570,.T.);
#91631=ADVANCED_FACE('',(#9167),#4940,.T.);
#91632=ADVANCED_FACE('',(#9168),#5791,.F.);
#91633=ADVANCED_FACE('',(#9169),#5792,.F.);
#91634=ADVANCED_FACE('',(#9170),#88132,.F.);
#91635=ADVANCED_FACE('',(#9171),#2571,.F.);
#91636=ADVANCED_FACE('',(#9172),#2572,.F.);
#91637=ADVANCED_FACE('',(#9173),#2573,.F.);
#91638=ADVANCED_FACE('',(#9174),#1991,.T.);
#91639=ADVANCED_FACE('',(#9175),#2574,.T.);
#91640=ADVANCED_FACE('',(#9176),#88133,.T.);
#91641=ADVANCED_FACE('',(#9177),#2575,.T.);
#91642=ADVANCED_FACE('',(#9178),#2576,.T.);
#91643=ADVANCED_FACE('',(#9179),#2577,.T.);
#91644=ADVANCED_FACE('',(#9180),#2578,.T.);
#91645=ADVANCED_FACE('',(#9181),#2579,.T.);
#91646=ADVANCED_FACE('',(#9182),#88134,.T.);
#91647=ADVANCED_FACE('',(#9183),#2580,.T.);
#91648=ADVANCED_FACE('',(#9184),#4941,.T.);
#91649=ADVANCED_FACE('',(#9185),#5793,.F.);
#91650=ADVANCED_FACE('',(#9186),#5794,.F.);
#91651=ADVANCED_FACE('',(#9187),#88135,.F.);
#91652=ADVANCED_FACE('',(#9188),#2581,.F.);
#91653=ADVANCED_FACE('',(#9189),#2582,.F.);
#91654=ADVANCED_FACE('',(#9190),#2583,.F.);
#91655=ADVANCED_FACE('',(#9191),#1992,.T.);
#91656=ADVANCED_FACE('',(#9192),#2584,.T.);
#91657=ADVANCED_FACE('',(#9193),#88136,.T.);
#91658=ADVANCED_FACE('',(#9194),#2585,.T.);
#91659=ADVANCED_FACE('',(#9195),#2586,.T.);
#91660=ADVANCED_FACE('',(#9196),#2587,.T.);
#91661=ADVANCED_FACE('',(#9197),#2588,.T.);
#91662=ADVANCED_FACE('',(#9198),#2589,.T.);
#91663=ADVANCED_FACE('',(#9199),#88137,.T.);
#91664=ADVANCED_FACE('',(#9200),#2590,.T.);
#91665=ADVANCED_FACE('',(#9201),#4942,.T.);
#91666=ADVANCED_FACE('',(#9202),#5795,.F.);
#91667=ADVANCED_FACE('',(#9203),#5796,.F.);
#91668=ADVANCED_FACE('',(#9204),#88138,.F.);
#91669=ADVANCED_FACE('',(#9205),#2591,.F.);
#91670=ADVANCED_FACE('',(#9206),#2592,.F.);
#91671=ADVANCED_FACE('',(#9207),#2593,.F.);
#91672=ADVANCED_FACE('',(#9208),#1993,.T.);
#91673=ADVANCED_FACE('',(#9209),#2594,.T.);
#91674=ADVANCED_FACE('',(#9210),#88139,.T.);
#91675=ADVANCED_FACE('',(#9211),#2595,.T.);
#91676=ADVANCED_FACE('',(#9212),#2596,.T.);
#91677=ADVANCED_FACE('',(#9213),#2597,.T.);
#91678=ADVANCED_FACE('',(#9214),#2598,.T.);
#91679=ADVANCED_FACE('',(#9215),#2599,.T.);
#91680=ADVANCED_FACE('',(#9216),#88140,.T.);
#91681=ADVANCED_FACE('',(#9217),#2600,.T.);
#91682=ADVANCED_FACE('',(#9218),#4943,.T.);
#91683=ADVANCED_FACE('',(#9219),#5797,.F.);
#91684=ADVANCED_FACE('',(#9220),#5798,.F.);
#91685=ADVANCED_FACE('',(#9221),#88141,.F.);
#91686=ADVANCED_FACE('',(#9222),#2601,.F.);
#91687=ADVANCED_FACE('',(#9223),#2602,.F.);
#91688=ADVANCED_FACE('',(#9224),#2603,.F.);
#91689=ADVANCED_FACE('',(#9225),#1994,.T.);
#91690=ADVANCED_FACE('',(#9226),#2604,.T.);
#91691=ADVANCED_FACE('',(#9227),#88142,.T.);
#91692=ADVANCED_FACE('',(#9228),#2605,.T.);
#91693=ADVANCED_FACE('',(#9229),#2606,.T.);
#91694=ADVANCED_FACE('',(#9230),#2607,.T.);
#91695=ADVANCED_FACE('',(#9231),#2608,.T.);
#91696=ADVANCED_FACE('',(#9232),#2609,.T.);
#91697=ADVANCED_FACE('',(#9233),#88143,.T.);
#91698=ADVANCED_FACE('',(#9234),#2610,.T.);
#91699=ADVANCED_FACE('',(#9235),#4944,.T.);
#91700=ADVANCED_FACE('',(#9236),#5799,.F.);
#91701=ADVANCED_FACE('',(#9237),#5800,.F.);
#91702=ADVANCED_FACE('',(#9238),#88144,.F.);
#91703=ADVANCED_FACE('',(#9239),#2611,.F.);
#91704=ADVANCED_FACE('',(#9240),#2612,.F.);
#91705=ADVANCED_FACE('',(#9241),#2613,.F.);
#91706=ADVANCED_FACE('',(#9242),#1995,.T.);
#91707=ADVANCED_FACE('',(#9243),#2614,.T.);
#91708=ADVANCED_FACE('',(#9244),#88145,.T.);
#91709=ADVANCED_FACE('',(#9245),#2615,.T.);
#91710=ADVANCED_FACE('',(#9246),#2616,.T.);
#91711=ADVANCED_FACE('',(#9247),#2617,.T.);
#91712=ADVANCED_FACE('',(#9248),#2618,.T.);
#91713=ADVANCED_FACE('',(#9249),#2619,.T.);
#91714=ADVANCED_FACE('',(#9250),#88146,.T.);
#91715=ADVANCED_FACE('',(#9251),#2620,.T.);
#91716=ADVANCED_FACE('',(#9252),#4945,.T.);
#91717=ADVANCED_FACE('',(#9253),#5801,.F.);
#91718=ADVANCED_FACE('',(#9254),#5802,.F.);
#91719=ADVANCED_FACE('',(#9255),#88147,.F.);
#91720=ADVANCED_FACE('',(#9256),#2621,.F.);
#91721=ADVANCED_FACE('',(#9257),#2622,.F.);
#91722=ADVANCED_FACE('',(#9258),#2623,.F.);
#91723=ADVANCED_FACE('',(#9259),#1996,.T.);
#91724=ADVANCED_FACE('',(#9260),#2624,.T.);
#91725=ADVANCED_FACE('',(#9261),#88148,.T.);
#91726=ADVANCED_FACE('',(#9262),#2625,.T.);
#91727=ADVANCED_FACE('',(#9263),#2626,.T.);
#91728=ADVANCED_FACE('',(#9264),#2627,.T.);
#91729=ADVANCED_FACE('',(#9265),#2628,.T.);
#91730=ADVANCED_FACE('',(#9266),#2629,.T.);
#91731=ADVANCED_FACE('',(#9267),#88149,.T.);
#91732=ADVANCED_FACE('',(#9268),#2630,.T.);
#91733=ADVANCED_FACE('',(#9269),#4946,.T.);
#91734=ADVANCED_FACE('',(#9270),#5803,.F.);
#91735=ADVANCED_FACE('',(#9271),#5804,.F.);
#91736=ADVANCED_FACE('',(#9272),#88150,.F.);
#91737=ADVANCED_FACE('',(#9273),#2631,.F.);
#91738=ADVANCED_FACE('',(#9274),#2632,.F.);
#91739=ADVANCED_FACE('',(#9275),#2633,.F.);
#91740=ADVANCED_FACE('',(#9276),#1997,.T.);
#91741=ADVANCED_FACE('',(#9277),#2634,.T.);
#91742=ADVANCED_FACE('',(#9278),#88151,.T.);
#91743=ADVANCED_FACE('',(#9279),#2635,.T.);
#91744=ADVANCED_FACE('',(#9280),#2636,.T.);
#91745=ADVANCED_FACE('',(#9281),#2637,.T.);
#91746=ADVANCED_FACE('',(#9282),#2638,.T.);
#91747=ADVANCED_FACE('',(#9283),#2639,.T.);
#91748=ADVANCED_FACE('',(#9284),#88152,.T.);
#91749=ADVANCED_FACE('',(#9285),#2640,.T.);
#91750=ADVANCED_FACE('',(#9286),#4947,.T.);
#91751=ADVANCED_FACE('',(#9287),#5805,.F.);
#91752=ADVANCED_FACE('',(#9288),#5806,.F.);
#91753=ADVANCED_FACE('',(#9289),#88153,.F.);
#91754=ADVANCED_FACE('',(#9290),#2641,.F.);
#91755=ADVANCED_FACE('',(#9291),#2642,.F.);
#91756=ADVANCED_FACE('',(#9292),#2643,.F.);
#91757=ADVANCED_FACE('',(#9293),#1998,.T.);
#91758=ADVANCED_FACE('',(#9294),#2644,.T.);
#91759=ADVANCED_FACE('',(#9295),#88154,.T.);
#91760=ADVANCED_FACE('',(#9296),#2645,.T.);
#91761=ADVANCED_FACE('',(#9297),#2646,.T.);
#91762=ADVANCED_FACE('',(#9298),#2647,.T.);
#91763=ADVANCED_FACE('',(#9299),#2648,.T.);
#91764=ADVANCED_FACE('',(#9300),#2649,.T.);
#91765=ADVANCED_FACE('',(#9301),#88155,.T.);
#91766=ADVANCED_FACE('',(#9302),#2650,.T.);
#91767=ADVANCED_FACE('',(#9303),#4948,.T.);
#91768=ADVANCED_FACE('',(#9304),#5807,.F.);
#91769=ADVANCED_FACE('',(#9305),#5808,.F.);
#91770=ADVANCED_FACE('',(#9306),#88156,.F.);
#91771=ADVANCED_FACE('',(#9307),#2651,.F.);
#91772=ADVANCED_FACE('',(#9308),#2652,.F.);
#91773=ADVANCED_FACE('',(#9309),#2653,.F.);
#91774=ADVANCED_FACE('',(#9310),#1999,.T.);
#91775=ADVANCED_FACE('',(#9311),#2654,.T.);
#91776=ADVANCED_FACE('',(#9312),#88157,.T.);
#91777=ADVANCED_FACE('',(#9313),#2655,.T.);
#91778=ADVANCED_FACE('',(#9314),#2656,.T.);
#91779=ADVANCED_FACE('',(#9315),#2657,.T.);
#91780=ADVANCED_FACE('',(#9316),#2658,.T.);
#91781=ADVANCED_FACE('',(#9317),#2659,.T.);
#91782=ADVANCED_FACE('',(#9318),#88158,.T.);
#91783=ADVANCED_FACE('',(#9319),#2660,.T.);
#91784=ADVANCED_FACE('',(#9320),#4949,.T.);
#91785=ADVANCED_FACE('',(#9321),#5809,.F.);
#91786=ADVANCED_FACE('',(#9322),#5810,.F.);
#91787=ADVANCED_FACE('',(#9323),#88159,.F.);
#91788=ADVANCED_FACE('',(#9324),#2661,.F.);
#91789=ADVANCED_FACE('',(#9325),#2662,.F.);
#91790=ADVANCED_FACE('',(#9326),#2663,.F.);
#91791=ADVANCED_FACE('',(#9327),#2000,.T.);
#91792=ADVANCED_FACE('',(#9328),#2664,.T.);
#91793=ADVANCED_FACE('',(#9329),#88160,.T.);
#91794=ADVANCED_FACE('',(#9330),#2665,.T.);
#91795=ADVANCED_FACE('',(#9331),#2666,.T.);
#91796=ADVANCED_FACE('',(#9332),#2667,.T.);
#91797=ADVANCED_FACE('',(#9333),#2668,.T.);
#91798=ADVANCED_FACE('',(#9334),#2669,.T.);
#91799=ADVANCED_FACE('',(#9335),#88161,.T.);
#91800=ADVANCED_FACE('',(#9336),#2670,.T.);
#91801=ADVANCED_FACE('',(#9337),#4950,.T.);
#91802=ADVANCED_FACE('',(#9338),#5811,.F.);
#91803=ADVANCED_FACE('',(#9339),#5812,.F.);
#91804=ADVANCED_FACE('',(#9340),#88162,.F.);
#91805=ADVANCED_FACE('',(#9341),#2671,.F.);
#91806=ADVANCED_FACE('',(#9342),#2672,.F.);
#91807=ADVANCED_FACE('',(#9343),#2673,.F.);
#91808=ADVANCED_FACE('',(#9344),#2001,.T.);
#91809=ADVANCED_FACE('',(#9345),#2674,.T.);
#91810=ADVANCED_FACE('',(#9346),#88163,.T.);
#91811=ADVANCED_FACE('',(#9347),#2675,.T.);
#91812=ADVANCED_FACE('',(#9348),#2676,.T.);
#91813=ADVANCED_FACE('',(#9349),#2677,.T.);
#91814=ADVANCED_FACE('',(#9350),#2678,.T.);
#91815=ADVANCED_FACE('',(#9351),#2679,.T.);
#91816=ADVANCED_FACE('',(#9352),#88164,.T.);
#91817=ADVANCED_FACE('',(#9353),#2680,.T.);
#91818=ADVANCED_FACE('',(#9354),#4951,.T.);
#91819=ADVANCED_FACE('',(#9355),#5813,.F.);
#91820=ADVANCED_FACE('',(#9356),#5814,.F.);
#91821=ADVANCED_FACE('',(#9357),#88165,.F.);
#91822=ADVANCED_FACE('',(#9358),#2681,.F.);
#91823=ADVANCED_FACE('',(#9359),#2682,.F.);
#91824=ADVANCED_FACE('',(#9360),#2683,.F.);
#91825=ADVANCED_FACE('',(#9361),#2002,.T.);
#91826=ADVANCED_FACE('',(#9362),#2684,.T.);
#91827=ADVANCED_FACE('',(#9363),#88166,.T.);
#91828=ADVANCED_FACE('',(#9364),#2685,.T.);
#91829=ADVANCED_FACE('',(#9365),#2686,.T.);
#91830=ADVANCED_FACE('',(#9366),#2687,.T.);
#91831=ADVANCED_FACE('',(#9367),#2688,.T.);
#91832=ADVANCED_FACE('',(#9368),#2689,.T.);
#91833=ADVANCED_FACE('',(#9369),#88167,.T.);
#91834=ADVANCED_FACE('',(#9370),#2690,.T.);
#91835=ADVANCED_FACE('',(#9371),#4952,.T.);
#91836=ADVANCED_FACE('',(#9372),#5815,.F.);
#91837=ADVANCED_FACE('',(#9373),#5816,.F.);
#91838=ADVANCED_FACE('',(#9374),#88168,.F.);
#91839=ADVANCED_FACE('',(#9375),#2691,.F.);
#91840=ADVANCED_FACE('',(#9376),#2692,.F.);
#91841=ADVANCED_FACE('',(#9377),#2693,.F.);
#91842=ADVANCED_FACE('',(#9378),#2003,.T.);
#91843=ADVANCED_FACE('',(#9379),#2694,.T.);
#91844=ADVANCED_FACE('',(#9380),#88169,.T.);
#91845=ADVANCED_FACE('',(#9381),#2695,.T.);
#91846=ADVANCED_FACE('',(#9382),#2696,.T.);
#91847=ADVANCED_FACE('',(#9383),#2697,.T.);
#91848=ADVANCED_FACE('',(#9384),#2698,.T.);
#91849=ADVANCED_FACE('',(#9385),#2699,.T.);
#91850=ADVANCED_FACE('',(#9386),#88170,.T.);
#91851=ADVANCED_FACE('',(#9387),#2700,.T.);
#91852=ADVANCED_FACE('',(#9388),#4953,.T.);
#91853=ADVANCED_FACE('',(#9389),#5817,.F.);
#91854=ADVANCED_FACE('',(#9390),#5818,.F.);
#91855=ADVANCED_FACE('',(#9391),#88171,.F.);
#91856=ADVANCED_FACE('',(#9392),#2701,.F.);
#91857=ADVANCED_FACE('',(#9393),#2702,.F.);
#91858=ADVANCED_FACE('',(#9394),#2703,.F.);
#91859=ADVANCED_FACE('',(#9395),#2004,.T.);
#91860=ADVANCED_FACE('',(#9396),#2704,.T.);
#91861=ADVANCED_FACE('',(#9397),#88172,.T.);
#91862=ADVANCED_FACE('',(#9398),#2705,.T.);
#91863=ADVANCED_FACE('',(#9399),#2706,.T.);
#91864=ADVANCED_FACE('',(#9400),#2707,.T.);
#91865=ADVANCED_FACE('',(#9401),#2708,.T.);
#91866=ADVANCED_FACE('',(#9402),#2709,.T.);
#91867=ADVANCED_FACE('',(#9403),#88173,.T.);
#91868=ADVANCED_FACE('',(#9404),#2710,.T.);
#91869=ADVANCED_FACE('',(#9405),#4954,.T.);
#91870=ADVANCED_FACE('',(#9406),#5819,.F.);
#91871=ADVANCED_FACE('',(#9407),#5820,.F.);
#91872=ADVANCED_FACE('',(#9408),#88174,.F.);
#91873=ADVANCED_FACE('',(#9409),#2711,.F.);
#91874=ADVANCED_FACE('',(#9410),#2712,.F.);
#91875=ADVANCED_FACE('',(#9411),#2713,.F.);
#91876=ADVANCED_FACE('',(#9412),#2005,.T.);
#91877=ADVANCED_FACE('',(#9413),#2714,.T.);
#91878=ADVANCED_FACE('',(#9414),#88175,.T.);
#91879=ADVANCED_FACE('',(#9415),#2715,.T.);
#91880=ADVANCED_FACE('',(#9416),#2716,.T.);
#91881=ADVANCED_FACE('',(#9417),#2717,.T.);
#91882=ADVANCED_FACE('',(#9418),#2718,.T.);
#91883=ADVANCED_FACE('',(#9419),#2719,.T.);
#91884=ADVANCED_FACE('',(#9420),#88176,.T.);
#91885=ADVANCED_FACE('',(#9421),#2720,.T.);
#91886=ADVANCED_FACE('',(#9422),#4955,.T.);
#91887=ADVANCED_FACE('',(#9423),#5821,.F.);
#91888=ADVANCED_FACE('',(#9424),#5822,.F.);
#91889=ADVANCED_FACE('',(#9425),#88177,.F.);
#91890=ADVANCED_FACE('',(#9426),#2721,.F.);
#91891=ADVANCED_FACE('',(#9427),#2722,.F.);
#91892=ADVANCED_FACE('',(#9428),#2723,.F.);
#91893=ADVANCED_FACE('',(#9429),#2006,.T.);
#91894=ADVANCED_FACE('',(#9430),#2724,.T.);
#91895=ADVANCED_FACE('',(#9431),#88178,.T.);
#91896=ADVANCED_FACE('',(#9432),#2725,.T.);
#91897=ADVANCED_FACE('',(#9433),#2726,.T.);
#91898=ADVANCED_FACE('',(#9434),#2727,.T.);
#91899=ADVANCED_FACE('',(#9435),#2728,.T.);
#91900=ADVANCED_FACE('',(#9436),#2729,.T.);
#91901=ADVANCED_FACE('',(#9437),#88179,.T.);
#91902=ADVANCED_FACE('',(#9438),#2730,.T.);
#91903=ADVANCED_FACE('',(#9439),#4956,.T.);
#91904=ADVANCED_FACE('',(#9440),#5823,.F.);
#91905=ADVANCED_FACE('',(#9441),#5824,.F.);
#91906=ADVANCED_FACE('',(#9442),#88180,.F.);
#91907=ADVANCED_FACE('',(#9443),#2731,.F.);
#91908=ADVANCED_FACE('',(#9444),#2732,.F.);
#91909=ADVANCED_FACE('',(#9445),#2733,.F.);
#91910=ADVANCED_FACE('',(#9446),#2007,.T.);
#91911=ADVANCED_FACE('',(#9447),#2734,.T.);
#91912=ADVANCED_FACE('',(#9448),#88181,.T.);
#91913=ADVANCED_FACE('',(#9449),#2735,.T.);
#91914=ADVANCED_FACE('',(#9450),#2736,.T.);
#91915=ADVANCED_FACE('',(#9451),#2737,.T.);
#91916=ADVANCED_FACE('',(#9452),#2738,.T.);
#91917=ADVANCED_FACE('',(#9453),#2739,.T.);
#91918=ADVANCED_FACE('',(#9454),#88182,.T.);
#91919=ADVANCED_FACE('',(#9455),#2740,.T.);
#91920=ADVANCED_FACE('',(#9456),#4957,.T.);
#91921=ADVANCED_FACE('',(#9457),#5825,.F.);
#91922=ADVANCED_FACE('',(#9458),#5826,.F.);
#91923=ADVANCED_FACE('',(#9459),#88183,.F.);
#91924=ADVANCED_FACE('',(#9460),#2741,.F.);
#91925=ADVANCED_FACE('',(#9461),#2742,.F.);
#91926=ADVANCED_FACE('',(#9462),#2743,.F.);
#91927=ADVANCED_FACE('',(#9463),#2008,.T.);
#91928=ADVANCED_FACE('',(#9464),#2744,.T.);
#91929=ADVANCED_FACE('',(#9465),#88184,.T.);
#91930=ADVANCED_FACE('',(#9466),#2745,.T.);
#91931=ADVANCED_FACE('',(#9467),#2746,.T.);
#91932=ADVANCED_FACE('',(#9468),#2747,.T.);
#91933=ADVANCED_FACE('',(#9469),#2748,.T.);
#91934=ADVANCED_FACE('',(#9470),#2749,.T.);
#91935=ADVANCED_FACE('',(#9471),#88185,.T.);
#91936=ADVANCED_FACE('',(#9472),#2750,.T.);
#91937=ADVANCED_FACE('',(#9473),#4958,.T.);
#91938=ADVANCED_FACE('',(#9474),#5827,.F.);
#91939=ADVANCED_FACE('',(#9475),#5828,.F.);
#91940=ADVANCED_FACE('',(#9476),#88186,.F.);
#91941=ADVANCED_FACE('',(#9477),#2751,.F.);
#91942=ADVANCED_FACE('',(#9478),#2752,.F.);
#91943=ADVANCED_FACE('',(#9479),#2753,.F.);
#91944=ADVANCED_FACE('',(#9480),#2009,.T.);
#91945=ADVANCED_FACE('',(#9481),#2754,.T.);
#91946=ADVANCED_FACE('',(#9482),#88187,.T.);
#91947=ADVANCED_FACE('',(#9483),#2755,.T.);
#91948=ADVANCED_FACE('',(#9484),#2756,.T.);
#91949=ADVANCED_FACE('',(#9485),#2757,.T.);
#91950=ADVANCED_FACE('',(#9486),#2758,.T.);
#91951=ADVANCED_FACE('',(#9487),#2759,.T.);
#91952=ADVANCED_FACE('',(#9488),#88188,.T.);
#91953=ADVANCED_FACE('',(#9489),#2760,.T.);
#91954=ADVANCED_FACE('',(#9490),#4959,.T.);
#91955=ADVANCED_FACE('',(#9491),#5829,.F.);
#91956=ADVANCED_FACE('',(#9492),#5830,.F.);
#91957=ADVANCED_FACE('',(#9493),#88189,.F.);
#91958=ADVANCED_FACE('',(#9494),#2761,.F.);
#91959=ADVANCED_FACE('',(#9495),#2762,.F.);
#91960=ADVANCED_FACE('',(#9496),#2763,.F.);
#91961=ADVANCED_FACE('',(#9497),#2010,.T.);
#91962=ADVANCED_FACE('',(#9498),#2764,.T.);
#91963=ADVANCED_FACE('',(#9499),#88190,.T.);
#91964=ADVANCED_FACE('',(#9500),#2765,.T.);
#91965=ADVANCED_FACE('',(#9501),#2766,.T.);
#91966=ADVANCED_FACE('',(#9502),#2767,.T.);
#91967=ADVANCED_FACE('',(#9503),#2768,.T.);
#91968=ADVANCED_FACE('',(#9504),#2769,.T.);
#91969=ADVANCED_FACE('',(#9505),#88191,.T.);
#91970=ADVANCED_FACE('',(#9506),#2770,.T.);
#91971=ADVANCED_FACE('',(#9507),#4960,.T.);
#91972=ADVANCED_FACE('',(#9508),#5831,.F.);
#91973=ADVANCED_FACE('',(#9509),#5832,.F.);
#91974=ADVANCED_FACE('',(#9510),#88192,.F.);
#91975=ADVANCED_FACE('',(#9511),#2771,.F.);
#91976=ADVANCED_FACE('',(#9512),#2772,.F.);
#91977=ADVANCED_FACE('',(#9513),#2773,.F.);
#91978=ADVANCED_FACE('',(#9514),#2011,.T.);
#91979=ADVANCED_FACE('',(#9515),#2774,.T.);
#91980=ADVANCED_FACE('',(#9516),#88193,.T.);
#91981=ADVANCED_FACE('',(#9517),#2775,.T.);
#91982=ADVANCED_FACE('',(#9518),#2776,.T.);
#91983=ADVANCED_FACE('',(#9519),#2777,.T.);
#91984=ADVANCED_FACE('',(#9520),#2778,.T.);
#91985=ADVANCED_FACE('',(#9521),#2779,.T.);
#91986=ADVANCED_FACE('',(#9522),#88194,.T.);
#91987=ADVANCED_FACE('',(#9523),#2780,.T.);
#91988=ADVANCED_FACE('',(#9524),#4961,.T.);
#91989=ADVANCED_FACE('',(#9525),#5833,.F.);
#91990=ADVANCED_FACE('',(#9526),#5834,.F.);
#91991=ADVANCED_FACE('',(#9527),#88195,.F.);
#91992=ADVANCED_FACE('',(#9528),#2781,.F.);
#91993=ADVANCED_FACE('',(#9529),#2782,.F.);
#91994=ADVANCED_FACE('',(#9530),#2783,.F.);
#91995=ADVANCED_FACE('',(#9531),#2012,.T.);
#91996=ADVANCED_FACE('',(#9532),#2784,.T.);
#91997=ADVANCED_FACE('',(#9533),#88196,.T.);
#91998=ADVANCED_FACE('',(#9534),#2785,.T.);
#91999=ADVANCED_FACE('',(#9535),#2786,.T.);
#92000=ADVANCED_FACE('',(#9536),#2787,.T.);
#92001=ADVANCED_FACE('',(#9537),#2788,.T.);
#92002=ADVANCED_FACE('',(#9538),#2789,.T.);
#92003=ADVANCED_FACE('',(#9539),#88197,.T.);
#92004=ADVANCED_FACE('',(#9540),#2790,.T.);
#92005=ADVANCED_FACE('',(#9541),#4962,.T.);
#92006=ADVANCED_FACE('',(#9542),#5835,.F.);
#92007=ADVANCED_FACE('',(#9543),#5836,.F.);
#92008=ADVANCED_FACE('',(#9544),#88198,.F.);
#92009=ADVANCED_FACE('',(#9545),#2791,.F.);
#92010=ADVANCED_FACE('',(#9546),#2792,.F.);
#92011=ADVANCED_FACE('',(#9547),#2793,.F.);
#92012=ADVANCED_FACE('',(#9548),#2013,.T.);
#92013=ADVANCED_FACE('',(#9549),#2794,.T.);
#92014=ADVANCED_FACE('',(#9550),#88199,.T.);
#92015=ADVANCED_FACE('',(#9551),#2795,.T.);
#92016=ADVANCED_FACE('',(#9552),#2796,.T.);
#92017=ADVANCED_FACE('',(#9553),#2797,.T.);
#92018=ADVANCED_FACE('',(#9554),#2798,.T.);
#92019=ADVANCED_FACE('',(#9555),#2799,.T.);
#92020=ADVANCED_FACE('',(#9556),#88200,.T.);
#92021=ADVANCED_FACE('',(#9557),#2800,.T.);
#92022=ADVANCED_FACE('',(#9558),#4963,.T.);
#92023=ADVANCED_FACE('',(#9559),#5837,.F.);
#92024=ADVANCED_FACE('',(#9560),#5838,.F.);
#92025=ADVANCED_FACE('',(#9561),#88201,.F.);
#92026=ADVANCED_FACE('',(#9562),#2801,.F.);
#92027=ADVANCED_FACE('',(#9563),#2802,.F.);
#92028=ADVANCED_FACE('',(#9564),#2803,.F.);
#92029=ADVANCED_FACE('',(#9565),#2014,.T.);
#92030=ADVANCED_FACE('',(#9566),#2804,.T.);
#92031=ADVANCED_FACE('',(#9567),#88202,.T.);
#92032=ADVANCED_FACE('',(#9568),#2805,.T.);
#92033=ADVANCED_FACE('',(#9569),#2806,.T.);
#92034=ADVANCED_FACE('',(#9570),#2807,.T.);
#92035=ADVANCED_FACE('',(#9571),#2808,.T.);
#92036=ADVANCED_FACE('',(#9572),#2809,.T.);
#92037=ADVANCED_FACE('',(#9573),#88203,.T.);
#92038=ADVANCED_FACE('',(#9574),#2810,.T.);
#92039=ADVANCED_FACE('',(#9575),#4964,.T.);
#92040=ADVANCED_FACE('',(#9576),#5839,.F.);
#92041=ADVANCED_FACE('',(#9577),#5840,.F.);
#92042=ADVANCED_FACE('',(#9578),#88204,.F.);
#92043=ADVANCED_FACE('',(#9579),#2811,.F.);
#92044=ADVANCED_FACE('',(#9580),#2812,.F.);
#92045=ADVANCED_FACE('',(#9581),#2813,.F.);
#92046=ADVANCED_FACE('',(#9582),#2015,.T.);
#92047=ADVANCED_FACE('',(#9583),#2814,.T.);
#92048=ADVANCED_FACE('',(#9584),#88205,.T.);
#92049=ADVANCED_FACE('',(#9585),#2815,.T.);
#92050=ADVANCED_FACE('',(#9586),#2816,.T.);
#92051=ADVANCED_FACE('',(#9587),#2817,.T.);
#92052=ADVANCED_FACE('',(#9588),#2818,.T.);
#92053=ADVANCED_FACE('',(#9589),#2819,.T.);
#92054=ADVANCED_FACE('',(#9590),#88206,.T.);
#92055=ADVANCED_FACE('',(#9591),#2820,.T.);
#92056=ADVANCED_FACE('',(#9592),#4965,.T.);
#92057=ADVANCED_FACE('',(#9593),#5841,.F.);
#92058=ADVANCED_FACE('',(#9594),#5842,.F.);
#92059=ADVANCED_FACE('',(#9595),#88207,.F.);
#92060=ADVANCED_FACE('',(#9596),#2821,.F.);
#92061=ADVANCED_FACE('',(#9597),#2822,.F.);
#92062=ADVANCED_FACE('',(#9598),#2823,.F.);
#92063=ADVANCED_FACE('',(#9599),#2016,.T.);
#92064=ADVANCED_FACE('',(#9600),#2824,.T.);
#92065=ADVANCED_FACE('',(#9601),#88208,.T.);
#92066=ADVANCED_FACE('',(#9602),#2825,.T.);
#92067=ADVANCED_FACE('',(#9603),#2826,.T.);
#92068=ADVANCED_FACE('',(#9604),#2827,.T.);
#92069=ADVANCED_FACE('',(#9605),#2828,.T.);
#92070=ADVANCED_FACE('',(#9606),#2829,.T.);
#92071=ADVANCED_FACE('',(#9607),#88209,.T.);
#92072=ADVANCED_FACE('',(#9608),#2830,.T.);
#92073=ADVANCED_FACE('',(#9609),#4966,.T.);
#92074=ADVANCED_FACE('',(#9610),#5843,.F.);
#92075=ADVANCED_FACE('',(#9611),#5844,.F.);
#92076=ADVANCED_FACE('',(#9612),#88210,.F.);
#92077=ADVANCED_FACE('',(#9613),#2831,.F.);
#92078=ADVANCED_FACE('',(#9614),#2832,.F.);
#92079=ADVANCED_FACE('',(#9615),#2833,.F.);
#92080=ADVANCED_FACE('',(#9616),#2017,.T.);
#92081=ADVANCED_FACE('',(#9617),#2834,.T.);
#92082=ADVANCED_FACE('',(#9618),#88211,.T.);
#92083=ADVANCED_FACE('',(#9619),#2835,.T.);
#92084=ADVANCED_FACE('',(#9620),#2836,.T.);
#92085=ADVANCED_FACE('',(#9621),#2837,.T.);
#92086=ADVANCED_FACE('',(#9622),#2838,.T.);
#92087=ADVANCED_FACE('',(#9623),#2839,.T.);
#92088=ADVANCED_FACE('',(#9624),#88212,.T.);
#92089=ADVANCED_FACE('',(#9625),#2840,.T.);
#92090=ADVANCED_FACE('',(#9626),#4967,.T.);
#92091=ADVANCED_FACE('',(#9627),#5845,.F.);
#92092=ADVANCED_FACE('',(#9628),#5846,.F.);
#92093=ADVANCED_FACE('',(#9629),#88213,.F.);
#92094=ADVANCED_FACE('',(#9630),#2841,.F.);
#92095=ADVANCED_FACE('',(#9631),#2842,.F.);
#92096=ADVANCED_FACE('',(#9632),#2843,.F.);
#92097=ADVANCED_FACE('',(#9633),#2018,.T.);
#92098=ADVANCED_FACE('',(#9634),#2844,.T.);
#92099=ADVANCED_FACE('',(#9635),#88214,.T.);
#92100=ADVANCED_FACE('',(#9636),#2845,.T.);
#92101=ADVANCED_FACE('',(#9637),#2846,.T.);
#92102=ADVANCED_FACE('',(#9638),#2847,.T.);
#92103=ADVANCED_FACE('',(#9639),#2848,.T.);
#92104=ADVANCED_FACE('',(#9640),#2849,.T.);
#92105=ADVANCED_FACE('',(#9641),#88215,.T.);
#92106=ADVANCED_FACE('',(#9642),#2850,.T.);
#92107=ADVANCED_FACE('',(#9643),#4968,.T.);
#92108=ADVANCED_FACE('',(#9644),#5847,.F.);
#92109=ADVANCED_FACE('',(#9645),#5848,.F.);
#92110=ADVANCED_FACE('',(#9646),#88216,.F.);
#92111=ADVANCED_FACE('',(#9647),#2851,.F.);
#92112=ADVANCED_FACE('',(#9648),#2852,.F.);
#92113=ADVANCED_FACE('',(#9649),#2853,.F.);
#92114=ADVANCED_FACE('',(#9650),#2019,.T.);
#92115=ADVANCED_FACE('',(#9651),#2854,.T.);
#92116=ADVANCED_FACE('',(#9652),#88217,.T.);
#92117=ADVANCED_FACE('',(#9653),#2855,.T.);
#92118=ADVANCED_FACE('',(#9654),#2856,.T.);
#92119=ADVANCED_FACE('',(#9655),#2857,.T.);
#92120=ADVANCED_FACE('',(#9656),#2858,.T.);
#92121=ADVANCED_FACE('',(#9657),#2859,.T.);
#92122=ADVANCED_FACE('',(#9658),#88218,.T.);
#92123=ADVANCED_FACE('',(#9659),#2860,.T.);
#92124=ADVANCED_FACE('',(#9660),#4969,.T.);
#92125=ADVANCED_FACE('',(#9661),#5849,.F.);
#92126=ADVANCED_FACE('',(#9662),#5850,.F.);
#92127=ADVANCED_FACE('',(#9663),#88219,.F.);
#92128=ADVANCED_FACE('',(#9664),#2861,.F.);
#92129=ADVANCED_FACE('',(#9665),#2862,.F.);
#92130=ADVANCED_FACE('',(#9666),#2863,.F.);
#92131=ADVANCED_FACE('',(#9667),#2020,.T.);
#92132=ADVANCED_FACE('',(#9668),#2864,.T.);
#92133=ADVANCED_FACE('',(#9669),#88220,.T.);
#92134=ADVANCED_FACE('',(#9670),#2865,.T.);
#92135=ADVANCED_FACE('',(#9671),#2866,.T.);
#92136=ADVANCED_FACE('',(#9672),#2867,.T.);
#92137=ADVANCED_FACE('',(#9673),#2868,.T.);
#92138=ADVANCED_FACE('',(#9674),#2869,.T.);
#92139=ADVANCED_FACE('',(#9675),#88221,.T.);
#92140=ADVANCED_FACE('',(#9676),#2870,.T.);
#92141=ADVANCED_FACE('',(#9677),#4970,.T.);
#92142=ADVANCED_FACE('',(#9678),#5851,.F.);
#92143=ADVANCED_FACE('',(#9679),#5852,.F.);
#92144=ADVANCED_FACE('',(#9680),#88222,.F.);
#92145=ADVANCED_FACE('',(#9681),#2871,.F.);
#92146=ADVANCED_FACE('',(#9682),#2872,.F.);
#92147=ADVANCED_FACE('',(#9683),#2873,.F.);
#92148=ADVANCED_FACE('',(#9684),#2021,.T.);
#92149=ADVANCED_FACE('',(#9685),#2874,.T.);
#92150=ADVANCED_FACE('',(#9686),#88223,.T.);
#92151=ADVANCED_FACE('',(#9687),#2875,.T.);
#92152=ADVANCED_FACE('',(#9688),#2876,.T.);
#92153=ADVANCED_FACE('',(#9689),#2877,.T.);
#92154=ADVANCED_FACE('',(#9690),#2878,.T.);
#92155=ADVANCED_FACE('',(#9691),#2879,.T.);
#92156=ADVANCED_FACE('',(#9692),#88224,.T.);
#92157=ADVANCED_FACE('',(#9693),#2880,.T.);
#92158=ADVANCED_FACE('',(#9694),#4971,.T.);
#92159=ADVANCED_FACE('',(#9695),#5853,.F.);
#92160=ADVANCED_FACE('',(#9696),#5854,.F.);
#92161=ADVANCED_FACE('',(#9697),#88225,.F.);
#92162=ADVANCED_FACE('',(#9698),#2881,.F.);
#92163=ADVANCED_FACE('',(#9699),#2882,.F.);
#92164=ADVANCED_FACE('',(#9700),#2883,.F.);
#92165=ADVANCED_FACE('',(#9701),#2022,.T.);
#92166=ADVANCED_FACE('',(#9702),#2884,.T.);
#92167=ADVANCED_FACE('',(#9703),#88226,.T.);
#92168=ADVANCED_FACE('',(#9704),#2885,.T.);
#92169=ADVANCED_FACE('',(#9705),#2886,.T.);
#92170=ADVANCED_FACE('',(#9706),#2887,.T.);
#92171=ADVANCED_FACE('',(#9707),#2888,.T.);
#92172=ADVANCED_FACE('',(#9708),#2889,.T.);
#92173=ADVANCED_FACE('',(#9709),#88227,.T.);
#92174=ADVANCED_FACE('',(#9710),#2890,.T.);
#92175=ADVANCED_FACE('',(#9711),#4972,.T.);
#92176=ADVANCED_FACE('',(#9712),#5855,.F.);
#92177=ADVANCED_FACE('',(#9713),#5856,.F.);
#92178=ADVANCED_FACE('',(#9714),#88228,.F.);
#92179=ADVANCED_FACE('',(#9715),#2891,.F.);
#92180=ADVANCED_FACE('',(#9716),#2892,.F.);
#92181=ADVANCED_FACE('',(#9717),#2893,.F.);
#92182=ADVANCED_FACE('',(#9718),#2023,.T.);
#92183=ADVANCED_FACE('',(#9719),#2894,.T.);
#92184=ADVANCED_FACE('',(#9720),#88229,.T.);
#92185=ADVANCED_FACE('',(#9721),#2895,.T.);
#92186=ADVANCED_FACE('',(#9722),#2896,.T.);
#92187=ADVANCED_FACE('',(#9723),#2897,.T.);
#92188=ADVANCED_FACE('',(#9724),#2898,.T.);
#92189=ADVANCED_FACE('',(#9725),#2899,.T.);
#92190=ADVANCED_FACE('',(#9726),#88230,.T.);
#92191=ADVANCED_FACE('',(#9727),#2900,.T.);
#92192=ADVANCED_FACE('',(#9728),#4973,.T.);
#92193=ADVANCED_FACE('',(#9729),#5857,.F.);
#92194=ADVANCED_FACE('',(#9730),#5858,.F.);
#92195=ADVANCED_FACE('',(#9731),#88231,.F.);
#92196=ADVANCED_FACE('',(#9732),#2901,.F.);
#92197=ADVANCED_FACE('',(#9733),#2902,.F.);
#92198=ADVANCED_FACE('',(#9734),#2903,.F.);
#92199=ADVANCED_FACE('',(#9735),#2024,.T.);
#92200=ADVANCED_FACE('',(#9736),#2904,.T.);
#92201=ADVANCED_FACE('',(#9737),#88232,.T.);
#92202=ADVANCED_FACE('',(#9738),#2905,.T.);
#92203=ADVANCED_FACE('',(#9739),#2906,.T.);
#92204=ADVANCED_FACE('',(#9740),#2907,.T.);
#92205=ADVANCED_FACE('',(#9741),#2908,.T.);
#92206=ADVANCED_FACE('',(#9742),#2909,.T.);
#92207=ADVANCED_FACE('',(#9743),#88233,.T.);
#92208=ADVANCED_FACE('',(#9744),#2910,.T.);
#92209=ADVANCED_FACE('',(#9745),#4974,.T.);
#92210=ADVANCED_FACE('',(#9746),#5859,.F.);
#92211=ADVANCED_FACE('',(#9747),#5860,.F.);
#92212=ADVANCED_FACE('',(#9748),#88234,.F.);
#92213=ADVANCED_FACE('',(#9749),#2911,.F.);
#92214=ADVANCED_FACE('',(#9750),#2912,.F.);
#92215=ADVANCED_FACE('',(#9751),#2913,.F.);
#92216=ADVANCED_FACE('',(#9752),#2025,.T.);
#92217=ADVANCED_FACE('',(#9753),#2914,.T.);
#92218=ADVANCED_FACE('',(#9754),#88235,.T.);
#92219=ADVANCED_FACE('',(#9755),#2915,.T.);
#92220=ADVANCED_FACE('',(#9756),#2916,.T.);
#92221=ADVANCED_FACE('',(#9757),#2917,.T.);
#92222=ADVANCED_FACE('',(#9758),#2918,.T.);
#92223=ADVANCED_FACE('',(#9759),#2919,.T.);
#92224=ADVANCED_FACE('',(#9760),#88236,.T.);
#92225=ADVANCED_FACE('',(#9761),#2920,.T.);
#92226=ADVANCED_FACE('',(#9762),#4975,.T.);
#92227=ADVANCED_FACE('',(#9763),#5861,.F.);
#92228=ADVANCED_FACE('',(#9764),#5862,.F.);
#92229=ADVANCED_FACE('',(#9765),#88237,.F.);
#92230=ADVANCED_FACE('',(#9766),#2921,.F.);
#92231=ADVANCED_FACE('',(#9767),#2922,.F.);
#92232=ADVANCED_FACE('',(#9768),#2923,.F.);
#92233=ADVANCED_FACE('',(#9769),#2026,.T.);
#92234=ADVANCED_FACE('',(#9770),#2924,.T.);
#92235=ADVANCED_FACE('',(#9771),#88238,.T.);
#92236=ADVANCED_FACE('',(#9772),#2925,.T.);
#92237=ADVANCED_FACE('',(#9773),#2926,.T.);
#92238=ADVANCED_FACE('',(#9774),#2927,.T.);
#92239=ADVANCED_FACE('',(#9775),#2928,.T.);
#92240=ADVANCED_FACE('',(#9776),#2929,.T.);
#92241=ADVANCED_FACE('',(#9777),#88239,.T.);
#92242=ADVANCED_FACE('',(#9778),#2930,.T.);
#92243=ADVANCED_FACE('',(#9779),#4976,.T.);
#92244=ADVANCED_FACE('',(#9780),#5863,.F.);
#92245=ADVANCED_FACE('',(#9781),#5864,.F.);
#92246=ADVANCED_FACE('',(#9782),#88240,.F.);
#92247=ADVANCED_FACE('',(#9783),#2931,.F.);
#92248=ADVANCED_FACE('',(#9784),#2932,.F.);
#92249=ADVANCED_FACE('',(#9785),#2933,.F.);
#92250=ADVANCED_FACE('',(#9786),#2027,.T.);
#92251=ADVANCED_FACE('',(#9787),#2934,.T.);
#92252=ADVANCED_FACE('',(#9788),#88241,.T.);
#92253=ADVANCED_FACE('',(#9789),#2935,.T.);
#92254=ADVANCED_FACE('',(#9790),#2936,.T.);
#92255=ADVANCED_FACE('',(#9791),#2937,.T.);
#92256=ADVANCED_FACE('',(#9792),#2938,.T.);
#92257=ADVANCED_FACE('',(#9793),#2939,.T.);
#92258=ADVANCED_FACE('',(#9794),#88242,.T.);
#92259=ADVANCED_FACE('',(#9795),#2940,.T.);
#92260=ADVANCED_FACE('',(#9796),#4977,.T.);
#92261=ADVANCED_FACE('',(#9797),#5865,.F.);
#92262=ADVANCED_FACE('',(#9798),#5866,.F.);
#92263=ADVANCED_FACE('',(#9799),#88243,.F.);
#92264=ADVANCED_FACE('',(#9800),#2941,.F.);
#92265=ADVANCED_FACE('',(#9801),#2942,.F.);
#92266=ADVANCED_FACE('',(#9802),#2943,.F.);
#92267=ADVANCED_FACE('',(#9803),#2028,.T.);
#92268=ADVANCED_FACE('',(#9804),#2944,.T.);
#92269=ADVANCED_FACE('',(#9805),#88244,.T.);
#92270=ADVANCED_FACE('',(#9806),#2945,.T.);
#92271=ADVANCED_FACE('',(#9807),#2946,.T.);
#92272=ADVANCED_FACE('',(#9808),#2947,.T.);
#92273=ADVANCED_FACE('',(#9809),#2948,.T.);
#92274=ADVANCED_FACE('',(#9810),#2949,.T.);
#92275=ADVANCED_FACE('',(#9811),#88245,.T.);
#92276=ADVANCED_FACE('',(#9812),#2950,.T.);
#92277=ADVANCED_FACE('',(#9813),#4978,.T.);
#92278=ADVANCED_FACE('',(#9814),#5867,.F.);
#92279=ADVANCED_FACE('',(#9815),#5868,.F.);
#92280=ADVANCED_FACE('',(#9816),#88246,.F.);
#92281=ADVANCED_FACE('',(#9817),#2951,.F.);
#92282=ADVANCED_FACE('',(#9818),#2952,.F.);
#92283=ADVANCED_FACE('',(#9819),#2953,.F.);
#92284=ADVANCED_FACE('',(#9820),#2029,.T.);
#92285=ADVANCED_FACE('',(#9821),#2954,.T.);
#92286=ADVANCED_FACE('',(#9822),#88247,.T.);
#92287=ADVANCED_FACE('',(#9823),#2955,.T.);
#92288=ADVANCED_FACE('',(#9824),#2956,.T.);
#92289=ADVANCED_FACE('',(#9825),#2957,.T.);
#92290=ADVANCED_FACE('',(#9826),#2958,.T.);
#92291=ADVANCED_FACE('',(#9827),#2959,.T.);
#92292=ADVANCED_FACE('',(#9828),#88248,.T.);
#92293=ADVANCED_FACE('',(#9829),#2960,.T.);
#92294=ADVANCED_FACE('',(#9830),#4979,.T.);
#92295=ADVANCED_FACE('',(#9831),#5869,.F.);
#92296=ADVANCED_FACE('',(#9832),#5870,.F.);
#92297=ADVANCED_FACE('',(#9833),#88249,.F.);
#92298=ADVANCED_FACE('',(#9834),#2961,.F.);
#92299=ADVANCED_FACE('',(#9835),#2962,.F.);
#92300=ADVANCED_FACE('',(#9836),#2963,.F.);
#92301=ADVANCED_FACE('',(#9837),#2030,.T.);
#92302=ADVANCED_FACE('',(#9838),#2964,.T.);
#92303=ADVANCED_FACE('',(#9839),#88250,.T.);
#92304=ADVANCED_FACE('',(#9840),#2965,.T.);
#92305=ADVANCED_FACE('',(#9841),#2966,.T.);
#92306=ADVANCED_FACE('',(#9842),#2967,.T.);
#92307=ADVANCED_FACE('',(#9843),#2968,.T.);
#92308=ADVANCED_FACE('',(#9844),#2969,.T.);
#92309=ADVANCED_FACE('',(#9845),#88251,.T.);
#92310=ADVANCED_FACE('',(#9846),#2970,.T.);
#92311=ADVANCED_FACE('',(#9847),#4980,.T.);
#92312=ADVANCED_FACE('',(#9848),#5871,.F.);
#92313=ADVANCED_FACE('',(#9849),#5872,.F.);
#92314=ADVANCED_FACE('',(#9850),#88252,.F.);
#92315=ADVANCED_FACE('',(#9851),#2971,.F.);
#92316=ADVANCED_FACE('',(#9852),#2972,.F.);
#92317=ADVANCED_FACE('',(#9853),#2973,.F.);
#92318=ADVANCED_FACE('',(#9854),#2031,.T.);
#92319=ADVANCED_FACE('',(#9855),#2974,.T.);
#92320=ADVANCED_FACE('',(#9856),#88253,.T.);
#92321=ADVANCED_FACE('',(#9857),#2975,.T.);
#92322=ADVANCED_FACE('',(#9858),#2976,.T.);
#92323=ADVANCED_FACE('',(#9859),#2977,.T.);
#92324=ADVANCED_FACE('',(#9860),#2978,.T.);
#92325=ADVANCED_FACE('',(#9861),#2979,.T.);
#92326=ADVANCED_FACE('',(#9862),#88254,.T.);
#92327=ADVANCED_FACE('',(#9863),#2980,.T.);
#92328=ADVANCED_FACE('',(#9864),#4981,.T.);
#92329=ADVANCED_FACE('',(#9865),#5873,.F.);
#92330=ADVANCED_FACE('',(#9866),#5874,.F.);
#92331=ADVANCED_FACE('',(#9867),#88255,.F.);
#92332=ADVANCED_FACE('',(#9868),#2981,.F.);
#92333=ADVANCED_FACE('',(#9869),#2982,.F.);
#92334=ADVANCED_FACE('',(#9870),#2983,.F.);
#92335=ADVANCED_FACE('',(#9871),#2032,.T.);
#92336=ADVANCED_FACE('',(#9872),#2984,.T.);
#92337=ADVANCED_FACE('',(#9873),#88256,.T.);
#92338=ADVANCED_FACE('',(#9874),#2985,.T.);
#92339=ADVANCED_FACE('',(#9875),#2986,.T.);
#92340=ADVANCED_FACE('',(#9876),#2987,.T.);
#92341=ADVANCED_FACE('',(#9877),#2988,.T.);
#92342=ADVANCED_FACE('',(#9878),#2989,.T.);
#92343=ADVANCED_FACE('',(#9879),#88257,.T.);
#92344=ADVANCED_FACE('',(#9880),#2990,.T.);
#92345=ADVANCED_FACE('',(#9881),#4982,.T.);
#92346=ADVANCED_FACE('',(#9882),#5875,.F.);
#92347=ADVANCED_FACE('',(#9883),#5876,.F.);
#92348=ADVANCED_FACE('',(#9884),#88258,.F.);
#92349=ADVANCED_FACE('',(#9885),#2991,.F.);
#92350=ADVANCED_FACE('',(#9886),#2992,.F.);
#92351=ADVANCED_FACE('',(#9887),#2993,.F.);
#92352=ADVANCED_FACE('',(#9888),#2033,.T.);
#92353=ADVANCED_FACE('',(#9889),#2994,.T.);
#92354=ADVANCED_FACE('',(#9890),#88259,.T.);
#92355=ADVANCED_FACE('',(#9891),#2995,.T.);
#92356=ADVANCED_FACE('',(#9892),#2996,.T.);
#92357=ADVANCED_FACE('',(#9893),#2997,.T.);
#92358=ADVANCED_FACE('',(#9894),#2998,.T.);
#92359=ADVANCED_FACE('',(#9895),#2999,.T.);
#92360=ADVANCED_FACE('',(#9896),#88260,.T.);
#92361=ADVANCED_FACE('',(#9897),#3000,.T.);
#92362=ADVANCED_FACE('',(#9898),#4983,.T.);
#92363=ADVANCED_FACE('',(#9899),#5877,.F.);
#92364=ADVANCED_FACE('',(#9900),#5878,.F.);
#92365=ADVANCED_FACE('',(#9901),#88261,.F.);
#92366=ADVANCED_FACE('',(#9902),#3001,.F.);
#92367=ADVANCED_FACE('',(#9903),#3002,.F.);
#92368=ADVANCED_FACE('',(#9904),#3003,.F.);
#92369=ADVANCED_FACE('',(#9905),#2034,.T.);
#92370=ADVANCED_FACE('',(#9906),#3004,.T.);
#92371=ADVANCED_FACE('',(#9907),#88262,.T.);
#92372=ADVANCED_FACE('',(#9908),#3005,.T.);
#92373=ADVANCED_FACE('',(#9909),#3006,.T.);
#92374=ADVANCED_FACE('',(#9910),#3007,.T.);
#92375=ADVANCED_FACE('',(#9911),#3008,.T.);
#92376=ADVANCED_FACE('',(#9912),#3009,.T.);
#92377=ADVANCED_FACE('',(#9913),#88263,.T.);
#92378=ADVANCED_FACE('',(#9914),#3010,.T.);
#92379=ADVANCED_FACE('',(#9915),#4984,.T.);
#92380=ADVANCED_FACE('',(#9916),#5879,.F.);
#92381=ADVANCED_FACE('',(#9917),#5880,.F.);
#92382=ADVANCED_FACE('',(#9918),#88264,.F.);
#92383=ADVANCED_FACE('',(#9919),#3011,.F.);
#92384=ADVANCED_FACE('',(#9920),#3012,.F.);
#92385=ADVANCED_FACE('',(#9921),#3013,.F.);
#92386=ADVANCED_FACE('',(#9922),#2035,.T.);
#92387=ADVANCED_FACE('',(#9923),#3014,.T.);
#92388=ADVANCED_FACE('',(#9924),#88265,.T.);
#92389=ADVANCED_FACE('',(#9925),#3015,.T.);
#92390=ADVANCED_FACE('',(#9926),#3016,.T.);
#92391=ADVANCED_FACE('',(#9927),#3017,.T.);
#92392=ADVANCED_FACE('',(#9928),#3018,.T.);
#92393=ADVANCED_FACE('',(#9929),#3019,.T.);
#92394=ADVANCED_FACE('',(#9930),#88266,.T.);
#92395=ADVANCED_FACE('',(#9931),#3020,.T.);
#92396=ADVANCED_FACE('',(#9932),#4985,.T.);
#92397=ADVANCED_FACE('',(#9933),#5881,.F.);
#92398=ADVANCED_FACE('',(#9934),#5882,.F.);
#92399=ADVANCED_FACE('',(#9935),#88267,.F.);
#92400=ADVANCED_FACE('',(#9936),#3021,.F.);
#92401=ADVANCED_FACE('',(#9937),#3022,.F.);
#92402=ADVANCED_FACE('',(#9938),#3023,.F.);
#92403=ADVANCED_FACE('',(#9939),#2036,.T.);
#92404=ADVANCED_FACE('',(#9940),#3024,.T.);
#92405=ADVANCED_FACE('',(#9941),#88268,.T.);
#92406=ADVANCED_FACE('',(#9942),#3025,.T.);
#92407=ADVANCED_FACE('',(#9943),#3026,.T.);
#92408=ADVANCED_FACE('',(#9944),#3027,.T.);
#92409=ADVANCED_FACE('',(#9945),#3028,.T.);
#92410=ADVANCED_FACE('',(#9946),#3029,.T.);
#92411=ADVANCED_FACE('',(#9947),#88269,.T.);
#92412=ADVANCED_FACE('',(#9948),#3030,.T.);
#92413=ADVANCED_FACE('',(#9949),#4986,.T.);
#92414=ADVANCED_FACE('',(#9950),#5883,.F.);
#92415=ADVANCED_FACE('',(#9951),#5884,.F.);
#92416=ADVANCED_FACE('',(#9952),#88270,.F.);
#92417=ADVANCED_FACE('',(#9953),#3031,.F.);
#92418=ADVANCED_FACE('',(#9954),#3032,.F.);
#92419=ADVANCED_FACE('',(#9955),#3033,.F.);
#92420=ADVANCED_FACE('',(#9956),#2037,.T.);
#92421=ADVANCED_FACE('',(#9957),#3034,.T.);
#92422=ADVANCED_FACE('',(#9958),#88271,.T.);
#92423=ADVANCED_FACE('',(#9959),#3035,.T.);
#92424=ADVANCED_FACE('',(#9960),#3036,.T.);
#92425=ADVANCED_FACE('',(#9961),#3037,.T.);
#92426=ADVANCED_FACE('',(#9962),#3038,.T.);
#92427=ADVANCED_FACE('',(#9963),#3039,.T.);
#92428=ADVANCED_FACE('',(#9964),#88272,.T.);
#92429=ADVANCED_FACE('',(#9965),#3040,.T.);
#92430=ADVANCED_FACE('',(#9966),#4987,.T.);
#92431=ADVANCED_FACE('',(#9967),#5885,.F.);
#92432=ADVANCED_FACE('',(#9968),#5886,.F.);
#92433=ADVANCED_FACE('',(#9969),#88273,.F.);
#92434=ADVANCED_FACE('',(#9970),#3041,.F.);
#92435=ADVANCED_FACE('',(#9971),#3042,.F.);
#92436=ADVANCED_FACE('',(#9972),#3043,.F.);
#92437=ADVANCED_FACE('',(#9973),#2038,.T.);
#92438=ADVANCED_FACE('',(#9974),#3044,.T.);
#92439=ADVANCED_FACE('',(#9975),#88274,.T.);
#92440=ADVANCED_FACE('',(#9976),#3045,.T.);
#92441=ADVANCED_FACE('',(#9977),#3046,.T.);
#92442=ADVANCED_FACE('',(#9978),#3047,.T.);
#92443=ADVANCED_FACE('',(#9979),#3048,.T.);
#92444=ADVANCED_FACE('',(#9980),#3049,.T.);
#92445=ADVANCED_FACE('',(#9981),#88275,.T.);
#92446=ADVANCED_FACE('',(#9982),#3050,.T.);
#92447=ADVANCED_FACE('',(#9983),#4988,.T.);
#92448=ADVANCED_FACE('',(#9984),#5887,.F.);
#92449=ADVANCED_FACE('',(#9985),#5888,.F.);
#92450=ADVANCED_FACE('',(#9986),#88276,.F.);
#92451=ADVANCED_FACE('',(#9987),#3051,.F.);
#92452=ADVANCED_FACE('',(#9988),#3052,.F.);
#92453=ADVANCED_FACE('',(#9989),#3053,.F.);
#92454=ADVANCED_FACE('',(#9990),#2039,.T.);
#92455=ADVANCED_FACE('',(#9991),#3054,.T.);
#92456=ADVANCED_FACE('',(#9992),#88277,.T.);
#92457=ADVANCED_FACE('',(#9993),#3055,.T.);
#92458=ADVANCED_FACE('',(#9994),#3056,.T.);
#92459=ADVANCED_FACE('',(#9995),#3057,.T.);
#92460=ADVANCED_FACE('',(#9996),#3058,.T.);
#92461=ADVANCED_FACE('',(#9997),#3059,.T.);
#92462=ADVANCED_FACE('',(#9998),#88278,.T.);
#92463=ADVANCED_FACE('',(#9999),#3060,.T.);
#92464=ADVANCED_FACE('',(#10000),#4989,.T.);
#92465=ADVANCED_FACE('',(#10001),#5889,.F.);
#92466=ADVANCED_FACE('',(#10002),#5890,.F.);
#92467=ADVANCED_FACE('',(#10003),#88279,.F.);
#92468=ADVANCED_FACE('',(#10004),#3061,.F.);
#92469=ADVANCED_FACE('',(#10005),#3062,.F.);
#92470=ADVANCED_FACE('',(#10006),#3063,.F.);
#92471=ADVANCED_FACE('',(#10007),#2040,.T.);
#92472=ADVANCED_FACE('',(#10008),#3064,.T.);
#92473=ADVANCED_FACE('',(#10009),#88280,.T.);
#92474=ADVANCED_FACE('',(#10010),#3065,.T.);
#92475=ADVANCED_FACE('',(#10011),#3066,.T.);
#92476=ADVANCED_FACE('',(#10012),#3067,.T.);
#92477=ADVANCED_FACE('',(#10013),#3068,.T.);
#92478=ADVANCED_FACE('',(#10014),#3069,.T.);
#92479=ADVANCED_FACE('',(#10015),#88281,.T.);
#92480=ADVANCED_FACE('',(#10016),#3070,.T.);
#92481=ADVANCED_FACE('',(#10017),#4990,.T.);
#92482=ADVANCED_FACE('',(#10018),#5891,.F.);
#92483=ADVANCED_FACE('',(#10019),#5892,.F.);
#92484=ADVANCED_FACE('',(#10020),#88282,.F.);
#92485=ADVANCED_FACE('',(#10021),#3071,.F.);
#92486=ADVANCED_FACE('',(#10022),#3072,.F.);
#92487=ADVANCED_FACE('',(#10023),#3073,.F.);
#92488=ADVANCED_FACE('',(#10024),#2041,.T.);
#92489=ADVANCED_FACE('',(#10025),#3074,.T.);
#92490=ADVANCED_FACE('',(#10026),#88283,.T.);
#92491=ADVANCED_FACE('',(#10027),#3075,.T.);
#92492=ADVANCED_FACE('',(#10028),#3076,.T.);
#92493=ADVANCED_FACE('',(#10029),#3077,.T.);
#92494=ADVANCED_FACE('',(#10030),#3078,.T.);
#92495=ADVANCED_FACE('',(#10031),#3079,.T.);
#92496=ADVANCED_FACE('',(#10032),#88284,.T.);
#92497=ADVANCED_FACE('',(#10033),#3080,.T.);
#92498=ADVANCED_FACE('',(#10034),#4991,.T.);
#92499=ADVANCED_FACE('',(#10035),#5893,.F.);
#92500=ADVANCED_FACE('',(#10036),#5894,.F.);
#92501=ADVANCED_FACE('',(#10037),#88285,.F.);
#92502=ADVANCED_FACE('',(#10038),#3081,.F.);
#92503=ADVANCED_FACE('',(#10039),#3082,.F.);
#92504=ADVANCED_FACE('',(#10040),#3083,.F.);
#92505=ADVANCED_FACE('',(#10041),#2042,.T.);
#92506=ADVANCED_FACE('',(#10042),#3084,.T.);
#92507=ADVANCED_FACE('',(#10043),#88286,.T.);
#92508=ADVANCED_FACE('',(#10044),#3085,.T.);
#92509=ADVANCED_FACE('',(#10045),#3086,.T.);
#92510=ADVANCED_FACE('',(#10046),#3087,.T.);
#92511=ADVANCED_FACE('',(#10047),#3088,.T.);
#92512=ADVANCED_FACE('',(#10048),#3089,.T.);
#92513=ADVANCED_FACE('',(#10049),#88287,.T.);
#92514=ADVANCED_FACE('',(#10050),#3090,.T.);
#92515=ADVANCED_FACE('',(#10051),#4992,.T.);
#92516=ADVANCED_FACE('',(#10052),#5895,.F.);
#92517=ADVANCED_FACE('',(#10053),#5896,.F.);
#92518=ADVANCED_FACE('',(#10054),#88288,.F.);
#92519=ADVANCED_FACE('',(#10055),#3091,.F.);
#92520=ADVANCED_FACE('',(#10056),#3092,.F.);
#92521=ADVANCED_FACE('',(#10057),#3093,.F.);
#92522=ADVANCED_FACE('',(#10058),#2043,.T.);
#92523=ADVANCED_FACE('',(#10059),#3094,.T.);
#92524=ADVANCED_FACE('',(#10060),#88289,.T.);
#92525=ADVANCED_FACE('',(#10061),#3095,.T.);
#92526=ADVANCED_FACE('',(#10062),#3096,.T.);
#92527=ADVANCED_FACE('',(#10063),#3097,.T.);
#92528=ADVANCED_FACE('',(#10064),#3098,.T.);
#92529=ADVANCED_FACE('',(#10065),#3099,.T.);
#92530=ADVANCED_FACE('',(#10066),#88290,.T.);
#92531=ADVANCED_FACE('',(#10067),#3100,.T.);
#92532=ADVANCED_FACE('',(#10068),#4993,.T.);
#92533=ADVANCED_FACE('',(#10069),#5897,.F.);
#92534=ADVANCED_FACE('',(#10070),#5898,.F.);
#92535=ADVANCED_FACE('',(#10071),#88291,.F.);
#92536=ADVANCED_FACE('',(#10072),#3101,.F.);
#92537=ADVANCED_FACE('',(#10073),#3102,.F.);
#92538=ADVANCED_FACE('',(#10074),#3103,.F.);
#92539=ADVANCED_FACE('',(#10075),#2044,.T.);
#92540=ADVANCED_FACE('',(#10076),#3104,.T.);
#92541=ADVANCED_FACE('',(#10077),#88292,.T.);
#92542=ADVANCED_FACE('',(#10078),#3105,.T.);
#92543=ADVANCED_FACE('',(#10079),#3106,.T.);
#92544=ADVANCED_FACE('',(#10080),#3107,.T.);
#92545=ADVANCED_FACE('',(#10081),#3108,.T.);
#92546=ADVANCED_FACE('',(#10082),#3109,.T.);
#92547=ADVANCED_FACE('',(#10083),#88293,.T.);
#92548=ADVANCED_FACE('',(#10084),#3110,.T.);
#92549=ADVANCED_FACE('',(#10085),#4994,.T.);
#92550=ADVANCED_FACE('',(#10086),#5899,.F.);
#92551=ADVANCED_FACE('',(#10087),#5900,.F.);
#92552=ADVANCED_FACE('',(#10088),#88294,.F.);
#92553=ADVANCED_FACE('',(#10089),#3111,.F.);
#92554=ADVANCED_FACE('',(#10090),#3112,.F.);
#92555=ADVANCED_FACE('',(#10091),#3113,.F.);
#92556=ADVANCED_FACE('',(#10092),#2045,.T.);
#92557=ADVANCED_FACE('',(#10093),#3114,.T.);
#92558=ADVANCED_FACE('',(#10094),#88295,.T.);
#92559=ADVANCED_FACE('',(#10095),#3115,.T.);
#92560=ADVANCED_FACE('',(#10096),#3116,.T.);
#92561=ADVANCED_FACE('',(#10097),#3117,.T.);
#92562=ADVANCED_FACE('',(#10098),#3118,.T.);
#92563=ADVANCED_FACE('',(#10099),#3119,.T.);
#92564=ADVANCED_FACE('',(#10100),#88296,.T.);
#92565=ADVANCED_FACE('',(#10101),#3120,.T.);
#92566=ADVANCED_FACE('',(#10102),#4995,.T.);
#92567=ADVANCED_FACE('',(#10103),#5901,.F.);
#92568=ADVANCED_FACE('',(#10104),#5902,.F.);
#92569=ADVANCED_FACE('',(#10105),#88297,.F.);
#92570=ADVANCED_FACE('',(#10106),#3121,.F.);
#92571=ADVANCED_FACE('',(#10107),#3122,.F.);
#92572=ADVANCED_FACE('',(#10108),#3123,.F.);
#92573=ADVANCED_FACE('',(#10109),#2046,.T.);
#92574=ADVANCED_FACE('',(#10110),#3124,.T.);
#92575=ADVANCED_FACE('',(#10111),#88298,.T.);
#92576=ADVANCED_FACE('',(#10112),#3125,.T.);
#92577=ADVANCED_FACE('',(#10113),#3126,.T.);
#92578=ADVANCED_FACE('',(#10114),#3127,.T.);
#92579=ADVANCED_FACE('',(#10115),#3128,.T.);
#92580=ADVANCED_FACE('',(#10116),#3129,.T.);
#92581=ADVANCED_FACE('',(#10117),#88299,.T.);
#92582=ADVANCED_FACE('',(#10118),#3130,.T.);
#92583=ADVANCED_FACE('',(#10119),#4996,.T.);
#92584=ADVANCED_FACE('',(#10120),#5903,.F.);
#92585=ADVANCED_FACE('',(#10121),#5904,.F.);
#92586=ADVANCED_FACE('',(#10122),#88300,.F.);
#92587=ADVANCED_FACE('',(#10123),#3131,.F.);
#92588=ADVANCED_FACE('',(#10124),#3132,.F.);
#92589=ADVANCED_FACE('',(#10125),#3133,.F.);
#92590=ADVANCED_FACE('',(#10126),#2047,.T.);
#92591=ADVANCED_FACE('',(#10127),#3134,.T.);
#92592=ADVANCED_FACE('',(#10128),#88301,.T.);
#92593=ADVANCED_FACE('',(#10129),#3135,.T.);
#92594=ADVANCED_FACE('',(#10130),#3136,.T.);
#92595=ADVANCED_FACE('',(#10131),#3137,.T.);
#92596=ADVANCED_FACE('',(#10132),#3138,.T.);
#92597=ADVANCED_FACE('',(#10133),#3139,.T.);
#92598=ADVANCED_FACE('',(#10134),#88302,.T.);
#92599=ADVANCED_FACE('',(#10135),#3140,.T.);
#92600=ADVANCED_FACE('',(#10136),#4997,.T.);
#92601=ADVANCED_FACE('',(#10137),#5905,.F.);
#92602=ADVANCED_FACE('',(#10138),#5906,.F.);
#92603=ADVANCED_FACE('',(#10139),#88303,.F.);
#92604=ADVANCED_FACE('',(#10140),#3141,.F.);
#92605=ADVANCED_FACE('',(#10141),#3142,.F.);
#92606=ADVANCED_FACE('',(#10142),#3143,.F.);
#92607=ADVANCED_FACE('',(#10143),#2048,.T.);
#92608=ADVANCED_FACE('',(#10144),#3144,.T.);
#92609=ADVANCED_FACE('',(#10145),#88304,.T.);
#92610=ADVANCED_FACE('',(#10146),#3145,.T.);
#92611=ADVANCED_FACE('',(#10147),#3146,.T.);
#92612=ADVANCED_FACE('',(#10148),#3147,.T.);
#92613=ADVANCED_FACE('',(#10149),#3148,.T.);
#92614=ADVANCED_FACE('',(#10150),#3149,.T.);
#92615=ADVANCED_FACE('',(#10151),#88305,.T.);
#92616=ADVANCED_FACE('',(#10152),#3150,.T.);
#92617=ADVANCED_FACE('',(#10153),#4998,.T.);
#92618=ADVANCED_FACE('',(#10154),#5907,.F.);
#92619=ADVANCED_FACE('',(#10155),#5908,.F.);
#92620=ADVANCED_FACE('',(#10156),#88306,.F.);
#92621=ADVANCED_FACE('',(#10157),#3151,.F.);
#92622=ADVANCED_FACE('',(#10158),#3152,.F.);
#92623=ADVANCED_FACE('',(#10159),#3153,.F.);
#92624=ADVANCED_FACE('',(#10160),#2049,.T.);
#92625=ADVANCED_FACE('',(#10161),#3154,.T.);
#92626=ADVANCED_FACE('',(#10162),#88307,.T.);
#92627=ADVANCED_FACE('',(#10163),#3155,.T.);
#92628=ADVANCED_FACE('',(#10164),#3156,.T.);
#92629=ADVANCED_FACE('',(#10165),#3157,.T.);
#92630=ADVANCED_FACE('',(#10166),#3158,.T.);
#92631=ADVANCED_FACE('',(#10167),#3159,.T.);
#92632=ADVANCED_FACE('',(#10168),#88308,.T.);
#92633=ADVANCED_FACE('',(#10169),#3160,.T.);
#92634=ADVANCED_FACE('',(#10170),#4999,.T.);
#92635=ADVANCED_FACE('',(#10171),#5909,.F.);
#92636=ADVANCED_FACE('',(#10172),#5910,.F.);
#92637=ADVANCED_FACE('',(#10173),#88309,.F.);
#92638=ADVANCED_FACE('',(#10174),#3161,.F.);
#92639=ADVANCED_FACE('',(#10175),#3162,.F.);
#92640=ADVANCED_FACE('',(#10176),#3163,.F.);
#92641=ADVANCED_FACE('',(#10177),#2050,.T.);
#92642=ADVANCED_FACE('',(#10178),#3164,.T.);
#92643=ADVANCED_FACE('',(#10179),#88310,.T.);
#92644=ADVANCED_FACE('',(#10180),#3165,.T.);
#92645=ADVANCED_FACE('',(#10181),#3166,.T.);
#92646=ADVANCED_FACE('',(#10182),#3167,.T.);
#92647=ADVANCED_FACE('',(#10183),#3168,.T.);
#92648=ADVANCED_FACE('',(#10184),#3169,.T.);
#92649=ADVANCED_FACE('',(#10185),#88311,.T.);
#92650=ADVANCED_FACE('',(#10186),#3170,.T.);
#92651=ADVANCED_FACE('',(#10187),#5000,.T.);
#92652=ADVANCED_FACE('',(#10188),#5911,.F.);
#92653=ADVANCED_FACE('',(#10189),#5912,.F.);
#92654=ADVANCED_FACE('',(#10190),#88312,.F.);
#92655=ADVANCED_FACE('',(#10191),#3171,.F.);
#92656=ADVANCED_FACE('',(#10192),#3172,.F.);
#92657=ADVANCED_FACE('',(#10193),#3173,.F.);
#92658=ADVANCED_FACE('',(#10194),#2051,.T.);
#92659=ADVANCED_FACE('',(#10195),#3174,.T.);
#92660=ADVANCED_FACE('',(#10196),#88313,.T.);
#92661=ADVANCED_FACE('',(#10197),#3175,.T.);
#92662=ADVANCED_FACE('',(#10198),#3176,.T.);
#92663=ADVANCED_FACE('',(#10199),#3177,.T.);
#92664=ADVANCED_FACE('',(#10200),#3178,.T.);
#92665=ADVANCED_FACE('',(#10201),#3179,.T.);
#92666=ADVANCED_FACE('',(#10202),#88314,.T.);
#92667=ADVANCED_FACE('',(#10203),#3180,.T.);
#92668=ADVANCED_FACE('',(#10204),#5001,.T.);
#92669=ADVANCED_FACE('',(#10205),#5913,.F.);
#92670=ADVANCED_FACE('',(#10206),#5914,.F.);
#92671=ADVANCED_FACE('',(#10207),#88315,.F.);
#92672=ADVANCED_FACE('',(#10208),#3181,.F.);
#92673=ADVANCED_FACE('',(#10209),#3182,.F.);
#92674=ADVANCED_FACE('',(#10210),#3183,.F.);
#92675=ADVANCED_FACE('',(#10211),#2052,.T.);
#92676=ADVANCED_FACE('',(#10212),#3184,.T.);
#92677=ADVANCED_FACE('',(#10213),#88316,.T.);
#92678=ADVANCED_FACE('',(#10214),#3185,.T.);
#92679=ADVANCED_FACE('',(#10215),#3186,.T.);
#92680=ADVANCED_FACE('',(#10216),#3187,.T.);
#92681=ADVANCED_FACE('',(#10217),#3188,.T.);
#92682=ADVANCED_FACE('',(#10218),#3189,.T.);
#92683=ADVANCED_FACE('',(#10219),#88317,.T.);
#92684=ADVANCED_FACE('',(#10220),#3190,.T.);
#92685=ADVANCED_FACE('',(#10221),#5002,.T.);
#92686=ADVANCED_FACE('',(#10222),#5915,.F.);
#92687=ADVANCED_FACE('',(#10223),#5916,.F.);
#92688=ADVANCED_FACE('',(#10224),#88318,.F.);
#92689=ADVANCED_FACE('',(#10225),#3191,.F.);
#92690=ADVANCED_FACE('',(#10226),#3192,.F.);
#92691=ADVANCED_FACE('',(#10227),#3193,.F.);
#92692=ADVANCED_FACE('',(#10228),#2053,.T.);
#92693=ADVANCED_FACE('',(#10229),#3194,.T.);
#92694=ADVANCED_FACE('',(#10230),#88319,.T.);
#92695=ADVANCED_FACE('',(#10231),#3195,.T.);
#92696=ADVANCED_FACE('',(#10232),#3196,.T.);
#92697=ADVANCED_FACE('',(#10233),#3197,.T.);
#92698=ADVANCED_FACE('',(#10234),#3198,.T.);
#92699=ADVANCED_FACE('',(#10235),#3199,.T.);
#92700=ADVANCED_FACE('',(#10236),#88320,.T.);
#92701=ADVANCED_FACE('',(#10237),#3200,.T.);
#92702=ADVANCED_FACE('',(#10238),#5003,.T.);
#92703=ADVANCED_FACE('',(#10239),#5917,.F.);
#92704=ADVANCED_FACE('',(#10240),#5918,.F.);
#92705=ADVANCED_FACE('',(#10241),#88321,.F.);
#92706=ADVANCED_FACE('',(#10242),#3201,.F.);
#92707=ADVANCED_FACE('',(#10243),#3202,.F.);
#92708=ADVANCED_FACE('',(#10244),#3203,.F.);
#92709=ADVANCED_FACE('',(#10245),#2054,.T.);
#92710=ADVANCED_FACE('',(#10246),#3204,.T.);
#92711=ADVANCED_FACE('',(#10247),#88322,.T.);
#92712=ADVANCED_FACE('',(#10248),#3205,.T.);
#92713=ADVANCED_FACE('',(#10249),#3206,.T.);
#92714=ADVANCED_FACE('',(#10250),#3207,.T.);
#92715=ADVANCED_FACE('',(#10251),#3208,.T.);
#92716=ADVANCED_FACE('',(#10252),#3209,.T.);
#92717=ADVANCED_FACE('',(#10253),#88323,.T.);
#92718=ADVANCED_FACE('',(#10254),#3210,.T.);
#92719=ADVANCED_FACE('',(#10255),#5004,.T.);
#92720=ADVANCED_FACE('',(#10256),#5919,.F.);
#92721=ADVANCED_FACE('',(#10257),#5920,.F.);
#92722=ADVANCED_FACE('',(#10258),#88324,.F.);
#92723=ADVANCED_FACE('',(#10259),#3211,.F.);
#92724=ADVANCED_FACE('',(#10260),#3212,.F.);
#92725=ADVANCED_FACE('',(#10261),#3213,.F.);
#92726=ADVANCED_FACE('',(#10262),#2055,.T.);
#92727=ADVANCED_FACE('',(#10263),#3214,.T.);
#92728=ADVANCED_FACE('',(#10264),#88325,.T.);
#92729=ADVANCED_FACE('',(#10265),#3215,.T.);
#92730=ADVANCED_FACE('',(#10266),#3216,.T.);
#92731=ADVANCED_FACE('',(#10267),#3217,.T.);
#92732=ADVANCED_FACE('',(#10268),#3218,.T.);
#92733=ADVANCED_FACE('',(#10269),#3219,.T.);
#92734=ADVANCED_FACE('',(#10270),#88326,.T.);
#92735=ADVANCED_FACE('',(#10271),#3220,.T.);
#92736=ADVANCED_FACE('',(#10272),#5005,.T.);
#92737=ADVANCED_FACE('',(#10273),#5921,.F.);
#92738=ADVANCED_FACE('',(#10274),#5922,.F.);
#92739=ADVANCED_FACE('',(#10275),#88327,.F.);
#92740=ADVANCED_FACE('',(#10276),#3221,.F.);
#92741=ADVANCED_FACE('',(#10277),#3222,.F.);
#92742=ADVANCED_FACE('',(#10278),#3223,.F.);
#92743=ADVANCED_FACE('',(#10279),#2056,.T.);
#92744=ADVANCED_FACE('',(#10280),#3224,.T.);
#92745=ADVANCED_FACE('',(#10281),#88328,.T.);
#92746=ADVANCED_FACE('',(#10282),#3225,.T.);
#92747=ADVANCED_FACE('',(#10283),#3226,.T.);
#92748=ADVANCED_FACE('',(#10284),#3227,.T.);
#92749=ADVANCED_FACE('',(#10285),#3228,.T.);
#92750=ADVANCED_FACE('',(#10286),#3229,.T.);
#92751=ADVANCED_FACE('',(#10287),#88329,.T.);
#92752=ADVANCED_FACE('',(#10288),#3230,.T.);
#92753=ADVANCED_FACE('',(#10289),#5006,.T.);
#92754=ADVANCED_FACE('',(#10290),#5923,.F.);
#92755=ADVANCED_FACE('',(#10291),#5924,.F.);
#92756=ADVANCED_FACE('',(#10292),#88330,.F.);
#92757=ADVANCED_FACE('',(#10293),#3231,.F.);
#92758=ADVANCED_FACE('',(#10294),#3232,.F.);
#92759=ADVANCED_FACE('',(#10295),#3233,.F.);
#92760=ADVANCED_FACE('',(#10296),#2057,.T.);
#92761=ADVANCED_FACE('',(#10297),#3234,.T.);
#92762=ADVANCED_FACE('',(#10298),#88331,.T.);
#92763=ADVANCED_FACE('',(#10299),#3235,.T.);
#92764=ADVANCED_FACE('',(#10300),#3236,.T.);
#92765=ADVANCED_FACE('',(#10301),#3237,.T.);
#92766=ADVANCED_FACE('',(#10302),#3238,.T.);
#92767=ADVANCED_FACE('',(#10303),#3239,.T.);
#92768=ADVANCED_FACE('',(#10304),#88332,.T.);
#92769=ADVANCED_FACE('',(#10305),#3240,.T.);
#92770=ADVANCED_FACE('',(#10306),#5007,.T.);
#92771=ADVANCED_FACE('',(#10307),#5925,.F.);
#92772=ADVANCED_FACE('',(#10308),#5926,.F.);
#92773=ADVANCED_FACE('',(#10309),#88333,.F.);
#92774=ADVANCED_FACE('',(#10310),#3241,.F.);
#92775=ADVANCED_FACE('',(#10311),#3242,.F.);
#92776=ADVANCED_FACE('',(#10312),#3243,.F.);
#92777=ADVANCED_FACE('',(#10313),#2058,.T.);
#92778=ADVANCED_FACE('',(#10314),#3244,.T.);
#92779=ADVANCED_FACE('',(#10315),#88334,.T.);
#92780=ADVANCED_FACE('',(#10316),#3245,.T.);
#92781=ADVANCED_FACE('',(#10317),#3246,.T.);
#92782=ADVANCED_FACE('',(#10318),#3247,.T.);
#92783=ADVANCED_FACE('',(#10319),#3248,.T.);
#92784=ADVANCED_FACE('',(#10320),#3249,.T.);
#92785=ADVANCED_FACE('',(#10321),#88335,.T.);
#92786=ADVANCED_FACE('',(#10322),#3250,.T.);
#92787=ADVANCED_FACE('',(#10323),#5008,.T.);
#92788=ADVANCED_FACE('',(#10324),#5927,.F.);
#92789=ADVANCED_FACE('',(#10325),#5928,.F.);
#92790=ADVANCED_FACE('',(#10326),#88336,.F.);
#92791=ADVANCED_FACE('',(#10327),#3251,.F.);
#92792=ADVANCED_FACE('',(#10328),#3252,.F.);
#92793=ADVANCED_FACE('',(#10329),#3253,.F.);
#92794=ADVANCED_FACE('',(#10330),#2059,.T.);
#92795=ADVANCED_FACE('',(#10331),#3254,.T.);
#92796=ADVANCED_FACE('',(#10332),#88337,.T.);
#92797=ADVANCED_FACE('',(#10333),#3255,.T.);
#92798=ADVANCED_FACE('',(#10334),#3256,.T.);
#92799=ADVANCED_FACE('',(#10335),#3257,.T.);
#92800=ADVANCED_FACE('',(#10336),#3258,.T.);
#92801=ADVANCED_FACE('',(#10337),#3259,.T.);
#92802=ADVANCED_FACE('',(#10338),#88338,.T.);
#92803=ADVANCED_FACE('',(#10339),#3260,.T.);
#92804=ADVANCED_FACE('',(#10340),#5009,.T.);
#92805=ADVANCED_FACE('',(#10341),#5929,.F.);
#92806=ADVANCED_FACE('',(#10342),#5930,.F.);
#92807=ADVANCED_FACE('',(#10343),#88339,.F.);
#92808=ADVANCED_FACE('',(#10344),#3261,.F.);
#92809=ADVANCED_FACE('',(#10345),#3262,.F.);
#92810=ADVANCED_FACE('',(#10346),#3263,.F.);
#92811=ADVANCED_FACE('',(#10347),#2060,.T.);
#92812=ADVANCED_FACE('',(#10348),#3264,.T.);
#92813=ADVANCED_FACE('',(#10349),#88340,.T.);
#92814=ADVANCED_FACE('',(#10350),#3265,.T.);
#92815=ADVANCED_FACE('',(#10351),#3266,.T.);
#92816=ADVANCED_FACE('',(#10352),#3267,.T.);
#92817=ADVANCED_FACE('',(#10353),#3268,.T.);
#92818=ADVANCED_FACE('',(#10354),#3269,.T.);
#92819=ADVANCED_FACE('',(#10355),#88341,.T.);
#92820=ADVANCED_FACE('',(#10356),#3270,.T.);
#92821=ADVANCED_FACE('',(#10357),#5010,.T.);
#92822=ADVANCED_FACE('',(#10358),#5931,.F.);
#92823=ADVANCED_FACE('',(#10359),#5932,.F.);
#92824=ADVANCED_FACE('',(#10360),#88342,.F.);
#92825=ADVANCED_FACE('',(#10361),#3271,.F.);
#92826=ADVANCED_FACE('',(#10362),#3272,.F.);
#92827=ADVANCED_FACE('',(#10363),#3273,.F.);
#92828=ADVANCED_FACE('',(#10364),#2061,.T.);
#92829=ADVANCED_FACE('',(#10365),#3274,.T.);
#92830=ADVANCED_FACE('',(#10366),#88343,.T.);
#92831=ADVANCED_FACE('',(#10367),#3275,.T.);
#92832=ADVANCED_FACE('',(#10368),#3276,.T.);
#92833=ADVANCED_FACE('',(#10369),#3277,.T.);
#92834=ADVANCED_FACE('',(#10370),#3278,.T.);
#92835=ADVANCED_FACE('',(#10371),#3279,.T.);
#92836=ADVANCED_FACE('',(#10372),#88344,.T.);
#92837=ADVANCED_FACE('',(#10373),#3280,.T.);
#92838=ADVANCED_FACE('',(#10374),#5011,.T.);
#92839=ADVANCED_FACE('',(#10375),#5933,.F.);
#92840=ADVANCED_FACE('',(#10376),#5934,.F.);
#92841=ADVANCED_FACE('',(#10377),#88345,.F.);
#92842=ADVANCED_FACE('',(#10378),#3281,.F.);
#92843=ADVANCED_FACE('',(#10379),#3282,.F.);
#92844=ADVANCED_FACE('',(#10380),#3283,.F.);
#92845=ADVANCED_FACE('',(#10381),#2062,.T.);
#92846=ADVANCED_FACE('',(#10382),#3284,.T.);
#92847=ADVANCED_FACE('',(#10383),#88346,.T.);
#92848=ADVANCED_FACE('',(#10384),#3285,.T.);
#92849=ADVANCED_FACE('',(#10385),#3286,.T.);
#92850=ADVANCED_FACE('',(#10386),#3287,.T.);
#92851=ADVANCED_FACE('',(#10387),#3288,.T.);
#92852=ADVANCED_FACE('',(#10388),#3289,.T.);
#92853=ADVANCED_FACE('',(#10389),#88347,.T.);
#92854=ADVANCED_FACE('',(#10390),#3290,.T.);
#92855=ADVANCED_FACE('',(#10391),#5012,.T.);
#92856=ADVANCED_FACE('',(#10392),#5935,.F.);
#92857=ADVANCED_FACE('',(#10393),#5936,.F.);
#92858=ADVANCED_FACE('',(#10394),#88348,.F.);
#92859=ADVANCED_FACE('',(#10395),#3291,.F.);
#92860=ADVANCED_FACE('',(#10396),#3292,.F.);
#92861=ADVANCED_FACE('',(#10397),#3293,.F.);
#92862=ADVANCED_FACE('',(#10398),#2063,.T.);
#92863=ADVANCED_FACE('',(#10399),#3294,.T.);
#92864=ADVANCED_FACE('',(#10400),#88349,.T.);
#92865=ADVANCED_FACE('',(#10401),#3295,.T.);
#92866=ADVANCED_FACE('',(#10402),#3296,.T.);
#92867=ADVANCED_FACE('',(#10403),#3297,.T.);
#92868=ADVANCED_FACE('',(#10404),#3298,.T.);
#92869=ADVANCED_FACE('',(#10405),#3299,.T.);
#92870=ADVANCED_FACE('',(#10406),#88350,.T.);
#92871=ADVANCED_FACE('',(#10407),#3300,.T.);
#92872=ADVANCED_FACE('',(#10408),#5013,.T.);
#94665=CLOSED_SHELL('',(#91015,#91016,#91017,#91018,#91019,#91020,#91021,
#91022,#91023,#91024,#91025,#91026,#91027,#91028,#91029,#91030,#91031,#91032,
#91033,#91034,#91035,#91036,#91037,#91038,#91039,#91040,#91041,#91042,#91043,
#91044,#91045,#91046,#91047,#91048,#91049,#91050,#91051,#91052,#91053,#91054,
#91055,#91056,#91057,#91058,#91059,#91060,#91061,#91062,#91063,#91064,#91065,
#91066,#91067,#91068,#91069,#91070,#91071,#91072,#91073,#91074,#91075,#91076,
#91077,#91078,#91079,#91080,#91081,#91082,#91083,#91084,#91085,#91086,#91087,
#91088,#91089,#91090,#91091,#91092,#91093,#91094,#91095,#91096,#91097,#91098,
#91099,#91100,#91101,#91102,#91103,#91104,#91105,#91106,#91107,#91108,#91109,
#91110,#91111,#91112,#91113,#91114,#91115,#91116,#91117,#91118,#91119,#91120,
#91121,#91122,#91123,#91124,#91125,#91126,#91127,#91128,#91129,#91130,#91131,
#91132,#91133,#91134,#91135,#91136,#91137,#91138,#91139,#91140,#91141,#91142,
#91143,#91144,#91145,#91146,#91147,#91148,#91149,#91150,#91151,#91152,#91153,
#91154,#91155,#91156,#91157,#91158,#91159,#91160,#91161,#91162,#91163,#91164,
#91165,#91166,#91167,#91168,#91169,#91170,#91171,#91172,#91173,#91174,#91175,
#91176,#91177,#91178,#91179,#91180,#91181,#91182,#91183,#91184,#91185,#91186,
#91187,#91188,#91189,#91190,#91191,#91192,#91193,#91194,#91195,#91196,#91197,
#91198,#91199,#91200,#91201,#91202,#91203,#91204,#91205,#91206,#91207,#91208,
#91209,#91210,#91211,#91212,#91213,#91214,#91215,#91216,#91217,#91218,#91219,
#91220,#91221,#91222,#91223,#91224,#91225,#91226,#91227,#91228,#91229,#91230,
#91231,#91232,#91233,#91234,#91235,#91236,#91237,#91238,#91239,#91240,#91241,
#91242,#91243,#91244,#91245,#91246,#91247,#91248,#91249,#91250,#91251,#91252,
#91253,#91254,#91255,#91256,#91257,#91258,#91259,#91260,#91261,#91262,#91263,
#91264,#91265,#91266,#91267,#91268,#91269,#91270,#91271,#91272,#91273,#91274,
#91275,#91276,#91277,#91278,#91279,#91280,#91281,#91282,#91283,#91284,#91285,
#91286,#91287,#91288,#91289,#91290,#91291,#91292,#91293,#91294,#91295,#91296,
#91297,#91298,#91299,#91300,#91301,#91302,#91303,#91304,#91305,#91306,#91307,
#91308,#91309,#91310,#91311,#91312,#91313,#91314,#91315,#91316,#91317,#91318,
#91319,#91320,#91321,#91322,#91323,#91324,#91325,#91326,#91327,#91328,#91329,
#91330,#91331,#91332,#91333,#91334,#91335,#91336,#91337,#91338,#91339,#91340,
#91341,#91342,#91343,#91344,#91345,#91346,#91347,#91348,#91349,#91350,#91351,
#91352,#91353,#91354,#91355,#91356,#91357,#91358,#91359,#91360,#91361,#91362,
#91363,#91364,#91365,#91366,#91367,#91368,#91369,#91370,#91371,#91372,#91373,
#91374,#91375,#91376,#91377,#91378,#91379,#91380,#91381,#91382,#91383,#91384,
#91385,#91386,#91387,#91388,#91389,#91390,#91391,#91392,#91393,#91394,#91395,
#91396,#91397,#91398,#91399,#91400,#91401,#91402,#91403,#91404,#91405,#91406,
#91407,#91408,#91409,#91410,#91411,#91412,#91413,#91414,#91415,#91416,#91417,
#91418,#91419,#91420,#91421,#91422,#91423,#91424,#91425,#91426,#91427,#91428,
#91429,#91430,#91431,#91432,#91433,#91434,#91435,#91436,#91437,#91438,#91439,
#91440,#91441,#91442,#91443,#91444,#91445,#91446,#91447,#91448,#91449,#91450,
#91451,#91452,#91453,#91454,#91455,#91456,#91457,#91458,#91459,#91460,#91461,
#91462,#91463,#91464,#91465,#91466,#91467,#91468,#91469,#91470,#91471,#91472,
#91473,#91474,#91475,#91476,#91477,#91478,#91479,#91480,#91481,#91482,#91483,
#91484,#91485,#91486,#91487,#91488,#91489,#91490,#91491,#91492,#91493,#91494,
#91495,#91496,#91497,#91498,#91499,#91500,#91501,#91502,#91503,#91504,#91505,
#91506,#91507,#91508,#91509,#91510,#91511,#91512,#91513,#91514,#91515,#91516,
#91517,#91518,#91519,#91520,#91521,#91522,#91523,#91524,#91525,#91526,#91527,
#91528,#91529,#91530,#91531,#91532,#91533,#91534,#91535,#91536,#91537,#91538,
#91539,#91540,#91541,#91542,#91543,#91544,#91545,#91546,#91547,#91548,#91549,
#91550,#91551,#91552,#91553,#91554,#91555,#91556,#91557,#91558,#91559,#91560,
#91561,#91562,#91563,#91564,#91565,#91566,#91567,#91568,#91569,#91570,#91571,
#91572,#91573,#91574,#91575,#91576,#91577,#91578,#91579,#91580,#91581,#91582,
#91583,#91584,#91585,#91586,#91587,#91588,#91589,#91590,#91591,#91592,#91593,
#91594,#91595,#91596,#91597,#91598,#91599,#91600,#91601,#91602,#91603,#91604,
#91605,#91606,#91607,#91608,#91609,#91610,#91611,#91612,#91613,#91614,#91615,
#91616,#91617,#91618,#91619,#91620,#91621,#91622,#91623,#91624,#91625,#91626,
#91627,#91628,#91629,#91630,#91631,#91632,#91633,#91634,#91635,#91636,#91637,
#91638,#91639,#91640,#91641,#91642,#91643,#91644,#91645,#91646,#91647,#91648,
#91649,#91650,#91651,#91652,#91653,#91654,#91655,#91656,#91657,#91658,#91659,
#91660,#91661,#91662,#91663,#91664,#91665,#91666,#91667,#91668,#91669,#91670,
#91671,#91672,#91673,#91674,#91675,#91676,#91677,#91678,#91679,#91680,#91681,
#91682,#91683,#91684,#91685,#91686,#91687,#91688,#91689,#91690,#91691,#91692,
#91693,#91694,#91695,#91696,#91697,#91698,#91699,#91700,#91701,#91702,#91703,
#91704,#91705,#91706,#91707,#91708,#91709,#91710,#91711,#91712,#91713,#91714,
#91715,#91716,#91717,#91718,#91719,#91720,#91721,#91722,#91723,#91724,#91725,
#91726,#91727,#91728,#91729,#91730,#91731,#91732,#91733,#91734,#91735,#91736,
#91737,#91738,#91739,#91740,#91741,#91742,#91743,#91744,#91745,#91746,#91747,
#91748,#91749,#91750,#91751,#91752,#91753,#91754,#91755,#91756,#91757,#91758,
#91759,#91760,#91761,#91762,#91763,#91764,#91765,#91766,#91767,#91768,#91769,
#91770,#91771,#91772,#91773,#91774,#91775,#91776,#91777,#91778,#91779,#91780,
#91781,#91782,#91783,#91784,#91785,#91786,#91787,#91788,#91789,#91790,#91791,
#91792,#91793,#91794,#91795,#91796,#91797,#91798,#91799,#91800,#91801,#91802,
#91803,#91804,#91805,#91806,#91807,#91808,#91809,#91810,#91811,#91812,#91813,
#91814,#91815,#91816,#91817,#91818,#91819,#91820,#91821,#91822,#91823,#91824,
#91825,#91826,#91827,#91828,#91829,#91830,#91831,#91832,#91833,#91834,#91835,
#91836,#91837,#91838,#91839,#91840,#91841,#91842,#91843,#91844,#91845,#91846,
#91847,#91848,#91849,#91850,#91851,#91852,#91853,#91854,#91855,#91856,#91857,
#91858,#91859,#91860,#91861,#91862,#91863,#91864,#91865,#91866,#91867,#91868,
#91869,#91870,#91871,#91872,#91873,#91874,#91875,#91876,#91877,#91878,#91879,
#91880,#91881,#91882,#91883,#91884,#91885,#91886,#91887,#91888,#91889,#91890,
#91891,#91892,#91893,#91894,#91895,#91896,#91897,#91898,#91899,#91900,#91901,
#91902,#91903,#91904,#91905,#91906,#91907,#91908,#91909,#91910,#91911,#91912,
#91913,#91914,#91915,#91916,#91917,#91918,#91919,#91920,#91921,#91922,#91923,
#91924,#91925,#91926,#91927,#91928,#91929,#91930,#91931,#91932,#91933,#91934,
#91935,#91936,#91937,#91938,#91939,#91940,#91941,#91942,#91943,#91944,#91945,
#91946,#91947,#91948,#91949,#91950,#91951,#91952,#91953,#91954,#91955,#91956,
#91957,#91958,#91959,#91960,#91961,#91962,#91963,#91964,#91965,#91966,#91967,
#91968,#91969,#91970,#91971,#91972,#91973,#91974,#91975,#91976,#91977,#91978,
#91979,#91980,#91981,#91982,#91983,#91984,#91985,#91986,#91987,#91988,#91989,
#91990,#91991,#91992,#91993,#91994,#91995,#91996,#91997,#91998,#91999,#92000,
#92001,#92002,#92003,#92004,#92005,#92006,#92007,#92008,#92009,#92010,#92011,
#92012,#92013,#92014,#92015,#92016,#92017,#92018,#92019,#92020,#92021,#92022,
#92023,#92024,#92025,#92026,#92027,#92028,#92029,#92030,#92031,#92032,#92033,
#92034,#92035,#92036,#92037,#92038,#92039,#92040,#92041,#92042,#92043,#92044,
#92045,#92046,#92047,#92048,#92049,#92050,#92051,#92052,#92053,#92054,#92055,
#92056,#92057,#92058,#92059,#92060,#92061,#92062,#92063,#92064,#92065,#92066,
#92067,#92068,#92069,#92070,#92071,#92072,#92073,#92074,#92075,#92076,#92077,
#92078,#92079,#92080,#92081,#92082,#92083,#92084,#92085,#92086,#92087,#92088,
#92089,#92090,#92091,#92092,#92093,#92094,#92095,#92096,#92097,#92098,#92099,
#92100,#92101,#92102,#92103,#92104,#92105,#92106,#92107,#92108,#92109,#92110,
#92111,#92112,#92113,#92114,#92115,#92116,#92117,#92118,#92119,#92120,#92121,
#92122,#92123,#92124,#92125,#92126,#92127,#92128,#92129,#92130,#92131,#92132,
#92133,#92134,#92135,#92136,#92137,#92138,#92139,#92140,#92141,#92142,#92143,
#92144,#92145,#92146,#92147,#92148,#92149,#92150,#92151,#92152,#92153,#92154,
#92155,#92156,#92157,#92158,#92159,#92160,#92161,#92162,#92163,#92164,#92165,
#92166,#92167,#92168,#92169,#92170,#92171,#92172,#92173,#92174,#92175,#92176,
#92177,#92178,#92179,#92180,#92181,#92182,#92183,#92184,#92185,#92186,#92187,
#92188,#92189,#92190,#92191,#92192,#92193,#92194,#92195,#92196,#92197,#92198,
#92199,#92200,#92201,#92202,#92203,#92204,#92205,#92206,#92207,#92208,#92209,
#92210,#92211,#92212,#92213,#92214,#92215,#92216,#92217,#92218,#92219,#92220,
#92221,#92222,#92223,#92224,#92225,#92226,#92227,#92228,#92229,#92230,#92231,
#92232,#92233,#92234,#92235,#92236,#92237,#92238,#92239,#92240,#92241,#92242,
#92243,#92244,#92245,#92246,#92247,#92248,#92249,#92250,#92251,#92252,#92253,
#92254,#92255,#92256,#92257,#92258,#92259,#92260,#92261,#92262,#92263,#92264,
#92265,#92266,#92267,#92268,#92269,#92270,#92271,#92272,#92273,#92274,#92275,
#92276,#92277,#92278,#92279,#92280,#92281,#92282,#92283,#92284,#92285,#92286,
#92287,#92288,#92289,#92290,#92291,#92292,#92293,#92294,#92295,#92296,#92297,
#92298,#92299,#92300,#92301,#92302,#92303,#92304,#92305,#92306,#92307,#92308,
#92309,#92310,#92311,#92312,#92313,#92314,#92315,#92316,#92317,#92318,#92319,
#92320,#92321,#92322,#92323,#92324,#92325,#92326,#92327,#92328,#92329,#92330,
#92331,#92332,#92333,#92334,#92335,#92336,#92337,#92338,#92339,#92340,#92341,
#92342,#92343,#92344,#92345,#92346,#92347,#92348,#92349,#92350,#92351,#92352,
#92353,#92354,#92355,#92356,#92357,#92358,#92359,#92360,#92361,#92362,#92363,
#92364,#92365,#92366,#92367,#92368,#92369,#92370,#92371,#92372,#92373,#92374,
#92375,#92376,#92377,#92378,#92379,#92380,#92381,#92382,#92383,#92384,#92385,
#92386,#92387,#92388,#92389,#92390,#92391,#92392,#92393,#92394,#92395,#92396,
#92397,#92398,#92399,#92400,#92401,#92402,#92403,#92404,#92405,#92406,#92407,
#92408,#92409,#92410,#92411,#92412,#92413,#92414,#92415,#92416,#92417,#92418,
#92419,#92420,#92421,#92422,#92423,#92424,#92425,#92426,#92427,#92428,#92429,
#92430,#92431,#92432,#92433,#92434,#92435,#92436,#92437,#92438,#92439,#92440,
#92441,#92442,#92443,#92444,#92445,#92446,#92447,#92448,#92449,#92450,#92451,
#92452,#92453,#92454,#92455,#92456,#92457,#92458,#92459,#92460,#92461,#92462,
#92463,#92464,#92465,#92466,#92467,#92468,#92469,#92470,#92471,#92472,#92473,
#92474,#92475,#92476,#92477,#92478,#92479,#92480,#92481,#92482,#92483,#92484,
#92485,#92486,#92487,#92488,#92489,#92490,#92491,#92492,#92493,#92494,#92495,
#92496,#92497,#92498,#92499,#92500,#92501,#92502,#92503,#92504,#92505,#92506,
#92507,#92508,#92509,#92510,#92511,#92512,#92513,#92514,#92515,#92516,#92517,
#92518,#92519,#92520,#92521,#92522,#92523,#92524,#92525,#92526,#92527,#92528,
#92529,#92530,#92531,#92532,#92533,#92534,#92535,#92536,#92537,#92538,#92539,
#92540,#92541,#92542,#92543,#92544,#92545,#92546,#92547,#92548,#92549,#92550,
#92551,#92552,#92553,#92554,#92555,#92556,#92557,#92558,#92559,#92560,#92561,
#92562,#92563,#92564,#92565,#92566,#92567,#92568,#92569,#92570,#92571,#92572,
#92573,#92574,#92575,#92576,#92577,#92578,#92579,#92580,#92581,#92582,#92583,
#92584,#92585,#92586,#92587,#92588,#92589,#92590,#92591,#92592,#92593,#92594,
#92595,#92596,#92597,#92598,#92599,#92600,#92601,#92602,#92603,#92604,#92605,
#92606,#92607,#92608,#92609,#92610,#92611,#92612,#92613,#92614,#92615,#92616,
#92617,#92618,#92619,#92620,#92621,#92622,#92623,#92624,#92625,#92626,#92627,
#92628,#92629,#92630,#92631,#92632,#92633,#92634,#92635,#92636,#92637,#92638,
#92639,#92640,#92641,#92642,#92643,#92644,#92645,#92646,#92647,#92648,#92649,
#92650,#92651,#92652,#92653,#92654,#92655,#92656,#92657,#92658,#92659,#92660,
#92661,#92662,#92663,#92664,#92665,#92666,#92667,#92668,#92669,#92670,#92671,
#92672,#92673,#92674,#92675,#92676,#92677,#92678,#92679,#92680,#92681,#92682,
#92683,#92684,#92685,#92686,#92687,#92688,#92689,#92690,#92691,#92692,#92693,
#92694,#92695,#92696,#92697,#92698,#92699,#92700,#92701,#92702,#92703,#92704,
#92705,#92706,#92707,#92708,#92709,#92710,#92711,#92712,#92713,#92714,#92715,
#92716,#92717,#92718,#92719,#92720,#92721,#92722,#92723,#92724,#92725,#92726,
#92727,#92728,#92729,#92730,#92731,#92732,#92733,#92734,#92735,#92736,#92737,
#92738,#92739,#92740,#92741,#92742,#92743,#92744,#92745,#92746,#92747,#92748,
#92749,#92750,#92751,#92752,#92753,#92754,#92755,#92756,#92757,#92758,#92759,
#92760,#92761,#92762,#92763,#92764,#92765,#92766,#92767,#92768,#92769,#92770,
#92771,#92772,#92773,#92774,#92775,#92776,#92777,#92778,#92779,#92780,#92781,
#92782,#92783,#92784,#92785,#92786,#92787,#92788,#92789,#92790,#92791,#92792,
#92793,#92794,#92795,#92796,#92797,#92798,#92799,#92800,#92801,#92802,#92803,
#92804,#92805,#92806,#92807,#92808,#92809,#92810,#92811,#92812,#92813,#92814,
#92815,#92816,#92817,#92818,#92819,#92820,#92821,#92822,#92823,#92824,#92825,
#92826,#92827,#92828,#92829,#92830,#92831,#92832,#92833,#92834,#92835,#92836,
#92837,#92838,#92839,#92840,#92841,#92842,#92843,#92844,#92845,#92846,#92847,
#92848,#92849,#92850,#92851,#92852,#92853,#92854,#92855,#92856,#92857,#92858,
#92859,#92860,#92861,#92862,#92863,#92864,#92865,#92866,#92867,#92868,#92869,
#92870,#92871,#92872));
#99385=AXIS2_PLACEMENT_3D('',#371607,#116568,#116569);
#99386=AXIS2_PLACEMENT_3D('',#371608,#116570,#116571);
#99387=AXIS2_PLACEMENT_3D('',#371616,#116573,#116574);
#99388=AXIS2_PLACEMENT_3D('',#371617,#116575,#116576);
#99389=AXIS2_PLACEMENT_3D('',#371647,#116578,#116579);
#99390=AXIS2_PLACEMENT_3D('',#371677,#116581,#116582);
#99391=AXIS2_PLACEMENT_3D('',#371707,#116584,#116585);
#99392=AXIS2_PLACEMENT_3D('',#371737,#116587,#116588);
#99393=AXIS2_PLACEMENT_3D('',#371767,#116590,#116591);
#99394=AXIS2_PLACEMENT_3D('',#371797,#116593,#116594);
#99395=AXIS2_PLACEMENT_3D('',#371827,#116596,#116597);
#99396=AXIS2_PLACEMENT_3D('',#371857,#116599,#116600);
#99397=AXIS2_PLACEMENT_3D('',#371887,#116602,#116603);
#99398=AXIS2_PLACEMENT_3D('',#371917,#116605,#116606);
#99399=AXIS2_PLACEMENT_3D('',#371947,#116608,#116609);
#99400=AXIS2_PLACEMENT_3D('',#371977,#116611,#116612);
#99401=AXIS2_PLACEMENT_3D('',#372007,#116614,#116615);
#99402=AXIS2_PLACEMENT_3D('',#372037,#116617,#116618);
#99403=AXIS2_PLACEMENT_3D('',#372067,#116620,#116621);
#99404=AXIS2_PLACEMENT_3D('',#372097,#116623,#116624);
#99405=AXIS2_PLACEMENT_3D('',#372127,#116626,#116627);
#99406=AXIS2_PLACEMENT_3D('',#372157,#116629,#116630);
#99407=AXIS2_PLACEMENT_3D('',#372187,#116632,#116633);
#99408=AXIS2_PLACEMENT_3D('',#372217,#116635,#116636);
#99409=AXIS2_PLACEMENT_3D('',#372247,#116638,#116639);
#99410=AXIS2_PLACEMENT_3D('',#372277,#116641,#116642);
#99411=AXIS2_PLACEMENT_3D('',#372307,#116644,#116645);
#99412=AXIS2_PLACEMENT_3D('',#372337,#116647,#116648);
#99413=AXIS2_PLACEMENT_3D('',#372367,#116650,#116651);
#99414=AXIS2_PLACEMENT_3D('',#372397,#116653,#116654);
#99415=AXIS2_PLACEMENT_3D('',#372427,#116656,#116657);
#99416=AXIS2_PLACEMENT_3D('',#372457,#116659,#116660);
#99417=AXIS2_PLACEMENT_3D('',#372483,#116662,#116663);
#99418=AXIS2_PLACEMENT_3D('',#372486,#116665,#116666);
#99419=AXIS2_PLACEMENT_3D('',#372488,#116667,#116668);
#99420=AXIS2_PLACEMENT_3D('',#372505,#116669,#116670);
#99421=AXIS2_PLACEMENT_3D('',#372581,#116672,#116673);
#99422=AXIS2_PLACEMENT_3D('',#372657,#116675,#116676);
#99423=AXIS2_PLACEMENT_3D('',#372735,#116678,#116679);
#99424=AXIS2_PLACEMENT_3D('',#372813,#116681,#116682);
#99425=AXIS2_PLACEMENT_3D('',#372889,#116684,#116685);
#99426=AXIS2_PLACEMENT_3D('',#372965,#116687,#116688);
#99427=AXIS2_PLACEMENT_3D('',#373041,#116690,#116691);
#99428=AXIS2_PLACEMENT_3D('',#373117,#116693,#116694);
#99429=AXIS2_PLACEMENT_3D('',#373193,#116696,#116697);
#99430=AXIS2_PLACEMENT_3D('',#373273,#116699,#116700);
#99431=AXIS2_PLACEMENT_3D('',#373349,#116702,#116703);
#99432=AXIS2_PLACEMENT_3D('',#373425,#116705,#116706);
#99433=AXIS2_PLACEMENT_3D('',#373501,#116708,#116709);
#99434=AXIS2_PLACEMENT_3D('',#373577,#116711,#116712);
#99435=AXIS2_PLACEMENT_3D('',#373653,#116714,#116715);
#99436=AXIS2_PLACEMENT_3D('',#373729,#116717,#116718);
#99437=AXIS2_PLACEMENT_3D('',#373809,#116720,#116721);
#99438=AXIS2_PLACEMENT_3D('',#373885,#116723,#116724);
#99439=AXIS2_PLACEMENT_3D('',#373961,#116726,#116727);
#99440=AXIS2_PLACEMENT_3D('',#374037,#116729,#116730);
#99441=AXIS2_PLACEMENT_3D('',#374113,#116732,#116733);
#99442=AXIS2_PLACEMENT_3D('',#374189,#116735,#116736);
#99443=AXIS2_PLACEMENT_3D('',#374267,#116738,#116739);
#99444=AXIS2_PLACEMENT_3D('',#374345,#116741,#116742);
#99445=AXIS2_PLACEMENT_3D('',#374421,#116744,#116745);
#99446=AXIS2_PLACEMENT_3D('',#374497,#116747,#116748);
#99447=AXIS2_PLACEMENT_3D('',#374573,#116750,#116751);
#99448=AXIS2_PLACEMENT_3D('',#374592,#116753,#116754);
#99449=AXIS2_PLACEMENT_3D('',#374603,#116755,#116756);
#99450=AXIS2_PLACEMENT_3D('',#374635,#116758,#116759);
#99451=AXIS2_PLACEMENT_3D('',#374636,#116760,#116761);
#99452=AXIS2_PLACEMENT_3D('',#374637,#116762,#116763);
#99453=AXIS2_PLACEMENT_3D('',#374654,#116764,#116765);
#99454=AXIS2_PLACEMENT_3D('',#374669,#116766,#116767);
#99455=AXIS2_PLACEMENT_3D('',#374702,#116768,#116769);
#99456=AXIS2_PLACEMENT_3D('',#374771,#116770,#116771);
#99457=AXIS2_PLACEMENT_3D('',#374773,#116772,#116773);
#99458=AXIS2_PLACEMENT_3D('',#374774,#116774,#116775);
#99459=AXIS2_PLACEMENT_3D('',#374775,#116776,#116777);
#99460=AXIS2_PLACEMENT_3D('',#374780,#116779,#116780);
#99461=AXIS2_PLACEMENT_3D('',#374782,#116781,#116782);
#99462=AXIS2_PLACEMENT_3D('',#374784,#116783,#116784);
#99463=AXIS2_PLACEMENT_3D('',#374786,#116785,#116786);
#99464=AXIS2_PLACEMENT_3D('',#374788,#116787,#116788);
#99465=AXIS2_PLACEMENT_3D('',#374789,#116789,#116790);
#99466=AXIS2_PLACEMENT_3D('',#374790,#116791,#116792);
#99467=AXIS2_PLACEMENT_3D('',#374796,#116793,#116794);
#99468=AXIS2_PLACEMENT_3D('',#374797,#116795,#116796);
#99469=AXIS2_PLACEMENT_3D('',#374799,#116797,#116798);
#99470=AXIS2_PLACEMENT_3D('',#374801,#116799,#116800);
#99471=AXIS2_PLACEMENT_3D('',#374802,#116801,#116802);
#99472=AXIS2_PLACEMENT_3D('',#374803,#116803,#116804);
#99473=AXIS2_PLACEMENT_3D('',#374805,#116805,#116806);
#99474=AXIS2_PLACEMENT_3D('',#374807,#116808,#116809);
#99475=AXIS2_PLACEMENT_3D('',#374809,#116810,#116811);
#99476=AXIS2_PLACEMENT_3D('',#374810,#116812,#116813);
#99477=AXIS2_PLACEMENT_3D('',#374811,#116814,#116815);
#99478=AXIS2_PLACEMENT_3D('',#374814,#116816,#116817);
#99479=AXIS2_PLACEMENT_3D('',#374824,#116818,#116819);
#99480=AXIS2_PLACEMENT_3D('',#374834,#116820,#116821);
#99481=AXIS2_PLACEMENT_3D('',#374844,#116822,#116823);
#99482=AXIS2_PLACEMENT_3D('',#374854,#116824,#116825);
#99483=AXIS2_PLACEMENT_3D('',#374864,#116826,#116827);
#99484=AXIS2_PLACEMENT_3D('',#374874,#116828,#116829);
#99485=AXIS2_PLACEMENT_3D('',#374884,#116830,#116831);
#99486=AXIS2_PLACEMENT_3D('',#374894,#116832,#116833);
#99487=AXIS2_PLACEMENT_3D('',#374904,#116834,#116835);
#99488=AXIS2_PLACEMENT_3D('',#374914,#116836,#116837);
#99489=AXIS2_PLACEMENT_3D('',#374924,#116838,#116839);
#99490=AXIS2_PLACEMENT_3D('',#374934,#116840,#116841);
#99491=AXIS2_PLACEMENT_3D('',#374944,#116842,#116843);
#99492=AXIS2_PLACEMENT_3D('',#374954,#116844,#116845);
#99493=AXIS2_PLACEMENT_3D('',#374964,#116846,#116847);
#99494=AXIS2_PLACEMENT_3D('',#374974,#116848,#116849);
#99495=AXIS2_PLACEMENT_3D('',#374984,#116850,#116851);
#99496=AXIS2_PLACEMENT_3D('',#374994,#116852,#116853);
#99497=AXIS2_PLACEMENT_3D('',#375004,#116854,#116855);
#99498=AXIS2_PLACEMENT_3D('',#375014,#116856,#116857);
#99499=AXIS2_PLACEMENT_3D('',#375024,#116858,#116859);
#99500=AXIS2_PLACEMENT_3D('',#375034,#116860,#116861);
#99501=AXIS2_PLACEMENT_3D('',#375044,#116862,#116863);
#99502=AXIS2_PLACEMENT_3D('',#375054,#116864,#116865);
#99503=AXIS2_PLACEMENT_3D('',#375064,#116866,#116867);
#99504=AXIS2_PLACEMENT_3D('',#375074,#116868,#116869);
#99505=AXIS2_PLACEMENT_3D('',#375084,#116870,#116871);
#99506=AXIS2_PLACEMENT_3D('',#375094,#116872,#116873);
#99507=AXIS2_PLACEMENT_3D('',#375104,#116874,#116875);
#99508=AXIS2_PLACEMENT_3D('',#375114,#116876,#116877);
#99509=AXIS2_PLACEMENT_3D('',#375124,#116878,#116879);
#99510=AXIS2_PLACEMENT_3D('',#375134,#116880,#116881);
#99511=AXIS2_PLACEMENT_3D('',#375144,#116882,#116883);
#99512=AXIS2_PLACEMENT_3D('',#375154,#116884,#116885);
#99513=AXIS2_PLACEMENT_3D('',#375164,#116886,#116887);
#99514=AXIS2_PLACEMENT_3D('',#375174,#116888,#116889);
#99515=AXIS2_PLACEMENT_3D('',#375184,#116890,#116891);
#99516=AXIS2_PLACEMENT_3D('',#375194,#116892,#116893);
#99517=AXIS2_PLACEMENT_3D('',#375204,#116894,#116895);
#99518=AXIS2_PLACEMENT_3D('',#375214,#116896,#116897);
#99519=AXIS2_PLACEMENT_3D('',#375224,#116898,#116899);
#99520=AXIS2_PLACEMENT_3D('',#375234,#116900,#116901);
#99521=AXIS2_PLACEMENT_3D('',#375244,#116902,#116903);
#99522=AXIS2_PLACEMENT_3D('',#375254,#116904,#116905);
#99523=AXIS2_PLACEMENT_3D('',#375264,#116906,#116907);
#99524=AXIS2_PLACEMENT_3D('',#375274,#116908,#116909);
#99525=AXIS2_PLACEMENT_3D('',#375284,#116910,#116911);
#99526=AXIS2_PLACEMENT_3D('',#375294,#116912,#116913);
#99527=AXIS2_PLACEMENT_3D('',#375304,#116914,#116915);
#99528=AXIS2_PLACEMENT_3D('',#375314,#116916,#116917);
#99529=AXIS2_PLACEMENT_3D('',#375324,#116918,#116919);
#99530=AXIS2_PLACEMENT_3D('',#375334,#116920,#116921);
#99531=AXIS2_PLACEMENT_3D('',#375344,#116922,#116923);
#99532=AXIS2_PLACEMENT_3D('',#375354,#116924,#116925);
#99533=AXIS2_PLACEMENT_3D('',#375364,#116926,#116927);
#99534=AXIS2_PLACEMENT_3D('',#375374,#116928,#116929);
#99535=AXIS2_PLACEMENT_3D('',#375384,#116930,#116931);
#99536=AXIS2_PLACEMENT_3D('',#375394,#116932,#116933);
#99537=AXIS2_PLACEMENT_3D('',#375404,#116934,#116935);
#99538=AXIS2_PLACEMENT_3D('',#375414,#116936,#116937);
#99539=AXIS2_PLACEMENT_3D('',#375424,#116938,#116939);
#99540=AXIS2_PLACEMENT_3D('',#375434,#116940,#116941);
#99541=AXIS2_PLACEMENT_3D('',#375444,#116942,#116943);
#99542=AXIS2_PLACEMENT_3D('',#375454,#116944,#116945);
#99543=AXIS2_PLACEMENT_3D('',#375464,#116946,#116947);
#99544=AXIS2_PLACEMENT_3D('',#375474,#116948,#116949);
#99545=AXIS2_PLACEMENT_3D('',#375484,#116950,#116951);
#99546=AXIS2_PLACEMENT_3D('',#375494,#116952,#116953);
#99547=AXIS2_PLACEMENT_3D('',#375504,#116954,#116955);
#99548=AXIS2_PLACEMENT_3D('',#375514,#116956,#116957);
#99549=AXIS2_PLACEMENT_3D('',#375524,#116958,#116959);
#99550=AXIS2_PLACEMENT_3D('',#375534,#116960,#116961);
#99551=AXIS2_PLACEMENT_3D('',#375544,#116962,#116963);
#99552=AXIS2_PLACEMENT_3D('',#375554,#116964,#116965);
#99553=AXIS2_PLACEMENT_3D('',#375564,#116966,#116967);
#99554=AXIS2_PLACEMENT_3D('',#375574,#116968,#116969);
#99555=AXIS2_PLACEMENT_3D('',#375584,#116970,#116971);
#99556=AXIS2_PLACEMENT_3D('',#375594,#116972,#116973);
#99557=AXIS2_PLACEMENT_3D('',#375604,#116974,#116975);
#99558=AXIS2_PLACEMENT_3D('',#375614,#116976,#116977);
#99559=AXIS2_PLACEMENT_3D('',#375624,#116978,#116979);
#99560=AXIS2_PLACEMENT_3D('',#375634,#116980,#116981);
#99561=AXIS2_PLACEMENT_3D('',#375644,#116982,#116983);
#99562=AXIS2_PLACEMENT_3D('',#375654,#116984,#116985);
#99563=AXIS2_PLACEMENT_3D('',#375664,#116986,#116987);
#99564=AXIS2_PLACEMENT_3D('',#375674,#116988,#116989);
#99565=AXIS2_PLACEMENT_3D('',#375684,#116990,#116991);
#99566=AXIS2_PLACEMENT_3D('',#375694,#116992,#116993);
#99567=AXIS2_PLACEMENT_3D('',#375704,#116994,#116995);
#99568=AXIS2_PLACEMENT_3D('',#375714,#116996,#116997);
#99569=AXIS2_PLACEMENT_3D('',#375724,#116998,#116999);
#99570=AXIS2_PLACEMENT_3D('',#375734,#117000,#117001);
#99571=AXIS2_PLACEMENT_3D('',#375744,#117002,#117003);
#99572=AXIS2_PLACEMENT_3D('',#375754,#117004,#117005);
#99573=AXIS2_PLACEMENT_3D('',#375764,#117006,#117007);
#99574=AXIS2_PLACEMENT_3D('',#375774,#117008,#117009);
#99575=AXIS2_PLACEMENT_3D('',#375784,#117010,#117011);
#99576=AXIS2_PLACEMENT_3D('',#375794,#117012,#117013);
#99577=AXIS2_PLACEMENT_3D('',#375798,#117015,#117016);
#99578=AXIS2_PLACEMENT_3D('',#375799,#117017,#117018);
#99579=AXIS2_PLACEMENT_3D('',#375801,#117019,#117020);
#99580=AXIS2_PLACEMENT_3D('',#375811,#117021,#117022);
#99581=AXIS2_PLACEMENT_3D('',#375821,#117023,#117024);
#99582=AXIS2_PLACEMENT_3D('',#375831,#117025,#117026);
#99583=AXIS2_PLACEMENT_3D('',#375841,#117027,#117028);
#99584=AXIS2_PLACEMENT_3D('',#375851,#117029,#117030);
#99585=AXIS2_PLACEMENT_3D('',#375861,#117031,#117032);
#99586=AXIS2_PLACEMENT_3D('',#375871,#117033,#117034);
#99587=AXIS2_PLACEMENT_3D('',#375881,#117035,#117036);
#99588=AXIS2_PLACEMENT_3D('',#375891,#117037,#117038);
#99589=AXIS2_PLACEMENT_3D('',#375901,#117039,#117040);
#99590=AXIS2_PLACEMENT_3D('',#375911,#117041,#117042);
#99591=AXIS2_PLACEMENT_3D('',#375921,#117043,#117044);
#99592=AXIS2_PLACEMENT_3D('',#375931,#117045,#117046);
#99593=AXIS2_PLACEMENT_3D('',#375941,#117047,#117048);
#99594=AXIS2_PLACEMENT_3D('',#375951,#117049,#117050);
#99595=AXIS2_PLACEMENT_3D('',#375961,#117051,#117052);
#99596=AXIS2_PLACEMENT_3D('',#375971,#117053,#117054);
#99597=AXIS2_PLACEMENT_3D('',#375981,#117055,#117056);
#99598=AXIS2_PLACEMENT_3D('',#375991,#117057,#117058);
#99599=AXIS2_PLACEMENT_3D('',#376001,#117059,#117060);
#99600=AXIS2_PLACEMENT_3D('',#376011,#117061,#117062);
#99601=AXIS2_PLACEMENT_3D('',#376021,#117063,#117064);
#99602=AXIS2_PLACEMENT_3D('',#376031,#117065,#117066);
#99603=AXIS2_PLACEMENT_3D('',#376041,#117067,#117068);
#99604=AXIS2_PLACEMENT_3D('',#376051,#117069,#117070);
#99605=AXIS2_PLACEMENT_3D('',#376061,#117071,#117072);
#99606=AXIS2_PLACEMENT_3D('',#376071,#117073,#117074);
#99607=AXIS2_PLACEMENT_3D('',#376081,#117075,#117076);
#99608=AXIS2_PLACEMENT_3D('',#376091,#117077,#117078);
#99609=AXIS2_PLACEMENT_3D('',#376101,#117079,#117080);
#99610=AXIS2_PLACEMENT_3D('',#376111,#117081,#117082);
#99611=AXIS2_PLACEMENT_3D('',#376121,#117083,#117084);
#99612=AXIS2_PLACEMENT_3D('',#376131,#117085,#117086);
#99613=AXIS2_PLACEMENT_3D('',#376141,#117087,#117088);
#99614=AXIS2_PLACEMENT_3D('',#376151,#117089,#117090);
#99615=AXIS2_PLACEMENT_3D('',#376161,#117091,#117092);
#99616=AXIS2_PLACEMENT_3D('',#376171,#117093,#117094);
#99617=AXIS2_PLACEMENT_3D('',#376181,#117095,#117096);
#99618=AXIS2_PLACEMENT_3D('',#376191,#117097,#117098);
#99619=AXIS2_PLACEMENT_3D('',#376201,#117099,#117100);
#99620=AXIS2_PLACEMENT_3D('',#376211,#117101,#117102);
#99621=AXIS2_PLACEMENT_3D('',#376221,#117103,#117104);
#99622=AXIS2_PLACEMENT_3D('',#376231,#117105,#117106);
#99623=AXIS2_PLACEMENT_3D('',#376241,#117107,#117108);
#99624=AXIS2_PLACEMENT_3D('',#376251,#117109,#117110);
#99625=AXIS2_PLACEMENT_3D('',#376261,#117111,#117112);
#99626=AXIS2_PLACEMENT_3D('',#376271,#117113,#117114);
#99627=AXIS2_PLACEMENT_3D('',#376281,#117115,#117116);
#99628=AXIS2_PLACEMENT_3D('',#376291,#117117,#117118);
#99629=AXIS2_PLACEMENT_3D('',#376301,#117119,#117120);
#99630=AXIS2_PLACEMENT_3D('',#376311,#117121,#117122);
#99631=AXIS2_PLACEMENT_3D('',#376321,#117123,#117124);
#99632=AXIS2_PLACEMENT_3D('',#376331,#117125,#117126);
#99633=AXIS2_PLACEMENT_3D('',#376341,#117127,#117128);
#99634=AXIS2_PLACEMENT_3D('',#376351,#117129,#117130);
#99635=AXIS2_PLACEMENT_3D('',#376361,#117131,#117132);
#99636=AXIS2_PLACEMENT_3D('',#376371,#117133,#117134);
#99637=AXIS2_PLACEMENT_3D('',#376381,#117135,#117136);
#99638=AXIS2_PLACEMENT_3D('',#376391,#117137,#117138);
#99639=AXIS2_PLACEMENT_3D('',#376401,#117139,#117140);
#99640=AXIS2_PLACEMENT_3D('',#376411,#117141,#117142);
#99641=AXIS2_PLACEMENT_3D('',#376421,#117143,#117144);
#99642=AXIS2_PLACEMENT_3D('',#376431,#117145,#117146);
#99643=AXIS2_PLACEMENT_3D('',#376441,#117147,#117148);
#99644=AXIS2_PLACEMENT_3D('',#376451,#117149,#117150);
#99645=AXIS2_PLACEMENT_3D('',#376461,#117151,#117152);
#99646=AXIS2_PLACEMENT_3D('',#376471,#117153,#117154);
#99647=AXIS2_PLACEMENT_3D('',#376481,#117155,#117156);
#99648=AXIS2_PLACEMENT_3D('',#376491,#117157,#117158);
#99649=AXIS2_PLACEMENT_3D('',#376501,#117159,#117160);
#99650=AXIS2_PLACEMENT_3D('',#376511,#117161,#117162);
#99651=AXIS2_PLACEMENT_3D('',#376521,#117163,#117164);
#99652=AXIS2_PLACEMENT_3D('',#376531,#117165,#117166);
#99653=AXIS2_PLACEMENT_3D('',#376541,#117167,#117168);
#99654=AXIS2_PLACEMENT_3D('',#376551,#117169,#117170);
#99655=AXIS2_PLACEMENT_3D('',#376561,#117171,#117172);
#99656=AXIS2_PLACEMENT_3D('',#376571,#117173,#117174);
#99657=AXIS2_PLACEMENT_3D('',#376581,#117175,#117176);
#99658=AXIS2_PLACEMENT_3D('',#376591,#117177,#117178);
#99659=AXIS2_PLACEMENT_3D('',#376601,#117179,#117180);
#99660=AXIS2_PLACEMENT_3D('',#376611,#117181,#117182);
#99661=AXIS2_PLACEMENT_3D('',#376621,#117183,#117184);
#99662=AXIS2_PLACEMENT_3D('',#376631,#117185,#117186);
#99663=AXIS2_PLACEMENT_3D('',#376641,#117187,#117188);
#99664=AXIS2_PLACEMENT_3D('',#376651,#117189,#117190);
#99665=AXIS2_PLACEMENT_3D('',#376661,#117191,#117192);
#99666=AXIS2_PLACEMENT_3D('',#376671,#117193,#117194);
#99667=AXIS2_PLACEMENT_3D('',#376681,#117195,#117196);
#99668=AXIS2_PLACEMENT_3D('',#376691,#117197,#117198);
#99669=AXIS2_PLACEMENT_3D('',#376701,#117199,#117200);
#99670=AXIS2_PLACEMENT_3D('',#376711,#117201,#117202);
#99671=AXIS2_PLACEMENT_3D('',#376721,#117203,#117204);
#99672=AXIS2_PLACEMENT_3D('',#376731,#117205,#117206);
#99673=AXIS2_PLACEMENT_3D('',#376741,#117207,#117208);
#99674=AXIS2_PLACEMENT_3D('',#376751,#117209,#117210);
#99675=AXIS2_PLACEMENT_3D('',#376761,#117211,#117212);
#99676=AXIS2_PLACEMENT_3D('',#376771,#117213,#117214);
#99677=AXIS2_PLACEMENT_3D('',#376779,#117215,#117216);
#99678=AXIS2_PLACEMENT_3D('',#376781,#117217,#117218);
#99679=AXIS2_PLACEMENT_3D('',#376782,#117219,#117220);
#99680=AXIS2_PLACEMENT_3D('',#376783,#117221,#117222);
#99681=AXIS2_PLACEMENT_3D('',#376786,#117223,#117224);
#99682=AXIS2_PLACEMENT_3D('',#376790,#117226,#117227);
#99683=AXIS2_PLACEMENT_3D('',#376792,#117228,#117229);
#99684=AXIS2_PLACEMENT_3D('',#376794,#117230,#117231);
#99685=AXIS2_PLACEMENT_3D('',#376798,#117233,#117234);
#99686=AXIS2_PLACEMENT_3D('',#376802,#117236,#117237);
#99687=AXIS2_PLACEMENT_3D('',#376804,#117238,#117239);
#99688=AXIS2_PLACEMENT_3D('',#376806,#117240,#117241);
#99689=AXIS2_PLACEMENT_3D('',#376810,#117243,#117244);
#99690=AXIS2_PLACEMENT_3D('',#376814,#117246,#117247);
#99691=AXIS2_PLACEMENT_3D('',#376816,#117248,#117249);
#99692=AXIS2_PLACEMENT_3D('',#376818,#117250,#117251);
#99693=AXIS2_PLACEMENT_3D('',#376822,#117253,#117254);
#99694=AXIS2_PLACEMENT_3D('',#376826,#117256,#117257);
#99695=AXIS2_PLACEMENT_3D('',#376828,#117258,#117259);
#99696=AXIS2_PLACEMENT_3D('',#376830,#117260,#117261);
#99697=AXIS2_PLACEMENT_3D('',#376834,#117263,#117264);
#99698=AXIS2_PLACEMENT_3D('',#376838,#117266,#117267);
#99699=AXIS2_PLACEMENT_3D('',#376840,#117268,#117269);
#99700=AXIS2_PLACEMENT_3D('',#376842,#117270,#117271);
#99701=AXIS2_PLACEMENT_3D('',#376846,#117273,#117274);
#99702=AXIS2_PLACEMENT_3D('',#376850,#117276,#117277);
#99703=AXIS2_PLACEMENT_3D('',#376852,#117278,#117279);
#99704=AXIS2_PLACEMENT_3D('',#376854,#117280,#117281);
#99705=AXIS2_PLACEMENT_3D('',#376858,#117283,#117284);
#99706=AXIS2_PLACEMENT_3D('',#376862,#117286,#117287);
#99707=AXIS2_PLACEMENT_3D('',#376864,#117288,#117289);
#99708=AXIS2_PLACEMENT_3D('',#376866,#117290,#117291);
#99709=AXIS2_PLACEMENT_3D('',#376870,#117293,#117294);
#99710=AXIS2_PLACEMENT_3D('',#376874,#117296,#117297);
#99711=AXIS2_PLACEMENT_3D('',#376876,#117298,#117299);
#99712=AXIS2_PLACEMENT_3D('',#376878,#117300,#117301);
#99713=AXIS2_PLACEMENT_3D('',#376882,#117303,#117304);
#99714=AXIS2_PLACEMENT_3D('',#376886,#117306,#117307);
#99715=AXIS2_PLACEMENT_3D('',#376888,#117308,#117309);
#99716=AXIS2_PLACEMENT_3D('',#376890,#117310,#117311);
#99717=AXIS2_PLACEMENT_3D('',#376894,#117313,#117314);
#99718=AXIS2_PLACEMENT_3D('',#376898,#117316,#117317);
#99719=AXIS2_PLACEMENT_3D('',#376900,#117318,#117319);
#99720=AXIS2_PLACEMENT_3D('',#376902,#117320,#117321);
#99721=AXIS2_PLACEMENT_3D('',#376906,#117323,#117324);
#99722=AXIS2_PLACEMENT_3D('',#376910,#117326,#117327);
#99723=AXIS2_PLACEMENT_3D('',#376912,#117328,#117329);
#99724=AXIS2_PLACEMENT_3D('',#376914,#117330,#117331);
#99725=AXIS2_PLACEMENT_3D('',#376918,#117333,#117334);
#99726=AXIS2_PLACEMENT_3D('',#376922,#117336,#117337);
#99727=AXIS2_PLACEMENT_3D('',#376924,#117338,#117339);
#99728=AXIS2_PLACEMENT_3D('',#376926,#117340,#117341);
#99729=AXIS2_PLACEMENT_3D('',#376930,#117343,#117344);
#99730=AXIS2_PLACEMENT_3D('',#376934,#117346,#117347);
#99731=AXIS2_PLACEMENT_3D('',#376936,#117348,#117349);
#99732=AXIS2_PLACEMENT_3D('',#376938,#117350,#117351);
#99733=AXIS2_PLACEMENT_3D('',#376942,#117353,#117354);
#99734=AXIS2_PLACEMENT_3D('',#376946,#117356,#117357);
#99735=AXIS2_PLACEMENT_3D('',#376948,#117358,#117359);
#99736=AXIS2_PLACEMENT_3D('',#376950,#117360,#117361);
#99737=AXIS2_PLACEMENT_3D('',#376954,#117363,#117364);
#99738=AXIS2_PLACEMENT_3D('',#376958,#117366,#117367);
#99739=AXIS2_PLACEMENT_3D('',#376960,#117368,#117369);
#99740=AXIS2_PLACEMENT_3D('',#376962,#117370,#117371);
#99741=AXIS2_PLACEMENT_3D('',#376966,#117373,#117374);
#99742=AXIS2_PLACEMENT_3D('',#376970,#117376,#117377);
#99743=AXIS2_PLACEMENT_3D('',#376972,#117378,#117379);
#99744=AXIS2_PLACEMENT_3D('',#376974,#117380,#117381);
#99745=AXIS2_PLACEMENT_3D('',#376978,#117383,#117384);
#99746=AXIS2_PLACEMENT_3D('',#376982,#117386,#117387);
#99747=AXIS2_PLACEMENT_3D('',#376984,#117388,#117389);
#99748=AXIS2_PLACEMENT_3D('',#376986,#117390,#117391);
#99749=AXIS2_PLACEMENT_3D('',#376990,#117393,#117394);
#99750=AXIS2_PLACEMENT_3D('',#376994,#117396,#117397);
#99751=AXIS2_PLACEMENT_3D('',#376996,#117398,#117399);
#99752=AXIS2_PLACEMENT_3D('',#376998,#117400,#117401);
#99753=AXIS2_PLACEMENT_3D('',#377002,#117403,#117404);
#99754=AXIS2_PLACEMENT_3D('',#377006,#117406,#117407);
#99755=AXIS2_PLACEMENT_3D('',#377008,#117408,#117409);
#99756=AXIS2_PLACEMENT_3D('',#377010,#117410,#117411);
#99757=AXIS2_PLACEMENT_3D('',#377014,#117413,#117414);
#99758=AXIS2_PLACEMENT_3D('',#377018,#117416,#117417);
#99759=AXIS2_PLACEMENT_3D('',#377020,#117418,#117419);
#99760=AXIS2_PLACEMENT_3D('',#377022,#117420,#117421);
#99761=AXIS2_PLACEMENT_3D('',#377026,#117423,#117424);
#99762=AXIS2_PLACEMENT_3D('',#377030,#117426,#117427);
#99763=AXIS2_PLACEMENT_3D('',#377032,#117428,#117429);
#99764=AXIS2_PLACEMENT_3D('',#377034,#117430,#117431);
#99765=AXIS2_PLACEMENT_3D('',#377038,#117433,#117434);
#99766=AXIS2_PLACEMENT_3D('',#377042,#117436,#117437);
#99767=AXIS2_PLACEMENT_3D('',#377044,#117438,#117439);
#99768=AXIS2_PLACEMENT_3D('',#377046,#117440,#117441);
#99769=AXIS2_PLACEMENT_3D('',#377050,#117443,#117444);
#99770=AXIS2_PLACEMENT_3D('',#377054,#117446,#117447);
#99771=AXIS2_PLACEMENT_3D('',#377056,#117448,#117449);
#99772=AXIS2_PLACEMENT_3D('',#377058,#117450,#117451);
#99773=AXIS2_PLACEMENT_3D('',#377062,#117453,#117454);
#99774=AXIS2_PLACEMENT_3D('',#377066,#117456,#117457);
#99775=AXIS2_PLACEMENT_3D('',#377068,#117458,#117459);
#99776=AXIS2_PLACEMENT_3D('',#377070,#117460,#117461);
#99777=AXIS2_PLACEMENT_3D('',#377074,#117463,#117464);
#99778=AXIS2_PLACEMENT_3D('',#377078,#117466,#117467);
#99779=AXIS2_PLACEMENT_3D('',#377080,#117468,#117469);
#99780=AXIS2_PLACEMENT_3D('',#377082,#117470,#117471);
#99781=AXIS2_PLACEMENT_3D('',#377086,#117473,#117474);
#99782=AXIS2_PLACEMENT_3D('',#377090,#117476,#117477);
#99783=AXIS2_PLACEMENT_3D('',#377092,#117478,#117479);
#99784=AXIS2_PLACEMENT_3D('',#377094,#117480,#117481);
#99785=AXIS2_PLACEMENT_3D('',#377098,#117483,#117484);
#99786=AXIS2_PLACEMENT_3D('',#377102,#117486,#117487);
#99787=AXIS2_PLACEMENT_3D('',#377104,#117488,#117489);
#99788=AXIS2_PLACEMENT_3D('',#377106,#117490,#117491);
#99789=AXIS2_PLACEMENT_3D('',#377110,#117493,#117494);
#99790=AXIS2_PLACEMENT_3D('',#377114,#117496,#117497);
#99791=AXIS2_PLACEMENT_3D('',#377116,#117498,#117499);
#99792=AXIS2_PLACEMENT_3D('',#377118,#117500,#117501);
#99793=AXIS2_PLACEMENT_3D('',#377122,#117503,#117504);
#99794=AXIS2_PLACEMENT_3D('',#377126,#117506,#117507);
#99795=AXIS2_PLACEMENT_3D('',#377128,#117508,#117509);
#99796=AXIS2_PLACEMENT_3D('',#377130,#117510,#117511);
#99797=AXIS2_PLACEMENT_3D('',#377134,#117513,#117514);
#99798=AXIS2_PLACEMENT_3D('',#377138,#117516,#117517);
#99799=AXIS2_PLACEMENT_3D('',#377140,#117518,#117519);
#99800=AXIS2_PLACEMENT_3D('',#377142,#117520,#117521);
#99801=AXIS2_PLACEMENT_3D('',#377146,#117523,#117524);
#99802=AXIS2_PLACEMENT_3D('',#377150,#117526,#117527);
#99803=AXIS2_PLACEMENT_3D('',#377152,#117528,#117529);
#99804=AXIS2_PLACEMENT_3D('',#377154,#117530,#117531);
#99805=AXIS2_PLACEMENT_3D('',#377158,#117533,#117534);
#99806=AXIS2_PLACEMENT_3D('',#377162,#117536,#117537);
#99807=AXIS2_PLACEMENT_3D('',#377164,#117538,#117539);
#99808=AXIS2_PLACEMENT_3D('',#377166,#117540,#117541);
#99809=AXIS2_PLACEMENT_3D('',#377170,#117543,#117544);
#99810=AXIS2_PLACEMENT_3D('',#377174,#117546,#117547);
#99811=AXIS2_PLACEMENT_3D('',#377176,#117548,#117549);
#99812=AXIS2_PLACEMENT_3D('',#377178,#117550,#117551);
#99813=AXIS2_PLACEMENT_3D('',#377182,#117553,#117554);
#99814=AXIS2_PLACEMENT_3D('',#377186,#117556,#117557);
#99815=AXIS2_PLACEMENT_3D('',#377188,#117558,#117559);
#99816=AXIS2_PLACEMENT_3D('',#377190,#117560,#117561);
#99817=AXIS2_PLACEMENT_3D('',#377194,#117563,#117564);
#99818=AXIS2_PLACEMENT_3D('',#377198,#117566,#117567);
#99819=AXIS2_PLACEMENT_3D('',#377200,#117568,#117569);
#99820=AXIS2_PLACEMENT_3D('',#377202,#117570,#117571);
#99821=AXIS2_PLACEMENT_3D('',#377206,#117573,#117574);
#99822=AXIS2_PLACEMENT_3D('',#377210,#117576,#117577);
#99823=AXIS2_PLACEMENT_3D('',#377212,#117578,#117579);
#99824=AXIS2_PLACEMENT_3D('',#377214,#117580,#117581);
#99825=AXIS2_PLACEMENT_3D('',#377218,#117583,#117584);
#99826=AXIS2_PLACEMENT_3D('',#377222,#117586,#117587);
#99827=AXIS2_PLACEMENT_3D('',#377224,#117588,#117589);
#99828=AXIS2_PLACEMENT_3D('',#377226,#117590,#117591);
#99829=AXIS2_PLACEMENT_3D('',#377230,#117593,#117594);
#99830=AXIS2_PLACEMENT_3D('',#377234,#117596,#117597);
#99831=AXIS2_PLACEMENT_3D('',#377236,#117598,#117599);
#99832=AXIS2_PLACEMENT_3D('',#377238,#117600,#117601);
#99833=AXIS2_PLACEMENT_3D('',#377242,#117603,#117604);
#99834=AXIS2_PLACEMENT_3D('',#377246,#117606,#117607);
#99835=AXIS2_PLACEMENT_3D('',#377248,#117608,#117609);
#99836=AXIS2_PLACEMENT_3D('',#377250,#117610,#117611);
#99837=AXIS2_PLACEMENT_3D('',#377254,#117613,#117614);
#99838=AXIS2_PLACEMENT_3D('',#377258,#117616,#117617);
#99839=AXIS2_PLACEMENT_3D('',#377260,#117618,#117619);
#99840=AXIS2_PLACEMENT_3D('',#377262,#117620,#117621);
#99841=AXIS2_PLACEMENT_3D('',#377266,#117623,#117624);
#99842=AXIS2_PLACEMENT_3D('',#377270,#117626,#117627);
#99843=AXIS2_PLACEMENT_3D('',#377272,#117628,#117629);
#99844=AXIS2_PLACEMENT_3D('',#377274,#117630,#117631);
#99845=AXIS2_PLACEMENT_3D('',#377278,#117633,#117634);
#99846=AXIS2_PLACEMENT_3D('',#377282,#117636,#117637);
#99847=AXIS2_PLACEMENT_3D('',#377284,#117638,#117639);
#99848=AXIS2_PLACEMENT_3D('',#377286,#117640,#117641);
#99849=AXIS2_PLACEMENT_3D('',#377290,#117643,#117644);
#99850=AXIS2_PLACEMENT_3D('',#377294,#117646,#117647);
#99851=AXIS2_PLACEMENT_3D('',#377296,#117648,#117649);
#99852=AXIS2_PLACEMENT_3D('',#377298,#117650,#117651);
#99853=AXIS2_PLACEMENT_3D('',#377302,#117653,#117654);
#99854=AXIS2_PLACEMENT_3D('',#377306,#117656,#117657);
#99855=AXIS2_PLACEMENT_3D('',#377308,#117658,#117659);
#99856=AXIS2_PLACEMENT_3D('',#377310,#117660,#117661);
#99857=AXIS2_PLACEMENT_3D('',#377314,#117663,#117664);
#99858=AXIS2_PLACEMENT_3D('',#377318,#117666,#117667);
#99859=AXIS2_PLACEMENT_3D('',#377320,#117668,#117669);
#99860=AXIS2_PLACEMENT_3D('',#377322,#117670,#117671);
#99861=AXIS2_PLACEMENT_3D('',#377326,#117673,#117674);
#99862=AXIS2_PLACEMENT_3D('',#377330,#117676,#117677);
#99863=AXIS2_PLACEMENT_3D('',#377332,#117678,#117679);
#99864=AXIS2_PLACEMENT_3D('',#377334,#117680,#117681);
#99865=AXIS2_PLACEMENT_3D('',#377338,#117683,#117684);
#99866=AXIS2_PLACEMENT_3D('',#377342,#117686,#117687);
#99867=AXIS2_PLACEMENT_3D('',#377344,#117688,#117689);
#99868=AXIS2_PLACEMENT_3D('',#377346,#117690,#117691);
#99869=AXIS2_PLACEMENT_3D('',#377350,#117693,#117694);
#99870=AXIS2_PLACEMENT_3D('',#377354,#117696,#117697);
#99871=AXIS2_PLACEMENT_3D('',#377356,#117698,#117699);
#99872=AXIS2_PLACEMENT_3D('',#377358,#117700,#117701);
#99873=AXIS2_PLACEMENT_3D('',#377362,#117703,#117704);
#99874=AXIS2_PLACEMENT_3D('',#377366,#117706,#117707);
#99875=AXIS2_PLACEMENT_3D('',#377368,#117708,#117709);
#99876=AXIS2_PLACEMENT_3D('',#377370,#117710,#117711);
#99877=AXIS2_PLACEMENT_3D('',#377374,#117713,#117714);
#99878=AXIS2_PLACEMENT_3D('',#377377,#117716,#117717);
#99879=AXIS2_PLACEMENT_3D('',#377381,#117719,#117720);
#99880=AXIS2_PLACEMENT_3D('',#377383,#117721,#117722);
#99881=AXIS2_PLACEMENT_3D('',#377385,#117723,#117724);
#99882=AXIS2_PLACEMENT_3D('',#377389,#117726,#117727);
#99883=AXIS2_PLACEMENT_3D('',#377393,#117729,#117730);
#99884=AXIS2_PLACEMENT_3D('',#377395,#117731,#117732);
#99885=AXIS2_PLACEMENT_3D('',#377397,#117733,#117734);
#99886=AXIS2_PLACEMENT_3D('',#377401,#117736,#117737);
#99887=AXIS2_PLACEMENT_3D('',#377405,#117739,#117740);
#99888=AXIS2_PLACEMENT_3D('',#377407,#117741,#117742);
#99889=AXIS2_PLACEMENT_3D('',#377409,#117743,#117744);
#99890=AXIS2_PLACEMENT_3D('',#377413,#117746,#117747);
#99891=AXIS2_PLACEMENT_3D('',#377417,#117749,#117750);
#99892=AXIS2_PLACEMENT_3D('',#377419,#117751,#117752);
#99893=AXIS2_PLACEMENT_3D('',#377421,#117753,#117754);
#99894=AXIS2_PLACEMENT_3D('',#377425,#117756,#117757);
#99895=AXIS2_PLACEMENT_3D('',#377429,#117759,#117760);
#99896=AXIS2_PLACEMENT_3D('',#377431,#117761,#117762);
#99897=AXIS2_PLACEMENT_3D('',#377433,#117763,#117764);
#99898=AXIS2_PLACEMENT_3D('',#377437,#117766,#117767);
#99899=AXIS2_PLACEMENT_3D('',#377441,#117769,#117770);
#99900=AXIS2_PLACEMENT_3D('',#377443,#117771,#117772);
#99901=AXIS2_PLACEMENT_3D('',#377445,#117773,#117774);
#99902=AXIS2_PLACEMENT_3D('',#377449,#117776,#117777);
#99903=AXIS2_PLACEMENT_3D('',#377453,#117779,#117780);
#99904=AXIS2_PLACEMENT_3D('',#377455,#117781,#117782);
#99905=AXIS2_PLACEMENT_3D('',#377457,#117783,#117784);
#99906=AXIS2_PLACEMENT_3D('',#377461,#117786,#117787);
#99907=AXIS2_PLACEMENT_3D('',#377465,#117789,#117790);
#99908=AXIS2_PLACEMENT_3D('',#377467,#117791,#117792);
#99909=AXIS2_PLACEMENT_3D('',#377469,#117793,#117794);
#99910=AXIS2_PLACEMENT_3D('',#377473,#117796,#117797);
#99911=AXIS2_PLACEMENT_3D('',#377477,#117799,#117800);
#99912=AXIS2_PLACEMENT_3D('',#377479,#117801,#117802);
#99913=AXIS2_PLACEMENT_3D('',#377481,#117803,#117804);
#99914=AXIS2_PLACEMENT_3D('',#377485,#117806,#117807);
#99915=AXIS2_PLACEMENT_3D('',#377489,#117809,#117810);
#99916=AXIS2_PLACEMENT_3D('',#377491,#117811,#117812);
#99917=AXIS2_PLACEMENT_3D('',#377493,#117813,#117814);
#99918=AXIS2_PLACEMENT_3D('',#377497,#117816,#117817);
#99919=AXIS2_PLACEMENT_3D('',#377501,#117819,#117820);
#99920=AXIS2_PLACEMENT_3D('',#377503,#117821,#117822);
#99921=AXIS2_PLACEMENT_3D('',#377505,#117823,#117824);
#99922=AXIS2_PLACEMENT_3D('',#377509,#117826,#117827);
#99923=AXIS2_PLACEMENT_3D('',#377513,#117829,#117830);
#99924=AXIS2_PLACEMENT_3D('',#377515,#117831,#117832);
#99925=AXIS2_PLACEMENT_3D('',#377517,#117833,#117834);
#99926=AXIS2_PLACEMENT_3D('',#377521,#117836,#117837);
#99927=AXIS2_PLACEMENT_3D('',#377525,#117839,#117840);
#99928=AXIS2_PLACEMENT_3D('',#377527,#117841,#117842);
#99929=AXIS2_PLACEMENT_3D('',#377529,#117843,#117844);
#99930=AXIS2_PLACEMENT_3D('',#377533,#117846,#117847);
#99931=AXIS2_PLACEMENT_3D('',#377537,#117849,#117850);
#99932=AXIS2_PLACEMENT_3D('',#377539,#117851,#117852);
#99933=AXIS2_PLACEMENT_3D('',#377541,#117853,#117854);
#99934=AXIS2_PLACEMENT_3D('',#377545,#117856,#117857);
#99935=AXIS2_PLACEMENT_3D('',#377549,#117859,#117860);
#99936=AXIS2_PLACEMENT_3D('',#377551,#117861,#117862);
#99937=AXIS2_PLACEMENT_3D('',#377553,#117863,#117864);
#99938=AXIS2_PLACEMENT_3D('',#377557,#117866,#117867);
#99939=AXIS2_PLACEMENT_3D('',#377561,#117869,#117870);
#99940=AXIS2_PLACEMENT_3D('',#377563,#117871,#117872);
#99941=AXIS2_PLACEMENT_3D('',#377565,#117873,#117874);
#99942=AXIS2_PLACEMENT_3D('',#377569,#117876,#117877);
#99943=AXIS2_PLACEMENT_3D('',#377573,#117879,#117880);
#99944=AXIS2_PLACEMENT_3D('',#377575,#117881,#117882);
#99945=AXIS2_PLACEMENT_3D('',#377577,#117883,#117884);
#99946=AXIS2_PLACEMENT_3D('',#377581,#117886,#117887);
#99947=AXIS2_PLACEMENT_3D('',#377585,#117889,#117890);
#99948=AXIS2_PLACEMENT_3D('',#377587,#117891,#117892);
#99949=AXIS2_PLACEMENT_3D('',#377589,#117893,#117894);
#99950=AXIS2_PLACEMENT_3D('',#377593,#117896,#117897);
#99951=AXIS2_PLACEMENT_3D('',#377597,#117899,#117900);
#99952=AXIS2_PLACEMENT_3D('',#377599,#117901,#117902);
#99953=AXIS2_PLACEMENT_3D('',#377601,#117903,#117904);
#99954=AXIS2_PLACEMENT_3D('',#377605,#117906,#117907);
#99955=AXIS2_PLACEMENT_3D('',#377609,#117909,#117910);
#99956=AXIS2_PLACEMENT_3D('',#377611,#117911,#117912);
#99957=AXIS2_PLACEMENT_3D('',#377613,#117913,#117914);
#99958=AXIS2_PLACEMENT_3D('',#377617,#117916,#117917);
#99959=AXIS2_PLACEMENT_3D('',#377621,#117919,#117920);
#99960=AXIS2_PLACEMENT_3D('',#377623,#117921,#117922);
#99961=AXIS2_PLACEMENT_3D('',#377625,#117923,#117924);
#99962=AXIS2_PLACEMENT_3D('',#377629,#117926,#117927);
#99963=AXIS2_PLACEMENT_3D('',#377633,#117929,#117930);
#99964=AXIS2_PLACEMENT_3D('',#377635,#117931,#117932);
#99965=AXIS2_PLACEMENT_3D('',#377637,#117933,#117934);
#99966=AXIS2_PLACEMENT_3D('',#377641,#117936,#117937);
#99967=AXIS2_PLACEMENT_3D('',#377645,#117939,#117940);
#99968=AXIS2_PLACEMENT_3D('',#377647,#117941,#117942);
#99969=AXIS2_PLACEMENT_3D('',#377649,#117943,#117944);
#99970=AXIS2_PLACEMENT_3D('',#377653,#117946,#117947);
#99971=AXIS2_PLACEMENT_3D('',#377657,#117949,#117950);
#99972=AXIS2_PLACEMENT_3D('',#377659,#117951,#117952);
#99973=AXIS2_PLACEMENT_3D('',#377661,#117953,#117954);
#99974=AXIS2_PLACEMENT_3D('',#377665,#117956,#117957);
#99975=AXIS2_PLACEMENT_3D('',#377669,#117959,#117960);
#99976=AXIS2_PLACEMENT_3D('',#377671,#117961,#117962);
#99977=AXIS2_PLACEMENT_3D('',#377673,#117963,#117964);
#99978=AXIS2_PLACEMENT_3D('',#377677,#117966,#117967);
#99979=AXIS2_PLACEMENT_3D('',#377681,#117969,#117970);
#99980=AXIS2_PLACEMENT_3D('',#377683,#117971,#117972);
#99981=AXIS2_PLACEMENT_3D('',#377685,#117973,#117974);
#99982=AXIS2_PLACEMENT_3D('',#377689,#117976,#117977);
#99983=AXIS2_PLACEMENT_3D('',#377693,#117979,#117980);
#99984=AXIS2_PLACEMENT_3D('',#377695,#117981,#117982);
#99985=AXIS2_PLACEMENT_3D('',#377697,#117983,#117984);
#99986=AXIS2_PLACEMENT_3D('',#377701,#117986,#117987);
#99987=AXIS2_PLACEMENT_3D('',#377705,#117989,#117990);
#99988=AXIS2_PLACEMENT_3D('',#377707,#117991,#117992);
#99989=AXIS2_PLACEMENT_3D('',#377709,#117993,#117994);
#99990=AXIS2_PLACEMENT_3D('',#377713,#117996,#117997);
#99991=AXIS2_PLACEMENT_3D('',#377717,#117999,#118000);
#99992=AXIS2_PLACEMENT_3D('',#377719,#118001,#118002);
#99993=AXIS2_PLACEMENT_3D('',#377721,#118003,#118004);
#99994=AXIS2_PLACEMENT_3D('',#377725,#118006,#118007);
#99995=AXIS2_PLACEMENT_3D('',#377729,#118009,#118010);
#99996=AXIS2_PLACEMENT_3D('',#377731,#118011,#118012);
#99997=AXIS2_PLACEMENT_3D('',#377733,#118013,#118014);
#99998=AXIS2_PLACEMENT_3D('',#377737,#118016,#118017);
#99999=AXIS2_PLACEMENT_3D('',#377741,#118019,#118020);
#100000=AXIS2_PLACEMENT_3D('',#377743,#118021,#118022);
#100001=AXIS2_PLACEMENT_3D('',#377745,#118023,#118024);
#100002=AXIS2_PLACEMENT_3D('',#377749,#118026,#118027);
#100003=AXIS2_PLACEMENT_3D('',#377753,#118029,#118030);
#100004=AXIS2_PLACEMENT_3D('',#377755,#118031,#118032);
#100005=AXIS2_PLACEMENT_3D('',#377757,#118033,#118034);
#100006=AXIS2_PLACEMENT_3D('',#377761,#118036,#118037);
#100007=AXIS2_PLACEMENT_3D('',#377765,#118039,#118040);
#100008=AXIS2_PLACEMENT_3D('',#377767,#118041,#118042);
#100009=AXIS2_PLACEMENT_3D('',#377769,#118043,#118044);
#100010=AXIS2_PLACEMENT_3D('',#377773,#118046,#118047);
#100011=AXIS2_PLACEMENT_3D('',#377777,#118049,#118050);
#100012=AXIS2_PLACEMENT_3D('',#377779,#118051,#118052);
#100013=AXIS2_PLACEMENT_3D('',#377781,#118053,#118054);
#100014=AXIS2_PLACEMENT_3D('',#377785,#118056,#118057);
#100015=AXIS2_PLACEMENT_3D('',#377789,#118059,#118060);
#100016=AXIS2_PLACEMENT_3D('',#377791,#118061,#118062);
#100017=AXIS2_PLACEMENT_3D('',#377793,#118063,#118064);
#100018=AXIS2_PLACEMENT_3D('',#377797,#118066,#118067);
#100019=AXIS2_PLACEMENT_3D('',#377801,#118069,#118070);
#100020=AXIS2_PLACEMENT_3D('',#377803,#118071,#118072);
#100021=AXIS2_PLACEMENT_3D('',#377805,#118073,#118074);
#100022=AXIS2_PLACEMENT_3D('',#377809,#118076,#118077);
#100023=AXIS2_PLACEMENT_3D('',#377813,#118079,#118080);
#100024=AXIS2_PLACEMENT_3D('',#377815,#118081,#118082);
#100025=AXIS2_PLACEMENT_3D('',#377817,#118083,#118084);
#100026=AXIS2_PLACEMENT_3D('',#377821,#118086,#118087);
#100027=AXIS2_PLACEMENT_3D('',#377825,#118089,#118090);
#100028=AXIS2_PLACEMENT_3D('',#377827,#118091,#118092);
#100029=AXIS2_PLACEMENT_3D('',#377829,#118093,#118094);
#100030=AXIS2_PLACEMENT_3D('',#377833,#118096,#118097);
#100031=AXIS2_PLACEMENT_3D('',#377837,#118099,#118100);
#100032=AXIS2_PLACEMENT_3D('',#377839,#118101,#118102);
#100033=AXIS2_PLACEMENT_3D('',#377841,#118103,#118104);
#100034=AXIS2_PLACEMENT_3D('',#377845,#118106,#118107);
#100035=AXIS2_PLACEMENT_3D('',#377849,#118109,#118110);
#100036=AXIS2_PLACEMENT_3D('',#377851,#118111,#118112);
#100037=AXIS2_PLACEMENT_3D('',#377853,#118113,#118114);
#100038=AXIS2_PLACEMENT_3D('',#377857,#118116,#118117);
#100039=AXIS2_PLACEMENT_3D('',#377861,#118119,#118120);
#100040=AXIS2_PLACEMENT_3D('',#377863,#118121,#118122);
#100041=AXIS2_PLACEMENT_3D('',#377865,#118123,#118124);
#100042=AXIS2_PLACEMENT_3D('',#377869,#118126,#118127);
#100043=AXIS2_PLACEMENT_3D('',#377873,#118129,#118130);
#100044=AXIS2_PLACEMENT_3D('',#377875,#118131,#118132);
#100045=AXIS2_PLACEMENT_3D('',#377877,#118133,#118134);
#100046=AXIS2_PLACEMENT_3D('',#377881,#118136,#118137);
#100047=AXIS2_PLACEMENT_3D('',#377885,#118139,#118140);
#100048=AXIS2_PLACEMENT_3D('',#377887,#118141,#118142);
#100049=AXIS2_PLACEMENT_3D('',#377889,#118143,#118144);
#100050=AXIS2_PLACEMENT_3D('',#377893,#118146,#118147);
#100051=AXIS2_PLACEMENT_3D('',#377897,#118149,#118150);
#100052=AXIS2_PLACEMENT_3D('',#377899,#118151,#118152);
#100053=AXIS2_PLACEMENT_3D('',#377901,#118153,#118154);
#100054=AXIS2_PLACEMENT_3D('',#377905,#118156,#118157);
#100055=AXIS2_PLACEMENT_3D('',#377909,#118159,#118160);
#100056=AXIS2_PLACEMENT_3D('',#377911,#118161,#118162);
#100057=AXIS2_PLACEMENT_3D('',#377913,#118163,#118164);
#100058=AXIS2_PLACEMENT_3D('',#377917,#118166,#118167);
#100059=AXIS2_PLACEMENT_3D('',#377921,#118169,#118170);
#100060=AXIS2_PLACEMENT_3D('',#377923,#118171,#118172);
#100061=AXIS2_PLACEMENT_3D('',#377925,#118173,#118174);
#100062=AXIS2_PLACEMENT_3D('',#377929,#118176,#118177);
#100063=AXIS2_PLACEMENT_3D('',#377933,#118179,#118180);
#100064=AXIS2_PLACEMENT_3D('',#377935,#118181,#118182);
#100065=AXIS2_PLACEMENT_3D('',#377937,#118183,#118184);
#100066=AXIS2_PLACEMENT_3D('',#377941,#118186,#118187);
#100067=AXIS2_PLACEMENT_3D('',#377945,#118189,#118190);
#100068=AXIS2_PLACEMENT_3D('',#377947,#118191,#118192);
#100069=AXIS2_PLACEMENT_3D('',#377949,#118193,#118194);
#100070=AXIS2_PLACEMENT_3D('',#377953,#118196,#118197);
#100071=AXIS2_PLACEMENT_3D('',#377957,#118199,#118200);
#100072=AXIS2_PLACEMENT_3D('',#377959,#118201,#118202);
#100073=AXIS2_PLACEMENT_3D('',#377961,#118203,#118204);
#100074=AXIS2_PLACEMENT_3D('',#377963,#118206,#118207);
#100075=AXIS2_PLACEMENT_3D('',#377964,#118208,#118209);
#100076=AXIS2_PLACEMENT_3D('',#377965,#118210,#118211);
#100077=AXIS2_PLACEMENT_3D('',#377966,#118212,#118213);
#100078=AXIS2_PLACEMENT_3D('',#377967,#118214,#118215);
#100079=AXIS2_PLACEMENT_3D('',#377968,#118216,#118217);
#100080=AXIS2_PLACEMENT_3D('',#377969,#118218,#118219);
#100081=AXIS2_PLACEMENT_3D('',#377970,#118220,#118221);
#100082=AXIS2_PLACEMENT_3D('',#377971,#118222,#118223);
#100083=AXIS2_PLACEMENT_3D('',#377972,#118224,#118225);
#100084=AXIS2_PLACEMENT_3D('',#377973,#118226,#118227);
#100085=AXIS2_PLACEMENT_3D('',#377974,#118228,#118229);
#100086=AXIS2_PLACEMENT_3D('',#377975,#118230,#118231);
#100087=AXIS2_PLACEMENT_3D('',#377976,#118232,#118233);
#100088=AXIS2_PLACEMENT_3D('',#377977,#118234,#118235);
#100089=AXIS2_PLACEMENT_3D('',#377978,#118236,#118237);
#100090=AXIS2_PLACEMENT_3D('',#377979,#118238,#118239);
#100091=AXIS2_PLACEMENT_3D('',#377980,#118240,#118241);
#100092=AXIS2_PLACEMENT_3D('',#377981,#118242,#118243);
#100093=AXIS2_PLACEMENT_3D('',#377982,#118244,#118245);
#100094=AXIS2_PLACEMENT_3D('',#377983,#118246,#118247);
#100095=AXIS2_PLACEMENT_3D('',#377984,#118248,#118249);
#100096=AXIS2_PLACEMENT_3D('',#377985,#118250,#118251);
#100097=AXIS2_PLACEMENT_3D('',#377986,#118252,#118253);
#100098=AXIS2_PLACEMENT_3D('',#377987,#118254,#118255);
#100099=AXIS2_PLACEMENT_3D('',#377988,#118256,#118257);
#100100=AXIS2_PLACEMENT_3D('',#377989,#118258,#118259);
#100101=AXIS2_PLACEMENT_3D('',#377990,#118260,#118261);
#100102=AXIS2_PLACEMENT_3D('',#377991,#118262,#118263);
#100103=AXIS2_PLACEMENT_3D('',#377992,#118264,#118265);
#100104=AXIS2_PLACEMENT_3D('',#377993,#118266,#118267);
#100105=AXIS2_PLACEMENT_3D('',#377994,#118268,#118269);
#100106=AXIS2_PLACEMENT_3D('',#377995,#118270,#118271);
#100107=AXIS2_PLACEMENT_3D('',#377996,#118272,#118273);
#100108=AXIS2_PLACEMENT_3D('',#377997,#118274,#118275);
#100109=AXIS2_PLACEMENT_3D('',#377998,#118276,#118277);
#100110=AXIS2_PLACEMENT_3D('',#377999,#118278,#118279);
#100111=AXIS2_PLACEMENT_3D('',#378000,#118280,#118281);
#100112=AXIS2_PLACEMENT_3D('',#378001,#118282,#118283);
#100113=AXIS2_PLACEMENT_3D('',#378002,#118284,#118285);
#100114=AXIS2_PLACEMENT_3D('',#378003,#118286,#118287);
#100115=AXIS2_PLACEMENT_3D('',#378004,#118288,#118289);
#100116=AXIS2_PLACEMENT_3D('',#378005,#118290,#118291);
#100117=AXIS2_PLACEMENT_3D('',#378006,#118292,#118293);
#100118=AXIS2_PLACEMENT_3D('',#378007,#118294,#118295);
#100119=AXIS2_PLACEMENT_3D('',#378008,#118296,#118297);
#100120=AXIS2_PLACEMENT_3D('',#378009,#118298,#118299);
#100121=AXIS2_PLACEMENT_3D('',#378010,#118300,#118301);
#100122=AXIS2_PLACEMENT_3D('',#378011,#118302,#118303);
#100123=AXIS2_PLACEMENT_3D('',#378012,#118304,#118305);
#100124=AXIS2_PLACEMENT_3D('',#378013,#118306,#118307);
#100125=AXIS2_PLACEMENT_3D('',#378014,#118308,#118309);
#100126=AXIS2_PLACEMENT_3D('',#378015,#118310,#118311);
#100127=AXIS2_PLACEMENT_3D('',#378016,#118312,#118313);
#100128=AXIS2_PLACEMENT_3D('',#378017,#118314,#118315);
#100129=AXIS2_PLACEMENT_3D('',#378018,#118316,#118317);
#100130=AXIS2_PLACEMENT_3D('',#378019,#118318,#118319);
#100131=AXIS2_PLACEMENT_3D('',#378020,#118320,#118321);
#100132=AXIS2_PLACEMENT_3D('',#378021,#118322,#118323);
#100133=AXIS2_PLACEMENT_3D('',#378022,#118324,#118325);
#100134=AXIS2_PLACEMENT_3D('',#378023,#118326,#118327);
#100135=AXIS2_PLACEMENT_3D('',#378024,#118328,#118329);
#100136=AXIS2_PLACEMENT_3D('',#378025,#118330,#118331);
#100137=AXIS2_PLACEMENT_3D('',#378026,#118332,#118333);
#100138=AXIS2_PLACEMENT_3D('',#378027,#118334,#118335);
#100139=AXIS2_PLACEMENT_3D('',#378028,#118336,#118337);
#100140=AXIS2_PLACEMENT_3D('',#378029,#118338,#118339);
#100141=AXIS2_PLACEMENT_3D('',#378030,#118340,#118341);
#100142=AXIS2_PLACEMENT_3D('',#378031,#118342,#118343);
#100143=AXIS2_PLACEMENT_3D('',#378032,#118344,#118345);
#100144=AXIS2_PLACEMENT_3D('',#378033,#118346,#118347);
#100145=AXIS2_PLACEMENT_3D('',#378034,#118348,#118349);
#100146=AXIS2_PLACEMENT_3D('',#378035,#118350,#118351);
#100147=AXIS2_PLACEMENT_3D('',#378036,#118352,#118353);
#100148=AXIS2_PLACEMENT_3D('',#378037,#118354,#118355);
#100149=AXIS2_PLACEMENT_3D('',#378038,#118356,#118357);
#100150=AXIS2_PLACEMENT_3D('',#378039,#118358,#118359);
#100151=AXIS2_PLACEMENT_3D('',#378040,#118360,#118361);
#100152=AXIS2_PLACEMENT_3D('',#378041,#118362,#118363);
#100153=AXIS2_PLACEMENT_3D('',#378042,#118364,#118365);
#100154=AXIS2_PLACEMENT_3D('',#378043,#118366,#118367);
#100155=AXIS2_PLACEMENT_3D('',#378044,#118368,#118369);
#100156=AXIS2_PLACEMENT_3D('',#378045,#118370,#118371);
#100157=AXIS2_PLACEMENT_3D('',#378046,#118372,#118373);
#100158=AXIS2_PLACEMENT_3D('',#378047,#118374,#118375);
#100159=AXIS2_PLACEMENT_3D('',#378048,#118376,#118377);
#100160=AXIS2_PLACEMENT_3D('',#378049,#118378,#118379);
#100161=AXIS2_PLACEMENT_3D('',#378050,#118380,#118381);
#100162=AXIS2_PLACEMENT_3D('',#378051,#118382,#118383);
#100163=AXIS2_PLACEMENT_3D('',#378052,#118384,#118385);
#100164=AXIS2_PLACEMENT_3D('',#378053,#118386,#118387);
#100165=AXIS2_PLACEMENT_3D('',#378054,#118388,#118389);
#100166=AXIS2_PLACEMENT_3D('',#378055,#118390,#118391);
#100167=AXIS2_PLACEMENT_3D('',#378056,#118392,#118393);
#100168=AXIS2_PLACEMENT_3D('',#378057,#118394,#118395);
#100169=AXIS2_PLACEMENT_3D('',#378058,#118396,#118397);
#100170=AXIS2_PLACEMENT_3D('',#378059,#118398,#118399);
#100171=AXIS2_PLACEMENT_3D('',#378060,#118400,#118401);
#100172=AXIS2_PLACEMENT_3D('',#378061,#118402,#118403);
#100173=AXIS2_PLACEMENT_3D('',#378062,#118404,#118405);
#100174=AXIS2_PLACEMENT_3D('',#378063,#118406,#118407);
#100175=AXIS2_PLACEMENT_3D('',#378064,#118408,#118409);
#100176=AXIS2_PLACEMENT_3D('',#378065,#118410,#118411);
#100177=AXIS2_PLACEMENT_3D('',#378066,#118412,#118413);
#100178=AXIS2_PLACEMENT_3D('',#378067,#118414,#118415);
#100179=AXIS2_PLACEMENT_3D('',#378068,#118416,#118417);
#100180=AXIS2_PLACEMENT_3D('',#378069,#118418,#118419);
#100181=AXIS2_PLACEMENT_3D('',#378070,#118420,#118421);
#100182=AXIS2_PLACEMENT_3D('',#378071,#118422,#118423);
#100183=AXIS2_PLACEMENT_3D('',#378072,#118424,#118425);
#100184=AXIS2_PLACEMENT_3D('',#378073,#118426,#118427);
#100185=AXIS2_PLACEMENT_3D('',#378074,#118428,#118429);
#100186=AXIS2_PLACEMENT_3D('',#378075,#118430,#118431);
#100187=AXIS2_PLACEMENT_3D('',#378076,#118432,#118433);
#100188=AXIS2_PLACEMENT_3D('',#378077,#118434,#118435);
#100189=AXIS2_PLACEMENT_3D('',#378078,#118436,#118437);
#100190=AXIS2_PLACEMENT_3D('',#378079,#118438,#118439);
#100191=AXIS2_PLACEMENT_3D('',#378080,#118440,#118441);
#100192=AXIS2_PLACEMENT_3D('',#378081,#118442,#118443);
#100193=AXIS2_PLACEMENT_3D('',#378082,#118444,#118445);
#100194=AXIS2_PLACEMENT_3D('',#378083,#118446,#118447);
#100195=AXIS2_PLACEMENT_3D('',#378084,#118448,#118449);
#100196=AXIS2_PLACEMENT_3D('',#378085,#118450,#118451);
#100197=AXIS2_PLACEMENT_3D('',#378086,#118452,#118453);
#100198=AXIS2_PLACEMENT_3D('',#378087,#118454,#118455);
#100199=AXIS2_PLACEMENT_3D('',#378088,#118456,#118457);
#100200=AXIS2_PLACEMENT_3D('',#378089,#118458,#118459);
#100201=AXIS2_PLACEMENT_3D('',#378090,#118460,#118461);
#100202=AXIS2_PLACEMENT_3D('',#378091,#118462,#118463);
#100203=AXIS2_PLACEMENT_3D('',#378092,#118464,#118465);
#100204=AXIS2_PLACEMENT_3D('',#378093,#118466,#118467);
#100205=AXIS2_PLACEMENT_3D('',#378094,#118468,#118469);
#100206=AXIS2_PLACEMENT_3D('',#378095,#118470,#118471);
#100207=AXIS2_PLACEMENT_3D('',#378096,#118472,#118473);
#100208=AXIS2_PLACEMENT_3D('',#378097,#118474,#118475);
#100209=AXIS2_PLACEMENT_3D('',#378098,#118476,#118477);
#100210=AXIS2_PLACEMENT_3D('',#378099,#118478,#118479);
#100211=AXIS2_PLACEMENT_3D('',#378100,#118480,#118481);
#100212=AXIS2_PLACEMENT_3D('',#378101,#118482,#118483);
#100213=AXIS2_PLACEMENT_3D('',#378102,#118484,#118485);
#100214=AXIS2_PLACEMENT_3D('',#378103,#118486,#118487);
#100215=AXIS2_PLACEMENT_3D('',#378104,#118488,#118489);
#100216=AXIS2_PLACEMENT_3D('',#378105,#118490,#118491);
#100217=AXIS2_PLACEMENT_3D('',#378106,#118492,#118493);
#100218=AXIS2_PLACEMENT_3D('',#378107,#118494,#118495);
#100219=AXIS2_PLACEMENT_3D('',#378108,#118496,#118497);
#100220=AXIS2_PLACEMENT_3D('',#378109,#118498,#118499);
#100221=AXIS2_PLACEMENT_3D('',#378110,#118500,#118501);
#100222=AXIS2_PLACEMENT_3D('',#378111,#118502,#118503);
#100223=AXIS2_PLACEMENT_3D('',#378112,#118504,#118505);
#100224=AXIS2_PLACEMENT_3D('',#378113,#118506,#118507);
#100225=AXIS2_PLACEMENT_3D('',#378114,#118508,#118509);
#100226=AXIS2_PLACEMENT_3D('',#378115,#118510,#118511);
#100227=AXIS2_PLACEMENT_3D('',#378116,#118512,#118513);
#100228=AXIS2_PLACEMENT_3D('',#378117,#118514,#118515);
#100229=AXIS2_PLACEMENT_3D('',#378118,#118516,#118517);
#100230=AXIS2_PLACEMENT_3D('',#378119,#118518,#118519);
#100231=AXIS2_PLACEMENT_3D('',#378120,#118520,#118521);
#100232=AXIS2_PLACEMENT_3D('',#378121,#118522,#118523);
#100233=AXIS2_PLACEMENT_3D('',#378122,#118524,#118525);
#100234=AXIS2_PLACEMENT_3D('',#378123,#118526,#118527);
#100235=AXIS2_PLACEMENT_3D('',#378124,#118528,#118529);
#100236=AXIS2_PLACEMENT_3D('',#378125,#118530,#118531);
#100237=AXIS2_PLACEMENT_3D('',#378126,#118532,#118533);
#100238=AXIS2_PLACEMENT_3D('',#378127,#118534,#118535);
#100239=AXIS2_PLACEMENT_3D('',#378128,#118536,#118537);
#100240=AXIS2_PLACEMENT_3D('',#378129,#118538,#118539);
#100241=AXIS2_PLACEMENT_3D('',#378130,#118540,#118541);
#100242=AXIS2_PLACEMENT_3D('',#378131,#118542,#118543);
#100243=AXIS2_PLACEMENT_3D('',#378132,#118544,#118545);
#100244=AXIS2_PLACEMENT_3D('',#378133,#118546,#118547);
#100245=AXIS2_PLACEMENT_3D('',#378134,#118548,#118549);
#100246=AXIS2_PLACEMENT_3D('',#378135,#118550,#118551);
#100247=AXIS2_PLACEMENT_3D('',#378136,#118552,#118553);
#100248=AXIS2_PLACEMENT_3D('',#378137,#118554,#118555);
#100249=AXIS2_PLACEMENT_3D('',#378138,#118556,#118557);
#100250=AXIS2_PLACEMENT_3D('',#378139,#118558,#118559);
#100251=AXIS2_PLACEMENT_3D('',#378140,#118560,#118561);
#100252=AXIS2_PLACEMENT_3D('',#378141,#118562,#118563);
#100253=AXIS2_PLACEMENT_3D('',#378142,#118564,#118565);
#100254=AXIS2_PLACEMENT_3D('',#378143,#118566,#118567);
#100255=AXIS2_PLACEMENT_3D('',#378144,#118568,#118569);
#100256=AXIS2_PLACEMENT_3D('',#378145,#118570,#118571);
#100257=AXIS2_PLACEMENT_3D('',#378146,#118572,#118573);
#100258=AXIS2_PLACEMENT_3D('',#378147,#118574,#118575);
#100259=AXIS2_PLACEMENT_3D('',#378148,#118576,#118577);
#100260=AXIS2_PLACEMENT_3D('',#378149,#118578,#118579);
#100261=AXIS2_PLACEMENT_3D('',#378150,#118580,#118581);
#100262=AXIS2_PLACEMENT_3D('',#378151,#118582,#118583);
#100263=AXIS2_PLACEMENT_3D('',#378152,#118584,#118585);
#100264=AXIS2_PLACEMENT_3D('',#378153,#118586,#118587);
#100265=AXIS2_PLACEMENT_3D('',#378154,#118588,#118589);
#100266=AXIS2_PLACEMENT_3D('',#378155,#118590,#118591);
#100267=AXIS2_PLACEMENT_3D('',#378156,#118592,#118593);
#100268=AXIS2_PLACEMENT_3D('',#378157,#118594,#118595);
#100269=AXIS2_PLACEMENT_3D('',#378158,#118596,#118597);
#100270=AXIS2_PLACEMENT_3D('',#378159,#118598,#118599);
#100271=AXIS2_PLACEMENT_3D('',#378160,#118600,#118601);
#100272=AXIS2_PLACEMENT_3D('',#378161,#118602,#118603);
#100273=AXIS2_PLACEMENT_3D('',#378162,#118604,#118605);
#100274=AXIS2_PLACEMENT_3D('',#378163,#118606,#118607);
#100275=AXIS2_PLACEMENT_3D('',#378164,#118608,#118609);
#100276=AXIS2_PLACEMENT_3D('',#378165,#118610,#118611);
#100277=AXIS2_PLACEMENT_3D('',#378166,#118612,#118613);
#100278=AXIS2_PLACEMENT_3D('',#378167,#118614,#118615);
#100279=AXIS2_PLACEMENT_3D('',#378168,#118616,#118617);
#100280=AXIS2_PLACEMENT_3D('',#378169,#118618,#118619);
#100281=AXIS2_PLACEMENT_3D('',#378170,#118620,#118621);
#100282=AXIS2_PLACEMENT_3D('',#378171,#118622,#118623);
#100283=AXIS2_PLACEMENT_3D('',#378172,#118624,#118625);
#100284=AXIS2_PLACEMENT_3D('',#378173,#118626,#118627);
#100285=AXIS2_PLACEMENT_3D('',#378174,#118628,#118629);
#100286=AXIS2_PLACEMENT_3D('',#378175,#118630,#118631);
#100287=AXIS2_PLACEMENT_3D('',#378176,#118632,#118633);
#100288=AXIS2_PLACEMENT_3D('',#378177,#118634,#118635);
#100289=AXIS2_PLACEMENT_3D('',#378178,#118636,#118637);
#100290=AXIS2_PLACEMENT_3D('',#378179,#118638,#118639);
#100291=AXIS2_PLACEMENT_3D('',#378180,#118640,#118641);
#100292=AXIS2_PLACEMENT_3D('',#378181,#118642,#118643);
#100293=AXIS2_PLACEMENT_3D('',#378182,#118644,#118645);
#100294=AXIS2_PLACEMENT_3D('',#378183,#118646,#118647);
#100295=AXIS2_PLACEMENT_3D('',#378184,#118648,#118649);
#100296=AXIS2_PLACEMENT_3D('',#378185,#118650,#118651);
#100297=AXIS2_PLACEMENT_3D('',#378186,#118652,#118653);
#100298=AXIS2_PLACEMENT_3D('',#378187,#118654,#118655);
#100299=AXIS2_PLACEMENT_3D('',#378188,#118656,#118657);
#100300=AXIS2_PLACEMENT_3D('',#378189,#118658,#118659);
#100301=AXIS2_PLACEMENT_3D('',#378190,#118660,#118661);
#100302=AXIS2_PLACEMENT_3D('',#378191,#118662,#118663);
#100303=AXIS2_PLACEMENT_3D('',#378192,#118664,#118665);
#100304=AXIS2_PLACEMENT_3D('',#378193,#118666,#118667);
#100305=AXIS2_PLACEMENT_3D('',#378194,#118668,#118669);
#100306=AXIS2_PLACEMENT_3D('',#378195,#118670,#118671);
#100307=AXIS2_PLACEMENT_3D('',#378196,#118672,#118673);
#100308=AXIS2_PLACEMENT_3D('',#378197,#118674,#118675);
#100309=AXIS2_PLACEMENT_3D('',#378198,#118676,#118677);
#100310=AXIS2_PLACEMENT_3D('',#378199,#118678,#118679);
#100311=AXIS2_PLACEMENT_3D('',#378200,#118680,#118681);
#100312=AXIS2_PLACEMENT_3D('',#378201,#118682,#118683);
#100313=AXIS2_PLACEMENT_3D('',#378202,#118684,#118685);
#100314=AXIS2_PLACEMENT_3D('',#378203,#118686,#118687);
#100315=AXIS2_PLACEMENT_3D('',#378204,#118688,#118689);
#100316=AXIS2_PLACEMENT_3D('',#378205,#118690,#118691);
#100317=AXIS2_PLACEMENT_3D('',#378206,#118692,#118693);
#100318=AXIS2_PLACEMENT_3D('',#378207,#118694,#118695);
#100319=AXIS2_PLACEMENT_3D('',#378208,#118696,#118697);
#100320=AXIS2_PLACEMENT_3D('',#378209,#118698,#118699);
#100321=AXIS2_PLACEMENT_3D('',#378210,#118700,#118701);
#100322=AXIS2_PLACEMENT_3D('',#378211,#118702,#118703);
#100323=AXIS2_PLACEMENT_3D('',#378212,#118704,#118705);
#100324=AXIS2_PLACEMENT_3D('',#378213,#118706,#118707);
#100325=AXIS2_PLACEMENT_3D('',#378214,#118708,#118709);
#100326=AXIS2_PLACEMENT_3D('',#378215,#118710,#118711);
#100327=AXIS2_PLACEMENT_3D('',#378216,#118712,#118713);
#100328=AXIS2_PLACEMENT_3D('',#378217,#118714,#118715);
#100329=AXIS2_PLACEMENT_3D('',#378218,#118716,#118717);
#100330=AXIS2_PLACEMENT_3D('',#378219,#118718,#118719);
#100331=AXIS2_PLACEMENT_3D('',#378220,#118720,#118721);
#100332=AXIS2_PLACEMENT_3D('',#378221,#118722,#118723);
#100333=AXIS2_PLACEMENT_3D('',#378222,#118724,#118725);
#100334=AXIS2_PLACEMENT_3D('',#378223,#118726,#118727);
#100335=AXIS2_PLACEMENT_3D('',#378224,#118728,#118729);
#100336=AXIS2_PLACEMENT_3D('',#378225,#118730,#118731);
#100337=AXIS2_PLACEMENT_3D('',#378226,#118732,#118733);
#100338=AXIS2_PLACEMENT_3D('',#378227,#118734,#118735);
#100339=AXIS2_PLACEMENT_3D('',#378228,#118736,#118737);
#100340=AXIS2_PLACEMENT_3D('',#378229,#118738,#118739);
#100341=AXIS2_PLACEMENT_3D('',#378230,#118740,#118741);
#100342=AXIS2_PLACEMENT_3D('',#378231,#118742,#118743);
#100343=AXIS2_PLACEMENT_3D('',#378232,#118744,#118745);
#100344=AXIS2_PLACEMENT_3D('',#378233,#118746,#118747);
#100345=AXIS2_PLACEMENT_3D('',#378234,#118748,#118749);
#100346=AXIS2_PLACEMENT_3D('',#378235,#118750,#118751);
#100347=AXIS2_PLACEMENT_3D('',#378236,#118752,#118753);
#100348=AXIS2_PLACEMENT_3D('',#378237,#118754,#118755);
#100349=AXIS2_PLACEMENT_3D('',#378238,#118756,#118757);
#100350=AXIS2_PLACEMENT_3D('',#378239,#118758,#118759);
#100351=AXIS2_PLACEMENT_3D('',#378240,#118760,#118761);
#100352=AXIS2_PLACEMENT_3D('',#378241,#118762,#118763);
#100353=AXIS2_PLACEMENT_3D('',#378242,#118764,#118765);
#100354=AXIS2_PLACEMENT_3D('',#378243,#118766,#118767);
#100355=AXIS2_PLACEMENT_3D('',#378244,#118768,#118769);
#100356=AXIS2_PLACEMENT_3D('',#378245,#118770,#118771);
#100357=AXIS2_PLACEMENT_3D('',#378246,#118772,#118773);
#100358=AXIS2_PLACEMENT_3D('',#378247,#118774,#118775);
#100359=AXIS2_PLACEMENT_3D('',#378248,#118776,#118777);
#100360=AXIS2_PLACEMENT_3D('',#378249,#118778,#118779);
#100361=AXIS2_PLACEMENT_3D('',#378250,#118780,#118781);
#100362=AXIS2_PLACEMENT_3D('',#378251,#118782,#118783);
#100363=AXIS2_PLACEMENT_3D('',#378252,#118784,#118785);
#100364=AXIS2_PLACEMENT_3D('',#378253,#118786,#118787);
#100365=AXIS2_PLACEMENT_3D('',#378254,#118788,#118789);
#100366=AXIS2_PLACEMENT_3D('',#378310,#118792,#118793);
#100367=AXIS2_PLACEMENT_3D('',#378311,#118794,#118795);
#100368=AXIS2_PLACEMENT_3D('',#378314,#118796,#118797);
#100369=AXIS2_PLACEMENT_3D('',#378328,#118799,#118800);
#100370=AXIS2_PLACEMENT_3D('',#378335,#118801,#118802);
#100371=AXIS2_PLACEMENT_3D('',#378345,#118804,#118805);
#100372=AXIS2_PLACEMENT_3D('',#378349,#118808,#118809);
#100373=AXIS2_PLACEMENT_3D('',#378353,#118812,#118813);
#100374=AXIS2_PLACEMENT_3D('',#378357,#118816,#118817);
#100375=AXIS2_PLACEMENT_3D('',#378361,#118820,#118821);
#100376=AXIS2_PLACEMENT_3D('',#378365,#118824,#118825);
#100377=AXIS2_PLACEMENT_3D('',#378368,#118826,#118827);
#100378=AXIS2_PLACEMENT_3D('',#378369,#118828,#118829);
#100379=AXIS2_PLACEMENT_3D('',#378371,#118830,#118831);
#100380=AXIS2_PLACEMENT_3D('',#378373,#118832,#118833);
#100381=AXIS2_PLACEMENT_3D('',#378374,#118834,#118835);
#100382=AXIS2_PLACEMENT_3D('',#378375,#118836,#118837);
#100383=AXIS2_PLACEMENT_3D('',#378376,#118838,#118839);
#100384=AXIS2_PLACEMENT_3D('',#378377,#118840,#118841);
#100385=AXIS2_PLACEMENT_3D('',#378378,#118842,#118843);
#100386=AXIS2_PLACEMENT_3D('',#378384,#118846,#118847);
#100387=AXIS2_PLACEMENT_3D('',#378386,#118849,#118850);
#100388=AXIS2_PLACEMENT_3D('',#378391,#118852,#118853);
#100389=AXIS2_PLACEMENT_3D('',#378398,#118856,#118857);
#100390=AXIS2_PLACEMENT_3D('',#378404,#118860,#118861);
#100391=AXIS2_PLACEMENT_3D('',#378408,#118862,#118863);
#100392=AXIS2_PLACEMENT_3D('',#378409,#118864,#118865);
#100393=AXIS2_PLACEMENT_3D('',#378410,#118866,#118867);
#100394=AXIS2_PLACEMENT_3D('',#378411,#118868,#118869);
#100395=AXIS2_PLACEMENT_3D('',#378412,#118870,#118871);
#100396=AXIS2_PLACEMENT_3D('',#378413,#118872,#118873);
#100397=AXIS2_PLACEMENT_3D('',#378414,#118874,#118875);
#100398=AXIS2_PLACEMENT_3D('',#378415,#118876,#118877);
#100399=AXIS2_PLACEMENT_3D('',#378416,#118878,#118879);
#100400=AXIS2_PLACEMENT_3D('',#379921,#118880,#118881);
#100401=AXIS2_PLACEMENT_3D('',#379933,#118882,#118883);
#100402=AXIS2_PLACEMENT_3D('',#379977,#118884,#118885);
#100403=AXIS2_PLACEMENT_3D('',#379978,#118886,#118887);
#100404=AXIS2_PLACEMENT_3D('',#379979,#118888,#118889);
#100405=AXIS2_PLACEMENT_3D('',#379980,#118890,#118891);
#100406=AXIS2_PLACEMENT_3D('',#379993,#118892,#118893);
#100407=AXIS2_PLACEMENT_3D('',#380006,#118894,#118895);
#100408=AXIS2_PLACEMENT_3D('',#380019,#118896,#118897);
#100409=AXIS2_PLACEMENT_3D('',#380066,#118898,#118899);
#100410=AXIS2_PLACEMENT_3D('',#380067,#118900,#118901);
#100411=AXIS2_PLACEMENT_3D('',#380080,#118902,#118903);
#100412=AXIS2_PLACEMENT_3D('',#380093,#118904,#118905);
#100413=AXIS2_PLACEMENT_3D('',#380106,#118906,#118907);
#100414=AXIS2_PLACEMENT_3D('',#380107,#118908,#118909);
#100415=AXIS2_PLACEMENT_3D('',#380108,#118910,#118911);
#100416=AXIS2_PLACEMENT_3D('',#380121,#118912,#118913);
#100417=AXIS2_PLACEMENT_3D('',#380134,#118914,#118915);
#100418=AXIS2_PLACEMENT_3D('',#380144,#118917,#118918);
#100419=AXIS2_PLACEMENT_3D('',#380154,#118920,#118921);
#100420=AXIS2_PLACEMENT_3D('',#380157,#118922,#118923);
#100421=AXIS2_PLACEMENT_3D('',#380174,#118926,#118927);
#100422=AXIS2_PLACEMENT_3D('',#380224,#118928,#118929);
#100423=AXIS2_PLACEMENT_3D('',#380270,#118930,#118931);
#100424=AXIS2_PLACEMENT_3D('',#380287,#118932,#118933);
#100425=AXIS2_PLACEMENT_3D('',#380339,#118934,#118935);
#100426=AXIS2_PLACEMENT_3D('',#380340,#118936,#118937);
#100427=AXIS2_PLACEMENT_3D('',#380341,#118938,#118939);
#100428=AXIS2_PLACEMENT_3D('',#380342,#118940,#118941);
#100429=AXIS2_PLACEMENT_3D('',#380355,#118942,#118943);
#100430=AXIS2_PLACEMENT_3D('',#380356,#118944,#118945);
#100431=AXIS2_PLACEMENT_3D('',#380357,#118946,#118947);
#100432=AXIS2_PLACEMENT_3D('',#380370,#118948,#118949);
#100433=AXIS2_PLACEMENT_3D('',#380383,#118950,#118951);
#100434=AXIS2_PLACEMENT_3D('',#380396,#118952,#118953);
#100435=AXIS2_PLACEMENT_3D('',#380409,#118954,#118955);
#100436=AXIS2_PLACEMENT_3D('',#380422,#118956,#118957);
#100437=AXIS2_PLACEMENT_3D('',#380423,#118958,#118959);
#100438=AXIS2_PLACEMENT_3D('',#380424,#118960,#118961);
#100439=AXIS2_PLACEMENT_3D('',#380437,#118962,#118963);
#100440=AXIS2_PLACEMENT_3D('',#380438,#118964,#118965);
#100441=AXIS2_PLACEMENT_3D('',#380448,#118967,#118968);
#100442=AXIS2_PLACEMENT_3D('',#380458,#118970,#118971);
#100443=AXIS2_PLACEMENT_3D('',#380461,#118972,#118973);
#100444=AXIS2_PLACEMENT_3D('',#380478,#118976,#118977);
#100445=AXIS2_PLACEMENT_3D('',#380528,#118978,#118979);
#100446=AXIS2_PLACEMENT_3D('',#380574,#118980,#118981);
#100447=AXIS2_PLACEMENT_3D('',#380591,#118982,#118983);
#100448=AXIS2_PLACEMENT_3D('',#380643,#118984,#118985);
#100449=AXIS2_PLACEMENT_3D('',#380644,#118986,#118987);
#100450=AXIS2_PLACEMENT_3D('',#380645,#118988,#118989);
#100451=AXIS2_PLACEMENT_3D('',#380646,#118990,#118991);
#100452=AXIS2_PLACEMENT_3D('',#380659,#118992,#118993);
#100453=AXIS2_PLACEMENT_3D('',#380660,#118994,#118995);
#100454=AXIS2_PLACEMENT_3D('',#380661,#118996,#118997);
#100455=AXIS2_PLACEMENT_3D('',#380674,#118998,#118999);
#100456=AXIS2_PLACEMENT_3D('',#380687,#119000,#119001);
#100457=AXIS2_PLACEMENT_3D('',#380700,#119002,#119003);
#100458=AXIS2_PLACEMENT_3D('',#380713,#119004,#119005);
#100459=AXIS2_PLACEMENT_3D('',#380726,#119006,#119007);
#100460=AXIS2_PLACEMENT_3D('',#380727,#119008,#119009);
#100461=AXIS2_PLACEMENT_3D('',#380728,#119010,#119011);
#100462=AXIS2_PLACEMENT_3D('',#380741,#119012,#119013);
#100463=AXIS2_PLACEMENT_3D('',#380742,#119014,#119015);
#100464=AXIS2_PLACEMENT_3D('',#380752,#119017,#119018);
#100465=AXIS2_PLACEMENT_3D('',#380762,#119020,#119021);
#100466=AXIS2_PLACEMENT_3D('',#380765,#119022,#119023);
#100467=AXIS2_PLACEMENT_3D('',#380782,#119026,#119027);
#100468=AXIS2_PLACEMENT_3D('',#380832,#119028,#119029);
#100469=AXIS2_PLACEMENT_3D('',#380878,#119030,#119031);
#100470=AXIS2_PLACEMENT_3D('',#380895,#119032,#119033);
#100471=AXIS2_PLACEMENT_3D('',#380947,#119034,#119035);
#100472=AXIS2_PLACEMENT_3D('',#380948,#119036,#119037);
#100473=AXIS2_PLACEMENT_3D('',#380949,#119038,#119039);
#100474=AXIS2_PLACEMENT_3D('',#380950,#119040,#119041);
#100475=AXIS2_PLACEMENT_3D('',#380963,#119042,#119043);
#100476=AXIS2_PLACEMENT_3D('',#380964,#119044,#119045);
#100477=AXIS2_PLACEMENT_3D('',#380965,#119046,#119047);
#100478=AXIS2_PLACEMENT_3D('',#380978,#119048,#119049);
#100479=AXIS2_PLACEMENT_3D('',#380991,#119050,#119051);
#100480=AXIS2_PLACEMENT_3D('',#381004,#119052,#119053);
#100481=AXIS2_PLACEMENT_3D('',#381017,#119054,#119055);
#100482=AXIS2_PLACEMENT_3D('',#381030,#119056,#119057);
#100483=AXIS2_PLACEMENT_3D('',#381031,#119058,#119059);
#100484=AXIS2_PLACEMENT_3D('',#381032,#119060,#119061);
#100485=AXIS2_PLACEMENT_3D('',#381045,#119062,#119063);
#100486=AXIS2_PLACEMENT_3D('',#381046,#119064,#119065);
#100487=AXIS2_PLACEMENT_3D('',#381056,#119067,#119068);
#100488=AXIS2_PLACEMENT_3D('',#381066,#119070,#119071);
#100489=AXIS2_PLACEMENT_3D('',#381069,#119072,#119073);
#100490=AXIS2_PLACEMENT_3D('',#381086,#119076,#119077);
#100491=AXIS2_PLACEMENT_3D('',#381136,#119078,#119079);
#100492=AXIS2_PLACEMENT_3D('',#381182,#119080,#119081);
#100493=AXIS2_PLACEMENT_3D('',#381199,#119082,#119083);
#100494=AXIS2_PLACEMENT_3D('',#381251,#119084,#119085);
#100495=AXIS2_PLACEMENT_3D('',#381252,#119086,#119087);
#100496=AXIS2_PLACEMENT_3D('',#381253,#119088,#119089);
#100497=AXIS2_PLACEMENT_3D('',#381254,#119090,#119091);
#100498=AXIS2_PLACEMENT_3D('',#381267,#119092,#119093);
#100499=AXIS2_PLACEMENT_3D('',#381268,#119094,#119095);
#100500=AXIS2_PLACEMENT_3D('',#381269,#119096,#119097);
#100501=AXIS2_PLACEMENT_3D('',#381282,#119098,#119099);
#100502=AXIS2_PLACEMENT_3D('',#381295,#119100,#119101);
#100503=AXIS2_PLACEMENT_3D('',#381308,#119102,#119103);
#100504=AXIS2_PLACEMENT_3D('',#381321,#119104,#119105);
#100505=AXIS2_PLACEMENT_3D('',#381334,#119106,#119107);
#100506=AXIS2_PLACEMENT_3D('',#381335,#119108,#119109);
#100507=AXIS2_PLACEMENT_3D('',#381336,#119110,#119111);
#100508=AXIS2_PLACEMENT_3D('',#381349,#119112,#119113);
#100509=AXIS2_PLACEMENT_3D('',#381350,#119114,#119115);
#100510=AXIS2_PLACEMENT_3D('',#381360,#119117,#119118);
#100511=AXIS2_PLACEMENT_3D('',#381370,#119120,#119121);
#100512=AXIS2_PLACEMENT_3D('',#381373,#119122,#119123);
#100513=AXIS2_PLACEMENT_3D('',#381390,#119126,#119127);
#100514=AXIS2_PLACEMENT_3D('',#381440,#119128,#119129);
#100515=AXIS2_PLACEMENT_3D('',#381486,#119130,#119131);
#100516=AXIS2_PLACEMENT_3D('',#381503,#119132,#119133);
#100517=AXIS2_PLACEMENT_3D('',#381555,#119134,#119135);
#100518=AXIS2_PLACEMENT_3D('',#381556,#119136,#119137);
#100519=AXIS2_PLACEMENT_3D('',#381557,#119138,#119139);
#100520=AXIS2_PLACEMENT_3D('',#381558,#119140,#119141);
#100521=AXIS2_PLACEMENT_3D('',#381571,#119142,#119143);
#100522=AXIS2_PLACEMENT_3D('',#381572,#119144,#119145);
#100523=AXIS2_PLACEMENT_3D('',#381573,#119146,#119147);
#100524=AXIS2_PLACEMENT_3D('',#381586,#119148,#119149);
#100525=AXIS2_PLACEMENT_3D('',#381599,#119150,#119151);
#100526=AXIS2_PLACEMENT_3D('',#381612,#119152,#119153);
#100527=AXIS2_PLACEMENT_3D('',#381625,#119154,#119155);
#100528=AXIS2_PLACEMENT_3D('',#381638,#119156,#119157);
#100529=AXIS2_PLACEMENT_3D('',#381639,#119158,#119159);
#100530=AXIS2_PLACEMENT_3D('',#381640,#119160,#119161);
#100531=AXIS2_PLACEMENT_3D('',#381653,#119162,#119163);
#100532=AXIS2_PLACEMENT_3D('',#381654,#119164,#119165);
#100533=AXIS2_PLACEMENT_3D('',#381664,#119167,#119168);
#100534=AXIS2_PLACEMENT_3D('',#381674,#119170,#119171);
#100535=AXIS2_PLACEMENT_3D('',#381677,#119172,#119173);
#100536=AXIS2_PLACEMENT_3D('',#381694,#119176,#119177);
#100537=AXIS2_PLACEMENT_3D('',#381744,#119178,#119179);
#100538=AXIS2_PLACEMENT_3D('',#381790,#119180,#119181);
#100539=AXIS2_PLACEMENT_3D('',#381807,#119182,#119183);
#100540=AXIS2_PLACEMENT_3D('',#381859,#119184,#119185);
#100541=AXIS2_PLACEMENT_3D('',#381860,#119186,#119187);
#100542=AXIS2_PLACEMENT_3D('',#381861,#119188,#119189);
#100543=AXIS2_PLACEMENT_3D('',#381862,#119190,#119191);
#100544=AXIS2_PLACEMENT_3D('',#381875,#119192,#119193);
#100545=AXIS2_PLACEMENT_3D('',#381876,#119194,#119195);
#100546=AXIS2_PLACEMENT_3D('',#381877,#119196,#119197);
#100547=AXIS2_PLACEMENT_3D('',#381890,#119198,#119199);
#100548=AXIS2_PLACEMENT_3D('',#381903,#119200,#119201);
#100549=AXIS2_PLACEMENT_3D('',#381916,#119202,#119203);
#100550=AXIS2_PLACEMENT_3D('',#381929,#119204,#119205);
#100551=AXIS2_PLACEMENT_3D('',#381942,#119206,#119207);
#100552=AXIS2_PLACEMENT_3D('',#381943,#119208,#119209);
#100553=AXIS2_PLACEMENT_3D('',#381944,#119210,#119211);
#100554=AXIS2_PLACEMENT_3D('',#381957,#119212,#119213);
#100555=AXIS2_PLACEMENT_3D('',#381958,#119214,#119215);
#100556=AXIS2_PLACEMENT_3D('',#381968,#119217,#119218);
#100557=AXIS2_PLACEMENT_3D('',#381978,#119220,#119221);
#100558=AXIS2_PLACEMENT_3D('',#381981,#119222,#119223);
#100559=AXIS2_PLACEMENT_3D('',#381998,#119226,#119227);
#100560=AXIS2_PLACEMENT_3D('',#382048,#119228,#119229);
#100561=AXIS2_PLACEMENT_3D('',#382094,#119230,#119231);
#100562=AXIS2_PLACEMENT_3D('',#382111,#119232,#119233);
#100563=AXIS2_PLACEMENT_3D('',#382163,#119234,#119235);
#100564=AXIS2_PLACEMENT_3D('',#382164,#119236,#119237);
#100565=AXIS2_PLACEMENT_3D('',#382165,#119238,#119239);
#100566=AXIS2_PLACEMENT_3D('',#382166,#119240,#119241);
#100567=AXIS2_PLACEMENT_3D('',#382179,#119242,#119243);
#100568=AXIS2_PLACEMENT_3D('',#382180,#119244,#119245);
#100569=AXIS2_PLACEMENT_3D('',#382181,#119246,#119247);
#100570=AXIS2_PLACEMENT_3D('',#382194,#119248,#119249);
#100571=AXIS2_PLACEMENT_3D('',#382207,#119250,#119251);
#100572=AXIS2_PLACEMENT_3D('',#382220,#119252,#119253);
#100573=AXIS2_PLACEMENT_3D('',#382233,#119254,#119255);
#100574=AXIS2_PLACEMENT_3D('',#382246,#119256,#119257);
#100575=AXIS2_PLACEMENT_3D('',#382247,#119258,#119259);
#100576=AXIS2_PLACEMENT_3D('',#382248,#119260,#119261);
#100577=AXIS2_PLACEMENT_3D('',#382261,#119262,#119263);
#100578=AXIS2_PLACEMENT_3D('',#382262,#119264,#119265);
#100579=AXIS2_PLACEMENT_3D('',#382272,#119267,#119268);
#100580=AXIS2_PLACEMENT_3D('',#382282,#119270,#119271);
#100581=AXIS2_PLACEMENT_3D('',#382285,#119272,#119273);
#100582=AXIS2_PLACEMENT_3D('',#382302,#119276,#119277);
#100583=AXIS2_PLACEMENT_3D('',#382352,#119278,#119279);
#100584=AXIS2_PLACEMENT_3D('',#382398,#119280,#119281);
#100585=AXIS2_PLACEMENT_3D('',#382415,#119282,#119283);
#100586=AXIS2_PLACEMENT_3D('',#382467,#119284,#119285);
#100587=AXIS2_PLACEMENT_3D('',#382468,#119286,#119287);
#100588=AXIS2_PLACEMENT_3D('',#382469,#119288,#119289);
#100589=AXIS2_PLACEMENT_3D('',#382470,#119290,#119291);
#100590=AXIS2_PLACEMENT_3D('',#382483,#119292,#119293);
#100591=AXIS2_PLACEMENT_3D('',#382484,#119294,#119295);
#100592=AXIS2_PLACEMENT_3D('',#382485,#119296,#119297);
#100593=AXIS2_PLACEMENT_3D('',#382498,#119298,#119299);
#100594=AXIS2_PLACEMENT_3D('',#382511,#119300,#119301);
#100595=AXIS2_PLACEMENT_3D('',#382524,#119302,#119303);
#100596=AXIS2_PLACEMENT_3D('',#382537,#119304,#119305);
#100597=AXIS2_PLACEMENT_3D('',#382550,#119306,#119307);
#100598=AXIS2_PLACEMENT_3D('',#382551,#119308,#119309);
#100599=AXIS2_PLACEMENT_3D('',#382552,#119310,#119311);
#100600=AXIS2_PLACEMENT_3D('',#382565,#119312,#119313);
#100601=AXIS2_PLACEMENT_3D('',#382566,#119314,#119315);
#100602=AXIS2_PLACEMENT_3D('',#382576,#119317,#119318);
#100603=AXIS2_PLACEMENT_3D('',#382586,#119320,#119321);
#100604=AXIS2_PLACEMENT_3D('',#382589,#119322,#119323);
#100605=AXIS2_PLACEMENT_3D('',#382606,#119326,#119327);
#100606=AXIS2_PLACEMENT_3D('',#382656,#119328,#119329);
#100607=AXIS2_PLACEMENT_3D('',#382702,#119330,#119331);
#100608=AXIS2_PLACEMENT_3D('',#382719,#119332,#119333);
#100609=AXIS2_PLACEMENT_3D('',#382771,#119334,#119335);
#100610=AXIS2_PLACEMENT_3D('',#382772,#119336,#119337);
#100611=AXIS2_PLACEMENT_3D('',#382773,#119338,#119339);
#100612=AXIS2_PLACEMENT_3D('',#382774,#119340,#119341);
#100613=AXIS2_PLACEMENT_3D('',#382787,#119342,#119343);
#100614=AXIS2_PLACEMENT_3D('',#382788,#119344,#119345);
#100615=AXIS2_PLACEMENT_3D('',#382789,#119346,#119347);
#100616=AXIS2_PLACEMENT_3D('',#382802,#119348,#119349);
#100617=AXIS2_PLACEMENT_3D('',#382815,#119350,#119351);
#100618=AXIS2_PLACEMENT_3D('',#382828,#119352,#119353);
#100619=AXIS2_PLACEMENT_3D('',#382841,#119354,#119355);
#100620=AXIS2_PLACEMENT_3D('',#382854,#119356,#119357);
#100621=AXIS2_PLACEMENT_3D('',#382855,#119358,#119359);
#100622=AXIS2_PLACEMENT_3D('',#382856,#119360,#119361);
#100623=AXIS2_PLACEMENT_3D('',#382869,#119362,#119363);
#100624=AXIS2_PLACEMENT_3D('',#382870,#119364,#119365);
#100625=AXIS2_PLACEMENT_3D('',#382880,#119367,#119368);
#100626=AXIS2_PLACEMENT_3D('',#382890,#119370,#119371);
#100627=AXIS2_PLACEMENT_3D('',#382893,#119372,#119373);
#100628=AXIS2_PLACEMENT_3D('',#382910,#119376,#119377);
#100629=AXIS2_PLACEMENT_3D('',#382960,#119378,#119379);
#100630=AXIS2_PLACEMENT_3D('',#383006,#119380,#119381);
#100631=AXIS2_PLACEMENT_3D('',#383023,#119382,#119383);
#100632=AXIS2_PLACEMENT_3D('',#383075,#119384,#119385);
#100633=AXIS2_PLACEMENT_3D('',#383076,#119386,#119387);
#100634=AXIS2_PLACEMENT_3D('',#383077,#119388,#119389);
#100635=AXIS2_PLACEMENT_3D('',#383078,#119390,#119391);
#100636=AXIS2_PLACEMENT_3D('',#383091,#119392,#119393);
#100637=AXIS2_PLACEMENT_3D('',#383092,#119394,#119395);
#100638=AXIS2_PLACEMENT_3D('',#383093,#119396,#119397);
#100639=AXIS2_PLACEMENT_3D('',#383106,#119398,#119399);
#100640=AXIS2_PLACEMENT_3D('',#383119,#119400,#119401);
#100641=AXIS2_PLACEMENT_3D('',#383132,#119402,#119403);
#100642=AXIS2_PLACEMENT_3D('',#383145,#119404,#119405);
#100643=AXIS2_PLACEMENT_3D('',#383158,#119406,#119407);
#100644=AXIS2_PLACEMENT_3D('',#383159,#119408,#119409);
#100645=AXIS2_PLACEMENT_3D('',#383160,#119410,#119411);
#100646=AXIS2_PLACEMENT_3D('',#383173,#119412,#119413);
#100647=AXIS2_PLACEMENT_3D('',#383174,#119414,#119415);
#100648=AXIS2_PLACEMENT_3D('',#383184,#119417,#119418);
#100649=AXIS2_PLACEMENT_3D('',#383194,#119420,#119421);
#100650=AXIS2_PLACEMENT_3D('',#383197,#119422,#119423);
#100651=AXIS2_PLACEMENT_3D('',#383214,#119426,#119427);
#100652=AXIS2_PLACEMENT_3D('',#383264,#119428,#119429);
#100653=AXIS2_PLACEMENT_3D('',#383310,#119430,#119431);
#100654=AXIS2_PLACEMENT_3D('',#383327,#119432,#119433);
#100655=AXIS2_PLACEMENT_3D('',#383379,#119434,#119435);
#100656=AXIS2_PLACEMENT_3D('',#383380,#119436,#119437);
#100657=AXIS2_PLACEMENT_3D('',#383381,#119438,#119439);
#100658=AXIS2_PLACEMENT_3D('',#383382,#119440,#119441);
#100659=AXIS2_PLACEMENT_3D('',#383395,#119442,#119443);
#100660=AXIS2_PLACEMENT_3D('',#383396,#119444,#119445);
#100661=AXIS2_PLACEMENT_3D('',#383397,#119446,#119447);
#100662=AXIS2_PLACEMENT_3D('',#383410,#119448,#119449);
#100663=AXIS2_PLACEMENT_3D('',#383423,#119450,#119451);
#100664=AXIS2_PLACEMENT_3D('',#383436,#119452,#119453);
#100665=AXIS2_PLACEMENT_3D('',#383449,#119454,#119455);
#100666=AXIS2_PLACEMENT_3D('',#383462,#119456,#119457);
#100667=AXIS2_PLACEMENT_3D('',#383463,#119458,#119459);
#100668=AXIS2_PLACEMENT_3D('',#383464,#119460,#119461);
#100669=AXIS2_PLACEMENT_3D('',#383477,#119462,#119463);
#100670=AXIS2_PLACEMENT_3D('',#383478,#119464,#119465);
#100671=AXIS2_PLACEMENT_3D('',#383488,#119467,#119468);
#100672=AXIS2_PLACEMENT_3D('',#383498,#119470,#119471);
#100673=AXIS2_PLACEMENT_3D('',#383501,#119472,#119473);
#100674=AXIS2_PLACEMENT_3D('',#383518,#119476,#119477);
#100675=AXIS2_PLACEMENT_3D('',#383568,#119478,#119479);
#100676=AXIS2_PLACEMENT_3D('',#383614,#119480,#119481);
#100677=AXIS2_PLACEMENT_3D('',#383631,#119482,#119483);
#100678=AXIS2_PLACEMENT_3D('',#383683,#119484,#119485);
#100679=AXIS2_PLACEMENT_3D('',#383684,#119486,#119487);
#100680=AXIS2_PLACEMENT_3D('',#383685,#119488,#119489);
#100681=AXIS2_PLACEMENT_3D('',#383686,#119490,#119491);
#100682=AXIS2_PLACEMENT_3D('',#383699,#119492,#119493);
#100683=AXIS2_PLACEMENT_3D('',#383700,#119494,#119495);
#100684=AXIS2_PLACEMENT_3D('',#383701,#119496,#119497);
#100685=AXIS2_PLACEMENT_3D('',#383714,#119498,#119499);
#100686=AXIS2_PLACEMENT_3D('',#383727,#119500,#119501);
#100687=AXIS2_PLACEMENT_3D('',#383740,#119502,#119503);
#100688=AXIS2_PLACEMENT_3D('',#383753,#119504,#119505);
#100689=AXIS2_PLACEMENT_3D('',#383766,#119506,#119507);
#100690=AXIS2_PLACEMENT_3D('',#383767,#119508,#119509);
#100691=AXIS2_PLACEMENT_3D('',#383768,#119510,#119511);
#100692=AXIS2_PLACEMENT_3D('',#383781,#119512,#119513);
#100693=AXIS2_PLACEMENT_3D('',#383782,#119514,#119515);
#100694=AXIS2_PLACEMENT_3D('',#383792,#119517,#119518);
#100695=AXIS2_PLACEMENT_3D('',#383802,#119520,#119521);
#100696=AXIS2_PLACEMENT_3D('',#383805,#119522,#119523);
#100697=AXIS2_PLACEMENT_3D('',#383822,#119526,#119527);
#100698=AXIS2_PLACEMENT_3D('',#383872,#119528,#119529);
#100699=AXIS2_PLACEMENT_3D('',#383918,#119530,#119531);
#100700=AXIS2_PLACEMENT_3D('',#383935,#119532,#119533);
#100701=AXIS2_PLACEMENT_3D('',#383987,#119534,#119535);
#100702=AXIS2_PLACEMENT_3D('',#383988,#119536,#119537);
#100703=AXIS2_PLACEMENT_3D('',#383989,#119538,#119539);
#100704=AXIS2_PLACEMENT_3D('',#383990,#119540,#119541);
#100705=AXIS2_PLACEMENT_3D('',#384003,#119542,#119543);
#100706=AXIS2_PLACEMENT_3D('',#384004,#119544,#119545);
#100707=AXIS2_PLACEMENT_3D('',#384005,#119546,#119547);
#100708=AXIS2_PLACEMENT_3D('',#384018,#119548,#119549);
#100709=AXIS2_PLACEMENT_3D('',#384031,#119550,#119551);
#100710=AXIS2_PLACEMENT_3D('',#384044,#119552,#119553);
#100711=AXIS2_PLACEMENT_3D('',#384057,#119554,#119555);
#100712=AXIS2_PLACEMENT_3D('',#384070,#119556,#119557);
#100713=AXIS2_PLACEMENT_3D('',#384071,#119558,#119559);
#100714=AXIS2_PLACEMENT_3D('',#384072,#119560,#119561);
#100715=AXIS2_PLACEMENT_3D('',#384085,#119562,#119563);
#100716=AXIS2_PLACEMENT_3D('',#384086,#119564,#119565);
#100717=AXIS2_PLACEMENT_3D('',#384096,#119567,#119568);
#100718=AXIS2_PLACEMENT_3D('',#384106,#119570,#119571);
#100719=AXIS2_PLACEMENT_3D('',#384109,#119572,#119573);
#100720=AXIS2_PLACEMENT_3D('',#384126,#119576,#119577);
#100721=AXIS2_PLACEMENT_3D('',#384176,#119578,#119579);
#100722=AXIS2_PLACEMENT_3D('',#384222,#119580,#119581);
#100723=AXIS2_PLACEMENT_3D('',#384239,#119582,#119583);
#100724=AXIS2_PLACEMENT_3D('',#384291,#119584,#119585);
#100725=AXIS2_PLACEMENT_3D('',#384292,#119586,#119587);
#100726=AXIS2_PLACEMENT_3D('',#384293,#119588,#119589);
#100727=AXIS2_PLACEMENT_3D('',#384294,#119590,#119591);
#100728=AXIS2_PLACEMENT_3D('',#384307,#119592,#119593);
#100729=AXIS2_PLACEMENT_3D('',#384308,#119594,#119595);
#100730=AXIS2_PLACEMENT_3D('',#384309,#119596,#119597);
#100731=AXIS2_PLACEMENT_3D('',#384322,#119598,#119599);
#100732=AXIS2_PLACEMENT_3D('',#384335,#119600,#119601);
#100733=AXIS2_PLACEMENT_3D('',#384348,#119602,#119603);
#100734=AXIS2_PLACEMENT_3D('',#384361,#119604,#119605);
#100735=AXIS2_PLACEMENT_3D('',#384374,#119606,#119607);
#100736=AXIS2_PLACEMENT_3D('',#384375,#119608,#119609);
#100737=AXIS2_PLACEMENT_3D('',#384376,#119610,#119611);
#100738=AXIS2_PLACEMENT_3D('',#384389,#119612,#119613);
#100739=AXIS2_PLACEMENT_3D('',#384390,#119614,#119615);
#100740=AXIS2_PLACEMENT_3D('',#384400,#119617,#119618);
#100741=AXIS2_PLACEMENT_3D('',#384410,#119620,#119621);
#100742=AXIS2_PLACEMENT_3D('',#384413,#119622,#119623);
#100743=AXIS2_PLACEMENT_3D('',#384430,#119626,#119627);
#100744=AXIS2_PLACEMENT_3D('',#384480,#119628,#119629);
#100745=AXIS2_PLACEMENT_3D('',#384526,#119630,#119631);
#100746=AXIS2_PLACEMENT_3D('',#384543,#119632,#119633);
#100747=AXIS2_PLACEMENT_3D('',#384595,#119634,#119635);
#100748=AXIS2_PLACEMENT_3D('',#384596,#119636,#119637);
#100749=AXIS2_PLACEMENT_3D('',#384597,#119638,#119639);
#100750=AXIS2_PLACEMENT_3D('',#384598,#119640,#119641);
#100751=AXIS2_PLACEMENT_3D('',#384611,#119642,#119643);
#100752=AXIS2_PLACEMENT_3D('',#384612,#119644,#119645);
#100753=AXIS2_PLACEMENT_3D('',#384613,#119646,#119647);
#100754=AXIS2_PLACEMENT_3D('',#384626,#119648,#119649);
#100755=AXIS2_PLACEMENT_3D('',#384639,#119650,#119651);
#100756=AXIS2_PLACEMENT_3D('',#384652,#119652,#119653);
#100757=AXIS2_PLACEMENT_3D('',#384665,#119654,#119655);
#100758=AXIS2_PLACEMENT_3D('',#384678,#119656,#119657);
#100759=AXIS2_PLACEMENT_3D('',#384679,#119658,#119659);
#100760=AXIS2_PLACEMENT_3D('',#384680,#119660,#119661);
#100761=AXIS2_PLACEMENT_3D('',#384693,#119662,#119663);
#100762=AXIS2_PLACEMENT_3D('',#384694,#119664,#119665);
#100763=AXIS2_PLACEMENT_3D('',#384704,#119667,#119668);
#100764=AXIS2_PLACEMENT_3D('',#384714,#119670,#119671);
#100765=AXIS2_PLACEMENT_3D('',#384717,#119672,#119673);
#100766=AXIS2_PLACEMENT_3D('',#384734,#119676,#119677);
#100767=AXIS2_PLACEMENT_3D('',#384784,#119678,#119679);
#100768=AXIS2_PLACEMENT_3D('',#384830,#119680,#119681);
#100769=AXIS2_PLACEMENT_3D('',#384847,#119682,#119683);
#100770=AXIS2_PLACEMENT_3D('',#384899,#119684,#119685);
#100771=AXIS2_PLACEMENT_3D('',#384900,#119686,#119687);
#100772=AXIS2_PLACEMENT_3D('',#384901,#119688,#119689);
#100773=AXIS2_PLACEMENT_3D('',#384902,#119690,#119691);
#100774=AXIS2_PLACEMENT_3D('',#384915,#119692,#119693);
#100775=AXIS2_PLACEMENT_3D('',#384916,#119694,#119695);
#100776=AXIS2_PLACEMENT_3D('',#384917,#119696,#119697);
#100777=AXIS2_PLACEMENT_3D('',#384930,#119698,#119699);
#100778=AXIS2_PLACEMENT_3D('',#384943,#119700,#119701);
#100779=AXIS2_PLACEMENT_3D('',#384956,#119702,#119703);
#100780=AXIS2_PLACEMENT_3D('',#384969,#119704,#119705);
#100781=AXIS2_PLACEMENT_3D('',#384982,#119706,#119707);
#100782=AXIS2_PLACEMENT_3D('',#384983,#119708,#119709);
#100783=AXIS2_PLACEMENT_3D('',#384984,#119710,#119711);
#100784=AXIS2_PLACEMENT_3D('',#384997,#119712,#119713);
#100785=AXIS2_PLACEMENT_3D('',#384998,#119714,#119715);
#100786=AXIS2_PLACEMENT_3D('',#385008,#119717,#119718);
#100787=AXIS2_PLACEMENT_3D('',#385018,#119720,#119721);
#100788=AXIS2_PLACEMENT_3D('',#385021,#119722,#119723);
#100789=AXIS2_PLACEMENT_3D('',#385038,#119726,#119727);
#100790=AXIS2_PLACEMENT_3D('',#385088,#119728,#119729);
#100791=AXIS2_PLACEMENT_3D('',#385134,#119730,#119731);
#100792=AXIS2_PLACEMENT_3D('',#385151,#119732,#119733);
#100793=AXIS2_PLACEMENT_3D('',#385203,#119734,#119735);
#100794=AXIS2_PLACEMENT_3D('',#385204,#119736,#119737);
#100795=AXIS2_PLACEMENT_3D('',#385205,#119738,#119739);
#100796=AXIS2_PLACEMENT_3D('',#385206,#119740,#119741);
#100797=AXIS2_PLACEMENT_3D('',#385219,#119742,#119743);
#100798=AXIS2_PLACEMENT_3D('',#385220,#119744,#119745);
#100799=AXIS2_PLACEMENT_3D('',#385221,#119746,#119747);
#100800=AXIS2_PLACEMENT_3D('',#385234,#119748,#119749);
#100801=AXIS2_PLACEMENT_3D('',#385247,#119750,#119751);
#100802=AXIS2_PLACEMENT_3D('',#385260,#119752,#119753);
#100803=AXIS2_PLACEMENT_3D('',#385273,#119754,#119755);
#100804=AXIS2_PLACEMENT_3D('',#385286,#119756,#119757);
#100805=AXIS2_PLACEMENT_3D('',#385287,#119758,#119759);
#100806=AXIS2_PLACEMENT_3D('',#385288,#119760,#119761);
#100807=AXIS2_PLACEMENT_3D('',#385301,#119762,#119763);
#100808=AXIS2_PLACEMENT_3D('',#385302,#119764,#119765);
#100809=AXIS2_PLACEMENT_3D('',#385312,#119767,#119768);
#100810=AXIS2_PLACEMENT_3D('',#385322,#119770,#119771);
#100811=AXIS2_PLACEMENT_3D('',#385325,#119772,#119773);
#100812=AXIS2_PLACEMENT_3D('',#385342,#119776,#119777);
#100813=AXIS2_PLACEMENT_3D('',#385392,#119778,#119779);
#100814=AXIS2_PLACEMENT_3D('',#385438,#119780,#119781);
#100815=AXIS2_PLACEMENT_3D('',#385455,#119782,#119783);
#100816=AXIS2_PLACEMENT_3D('',#385507,#119784,#119785);
#100817=AXIS2_PLACEMENT_3D('',#385508,#119786,#119787);
#100818=AXIS2_PLACEMENT_3D('',#385509,#119788,#119789);
#100819=AXIS2_PLACEMENT_3D('',#385510,#119790,#119791);
#100820=AXIS2_PLACEMENT_3D('',#385523,#119792,#119793);
#100821=AXIS2_PLACEMENT_3D('',#385524,#119794,#119795);
#100822=AXIS2_PLACEMENT_3D('',#385525,#119796,#119797);
#100823=AXIS2_PLACEMENT_3D('',#385538,#119798,#119799);
#100824=AXIS2_PLACEMENT_3D('',#385551,#119800,#119801);
#100825=AXIS2_PLACEMENT_3D('',#385564,#119802,#119803);
#100826=AXIS2_PLACEMENT_3D('',#385577,#119804,#119805);
#100827=AXIS2_PLACEMENT_3D('',#385590,#119806,#119807);
#100828=AXIS2_PLACEMENT_3D('',#385591,#119808,#119809);
#100829=AXIS2_PLACEMENT_3D('',#385592,#119810,#119811);
#100830=AXIS2_PLACEMENT_3D('',#385605,#119812,#119813);
#100831=AXIS2_PLACEMENT_3D('',#385606,#119814,#119815);
#100832=AXIS2_PLACEMENT_3D('',#385616,#119817,#119818);
#100833=AXIS2_PLACEMENT_3D('',#385626,#119820,#119821);
#100834=AXIS2_PLACEMENT_3D('',#385629,#119822,#119823);
#100835=AXIS2_PLACEMENT_3D('',#385646,#119826,#119827);
#100836=AXIS2_PLACEMENT_3D('',#385696,#119828,#119829);
#100837=AXIS2_PLACEMENT_3D('',#385742,#119830,#119831);
#100838=AXIS2_PLACEMENT_3D('',#385759,#119832,#119833);
#100839=AXIS2_PLACEMENT_3D('',#385811,#119834,#119835);
#100840=AXIS2_PLACEMENT_3D('',#385812,#119836,#119837);
#100841=AXIS2_PLACEMENT_3D('',#385813,#119838,#119839);
#100842=AXIS2_PLACEMENT_3D('',#385814,#119840,#119841);
#100843=AXIS2_PLACEMENT_3D('',#385827,#119842,#119843);
#100844=AXIS2_PLACEMENT_3D('',#385828,#119844,#119845);
#100845=AXIS2_PLACEMENT_3D('',#385829,#119846,#119847);
#100846=AXIS2_PLACEMENT_3D('',#385842,#119848,#119849);
#100847=AXIS2_PLACEMENT_3D('',#385855,#119850,#119851);
#100848=AXIS2_PLACEMENT_3D('',#385868,#119852,#119853);
#100849=AXIS2_PLACEMENT_3D('',#385881,#119854,#119855);
#100850=AXIS2_PLACEMENT_3D('',#385894,#119856,#119857);
#100851=AXIS2_PLACEMENT_3D('',#385895,#119858,#119859);
#100852=AXIS2_PLACEMENT_3D('',#385896,#119860,#119861);
#100853=AXIS2_PLACEMENT_3D('',#385909,#119862,#119863);
#100854=AXIS2_PLACEMENT_3D('',#385910,#119864,#119865);
#100855=AXIS2_PLACEMENT_3D('',#385920,#119867,#119868);
#100856=AXIS2_PLACEMENT_3D('',#385930,#119870,#119871);
#100857=AXIS2_PLACEMENT_3D('',#385933,#119872,#119873);
#100858=AXIS2_PLACEMENT_3D('',#385950,#119876,#119877);
#100859=AXIS2_PLACEMENT_3D('',#386000,#119878,#119879);
#100860=AXIS2_PLACEMENT_3D('',#386046,#119880,#119881);
#100861=AXIS2_PLACEMENT_3D('',#386063,#119882,#119883);
#100862=AXIS2_PLACEMENT_3D('',#386115,#119884,#119885);
#100863=AXIS2_PLACEMENT_3D('',#386116,#119886,#119887);
#100864=AXIS2_PLACEMENT_3D('',#386117,#119888,#119889);
#100865=AXIS2_PLACEMENT_3D('',#386118,#119890,#119891);
#100866=AXIS2_PLACEMENT_3D('',#386131,#119892,#119893);
#100867=AXIS2_PLACEMENT_3D('',#386132,#119894,#119895);
#100868=AXIS2_PLACEMENT_3D('',#386133,#119896,#119897);
#100869=AXIS2_PLACEMENT_3D('',#386146,#119898,#119899);
#100870=AXIS2_PLACEMENT_3D('',#386159,#119900,#119901);
#100871=AXIS2_PLACEMENT_3D('',#386172,#119902,#119903);
#100872=AXIS2_PLACEMENT_3D('',#386185,#119904,#119905);
#100873=AXIS2_PLACEMENT_3D('',#386198,#119906,#119907);
#100874=AXIS2_PLACEMENT_3D('',#386199,#119908,#119909);
#100875=AXIS2_PLACEMENT_3D('',#386200,#119910,#119911);
#100876=AXIS2_PLACEMENT_3D('',#386213,#119912,#119913);
#100877=AXIS2_PLACEMENT_3D('',#386214,#119914,#119915);
#100878=AXIS2_PLACEMENT_3D('',#386224,#119917,#119918);
#100879=AXIS2_PLACEMENT_3D('',#386234,#119920,#119921);
#100880=AXIS2_PLACEMENT_3D('',#386237,#119922,#119923);
#100881=AXIS2_PLACEMENT_3D('',#386254,#119926,#119927);
#100882=AXIS2_PLACEMENT_3D('',#386304,#119928,#119929);
#100883=AXIS2_PLACEMENT_3D('',#386350,#119930,#119931);
#100884=AXIS2_PLACEMENT_3D('',#386367,#119932,#119933);
#100885=AXIS2_PLACEMENT_3D('',#386419,#119934,#119935);
#100886=AXIS2_PLACEMENT_3D('',#386420,#119936,#119937);
#100887=AXIS2_PLACEMENT_3D('',#386421,#119938,#119939);
#100888=AXIS2_PLACEMENT_3D('',#386422,#119940,#119941);
#100889=AXIS2_PLACEMENT_3D('',#386435,#119942,#119943);
#100890=AXIS2_PLACEMENT_3D('',#386436,#119944,#119945);
#100891=AXIS2_PLACEMENT_3D('',#386437,#119946,#119947);
#100892=AXIS2_PLACEMENT_3D('',#386450,#119948,#119949);
#100893=AXIS2_PLACEMENT_3D('',#386463,#119950,#119951);
#100894=AXIS2_PLACEMENT_3D('',#386476,#119952,#119953);
#100895=AXIS2_PLACEMENT_3D('',#386489,#119954,#119955);
#100896=AXIS2_PLACEMENT_3D('',#386502,#119956,#119957);
#100897=AXIS2_PLACEMENT_3D('',#386503,#119958,#119959);
#100898=AXIS2_PLACEMENT_3D('',#386504,#119960,#119961);
#100899=AXIS2_PLACEMENT_3D('',#386517,#119962,#119963);
#100900=AXIS2_PLACEMENT_3D('',#386518,#119964,#119965);
#100901=AXIS2_PLACEMENT_3D('',#386528,#119967,#119968);
#100902=AXIS2_PLACEMENT_3D('',#386538,#119970,#119971);
#100903=AXIS2_PLACEMENT_3D('',#386541,#119972,#119973);
#100904=AXIS2_PLACEMENT_3D('',#386558,#119976,#119977);
#100905=AXIS2_PLACEMENT_3D('',#386608,#119978,#119979);
#100906=AXIS2_PLACEMENT_3D('',#386654,#119980,#119981);
#100907=AXIS2_PLACEMENT_3D('',#386671,#119982,#119983);
#100908=AXIS2_PLACEMENT_3D('',#386723,#119984,#119985);
#100909=AXIS2_PLACEMENT_3D('',#386724,#119986,#119987);
#100910=AXIS2_PLACEMENT_3D('',#386725,#119988,#119989);
#100911=AXIS2_PLACEMENT_3D('',#386726,#119990,#119991);
#100912=AXIS2_PLACEMENT_3D('',#386739,#119992,#119993);
#100913=AXIS2_PLACEMENT_3D('',#386740,#119994,#119995);
#100914=AXIS2_PLACEMENT_3D('',#386741,#119996,#119997);
#100915=AXIS2_PLACEMENT_3D('',#386754,#119998,#119999);
#100916=AXIS2_PLACEMENT_3D('',#386767,#120000,#120001);
#100917=AXIS2_PLACEMENT_3D('',#386780,#120002,#120003);
#100918=AXIS2_PLACEMENT_3D('',#386793,#120004,#120005);
#100919=AXIS2_PLACEMENT_3D('',#386806,#120006,#120007);
#100920=AXIS2_PLACEMENT_3D('',#386807,#120008,#120009);
#100921=AXIS2_PLACEMENT_3D('',#386808,#120010,#120011);
#100922=AXIS2_PLACEMENT_3D('',#386821,#120012,#120013);
#100923=AXIS2_PLACEMENT_3D('',#386822,#120014,#120015);
#100924=AXIS2_PLACEMENT_3D('',#386832,#120017,#120018);
#100925=AXIS2_PLACEMENT_3D('',#386842,#120020,#120021);
#100926=AXIS2_PLACEMENT_3D('',#386845,#120022,#120023);
#100927=AXIS2_PLACEMENT_3D('',#386862,#120026,#120027);
#100928=AXIS2_PLACEMENT_3D('',#386912,#120028,#120029);
#100929=AXIS2_PLACEMENT_3D('',#386958,#120030,#120031);
#100930=AXIS2_PLACEMENT_3D('',#386975,#120032,#120033);
#100931=AXIS2_PLACEMENT_3D('',#387027,#120034,#120035);
#100932=AXIS2_PLACEMENT_3D('',#387028,#120036,#120037);
#100933=AXIS2_PLACEMENT_3D('',#387029,#120038,#120039);
#100934=AXIS2_PLACEMENT_3D('',#387030,#120040,#120041);
#100935=AXIS2_PLACEMENT_3D('',#387043,#120042,#120043);
#100936=AXIS2_PLACEMENT_3D('',#387044,#120044,#120045);
#100937=AXIS2_PLACEMENT_3D('',#387045,#120046,#120047);
#100938=AXIS2_PLACEMENT_3D('',#387058,#120048,#120049);
#100939=AXIS2_PLACEMENT_3D('',#387071,#120050,#120051);
#100940=AXIS2_PLACEMENT_3D('',#387084,#120052,#120053);
#100941=AXIS2_PLACEMENT_3D('',#387097,#120054,#120055);
#100942=AXIS2_PLACEMENT_3D('',#387110,#120056,#120057);
#100943=AXIS2_PLACEMENT_3D('',#387111,#120058,#120059);
#100944=AXIS2_PLACEMENT_3D('',#387112,#120060,#120061);
#100945=AXIS2_PLACEMENT_3D('',#387125,#120062,#120063);
#100946=AXIS2_PLACEMENT_3D('',#387126,#120064,#120065);
#100947=AXIS2_PLACEMENT_3D('',#387136,#120067,#120068);
#100948=AXIS2_PLACEMENT_3D('',#387146,#120070,#120071);
#100949=AXIS2_PLACEMENT_3D('',#387149,#120072,#120073);
#100950=AXIS2_PLACEMENT_3D('',#387166,#120076,#120077);
#100951=AXIS2_PLACEMENT_3D('',#387216,#120078,#120079);
#100952=AXIS2_PLACEMENT_3D('',#387262,#120080,#120081);
#100953=AXIS2_PLACEMENT_3D('',#387279,#120082,#120083);
#100954=AXIS2_PLACEMENT_3D('',#387331,#120084,#120085);
#100955=AXIS2_PLACEMENT_3D('',#387332,#120086,#120087);
#100956=AXIS2_PLACEMENT_3D('',#387333,#120088,#120089);
#100957=AXIS2_PLACEMENT_3D('',#387334,#120090,#120091);
#100958=AXIS2_PLACEMENT_3D('',#387347,#120092,#120093);
#100959=AXIS2_PLACEMENT_3D('',#387348,#120094,#120095);
#100960=AXIS2_PLACEMENT_3D('',#387349,#120096,#120097);
#100961=AXIS2_PLACEMENT_3D('',#387362,#120098,#120099);
#100962=AXIS2_PLACEMENT_3D('',#387375,#120100,#120101);
#100963=AXIS2_PLACEMENT_3D('',#387388,#120102,#120103);
#100964=AXIS2_PLACEMENT_3D('',#387401,#120104,#120105);
#100965=AXIS2_PLACEMENT_3D('',#387414,#120106,#120107);
#100966=AXIS2_PLACEMENT_3D('',#387415,#120108,#120109);
#100967=AXIS2_PLACEMENT_3D('',#387416,#120110,#120111);
#100968=AXIS2_PLACEMENT_3D('',#387429,#120112,#120113);
#100969=AXIS2_PLACEMENT_3D('',#387430,#120114,#120115);
#100970=AXIS2_PLACEMENT_3D('',#387440,#120117,#120118);
#100971=AXIS2_PLACEMENT_3D('',#387450,#120120,#120121);
#100972=AXIS2_PLACEMENT_3D('',#387453,#120122,#120123);
#100973=AXIS2_PLACEMENT_3D('',#387470,#120126,#120127);
#100974=AXIS2_PLACEMENT_3D('',#387520,#120128,#120129);
#100975=AXIS2_PLACEMENT_3D('',#387566,#120130,#120131);
#100976=AXIS2_PLACEMENT_3D('',#387583,#120132,#120133);
#100977=AXIS2_PLACEMENT_3D('',#387635,#120134,#120135);
#100978=AXIS2_PLACEMENT_3D('',#387636,#120136,#120137);
#100979=AXIS2_PLACEMENT_3D('',#387637,#120138,#120139);
#100980=AXIS2_PLACEMENT_3D('',#387638,#120140,#120141);
#100981=AXIS2_PLACEMENT_3D('',#387651,#120142,#120143);
#100982=AXIS2_PLACEMENT_3D('',#387652,#120144,#120145);
#100983=AXIS2_PLACEMENT_3D('',#387653,#120146,#120147);
#100984=AXIS2_PLACEMENT_3D('',#387666,#120148,#120149);
#100985=AXIS2_PLACEMENT_3D('',#387679,#120150,#120151);
#100986=AXIS2_PLACEMENT_3D('',#387692,#120152,#120153);
#100987=AXIS2_PLACEMENT_3D('',#387705,#120154,#120155);
#100988=AXIS2_PLACEMENT_3D('',#387718,#120156,#120157);
#100989=AXIS2_PLACEMENT_3D('',#387719,#120158,#120159);
#100990=AXIS2_PLACEMENT_3D('',#387720,#120160,#120161);
#100991=AXIS2_PLACEMENT_3D('',#387733,#120162,#120163);
#100992=AXIS2_PLACEMENT_3D('',#387734,#120164,#120165);
#100993=AXIS2_PLACEMENT_3D('',#387744,#120167,#120168);
#100994=AXIS2_PLACEMENT_3D('',#387754,#120170,#120171);
#100995=AXIS2_PLACEMENT_3D('',#387757,#120172,#120173);
#100996=AXIS2_PLACEMENT_3D('',#387774,#120176,#120177);
#100997=AXIS2_PLACEMENT_3D('',#387824,#120178,#120179);
#100998=AXIS2_PLACEMENT_3D('',#387870,#120180,#120181);
#100999=AXIS2_PLACEMENT_3D('',#387887,#120182,#120183);
#101000=AXIS2_PLACEMENT_3D('',#387939,#120184,#120185);
#101001=AXIS2_PLACEMENT_3D('',#387940,#120186,#120187);
#101002=AXIS2_PLACEMENT_3D('',#387941,#120188,#120189);
#101003=AXIS2_PLACEMENT_3D('',#387942,#120190,#120191);
#101004=AXIS2_PLACEMENT_3D('',#387955,#120192,#120193);
#101005=AXIS2_PLACEMENT_3D('',#387956,#120194,#120195);
#101006=AXIS2_PLACEMENT_3D('',#387957,#120196,#120197);
#101007=AXIS2_PLACEMENT_3D('',#387970,#120198,#120199);
#101008=AXIS2_PLACEMENT_3D('',#387983,#120200,#120201);
#101009=AXIS2_PLACEMENT_3D('',#387996,#120202,#120203);
#101010=AXIS2_PLACEMENT_3D('',#388009,#120204,#120205);
#101011=AXIS2_PLACEMENT_3D('',#388022,#120206,#120207);
#101012=AXIS2_PLACEMENT_3D('',#388023,#120208,#120209);
#101013=AXIS2_PLACEMENT_3D('',#388024,#120210,#120211);
#101014=AXIS2_PLACEMENT_3D('',#388037,#120212,#120213);
#101015=AXIS2_PLACEMENT_3D('',#388038,#120214,#120215);
#101016=AXIS2_PLACEMENT_3D('',#388048,#120217,#120218);
#101017=AXIS2_PLACEMENT_3D('',#388058,#120220,#120221);
#101018=AXIS2_PLACEMENT_3D('',#388061,#120222,#120223);
#101019=AXIS2_PLACEMENT_3D('',#388078,#120226,#120227);
#101020=AXIS2_PLACEMENT_3D('',#388128,#120228,#120229);
#101021=AXIS2_PLACEMENT_3D('',#388174,#120230,#120231);
#101022=AXIS2_PLACEMENT_3D('',#388191,#120232,#120233);
#101023=AXIS2_PLACEMENT_3D('',#388243,#120234,#120235);
#101024=AXIS2_PLACEMENT_3D('',#388244,#120236,#120237);
#101025=AXIS2_PLACEMENT_3D('',#388245,#120238,#120239);
#101026=AXIS2_PLACEMENT_3D('',#388246,#120240,#120241);
#101027=AXIS2_PLACEMENT_3D('',#388259,#120242,#120243);
#101028=AXIS2_PLACEMENT_3D('',#388260,#120244,#120245);
#101029=AXIS2_PLACEMENT_3D('',#388261,#120246,#120247);
#101030=AXIS2_PLACEMENT_3D('',#388274,#120248,#120249);
#101031=AXIS2_PLACEMENT_3D('',#388287,#120250,#120251);
#101032=AXIS2_PLACEMENT_3D('',#388300,#120252,#120253);
#101033=AXIS2_PLACEMENT_3D('',#388313,#120254,#120255);
#101034=AXIS2_PLACEMENT_3D('',#388326,#120256,#120257);
#101035=AXIS2_PLACEMENT_3D('',#388327,#120258,#120259);
#101036=AXIS2_PLACEMENT_3D('',#388328,#120260,#120261);
#101037=AXIS2_PLACEMENT_3D('',#388341,#120262,#120263);
#101038=AXIS2_PLACEMENT_3D('',#388342,#120264,#120265);
#101039=AXIS2_PLACEMENT_3D('',#388352,#120267,#120268);
#101040=AXIS2_PLACEMENT_3D('',#388362,#120270,#120271);
#101041=AXIS2_PLACEMENT_3D('',#388365,#120272,#120273);
#101042=AXIS2_PLACEMENT_3D('',#388382,#120276,#120277);
#101043=AXIS2_PLACEMENT_3D('',#388432,#120278,#120279);
#101044=AXIS2_PLACEMENT_3D('',#388478,#120280,#120281);
#101045=AXIS2_PLACEMENT_3D('',#388495,#120282,#120283);
#101046=AXIS2_PLACEMENT_3D('',#388547,#120284,#120285);
#101047=AXIS2_PLACEMENT_3D('',#388548,#120286,#120287);
#101048=AXIS2_PLACEMENT_3D('',#388549,#120288,#120289);
#101049=AXIS2_PLACEMENT_3D('',#388550,#120290,#120291);
#101050=AXIS2_PLACEMENT_3D('',#388563,#120292,#120293);
#101051=AXIS2_PLACEMENT_3D('',#388564,#120294,#120295);
#101052=AXIS2_PLACEMENT_3D('',#388565,#120296,#120297);
#101053=AXIS2_PLACEMENT_3D('',#388578,#120298,#120299);
#101054=AXIS2_PLACEMENT_3D('',#388591,#120300,#120301);
#101055=AXIS2_PLACEMENT_3D('',#388604,#120302,#120303);
#101056=AXIS2_PLACEMENT_3D('',#388617,#120304,#120305);
#101057=AXIS2_PLACEMENT_3D('',#388630,#120306,#120307);
#101058=AXIS2_PLACEMENT_3D('',#388631,#120308,#120309);
#101059=AXIS2_PLACEMENT_3D('',#388632,#120310,#120311);
#101060=AXIS2_PLACEMENT_3D('',#388645,#120312,#120313);
#101061=AXIS2_PLACEMENT_3D('',#388646,#120314,#120315);
#101062=AXIS2_PLACEMENT_3D('',#388656,#120317,#120318);
#101063=AXIS2_PLACEMENT_3D('',#388666,#120320,#120321);
#101064=AXIS2_PLACEMENT_3D('',#388669,#120322,#120323);
#101065=AXIS2_PLACEMENT_3D('',#388686,#120326,#120327);
#101066=AXIS2_PLACEMENT_3D('',#388736,#120328,#120329);
#101067=AXIS2_PLACEMENT_3D('',#388782,#120330,#120331);
#101068=AXIS2_PLACEMENT_3D('',#388799,#120332,#120333);
#101069=AXIS2_PLACEMENT_3D('',#388851,#120334,#120335);
#101070=AXIS2_PLACEMENT_3D('',#388852,#120336,#120337);
#101071=AXIS2_PLACEMENT_3D('',#388853,#120338,#120339);
#101072=AXIS2_PLACEMENT_3D('',#388854,#120340,#120341);
#101073=AXIS2_PLACEMENT_3D('',#388867,#120342,#120343);
#101074=AXIS2_PLACEMENT_3D('',#388868,#120344,#120345);
#101075=AXIS2_PLACEMENT_3D('',#388869,#120346,#120347);
#101076=AXIS2_PLACEMENT_3D('',#388882,#120348,#120349);
#101077=AXIS2_PLACEMENT_3D('',#388895,#120350,#120351);
#101078=AXIS2_PLACEMENT_3D('',#388908,#120352,#120353);
#101079=AXIS2_PLACEMENT_3D('',#388921,#120354,#120355);
#101080=AXIS2_PLACEMENT_3D('',#388934,#120356,#120357);
#101081=AXIS2_PLACEMENT_3D('',#388935,#120358,#120359);
#101082=AXIS2_PLACEMENT_3D('',#388936,#120360,#120361);
#101083=AXIS2_PLACEMENT_3D('',#388949,#120362,#120363);
#101084=AXIS2_PLACEMENT_3D('',#388950,#120364,#120365);
#101085=AXIS2_PLACEMENT_3D('',#388960,#120367,#120368);
#101086=AXIS2_PLACEMENT_3D('',#388970,#120370,#120371);
#101087=AXIS2_PLACEMENT_3D('',#388973,#120372,#120373);
#101088=AXIS2_PLACEMENT_3D('',#388990,#120376,#120377);
#101089=AXIS2_PLACEMENT_3D('',#389040,#120378,#120379);
#101090=AXIS2_PLACEMENT_3D('',#389086,#120380,#120381);
#101091=AXIS2_PLACEMENT_3D('',#389103,#120382,#120383);
#101092=AXIS2_PLACEMENT_3D('',#389155,#120384,#120385);
#101093=AXIS2_PLACEMENT_3D('',#389156,#120386,#120387);
#101094=AXIS2_PLACEMENT_3D('',#389157,#120388,#120389);
#101095=AXIS2_PLACEMENT_3D('',#389158,#120390,#120391);
#101096=AXIS2_PLACEMENT_3D('',#389171,#120392,#120393);
#101097=AXIS2_PLACEMENT_3D('',#389172,#120394,#120395);
#101098=AXIS2_PLACEMENT_3D('',#389173,#120396,#120397);
#101099=AXIS2_PLACEMENT_3D('',#389186,#120398,#120399);
#101100=AXIS2_PLACEMENT_3D('',#389199,#120400,#120401);
#101101=AXIS2_PLACEMENT_3D('',#389212,#120402,#120403);
#101102=AXIS2_PLACEMENT_3D('',#389225,#120404,#120405);
#101103=AXIS2_PLACEMENT_3D('',#389238,#120406,#120407);
#101104=AXIS2_PLACEMENT_3D('',#389239,#120408,#120409);
#101105=AXIS2_PLACEMENT_3D('',#389240,#120410,#120411);
#101106=AXIS2_PLACEMENT_3D('',#389253,#120412,#120413);
#101107=AXIS2_PLACEMENT_3D('',#389254,#120414,#120415);
#101108=AXIS2_PLACEMENT_3D('',#389264,#120417,#120418);
#101109=AXIS2_PLACEMENT_3D('',#389274,#120420,#120421);
#101110=AXIS2_PLACEMENT_3D('',#389277,#120422,#120423);
#101111=AXIS2_PLACEMENT_3D('',#389294,#120426,#120427);
#101112=AXIS2_PLACEMENT_3D('',#389344,#120428,#120429);
#101113=AXIS2_PLACEMENT_3D('',#389390,#120430,#120431);
#101114=AXIS2_PLACEMENT_3D('',#389407,#120432,#120433);
#101115=AXIS2_PLACEMENT_3D('',#389459,#120434,#120435);
#101116=AXIS2_PLACEMENT_3D('',#389460,#120436,#120437);
#101117=AXIS2_PLACEMENT_3D('',#389461,#120438,#120439);
#101118=AXIS2_PLACEMENT_3D('',#389462,#120440,#120441);
#101119=AXIS2_PLACEMENT_3D('',#389475,#120442,#120443);
#101120=AXIS2_PLACEMENT_3D('',#389476,#120444,#120445);
#101121=AXIS2_PLACEMENT_3D('',#389477,#120446,#120447);
#101122=AXIS2_PLACEMENT_3D('',#389490,#120448,#120449);
#101123=AXIS2_PLACEMENT_3D('',#389503,#120450,#120451);
#101124=AXIS2_PLACEMENT_3D('',#389516,#120452,#120453);
#101125=AXIS2_PLACEMENT_3D('',#389529,#120454,#120455);
#101126=AXIS2_PLACEMENT_3D('',#389542,#120456,#120457);
#101127=AXIS2_PLACEMENT_3D('',#389543,#120458,#120459);
#101128=AXIS2_PLACEMENT_3D('',#389544,#120460,#120461);
#101129=AXIS2_PLACEMENT_3D('',#389557,#120462,#120463);
#101130=AXIS2_PLACEMENT_3D('',#389558,#120464,#120465);
#101131=AXIS2_PLACEMENT_3D('',#389568,#120467,#120468);
#101132=AXIS2_PLACEMENT_3D('',#389578,#120470,#120471);
#101133=AXIS2_PLACEMENT_3D('',#389581,#120472,#120473);
#101134=AXIS2_PLACEMENT_3D('',#389598,#120476,#120477);
#101135=AXIS2_PLACEMENT_3D('',#389648,#120478,#120479);
#101136=AXIS2_PLACEMENT_3D('',#389694,#120480,#120481);
#101137=AXIS2_PLACEMENT_3D('',#389711,#120482,#120483);
#101138=AXIS2_PLACEMENT_3D('',#389763,#120484,#120485);
#101139=AXIS2_PLACEMENT_3D('',#389764,#120486,#120487);
#101140=AXIS2_PLACEMENT_3D('',#389765,#120488,#120489);
#101141=AXIS2_PLACEMENT_3D('',#389766,#120490,#120491);
#101142=AXIS2_PLACEMENT_3D('',#389779,#120492,#120493);
#101143=AXIS2_PLACEMENT_3D('',#389780,#120494,#120495);
#101144=AXIS2_PLACEMENT_3D('',#389781,#120496,#120497);
#101145=AXIS2_PLACEMENT_3D('',#389794,#120498,#120499);
#101146=AXIS2_PLACEMENT_3D('',#389807,#120500,#120501);
#101147=AXIS2_PLACEMENT_3D('',#389820,#120502,#120503);
#101148=AXIS2_PLACEMENT_3D('',#389833,#120504,#120505);
#101149=AXIS2_PLACEMENT_3D('',#389846,#120506,#120507);
#101150=AXIS2_PLACEMENT_3D('',#389847,#120508,#120509);
#101151=AXIS2_PLACEMENT_3D('',#389848,#120510,#120511);
#101152=AXIS2_PLACEMENT_3D('',#389861,#120512,#120513);
#101153=AXIS2_PLACEMENT_3D('',#389862,#120514,#120515);
#101154=AXIS2_PLACEMENT_3D('',#389872,#120517,#120518);
#101155=AXIS2_PLACEMENT_3D('',#389882,#120520,#120521);
#101156=AXIS2_PLACEMENT_3D('',#389885,#120522,#120523);
#101157=AXIS2_PLACEMENT_3D('',#389902,#120526,#120527);
#101158=AXIS2_PLACEMENT_3D('',#389952,#120528,#120529);
#101159=AXIS2_PLACEMENT_3D('',#389998,#120530,#120531);
#101160=AXIS2_PLACEMENT_3D('',#390015,#120532,#120533);
#101161=AXIS2_PLACEMENT_3D('',#390067,#120534,#120535);
#101162=AXIS2_PLACEMENT_3D('',#390068,#120536,#120537);
#101163=AXIS2_PLACEMENT_3D('',#390069,#120538,#120539);
#101164=AXIS2_PLACEMENT_3D('',#390070,#120540,#120541);
#101165=AXIS2_PLACEMENT_3D('',#390083,#120542,#120543);
#101166=AXIS2_PLACEMENT_3D('',#390084,#120544,#120545);
#101167=AXIS2_PLACEMENT_3D('',#390085,#120546,#120547);
#101168=AXIS2_PLACEMENT_3D('',#390098,#120548,#120549);
#101169=AXIS2_PLACEMENT_3D('',#390111,#120550,#120551);
#101170=AXIS2_PLACEMENT_3D('',#390124,#120552,#120553);
#101171=AXIS2_PLACEMENT_3D('',#390137,#120554,#120555);
#101172=AXIS2_PLACEMENT_3D('',#390150,#120556,#120557);
#101173=AXIS2_PLACEMENT_3D('',#390151,#120558,#120559);
#101174=AXIS2_PLACEMENT_3D('',#390152,#120560,#120561);
#101175=AXIS2_PLACEMENT_3D('',#390165,#120562,#120563);
#101176=AXIS2_PLACEMENT_3D('',#390166,#120564,#120565);
#101177=AXIS2_PLACEMENT_3D('',#390176,#120567,#120568);
#101178=AXIS2_PLACEMENT_3D('',#390186,#120570,#120571);
#101179=AXIS2_PLACEMENT_3D('',#390189,#120572,#120573);
#101180=AXIS2_PLACEMENT_3D('',#390206,#120576,#120577);
#101181=AXIS2_PLACEMENT_3D('',#390256,#120578,#120579);
#101182=AXIS2_PLACEMENT_3D('',#390302,#120580,#120581);
#101183=AXIS2_PLACEMENT_3D('',#390319,#120582,#120583);
#101184=AXIS2_PLACEMENT_3D('',#390371,#120584,#120585);
#101185=AXIS2_PLACEMENT_3D('',#390372,#120586,#120587);
#101186=AXIS2_PLACEMENT_3D('',#390373,#120588,#120589);
#101187=AXIS2_PLACEMENT_3D('',#390374,#120590,#120591);
#101188=AXIS2_PLACEMENT_3D('',#390387,#120592,#120593);
#101189=AXIS2_PLACEMENT_3D('',#390388,#120594,#120595);
#101190=AXIS2_PLACEMENT_3D('',#390389,#120596,#120597);
#101191=AXIS2_PLACEMENT_3D('',#390402,#120598,#120599);
#101192=AXIS2_PLACEMENT_3D('',#390415,#120600,#120601);
#101193=AXIS2_PLACEMENT_3D('',#390428,#120602,#120603);
#101194=AXIS2_PLACEMENT_3D('',#390441,#120604,#120605);
#101195=AXIS2_PLACEMENT_3D('',#390454,#120606,#120607);
#101196=AXIS2_PLACEMENT_3D('',#390455,#120608,#120609);
#101197=AXIS2_PLACEMENT_3D('',#390456,#120610,#120611);
#101198=AXIS2_PLACEMENT_3D('',#390469,#120612,#120613);
#101199=AXIS2_PLACEMENT_3D('',#390470,#120614,#120615);
#101200=AXIS2_PLACEMENT_3D('',#390480,#120617,#120618);
#101201=AXIS2_PLACEMENT_3D('',#390490,#120620,#120621);
#101202=AXIS2_PLACEMENT_3D('',#390493,#120622,#120623);
#101203=AXIS2_PLACEMENT_3D('',#390510,#120626,#120627);
#101204=AXIS2_PLACEMENT_3D('',#390560,#120628,#120629);
#101205=AXIS2_PLACEMENT_3D('',#390606,#120630,#120631);
#101206=AXIS2_PLACEMENT_3D('',#390623,#120632,#120633);
#101207=AXIS2_PLACEMENT_3D('',#390675,#120634,#120635);
#101208=AXIS2_PLACEMENT_3D('',#390676,#120636,#120637);
#101209=AXIS2_PLACEMENT_3D('',#390677,#120638,#120639);
#101210=AXIS2_PLACEMENT_3D('',#390678,#120640,#120641);
#101211=AXIS2_PLACEMENT_3D('',#390691,#120642,#120643);
#101212=AXIS2_PLACEMENT_3D('',#390692,#120644,#120645);
#101213=AXIS2_PLACEMENT_3D('',#390693,#120646,#120647);
#101214=AXIS2_PLACEMENT_3D('',#390706,#120648,#120649);
#101215=AXIS2_PLACEMENT_3D('',#390719,#120650,#120651);
#101216=AXIS2_PLACEMENT_3D('',#390732,#120652,#120653);
#101217=AXIS2_PLACEMENT_3D('',#390745,#120654,#120655);
#101218=AXIS2_PLACEMENT_3D('',#390758,#120656,#120657);
#101219=AXIS2_PLACEMENT_3D('',#390759,#120658,#120659);
#101220=AXIS2_PLACEMENT_3D('',#390760,#120660,#120661);
#101221=AXIS2_PLACEMENT_3D('',#390773,#120662,#120663);
#101222=AXIS2_PLACEMENT_3D('',#390774,#120664,#120665);
#101223=AXIS2_PLACEMENT_3D('',#390784,#120667,#120668);
#101224=AXIS2_PLACEMENT_3D('',#390794,#120670,#120671);
#101225=AXIS2_PLACEMENT_3D('',#390797,#120672,#120673);
#101226=AXIS2_PLACEMENT_3D('',#390814,#120676,#120677);
#101227=AXIS2_PLACEMENT_3D('',#390864,#120678,#120679);
#101228=AXIS2_PLACEMENT_3D('',#390910,#120680,#120681);
#101229=AXIS2_PLACEMENT_3D('',#390927,#120682,#120683);
#101230=AXIS2_PLACEMENT_3D('',#390979,#120684,#120685);
#101231=AXIS2_PLACEMENT_3D('',#390980,#120686,#120687);
#101232=AXIS2_PLACEMENT_3D('',#390981,#120688,#120689);
#101233=AXIS2_PLACEMENT_3D('',#390982,#120690,#120691);
#101234=AXIS2_PLACEMENT_3D('',#390995,#120692,#120693);
#101235=AXIS2_PLACEMENT_3D('',#390996,#120694,#120695);
#101236=AXIS2_PLACEMENT_3D('',#390997,#120696,#120697);
#101237=AXIS2_PLACEMENT_3D('',#391010,#120698,#120699);
#101238=AXIS2_PLACEMENT_3D('',#391023,#120700,#120701);
#101239=AXIS2_PLACEMENT_3D('',#391036,#120702,#120703);
#101240=AXIS2_PLACEMENT_3D('',#391049,#120704,#120705);
#101241=AXIS2_PLACEMENT_3D('',#391062,#120706,#120707);
#101242=AXIS2_PLACEMENT_3D('',#391063,#120708,#120709);
#101243=AXIS2_PLACEMENT_3D('',#391064,#120710,#120711);
#101244=AXIS2_PLACEMENT_3D('',#391077,#120712,#120713);
#101245=AXIS2_PLACEMENT_3D('',#391078,#120714,#120715);
#101246=AXIS2_PLACEMENT_3D('',#391088,#120717,#120718);
#101247=AXIS2_PLACEMENT_3D('',#391098,#120720,#120721);
#101248=AXIS2_PLACEMENT_3D('',#391101,#120722,#120723);
#101249=AXIS2_PLACEMENT_3D('',#391118,#120726,#120727);
#101250=AXIS2_PLACEMENT_3D('',#391168,#120728,#120729);
#101251=AXIS2_PLACEMENT_3D('',#391214,#120730,#120731);
#101252=AXIS2_PLACEMENT_3D('',#391231,#120732,#120733);
#101253=AXIS2_PLACEMENT_3D('',#391283,#120734,#120735);
#101254=AXIS2_PLACEMENT_3D('',#391284,#120736,#120737);
#101255=AXIS2_PLACEMENT_3D('',#391285,#120738,#120739);
#101256=AXIS2_PLACEMENT_3D('',#391286,#120740,#120741);
#101257=AXIS2_PLACEMENT_3D('',#391299,#120742,#120743);
#101258=AXIS2_PLACEMENT_3D('',#391300,#120744,#120745);
#101259=AXIS2_PLACEMENT_3D('',#391301,#120746,#120747);
#101260=AXIS2_PLACEMENT_3D('',#391314,#120748,#120749);
#101261=AXIS2_PLACEMENT_3D('',#391327,#120750,#120751);
#101262=AXIS2_PLACEMENT_3D('',#391340,#120752,#120753);
#101263=AXIS2_PLACEMENT_3D('',#391353,#120754,#120755);
#101264=AXIS2_PLACEMENT_3D('',#391366,#120756,#120757);
#101265=AXIS2_PLACEMENT_3D('',#391367,#120758,#120759);
#101266=AXIS2_PLACEMENT_3D('',#391368,#120760,#120761);
#101267=AXIS2_PLACEMENT_3D('',#391381,#120762,#120763);
#101268=AXIS2_PLACEMENT_3D('',#391382,#120764,#120765);
#101269=AXIS2_PLACEMENT_3D('',#391392,#120767,#120768);
#101270=AXIS2_PLACEMENT_3D('',#391402,#120770,#120771);
#101271=AXIS2_PLACEMENT_3D('',#391405,#120772,#120773);
#101272=AXIS2_PLACEMENT_3D('',#391422,#120776,#120777);
#101273=AXIS2_PLACEMENT_3D('',#391472,#120778,#120779);
#101274=AXIS2_PLACEMENT_3D('',#391518,#120780,#120781);
#101275=AXIS2_PLACEMENT_3D('',#391535,#120782,#120783);
#101276=AXIS2_PLACEMENT_3D('',#391587,#120784,#120785);
#101277=AXIS2_PLACEMENT_3D('',#391588,#120786,#120787);
#101278=AXIS2_PLACEMENT_3D('',#391589,#120788,#120789);
#101279=AXIS2_PLACEMENT_3D('',#391590,#120790,#120791);
#101280=AXIS2_PLACEMENT_3D('',#391603,#120792,#120793);
#101281=AXIS2_PLACEMENT_3D('',#391604,#120794,#120795);
#101282=AXIS2_PLACEMENT_3D('',#391605,#120796,#120797);
#101283=AXIS2_PLACEMENT_3D('',#391618,#120798,#120799);
#101284=AXIS2_PLACEMENT_3D('',#391631,#120800,#120801);
#101285=AXIS2_PLACEMENT_3D('',#391644,#120802,#120803);
#101286=AXIS2_PLACEMENT_3D('',#391657,#120804,#120805);
#101287=AXIS2_PLACEMENT_3D('',#391670,#120806,#120807);
#101288=AXIS2_PLACEMENT_3D('',#391671,#120808,#120809);
#101289=AXIS2_PLACEMENT_3D('',#391672,#120810,#120811);
#101290=AXIS2_PLACEMENT_3D('',#391685,#120812,#120813);
#101291=AXIS2_PLACEMENT_3D('',#391686,#120814,#120815);
#101292=AXIS2_PLACEMENT_3D('',#391696,#120817,#120818);
#101293=AXIS2_PLACEMENT_3D('',#391706,#120820,#120821);
#101294=AXIS2_PLACEMENT_3D('',#391709,#120822,#120823);
#101295=AXIS2_PLACEMENT_3D('',#391726,#120826,#120827);
#101296=AXIS2_PLACEMENT_3D('',#391776,#120828,#120829);
#101297=AXIS2_PLACEMENT_3D('',#391822,#120830,#120831);
#101298=AXIS2_PLACEMENT_3D('',#391839,#120832,#120833);
#101299=AXIS2_PLACEMENT_3D('',#391891,#120834,#120835);
#101300=AXIS2_PLACEMENT_3D('',#391892,#120836,#120837);
#101301=AXIS2_PLACEMENT_3D('',#391893,#120838,#120839);
#101302=AXIS2_PLACEMENT_3D('',#391894,#120840,#120841);
#101303=AXIS2_PLACEMENT_3D('',#391907,#120842,#120843);
#101304=AXIS2_PLACEMENT_3D('',#391908,#120844,#120845);
#101305=AXIS2_PLACEMENT_3D('',#391909,#120846,#120847);
#101306=AXIS2_PLACEMENT_3D('',#391922,#120848,#120849);
#101307=AXIS2_PLACEMENT_3D('',#391935,#120850,#120851);
#101308=AXIS2_PLACEMENT_3D('',#391948,#120852,#120853);
#101309=AXIS2_PLACEMENT_3D('',#391961,#120854,#120855);
#101310=AXIS2_PLACEMENT_3D('',#391974,#120856,#120857);
#101311=AXIS2_PLACEMENT_3D('',#391975,#120858,#120859);
#101312=AXIS2_PLACEMENT_3D('',#391976,#120860,#120861);
#101313=AXIS2_PLACEMENT_3D('',#391989,#120862,#120863);
#101314=AXIS2_PLACEMENT_3D('',#391990,#120864,#120865);
#101315=AXIS2_PLACEMENT_3D('',#392000,#120867,#120868);
#101316=AXIS2_PLACEMENT_3D('',#392010,#120870,#120871);
#101317=AXIS2_PLACEMENT_3D('',#392013,#120872,#120873);
#101318=AXIS2_PLACEMENT_3D('',#392030,#120876,#120877);
#101319=AXIS2_PLACEMENT_3D('',#392080,#120878,#120879);
#101320=AXIS2_PLACEMENT_3D('',#392126,#120880,#120881);
#101321=AXIS2_PLACEMENT_3D('',#392143,#120882,#120883);
#101322=AXIS2_PLACEMENT_3D('',#392195,#120884,#120885);
#101323=AXIS2_PLACEMENT_3D('',#392196,#120886,#120887);
#101324=AXIS2_PLACEMENT_3D('',#392197,#120888,#120889);
#101325=AXIS2_PLACEMENT_3D('',#392198,#120890,#120891);
#101326=AXIS2_PLACEMENT_3D('',#392211,#120892,#120893);
#101327=AXIS2_PLACEMENT_3D('',#392212,#120894,#120895);
#101328=AXIS2_PLACEMENT_3D('',#392213,#120896,#120897);
#101329=AXIS2_PLACEMENT_3D('',#392226,#120898,#120899);
#101330=AXIS2_PLACEMENT_3D('',#392239,#120900,#120901);
#101331=AXIS2_PLACEMENT_3D('',#392252,#120902,#120903);
#101332=AXIS2_PLACEMENT_3D('',#392265,#120904,#120905);
#101333=AXIS2_PLACEMENT_3D('',#392278,#120906,#120907);
#101334=AXIS2_PLACEMENT_3D('',#392279,#120908,#120909);
#101335=AXIS2_PLACEMENT_3D('',#392280,#120910,#120911);
#101336=AXIS2_PLACEMENT_3D('',#392293,#120912,#120913);
#101337=AXIS2_PLACEMENT_3D('',#392294,#120914,#120915);
#101338=AXIS2_PLACEMENT_3D('',#392304,#120917,#120918);
#101339=AXIS2_PLACEMENT_3D('',#392314,#120920,#120921);
#101340=AXIS2_PLACEMENT_3D('',#392317,#120922,#120923);
#101341=AXIS2_PLACEMENT_3D('',#392334,#120926,#120927);
#101342=AXIS2_PLACEMENT_3D('',#392384,#120928,#120929);
#101343=AXIS2_PLACEMENT_3D('',#392430,#120930,#120931);
#101344=AXIS2_PLACEMENT_3D('',#392447,#120932,#120933);
#101345=AXIS2_PLACEMENT_3D('',#392499,#120934,#120935);
#101346=AXIS2_PLACEMENT_3D('',#392500,#120936,#120937);
#101347=AXIS2_PLACEMENT_3D('',#392501,#120938,#120939);
#101348=AXIS2_PLACEMENT_3D('',#392502,#120940,#120941);
#101349=AXIS2_PLACEMENT_3D('',#392515,#120942,#120943);
#101350=AXIS2_PLACEMENT_3D('',#392516,#120944,#120945);
#101351=AXIS2_PLACEMENT_3D('',#392517,#120946,#120947);
#101352=AXIS2_PLACEMENT_3D('',#392530,#120948,#120949);
#101353=AXIS2_PLACEMENT_3D('',#392543,#120950,#120951);
#101354=AXIS2_PLACEMENT_3D('',#392556,#120952,#120953);
#101355=AXIS2_PLACEMENT_3D('',#392569,#120954,#120955);
#101356=AXIS2_PLACEMENT_3D('',#392582,#120956,#120957);
#101357=AXIS2_PLACEMENT_3D('',#392583,#120958,#120959);
#101358=AXIS2_PLACEMENT_3D('',#392584,#120960,#120961);
#101359=AXIS2_PLACEMENT_3D('',#392597,#120962,#120963);
#101360=AXIS2_PLACEMENT_3D('',#392598,#120964,#120965);
#101361=AXIS2_PLACEMENT_3D('',#392608,#120967,#120968);
#101362=AXIS2_PLACEMENT_3D('',#392618,#120970,#120971);
#101363=AXIS2_PLACEMENT_3D('',#392621,#120972,#120973);
#101364=AXIS2_PLACEMENT_3D('',#392638,#120976,#120977);
#101365=AXIS2_PLACEMENT_3D('',#392688,#120978,#120979);
#101366=AXIS2_PLACEMENT_3D('',#392734,#120980,#120981);
#101367=AXIS2_PLACEMENT_3D('',#392751,#120982,#120983);
#101368=AXIS2_PLACEMENT_3D('',#392803,#120984,#120985);
#101369=AXIS2_PLACEMENT_3D('',#392804,#120986,#120987);
#101370=AXIS2_PLACEMENT_3D('',#392805,#120988,#120989);
#101371=AXIS2_PLACEMENT_3D('',#392806,#120990,#120991);
#101372=AXIS2_PLACEMENT_3D('',#392819,#120992,#120993);
#101373=AXIS2_PLACEMENT_3D('',#392820,#120994,#120995);
#101374=AXIS2_PLACEMENT_3D('',#392821,#120996,#120997);
#101375=AXIS2_PLACEMENT_3D('',#392834,#120998,#120999);
#101376=AXIS2_PLACEMENT_3D('',#392847,#121000,#121001);
#101377=AXIS2_PLACEMENT_3D('',#392860,#121002,#121003);
#101378=AXIS2_PLACEMENT_3D('',#392873,#121004,#121005);
#101379=AXIS2_PLACEMENT_3D('',#392886,#121006,#121007);
#101380=AXIS2_PLACEMENT_3D('',#392887,#121008,#121009);
#101381=AXIS2_PLACEMENT_3D('',#392888,#121010,#121011);
#101382=AXIS2_PLACEMENT_3D('',#392901,#121012,#121013);
#101383=AXIS2_PLACEMENT_3D('',#392902,#121014,#121015);
#101384=AXIS2_PLACEMENT_3D('',#392912,#121017,#121018);
#101385=AXIS2_PLACEMENT_3D('',#392922,#121020,#121021);
#101386=AXIS2_PLACEMENT_3D('',#392925,#121022,#121023);
#101387=AXIS2_PLACEMENT_3D('',#392942,#121026,#121027);
#101388=AXIS2_PLACEMENT_3D('',#392992,#121028,#121029);
#101389=AXIS2_PLACEMENT_3D('',#393038,#121030,#121031);
#101390=AXIS2_PLACEMENT_3D('',#393055,#121032,#121033);
#101391=AXIS2_PLACEMENT_3D('',#393107,#121034,#121035);
#101392=AXIS2_PLACEMENT_3D('',#393108,#121036,#121037);
#101393=AXIS2_PLACEMENT_3D('',#393109,#121038,#121039);
#101394=AXIS2_PLACEMENT_3D('',#393110,#121040,#121041);
#101395=AXIS2_PLACEMENT_3D('',#393123,#121042,#121043);
#101396=AXIS2_PLACEMENT_3D('',#393124,#121044,#121045);
#101397=AXIS2_PLACEMENT_3D('',#393125,#121046,#121047);
#101398=AXIS2_PLACEMENT_3D('',#393138,#121048,#121049);
#101399=AXIS2_PLACEMENT_3D('',#393151,#121050,#121051);
#101400=AXIS2_PLACEMENT_3D('',#393164,#121052,#121053);
#101401=AXIS2_PLACEMENT_3D('',#393177,#121054,#121055);
#101402=AXIS2_PLACEMENT_3D('',#393190,#121056,#121057);
#101403=AXIS2_PLACEMENT_3D('',#393191,#121058,#121059);
#101404=AXIS2_PLACEMENT_3D('',#393192,#121060,#121061);
#101405=AXIS2_PLACEMENT_3D('',#393205,#121062,#121063);
#101406=AXIS2_PLACEMENT_3D('',#393206,#121064,#121065);
#101407=AXIS2_PLACEMENT_3D('',#393216,#121067,#121068);
#101408=AXIS2_PLACEMENT_3D('',#393226,#121070,#121071);
#101409=AXIS2_PLACEMENT_3D('',#393229,#121072,#121073);
#101410=AXIS2_PLACEMENT_3D('',#393246,#121076,#121077);
#101411=AXIS2_PLACEMENT_3D('',#393296,#121078,#121079);
#101412=AXIS2_PLACEMENT_3D('',#393342,#121080,#121081);
#101413=AXIS2_PLACEMENT_3D('',#393359,#121082,#121083);
#101414=AXIS2_PLACEMENT_3D('',#393411,#121084,#121085);
#101415=AXIS2_PLACEMENT_3D('',#393412,#121086,#121087);
#101416=AXIS2_PLACEMENT_3D('',#393413,#121088,#121089);
#101417=AXIS2_PLACEMENT_3D('',#393414,#121090,#121091);
#101418=AXIS2_PLACEMENT_3D('',#393427,#121092,#121093);
#101419=AXIS2_PLACEMENT_3D('',#393428,#121094,#121095);
#101420=AXIS2_PLACEMENT_3D('',#393429,#121096,#121097);
#101421=AXIS2_PLACEMENT_3D('',#393442,#121098,#121099);
#101422=AXIS2_PLACEMENT_3D('',#393455,#121100,#121101);
#101423=AXIS2_PLACEMENT_3D('',#393468,#121102,#121103);
#101424=AXIS2_PLACEMENT_3D('',#393481,#121104,#121105);
#101425=AXIS2_PLACEMENT_3D('',#393494,#121106,#121107);
#101426=AXIS2_PLACEMENT_3D('',#393495,#121108,#121109);
#101427=AXIS2_PLACEMENT_3D('',#393496,#121110,#121111);
#101428=AXIS2_PLACEMENT_3D('',#393509,#121112,#121113);
#101429=AXIS2_PLACEMENT_3D('',#393510,#121114,#121115);
#101430=AXIS2_PLACEMENT_3D('',#393520,#121117,#121118);
#101431=AXIS2_PLACEMENT_3D('',#393530,#121120,#121121);
#101432=AXIS2_PLACEMENT_3D('',#393533,#121122,#121123);
#101433=AXIS2_PLACEMENT_3D('',#393550,#121126,#121127);
#101434=AXIS2_PLACEMENT_3D('',#393600,#121128,#121129);
#101435=AXIS2_PLACEMENT_3D('',#393646,#121130,#121131);
#101436=AXIS2_PLACEMENT_3D('',#393663,#121132,#121133);
#101437=AXIS2_PLACEMENT_3D('',#393715,#121134,#121135);
#101438=AXIS2_PLACEMENT_3D('',#393716,#121136,#121137);
#101439=AXIS2_PLACEMENT_3D('',#393717,#121138,#121139);
#101440=AXIS2_PLACEMENT_3D('',#393718,#121140,#121141);
#101441=AXIS2_PLACEMENT_3D('',#393731,#121142,#121143);
#101442=AXIS2_PLACEMENT_3D('',#393732,#121144,#121145);
#101443=AXIS2_PLACEMENT_3D('',#393733,#121146,#121147);
#101444=AXIS2_PLACEMENT_3D('',#393746,#121148,#121149);
#101445=AXIS2_PLACEMENT_3D('',#393759,#121150,#121151);
#101446=AXIS2_PLACEMENT_3D('',#393772,#121152,#121153);
#101447=AXIS2_PLACEMENT_3D('',#393785,#121154,#121155);
#101448=AXIS2_PLACEMENT_3D('',#393798,#121156,#121157);
#101449=AXIS2_PLACEMENT_3D('',#393799,#121158,#121159);
#101450=AXIS2_PLACEMENT_3D('',#393800,#121160,#121161);
#101451=AXIS2_PLACEMENT_3D('',#393813,#121162,#121163);
#101452=AXIS2_PLACEMENT_3D('',#393814,#121164,#121165);
#101453=AXIS2_PLACEMENT_3D('',#393824,#121167,#121168);
#101454=AXIS2_PLACEMENT_3D('',#393834,#121170,#121171);
#101455=AXIS2_PLACEMENT_3D('',#393837,#121172,#121173);
#101456=AXIS2_PLACEMENT_3D('',#393854,#121176,#121177);
#101457=AXIS2_PLACEMENT_3D('',#393904,#121178,#121179);
#101458=AXIS2_PLACEMENT_3D('',#393950,#121180,#121181);
#101459=AXIS2_PLACEMENT_3D('',#393967,#121182,#121183);
#101460=AXIS2_PLACEMENT_3D('',#394019,#121184,#121185);
#101461=AXIS2_PLACEMENT_3D('',#394020,#121186,#121187);
#101462=AXIS2_PLACEMENT_3D('',#394021,#121188,#121189);
#101463=AXIS2_PLACEMENT_3D('',#394022,#121190,#121191);
#101464=AXIS2_PLACEMENT_3D('',#394035,#121192,#121193);
#101465=AXIS2_PLACEMENT_3D('',#394036,#121194,#121195);
#101466=AXIS2_PLACEMENT_3D('',#394037,#121196,#121197);
#101467=AXIS2_PLACEMENT_3D('',#394050,#121198,#121199);
#101468=AXIS2_PLACEMENT_3D('',#394063,#121200,#121201);
#101469=AXIS2_PLACEMENT_3D('',#394076,#121202,#121203);
#101470=AXIS2_PLACEMENT_3D('',#394089,#121204,#121205);
#101471=AXIS2_PLACEMENT_3D('',#394102,#121206,#121207);
#101472=AXIS2_PLACEMENT_3D('',#394103,#121208,#121209);
#101473=AXIS2_PLACEMENT_3D('',#394104,#121210,#121211);
#101474=AXIS2_PLACEMENT_3D('',#394117,#121212,#121213);
#101475=AXIS2_PLACEMENT_3D('',#394118,#121214,#121215);
#101476=AXIS2_PLACEMENT_3D('',#394128,#121217,#121218);
#101477=AXIS2_PLACEMENT_3D('',#394138,#121220,#121221);
#101478=AXIS2_PLACEMENT_3D('',#394141,#121222,#121223);
#101479=AXIS2_PLACEMENT_3D('',#394158,#121226,#121227);
#101480=AXIS2_PLACEMENT_3D('',#394208,#121228,#121229);
#101481=AXIS2_PLACEMENT_3D('',#394254,#121230,#121231);
#101482=AXIS2_PLACEMENT_3D('',#394271,#121232,#121233);
#101483=AXIS2_PLACEMENT_3D('',#394323,#121234,#121235);
#101484=AXIS2_PLACEMENT_3D('',#394324,#121236,#121237);
#101485=AXIS2_PLACEMENT_3D('',#394325,#121238,#121239);
#101486=AXIS2_PLACEMENT_3D('',#394326,#121240,#121241);
#101487=AXIS2_PLACEMENT_3D('',#394339,#121242,#121243);
#101488=AXIS2_PLACEMENT_3D('',#394340,#121244,#121245);
#101489=AXIS2_PLACEMENT_3D('',#394341,#121246,#121247);
#101490=AXIS2_PLACEMENT_3D('',#394354,#121248,#121249);
#101491=AXIS2_PLACEMENT_3D('',#394367,#121250,#121251);
#101492=AXIS2_PLACEMENT_3D('',#394380,#121252,#121253);
#101493=AXIS2_PLACEMENT_3D('',#394393,#121254,#121255);
#101494=AXIS2_PLACEMENT_3D('',#394406,#121256,#121257);
#101495=AXIS2_PLACEMENT_3D('',#394407,#121258,#121259);
#101496=AXIS2_PLACEMENT_3D('',#394408,#121260,#121261);
#101497=AXIS2_PLACEMENT_3D('',#394421,#121262,#121263);
#101498=AXIS2_PLACEMENT_3D('',#394422,#121264,#121265);
#101499=AXIS2_PLACEMENT_3D('',#394432,#121267,#121268);
#101500=AXIS2_PLACEMENT_3D('',#394442,#121270,#121271);
#101501=AXIS2_PLACEMENT_3D('',#394445,#121272,#121273);
#101502=AXIS2_PLACEMENT_3D('',#394462,#121276,#121277);
#101503=AXIS2_PLACEMENT_3D('',#394512,#121278,#121279);
#101504=AXIS2_PLACEMENT_3D('',#394558,#121280,#121281);
#101505=AXIS2_PLACEMENT_3D('',#394575,#121282,#121283);
#101506=AXIS2_PLACEMENT_3D('',#394627,#121284,#121285);
#101507=AXIS2_PLACEMENT_3D('',#394628,#121286,#121287);
#101508=AXIS2_PLACEMENT_3D('',#394629,#121288,#121289);
#101509=AXIS2_PLACEMENT_3D('',#394630,#121290,#121291);
#101510=AXIS2_PLACEMENT_3D('',#394643,#121292,#121293);
#101511=AXIS2_PLACEMENT_3D('',#394644,#121294,#121295);
#101512=AXIS2_PLACEMENT_3D('',#394645,#121296,#121297);
#101513=AXIS2_PLACEMENT_3D('',#394658,#121298,#121299);
#101514=AXIS2_PLACEMENT_3D('',#394671,#121300,#121301);
#101515=AXIS2_PLACEMENT_3D('',#394684,#121302,#121303);
#101516=AXIS2_PLACEMENT_3D('',#394697,#121304,#121305);
#101517=AXIS2_PLACEMENT_3D('',#394710,#121306,#121307);
#101518=AXIS2_PLACEMENT_3D('',#394711,#121308,#121309);
#101519=AXIS2_PLACEMENT_3D('',#394712,#121310,#121311);
#101520=AXIS2_PLACEMENT_3D('',#394725,#121312,#121313);
#101521=AXIS2_PLACEMENT_3D('',#394726,#121314,#121315);
#101522=AXIS2_PLACEMENT_3D('',#394736,#121317,#121318);
#101523=AXIS2_PLACEMENT_3D('',#394746,#121320,#121321);
#101524=AXIS2_PLACEMENT_3D('',#394749,#121322,#121323);
#101525=AXIS2_PLACEMENT_3D('',#394766,#121326,#121327);
#101526=AXIS2_PLACEMENT_3D('',#394816,#121328,#121329);
#101527=AXIS2_PLACEMENT_3D('',#394862,#121330,#121331);
#101528=AXIS2_PLACEMENT_3D('',#394879,#121332,#121333);
#101529=AXIS2_PLACEMENT_3D('',#394931,#121334,#121335);
#101530=AXIS2_PLACEMENT_3D('',#394932,#121336,#121337);
#101531=AXIS2_PLACEMENT_3D('',#394933,#121338,#121339);
#101532=AXIS2_PLACEMENT_3D('',#394934,#121340,#121341);
#101533=AXIS2_PLACEMENT_3D('',#394947,#121342,#121343);
#101534=AXIS2_PLACEMENT_3D('',#394948,#121344,#121345);
#101535=AXIS2_PLACEMENT_3D('',#394949,#121346,#121347);
#101536=AXIS2_PLACEMENT_3D('',#394962,#121348,#121349);
#101537=AXIS2_PLACEMENT_3D('',#394975,#121350,#121351);
#101538=AXIS2_PLACEMENT_3D('',#394988,#121352,#121353);
#101539=AXIS2_PLACEMENT_3D('',#395001,#121354,#121355);
#101540=AXIS2_PLACEMENT_3D('',#395014,#121356,#121357);
#101541=AXIS2_PLACEMENT_3D('',#395015,#121358,#121359);
#101542=AXIS2_PLACEMENT_3D('',#395016,#121360,#121361);
#101543=AXIS2_PLACEMENT_3D('',#395029,#121362,#121363);
#101544=AXIS2_PLACEMENT_3D('',#395030,#121364,#121365);
#101545=AXIS2_PLACEMENT_3D('',#395040,#121367,#121368);
#101546=AXIS2_PLACEMENT_3D('',#395050,#121370,#121371);
#101547=AXIS2_PLACEMENT_3D('',#395053,#121372,#121373);
#101548=AXIS2_PLACEMENT_3D('',#395070,#121376,#121377);
#101549=AXIS2_PLACEMENT_3D('',#395120,#121378,#121379);
#101550=AXIS2_PLACEMENT_3D('',#395166,#121380,#121381);
#101551=AXIS2_PLACEMENT_3D('',#395183,#121382,#121383);
#101552=AXIS2_PLACEMENT_3D('',#395235,#121384,#121385);
#101553=AXIS2_PLACEMENT_3D('',#395236,#121386,#121387);
#101554=AXIS2_PLACEMENT_3D('',#395237,#121388,#121389);
#101555=AXIS2_PLACEMENT_3D('',#395238,#121390,#121391);
#101556=AXIS2_PLACEMENT_3D('',#395251,#121392,#121393);
#101557=AXIS2_PLACEMENT_3D('',#395252,#121394,#121395);
#101558=AXIS2_PLACEMENT_3D('',#395253,#121396,#121397);
#101559=AXIS2_PLACEMENT_3D('',#395266,#121398,#121399);
#101560=AXIS2_PLACEMENT_3D('',#395279,#121400,#121401);
#101561=AXIS2_PLACEMENT_3D('',#395292,#121402,#121403);
#101562=AXIS2_PLACEMENT_3D('',#395305,#121404,#121405);
#101563=AXIS2_PLACEMENT_3D('',#395318,#121406,#121407);
#101564=AXIS2_PLACEMENT_3D('',#395319,#121408,#121409);
#101565=AXIS2_PLACEMENT_3D('',#395320,#121410,#121411);
#101566=AXIS2_PLACEMENT_3D('',#395333,#121412,#121413);
#101567=AXIS2_PLACEMENT_3D('',#395334,#121414,#121415);
#101568=AXIS2_PLACEMENT_3D('',#395344,#121417,#121418);
#101569=AXIS2_PLACEMENT_3D('',#395354,#121420,#121421);
#101570=AXIS2_PLACEMENT_3D('',#395357,#121422,#121423);
#101571=AXIS2_PLACEMENT_3D('',#395374,#121426,#121427);
#101572=AXIS2_PLACEMENT_3D('',#395424,#121428,#121429);
#101573=AXIS2_PLACEMENT_3D('',#395470,#121430,#121431);
#101574=AXIS2_PLACEMENT_3D('',#395487,#121432,#121433);
#101575=AXIS2_PLACEMENT_3D('',#395539,#121434,#121435);
#101576=AXIS2_PLACEMENT_3D('',#395540,#121436,#121437);
#101577=AXIS2_PLACEMENT_3D('',#395541,#121438,#121439);
#101578=AXIS2_PLACEMENT_3D('',#395542,#121440,#121441);
#101579=AXIS2_PLACEMENT_3D('',#395555,#121442,#121443);
#101580=AXIS2_PLACEMENT_3D('',#395556,#121444,#121445);
#101581=AXIS2_PLACEMENT_3D('',#395557,#121446,#121447);
#101582=AXIS2_PLACEMENT_3D('',#395570,#121448,#121449);
#101583=AXIS2_PLACEMENT_3D('',#395583,#121450,#121451);
#101584=AXIS2_PLACEMENT_3D('',#395596,#121452,#121453);
#101585=AXIS2_PLACEMENT_3D('',#395609,#121454,#121455);
#101586=AXIS2_PLACEMENT_3D('',#395622,#121456,#121457);
#101587=AXIS2_PLACEMENT_3D('',#395623,#121458,#121459);
#101588=AXIS2_PLACEMENT_3D('',#395624,#121460,#121461);
#101589=AXIS2_PLACEMENT_3D('',#395637,#121462,#121463);
#101590=AXIS2_PLACEMENT_3D('',#395638,#121464,#121465);
#101591=AXIS2_PLACEMENT_3D('',#395648,#121467,#121468);
#101592=AXIS2_PLACEMENT_3D('',#395658,#121470,#121471);
#101593=AXIS2_PLACEMENT_3D('',#395661,#121472,#121473);
#101594=AXIS2_PLACEMENT_3D('',#395678,#121476,#121477);
#101595=AXIS2_PLACEMENT_3D('',#395728,#121478,#121479);
#101596=AXIS2_PLACEMENT_3D('',#395774,#121480,#121481);
#101597=AXIS2_PLACEMENT_3D('',#395791,#121482,#121483);
#101598=AXIS2_PLACEMENT_3D('',#395843,#121484,#121485);
#101599=AXIS2_PLACEMENT_3D('',#395844,#121486,#121487);
#101600=AXIS2_PLACEMENT_3D('',#395845,#121488,#121489);
#101601=AXIS2_PLACEMENT_3D('',#395846,#121490,#121491);
#101602=AXIS2_PLACEMENT_3D('',#395859,#121492,#121493);
#101603=AXIS2_PLACEMENT_3D('',#395860,#121494,#121495);
#101604=AXIS2_PLACEMENT_3D('',#395861,#121496,#121497);
#101605=AXIS2_PLACEMENT_3D('',#395874,#121498,#121499);
#101606=AXIS2_PLACEMENT_3D('',#395887,#121500,#121501);
#101607=AXIS2_PLACEMENT_3D('',#395900,#121502,#121503);
#101608=AXIS2_PLACEMENT_3D('',#395913,#121504,#121505);
#101609=AXIS2_PLACEMENT_3D('',#395926,#121506,#121507);
#101610=AXIS2_PLACEMENT_3D('',#395927,#121508,#121509);
#101611=AXIS2_PLACEMENT_3D('',#395928,#121510,#121511);
#101612=AXIS2_PLACEMENT_3D('',#395941,#121512,#121513);
#101613=AXIS2_PLACEMENT_3D('',#395942,#121514,#121515);
#101614=AXIS2_PLACEMENT_3D('',#395952,#121517,#121518);
#101615=AXIS2_PLACEMENT_3D('',#395962,#121520,#121521);
#101616=AXIS2_PLACEMENT_3D('',#395965,#121522,#121523);
#101617=AXIS2_PLACEMENT_3D('',#395982,#121526,#121527);
#101618=AXIS2_PLACEMENT_3D('',#396032,#121528,#121529);
#101619=AXIS2_PLACEMENT_3D('',#396078,#121530,#121531);
#101620=AXIS2_PLACEMENT_3D('',#396095,#121532,#121533);
#101621=AXIS2_PLACEMENT_3D('',#396147,#121534,#121535);
#101622=AXIS2_PLACEMENT_3D('',#396148,#121536,#121537);
#101623=AXIS2_PLACEMENT_3D('',#396149,#121538,#121539);
#101624=AXIS2_PLACEMENT_3D('',#396150,#121540,#121541);
#101625=AXIS2_PLACEMENT_3D('',#396163,#121542,#121543);
#101626=AXIS2_PLACEMENT_3D('',#396164,#121544,#121545);
#101627=AXIS2_PLACEMENT_3D('',#396165,#121546,#121547);
#101628=AXIS2_PLACEMENT_3D('',#396178,#121548,#121549);
#101629=AXIS2_PLACEMENT_3D('',#396191,#121550,#121551);
#101630=AXIS2_PLACEMENT_3D('',#396204,#121552,#121553);
#101631=AXIS2_PLACEMENT_3D('',#396217,#121554,#121555);
#101632=AXIS2_PLACEMENT_3D('',#396230,#121556,#121557);
#101633=AXIS2_PLACEMENT_3D('',#396231,#121558,#121559);
#101634=AXIS2_PLACEMENT_3D('',#396232,#121560,#121561);
#101635=AXIS2_PLACEMENT_3D('',#396245,#121562,#121563);
#101636=AXIS2_PLACEMENT_3D('',#396246,#121564,#121565);
#101637=AXIS2_PLACEMENT_3D('',#396256,#121567,#121568);
#101638=AXIS2_PLACEMENT_3D('',#396266,#121570,#121571);
#101639=AXIS2_PLACEMENT_3D('',#396269,#121572,#121573);
#101640=AXIS2_PLACEMENT_3D('',#396286,#121576,#121577);
#101641=AXIS2_PLACEMENT_3D('',#396336,#121578,#121579);
#101642=AXIS2_PLACEMENT_3D('',#396382,#121580,#121581);
#101643=AXIS2_PLACEMENT_3D('',#396399,#121582,#121583);
#101644=AXIS2_PLACEMENT_3D('',#396451,#121584,#121585);
#101645=AXIS2_PLACEMENT_3D('',#396452,#121586,#121587);
#101646=AXIS2_PLACEMENT_3D('',#396453,#121588,#121589);
#101647=AXIS2_PLACEMENT_3D('',#396454,#121590,#121591);
#101648=AXIS2_PLACEMENT_3D('',#396467,#121592,#121593);
#101649=AXIS2_PLACEMENT_3D('',#396468,#121594,#121595);
#101650=AXIS2_PLACEMENT_3D('',#396469,#121596,#121597);
#101651=AXIS2_PLACEMENT_3D('',#396482,#121598,#121599);
#101652=AXIS2_PLACEMENT_3D('',#396495,#121600,#121601);
#101653=AXIS2_PLACEMENT_3D('',#396508,#121602,#121603);
#101654=AXIS2_PLACEMENT_3D('',#396521,#121604,#121605);
#101655=AXIS2_PLACEMENT_3D('',#396534,#121606,#121607);
#101656=AXIS2_PLACEMENT_3D('',#396535,#121608,#121609);
#101657=AXIS2_PLACEMENT_3D('',#396536,#121610,#121611);
#101658=AXIS2_PLACEMENT_3D('',#396549,#121612,#121613);
#101659=AXIS2_PLACEMENT_3D('',#396550,#121614,#121615);
#101660=AXIS2_PLACEMENT_3D('',#396560,#121617,#121618);
#101661=AXIS2_PLACEMENT_3D('',#396570,#121620,#121621);
#101662=AXIS2_PLACEMENT_3D('',#396573,#121622,#121623);
#101663=AXIS2_PLACEMENT_3D('',#396590,#121626,#121627);
#101664=AXIS2_PLACEMENT_3D('',#396640,#121628,#121629);
#101665=AXIS2_PLACEMENT_3D('',#396686,#121630,#121631);
#101666=AXIS2_PLACEMENT_3D('',#396703,#121632,#121633);
#101667=AXIS2_PLACEMENT_3D('',#396755,#121634,#121635);
#101668=AXIS2_PLACEMENT_3D('',#396756,#121636,#121637);
#101669=AXIS2_PLACEMENT_3D('',#396757,#121638,#121639);
#101670=AXIS2_PLACEMENT_3D('',#396758,#121640,#121641);
#101671=AXIS2_PLACEMENT_3D('',#396771,#121642,#121643);
#101672=AXIS2_PLACEMENT_3D('',#396772,#121644,#121645);
#101673=AXIS2_PLACEMENT_3D('',#396773,#121646,#121647);
#101674=AXIS2_PLACEMENT_3D('',#396786,#121648,#121649);
#101675=AXIS2_PLACEMENT_3D('',#396799,#121650,#121651);
#101676=AXIS2_PLACEMENT_3D('',#396812,#121652,#121653);
#101677=AXIS2_PLACEMENT_3D('',#396825,#121654,#121655);
#101678=AXIS2_PLACEMENT_3D('',#396838,#121656,#121657);
#101679=AXIS2_PLACEMENT_3D('',#396839,#121658,#121659);
#101680=AXIS2_PLACEMENT_3D('',#396840,#121660,#121661);
#101681=AXIS2_PLACEMENT_3D('',#396853,#121662,#121663);
#101682=AXIS2_PLACEMENT_3D('',#396854,#121664,#121665);
#101683=AXIS2_PLACEMENT_3D('',#396864,#121667,#121668);
#101684=AXIS2_PLACEMENT_3D('',#396874,#121670,#121671);
#101685=AXIS2_PLACEMENT_3D('',#396877,#121672,#121673);
#101686=AXIS2_PLACEMENT_3D('',#396894,#121676,#121677);
#101687=AXIS2_PLACEMENT_3D('',#396944,#121678,#121679);
#101688=AXIS2_PLACEMENT_3D('',#396990,#121680,#121681);
#101689=AXIS2_PLACEMENT_3D('',#397007,#121682,#121683);
#101690=AXIS2_PLACEMENT_3D('',#397059,#121684,#121685);
#101691=AXIS2_PLACEMENT_3D('',#397060,#121686,#121687);
#101692=AXIS2_PLACEMENT_3D('',#397061,#121688,#121689);
#101693=AXIS2_PLACEMENT_3D('',#397062,#121690,#121691);
#101694=AXIS2_PLACEMENT_3D('',#397075,#121692,#121693);
#101695=AXIS2_PLACEMENT_3D('',#397076,#121694,#121695);
#101696=AXIS2_PLACEMENT_3D('',#397077,#121696,#121697);
#101697=AXIS2_PLACEMENT_3D('',#397090,#121698,#121699);
#101698=AXIS2_PLACEMENT_3D('',#397103,#121700,#121701);
#101699=AXIS2_PLACEMENT_3D('',#397116,#121702,#121703);
#101700=AXIS2_PLACEMENT_3D('',#397129,#121704,#121705);
#101701=AXIS2_PLACEMENT_3D('',#397142,#121706,#121707);
#101702=AXIS2_PLACEMENT_3D('',#397143,#121708,#121709);
#101703=AXIS2_PLACEMENT_3D('',#397144,#121710,#121711);
#101704=AXIS2_PLACEMENT_3D('',#397157,#121712,#121713);
#101705=AXIS2_PLACEMENT_3D('',#397158,#121714,#121715);
#101706=AXIS2_PLACEMENT_3D('',#397168,#121717,#121718);
#101707=AXIS2_PLACEMENT_3D('',#397178,#121720,#121721);
#101708=AXIS2_PLACEMENT_3D('',#397181,#121722,#121723);
#101709=AXIS2_PLACEMENT_3D('',#397198,#121726,#121727);
#101710=AXIS2_PLACEMENT_3D('',#397248,#121728,#121729);
#101711=AXIS2_PLACEMENT_3D('',#397294,#121730,#121731);
#101712=AXIS2_PLACEMENT_3D('',#397311,#121732,#121733);
#101713=AXIS2_PLACEMENT_3D('',#397363,#121734,#121735);
#101714=AXIS2_PLACEMENT_3D('',#397364,#121736,#121737);
#101715=AXIS2_PLACEMENT_3D('',#397365,#121738,#121739);
#101716=AXIS2_PLACEMENT_3D('',#397366,#121740,#121741);
#101717=AXIS2_PLACEMENT_3D('',#397379,#121742,#121743);
#101718=AXIS2_PLACEMENT_3D('',#397380,#121744,#121745);
#101719=AXIS2_PLACEMENT_3D('',#397381,#121746,#121747);
#101720=AXIS2_PLACEMENT_3D('',#397394,#121748,#121749);
#101721=AXIS2_PLACEMENT_3D('',#397407,#121750,#121751);
#101722=AXIS2_PLACEMENT_3D('',#397420,#121752,#121753);
#101723=AXIS2_PLACEMENT_3D('',#397433,#121754,#121755);
#101724=AXIS2_PLACEMENT_3D('',#397446,#121756,#121757);
#101725=AXIS2_PLACEMENT_3D('',#397447,#121758,#121759);
#101726=AXIS2_PLACEMENT_3D('',#397448,#121760,#121761);
#101727=AXIS2_PLACEMENT_3D('',#397461,#121762,#121763);
#101728=AXIS2_PLACEMENT_3D('',#397462,#121764,#121765);
#101729=AXIS2_PLACEMENT_3D('',#397472,#121767,#121768);
#101730=AXIS2_PLACEMENT_3D('',#397482,#121770,#121771);
#101731=AXIS2_PLACEMENT_3D('',#397485,#121772,#121773);
#101732=AXIS2_PLACEMENT_3D('',#397502,#121776,#121777);
#101733=AXIS2_PLACEMENT_3D('',#397552,#121778,#121779);
#101734=AXIS2_PLACEMENT_3D('',#397598,#121780,#121781);
#101735=AXIS2_PLACEMENT_3D('',#397615,#121782,#121783);
#101736=AXIS2_PLACEMENT_3D('',#397667,#121784,#121785);
#101737=AXIS2_PLACEMENT_3D('',#397668,#121786,#121787);
#101738=AXIS2_PLACEMENT_3D('',#397669,#121788,#121789);
#101739=AXIS2_PLACEMENT_3D('',#397670,#121790,#121791);
#101740=AXIS2_PLACEMENT_3D('',#397683,#121792,#121793);
#101741=AXIS2_PLACEMENT_3D('',#397684,#121794,#121795);
#101742=AXIS2_PLACEMENT_3D('',#397685,#121796,#121797);
#101743=AXIS2_PLACEMENT_3D('',#397698,#121798,#121799);
#101744=AXIS2_PLACEMENT_3D('',#397711,#121800,#121801);
#101745=AXIS2_PLACEMENT_3D('',#397724,#121802,#121803);
#101746=AXIS2_PLACEMENT_3D('',#397737,#121804,#121805);
#101747=AXIS2_PLACEMENT_3D('',#397750,#121806,#121807);
#101748=AXIS2_PLACEMENT_3D('',#397751,#121808,#121809);
#101749=AXIS2_PLACEMENT_3D('',#397752,#121810,#121811);
#101750=AXIS2_PLACEMENT_3D('',#397765,#121812,#121813);
#101751=AXIS2_PLACEMENT_3D('',#397766,#121814,#121815);
#101752=AXIS2_PLACEMENT_3D('',#397776,#121817,#121818);
#101753=AXIS2_PLACEMENT_3D('',#397786,#121820,#121821);
#101754=AXIS2_PLACEMENT_3D('',#397789,#121822,#121823);
#101755=AXIS2_PLACEMENT_3D('',#397806,#121826,#121827);
#101756=AXIS2_PLACEMENT_3D('',#397856,#121828,#121829);
#101757=AXIS2_PLACEMENT_3D('',#397902,#121830,#121831);
#101758=AXIS2_PLACEMENT_3D('',#397919,#121832,#121833);
#101759=AXIS2_PLACEMENT_3D('',#397971,#121834,#121835);
#101760=AXIS2_PLACEMENT_3D('',#397972,#121836,#121837);
#101761=AXIS2_PLACEMENT_3D('',#397973,#121838,#121839);
#101762=AXIS2_PLACEMENT_3D('',#397974,#121840,#121841);
#101763=AXIS2_PLACEMENT_3D('',#397987,#121842,#121843);
#101764=AXIS2_PLACEMENT_3D('',#397988,#121844,#121845);
#101765=AXIS2_PLACEMENT_3D('',#397989,#121846,#121847);
#101766=AXIS2_PLACEMENT_3D('',#398002,#121848,#121849);
#101767=AXIS2_PLACEMENT_3D('',#398015,#121850,#121851);
#101768=AXIS2_PLACEMENT_3D('',#398028,#121852,#121853);
#101769=AXIS2_PLACEMENT_3D('',#398041,#121854,#121855);
#101770=AXIS2_PLACEMENT_3D('',#398054,#121856,#121857);
#101771=AXIS2_PLACEMENT_3D('',#398055,#121858,#121859);
#101772=AXIS2_PLACEMENT_3D('',#398056,#121860,#121861);
#101773=AXIS2_PLACEMENT_3D('',#398069,#121862,#121863);
#101774=AXIS2_PLACEMENT_3D('',#398070,#121864,#121865);
#101775=AXIS2_PLACEMENT_3D('',#398080,#121867,#121868);
#101776=AXIS2_PLACEMENT_3D('',#398090,#121870,#121871);
#101777=AXIS2_PLACEMENT_3D('',#398093,#121872,#121873);
#101778=AXIS2_PLACEMENT_3D('',#398110,#121876,#121877);
#101779=AXIS2_PLACEMENT_3D('',#398160,#121878,#121879);
#101780=AXIS2_PLACEMENT_3D('',#398206,#121880,#121881);
#101781=AXIS2_PLACEMENT_3D('',#398223,#121882,#121883);
#101782=AXIS2_PLACEMENT_3D('',#398275,#121884,#121885);
#101783=AXIS2_PLACEMENT_3D('',#398276,#121886,#121887);
#101784=AXIS2_PLACEMENT_3D('',#398277,#121888,#121889);
#101785=AXIS2_PLACEMENT_3D('',#398278,#121890,#121891);
#101786=AXIS2_PLACEMENT_3D('',#398291,#121892,#121893);
#101787=AXIS2_PLACEMENT_3D('',#398292,#121894,#121895);
#101788=AXIS2_PLACEMENT_3D('',#398293,#121896,#121897);
#101789=AXIS2_PLACEMENT_3D('',#398306,#121898,#121899);
#101790=AXIS2_PLACEMENT_3D('',#398319,#121900,#121901);
#101791=AXIS2_PLACEMENT_3D('',#398332,#121902,#121903);
#101792=AXIS2_PLACEMENT_3D('',#398345,#121904,#121905);
#101793=AXIS2_PLACEMENT_3D('',#398358,#121906,#121907);
#101794=AXIS2_PLACEMENT_3D('',#398359,#121908,#121909);
#101795=AXIS2_PLACEMENT_3D('',#398360,#121910,#121911);
#101796=AXIS2_PLACEMENT_3D('',#398373,#121912,#121913);
#101797=AXIS2_PLACEMENT_3D('',#398374,#121914,#121915);
#101798=AXIS2_PLACEMENT_3D('',#398384,#121917,#121918);
#101799=AXIS2_PLACEMENT_3D('',#398394,#121920,#121921);
#101800=AXIS2_PLACEMENT_3D('',#398397,#121922,#121923);
#101801=AXIS2_PLACEMENT_3D('',#398414,#121926,#121927);
#101802=AXIS2_PLACEMENT_3D('',#398464,#121928,#121929);
#101803=AXIS2_PLACEMENT_3D('',#398510,#121930,#121931);
#101804=AXIS2_PLACEMENT_3D('',#398527,#121932,#121933);
#101805=AXIS2_PLACEMENT_3D('',#398579,#121934,#121935);
#101806=AXIS2_PLACEMENT_3D('',#398580,#121936,#121937);
#101807=AXIS2_PLACEMENT_3D('',#398581,#121938,#121939);
#101808=AXIS2_PLACEMENT_3D('',#398582,#121940,#121941);
#101809=AXIS2_PLACEMENT_3D('',#398595,#121942,#121943);
#101810=AXIS2_PLACEMENT_3D('',#398596,#121944,#121945);
#101811=AXIS2_PLACEMENT_3D('',#398597,#121946,#121947);
#101812=AXIS2_PLACEMENT_3D('',#398610,#121948,#121949);
#101813=AXIS2_PLACEMENT_3D('',#398623,#121950,#121951);
#101814=AXIS2_PLACEMENT_3D('',#398636,#121952,#121953);
#101815=AXIS2_PLACEMENT_3D('',#398649,#121954,#121955);
#101816=AXIS2_PLACEMENT_3D('',#398662,#121956,#121957);
#101817=AXIS2_PLACEMENT_3D('',#398663,#121958,#121959);
#101818=AXIS2_PLACEMENT_3D('',#398664,#121960,#121961);
#101819=AXIS2_PLACEMENT_3D('',#398677,#121962,#121963);
#101820=AXIS2_PLACEMENT_3D('',#398678,#121964,#121965);
#101821=AXIS2_PLACEMENT_3D('',#398688,#121967,#121968);
#101822=AXIS2_PLACEMENT_3D('',#398698,#121970,#121971);
#101823=AXIS2_PLACEMENT_3D('',#398701,#121972,#121973);
#101824=AXIS2_PLACEMENT_3D('',#398718,#121976,#121977);
#101825=AXIS2_PLACEMENT_3D('',#398768,#121978,#121979);
#101826=AXIS2_PLACEMENT_3D('',#398814,#121980,#121981);
#101827=AXIS2_PLACEMENT_3D('',#398831,#121982,#121983);
#101828=AXIS2_PLACEMENT_3D('',#398883,#121984,#121985);
#101829=AXIS2_PLACEMENT_3D('',#398884,#121986,#121987);
#101830=AXIS2_PLACEMENT_3D('',#398885,#121988,#121989);
#101831=AXIS2_PLACEMENT_3D('',#398886,#121990,#121991);
#101832=AXIS2_PLACEMENT_3D('',#398899,#121992,#121993);
#101833=AXIS2_PLACEMENT_3D('',#398900,#121994,#121995);
#101834=AXIS2_PLACEMENT_3D('',#398901,#121996,#121997);
#101835=AXIS2_PLACEMENT_3D('',#398914,#121998,#121999);
#101836=AXIS2_PLACEMENT_3D('',#398927,#122000,#122001);
#101837=AXIS2_PLACEMENT_3D('',#398940,#122002,#122003);
#101838=AXIS2_PLACEMENT_3D('',#398953,#122004,#122005);
#101839=AXIS2_PLACEMENT_3D('',#398966,#122006,#122007);
#101840=AXIS2_PLACEMENT_3D('',#398967,#122008,#122009);
#101841=AXIS2_PLACEMENT_3D('',#398968,#122010,#122011);
#101842=AXIS2_PLACEMENT_3D('',#398981,#122012,#122013);
#101843=AXIS2_PLACEMENT_3D('',#398982,#122014,#122015);
#101844=AXIS2_PLACEMENT_3D('',#398992,#122017,#122018);
#101845=AXIS2_PLACEMENT_3D('',#399002,#122020,#122021);
#101846=AXIS2_PLACEMENT_3D('',#399005,#122022,#122023);
#101847=AXIS2_PLACEMENT_3D('',#399022,#122026,#122027);
#101848=AXIS2_PLACEMENT_3D('',#399072,#122028,#122029);
#101849=AXIS2_PLACEMENT_3D('',#399118,#122030,#122031);
#101850=AXIS2_PLACEMENT_3D('',#399135,#122032,#122033);
#101851=AXIS2_PLACEMENT_3D('',#399187,#122034,#122035);
#101852=AXIS2_PLACEMENT_3D('',#399188,#122036,#122037);
#101853=AXIS2_PLACEMENT_3D('',#399189,#122038,#122039);
#101854=AXIS2_PLACEMENT_3D('',#399190,#122040,#122041);
#101855=AXIS2_PLACEMENT_3D('',#399203,#122042,#122043);
#101856=AXIS2_PLACEMENT_3D('',#399204,#122044,#122045);
#101857=AXIS2_PLACEMENT_3D('',#399205,#122046,#122047);
#101858=AXIS2_PLACEMENT_3D('',#399218,#122048,#122049);
#101859=AXIS2_PLACEMENT_3D('',#399231,#122050,#122051);
#101860=AXIS2_PLACEMENT_3D('',#399244,#122052,#122053);
#101861=AXIS2_PLACEMENT_3D('',#399257,#122054,#122055);
#101862=AXIS2_PLACEMENT_3D('',#399270,#122056,#122057);
#101863=AXIS2_PLACEMENT_3D('',#399271,#122058,#122059);
#101864=AXIS2_PLACEMENT_3D('',#399272,#122060,#122061);
#101865=AXIS2_PLACEMENT_3D('',#399285,#122062,#122063);
#101866=AXIS2_PLACEMENT_3D('',#399286,#122064,#122065);
#101867=AXIS2_PLACEMENT_3D('',#399296,#122067,#122068);
#101868=AXIS2_PLACEMENT_3D('',#399306,#122070,#122071);
#101869=AXIS2_PLACEMENT_3D('',#399309,#122072,#122073);
#101870=AXIS2_PLACEMENT_3D('',#399326,#122076,#122077);
#101871=AXIS2_PLACEMENT_3D('',#399376,#122078,#122079);
#101872=AXIS2_PLACEMENT_3D('',#399422,#122080,#122081);
#101873=AXIS2_PLACEMENT_3D('',#399439,#122082,#122083);
#101874=AXIS2_PLACEMENT_3D('',#399491,#122084,#122085);
#101875=AXIS2_PLACEMENT_3D('',#399492,#122086,#122087);
#101876=AXIS2_PLACEMENT_3D('',#399493,#122088,#122089);
#101877=AXIS2_PLACEMENT_3D('',#399494,#122090,#122091);
#101878=AXIS2_PLACEMENT_3D('',#399507,#122092,#122093);
#101879=AXIS2_PLACEMENT_3D('',#399508,#122094,#122095);
#101880=AXIS2_PLACEMENT_3D('',#399509,#122096,#122097);
#101881=AXIS2_PLACEMENT_3D('',#399522,#122098,#122099);
#101882=AXIS2_PLACEMENT_3D('',#399535,#122100,#122101);
#101883=AXIS2_PLACEMENT_3D('',#399548,#122102,#122103);
#101884=AXIS2_PLACEMENT_3D('',#399561,#122104,#122105);
#101885=AXIS2_PLACEMENT_3D('',#399574,#122106,#122107);
#101886=AXIS2_PLACEMENT_3D('',#399575,#122108,#122109);
#101887=AXIS2_PLACEMENT_3D('',#399576,#122110,#122111);
#101888=AXIS2_PLACEMENT_3D('',#399589,#122112,#122113);
#101889=AXIS2_PLACEMENT_3D('',#399590,#122114,#122115);
#101890=AXIS2_PLACEMENT_3D('',#399600,#122117,#122118);
#101891=AXIS2_PLACEMENT_3D('',#399610,#122120,#122121);
#101892=AXIS2_PLACEMENT_3D('',#399613,#122122,#122123);
#101893=AXIS2_PLACEMENT_3D('',#399630,#122126,#122127);
#101894=AXIS2_PLACEMENT_3D('',#399680,#122128,#122129);
#101895=AXIS2_PLACEMENT_3D('',#399726,#122130,#122131);
#101896=AXIS2_PLACEMENT_3D('',#399743,#122132,#122133);
#101897=AXIS2_PLACEMENT_3D('',#399795,#122134,#122135);
#101898=AXIS2_PLACEMENT_3D('',#399796,#122136,#122137);
#101899=AXIS2_PLACEMENT_3D('',#399797,#122138,#122139);
#101900=AXIS2_PLACEMENT_3D('',#399798,#122140,#122141);
#101901=AXIS2_PLACEMENT_3D('',#399811,#122142,#122143);
#101902=AXIS2_PLACEMENT_3D('',#399812,#122144,#122145);
#101903=AXIS2_PLACEMENT_3D('',#399813,#122146,#122147);
#101904=AXIS2_PLACEMENT_3D('',#399826,#122148,#122149);
#101905=AXIS2_PLACEMENT_3D('',#399839,#122150,#122151);
#101906=AXIS2_PLACEMENT_3D('',#399852,#122152,#122153);
#101907=AXIS2_PLACEMENT_3D('',#399865,#122154,#122155);
#101908=AXIS2_PLACEMENT_3D('',#399878,#122156,#122157);
#101909=AXIS2_PLACEMENT_3D('',#399879,#122158,#122159);
#101910=AXIS2_PLACEMENT_3D('',#399880,#122160,#122161);
#101911=AXIS2_PLACEMENT_3D('',#399893,#122162,#122163);
#101912=AXIS2_PLACEMENT_3D('',#399894,#122164,#122165);
#101913=AXIS2_PLACEMENT_3D('',#399904,#122167,#122168);
#101914=AXIS2_PLACEMENT_3D('',#399914,#122170,#122171);
#101915=AXIS2_PLACEMENT_3D('',#399917,#122172,#122173);
#101916=AXIS2_PLACEMENT_3D('',#399934,#122176,#122177);
#101917=AXIS2_PLACEMENT_3D('',#399984,#122178,#122179);
#101918=AXIS2_PLACEMENT_3D('',#400030,#122180,#122181);
#101919=AXIS2_PLACEMENT_3D('',#400047,#122182,#122183);
#101920=AXIS2_PLACEMENT_3D('',#400099,#122184,#122185);
#101921=AXIS2_PLACEMENT_3D('',#400100,#122186,#122187);
#101922=AXIS2_PLACEMENT_3D('',#400101,#122188,#122189);
#101923=AXIS2_PLACEMENT_3D('',#400102,#122190,#122191);
#101924=AXIS2_PLACEMENT_3D('',#400115,#122192,#122193);
#101925=AXIS2_PLACEMENT_3D('',#400116,#122194,#122195);
#101926=AXIS2_PLACEMENT_3D('',#400117,#122196,#122197);
#101927=AXIS2_PLACEMENT_3D('',#400130,#122198,#122199);
#101928=AXIS2_PLACEMENT_3D('',#400143,#122200,#122201);
#101929=AXIS2_PLACEMENT_3D('',#400156,#122202,#122203);
#101930=AXIS2_PLACEMENT_3D('',#400169,#122204,#122205);
#101931=AXIS2_PLACEMENT_3D('',#400182,#122206,#122207);
#101932=AXIS2_PLACEMENT_3D('',#400183,#122208,#122209);
#101933=AXIS2_PLACEMENT_3D('',#400184,#122210,#122211);
#101934=AXIS2_PLACEMENT_3D('',#400197,#122212,#122213);
#101935=AXIS2_PLACEMENT_3D('',#400198,#122214,#122215);
#101936=AXIS2_PLACEMENT_3D('',#400208,#122217,#122218);
#101937=AXIS2_PLACEMENT_3D('',#400218,#122220,#122221);
#101938=AXIS2_PLACEMENT_3D('',#400221,#122222,#122223);
#101939=AXIS2_PLACEMENT_3D('',#400238,#122226,#122227);
#101940=AXIS2_PLACEMENT_3D('',#400288,#122228,#122229);
#101941=AXIS2_PLACEMENT_3D('',#400334,#122230,#122231);
#101942=AXIS2_PLACEMENT_3D('',#400351,#122232,#122233);
#101943=AXIS2_PLACEMENT_3D('',#400403,#122234,#122235);
#101944=AXIS2_PLACEMENT_3D('',#400404,#122236,#122237);
#101945=AXIS2_PLACEMENT_3D('',#400405,#122238,#122239);
#101946=AXIS2_PLACEMENT_3D('',#400406,#122240,#122241);
#101947=AXIS2_PLACEMENT_3D('',#400419,#122242,#122243);
#101948=AXIS2_PLACEMENT_3D('',#400420,#122244,#122245);
#101949=AXIS2_PLACEMENT_3D('',#400421,#122246,#122247);
#101950=AXIS2_PLACEMENT_3D('',#400434,#122248,#122249);
#101951=AXIS2_PLACEMENT_3D('',#400447,#122250,#122251);
#101952=AXIS2_PLACEMENT_3D('',#400460,#122252,#122253);
#101953=AXIS2_PLACEMENT_3D('',#400473,#122254,#122255);
#101954=AXIS2_PLACEMENT_3D('',#400486,#122256,#122257);
#101955=AXIS2_PLACEMENT_3D('',#400487,#122258,#122259);
#101956=AXIS2_PLACEMENT_3D('',#400488,#122260,#122261);
#101957=AXIS2_PLACEMENT_3D('',#400501,#122262,#122263);
#101958=AXIS2_PLACEMENT_3D('',#400502,#122264,#122265);
#101959=AXIS2_PLACEMENT_3D('',#400512,#122267,#122268);
#101960=AXIS2_PLACEMENT_3D('',#400522,#122270,#122271);
#101961=AXIS2_PLACEMENT_3D('',#400525,#122272,#122273);
#101962=AXIS2_PLACEMENT_3D('',#400542,#122276,#122277);
#101963=AXIS2_PLACEMENT_3D('',#400592,#122278,#122279);
#101964=AXIS2_PLACEMENT_3D('',#400638,#122280,#122281);
#101965=AXIS2_PLACEMENT_3D('',#400655,#122282,#122283);
#101966=AXIS2_PLACEMENT_3D('',#400707,#122284,#122285);
#101967=AXIS2_PLACEMENT_3D('',#400708,#122286,#122287);
#101968=AXIS2_PLACEMENT_3D('',#400709,#122288,#122289);
#101969=AXIS2_PLACEMENT_3D('',#400710,#122290,#122291);
#101970=AXIS2_PLACEMENT_3D('',#400723,#122292,#122293);
#101971=AXIS2_PLACEMENT_3D('',#400724,#122294,#122295);
#101972=AXIS2_PLACEMENT_3D('',#400725,#122296,#122297);
#101973=AXIS2_PLACEMENT_3D('',#400738,#122298,#122299);
#101974=AXIS2_PLACEMENT_3D('',#400751,#122300,#122301);
#101975=AXIS2_PLACEMENT_3D('',#400764,#122302,#122303);
#101976=AXIS2_PLACEMENT_3D('',#400777,#122304,#122305);
#101977=AXIS2_PLACEMENT_3D('',#400790,#122306,#122307);
#101978=AXIS2_PLACEMENT_3D('',#400791,#122308,#122309);
#101979=AXIS2_PLACEMENT_3D('',#400792,#122310,#122311);
#101980=AXIS2_PLACEMENT_3D('',#400805,#122312,#122313);
#101981=AXIS2_PLACEMENT_3D('',#400806,#122314,#122315);
#101982=AXIS2_PLACEMENT_3D('',#400816,#122317,#122318);
#101983=AXIS2_PLACEMENT_3D('',#400826,#122320,#122321);
#101984=AXIS2_PLACEMENT_3D('',#400829,#122322,#122323);
#101985=AXIS2_PLACEMENT_3D('',#400846,#122326,#122327);
#101986=AXIS2_PLACEMENT_3D('',#400896,#122328,#122329);
#101987=AXIS2_PLACEMENT_3D('',#400942,#122330,#122331);
#101988=AXIS2_PLACEMENT_3D('',#400959,#122332,#122333);
#101989=AXIS2_PLACEMENT_3D('',#401011,#122334,#122335);
#101990=AXIS2_PLACEMENT_3D('',#401012,#122336,#122337);
#101991=AXIS2_PLACEMENT_3D('',#401013,#122338,#122339);
#101992=AXIS2_PLACEMENT_3D('',#401014,#122340,#122341);
#101993=AXIS2_PLACEMENT_3D('',#401027,#122342,#122343);
#101994=AXIS2_PLACEMENT_3D('',#401028,#122344,#122345);
#101995=AXIS2_PLACEMENT_3D('',#401029,#122346,#122347);
#101996=AXIS2_PLACEMENT_3D('',#401042,#122348,#122349);
#101997=AXIS2_PLACEMENT_3D('',#401055,#122350,#122351);
#101998=AXIS2_PLACEMENT_3D('',#401068,#122352,#122353);
#101999=AXIS2_PLACEMENT_3D('',#401081,#122354,#122355);
#102000=AXIS2_PLACEMENT_3D('',#401094,#122356,#122357);
#102001=AXIS2_PLACEMENT_3D('',#401095,#122358,#122359);
#102002=AXIS2_PLACEMENT_3D('',#401096,#122360,#122361);
#102003=AXIS2_PLACEMENT_3D('',#401109,#122362,#122363);
#102004=AXIS2_PLACEMENT_3D('',#401110,#122364,#122365);
#102005=AXIS2_PLACEMENT_3D('',#401120,#122367,#122368);
#102006=AXIS2_PLACEMENT_3D('',#401130,#122370,#122371);
#102007=AXIS2_PLACEMENT_3D('',#401133,#122372,#122373);
#102008=AXIS2_PLACEMENT_3D('',#401150,#122376,#122377);
#102009=AXIS2_PLACEMENT_3D('',#401200,#122378,#122379);
#102010=AXIS2_PLACEMENT_3D('',#401246,#122380,#122381);
#102011=AXIS2_PLACEMENT_3D('',#401263,#122382,#122383);
#102012=AXIS2_PLACEMENT_3D('',#401315,#122384,#122385);
#102013=AXIS2_PLACEMENT_3D('',#401316,#122386,#122387);
#102014=AXIS2_PLACEMENT_3D('',#401317,#122388,#122389);
#102015=AXIS2_PLACEMENT_3D('',#401318,#122390,#122391);
#102016=AXIS2_PLACEMENT_3D('',#401331,#122392,#122393);
#102017=AXIS2_PLACEMENT_3D('',#401332,#122394,#122395);
#102018=AXIS2_PLACEMENT_3D('',#401333,#122396,#122397);
#102019=AXIS2_PLACEMENT_3D('',#401346,#122398,#122399);
#102020=AXIS2_PLACEMENT_3D('',#401359,#122400,#122401);
#102021=AXIS2_PLACEMENT_3D('',#401372,#122402,#122403);
#102022=AXIS2_PLACEMENT_3D('',#401385,#122404,#122405);
#102023=AXIS2_PLACEMENT_3D('',#401398,#122406,#122407);
#102024=AXIS2_PLACEMENT_3D('',#401399,#122408,#122409);
#102025=AXIS2_PLACEMENT_3D('',#401400,#122410,#122411);
#102026=AXIS2_PLACEMENT_3D('',#401413,#122412,#122413);
#102027=AXIS2_PLACEMENT_3D('',#401414,#122414,#122415);
#102028=AXIS2_PLACEMENT_3D('',#401424,#122417,#122418);
#102029=AXIS2_PLACEMENT_3D('',#401434,#122420,#122421);
#102030=AXIS2_PLACEMENT_3D('',#401437,#122422,#122423);
#102031=AXIS2_PLACEMENT_3D('',#401454,#122426,#122427);
#102032=AXIS2_PLACEMENT_3D('',#401504,#122428,#122429);
#102033=AXIS2_PLACEMENT_3D('',#401550,#122430,#122431);
#102034=AXIS2_PLACEMENT_3D('',#401567,#122432,#122433);
#102035=AXIS2_PLACEMENT_3D('',#401619,#122434,#122435);
#102036=AXIS2_PLACEMENT_3D('',#401620,#122436,#122437);
#102037=AXIS2_PLACEMENT_3D('',#401621,#122438,#122439);
#102038=AXIS2_PLACEMENT_3D('',#401622,#122440,#122441);
#102039=AXIS2_PLACEMENT_3D('',#401635,#122442,#122443);
#102040=AXIS2_PLACEMENT_3D('',#401636,#122444,#122445);
#102041=AXIS2_PLACEMENT_3D('',#401637,#122446,#122447);
#102042=AXIS2_PLACEMENT_3D('',#401650,#122448,#122449);
#102043=AXIS2_PLACEMENT_3D('',#401663,#122450,#122451);
#102044=AXIS2_PLACEMENT_3D('',#401676,#122452,#122453);
#102045=AXIS2_PLACEMENT_3D('',#401689,#122454,#122455);
#102046=AXIS2_PLACEMENT_3D('',#401702,#122456,#122457);
#102047=AXIS2_PLACEMENT_3D('',#401703,#122458,#122459);
#102048=AXIS2_PLACEMENT_3D('',#401704,#122460,#122461);
#102049=AXIS2_PLACEMENT_3D('',#401717,#122462,#122463);
#102050=AXIS2_PLACEMENT_3D('',#401718,#122464,#122465);
#102051=AXIS2_PLACEMENT_3D('',#401728,#122467,#122468);
#102052=AXIS2_PLACEMENT_3D('',#401738,#122470,#122471);
#102053=AXIS2_PLACEMENT_3D('',#401741,#122472,#122473);
#102054=AXIS2_PLACEMENT_3D('',#401758,#122476,#122477);
#102055=AXIS2_PLACEMENT_3D('',#401808,#122478,#122479);
#102056=AXIS2_PLACEMENT_3D('',#401854,#122480,#122481);
#102057=AXIS2_PLACEMENT_3D('',#401871,#122482,#122483);
#102058=AXIS2_PLACEMENT_3D('',#401923,#122484,#122485);
#102059=AXIS2_PLACEMENT_3D('',#401924,#122486,#122487);
#102060=AXIS2_PLACEMENT_3D('',#401925,#122488,#122489);
#102061=AXIS2_PLACEMENT_3D('',#401926,#122490,#122491);
#102062=AXIS2_PLACEMENT_3D('',#401939,#122492,#122493);
#102063=AXIS2_PLACEMENT_3D('',#401940,#122494,#122495);
#102064=AXIS2_PLACEMENT_3D('',#401941,#122496,#122497);
#102065=AXIS2_PLACEMENT_3D('',#401954,#122498,#122499);
#102066=AXIS2_PLACEMENT_3D('',#401967,#122500,#122501);
#102067=AXIS2_PLACEMENT_3D('',#401980,#122502,#122503);
#102068=AXIS2_PLACEMENT_3D('',#401993,#122504,#122505);
#102069=AXIS2_PLACEMENT_3D('',#402006,#122506,#122507);
#102070=AXIS2_PLACEMENT_3D('',#402007,#122508,#122509);
#102071=AXIS2_PLACEMENT_3D('',#402008,#122510,#122511);
#102072=AXIS2_PLACEMENT_3D('',#402021,#122512,#122513);
#102073=AXIS2_PLACEMENT_3D('',#402022,#122514,#122515);
#102074=AXIS2_PLACEMENT_3D('',#402032,#122517,#122518);
#102075=AXIS2_PLACEMENT_3D('',#402042,#122520,#122521);
#102076=AXIS2_PLACEMENT_3D('',#402045,#122522,#122523);
#102077=AXIS2_PLACEMENT_3D('',#402062,#122526,#122527);
#102078=AXIS2_PLACEMENT_3D('',#402112,#122528,#122529);
#102079=AXIS2_PLACEMENT_3D('',#402158,#122530,#122531);
#102080=AXIS2_PLACEMENT_3D('',#402175,#122532,#122533);
#102081=AXIS2_PLACEMENT_3D('',#402227,#122534,#122535);
#102082=AXIS2_PLACEMENT_3D('',#402228,#122536,#122537);
#102083=AXIS2_PLACEMENT_3D('',#402229,#122538,#122539);
#102084=AXIS2_PLACEMENT_3D('',#402230,#122540,#122541);
#102085=AXIS2_PLACEMENT_3D('',#402243,#122542,#122543);
#102086=AXIS2_PLACEMENT_3D('',#402244,#122544,#122545);
#102087=AXIS2_PLACEMENT_3D('',#402245,#122546,#122547);
#102088=AXIS2_PLACEMENT_3D('',#402258,#122548,#122549);
#102089=AXIS2_PLACEMENT_3D('',#402271,#122550,#122551);
#102090=AXIS2_PLACEMENT_3D('',#402284,#122552,#122553);
#102091=AXIS2_PLACEMENT_3D('',#402297,#122554,#122555);
#102092=AXIS2_PLACEMENT_3D('',#402310,#122556,#122557);
#102093=AXIS2_PLACEMENT_3D('',#402311,#122558,#122559);
#102094=AXIS2_PLACEMENT_3D('',#402312,#122560,#122561);
#102095=AXIS2_PLACEMENT_3D('',#402325,#122562,#122563);
#102096=AXIS2_PLACEMENT_3D('',#402326,#122564,#122565);
#102097=AXIS2_PLACEMENT_3D('',#402336,#122567,#122568);
#102098=AXIS2_PLACEMENT_3D('',#402346,#122570,#122571);
#102099=AXIS2_PLACEMENT_3D('',#402349,#122572,#122573);
#102100=AXIS2_PLACEMENT_3D('',#402366,#122576,#122577);
#102101=AXIS2_PLACEMENT_3D('',#402416,#122578,#122579);
#102102=AXIS2_PLACEMENT_3D('',#402462,#122580,#122581);
#102103=AXIS2_PLACEMENT_3D('',#402479,#122582,#122583);
#102104=AXIS2_PLACEMENT_3D('',#402531,#122584,#122585);
#102105=AXIS2_PLACEMENT_3D('',#402532,#122586,#122587);
#102106=AXIS2_PLACEMENT_3D('',#402533,#122588,#122589);
#102107=AXIS2_PLACEMENT_3D('',#402534,#122590,#122591);
#102108=AXIS2_PLACEMENT_3D('',#402547,#122592,#122593);
#102109=AXIS2_PLACEMENT_3D('',#402548,#122594,#122595);
#102110=AXIS2_PLACEMENT_3D('',#402549,#122596,#122597);
#102111=AXIS2_PLACEMENT_3D('',#402562,#122598,#122599);
#102112=AXIS2_PLACEMENT_3D('',#402575,#122600,#122601);
#102113=AXIS2_PLACEMENT_3D('',#402588,#122602,#122603);
#102114=AXIS2_PLACEMENT_3D('',#402601,#122604,#122605);
#102115=AXIS2_PLACEMENT_3D('',#402614,#122606,#122607);
#102116=AXIS2_PLACEMENT_3D('',#402615,#122608,#122609);
#102117=AXIS2_PLACEMENT_3D('',#402616,#122610,#122611);
#102118=AXIS2_PLACEMENT_3D('',#402629,#122612,#122613);
#102119=AXIS2_PLACEMENT_3D('',#402630,#122614,#122615);
#102120=AXIS2_PLACEMENT_3D('',#402640,#122617,#122618);
#102121=AXIS2_PLACEMENT_3D('',#402650,#122620,#122621);
#102122=AXIS2_PLACEMENT_3D('',#402653,#122622,#122623);
#102123=AXIS2_PLACEMENT_3D('',#402670,#122626,#122627);
#102124=AXIS2_PLACEMENT_3D('',#402720,#122628,#122629);
#102125=AXIS2_PLACEMENT_3D('',#402766,#122630,#122631);
#102126=AXIS2_PLACEMENT_3D('',#402783,#122632,#122633);
#102127=AXIS2_PLACEMENT_3D('',#402835,#122634,#122635);
#102128=AXIS2_PLACEMENT_3D('',#402836,#122636,#122637);
#102129=AXIS2_PLACEMENT_3D('',#402837,#122638,#122639);
#102130=AXIS2_PLACEMENT_3D('',#402838,#122640,#122641);
#102131=AXIS2_PLACEMENT_3D('',#402851,#122642,#122643);
#102132=AXIS2_PLACEMENT_3D('',#402852,#122644,#122645);
#102133=AXIS2_PLACEMENT_3D('',#402853,#122646,#122647);
#102134=AXIS2_PLACEMENT_3D('',#402866,#122648,#122649);
#102135=AXIS2_PLACEMENT_3D('',#402879,#122650,#122651);
#102136=AXIS2_PLACEMENT_3D('',#402892,#122652,#122653);
#102137=AXIS2_PLACEMENT_3D('',#402905,#122654,#122655);
#102138=AXIS2_PLACEMENT_3D('',#402918,#122656,#122657);
#102139=AXIS2_PLACEMENT_3D('',#402919,#122658,#122659);
#102140=AXIS2_PLACEMENT_3D('',#402920,#122660,#122661);
#102141=AXIS2_PLACEMENT_3D('',#402933,#122662,#122663);
#102142=AXIS2_PLACEMENT_3D('',#402934,#122664,#122665);
#102143=AXIS2_PLACEMENT_3D('',#402944,#122667,#122668);
#102144=AXIS2_PLACEMENT_3D('',#402954,#122670,#122671);
#102145=AXIS2_PLACEMENT_3D('',#402957,#122672,#122673);
#102146=AXIS2_PLACEMENT_3D('',#402974,#122676,#122677);
#102147=AXIS2_PLACEMENT_3D('',#403024,#122678,#122679);
#102148=AXIS2_PLACEMENT_3D('',#403070,#122680,#122681);
#102149=AXIS2_PLACEMENT_3D('',#403087,#122682,#122683);
#102150=AXIS2_PLACEMENT_3D('',#403139,#122684,#122685);
#102151=AXIS2_PLACEMENT_3D('',#403140,#122686,#122687);
#102152=AXIS2_PLACEMENT_3D('',#403141,#122688,#122689);
#102153=AXIS2_PLACEMENT_3D('',#403142,#122690,#122691);
#102154=AXIS2_PLACEMENT_3D('',#403155,#122692,#122693);
#102155=AXIS2_PLACEMENT_3D('',#403156,#122694,#122695);
#102156=AXIS2_PLACEMENT_3D('',#403157,#122696,#122697);
#102157=AXIS2_PLACEMENT_3D('',#403170,#122698,#122699);
#102158=AXIS2_PLACEMENT_3D('',#403183,#122700,#122701);
#102159=AXIS2_PLACEMENT_3D('',#403196,#122702,#122703);
#102160=AXIS2_PLACEMENT_3D('',#403209,#122704,#122705);
#102161=AXIS2_PLACEMENT_3D('',#403222,#122706,#122707);
#102162=AXIS2_PLACEMENT_3D('',#403223,#122708,#122709);
#102163=AXIS2_PLACEMENT_3D('',#403224,#122710,#122711);
#102164=AXIS2_PLACEMENT_3D('',#403237,#122712,#122713);
#102165=AXIS2_PLACEMENT_3D('',#403238,#122714,#122715);
#102166=AXIS2_PLACEMENT_3D('',#403248,#122717,#122718);
#102167=AXIS2_PLACEMENT_3D('',#403258,#122720,#122721);
#102168=AXIS2_PLACEMENT_3D('',#403261,#122722,#122723);
#102169=AXIS2_PLACEMENT_3D('',#403278,#122726,#122727);
#102170=AXIS2_PLACEMENT_3D('',#403328,#122728,#122729);
#102171=AXIS2_PLACEMENT_3D('',#403374,#122730,#122731);
#102172=AXIS2_PLACEMENT_3D('',#403391,#122732,#122733);
#102173=AXIS2_PLACEMENT_3D('',#403443,#122734,#122735);
#102174=AXIS2_PLACEMENT_3D('',#403444,#122736,#122737);
#102175=AXIS2_PLACEMENT_3D('',#403445,#122738,#122739);
#102176=AXIS2_PLACEMENT_3D('',#403446,#122740,#122741);
#102177=AXIS2_PLACEMENT_3D('',#403459,#122742,#122743);
#102178=AXIS2_PLACEMENT_3D('',#403460,#122744,#122745);
#102179=AXIS2_PLACEMENT_3D('',#403461,#122746,#122747);
#102180=AXIS2_PLACEMENT_3D('',#403474,#122748,#122749);
#102181=AXIS2_PLACEMENT_3D('',#403487,#122750,#122751);
#102182=AXIS2_PLACEMENT_3D('',#403500,#122752,#122753);
#102183=AXIS2_PLACEMENT_3D('',#403513,#122754,#122755);
#102184=AXIS2_PLACEMENT_3D('',#403526,#122756,#122757);
#102185=AXIS2_PLACEMENT_3D('',#403527,#122758,#122759);
#102186=AXIS2_PLACEMENT_3D('',#403528,#122760,#122761);
#102187=AXIS2_PLACEMENT_3D('',#403541,#122762,#122763);
#102188=AXIS2_PLACEMENT_3D('',#403542,#122764,#122765);
#102189=AXIS2_PLACEMENT_3D('',#403552,#122767,#122768);
#102190=AXIS2_PLACEMENT_3D('',#403562,#122770,#122771);
#102191=AXIS2_PLACEMENT_3D('',#403565,#122772,#122773);
#102192=AXIS2_PLACEMENT_3D('',#403582,#122776,#122777);
#102193=AXIS2_PLACEMENT_3D('',#403632,#122778,#122779);
#102194=AXIS2_PLACEMENT_3D('',#403678,#122780,#122781);
#102195=AXIS2_PLACEMENT_3D('',#403695,#122782,#122783);
#102196=AXIS2_PLACEMENT_3D('',#403747,#122784,#122785);
#102197=AXIS2_PLACEMENT_3D('',#403748,#122786,#122787);
#102198=AXIS2_PLACEMENT_3D('',#403749,#122788,#122789);
#102199=AXIS2_PLACEMENT_3D('',#403750,#122790,#122791);
#102200=AXIS2_PLACEMENT_3D('',#403763,#122792,#122793);
#102201=AXIS2_PLACEMENT_3D('',#403764,#122794,#122795);
#102202=AXIS2_PLACEMENT_3D('',#403765,#122796,#122797);
#102203=AXIS2_PLACEMENT_3D('',#403778,#122798,#122799);
#102204=AXIS2_PLACEMENT_3D('',#403791,#122800,#122801);
#102205=AXIS2_PLACEMENT_3D('',#403804,#122802,#122803);
#102206=AXIS2_PLACEMENT_3D('',#403817,#122804,#122805);
#102207=AXIS2_PLACEMENT_3D('',#403830,#122806,#122807);
#102208=AXIS2_PLACEMENT_3D('',#403831,#122808,#122809);
#102209=AXIS2_PLACEMENT_3D('',#403832,#122810,#122811);
#102210=AXIS2_PLACEMENT_3D('',#403845,#122812,#122813);
#102211=AXIS2_PLACEMENT_3D('',#403846,#122814,#122815);
#102212=AXIS2_PLACEMENT_3D('',#403856,#122817,#122818);
#102213=AXIS2_PLACEMENT_3D('',#403866,#122820,#122821);
#102214=AXIS2_PLACEMENT_3D('',#403869,#122822,#122823);
#102215=AXIS2_PLACEMENT_3D('',#403886,#122826,#122827);
#102216=AXIS2_PLACEMENT_3D('',#403936,#122828,#122829);
#102217=AXIS2_PLACEMENT_3D('',#403982,#122830,#122831);
#102218=AXIS2_PLACEMENT_3D('',#403999,#122832,#122833);
#102219=AXIS2_PLACEMENT_3D('',#404051,#122834,#122835);
#102220=AXIS2_PLACEMENT_3D('',#404052,#122836,#122837);
#102221=AXIS2_PLACEMENT_3D('',#404053,#122838,#122839);
#102222=AXIS2_PLACEMENT_3D('',#404054,#122840,#122841);
#102223=AXIS2_PLACEMENT_3D('',#404067,#122842,#122843);
#102224=AXIS2_PLACEMENT_3D('',#404068,#122844,#122845);
#102225=AXIS2_PLACEMENT_3D('',#404069,#122846,#122847);
#102226=AXIS2_PLACEMENT_3D('',#404082,#122848,#122849);
#102227=AXIS2_PLACEMENT_3D('',#404095,#122850,#122851);
#102228=AXIS2_PLACEMENT_3D('',#404108,#122852,#122853);
#102229=AXIS2_PLACEMENT_3D('',#404121,#122854,#122855);
#102230=AXIS2_PLACEMENT_3D('',#404134,#122856,#122857);
#102231=AXIS2_PLACEMENT_3D('',#404135,#122858,#122859);
#102232=AXIS2_PLACEMENT_3D('',#404136,#122860,#122861);
#102233=AXIS2_PLACEMENT_3D('',#404149,#122862,#122863);
#102234=AXIS2_PLACEMENT_3D('',#404150,#122864,#122865);
#102235=AXIS2_PLACEMENT_3D('',#404160,#122867,#122868);
#102236=AXIS2_PLACEMENT_3D('',#404170,#122870,#122871);
#102237=AXIS2_PLACEMENT_3D('',#404173,#122872,#122873);
#102238=AXIS2_PLACEMENT_3D('',#404190,#122876,#122877);
#102239=AXIS2_PLACEMENT_3D('',#404240,#122878,#122879);
#102240=AXIS2_PLACEMENT_3D('',#404286,#122880,#122881);
#102241=AXIS2_PLACEMENT_3D('',#404303,#122882,#122883);
#102242=AXIS2_PLACEMENT_3D('',#404355,#122884,#122885);
#102243=AXIS2_PLACEMENT_3D('',#404356,#122886,#122887);
#102244=AXIS2_PLACEMENT_3D('',#404357,#122888,#122889);
#102245=AXIS2_PLACEMENT_3D('',#404358,#122890,#122891);
#102246=AXIS2_PLACEMENT_3D('',#404371,#122892,#122893);
#102247=AXIS2_PLACEMENT_3D('',#404372,#122894,#122895);
#102248=AXIS2_PLACEMENT_3D('',#404373,#122896,#122897);
#102249=AXIS2_PLACEMENT_3D('',#404386,#122898,#122899);
#102250=AXIS2_PLACEMENT_3D('',#404399,#122900,#122901);
#102251=AXIS2_PLACEMENT_3D('',#404412,#122902,#122903);
#102252=AXIS2_PLACEMENT_3D('',#404425,#122904,#122905);
#102253=AXIS2_PLACEMENT_3D('',#404438,#122906,#122907);
#102254=AXIS2_PLACEMENT_3D('',#404439,#122908,#122909);
#102255=AXIS2_PLACEMENT_3D('',#404440,#122910,#122911);
#102256=AXIS2_PLACEMENT_3D('',#404453,#122912,#122913);
#102257=AXIS2_PLACEMENT_3D('',#404454,#122914,#122915);
#102258=AXIS2_PLACEMENT_3D('',#404464,#122917,#122918);
#102259=AXIS2_PLACEMENT_3D('',#404474,#122920,#122921);
#102260=AXIS2_PLACEMENT_3D('',#404477,#122922,#122923);
#102261=AXIS2_PLACEMENT_3D('',#404494,#122926,#122927);
#102262=AXIS2_PLACEMENT_3D('',#404544,#122928,#122929);
#102263=AXIS2_PLACEMENT_3D('',#404590,#122930,#122931);
#102264=AXIS2_PLACEMENT_3D('',#404607,#122932,#122933);
#102265=AXIS2_PLACEMENT_3D('',#404659,#122934,#122935);
#102266=AXIS2_PLACEMENT_3D('',#404660,#122936,#122937);
#102267=AXIS2_PLACEMENT_3D('',#404661,#122938,#122939);
#102268=AXIS2_PLACEMENT_3D('',#404662,#122940,#122941);
#102269=AXIS2_PLACEMENT_3D('',#404675,#122942,#122943);
#102270=AXIS2_PLACEMENT_3D('',#404676,#122944,#122945);
#102271=AXIS2_PLACEMENT_3D('',#404677,#122946,#122947);
#102272=AXIS2_PLACEMENT_3D('',#404690,#122948,#122949);
#102273=AXIS2_PLACEMENT_3D('',#404703,#122950,#122951);
#102274=AXIS2_PLACEMENT_3D('',#404716,#122952,#122953);
#102275=AXIS2_PLACEMENT_3D('',#404729,#122954,#122955);
#102276=AXIS2_PLACEMENT_3D('',#404742,#122956,#122957);
#102277=AXIS2_PLACEMENT_3D('',#404743,#122958,#122959);
#102278=AXIS2_PLACEMENT_3D('',#404744,#122960,#122961);
#102279=AXIS2_PLACEMENT_3D('',#404757,#122962,#122963);
#102280=AXIS2_PLACEMENT_3D('',#404758,#122964,#122965);
#102281=AXIS2_PLACEMENT_3D('',#404768,#122967,#122968);
#102282=AXIS2_PLACEMENT_3D('',#404778,#122970,#122971);
#102283=AXIS2_PLACEMENT_3D('',#404781,#122972,#122973);
#102284=AXIS2_PLACEMENT_3D('',#404798,#122976,#122977);
#102285=AXIS2_PLACEMENT_3D('',#404848,#122978,#122979);
#102286=AXIS2_PLACEMENT_3D('',#404894,#122980,#122981);
#102287=AXIS2_PLACEMENT_3D('',#404911,#122982,#122983);
#102288=AXIS2_PLACEMENT_3D('',#404963,#122984,#122985);
#102289=AXIS2_PLACEMENT_3D('',#404964,#122986,#122987);
#102290=AXIS2_PLACEMENT_3D('',#404965,#122988,#122989);
#102291=AXIS2_PLACEMENT_3D('',#404966,#122990,#122991);
#102292=AXIS2_PLACEMENT_3D('',#404979,#122992,#122993);
#102293=AXIS2_PLACEMENT_3D('',#404980,#122994,#122995);
#102294=AXIS2_PLACEMENT_3D('',#404981,#122996,#122997);
#102295=AXIS2_PLACEMENT_3D('',#404994,#122998,#122999);
#102296=AXIS2_PLACEMENT_3D('',#405007,#123000,#123001);
#102297=AXIS2_PLACEMENT_3D('',#405020,#123002,#123003);
#102298=AXIS2_PLACEMENT_3D('',#405033,#123004,#123005);
#102299=AXIS2_PLACEMENT_3D('',#405046,#123006,#123007);
#102300=AXIS2_PLACEMENT_3D('',#405047,#123008,#123009);
#102301=AXIS2_PLACEMENT_3D('',#405048,#123010,#123011);
#102302=AXIS2_PLACEMENT_3D('',#405061,#123012,#123013);
#102303=AXIS2_PLACEMENT_3D('',#405062,#123014,#123015);
#102304=AXIS2_PLACEMENT_3D('',#405072,#123017,#123018);
#102305=AXIS2_PLACEMENT_3D('',#405082,#123020,#123021);
#102306=AXIS2_PLACEMENT_3D('',#405085,#123022,#123023);
#102307=AXIS2_PLACEMENT_3D('',#405102,#123026,#123027);
#102308=AXIS2_PLACEMENT_3D('',#405152,#123028,#123029);
#102309=AXIS2_PLACEMENT_3D('',#405198,#123030,#123031);
#102310=AXIS2_PLACEMENT_3D('',#405215,#123032,#123033);
#102311=AXIS2_PLACEMENT_3D('',#405267,#123034,#123035);
#102312=AXIS2_PLACEMENT_3D('',#405268,#123036,#123037);
#102313=AXIS2_PLACEMENT_3D('',#405269,#123038,#123039);
#102314=AXIS2_PLACEMENT_3D('',#405270,#123040,#123041);
#102315=AXIS2_PLACEMENT_3D('',#405283,#123042,#123043);
#102316=AXIS2_PLACEMENT_3D('',#405284,#123044,#123045);
#102317=AXIS2_PLACEMENT_3D('',#405285,#123046,#123047);
#102318=AXIS2_PLACEMENT_3D('',#405298,#123048,#123049);
#102319=AXIS2_PLACEMENT_3D('',#405311,#123050,#123051);
#102320=AXIS2_PLACEMENT_3D('',#405324,#123052,#123053);
#102321=AXIS2_PLACEMENT_3D('',#405337,#123054,#123055);
#102322=AXIS2_PLACEMENT_3D('',#405350,#123056,#123057);
#102323=AXIS2_PLACEMENT_3D('',#405351,#123058,#123059);
#102324=AXIS2_PLACEMENT_3D('',#405352,#123060,#123061);
#102325=AXIS2_PLACEMENT_3D('',#405365,#123062,#123063);
#102326=AXIS2_PLACEMENT_3D('',#405366,#123064,#123065);
#102327=AXIS2_PLACEMENT_3D('',#405376,#123067,#123068);
#102328=AXIS2_PLACEMENT_3D('',#405386,#123070,#123071);
#102329=AXIS2_PLACEMENT_3D('',#405389,#123072,#123073);
#102330=AXIS2_PLACEMENT_3D('',#405406,#123076,#123077);
#102331=AXIS2_PLACEMENT_3D('',#405456,#123078,#123079);
#102332=AXIS2_PLACEMENT_3D('',#405502,#123080,#123081);
#102333=AXIS2_PLACEMENT_3D('',#405519,#123082,#123083);
#102334=AXIS2_PLACEMENT_3D('',#405571,#123084,#123085);
#102335=AXIS2_PLACEMENT_3D('',#405572,#123086,#123087);
#102336=AXIS2_PLACEMENT_3D('',#405573,#123088,#123089);
#102337=AXIS2_PLACEMENT_3D('',#405574,#123090,#123091);
#102338=AXIS2_PLACEMENT_3D('',#405587,#123092,#123093);
#102339=AXIS2_PLACEMENT_3D('',#405588,#123094,#123095);
#102340=AXIS2_PLACEMENT_3D('',#405589,#123096,#123097);
#102341=AXIS2_PLACEMENT_3D('',#405602,#123098,#123099);
#102342=AXIS2_PLACEMENT_3D('',#405615,#123100,#123101);
#102343=AXIS2_PLACEMENT_3D('',#405628,#123102,#123103);
#102344=AXIS2_PLACEMENT_3D('',#405641,#123104,#123105);
#102345=AXIS2_PLACEMENT_3D('',#405654,#123106,#123107);
#102346=AXIS2_PLACEMENT_3D('',#405655,#123108,#123109);
#102347=AXIS2_PLACEMENT_3D('',#405656,#123110,#123111);
#102348=AXIS2_PLACEMENT_3D('',#405669,#123112,#123113);
#102349=AXIS2_PLACEMENT_3D('',#405670,#123114,#123115);
#102350=AXIS2_PLACEMENT_3D('',#405680,#123117,#123118);
#102351=AXIS2_PLACEMENT_3D('',#405690,#123120,#123121);
#102352=AXIS2_PLACEMENT_3D('',#405693,#123122,#123123);
#102353=AXIS2_PLACEMENT_3D('',#405710,#123126,#123127);
#102354=AXIS2_PLACEMENT_3D('',#405760,#123128,#123129);
#102355=AXIS2_PLACEMENT_3D('',#405806,#123130,#123131);
#102356=AXIS2_PLACEMENT_3D('',#405823,#123132,#123133);
#102357=AXIS2_PLACEMENT_3D('',#405875,#123134,#123135);
#102358=AXIS2_PLACEMENT_3D('',#405876,#123136,#123137);
#102359=AXIS2_PLACEMENT_3D('',#405877,#123138,#123139);
#102360=AXIS2_PLACEMENT_3D('',#405878,#123140,#123141);
#102361=AXIS2_PLACEMENT_3D('',#405891,#123142,#123143);
#102362=AXIS2_PLACEMENT_3D('',#405892,#123144,#123145);
#102363=AXIS2_PLACEMENT_3D('',#405893,#123146,#123147);
#102364=AXIS2_PLACEMENT_3D('',#405906,#123148,#123149);
#102365=AXIS2_PLACEMENT_3D('',#405919,#123150,#123151);
#102366=AXIS2_PLACEMENT_3D('',#405932,#123152,#123153);
#102367=AXIS2_PLACEMENT_3D('',#405945,#123154,#123155);
#102368=AXIS2_PLACEMENT_3D('',#405958,#123156,#123157);
#102369=AXIS2_PLACEMENT_3D('',#405959,#123158,#123159);
#102370=AXIS2_PLACEMENT_3D('',#405960,#123160,#123161);
#102371=AXIS2_PLACEMENT_3D('',#405973,#123162,#123163);
#102372=AXIS2_PLACEMENT_3D('',#405974,#123164,#123165);
#102373=AXIS2_PLACEMENT_3D('',#405984,#123167,#123168);
#102374=AXIS2_PLACEMENT_3D('',#405994,#123170,#123171);
#102375=AXIS2_PLACEMENT_3D('',#405997,#123172,#123173);
#102376=AXIS2_PLACEMENT_3D('',#406014,#123176,#123177);
#102377=AXIS2_PLACEMENT_3D('',#406064,#123178,#123179);
#102378=AXIS2_PLACEMENT_3D('',#406110,#123180,#123181);
#102379=AXIS2_PLACEMENT_3D('',#406127,#123182,#123183);
#102380=AXIS2_PLACEMENT_3D('',#406179,#123184,#123185);
#102381=AXIS2_PLACEMENT_3D('',#406180,#123186,#123187);
#102382=AXIS2_PLACEMENT_3D('',#406181,#123188,#123189);
#102383=AXIS2_PLACEMENT_3D('',#406182,#123190,#123191);
#102384=AXIS2_PLACEMENT_3D('',#406195,#123192,#123193);
#102385=AXIS2_PLACEMENT_3D('',#406196,#123194,#123195);
#102386=AXIS2_PLACEMENT_3D('',#406197,#123196,#123197);
#102387=AXIS2_PLACEMENT_3D('',#406210,#123198,#123199);
#102388=AXIS2_PLACEMENT_3D('',#406223,#123200,#123201);
#102389=AXIS2_PLACEMENT_3D('',#406236,#123202,#123203);
#102390=AXIS2_PLACEMENT_3D('',#406249,#123204,#123205);
#102391=AXIS2_PLACEMENT_3D('',#406262,#123206,#123207);
#102392=AXIS2_PLACEMENT_3D('',#406263,#123208,#123209);
#102393=AXIS2_PLACEMENT_3D('',#406264,#123210,#123211);
#102394=AXIS2_PLACEMENT_3D('',#406277,#123212,#123213);
#102395=AXIS2_PLACEMENT_3D('',#406278,#123214,#123215);
#102396=AXIS2_PLACEMENT_3D('',#406288,#123217,#123218);
#102397=AXIS2_PLACEMENT_3D('',#406298,#123220,#123221);
#102398=AXIS2_PLACEMENT_3D('',#406301,#123222,#123223);
#102399=AXIS2_PLACEMENT_3D('',#406318,#123226,#123227);
#102400=AXIS2_PLACEMENT_3D('',#406368,#123228,#123229);
#102401=AXIS2_PLACEMENT_3D('',#406414,#123230,#123231);
#102402=AXIS2_PLACEMENT_3D('',#406431,#123232,#123233);
#102403=AXIS2_PLACEMENT_3D('',#406483,#123234,#123235);
#102404=AXIS2_PLACEMENT_3D('',#406484,#123236,#123237);
#102405=AXIS2_PLACEMENT_3D('',#406485,#123238,#123239);
#102406=AXIS2_PLACEMENT_3D('',#406486,#123240,#123241);
#102407=AXIS2_PLACEMENT_3D('',#406499,#123242,#123243);
#102408=AXIS2_PLACEMENT_3D('',#406500,#123244,#123245);
#102409=AXIS2_PLACEMENT_3D('',#406501,#123246,#123247);
#102410=AXIS2_PLACEMENT_3D('',#406514,#123248,#123249);
#102411=AXIS2_PLACEMENT_3D('',#406527,#123250,#123251);
#102412=AXIS2_PLACEMENT_3D('',#406540,#123252,#123253);
#102413=AXIS2_PLACEMENT_3D('',#406553,#123254,#123255);
#102414=AXIS2_PLACEMENT_3D('',#406566,#123256,#123257);
#102415=AXIS2_PLACEMENT_3D('',#406567,#123258,#123259);
#102416=AXIS2_PLACEMENT_3D('',#406568,#123260,#123261);
#102417=AXIS2_PLACEMENT_3D('',#406581,#123262,#123263);
#102418=AXIS2_PLACEMENT_3D('',#406582,#123264,#123265);
#102419=AXIS2_PLACEMENT_3D('',#406592,#123267,#123268);
#102420=AXIS2_PLACEMENT_3D('',#406602,#123270,#123271);
#102421=AXIS2_PLACEMENT_3D('',#406605,#123272,#123273);
#102422=AXIS2_PLACEMENT_3D('',#406622,#123276,#123277);
#102423=AXIS2_PLACEMENT_3D('',#406672,#123278,#123279);
#102424=AXIS2_PLACEMENT_3D('',#406718,#123280,#123281);
#102425=AXIS2_PLACEMENT_3D('',#406735,#123282,#123283);
#102426=AXIS2_PLACEMENT_3D('',#406787,#123284,#123285);
#102427=AXIS2_PLACEMENT_3D('',#406788,#123286,#123287);
#102428=AXIS2_PLACEMENT_3D('',#406789,#123288,#123289);
#102429=AXIS2_PLACEMENT_3D('',#406790,#123290,#123291);
#102430=AXIS2_PLACEMENT_3D('',#406803,#123292,#123293);
#102431=AXIS2_PLACEMENT_3D('',#406804,#123294,#123295);
#102432=AXIS2_PLACEMENT_3D('',#406805,#123296,#123297);
#102433=AXIS2_PLACEMENT_3D('',#406818,#123298,#123299);
#102434=AXIS2_PLACEMENT_3D('',#406831,#123300,#123301);
#102435=AXIS2_PLACEMENT_3D('',#406844,#123302,#123303);
#102436=AXIS2_PLACEMENT_3D('',#406857,#123304,#123305);
#102437=AXIS2_PLACEMENT_3D('',#406870,#123306,#123307);
#102438=AXIS2_PLACEMENT_3D('',#406871,#123308,#123309);
#102439=AXIS2_PLACEMENT_3D('',#406872,#123310,#123311);
#102440=AXIS2_PLACEMENT_3D('',#406885,#123312,#123313);
#102441=AXIS2_PLACEMENT_3D('',#406886,#123314,#123315);
#102442=AXIS2_PLACEMENT_3D('',#406896,#123317,#123318);
#102443=AXIS2_PLACEMENT_3D('',#406906,#123320,#123321);
#102444=AXIS2_PLACEMENT_3D('',#406909,#123322,#123323);
#102445=AXIS2_PLACEMENT_3D('',#406926,#123326,#123327);
#102446=AXIS2_PLACEMENT_3D('',#406976,#123328,#123329);
#102447=AXIS2_PLACEMENT_3D('',#407022,#123330,#123331);
#102448=AXIS2_PLACEMENT_3D('',#407039,#123332,#123333);
#102449=AXIS2_PLACEMENT_3D('',#407091,#123334,#123335);
#102450=AXIS2_PLACEMENT_3D('',#407092,#123336,#123337);
#102451=AXIS2_PLACEMENT_3D('',#407093,#123338,#123339);
#102452=AXIS2_PLACEMENT_3D('',#407094,#123340,#123341);
#102453=AXIS2_PLACEMENT_3D('',#407107,#123342,#123343);
#102454=AXIS2_PLACEMENT_3D('',#407108,#123344,#123345);
#102455=AXIS2_PLACEMENT_3D('',#407109,#123346,#123347);
#102456=AXIS2_PLACEMENT_3D('',#407122,#123348,#123349);
#102457=AXIS2_PLACEMENT_3D('',#407135,#123350,#123351);
#102458=AXIS2_PLACEMENT_3D('',#407148,#123352,#123353);
#102459=AXIS2_PLACEMENT_3D('',#407161,#123354,#123355);
#102460=AXIS2_PLACEMENT_3D('',#407174,#123356,#123357);
#102461=AXIS2_PLACEMENT_3D('',#407175,#123358,#123359);
#102462=AXIS2_PLACEMENT_3D('',#407176,#123360,#123361);
#102463=AXIS2_PLACEMENT_3D('',#407189,#123362,#123363);
#102464=AXIS2_PLACEMENT_3D('',#407190,#123364,#123365);
#102465=AXIS2_PLACEMENT_3D('',#407200,#123367,#123368);
#102466=AXIS2_PLACEMENT_3D('',#407210,#123370,#123371);
#102467=AXIS2_PLACEMENT_3D('',#407213,#123372,#123373);
#102468=AXIS2_PLACEMENT_3D('',#407230,#123376,#123377);
#102469=AXIS2_PLACEMENT_3D('',#407280,#123378,#123379);
#102470=AXIS2_PLACEMENT_3D('',#407326,#123380,#123381);
#102471=AXIS2_PLACEMENT_3D('',#407343,#123382,#123383);
#102472=AXIS2_PLACEMENT_3D('',#407395,#123384,#123385);
#102473=AXIS2_PLACEMENT_3D('',#407396,#123386,#123387);
#102474=AXIS2_PLACEMENT_3D('',#407397,#123388,#123389);
#102475=AXIS2_PLACEMENT_3D('',#407398,#123390,#123391);
#102476=AXIS2_PLACEMENT_3D('',#407411,#123392,#123393);
#102477=AXIS2_PLACEMENT_3D('',#407412,#123394,#123395);
#102478=AXIS2_PLACEMENT_3D('',#407413,#123396,#123397);
#102479=AXIS2_PLACEMENT_3D('',#407426,#123398,#123399);
#102480=AXIS2_PLACEMENT_3D('',#407439,#123400,#123401);
#102481=AXIS2_PLACEMENT_3D('',#407452,#123402,#123403);
#102482=AXIS2_PLACEMENT_3D('',#407465,#123404,#123405);
#102483=AXIS2_PLACEMENT_3D('',#407478,#123406,#123407);
#102484=AXIS2_PLACEMENT_3D('',#407479,#123408,#123409);
#102485=AXIS2_PLACEMENT_3D('',#407480,#123410,#123411);
#102486=AXIS2_PLACEMENT_3D('',#407493,#123412,#123413);
#102487=AXIS2_PLACEMENT_3D('',#407494,#123414,#123415);
#102488=AXIS2_PLACEMENT_3D('',#407504,#123417,#123418);
#102489=AXIS2_PLACEMENT_3D('',#407514,#123420,#123421);
#102490=AXIS2_PLACEMENT_3D('',#407517,#123422,#123423);
#102491=AXIS2_PLACEMENT_3D('',#407534,#123426,#123427);
#102492=AXIS2_PLACEMENT_3D('',#407584,#123428,#123429);
#102493=AXIS2_PLACEMENT_3D('',#407630,#123430,#123431);
#102494=AXIS2_PLACEMENT_3D('',#407647,#123432,#123433);
#102495=AXIS2_PLACEMENT_3D('',#407699,#123434,#123435);
#102496=AXIS2_PLACEMENT_3D('',#407700,#123436,#123437);
#102497=AXIS2_PLACEMENT_3D('',#407701,#123438,#123439);
#102498=AXIS2_PLACEMENT_3D('',#407702,#123440,#123441);
#102499=AXIS2_PLACEMENT_3D('',#407715,#123442,#123443);
#102500=AXIS2_PLACEMENT_3D('',#407716,#123444,#123445);
#102501=AXIS2_PLACEMENT_3D('',#407717,#123446,#123447);
#102502=AXIS2_PLACEMENT_3D('',#407730,#123448,#123449);
#102503=AXIS2_PLACEMENT_3D('',#407743,#123450,#123451);
#102504=AXIS2_PLACEMENT_3D('',#407756,#123452,#123453);
#102505=AXIS2_PLACEMENT_3D('',#407769,#123454,#123455);
#102506=AXIS2_PLACEMENT_3D('',#407782,#123456,#123457);
#102507=AXIS2_PLACEMENT_3D('',#407783,#123458,#123459);
#102508=AXIS2_PLACEMENT_3D('',#407784,#123460,#123461);
#102509=AXIS2_PLACEMENT_3D('',#407797,#123462,#123463);
#102510=AXIS2_PLACEMENT_3D('',#407798,#123464,#123465);
#102511=AXIS2_PLACEMENT_3D('',#407808,#123467,#123468);
#102512=AXIS2_PLACEMENT_3D('',#407818,#123470,#123471);
#102513=AXIS2_PLACEMENT_3D('',#407821,#123472,#123473);
#102514=AXIS2_PLACEMENT_3D('',#407838,#123476,#123477);
#102515=AXIS2_PLACEMENT_3D('',#407888,#123478,#123479);
#102516=AXIS2_PLACEMENT_3D('',#407934,#123480,#123481);
#102517=AXIS2_PLACEMENT_3D('',#407951,#123482,#123483);
#102518=AXIS2_PLACEMENT_3D('',#408003,#123484,#123485);
#102519=AXIS2_PLACEMENT_3D('',#408004,#123486,#123487);
#102520=AXIS2_PLACEMENT_3D('',#408005,#123488,#123489);
#102521=AXIS2_PLACEMENT_3D('',#408006,#123490,#123491);
#102522=AXIS2_PLACEMENT_3D('',#408019,#123492,#123493);
#102523=AXIS2_PLACEMENT_3D('',#408020,#123494,#123495);
#102524=AXIS2_PLACEMENT_3D('',#408021,#123496,#123497);
#102525=AXIS2_PLACEMENT_3D('',#408034,#123498,#123499);
#102526=AXIS2_PLACEMENT_3D('',#408047,#123500,#123501);
#102527=AXIS2_PLACEMENT_3D('',#408060,#123502,#123503);
#102528=AXIS2_PLACEMENT_3D('',#408073,#123504,#123505);
#102529=AXIS2_PLACEMENT_3D('',#408086,#123506,#123507);
#102530=AXIS2_PLACEMENT_3D('',#408087,#123508,#123509);
#102531=AXIS2_PLACEMENT_3D('',#408088,#123510,#123511);
#102532=AXIS2_PLACEMENT_3D('',#408101,#123512,#123513);
#102533=AXIS2_PLACEMENT_3D('',#408102,#123514,#123515);
#102534=AXIS2_PLACEMENT_3D('',#408112,#123517,#123518);
#102535=AXIS2_PLACEMENT_3D('',#408122,#123520,#123521);
#102536=AXIS2_PLACEMENT_3D('',#408125,#123522,#123523);
#102537=AXIS2_PLACEMENT_3D('',#408142,#123526,#123527);
#102538=AXIS2_PLACEMENT_3D('',#408192,#123528,#123529);
#102539=AXIS2_PLACEMENT_3D('',#408238,#123530,#123531);
#102540=AXIS2_PLACEMENT_3D('',#408255,#123532,#123533);
#102541=AXIS2_PLACEMENT_3D('',#408307,#123534,#123535);
#102542=AXIS2_PLACEMENT_3D('',#408308,#123536,#123537);
#102543=AXIS2_PLACEMENT_3D('',#408309,#123538,#123539);
#102544=AXIS2_PLACEMENT_3D('',#408310,#123540,#123541);
#102545=AXIS2_PLACEMENT_3D('',#408323,#123542,#123543);
#102546=AXIS2_PLACEMENT_3D('',#408324,#123544,#123545);
#102547=AXIS2_PLACEMENT_3D('',#408325,#123546,#123547);
#102548=AXIS2_PLACEMENT_3D('',#408338,#123548,#123549);
#102549=AXIS2_PLACEMENT_3D('',#408351,#123550,#123551);
#102550=AXIS2_PLACEMENT_3D('',#408364,#123552,#123553);
#102551=AXIS2_PLACEMENT_3D('',#408377,#123554,#123555);
#102552=AXIS2_PLACEMENT_3D('',#408390,#123556,#123557);
#102553=AXIS2_PLACEMENT_3D('',#408391,#123558,#123559);
#102554=AXIS2_PLACEMENT_3D('',#408392,#123560,#123561);
#102555=AXIS2_PLACEMENT_3D('',#408405,#123562,#123563);
#102556=AXIS2_PLACEMENT_3D('',#408406,#123564,#123565);
#102557=AXIS2_PLACEMENT_3D('',#408416,#123567,#123568);
#102558=AXIS2_PLACEMENT_3D('',#408426,#123570,#123571);
#102559=AXIS2_PLACEMENT_3D('',#408429,#123572,#123573);
#102560=AXIS2_PLACEMENT_3D('',#408446,#123576,#123577);
#102561=AXIS2_PLACEMENT_3D('',#408496,#123578,#123579);
#102562=AXIS2_PLACEMENT_3D('',#408542,#123580,#123581);
#102563=AXIS2_PLACEMENT_3D('',#408559,#123582,#123583);
#102564=AXIS2_PLACEMENT_3D('',#408611,#123584,#123585);
#102565=AXIS2_PLACEMENT_3D('',#408612,#123586,#123587);
#102566=AXIS2_PLACEMENT_3D('',#408613,#123588,#123589);
#102567=AXIS2_PLACEMENT_3D('',#408614,#123590,#123591);
#102568=AXIS2_PLACEMENT_3D('',#408627,#123592,#123593);
#102569=AXIS2_PLACEMENT_3D('',#408628,#123594,#123595);
#102570=AXIS2_PLACEMENT_3D('',#408629,#123596,#123597);
#102571=AXIS2_PLACEMENT_3D('',#408642,#123598,#123599);
#102572=AXIS2_PLACEMENT_3D('',#408655,#123600,#123601);
#102573=AXIS2_PLACEMENT_3D('',#408668,#123602,#123603);
#102574=AXIS2_PLACEMENT_3D('',#408681,#123604,#123605);
#102575=AXIS2_PLACEMENT_3D('',#408694,#123606,#123607);
#102576=AXIS2_PLACEMENT_3D('',#408695,#123608,#123609);
#102577=AXIS2_PLACEMENT_3D('',#408696,#123610,#123611);
#102578=AXIS2_PLACEMENT_3D('',#408709,#123612,#123613);
#102579=AXIS2_PLACEMENT_3D('',#408710,#123614,#123615);
#102580=AXIS2_PLACEMENT_3D('',#408720,#123617,#123618);
#102581=AXIS2_PLACEMENT_3D('',#408730,#123620,#123621);
#102582=AXIS2_PLACEMENT_3D('',#408733,#123622,#123623);
#102583=AXIS2_PLACEMENT_3D('',#408750,#123626,#123627);
#102584=AXIS2_PLACEMENT_3D('',#408800,#123628,#123629);
#102585=AXIS2_PLACEMENT_3D('',#408846,#123630,#123631);
#102586=AXIS2_PLACEMENT_3D('',#408863,#123632,#123633);
#102587=AXIS2_PLACEMENT_3D('',#408915,#123634,#123635);
#102588=AXIS2_PLACEMENT_3D('',#408916,#123636,#123637);
#102589=AXIS2_PLACEMENT_3D('',#408917,#123638,#123639);
#102590=AXIS2_PLACEMENT_3D('',#408918,#123640,#123641);
#102591=AXIS2_PLACEMENT_3D('',#408931,#123642,#123643);
#102592=AXIS2_PLACEMENT_3D('',#408932,#123644,#123645);
#102593=AXIS2_PLACEMENT_3D('',#408933,#123646,#123647);
#102594=AXIS2_PLACEMENT_3D('',#408946,#123648,#123649);
#102595=AXIS2_PLACEMENT_3D('',#408959,#123650,#123651);
#102596=AXIS2_PLACEMENT_3D('',#408972,#123652,#123653);
#102597=AXIS2_PLACEMENT_3D('',#408985,#123654,#123655);
#102598=AXIS2_PLACEMENT_3D('',#408998,#123656,#123657);
#102599=AXIS2_PLACEMENT_3D('',#408999,#123658,#123659);
#102600=AXIS2_PLACEMENT_3D('',#409000,#123660,#123661);
#102601=AXIS2_PLACEMENT_3D('',#409013,#123662,#123663);
#102602=AXIS2_PLACEMENT_3D('',#409014,#123664,#123665);
#102603=AXIS2_PLACEMENT_3D('',#409024,#123667,#123668);
#102604=AXIS2_PLACEMENT_3D('',#409034,#123670,#123671);
#102605=AXIS2_PLACEMENT_3D('',#409037,#123672,#123673);
#102606=AXIS2_PLACEMENT_3D('',#409054,#123676,#123677);
#102607=AXIS2_PLACEMENT_3D('',#409104,#123678,#123679);
#102608=AXIS2_PLACEMENT_3D('',#409150,#123680,#123681);
#102609=AXIS2_PLACEMENT_3D('',#409167,#123682,#123683);
#102610=AXIS2_PLACEMENT_3D('',#409219,#123684,#123685);
#102611=AXIS2_PLACEMENT_3D('',#409220,#123686,#123687);
#102612=AXIS2_PLACEMENT_3D('',#409221,#123688,#123689);
#102613=AXIS2_PLACEMENT_3D('',#409222,#123690,#123691);
#102614=AXIS2_PLACEMENT_3D('',#409235,#123692,#123693);
#102615=AXIS2_PLACEMENT_3D('',#409236,#123694,#123695);
#102616=AXIS2_PLACEMENT_3D('',#409237,#123696,#123697);
#102617=AXIS2_PLACEMENT_3D('',#409250,#123698,#123699);
#102618=AXIS2_PLACEMENT_3D('',#409263,#123700,#123701);
#102619=AXIS2_PLACEMENT_3D('',#409276,#123702,#123703);
#102620=AXIS2_PLACEMENT_3D('',#409289,#123704,#123705);
#102621=AXIS2_PLACEMENT_3D('',#409302,#123706,#123707);
#102622=AXIS2_PLACEMENT_3D('',#409303,#123708,#123709);
#102623=AXIS2_PLACEMENT_3D('',#409304,#123710,#123711);
#102624=AXIS2_PLACEMENT_3D('',#409317,#123712,#123713);
#102625=AXIS2_PLACEMENT_3D('',#409318,#123714,#123715);
#102626=AXIS2_PLACEMENT_3D('',#409328,#123717,#123718);
#102627=AXIS2_PLACEMENT_3D('',#409338,#123720,#123721);
#102628=AXIS2_PLACEMENT_3D('',#409341,#123722,#123723);
#102629=AXIS2_PLACEMENT_3D('',#409358,#123726,#123727);
#102630=AXIS2_PLACEMENT_3D('',#409408,#123728,#123729);
#102631=AXIS2_PLACEMENT_3D('',#409454,#123730,#123731);
#102632=AXIS2_PLACEMENT_3D('',#409471,#123732,#123733);
#102633=AXIS2_PLACEMENT_3D('',#409523,#123734,#123735);
#102634=AXIS2_PLACEMENT_3D('',#409524,#123736,#123737);
#102635=AXIS2_PLACEMENT_3D('',#409525,#123738,#123739);
#102636=AXIS2_PLACEMENT_3D('',#409526,#123740,#123741);
#102637=AXIS2_PLACEMENT_3D('',#409539,#123742,#123743);
#102638=AXIS2_PLACEMENT_3D('',#409540,#123744,#123745);
#102639=AXIS2_PLACEMENT_3D('',#409541,#123746,#123747);
#102640=AXIS2_PLACEMENT_3D('',#409554,#123748,#123749);
#102641=AXIS2_PLACEMENT_3D('',#409567,#123750,#123751);
#102642=AXIS2_PLACEMENT_3D('',#409580,#123752,#123753);
#102643=AXIS2_PLACEMENT_3D('',#409593,#123754,#123755);
#102644=AXIS2_PLACEMENT_3D('',#409606,#123756,#123757);
#102645=AXIS2_PLACEMENT_3D('',#409607,#123758,#123759);
#102646=AXIS2_PLACEMENT_3D('',#409608,#123760,#123761);
#102647=AXIS2_PLACEMENT_3D('',#409621,#123762,#123763);
#116568=DIRECTION('axis',(0.,0.,1.));
#116569=DIRECTION('refdir',(1.,0.,0.));
#116570=DIRECTION('center_axis',(0.,0.,1.));
#116571=DIRECTION('ref_axis',(-5.9042332696092E-17,1.,0.));
#116572=DIRECTION('',(0.,0.,-1.));
#116573=DIRECTION('center_axis',(0.,0.,1.));
#116574=DIRECTION('ref_axis',(1.,0.,0.));
#116575=DIRECTION('center_axis',(0.,0.,1.));
#116576=DIRECTION('ref_axis',(-5.9042332696092E-17,1.,0.));
#116577=DIRECTION('',(0.,0.,-1.));
#116578=DIRECTION('center_axis',(0.,0.,1.));
#116579=DIRECTION('ref_axis',(-5.9042332696092E-17,1.,0.));
#116580=DIRECTION('',(0.,0.,-1.));
#116581=DIRECTION('center_axis',(0.,0.,1.));
#116582=DIRECTION('ref_axis',(-5.9042332696092E-17,1.,0.));
#116583=DIRECTION('',(0.,0.,-1.));
#116584=DIRECTION('center_axis',(0.,0.,1.));
#116585=DIRECTION('ref_axis',(-5.9042332696092E-17,1.,0.));
#116586=DIRECTION('',(0.,0.,-1.));
#116587=DIRECTION('center_axis',(0.,0.,1.));
#116588=DIRECTION('ref_axis',(-5.9042332696092E-17,1.,0.));
#116589=DIRECTION('',(0.,0.,-1.));
#116590=DIRECTION('center_axis',(0.,0.,1.));
#116591=DIRECTION('ref_axis',(-5.9042332696092E-17,1.,0.));
#116592=DIRECTION('',(0.,0.,-1.));
#116593=DIRECTION('center_axis',(0.,0.,1.));
#116594=DIRECTION('ref_axis',(-5.9042332696092E-17,1.,0.));
#116595=DIRECTION('',(0.,0.,-1.));
#116596=DIRECTION('center_axis',(0.,0.,1.));
#116597=DIRECTION('ref_axis',(-5.9042332696092E-17,1.,0.));
#116598=DIRECTION('',(0.,0.,-1.));
#116599=DIRECTION('center_axis',(0.,0.,1.));
#116600=DIRECTION('ref_axis',(-5.9042332696092E-17,1.,0.));
#116601=DIRECTION('',(0.,0.,-1.));
#116602=DIRECTION('center_axis',(0.,0.,1.));
#116603=DIRECTION('ref_axis',(-5.9042332696092E-17,1.,0.));
#116604=DIRECTION('',(0.,0.,-1.));
#116605=DIRECTION('center_axis',(0.,0.,1.));
#116606=DIRECTION('ref_axis',(-5.9042332696092E-17,1.,0.));
#116607=DIRECTION('',(0.,0.,-1.));
#116608=DIRECTION('center_axis',(0.,0.,1.));
#116609=DIRECTION('ref_axis',(-5.9042332696092E-17,1.,0.));
#116610=DIRECTION('',(0.,0.,-1.));
#116611=DIRECTION('center_axis',(0.,0.,1.));
#116612=DIRECTION('ref_axis',(-5.9042332696092E-17,1.,0.));
#116613=DIRECTION('',(0.,0.,-1.));
#116614=DIRECTION('center_axis',(0.,0.,1.));
#116615=DIRECTION('ref_axis',(-5.9042332696092E-17,1.,0.));
#116616=DIRECTION('',(0.,0.,-1.));
#116617=DIRECTION('center_axis',(0.,0.,1.));
#116618=DIRECTION('ref_axis',(-5.9042332696092E-17,1.,0.));
#116619=DIRECTION('',(0.,0.,-1.));
#116620=DIRECTION('center_axis',(0.,0.,1.));
#116621=DIRECTION('ref_axis',(-5.9042332696092E-17,1.,0.));
#116622=DIRECTION('',(0.,0.,-1.));
#116623=DIRECTION('center_axis',(0.,0.,1.));
#116624=DIRECTION('ref_axis',(-5.9042332696092E-17,1.,0.));
#116625=DIRECTION('',(0.,0.,-1.));
#116626=DIRECTION('center_axis',(0.,0.,1.));
#116627=DIRECTION('ref_axis',(-5.9042332696092E-17,1.,0.));
#116628=DIRECTION('',(0.,0.,-1.));
#116629=DIRECTION('center_axis',(0.,0.,1.));
#116630=DIRECTION('ref_axis',(-5.9042332696092E-17,1.,0.));
#116631=DIRECTION('',(0.,0.,-1.));
#116632=DIRECTION('center_axis',(0.,0.,1.));
#116633=DIRECTION('ref_axis',(-5.9042332696092E-17,1.,0.));
#116634=DIRECTION('',(0.,0.,-1.));
#116635=DIRECTION('center_axis',(0.,0.,1.));
#116636=DIRECTION('ref_axis',(-5.9042332696092E-17,1.,0.));
#116637=DIRECTION('',(0.,0.,-1.));
#116638=DIRECTION('center_axis',(0.,0.,1.));
#116639=DIRECTION('ref_axis',(-5.9042332696092E-17,1.,0.));
#116640=DIRECTION('',(0.,0.,-1.));
#116641=DIRECTION('center_axis',(0.,0.,1.));
#116642=DIRECTION('ref_axis',(-5.9042332696092E-17,1.,0.));
#116643=DIRECTION('',(0.,0.,-1.));
#116644=DIRECTION('center_axis',(0.,0.,1.));
#116645=DIRECTION('ref_axis',(-5.9042332696092E-17,1.,0.));
#116646=DIRECTION('',(0.,0.,-1.));
#116647=DIRECTION('center_axis',(0.,0.,1.));
#116648=DIRECTION('ref_axis',(-5.9042332696092E-17,1.,0.));
#116649=DIRECTION('',(0.,0.,-1.));
#116650=DIRECTION('center_axis',(0.,0.,1.));
#116651=DIRECTION('ref_axis',(-5.9042332696092E-17,1.,0.));
#116652=DIRECTION('',(0.,0.,-1.));
#116653=DIRECTION('center_axis',(0.,0.,1.));
#116654=DIRECTION('ref_axis',(-5.9042332696092E-17,1.,0.));
#116655=DIRECTION('',(0.,0.,-1.));
#116656=DIRECTION('center_axis',(0.,0.,1.));
#116657=DIRECTION('ref_axis',(-5.9042332696092E-17,1.,0.));
#116658=DIRECTION('',(0.,0.,-1.));
#116659=DIRECTION('center_axis',(0.,1.19813586852189E-16,-1.));
#116660=DIRECTION('ref_axis',(0.,1.,1.19813586852189E-16));
#116661=DIRECTION('',(0.,-1.19813586852189E-16,1.));
#116662=DIRECTION('center_axis',(0.,1.19813586852189E-16,-1.));
#116663=DIRECTION('ref_axis',(0.,1.,1.19813586852189E-16));
#116664=DIRECTION('',(0.,-1.19813586852189E-16,1.));
#116665=DIRECTION('center_axis',(0.,1.19813586852189E-16,-1.));
#116666=DIRECTION('ref_axis',(0.,1.,1.19813586852189E-16));
#116667=DIRECTION('center_axis',(0.,1.19813586852189E-16,-1.));
#116668=DIRECTION('ref_axis',(0.,1.,1.19813586852189E-16));
#116669=DIRECTION('center_axis',(0.,1.19813586852189E-16,-1.));
#116670=DIRECTION('ref_axis',(0.,1.,1.19813586852189E-16));
#116671=DIRECTION('',(0.,-1.19813586852189E-16,1.));
#116672=DIRECTION('center_axis',(0.,1.19813586852189E-16,-1.));
#116673=DIRECTION('ref_axis',(0.,1.,1.19813586852189E-16));
#116674=DIRECTION('',(0.,-1.19813586852189E-16,1.));
#116675=DIRECTION('center_axis',(0.,1.19813586852189E-16,-1.));
#116676=DIRECTION('ref_axis',(0.,1.,1.19813586852189E-16));
#116677=DIRECTION('',(0.,-1.19813586852189E-16,1.));
#116678=DIRECTION('center_axis',(0.,1.19813586852189E-16,-1.));
#116679=DIRECTION('ref_axis',(0.,1.,1.19813586852189E-16));
#116680=DIRECTION('',(0.,-1.19813586852189E-16,1.));
#116681=DIRECTION('center_axis',(0.,1.19813586852189E-16,-1.));
#116682=DIRECTION('ref_axis',(0.,1.,1.19813586852189E-16));
#116683=DIRECTION('',(0.,-1.19813586852189E-16,1.));
#116684=DIRECTION('center_axis',(0.,1.19813586852189E-16,-1.));
#116685=DIRECTION('ref_axis',(0.,1.,1.19813586852189E-16));
#116686=DIRECTION('',(0.,-1.19813586852189E-16,1.));
#116687=DIRECTION('center_axis',(0.,1.19813586852189E-16,-1.));
#116688=DIRECTION('ref_axis',(0.,1.,1.19813586852189E-16));
#116689=DIRECTION('',(0.,-1.19813586852189E-16,1.));
#116690=DIRECTION('center_axis',(0.,1.19813586852189E-16,-1.));
#116691=DIRECTION('ref_axis',(0.,1.,1.19813586852189E-16));
#116692=DIRECTION('',(0.,-1.19813586852189E-16,1.));
#116693=DIRECTION('center_axis',(0.,1.19813586852189E-16,-1.));
#116694=DIRECTION('ref_axis',(0.,1.,1.19813586852189E-16));
#116695=DIRECTION('',(0.,-1.19813586852189E-16,1.));
#116696=DIRECTION('center_axis',(0.,1.19813586852189E-16,-1.));
#116697=DIRECTION('ref_axis',(0.,1.,1.19813586852189E-16));
#116698=DIRECTION('',(0.,-1.19813586852189E-16,1.));
#116699=DIRECTION('center_axis',(0.,1.19813586852189E-16,-1.));
#116700=DIRECTION('ref_axis',(0.,1.,1.19813586852189E-16));
#116701=DIRECTION('',(0.,-1.19813586852189E-16,1.));
#116702=DIRECTION('center_axis',(0.,1.19813586852189E-16,-1.));
#116703=DIRECTION('ref_axis',(0.,1.,1.19813586852189E-16));
#116704=DIRECTION('',(0.,-1.19813586852189E-16,1.));
#116705=DIRECTION('center_axis',(0.,1.19813586852189E-16,-1.));
#116706=DIRECTION('ref_axis',(0.,1.,1.19813586852189E-16));
#116707=DIRECTION('',(0.,-1.19813586852189E-16,1.));
#116708=DIRECTION('center_axis',(0.,1.19813586852189E-16,-1.));
#116709=DIRECTION('ref_axis',(0.,1.,1.19813586852189E-16));
#116710=DIRECTION('',(0.,-1.19813586852189E-16,1.));
#116711=DIRECTION('center_axis',(0.,1.19813586852189E-16,-1.));
#116712=DIRECTION('ref_axis',(0.,1.,1.19813586852189E-16));
#116713=DIRECTION('',(0.,-1.19813586852189E-16,1.));
#116714=DIRECTION('center_axis',(0.,1.19813586852189E-16,-1.));
#116715=DIRECTION('ref_axis',(0.,1.,1.19813586852189E-16));
#116716=DIRECTION('',(0.,-1.19813586852189E-16,1.));
#116717=DIRECTION('center_axis',(0.,1.19813586852189E-16,-1.));
#116718=DIRECTION('ref_axis',(0.,1.,1.19813586852189E-16));
#116719=DIRECTION('',(0.,-1.19813586852189E-16,1.));
#116720=DIRECTION('center_axis',(0.,1.19813586852189E-16,-1.));
#116721=DIRECTION('ref_axis',(0.,1.,1.19813586852189E-16));
#116722=DIRECTION('',(0.,-1.19813586852189E-16,1.));
#116723=DIRECTION('center_axis',(0.,1.19813586852189E-16,-1.));
#116724=DIRECTION('ref_axis',(0.,1.,1.19813586852189E-16));
#116725=DIRECTION('',(0.,-1.19813586852189E-16,1.));
#116726=DIRECTION('center_axis',(0.,1.19813586852189E-16,-1.));
#116727=DIRECTION('ref_axis',(0.,1.,1.19813586852189E-16));
#116728=DIRECTION('',(0.,-1.19813586852189E-16,1.));
#116729=DIRECTION('center_axis',(0.,1.19813586852189E-16,-1.));
#116730=DIRECTION('ref_axis',(0.,1.,1.19813586852189E-16));
#116731=DIRECTION('',(0.,-1.19813586852189E-16,1.));
#116732=DIRECTION('center_axis',(0.,1.19813586852189E-16,-1.));
#116733=DIRECTION('ref_axis',(0.,1.,1.19813586852189E-16));
#116734=DIRECTION('',(0.,-1.19813586852189E-16,1.));
#116735=DIRECTION('center_axis',(0.,1.19813586852189E-16,-1.));
#116736=DIRECTION('ref_axis',(0.,1.,1.19813586852189E-16));
#116737=DIRECTION('',(0.,-1.19813586852189E-16,1.));
#116738=DIRECTION('center_axis',(0.,1.19813586852189E-16,-1.));
#116739=DIRECTION('ref_axis',(0.,1.,1.19813586852189E-16));
#116740=DIRECTION('',(0.,-1.19813586852189E-16,1.));
#116741=DIRECTION('center_axis',(0.,1.19813586852189E-16,-1.));
#116742=DIRECTION('ref_axis',(0.,1.,1.19813586852189E-16));
#116743=DIRECTION('',(0.,-1.19813586852189E-16,1.));
#116744=DIRECTION('center_axis',(0.,1.19813586852189E-16,-1.));
#116745=DIRECTION('ref_axis',(0.,1.,1.19813586852189E-16));
#116746=DIRECTION('',(0.,-1.19813586852189E-16,1.));
#116747=DIRECTION('center_axis',(0.,1.19813586852189E-16,-1.));
#116748=DIRECTION('ref_axis',(0.,1.,1.19813586852189E-16));
#116749=DIRECTION('',(0.,-1.19813586852189E-16,1.));
#116750=DIRECTION('center_axis',(0.,-1.19813586852189E-16,1.));
#116751=DIRECTION('ref_axis',(0.,-1.,-1.19813586852189E-16));
#116752=DIRECTION('',(8.65956056235489E-17,-0.707106781186543,-0.707106781186552));
#116753=DIRECTION('center_axis',(0.,0.,-1.));
#116754=DIRECTION('ref_axis',(0.989119496180713,-0.147114317030034,0.));
#116755=DIRECTION('center_axis',(0.,0.,1.));
#116756=DIRECTION('ref_axis',(1.,0.,0.));
#116757=DIRECTION('',(0.707106781186551,8.65956056235497E-17,-0.707106781186544));
#116758=DIRECTION('center_axis',(0.,0.,1.));
#116759=DIRECTION('ref_axis',(1.,0.,0.));
#116760=DIRECTION('center_axis',(0.,0.,1.));
#116761=DIRECTION('ref_axis',(1.,0.,0.));
#116762=DIRECTION('center_axis',(0.,0.,1.));
#116763=DIRECTION('ref_axis',(1.,0.,0.));
#116764=DIRECTION('center_axis',(0.,0.,1.));
#116765=DIRECTION('ref_axis',(1.,0.,0.));
#116766=DIRECTION('center_axis',(0.,-1.19813586852189E-16,1.));
#116767=DIRECTION('ref_axis',(0.,-1.,-1.19813586852189E-16));
#116768=DIRECTION('center_axis',(0.,1.19813586852189E-16,-1.));
#116769=DIRECTION('ref_axis',(0.,1.,1.19813586852189E-16));
#116770=DIRECTION('center_axis',(0.,1.19813586852189E-16,-1.));
#116771=DIRECTION('ref_axis',(0.,1.,0.));
#116772=DIRECTION('center_axis',(1.,-1.22464679914735E-16,-1.46729325632897E-32));
#116773=DIRECTION('ref_axis',(-1.22464679914735E-16,-1.,0.));
#116774=DIRECTION('center_axis',(0.,1.19813586852189E-16,-1.));
#116775=DIRECTION('ref_axis',(0.,1.,1.19813586852189E-16));
#116776=DIRECTION('center_axis',(0.,0.,1.));
#116777=DIRECTION('ref_axis',(1.,0.,0.));
#116778=DIRECTION('',(-0.86602540378444,-1.06057523872491E-16,0.499999999999998));
#116779=DIRECTION('center_axis',(0.,0.,-1.));
#116780=DIRECTION('ref_axis',(-1.,0.,0.));
#116781=DIRECTION('center_axis',(0.,0.,-1.));
#116782=DIRECTION('ref_axis',(-1.,0.,0.));
#116783=DIRECTION('center_axis',(0.,0.,-1.));
#116784=DIRECTION('ref_axis',(-1.,0.,0.));
#116785=DIRECTION('center_axis',(0.,0.,1.));
#116786=DIRECTION('ref_axis',(1.,0.,0.));
#116787=DIRECTION('center_axis',(0.,0.,-1.));
#116788=DIRECTION('ref_axis',(-1.,0.,0.));
#116789=DIRECTION('center_axis',(0.,0.,-1.));
#116790=DIRECTION('ref_axis',(-1.,0.,0.));
#116791=DIRECTION('center_axis',(0.,0.,1.));
#116792=DIRECTION('ref_axis',(1.,0.,0.));
#116793=DIRECTION('center_axis',(0.,0.,1.));
#116794=DIRECTION('ref_axis',(1.,0.,0.));
#116795=DIRECTION('center_axis',(0.,0.,1.));
#116796=DIRECTION('ref_axis',(1.,0.,0.));
#116797=DIRECTION('center_axis',(0.,0.,1.));
#116798=DIRECTION('ref_axis',(1.,0.,0.));
#116799=DIRECTION('center_axis',(1.22464679914735E-16,-1.,0.));
#116800=DIRECTION('ref_axis',(-1.,-1.22464679914735E-16,0.));
#116801=DIRECTION('center_axis',(0.,0.,1.));
#116802=DIRECTION('ref_axis',(1.,0.,0.));
#116803=DIRECTION('center_axis',(0.,0.,1.));
#116804=DIRECTION('ref_axis',(1.,0.,0.));
#116805=DIRECTION('center_axis',(0.,0.,1.));
#116806=DIRECTION('ref_axis',(1.,0.,0.));
#116807=DIRECTION('',(0.707106781186541,8.65956056235485E-17,-0.707106781186554));
#116808=DIRECTION('center_axis',(0.,0.,1.));
#116809=DIRECTION('ref_axis',(1.,0.,0.));
#116810=DIRECTION('center_axis',(0.,0.,1.));
#116811=DIRECTION('ref_axis',(1.,0.,0.));
#116812=DIRECTION('center_axis',(1.22464679914735E-16,-1.,0.));
#116813=DIRECTION('ref_axis',(-1.,-1.22464679914735E-16,0.));
#116814=DIRECTION('center_axis',(0.,0.,-1.));
#116815=DIRECTION('ref_axis',(-1.,0.,0.));
#116816=DIRECTION('center_axis',(0.,0.,1.));
#116817=DIRECTION('ref_axis',(1.,0.,0.));
#116818=DIRECTION('center_axis',(0.708643409675333,0.0227248148575671,-0.705200752065259));
#116819=DIRECTION('ref_axis',(0.704838421157334,0.0226031142521084,0.709007686338126));
#116820=DIRECTION('center_axis',(0.,0.,1.));
#116821=DIRECTION('ref_axis',(1.,0.,0.));
#116822=DIRECTION('center_axis',(0.705731441901385,0.068081063433995,-0.705200752065317));
#116823=DIRECTION('ref_axis',(0.701942068525029,0.067715826424425,0.709007686338069));
#116824=DIRECTION('center_axis',(0.,0.,1.));
#116825=DIRECTION('ref_axis',(1.,0.,0.));
#116826=DIRECTION('center_axis',(0.699919472253828,0.113157552317439,-0.705200752065289));
#116827=DIRECTION('ref_axis',(0.696161285367033,0.112550279740303,0.709007686338096));
#116828=DIRECTION('center_axis',(0.,0.,1.));
#116829=DIRECTION('ref_axis',(1.,0.,0.));
#116830=DIRECTION('center_axis',(0.691231383362495,0.15776905254617,-0.705200752065293));
#116831=DIRECTION('ref_axis',(0.687519826161253,0.156922239815477,0.709007686338092));
#116832=DIRECTION('center_axis',(0.,0.,1.));
#116833=DIRECTION('ref_axis',(1.,0.,0.));
#116834=DIRECTION('center_axis',(0.679702876448271,0.201732245896655,-0.705200752065281));
#116835=DIRECTION('ref_axis',(0.676053200517231,0.200649372747332,0.709007686338104));
#116836=DIRECTION('center_axis',(0.,0.,1.));
#116837=DIRECTION('ref_axis',(1.,0.,0.));
#116838=DIRECTION('center_axis',(0.665381324618886,0.244866478177282,-0.705200752065305));
#116839=DIRECTION('ref_axis',(0.661808527259506,0.243551994366965,0.709007686338081));
#116840=DIRECTION('center_axis',(0.,0.,1.));
#116841=DIRECTION('ref_axis',(1.,0.,0.));
#116842=DIRECTION('center_axis',(0.648325578202831,0.286994501575423,-0.705200752065282));
#116843=DIRECTION('ref_axis',(0.64484434080553,0.28545380860057,0.709007686338103));
#116844=DIRECTION('center_axis',(0.,0.,1.));
#116845=DIRECTION('ref_axis',(1.,0.,0.));
#116846=DIRECTION('center_axis',(0.628605722920504,0.327943203006452,-0.705200752065297));
#116847=DIRECTION('ref_axis',(0.625230350636733,0.326182631904548,0.709007686338089));
#116848=DIRECTION('center_axis',(0.,0.,1.));
#116849=DIRECTION('ref_axis',(1.,0.,0.));
#116850=DIRECTION('center_axis',(0.606302791887208,0.367544315472732,-0.705200752065295));
#116851=DIRECTION('ref_axis',(0.603047154845681,0.365571100808089,0.70900768633809));
#116852=DIRECTION('center_axis',(0.,0.,1.));
#116853=DIRECTION('ref_axis',(1.,0.,0.));
#116854=DIRECTION('center_axis',(0.581508432630507,0.40563510950871,-0.705200752065302));
#116855=DIRECTION('ref_axis',(0.578385908942004,0.403457359643929,0.709007686338083));
#116856=DIRECTION('center_axis',(0.,0.,1.));
#116857=DIRECTION('ref_axis',(1.,0.,0.));
#116858=DIRECTION('center_axis',(0.55432453049096,0.442059061871265,-0.705200752065307));
#116859=DIRECTION('ref_axis',(0.551347951275109,0.439685725647609,0.709007686338079));
#116860=DIRECTION('center_axis',(0.,0.,1.));
#116861=DIRECTION('ref_axis',(1.,0.,0.));
#116862=DIRECTION('center_axis',(0.524862789953404,0.47666649872725,-0.705200752065278));
#116863=DIRECTION('ref_axis',(0.522044386613039,0.474107328691827,0.709007686338108));
#116864=DIRECTION('center_axis',(0.,0.,1.));
#116865=DIRECTION('ref_axis',(1.,0.,0.));
#116866=DIRECTION('center_axis',(0.49324427562918,0.509315210695285,-0.705200752065299));
#116867=DIRECTION('ref_axis',(0.490595629587655,0.506580723027443,0.709007686338087));
#116868=DIRECTION('center_axis',(0.,0.,1.));
#116869=DIRECTION('ref_axis',(1.,0.,0.));
#116870=DIRECTION('center_axis',(0.459598914775843,0.53987103721482,-0.705200752065298));
#116871=DIRECTION('ref_axis',(0.457130909888052,0.536972468510662,0.709007686338087));
#116872=DIRECTION('center_axis',(0.,0.,1.));
#116873=DIRECTION('ref_axis',(1.,0.,0.));
#116874=DIRECTION('center_axis',(0.424064963398038,0.568208417840459,-0.705200752065299));
#116875=DIRECTION('ref_axis',(0.421787741225521,0.565157678940477,0.709007686338086));
#116876=DIRECTION('center_axis',(0.,0.,1.));
#116877=DIRECTION('ref_axis',(1.,0.,0.));
#116878=DIRECTION('center_axis',(0.386788438123989,0.594210908196879,-0.705200752065287));
#116879=DIRECTION('ref_axis',(0.384711356260997,0.591020535241645,0.709007686338099));
#116880=DIRECTION('center_axis',(0.,0.,1.));
#116881=DIRECTION('ref_axis',(1.,0.,0.));
#116882=DIRECTION('center_axis',(0.347922516191844,0.617771658473695,-0.705200752065251));
#116883=DIRECTION('ref_axis',(0.346054109813753,0.614454761389687,0.709007686338133));
#116884=DIRECTION('center_axis',(0.,0.,1.));
#116885=DIRECTION('ref_axis',(1.,0.,0.));
#116886=DIRECTION('center_axis',(0.307626906011472,0.638793852494177,-0.705200752065294));
#116887=DIRECTION('ref_axis',(0.305974852800091,0.635364061123597,0.709007686338091));
#116888=DIRECTION('center_axis',(0.,0.,1.));
#116889=DIRECTION('ref_axis',(1.,0.,0.));
#116890=DIRECTION('center_axis',(0.266067190888551,0.657191105553966,-0.705200752065277));
#116891=DIRECTION('ref_axis',(0.264638279485051,0.653662513644981,0.709007686338108));
#116892=DIRECTION('center_axis',(0.,0.,1.));
#116893=DIRECTION('ref_axis',(1.,0.,0.));
#116894=DIRECTION('center_axis',(0.223414148607074,0.672887819393937,-0.705200752065289));
#116895=DIRECTION('ref_axis',(0.22221425071527,0.669274926687495,0.709007686338096));
#116896=DIRECTION('center_axis',(0.,0.,1.));
#116897=DIRECTION('ref_axis',(1.,0.,0.));
#116898=DIRECTION('center_axis',(0.17984304966674,0.685819492850107,-0.705200752065246));
#116899=DIRECTION('ref_axis',(0.17887709592441,0.682137145497215,0.709007686338139));
#116900=DIRECTION('center_axis',(0.,0.,1.));
#116901=DIRECTION('ref_axis',(1.,0.,0.));
#116902=DIRECTION('center_axis',(0.135532937059139,0.695932986902273,-0.705200752065257));
#116903=DIRECTION('ref_axis',(0.134804896777401,0.692196316458192,0.709007686338127));
#116904=DIRECTION('center_axis',(0.,0.,1.));
#116905=DIRECTION('ref_axis',(1.,0.,0.));
#116906=DIRECTION('center_axis',(0.0906658905414403,0.703186743034099,-0.705200752065271));
#116907=DIRECTION('ref_axis',(0.0901787553937343,0.699411104279244,0.709007686338114));
#116908=DIRECTION('center_axis',(0.,0.,1.));
#116909=DIRECTION('ref_axis',(1.,0.,0.));
#116910=DIRECTION('center_axis',(0.0454262784316856,0.70755095400576,-0.705200752065244));
#116911=DIRECTION('ref_axis',(0.0451820501609615,0.703751861849536,0.709007686338141));
#116912=DIRECTION('center_axis',(0.,0.,1.));
#116913=DIRECTION('ref_axis',(1.,0.,0.));
#116914=DIRECTION('center_axis',(0.,0.709007686338145,-0.705200752065276));
#116915=DIRECTION('ref_axis',(-3.17807183472368E-7,0.70520075206524,0.709007686338109));
#116916=DIRECTION('center_axis',(0.,0.,1.));
#116917=DIRECTION('ref_axis',(1.,0.,0.));
#116918=DIRECTION('center_axis',(-0.0454262784316862,0.707550954005719,
-0.705200752065285));
#116919=DIRECTION('ref_axis',(-0.0451826844694947,0.703751821125619,0.7090076863381));
#116920=DIRECTION('center_axis',(0.,0.,1.));
#116921=DIRECTION('ref_axis',(1.,0.,0.));
#116922=DIRECTION('center_axis',(-0.0906658905414509,0.70318674303409,-0.705200752065278));
#116923=DIRECTION('ref_axis',(-0.0901793857895431,0.699411022998713,0.709007686338107));
#116924=DIRECTION('center_axis',(0.,0.,1.));
#116925=DIRECTION('ref_axis',(1.,0.,0.));
#116926=DIRECTION('center_axis',(-0.135532937059151,0.695932986902274,-0.705200752065254));
#116927=DIRECTION('ref_axis',(-0.134805520670624,0.692196194954994,0.709007686338131));
#116928=DIRECTION('center_axis',(0.,0.,1.));
#116929=DIRECTION('ref_axis',(1.,0.,0.));
#116930=DIRECTION('center_axis',(-0.179843049666727,0.685819492850053,-0.705200752065302));
#116931=DIRECTION('ref_axis',(-0.178877710751454,0.682136984270636,0.709007686338083));
#116932=DIRECTION('center_axis',(0.,0.,1.));
#116933=DIRECTION('ref_axis',(1.,0.,0.));
#116934=DIRECTION('center_axis',(-0.223414148607083,0.672887819393958,-0.705200752065266));
#116935=DIRECTION('ref_axis',(-0.222214853948597,0.669274726400206,0.709007686338119));
#116936=DIRECTION('center_axis',(0.,0.,1.));
#116937=DIRECTION('ref_axis',(1.,0.,0.));
#116938=DIRECTION('center_axis',(-0.266067190888595,0.657191105553951,-0.705200752065274));
#116939=DIRECTION('ref_axis',(-0.264638868646668,0.653662275119875,0.709007686338111));
#116940=DIRECTION('center_axis',(0.,0.,1.));
#116941=DIRECTION('ref_axis',(1.,0.,0.));
#116942=DIRECTION('center_axis',(-0.307626906011484,0.638793852494172,-0.705200752065293));
#116943=DIRECTION('ref_axis',(-0.305975425468794,0.635363785340884,0.709007686338092));
#116944=DIRECTION('center_axis',(0.,0.,1.));
#116945=DIRECTION('ref_axis',(1.,0.,0.));
#116946=DIRECTION('center_axis',(-0.347922516191818,0.61777165847369,-0.705200752065269));
#116947=DIRECTION('ref_axis',(-0.346054663636128,0.614454449482756,0.709007686338117));
#116948=DIRECTION('center_axis',(0.,0.,1.));
#116949=DIRECTION('ref_axis',(1.,0.,0.));
#116950=DIRECTION('center_axis',(-0.386788438124013,0.594210908196864,-0.705200752065286));
#116951=DIRECTION('ref_axis',(-0.384711888962196,0.59102018849159,0.709007686338099));
#116952=DIRECTION('center_axis',(0.,0.,1.));
#116953=DIRECTION('ref_axis',(1.,0.,0.));
#116954=DIRECTION('center_axis',(-0.424064963398083,0.568208417840489,-0.705200752065248));
#116955=DIRECTION('ref_axis',(-0.421788250615727,0.565157298772622,0.709007686338137));
#116956=DIRECTION('center_axis',(0.,0.,1.));
#116957=DIRECTION('ref_axis',(1.,0.,0.));
#116958=DIRECTION('center_axis',(-0.459598914775863,0.539871037214812,-0.705200752065291));
#116959=DIRECTION('ref_axis',(-0.457131393874339,0.53697205648712,0.709007686338094));
#116960=DIRECTION('center_axis',(0.,0.,1.));
#116961=DIRECTION('ref_axis',(1.,0.,0.));
#116962=DIRECTION('center_axis',(-0.493244275629213,0.50931521069529,-0.705200752065272));
#116963=DIRECTION('ref_axis',(-0.490596086180789,0.506580280841613,0.709007686338113));
#116964=DIRECTION('center_axis',(0.,0.,1.));
#116965=DIRECTION('ref_axis',(1.,0.,0.));
#116966=DIRECTION('center_axis',(-0.524862789953399,0.476666498727232,-0.705200752065294));
#116967=DIRECTION('ref_axis',(-0.522044813936732,0.474106858160974,0.709007686338091));
#116968=DIRECTION('center_axis',(0.,0.,1.));
#116969=DIRECTION('ref_axis',(1.,0.,0.));
#116970=DIRECTION('center_axis',(-0.554324530490975,0.442059061871271,-0.705200752065291));
#116971=DIRECTION('ref_axis',(-0.551348347574532,0.439685228703826,0.709007686338094));
#116972=DIRECTION('center_axis',(0.,0.,1.));
#116973=DIRECTION('ref_axis',(1.,0.,0.));
#116974=DIRECTION('center_axis',(-0.581508432630519,0.405635109508721,-0.705200752065286));
#116975=DIRECTION('ref_axis',(0.578386272587459,-0.403456838330795,-0.709007686338099));
#116976=DIRECTION('center_axis',(0.,0.,1.));
#116977=DIRECTION('ref_axis',(1.,0.,0.));
#116978=DIRECTION('center_axis',(-0.606302791887217,0.367544315472719,-0.705200752065294));
#116979=DIRECTION('ref_axis',(0.603047484343626,-0.365570557266762,-0.709007686338091));
#116980=DIRECTION('center_axis',(0.,0.,1.));
#116981=DIRECTION('ref_axis',(1.,0.,0.));
#116982=DIRECTION('center_axis',(-0.628605722920505,0.32794320300644,-0.705200752065301));
#116983=DIRECTION('ref_axis',(0.625230644632876,-0.326182068368994,-0.709007686338084));
#116984=DIRECTION('center_axis',(0.,0.,1.));
#116985=DIRECTION('ref_axis',(1.,0.,0.));
#116986=DIRECTION('center_axis',(-0.648325578202841,0.286994501575399,-0.705200752065283));
#116987=DIRECTION('ref_axis',(0.644844598091737,-0.28545322738655,-0.709007686338102));
#116988=DIRECTION('center_axis',(0.,0.,1.));
#116989=DIRECTION('ref_axis',(1.,0.,0.));
#116990=DIRECTION('center_axis',(-0.665381324618884,0.244866478177285,-0.705200752065305));
#116991=DIRECTION('ref_axis',(0.661808746778622,-0.243551397862613,-0.70900768633808));
#116992=DIRECTION('center_axis',(0.,0.,1.));
#116993=DIRECTION('ref_axis',(1.,0.,0.));
#116994=DIRECTION('center_axis',(-0.679702876448276,0.201732245896628,-0.705200752065284));
#116995=DIRECTION('ref_axis',(0.676053381367121,-0.200648763404049,-0.709007686338101));
#116996=DIRECTION('center_axis',(0.,0.,1.));
#116997=DIRECTION('ref_axis',(1.,0.,0.));
#116998=DIRECTION('center_axis',(-0.69123138336253,0.157769052546159,-0.705200752065261));
#116999=DIRECTION('ref_axis',(0.687519967598698,-0.1569216201374,-0.709007686338124));
#117000=DIRECTION('center_axis',(0.,0.,1.));
#117001=DIRECTION('ref_axis',(1.,0.,0.));
#117002=DIRECTION('center_axis',(-0.699919472253854,0.113157552317423,-0.705200752065265));
#117003=DIRECTION('ref_axis',(0.696161386810957,-0.112549652273613,-0.70900768633812));
#117004=DIRECTION('center_axis',(0.,0.,1.));
#117005=DIRECTION('ref_axis',(1.,0.,0.));
#117006=DIRECTION('center_axis',(-0.705731441901413,0.0680810634339954,
-0.705200752065289));
#117007=DIRECTION('ref_axis',(0.701942129558611,-0.0677151937472035,-0.709007686338097));
#117008=DIRECTION('center_axis',(0.,0.,1.));
#117009=DIRECTION('ref_axis',(1.,0.,0.));
#117010=DIRECTION('center_axis',(-0.708643409675306,0.0227248148575655,
-0.705200752065287));
#117011=DIRECTION('ref_axis',(0.704838441529815,-0.0226024789640054,-0.709007686338098));
#117012=DIRECTION('center_axis',(0.,0.,1.));
#117013=DIRECTION('ref_axis',(1.,0.,0.));
#117014=DIRECTION('',(-0.707106781186552,8.659560562355E-17,0.707106781186543));
#117015=DIRECTION('center_axis',(0.,0.,1.));
#117016=DIRECTION('ref_axis',(1.,0.,0.));
#117017=DIRECTION('center_axis',(0.,0.,1.));
#117018=DIRECTION('ref_axis',(1.,0.,0.));
#117019=DIRECTION('center_axis',(0.,0.,1.));
#117020=DIRECTION('ref_axis',(1.,0.,0.));
#117021=DIRECTION('center_axis',(-0.708643409675315,-0.0227248148575665,
-0.705200752065277));
#117022=DIRECTION('ref_axis',(0.70483842115735,0.0226031142522111,-0.709007686338108));
#117023=DIRECTION('center_axis',(0.,0.,1.));
#117024=DIRECTION('ref_axis',(1.,0.,0.));
#117025=DIRECTION('center_axis',(-0.705731441901445,-0.0680810634340008,
-0.705200752065256));
#117026=DIRECTION('ref_axis',(0.701942068524995,0.0677158264241434,-0.709007686338128));
#117027=DIRECTION('center_axis',(0.,0.,1.));
#117028=DIRECTION('ref_axis',(1.,0.,0.));
#117029=DIRECTION('center_axis',(-0.699919472253843,-0.113157552317429,
-0.705200752065276));
#117030=DIRECTION('ref_axis',(0.696161285367009,0.112550279740369,-0.709007686338109));
#117031=DIRECTION('center_axis',(0.,0.,1.));
#117032=DIRECTION('ref_axis',(1.,0.,0.));
#117033=DIRECTION('center_axis',(-0.691231383362506,-0.157769052546184,
-0.705200752065279));
#117034=DIRECTION('ref_axis',(0.687519826161262,0.156922239815375,-0.709007686338106));
#117035=DIRECTION('center_axis',(0.,0.,1.));
#117036=DIRECTION('ref_axis',(1.,0.,0.));
#117037=DIRECTION('center_axis',(-0.679702876448284,-0.20173224589665,-0.70520075206527));
#117038=DIRECTION('ref_axis',(0.676053200517185,0.200649372747448,-0.709007686338115));
#117039=DIRECTION('center_axis',(0.,0.,1.));
#117040=DIRECTION('ref_axis',(1.,0.,0.));
#117041=DIRECTION('center_axis',(-0.665381324618884,-0.244866478177317,
-0.705200752065294));
#117042=DIRECTION('ref_axis',(0.661808527259463,0.243551994367051,-0.709007686338091));
#117043=DIRECTION('center_axis',(0.,0.,1.));
#117044=DIRECTION('ref_axis',(1.,0.,0.));
#117045=DIRECTION('center_axis',(-0.648325578202812,-0.286994501575426,
-0.705200752065298));
#117046=DIRECTION('ref_axis',(0.644844340805595,0.285453808600464,-0.709007686338087));
#117047=DIRECTION('center_axis',(0.,0.,1.));
#117048=DIRECTION('ref_axis',(1.,0.,0.));
#117049=DIRECTION('center_axis',(-0.628605722920495,-0.327943203006455,
-0.705200752065303));
#117050=DIRECTION('ref_axis',(0.625230350636678,0.326182631904669,-0.709007686338082));
#117051=DIRECTION('center_axis',(0.,0.,1.));
#117052=DIRECTION('ref_axis',(1.,0.,0.));
#117053=DIRECTION('center_axis',(-0.606302791887218,-0.367544315472729,
-0.705200752065288));
#117054=DIRECTION('ref_axis',(0.603047154845577,0.365571100808246,-0.709007686338097));
#117055=DIRECTION('center_axis',(0.,0.,1.));
#117056=DIRECTION('ref_axis',(1.,0.,0.));
#117057=DIRECTION('center_axis',(-0.581508432630516,-0.405635109508724,
-0.705200752065287));
#117058=DIRECTION('ref_axis',(0.578385908942077,0.403457359643798,-0.709007686338099));
#117059=DIRECTION('center_axis',(0.,0.,1.));
#117060=DIRECTION('ref_axis',(1.,0.,0.));
#117061=DIRECTION('center_axis',(-0.55432453049095,-0.442059061871284,-0.705200752065303));
#117062=DIRECTION('ref_axis',(0.551347951275536,0.439685725647067,-0.709007686338082));
#117063=DIRECTION('center_axis',(0.,0.,1.));
#117064=DIRECTION('ref_axis',(1.,0.,0.));
#117065=DIRECTION('center_axis',(-0.524862789953383,-0.476666498727248,
-0.705200752065295));
#117066=DIRECTION('ref_axis',(0.522044386612722,0.474107328692201,-0.709007686338091));
#117067=DIRECTION('center_axis',(0.,0.,1.));
#117068=DIRECTION('ref_axis',(1.,0.,0.));
#117069=DIRECTION('center_axis',(-0.49324427562918,-0.50931521069529,-0.705200752065295));
#117070=DIRECTION('ref_axis',(0.490595629587509,0.506580723027578,-0.70900768633809));
#117071=DIRECTION('center_axis',(0.,0.,1.));
#117072=DIRECTION('ref_axis',(1.,0.,0.));
#117073=DIRECTION('center_axis',(-0.459598914775862,-0.539871037214824,
-0.705200752065283));
#117074=DIRECTION('ref_axis',(0.457130909888059,0.536972468510637,-0.709007686338102));
#117075=DIRECTION('center_axis',(0.,0.,1.));
#117076=DIRECTION('ref_axis',(1.,0.,0.));
#117077=DIRECTION('center_axis',(-0.424064963398045,-0.568208417840474,
-0.705200752065282));
#117078=DIRECTION('ref_axis',(0.421787741225687,0.565157678940332,-0.709007686338103));
#117079=DIRECTION('center_axis',(0.,0.,1.));
#117080=DIRECTION('ref_axis',(1.,0.,0.));
#117081=DIRECTION('center_axis',(-0.386788438123993,-0.594210908196879,
-0.705200752065284));
#117082=DIRECTION('ref_axis',(0.384711356261092,0.59102053524158,-0.709007686338101));
#117083=DIRECTION('center_axis',(0.,0.,1.));
#117084=DIRECTION('ref_axis',(1.,0.,0.));
#117085=DIRECTION('center_axis',(-0.347922516191811,-0.617771658473671,
-0.705200752065289));
#117086=DIRECTION('ref_axis',(0.346054109813453,0.614454761389899,-0.709007686338097));
#117087=DIRECTION('center_axis',(0.,0.,1.));
#117088=DIRECTION('ref_axis',(1.,0.,0.));
#117089=DIRECTION('center_axis',(-0.30762690601146,-0.638793852494167,-0.705200752065309));
#117090=DIRECTION('ref_axis',(0.305974852800018,0.635364061123648,-0.709007686338077));
#117091=DIRECTION('center_axis',(0.,0.,1.));
#117092=DIRECTION('ref_axis',(1.,0.,0.));
#117093=DIRECTION('center_axis',(-0.266067190888571,-0.657191105553954,
-0.70520075206528));
#117094=DIRECTION('ref_axis',(0.264638279485338,0.653662513644868,-0.709007686338105));
#117095=DIRECTION('center_axis',(0.,0.,1.));
#117096=DIRECTION('ref_axis',(1.,0.,0.));
#117097=DIRECTION('center_axis',(-0.223414148607049,-0.672887819393935,
-0.705200752065299));
#117098=DIRECTION('ref_axis',(0.22221425071552,0.669274926687422,-0.709007686338086));
#117099=DIRECTION('center_axis',(0.,0.,1.));
#117100=DIRECTION('ref_axis',(1.,0.,0.));
#117101=DIRECTION('center_axis',(-0.179843049666729,-0.685819492850059,
-0.705200752065295));
#117102=DIRECTION('ref_axis',(0.178877095924088,0.68213714549735,-0.70900768633809));
#117103=DIRECTION('center_axis',(0.,0.,1.));
#117104=DIRECTION('ref_axis',(1.,0.,0.));
#117105=DIRECTION('center_axis',(-0.135532937059131,-0.695932986902283,
-0.705200752065249));
#117106=DIRECTION('ref_axis',(0.134804896777495,0.692196316458165,-0.709007686338136));
#117107=DIRECTION('center_axis',(0.,0.,1.));
#117108=DIRECTION('ref_axis',(1.,0.,0.));
#117109=DIRECTION('center_axis',(-0.0906658905414127,-0.703186743034061,
-0.705200752065312));
#117110=DIRECTION('ref_axis',(0.0901787553939383,0.699411104279259,-0.709007686338073));
#117111=DIRECTION('center_axis',(0.,0.,1.));
#117112=DIRECTION('ref_axis',(1.,0.,0.));
#117113=DIRECTION('center_axis',(-0.0454262784316981,-0.707550954005724,
-0.705200752065279));
#117114=DIRECTION('ref_axis',(0.045182050161025,0.703751861849567,-0.709007686338106));
#117115=DIRECTION('center_axis',(0.,0.,1.));
#117116=DIRECTION('ref_axis',(1.,0.,0.));
#117117=DIRECTION('center_axis',(0.,-0.709007686338126,-0.705200752065295));
#117118=DIRECTION('ref_axis',(-3.17807545014534E-7,0.705200752065259,-0.70900768633809));
#117119=DIRECTION('center_axis',(0.,0.,1.));
#117120=DIRECTION('ref_axis',(1.,0.,0.));
#117121=DIRECTION('center_axis',(0.0454262784316969,-0.707550954005706,
-0.705200752065298));
#117122=DIRECTION('ref_axis',(-0.0451826844697783,0.703751821125613,-0.709007686338088));
#117123=DIRECTION('center_axis',(0.,0.,1.));
#117124=DIRECTION('ref_axis',(1.,0.,0.));
#117125=DIRECTION('center_axis',(0.0906658905414092,-0.703186743034074,
-0.7052007520653));
#117126=DIRECTION('ref_axis',(-0.0901793857898937,0.699411022998689,-0.709007686338085));
#117127=DIRECTION('center_axis',(0.,0.,1.));
#117128=DIRECTION('ref_axis',(1.,0.,0.));
#117129=DIRECTION('center_axis',(0.135532937059137,-0.69593298690225,-0.70520075206528));
#117130=DIRECTION('ref_axis',(-0.134805520670637,0.692196194955019,-0.709007686338105));
#117131=DIRECTION('center_axis',(0.,0.,1.));
#117132=DIRECTION('ref_axis',(1.,0.,0.));
#117133=DIRECTION('center_axis',(0.179843049666742,-0.685819492850065,-0.705200752065287));
#117134=DIRECTION('ref_axis',(-0.17887771075135,0.682136984270647,-0.709007686338099));
#117135=DIRECTION('center_axis',(0.,0.,1.));
#117136=DIRECTION('ref_axis',(1.,0.,0.));
#117137=DIRECTION('center_axis',(0.22341414860707,-0.672887819393955,-0.705200752065273));
#117138=DIRECTION('ref_axis',(-0.222214853948978,0.669274726400087,-0.709007686338112));
#117139=DIRECTION('center_axis',(0.,0.,1.));
#117140=DIRECTION('ref_axis',(1.,0.,0.));
#117141=DIRECTION('center_axis',(0.266067190888564,-0.657191105553934,-0.705200752065302));
#117142=DIRECTION('ref_axis',(-0.264638868646705,0.653662275119889,-0.709007686338084));
#117143=DIRECTION('center_axis',(0.,0.,1.));
#117144=DIRECTION('ref_axis',(1.,0.,0.));
#117145=DIRECTION('center_axis',(0.307626906011474,-0.638793852494176,-0.705200752065295));
#117146=DIRECTION('ref_axis',(-0.305975425469023,0.635363785340775,-0.709007686338091));
#117147=DIRECTION('center_axis',(0.,0.,1.));
#117148=DIRECTION('ref_axis',(1.,0.,0.));
#117149=DIRECTION('center_axis',(0.347922516191819,-0.617771658473665,-0.705200752065291));
#117150=DIRECTION('ref_axis',(-0.346054663636103,0.614454449482796,-0.709007686338095));
#117151=DIRECTION('center_axis',(0.,0.,1.));
#117152=DIRECTION('ref_axis',(1.,0.,0.));
#117153=DIRECTION('center_axis',(0.386788438123997,-0.594210908196884,-0.705200752065278));
#117154=DIRECTION('ref_axis',(-0.384711888962051,0.591020188491674,-0.709007686338108));
#117155=DIRECTION('center_axis',(0.,0.,1.));
#117156=DIRECTION('ref_axis',(1.,0.,0.));
#117157=DIRECTION('center_axis',(0.424064963398043,-0.568208417840467,-0.705200752065289));
#117158=DIRECTION('ref_axis',(-0.421788250615591,0.565157298772775,-0.709007686338096));
#117159=DIRECTION('center_axis',(0.,0.,1.));
#117160=DIRECTION('ref_axis',(1.,0.,0.));
#117161=DIRECTION('center_axis',(0.45959891477585,-0.53987103721481,-0.705200752065301));
#117162=DIRECTION('ref_axis',(-0.457131393874177,0.536972056487271,-0.709007686338084));
#117163=DIRECTION('center_axis',(0.,0.,1.));
#117164=DIRECTION('ref_axis',(1.,0.,0.));
#117165=DIRECTION('center_axis',(0.493244275629187,-0.509315210695281,-0.705200752065297));
#117166=DIRECTION('ref_axis',(-0.490596086180762,0.506580280841674,-0.709007686338088));
#117167=DIRECTION('center_axis',(0.,0.,1.));
#117168=DIRECTION('ref_axis',(1.,0.,0.));
#117169=DIRECTION('center_axis',(0.524862789953382,-0.47666649872723,-0.705200752065308));
#117170=DIRECTION('ref_axis',(-0.522044813937081,0.47410685816061,-0.709007686338077));
#117171=DIRECTION('center_axis',(0.,0.,1.));
#117172=DIRECTION('ref_axis',(1.,0.,0.));
#117173=DIRECTION('center_axis',(0.554324530490965,-0.442059061871282,-0.705200752065292));
#117174=DIRECTION('ref_axis',(-0.55134834757427,0.439685228704155,-0.709007686338094));
#117175=DIRECTION('center_axis',(0.,0.,1.));
#117176=DIRECTION('ref_axis',(1.,0.,0.));
#117177=DIRECTION('center_axis',(0.581508432630509,-0.405635109508715,-0.705200752065298));
#117178=DIRECTION('ref_axis',(0.578386272587666,-0.40345683833052,0.709007686338087));
#117179=DIRECTION('center_axis',(0.,0.,1.));
#117180=DIRECTION('ref_axis',(1.,0.,0.));
#117181=DIRECTION('center_axis',(0.606302791887227,-0.367544315472725,-0.705200752065283));
#117182=DIRECTION('ref_axis',(0.603047484343378,-0.36557055726715,0.709007686338102));
#117183=DIRECTION('center_axis',(0.,0.,1.));
#117184=DIRECTION('ref_axis',(1.,0.,0.));
#117185=DIRECTION('center_axis',(0.628605722920507,-0.327943203006441,-0.705200752065299));
#117186=DIRECTION('ref_axis',(0.625230644632778,-0.326182068369178,0.709007686338086));
#117187=DIRECTION('center_axis',(0.,0.,1.));
#117188=DIRECTION('ref_axis',(1.,0.,0.));
#117189=DIRECTION('center_axis',(0.648325578202825,-0.286994501575435,-0.705200752065283));
#117190=DIRECTION('ref_axis',(0.644844598091824,-0.285453227386353,0.709007686338102));
#117191=DIRECTION('center_axis',(0.,0.,1.));
#117192=DIRECTION('ref_axis',(1.,0.,0.));
#117193=DIRECTION('center_axis',(0.665381324618895,-0.24486647817731,-0.705200752065287));
#117194=DIRECTION('ref_axis',(0.661808746778473,-0.243551397862965,0.709007686338098));
#117195=DIRECTION('center_axis',(0.,0.,1.));
#117196=DIRECTION('ref_axis',(1.,0.,0.));
#117197=DIRECTION('center_axis',(0.679702876448274,-0.201732245896636,-0.705200752065284));
#117198=DIRECTION('ref_axis',(0.6760533813671,-0.200648763404121,0.709007686338102));
#117199=DIRECTION('center_axis',(0.,0.,1.));
#117200=DIRECTION('ref_axis',(1.,0.,0.));
#117201=DIRECTION('center_axis',(0.69123138336251,-0.157769052546173,-0.705200752065278));
#117202=DIRECTION('ref_axis',(0.687519967598833,-0.15692162013688,0.709007686338107));
#117203=DIRECTION('center_axis',(0.,0.,1.));
#117204=DIRECTION('ref_axis',(1.,0.,0.));
#117205=DIRECTION('center_axis',(0.699919472253825,-0.113157552317415,-0.705200752065296));
#117206=DIRECTION('ref_axis',(0.696161386811017,-0.112549652273433,0.709007686338089));
#117207=DIRECTION('center_axis',(0.,0.,1.));
#117208=DIRECTION('ref_axis',(1.,0.,0.));
#117209=DIRECTION('center_axis',(0.705731441901455,-0.0680810634339902,
-0.705200752065247));
#117210=DIRECTION('ref_axis',(0.701942129558587,-0.0677151937470296,0.709007686338137));
#117211=DIRECTION('center_axis',(0.,0.,1.));
#117212=DIRECTION('ref_axis',(1.,0.,0.));
#117213=DIRECTION('center_axis',(0.708643409675344,-0.0227248148575675,
-0.705200752065248));
#117214=DIRECTION('ref_axis',(0.704838441529764,-0.0226024789643774,0.709007686338137));
#117215=DIRECTION('center_axis',(0.,0.,1.));
#117216=DIRECTION('ref_axis',(1.,0.,0.));
#117217=DIRECTION('center_axis',(0.,0.,1.));
#117218=DIRECTION('ref_axis',(1.,0.,0.));
#117219=DIRECTION('center_axis',(1.22464679914735E-16,-1.,0.));
#117220=DIRECTION('ref_axis',(-1.,-1.22464679914735E-16,0.));
#117221=DIRECTION('center_axis',(0.,0.,1.));
#117222=DIRECTION('ref_axis',(1.,0.,0.));
#117223=DIRECTION('center_axis',(0.,0.,1.));
#117224=DIRECTION('ref_axis',(1.,0.,0.));
#117225=DIRECTION('',(0.,0.,-1.));
#117226=DIRECTION('center_axis',(0.999875322485695,-0.015751302085643,0.00111174040829824));
#117227=DIRECTION('ref_axis',(0.00831475628134585,0.465340995336109,-0.885092437481861));
#117228=DIRECTION('center_axis',(0.,0.,-1.));
#117229=DIRECTION('ref_axis',(0.0320515775716446,0.999486216200688,0.));
#117230=DIRECTION('center_axis',(0.998830238638869,-0.0483416538578448,
0.00111305117022865));
#117231=DIRECTION('ref_axis',(-0.0215571677327655,-0.465780464937779,-0.884637692505631));
#117232=DIRECTION('',(0.,0.,1.));
#117233=DIRECTION('center_axis',(0.,0.,1.));
#117234=DIRECTION('ref_axis',(1.,0.,0.));
#117235=DIRECTION('',(0.,0.,-1.));
#117236=DIRECTION('center_axis',(0.996811782009738,-0.0797811712112251,
0.00111174040838231));
#117237=DIRECTION('ref_axis',(0.0381121726600761,0.463852174088461,-0.8850924374824));
#117238=DIRECTION('center_axis',(0.,0.,-1.));
#117239=DIRECTION('ref_axis',(0.0960230259076709,0.995379112949199,0.));
#117240=DIRECTION('center_axis',(0.993680774392475,-0.112237603858347,0.00111305117023333));
#117241=DIRECTION('ref_axis',(-0.0513555330708394,-0.463442296538108,-0.884637692506087));
#117242=DIRECTION('',(0.,0.,1.));
#117243=DIRECTION('center_axis',(0.,0.,1.));
#117244=DIRECTION('ref_axis',(1.,0.,0.));
#117245=DIRECTION('',(0.,0.,-1.));
#117246=DIRECTION('center_axis',(0.989652128106051,-0.143483202391184,0.00111174040840064));
#117247=DIRECTION('ref_axis',(0.0677529779465081,0.460457284764545,-0.88509243748133));
#117248=DIRECTION('center_axis',(0.,0.,-1.));
#117249=DIRECTION('ref_axis',(0.159599895033369,0.987181783414452,0.));
#117250=DIRECTION('center_axis',(0.984448062700241,-0.175672345469724,0.00111305117024819));
#117251=DIRECTION('ref_axis',(-0.0809428675080738,-0.459199744336065,-0.884637692505391));
#117252=DIRECTION('',(0.,0.,1.));
#117253=DIRECTION('center_axis',(0.,0.,1.));
#117254=DIRECTION('ref_axis',(1.,0.,0.));
#117255=DIRECTION('',(0.,0.,-1.));
#117256=DIRECTION('center_axis',(0.978425781328247,-0.206595630315535,0.00111174040841298));
#117257=DIRECTION('ref_axis',(0.0971153717128268,0.455170277684735,-0.885092437482933));
#117258=DIRECTION('center_axis',(0.,0.,-1.));
#117259=DIRECTION('ref_axis',(0.222520933956304,0.974927912181826,0.));
#117260=DIRECTION('center_axis',(0.971170042754934,-0.238385211731921,0.00111305117026388));
#117261=DIRECTION('ref_axis',(-0.110197590339834,-0.453070241883085,-0.884637692506541));
#117262=DIRECTION('',(0.,0.,1.));
#117263=DIRECTION('center_axis',(0.,0.,1.));
#117264=DIRECTION('ref_axis',(1.,0.,0.));
#117265=DIRECTION('',(0.,0.,-1.));
#117266=DIRECTION('center_axis',(0.963178873143288,-0.26885911248029,0.00111174040845783));
#117267=DIRECTION('ref_axis',(0.126078697585652,0.448012878301757,-0.885092437483724));
#117268=DIRECTION('center_axis',(0.,0.,-1.));
#117269=DIRECTION('ref_axis',(0.284527586631023,0.958667853036663,0.));
#117270=DIRECTION('center_axis',(0.953901276788614,-0.300118502025689,0.00111305117024521));
#117271=DIRECTION('ref_axis',(-0.138999487636299,-0.445078976625978,-0.884637692506044));
#117272=DIRECTION('',(0.,0.,1.));
#117273=DIRECTION('center_axis',(0.,0.,1.));
#117274=DIRECTION('ref_axis',(1.,0.,0.));
#117275=DIRECTION('',(0.,0.,-1.));
#117276=DIRECTION('center_axis',(0.943974056367375,-0.330017794881712,0.00111174040846252));
#117277=DIRECTION('ref_axis',(0.154523939046571,0.439014497904912,-0.885092437483696));
#117278=DIRECTION('center_axis',(0.,0.,-1.));
#117279=DIRECTION('ref_axis',(0.345365054421298,0.938468422049764,0.));
#117280=DIRECTION('center_axis',(0.932712725864775,-0.360618541019444,0.00111305117022834));
#117281=DIRECTION('ref_axis',(-0.16723020622334,-0.435258786385882,-0.884637692504897));
#117282=DIRECTION('',(0.,0.,1.));
#117283=DIRECTION('center_axis',(0.,0.,1.));
#117284=DIRECTION('ref_axis',(1.,0.,0.));
#117285=DIRECTION('',(0.,0.,-1.));
#117286=DIRECTION('center_axis',(0.920890247712054,-0.389820363375359,0.00111174040842101));
#117287=DIRECTION('ref_axis',(0.182334208497475,0.428212112769879,-0.885092437482524));
#117288=DIRECTION('center_axis',(0.,0.,-1.));
#117289=DIRECTION('ref_axis',(0.404783343122385,0.914412623015816,0.));
#117290=DIRECTION('center_axis',(0.907691458284136,-0.419636721075635,0.00111305117023417));
#117291=DIRECTION('ref_axis',(-0.194773740020739,-0.423650024426041,-0.884637692505892));
#117292=DIRECTION('',(0.,0.,1.));
#117293=DIRECTION('center_axis',(0.,0.,1.));
#117294=DIRECTION('ref_axis',(1.,0.,0.));
#117295=DIRECTION('',(0.,0.,-1.));
#117296=DIRECTION('center_axis',(0.894022303498553,-0.448021076379678,0.0011117404084274));
#117297=DIRECTION('ref_axis',(0.209395227573944,0.415650112209241,-0.885092437483059));
#117298=DIRECTION('center_axis',(0.,0.,-1.));
#117299=DIRECTION('ref_axis',(0.462538290240827,0.886599306373005,0.));
#117300=DIRECTION('center_axis',(0.878940291802186,-0.476930523833169,0.00111305117021906));
#117301=DIRECTION('ref_axis',(-0.221516906742537,-0.410300393645422,-0.884637692505599));
#117302=DIRECTION('',(0.,0.,1.));
#117303=DIRECTION('center_axis',(0.,0.,1.));
#117304=DIRECTION('ref_axis',(1.,0.,0.));
#117305=DIRECTION('',(0.,0.,-1.));
#117306=DIRECTION('center_axis',(0.863480629872782,-0.504380774680963,0.00111174040840051));
#117307=DIRECTION('ref_axis',(0.235595796746304,0.401380116183086,-0.885092437482282));
#117308=DIRECTION('center_axis',(0.,0.,-1.));
#117309=DIRECTION('ref_axis',(0.518392568310517,0.855142763005351,0.));
#117310=DIRECTION('center_axis',(0.846577371129118,-0.532264516766997,0.00111305117023412));
#117311=DIRECTION('ref_axis',(-0.247349812978024,-0.395264750536038,-0.884637692506611));
#117312=DIRECTION('',(0.,0.,1.));
#117313=DIRECTION('center_axis',(0.,0.,1.));
#117314=DIRECTION('ref_axis',(1.,0.,0.));
#117315=DIRECTION('',(0.,0.,-1.));
#117316=DIRECTION('center_axis',(0.829390729122881,-0.558667864189699,0.00111174040836604));
#117317=DIRECTION('ref_axis',(0.260828252253777,0.385460763162129,-0.885092437482498));
#117318=DIRECTION('center_axis',(0.,0.,-1.));
#117319=DIRECTION('ref_axis',(0.572116660122162,0.820172254596961,0.));
#117320=DIRECTION('center_axis',(0.810735682447807,-0.585411320631042,0.00111305117023414));
#117321=DIRECTION('ref_axis',(-0.27216630577768,-0.378604879785937,-0.884637692505585));
#117322=DIRECTION('',(0.,0.,1.));
#117323=DIRECTION('center_axis',(0.,0.,1.));
#117324=DIRECTION('ref_axis',(1.,0.,0.));
#117325=DIRECTION('',(0.,0.,-1.));
#117326=DIRECTION('center_axis',(0.791892683963227,-0.610659267610654,0.00111174040838973));
#117327=DIRECTION('ref_axis',(0.284988908526042,0.367957469185241,-0.885092437482056));
#117328=DIRECTION('center_axis',(0.,0.,-1.));
#117329=DIRECTION('ref_axis',(0.623489801858726,0.781831482468036,0.));
#117330=DIRECTION('center_axis',(0.77156250694505,-0.636152543808293,0.00111305117021684));
#117331=DIRECTION('ref_axis',(-0.295864408844889,-0.360389240370828,-0.884637692506826));
#117332=DIRECTION('',(0.,0.,1.));
#117333=DIRECTION('center_axis',(0.,0.,1.));
#117334=DIRECTION('ref_axis',(1.,0.,0.));
#117335=DIRECTION('',(0.,0.,-1.));
#117336=DIRECTION('center_axis',(0.751140581904703,-0.660141341115014,0.00111174040841524));
#117337=DIRECTION('ref_axis',(0.307978484242966,0.34894215904034,-0.885092437481912));
#117338=DIRECTION('center_axis',(0.,0.,-1.));
#117339=DIRECTION('ref_axis',(0.67230089026131,0.740277997075322,0.));
#117340=DIRECTION('center_axis',(0.729218815601603,-0.684279679728756,0.00111305117020348));
#117341=DIRECTION('ref_axis',(-0.318346741594962,-0.340692684265839,-0.884637692506716));
#117342=DIRECTION('',(0.,0.,1.));
#117343=DIRECTION('center_axis',(0.,0.,1.));
#117344=DIRECTION('ref_axis',(1.,0.,0.));
#117345=DIRECTION('',(0.,0.,-1.));
#117346=DIRECTION('center_axis',(0.707301882076007,-0.706910752248827,0.00111174040839121));
#117347=DIRECTION('ref_axis',(0.329702510308574,0.32849297071774,-0.885092437480549));
#117348=DIRECTION('center_axis',(0.,0.,-1.));
#117349=DIRECTION('ref_axis',(0.718349350097721,0.695682550603493,0.));
#117350=DIRECTION('center_axis',(0.68387860772793,-0.729594963667651,0.00111305117020451));
#117351=DIRECTION('ref_axis',(-0.339520919298581,-0.319596148842784,-0.88463769250666));
#117352=DIRECTION('',(0.,0.,1.));
#117353=DIRECTION('center_axis',(0.,0.,1.));
#117354=DIRECTION('ref_axis',(1.,0.,0.));
#117355=DIRECTION('',(0.,0.,-1.));
#117356=DIRECTION('center_axis',(0.66055672709807,-0.750775315469781,0.00111174040841501));
#117357=DIRECTION('ref_axis',(0.350071718032401,0.306693934311185,-0.885092437483549));
#117358=DIRECTION('center_axis',(0.,0.,-1.));
#117359=DIRECTION('ref_axis',(0.761445958369129,0.648228395307795,0.));
#117360=DIRECTION('center_axis',(0.635728195963613,-0.771912185403199,0.00111305117021925));
#117361=DIRECTION('ref_axis',(-0.359299932720418,-0.29718632429314,-0.884637692504811));
#117362=DIRECTION('',(0.,0.,1.));
#117363=DIRECTION('center_axis',(0.,0.,1.));
#117364=DIRECTION('ref_axis',(1.,0.,0.));
#117365=DIRECTION('',(0.,0.,-1.));
#117366=DIRECTION('center_axis',(0.61109720283957,-0.791554781878625,0.00111174040836773));
#117367=DIRECTION('ref_axis',(0.369002405982045,0.283634626748089,-0.885092437482625));
#117368=DIRECTION('center_axis',(0.,0.,-1.));
#117369=DIRECTION('ref_axis',(0.801413621867952,0.598110530491223,0.));
#117370=DIRECTION('center_axis',(0.584965440678803,-0.811057454394291,0.00111305117022841));
#117371=DIRECTION('ref_axis',(-0.377602505644605,-0.273555297386895,-0.884637692506081));
#117372=DIRECTION('',(0.,0.,1.));
#117373=DIRECTION('center_axis',(0.,0.,1.));
#117374=DIRECTION('ref_axis',(1.,0.,0.));
#117375=DIRECTION('',(0.,0.,-1.));
#117376=DIRECTION('center_axis',(0.559126549094596,-0.829081579900816,0.00111174040838601));
#117377=DIRECTION('ref_axis',(0.386416783895308,0.259409803664243,-0.885092437481468));
#117378=DIRECTION('center_axis',(0.,0.,-1.));
#117379=DIRECTION('ref_axis',(0.838088104891836,0.545534901210556,0.));
#117380=DIRECTION('center_axis',(0.531798936923567,-0.846869914333988,0.00111305117024416));
#117381=DIRECTION('ref_axis',(-0.39435342887895,-0.24880017308748,-0.884637692506404));
#117382=DIRECTION('',(0.,0.,1.));
#117383=DIRECTION('center_axis',(0.,0.,1.));
#117384=DIRECTION('ref_axis',(1.,0.,0.));
#117385=DIRECTION('',(0.,0.,-1.));
#117386=DIRECTION('center_axis',(0.504858324427174,-0.86320150387372,0.00111174040834681));
#117387=DIRECTION('ref_axis',(0.402243292355672,0.234119010052661,-0.885092437481437));
#117388=DIRECTION('center_axis',(0.,0.,-1.));
#117389=DIRECTION('ref_axis',(0.871318704123385,0.490717552003945,0.));
#117390=DIRECTION('center_axis',(0.476447157265946,-0.879202404142693,0.00111305117023455));
#117391=DIRECTION('ref_axis',(-0.409483869284568,-0.223022675508913,-0.884637692507269));
#117392=DIRECTION('',(0.,0.,1.));
#117393=DIRECTION('center_axis',(0.,0.,1.));
#117394=DIRECTION('ref_axis',(1.,0.,0.));
#117395=DIRECTION('',(0.,0.,-1.));
#117396=DIRECTION('center_axis',(0.448515528612856,-0.893774347711096,0.00111174040839922));
#117397=DIRECTION('ref_axis',(0.416416896849112,0.20786617121142,-0.885092437480098));
#117398=DIRECTION('center_axis',(0.,0.,-1.));
#117399=DIRECTION('ref_axis',(0.900968867902415,0.433883739117566,0.));
#117400=DIRECTION('center_axis',(0.419137554041588,-0.907922062684417,0.00111305117024988));
#117401=DIRECTION('ref_axis',(-0.422931652641499,-0.196328729920701,-0.884637692505613));
#117402=DIRECTION('',(0.,0.,1.));
#117403=DIRECTION('center_axis',(0.,0.,1.));
#117404=DIRECTION('ref_axis',(1.,0.,0.));
#117405=DIRECTION('',(0.,0.,-1.));
#117406=DIRECTION('center_axis',(0.390329686285115,-0.920674481039758,0.00111174040847326));
#117407=DIRECTION('ref_axis',(0.42887935498825,0.1807591656834,-0.885092437481139));
#117408=DIRECTION('center_axis',(0.,0.,-1.));
#117409=DIRECTION('ref_axis',(0.926916757346019,0.375267004879382,0.));
#117410=DIRECTION('center_axis',(0.360105624702917,-0.932910874721918,0.00111305117025848));
#117411=DIRECTION('ref_axis',(-0.434641519116407,-0.168828027467345,-0.88463769250562));
#117412=DIRECTION('',(0.,0.,1.));
#117413=DIRECTION('center_axis',(0.,0.,1.));
#117414=DIRECTION('ref_axis',(1.,0.,0.));
#117415=DIRECTION('',(0.,0.,-1.));
#117416=DIRECTION('center_axis',(0.330539895551113,-0.943791365441708,0.00111174040842785));
#117417=DIRECTION('ref_axis',(0.439579455860902,0.152909381970445,-0.885092437483481));
#117418=DIRECTION('center_axis',(0.,0.,-1.));
#117419=DIRECTION('ref_axis',(0.949055747010666,0.315108218023628,0.));
#117420=DIRECTION('center_axis',(0.29959394410987,-0.95406615586645,0.00111305117019356));
#117421=DIRECTION('ref_axis',(-0.444565350357212,-0.140633574434986,-0.884637692506604));
#117422=DIRECTION('',(0.,0.,1.));
#117423=DIRECTION('center_axis',(0.,0.,1.));
#117424=DIRECTION('ref_axis',(1.,0.,0.));
#117425=DIRECTION('',(0.,0.,-1.));
#117426=DIRECTION('center_axis',(0.269391845485697,-0.963030008680454,0.00111174040839746));
#117427=DIRECTION('ref_axis',(0.448473230463594,0.124431260809614,-0.885092437483723));
#117428=DIRECTION('center_axis',(0.,0.,-1.));
#117429=DIRECTION('ref_axis',(0.967294863039028,0.253654583909515,0.));
#117430=DIRECTION('center_axis',(0.237851167737837,-0.971300974529955,0.00111305117021558));
#117431=DIRECTION('ref_axis',(-0.452662367216689,-0.111861227880374,-0.884637692506304));
#117432=DIRECTION('',(0.,0.,1.));
#117433=DIRECTION('center_axis',(0.,0.,1.));
#117434=DIRECTION('ref_axis',(1.,0.,0.));
#117435=DIRECTION('',(0.,0.,-1.));
#117436=DIRECTION('center_axis',(0.207136806542801,-0.978311355044249,0.00111174040839084));
#117437=DIRECTION('ref_axis',(0.455524132365643,0.0954418249078427,-0.885092437483673));
#117438=DIRECTION('center_axis',(0.,0.,-1.));
#117439=DIRECTION('ref_axis',(0.981559156991064,0.19115862870138,0.));
#117440=DIRECTION('center_axis',(0.175131009898625,-0.984544509145717,0.00111305117022153));
#117441=DIRECTION('ref_axis',(-0.458899297309475,-0.0826292195454268,-0.884637692508173));
#117442=DIRECTION('',(0.,0.,1.));
#117443=DIRECTION('center_axis',(0.,0.,1.));
#117444=DIRECTION('ref_axis',(1.,0.,0.));
#117445=DIRECTION('',(0.,0.,-1.));
#117446=DIRECTION('center_axis',(0.144030598031156,-0.989572610203037,0.00111174040831266));
#117447=DIRECTION('ref_axis',(0.460703187901393,0.0660601980758584,-0.885092437481912));
#117448=DIRECTION('center_axis',(0.,0.,-1.));
#117449=DIRECTION('ref_axis',(0.991790013823245,0.127877161684513,0.));
#117450=DIRECTION('center_axis',(0.111691201174308,-0.993742339189255,0.00111305117022928));
#117451=DIRECTION('ref_axis',(-0.463250511766096,-0.0530576700250649,-0.884637692504655));
#117452=DIRECTION('',(0.,0.,1.));
#117453=DIRECTION('center_axis',(0.,0.,1.));
#117454=DIRECTION('ref_axis',(1.,0.,0.));
#117455=DIRECTION('',(0.,0.,-1.));
#117456=DIRECTION('center_axis',(0.0803325368976722,-0.996767499243855,
0.00111174040833762));
#117457=DIRECTION('ref_axis',(0.463989115216096,0.0364071157194459,-0.885092437480953));
#117458=DIRECTION('center_axis',(0.,0.,-1.));
#117459=DIRECTION('ref_axis',(0.997945392750336,0.0640702199807201,0.));
#117460=DIRECTION('center_axis',(0.0477924293465913,-0.99885666880401,0.00111305117018364));
#117461=DIRECTION('ref_axis',(-0.465698130493557,-0.023268095156349,-0.884637692506148));
#117462=DIRECTION('',(0.,0.,1.));
#117463=DIRECTION('center_axis',(0.,0.,1.));
#117464=DIRECTION('ref_axis',(1.,0.,0.));
#117465=DIRECTION('',(0.,0.,-1.));
#117466=DIRECTION('center_axis',(0.0163043721387329,-0.999866456824323,
0.00111174040837426));
#117467=DIRECTION('ref_axis',(0.465368411727477,0.00660442871490491,-0.885092437481868));
#117468=DIRECTION('center_axis',(0.,0.,-1.));
#117469=DIRECTION('ref_axis',(1.,0.,0.));
#117470=DIRECTION('center_axis',(-0.0163027318246417,-0.99986648211256,
0.00111305117021138));
#117471=DIRECTION('ref_axis',(-0.466232095712976,0.00661709330591105,-0.884637692506524));
#117472=DIRECTION('',(0.,0.,1.));
#117473=DIRECTION('center_axis',(0.,0.,1.));
#117474=DIRECTION('ref_axis',(1.,0.,0.));
#117475=DIRECTION('',(0.,0.,-1.));
#117476=DIRECTION('center_axis',(-0.0477907907824984,-0.998856748663014,
0.0011117404083719));
#117477=DIRECTION('ref_axis',(0.464835409613913,-0.0232253973035688,-0.885092437482751));
#117478=DIRECTION('center_axis',(0.,0.,-1.));
#117479=DIRECTION('ref_axis',(0.997945392750337,-0.0640702199807057,0.));
#117480=DIRECTION('center_axis',(-0.080330901573938,-0.996767629575425,
0.00111305117021671));
#117481=DIRECTION('ref_axis',(-0.464850213245993,0.0364750907124789,-0.884637692506187));
#117482=DIRECTION('',(0.,0.,1.));
#117483=DIRECTION('center_axis',(0.,0.,1.));
#117484=DIRECTION('ref_axis',(1.,0.,0.));
#117485=DIRECTION('',(0.,0.,-1.));
#117486=DIRECTION('center_axis',(-0.111689571093344,-0.993742523867349,
0.0011117404083511));
#117487=DIRECTION('ref_axis',(0.462392299100626,-0.0529597851830607,-0.885092437480855));
#117488=DIRECTION('center_axis',(0.,0.,-1.));
#117489=DIRECTION('ref_axis',(0.991790013823247,-0.127877161684499,0.));
#117490=DIRECTION('center_axis',(-0.144028974417756,-0.989572845042376,
0.0011130511702303));
#117491=DIRECTION('ref_axis',(-0.461558161541928,0.0661832041473919,-0.884637692506271));
#117492=DIRECTION('',(0.,0.,1.));
#117493=DIRECTION('center_axis',(0.,0.,1.));
#117494=DIRECTION('ref_axis',(1.,0.,0.));
#117495=DIRECTION('',(0.,0.,-1.));
#117496=DIRECTION('center_axis',(-0.175129394999318,-0.984544797883995,
0.00111174040840423));
#117497=DIRECTION('ref_axis',(0.458049119438637,-0.082476549944404,-0.885092437483655));
#117498=DIRECTION('center_axis',(0.,0.,-1.));
#117499=DIRECTION('ref_axis',(0.981559156991067,-0.191158628701366,0.));
#117500=DIRECTION('center_axis',(-0.207135201311547,-0.978311693426342,
0.00111305117022879));
#117501=DIRECTION('ref_axis',(-0.456369468349654,0.0956193566005051,-0.884637692505559));
#117502=DIRECTION('',(0.,0.,1.));
#117503=DIRECTION('center_axis',(0.,0.,1.));
#117504=DIRECTION('ref_axis',(1.,0.,0.));
#117505=DIRECTION('',(0.,0.,-1.));
#117506=DIRECTION('center_axis',(-0.237849574656071,-0.971301366141936,
0.00111174040845007));
#117507=DIRECTION('ref_axis',(0.451823717701448,-0.111654400872045,-0.885092437482293));
#117508=DIRECTION('center_axis',(0.,0.,-1.));
#117509=DIRECTION('ref_axis',(0.967294863039031,-0.253654583909501,0.));
#117510=DIRECTION('center_axis',(-0.269390265232804,-0.963030449214817,
0.0011130511702463));
#117511=DIRECTION('ref_axis',(-0.449305455119068,0.124662588606691,-0.884637692505879));
#117512=DIRECTION('',(0.,0.,1.));
#117513=DIRECTION('center_axis',(0.,0.,1.));
#117514=DIRECTION('ref_axis',(1.,0.,0.));
#117515=DIRECTION('',(0.,0.,-1.));
#117516=DIRECTION('center_axis',(-0.299592379391908,-0.954066648742927,
0.00111174040843038));
#117517=DIRECTION('ref_axis',(0.443741675391016,-0.140373439916541,-0.885092437481629));
#117518=DIRECTION('center_axis',(0.,0.,-1.));
#117519=DIRECTION('ref_axis',(0.949055747010671,-0.315108218023615,0.));
#117520=DIRECTION('center_axis',(-0.33053834677016,-0.943791906318094,0.00111305117024269));
#117521=DIRECTION('ref_axis',(-0.440395149396347,0.153193555295706,-0.884637692506956));
#117522=DIRECTION('',(0.,0.,1.));
#117523=DIRECTION('center_axis',(0.,0.,1.));
#117524=DIRECTION('ref_axis',(1.,0.,0.));
#117525=DIRECTION('',(0.,0.,-1.));
#117526=DIRECTION('center_axis',(-0.360104094778504,-0.932911466837566,
0.00111174040845034));
#117527=DIRECTION('ref_axis',(0.433836203352379,-0.168515654385977,-0.885092437481905));
#117528=DIRECTION('center_axis',(0.,0.,-1.));
#117529=DIRECTION('ref_axis',(0.926916757346024,-0.375267004879368,0.));
#117530=DIRECTION('center_axis',(-0.390328175340464,-0.920675120035551,
0.0011130511702119));
#117531=DIRECTION('ref_axis',(-0.429675165543775,0.18109501680736,-0.884637692506074));
#117532=DIRECTION('',(0.,0.,1.));
#117533=DIRECTION('center_axis',(0.,0.,1.));
#117534=DIRECTION('ref_axis',(1.,0.,0.));
#117535=DIRECTION('',(0.,0.,-1.));
#117536=DIRECTION('center_axis',(-0.419136065197508,-0.907922751606112,
0.00111174040842796));
#117537=DIRECTION('ref_axis',(0.422148005297344,-0.195965401885244,-0.885092437481774));
#117538=DIRECTION('center_axis',(0.,0.,-1.));
#117539=DIRECTION('ref_axis',(0.900968867902422,-0.433883739117553,0.));
#117540=DIRECTION('center_axis',(-0.448514061713085,-0.893775082200619,
0.00111305117023053));
#117541=DIRECTION('ref_axis',(-0.417189554269875,0.2082523200498,-0.884637692505796));
#117542=DIRECTION('',(0.,0.,1.));
#117543=DIRECTION('center_axis',(0.,0.,1.));
#117544=DIRECTION('ref_axis',(1.,0.,0.));
#117545=DIRECTION('',(0.,0.,-1.));
#117546=DIRECTION('center_axis',(-0.476445715620178,-0.879203187039515,
0.00111174040833913));
#117547=DIRECTION('ref_axis',(0.408725110535429,-0.22260988551223,-0.885092437483246));
#117548=DIRECTION('center_axis',(0.,0.,-1.));
#117549=DIRECTION('ref_axis',(0.871318704123392,-0.490717552003933,0.));
#117550=DIRECTION('center_axis',(-0.504856907600188,-0.86320233083876,0.00111305117023049));
#117551=DIRECTION('ref_axis',(-0.402989621631756,0.234553869839961,-0.884637692504786));
#117552=DIRECTION('',(0.,0.,1.));
#117553=DIRECTION('center_axis',(0.,0.,1.));
#117554=DIRECTION('ref_axis',(1.,0.,0.));
#117555=DIRECTION('',(0.,0.,-1.));
#117556=DIRECTION('center_axis',(-0.531797548400216,-0.846870787988808,
0.00111174040840245));
#117557=DIRECTION('ref_axis',(0.393622676626104,-0.248339617371704,-0.885092437482875));
#117558=DIRECTION('center_axis',(0.,0.,-1.));
#117559=DIRECTION('ref_axis',(0.838088104891844,-0.545534901210544,0.));
#117560=DIRECTION('center_axis',(-0.5591251881625,-0.829082495943161,0.00111305117022958));
#117561=DIRECTION('ref_axis',(-0.387133718195221,0.259891587466167,-0.88463769250505));
#117562=DIRECTION('',(0.,0.,1.));
#117563=DIRECTION('center_axis',(0.,0.,1.));
#117564=DIRECTION('ref_axis',(1.,0.,0.));
#117565=DIRECTION('',(0.,0.,-1.));
#117566=DIRECTION('center_axis',(-0.584964110983601,-0.811058415217073,
0.00111174040840115));
#117567=DIRECTION('ref_axis',(0.376902762709354,-0.273048868476615,-0.885092437480796));
#117568=DIRECTION('center_axis',(0.,0.,-1.));
#117569=DIRECTION('ref_axis',(0.80141362186796,-0.598110530491212,0.));
#117570=DIRECTION('center_axis',(-0.611095903394664,-0.791555783234102,
0.00111305117022297));
#117571=DIRECTION('ref_axis',(-0.369686999267188,0.284161354810104,-0.884637692507678));
#117572=DIRECTION('',(0.,0.,1.));
#117573=DIRECTION('center_axis',(0.,0.,1.));
#117574=DIRECTION('ref_axis',(1.,0.,0.));
#117575=DIRECTION('',(0.,0.,-1.));
#117576=DIRECTION('center_axis',(-0.635726930560603,-0.771913229445679,
0.00111174040844382));
#117577=DIRECTION('ref_axis',(0.358634074491183,-0.296636103209566,-0.885092437481248));
#117578=DIRECTION('center_axis',(0.,0.,-1.));
#117579=DIRECTION('ref_axis',(0.761445958369138,-0.648228395307784,0.));
#117580=DIRECTION('center_axis',(-0.660555494480139,-0.750776398023534,
0.00111305117020747));
#117581=DIRECTION('ref_axis',(-0.350721157168823,0.307263442200289,-0.884637692505464));
#117582=DIRECTION('',(0.,0.,1.));
#117583=DIRECTION('center_axis',(0.,0.,1.));
#117584=DIRECTION('ref_axis',(1.,0.,0.));
#117585=DIRECTION('',(0.,0.,-1.));
#117586=DIRECTION('center_axis',(-0.683877411816869,-0.729596086639673,
0.00111174040844086));
#117587=DIRECTION('ref_axis',(0.338891681935284,-0.319004396566983,-0.885092437480973));
#117588=DIRECTION('center_axis',(0.,0.,-1.));
#117589=DIRECTION('ref_axis',(0.718349350097731,-0.695682550603482,0.));
#117590=DIRECTION('center_axis',(-0.707300721350047,-0.70691191155249,0.00111305117022843));
#117591=DIRECTION('ref_axis',(-0.330314126603104,0.329102918196251,-0.884637692505322));
#117592=DIRECTION('',(0.,0.,1.));
#117593=DIRECTION('center_axis',(0.,0.,1.));
#117594=DIRECTION('ref_axis',(1.,0.,0.));
#117595=DIRECTION('',(0.,0.,-1.));
#117596=DIRECTION('center_axis',(-0.729217694096715,-0.684280877015816,
0.00111174040841947));
#117597=DIRECTION('ref_axis',(0.317756710764416,-0.340061832430751,-0.885092437482108));
#117598=DIRECTION('center_axis',(0.,0.,-1.));
#117599=DIRECTION('ref_axis',(0.672300890261321,-0.740277997075312,0.));
#117600=DIRECTION('center_axis',(-0.751139497840457,-0.660142572404688,
0.00111305117020688));
#117601=DIRECTION('ref_axis',(-0.308549764438105,0.349590039708122,-0.884637692505844));
#117602=DIRECTION('',(0.,0.,1.));
#117603=DIRECTION('center_axis',(0.,0.,1.));
#117604=DIRECTION('ref_axis',(1.,0.,0.));
#117605=DIRECTION('',(0.,0.,-1.));
#117606=DIRECTION('center_axis',(-0.771561464454877,-0.636153810490442,
0.00111174040844761));
#117607=DIRECTION('ref_axis',(0.295316009111902,-0.359721881283532,-0.885092437482129));
#117608=DIRECTION('center_axis',(0.,0.,-1.));
#117609=DIRECTION('ref_axis',(0.623489801858737,-0.781831482468027,0.));
#117610=DIRECTION('center_axis',(-0.791891681015239,-0.610660565826836,
0.00111305117025773));
#117611=DIRECTION('ref_axis',(-0.285517505108882,0.368640620761629,-0.884637692505175));
#117612=DIRECTION('',(0.,0.,1.));
#117613=DIRECTION('center_axis',(0.,0.,1.));
#117614=DIRECTION('ref_axis',(1.,0.,0.));
#117615=DIRECTION('',(0.,0.,-1.));
#117616=DIRECTION('center_axis',(-0.810734723256083,-0.58541265150332,0.00111174040839212));
#117617=DIRECTION('ref_axis',(0.27166179063417,-0.37790375576757,-0.885092437481081));
#117618=DIRECTION('center_axis',(0.,0.,-1.));
#117619=DIRECTION('ref_axis',(0.572116660122174,-0.820172254596953,0.));
#117620=DIRECTION('center_axis',(-0.829389811412563,-0.558669223997641,
0.0011130511702312));
#117621=DIRECTION('ref_axis',(-0.261311993106491,0.386176378429736,-0.884637692505585));
#117622=DIRECTION('',(0.,0.,1.));
#117623=DIRECTION('center_axis',(0.,0.,1.));
#117624=DIRECTION('ref_axis',(1.,0.,0.));
#117625=DIRECTION('',(0.,0.,-1.));
#117626=DIRECTION('center_axis',(-0.846576499177438,-0.532265906360475,
0.00111174040837876));
#117627=DIRECTION('ref_axis',(0.24689125558553,-0.394532742656637,-0.885092437481663));
#117628=DIRECTION('center_axis',(0.,0.,-1.));
#117629=DIRECTION('ref_axis',(0.518392568310529,-0.855142763005344,0.));
#117630=DIRECTION('center_axis',(-0.863479801171224,-0.504382190492881,
0.00111305117024995));
#117631=DIRECTION('ref_axis',(-0.236032694073528,0.402125254524605,-0.884637692505759));
#117632=DIRECTION('',(0.,0.,1.));
#117633=DIRECTION('center_axis',(0.,0.,1.));
#117634=DIRECTION('ref_axis',(1.,0.,0.));
#117635=DIRECTION('',(0.,0.,-1.));
#117636=DIRECTION('center_axis',(-0.878939510673589,-0.476931966437705,
0.00111174040842802));
#117637=DIRECTION('ref_axis',(0.221106191408716,-0.409540509877175,-0.885092437483383));
#117638=DIRECTION('center_axis',(0.,0.,-1.));
#117639=DIRECTION('ref_axis',(0.462538290240839,-0.886599306372998,0.));
#117640=DIRECTION('center_axis',(-0.894021567211032,-0.448022542377749,
0.00111305117021993));
#117641=DIRECTION('ref_axis',(-0.20978348607306,0.416421711695626,-0.884637692504406));
#117642=DIRECTION('',(0.,0.,1.));
#117643=DIRECTION('center_axis',(0.,0.,1.));
#117644=DIRECTION('ref_axis',(1.,0.,0.));
#117645=DIRECTION('',(0.,0.,-1.));
#117646=DIRECTION('center_axis',(-0.90769077118845,-0.41963821076325,0.00111174040843185));
#117647=DIRECTION('ref_axis',(0.194412554465174,-0.422865387297326,-0.885092437484475));
#117648=DIRECTION('center_axis',(0.,0.,-1.));
#117649=DIRECTION('ref_axis',(0.404783343122398,-0.914412623015811,0.));
#117650=DIRECTION('center_axis',(-0.920889606864142,-0.389821873535463,
0.00111305117023524));
#117651=DIRECTION('ref_axis',(-0.182672232726664,0.429007002724181,-0.884637692507091));
#117652=DIRECTION('',(0.,0.,1.));
#117653=DIRECTION('center_axis',(0.,0.,1.));
#117654=DIRECTION('ref_axis',(1.,0.,0.));
#117655=DIRECTION('',(0.,0.,-1.));
#117656=DIRECTION('center_axis',(-0.932712135625445,-0.360620071668627,
0.00111174040843274));
#117657=DIRECTION('ref_axis',(0.166920034636322,-0.434452620142095,-0.88509243748248));
#117658=DIRECTION('center_axis',(0.,0.,-1.));
#117659=DIRECTION('ref_axis',(0.345365054421312,-0.938468422049759,0.));
#117660=DIRECTION('center_axis',(-0.94397351359246,-0.330019342998253,0.00111305117020751));
#117661=DIRECTION('ref_axis',(-0.154810339995289,0.439829411961803,-0.884637692506869));
#117662=DIRECTION('',(0.,0.,1.));
#117663=DIRECTION('center_axis',(0.,0.,1.));
#117664=DIRECTION('ref_axis',(1.,0.,0.));
#117665=DIRECTION('',(0.,0.,-1.));
#117666=DIRECTION('center_axis',(-0.953900785830999,-0.300120067346832,
0.00111174040841854));
#117667=DIRECTION('ref_axis',(0.138741604580049,-0.444254593979597,-0.885092437481293));
#117668=DIRECTION('center_axis',(0.,0.,-1.));
#117669=DIRECTION('ref_axis',(0.284527586631037,-0.958667853036659,0.));
#117670=DIRECTION('center_axis',(-0.963178430671724,-0.268860692191788,
0.00111305117022739));
#117671=DIRECTION('ref_axis',(-0.126312298370754,0.44884446780464,-0.884637692505506));
#117672=DIRECTION('',(0.,0.,1.));
#117673=DIRECTION('center_axis',(0.,0.,1.));
#117674=DIRECTION('ref_axis',(1.,0.,0.));
#117675=DIRECTION('',(0.,0.,-1.));
#117676=DIRECTION('center_axis',(-0.971169653096488,-0.23838680529281,0.00111174040838518));
#117677=DIRECTION('ref_axis',(0.109993055508693,-0.452231030391505,-0.885092437483735));
#117678=DIRECTION('center_axis',(0.,0.,-1.));
#117679=DIRECTION('ref_axis',(0.222520933956318,-0.974927912181823,0.));
#117680=DIRECTION('center_axis',(-0.978425440978236,-0.206597235130671,
0.00111305117026458));
#117681=DIRECTION('ref_axis',(-0.0972952124163602,0.456015125444704,-0.884637692508355));
#117682=DIRECTION('',(0.,0.,1.));
#117683=DIRECTION('center_axis',(0.,0.,1.));
#117684=DIRECTION('ref_axis',(1.,0.,0.));
#117685=DIRECTION('',(0.,0.,-1.));
#117686=DIRECTION('center_axis',(-0.984447775942192,-0.175673960721946,
0.00111174040835251));
#117687=DIRECTION('ref_axis',(0.0807925213806202,-0.45834915250323,-0.885092437482398));
#117688=DIRECTION('center_axis',(0.,0.,-1.));
#117689=DIRECTION('ref_axis',(0.159599895033383,-0.98718178341445,0.));
#117690=DIRECTION('center_axis',(-0.989651891276182,-0.143484825715362,
0.00111305117019654));
#117691=DIRECTION('ref_axis',(-0.0678783195668276,0.461311919132307,-0.884637692504254));
#117692=DIRECTION('',(0.,0.,1.));
#117693=DIRECTION('center_axis',(0.,0.,1.));
#117694=DIRECTION('ref_axis',(1.,0.,0.));
#117695=DIRECTION('',(0.,0.,-1.));
#117696=DIRECTION('center_axis',(-0.993680591713171,-0.112239234164467,
0.00111174040842588));
#117697=DIRECTION('ref_axis',(0.0512599934516135,-0.462583819630076,-0.885092437481979));
#117698=DIRECTION('center_axis',(0.,0.,-1.));
#117699=DIRECTION('ref_axis',(0.0960230259076855,-0.995379112949198,0.));
#117700=DIRECTION('center_axis',(-0.996811649673197,-0.0797828063738752,
0.00111305117024778));
#117701=DIRECTION('ref_axis',(-0.0381825001404204,0.464713083179655,-0.884637692507326));
#117702=DIRECTION('',(0.,0.,1.));
#117703=DIRECTION('center_axis',(0.,0.,1.));
#117704=DIRECTION('ref_axis',(1.,0.,0.));
#117705=DIRECTION('',(0.,0.,-1.));
#117706=DIRECTION('center_axis',(-0.998830160788971,-0.0483432925186426,
0.00111174040839743));
#117707=DIRECTION('ref_axis',(0.0215168272142622,-0.464917630617288,-0.885092437482006));
#117708=DIRECTION('center_axis',(0.,0.,-1.));
#117709=DIRECTION('ref_axis',(0.0320515775716588,-0.999486216200688,0.));
#117710=DIRECTION('center_axis',(-0.999875295186283,-0.0157529423675828,
0.00111305117023515));
#117711=DIRECTION('ref_axis',(-0.00832978063163596,0.466204641497983,-0.884637692504884));
#117712=DIRECTION('',(0.,0.,1.));
#117713=DIRECTION('center_axis',(0.,0.,1.));
#117714=DIRECTION('ref_axis',(1.,0.,0.));
#117715=DIRECTION('',(0.,0.,-1.));
#117716=DIRECTION('center_axis',(0.,0.,1.));
#117717=DIRECTION('ref_axis',(1.,0.,0.));
#117718=DIRECTION('',(0.,0.,-1.));
#117719=DIRECTION('center_axis',(-0.999875322485693,0.0157513020857083,
0.00111174040835038));
#117720=DIRECTION('ref_axis',(0.00831475628145211,0.46534099533807,0.885092437480829));
#117721=DIRECTION('center_axis',(0.,0.,-1.));
#117722=DIRECTION('ref_axis',(-0.0320515775716516,-0.999486216200688,0.));
#117723=DIRECTION('center_axis',(-0.998830238638868,0.0483416538578713,
0.00111305117023196));
#117724=DIRECTION('ref_axis',(-0.0215571677330446,-0.465780464943283,0.884637692502727));
#117725=DIRECTION('',(0.,0.,1.));
#117726=DIRECTION('center_axis',(0.,0.,1.));
#117727=DIRECTION('ref_axis',(1.,0.,0.));
#117728=DIRECTION('',(0.,0.,-1.));
#117729=DIRECTION('center_axis',(-0.996811782009744,0.0797811712111581,
0.00111174040832857));
#117730=DIRECTION('ref_axis',(0.0381121726602704,0.463852174091903,0.885092437480588));
#117731=DIRECTION('center_axis',(0.,0.,-1.));
#117732=DIRECTION('ref_axis',(-0.0960230259076784,-0.995379112949199,0.));
#117733=DIRECTION('center_axis',(-0.99368077439247,0.112237603858393,0.00111305117019787));
#117734=DIRECTION('ref_axis',(-0.0513555330715939,-0.463442296544281,0.884637692502809));
#117735=DIRECTION('',(0.,0.,1.));
#117736=DIRECTION('center_axis',(0.,0.,1.));
#117737=DIRECTION('ref_axis',(1.,0.,0.));
#117738=DIRECTION('',(0.,0.,-1.));
#117739=DIRECTION('center_axis',(-0.989652128106054,0.143483202391165,0.00111174040836139));
#117740=DIRECTION('ref_axis',(0.0677529779465448,0.460457284765106,0.885092437481036));
#117741=DIRECTION('center_axis',(0.,0.,-1.));
#117742=DIRECTION('ref_axis',(-0.159599895033376,-0.987181783414451,0.));
#117743=DIRECTION('center_axis',(-0.984448062700232,0.17567234546978,0.00111305117020119));
#117744=DIRECTION('ref_axis',(-0.0809428675080601,-0.459199744335604,0.884637692505632));
#117745=DIRECTION('',(0.,0.,1.));
#117746=DIRECTION('center_axis',(0.,0.,1.));
#117747=DIRECTION('ref_axis',(1.,0.,0.));
#117748=DIRECTION('',(0.,0.,-1.));
#117749=DIRECTION('center_axis',(-0.978425781328237,0.206595630315586,0.0011117404084298));
#117750=DIRECTION('ref_axis',(0.0971153717123804,0.455170277682427,0.885092437484169));
#117751=DIRECTION('center_axis',(0.,0.,-1.));
#117752=DIRECTION('ref_axis',(-0.222520933956311,-0.974927912181824,0.));
#117753=DIRECTION('center_axis',(-0.971170042754915,0.238385211731998,0.00111305117020032));
#117754=DIRECTION('ref_axis',(-0.110197590340416,-0.453070241885056,0.884637692505459));
#117755=DIRECTION('',(0.,0.,1.));
#117756=DIRECTION('center_axis',(0.,0.,1.));
#117757=DIRECTION('ref_axis',(1.,0.,0.));
#117758=DIRECTION('',(0.,0.,-1.));
#117759=DIRECTION('center_axis',(-0.963178873143292,0.268859112480276,0.00111174040842531));
#117760=DIRECTION('ref_axis',(0.126078697585534,0.448012878301467,0.885092437483888));
#117761=DIRECTION('center_axis',(0.,0.,-1.));
#117762=DIRECTION('ref_axis',(-0.28452758663103,-0.958667853036661,0.));
#117763=DIRECTION('center_axis',(-0.953901276788603,0.300118502025727,0.00111305117022384));
#117764=DIRECTION('ref_axis',(-0.138999487636523,-0.445078976626565,0.884637692505714));
#117765=DIRECTION('',(0.,0.,1.));
#117766=DIRECTION('center_axis',(0.,0.,1.));
#117767=DIRECTION('ref_axis',(1.,0.,0.));
#117768=DIRECTION('',(0.,0.,-1.));
#117769=DIRECTION('center_axis',(-0.943974056367406,0.330017794881624,0.00111174040836656));
#117770=DIRECTION('ref_axis',(0.154523939047705,0.439014497908551,0.885092437481693));
#117771=DIRECTION('center_axis',(0.,0.,-1.));
#117772=DIRECTION('ref_axis',(-0.345365054421305,-0.938468422049761,0.));
#117773=DIRECTION('center_axis',(-0.932712725864767,0.360618541019467,0.00111305117019595));
#117774=DIRECTION('ref_axis',(-0.1672302062231,-0.435258786385151,0.884637692505302));
#117775=DIRECTION('',(0.,0.,1.));
#117776=DIRECTION('center_axis',(0.,0.,1.));
#117777=DIRECTION('ref_axis',(1.,0.,0.));
#117778=DIRECTION('',(0.,0.,-1.));
#117779=DIRECTION('center_axis',(-0.920890247712068,0.389820363375324,0.00111174040842408));
#117780=DIRECTION('ref_axis',(0.182334208498282,0.428212112771826,0.885092437481416));
#117781=DIRECTION('center_axis',(0.,0.,-1.));
#117782=DIRECTION('ref_axis',(-0.404783343122391,-0.914412623015814,0.));
#117783=DIRECTION('center_axis',(-0.90769145828413,0.41963672107565,0.00111305117023458));
#117784=DIRECTION('ref_axis',(-0.194773740019573,-0.423650024423506,0.884637692507363));
#117785=DIRECTION('',(0.,0.,1.));
#117786=DIRECTION('center_axis',(0.,0.,1.));
#117787=DIRECTION('ref_axis',(1.,0.,0.));
#117788=DIRECTION('',(0.,0.,-1.));
#117789=DIRECTION('center_axis',(-0.894022303498565,0.448021076379655,0.00111174040838539));
#117790=DIRECTION('ref_axis',(0.209395227575178,0.415650112211817,0.885092437481557));
#117791=DIRECTION('center_axis',(0.,0.,-1.));
#117792=DIRECTION('ref_axis',(-0.462538290240833,-0.886599306373001,0.));
#117793=DIRECTION('center_axis',(-0.878940291802164,0.476930523833209,0.0011130511702021));
#117794=DIRECTION('ref_axis',(-0.221516906744134,-0.410300393648285,0.884637692503871));
#117795=DIRECTION('',(0.,0.,1.));
#117796=DIRECTION('center_axis',(0.,0.,1.));
#117797=DIRECTION('ref_axis',(1.,0.,0.));
#117798=DIRECTION('',(0.,0.,-1.));
#117799=DIRECTION('center_axis',(-0.863480629872792,0.504380774680945,0.0011117404083924));
#117800=DIRECTION('ref_axis',(0.235595796745034,0.401380116180943,0.885092437483592));
#117801=DIRECTION('center_axis',(0.,0.,-1.));
#117802=DIRECTION('ref_axis',(-0.518392568310523,-0.855142763005347,0.));
#117803=DIRECTION('center_axis',(-0.846577371129116,0.532264516766999,0.00111305117022969));
#117804=DIRECTION('ref_axis',(-0.247349812978163,-0.39526475053625,0.884637692506477));
#117805=DIRECTION('',(0.,0.,1.));
#117806=DIRECTION('center_axis',(0.,0.,1.));
#117807=DIRECTION('ref_axis',(1.,0.,0.));
#117808=DIRECTION('',(0.,0.,-1.));
#117809=DIRECTION('center_axis',(-0.829390729122839,0.558667864189761,0.00111174040843866));
#117810=DIRECTION('ref_axis',(0.260828252254867,0.385460763163573,0.885092437481548));
#117811=DIRECTION('center_axis',(0.,0.,-1.));
#117812=DIRECTION('ref_axis',(-0.572116660122168,-0.820172254596957,0.));
#117813=DIRECTION('center_axis',(-0.810735682447803,0.585411320631048,0.0011130511702297));
#117814=DIRECTION('ref_axis',(-0.272166305775388,-0.378604879782754,0.884637692507653));
#117815=DIRECTION('',(0.,0.,1.));
#117816=DIRECTION('center_axis',(0.,0.,1.));
#117817=DIRECTION('ref_axis',(1.,0.,0.));
#117818=DIRECTION('',(0.,0.,-1.));
#117819=DIRECTION('center_axis',(-0.791892683963201,0.610659267610688,0.00111174040839811));
#117820=DIRECTION('ref_axis',(0.284988908527034,0.367957469186484,0.88509243748122));
#117821=DIRECTION('center_axis',(0.,0.,-1.));
#117822=DIRECTION('ref_axis',(-0.623489801858732,-0.781831482468031,0.));
#117823=DIRECTION('center_axis',(-0.771562506945055,0.636152543808287,0.00111305117023686));
#117824=DIRECTION('ref_axis',(-0.295864408845534,-0.360389240371643,0.884637692506278));
#117825=DIRECTION('',(0.,0.,1.));
#117826=DIRECTION('center_axis',(0.,0.,1.));
#117827=DIRECTION('ref_axis',(1.,0.,0.));
#117828=DIRECTION('',(0.,0.,-1.));
#117829=DIRECTION('center_axis',(-0.751140581904671,0.66014134111505,0.00111174040842861));
#117830=DIRECTION('ref_axis',(0.307978484240853,0.348942159037881,0.885092437483616));
#117831=DIRECTION('center_axis',(0.,0.,-1.));
#117832=DIRECTION('ref_axis',(-0.672300890261315,-0.740277997075317,0.));
#117833=DIRECTION('center_axis',(-0.729218815601615,0.684279679728743,0.00111305117020919));
#117834=DIRECTION('ref_axis',(-0.318346741595325,-0.340692684266245,0.88463769250643));
#117835=DIRECTION('',(0.,0.,1.));
#117836=DIRECTION('center_axis',(0.,0.,1.));
#117837=DIRECTION('ref_axis',(1.,0.,0.));
#117838=DIRECTION('',(0.,0.,-1.));
#117839=DIRECTION('center_axis',(-0.707301882075936,0.706910752248898,0.00111174040847968));
#117840=DIRECTION('ref_axis',(0.329702510302864,0.328492970711844,0.885092437484864));
#117841=DIRECTION('center_axis',(0.,0.,-1.));
#117842=DIRECTION('ref_axis',(-0.718349350097726,-0.695682550603488,0.));
#117843=DIRECTION('center_axis',(-0.683878607727921,0.729594963667659,0.00111305117020185));
#117844=DIRECTION('ref_axis',(-0.339520919299509,-0.319596148843642,0.884637692505994));
#117845=DIRECTION('',(0.,0.,1.));
#117846=DIRECTION('center_axis',(0.,0.,1.));
#117847=DIRECTION('ref_axis',(1.,0.,0.));
#117848=DIRECTION('',(0.,0.,-1.));
#117849=DIRECTION('center_axis',(-0.660556727098059,0.750775315469792,0.00111174040841113));
#117850=DIRECTION('ref_axis',(0.350071718034447,0.306693934312982,0.885092437482117));
#117851=DIRECTION('center_axis',(0.,0.,-1.));
#117852=DIRECTION('ref_axis',(-0.761445958369133,-0.64822839530779,0.));
#117853=DIRECTION('center_axis',(-0.635728195963607,0.771912185403204,0.0011130511702301));
#117854=DIRECTION('ref_axis',(-0.359299932716183,-0.297186324289664,0.884637692507699));
#117855=DIRECTION('',(0.,0.,1.));
#117856=DIRECTION('center_axis',(0.,0.,1.));
#117857=DIRECTION('ref_axis',(1.,0.,0.));
#117858=DIRECTION('',(0.,0.,-1.));
#117859=DIRECTION('center_axis',(-0.611097202839554,0.791554781878637,0.00111174040838367));
#117860=DIRECTION('ref_axis',(0.369002405982202,0.283634626748181,0.88509243748253));
#117861=DIRECTION('center_axis',(0.,0.,-1.));
#117862=DIRECTION('ref_axis',(-0.801413621867956,-0.598110530491217,0.));
#117863=DIRECTION('center_axis',(-0.584965440678792,0.811057454394299,0.00111305117022861));
#117864=DIRECTION('ref_axis',(-0.377602505645107,-0.273555297387249,0.884637692505757));
#117865=DIRECTION('',(0.,0.,1.));
#117866=DIRECTION('center_axis',(0.,0.,1.));
#117867=DIRECTION('ref_axis',(1.,0.,0.));
#117868=DIRECTION('',(0.,0.,-1.));
#117869=DIRECTION('center_axis',(-0.559126549094541,0.829081579900853,0.00111174040843286));
#117870=DIRECTION('ref_axis',(0.386416783897541,0.259409803665663,0.885092437480077));
#117871=DIRECTION('center_axis',(0.,0.,-1.));
#117872=DIRECTION('ref_axis',(-0.83808810489184,-0.54553490121055,0.));
#117873=DIRECTION('center_axis',(-0.531798936923542,0.846869914334004,0.0011130511702308));
#117874=DIRECTION('ref_axis',(-0.394353428875946,-0.248800173085565,0.884637692508282));
#117875=DIRECTION('',(0.,0.,1.));
#117876=DIRECTION('center_axis',(0.,0.,1.));
#117877=DIRECTION('ref_axis',(1.,0.,0.));
#117878=DIRECTION('',(0.,0.,-1.));
#117879=DIRECTION('center_axis',(-0.504858324427129,0.863201503873746,0.00111174040838814));
#117880=DIRECTION('ref_axis',(0.40224329235191,0.234119010050388,0.885092437483748));
#117881=DIRECTION('center_axis',(0.,0.,-1.));
#117882=DIRECTION('ref_axis',(-0.871318704123389,-0.490717552003939,0.));
#117883=DIRECTION('center_axis',(-0.476447157265943,0.879202404142695,0.00111305117023216));
#117884=DIRECTION('ref_axis',(-0.40948386928874,-0.223022675511165,0.88463769250477));
#117885=DIRECTION('',(0.,0.,1.));
#117886=DIRECTION('center_axis',(0.,0.,1.));
#117887=DIRECTION('ref_axis',(1.,0.,0.));
#117888=DIRECTION('',(0.,0.,-1.));
#117889=DIRECTION('center_axis',(-0.448515528612877,0.893774347711085,0.00111174040835437));
#117890=DIRECTION('ref_axis',(0.416416896846687,0.207866171210257,0.885092437481512));
#117891=DIRECTION('center_axis',(0.,0.,-1.));
#117892=DIRECTION('ref_axis',(-0.900968867902419,-0.433883739117559,0.));
#117893=DIRECTION('center_axis',(-0.419137554041534,0.907922062684443,0.00111305117022494));
#117894=DIRECTION('ref_axis',(-0.422931652641721,-0.196328729920749,0.884637692505496));
#117895=DIRECTION('',(0.,0.,1.));
#117896=DIRECTION('center_axis',(0.,0.,1.));
#117897=DIRECTION('ref_axis',(1.,0.,0.));
#117898=DIRECTION('',(0.,0.,-1.));
#117899=DIRECTION('center_axis',(-0.3903296862852,0.920674481039722,0.00111174040838437));
#117900=DIRECTION('ref_axis',(0.428879354989089,0.180759165683889,0.885092437480632));
#117901=DIRECTION('center_axis',(0.,0.,-1.));
#117902=DIRECTION('ref_axis',(-0.926916757346021,-0.375267004879375,0.));
#117903=DIRECTION('center_axis',(-0.360105624702816,0.932910874721957,0.00111305117018534));
#117904=DIRECTION('ref_axis',(-0.434641519118859,-0.168828027468166,0.884637692504258));
#117905=DIRECTION('',(0.,0.,1.));
#117906=DIRECTION('center_axis',(0.,0.,1.));
#117907=DIRECTION('ref_axis',(1.,0.,0.));
#117908=DIRECTION('',(0.,0.,-1.));
#117909=DIRECTION('center_axis',(-0.330539895551137,0.9437913654417,0.00111174040838563));
#117910=DIRECTION('ref_axis',(0.439579455865073,0.15290938197196,0.885092437481148));
#117911=DIRECTION('center_axis',(0.,0.,-1.));
#117912=DIRECTION('ref_axis',(-0.949055747010669,-0.315108218023621,0.));
#117913=DIRECTION('center_axis',(-0.299593944109832,0.954066155866462,0.00111305117019288));
#117914=DIRECTION('ref_axis',(-0.444565350358382,-0.140633574435332,0.884637692505961));
#117915=DIRECTION('',(0.,0.,1.));
#117916=DIRECTION('center_axis',(0.,0.,1.));
#117917=DIRECTION('ref_axis',(1.,0.,0.));
#117918=DIRECTION('',(0.,0.,-1.));
#117919=DIRECTION('center_axis',(-0.269391845485652,0.963030008680466,0.0011117404084127));
#117920=DIRECTION('ref_axis',(0.448473230466308,0.124431260810338,0.885092437482246));
#117921=DIRECTION('center_axis',(0.,0.,-1.));
#117922=DIRECTION('ref_axis',(-0.967294863039029,-0.253654583909508,0.));
#117923=DIRECTION('center_axis',(-0.237851167737863,0.971300974529948,0.00111305117023085));
#117924=DIRECTION('ref_axis',(-0.452662367215052,-0.11186122788,0.884637692507189));
#117925=DIRECTION('',(0.,0.,1.));
#117926=DIRECTION('center_axis',(0.,0.,1.));
#117927=DIRECTION('ref_axis',(1.,0.,0.));
#117928=DIRECTION('',(0.,0.,-1.));
#117929=DIRECTION('center_axis',(-0.207136806542691,0.978311355044272,0.00111174040845613));
#117930=DIRECTION('ref_axis',(0.455524132369569,0.095441824908564,0.885092437481574));
#117931=DIRECTION('center_axis',(0.,0.,-1.));
#117932=DIRECTION('ref_axis',(-0.981559156991065,-0.191158628701373,0.));
#117933=DIRECTION('center_axis',(-0.175131009898648,0.984544509145713,0.00111305117023712));
#117934=DIRECTION('ref_axis',(-0.458899297314163,-0.0826292195462833,0.884637692505661));
#117935=DIRECTION('',(0.,0.,1.));
#117936=DIRECTION('center_axis',(0.,0.,1.));
#117937=DIRECTION('ref_axis',(1.,0.,0.));
#117938=DIRECTION('',(0.,0.,-1.));
#117939=DIRECTION('center_axis',(-0.144030598031138,0.98957261020304,0.00111174040835033));
#117940=DIRECTION('ref_axis',(0.460703187898021,0.0660601980753236,0.885092437483707));
#117941=DIRECTION('center_axis',(0.,0.,-1.));
#117942=DIRECTION('ref_axis',(-0.991790013823246,-0.127877161684506,0.));
#117943=DIRECTION('center_axis',(-0.111691201174306,0.993742339189255,0.00111305117022436));
#117944=DIRECTION('ref_axis',(-0.463250511765016,-0.0530576700249386,0.884637692505229));
#117945=DIRECTION('',(0.,0.,1.));
#117946=DIRECTION('center_axis',(0.,0.,1.));
#117947=DIRECTION('ref_axis',(1.,0.,0.));
#117948=DIRECTION('',(0.,0.,-1.));
#117949=DIRECTION('center_axis',(-0.0803325368976281,0.996767499243859,
0.00111174040834946));
#117950=DIRECTION('ref_axis',(0.463989115215465,0.0364071157193635,0.885092437481288));
#117951=DIRECTION('center_axis',(0.,0.,-1.));
#117952=DIRECTION('ref_axis',(-0.997945392750336,-0.0640702199807131,0.));
#117953=DIRECTION('center_axis',(-0.0477924293466603,0.998856668804007,
0.00111305117023892));
#117954=DIRECTION('ref_axis',(-0.465698130493318,-0.0232680951564189,0.884637692506271));
#117955=DIRECTION('',(0.,0.,1.));
#117956=DIRECTION('center_axis',(0.,0.,1.));
#117957=DIRECTION('ref_axis',(1.,0.,0.));
#117958=DIRECTION('',(0.,0.,-1.));
#117959=DIRECTION('center_axis',(-0.0163043721387329,0.999866456824323,
0.00111174040837426));
#117960=DIRECTION('ref_axis',(0.465368411727477,0.00660442871490491,0.885092437481868));
#117961=DIRECTION('center_axis',(0.,0.,-1.));
#117962=DIRECTION('ref_axis',(-1.,0.,0.));
#117963=DIRECTION('center_axis',(0.016302731824642,0.99986648211256,0.0011130511702149));
#117964=DIRECTION('ref_axis',(-0.466232095711021,0.00661709330587505,0.884637692507555));
#117965=DIRECTION('',(0.,0.,1.));
#117966=DIRECTION('center_axis',(0.,0.,1.));
#117967=DIRECTION('ref_axis',(1.,0.,0.));
#117968=DIRECTION('',(0.,0.,-1.));
#117969=DIRECTION('center_axis',(0.0477907907825636,0.998856748663011,0.00111174040842402));
#117970=DIRECTION('ref_axis',(0.464835409616116,-0.0232253973037494,0.885092437481589));
#117971=DIRECTION('center_axis',(0.,0.,-1.));
#117972=DIRECTION('ref_axis',(-0.997945392750337,0.0640702199806987,0.));
#117973=DIRECTION('center_axis',(0.0803309015739928,0.99676762957542,0.00111305117017054));
#117974=DIRECTION('ref_axis',(-0.464850213248175,0.0364750907127227,0.88463769250503));
#117975=DIRECTION('',(0.,0.,1.));
#117976=DIRECTION('center_axis',(0.,0.,1.));
#117977=DIRECTION('ref_axis',(1.,0.,0.));
#117978=DIRECTION('',(0.,0.,-1.));
#117979=DIRECTION('center_axis',(0.111689571093429,0.99374252386734,0.00111174040844294));
#117980=DIRECTION('ref_axis',(0.462392299099744,-0.0529597851830843,0.885092437481314));
#117981=DIRECTION('center_axis',(0.,0.,-1.));
#117982=DIRECTION('ref_axis',(-0.991790013823248,0.127877161684492,0.));
#117983=DIRECTION('center_axis',(0.144028974417742,0.989572845042378,0.00111305117021856));
#117984=DIRECTION('ref_axis',(-0.461558161541436,0.066183204147324,0.884637692506533));
#117985=DIRECTION('',(0.,0.,1.));
#117986=DIRECTION('center_axis',(0.,0.,1.));
#117987=DIRECTION('ref_axis',(1.,0.,0.));
#117988=DIRECTION('',(0.,0.,-1.));
#117989=DIRECTION('center_axis',(0.175129394999254,0.984544797884007,0.00111174040835243));
#117990=DIRECTION('ref_axis',(0.45804911944098,-0.0824765499447419,0.885092437482411));
#117991=DIRECTION('center_axis',(0.,0.,-1.));
#117992=DIRECTION('ref_axis',(-0.981559156991068,0.191158628701359,0.));
#117993=DIRECTION('center_axis',(0.207135201311576,0.978311693426336,0.00111305117018698));
#117994=DIRECTION('ref_axis',(-0.456369468348504,0.0956193566003131,0.884637692506173));
#117995=DIRECTION('',(0.,0.,1.));
#117996=DIRECTION('center_axis',(0.,0.,1.));
#117997=DIRECTION('ref_axis',(1.,0.,0.));
#117998=DIRECTION('',(0.,0.,-1.));
#117999=DIRECTION('center_axis',(0.237849574656022,0.971301366141948,0.00111174040843417));
#118000=DIRECTION('ref_axis',(0.45182371770191,-0.111654400872119,0.885092437482048));
#118001=DIRECTION('center_axis',(0.,0.,-1.));
#118002=DIRECTION('ref_axis',(-0.967294863039033,0.253654583909494,0.));
#118003=DIRECTION('center_axis',(0.269390265232794,0.96303044921482,0.00111305117023979));
#118004=DIRECTION('ref_axis',(-0.449305455119629,0.12466258860685,0.884637692505571));
#118005=DIRECTION('',(0.,0.,1.));
#118006=DIRECTION('center_axis',(0.,0.,1.));
#118007=DIRECTION('ref_axis',(1.,0.,0.));
#118008=DIRECTION('',(0.,0.,-1.));
#118009=DIRECTION('center_axis',(0.299592379391923,0.954066648742922,0.00111174040846479));
#118010=DIRECTION('ref_axis',(0.443741675387824,-0.14037343991558,0.885092437483382));
#118011=DIRECTION('center_axis',(0.,0.,-1.));
#118012=DIRECTION('ref_axis',(-0.949055747010673,0.315108218023608,0.));
#118013=DIRECTION('center_axis',(0.330538346770186,0.943791906318085,0.00111305117021856));
#118014=DIRECTION('ref_axis',(-0.440395149399512,0.153193555296853,0.884637692505181));
#118015=DIRECTION('',(0.,0.,1.));
#118016=DIRECTION('center_axis',(0.,0.,1.));
#118017=DIRECTION('ref_axis',(1.,0.,0.));
#118018=DIRECTION('',(0.,0.,-1.));
#118019=DIRECTION('center_axis',(0.360104094778424,0.932911466837597,0.00111174040835927));
#118020=DIRECTION('ref_axis',(0.433836203352636,-0.168515654385946,0.885092437481785));
#118021=DIRECTION('center_axis',(0.,0.,-1.));
#118022=DIRECTION('ref_axis',(-0.926916757346027,0.375267004879361,0.));
#118023=DIRECTION('center_axis',(0.390328175340436,0.920675120035563,0.00111305117023836));
#118024=DIRECTION('ref_axis',(-0.429675165541279,0.181095016806259,0.884637692507512));
#118025=DIRECTION('',(0.,0.,1.));
#118026=DIRECTION('center_axis',(0.,0.,1.));
#118027=DIRECTION('ref_axis',(1.,0.,0.));
#118028=DIRECTION('',(0.,0.,-1.));
#118029=DIRECTION('center_axis',(0.419136065197424,0.907922751606151,0.00111174040833283));
#118030=DIRECTION('ref_axis',(0.422148005295169,-0.195965401884101,0.885092437483065));
#118031=DIRECTION('center_axis',(0.,0.,-1.));
#118032=DIRECTION('ref_axis',(-0.900968867902425,0.433883739117546,0.));
#118033=DIRECTION('center_axis',(0.448514061713074,0.893775082200625,0.00111305117023013));
#118034=DIRECTION('ref_axis',(-0.41718955427032,0.208252320050018,0.884637692505534));
#118035=DIRECTION('',(0.,0.,1.));
#118036=DIRECTION('center_axis',(0.,0.,1.));
#118037=DIRECTION('ref_axis',(1.,0.,0.));
#118038=DIRECTION('',(0.,0.,-1.));
#118039=DIRECTION('center_axis',(0.476445715620265,0.879203187039468,0.00111174040839801));
#118040=DIRECTION('ref_axis',(0.408725110535094,-0.222609885512161,0.885092437483418));
#118041=DIRECTION('center_axis',(0.,0.,-1.));
#118042=DIRECTION('ref_axis',(-0.871318704123396,0.490717552003926,0.));
#118043=DIRECTION('center_axis',(0.504856907600187,0.86320233083876,0.00111305117021984));
#118044=DIRECTION('ref_axis',(-0.402989621629229,0.234553869838492,0.884637692506327));
#118045=DIRECTION('',(0.,0.,1.));
#118046=DIRECTION('center_axis',(0.,0.,1.));
#118047=DIRECTION('ref_axis',(1.,0.,0.));
#118048=DIRECTION('',(0.,0.,-1.));
#118049=DIRECTION('center_axis',(0.531797548400194,0.846870787988822,0.00111174040839575));
#118050=DIRECTION('ref_axis',(0.39362267662406,-0.248339617370401,0.885092437484149));
#118051=DIRECTION('center_axis',(0.,0.,-1.));
#118052=DIRECTION('ref_axis',(-0.838088104891848,0.545534901210538,0.));
#118053=DIRECTION('center_axis',(0.559125188162458,0.82908249594319,0.00111305117024803));
#118054=DIRECTION('ref_axis',(-0.387133718194512,0.259891587465639,0.884637692505515));
#118055=DIRECTION('',(0.,0.,1.));
#118056=DIRECTION('center_axis',(0.,0.,1.));
#118057=DIRECTION('ref_axis',(1.,0.,0.));
#118058=DIRECTION('',(0.,0.,-1.));
#118059=DIRECTION('center_axis',(0.584964110983611,0.811058415217065,0.00111174040840853));
#118060=DIRECTION('ref_axis',(0.376902762707542,-0.273048868475325,0.885092437481966));
#118061=DIRECTION('center_axis',(0.,0.,-1.));
#118062=DIRECTION('ref_axis',(-0.801413621867964,0.598110530491206,0.));
#118063=DIRECTION('center_axis',(0.61109590339468,0.791555783234089,0.00111305117019012));
#118064=DIRECTION('ref_axis',(-0.369686999269125,0.28416135481165,0.884637692506372));
#118065=DIRECTION('',(0.,0.,1.));
#118066=DIRECTION('center_axis',(0.,0.,1.));
#118067=DIRECTION('ref_axis',(1.,0.,0.));
#118068=DIRECTION('',(0.,0.,-1.));
#118069=DIRECTION('center_axis',(0.635726930560454,0.771913229445802,0.00111174040830727));
#118070=DIRECTION('ref_axis',(0.358634074488608,-0.296636103207175,0.885092437483093));
#118071=DIRECTION('center_axis',(0.,0.,-1.));
#118072=DIRECTION('ref_axis',(-0.761445958369143,0.648228395307779,0.));
#118073=DIRECTION('center_axis',(0.660555494480137,0.750776398023536,0.0011130511702097));
#118074=DIRECTION('ref_axis',(-0.350721157168176,0.307263442199714,0.88463769250592));
#118075=DIRECTION('',(0.,0.,1.));
#118076=DIRECTION('center_axis',(0.,0.,1.));
#118077=DIRECTION('ref_axis',(1.,0.,0.));
#118078=DIRECTION('',(0.,0.,-1.));
#118079=DIRECTION('center_axis',(0.683877411816847,0.729596086639694,0.00111174040843297));
#118080=DIRECTION('ref_axis',(0.338891681935678,-0.319004396567322,0.8850924374807));
#118081=DIRECTION('center_axis',(0.,0.,-1.));
#118082=DIRECTION('ref_axis',(-0.718349350097736,0.695682550603478,0.));
#118083=DIRECTION('center_axis',(0.707300721350063,0.706911911552474,0.00111305117020991));
#118084=DIRECTION('ref_axis',(-0.330314126601671,0.329102918194854,0.884637692506377));
#118085=DIRECTION('',(0.,0.,1.));
#118086=DIRECTION('center_axis',(0.,0.,1.));
#118087=DIRECTION('ref_axis',(1.,0.,0.));
#118088=DIRECTION('',(0.,0.,-1.));
#118089=DIRECTION('center_axis',(0.729217694096672,0.684280877015861,0.00111174040837837));
#118090=DIRECTION('ref_axis',(0.317756710765229,-0.34006183243152,0.885092437481521));
#118091=DIRECTION('center_axis',(0.,0.,-1.));
#118092=DIRECTION('ref_axis',(-0.672300890261326,0.740277997075307,0.));
#118093=DIRECTION('center_axis',(0.751139497840413,0.660142572404738,0.00111305117025266));
#118094=DIRECTION('ref_axis',(-0.308549764436205,0.349590039705849,0.884637692507405));
#118095=DIRECTION('',(0.,0.,1.));
#118096=DIRECTION('center_axis',(0.,0.,1.));
#118097=DIRECTION('ref_axis',(1.,0.,0.));
#118098=DIRECTION('',(0.,0.,-1.));
#118099=DIRECTION('center_axis',(0.77156146445479,0.636153810490548,0.00111174040834627));
#118100=DIRECTION('ref_axis',(0.29531600911316,-0.359721881284815,0.885092437481187));
#118101=DIRECTION('center_axis',(0.,0.,-1.));
#118102=DIRECTION('ref_axis',(-0.623489801858743,0.781831482468022,0.));
#118103=DIRECTION('center_axis',(0.791891681015259,0.610660565826811,0.00111305117023235));
#118104=DIRECTION('ref_axis',(-0.285517505107271,0.368640620759599,0.884637692506541));
#118105=DIRECTION('',(0.,0.,1.));
#118106=DIRECTION('center_axis',(0.,0.,1.));
#118107=DIRECTION('ref_axis',(1.,0.,0.));
#118108=DIRECTION('',(0.,0.,-1.));
#118109=DIRECTION('center_axis',(0.810734723256142,0.585412651503238,0.0011117404084541));
#118110=DIRECTION('ref_axis',(0.271661790633098,-0.37790375576626,0.885092437481969));
#118111=DIRECTION('center_axis',(0.,0.,-1.));
#118112=DIRECTION('ref_axis',(-0.57211666012218,0.820172254596949,0.));
#118113=DIRECTION('center_axis',(0.829389811412555,0.558669223997653,0.0011130511702394));
#118114=DIRECTION('ref_axis',(-0.2613119931069,0.386176378430318,0.88463769250521));
#118115=DIRECTION('',(0.,0.,1.));
#118116=DIRECTION('center_axis',(0.,0.,1.));
#118117=DIRECTION('ref_axis',(1.,0.,0.));
#118118=DIRECTION('',(0.,0.,-1.));
#118119=DIRECTION('center_axis',(0.846576499177451,0.532265906360454,0.00111174040841854));
#118120=DIRECTION('ref_axis',(0.246891255584571,-0.394532742655201,0.885092437482571));
#118121=DIRECTION('center_axis',(0.,0.,-1.));
#118122=DIRECTION('ref_axis',(-0.518392568310535,0.85514276300534,0.));
#118123=DIRECTION('center_axis',(0.863479801171241,0.50438219049285,0.00111305117019087));
#118124=DIRECTION('ref_axis',(-0.236032694072651,0.402125254523237,0.884637692506615));
#118125=DIRECTION('',(0.,0.,1.));
#118126=DIRECTION('center_axis',(0.,0.,1.));
#118127=DIRECTION('ref_axis',(1.,0.,0.));
#118128=DIRECTION('',(0.,0.,-1.));
#118129=DIRECTION('center_axis',(0.878939510673582,0.476931966437718,0.00111174040838566));
#118130=DIRECTION('ref_axis',(0.221106191409744,-0.409540509878976,0.885092437482293));
#118131=DIRECTION('center_axis',(0.,0.,-1.));
#118132=DIRECTION('ref_axis',(-0.462538290240846,0.886599306372994,0.));
#118133=DIRECTION('center_axis',(0.894021567211031,0.448022542377751,0.00111305117023196));
#118134=DIRECTION('ref_axis',(-0.209783486071203,0.416421711691889,0.884637692506605));
#118135=DIRECTION('',(0.,0.,1.));
#118136=DIRECTION('center_axis',(0.,0.,1.));
#118137=DIRECTION('ref_axis',(1.,0.,0.));
#118138=DIRECTION('',(0.,0.,-1.));
#118139=DIRECTION('center_axis',(0.90769077118846,0.419638210763228,0.00111174040845409));
#118140=DIRECTION('ref_axis',(0.194412554467475,-0.422865387302372,0.885092437481558));
#118141=DIRECTION('center_axis',(0.,0.,-1.));
#118142=DIRECTION('ref_axis',(-0.404783343122404,0.914412623015808,0.));
#118143=DIRECTION('center_axis',(0.92088960686414,0.389821873535468,0.0011130511702349));
#118144=DIRECTION('ref_axis',(-0.182672232728254,0.429007002727937,0.884637692504941));
#118145=DIRECTION('',(0.,0.,1.));
#118146=DIRECTION('center_axis',(0.,0.,1.));
#118147=DIRECTION('ref_axis',(1.,0.,0.));
#118148=DIRECTION('',(0.,0.,-1.));
#118149=DIRECTION('center_axis',(0.932712135625401,0.360620071668741,0.00111174040835477));
#118150=DIRECTION('ref_axis',(0.166920034636893,-0.434452620143221,0.88509243748182));
#118151=DIRECTION('center_axis',(0.,0.,-1.));
#118152=DIRECTION('ref_axis',(-0.345365054421319,0.938468422049756,0.));
#118153=DIRECTION('center_axis',(0.943973513592441,0.330019342998308,0.00111305117024185));
#118154=DIRECTION('ref_axis',(-0.154810339995216,0.439829411961417,0.884637692507074));
#118155=DIRECTION('',(0.,0.,1.));
#118156=DIRECTION('center_axis',(0.,0.,1.));
#118157=DIRECTION('ref_axis',(1.,0.,0.));
#118158=DIRECTION('',(0.,0.,-1.));
#118159=DIRECTION('center_axis',(0.953900785830986,0.300120067346872,0.00111174040840669));
#118160=DIRECTION('ref_axis',(0.13874160457993,-0.44425459397912,0.885092437481551));
#118161=DIRECTION('center_axis',(0.,0.,-1.));
#118162=DIRECTION('ref_axis',(-0.284527586631043,0.958667853036657,0.));
#118163=DIRECTION('center_axis',(0.963178430671713,0.268860692191828,0.0011130511702472));
#118164=DIRECTION('ref_axis',(-0.126312298370385,0.448844467803181,0.884637692506299));
#118165=DIRECTION('',(0.,0.,1.));
#118166=DIRECTION('center_axis',(0.,0.,1.));
#118167=DIRECTION('ref_axis',(1.,0.,0.));
#118168=DIRECTION('',(0.,0.,-1.));
#118169=DIRECTION('center_axis',(0.971169653096497,0.238386805292774,0.00111174040839145));
#118170=DIRECTION('ref_axis',(0.109993055509511,-0.452231030394927,0.885092437481884));
#118171=DIRECTION('center_axis',(0.,0.,-1.));
#118172=DIRECTION('ref_axis',(-0.222520933956325,0.974927912181821,0.));
#118173=DIRECTION('center_axis',(0.978425440978244,0.20659723513063,0.0011130511702072));
#118174=DIRECTION('ref_axis',(-0.0972952124173608,0.456015125449797,0.884637692505619));
#118175=DIRECTION('',(0.,0.,1.));
#118176=DIRECTION('center_axis',(0.,0.,1.));
#118177=DIRECTION('ref_axis',(1.,0.,0.));
#118178=DIRECTION('',(0.,0.,-1.));
#118179=DIRECTION('center_axis',(0.984447775942196,0.175673960721926,0.00111174040839208));
#118180=DIRECTION('ref_axis',(0.080792521380986,-0.458349152505527,0.885092437481175));
#118181=DIRECTION('center_axis',(0.,0.,-1.));
#118182=DIRECTION('ref_axis',(-0.15959989503339,0.987181783414448,0.));
#118183=DIRECTION('center_axis',(0.989651891276176,0.143484825715403,0.00111305117024872));
#118184=DIRECTION('ref_axis',(-0.0678783195662134,0.461311919127594,0.884637692506759));
#118185=DIRECTION('',(0.,0.,1.));
#118186=DIRECTION('center_axis',(0.,0.,1.));
#118187=DIRECTION('ref_axis',(1.,0.,0.));
#118188=DIRECTION('',(0.,0.,-1.));
#118189=DIRECTION('center_axis',(0.993680591713164,0.112239234164531,0.00111174040837401));
#118190=DIRECTION('ref_axis',(0.0512599934515281,-0.46258381962865,0.885092437482728));
#118191=DIRECTION('center_axis',(0.,0.,-1.));
#118192=DIRECTION('ref_axis',(-0.0960230259076927,0.995379112949197,0.));
#118193=DIRECTION('center_axis',(0.996811649673195,0.0797828063739037,0.00111305117025078));
#118194=DIRECTION('ref_axis',(-0.0381825001405106,0.464713083180589,0.884637692506832));
#118195=DIRECTION('',(0.,0.,1.));
#118196=DIRECTION('center_axis',(0.,0.,1.));
#118197=DIRECTION('ref_axis',(1.,0.,0.));
#118198=DIRECTION('',(0.,0.,-1.));
#118199=DIRECTION('center_axis',(0.998830160788972,0.048343292518622,0.00111174040843717));
#118200=DIRECTION('ref_axis',(0.0215168272142989,-0.464917630618952,0.885092437481131));
#118201=DIRECTION('center_axis',(0.,0.,-1.));
#118202=DIRECTION('ref_axis',(-0.0320515775716664,0.999486216200688,0.));
#118203=DIRECTION('center_axis',(0.999875295186283,0.0157529423675647,0.00111305117019787));
#118204=DIRECTION('ref_axis',(-0.00832978063156192,0.466204641495832,0.884637692506019));
#118205=DIRECTION('',(0.,0.,1.));
#118206=DIRECTION('center_axis',(0.,0.,1.));
#118207=DIRECTION('ref_axis',(1.,0.,0.));
#118208=DIRECTION('center_axis',(-0.361755711857553,-0.932272915508417,
0.000126284884494543));
#118209=DIRECTION('ref_axis',(0.931874611709867,-0.361597189609634,0.029277645345883));
#118210=DIRECTION('center_axis',(-0.363356221121508,0.931650066446612,-0.000640517230190088));
#118211=DIRECTION('ref_axis',(0.727365888769779,0.283252870473557,-0.625065336762998));
#118212=DIRECTION('center_axis',(0.,0.,1.));
#118213=DIRECTION('ref_axis',(1.,0.,0.));
#118214=DIRECTION('center_axis',(0.14057796820823,0.990069403926878,-0.000640517230188182));
#118215=DIRECTION('ref_axis',(0.772764658753017,-0.110127684298105,-0.625065336851653));
#118216=DIRECTION('center_axis',(-0.772687200962828,-0.63478695128394,0.000126284884494751));
#118217=DIRECTION('ref_axis',(0.634517691386154,-0.772353622901137,0.0292776452173503));
#118218=DIRECTION('center_axis',(0.,0.,1.));
#118219=DIRECTION('ref_axis',(1.,0.,0.));
#118220=DIRECTION('center_axis',(-0.811770571847688,-0.583976474469825,
0.000126284884456442));
#118221=DIRECTION('ref_axis',(0.583729140212326,-0.811420427613029,0.0292776453846311));
#118222=DIRECTION('center_axis',(0.203723100201392,0.979028338804353,-0.000640517230187342));
#118223=DIRECTION('ref_axis',(0.764121025944983,-0.159412616843564,-0.625065336824778));
#118224=DIRECTION('center_axis',(0.,0.,1.));
#118225=DIRECTION('ref_axis',(1.,0.,0.));
#118226=DIRECTION('center_axis',(-0.847518203328563,-0.530766313059573,
0.000126284884449419));
#118227=DIRECTION('ref_axis',(0.530541920796553,-0.84715293174505,0.029277645282204));
#118228=DIRECTION('center_axis',(0.266031090277401,0.963964236236747,-0.000640517230154732));
#118229=DIRECTION('ref_axis',(0.752337455993016,-0.208042488770549,-0.62506533672578));
#118230=DIRECTION('center_axis',(0.,0.,1.));
#118231=DIRECTION('ref_axis',(1.,0.,0.));
#118232=DIRECTION('center_axis',(-0.879783200719837,-0.475375119020008,
0.000126284884469973));
#118233=DIRECTION('ref_axis',(0.47517459082445,-0.879404302762036,0.0292776453703841));
#118234=DIRECTION('center_axis',(0.327245901539894,0.944938997852782,-0.000640517230163509));
#118235=DIRECTION('ref_axis',(0.737462369919026,-0.255817469448713,-0.625065336807497));
#118236=DIRECTION('center_axis',(0.,0.,1.));
#118237=DIRECTION('ref_axis',(1.,0.,0.));
#118238=DIRECTION('center_axis',(-0.908432980226483,-0.418030506648687,
0.000126284884465053));
#118239=DIRECTION('ref_axis',(0.417854666536792,-0.908042012872807,0.0292776452490184));
#118240=DIRECTION('center_axis',(0.387115989199014,0.922030802437829,-0.00064051723013517));
#118241=DIRECTION('ref_axis',(0.719556892879681,-0.302541241304193,-0.625065336760452));
#118242=DIRECTION('center_axis',(0.,0.,1.));
#118243=DIRECTION('ref_axis',(1.,0.,0.));
#118244=DIRECTION('center_axis',(-0.933349813759075,-0.358968117258382,
0.000126284884510345));
#118245=DIRECTION('ref_axis',(0.358817687792907,-0.932948383574305,0.0292776452783369));
#118246=DIRECTION('center_axis',(0.445395334222083,0.895333784680818,-0.000640517230242528));
#118247=DIRECTION('ref_axis',(0.698694602122832,-0.348021806259692,-0.625065336850603));
#118248=DIRECTION('center_axis',(0.,0.,1.));
#118249=DIRECTION('ref_axis',(1.,0.,0.));
#118250=DIRECTION('center_axis',(-0.954431312704106,-0.298430650875619,
0.000126284884428326));
#118251=DIRECTION('ref_axis',(0.298306250203974,-0.954021069252139,0.0292776452647741));
#118252=DIRECTION('center_axis',(0.501844454280421,0.864957648353759,-0.000640517230093126));
#118253=DIRECTION('ref_axis',(0.674961225544822,-0.39207227505014,-0.625065336703324));
#118254=DIRECTION('center_axis',(0.,0.,1.));
#118255=DIRECTION('ref_axis',(1.,0.,0.));
#118256=DIRECTION('center_axis',(-0.971590848660291,-0.236666868935438,
0.000126284884461063));
#118257=DIRECTION('ref_axis',(0.236569008246495,-0.971173477718955,0.0292776452697189));
#118258=DIRECTION('center_axis',(0.556231387830254,0.831027215517102,-0.000640517230226317));
#118259=DIRECTION('ref_axis',(0.648454288320632,-0.434511634652827,-0.625065336832807));
#118260=DIRECTION('center_axis',(0.,0.,1.));
#118261=DIRECTION('ref_axis',(1.,0.,0.));
#118262=DIRECTION('center_axis',(-0.984757909413755,-0.17393057206592,0.000126284884500403));
#118263=DIRECTION('ref_axis',(0.173859653489982,-0.984335126048153,0.0292776453306897));
#118264=DIRECTION('center_axis',(0.608332647296512,0.793681913596937,-0.000640517230195856));
#118265=DIRECTION('ref_axis',(0.619282713433725,-0.475165492807053,-0.625065336814955));
#118266=DIRECTION('center_axis',(0.,0.,1.));
#118267=DIRECTION('ref_axis',(1.,0.,0.));
#118268=DIRECTION('center_axis',(-0.993878388687547,-0.110479557167707,
0.000126284884483687));
#118269=DIRECTION('ref_axis',(0.110435872124621,-0.993451930205023,0.0292776453969324));
#118270=DIRECTION('center_axis',(0.657934137428239,0.753075202449421,-0.000640517230047103));
#118271=DIRECTION('ref_axis',(0.58756637302375,-0.513866794015637,-0.625065336824725));
#118272=DIRECTION('center_axis',(0.,0.,1.));
#118273=DIRECTION('ref_axis',(1.,0.,0.));
#118274=DIRECTION('center_axis',(-0.998914808475977,-0.046574558071235,
0.000126284884446421));
#118275=DIRECTION('ref_axis',(0.0465582860727343,-0.998486427292382,0.0292776452411194));
#118276=DIRECTION('center_axis',(0.704832035062552,0.709373943761159,-0.000640517230105989));
#118277=DIRECTION('ref_axis',(0.553435596395122,-0.550456506382256,-0.625065336764259));
#118278=DIRECTION('center_axis',(0.,0.,1.));
#118279=DIRECTION('ref_axis',(1.,0.,0.));
#118280=DIRECTION('center_axis',(-0.999846473049816,0.0175218258743651,
0.000126284884492773));
#118281=DIRECTION('ref_axis',(0.0175106179635939,0.999417929469137,-0.0292776452973284));
#118282=DIRECTION('center_axis',(0.748833626678851,0.662757715377707,-0.000640517230120071));
#118283=DIRECTION('ref_axis',(0.517030634109736,-0.58478427481117,-0.625065336845404));
#118284=DIRECTION('center_axis',(0.,0.,1.));
#118285=DIRECTION('ref_axis',(1.,0.,0.));
#118286=DIRECTION('center_axis',(-0.996669553999495,0.0815462088792301,
0.000126284884460216));
#118287=DIRECTION('ref_axis',(0.0815075671148035,0.996242609000576,-0.029277645307502));
#118288=DIRECTION('center_axis',(0.789758100298867,0.61341807338063,-0.000640517230110011));
#118289=DIRECTION('ref_axis',(0.478501082104711,-0.616709039280961,-0.625065336819899));
#118290=DIRECTION('center_axis',(0.,0.,1.));
#118291=DIRECTION('ref_axis',(1.,0.,0.));
#118292=DIRECTION('center_axis',(-0.989397105966853,0.145235501020045,0.000126284884481098));
#118293=DIRECTION('ref_axis',(0.145169584189564,0.988973513960531,-0.0292776452398204));
#118294=DIRECTION('center_axis',(0.82743728848207,0.561557764942412,-0.000640517230185528));
#118295=DIRECTION('ref_axis',(0.438005266458827,-0.646099613946308,-0.625065336915081));
#118296=DIRECTION('center_axis',(0.,0.,1.));
#118297=DIRECTION('ref_axis',(1.,0.,0.));
#118298=DIRECTION('center_axis',(-0.97805901300076,0.208327989334383,0.000126284884461078));
#118299=DIRECTION('ref_axis',(0.208235068303793,0.97764051461419,-0.0292776452846884));
#118300=DIRECTION('center_axis',(0.861716359362257,0.507389895194155,-0.000640517230175486));
#118301=DIRECTION('ref_axis',(0.395709593338075,-0.672835226889058,-0.62506533674278));
#118302=DIRECTION('center_axis',(0.,0.,1.));
#118303=DIRECTION('ref_axis',(1.,0.,0.));
#118304=DIRECTION('center_axis',(-0.962701865757276,0.270564413254197,0.00012628488448173));
#118305=DIRECTION('ref_axis',(0.270444869856439,0.962290180692441,-0.0292776452475763));
#118306=DIRECTION('center_axis',(0.892454452884261,0.451137051531718,-0.000640517230158825));
#118307=DIRECTION('ref_axis',(0.351787864496278,-0.696806015358918,-0.625065336867096));
#118308=DIRECTION('center_axis',(0.,0.,1.));
#118309=DIRECTION('ref_axis',(1.,0.,0.));
#118310=DIRECTION('center_axis',(-0.94338877004846,0.331689029964185,0.000126284884468416));
#118311=DIRECTION('ref_axis',(0.331543355428736,0.942985590007218,-0.0292776452228328));
#118312=DIRECTION('center_axis',(0.919525259628521,0.39303038895584,-0.000640517230085256));
#118313=DIRECTION('ref_axis',(0.306420563932946,-0.717913478582981,-0.625065336799201));
#118314=DIRECTION('center_axis',(0.,0.,1.));
#118315=DIRECTION('ref_axis',(1.,0.,0.));
#118316=DIRECTION('center_axis',(-0.920199087527283,0.391450665302901,0.000126284884478618));
#118317=DIRECTION('ref_axis',(0.391279458236672,0.919806069260345,-0.0292776452921088));
#118318=DIRECTION('center_axis',(0.942817539843289,0.33330868020729,-0.000640517230158263));
#118319=DIRECTION('ref_axis',(0.259794115496682,-0.736070881214429,-0.625065336890081));
#118320=DIRECTION('center_axis',(0.,0.,1.));
#118321=DIRECTION('ref_axis',(1.,0.,0.));
#118322=DIRECTION('center_axis',(-0.893228109573398,0.449603745891936,0.000126284884511285));
#118323=DIRECTION('ref_axis',(0.449407709821742,0.892846868078202,-0.0292776453240885));
#118324=DIRECTION('center_axis',(0.962235580553193,0.272217334597077,-0.000640517230136661));
#118325=DIRECTION('ref_axis',(0.212100117373058,-0.751203610882064,-0.625065336751353));
#118326=DIRECTION('center_axis',(0.,0.,1.));
#118327=DIRECTION('ref_axis',(1.,0.,0.));
#118328=DIRECTION('center_axis',(-0.862586665720392,0.505909308249518,0.000126284884486337));
#118329=DIRECTION('ref_axis',(0.505689248728111,0.862218767597701,-0.0292776454500831));
#118330=DIRECTION('center_axis',(0.977699588863675,0.210007389568744,-0.000640517230195052));
#118331=DIRECTION('ref_axis',(0.163534554311268,-0.763249483566092,-0.62506533689072));
#118332=DIRECTION('center_axis',(0.,0.,1.));
#118333=DIRECTION('ref_axis',(1.,0.,0.));
#118334=DIRECTION('center_axis',(-0.828400668233655,0.560135980742322,0.000126284884450437));
#118335=DIRECTION('ref_axis',(0.559892802045009,0.828047625261779,-0.0292776453376336));
#118336=DIRECTION('center_axis',(0.98914601984768,0.146934479129885,-0.000640517230091587));
#118337=DIRECTION('ref_axis',(0.114296992727732,-0.772159000577822,-0.625065336808926));
#118338=DIRECTION('center_axis',(0.,0.,1.));
#118339=DIRECTION('ref_axis',(1.,0.,0.));
#118340=DIRECTION('center_axis',(-0.790810594709803,0.612060934341391,0.000126284884451835));
#118341=DIRECTION('ref_axis',(0.611795635740747,0.790473857616266,-0.0292776452918216));
#118342=DIRECTION('center_axis',(0.996527837664906,0.0832577833994178,-0.000640517230214658));
#118343=DIRECTION('ref_axis',(0.0645897602651711,-0.77789555049683,-0.625065336893769));
#118344=DIRECTION('center_axis',(0.,0.,1.));
#118345=DIRECTION('ref_axis',(1.,0.,0.));
#118346=DIRECTION('center_axis',(-0.749970910824048,0.661470798274478,0.000126284884518839));
#118347=DIRECTION('ref_axis',(0.661184469937621,0.749651863331586,-0.0292776453422865));
#118348=DIRECTION('center_axis',(0.999814708842655,0.0192389635779676,-0.000640517230218305));
#118349=DIRECTION('ref_axis',(0.0146171146338988,-0.780435560846329,-0.625065336845881));
#118350=DIRECTION('center_axis',(0.,0.,1.));
#118351=DIRECTION('ref_axis',(1.,0.,0.));
#118352=DIRECTION('center_axis',(-0.706049435597256,0.708162536812647,0.000126284884441525));
#118353=DIRECTION('ref_axis',(0.70785635532787,0.705749388744407,-0.0292776452065499));
#118354=DIRECTION('center_axis',(0.998993126922184,-0.0448589132716746,
-0.000640517230175121));
#118355=DIRECTION('ref_axis',(0.0354155958618559,0.779768594076331,0.62506533679446));
#118356=DIRECTION('center_axis',(0.,0.,1.));
#118357=DIRECTION('ref_axis',(1.,0.,0.));
#118358=DIRECTION('center_axis',(-0.659226651792583,0.751944283586536,0.000126284884470978));
#118359=DIRECTION('ref_axis',(0.751619507115029,0.658946838531902,-0.0292776452771253));
#118360=DIRECTION('center_axis',(0.994066467959853,-0.108772455224202,-0.000640517230255248));
#118361=DIRECTION('ref_axis',(0.0853027760737053,0.77589739081015,0.625065336847374));
#118362=DIRECTION('center_axis',(0.,0.,1.));
#118363=DIRECTION('ref_axis',(1.,0.,0.));
#118364=DIRECTION('center_axis',(-0.60969496427202,0.792636130007627,0.000126284884468304));
#118365=DIRECTION('ref_axis',(0.792294093126352,0.609436534417136,-0.0292776453070061));
#118366=DIRECTION('center_axis',(0.985054976653998,-0.172239027827231,-0.000640517230033179));
#118367=DIRECTION('ref_axis',(0.134839428896953,0.768837858855506,0.625065336749068));
#118368=DIRECTION('center_axis',(0.,0.,1.));
#118369=DIRECTION('ref_axis',(1.,0.,0.));
#118370=DIRECTION('center_axis',(-0.557657909364172,0.830070864550557,0.000126284884498765));
#118371=DIRECTION('ref_axis',(0.829712972761951,0.557421924858611,-0.0292776453535321));
#118372=DIRECTION('center_axis',(0.97199568315554,-0.234997833319103,-0.000640517230122774));
#118373=DIRECTION('ref_axis',(0.183821997560134,0.758619007083397,0.625065336828721));
#118374=DIRECTION('center_axis',(0.,0.,1.));
#118375=DIRECTION('ref_axis',(1.,0.,0.));
#118376=DIRECTION('center_axis',(-0.503329318489423,0.864094659861465,0.000126284884503691));
#118377=DIRECTION('ref_axis',(0.863722383821058,0.503116749045148,-0.0292776453409534));
#118378=DIRECTION('center_axis',(0.954942250902603,-0.29679098230699,-0.000640517230234924));
#118379=DIRECTION('ref_axis',(0.232049202209861,0.745282827129038,0.625065336857128));
#118380=DIRECTION('center_axis',(0.,0.,1.));
#118381=DIRECTION('ref_axis',(1.,0.,0.));
#118382=DIRECTION('center_axis',(-0.446932439481191,0.894567704867284,0.000126284884495058));
#118383=DIRECTION('ref_axis',(0.894182574335424,0.446744158590724,-0.0292776453961113));
#118384=DIRECTION('center_axis',(0.933964756106179,-0.357364553487335,-0.000640517230227479));
#118385=DIRECTION('ref_axis',(0.279322866935046,0.728884120240152,0.625065336800023));
#118386=DIRECTION('center_axis',(0.,0.,1.));
#118387=DIRECTION('ref_axis',(1.,0.,0.));
#118388=DIRECTION('center_axis',(-0.388699019212414,0.921364779289634,0.000126284884490976));
#118389=DIRECTION('ref_axis',(0.920968376854869,0.388535800564453,-0.0292776452784002));
#118390=DIRECTION('center_axis',(0.909149399791967,-0.416469637063238,-0.000640517230049945));
#118391=DIRECTION('ref_axis',(0.325448734069691,0.709490272107199,0.625065336807032));
#118392=DIRECTION('center_axis',(0.,0.,1.));
#118393=DIRECTION('ref_axis',(1.,0.,0.));
#118394=DIRECTION('center_axis',(-0.328868351297934,0.944375768201783,0.000126284884436866));
#118395=DIRECTION('ref_axis',(0.943969722761784,0.328730865590743,-0.0292776453459248));
#118396=DIRECTION('center_axis',(0.880598153582212,-0.473863357567639,-0.000640517230077695));
#118397=DIRECTION('ref_axis',(0.370237262513772,0.687180976200024,0.625065336900943));
#118398=DIRECTION('center_axis',(0.,0.,1.));
#118399=DIRECTION('ref_axis',(1.,0.,0.));
#118400=DIRECTION('center_axis',(-0.267686292786117,0.963506114514357,0.000126284884480119));
#118401=DIRECTION('ref_axis',(0.963092094599988,0.267575104979056,-0.0292776453024285));
#118402=DIRECTION('center_axis',(0.848428340671705,-0.529309871892387,-0.000640517230104159));
#118403=DIRECTION('ref_axis',(0.413504406671045,0.662047906345087,0.625065336879044));
#118404=DIRECTION('center_axis',(0.,0.,1.));
#118405=DIRECTION('ref_axis',(1.,0.,0.));
#118406=DIRECTION('center_axis',(-0.205404253878637,0.978677207531006,0.000126284884487081));
#118407=DIRECTION('ref_axis',(0.978256914438321,0.20531982086597,-0.0292776452806701));
#118408=DIRECTION('center_axis',(0.812772153722126,-0.582581338416855,-0.00064051723019751));
#118409=DIRECTION('ref_axis',(0.455072372561575,0.634194339681601,0.625065336782482));
#118410=DIRECTION('center_axis',(0.,0.,1.));
#118411=DIRECTION('ref_axis',(1.,0.,0.));
#118412=DIRECTION('center_axis',(-0.142278164832865,0.989826705976314,0.000126284884472221));
#118413=DIRECTION('ref_axis',(0.989401866778534,0.142220833567693,-0.0292776453025551));
#118414=DIRECTION('center_axis',(0.773776111653791,-0.633458853258534,-0.000640517230214162));
#118415=DIRECTION('ref_axis',(0.494770348363902,0.603734732308235,0.625065336892526));
#118416=DIRECTION('center_axis',(0.,0.,1.));
#118417=DIRECTION('ref_axis',(1.,0.,0.));
#118418=DIRECTION('center_axis',(-0.0785674242892295,0.996908794169599,
0.00012628488446824));
#118419=DIRECTION('ref_axis',(0.996481154625446,0.07853743035835,-0.0292776452100469));
#118420=DIRECTION('center_axis',(0.731600457568146,-0.681733349795767,-0.000640517230208434));
#118421=DIRECTION('ref_axis',(0.532435206693651,0.570794249453564,0.62506533695593));
#118422=DIRECTION('center_axis',(0.,0.,1.));
#118423=DIRECTION('ref_axis',(1.,0.,0.));
#118424=DIRECTION('center_axis',(-0.0145338333465579,0.999894370291374,
0.000126284884474479));
#118425=DIRECTION('ref_axis',(0.999465687656448,0.0145313000010485,-0.0292776453579056));
#118426=DIRECTION('center_axis',(0.686418500274563,-0.727206457767324,-0.000640517230213062));
#118427=DIRECTION('ref_axis',(0.567912174657105,0.535508250701133,0.625065336830679));
#118428=DIRECTION('center_axis',(0.,0.,1.));
#118429=DIRECTION('ref_axis',(1.,0.,0.));
#118430=DIRECTION('center_axis',(0.0495594802348922,0.99877116596895,0.000126284884456217));
#118431=DIRECTION('ref_axis',(0.99834320179932,-0.0495345425848042,-0.0292776452604417));
#118432=DIRECTION('center_axis',(0.638415902127094,-0.769691318418577,-0.00064051723024534));
#118433=DIRECTION('ref_axis',(0.601055469620602,0.498021733615997,0.625065336813101));
#118434=DIRECTION('center_axis',(0.,0.,1.));
#118435=DIRECTION('ref_axis',(1.,0.,0.));
#118436=DIRECTION('center_axis',(0.113449143281512,0.993543796689818,0.000126284884464334));
#118437=DIRECTION('ref_axis',(0.993118309578601,-0.113396837109937,-0.029277645281071));
#118438=DIRECTION('center_axis',(0.587789916097745,-0.809013352344375,-0.000640517230114493));
#118439=DIRECTION('ref_axis',(0.631728898747964,0.458488738410268,0.625065336775001));
#118440=DIRECTION('center_axis',(0.,0.,1.));
#118441=DIRECTION('ref_axis',(1.,0.,0.));
#118442=DIRECTION('center_axis',(0.17687261946363,0.984233742835614,0.000126284884474159));
#118443=DIRECTION('ref_axis',(0.983812481197468,-0.176793159707189,-0.0292776454112945));
#118444=DIRECTION('center_axis',(0.534748575223039,-0.845010976872258,-0.000640517230234913));
#118445=DIRECTION('ref_axis',(0.659806418230897,0.417071714568949,0.625065336879139));
#118446=DIRECTION('center_axis',(0.,0.,1.));
#118447=DIRECTION('ref_axis',(1.,0.,0.));
#118448=DIRECTION('center_axis',(0.239569288113328,0.970879261414622,0.00012628488447836));
#118449=DIRECTION('ref_axis',(0.970463956311392,-0.239463001290564,-0.0292776452836567));
#118450=DIRECTION('center_axis',(0.479509837749238,-0.877536270042086,-0.000640517230187807));
#118451=DIRECTION('ref_axis',(0.68517265178832,0.373940853698649,0.625065336726079));
#118452=DIRECTION('center_axis',(0.,0.,1.));
#118453=DIRECTION('ref_axis',(1.,0.,0.));
#118454=DIRECTION('center_axis',(0.301281515170711,0.95353522885553,0.000126284884482297));
#118455=DIRECTION('ref_axis',(0.953127586862438,-0.301148838036668,-0.0292776452425659));
#118456=DIRECTION('center_axis',(0.422300691497727,-0.906455578447295,-0.000640517230230884));
#118457=DIRECTION('ref_axis',(0.707723363756038,0.329273389542445,0.625065336851331));
#118458=DIRECTION('center_axis',(0.,0.,1.));
#118459=DIRECTION('ref_axis',(-1.,-4.31842741858589E-15,0.));
#118460=DIRECTION('center_axis',(0.361755711857575,0.932272915508408,0.000126284884481746));
#118461=DIRECTION('ref_axis',(0.931874611712475,-0.361597189610684,-0.0292776452498897));
#118462=DIRECTION('center_axis',(0.363356221121569,-0.931650066446588,-0.000640517230229525));
#118463=DIRECTION('ref_axis',(0.727365888744316,0.283252870463631,0.625065336797126));
#118464=DIRECTION('center_axis',(0.,0.,1.));
#118465=DIRECTION('ref_axis',(1.,0.,0.));
#118466=DIRECTION('center_axis',(0.420743376728019,0.907179692779568,0.000126284884514263));
#118467=DIRECTION('ref_axis',(0.906792363896192,-0.420559660770008,-0.0292776452702861));
#118468=DIRECTION('center_axis',(0.302918642092976,-0.953016204484596,-0.0006405172301338));
#118469=DIRECTION('ref_axis',(0.744019511233333,0.236068404562933,0.62506533680186));
#118470=DIRECTION('center_axis',(0.,0.,1.));
#118471=DIRECTION('ref_axis',(1.,0.,0.));
#118472=DIRECTION('center_axis',(0.478002116814432,0.878358674103609,0.000126284884485614));
#118473=DIRECTION('ref_axis',(0.877983911747608,-0.477793962072038,-0.0292776453949441));
#118474=DIRECTION('center_axis',(0.241236305388488,-0.970466194516939,-0.000640517230195009));
#118475=DIRECTION('ref_axis',(0.757615797893118,0.187913882935597,0.625065336891145));
#118476=DIRECTION('center_axis',(0.,0.,1.));
#118477=DIRECTION('ref_axis',(1.,0.,0.));
#118478=DIRECTION('center_axis',(0.533296643671695,0.845928291228419,0.000126284884457567));
#118479=DIRECTION('ref_axis',(0.845567635386527,-0.533064905501832,-0.0292776452120096));
#118480=DIRECTION('center_axis',(0.178562676959983,-0.983928330791711,-0.000640517230183268));
#118481=DIRECTION('ref_axis',(0.768098878849436,0.138987182886634,0.625065336827661));
#118482=DIRECTION('center_axis',(0.,0.,1.));
#118483=DIRECTION('ref_axis',(1.,0.,0.));
#118484=DIRECTION('center_axis',(0.586399740228354,0.810021807553505,0.000126284884436625));
#118485=DIRECTION('ref_axis',(0.809676740231543,-0.586145370889048,-0.0292776452837664));
#118486=DIRECTION('center_axis',(0.115155296190304,-0.993347294503288,-0.000640517230180079));
#118487=DIRECTION('ref_axis',(0.775425676711713,0.0894893546788511,0.625065336821156));
#118488=DIRECTION('center_axis',(0.,0.,1.));
#118489=DIRECTION('ref_axis',(1.,0.,0.));
#118490=DIRECTION('center_axis',(0.637093194469948,0.770786770522305,0.000126284884462103));
#118491=DIRECTION('ref_axis',(0.770458709676092,-0.63681723921917,-0.0292776453548837));
#118492=DIRECTION('center_axis',(0.0512747176077349,-0.99868438110943,-0.000640517230136019));
#118493=DIRECTION('ref_axis',(0.779566084139717,0.0396237955165384,0.625065336815226));
#118494=DIRECTION('center_axis',(0.,0.,1.));
#118495=DIRECTION('ref_axis',(1.,0.,0.));
#118496=DIRECTION('center_axis',(0.685168696119518,0.728384405317692,0.000126284884426764));
#118497=DIRECTION('ref_axis',(0.7280746990243,-0.68487228892067,-0.0292776452133255));
#118498=DIRECTION('center_axis',(-0.0128165597878282,-0.999917659376452,
-0.000640517230123854));
#118499=DIRECTION('ref_axis',(0.780503087305324,-0.0104045863213432,0.625065336817152));
#118500=DIRECTION('center_axis',(0.,0.,1.));
#118501=DIRECTION('ref_axis',(1.,0.,0.));
#118502=DIRECTION('center_axis',(0.730428692628412,0.682988952353753,0.000126284884449094));
#118503=DIRECTION('ref_axis',(0.682698873258233,-0.730113051478129,-0.0292776452815721));
#118504=DIRECTION('center_axis',(-0.0768551711899076,-0.997042061499437,
-0.000640517230164196));
#118505=DIRECTION('ref_axis',(0.77823283585057,-0.0603902134806393,0.625065336840671));
#118506=DIRECTION('center_axis',(0.,0.,1.));
#118507=DIRECTION('ref_axis',(1.,0.,0.));
#118508=DIRECTION('center_axis',(0.772687200962842,0.634786951283922,0.00012628488448787));
#118509=DIRECTION('ref_axis',(0.634517691386124,-0.772353622901137,-0.02927764521803));
#118510=DIRECTION('center_axis',(-0.140577968208273,-0.990069403926872,
-0.000640517230174936));
#118511=DIRECTION('ref_axis',(0.77276465884658,-0.110127684311339,0.62506533673365));
#118512=DIRECTION('center_axis',(0.,0.,1.));
#118513=DIRECTION('ref_axis',(1.,0.,0.));
#118514=DIRECTION('center_axis',(0.811770571847666,0.583976474469855,0.000126284884490396));
#118515=DIRECTION('ref_axis',(0.58372914021539,-0.811420427617263,-0.0292776452061936));
#118516=DIRECTION('center_axis',(-0.203723100201364,-0.979028338804359,
-0.000640517230211191));
#118517=DIRECTION('ref_axis',(0.764121025913825,-0.159412616837099,0.625065336864517));
#118518=DIRECTION('center_axis',(0.,0.,1.));
#118519=DIRECTION('ref_axis',(1.,0.,0.));
#118520=DIRECTION('center_axis',(0.847518203328528,0.530766313059629,0.000126284884478973));
#118521=DIRECTION('ref_axis',(0.530541920795968,-0.847152931743979,-0.0292776453237979));
#118522=DIRECTION('center_axis',(-0.266031090277392,-0.96396423623675,-0.000640517230166038));
#118523=DIRECTION('ref_axis',(0.752337455883405,-0.208042488740392,0.625065336867747));
#118524=DIRECTION('center_axis',(0.,0.,1.));
#118525=DIRECTION('ref_axis',(1.,0.,0.));
#118526=DIRECTION('center_axis',(0.879783200719825,0.47537511902003,0.000126284884493913));
#118527=DIRECTION('ref_axis',(0.475174590823935,-0.879404302761019,-0.0292776454092863));
#118528=DIRECTION('center_axis',(-0.32724590153985,-0.944938997852797,-0.000640517230195817));
#118529=DIRECTION('ref_axis',(0.737462369950221,-0.255817469459471,0.62506533676629));
#118530=DIRECTION('center_axis',(0.,0.,1.));
#118531=DIRECTION('ref_axis',(1.,0.,0.));
#118532=DIRECTION('center_axis',(0.908432980226467,0.418030506648722,0.000126284884497972));
#118533=DIRECTION('ref_axis',(0.417854666536127,-0.908042012871251,-0.0292776453067762));
#118534=DIRECTION('center_axis',(-0.387115989198804,-0.922030802437917,
-0.000640517230236988));
#118535=DIRECTION('ref_axis',(0.719556892801567,-0.302541241271347,0.625065336866272));
#118536=DIRECTION('center_axis',(0.,0.,1.));
#118537=DIRECTION('ref_axis',(1.,0.,0.));
#118538=DIRECTION('center_axis',(0.933349813759075,0.358968117258384,0.000126284884506072));
#118539=DIRECTION('ref_axis',(0.358817687792876,-0.932948383574218,-0.0292776452814723));
#118540=DIRECTION('center_axis',(-0.445395334222409,-0.895333784680656,
-0.000640517230092827));
#118541=DIRECTION('ref_axis',(0.698694602184768,-0.348021806290653,0.625065336764134));
#118542=DIRECTION('center_axis',(0.,0.,1.));
#118543=DIRECTION('ref_axis',(1.,0.,0.));
#118544=DIRECTION('center_axis',(0.954431312704091,0.298430650875666,0.000126284884468639));
#118545=DIRECTION('ref_axis',(0.298306250203729,-0.954021069251171,-0.0292776452988035));
#118546=DIRECTION('center_axis',(-0.501844454280232,-0.864957648353868,
-0.00064051723019065));
#118547=DIRECTION('ref_axis',(0.674961225480966,-0.392072275013033,0.625065336795552));
#118548=DIRECTION('center_axis',(0.,0.,1.));
#118549=DIRECTION('ref_axis',(1.,0.,0.));
#118550=DIRECTION('center_axis',(0.971590848660297,0.236666868935413,0.000126284884465081));
#118551=DIRECTION('ref_axis',(0.236569008247039,-0.97117347772134,-0.029277645186219));
#118552=DIRECTION('center_axis',(-0.556231387830428,-0.831027215516985,
-0.000640517230122861));
#118553=DIRECTION('ref_axis',(0.648454288298381,-0.434511634638079,0.625065336866143));
#118554=DIRECTION('center_axis',(0.,0.,1.));
#118555=DIRECTION('ref_axis',(1.,0.,0.));
#118556=DIRECTION('center_axis',(0.984757909413759,0.173930572065897,0.000126284884492896));
#118557=DIRECTION('ref_axis',(0.173859653489961,-0.984335126048177,-0.029277645330005));
#118558=DIRECTION('center_axis',(-0.608332647296499,-0.793681913596947,
-0.000640517230193171));
#118559=DIRECTION('ref_axis',(0.619282713485376,-0.475165492846558,0.625065336733751));
#118560=DIRECTION('center_axis',(0.,0.,1.));
#118561=DIRECTION('ref_axis',(1.,0.,0.));
#118562=DIRECTION('center_axis',(0.993878388687544,0.110479557167738,0.000126284884499037));
#118563=DIRECTION('ref_axis',(0.110435872124856,-0.993451930206933,-0.029277645331228));
#118564=DIRECTION('center_axis',(-0.657934137428163,-0.753075202449488,
-0.000640517230102684));
#118565=DIRECTION('ref_axis',(0.587566373093202,-0.513866794076159,0.625065336709684));
#118566=DIRECTION('center_axis',(0.,0.,1.));
#118567=DIRECTION('ref_axis',(1.,0.,0.));
#118568=DIRECTION('center_axis',(0.998914808475976,0.0465745580712427,0.00012628488445277));
#118569=DIRECTION('ref_axis',(0.0465582860724865,-0.998486427286337,-0.0292776454476564));
#118570=DIRECTION('center_axis',(-0.704832035062462,-0.709373943761248,
-0.000640517230175122));
#118571=DIRECTION('ref_axis',(0.553435596364022,-0.550456506351326,0.625065336819034));
#118572=DIRECTION('center_axis',(0.,0.,1.));
#118573=DIRECTION('ref_axis',(1.,0.,0.));
#118574=DIRECTION('center_axis',(0.999846473049815,-0.0175218258744245,
0.000126284884473359));
#118575=DIRECTION('ref_axis',(0.0175106179635388,0.999417929463863,0.0292776454773875));
#118576=DIRECTION('center_axis',(-0.748833626678827,-0.662757715377734,
-0.000640517230154864));
#118577=DIRECTION('ref_axis',(0.517030634121038,-0.584784274823909,0.625065336824138));
#118578=DIRECTION('center_axis',(0.,0.,1.));
#118579=DIRECTION('ref_axis',(1.,0.,0.));
#118580=DIRECTION('center_axis',(0.996669553999503,-0.0815462088791361,
0.000126284884502308));
#118581=DIRECTION('ref_axis',(0.0815075671145944,0.996242608999261,0.0292776453528275));
#118582=DIRECTION('center_axis',(-0.789758100298809,-0.613418073380703,
-0.000640517230177985));
#118583=DIRECTION('ref_axis',(0.478501082108721,-0.616709039286066,0.625065336811793));
#118584=DIRECTION('center_axis',(0.,0.,1.));
#118585=DIRECTION('ref_axis',(1.,0.,0.));
#118586=DIRECTION('center_axis',(0.989397105966854,-0.145235501020041,0.000126284884492392));
#118587=DIRECTION('ref_axis',(0.145169584189202,0.988973513958171,0.0292776453213211));
#118588=DIRECTION('center_axis',(-0.827437288482004,-0.56155776494251,-0.000640517230231779));
#118589=DIRECTION('ref_axis',(0.438005266472051,-0.646099613965648,0.625065336885824));
#118590=DIRECTION('center_axis',(0.,0.,1.));
#118591=DIRECTION('ref_axis',(1.,0.,0.));
#118592=DIRECTION('center_axis',(0.978059013000762,-0.208327989334377,0.000126284884459322));
#118593=DIRECTION('ref_axis',(0.208235068303449,0.977640514612639,0.0292776453389273));
#118594=DIRECTION('center_axis',(-0.861716359362261,-0.507389895194147,
-0.000640517230179385));
#118595=DIRECTION('ref_axis',(0.395709593315104,-0.672835226850135,0.62506533679922));
#118596=DIRECTION('center_axis',(0.,0.,1.));
#118597=DIRECTION('ref_axis',(1.,0.,0.));
#118598=DIRECTION('center_axis',(0.076855171189824,0.997042061499444,-0.00064051723019405));
#118599=DIRECTION('ref_axis',(0.778232835837226,-0.0603902134795745,-0.625065336857388));
#118600=DIRECTION('center_axis',(-0.730428692628325,-0.682988952353846,
0.000126284884508401));
#118601=DIRECTION('ref_axis',(0.682698873257609,-0.730113051477267,0.0292776453176158));
#118602=DIRECTION('center_axis',(0.,0.,1.));
#118603=DIRECTION('ref_axis',(1.,0.,0.));
#118604=DIRECTION('center_axis',(0.0128165597878328,0.999917659376452,-0.000640517230111141));
#118605=DIRECTION('ref_axis',(0.780503087340716,-0.0104045863217641,-0.625065336772952));
#118606=DIRECTION('center_axis',(-0.685168696119438,-0.728384405317767,
0.000126284884473155));
#118607=DIRECTION('ref_axis',(0.728074699020922,-0.684872288917312,0.0292776453758732));
#118608=DIRECTION('center_axis',(0.,0.,1.));
#118609=DIRECTION('ref_axis',(1.,0.,0.));
#118610=DIRECTION('center_axis',(-0.0512747176076207,0.998684381109436,
-0.000640517230077118));
#118611=DIRECTION('ref_axis',(0.779566084098042,0.0396237955143128,-0.625065336867343));
#118612=DIRECTION('center_axis',(-0.637093194469926,-0.770786770522324,
0.000126284884463446));
#118613=DIRECTION('ref_axis',(0.770458709677825,-0.636817239220578,0.0292776452786474));
#118614=DIRECTION('center_axis',(0.,0.,1.));
#118615=DIRECTION('ref_axis',(1.,0.,0.));
#118616=DIRECTION('center_axis',(-0.115155296190241,0.993347294503295,-0.000640517230157329));
#118617=DIRECTION('ref_axis',(0.775425676771399,0.0894893546857832,-0.62506533674612));
#118618=DIRECTION('center_axis',(-0.586399740228206,-0.810021807553612,
0.000126284884506732));
#118619=DIRECTION('ref_axis',(0.809676740229673,-0.586145370887453,0.0292776453674271));
#118620=DIRECTION('center_axis',(0.,0.,1.));
#118621=DIRECTION('ref_axis',(1.,0.,0.));
#118622=DIRECTION('center_axis',(-0.178562676960012,0.983928330791706,-0.000640517230193345));
#118623=DIRECTION('ref_axis',(0.768098878947061,0.13898718290445,-0.625065336703734));
#118624=DIRECTION('center_axis',(-0.533296643671567,-0.8459282912285,0.000126284884524021));
#118625=DIRECTION('ref_axis',(0.845567635383503,-0.533064905499726,0.0292776453376993));
#118626=DIRECTION('center_axis',(0.,0.,1.));
#118627=DIRECTION('ref_axis',(1.,0.,0.));
#118628=DIRECTION('center_axis',(-0.241236305388322,0.970466194516981,-0.00064051723011321));
#118629=DIRECTION('ref_axis',(0.757615797916166,0.187913882941261,-0.625065336861507));
#118630=DIRECTION('center_axis',(-0.478002116814468,-0.87835867410359,0.000126284884448764));
#118631=DIRECTION('ref_axis',(0.877983911749062,-0.477793962072885,0.0292776453375163));
#118632=DIRECTION('center_axis',(0.,0.,1.));
#118633=DIRECTION('ref_axis',(1.,0.,0.));
#118634=DIRECTION('center_axis',(-0.302918642093179,0.953016204484531,-0.00064051723023523));
#118635=DIRECTION('ref_axis',(0.744019511174325,0.236068404544233,-0.625065336879161));
#118636=DIRECTION('center_axis',(-0.420743376728091,-0.907179692779535,
0.000126284884464857));
#118637=DIRECTION('ref_axis',(0.906792363893399,-0.420559660768787,0.0292776453743162));
#118638=DIRECTION('center_axis',(0.,0.,1.));
#118639=DIRECTION('ref_axis',(1.,0.,0.));
#118640=DIRECTION('center_axis',(-0.42230069149759,0.906455578447358,-0.000640517230146995));
#118641=DIRECTION('ref_axis',(0.707723363773355,0.329273389550458,-0.625065336827504));
#118642=DIRECTION('center_axis',(-0.301281515170749,-0.953535228855518,
0.000126284884461136));
#118643=DIRECTION('ref_axis',(0.953127586860523,-0.301148838036096,0.0292776453107957));
#118644=DIRECTION('center_axis',(0.,0.,1.));
#118645=DIRECTION('ref_axis',(1.,0.,0.));
#118646=DIRECTION('center_axis',(-0.479509837749294,0.877536270042056,-0.00064051723022099));
#118647=DIRECTION('ref_axis',(0.685172651693589,0.373940853646821,-0.625065336860926));
#118648=DIRECTION('center_axis',(-0.239569288113379,-0.970879261414609,
0.000126284884448227));
#118649=DIRECTION('ref_axis',(0.970463956312834,-0.239463001290981,0.0292776452324618));
#118650=DIRECTION('center_axis',(0.,0.,1.));
#118651=DIRECTION('ref_axis',(1.,0.,0.));
#118652=DIRECTION('center_axis',(-0.534748575222834,0.845010976872388,-0.000640517230120457));
#118653=DIRECTION('ref_axis',(0.659806418276669,0.417071714597827,-0.625065336811554));
#118654=DIRECTION('center_axis',(-0.176872619463615,-0.984233742835617,
0.000126284884477445));
#118655=DIRECTION('ref_axis',(0.983812481200434,-0.176793159707719,0.0292776453084223));
#118656=DIRECTION('center_axis',(0.,0.,1.));
#118657=DIRECTION('ref_axis',(1.,0.,0.));
#118658=DIRECTION('center_axis',(-0.587789916097922,0.809013352344247,-0.000640517230203535));
#118659=DIRECTION('ref_axis',(0.631728898720485,0.458488738390412,-0.625065336817337));
#118660=DIRECTION('center_axis',(-0.113449143281533,-0.993543796689816,
0.000126284884456771));
#118661=DIRECTION('ref_axis',(0.993118309577297,-0.113396837109804,0.0292776453258326));
#118662=DIRECTION('center_axis',(0.,0.,1.));
#118663=DIRECTION('ref_axis',(1.,0.,0.));
#118664=DIRECTION('center_axis',(-0.638415902126943,0.769691318418702,-0.000640517230140775));
#118665=DIRECTION('ref_axis',(0.601055469599138,0.498021733598052,-0.625065336848038));
#118666=DIRECTION('center_axis',(-0.0495594802348531,-0.998771165968952,
0.000126284884467267));
#118667=DIRECTION('ref_axis',(0.998343201794375,-0.0495345425844979,0.0292776454296004));
#118668=DIRECTION('center_axis',(0.,0.,1.));
#118669=DIRECTION('ref_axis',(1.,0.,0.));
#118670=DIRECTION('center_axis',(-0.686418500274535,0.72720645776735,-0.000640517230207348));
#118671=DIRECTION('ref_axis',(0.567912174657334,0.535508250701313,-0.625065336830317));
#118672=DIRECTION('center_axis',(0.0145338333465769,-0.999894370291373,
0.000126284884478989));
#118673=DIRECTION('ref_axis',(0.999465687656356,0.0145313000010667,0.0292776453610361));
#118674=DIRECTION('center_axis',(0.,0.,1.));
#118675=DIRECTION('ref_axis',(1.,0.,0.));
#118676=DIRECTION('center_axis',(-0.731600457568012,0.68173334979591,-0.000640517230123058));
#118677=DIRECTION('ref_axis',(0.532435206756676,0.570794249521162,-0.625065336840516));
#118678=DIRECTION('center_axis',(0.0785674242892662,-0.996908794169596,
0.000126284884477587));
#118679=DIRECTION('ref_axis',(0.996481154621252,0.0785374303580749,0.0292776453535325));
#118680=DIRECTION('center_axis',(0.,0.,1.));
#118681=DIRECTION('ref_axis',(1.,0.,0.));
#118682=DIRECTION('center_axis',(-0.773776111653631,0.63345885325873,-0.000640517230106446));
#118683=DIRECTION('ref_axis',(0.494770348382416,0.60373473233068,-0.625065336856192));
#118684=DIRECTION('center_axis',(0.142278164832833,-0.989826705976318,0.00012628488445795));
#118685=DIRECTION('ref_axis',(0.989401866783126,0.1422208335683,0.0292776451444397));
#118686=DIRECTION('center_axis',(0.,0.,1.));
#118687=DIRECTION('ref_axis',(1.,0.,0.));
#118688=DIRECTION('center_axis',(-0.812772153722213,0.582581338416733,-0.000640517230245157));
#118689=DIRECTION('ref_axis',(0.455072372516387,0.634194339618601,-0.6250653368793));
#118690=DIRECTION('center_axis',(0.205404253878618,-0.97867720753101,0.00012628488447263));
#118691=DIRECTION('ref_axis',(0.978256914435842,0.20531982086544,0.0292776453672486));
#118692=DIRECTION('center_axis',(0.,0.,1.));
#118693=DIRECTION('ref_axis',(1.,0.,0.));
#118694=DIRECTION('center_axis',(-0.848428340671752,0.529309871892312,-0.000640517230142603));
#118695=DIRECTION('ref_axis',(0.413504406708692,0.662047906405623,-0.625065336790022));
#118696=DIRECTION('center_axis',(0.26768629278616,-0.963506114514345,0.00012628488448624));
#118697=DIRECTION('ref_axis',(0.963092094599376,0.267575104978935,0.0292776453236817));
#118698=DIRECTION('center_axis',(0.,0.,1.));
#118699=DIRECTION('ref_axis',(1.,0.,0.));
#118700=DIRECTION('center_axis',(-0.880598153582283,0.473863357567508,-0.00064051723016054));
#118701=DIRECTION('ref_axis',(0.370237262580095,0.687180976323646,-0.625065336725752));
#118702=DIRECTION('center_axis',(0.328868351298007,-0.944375768201757,0.000126284884457867));
#118703=DIRECTION('ref_axis',(0.943969722761657,0.328730865590781,0.0292776453495876));
#118704=DIRECTION('center_axis',(0.,0.,1.));
#118705=DIRECTION('ref_axis',(1.,0.,0.));
#118706=DIRECTION('center_axis',(-0.909149399792093,0.416469637062962,-0.000640517230189422));
#118707=DIRECTION('ref_axis',(0.325448734056368,0.709490272078413,-0.625065336846642));
#118708=DIRECTION('center_axis',(0.388699019212475,-0.921364779289608,0.000126284884524275));
#118709=DIRECTION('ref_axis',(0.920968376853952,0.388535800564144,0.0292776453113384));
#118710=DIRECTION('center_axis',(0.,0.,1.));
#118711=DIRECTION('ref_axis',(1.,0.,0.));
#118712=DIRECTION('center_axis',(-0.933964756106238,0.357364553487182,-0.000640517230307371));
#118713=DIRECTION('ref_axis',(0.279322866946701,0.728884120270902,-0.625065336758957));
#118714=DIRECTION('center_axis',(0.446932439481096,-0.894567704867331,0.000126284884460302));
#118715=DIRECTION('ref_axis',(0.894182574336947,0.446744158591356,0.0292776453399457));
#118716=DIRECTION('center_axis',(0.,0.,1.));
#118717=DIRECTION('ref_axis',(1.,0.,0.));
#118718=DIRECTION('center_axis',(-0.954942250902568,0.296790982307101,-0.000640517230162724));
#118719=DIRECTION('ref_axis',(0.232049202230339,0.745282827194961,-0.625065336770925));
#118720=DIRECTION('center_axis',(0.503329318489387,-0.864094659861486,0.000126284884485404));
#118721=DIRECTION('ref_axis',(0.863722383823579,0.503116749046554,0.0292776452424264));
#118722=DIRECTION('center_axis',(0.,0.,1.));
#118723=DIRECTION('ref_axis',(1.,0.,0.));
#118724=DIRECTION('center_axis',(-0.971995683155537,0.234997833319116,-0.000640517230128928));
#118725=DIRECTION('ref_axis',(0.18382199756744,0.758619007113659,-0.625065336789845));
#118726=DIRECTION('center_axis',(0.557657909364124,-0.830070864550589,0.000126284884479074));
#118727=DIRECTION('ref_axis',(0.829712972761687,0.557421924858367,0.0292776453656659));
#118728=DIRECTION('center_axis',(0.,0.,1.));
#118729=DIRECTION('ref_axis',(1.,0.,0.));
#118730=DIRECTION('center_axis',(-0.98505497665405,0.172239027826935,-0.000640517230198739));
#118731=DIRECTION('ref_axis',(0.134839428888974,0.768837858810419,-0.625065336806246));
#118732=DIRECTION('center_axis',(0.609694964272102,-0.792636130007564,0.000126284884514757));
#118733=DIRECTION('ref_axis',(0.792294093126998,0.60943653441776,0.0292776452765282));
#118734=DIRECTION('center_axis',(0.,0.,1.));
#118735=DIRECTION('ref_axis',(1.,0.,0.));
#118736=DIRECTION('center_axis',(-0.994066467959822,0.108772455224486,-0.000640517230136566));
#118737=DIRECTION('ref_axis',(0.0853027760785172,0.775897390853078,-0.62506533679343));
#118738=DIRECTION('center_axis',(0.659226651792606,-0.751944283586515,0.000126284884470909));
#118739=DIRECTION('ref_axis',(0.751619507115677,0.658946838532506,0.0292776452468731));
#118740=DIRECTION('center_axis',(0.,0.,1.));
#118741=DIRECTION('ref_axis',(1.,0.,0.));
#118742=DIRECTION('center_axis',(-0.998993126922188,0.0448589132715698,
-0.00064051723020566));
#118743=DIRECTION('ref_axis',(0.0354155958590675,0.77976859401453,-0.625065336871715));
#118744=DIRECTION('center_axis',(0.706049435597307,-0.708162536812597,0.000126284884470886));
#118745=DIRECTION('ref_axis',(0.707856355326067,0.705749388742727,0.0292776452906457));
#118746=DIRECTION('center_axis',(0.,0.,1.));
#118747=DIRECTION('ref_axis',(1.,0.,0.));
#118748=DIRECTION('center_axis',(-0.999814708842659,-0.0192389635777686,
-0.000640517230114542));
#118749=DIRECTION('ref_axis',(0.0146171146340831,-0.780435560860042,0.625065336828756));
#118750=DIRECTION('center_axis',(0.749970910823934,-0.661470798274608,0.000126284884429514));
#118751=DIRECTION('ref_axis',(0.661184469940119,0.74965186333413,0.0292776452207336));
#118752=DIRECTION('center_axis',(0.,0.,1.));
#118753=DIRECTION('ref_axis',(1.,0.,0.));
#118754=DIRECTION('center_axis',(-0.996527837664922,-0.083257783399226,
-0.000640517230122777));
#118755=DIRECTION('ref_axis',(0.0645897602705995,-0.777895550562288,0.625065336811746));
#118756=DIRECTION('center_axis',(0.790810594709797,-0.612060934341398,0.000126284884444494));
#118757=DIRECTION('ref_axis',(0.611795635740334,0.79047385761572,0.0292776453151959));
#118758=DIRECTION('center_axis',(0.,0.,1.));
#118759=DIRECTION('ref_axis',(1.,0.,0.));
#118760=DIRECTION('center_axis',(-0.989146019847667,-0.146934479129973,
-0.000640517230129196));
#118761=DIRECTION('ref_axis',(0.114296992734883,-0.772159000625384,0.625065336748863));
#118762=DIRECTION('center_axis',(0.828400668233701,-0.560135980742254,0.00012628488448557));
#118763=DIRECTION('ref_axis',(0.559892802046617,0.828047625264283,0.0292776452360898));
#118764=DIRECTION('center_axis',(0.,0.,1.));
#118765=DIRECTION('ref_axis',(1.,0.,0.));
#118766=DIRECTION('center_axis',(-0.977699588863672,-0.210007389568759,
-0.000640517230193698));
#118767=DIRECTION('ref_axis',(0.163534554324716,-0.763249483628396,0.625065336811123));
#118768=DIRECTION('center_axis',(0.862586665720386,-0.505909308249527,0.000126284884483891));
#118769=DIRECTION('ref_axis',(0.505689248729257,0.862218767599615,0.0292776453739221));
#118770=DIRECTION('center_axis',(0.,0.,1.));
#118771=DIRECTION('ref_axis',(1.,0.,0.));
#118772=DIRECTION('center_axis',(-0.962235580553159,-0.2722173345972,-0.000640517230194249));
#118773=DIRECTION('ref_axis',(0.212100117352834,-0.751203610810562,0.625065336844148));
#118774=DIRECTION('center_axis',(0.893228109573352,-0.44960374589203,0.000126284884462287));
#118775=DIRECTION('ref_axis',(0.449407709822873,0.892846868080192,0.0292776452460509));
#118776=DIRECTION('center_axis',(0.,0.,1.));
#118777=DIRECTION('ref_axis',(1.,0.,0.));
#118778=DIRECTION('center_axis',(-0.942817539843282,-0.333308680207309,
-0.000640517230161676));
#118779=DIRECTION('ref_axis',(0.259794115520574,-0.736070881281797,0.625065336800819));
#118780=DIRECTION('center_axis',(0.920199087527283,-0.391450665302901,0.000126284884478618));
#118781=DIRECTION('ref_axis',(0.391279458236672,0.919806069260345,0.0292776452921088));
#118782=DIRECTION('center_axis',(0.,0.,1.));
#118783=DIRECTION('ref_axis',(1.,0.,0.));
#118784=DIRECTION('center_axis',(0.962701865757272,-0.270564413254211,0.00012628488448324));
#118785=DIRECTION('ref_axis',(0.27044486985633,0.962290180692004,0.0292776452629509));
#118786=DIRECTION('center_axis',(-0.892454452884192,-0.451137051531855,
-0.00064051723023769));
#118787=DIRECTION('ref_axis',(0.351787864490119,-0.696806015346603,0.62506533688429));
#118788=DIRECTION('center_axis',(0.,0.,1.));
#118789=DIRECTION('ref_axis',(1.,0.,0.));
#118790=DIRECTION('',(0.,0.,1.));
#118791=DIRECTION('',(0.,0.,1.));
#118792=DIRECTION('center_axis',(0.,0.,-1.));
#118793=DIRECTION('ref_axis',(-1.,0.,0.));
#118794=DIRECTION('center_axis',(-0.878337211800797,-0.47804156970498,0.));
#118795=DIRECTION('ref_axis',(0.47804156970498,-0.878337211800797,0.));
#118796=DIRECTION('center_axis',(0.878337211800815,0.478041569704948,-1.94241554282581E-14));
#118797=DIRECTION('ref_axis',(0.477399717843322,-0.877157895167585,-0.0518028604257383));
#118798=DIRECTION('',(0.,0.,1.));
#118799=DIRECTION('center_axis',(0.878337211800797,-0.47804156970498,0.));
#118800=DIRECTION('ref_axis',(0.47804156970498,0.878337211800797,0.));
#118801=DIRECTION('center_axis',(-0.878334869807783,0.478045872772184,2.28597554380844E-6));
#118802=DIRECTION('ref_axis',(0.452531252665384,0.831457268774235,-0.322326349471446));
#118803=DIRECTION('',(0.,0.,-1.));
#118804=DIRECTION('center_axis',(0.,0.,-1.));
#118805=DIRECTION('ref_axis',(-1.,0.,0.));
#118806=DIRECTION('',(-1.50231459873716E-16,-1.,0.));
#118807=DIRECTION('',(-0.866025403784439,-0.5,0.));
#118808=DIRECTION('center_axis',(0.,0.,-1.));
#118809=DIRECTION('ref_axis',(-1.,0.,0.));
#118810=DIRECTION('',(-0.866025403784439,-0.5,0.));
#118811=DIRECTION('',(-0.866025403784439,0.5,0.));
#118812=DIRECTION('center_axis',(0.,0.,-1.));
#118813=DIRECTION('ref_axis',(-1.,0.,0.));
#118814=DIRECTION('',(-0.866025403784439,0.5,0.));
#118815=DIRECTION('',(4.50694379621148E-16,1.,0.));
#118816=DIRECTION('center_axis',(0.,0.,-1.));
#118817=DIRECTION('ref_axis',(-1.,0.,0.));
#118818=DIRECTION('',(4.50694379621148E-16,1.,0.));
#118819=DIRECTION('',(0.866025403784439,0.5,0.));
#118820=DIRECTION('center_axis',(0.,0.,-1.));
#118821=DIRECTION('ref_axis',(-1.,0.,0.));
#118822=DIRECTION('',(0.866025403784439,0.5,0.));
#118823=DIRECTION('',(0.866025403784438,-0.5,0.));
#118824=DIRECTION('center_axis',(0.,0.,-1.));
#118825=DIRECTION('ref_axis',(-1.,0.,0.));
#118826=DIRECTION('center_axis',(0.,0.,1.));
#118827=DIRECTION('ref_axis',(1.,0.,0.));
#118828=DIRECTION('center_axis',(0.,0.,1.));
#118829=DIRECTION('ref_axis',(1.,0.,0.));
#118830=DIRECTION('center_axis',(0.,0.,1.));
#118831=DIRECTION('ref_axis',(1.,0.,0.));
#118832=DIRECTION('center_axis',(0.,0.,1.));
#118833=DIRECTION('ref_axis',(1.,0.,0.));
#118834=DIRECTION('center_axis',(0.,0.,1.));
#118835=DIRECTION('ref_axis',(1.,0.,0.));
#118836=DIRECTION('center_axis',(0.,0.,1.));
#118837=DIRECTION('ref_axis',(1.,0.,0.));
#118838=DIRECTION('center_axis',(0.943388770048457,-0.331689029964193,0.000126284884467552));
#118839=DIRECTION('ref_axis',(0.331543355428355,0.942985590006125,0.0292776452623501));
#118840=DIRECTION('center_axis',(-0.919525259628521,-0.39303038895584,-0.000640517230085256));
#118841=DIRECTION('ref_axis',(0.306420563932946,-0.717913478582981,0.625065336799201));
#118842=DIRECTION('center_axis',(0.5,0.866025403784439,0.));
#118843=DIRECTION('ref_axis',(-0.866025403784439,0.5,0.));
#118844=DIRECTION('',(0.,0.,1.));
#118845=DIRECTION('',(0.,0.,1.));
#118846=DIRECTION('center_axis',(1.,-4.50694379621148E-16,0.));
#118847=DIRECTION('ref_axis',(4.50694379621148E-16,1.,0.));
#118848=DIRECTION('',(0.,0.,1.));
#118849=DIRECTION('center_axis',(0.5,-0.866025403784439,0.));
#118850=DIRECTION('ref_axis',(0.866025403784439,0.5,0.));
#118851=DIRECTION('',(0.,0.,1.));
#118852=DIRECTION('center_axis',(-0.5,-0.866025403784439,0.));
#118853=DIRECTION('ref_axis',(0.866025403784439,-0.5,0.));
#118854=DIRECTION('',(0.,0.,1.));
#118855=DIRECTION('',(0.866025403784438,-0.5,0.));
#118856=DIRECTION('center_axis',(-1.,1.50231459873716E-16,0.));
#118857=DIRECTION('ref_axis',(-1.50231459873716E-16,-1.,0.));
#118858=DIRECTION('',(0.,0.,1.));
#118859=DIRECTION('',(-1.50231459873716E-16,-1.,0.));
#118860=DIRECTION('center_axis',(-0.5,0.866025403784439,0.));
#118861=DIRECTION('ref_axis',(-0.866025403784439,-0.5,0.));
#118862=DIRECTION('center_axis',(0.,0.,-1.));
#118863=DIRECTION('ref_axis',(-1.,0.,0.));
#118864=DIRECTION('center_axis',(0.,0.,1.));
#118865=DIRECTION('ref_axis',(1.,0.,0.));
#118866=DIRECTION('center_axis',(0.,0.,1.));
#118867=DIRECTION('ref_axis',(1.,0.,0.));
#118868=DIRECTION('center_axis',(0.,0.,1.));
#118869=DIRECTION('ref_axis',(1.,0.,0.));
#118870=DIRECTION('center_axis',(0.,0.,1.));
#118871=DIRECTION('ref_axis',(-1.,-1.22464679914735E-16,0.));
#118872=DIRECTION('center_axis',(0.,0.,1.));
#118873=DIRECTION('ref_axis',(1.,0.,0.));
#118874=DIRECTION('center_axis',(0.,0.,-1.));
#118875=DIRECTION('ref_axis',(-1.,0.,0.));
#118876=DIRECTION('center_axis',(0.,0.,1.));
#118877=DIRECTION('ref_axis',(1.,0.,0.));
#118878=DIRECTION('center_axis',(0.,0.,1.));
#118879=DIRECTION('ref_axis',(-5.9042332696092E-17,1.,0.));
#118880=DIRECTION('center_axis',(0.,0.,-1.));
#118881=DIRECTION('ref_axis',(1.,0.,0.));
#118882=DIRECTION('center_axis',(0.,0.,1.));
#118883=DIRECTION('ref_axis',(1.,0.,0.));
#118884=DIRECTION('center_axis',(-0.942660163734981,0.236130725428042,-0.235868811452395));
#118885=DIRECTION('ref_axis',(0.333754100353815,0.666661575414249,-0.666461209946391));
#118886=DIRECTION('center_axis',(0.,0.,1.));
#118887=DIRECTION('ref_axis',(1.,0.,0.));
#118888=DIRECTION('center_axis',(0.,0.,1.));
#118889=DIRECTION('ref_axis',(1.,0.,0.));
#118890=DIRECTION('center_axis',(0.,0.,-1.));
#118891=DIRECTION('ref_axis',(-1.,0.,0.));
#118892=DIRECTION('center_axis',(-0.942660163734966,-0.236130725428143,
0.235868811452354));
#118893=DIRECTION('ref_axis',(0.333754100353857,-0.6666615754131,0.666461209947519));
#118894=DIRECTION('center_axis',(0.999898588892179,0.0142412054064829,-6.76296429840134E-17));
#118895=DIRECTION('ref_axis',(0.0142412054064829,-0.999898588892179,-3.2740809054583E-33));
#118896=DIRECTION('center_axis',(0.357599031314712,-0.657040215773436,0.663642288932205));
#118897=DIRECTION('ref_axis',(-4.21884749357559E-15,-0.710632718732581,
-0.703563173472532));
#118898=DIRECTION('center_axis',(0.,0.,-1.));
#118899=DIRECTION('ref_axis',(-1.,0.,0.));
#118900=DIRECTION('center_axis',(0.999898588892179,-0.0142412054064834,
-1.38914942345546E-16));
#118901=DIRECTION('ref_axis',(0.0142412054064834,0.999898588892179,3.85185988877447E-34));
#118902=DIRECTION('center_axis',(0.358627514811599,-0.658929916134845,0.661209249211309));
#118903=DIRECTION('ref_axis',(9.74220704108575E-15,-0.70832660567291,-0.705884848750767));
#118904=DIRECTION('center_axis',(0.,0.,1.));
#118905=DIRECTION('ref_axis',(-1.,0.,0.));
#118906=DIRECTION('center_axis',(0.358627514811598,0.658929916134846,-0.661209249211308));
#118907=DIRECTION('ref_axis',(9.24260668000443E-15,0.708326605672909,0.705884848750768));
#118908=DIRECTION('center_axis',(0.,0.,1.));
#118909=DIRECTION('ref_axis',(1.,0.,0.));
#118910=DIRECTION('center_axis',(0.,0.,1.));
#118911=DIRECTION('ref_axis',(1.,0.,0.));
#118912=DIRECTION('center_axis',(0.35759903131472,0.657040215773453,-0.663642288932184));
#118913=DIRECTION('ref_axis',(-5.60662627435704E-15,0.710632718732561,0.703563173472552));
#118914=DIRECTION('center_axis',(0.907160802328706,-0.4207841236529,0.));
#118915=DIRECTION('ref_axis',(0.4207841236529,0.907160802328706,0.));
#118916=DIRECTION('',(0.,0.,1.));
#118917=DIRECTION('center_axis',(-0.907158740845994,0.420788567931076,2.28597559952643E-6));
#118918=DIRECTION('ref_axis',(0.398329828542875,0.858742727515624,-0.322326349577615));
#118919=DIRECTION('',(0.,0.,-1.));
#118920=DIRECTION('center_axis',(-0.845904345266859,-0.533334640407547,
0.));
#118921=DIRECTION('ref_axis',(0.533334640407547,-0.845904345266859,0.));
#118922=DIRECTION('center_axis',(0.845904345266846,0.533334640407567,1.08502118212513E-14));
#118923=DIRECTION('ref_axis',(0.532618548222918,-0.844768575255463,-0.0518028604399965));
#118924=DIRECTION('',(0.,0.,1.));
#118925=DIRECTION('',(0.,0.,1.));
#118926=DIRECTION('center_axis',(0.,0.,1.));
#118927=DIRECTION('ref_axis',(0.997945392750336,0.0640702199807127,0.));
#118928=DIRECTION('center_axis',(0.,0.,-1.));
#118929=DIRECTION('ref_axis',(-0.997945392750336,-0.0640702199807127,0.));
#118930=DIRECTION('center_axis',(-0.955852314850969,0.175249125470288,-0.23586881145235));
#118931=DIRECTION('ref_axis',(0.290355212970421,0.686675546334093,-0.666461209949743));
#118932=DIRECTION('center_axis',(-0.925594419806206,-0.296042013585335,
0.23586881145237));
#118933=DIRECTION('ref_axis',(0.375781520548681,-0.643908149072147,0.66646120995344));
#118934=DIRECTION('center_axis',(0.,0.,-1.));
#118935=DIRECTION('ref_axis',(-0.997945392750336,-0.0640702199807131,0.));
#118936=DIRECTION('center_axis',(0.996931752839329,0.0782756678713373,-6.76296429840134E-17));
#118937=DIRECTION('ref_axis',(0.0782756678713373,-0.996931752839329,-6.93889390390711E-14));
#118938=DIRECTION('center_axis',(0.,0.,1.));
#118939=DIRECTION('ref_axis',(0.997945392750336,0.0640702199807131,0.));
#118940=DIRECTION('center_axis',(0.998756627165696,0.0498517772261152,-1.38914942345546E-16));
#118941=DIRECTION('ref_axis',(-0.0498517772261152,0.998756627165696,-2.31111593326468E-32));
#118942=DIRECTION('center_axis',(0.,0.,-1.));
#118943=DIRECTION('ref_axis',(-0.997945392750337,-0.0640702199806997,0.));
#118944=DIRECTION('center_axis',(0.,0.,1.));
#118945=DIRECTION('ref_axis',(0.997945392750337,0.0640702199806998,0.));
#118946=DIRECTION('center_axis',(0.,0.,1.));
#118947=DIRECTION('ref_axis',(0.997945392750337,0.0640702199806998,0.));
#118948=DIRECTION('center_axis',(0.398961016913279,-0.632778807581564,0.663642288932205));
#118949=DIRECTION('ref_axis',(0.0455303946146861,-0.709172647596825,-0.703563173472533));
#118950=DIRECTION('center_axis',(0.400108460798371,-0.634598730187018,0.661209249211309));
#118951=DIRECTION('ref_axis',(0.0453826414436699,-0.706871272693763,-0.705884848750769));
#118952=DIRECTION('center_axis',(0.315672891441105,0.68055341771725,-0.661209249211308));
#118953=DIRECTION('ref_axis',(-0.0453826414436428,0.706871272693764,0.705884848750769));
#118954=DIRECTION('center_axis',(0.314767594591728,0.678601704784028,-0.663642288932184));
#118955=DIRECTION('ref_axis',(-0.0455303946146921,0.709172647596805,0.703563173472552));
#118956=DIRECTION('center_axis',(0.,0.,1.));
#118957=DIRECTION('ref_axis',(0.997945392750337,0.0640702199806998,0.));
#118958=DIRECTION('center_axis',(0.,0.,1.));
#118959=DIRECTION('ref_axis',(0.997945392750337,0.0640702199806998,0.));
#118960=DIRECTION('center_axis',(0.,0.,1.));
#118961=DIRECTION('ref_axis',(-0.997945392750335,-0.0640702199807343,0.));
#118962=DIRECTION('center_axis',(0.,0.,-1.));
#118963=DIRECTION('ref_axis',(0.997945392750336,0.0640702199807131,0.));
#118964=DIRECTION('center_axis',(0.845904345266866,-0.533334640407535,0.));
#118965=DIRECTION('ref_axis',(0.533334640407535,0.845904345266866,0.));
#118966=DIRECTION('',(0.,0.,1.));
#118967=DIRECTION('center_axis',(-0.845901732387246,0.533338784581648,2.28597556045616E-6));
#118968=DIRECTION('ref_axis',(0.504873128786825,0.800755173733894,-0.322326349477363));
#118969=DIRECTION('',(0.,0.,-1.));
#118970=DIRECTION('center_axis',(-0.907160802328699,-0.420784123652913,
0.));
#118971=DIRECTION('ref_axis',(0.420784123652913,-0.907160802328699,0.));
#118972=DIRECTION('center_axis',(0.907160802328718,0.420784123652874,-2.15297035264327E-14));
#118973=DIRECTION('ref_axis',(0.420219149620008,-0.905942785136197,-0.0518028604645239));
#118974=DIRECTION('',(0.,0.,1.));
#118975=DIRECTION('',(0.,0.,1.));
#118976=DIRECTION('center_axis',(0.,0.,1.));
#118977=DIRECTION('ref_axis',(0.997945392750336,-0.0640702199807125,0.));
#118978=DIRECTION('center_axis',(0.,0.,-1.));
#118979=DIRECTION('ref_axis',(-0.997945392750336,0.0640702199807125,0.));
#118980=DIRECTION('center_axis',(-0.92559441980614,0.296042013585654,-0.23586881145223));
#118981=DIRECTION('ref_axis',(0.375781520549103,0.643908149076686,-0.666461209948816));
#118982=DIRECTION('center_axis',(-0.95585231485097,-0.175249125470276,0.235868811452355));
#118983=DIRECTION('ref_axis',(0.290355212970749,-0.686675546328891,0.66646120995496));
#118984=DIRECTION('center_axis',(0.,0.,-1.));
#118985=DIRECTION('ref_axis',(-0.997945392750337,0.0640702199806987,0.));
#118986=DIRECTION('center_axis',(0.998756627165697,-0.0498517772261013,
-6.76296429840134E-17));
#118987=DIRECTION('ref_axis',(-0.0498517772261013,-0.998756627165697,-7.04890359645728E-32));
#118988=DIRECTION('center_axis',(0.,0.,1.));
#118989=DIRECTION('ref_axis',(0.997945392750337,-0.0640702199806987,0.));
#118990=DIRECTION('center_axis',(0.99693175283933,-0.0782756678713235,-1.38914942345546E-16));
#118991=DIRECTION('ref_axis',(0.0782756678713235,0.99693175283933,-1.27881748307313E-31));
#118992=DIRECTION('center_axis',(0.,0.,-1.));
#118993=DIRECTION('ref_axis',(-0.997945392750337,0.0640702199806997,0.));
#118994=DIRECTION('center_axis',(0.,0.,1.));
#118995=DIRECTION('ref_axis',(0.997945392750337,-0.0640702199806996,0.));
#118996=DIRECTION('center_axis',(0.,0.,1.));
#118997=DIRECTION('ref_axis',(0.997945392750337,-0.0640702199806997,0.));
#118998=DIRECTION('center_axis',(0.31476759459173,-0.678601704784007,0.663642288932205));
#118999=DIRECTION('ref_axis',(-0.0455303946146791,-0.709172647596825,-0.703563173472533));
#119000=DIRECTION('center_axis',(0.315672891441116,-0.680553417717245,0.661209249211309));
#119001=DIRECTION('ref_axis',(-0.0453826414436315,-0.706871272693765,-0.705884848750768));
#119002=DIRECTION('center_axis',(0.400108460798361,0.634598730187025,-0.661209249211308));
#119003=DIRECTION('ref_axis',(0.0453826414436588,0.706871272693763,0.70588484875077));
#119004=DIRECTION('center_axis',(0.39896101691328,0.632778807581586,-0.663642288932184));
#119005=DIRECTION('ref_axis',(0.0455303946146747,0.709172647596805,0.703563173472553));
#119006=DIRECTION('center_axis',(0.,0.,1.));
#119007=DIRECTION('ref_axis',(0.997945392750337,-0.0640702199806997,0.));
#119008=DIRECTION('center_axis',(0.,0.,1.));
#119009=DIRECTION('ref_axis',(0.997945392750337,-0.0640702199806997,0.));
#119010=DIRECTION('center_axis',(0.,0.,1.));
#119011=DIRECTION('ref_axis',(-0.997945392750337,0.0640702199806997,0.));
#119012=DIRECTION('center_axis',(0.,0.,-1.));
#119013=DIRECTION('ref_axis',(0.997945392750337,-0.0640702199806987,0.));
#119014=DIRECTION('center_axis',(0.809995476332314,-0.586436124672745,0.));
#119015=DIRECTION('ref_axis',(0.586436124672745,0.809995476332314,0.));
#119016=DIRECTION('',(0.,0.,1.));
#119017=DIRECTION('center_axis',(-0.809992603302981,0.586440092924448,2.28597557991567E-6));
#119018=DIRECTION('ref_axis',(0.555140372897279,0.766762603882455,-0.322326349631654));
#119019=DIRECTION('',(0.,0.,-1.));
#119020=DIRECTION('center_axis',(-0.932256674534458,-0.361797585378833,
0.));
#119021=DIRECTION('ref_axis',(0.361797585378833,-0.932256674534458,0.));
#119022=DIRECTION('center_axis',(0.932256674534446,0.361797585378863,9.65517100877403E-15));
#119023=DIRECTION('ref_axis',(0.361311810776095,-0.9310049618806,-0.0518028604171809));
#119024=DIRECTION('',(0.,0.,1.));
#119025=DIRECTION('',(0.,0.,1.));
#119026=DIRECTION('center_axis',(0.,0.,1.));
#119027=DIRECTION('ref_axis',(0.991790013823251,-0.127877161684469,0.));
#119028=DIRECTION('center_axis',(0.,0.,-1.));
#119029=DIRECTION('ref_axis',(-0.991790013823251,0.127877161684469,0.));
#119030=DIRECTION('center_axis',(-0.904725209867088,0.354736801607889,-0.23586881145238));
#119031=DIRECTION('ref_axis',(0.416264773871857,0.618508766043805,-0.666461209944271));
#119032=DIRECTION('center_axis',(-0.96511666377558,-0.113647389264867,0.235868811452411));
#119033=DIRECTION('ref_axis',(0.245763193736037,-0.703867820144193,0.666461209951581));
#119034=DIRECTION('center_axis',(0.,0.,-1.));
#119035=DIRECTION('ref_axis',(-0.991790013823248,0.127877161684492,0.));
#119036=DIRECTION('center_axis',(0.993510560225567,-0.113739908212905,-6.76296429840134E-17));
#119037=DIRECTION('ref_axis',(-0.113739908212905,-0.993510560225567,2.46519032881566E-32));
#119038=DIRECTION('center_axis',(0.,0.,1.));
#119039=DIRECTION('ref_axis',(0.991790013823248,-0.127877161684492,0.));
#119040=DIRECTION('center_axis',(0.989868310372873,-0.141988478826816,-1.38914942345546E-16));
#119041=DIRECTION('ref_axis',(0.141988478826816,0.989868310372873,1.41748443906901E-31));
#119042=DIRECTION('center_axis',(0.,0.,-1.));
#119043=DIRECTION('ref_axis',(-0.99179001382325,0.127877161684477,0.));
#119044=DIRECTION('center_axis',(0.,0.,1.));
#119045=DIRECTION('ref_axis',(0.99179001382325,-0.127877161684477,0.));
#119046=DIRECTION('center_axis',(0.,0.,1.));
#119047=DIRECTION('ref_axis',(0.99179001382325,-0.127877161684477,0.));
#119048=DIRECTION('center_axis',(0.270642710305125,-0.697374673830015,0.663642288932205));
#119049=DIRECTION('ref_axis',(-0.0908736950716529,-0.704798433935037,-0.703563173472534));
#119050=DIRECTION('center_axis',(0.271421100448069,-0.699380379327999,0.661209249211309));
#119051=DIRECTION('ref_axis',(-0.0905787958790508,-0.702511254031711,-0.705884848750768));
#119052=DIRECTION('center_axis',(0.439945275296716,0.60765984193586,-0.661209249211308));
#119053=DIRECTION('ref_axis',(0.0905787958790733,0.702511254031707,0.705884848750769));
#119054=DIRECTION('center_axis',(0.438683586116482,0.605917175538733,-0.663642288932184));
#119055=DIRECTION('ref_axis',(0.0908736950716462,0.704798433935021,0.703563173472551));
#119056=DIRECTION('center_axis',(0.,0.,1.));
#119057=DIRECTION('ref_axis',(0.99179001382325,-0.127877161684477,0.));
#119058=DIRECTION('center_axis',(0.,0.,1.));
#119059=DIRECTION('ref_axis',(0.99179001382325,-0.127877161684477,0.));
#119060=DIRECTION('center_axis',(0.,0.,1.));
#119061=DIRECTION('ref_axis',(-0.991790013823245,0.127877161684512,0.));
#119062=DIRECTION('center_axis',(0.,0.,-1.));
#119063=DIRECTION('ref_axis',(0.991790013823248,-0.127877161684492,0.));
#119064=DIRECTION('center_axis',(0.770758162242027,-0.637127817111522,0.));
#119065=DIRECTION('ref_axis',(0.637127817111522,0.770758162242027,0.));
#119066=DIRECTION('',(0.,0.,1.));
#119067=DIRECTION('center_axis',(-0.770755040868878,0.637131593134407,2.28597557558209E-6));
#119068=DIRECTION('ref_axis',(0.6031264261884,0.729619242092798,-0.322326349529696));
#119069=DIRECTION('',(0.,0.,-1.));
#119070=DIRECTION('center_axis',(-0.953521704096125,-0.301324343221092,
0.));
#119071=DIRECTION('ref_axis',(0.301324343221092,-0.953521704096125,0.));
#119072=DIRECTION('center_axis',(0.953521704096107,0.301324343221148,2.82636636602641E-14));
#119073=DIRECTION('ref_axis',(0.3009197642001,-0.952241439536436,-0.0518028603779049));
#119074=DIRECTION('',(0.,0.,1.));
#119075=DIRECTION('',(0.,0.,1.));
#119076=DIRECTION('center_axis',(0.,0.,1.));
#119077=DIRECTION('ref_axis',(0.981559156991069,-0.191158628701354,0.));
#119078=DIRECTION('center_axis',(0.,0.,-1.));
#119079=DIRECTION('ref_axis',(-0.981559156991069,0.191158628701354,0.));
#119080=DIRECTION('center_axis',(-0.880138289977599,0.411973900022062,-0.235868811452301));
#119081=DIRECTION('ref_axis',(0.455037505948351,0.59056779780744,-0.666461209953869));
#119082=DIRECTION('center_axis',(-0.970415141311856,-0.0515786515599852,
0.235868811452352));
#119083=DIRECTION('ref_axis',(0.200161280821658,-0.718167750108659,0.666461209946761));
#119084=DIRECTION('center_axis',(0.,0.,-1.));
#119085=DIRECTION('ref_axis',(-0.981559156991068,0.191158628701359,0.));
#119086=DIRECTION('center_axis',(0.984181945286123,-0.177160657519729,-6.76296429840134E-17));
#119087=DIRECTION('ref_axis',(-0.177160657519728,-0.984181945286123,-1.86430018616684E-31));
#119088=DIRECTION('center_axis',(0.,0.,1.));
#119089=DIRECTION('ref_axis',(0.981559156991068,-0.191158628701359,0.));
#119090=DIRECTION('center_axis',(0.978737286693008,-0.205117828666377,-1.38914942345546E-16));
#119091=DIRECTION('ref_axis',(0.205117828666377,0.978737286693008,2.65007960347684E-31));
#119092=DIRECTION('center_axis',(0.,0.,-1.));
#119093=DIRECTION('ref_axis',(-0.981559156991067,0.191158628701365,0.));
#119094=DIRECTION('center_axis',(0.,0.,1.));
#119095=DIRECTION('ref_axis',(0.981559156991067,-0.191158628701365,0.));
#119096=DIRECTION('center_axis',(0.,0.,1.));
#119097=DIRECTION('ref_axis',(0.981559156991067,-0.191158628701365,0.));
#119098=DIRECTION('center_axis',(0.225405697069196,-0.713281980754858,0.663642288932205));
#119099=DIRECTION('ref_axis',(-0.135843576023237,-0.697528052329422,-0.703563173472533));
#119100=DIRECTION('center_axis',(0.226053981933637,-0.715333436943475,0.661209249211309));
#119101=DIRECTION('ref_axis',(-0.135402742613109,-0.695264465938648,-0.705884848750768));
#119102=DIRECTION('center_axis',(0.477974260290913,0.578223949051553,-0.661209249211308));
#119103=DIRECTION('ref_axis',(0.135402742613123,0.695264465938647,0.705884848750766));
#119104=DIRECTION('center_axis',(0.476603510366998,0.576565699852764,-0.663642288932184));
#119105=DIRECTION('ref_axis',(0.135843576023234,0.697528052329402,0.703563173472553));
#119106=DIRECTION('center_axis',(0.,0.,1.));
#119107=DIRECTION('ref_axis',(0.981559156991067,-0.191158628701365,0.));
#119108=DIRECTION('center_axis',(0.,0.,1.));
#119109=DIRECTION('ref_axis',(0.981559156991067,-0.191158628701365,0.));
#119110=DIRECTION('center_axis',(0.,0.,1.));
#119111=DIRECTION('ref_axis',(-0.981559156991053,0.191158628701434,0.));
#119112=DIRECTION('center_axis',(0.,0.,-1.));
#119113=DIRECTION('ref_axis',(0.981559156991068,-0.191158628701359,0.));
#119114=DIRECTION('center_axis',(0.72835363753598,-0.685201414686299,0.));
#119115=DIRECTION('ref_axis',(0.685201414686299,0.72835363753598,0.));
#119116=DIRECTION('',(0.,0.,1.));
#119117=DIRECTION('center_axis',(-0.728350280645418,0.685204982963868,2.28597556927344E-6));
#119118=DIRECTION('ref_axis',(0.64863410361422,0.689477718317584,-0.322326349484735));
#119119=DIRECTION('',(0.,0.,-1.));
#119120=DIRECTION('center_axis',(-0.970868508445896,-0.239612894703187,
0.));
#119121=DIRECTION('ref_axis',(0.239612894703187,-0.970868508445896,0.));
#119122=DIRECTION('center_axis',(0.970868508445893,0.2396128947032,6.25973758918642E-15));
#119123=DIRECTION('ref_axis',(0.239291173764822,-0.969564952859012,-0.0518028604012878));
#119124=DIRECTION('',(0.,0.,1.));
#119125=DIRECTION('',(0.,0.,1.));
#119126=DIRECTION('center_axis',(0.,0.,1.));
#119127=DIRECTION('ref_axis',(0.967294863039036,-0.253654583909484,0.));
#119128=DIRECTION('center_axis',(0.,0.,-1.));
#119129=DIRECTION('ref_axis',(-0.967294863039036,0.253654583909484,0.));
#119130=DIRECTION('center_axis',(-0.851934693065667,0.467518109312524,-0.235868811452362));
#119131=DIRECTION('ref_axis',(0.491940391308073,0.560200059820671,-0.666461209956421));
#119132=DIRECTION('center_axis',(-0.971725974879091,0.0107020338878708,
0.235868811452347));
#119133=DIRECTION('ref_axis',(0.153736862270404,-0.729516574736984,0.666461209946437));
#119134=DIRECTION('center_axis',(0.,0.,-1.));
#119135=DIRECTION('ref_axis',(-0.967294863039033,0.253654583909494,0.));
#119136=DIRECTION('center_axis',(0.970809115627134,-0.239853415683961,-6.76296429840134E-17));
#119137=DIRECTION('ref_axis',(-0.239853415683961,-0.970809115627134,2.49600520792586E-31));
#119138=DIRECTION('center_axis',(0.,0.,1.));
#119139=DIRECTION('ref_axis',(0.967294863039033,-0.253654583909494,0.));
#119140=DIRECTION('center_axis',(0.963584421563631,-0.267404305350311,-1.38914942345546E-16));
#119141=DIRECTION('ref_axis',(0.267404305350311,0.963584421563631,-5.17689969051289E-31));
#119142=DIRECTION('center_axis',(0.,0.,-1.));
#119143=DIRECTION('ref_axis',(-0.967294863039033,0.253654583909495,0.));
#119144=DIRECTION('center_axis',(0.,0.,1.));
#119145=DIRECTION('ref_axis',(0.967294863039033,-0.253654583909495,0.));
#119146=DIRECTION('center_axis',(0.,0.,1.));
#119147=DIRECTION('ref_axis',(0.967294863039033,-0.253654583909495,0.));
#119148=DIRECTION('center_axis',(0.17924244347464,-0.726258259022274,0.663642288932205));
#119149=DIRECTION('ref_axis',(-0.180255246582584,-0.687391378337487,-0.703563173472534));
#119150=DIRECTION('center_axis',(0.179757959119013,-0.728347036028008,0.661209249211309));
#119151=DIRECTION('ref_axis',(-0.179670290433975,-0.685160687021283,-0.705884848750768));
#119152=DIRECTION('center_axis',(0.514039146524416,0.546412009931945,-0.661209249211308));
#119153=DIRECTION('ref_axis',(0.179670290433995,0.685160687021278,0.705884848750768));
#119154=DIRECTION('center_axis',(0.512564968562283,0.544844992033145,-0.663642288932184));
#119155=DIRECTION('ref_axis',(0.18025524658258,0.687391378337467,0.703563173472554));
#119156=DIRECTION('center_axis',(0.,0.,1.));
#119157=DIRECTION('ref_axis',(0.967294863039033,-0.253654583909495,0.));
#119158=DIRECTION('center_axis',(0.,0.,1.));
#119159=DIRECTION('ref_axis',(0.967294863039033,-0.253654583909495,0.));
#119160=DIRECTION('center_axis',(0.,0.,1.));
#119161=DIRECTION('ref_axis',(-0.967294863039023,0.253654583909532,0.));
#119162=DIRECTION('center_axis',(0.,0.,-1.));
#119163=DIRECTION('ref_axis',(0.967294863039033,-0.253654583909494,0.));
#119164=DIRECTION('center_axis',(0.682956151501933,-0.730459372672888,0.));
#119165=DIRECTION('ref_axis',(0.730459372672888,0.682956151501933,0.));
#119166=DIRECTION('',(0.,0.,1.));
#119167=DIRECTION('center_axis',(-0.68295257288816,0.730462718542307,2.28597555346301E-6));
#119168=DIRECTION('ref_axis',(0.691476404350399,0.646502982678044,-0.322326349551254));
#119169=DIRECTION('',(0.,0.,-1.));
#119170=DIRECTION('center_axis',(-0.984225805843822,-0.176916825404141,
0.));
#119171=DIRECTION('ref_axis',(0.176916825404141,-0.984225805843822,0.));
#119172=DIRECTION('center_axis',(0.98422580584382,0.176916825404152,4.71377209367484E-15));
#119173=DIRECTION('ref_axis',(0.176679284569281,-0.982904315821103,-0.0518028603875932));
#119174=DIRECTION('',(0.,0.,1.));
#119175=DIRECTION('',(0.,0.,1.));
#119176=DIRECTION('center_axis',(0.,0.,1.));
#119177=DIRECTION('ref_axis',(0.949055747010676,-0.315108218023599,0.));
#119178=DIRECTION('center_axis',(0.,0.,-1.));
#119179=DIRECTION('ref_axis',(-0.949055747010676,0.315108218023599,0.));
#119180=DIRECTION('center_axis',(-0.820230313760466,0.521141186409628,-0.23586881145241));
#119181=DIRECTION('ref_axis',(0.526821788086614,0.527530339649154,-0.666461209934135));
#119182=DIRECTION('center_axis',(-0.969043777980991,0.0729387423828848,
0.235868811452321));
#119183=DIRECTION('ref_axis',(0.106680705972949,-0.737867659286837,0.666461209937741));
#119184=DIRECTION('center_axis',(0.,0.,-1.));
#119185=DIRECTION('ref_axis',(-0.949055747010673,0.315108218023608,0.));
#119186=DIRECTION('center_axis',(0.95344702307413,-0.301560564714753,-6.76296429840134E-17));
#119187=DIRECTION('ref_axis',(-0.301560564714752,-0.953447023074129,4.31408307542741E-31));
#119188=DIRECTION('center_axis',(0.,0.,1.));
#119189=DIRECTION('ref_axis',(0.949055747010673,-0.315108218023608,0.));
#119190=DIRECTION('center_axis',(0.944471981357839,-0.328591960385517,-1.38914942345546E-16));
#119191=DIRECTION('ref_axis',(0.328591960385517,0.944471981357839,-5.54667823983524E-32));
#119192=DIRECTION('center_axis',(0.,0.,-1.));
#119193=DIRECTION('ref_axis',(-0.949055747010673,0.315108218023608,0.));
#119194=DIRECTION('center_axis',(0.,0.,1.));
#119195=DIRECTION('ref_axis',(0.949055747010673,-0.315108218023608,0.));
#119196=DIRECTION('center_axis',(0.,0.,1.));
#119197=DIRECTION('ref_axis',(0.949055747010673,-0.315108218023608,0.));
#119198=DIRECTION('center_axis',(0.132342644232462,-0.73625018632146,0.663642288932205));
#119199=DIRECTION('ref_axis',(-0.223926209669094,-0.674430065726974,-0.703563173472534));
#119200=DIRECTION('center_axis',(0.132723272292407,-0.738367700911553,0.661209249211309));
#119201=DIRECTION('ref_axis',(-0.223199534492288,-0.672241435874441,-0.705884848750768));
#119202=DIRECTION('center_axis',(0.547991735643799,0.512354746658518,-0.661209249211308));
#119203=DIRECTION('ref_axis',(0.223199534492304,0.672241435874438,0.705884848750766));
#119204=DIRECTION('center_axis',(0.546420187356905,0.510885399272378,-0.663642288932184));
#119205=DIRECTION('ref_axis',(0.223926209669088,0.674430065726956,0.703563173472553));
#119206=DIRECTION('center_axis',(0.,0.,1.));
#119207=DIRECTION('ref_axis',(0.949055747010673,-0.315108218023608,0.));
#119208=DIRECTION('center_axis',(0.,0.,1.));
#119209=DIRECTION('ref_axis',(0.949055747010673,-0.315108218023608,0.));
#119210=DIRECTION('center_axis',(0.,0.,1.));
#119211=DIRECTION('ref_axis',(-0.949055747010673,0.315108218023608,0.));
#119212=DIRECTION('center_axis',(0.,0.,-1.));
#119213=DIRECTION('ref_axis',(0.949055747010673,-0.315108218023608,0.));
#119214=DIRECTION('center_axis',(0.634752252147729,-0.772715716414119,0.));
#119215=DIRECTION('ref_axis',(0.772715716414119,0.634752252147729,0.));
#119216=DIRECTION('',(0.,0.,1.));
#119217=DIRECTION('center_axis',(-0.634748466516036,0.7727188261265,2.28597554464543E-6));
#119218=DIRECTION('ref_axis',(0.731477280222137,0.600871627613825,-0.32232634960167));
#119219=DIRECTION('',(0.,0.,-1.));
#119220=DIRECTION('center_axis',(-0.993538708289762,-0.11349376692097,0.));
#119221=DIRECTION('ref_axis',(0.11349376692097,-0.993538708289762,0.));
#119222=DIRECTION('center_axis',(0.993538708289754,0.113493766921037,4.01381961779349E-14));
#119223=DIRECTION('ref_axis',(0.113341382295796,-0.992204714116904,-0.0518028603792472));
#119224=DIRECTION('',(0.,0.,1.));
#119225=DIRECTION('',(0.,0.,1.));
#119226=DIRECTION('center_axis',(0.,0.,1.));
#119227=DIRECTION('ref_axis',(0.926916757346023,-0.375267004879372,0.));
#119228=DIRECTION('center_axis',(0.,0.,-1.));
#119229=DIRECTION('ref_axis',(-0.926916757346023,0.375267004879372,0.));
#119230=DIRECTION('center_axis',(-0.785155432156975,0.5726227825877,-0.235868811452283));
#119231=DIRECTION('ref_axis',(0.559538361126876,0.492692884129058,-0.666461209941013));
#119232=DIRECTION('center_axis',(-0.962379572339952,0.13487572994007,0.235868811452266));
#119233=DIRECTION('ref_axis',(0.059186175777223,-0.74318668733606,0.666461209946476));
#119234=DIRECTION('center_axis',(0.,0.,-1.));
#119235=DIRECTION('ref_axis',(-0.926916757346027,0.375267004879361,0.));
#119236=DIRECTION('center_axis',(0.932167012189569,-0.362028536700592,-6.76296429840134E-17));
#119237=DIRECTION('ref_axis',(-0.362028536700592,-0.932167012189569,3.6669706141133E-31));
#119238=DIRECTION('center_axis',(0.,0.,1.));
#119239=DIRECTION('ref_axis',(0.926916757346027,-0.375267004879361,0.));
#119240=DIRECTION('center_axis',(0.921478503192044,-0.388429360572744,-1.38914942345546E-16));
#119241=DIRECTION('ref_axis',(0.388429360572744,0.921478503192044,-5.91645678915759E-31));
#119242=DIRECTION('center_axis',(0.,0.,-1.));
#119243=DIRECTION('ref_axis',(-0.926916757346032,0.375267004879348,0.));
#119244=DIRECTION('center_axis',(0.,0.,1.));
#119245=DIRECTION('ref_axis',(0.926916757346034,-0.375267004879345,0.));
#119246=DIRECTION('center_axis',(0.,0.,1.));
#119247=DIRECTION('ref_axis',(0.926916757346032,-0.375267004879348,0.));
#119248=DIRECTION('center_axis',(0.084899020677726,-0.74321670367988,0.663642288932205));
#119249=DIRECTION('ref_axis',(-0.266677011928052,-0.658697375311594,-0.703563173472533));
#119250=DIRECTION('center_axis',(0.0851431970709001,-0.745354254532677,
0.661209249211309));
#119251=DIRECTION('ref_axis',(-0.265811603787226,-0.656559800472256,-0.705884848750768));
#119252=DIRECTION('center_axis',(0.579692509177563,0.476192107831323,-0.661209249211308));
#119253=DIRECTION('ref_axis',(0.265811603787246,0.656559800472247,0.705884848750769));
#119254=DIRECTION('center_axis',(0.578030048394914,0.474826468821427,-0.663642288932184));
#119255=DIRECTION('ref_axis',(0.266677011928042,0.658697375311578,0.703563173472553));
#119256=DIRECTION('center_axis',(0.,0.,1.));
#119257=DIRECTION('ref_axis',(0.926916757346032,-0.375267004879348,0.));
#119258=DIRECTION('center_axis',(0.,0.,1.));
#119259=DIRECTION('ref_axis',(0.926916757346032,-0.375267004879348,0.));
#119260=DIRECTION('center_axis',(0.,0.,1.));
#119261=DIRECTION('ref_axis',(-0.92691675734602,0.375267004879378,0.));
#119262=DIRECTION('center_axis',(0.,0.,-1.));
#119263=DIRECTION('ref_axis',(0.926916757346027,-0.375267004879361,0.));
#119264=DIRECTION('center_axis',(0.583940019635519,-0.811796805529604,0.));
#119265=DIRECTION('ref_axis',(0.811796805529604,0.583940019635519,0.));
#119266=DIRECTION('',(0.,0.,1.));
#119267=DIRECTION('center_axis',(-0.583936042541851,0.811799666306495,2.28597553788018E-6));
#119268=DIRECTION('ref_axis',(0.768472359063816,0.552771162159179,-0.322326349590107));
#119269=DIRECTION('',(0.,0.,-1.));
#119270=DIRECTION('center_axis',(-0.998768947069955,-0.0496043382051838,
0.));
#119271=DIRECTION('ref_axis',(0.0496043382051838,-0.998768947069955,0.));
#119272=DIRECTION('center_axis',(0.998768947069955,0.0496043382051736,2.70781072986654E-15));
#119273=DIRECTION('ref_axis',(0.0495377359703026,-0.997427930408881,-0.0518028604923819));
#119274=DIRECTION('',(0.,0.,1.));
#119275=DIRECTION('',(0.,0.,1.));
#119276=DIRECTION('center_axis',(0.,0.,1.));
#119277=DIRECTION('ref_axis',(0.900968867902423,-0.433883739117549,0.));
#119278=DIRECTION('center_axis',(0.,0.,-1.));
#119279=DIRECTION('ref_axis',(-0.900968867902423,0.433883739117549,0.));
#119280=DIRECTION('center_axis',(-0.746854178467622,0.621751348924587,-0.235868811452277));
#119281=DIRECTION('ref_axis',(0.589955671021752,0.455830847870496,-0.666461209943188));
#119282=DIRECTION('center_axis',(-0.951760742606293,0.196258484192558,0.23586881145238));
#119283=DIRECTION('ref_axis',(0.0114484368870036,-0.745451801882072,0.666461209946698));
#119284=DIRECTION('center_axis',(0.,0.,-1.));
#119285=DIRECTION('ref_axis',(-0.900968867902425,0.433883739117546,0.));
#119286=DIRECTION('center_axis',(0.907056527102724,-0.421008855774252,-6.76296429840134E-17));
#119287=DIRECTION('ref_axis',(-0.421008855774252,-0.907056527102724,-4.77630626208034E-31));
#119288=DIRECTION('center_axis',(0.,0.,1.));
#119289=DIRECTION('ref_axis',(0.900968867902425,-0.433883739117546,0.));
#119290=DIRECTION('center_axis',(0.894698472200112,-0.446670621199542,-1.38914942345546E-16));
#119291=DIRECTION('ref_axis',(0.446670621199542,0.894698472200112,1.0230539864585E-30));
#119292=DIRECTION('center_axis',(0.,0.,-1.));
#119293=DIRECTION('ref_axis',(-0.900968867902428,0.433883739117539,0.));
#119294=DIRECTION('center_axis',(0.,0.,1.));
#119295=DIRECTION('ref_axis',(0.900968867902428,-0.433883739117539,0.));
#119296=DIRECTION('center_axis',(0.,0.,1.));
#119297=DIRECTION('ref_axis',(0.900968867902428,-0.433883739117539,0.));
#119298=DIRECTION('center_axis',(0.0371065288362414,-0.747129184183397,
0.663642288932205));
#119299=DIRECTION('ref_axis',(-0.308331981142967,-0.640257956090913,-0.703563173472531));
#119300=DIRECTION('center_axis',(0.0372132501894693,-0.74927798764394,0.661209249211309));
#119301=DIRECTION('ref_axis',(-0.307331396185796,-0.638180220018293,-0.705884848750767));
#119302=DIRECTION('center_axis',(0.609011201847464,0.438072693490162,-0.661209249211308));
#119303=DIRECTION('ref_axis',(0.307331396185818,0.638180220018277,0.705884848750771));
#119304=DIRECTION('center_axis',(0.607264659977013,0.436816374560129,-0.663642288932184));
#119305=DIRECTION('ref_axis',(0.308331981142939,0.640257956090907,0.703563173472549));
#119306=DIRECTION('center_axis',(0.,0.,1.));
#119307=DIRECTION('ref_axis',(0.900968867902428,-0.433883739117539,0.));
#119308=DIRECTION('center_axis',(0.,0.,1.));
#119309=DIRECTION('ref_axis',(0.900968867902428,-0.433883739117539,0.));
#119310=DIRECTION('center_axis',(0.,0.,1.));
#119311=DIRECTION('ref_axis',(-0.900968867902391,0.433883739117616,0.));
#119312=DIRECTION('center_axis',(0.,0.,-1.));
#119313=DIRECTION('ref_axis',(0.900968867902425,-0.433883739117546,0.));
#119314=DIRECTION('center_axis',(0.530728252327885,-0.847542047441299,0.));
#119315=DIRECTION('ref_axis',(0.847542047441299,0.530728252327885,0.));
#119316=DIRECTION('',(0.,0.,1.));
#119317=DIRECTION('center_axis',(-0.530724100114921,0.847544647527186,2.28597557003377E-6));
#119318=DIRECTION('ref_axis',(0.802309620145797,0.502399241429844,-0.322326349577915));
#119319=DIRECTION('',(0.,0.,-1.));
#119320=DIRECTION('center_axis',(-0.99989503001137,0.0144889253763841,0.));
#119321=DIRECTION('ref_axis',(-0.0144889253763841,-0.99989503001137,0.));
#119322=DIRECTION('center_axis',(0.999895030011368,-0.0144889253764847,
-4.6873341868105E-14));
#119323=DIRECTION('ref_axis',(0.0144694715375623,0.998552501400717,0.05180286034375));
#119324=DIRECTION('',(0.,0.,1.));
#119325=DIRECTION('',(0.,0.,1.));
#119326=DIRECTION('center_axis',(0.,0.,1.));
#119327=DIRECTION('ref_axis',(0.871318704123387,-0.490717552003943,0.));
#119328=DIRECTION('center_axis',(0.,0.,-1.));
#119329=DIRECTION('ref_axis',(-0.871318704123387,0.490717552003943,0.));
#119330=DIRECTION('center_axis',(-0.705483940759205,0.668325005603511,-0.235868811452319));
#119331=DIRECTION('ref_axis',(0.61794872651875,0.417095704882099,-0.666461209946056));
#119332=DIRECTION('center_axis',(-0.937230923829315,0.256834770235852,0.235868811452352));
#119333=DIRECTION('ref_axis',(-0.0363363460779518,-0.744653695061158,0.666461209963091));
#119334=DIRECTION('center_axis',(0.,0.,-1.));
#119335=DIRECTION('ref_axis',(-0.871318704123396,0.490717552003926,0.));
#119336=DIRECTION('center_axis',(0.878218752183,-0.478259159153418,-6.76296429840134E-17));
#119337=DIRECTION('ref_axis',(-0.478259159153418,-0.878218752183,-8.62816615085482E-32));
#119338=DIRECTION('center_axis',(0.,0.,1.));
#119339=DIRECTION('ref_axis',(0.871318704123396,-0.490717552003926,0.));
#119340=DIRECTION('center_axis',(0.864241933273691,-0.503076416433282,-1.38914942345546E-16));
#119341=DIRECTION('ref_axis',(0.503076416433282,0.864241933273691,-4.31408307542741E-31));
#119342=DIRECTION('center_axis',(0.,0.,-1.));
#119343=DIRECTION('ref_axis',(-0.871318704123396,0.490717552003927,0.));
#119344=DIRECTION('center_axis',(0.,0.,1.));
#119345=DIRECTION('ref_axis',(0.871318704123396,-0.490717552003927,0.));
#119346=DIRECTION('center_axis',(0.,0.,1.));
#119347=DIRECTION('ref_axis',(0.871318704123396,-0.490717552003927,0.));
#119348=DIRECTION('center_axis',(-0.0108384416915561,-0.747971550610398,
0.663642288932205));
#119349=DIRECTION('ref_axis',(-0.348719948110342,-0.619187579593758,-0.703563173472534));
#119350=DIRECTION('center_axis',(-0.0108696139192065,-0.750122776784351,
0.661209249211309));
#119351=DIRECTION('ref_axis',(-0.347588297955049,-0.617178220151049,-0.705884848750768));
#119352=DIRECTION('center_axis',(0.63582733685648,0.398153144485152,-0.661209249211308));
#119353=DIRECTION('ref_axis',(0.347588297955068,0.617178220151039,0.705884848750768));
#119354=DIRECTION('center_axis',(0.634003890813404,0.397011308118946,-0.663642288932184));
#119355=DIRECTION('ref_axis',(0.348719948110339,0.619187579593737,0.703563173472554));
#119356=DIRECTION('center_axis',(0.,0.,1.));
#119357=DIRECTION('ref_axis',(0.871318704123396,-0.490717552003927,0.));
#119358=DIRECTION('center_axis',(0.,0.,1.));
#119359=DIRECTION('ref_axis',(0.871318704123396,-0.490717552003927,0.));
#119360=DIRECTION('center_axis',(0.,0.,1.));
#119361=DIRECTION('ref_axis',(-0.871318704123415,0.490717552003893,0.));
#119362=DIRECTION('center_axis',(0.,0.,-1.));
#119363=DIRECTION('ref_axis',(0.871318704123396,-0.490717552003926,0.));
#119364=DIRECTION('center_axis',(0.475335608790583,-0.879804557282858,0.));
#119365=DIRECTION('ref_axis',(0.879804557282858,0.475335608790583,0.));
#119366=DIRECTION('',(0.,0.,1.));
#119367=DIRECTION('center_axis',(-0.475331298520572,0.879806885993467,2.28597565699215E-6));
#119368=DIRECTION('ref_axis',(0.832850018902371,0.449962854451761,-0.322326349571275));
#119369=DIRECTION('',(0.,0.,-1.));
#119370=DIRECTION('center_axis',(-0.996912329797656,0.0785226508557165,
0.));
#119371=DIRECTION('ref_axis',(-0.0785226508557165,-0.996912329797657,0.));
#119372=DIRECTION('center_axis',(0.996912329797651,-0.0785226508557882,
-4.24618866466413E-14));
#119373=DIRECTION('ref_axis',(0.0784172208830047,0.99557380596211,0.0518028604529189));
#119374=DIRECTION('',(0.,0.,1.));
#119375=DIRECTION('',(0.,0.,1.));
#119376=DIRECTION('center_axis',(0.,0.,1.));
#119377=DIRECTION('ref_axis',(0.83808810489185,-0.545534901210534,0.));
#119378=DIRECTION('center_axis',(0.,0.,-1.));
#119379=DIRECTION('ref_axis',(-0.83808810489185,0.545534901210534,0.));
#119380=DIRECTION('center_axis',(-0.66121471821246,0.712152371479069,-0.235868811452374));
#119381=DIRECTION('ref_axis',(0.64340249813794,0.376646626159565,-0.666461209968348));
#119382=DIRECTION('center_axis',(-0.918849822150842,0.316355667117557,0.235868811452406));
#119383=DIRECTION('ref_axis',(-0.0839718152189302,-0.740795646508069,0.666461209946633));
#119384=DIRECTION('center_axis',(0.,0.,-1.));
#119385=DIRECTION('ref_axis',(-0.838088104891848,0.545534901210538,0.));
#119386=DIRECTION('center_axis',(0.845772188033224,-0.533544193061356,-6.76296429840134E-17));
#119387=DIRECTION('ref_axis',(-0.533544193061356,-0.845772188033224,-4.93038065763132E-32));
#119388=DIRECTION('center_axis',(0.,0.,1.));
#119389=DIRECTION('ref_axis',(0.838088104891848,-0.545534901210538,0.));
#119390=DIRECTION('center_axis',(0.830234038864134,-0.557414962762346,-1.38914942345546E-16));
#119391=DIRECTION('ref_axis',(0.557414962762346,0.830234038864134,1.72563323017096E-30));
#119392=DIRECTION('center_axis',(0.,0.,-1.));
#119393=DIRECTION('ref_axis',(-0.838088104891851,0.545534901210533,0.));
#119394=DIRECTION('center_axis',(0.,0.,1.));
#119395=DIRECTION('ref_axis',(0.838088104891851,-0.545534901210533,0.));
#119396=DIRECTION('center_axis',(0.,0.,1.));
#119397=DIRECTION('ref_axis',(0.838088104891851,-0.545534901210533,0.));
#119398=DIRECTION('center_axis',(-0.058738874737605,-0.745740341496545,
0.663642288932205));
#119399=DIRECTION('ref_axis',(-0.387674950010748,-0.595572828516731,-0.703563173472535));
#119400=DIRECTION('center_axis',(-0.0589078124527641,-0.747885150534123,
0.661209249211309));
#119401=DIRECTION('ref_axis',(-0.38641688485055,-0.593640102592892,-0.70588484875077));
#119402=DIRECTION('center_axis',(0.660030720953817,0.356597498805871,-0.661209249211308));
#119403=DIRECTION('ref_axis',(0.386416884850569,0.593640102592884,0.705884848750766));
#119404=DIRECTION('center_axis',(0.658137863669036,0.355574837054044,-0.663642288932184));
#119405=DIRECTION('ref_axis',(0.387674950010745,0.595572828516711,0.703563173472554));
#119406=DIRECTION('center_axis',(0.,0.,1.));
#119407=DIRECTION('ref_axis',(0.838088104891851,-0.545534901210533,0.));
#119408=DIRECTION('center_axis',(0.,0.,1.));
#119409=DIRECTION('ref_axis',(0.838088104891851,-0.545534901210533,0.));
#119410=DIRECTION('center_axis',(0.,0.,1.));
#119411=DIRECTION('ref_axis',(-0.838088104891867,0.545534901210509,0.));
#119412=DIRECTION('center_axis',(0.,0.,-1.));
#119413=DIRECTION('ref_axis',(0.838088104891848,-0.545534901210538,0.));
#119414=DIRECTION('center_axis',(0.417989709277592,-0.908451761481056,0.));
#119415=DIRECTION('ref_axis',(0.908451761481056,0.417989709277592,0.));
#119416=DIRECTION('',(0.,0.,1.));
#119417=DIRECTION('center_axis',(-0.41798525866263,0.908453809247068,2.28597557900283E-6));
#119418=DIRECTION('ref_axis',(0.859968058305883,0.395677473597326,-0.322326349498837));
#119419=DIRECTION('',(0.,0.,-1.));
#119420=DIRECTION('center_axis',(-0.989833102983781,0.142233709919626,0.));
#119421=DIRECTION('ref_axis',(-0.142233709919626,-0.989833102983781,0.));
#119422=DIRECTION('center_axis',(0.989833102983778,-0.142233709919645,-2.73152185709842E-15));
#119423=DIRECTION('ref_axis',(0.142042737047654,0.988504084211958,0.051802860425751));
#119424=DIRECTION('',(0.,0.,1.));
#119425=DIRECTION('',(0.,0.,1.));
#119426=DIRECTION('center_axis',(0.,0.,1.));
#119427=DIRECTION('ref_axis',(0.801413621867962,-0.59811053049121,0.));
#119428=DIRECTION('center_axis',(0.,0.,-1.));
#119429=DIRECTION('ref_axis',(-0.801413621867962,0.59811053049121,0.));
#119430=DIRECTION('center_axis',(-0.614228422558396,0.753053350504116,-0.235868811452362));
#119431=DIRECTION('ref_axis',(0.666212390911554,0.334649825702797,-0.666461209938732));
#119432=DIRECTION('center_axis',(-0.896692969460608,0.374576590704729,0.235868811452338));
#119433=DIRECTION('ref_axis',(-0.131262226158804,-0.733893509739356,0.666461209933695));
#119434=DIRECTION('center_axis',(0.,0.,-1.));
#119435=DIRECTION('ref_axis',(-0.801413621867964,0.598110530491206,0.));
#119436=DIRECTION('center_axis',(0.809850164545254,-0.586636779435134,-6.76296429840134E-17));
#119437=DIRECTION('ref_axis',(-0.586636779435134,-0.809850164545254,-1.04770588974666E-31));
#119438=DIRECTION('center_axis',(0.,0.,1.));
#119439=DIRECTION('ref_axis',(0.801413621867964,-0.598110530491206,0.));
#119440=DIRECTION('center_axis',(0.792814534704242,-0.609462971444285,-1.38914942345546E-16));
#119441=DIRECTION('ref_axis',(0.609462971444284,0.792814534704242,-1.01072803481442E-30));
#119442=DIRECTION('center_axis',(0.,0.,-1.));
#119443=DIRECTION('ref_axis',(-0.801413621867966,0.598110530491204,0.));
#119444=DIRECTION('center_axis',(0.,0.,1.));
#119445=DIRECTION('ref_axis',(0.801413621867966,-0.598110530491204,0.));
#119446=DIRECTION('center_axis',(0.,0.,1.));
#119447=DIRECTION('ref_axis',(0.801413621867966,-0.598110530491204,0.));
#119448=DIRECTION('center_axis',(-0.106397937147908,-0.740444725358682,
0.663642288932205));
#119449=DIRECTION('ref_axis',(-0.425036912385557,-0.569510740937353,-0.703563173472532));
#119450=DIRECTION('center_axis',(-0.106703946149267,-0.742574303779488,
0.661209249211309));
#119451=DIRECTION('ref_axis',(-0.423657601880047,-0.567662590517776,-0.705884848750769));
#119452=DIRECTION('center_axis',(0.681521897242608,0.313576517514073,-0.661209249211308));
#119453=DIRECTION('ref_axis',(0.423657601880068,0.56766259051776,0.705884848750769));
#119454=DIRECTION('center_axis',(0.679567406872722,0.312677232713123,-0.663642288932184));
#119455=DIRECTION('ref_axis',(0.425036912385534,0.569510740937346,0.703563173472551));
#119456=DIRECTION('center_axis',(0.,0.,1.));
#119457=DIRECTION('ref_axis',(0.801413621867966,-0.598110530491204,0.));
#119458=DIRECTION('center_axis',(0.,0.,1.));
#119459=DIRECTION('ref_axis',(0.801413621867966,-0.598110530491204,0.));
#119460=DIRECTION('center_axis',(0.,0.,1.));
#119461=DIRECTION('ref_axis',(-0.801413621867943,0.598110530491235,0.));
#119462=DIRECTION('center_axis',(0.,0.,-1.));
#119463=DIRECTION('ref_axis',(0.801413621867964,-0.598110530491206,0.));
#119464=DIRECTION('center_axis',(0.358926200390668,-0.933365942529037,0.));
#119465=DIRECTION('ref_axis',(0.933365942529037,0.358926200390668,0.));
#119466=DIRECTION('',(0.,0.,1.));
#119467=DIRECTION('center_axis',(-0.358921627719167,0.933367700935809,2.28597557391108E-6));
#119468=DIRECTION('ref_axis',(0.883552304462217,0.339766169115136,-0.322326349534645));
#119469=DIRECTION('',(0.,0.,-1.));
#119470=DIRECTION('center_axis',(-0.97868643963121,0.205360300160442,0.));
#119471=DIRECTION('ref_axis',(-0.205360300160442,-0.97868643963121,0.));
#119472=DIRECTION('center_axis',(0.978686439631201,-0.205360300160485,-1.98414712675372E-14));
#119473=DIRECTION('ref_axis',(0.205084569137981,0.977372387146371,0.0518028603968221));
#119474=DIRECTION('',(0.,0.,1.));
#119475=DIRECTION('',(0.,0.,1.));
#119476=DIRECTION('center_axis',(0.,0.,1.));
#119477=DIRECTION('ref_axis',(0.761445958369139,-0.648228395307783,0.));
#119478=DIRECTION('center_axis',(0.,0.,-1.));
#119479=DIRECTION('ref_axis',(-0.761445958369139,0.648228395307783,0.));
#119480=DIRECTION('center_axis',(-0.564718130564452,0.790859871782495,-0.235868811452398));
#119481=DIRECTION('ref_axis',(0.686284674041221,0.291277877291778,-0.666461209956387));
#119482=DIRECTION('center_axis',(-0.870851413018789,0.431258298734362,0.235868811452302));
#119483=DIRECTION('ref_axis',(-0.178013252440605,-0.723975647099069,0.666461209946237));
#119484=DIRECTION('center_axis',(0.,0.,-1.));
#119485=DIRECTION('ref_axis',(-0.761445958369143,0.648228395307779,0.));
#119486=DIRECTION('center_axis',(0.770600293018851,-0.637318749449018,-6.76296429840134E-17));
#119487=DIRECTION('ref_axis',(-0.637318749449018,-0.770600293018851,-5.73156751449641E-31));
#119488=DIRECTION('center_axis',(0.,0.,1.));
#119489=DIRECTION('ref_axis',(0.761445958369143,-0.648228395307779,0.));
#119490=DIRECTION('center_axis',(0.752137185563065,-0.659006566047161,-1.38914942345546E-16));
#119491=DIRECTION('ref_axis',(0.659006566047161,0.752137185563065,2.2186712959341E-31));
#119492=DIRECTION('center_axis',(0.,0.,-1.));
#119493=DIRECTION('ref_axis',(-0.761445958369147,0.648228395307773,0.));
#119494=DIRECTION('center_axis',(0.,0.,1.));
#119495=DIRECTION('ref_axis',(0.761445958369147,-0.648228395307773,0.));
#119496=DIRECTION('center_axis',(0.,0.,1.));
#119497=DIRECTION('ref_axis',(0.761445958369147,-0.648228395307773,0.));
#119498=DIRECTION('center_axis',(-0.153619787612184,-0.732106463019424,
0.663642288932205));
#119499=DIRECTION('ref_axis',(-0.460652306917222,-0.5411084115638,-0.703563173472534));
#119500=DIRECTION('center_axis',(-0.154061610443117,-0.734212059928935,
0.661209249211309));
#119501=DIRECTION('ref_axis',(-0.459157418949154,-0.539352431094975,-0.705884848750766));
#119502=DIRECTION('center_axis',(0.700212553869642,0.269266983049857,-0.661209249211308));
#119503=DIRECTION('ref_axis',(0.45915741894917,0.539352431094954,0.705884848750772));
#119504=DIRECTION('center_axis',(0.698204461834817,0.268494770553928,-0.663642288932184));
#119505=DIRECTION('ref_axis',(0.460652306917214,0.54110841156378,0.703563173472555));
#119506=DIRECTION('center_axis',(0.,0.,1.));
#119507=DIRECTION('ref_axis',(0.761445958369147,-0.648228395307773,0.));
#119508=DIRECTION('center_axis',(0.,0.,1.));
#119509=DIRECTION('ref_axis',(0.761445958369147,-0.648228395307773,0.));
#119510=DIRECTION('center_axis',(0.,0.,1.));
#119511=DIRECTION('ref_axis',(-0.761445958369123,0.648228395307802,0.));
#119512=DIRECTION('center_axis',(0.,0.,-1.));
#119513=DIRECTION('ref_axis',(0.761445958369143,-0.648228395307779,0.));
#119514=DIRECTION('center_axis',(0.29838778675691,-0.9544447227128,0.));
#119515=DIRECTION('ref_axis',(0.9544447227128,0.29838778675691,0.));
#119516=DIRECTION('',(0.,0.,1.));
#119517=DIRECTION('center_axis',(-0.298383110818907,0.954446184534679,2.2859755847042E-6));
#119518=DIRECTION('ref_axis',(0.903505844681347,0.282458692567024,-0.322326349558911));
#119519=DIRECTION('',(0.,0.,-1.));
#119520=DIRECTION('center_axis',(-0.963518143770611,0.267643020878251,0.));
#119521=DIRECTION('ref_axis',(-0.267643020878251,-0.963518143770611,0.));
#119522=DIRECTION('center_axis',(0.963518143770624,-0.267643020878204,2.53424527853122E-14));
#119523=DIRECTION('ref_axis',(0.267283664743288,0.962224457296271,0.0518028603678789));
#119524=DIRECTION('',(0.,0.,1.));
#119525=DIRECTION('',(0.,0.,1.));
#119526=DIRECTION('center_axis',(0.,0.,1.));
#119527=DIRECTION('ref_axis',(0.718349350097745,-0.695682550603468,0.));
#119528=DIRECTION('center_axis',(0.,0.,-1.));
#119529=DIRECTION('ref_axis',(-0.718349350097745,0.695682550603468,0.));
#119530=DIRECTION('center_axis',(-0.512887290640128,0.825416580209004,-0.235868811452262));
#119531=DIRECTION('ref_axis',(0.703536866256498,0.246709005626625,-0.666461209944516));
#119532=DIRECTION('center_axis',(-0.841431341323772,0.486167873909974,0.235868811452326));
#119533=DIRECTION('ref_axis',(-0.224032784085981,-0.711082813236446,0.666461209954807));
#119534=DIRECTION('center_axis',(0.,0.,-1.));
#119535=DIRECTION('ref_axis',(-0.718349350097736,0.695682550603477,0.));
#119536=DIRECTION('center_axis',(0.72818385959519,-0.685381840016973,-6.76296429840134E-17));
#119537=DIRECTION('ref_axis',(-0.685381840016973,-0.72818385959519,6.93889390390717E-14));
#119538=DIRECTION('center_axis',(0.,0.,1.));
#119539=DIRECTION('ref_axis',(0.718349350097736,-0.695682550603477,0.));
#119540=DIRECTION('center_axis',(0.70836914339349,-0.705842161313684,-1.38914942345546E-16));
#119541=DIRECTION('ref_axis',(0.705842161313684,0.70836914339349,3.32800694390114E-31));
#119542=DIRECTION('center_axis',(0.,0.,-1.));
#119543=DIRECTION('ref_axis',(-0.718349350097744,0.69568255060347,0.));
#119544=DIRECTION('center_axis',(0.,0.,1.));
#119545=DIRECTION('ref_axis',(0.718349350097744,-0.69568255060347,0.));
#119546=DIRECTION('center_axis',(0.,0.,1.));
#119547=DIRECTION('ref_axis',(0.718349350097744,-0.69568255060347,0.));
#119548=DIRECTION('center_axis',(-0.20021038141782,-0.720759818187276,0.663642288932205));
#119549=DIRECTION('ref_axis',(-0.494374782310168,-0.510482551659734,-0.703563173472532));
#119550=DIRECTION('center_axis',(-0.200786202533545,-0.722832781236141,
0.661209249211309));
#119551=DIRECTION('ref_axis',(-0.492770459694828,-0.508825956842077,-0.705884848750767));
#119552=DIRECTION('center_axis',(0.716025886917703,0.223850972794703,-0.661209249211308));
#119553=DIRECTION('ref_axis',(0.492770459694841,0.508825956842061,0.705884848750769));
#119554=DIRECTION('center_axis',(0.713972444898844,0.223209005790579,-0.663642288932184));
#119555=DIRECTION('ref_axis',(0.494374782310151,0.510482551659721,0.703563173472554));
#119556=DIRECTION('center_axis',(0.,0.,1.));
#119557=DIRECTION('ref_axis',(0.718349350097735,-0.695682550603479,0.));
#119558=DIRECTION('center_axis',(0.,0.,1.));
#119559=DIRECTION('ref_axis',(0.718349350097735,-0.695682550603479,0.));
#119560=DIRECTION('center_axis',(0.,0.,1.));
#119561=DIRECTION('ref_axis',(-0.718349350097761,0.695682550603452,0.));
#119562=DIRECTION('center_axis',(0.,0.,-1.));
#119563=DIRECTION('ref_axis',(0.718349350097736,-0.695682550603478,0.));
#119564=DIRECTION('center_axis',(0.236623233703389,-0.971601484803184,0.));
#119565=DIRECTION('ref_axis',(0.971601484803184,0.236623233703389,0.));
#119566=DIRECTION('',(0.,0.,1.));
#119567=DIRECTION('center_axis',(-0.236618473713347,0.971602644033218,2.28597559428171E-6));
#119568=DIRECTION('ref_axis',(0.919746685602177,0.223990532669675,-0.322326349525081));
#119569=DIRECTION('',(0.,0.,-1.));
#119570=DIRECTION('center_axis',(-0.944390545183265,0.328825939014024,0.));
#119571=DIRECTION('ref_axis',(-0.328825939014024,-0.944390545183266,0.));
#119572=DIRECTION('center_axis',(0.944390545183307,-0.328825939013906,4.97743982849312E-14));
#119573=DIRECTION('ref_axis',(0.328384434437419,0.943122540752338,0.0518028603850272));
#119574=DIRECTION('',(0.,0.,1.));
#119575=DIRECTION('',(0.,0.,1.));
#119576=DIRECTION('center_axis',(0.,0.,1.));
#119577=DIRECTION('ref_axis',(0.672300890261307,-0.740277997075324,0.));
#119578=DIRECTION('center_axis',(0.,0.,-1.));
#119579=DIRECTION('ref_axis',(-0.672300890261307,0.740277997075324,0.));
#119580=DIRECTION('center_axis',(-0.458948886825295,0.856581474855607,-0.235868811452501));
#119581=DIRECTION('ref_axis',(0.717898074561625,0.201126353720061,-0.666461209958978));
#119582=DIRECTION('center_axis',(-0.808553647760812,0.539079681008978,0.235868811452348));
#119583=DIRECTION('ref_axis',(-0.269131716978108,-0.695267987579348,0.66646120994682));
#119584=DIRECTION('center_axis',(0.,0.,-1.));
#119585=DIRECTION('ref_axis',(-0.672300890261326,0.740277997075307,0.));
#119586=DIRECTION('center_axis',(0.682775162497505,-0.730628549590355,-6.76296429840134E-17));
#119587=DIRECTION('ref_axis',(-0.730628549590355,-0.682775162497505,-7.33394122822659E-31));
#119588=DIRECTION('center_axis',(0.,0.,1.));
#119589=DIRECTION('ref_axis',(0.672300890261326,-0.740277997075307,0.));
#119590=DIRECTION('center_axis',(0.661690260469006,-0.749777299736701,-1.38914942345546E-16));
#119591=DIRECTION('ref_axis',(0.749777299736701,0.661690260469006,-1.04770588974666E-30));
#119592=DIRECTION('center_axis',(0.,0.,-1.));
#119593=DIRECTION('ref_axis',(-0.672300890261324,0.740277997075309,0.));
#119594=DIRECTION('center_axis',(0.,0.,1.));
#119595=DIRECTION('ref_axis',(0.672300890261324,-0.740277997075309,0.));
#119596=DIRECTION('center_axis',(0.,0.,1.));
#119597=DIRECTION('ref_axis',(0.672300890261324,-0.740277997075309,0.));
#119598=DIRECTION('center_axis',(-0.245978267821218,-0.7064514166597,0.663642288932205));
#119599=DIRECTION('ref_axis',(-0.52606576567953,-0.477759009452743,-0.703563173472534));
#119600=DIRECTION('center_axis',(-0.246685721049257,-0.708483227598103,
0.661209249211309));
#119601=DIRECTION('ref_axis',(-0.524358600922692,-0.476208607589685,-0.705884848750766));
#119602=DIRECTION('center_axis',(0.728896916009348,0.177515110876453,-0.661209249211308));
#119603=DIRECTION('ref_axis',(0.524358600922699,0.476208607589672,0.705884848750769));
#119604=DIRECTION('center_axis',(0.726806562040174,0.177006027344255,-0.663642288932184));
#119605=DIRECTION('ref_axis',(0.526065765679518,0.47775900945273,0.703563173472553));
#119606=DIRECTION('center_axis',(0.,0.,1.));
#119607=DIRECTION('ref_axis',(0.672300890261324,-0.740277997075309,0.));
#119608=DIRECTION('center_axis',(0.,0.,1.));
#119609=DIRECTION('ref_axis',(0.672300890261324,-0.740277997075309,0.));
#119610=DIRECTION('center_axis',(0.,0.,1.));
#119611=DIRECTION('ref_axis',(-0.672300890261287,0.740277997075342,0.));
#119612=DIRECTION('center_axis',(0.,0.,-1.));
#119613=DIRECTION('ref_axis',(0.672300890261326,-0.740277997075307,0.));
#119614=DIRECTION('center_axis',(0.173886345027055,-0.984765727984647,0.));
#119615=DIRECTION('ref_axis',(0.984765727984647,0.173886345027055,0.));
#119616=DIRECTION('',(0.,0.,1.));
#119617=DIRECTION('center_axis',(-0.173881520544928,0.984766579859287,2.28597550967989E-6));
#119618=DIRECTION('ref_axis',(0.932208090064288,0.164601947618861,-0.322326349619095));
#119619=DIRECTION('',(0.,0.,-1.));
#119620=DIRECTION('center_axis',(-0.921382243274625,0.388657640833446,0.));
#119621=DIRECTION('ref_axis',(-0.388657640833446,-0.921382243274625,0.));
#119622=DIRECTION('center_axis',(0.92138224327465,-0.388657640833387,2.24022730085659E-14));
#119623=DIRECTION('ref_axis',(0.388135802052356,0.920145131389595,0.0518028603959105));
#119624=DIRECTION('',(0.,0.,1.));
#119625=DIRECTION('',(0.,0.,1.));
#119626=DIRECTION('center_axis',(0.,0.,1.));
#119627=DIRECTION('ref_axis',(0.623489801858758,-0.781831482468011,0.));
#119628=DIRECTION('center_axis',(0.,0.,-1.));
#119629=DIRECTION('ref_axis',(-0.623489801858758,0.781831482468011,0.));
#119630=DIRECTION('center_axis',(-0.403124563589482,0.884226492486425,-0.235868811452349));
#119631=DIRECTION('ref_axis',(0.729309285704228,0.154717230497998,-0.666461209953451));
#119632=DIRECTION('center_axis',(-0.772353433824917,0.589776294066571,0.235868811452385));
#119633=DIRECTION('ref_axis',(-0.313124729919898,-0.676596156628014,0.666461209935575));
#119634=DIRECTION('center_axis',(0.,0.,-1.));
#119635=DIRECTION('ref_axis',(-0.623489801858743,0.781831482468022,0.));
#119636=DIRECTION('center_axis',(0.634560795802304,-0.772872949734138,-6.76296429840134E-17));
#119637=DIRECTION('ref_axis',(-0.772872949734138,-0.634560795802304,9.86076131526265E-31));
#119638=DIRECTION('center_axis',(0.,0.,1.));
#119639=DIRECTION('ref_axis',(0.623489801858743,-0.781831482468022,0.));
#119640=DIRECTION('center_axis',(0.612292350332139,-0.790631442408374,-1.38914942345546E-16));
#119641=DIRECTION('ref_axis',(0.790631442408374,0.612292350332139,4.43734259186819E-31));
#119642=DIRECTION('center_axis',(0.,0.,-1.));
#119643=DIRECTION('ref_axis',(-0.623489801858737,0.781831482468027,0.));
#119644=DIRECTION('center_axis',(0.,0.,1.));
#119645=DIRECTION('ref_axis',(0.623489801858737,-0.781831482468027,0.));
#119646=DIRECTION('center_axis',(0.,0.,1.));
#119647=DIRECTION('ref_axis',(0.623489801858737,-0.781831482468027,0.));
#119648=DIRECTION('center_axis',(-0.290735376759967,-0.689240054727715,
0.663642288932205));
#119649=DIRECTION('ref_axis',(-0.55559503197698,-0.443072252996912,-0.703563173472531));
#119650=DIRECTION('center_axis',(-0.291571555023257,-0.691222364408688,
0.661209249211309));
#119651=DIRECTION('ref_axis',(-0.553792040184789,-0.441634415022285,-0.705884848750767));
#119652=DIRECTION('center_axis',(0.738772751325213,0.130449801290739,-0.661209249211308));
#119653=DIRECTION('ref_axis',(0.553792040184798,0.441634415022272,0.705884848750768));
#119654=DIRECTION('center_axis',(0.736654075118561,0.130075693163899,-0.663642288932184));
#119655=DIRECTION('ref_axis',(0.555595031976954,0.443072252996912,0.703563173472551));
#119656=DIRECTION('center_axis',(0.,0.,1.));
#119657=DIRECTION('ref_axis',(0.623489801858737,-0.781831482468027,0.));
#119658=DIRECTION('center_axis',(0.,0.,1.));
#119659=DIRECTION('ref_axis',(0.623489801858737,-0.781831482468027,0.));
#119660=DIRECTION('center_axis',(0.,0.,1.));
#119661=DIRECTION('ref_axis',(-0.623489801858669,0.781831482468081,0.));
#119662=DIRECTION('center_axis',(0.,0.,-1.));
#119663=DIRECTION('ref_axis',(0.623489801858743,-0.781831482468022,0.));
#119664=DIRECTION('center_axis',(0.110434920060502,-0.993883357558235,0.));
#119665=DIRECTION('ref_axis',(0.993883357558235,0.110434920060502,0.));
#119666=DIRECTION('',(0.,0.,1.));
#119667=DIRECTION('center_axis',(-0.110430050910949,0.993883898576981,2.2859755452158E-6));
#119668=DIRECTION('ref_axis',(0.940838851613951,0.104536977872,-0.322326349452121));
#119669=DIRECTION('',(0.,0.,-1.));
#119670=DIRECTION('center_axis',(-0.894587784092498,0.44689226503988,0.));
#119671=DIRECTION('ref_axis',(-0.44689226503988,-0.894587784092498,0.));
#119672=DIRECTION('center_axis',(0.894587784092481,-0.446892265039914,-4.03278851957784E-14));
#119673=DIRECTION('ref_axis',(0.446292236401178,0.893386648310297,0.0518028604319265));
#119674=DIRECTION('',(0.,0.,1.));
#119675=DIRECTION('',(0.,0.,1.));
#119676=DIRECTION('center_axis',(0.,0.,1.));
#119677=DIRECTION('ref_axis',(0.572116660122175,-0.820172254596952,0.));
#119678=DIRECTION('center_axis',(0.,0.,-1.));
#119679=DIRECTION('ref_axis',(-0.572116660122175,0.820172254596952,0.));
#119680=DIRECTION('center_axis',(-0.345643715052168,0.908238033793455,-0.235868811452328));
#119681=DIRECTION('ref_axis',(0.737723608568493,0.107672340997408,-0.666461209932595));
#119682=DIRECTION('center_axis',(-0.732979453960528,0.638049389824842,0.235868811452201));
#119683=DIRECTION('ref_axis',(-0.355831046170335,-0.655144046930467,0.666461209938654));
#119684=DIRECTION('center_axis',(0.,0.,-1.));
#119685=DIRECTION('ref_axis',(-0.57211666012218,0.820172254596949,0.));
#119686=DIRECTION('center_axis',(0.583738882684287,-0.811941449146735,-6.76296429840134E-17));
#119687=DIRECTION('ref_axis',(-0.811941449146735,-0.583738882684287,-4.80712114119054E-31));
#119688=DIRECTION('center_axis',(0.,0.,1.));
#119689=DIRECTION('ref_axis',(0.57211666012218,-0.820172254596949,0.));
#119690=DIRECTION('center_axis',(0.56037839959146,-0.828236710893277,-1.38914942345546E-16));
#119691=DIRECTION('ref_axis',(0.828236710893277,0.56037839959146,1.45446229400124E-30));
#119692=DIRECTION('center_axis',(0.,0.,-1.));
#119693=DIRECTION('ref_axis',(-0.572116660122189,0.820172254596943,0.));
#119694=DIRECTION('center_axis',(0.,0.,1.));
#119695=DIRECTION('ref_axis',(0.572116660122189,-0.820172254596943,0.));
#119696=DIRECTION('center_axis',(0.,0.,1.));
#119697=DIRECTION('ref_axis',(0.572116660122189,-0.820172254596943,0.));
#119698=DIRECTION('center_axis',(-0.334297791673065,-0.669196457569327,
0.663642288932205));
#119699=DIRECTION('ref_axis',(-0.582841239113249,-0.406564817614837,-0.703563173472537));
#119700=DIRECTION('center_axis',(-0.335259258935764,-0.671121120257186,
0.661209249211309));
#119701=DIRECTION('ref_axis',(-0.580949829165753,-0.40524545191327,-0.705884848750766));
#119702=DIRECTION('center_axis',(0.745612810939624,0.0828484454901269,-0.661209249211308));
#119703=DIRECTION('ref_axis',(0.580949829165761,0.405245451913251,0.70588484875077));
#119704=DIRECTION('center_axis',(0.743474518590483,0.082610850059185,-0.663642288932184));
#119705=DIRECTION('ref_axis',(0.582841239113242,0.406564817614819,0.703563173472553));
#119706=DIRECTION('center_axis',(0.,0.,1.));
#119707=DIRECTION('ref_axis',(0.572116660122189,-0.820172254596943,0.));
#119708=DIRECTION('center_axis',(0.,0.,1.));
#119709=DIRECTION('ref_axis',(0.572116660122189,-0.820172254596943,0.));
#119710=DIRECTION('center_axis',(0.,0.,1.));
#119711=DIRECTION('ref_axis',(-0.572116660122197,0.820172254596937,0.));
#119712=DIRECTION('center_axis',(0.,0.,-1.));
#119713=DIRECTION('ref_axis',(0.57211666012218,-0.820172254596949,0.));
#119714=DIRECTION('center_axis',(0.0465296943192034,-0.998916907228305,
0.));
#119715=DIRECTION('ref_axis',(0.998916907228305,0.0465296943192034,0.));
#119716=DIRECTION('',(0.,0.,1.));
#119717=DIRECTION('center_axis',(-0.0465248005107585,0.998917135167982,
2.28597549106619E-6));
#119718=DIRECTION('ref_axis',(0.945603504432372,0.0440424432490359,-0.322326349524629));
#119719=DIRECTION('',(0.,0.,-1.));
#119720=DIRECTION('center_axis',(-0.864117271817056,0.503290513071176,0.));
#119721=DIRECTION('ref_axis',(-0.503290513071176,-0.864117271817056,0.));
#119722=DIRECTION('center_axis',(0.864117271817016,-0.503290513071245,-2.23453663032148E-14));
#119723=DIRECTION('ref_axis',(0.502614760223022,0.862957047865909,0.0518028603892732));
#119724=DIRECTION('',(0.,0.,1.));
#119725=DIRECTION('',(0.,0.,1.));
#119726=DIRECTION('center_axis',(0.,0.,1.));
#119727=DIRECTION('ref_axis',(0.518392568310538,-0.855142763005338,0.));
#119728=DIRECTION('center_axis',(0.,0.,-1.));
#119729=DIRECTION('ref_axis',(-0.518392568310538,0.855142763005338,0.));
#119730=DIRECTION('center_axis',(-0.286742542349322,0.92851743020319,-0.235868811452281));
#119731=DIRECTION('ref_axis',(0.743106466860159,0.0601850027344822,-0.66646120994133));
#119732=DIRECTION('center_axis',(-0.690593504295639,0.683700603779688,0.235868811452381));
#119733=DIRECTION('ref_axis',(-0.39707517632656,-0.630999809816269,0.666461209941782));
#119734=DIRECTION('center_axis',(0.,0.,-1.));
#119735=DIRECTION('ref_axis',(-0.518392568310535,0.85514276300534,0.));
#119736=DIRECTION('center_axis',(0.530518261285723,-0.847673506983894,-6.76296429840134E-17));
#119737=DIRECTION('ref_axis',(-0.847673506983894,-0.530518261285723,6.93889390390721E-14));
#119738=DIRECTION('center_axis',(0.,0.,1.));
#119739=DIRECTION('ref_axis',(0.518392568310535,-0.85514276300534,0.));
#119740=DIRECTION('center_axis',(0.50616173380607,-0.862438577076903,-1.38914942345546E-16));
#119741=DIRECTION('ref_axis',(0.862438577076903,0.50616173380607,-2.46519032881566E-31));
#119742=DIRECTION('center_axis',(0.,0.,-1.));
#119743=DIRECTION('ref_axis',(-0.518392568310539,0.855142763005338,0.));
#119744=DIRECTION('center_axis',(0.,0.,1.));
#119745=DIRECTION('ref_axis',(0.518392568310539,-0.855142763005338,0.));
#119746=DIRECTION('center_axis',(0.,0.,1.));
#119747=DIRECTION('ref_axis',(0.518392568310539,-0.855142763005338,0.));
#119748=DIRECTION('center_axis',(-0.376486505253528,-0.646402988624595,
0.663642288932205));
#119749=DIRECTION('ref_axis',(-0.60769242657897,-0.368386720189285,-0.703563173472535));
#119750=DIRECTION('center_axis',(-0.377569310640418,-0.648262095467517,
0.661209249211309));
#119751=DIRECTION('ref_axis',(-0.605720370685326,-0.367191248317468,-0.705884848750766));
#119752=DIRECTION('center_axis',(0.749388987580438,0.0349066476560596,-0.661209249211308));
#119753=DIRECTION('ref_axis',(0.605720370685331,0.367191248317453,0.705884848750769));
#119754=DIRECTION('center_axis',(0.747239865790733,0.0348065412516053,-0.663642288932184));
#119755=DIRECTION('ref_axis',(0.607692426578956,0.368386720189279,0.703563173472551));
#119756=DIRECTION('center_axis',(0.,0.,1.));
#119757=DIRECTION('ref_axis',(0.518392568310539,-0.855142763005338,0.));
#119758=DIRECTION('center_axis',(0.,0.,1.));
#119759=DIRECTION('ref_axis',(0.518392568310539,-0.855142763005338,0.));
#119760=DIRECTION('center_axis',(0.,0.,1.));
#119761=DIRECTION('ref_axis',(-0.518392568310514,0.855142763005353,0.));
#119762=DIRECTION('center_axis',(0.,0.,-1.));
#119763=DIRECTION('ref_axis',(0.518392568310535,-0.85514276300534,0.));
#119764=DIRECTION('center_axis',(-0.0175667319166402,-0.999845693059568,
0.));
#119765=DIRECTION('ref_axis',(0.999845693059568,-0.0175667319166402,0.));
#119766=DIRECTION('',(0.,0.,1.));
#119767=DIRECTION('center_axis',(0.0175716302745468,0.999845606983533,2.2859755779574E-6));
#119768=DIRECTION('ref_axis',(0.946482469611886,-0.016633071217235,-0.322326349619865));
#119769=DIRECTION('',(0.,0.,-1.));
#119770=DIRECTION('center_axis',(-0.830095916319145,0.557620632428785,0.));
#119771=DIRECTION('ref_axis',(-0.557620632428785,-0.830095916319145,0.));
#119772=DIRECTION('center_axis',(0.830095916319116,-0.557620632428829,-3.21712574280547E-14));
#119773=DIRECTION('ref_axis',(0.556871932182353,0.828981371804431,0.0518028604300564));
#119774=DIRECTION('',(0.,0.,1.));
#119775=DIRECTION('',(0.,0.,1.));
#119776=DIRECTION('center_axis',(0.,0.,1.));
#119777=DIRECTION('ref_axis',(0.46253829024085,-0.886599306372992,0.));
#119778=DIRECTION('center_axis',(0.,0.,-1.));
#119779=DIRECTION('ref_axis',(-0.46253829024085,0.886599306372992,0.));
#119780=DIRECTION('center_axis',(-0.226663083034188,0.944981349325736,-0.235868811452359));
#119781=DIRECTION('ref_axis',(0.745435741273968,0.0124503513820484,-0.666461209960335));
#119782=DIRECTION('center_axis',(-0.645369757790036,0.72654234530004,0.235868811452359));
#119783=DIRECTION('ref_axis',(-0.436687639408886,-0.604262659134024,0.666461209946816));
#119784=DIRECTION('center_axis',(0.,0.,-1.));
#119785=DIRECTION('ref_axis',(-0.462538290240846,0.886599306372994,0.));
#119786=DIRECTION('center_axis',(0.475117626555726,-0.879922292555458,-6.76296429840134E-17));
#119787=DIRECTION('ref_axis',(-0.879922292555458,-0.475117626555726,-4.99201041585171E-31));
#119788=DIRECTION('center_axis',(0.,0.,1.));
#119789=DIRECTION('ref_axis',(0.462538290240846,-0.886599306372994,0.));
#119790=DIRECTION('center_axis',(0.449865140885119,-0.893096498154825,-1.38914942345546E-16));
#119791=DIRECTION('ref_axis',(0.893096498154825,0.449865140885119,-6.16297582203916E-32));
#119792=DIRECTION('center_axis',(0.,0.,-1.));
#119793=DIRECTION('ref_axis',(-0.46253829024085,0.886599306372993,0.));
#119794=DIRECTION('center_axis',(0.,0.,1.));
#119795=DIRECTION('ref_axis',(0.46253829024085,-0.886599306372993,0.));
#119796=DIRECTION('center_axis',(0.,0.,1.));
#119797=DIRECTION('ref_axis',(0.46253829024085,-0.886599306372993,0.));
#119798=DIRECTION('center_axis',(-0.417128155027802,-0.6209533111466,0.663642288932205));
#119799=DIRECTION('ref_axis',(-0.63004647551427,-0.328694842711761,-0.70356317347253));
#119800=DIRECTION('center_axis',(-0.418327849059288,-0.62273922267579,0.661209249211309));
#119801=DIRECTION('ref_axis',(-0.628001877275145,-0.327628177120048,-0.705884848750764));
#119802=DIRECTION('center_axis',(0.75008576412785,-0.0131785890806782,-0.661209249211308));
#119803=DIRECTION('ref_axis',(0.628001877275145,0.327628177120031,0.705884848750771));
#119804=DIRECTION('center_axis',(0.747934644099999,-0.0131407950999565,
-0.663642288932184));
#119805=DIRECTION('ref_axis',(0.630046475514241,0.328694842711771,0.703563173472551));
#119806=DIRECTION('center_axis',(0.,0.,1.));
#119807=DIRECTION('ref_axis',(0.46253829024085,-0.886599306372993,0.));
#119808=DIRECTION('center_axis',(0.,0.,1.));
#119809=DIRECTION('ref_axis',(0.46253829024085,-0.886599306372993,0.));
#119810=DIRECTION('center_axis',(0.,0.,1.));
#119811=DIRECTION('ref_axis',(-0.46253829024085,0.886599306372993,0.));
#119812=DIRECTION('center_axis',(0.,0.,-1.));
#119813=DIRECTION('ref_axis',(0.462538290240846,-0.886599306372994,0.));
#119814=DIRECTION('center_axis',(-0.0815909726829869,-0.996665898471822,
0.));
#119815=DIRECTION('ref_axis',(0.996665898471822,-0.0815909726829869,0.));
#119816=DIRECTION('',(0.,0.,1.));
#119817=DIRECTION('center_axis',(0.0815958554617184,0.996665498733775,2.28597554272536E-6));
#119818=DIRECTION('ref_axis',(0.943472135374849,-0.0772402368275582,-0.322326349506282));
#119819=DIRECTION('',(0.,0.,-1.));
#119820=DIRECTION('center_axis',(-0.792663518646063,0.609659368998495,0.));
#119821=DIRECTION('ref_axis',(-0.609659368998495,-0.792663518646063,0.));
#119822=DIRECTION('center_axis',(0.792663518646077,-0.609659368998476,2.23833041067856E-15));
#119823=DIRECTION('ref_axis',(0.608840797926023,0.79159923347382,0.051802860388826));
#119824=DIRECTION('',(0.,0.,1.));
#119825=DIRECTION('',(0.,0.,1.));
#119826=DIRECTION('center_axis',(0.,0.,1.));
#119827=DIRECTION('ref_axis',(0.40478334312238,-0.914412623015818,0.));
#119828=DIRECTION('center_axis',(0.,0.,-1.));
#119829=DIRECTION('ref_axis',(-0.40478334312238,0.914412623015818,0.));
#119830=DIRECTION('center_axis',(-0.165652216491324,0.957562137386193,-0.235868811452249));
#119831=DIRECTION('ref_axis',(0.744701860367215,-0.0353354611165464,-0.666461209938951));
#119832=DIRECTION('center_axis',(-0.597494048518295,0.766398568480695,0.235868811452383));
#119833=DIRECTION('ref_axis',(-0.474505659318943,-0.575042463575424,0.666461209943536));
#119834=DIRECTION('center_axis',(0.,0.,-1.));
#119835=DIRECTION('ref_axis',(-0.404783343122404,0.914412623015808,0.));
#119836=DIRECTION('center_axis',(0.4177646315858,-0.908555288684173,-6.76296429840134E-17));
#119837=DIRECTION('ref_axis',(-0.908555288684173,-0.4177646315858,-6.44030973403092E-31));
#119838=DIRECTION('center_axis',(0.,0.,1.));
#119839=DIRECTION('ref_axis',(0.404783343122404,-0.914412623015808,0.));
#119840=DIRECTION('center_axis',(0.391719955604501,-0.920084494153231,-1.38914942345546E-16));
#119841=DIRECTION('ref_axis',(0.920084494153231,0.391719955604501,3.75941525144388E-31));
#119842=DIRECTION('center_axis',(0.,0.,-1.));
#119843=DIRECTION('ref_axis',(-0.40478334312241,0.914412623015806,0.));
#119844=DIRECTION('center_axis',(0.,0.,1.));
#119845=DIRECTION('ref_axis',(0.40478334312241,-0.914412623015806,0.));
#119846=DIRECTION('center_axis',(0.,0.,1.));
#119847=DIRECTION('ref_axis',(0.40478334312241,-0.914412623015806,0.));
#119848=DIRECTION('center_axis',(-0.456055735739358,-0.592952003319035,
0.663642288932205));
#119849=DIRECTION('ref_axis',(-0.649811528337108,-0.287652287620744,-0.703563173472535));
#119850=DIRECTION('center_axis',(-0.457367388615331,-0.594657380840943,
0.661209249211309));
#119851=DIRECTION('ref_axis',(-0.647702789445248,-0.286718811466832,-0.705884848750766));
#119852=DIRECTION('center_axis',(0.747700277377569,-0.0612096721680857,
-0.661209249211308));
#119853=DIRECTION('ref_axis',(0.647702789445253,0.286718811466814,0.705884848750769));
#119854=DIRECTION('center_axis',(0.745555998525181,-0.0610341331057615,
-0.663642288932184));
#119855=DIRECTION('ref_axis',(0.649811528337093,0.28765228762074,0.70356317347255));
#119856=DIRECTION('center_axis',(0.,0.,1.));
#119857=DIRECTION('ref_axis',(0.40478334312241,-0.914412623015806,0.));
#119858=DIRECTION('center_axis',(0.,0.,1.));
#119859=DIRECTION('ref_axis',(0.40478334312241,-0.914412623015806,0.));
#119860=DIRECTION('center_axis',(0.,0.,1.));
#119861=DIRECTION('ref_axis',(-0.404783343122445,0.91441262301579,0.));
#119862=DIRECTION('center_axis',(0.,0.,-1.));
#119863=DIRECTION('ref_axis',(0.404783343122404,-0.914412623015808,0.));
#119864=DIRECTION('center_axis',(-0.14527993864137,-0.98939058992309,0.));
#119865=DIRECTION('ref_axis',(0.98939058992309,-0.14527993864137,0.));
#119866=DIRECTION('',(0.,0.,1.));
#119867=DIRECTION('center_axis',(0.145284785776622,0.989389878165638,2.28597555524793E-6));
#119868=DIRECTION('ref_axis',(0.936584871728724,-0.137530005737331,-0.322326349482602));
#119869=DIRECTION('',(0.,0.,-1.));
#119870=DIRECTION('center_axis',(-0.751973896549073,0.659192884449464,0.));
#119871=DIRECTION('ref_axis',(-0.659192884449464,-0.751973896549073,0.));
#119872=DIRECTION('center_axis',(0.751973896549014,-0.659192884449531,-3.70652340886886E-14));
#119873=DIRECTION('ref_axis',(0.658307806233437,0.750964244092793,0.051802860406156));
#119874=DIRECTION('',(0.,0.,1.));
#119875=DIRECTION('',(0.,0.,1.));
#119876=DIRECTION('center_axis',(0.,0.,1.));
#119877=DIRECTION('ref_axis',(0.345365054421307,-0.938468422049761,0.));
#119878=DIRECTION('center_axis',(0.,0.,-1.));
#119879=DIRECTION('ref_axis',(-0.345365054421307,0.938468422049761,0.));
#119880=DIRECTION('center_axis',(-0.103960649459011,0.966208097227576,-0.235868811452315));
#119881=DIRECTION('ref_axis',(0.740907839753009,-0.0829760726379563,-0.666461209945567));
#119882=DIRECTION('center_axis',(-0.547163108039041,0.803105495551539,0.235868811452412));
#119883=DIRECTION('ref_axis',(-0.510373833681244,-0.543459295182668,0.666461209953789));
#119884=DIRECTION('center_axis',(0.,0.,-1.));
#119885=DIRECTION('ref_axis',(-0.345365054421319,0.938468422049756,0.));
#119886=DIRECTION('center_axis',(0.358694952134456,-0.933454836247186,-6.76296429840134E-17));
#119887=DIRECTION('ref_axis',(-0.933454836247186,-0.358694952134456,2.1570415377137E-31));
#119888=DIRECTION('center_axis',(0.,0.,1.));
#119889=DIRECTION('ref_axis',(0.345365054421319,-0.938468422049756,0.));
#119890=DIRECTION('center_axis',(0.331965109002638,-0.943291665607657,-1.38914942345546E-16));
#119891=DIRECTION('ref_axis',(0.943291665607656,0.331965109002638,-2.03378202127292E-31));
#119892=DIRECTION('center_axis',(0.,0.,-1.));
#119893=DIRECTION('ref_axis',(-0.345365054421309,0.93846842204976,0.));
#119894=DIRECTION('center_axis',(0.,0.,1.));
#119895=DIRECTION('ref_axis',(0.345365054421309,-0.93846842204976,0.));
#119896=DIRECTION('center_axis',(0.,0.,1.));
#119897=DIRECTION('ref_axis',(0.345365054421309,-0.93846842204976,0.));
#119898=DIRECTION('center_axis',(-0.493109285609112,-0.562514128522027,
0.663642288932205));
#119899=DIRECTION('ref_axis',(-0.666906366205899,-0.245427707578639,-0.70356317347253));
#119900=DIRECTION('center_axis',(-0.494527507466555,-0.564131964274613,
0.661209249211309));
#119901=DIRECTION('ref_axis',(-0.664742151921718,-0.244631256716294,-0.705884848750765));
#119902=DIRECTION('center_axis',(0.742242329806337,-0.10898923158312,-0.661209249211308));
#119903=DIRECTION('ref_axis',(0.664742151921719,0.244631256716282,0.705884848750769));
#119904=DIRECTION('center_axis',(0.740113703431163,-0.108676668766854,-0.663642288932184));
#119905=DIRECTION('ref_axis',(0.666906366205873,0.245427707578649,0.703563173472551));
#119906=DIRECTION('center_axis',(0.,0.,1.));
#119907=DIRECTION('ref_axis',(0.345365054421309,-0.93846842204976,0.));
#119908=DIRECTION('center_axis',(0.,0.,1.));
#119909=DIRECTION('ref_axis',(0.345365054421309,-0.93846842204976,0.));
#119910=DIRECTION('center_axis',(0.,0.,1.));
#119911=DIRECTION('ref_axis',(-0.345365054421342,0.938468422049748,0.));
#119912=DIRECTION('center_axis',(0.,0.,-1.));
#119913=DIRECTION('ref_axis',(0.345365054421319,-0.938468422049756,0.));
#119914=DIRECTION('center_axis',(-0.208371918169427,-0.978049663216748,
0.));
#119915=DIRECTION('ref_axis',(0.978049663216748,-0.208371918169427,0.));
#119916=DIRECTION('',(0.,0.,1.));
#119917=DIRECTION('center_axis',(0.208376709743215,0.978048642364666,2.28597553727221E-6));
#119918=DIRECTION('ref_axis',(0.925848979935386,-0.19725463435178,-0.322326349495898));
#119919=DIRECTION('',(0.,0.,-1.));
#119920=DIRECTION('center_axis',(-0.708194252413267,0.706017634941801,0.));
#119921=DIRECTION('ref_axis',(-0.706017634941801,-0.708194252413267,0.));
#119922=DIRECTION('center_axis',(0.708194252413259,-0.706017634941809,-1.13434032676751E-14));
#119923=DIRECTION('ref_axis',(0.705069686558746,0.707243381552184,0.051802860409279));
#119924=DIRECTION('',(0.,0.,1.));
#119925=DIRECTION('',(0.,0.,1.));
#119926=DIRECTION('center_axis',(0.,0.,1.));
#119927=DIRECTION('ref_axis',(0.28452758663103,-0.958667853036661,0.));
#119928=DIRECTION('center_axis',(0.,0.,-1.));
#119929=DIRECTION('ref_axis',(-0.28452758663103,0.958667853036661,0.));
#119930=DIRECTION('center_axis',(-0.0418418858186911,0.97088370074647,-0.235868811452413));
#119931=DIRECTION('ref_axis',(0.734069269906997,-0.130275717675883,-0.666461209945667));
#119932=DIRECTION('center_axis',(-0.494583756983052,0.836512289875412,0.235868811452306));
#119933=DIRECTION('ref_axis',(-0.544144772509927,-0.509642935982952,0.666461209938581));
#119934=DIRECTION('center_axis',(0.,0.,-1.));
#119935=DIRECTION('ref_axis',(-0.284527586631043,0.958667853036657,0.));
#119936=DIRECTION('center_axis',(0.298151318184964,-0.954518617662625,-6.76296429840134E-17));
#119937=DIRECTION('ref_axis',(-0.954518617662625,-0.298151318184964,-1.87970762572194E-31));
#119938=DIRECTION('center_axis',(0.,0.,1.));
#119939=DIRECTION('ref_axis',(0.284527586631043,-0.958667853036657,0.));
#119940=DIRECTION('center_axis',(0.27084614656159,-0.962622649272672,-1.38914942345546E-16));
#119941=DIRECTION('ref_axis',(0.962622649272672,0.27084614656159,5.8548270309372E-31));
#119942=DIRECTION('center_axis',(0.,0.,-1.));
#119943=DIRECTION('ref_axis',(-0.284527586631029,0.958667853036662,0.));
#119944=DIRECTION('center_axis',(0.,0.,1.));
#119945=DIRECTION('ref_axis',(0.284527586631029,-0.958667853036662,0.));
#119946=DIRECTION('center_axis',(0.,0.,1.));
#119947=DIRECTION('ref_axis',(0.284527586631029,-0.958667853036662,0.));
#119948=DIRECTION('center_axis',(-0.528136543652689,-0.529764762512019,
0.663642288932205));
#119949=DIRECTION('ref_axis',(-0.681260742764966,-0.202194612442037,-0.703563173472533));
#119950=DIRECTION('center_axis',(-0.529655506713783,-0.531288408461151,
0.661209249211309));
#119951=DIRECTION('ref_axis',(-0.679049946309191,-0.201538459658678,-0.705884848750767));
#119952=DIRECTION('center_axis',(0.73373434929145,-0.156320930867464,-0.661209249211308));
#119953=DIRECTION('ref_axis',(0.679049946309194,0.201538459658659,0.705884848750769));
#119954=DIRECTION('center_axis',(0.731630122375854,-0.155872628684911,-0.663642288932184));
#119955=DIRECTION('ref_axis',(0.681260742764946,0.202194612442041,0.703563173472551));
#119956=DIRECTION('center_axis',(0.,0.,1.));
#119957=DIRECTION('ref_axis',(0.284527586631029,-0.958667853036662,0.));
#119958=DIRECTION('center_axis',(0.,0.,1.));
#119959=DIRECTION('ref_axis',(0.284527586631029,-0.958667853036662,0.));
#119960=DIRECTION('center_axis',(0.,0.,1.));
#119961=DIRECTION('ref_axis',(-0.284527586631029,0.958667853036662,0.));
#119962=DIRECTION('center_axis',(0.,0.,-1.));
#119963=DIRECTION('ref_axis',(0.284527586631043,-0.958667853036657,0.));
#119964=DIRECTION('center_axis',(-0.270607652790088,-0.962689720653253,
0.));
#119965=DIRECTION('ref_axis',(0.962689720653253,-0.270607652790088,0.));
#119966=DIRECTION('',(0.,0.,1.));
#119967=DIRECTION('center_axis',(0.270612369112889,0.962688394901426,2.28597555798509E-6));
#119968=DIRECTION('ref_axis',(0.911308576064988,-0.256168701355266,-0.322326349584331));
#119969=DIRECTION('',(0.,0.,-1.));
#119970=DIRECTION('center_axis',(-0.661504486187105,0.749941207531853,0.));
#119971=DIRECTION('ref_axis',(-0.749941207531853,-0.661504486187105,0.));
#119972=DIRECTION('center_axis',(0.661504486187064,-0.749941207531889,-2.68599649281396E-14));
#119973=DIRECTION('ref_axis',(0.748934284305921,0.660616304254221,0.0518028603908362));
#119974=DIRECTION('',(0.,0.,1.));
#119975=DIRECTION('',(0.,0.,1.));
#119976=DIRECTION('center_axis',(0.,0.,1.));
#119977=DIRECTION('ref_axis',(0.222520933956302,-0.974927912181827,0.));
#119978=DIRECTION('center_axis',(0.,0.,-1.));
#119979=DIRECTION('ref_axis',(-0.222520933956302,0.974927912181827,0.));
#119980=DIRECTION('center_axis',(0.0204488151059505,0.97156973488516,-0.235868811452347));
#119981=DIRECTION('ref_axis',(0.724214251961581,-0.17704003184875,-0.66646120995803));
#119982=DIRECTION('center_axis',(-0.439972055181341,0.866481675769055,0.235868811452378));
#119983=DIRECTION('ref_axis',(-0.57567970371943,-0.473732344632131,0.666461209955128));
#119984=DIRECTION('center_axis',(0.,0.,-1.));
#119985=DIRECTION('ref_axis',(-0.222520933956325,0.974927912181821,0.));
#119986=DIRECTION('center_axis',(0.236382516515794,-0.971660077334486,-6.76296429840134E-17));
#119987=DIRECTION('ref_axis',(-0.971660077334487,-0.236382516515794,-1.29422492262822E-31));
#119988=DIRECTION('center_axis',(0.,0.,1.));
#119989=DIRECTION('ref_axis',(0.222520933956325,-0.974927912181821,0.));
#119990=DIRECTION('center_axis',(0.208614219208004,-0.977998009989916,-1.38914942345546E-16));
#119991=DIRECTION('ref_axis',(0.977998009989915,0.208614219208004,6.77927340424307E-31));
#119992=DIRECTION('center_axis',(0.,0.,-1.));
#119993=DIRECTION('ref_axis',(-0.222520933956319,0.974927912181823,0.));
#119994=DIRECTION('center_axis',(0.,0.,1.));
#119995=DIRECTION('ref_axis',(0.222520933956319,-0.974927912181823,0.));
#119996=DIRECTION('center_axis',(0.,0.,1.));
#119997=DIRECTION('ref_axis',(0.222520933956319,-0.974927912181823,0.));
#119998=DIRECTION('center_axis',(-0.560993575353463,-0.494838479458664,
0.663642288932205));
#119999=DIRECTION('ref_axis',(-0.692815672802044,-0.1581306562723,-0.703563173472534));
#120000=DIRECTION('center_axis',(-0.562607037873173,-0.496261674616316,
0.661209249211309));
#120001=DIRECTION('ref_axis',(-0.690567378811524,-0.157617497840459,-0.705884848750767));
#120002=DIRECTION('center_axis',(0.7222112969498,-0.203010273916138,-0.661209249211308));
#120003=DIRECTION('ref_axis',(0.690567378811528,0.157617497840441,0.705884848750768));
#120004=DIRECTION('center_axis',(0.720140116213534,-0.202428074537128,-0.663642288932184));
#120005=DIRECTION('ref_axis',(0.692815672802026,0.158130656272298,0.703563173472552));
#120006=DIRECTION('center_axis',(0.,0.,1.));
#120007=DIRECTION('ref_axis',(0.222520933956319,-0.974927912181823,0.));
#120008=DIRECTION('center_axis',(0.,0.,1.));
#120009=DIRECTION('ref_axis',(0.222520933956319,-0.974927912181823,0.));
#120010=DIRECTION('center_axis',(0.,0.,1.));
#120011=DIRECTION('ref_axis',(-0.222520933956353,0.974927912181815,0.));
#120012=DIRECTION('center_axis',(0.,0.,-1.));
#120013=DIRECTION('ref_axis',(0.222520933956325,-0.974927912181821,0.));
#120014=DIRECTION('center_axis',(-0.331731402520277,-0.943373879531297,
0.));
#120015=DIRECTION('ref_axis',(0.943373879531297,-0.331731402520277,0.));
#120016=DIRECTION('',(0.,0.,1.));
#120017=DIRECTION('center_axis',(0.331736024211709,0.943372254327518,2.28597557033843E-6));
#120018=DIRECTION('ref_axis',(0.893023409828756,-0.314030116229774,-0.322326349525658));
#120019=DIRECTION('',(0.,0.,-1.));
#120020=DIRECTION('center_axis',(-0.612096456134932,0.790783110838274,0.));
#120021=DIRECTION('ref_axis',(-0.790783110838274,-0.612096456134932,0.));
#120022=DIRECTION('center_axis',(0.612096456134955,-0.790783110838255,8.80157042843185E-15));
#120023=DIRECTION('ref_axis',(0.789721350432804,0.61127461286019,0.0518028603767528));
#120024=DIRECTION('',(0.,0.,1.));
#120025=DIRECTION('',(0.,0.,1.));
#120026=DIRECTION('center_axis',(0.,0.,1.));
#120027=DIRECTION('ref_axis',(0.159599895033413,-0.987181783414445,0.));
#120028=DIRECTION('center_axis',(0.,0.,-1.));
#120029=DIRECTION('ref_axis',(-0.159599895033413,0.987181783414445,0.));
#120030=DIRECTION('center_axis',(0.0826554874630245,0.968263380582131,-0.235868811452285));
#120031=DIRECTION('ref_axis',(0.711383282330738,-0.223076850551026,-0.666461209950423));
#120032=DIRECTION('center_axis',(-0.383552413831434,0.892890502597124,0.235868811452331));
#120033=DIRECTION('ref_axis',(-0.60484904357645,-0.435875085469539,0.666461209937664));
#120034=DIRECTION('center_axis',(0.,0.,-1.));
#120035=DIRECTION('ref_axis',(-0.15959989503339,0.987181783414449,0.));
#120036=DIRECTION('center_axis',(0.17364236838237,-0.984808777328148,-6.76296429840134E-17));
#120037=DIRECTION('ref_axis',(-0.984808777328148,-0.17364236838237,9.09038933750775E-32));
#120038=DIRECTION('center_axis',(0.,0.,1.));
#120039=DIRECTION('ref_axis',(0.15959989503339,-0.987181783414448,0.));
#120040=DIRECTION('center_axis',(0.145525051280083,-0.989354567104195,-1.38914942345546E-16));
#120041=DIRECTION('ref_axis',(0.989354567104195,0.145525051280083,4.25245331720702E-31));
#120042=DIRECTION('center_axis',(0.,0.,-1.));
#120043=DIRECTION('ref_axis',(-0.159599895033397,0.987181783414447,0.));
#120044=DIRECTION('center_axis',(0.,0.,1.));
#120045=DIRECTION('ref_axis',(0.159599895033398,-0.987181783414447,0.));
#120046=DIRECTION('center_axis',(0.,0.,1.));
#120047=DIRECTION('ref_axis',(0.159599895033398,-0.987181783414447,0.));
#120048=DIRECTION('center_axis',(-0.591545364120365,-0.457878798950692,
0.663642288932205));
#120049=DIRECTION('ref_axis',(-0.701523674631087,-0.113416907317011,-0.703563173472533));
#120050=DIRECTION('center_axis',(-0.593246696035112,-0.459195695102688,
0.661209249211309));
#120051=DIRECTION('ref_axis',(-0.699247121828083,-0.113048851914766,-0.705884848750768));
#120052=DIRECTION('center_axis',(0.707720523475147,-0.248865404203723,-0.661209249211308));
#120053=DIRECTION('ref_axis',(0.699247121828087,0.113048851914743,0.705884848750769));
#120054=DIRECTION('center_axis',(0.705690899844122,-0.248151700010386,-0.663642288932184));
#120055=DIRECTION('ref_axis',(0.701523674631067,0.113416907317012,0.703563173472553));
#120056=DIRECTION('center_axis',(0.,0.,1.));
#120057=DIRECTION('ref_axis',(0.159599895033398,-0.987181783414447,0.));
#120058=DIRECTION('center_axis',(0.,0.,1.));
#120059=DIRECTION('ref_axis',(0.159599895033398,-0.987181783414447,0.));
#120060=DIRECTION('center_axis',(0.,0.,1.));
#120061=DIRECTION('ref_axis',(-0.159599895033398,0.987181783414447,0.));
#120062=DIRECTION('center_axis',(0.,0.,-1.));
#120063=DIRECTION('ref_axis',(0.15959989503339,-0.987181783414448,0.));
#120064=DIRECTION('center_axis',(-0.391491996761346,-0.920181512785284,
0.));
#120065=DIRECTION('ref_axis',(0.920181512785284,-0.391491996761346,0.));
#120066=DIRECTION('',(0.,0.,1.));
#120067=DIRECTION('center_axis',(0.391496504829889,0.920179594807859,2.28597558341214E-6));
#120068=DIRECTION('ref_axis',(0.871068618823477,-0.370601113989528,-0.322326349544497));
#120069=DIRECTION('',(0.,0.,-1.));
#120070=DIRECTION('center_axis',(-0.560173190450223,0.828375516719813,0.));
#120071=DIRECTION('ref_axis',(-0.828375516719814,-0.560173190450223,0.));
#120072=DIRECTION('center_axis',(0.560173190450257,-0.82837551671979,1.65788201604461E-14));
#120073=DIRECTION('ref_axis',(0.827263282131684,0.559421062960764,0.051802860466998));
#120074=DIRECTION('',(0.,0.,1.));
#120075=DIRECTION('',(0.,0.,1.));
#120076=DIRECTION('center_axis',(0.,0.,1.));
#120077=DIRECTION('ref_axis',(0.096023025907694,-0.995379112949197,0.));
#120078=DIRECTION('center_axis',(0.,0.,-1.));
#120079=DIRECTION('ref_axis',(-0.096023025907694,0.995379112949197,0.));
#120080=DIRECTION('center_axis',(0.144522510692308,0.960978224356439,-0.235868811452334));
#120081=DIRECTION('ref_axis',(-0.695629086194335,0.26819699862612,0.666461209950268));
#120082=DIRECTION('center_axis',(-0.325556673341165,0.915630250825671,0.235868811452369));
#120083=DIRECTION('ref_axis',(-0.631532928946986,-0.396226722080935,0.666461209947465));
#120084=DIRECTION('center_axis',(0.,0.,-1.));
#120085=DIRECTION('ref_axis',(-0.0960230259076927,0.995379112949197,0.));
#120086=DIRECTION('center_axis',(0.110188686511091,-0.993910686814947,-6.76296429840134E-17));
#120087=DIRECTION('ref_axis',(-0.993910686814947,-0.110188686511091,-2.00296714216273E-32));
#120088=DIRECTION('center_axis',(0.,0.,1.));
#120089=DIRECTION('ref_axis',(0.0960230259076927,-0.995379112949197,0.));
#120090=DIRECTION('center_axis',(0.0818378897014263,-0.996645654086355,
-1.38914942345546E-16));
#120091=DIRECTION('ref_axis',(0.996645654086354,0.0818378897014263,5.8548270309372E-32));
#120092=DIRECTION('center_axis',(0.,0.,-1.));
#120093=DIRECTION('ref_axis',(-0.0960230259076935,0.995379112949197,0.));
#120094=DIRECTION('center_axis',(0.,0.,1.));
#120095=DIRECTION('ref_axis',(0.0960230259076935,-0.995379112949197,0.));
#120096=DIRECTION('center_axis',(0.,0.,1.));
#120097=DIRECTION('ref_axis',(0.0960230259076935,-0.995379112949197,0.));
#120098=DIRECTION('center_axis',(-0.619666366100014,-0.419037596243138,
0.663642288932205));
#120099=DIRECTION('ref_axis',(-0.707348965204713,-0.0682371039617093,-0.703563173472532));
#120100=DIRECTION('center_axis',(-0.621448576272025,-0.420242781980715,
0.661209249211309));
#120101=DIRECTION('ref_axis',(-0.705053508433015,-0.0680156640076522,-0.705884848750769));
#120102=DIRECTION('center_axis',(0.690321574563957,-0.293697893163974,-0.661209249211308));
#120103=DIRECTION('ref_axis',(0.705053508433017,0.0680156640076259,0.705884848750769));
#120104=DIRECTION('center_axis',(0.688341848197028,-0.292855616919928,-0.663642288932184));
#120105=DIRECTION('ref_axis',(0.707348965204693,0.0682371039617151,0.703563173472552));
#120106=DIRECTION('center_axis',(0.,0.,1.));
#120107=DIRECTION('ref_axis',(0.0960230259076933,-0.995379112949197,0.));
#120108=DIRECTION('center_axis',(0.,0.,1.));
#120109=DIRECTION('ref_axis',(0.0960230259076933,-0.995379112949197,0.));
#120110=DIRECTION('center_axis',(0.,0.,1.));
#120111=DIRECTION('ref_axis',(-0.0960230259076933,0.995379112949197,0.));
#120112=DIRECTION('center_axis',(0.,0.,-1.));
#120113=DIRECTION('ref_axis',(0.0960230259076927,-0.995379112949197,0.));
#120114=DIRECTION('center_axis',(-0.449643866412953,-0.893207922824921,
0.));
#120115=DIRECTION('ref_axis',(0.893207922824921,-0.449643866412953,0.));
#120116=DIRECTION('',(0.,0.,1.));
#120117=DIRECTION('center_axis',(0.449648242333875,0.893205719955281,2.28597553924879E-6));
#120118=DIRECTION('ref_axis',(0.845534420026475,-0.425649232280533,-0.322326349542641));
#120119=DIRECTION('',(0.,0.,-1.));
#120120=DIRECTION('center_axis',(-0.505948052969182,0.86256394991716,0.));
#120121=DIRECTION('ref_axis',(-0.862563949917161,-0.505948052969182,0.));
#120122=DIRECTION('center_axis',(0.505948052969246,-0.862563949917123,4.09728278564901E-14));
#120123=DIRECTION('ref_axis',(0.861405811564763,0.505268731923542,0.0518028603730392));
#120124=DIRECTION('',(0.,0.,1.));
#120125=DIRECTION('',(0.,0.,1.));
#120126=DIRECTION('center_axis',(0.,0.,1.));
#120127=DIRECTION('ref_axis',(0.0320515775716953,-0.999486216200687,0.));
#120128=DIRECTION('center_axis',(0.,0.,-1.));
#120129=DIRECTION('ref_axis',(-0.0320515775716953,0.999486216200687,0.));
#120130=DIRECTION('center_axis',(0.205795659925261,0.94974420247769,-0.235868811452346));
#120131=DIRECTION('ref_axis',(-0.677016400916227,0.312215067706304,0.666461209964681));
#120132=DIRECTION('center_axis',(-0.266223150648821,0.934607477951421,0.235868811452256));
#120133=DIRECTION('ref_axis',(-0.655621710062707,-0.354950178102783,0.666461209943425));
#120134=DIRECTION('center_axis',(0.,0.,-1.));
#120135=DIRECTION('ref_axis',(-0.0320515775716664,0.999486216200688,0.));
#120136=DIRECTION('center_axis',(0.0462822156915398,-0.998928404096451,
-6.76296429840134E-17));
#120137=DIRECTION('ref_axis',(-0.998928404096451,-0.0462822156915398,6.39408741536562E-32));
#120138=DIRECTION('center_axis',(0.,0.,1.));
#120139=DIRECTION('ref_axis',(0.0320515775716664,-0.999486216200687,0.));
#120140=DIRECTION('center_axis',(0.0178144386798146,-0.999841310296051,
-1.38914942345546E-16));
#120141=DIRECTION('ref_axis',(0.999841310296051,0.0178144386798146,1.54074395550979E-33));
#120142=DIRECTION('center_axis',(0.,0.,-1.));
#120143=DIRECTION('ref_axis',(-0.0320515775716762,0.999486216200687,0.));
#120144=DIRECTION('center_axis',(0.,0.,1.));
#120145=DIRECTION('ref_axis',(0.0320515775716762,-0.999486216200687,0.));
#120146=DIRECTION('center_axis',(0.,0.,1.));
#120147=DIRECTION('ref_axis',(0.0320515775716762,-0.999486216200687,0.));
#120148=DIRECTION('center_axis',(-0.645241026063339,-0.378474478169339,
0.663642288932205));
#120149=DIRECTION('ref_axis',(-0.710267607154434,-0.0227768997094196,-0.703563173472533));
#120150=DIRECTION('center_axis',(-0.647096791008734,-0.379563001125789,
0.661209249211309));
#120151=DIRECTION('ref_axis',(-0.707962678938293,-0.0227029851478096,-0.705884848750767));
#120152=DIRECTION('center_axis',(0.670085946229371,-0.337323514483213,-0.661209249211308));
#120153=DIRECTION('ref_axis',(0.707962678938293,0.022702985147791,0.705884848750768));
#120154=DIRECTION('center_axis',(0.668164252246828,-0.336356127282214,-0.663642288932184));
#120155=DIRECTION('ref_axis',(0.710267607154415,0.0227768997094241,0.703563173472553));
#120156=DIRECTION('center_axis',(0.,0.,1.));
#120157=DIRECTION('ref_axis',(0.0320515775716762,-0.999486216200687,0.));
#120158=DIRECTION('center_axis',(0.,0.,1.));
#120159=DIRECTION('ref_axis',(0.0320515775716762,-0.999486216200687,0.));
#120160=DIRECTION('center_axis',(0.,0.,1.));
#120161=DIRECTION('ref_axis',(-0.0320515775716415,0.999486216200688,0.));
#120162=DIRECTION('center_axis',(0.,0.,-1.));
#120163=DIRECTION('ref_axis',(0.0320515775716664,-0.999486216200688,0.));
#120164=DIRECTION('center_axis',(-0.505948052969163,-0.862563949917171,
0.));
#120165=DIRECTION('ref_axis',(0.862563949917172,-0.505948052969163,0.));
#120166=DIRECTION('',(0.,0.,1.));
#120167=DIRECTION('center_axis',(0.505952278760864,0.862561471207394,2.28597549516116E-6));
#120168=DIRECTION('ref_axis',(0.816525738978556,-0.478948266602592,-0.322326349378848));
#120169=DIRECTION('',(0.,0.,-1.));
#120170=DIRECTION('center_axis',(-0.449643866412973,0.893207922824911,0.));
#120171=DIRECTION('ref_axis',(-0.893207922824911,-0.449643866412973,0.));
#120172=DIRECTION('center_axis',(0.449643866412962,-0.893207922824917,-1.47198677854773E-14));
#120173=DIRECTION('ref_axis',(0.892008639741106,0.449040143283163,0.0518028604177202));
#120174=DIRECTION('',(0.,0.,1.));
#120175=DIRECTION('',(0.,0.,1.));
#120176=DIRECTION('center_axis',(0.,0.,1.));
#120177=DIRECTION('ref_axis',(-0.0320515775716322,-0.999486216200689,0.));
#120178=DIRECTION('center_axis',(0.,0.,-1.));
#120179=DIRECTION('ref_axis',(0.0320515775716322,0.999486216200689,0.));
#120180=DIRECTION('center_axis',(0.266223150648561,0.934607477951468,-0.235868811452362));
#120181=DIRECTION('ref_axis',(-0.655621710047066,0.354950178102169,0.666461209959138));
#120182=DIRECTION('center_axis',(-0.205795659925299,0.949744202477684,0.235868811452338));
#120183=DIRECTION('ref_axis',(-0.677016400940734,-0.312215067705544,0.666461209940142));
#120184=DIRECTION('center_axis',(0.,0.,-1.));
#120185=DIRECTION('ref_axis',(0.0320515775716446,0.999486216200688,0.));
#120186=DIRECTION('center_axis',(-0.0178144386797932,-0.999841310296051,
-6.76296429840134E-17));
#120187=DIRECTION('ref_axis',(-0.999841310296051,0.0178144386797932,-1.30963236218332E-32));
#120188=DIRECTION('center_axis',(0.,0.,1.));
#120189=DIRECTION('ref_axis',(-0.0320515775716446,-0.999486216200688,0.));
#120190=DIRECTION('center_axis',(-0.0462822156915185,-0.998928404096452,
-1.38914942345546E-16));
#120191=DIRECTION('ref_axis',(0.998928404096452,-0.0462822156915185,8.78224054640579E-32));
#120192=DIRECTION('center_axis',(0.,0.,-1.));
#120193=DIRECTION('ref_axis',(0.0320515775716415,0.999486216200688,0.));
#120194=DIRECTION('center_axis',(0.,0.,1.));
#120195=DIRECTION('ref_axis',(-0.0320515775716415,-0.999486216200688,0.));
#120196=DIRECTION('center_axis',(0.,0.,1.));
#120197=DIRECTION('ref_axis',(-0.0320515775716415,-0.999486216200688,0.));
#120198=DIRECTION('center_axis',(-0.668164252246804,-0.33635612728222,0.663642288932205));
#120199=DIRECTION('ref_axis',(-0.710267607154435,0.022776899709407,-0.703563173472533));
#120200=DIRECTION('center_axis',(-0.670085946229363,-0.337323514483229,
0.661209249211309));
#120201=DIRECTION('ref_axis',(-0.707962678938294,0.0227029851477752,-0.705884848750767));
#120202=DIRECTION('center_axis',(0.647096791008744,-0.379563001125774,-0.661209249211308));
#120203=DIRECTION('ref_axis',(0.707962678938293,-0.022702985147794,0.705884848750768));
#120204=DIRECTION('center_axis',(0.645241026063363,-0.378474478169334,-0.663642288932184));
#120205=DIRECTION('ref_axis',(0.710267607154415,-0.0227768997094036,0.703563173472553));
#120206=DIRECTION('center_axis',(0.,0.,1.));
#120207=DIRECTION('ref_axis',(-0.0320515775716415,-0.999486216200688,0.));
#120208=DIRECTION('center_axis',(0.,0.,1.));
#120209=DIRECTION('ref_axis',(-0.0320515775716415,-0.999486216200688,0.));
#120210=DIRECTION('center_axis',(0.,0.,1.));
#120211=DIRECTION('ref_axis',(0.0320515775716068,0.999486216200689,0.));
#120212=DIRECTION('center_axis',(0.,0.,-1.));
#120213=DIRECTION('ref_axis',(-0.0320515775716446,-0.999486216200688,0.));
#120214=DIRECTION('center_axis',(-0.560173190450205,-0.828375516719826,
0.));
#120215=DIRECTION('ref_axis',(0.828375516719826,-0.560173190450205,0.));
#120216=DIRECTION('',(0.,0.,1.));
#120217=DIRECTION('center_axis',(0.560177248748154,0.828372772355371,2.28597553347141E-6));
#120218=DIRECTION('ref_axis',(0.784161778440321,-0.530279199714647,-0.322326349502033));
#120219=DIRECTION('',(0.,0.,-1.));
#120220=DIRECTION('center_axis',(-0.391491996761366,0.920181512785276,0.));
#120221=DIRECTION('ref_axis',(-0.920181512785276,-0.391491996761366,0.));
#120222=DIRECTION('center_axis',(0.391491996761285,-0.92018151278531,-3.69893584815328E-14));
#120223=DIRECTION('ref_axis',(0.918946013078971,0.390966352374483,0.0518028605122913));
#120224=DIRECTION('',(0.,0.,1.));
#120225=DIRECTION('',(0.,0.,1.));
#120226=DIRECTION('center_axis',(0.,0.,1.));
#120227=DIRECTION('ref_axis',(-0.0960230259076932,-0.995379112949197,0.));
#120228=DIRECTION('center_axis',(0.,0.,-1.));
#120229=DIRECTION('ref_axis',(0.0960230259076932,0.995379112949197,0.));
#120230=DIRECTION('center_axis',(0.325556673341087,0.915630250825694,-0.235868811452387));
#120231=DIRECTION('ref_axis',(-0.631532928939842,0.3962267220802,0.666461209954672));
#120232=DIRECTION('center_axis',(-0.144522510692294,0.960978224356439,0.235868811452346));
#120233=DIRECTION('ref_axis',(-0.695629086202631,-0.26819699862532,0.666461209941931));
#120234=DIRECTION('center_axis',(0.,0.,-1.));
#120235=DIRECTION('ref_axis',(0.096023025907671,0.995379112949199,0.));
#120236=DIRECTION('center_axis',(-0.081837889701405,-0.996645654086356,
-6.76296429840134E-17));
#120237=DIRECTION('ref_axis',(-0.996645654086356,0.081837889701405,4.77630626208035E-32));
#120238=DIRECTION('center_axis',(0.,0.,1.));
#120239=DIRECTION('ref_axis',(-0.096023025907671,-0.995379112949199,0.));
#120240=DIRECTION('center_axis',(-0.11018868651107,-0.99391068681495,-1.38914942345546E-16));
#120241=DIRECTION('ref_axis',(0.99391068681495,-0.11018868651107,-6.16297582203915E-32));
#120242=DIRECTION('center_axis',(0.,0.,-1.));
#120243=DIRECTION('ref_axis',(0.0960230259076587,0.9953791129492,0.));
#120244=DIRECTION('center_axis',(0.,0.,1.));
#120245=DIRECTION('ref_axis',(-0.0960230259076587,-0.9953791129492,0.));
#120246=DIRECTION('center_axis',(0.,0.,1.));
#120247=DIRECTION('ref_axis',(-0.0960230259076587,-0.9953791129492,0.));
#120248=DIRECTION('center_axis',(-0.688341848197004,-0.292855616919936,
0.663642288932205));
#120249=DIRECTION('ref_axis',(-0.707348965204713,0.0682371039616992,-0.703563173472533));
#120250=DIRECTION('center_axis',(-0.69032157456395,-0.29369789316399,0.661209249211309));
#120251=DIRECTION('ref_axis',(-0.705053508433019,0.0680156640076101,-0.705884848750768));
#120252=DIRECTION('center_axis',(0.621448576272035,-0.4202427819807,-0.661209249211308));
#120253=DIRECTION('ref_axis',(0.705053508433016,-0.068015664007635,0.705884848750769));
#120254=DIRECTION('center_axis',(0.619666366100039,-0.419037596243135,-0.663642288932184));
#120255=DIRECTION('ref_axis',(0.707348965204694,-0.0682371039616922,0.703563173472553));
#120256=DIRECTION('center_axis',(0.,0.,1.));
#120257=DIRECTION('ref_axis',(-0.0960230259076587,-0.9953791129492,0.));
#120258=DIRECTION('center_axis',(0.,0.,1.));
#120259=DIRECTION('ref_axis',(-0.0960230259076587,-0.9953791129492,0.));
#120260=DIRECTION('center_axis',(0.,0.,1.));
#120261=DIRECTION('ref_axis',(0.0960230259076239,0.995379112949204,0.));
#120262=DIRECTION('center_axis',(0.,0.,-1.));
#120263=DIRECTION('ref_axis',(-0.0960230259076709,-0.995379112949199,0.));
#120264=DIRECTION('center_axis',(-0.612096456134915,-0.790783110838286,
0.));
#120265=DIRECTION('ref_axis',(0.790783110838286,-0.612096456134915,0.));
#120266=DIRECTION('',(0.,0.,1.));
#120267=DIRECTION('center_axis',(0.612100330262687,0.79078011209633,2.28597557930745E-6));
#120268=DIRECTION('ref_axis',(0.748575528964249,-0.579431101853004,-0.322326349592007));
#120269=DIRECTION('',(0.,0.,-1.));
#120270=DIRECTION('center_axis',(-0.331731402520297,0.94337387953129,0.));
#120271=DIRECTION('ref_axis',(-0.94337387953129,-0.331731402520297,0.));
#120272=DIRECTION('center_axis',(0.331731402520233,-0.943373879531312,-3.55097841422777E-14));
#120273=DIRECTION('ref_axis',(0.942107240142804,0.331285996865109,0.0518028604576939));
#120274=DIRECTION('',(0.,0.,1.));
#120275=DIRECTION('',(0.,0.,1.));
#120276=DIRECTION('center_axis',(0.,0.,1.));
#120277=DIRECTION('ref_axis',(-0.159599895033352,-0.987181783414455,0.));
#120278=DIRECTION('center_axis',(0.,0.,-1.));
#120279=DIRECTION('ref_axis',(0.159599895033352,0.987181783414455,0.));
#120280=DIRECTION('center_axis',(0.383552413831463,0.89289050259712,-0.235868811452298));
#120281=DIRECTION('ref_axis',(-0.604849043555148,0.435875085466088,0.666461209959254));
#120282=DIRECTION('center_axis',(-0.0826554874630613,0.968263380582129,
0.23586881145228));
#120283=DIRECTION('ref_axis',(0.711383282352891,0.223076850547471,-0.666461209927966));
#120284=DIRECTION('center_axis',(0.,0.,-1.));
#120285=DIRECTION('ref_axis',(0.159599895033369,0.987181783414452,0.));
#120286=DIRECTION('center_axis',(-0.145525051280062,-0.989354567104198,
-6.76296429840134E-17));
#120287=DIRECTION('ref_axis',(-0.989354567104198,0.145525051280062,-1.38666955995881E-32));
#120288=DIRECTION('center_axis',(0.,0.,1.));
#120289=DIRECTION('ref_axis',(-0.159599895033369,-0.987181783414452,0.));
#120290=DIRECTION('center_axis',(-0.17364236838235,-0.984808777328152,-1.38914942345546E-16));
#120291=DIRECTION('ref_axis',(0.984808777328151,-0.173642368382349,6.47112461314111E-32));
#120292=DIRECTION('center_axis',(0.,0.,-1.));
#120293=DIRECTION('ref_axis',(0.159599895033363,0.987181783414453,0.));
#120294=DIRECTION('center_axis',(0.,0.,1.));
#120295=DIRECTION('ref_axis',(-0.159599895033363,-0.987181783414453,0.));
#120296=DIRECTION('center_axis',(0.,0.,1.));
#120297=DIRECTION('ref_axis',(-0.159599895033363,-0.987181783414453,0.));
#120298=DIRECTION('center_axis',(-0.705690899844099,-0.248151700010395,
0.663642288932205));
#120299=DIRECTION('ref_axis',(-0.701523674631089,0.113416907316999,-0.703563173472533));
#120300=DIRECTION('center_axis',(-0.70772052347514,-0.24886540420374,0.661209249211309));
#120301=DIRECTION('ref_axis',(-0.69924712182809,0.113048851914729,-0.705884848750768));
#120302=DIRECTION('center_axis',(0.593246696035123,-0.459195695102674,-0.661209249211308));
#120303=DIRECTION('ref_axis',(0.699247121828084,-0.113048851914753,0.70588484875077));
#120304=DIRECTION('center_axis',(0.591545364120389,-0.457878798950691,-0.663642288932184));
#120305=DIRECTION('ref_axis',(0.701523674631069,-0.113416907316995,0.703563173472554));
#120306=DIRECTION('center_axis',(0.,0.,1.));
#120307=DIRECTION('ref_axis',(-0.159599895033363,-0.987181783414453,0.));
#120308=DIRECTION('center_axis',(0.,0.,1.));
#120309=DIRECTION('ref_axis',(-0.159599895033363,-0.987181783414453,0.));
#120310=DIRECTION('center_axis',(0.,0.,1.));
#120311=DIRECTION('ref_axis',(0.159599895033294,0.987181783414464,0.));
#120312=DIRECTION('center_axis',(0.,0.,-1.));
#120313=DIRECTION('ref_axis',(-0.159599895033369,-0.987181783414452,0.));
#120314=DIRECTION('center_axis',(-0.661504486187089,-0.749941207531868,
0.));
#120315=DIRECTION('ref_axis',(0.749941207531868,-0.661504486187089,0.));
#120316=DIRECTION('',(0.,0.,1.));
#120317=DIRECTION('center_axis',(0.661508160225006,0.749937966734918,2.28597557930792E-6));
#120318=DIRECTION('ref_axis',(0.709913222114901,-0.626201997339955,-0.32232634951845));
#120319=DIRECTION('',(0.,0.,-1.));
#120320=DIRECTION('center_axis',(-0.270607652790109,0.962689720653247,0.));
#120321=DIRECTION('ref_axis',(-0.962689720653248,-0.270607652790109,0.));
#120322=DIRECTION('center_axis',(0.270607652790095,-0.962689720653252,-1.3695547089062E-14));
#120323=DIRECTION('ref_axis',(0.961397146474936,0.270244316133488,0.0518028604171078));
#120324=DIRECTION('',(0.,0.,1.));
#120325=DIRECTION('',(0.,0.,1.));
#120326=DIRECTION('center_axis',(0.,0.,1.));
#120327=DIRECTION('ref_axis',(-0.222520933956302,-0.974927912181827,0.));
#120328=DIRECTION('center_axis',(0.,0.,-1.));
#120329=DIRECTION('ref_axis',(0.222520933956302,0.974927912181827,0.));
#120330=DIRECTION('center_axis',(0.439972055181506,0.866481675768994,-0.235868811452296));
#120331=DIRECTION('ref_axis',(-0.575679703725262,0.473732344633531,0.666461209949095));
#120332=DIRECTION('center_axis',(-0.0204488151061702,0.971569734885175,
0.235868811452267));
#120333=DIRECTION('ref_axis',(0.724214251971472,0.177040031846594,-0.666461209947854));
#120334=DIRECTION('center_axis',(0.,0.,-1.));
#120335=DIRECTION('ref_axis',(0.222520933956304,0.974927912181826,0.));
#120336=DIRECTION('center_axis',(-0.208614219207983,-0.97799800998992,-6.76296429840134E-17));
#120337=DIRECTION('ref_axis',(-0.97799800998992,0.208614219207983,3.85185988877447E-32));
#120338=DIRECTION('center_axis',(0.,0.,1.));
#120339=DIRECTION('ref_axis',(-0.222520933956304,-0.974927912181826,0.));
#120340=DIRECTION('center_axis',(-0.236382516515774,-0.971660077334491,
-1.38914942345546E-16));
#120341=DIRECTION('ref_axis',(0.971660077334492,-0.236382516515774,3.57452597678271E-31));
#120342=DIRECTION('center_axis',(0.,0.,-1.));
#120343=DIRECTION('ref_axis',(0.222520933956319,0.974927912181823,0.));
#120344=DIRECTION('center_axis',(0.,0.,1.));
#120345=DIRECTION('ref_axis',(-0.222520933956319,-0.974927912181823,0.));
#120346=DIRECTION('center_axis',(0.,0.,1.));
#120347=DIRECTION('ref_axis',(-0.222520933956319,-0.974927912181823,0.));
#120348=DIRECTION('center_axis',(-0.720140116213512,-0.202428074537138,
0.663642288932205));
#120349=DIRECTION('ref_axis',(-0.692815672802049,0.158130656272285,-0.703563173472532));
#120350=DIRECTION('center_axis',(-0.722211296949795,-0.203010273916155,
0.661209249211309));
#120351=DIRECTION('ref_axis',(-0.690567378811532,0.157617497840423,-0.705884848750768));
#120352=DIRECTION('center_axis',(0.562607037873186,-0.496261674616303,-0.661209249211308));
#120353=DIRECTION('ref_axis',(0.690567378811527,-0.157617497840443,0.705884848750768));
#120354=DIRECTION('center_axis',(0.560993575353487,-0.494838479458664,-0.663642288932184));
#120355=DIRECTION('ref_axis',(0.692815672802032,-0.158130656272272,0.703563173472552));
#120356=DIRECTION('center_axis',(0.,0.,1.));
#120357=DIRECTION('ref_axis',(-0.222520933956319,-0.974927912181823,0.));
#120358=DIRECTION('center_axis',(0.,0.,1.));
#120359=DIRECTION('ref_axis',(-0.222520933956319,-0.974927912181823,0.));
#120360=DIRECTION('center_axis',(0.,0.,1.));
#120361=DIRECTION('ref_axis',(0.222520933956214,0.974927912181846,0.));
#120362=DIRECTION('center_axis',(0.,0.,-1.));
#120363=DIRECTION('ref_axis',(-0.222520933956304,-0.974927912181826,0.));
#120364=DIRECTION('center_axis',(-0.708194252413252,-0.706017634941816,
0.));
#120365=DIRECTION('ref_axis',(0.706017634941816,-0.708194252413252,0.));
#120366=DIRECTION('',(0.,0.,1.));
#120367=DIRECTION('center_axis',(0.708197711263826,0.706014165407078,2.2859755326348E-6));
#120368=DIRECTION('ref_axis',(0.668333729574852,-0.670399694519265,-0.322326349374426));
#120369=DIRECTION('',(0.,0.,-1.));
#120370=DIRECTION('center_axis',(-0.208371918169447,0.978049663216743,0.));
#120371=DIRECTION('ref_axis',(-0.978049663216743,-0.208371918169447,0.));
#120372=DIRECTION('center_axis',(0.208371918169387,-0.978049663216756,-3.18487860976942E-14));
#120373=DIRECTION('ref_axis',(0.976736465712491,0.208092143539129,0.051802860391711));
#120374=DIRECTION('',(0.,0.,1.));
#120375=DIRECTION('',(0.,0.,1.));
#120376=DIRECTION('center_axis',(0.,0.,1.));
#120377=DIRECTION('ref_axis',(-0.28452758663103,-0.958667853036661,0.));
#120378=DIRECTION('center_axis',(0.,0.,-1.));
#120379=DIRECTION('ref_axis',(0.28452758663103,0.958667853036661,0.));
#120380=DIRECTION('center_axis',(0.494583756983005,0.83651228987544,-0.235868811452307));
#120381=DIRECTION('ref_axis',(-0.544144772498854,0.509642935979625,0.666461209950166));
#120382=DIRECTION('center_axis',(0.0418418858184532,0.9708837007465,0.235868811452332));
#120383=DIRECTION('ref_axis',(0.734069269910964,0.13027571767482,-0.666461209941504));
#120384=DIRECTION('center_axis',(0.,0.,-1.));
#120385=DIRECTION('ref_axis',(0.284527586631023,0.958667853036663,0.));
#120386=DIRECTION('center_axis',(-0.27084614656157,-0.962622649272678,-6.76296429840134E-17));
#120387=DIRECTION('ref_axis',(-0.962622649272678,0.27084614656157,2.46519032881566E-32));
#120388=DIRECTION('center_axis',(0.,0.,1.));
#120389=DIRECTION('ref_axis',(-0.284527586631023,-0.958667853036663,0.));
#120390=DIRECTION('center_axis',(-0.298151318184945,-0.954518617662631,
-1.38914942345546E-16));
#120391=DIRECTION('ref_axis',(0.954518617662631,-0.298151318184945,1.60237371373018E-31));
#120392=DIRECTION('center_axis',(0.,0.,-1.));
#120393=DIRECTION('ref_axis',(0.284527586631027,0.958667853036662,0.));
#120394=DIRECTION('center_axis',(0.,0.,1.));
#120395=DIRECTION('ref_axis',(-0.284527586631027,-0.958667853036662,0.));
#120396=DIRECTION('center_axis',(0.,0.,1.));
#120397=DIRECTION('ref_axis',(-0.284527586631027,-0.958667853036662,0.));
#120398=DIRECTION('center_axis',(-0.731630122375833,-0.155872628684923,
0.663642288932205));
#120399=DIRECTION('ref_axis',(-0.681260742764969,0.202194612442027,-0.703563173472532));
#120400=DIRECTION('center_axis',(-0.733734349291446,-0.156320930867481,
0.661209249211309));
#120401=DIRECTION('ref_axis',(-0.679049946309199,0.20153845965865,-0.705884848750767));
#120402=DIRECTION('center_axis',(0.529655506713796,-0.531288408461139,-0.661209249211308));
#120403=DIRECTION('ref_axis',(0.679049946309191,-0.201538459658669,0.705884848750769));
#120404=DIRECTION('center_axis',(0.528136543652713,-0.529764762512021,-0.663642288932184));
#120405=DIRECTION('ref_axis',(0.681260742764956,-0.202194612442008,0.70356317347255));
#120406=DIRECTION('center_axis',(0.,0.,1.));
#120407=DIRECTION('ref_axis',(-0.284527586631027,-0.958667853036662,0.));
#120408=DIRECTION('center_axis',(0.,0.,1.));
#120409=DIRECTION('ref_axis',(-0.284527586631027,-0.958667853036662,0.));
#120410=DIRECTION('center_axis',(0.,0.,1.));
#120411=DIRECTION('ref_axis',(0.284527586631061,0.958667853036652,0.));
#120412=DIRECTION('center_axis',(0.,0.,-1.));
#120413=DIRECTION('ref_axis',(-0.284527586631023,-0.958667853036663,0.));
#120414=DIRECTION('center_axis',(-0.751973896549059,-0.65919288444948,0.));
#120415=DIRECTION('ref_axis',(0.65919288444948,-0.751973896549059,0.));
#120416=DIRECTION('',(0.,0.,1.));
#120417=DIRECTION('center_axis',(0.751977125999241,0.659189200433909,2.28597558120709E-6));
#120418=DIRECTION('ref_axis',(0.62400791032486,-0.711842575497053,-0.322326349468552));
#120419=DIRECTION('',(0.,0.,-1.));
#120420=DIRECTION('center_axis',(-0.145279938641391,0.989390589923087,0.));
#120421=DIRECTION('ref_axis',(-0.989390589923087,-0.145279938641391,0.));
#120422=DIRECTION('center_axis',(0.145279938641321,-0.989390589923097,-3.55951442003013E-14));
#120423=DIRECTION('ref_axis',(0.988062165298661,0.145084875690556,0.0518028604536278));
#120424=DIRECTION('',(0.,0.,1.));
#120425=DIRECTION('',(0.,0.,1.));
#120426=DIRECTION('center_axis',(0.,0.,1.));
#120427=DIRECTION('ref_axis',(-0.345365054421307,-0.938468422049761,0.));
#120428=DIRECTION('center_axis',(0.,0.,-1.));
#120429=DIRECTION('ref_axis',(0.345365054421307,0.938468422049761,0.));
#120430=DIRECTION('center_axis',(0.547163108039205,0.803105495551452,-0.235868811452329));
#120431=DIRECTION('ref_axis',(-0.510373833698617,0.543459295189141,0.666461209935206));
#120432=DIRECTION('center_axis',(0.10396064945919,0.966208097227539,0.235868811452387));
#120433=DIRECTION('ref_axis',(0.740907839746693,0.0829760726401972,-0.66646120995231));
#120434=DIRECTION('center_axis',(0.,0.,-1.));
#120435=DIRECTION('ref_axis',(0.345365054421298,0.938468422049764,0.));
#120436=DIRECTION('center_axis',(-0.331965109002618,-0.943291665607664,
-6.76296429840134E-17));
#120437=DIRECTION('ref_axis',(-0.943291665607663,0.331965109002618,1.10933564796705E-31));
#120438=DIRECTION('center_axis',(0.,0.,1.));
#120439=DIRECTION('ref_axis',(-0.345365054421298,-0.938468422049764,0.));
#120440=DIRECTION('center_axis',(-0.358694952134436,-0.933454836247193,
-1.38914942345546E-16));
#120441=DIRECTION('ref_axis',(0.933454836247194,-0.358694952134436,1.14631350289928E-30));
#120442=DIRECTION('center_axis',(0.,0.,-1.));
#120443=DIRECTION('ref_axis',(0.345365054421306,0.938468422049761,0.));
#120444=DIRECTION('center_axis',(0.,0.,1.));
#120445=DIRECTION('ref_axis',(-0.345365054421306,-0.938468422049761,0.));
#120446=DIRECTION('center_axis',(0.,0.,1.));
#120447=DIRECTION('ref_axis',(-0.345365054421306,-0.938468422049761,0.));
#120448=DIRECTION('center_axis',(-0.740113703431142,-0.108676668766867,
0.663642288932205));
#120449=DIRECTION('ref_axis',(-0.666906366205898,0.245427707578635,-0.703563173472533));
#120450=DIRECTION('center_axis',(-0.742242329806334,-0.108989231583138,
0.661209249211309));
#120451=DIRECTION('ref_axis',(-0.664742151921725,0.24463125671627,-0.705884848750767));
#120452=DIRECTION('center_axis',(0.494527507466569,-0.564131964274601,-0.661209249211308));
#120453=DIRECTION('ref_axis',(0.664742151921719,-0.244631256716284,0.705884848750767));
#120454=DIRECTION('center_axis',(0.493109285609137,-0.56251412852203,-0.663642288932184));
#120455=DIRECTION('ref_axis',(0.66690636620588,-0.245427707578625,0.703563173472553));
#120456=DIRECTION('center_axis',(0.,0.,1.));
#120457=DIRECTION('ref_axis',(-0.345365054421309,-0.93846842204976,0.));
#120458=DIRECTION('center_axis',(0.,0.,1.));
#120459=DIRECTION('ref_axis',(-0.345365054421309,-0.93846842204976,0.));
#120460=DIRECTION('center_axis',(0.,0.,1.));
#120461=DIRECTION('ref_axis',(0.345365054421242,0.938468422049785,0.));
#120462=DIRECTION('center_axis',(0.,0.,-1.));
#120463=DIRECTION('ref_axis',(-0.345365054421298,-0.938468422049764,0.));
#120464=DIRECTION('center_axis',(-0.79266351864605,-0.609659368998511,0.));
#120465=DIRECTION('ref_axis',(0.609659368998511,-0.79266351864605,0.));
#120466=DIRECTION('',(0.,0.,1.));
#120467=DIRECTION('center_axis',(0.792666505425246,0.609655485640622,2.28597555338679E-6));
#120468=DIRECTION('ref_axis',(0.577117908741423,-0.750360342660638,-0.322326349484704));
#120469=DIRECTION('',(0.,0.,-1.));
#120470=DIRECTION('center_axis',(-0.0815909726830077,0.99666589847182,0.));
#120471=DIRECTION('ref_axis',(-0.99666589847182,-0.0815909726830077,0.));
#120472=DIRECTION('center_axis',(0.0815909726830078,-0.99666589847182,1.83998347318489E-15));
#120473=DIRECTION('ref_axis',(0.995327705518496,0.0814814229684379,0.0518028603295646));
#120474=DIRECTION('',(0.,0.,1.));
#120475=DIRECTION('',(0.,0.,1.));
#120476=DIRECTION('center_axis',(0.,0.,1.));
#120477=DIRECTION('ref_axis',(-0.40478334312238,-0.914412623015818,0.));
#120478=DIRECTION('center_axis',(0.,0.,-1.));
#120479=DIRECTION('ref_axis',(0.40478334312238,0.914412623015818,0.));
#120480=DIRECTION('center_axis',(0.597494048518593,0.766398568480514,-0.235868811452214));
#120481=DIRECTION('ref_axis',(-0.474505659311212,0.575042463572137,0.666461209951876));
#120482=DIRECTION('center_axis',(0.165652216491514,0.957562137386137,0.235868811452343));
#120483=DIRECTION('ref_axis',(0.744701860364663,0.0353354611175966,-0.666461209941747));
#120484=DIRECTION('center_axis',(0.,0.,-1.));
#120485=DIRECTION('ref_axis',(0.404783343122385,0.914412623015816,0.));
#120486=DIRECTION('center_axis',(-0.391719955604482,-0.920084494153239,
-6.76296429840134E-17));
#120487=DIRECTION('ref_axis',(-0.920084494153239,0.391719955604482,7.9810536895407E-31));
#120488=DIRECTION('center_axis',(0.,0.,1.));
#120489=DIRECTION('ref_axis',(-0.404783343122385,-0.914412623015816,0.));
#120490=DIRECTION('center_axis',(-0.417764631585781,-0.908555288684182,
-1.38914942345546E-16));
#120491=DIRECTION('ref_axis',(0.908555288684182,-0.417764631585781,-6.71764364602268E-31));
#120492=DIRECTION('center_axis',(0.,0.,-1.));
#120493=DIRECTION('ref_axis',(0.404783343122381,0.914412623015818,0.));
#120494=DIRECTION('center_axis',(0.,0.,1.));
#120495=DIRECTION('ref_axis',(-0.404783343122381,-0.914412623015818,0.));
#120496=DIRECTION('center_axis',(0.,0.,1.));
#120497=DIRECTION('ref_axis',(-0.404783343122381,-0.914412623015818,0.));
#120498=DIRECTION('center_axis',(-0.745555998525161,-0.0610341331057755,
0.663642288932205));
#120499=DIRECTION('ref_axis',(-0.64981152833712,0.287652287620717,-0.703563173472535));
#120500=DIRECTION('center_axis',(-0.747700277377567,-0.0612096721681029,
0.661209249211309));
#120501=DIRECTION('ref_axis',(-0.64770278944526,0.286718811466798,-0.705884848750769));
#120502=DIRECTION('center_axis',(0.457367388615345,-0.594657380840933,-0.661209249211308));
#120503=DIRECTION('ref_axis',(0.647702789445253,-0.286718811466818,0.705884848750767));
#120504=DIRECTION('center_axis',(0.456055735739382,-0.59295200331904,-0.663642288932184));
#120505=DIRECTION('ref_axis',(0.649811528337101,-0.287652287620715,0.703563173472553));
#120506=DIRECTION('center_axis',(0.,0.,1.));
#120507=DIRECTION('ref_axis',(-0.404783343122381,-0.914412623015818,0.));
#120508=DIRECTION('center_axis',(0.,0.,1.));
#120509=DIRECTION('ref_axis',(-0.404783343122381,-0.914412623015818,0.));
#120510=DIRECTION('center_axis',(0.,0.,1.));
#120511=DIRECTION('ref_axis',(0.404783343122381,0.914412623015818,0.));
#120512=DIRECTION('center_axis',(0.,0.,-1.));
#120513=DIRECTION('ref_axis',(-0.404783343122385,-0.914412623015816,0.));
#120514=DIRECTION('center_axis',(-0.830095916319133,-0.557620632428803,
0.));
#120515=DIRECTION('ref_axis',(0.557620632428803,-0.830095916319133,0.));
#120516=DIRECTION('',(0.,0.,1.));
#120517=DIRECTION('center_axis',(0.830098648154146,0.557616565685985,2.28597558462761E-6));
#120518=DIRECTION('ref_axis',(0.527856405870552,-0.78579471821007,-0.322326349550545));
#120519=DIRECTION('',(0.,0.,-1.));
#120520=DIRECTION('center_axis',(-0.017566731916662,0.999845693059568,0.));
#120521=DIRECTION('ref_axis',(-0.999845693059568,-0.017566731916662,0.));
#120522=DIRECTION('center_axis',(0.0175667319166711,-0.999845693059568,
8.91538383914289E-16));
#120523=DIRECTION('ref_axis',(0.998503230687169,0.0175431456005347,0.0518028604396023));
#120524=DIRECTION('',(0.,0.,1.));
#120525=DIRECTION('',(0.,0.,1.));
#120526=DIRECTION('center_axis',(0.,0.,1.));
#120527=DIRECTION('ref_axis',(-0.46253829024085,-0.886599306372992,0.));
#120528=DIRECTION('center_axis',(0.,0.,-1.));
#120529=DIRECTION('ref_axis',(0.46253829024085,0.886599306372992,0.));
#120530=DIRECTION('center_axis',(0.645369757790118,0.726542345299973,-0.235868811452341));
#120531=DIRECTION('ref_axis',(-0.436687639413051,0.604262659136266,0.666461209942054));
#120532=DIRECTION('center_axis',(0.226663083034076,0.944981349325769,0.235868811452334));
#120533=DIRECTION('ref_axis',(0.745435741282765,-0.0124503513865644,-0.666461209950411));
#120534=DIRECTION('center_axis',(0.,0.,-1.));
#120535=DIRECTION('ref_axis',(0.462538290240827,0.886599306373005,0.));
#120536=DIRECTION('center_axis',(-0.4498651408851,-0.893096498154835,-6.76296429840134E-17));
#120537=DIRECTION('ref_axis',(-0.893096498154835,0.4498651408851,-4.19082355898662E-31));
#120538=DIRECTION('center_axis',(0.,0.,1.));
#120539=DIRECTION('ref_axis',(-0.462538290240827,-0.886599306373005,0.));
#120540=DIRECTION('center_axis',(-0.475117626555707,-0.879922292555468,
-1.38914942345546E-16));
#120541=DIRECTION('ref_axis',(0.879922292555468,-0.475117626555707,-1.84889274661175E-31));
#120542=DIRECTION('center_axis',(0.,0.,-1.));
#120543=DIRECTION('ref_axis',(0.462538290240815,0.886599306373011,0.));
#120544=DIRECTION('center_axis',(0.,0.,1.));
#120545=DIRECTION('ref_axis',(-0.462538290240815,-0.886599306373011,0.));
#120546=DIRECTION('center_axis',(0.,0.,1.));
#120547=DIRECTION('ref_axis',(-0.462538290240815,-0.886599306373011,0.));
#120548=DIRECTION('center_axis',(-0.74793464409998,-0.0131407950999725,
0.663642288932205));
#120549=DIRECTION('ref_axis',(-0.630046475514267,0.328694842711764,-0.703563173472532));
#120550=DIRECTION('center_axis',(-0.750085764127849,-0.0131785890806962,
0.661209249211309));
#120551=DIRECTION('ref_axis',(-0.628001877275151,0.327628177120031,-0.705884848750766));
#120552=DIRECTION('center_axis',(0.418327849059303,-0.62273922267578,-0.661209249211308));
#120553=DIRECTION('ref_axis',(0.628001877275142,-0.327628177120044,0.705884848750768));
#120554=DIRECTION('center_axis',(0.417128155027826,-0.620953311146606,-0.663642288932184));
#120555=DIRECTION('ref_axis',(0.63004647551425,-0.328694842711749,0.703563173472554));
#120556=DIRECTION('center_axis',(0.,0.,1.));
#120557=DIRECTION('ref_axis',(-0.462538290240815,-0.886599306373011,0.));
#120558=DIRECTION('center_axis',(0.,0.,1.));
#120559=DIRECTION('ref_axis',(-0.462538290240815,-0.886599306373011,0.));
#120560=DIRECTION('center_axis',(0.,0.,1.));
#120561=DIRECTION('ref_axis',(0.462538290240815,0.886599306373011,0.));
#120562=DIRECTION('center_axis',(0.,0.,-1.));
#120563=DIRECTION('ref_axis',(-0.462538290240827,-0.886599306373005,0.));
#120564=DIRECTION('center_axis',(0.932256674534463,-0.361797585378819,0.));
#120565=DIRECTION('ref_axis',(0.361797585378819,0.932256674534463,0.));
#120566=DIRECTION('',(0.,0.,1.));
#120567=DIRECTION('center_axis',(-0.932254902033239,0.361802152605218,2.28597549637726E-6));
#120568=DIRECTION('ref_axis',(0.34249158175089,0.882499428274317,-0.322326349412015));
#120569=DIRECTION('',(0.,0.,-1.));
#120570=DIRECTION('center_axis',(-0.809995476332305,-0.586436124672757,
0.));
#120571=DIRECTION('ref_axis',(0.586436124672757,-0.809995476332305,0.));
#120572=DIRECTION('center_axis',(0.809995476332245,0.586436124672841,4.63599959635485E-14));
#120573=DIRECTION('ref_axis',(0.585648734744104,-0.808907920068986,-0.0518028603679146));
#120574=DIRECTION('',(0.,0.,1.));
#120575=DIRECTION('',(0.,0.,1.));
#120576=DIRECTION('center_axis',(0.,0.,1.));
#120577=DIRECTION('ref_axis',(0.991790013823243,0.127877161684531,0.));
#120578=DIRECTION('center_axis',(0.,0.,-1.));
#120579=DIRECTION('ref_axis',(-0.991790013823243,-0.127877161684531,0.));
#120580=DIRECTION('center_axis',(-0.965116663775573,0.113647389265203,-0.235868811452279));
#120581=DIRECTION('ref_axis',(0.245763193734801,0.703867820154899,-0.666461209940729));
#120582=DIRECTION('center_axis',(-0.904725209867097,-0.354736801607849,
0.235868811452407));
#120583=DIRECTION('ref_axis',(0.416264773870225,-0.618508766031246,0.666461209956945));
#120584=DIRECTION('center_axis',(0.,0.,-1.));
#120585=DIRECTION('ref_axis',(-0.991790013823246,-0.127877161684506,0.));
#120586=DIRECTION('center_axis',(0.989868310372871,0.14198847882683,-6.76296429840134E-17));
#120587=DIRECTION('ref_axis',(0.14198847882683,-0.989868310372871,-2.31111593326468E-32));
#120588=DIRECTION('center_axis',(0.,0.,1.));
#120589=DIRECTION('ref_axis',(0.991790013823246,0.127877161684506,0.));
#120590=DIRECTION('center_axis',(0.993510560225565,0.113739908212919,-1.38914942345546E-16));
#120591=DIRECTION('ref_axis',(-0.113739908212919,0.993510560225565,-3.57452597678271E-31));
#120592=DIRECTION('center_axis',(0.,0.,-1.));
#120593=DIRECTION('ref_axis',(-0.991790013823245,-0.127877161684511,0.));
#120594=DIRECTION('center_axis',(0.,0.,1.));
#120595=DIRECTION('ref_axis',(0.991790013823245,0.127877161684511,0.));
#120596=DIRECTION('center_axis',(0.,0.,1.));
#120597=DIRECTION('ref_axis',(0.991790013823245,0.127877161684512,0.));
#120598=DIRECTION('center_axis',(0.43868358611648,-0.605917175538711,0.663642288932205));
#120599=DIRECTION('ref_axis',(0.0908736950716699,-0.704798433935035,-0.703563173472534));
#120600=DIRECTION('center_axis',(0.439945275296726,-0.607659841935852,0.661209249211309));
#120601=DIRECTION('ref_axis',(0.0905787958790825,-0.702511254031707,-0.705884848750768));
#120602=DIRECTION('center_axis',(0.271421100448058,0.699380379328004,-0.661209249211308));
#120603=DIRECTION('ref_axis',(-0.0905787958790601,0.702511254031708,0.705884848750769));
#120604=DIRECTION('center_axis',(0.270642710305121,0.697374673830037,-0.663642288932184));
#120605=DIRECTION('ref_axis',(-0.090873695071669,0.704798433935017,0.703563173472552));
#120606=DIRECTION('center_axis',(0.,0.,1.));
#120607=DIRECTION('ref_axis',(0.991790013823245,0.127877161684511,0.));
#120608=DIRECTION('center_axis',(0.,0.,1.));
#120609=DIRECTION('ref_axis',(0.991790013823245,0.127877161684511,0.));
#120610=DIRECTION('center_axis',(0.,0.,1.));
#120611=DIRECTION('ref_axis',(-0.991790013823245,-0.127877161684511,0.));
#120612=DIRECTION('center_axis',(0.,0.,-1.));
#120613=DIRECTION('ref_axis',(0.991790013823246,0.127877161684506,0.));
#120614=DIRECTION('center_axis',(0.953521704096129,-0.301324343221078,0.));
#120615=DIRECTION('ref_axis',(0.301324343221078,0.953521704096129,0.));
#120616=DIRECTION('',(0.,0.,1.));
#120617=DIRECTION('center_axis',(-0.953520227859872,0.301329014628251,2.28597553491565E-6));
#120618=DIRECTION('ref_axis',(0.285245963560465,0.902629749531369,-0.322326349424615));
#120619=DIRECTION('',(0.,0.,-1.));
#120620=DIRECTION('center_axis',(-0.770758162242018,-0.637127817111533,
0.));
#120621=DIRECTION('ref_axis',(0.637127817111533,-0.770758162242018,0.));
#120622=DIRECTION('center_axis',(0.770758162241952,0.637127817111612,3.80136791779655E-14));
#120623=DIRECTION('ref_axis',(0.636272364989511,-0.769723288723939,-0.0518028604099999));
#120624=DIRECTION('',(0.,0.,1.));
#120625=DIRECTION('',(0.,0.,1.));
#120626=DIRECTION('center_axis',(0.,0.,1.));
#120627=DIRECTION('ref_axis',(0.981559156991069,0.191158628701354,0.));
#120628=DIRECTION('center_axis',(0.,0.,-1.));
#120629=DIRECTION('ref_axis',(-0.981559156991069,-0.191158628701354,0.));
#120630=DIRECTION('center_axis',(-0.970415141311867,0.051578651560199,-0.235868811452257));
#120631=DIRECTION('ref_axis',(0.20016128082009,0.718167750117156,-0.666461209938076));
#120632=DIRECTION('center_axis',(-0.880138289977527,-0.411973900022255,
0.235868811452231));
#120633=DIRECTION('ref_axis',(0.455037505952914,-0.590567797830352,0.66646120993045));
#120634=DIRECTION('center_axis',(0.,0.,-1.));
#120635=DIRECTION('ref_axis',(-0.981559156991065,-0.191158628701373,0.));
#120636=DIRECTION('center_axis',(0.978737286693005,0.205117828666391,-6.76296429840134E-17));
#120637=DIRECTION('ref_axis',(0.205117828666391,-0.978737286693005,-2.28030105415449E-31));
#120638=DIRECTION('center_axis',(0.,0.,1.));
#120639=DIRECTION('ref_axis',(0.981559156991065,0.191158628701373,0.));
#120640=DIRECTION('center_axis',(0.984181945286121,0.177160657519742,-1.38914942345546E-16));
#120641=DIRECTION('ref_axis',(-0.177160657519742,0.984181945286121,-2.40356057059527E-31));
#120642=DIRECTION('center_axis',(0.,0.,-1.));
#120643=DIRECTION('ref_axis',(-0.981559156991067,-0.191158628701365,0.));
#120644=DIRECTION('center_axis',(0.,0.,1.));
#120645=DIRECTION('ref_axis',(0.981559156991067,0.191158628701365,0.));
#120646=DIRECTION('center_axis',(0.,0.,1.));
#120647=DIRECTION('ref_axis',(0.981559156991067,0.191158628701365,0.));
#120648=DIRECTION('center_axis',(0.476603510366994,-0.576565699852742,0.663642288932205));
#120649=DIRECTION('ref_axis',(0.135843576023249,-0.69752805232942,-0.703563173472533));
#120650=DIRECTION('center_axis',(0.477974260290922,-0.578223949051545,0.661209249211309));
#120651=DIRECTION('ref_axis',(0.135402742613138,-0.695264465938644,-0.705884848750766));
#120652=DIRECTION('center_axis',(0.226053981933626,0.715333436943479,-0.661209249211308));
#120653=DIRECTION('ref_axis',(-0.135402742613124,0.695264465938645,0.705884848750768));
#120654=DIRECTION('center_axis',(0.225405697069191,0.713281980754879,-0.663642288932184));
#120655=DIRECTION('ref_axis',(-0.13584357602325,0.697528052329401,0.703563173472552));
#120656=DIRECTION('center_axis',(0.,0.,1.));
#120657=DIRECTION('ref_axis',(0.981559156991067,0.191158628701365,0.));
#120658=DIRECTION('center_axis',(0.,0.,1.));
#120659=DIRECTION('ref_axis',(0.981559156991067,0.191158628701365,0.));
#120660=DIRECTION('center_axis',(0.,0.,1.));
#120661=DIRECTION('ref_axis',(-0.981559156991073,-0.191158628701331,0.));
#120662=DIRECTION('center_axis',(0.,0.,-1.));
#120663=DIRECTION('ref_axis',(0.981559156991065,0.191158628701373,0.));
#120664=DIRECTION('center_axis',(0.9708685084459,-0.239612894703173,0.));
#120665=DIRECTION('ref_axis',(0.239612894703173,0.9708685084459,0.));
#120666=DIRECTION('',(0.,0.,1.));
#120667=DIRECTION('center_axis',(-0.97086733454081,0.239617651095234,2.28597555627519E-6));
#120668=DIRECTION('ref_axis',(0.226828208513217,0.919050971501784,-0.322326349534615));
#120669=DIRECTION('',(0.,0.,-1.));
#120670=DIRECTION('center_axis',(-0.72835363753597,-0.68520141468631,0.));
#120671=DIRECTION('ref_axis',(0.68520141468631,-0.72835363753597,0.));
#120672=DIRECTION('center_axis',(0.728353637535986,0.685201414686293,-1.66926335711597E-15));
#120673=DIRECTION('ref_axis',(0.684281415609636,-0.727375699283596,-0.0518028603744199));
#120674=DIRECTION('',(0.,0.,1.));
#120675=DIRECTION('',(0.,0.,1.));
#120676=DIRECTION('center_axis',(0.,0.,1.));
#120677=DIRECTION('ref_axis',(0.967294863039035,0.253654583909488,0.));
#120678=DIRECTION('center_axis',(0.,0.,-1.));
#120679=DIRECTION('ref_axis',(-0.967294863039035,-0.253654583909488,0.));
#120680=DIRECTION('center_axis',(-0.971725974879091,-0.0107020338879219,
-0.235868811452346));
#120681=DIRECTION('ref_axis',(0.153736862267503,0.729516574747913,-0.666461209935144));
#120682=DIRECTION('center_axis',(-0.851934693065551,-0.467518109312767,
0.235868811452302));
#120683=DIRECTION('ref_axis',(0.49194039131489,-0.560200059846077,0.666461209930034));
#120684=DIRECTION('center_axis',(0.,0.,-1.));
#120685=DIRECTION('ref_axis',(-0.967294863039029,-0.253654583909508,0.));
#120686=DIRECTION('center_axis',(0.963584421563627,0.267404305350324,-6.76296429840134E-17));
#120687=DIRECTION('ref_axis',(0.267404305350324,-0.963584421563627,-1.84889274661175E-32));
#120688=DIRECTION('center_axis',(0.,0.,1.));
#120689=DIRECTION('ref_axis',(0.967294863039029,0.253654583909508,0.));
#120690=DIRECTION('center_axis',(0.97080911562713,0.239853415683975,-1.38914942345546E-16));
#120691=DIRECTION('ref_axis',(-0.239853415683975,0.97080911562713,1.60237371373018E-31));
#120692=DIRECTION('center_axis',(0.,0.,-1.));
#120693=DIRECTION('ref_axis',(-0.967294863039032,-0.253654583909497,0.));
#120694=DIRECTION('center_axis',(0.,0.,1.));
#120695=DIRECTION('ref_axis',(0.967294863039032,0.253654583909497,0.));
#120696=DIRECTION('center_axis',(0.,0.,1.));
#120697=DIRECTION('ref_axis',(0.967294863039032,0.253654583909497,0.));
#120698=DIRECTION('center_axis',(0.512564968562278,-0.544844992033124,0.663642288932205));
#120699=DIRECTION('ref_axis',(0.180255246582588,-0.687391378337488,-0.703563173472531));
#120700=DIRECTION('center_axis',(0.514039146524425,-0.546412009931936,0.661209249211309));
#120701=DIRECTION('ref_axis',(0.179670290434003,-0.685160687021277,-0.705884848750767));
#120702=DIRECTION('center_axis',(0.179757959119001,0.728347036028012,-0.661209249211308));
#120703=DIRECTION('ref_axis',(-0.179670290433984,0.68516068702128,0.705884848750769));
#120704=DIRECTION('center_axis',(0.179242443474634,0.726258259022295,-0.663642288932184));
#120705=DIRECTION('ref_axis',(-0.180255246582597,0.687391378337464,0.703563173472552));
#120706=DIRECTION('center_axis',(0.,0.,1.));
#120707=DIRECTION('ref_axis',(0.967294863039032,0.253654583909497,0.));
#120708=DIRECTION('center_axis',(0.,0.,1.));
#120709=DIRECTION('ref_axis',(0.967294863039032,0.253654583909497,0.));
#120710=DIRECTION('center_axis',(0.,0.,1.));
#120711=DIRECTION('ref_axis',(-0.967294863039023,-0.25365458390953,0.));
#120712=DIRECTION('center_axis',(0.,0.,-1.));
#120713=DIRECTION('ref_axis',(0.967294863039029,0.253654583909508,0.));
#120714=DIRECTION('center_axis',(0.984225805843825,-0.176916825404127,0.));
#120715=DIRECTION('ref_axis',(0.176916825404127,0.984225805843824,0.));
#120716=DIRECTION('',(0.,0.,1.));
#120717=DIRECTION('center_axis',(-0.984224939093732,0.176921647236042,2.28597555699675E-6));
#120718=DIRECTION('ref_axis',(0.167478367719591,0.93169561596139,-0.322326349441536));
#120719=DIRECTION('',(0.,0.,-1.));
#120720=DIRECTION('center_axis',(-0.682956151501922,-0.730459372672898,
0.));
#120721=DIRECTION('ref_axis',(0.730459372672898,-0.682956151501922,0.));
#120722=DIRECTION('center_axis',(0.682956151501907,0.730459372672912,-3.56615353565696E-15));
#120723=DIRECTION('ref_axis',(0.729478607113612,-0.682039167071338,-0.0518028603864715));
#120724=DIRECTION('',(0.,0.,1.));
#120725=DIRECTION('',(0.,0.,1.));
#120726=DIRECTION('center_axis',(0.,0.,1.));
#120727=DIRECTION('ref_axis',(0.949055747010676,0.315108218023599,0.));
#120728=DIRECTION('center_axis',(0.,0.,-1.));
#120729=DIRECTION('ref_axis',(-0.949055747010676,-0.315108218023599,0.));
#120730=DIRECTION('center_axis',(-0.969043777980947,-0.0729387423831519,
-0.235868811452418));
#120731=DIRECTION('ref_axis',(0.106680705980105,0.737867659264888,-0.666461209960896));
#120732=DIRECTION('center_axis',(-0.820230313760265,-0.521141186410019,
0.235868811452246));
#120733=DIRECTION('ref_axis',(0.52682178808489,-0.527530339643357,0.666461209940087));
#120734=DIRECTION('center_axis',(0.,0.,-1.));
#120735=DIRECTION('ref_axis',(-0.949055747010669,-0.315108218023621,0.));
#120736=DIRECTION('center_axis',(0.944471981357835,0.32859196038553,-6.76296429840134E-17));
#120737=DIRECTION('ref_axis',(0.32859196038553,-0.944471981357835,1.60237371373018E-31));
#120738=DIRECTION('center_axis',(0.,0.,1.));
#120739=DIRECTION('ref_axis',(0.949055747010668,0.315108218023621,0.));
#120740=DIRECTION('center_axis',(0.953447023074125,0.301560564714766,-1.38914942345546E-16));
#120741=DIRECTION('ref_axis',(-0.301560564714766,0.953447023074125,-9.4909827659403E-31));
#120742=DIRECTION('center_axis',(0.,0.,-1.));
#120743=DIRECTION('ref_axis',(-0.949055747010673,-0.315108218023608,0.));
#120744=DIRECTION('center_axis',(0.,0.,1.));
#120745=DIRECTION('ref_axis',(0.949055747010673,0.315108218023608,0.));
#120746=DIRECTION('center_axis',(0.,0.,1.));
#120747=DIRECTION('ref_axis',(0.949055747010672,0.31510821802361,0.));
#120748=DIRECTION('center_axis',(0.546420187356898,-0.510885399272357,0.663642288932205));
#120749=DIRECTION('ref_axis',(0.223926209669101,-0.674430065726973,-0.703563173472532));
#120750=DIRECTION('center_axis',(0.547991735643807,-0.512354746658509,0.661209249211309));
#120751=DIRECTION('ref_axis',(0.223199534492313,-0.672241435874437,-0.705884848750765));
#120752=DIRECTION('center_axis',(0.132723272292395,0.738367700911556,-0.661209249211308));
#120753=DIRECTION('ref_axis',(-0.223199534492297,0.672241435874437,0.70588484875077));
#120754=DIRECTION('center_axis',(0.132342644232455,0.73625018632148,-0.663642288932184));
#120755=DIRECTION('ref_axis',(-0.223926209669108,0.674430065726951,0.703563173472551));
#120756=DIRECTION('center_axis',(0.,0.,1.));
#120757=DIRECTION('ref_axis',(0.949055747010673,0.315108218023608,0.));
#120758=DIRECTION('center_axis',(0.,0.,1.));
#120759=DIRECTION('ref_axis',(0.949055747010673,0.315108218023608,0.));
#120760=DIRECTION('center_axis',(0.,0.,1.));
#120761=DIRECTION('ref_axis',(-0.949055747010661,-0.315108218023644,0.));
#120762=DIRECTION('center_axis',(0.,0.,-1.));
#120763=DIRECTION('ref_axis',(0.949055747010669,0.315108218023621,0.));
#120764=DIRECTION('center_axis',(0.993538708289764,-0.113493766920956,0.));
#120765=DIRECTION('ref_axis',(0.113493766920956,0.993538708289764,0.));
#120766=DIRECTION('',(0.,0.,1.));
#120767=DIRECTION('center_axis',(-0.993538152256329,0.113498634378806,2.28597556007661E-6));
#120768=DIRECTION('ref_axis',(0.10744032238041,0.940511723247201,-0.322326349468011));
#120769=DIRECTION('',(0.,0.,-1.));
#120770=DIRECTION('center_axis',(-0.634752252147718,-0.772715716414129,
0.));
#120771=DIRECTION('ref_axis',(0.772715716414129,-0.634752252147718,0.));
#120772=DIRECTION('center_axis',(0.634752252147689,0.772715716414153,3.29300134994633E-14));
#120773=DIRECTION('ref_axis',(0.771678214545083,-0.633899989622142,-0.0518028604766313));
#120774=DIRECTION('',(0.,0.,1.));
#120775=DIRECTION('',(0.,0.,1.));
#120776=DIRECTION('center_axis',(0.,0.,1.));
#120777=DIRECTION('ref_axis',(0.926916757346018,0.375267004879383,0.));
#120778=DIRECTION('center_axis',(0.,0.,-1.));
#120779=DIRECTION('ref_axis',(-0.926916757346018,-0.375267004879383,0.));
#120780=DIRECTION('center_axis',(-0.962379572339892,-0.134875729940312,
-0.235868811452373));
#120781=DIRECTION('ref_axis',(0.0591861757772453,0.743186687335741,-0.66646120994683));
#120782=DIRECTION('center_axis',(-0.785155432157059,-0.572622782587562,
0.235868811452338));
#120783=DIRECTION('ref_axis',(0.55953836112639,-0.492692884128054,0.666461209942165));
#120784=DIRECTION('center_axis',(0.,0.,-1.));
#120785=DIRECTION('ref_axis',(-0.926916757346021,-0.375267004879375,0.));
#120786=DIRECTION('center_axis',(0.921478503192038,0.388429360572757,-6.76296429840134E-17));
#120787=DIRECTION('ref_axis',(0.388429360572757,-0.921478503192038,-1.63318859284038E-31));
#120788=DIRECTION('center_axis',(0.,0.,1.));
#120789=DIRECTION('ref_axis',(0.926916757346021,0.375267004879375,0.));
#120790=DIRECTION('center_axis',(0.932167012189564,0.362028536700605,-1.38914942345546E-16));
#120791=DIRECTION('ref_axis',(-0.362028536700605,0.932167012189564,4.62223186652937E-31));
#120792=DIRECTION('center_axis',(0.,0.,-1.));
#120793=DIRECTION('ref_axis',(-0.92691675734602,-0.375267004879378,0.));
#120794=DIRECTION('center_axis',(0.,0.,1.));
#120795=DIRECTION('ref_axis',(0.92691675734602,0.375267004879378,0.));
#120796=DIRECTION('center_axis',(0.,0.,1.));
#120797=DIRECTION('ref_axis',(0.92691675734602,0.375267004879378,0.));
#120798=DIRECTION('center_axis',(0.578030048394907,-0.474826468821406,0.663642288932205));
#120799=DIRECTION('ref_axis',(0.26667701192807,-0.658697375311585,-0.703563173472536));
#120800=DIRECTION('center_axis',(0.579692509177571,-0.476192107831313,0.661209249211309));
#120801=DIRECTION('ref_axis',(0.26581160378726,-0.656559800472242,-0.705884848750769));
#120802=DIRECTION('center_axis',(0.0851431970708876,0.745354254532679,-0.661209249211308));
#120803=DIRECTION('ref_axis',(-0.265811603787243,0.65655980047225,0.705884848750767));
#120804=DIRECTION('center_axis',(0.0848990206777172,0.7432167036799,-0.663642288932184));
#120805=DIRECTION('ref_axis',(-0.266677011928067,0.65869737531157,0.70356317347255));
#120806=DIRECTION('center_axis',(0.,0.,1.));
#120807=DIRECTION('ref_axis',(0.926916757346019,0.375267004879381,0.));
#120808=DIRECTION('center_axis',(0.,0.,1.));
#120809=DIRECTION('ref_axis',(0.926916757346019,0.375267004879381,0.));
#120810=DIRECTION('center_axis',(0.,0.,1.));
#120811=DIRECTION('ref_axis',(-0.926916757346005,-0.375267004879417,0.));
#120812=DIRECTION('center_axis',(0.,0.,-1.));
#120813=DIRECTION('ref_axis',(0.926916757346021,0.375267004879375,0.));
#120814=DIRECTION('center_axis',(0.998768947069955,-0.0496043382051697,
0.));
#120815=DIRECTION('ref_axis',(0.0496043382051697,0.998768947069955,0.));
#120816=DIRECTION('',(0.,0.,1.));
#120817=DIRECTION('center_axis',(-0.998768704038047,0.0496092312874756,
2.28597555336781E-6));
#120818=DIRECTION('ref_axis',(0.0469607817104218,0.945463066095288,-0.322326349575773));
#120819=DIRECTION('',(0.,0.,-1.));
#120820=DIRECTION('center_axis',(-0.583940019635507,-0.811796805529612,
0.));
#120821=DIRECTION('ref_axis',(0.811796805529613,-0.583940019635507,0.));
#120822=DIRECTION('center_axis',(0.583940019635613,0.811796805529536,-6.02452320704585E-14));
#120823=DIRECTION('ref_axis',(0.810706830674114,-0.583155981149456,-0.0518028604224596));
#120824=DIRECTION('',(0.,0.,1.));
#120825=DIRECTION('',(0.,0.,1.));
#120826=DIRECTION('center_axis',(0.,0.,1.));
#120827=DIRECTION('ref_axis',(0.900968867902417,0.433883739117562,0.));
#120828=DIRECTION('center_axis',(0.,0.,-1.));
#120829=DIRECTION('ref_axis',(-0.900968867902417,-0.433883739117562,0.));
#120830=DIRECTION('center_axis',(-0.951760742606324,-0.196258484192461,
-0.235868811452332));
#120831=DIRECTION('ref_axis',(0.0114484368858726,0.74545180188451,-0.66646120994399));
#120832=DIRECTION('center_axis',(-0.746854178467695,-0.621751348924477,
0.235868811452334));
#120833=DIRECTION('ref_axis',(0.589955671023616,-0.455830847874484,0.666461209938811));
#120834=DIRECTION('center_axis',(0.,0.,-1.));
#120835=DIRECTION('ref_axis',(-0.900968867902419,-0.433883739117559,0.));
#120836=DIRECTION('center_axis',(0.894698472200106,0.446670621199554,-6.76296429840134E-17));
#120837=DIRECTION('ref_axis',(0.446670621199554,-0.894698472200106,6.93889390390721E-14));
#120838=DIRECTION('center_axis',(0.,0.,1.));
#120839=DIRECTION('ref_axis',(0.900968867902419,0.433883739117559,0.));
#120840=DIRECTION('center_axis',(0.907056527102719,0.421008855774264,-1.38914942345546E-16));
#120841=DIRECTION('ref_axis',(-0.421008855774264,0.907056527102718,-1.26957301934007E-30));
#120842=DIRECTION('center_axis',(0.,0.,-1.));
#120843=DIRECTION('ref_axis',(-0.900968867902412,-0.433883739117574,0.));
#120844=DIRECTION('center_axis',(0.,0.,1.));
#120845=DIRECTION('ref_axis',(0.900968867902412,0.433883739117574,0.));
#120846=DIRECTION('center_axis',(0.,0.,1.));
#120847=DIRECTION('ref_axis',(0.900968867902412,0.433883739117574,0.));
#120848=DIRECTION('center_axis',(0.607264659977004,-0.43681637456011,0.663642288932205));
#120849=DIRECTION('ref_axis',(0.308331981142967,-0.640257956090912,-0.703563173472532));
#120850=DIRECTION('center_axis',(0.60901120184747,-0.438072693490152,0.661209249211309));
#120851=DIRECTION('ref_axis',(0.307331396185821,-0.63818022001828,-0.705884848750768));
#120852=DIRECTION('center_axis',(0.0372132501894571,0.749277987643942,-0.661209249211308));
#120853=DIRECTION('ref_axis',(-0.307331396185796,0.638180220018289,0.70588484875077));
#120854=DIRECTION('center_axis',(0.0371065288362318,0.747129184183417,-0.663642288932184));
#120855=DIRECTION('ref_axis',(-0.308331981142974,0.64025795609089,0.70356317347255));
#120856=DIRECTION('center_axis',(0.,0.,1.));
#120857=DIRECTION('ref_axis',(0.900968867902412,0.433883739117574,0.));
#120858=DIRECTION('center_axis',(0.,0.,1.));
#120859=DIRECTION('ref_axis',(0.900968867902412,0.433883739117574,0.));
#120860=DIRECTION('center_axis',(0.,0.,1.));
#120861=DIRECTION('ref_axis',(-0.900968867902445,-0.433883739117504,0.));
#120862=DIRECTION('center_axis',(0.,0.,-1.));
#120863=DIRECTION('ref_axis',(0.900968867902419,0.433883739117559,0.));
#120864=DIRECTION('center_axis',(0.999895030011369,0.0144889253763986,0.));
#120865=DIRECTION('ref_axis',(-0.0144889253763986,0.999895030011369,0.));
#120866=DIRECTION('',(0.,0.,1.));
#120867=DIRECTION('center_axis',(-0.999895100979656,-0.0144840267763469,
2.28597557413844E-6));
#120868=DIRECTION('ref_axis',(0.01371173088091,-0.946529298468286,0.322326349492845));
#120869=DIRECTION('',(0.,0.,-1.));
#120870=DIRECTION('center_axis',(-0.530728252327873,-0.847542047441306,
0.));
#120871=DIRECTION('ref_axis',(0.847542047441306,-0.530728252327873,0.));
#120872=DIRECTION('center_axis',(0.530728252327903,0.847542047441288,-2.55700796067318E-14));
#120873=DIRECTION('ref_axis',(0.846404078537503,-0.530015659661461,-0.0518028604297697));
#120874=DIRECTION('',(0.,0.,1.));
#120875=DIRECTION('',(0.,0.,1.));
#120876=DIRECTION('center_axis',(0.,0.,1.));
#120877=DIRECTION('ref_axis',(0.871318704123387,0.490717552003943,0.));
#120878=DIRECTION('center_axis',(0.,0.,-1.));
#120879=DIRECTION('ref_axis',(-0.871318704123387,-0.490717552003943,0.));
#120880=DIRECTION('center_axis',(-0.937230923829303,-0.256834770235895,
-0.235868811452356));
#120881=DIRECTION('ref_axis',(-0.0363363460881284,0.744653695079178,-0.666461209942402));
#120882=DIRECTION('center_axis',(-0.705483940759338,-0.668325005603341,
0.235868811452404));
#120883=DIRECTION('ref_axis',(0.617948726522513,-0.417095704888963,0.66646120993827));
#120884=DIRECTION('center_axis',(0.,0.,-1.));
#120885=DIRECTION('ref_axis',(-0.871318704123389,-0.490717552003939,0.));
#120886=DIRECTION('center_axis',(0.864241933273684,0.503076416433295,-6.76296429840134E-17));
#120887=DIRECTION('ref_axis',(0.503076416433295,-0.864241933273684,-1.54074395550979E-31));
#120888=DIRECTION('center_axis',(0.,0.,1.));
#120889=DIRECTION('ref_axis',(0.871318704123389,0.490717552003939,0.));
#120890=DIRECTION('center_axis',(0.878218752182993,0.478259159153431,-1.38914942345546E-16));
#120891=DIRECTION('ref_axis',(-0.478259159153431,0.878218752182993,-3.57452597678271E-31));
#120892=DIRECTION('center_axis',(0.,0.,-1.));
#120893=DIRECTION('ref_axis',(-0.871318704123391,-0.490717552003934,0.));
#120894=DIRECTION('center_axis',(0.,0.,1.));
#120895=DIRECTION('ref_axis',(0.871318704123391,0.490717552003934,0.));
#120896=DIRECTION('center_axis',(0.,0.,1.));
#120897=DIRECTION('ref_axis',(0.871318704123391,0.490717552003934,0.));
#120898=DIRECTION('center_axis',(0.634003890813394,-0.397011308118927,0.663642288932205));
#120899=DIRECTION('ref_axis',(0.34871994811035,-0.619187579593757,-0.703563173472531));
#120900=DIRECTION('center_axis',(0.635827336856486,-0.398153144485142,0.661209249211309));
#120901=DIRECTION('ref_axis',(0.347588297955079,-0.617178220151033,-0.705884848750768));
#120902=DIRECTION('center_axis',(-0.010869613919219,0.750122776784351,-0.661209249211308));
#120903=DIRECTION('ref_axis',(-0.347588297955064,0.617178220151042,0.705884848750767));
#120904=DIRECTION('center_axis',(-0.0108384416915672,0.747971550610416,
-0.663642288932184));
#120905=DIRECTION('ref_axis',(-0.34871994811035,0.619187579593734,0.703563173472552));
#120906=DIRECTION('center_axis',(0.,0.,1.));
#120907=DIRECTION('ref_axis',(0.871318704123391,0.490717552003934,0.));
#120908=DIRECTION('center_axis',(0.,0.,1.));
#120909=DIRECTION('ref_axis',(0.871318704123391,0.490717552003934,0.));
#120910=DIRECTION('center_axis',(0.,0.,1.));
#120911=DIRECTION('ref_axis',(-0.871318704123391,-0.490717552003934,0.));
#120912=DIRECTION('center_axis',(0.,0.,-1.));
#120913=DIRECTION('ref_axis',(0.871318704123389,0.490717552003939,0.));
#120914=DIRECTION('center_axis',(0.996912329797655,0.0785226508557306,0.));
#120915=DIRECTION('ref_axis',(-0.0785226508557306,0.996912329797655,0.));
#120916=DIRECTION('',(0.,0.,1.));
#120917=DIRECTION('center_axis',(-0.996912714474511,-0.0785177668673624,
2.28597554219387E-6));
#120918=DIRECTION('ref_axis',(0.0743278990302071,-0.94370603889449,0.322326349496635));
#120919=DIRECTION('',(0.,0.,-1.));
#120920=DIRECTION('center_axis',(-0.47533560879057,-0.879804557282865,0.));
#120921=DIRECTION('ref_axis',(0.879804557282865,-0.47533560879057,0.));
#120922=DIRECTION('center_axis',(0.475335608790533,0.879804557282885,3.13366257494963E-14));
#120923=DIRECTION('ref_axis',(0.878623270491977,-0.474697390141555,-0.051802860372563));
#120924=DIRECTION('',(0.,0.,1.));
#120925=DIRECTION('',(0.,0.,1.));
#120926=DIRECTION('center_axis',(0.,0.,1.));
#120927=DIRECTION('ref_axis',(0.838088104891841,0.545534901210548,0.));
#120928=DIRECTION('center_axis',(0.,0.,-1.));
#120929=DIRECTION('ref_axis',(-0.838088104891841,-0.545534901210548,0.));
#120930=DIRECTION('center_axis',(-0.918849822150867,-0.316355667117503,
-0.235868811452382));
#120931=DIRECTION('ref_axis',(-0.0839718152146669,0.740795646501562,-0.666461209954403));
#120932=DIRECTION('center_axis',(-0.661214718212259,-0.712152371479299,
0.235868811452244));
#120933=DIRECTION('ref_axis',(0.643402498151158,-0.376646626179641,0.666461209944242));
#120934=DIRECTION('center_axis',(0.,0.,-1.));
#120935=DIRECTION('ref_axis',(-0.83808810489184,-0.54553490121055,0.));
#120936=DIRECTION('center_axis',(0.830234038864126,0.557414962762358,-6.76296429840134E-17));
#120937=DIRECTION('ref_axis',(0.557414962762358,-0.830234038864126,-8.62816615085482E-32));
#120938=DIRECTION('center_axis',(0.,0.,1.));
#120939=DIRECTION('ref_axis',(0.83808810489184,0.54553490121055,0.));
#120940=DIRECTION('center_axis',(0.845772188033216,0.533544193061368,-1.38914942345546E-16));
#120941=DIRECTION('ref_axis',(-0.533544193061368,0.845772188033216,-2.46519032881566E-31));
#120942=DIRECTION('center_axis',(0.,0.,-1.));
#120943=DIRECTION('ref_axis',(-0.838088104891845,-0.545534901210541,0.));
#120944=DIRECTION('center_axis',(0.,0.,1.));
#120945=DIRECTION('ref_axis',(0.838088104891845,0.545534901210541,0.));
#120946=DIRECTION('center_axis',(0.,0.,1.));
#120947=DIRECTION('ref_axis',(0.838088104891845,0.545534901210541,0.));
#120948=DIRECTION('center_axis',(0.658137863669024,-0.355574837054025,0.663642288932205));
#120949=DIRECTION('ref_axis',(0.387674950010772,-0.595572828516713,-0.703563173472537));
#120950=DIRECTION('center_axis',(0.660030720953822,-0.35659749880586,0.661209249211309));
#120951=DIRECTION('ref_axis',(0.38641688485058,-0.593640102592878,-0.705884848750766));
#120952=DIRECTION('center_axis',(-0.0589078124527763,0.747885150534122,
-0.661209249211308));
#120953=DIRECTION('ref_axis',(-0.386416884850565,0.593640102592884,0.705884848750769));
#120954=DIRECTION('center_axis',(-0.0587388747376171,0.745740341496563,
-0.663642288932184));
#120955=DIRECTION('ref_axis',(-0.387674950010756,0.595572828516706,0.703563173472552));
#120956=DIRECTION('center_axis',(0.,0.,1.));
#120957=DIRECTION('ref_axis',(0.838088104891845,0.545534901210541,0.));
#120958=DIRECTION('center_axis',(0.,0.,1.));
#120959=DIRECTION('ref_axis',(0.838088104891845,0.545534901210541,0.));
#120960=DIRECTION('center_axis',(0.,0.,1.));
#120961=DIRECTION('ref_axis',(-0.838088104891825,-0.545534901210574,0.));
#120962=DIRECTION('center_axis',(0.,0.,-1.));
#120963=DIRECTION('ref_axis',(0.83808810489184,0.54553490121055,0.));
#120964=DIRECTION('center_axis',(0.989833102983779,0.14223370991964,0.));
#120965=DIRECTION('ref_axis',(-0.14223370991964,0.989833102983779,0.));
#120966=DIRECTION('',(0.,0.,1.));
#120967=DIRECTION('center_axis',(-0.989833799788485,-0.14222886061227,2.2859755500044E-6));
#120968=DIRECTION('ref_axis',(0.134638637897969,-0.937004888776007,0.322326349519926));
#120969=DIRECTION('',(0.,0.,-1.));
#120970=DIRECTION('center_axis',(-0.417989709277579,-0.908451761481062,
0.));
#120971=DIRECTION('ref_axis',(0.908451761481062,-0.417989709277579,0.));
#120972=DIRECTION('center_axis',(0.417989709277481,0.908451761481108,5.45355926330684E-14));
#120973=DIRECTION('ref_axis',(0.907232010961355,-0.417428487221712,-0.0518028603728525));
#120974=DIRECTION('',(0.,0.,1.));
#120975=DIRECTION('',(0.,0.,1.));
#120976=DIRECTION('center_axis',(0.,0.,1.));
#120977=DIRECTION('ref_axis',(0.801413621867962,0.59811053049121,0.));
#120978=DIRECTION('center_axis',(0.,0.,-1.));
#120979=DIRECTION('ref_axis',(-0.801413621867962,-0.59811053049121,0.));
#120980=DIRECTION('center_axis',(-0.896692969460631,-0.374576590704683,
-0.235868811452323));
#120981=DIRECTION('ref_axis',(-0.131262226152734,0.733893509731262,-0.666461209943803));
#120982=DIRECTION('center_axis',(-0.614228422558364,-0.753053350504152,
0.235868811452332));
#120983=DIRECTION('ref_axis',(0.666212390915799,-0.334649825708461,0.666461209931644));
#120984=DIRECTION('center_axis',(0.,0.,-1.));
#120985=DIRECTION('ref_axis',(-0.801413621867956,-0.598110530491217,0.));
#120986=DIRECTION('center_axis',(0.792814534704233,0.609462971444295,-6.76296429840134E-17));
#120987=DIRECTION('ref_axis',(0.609462971444295,-0.792814534704233,-4.93038065763132E-31));
#120988=DIRECTION('center_axis',(0.,0.,1.));
#120989=DIRECTION('ref_axis',(0.801413621867956,0.598110530491217,0.));
#120990=DIRECTION('center_axis',(0.809850164545245,0.586636779435145,-1.38914942345546E-16));
#120991=DIRECTION('ref_axis',(-0.586636779435145,0.809850164545245,-2.58844984525644E-31));
#120992=DIRECTION('center_axis',(0.,0.,-1.));
#120993=DIRECTION('ref_axis',(-0.801413621867959,-0.598110530491212,0.));
#120994=DIRECTION('center_axis',(0.,0.,1.));
#120995=DIRECTION('ref_axis',(0.801413621867959,0.598110530491212,0.));
#120996=DIRECTION('center_axis',(0.,0.,1.));
#120997=DIRECTION('ref_axis',(0.801413621867959,0.598110530491212,0.));
#120998=DIRECTION('center_axis',(0.679567406872709,-0.312677232713105,0.663642288932205));
#120999=DIRECTION('ref_axis',(0.42503691238556,-0.569510740937348,-0.703563173472534));
#121000=DIRECTION('center_axis',(0.681521897242613,-0.313576517514062,0.661209249211309));
#121001=DIRECTION('ref_axis',(0.423657601880077,-0.567662590517754,-0.705884848750768));
#121002=DIRECTION('center_axis',(-0.106703946149279,0.742574303779487,-0.661209249211308));
#121003=DIRECTION('ref_axis',(-0.423657601880061,0.567662590517767,0.705884848750768));
#121004=DIRECTION('center_axis',(-0.106397937147921,0.740444725358699,-0.663642288932184));
#121005=DIRECTION('ref_axis',(-0.425036912385554,0.569510740937331,0.703563173472552));
#121006=DIRECTION('center_axis',(0.,0.,1.));
#121007=DIRECTION('ref_axis',(0.801413621867959,0.598110530491212,0.));
#121008=DIRECTION('center_axis',(0.,0.,1.));
#121009=DIRECTION('ref_axis',(0.801413621867959,0.598110530491212,0.));
#121010=DIRECTION('center_axis',(0.,0.,1.));
#121011=DIRECTION('ref_axis',(-0.801413621867914,-0.598110530491273,0.));
#121012=DIRECTION('center_axis',(0.,0.,-1.));
#121013=DIRECTION('ref_axis',(0.801413621867956,0.598110530491217,0.));
#121014=DIRECTION('center_axis',(0.978686439631207,0.205360300160456,0.));
#121015=DIRECTION('ref_axis',(-0.205360300160456,0.978686439631207,0.));
#121016=DIRECTION('',(0.,0.,1.));
#121017=DIRECTION('center_axis',(-0.978687445700444,-0.205355505460931,
2.28597554707789E-6));
#121018=DIRECTION('ref_axis',(0.194396117720302,-0.926453384576079,0.322326349563298));
#121019=DIRECTION('',(0.,0.,-1.));
#121020=DIRECTION('center_axis',(-0.358926200390655,-0.933365942529042,
0.));
#121021=DIRECTION('ref_axis',(0.933365942529042,-0.358926200390655,0.));
#121022=DIRECTION('center_axis',(0.358926200390684,0.933365942529031,4.98882116956285E-15));
#121023=DIRECTION('ref_axis',(0.932112740497134,-0.358444281110008,-0.0518028603694038));
#121024=DIRECTION('',(0.,0.,1.));
#121025=DIRECTION('',(0.,0.,1.));
#121026=DIRECTION('center_axis',(0.,0.,1.));
#121027=DIRECTION('ref_axis',(0.761445958369139,0.648228395307783,0.));
#121028=DIRECTION('center_axis',(0.,0.,-1.));
#121029=DIRECTION('ref_axis',(-0.761445958369139,-0.648228395307783,0.));
#121030=DIRECTION('center_axis',(-0.870851413018747,-0.431258298734428,
-0.235868811452339));
#121031=DIRECTION('ref_axis',(-0.178013252440888,0.723975647099357,-0.666461209945848));
#121032=DIRECTION('center_axis',(-0.564718130564378,-0.790859871782574,
0.235868811452309));
#121033=DIRECTION('ref_axis',(0.68628467405606,-0.29127787730918,0.666461209933501));
#121034=DIRECTION('center_axis',(0.,0.,-1.));
#121035=DIRECTION('ref_axis',(-0.761445958369133,-0.64822839530779,0.));
#121036=DIRECTION('center_axis',(0.752137185563056,0.659006566047171,-6.76296429840134E-17));
#121037=DIRECTION('ref_axis',(0.659006566047171,-0.752137185563056,8.0118685686509E-32));
#121038=DIRECTION('center_axis',(0.,0.,1.));
#121039=DIRECTION('ref_axis',(0.761445958369133,0.64822839530779,0.));
#121040=DIRECTION('center_axis',(0.770600293018843,0.637318749449029,-1.38914942345546E-16));
#121041=DIRECTION('ref_axis',(-0.637318749449029,0.770600293018843,7.02579243712463E-31));
#121042=DIRECTION('center_axis',(0.,0.,-1.));
#121043=DIRECTION('ref_axis',(-0.76144595836914,-0.648228395307782,0.));
#121044=DIRECTION('center_axis',(0.,0.,1.));
#121045=DIRECTION('ref_axis',(0.76144595836914,0.648228395307782,0.));
#121046=DIRECTION('center_axis',(0.,0.,1.));
#121047=DIRECTION('ref_axis',(0.76144595836914,0.648228395307782,0.));
#121048=DIRECTION('center_axis',(0.698204461834803,-0.268494770553911,0.663642288932205));
#121049=DIRECTION('ref_axis',(0.46065230691723,-0.541108411563795,-0.703563173472532));
#121050=DIRECTION('center_axis',(0.700212553869646,-0.269266983049846,0.661209249211309));
#121051=DIRECTION('ref_axis',(0.459157418949173,-0.539352431094955,-0.705884848750768));
#121052=DIRECTION('center_axis',(-0.154061610443129,0.734212059928933,-0.661209249211308));
#121053=DIRECTION('ref_axis',(-0.459157418949153,0.539352431094971,0.705884848750769));
#121054=DIRECTION('center_axis',(-0.153619787612198,0.73210646301944,-0.663642288932184));
#121055=DIRECTION('ref_axis',(-0.46065230691723,0.541108411563772,0.70356317347255));
#121056=DIRECTION('center_axis',(0.,0.,1.));
#121057=DIRECTION('ref_axis',(0.76144595836914,0.648228395307782,0.));
#121058=DIRECTION('center_axis',(0.,0.,1.));
#121059=DIRECTION('ref_axis',(0.76144595836914,0.648228395307782,0.));
#121060=DIRECTION('center_axis',(0.,0.,1.));
#121061=DIRECTION('ref_axis',(-0.761445958369116,-0.648228395307811,0.));
#121062=DIRECTION('center_axis',(0.,0.,-1.));
#121063=DIRECTION('ref_axis',(0.761445958369133,0.64822839530779,0.));
#121064=DIRECTION('center_axis',(0.963518143770607,0.267643020878265,0.));
#121065=DIRECTION('ref_axis',(-0.267643020878265,0.963518143770607,0.));
#121066=DIRECTION('',(0.,0.,1.));
#121067=DIRECTION('center_axis',(-0.963519454970215,-0.267638300489063,
2.28597553609503E-6));
#121068=DIRECTION('ref_axis',(0.253354782203448,-0.912094884725178,0.322326349516771));
#121069=DIRECTION('',(0.,0.,-1.));
#121070=DIRECTION('center_axis',(-0.298387786756896,-0.954444722712804,
0.));
#121071=DIRECTION('ref_axis',(0.954444722712804,-0.298387786756896,0.));
#121072=DIRECTION('center_axis',(0.298387786756783,0.954444722712839,7.13989463202568E-14));
#121073=DIRECTION('ref_axis',(0.953163218841613,-0.297987150559883,-0.0518028604296759));
#121074=DIRECTION('',(0.,0.,1.));
#121075=DIRECTION('',(0.,0.,1.));
#121076=DIRECTION('center_axis',(0.,0.,1.));
#121077=DIRECTION('ref_axis',(0.718349350097714,0.6956825506035,0.));
#121078=DIRECTION('center_axis',(0.,0.,-1.));
#121079=DIRECTION('ref_axis',(-0.718349350097714,-0.6956825506035,0.));
#121080=DIRECTION('center_axis',(-0.84143134132374,-0.486167873910019,-0.235868811452348));
#121081=DIRECTION('ref_axis',(-0.224032784084857,0.711082813235251,-0.666461209956461));
#121082=DIRECTION('center_axis',(-0.512887290640372,-0.825416580208818,
0.235868811452382));
#121083=DIRECTION('ref_axis',(0.703536866258162,-0.246709005628528,0.666461209942055));
#121084=DIRECTION('center_axis',(0.,0.,-1.));
#121085=DIRECTION('ref_axis',(-0.718349350097726,-0.695682550603488,0.));
#121086=DIRECTION('center_axis',(0.70836914339348,0.705842161313694,-6.76296429840134E-17));
#121087=DIRECTION('ref_axis',(0.705842161313694,-0.70836914339348,4.93038065763132E-32));
#121088=DIRECTION('center_axis',(0.,0.,1.));
#121089=DIRECTION('ref_axis',(0.718349350097726,0.695682550603488,0.));
#121090=DIRECTION('center_axis',(0.728183859595181,0.685381840016984,-1.38914942345546E-16));
#121091=DIRECTION('ref_axis',(-0.685381840016983,0.728183859595181,-2.26797510251041E-30));
#121092=DIRECTION('center_axis',(0.,0.,-1.));
#121093=DIRECTION('ref_axis',(-0.718349350097727,-0.695682550603487,0.));
#121094=DIRECTION('center_axis',(0.,0.,1.));
#121095=DIRECTION('ref_axis',(0.718349350097727,0.695682550603487,0.));
#121096=DIRECTION('center_axis',(0.,0.,1.));
#121097=DIRECTION('ref_axis',(0.718349350097727,0.695682550603487,0.));
#121098=DIRECTION('center_axis',(0.71397244489883,-0.223209005790563,0.663642288932205));
#121099=DIRECTION('ref_axis',(0.49437478231017,-0.510482551659733,-0.703563173472532));
#121100=DIRECTION('center_axis',(0.716025886917706,-0.223850972794691,0.661209249211309));
#121101=DIRECTION('ref_axis',(0.492770459694845,-0.508825956842062,-0.705884848750766));
#121102=DIRECTION('center_axis',(-0.200786202533557,0.722832781236139,-0.661209249211308));
#121103=DIRECTION('ref_axis',(-0.492770459694827,0.508825956842073,0.70588484875077));
#121104=DIRECTION('center_axis',(-0.200210381417836,0.720759818187291,-0.663642288932184));
#121105=DIRECTION('ref_axis',(-0.494374782310162,0.510482551659712,0.703563173472552));
#121106=DIRECTION('center_axis',(0.,0.,1.));
#121107=DIRECTION('ref_axis',(0.718349350097718,0.695682550603496,0.));
#121108=DIRECTION('center_axis',(0.,0.,1.));
#121109=DIRECTION('ref_axis',(0.718349350097718,0.695682550603496,0.));
#121110=DIRECTION('center_axis',(0.,0.,1.));
#121111=DIRECTION('ref_axis',(-0.71834935009771,-0.695682550603505,0.));
#121112=DIRECTION('center_axis',(0.,0.,-1.));
#121113=DIRECTION('ref_axis',(0.718349350097726,0.695682550603488,0.));
#121114=DIRECTION('center_axis',(0.944390545183261,0.328825939014038,0.));
#121115=DIRECTION('ref_axis',(-0.328825939014038,0.944390545183261,0.));
#121116=DIRECTION('',(0.,0.,1.));
#121117=DIRECTION('center_axis',(-0.944392156125254,-0.328821312332196,
2.28597555969625E-6));
#121118=DIRECTION('ref_axis',(0.311272357538725,-0.893988391333502,0.322326349517413));
#121119=DIRECTION('',(0.,0.,-1.));
#121120=DIRECTION('center_axis',(-0.236623233703374,-0.971601484803187,
0.));
#121121=DIRECTION('ref_axis',(0.971601484803187,-0.236623233703375,0.));
#121122=DIRECTION('center_axis',(0.236623233703522,0.971601484803151,-7.0412563427439E-14));
#121123=DIRECTION('ref_axis',(0.970296945070278,-0.236305526891715,-0.051802860420206));
#121124=DIRECTION('',(0.,0.,1.));
#121125=DIRECTION('',(0.,0.,1.));
#121126=DIRECTION('center_axis',(0.,0.,1.));
#121127=DIRECTION('ref_axis',(0.672300890261307,0.740277997075324,0.));
#121128=DIRECTION('center_axis',(0.,0.,-1.));
#121129=DIRECTION('ref_axis',(-0.672300890261307,-0.740277997075324,0.));
#121130=DIRECTION('center_axis',(-0.808553647760786,-0.539079681009014,
-0.235868811452357));
#121131=DIRECTION('ref_axis',(-0.269131716968951,0.695267987570997,-0.66646120995923));
#121132=DIRECTION('center_axis',(-0.458948886824907,-0.856581474855869,
0.235868811452304));
#121133=DIRECTION('ref_axis',(0.717898074569612,-0.201126353727058,0.666461209948262));
#121134=DIRECTION('center_axis',(0.,0.,-1.));
#121135=DIRECTION('ref_axis',(-0.672300890261315,-0.740277997075317,0.));
#121136=DIRECTION('center_axis',(0.661690260468995,0.74977729973671,-6.76296429840134E-17));
#121137=DIRECTION('ref_axis',(0.74977729973671,-0.661690260468995,9.24446373305873E-32));
#121138=DIRECTION('center_axis',(0.,0.,1.));
#121139=DIRECTION('ref_axis',(0.672300890261315,0.740277997075317,0.));
#121140=DIRECTION('center_axis',(0.682775162497494,0.730628549590365,-1.38914942345546E-16));
#121141=DIRECTION('ref_axis',(-0.730628549590365,0.682775162497494,5.05364017407211E-31));
#121142=DIRECTION('center_axis',(0.,0.,-1.));
#121143=DIRECTION('ref_axis',(-0.672300890261315,-0.740277997075317,0.));
#121144=DIRECTION('center_axis',(0.,0.,1.));
#121145=DIRECTION('ref_axis',(0.672300890261315,0.740277997075317,0.));
#121146=DIRECTION('center_axis',(0.,0.,1.));
#121147=DIRECTION('ref_axis',(0.672300890261315,0.740277997075317,0.));
#121148=DIRECTION('center_axis',(0.726806562040158,-0.17700602734424,0.663642288932205));
#121149=DIRECTION('ref_axis',(0.52606576567954,-0.477759009452735,-0.703563173472532));
#121150=DIRECTION('center_axis',(0.72889691600935,-0.17751511087644,0.661209249211309));
#121151=DIRECTION('ref_axis',(0.524358600922709,-0.47620860758966,-0.705884848750769));
#121152=DIRECTION('center_axis',(-0.24668572104927,0.708483227598099,-0.661209249211308));
#121153=DIRECTION('ref_axis',(-0.524358600922702,0.476208607589674,0.705884848750765));
#121154=DIRECTION('center_axis',(-0.245978267821235,0.706451416659714,-0.663642288932184));
#121155=DIRECTION('ref_axis',(-0.526065765679537,0.477759009452712,0.70356317347255));
#121156=DIRECTION('center_axis',(0.,0.,1.));
#121157=DIRECTION('ref_axis',(0.672300890261315,0.740277997075317,0.));
#121158=DIRECTION('center_axis',(0.,0.,1.));
#121159=DIRECTION('ref_axis',(0.672300890261315,0.740277997075317,0.));
#121160=DIRECTION('center_axis',(0.,0.,1.));
#121161=DIRECTION('ref_axis',(-0.672300890261315,-0.740277997075317,0.));
#121162=DIRECTION('center_axis',(0.,0.,-1.));
#121163=DIRECTION('ref_axis',(0.672300890261315,0.740277997075317,0.));
#121164=DIRECTION('center_axis',(0.921382243274619,0.388657640833459,0.));
#121165=DIRECTION('ref_axis',(-0.388657640833459,0.921382243274619,0.));
#121166=DIRECTION('',(0.,0.,1.));
#121167=DIRECTION('center_axis',(-0.921384147339256,-0.388653126871104,
2.2859755282268E-6));
#121168=DIRECTION('ref_axis',(0.367910847994899,-0.872208307895385,0.3223263494751));
#121169=DIRECTION('',(0.,0.,-1.));
#121170=DIRECTION('center_axis',(-0.173886345027041,-0.98476572798465,0.));
#121171=DIRECTION('ref_axis',(0.98476572798465,-0.173886345027041,0.));
#121172=DIRECTION('center_axis',(0.173886345027122,0.984765727984635,-4.96795537759849E-14));
#121173=DIRECTION('ref_axis',(0.983443513024248,-0.173652873125871,-0.0518028604003333));
#121174=DIRECTION('',(0.,0.,1.));
#121175=DIRECTION('',(0.,0.,1.));
#121176=DIRECTION('center_axis',(0.,0.,1.));
#121177=DIRECTION('ref_axis',(0.623489801858719,0.781831482468041,0.));
#121178=DIRECTION('center_axis',(0.,0.,-1.));
#121179=DIRECTION('ref_axis',(-0.623489801858719,-0.781831482468041,0.));
#121180=DIRECTION('center_axis',(-0.772353433825047,-0.589776294066432,
-0.235868811452307));
#121181=DIRECTION('ref_axis',(-0.313124729920872,0.676596156628891,-0.666461209934227));
#121182=DIRECTION('center_axis',(-0.403124563589635,-0.884226492486333,
0.235868811452432));
#121183=DIRECTION('ref_axis',(0.729309285717962,-0.154717230509031,0.66646120993586));
#121184=DIRECTION('center_axis',(0.,0.,-1.));
#121185=DIRECTION('ref_axis',(-0.623489801858732,-0.781831482468031,0.));
#121186=DIRECTION('center_axis',(0.612292350332128,0.790631442408382,-6.76296429840134E-17));
#121187=DIRECTION('ref_axis',(0.790631442408382,-0.612292350332128,2.09541177949331E-31));
#121188=DIRECTION('center_axis',(0.,0.,1.));
#121189=DIRECTION('ref_axis',(0.623489801858732,0.781831482468031,0.));
#121190=DIRECTION('center_axis',(0.634560795802293,0.772872949734147,-1.38914942345546E-16));
#121191=DIRECTION('ref_axis',(-0.772872949734147,0.634560795802293,-9.73750179882187E-31));
#121192=DIRECTION('center_axis',(0.,0.,-1.));
#121193=DIRECTION('ref_axis',(-0.623489801858737,-0.781831482468027,0.));
#121194=DIRECTION('center_axis',(0.,0.,1.));
#121195=DIRECTION('ref_axis',(0.623489801858737,0.781831482468027,0.));
#121196=DIRECTION('center_axis',(0.,0.,1.));
#121197=DIRECTION('ref_axis',(0.623489801858737,0.781831482468027,0.));
#121198=DIRECTION('center_axis',(0.736654075118545,-0.130075693163885,0.663642288932205));
#121199=DIRECTION('ref_axis',(0.555595031976982,-0.443072252996905,-0.703563173472534));
#121200=DIRECTION('center_axis',(0.738772751325214,-0.130449801290727,0.661209249211309));
#121201=DIRECTION('ref_axis',(0.553792040184808,-0.441634415022259,-0.705884848750768));
#121202=DIRECTION('center_axis',(-0.291571555023269,0.691222364408683,-0.661209249211308));
#121203=DIRECTION('ref_axis',(-0.553792040184795,0.441634415022276,0.705884848750768));
#121204=DIRECTION('center_axis',(-0.290735376759984,0.689240054727728,-0.663642288932184));
#121205=DIRECTION('ref_axis',(-0.555595031976965,0.443072252996895,0.703563173472553));
#121206=DIRECTION('center_axis',(0.,0.,1.));
#121207=DIRECTION('ref_axis',(0.623489801858737,0.781831482468027,0.));
#121208=DIRECTION('center_axis',(0.,0.,1.));
#121209=DIRECTION('ref_axis',(0.623489801858737,0.781831482468027,0.));
#121210=DIRECTION('center_axis',(0.,0.,1.));
#121211=DIRECTION('ref_axis',(-0.623489801858745,-0.78183148246802,0.));
#121212=DIRECTION('center_axis',(0.,0.,-1.));
#121213=DIRECTION('ref_axis',(0.623489801858732,0.781831482468031,0.));
#121214=DIRECTION('center_axis',(0.894587784092491,0.446892265039893,0.));
#121215=DIRECTION('ref_axis',(-0.446892265039893,0.894587784092491,0.));
#121216=DIRECTION('',(0.,0.,1.));
#121217=DIRECTION('center_axis',(-0.894589973455614,-0.446887882345739,
2.2859755604554E-6));
#121218=DIRECTION('ref_axis',(0.423037513844087,-0.846844133396228,0.322326349548103));
#121219=DIRECTION('',(0.,0.,-1.));
#121220=DIRECTION('center_axis',(-0.110434920060487,-0.993883357558237,
0.));
#121221=DIRECTION('ref_axis',(0.993883357558237,-0.110434920060487,0.));
#121222=DIRECTION('center_axis',(0.110434920060531,0.993883357558232,-1.65883046113383E-14));
#121223=DIRECTION('ref_axis',(0.992548900634615,-0.110286642455757,-0.051802860392579));
#121224=DIRECTION('',(0.,0.,1.));
#121225=DIRECTION('',(0.,0.,1.));
#121226=DIRECTION('center_axis',(0.,0.,1.));
#121227=DIRECTION('ref_axis',(0.572116660122161,0.820172254596962,0.));
#121228=DIRECTION('center_axis',(0.,0.,-1.));
#121229=DIRECTION('ref_axis',(-0.572116660122161,-0.820172254596962,0.));
#121230=DIRECTION('center_axis',(-0.732979453960466,-0.638049389824897,
-0.235868811452243));
#121231=DIRECTION('ref_axis',(-0.355831046170119,0.655144046930282,-0.666461209938951));
#121232=DIRECTION('center_axis',(-0.345643715052351,-0.908238033793365,
0.235868811452408));
#121233=DIRECTION('ref_axis',(0.737723608565327,-0.107672340995304,0.66646120993644));
#121234=DIRECTION('center_axis',(0.,0.,-1.));
#121235=DIRECTION('ref_axis',(-0.572116660122168,-0.820172254596957,0.));
#121236=DIRECTION('center_axis',(0.560378399591449,0.828236710893285,-6.76296429840134E-17));
#121237=DIRECTION('ref_axis',(0.828236710893285,-0.560378399591449,7.33394122822659E-31));
#121238=DIRECTION('center_axis',(0.,0.,1.));
#121239=DIRECTION('ref_axis',(0.572116660122168,0.820172254596957,0.));
#121240=DIRECTION('center_axis',(0.583738882684276,0.811941449146743,-1.38914942345546E-16));
#121241=DIRECTION('ref_axis',(-0.811941449146743,0.583738882684276,9.73750179882187E-31));
#121242=DIRECTION('center_axis',(0.,0.,-1.));
#121243=DIRECTION('ref_axis',(-0.572116660122157,-0.820172254596965,0.));
#121244=DIRECTION('center_axis',(0.,0.,1.));
#121245=DIRECTION('ref_axis',(0.572116660122157,0.820172254596965,0.));
#121246=DIRECTION('center_axis',(0.,0.,1.));
#121247=DIRECTION('ref_axis',(0.572116660122157,0.820172254596965,0.));
#121248=DIRECTION('center_axis',(0.743474518590466,-0.0826108500591721,
0.663642288932205));
#121249=DIRECTION('ref_axis',(0.582841239113268,-0.406564817614812,-0.703563173472535));
#121250=DIRECTION('center_axis',(0.745612810939625,-0.0828484454901143,
0.661209249211309));
#121251=DIRECTION('ref_axis',(0.580949829165765,-0.405245451913252,-0.705884848750767));
#121252=DIRECTION('center_axis',(-0.335259258935775,0.67112112025718,-0.661209249211308));
#121253=DIRECTION('ref_axis',(-0.580949829165751,0.405245451913267,0.705884848750769));
#121254=DIRECTION('center_axis',(-0.334297791673084,0.669196457569339,-0.663642288932184));
#121255=DIRECTION('ref_axis',(-0.582841239113247,0.40656481761481,0.703563173472554));
#121256=DIRECTION('center_axis',(0.,0.,1.));
#121257=DIRECTION('ref_axis',(0.572116660122157,0.820172254596965,0.));
#121258=DIRECTION('center_axis',(0.,0.,1.));
#121259=DIRECTION('ref_axis',(0.572116660122157,0.820172254596965,0.));
#121260=DIRECTION('center_axis',(0.,0.,1.));
#121261=DIRECTION('ref_axis',(-0.572116660122118,-0.820172254596992,0.));
#121262=DIRECTION('center_axis',(0.,0.,-1.));
#121263=DIRECTION('ref_axis',(0.572116660122168,0.820172254596957,0.));
#121264=DIRECTION('center_axis',(0.864117271817049,0.503290513071188,0.));
#121265=DIRECTION('ref_axis',(-0.503290513071188,0.864117271817049,0.));
#121266=DIRECTION('',(0.,0.,1.));
#121267=DIRECTION('center_axis',(-0.864119737482087,-0.503286279654695,
2.28597557710273E-6));
#121268=DIRECTION('ref_axis',(0.476425827820026,-0.818000094733008,0.32232634953226));
#121269=DIRECTION('',(0.,0.,-1.));
#121270=DIRECTION('center_axis',(-0.0465296943191892,-0.998916907228305,
0.));
#121271=DIRECTION('ref_axis',(0.998916907228306,-0.0465296943191892,0.));
#121272=DIRECTION('center_axis',(0.0465296943190989,0.99891690722831,4.37256897280986E-14));
#121273=DIRECTION('ref_axis',(0.997575691911876,-0.0464672203152649,-0.0518028603719455));
#121274=DIRECTION('',(0.,0.,1.));
#121275=DIRECTION('',(0.,0.,1.));
#121276=DIRECTION('center_axis',(0.,0.,1.));
#121277=DIRECTION('ref_axis',(0.518392568310538,0.855142763005338,0.));
#121278=DIRECTION('center_axis',(0.,0.,-1.));
#121279=DIRECTION('ref_axis',(-0.518392568310538,-0.855142763005338,0.));
#121280=DIRECTION('center_axis',(-0.690593504295622,-0.683700603779703,
-0.23586881145239));
#121281=DIRECTION('ref_axis',(-0.397075176318766,0.630999809811531,-0.666461209950911));
#121282=DIRECTION('center_axis',(-0.28674254234948,-0.928517430203127,0.235868811452334));
#121283=DIRECTION('ref_axis',(0.743106466853929,-0.0601850027308018,0.666461209948609));
#121284=DIRECTION('center_axis',(0.,0.,-1.));
#121285=DIRECTION('ref_axis',(-0.518392568310523,-0.855142763005347,0.));
#121286=DIRECTION('center_axis',(0.506161733806058,0.86243857707691,-6.76296429840134E-17));
#121287=DIRECTION('ref_axis',(0.86243857707691,-0.506161733806058,-1.0538688655687E-30));
#121288=DIRECTION('center_axis',(0.,0.,1.));
#121289=DIRECTION('ref_axis',(0.518392568310523,0.855142763005347,0.));
#121290=DIRECTION('center_axis',(0.530518261285711,0.847673506983901,-1.38914942345546E-16));
#121291=DIRECTION('ref_axis',(-0.847673506983901,0.530518261285711,1.07235779303481E-30));
#121292=DIRECTION('center_axis',(0.,0.,-1.));
#121293=DIRECTION('ref_axis',(-0.518392568310514,-0.855142763005353,0.));
#121294=DIRECTION('center_axis',(0.,0.,1.));
#121295=DIRECTION('ref_axis',(0.518392568310514,0.855142763005353,0.));
#121296=DIRECTION('center_axis',(0.,0.,1.));
#121297=DIRECTION('ref_axis',(0.518392568310514,0.855142763005353,0.));
#121298=DIRECTION('center_axis',(0.747239865790714,-0.0348065412515937,
0.663642288932205));
#121299=DIRECTION('ref_axis',(0.60769242657898,-0.368386720189271,-0.703563173472533));
#121300=DIRECTION('center_axis',(0.749388987580438,-0.0349066476560473,
0.661209249211309));
#121301=DIRECTION('ref_axis',(0.605720370685339,-0.367191248317438,-0.70588484875077));
#121302=DIRECTION('center_axis',(-0.377569310640429,0.648262095467512,-0.661209249211308));
#121303=DIRECTION('ref_axis',(-0.605720370685332,0.367191248317457,0.705884848750766));
#121304=DIRECTION('center_axis',(-0.376486505253547,0.646402988624606,-0.663642288932184));
#121305=DIRECTION('ref_axis',(-0.607692426578967,0.368386720189258,0.703563173472552));
#121306=DIRECTION('center_axis',(0.,0.,1.));
#121307=DIRECTION('ref_axis',(0.518392568310514,0.855142763005353,0.));
#121308=DIRECTION('center_axis',(0.,0.,1.));
#121309=DIRECTION('ref_axis',(0.518392568310514,0.855142763005353,0.));
#121310=DIRECTION('center_axis',(0.,0.,1.));
#121311=DIRECTION('ref_axis',(-0.51839256831048,-0.855142763005373,0.));
#121312=DIRECTION('center_axis',(0.,0.,-1.));
#121313=DIRECTION('ref_axis',(0.518392568310523,0.855142763005347,0.));
#121314=DIRECTION('center_axis',(0.830095916319137,0.557620632428797,0.));
#121315=DIRECTION('ref_axis',(-0.557620632428797,0.830095916319137,0.));
#121316=DIRECTION('',(0.,0.,1.));
#121317=DIRECTION('center_axis',(-0.830098648154097,-0.557616565686059,
2.28597554586136E-6));
#121318=DIRECTION('ref_axis',(0.527856405890103,-0.785794718239048,0.322326349447883));
#121319=DIRECTION('',(0.,0.,-1.));
#121320=DIRECTION('center_axis',(0.0175667319166547,-0.999845693059568,
0.));
#121321=DIRECTION('ref_axis',(0.999845693059568,0.0175667319166547,0.));
#121322=DIRECTION('center_axis',(-0.0175667319166504,0.999845693059568,
-4.11269501834901E-15));
#121323=DIRECTION('ref_axis',(0.998503230691027,0.0175431456005816,-0.0518028603652222));
#121324=DIRECTION('',(0.,0.,1.));
#121325=DIRECTION('',(0.,0.,1.));
#121326=DIRECTION('center_axis',(0.,0.,1.));
#121327=DIRECTION('ref_axis',(0.46253829024085,0.886599306372992,0.));
#121328=DIRECTION('center_axis',(0.,0.,-1.));
#121329=DIRECTION('ref_axis',(-0.46253829024085,-0.886599306372992,0.));
#121330=DIRECTION('center_axis',(-0.64536975779005,-0.726542345300028,-0.235868811452357));
#121331=DIRECTION('ref_axis',(-0.436687639407675,0.604262659133404,-0.666461209948171));
#121332=DIRECTION('center_axis',(-0.226663083034028,-0.94498134932579,0.235868811452296));
#121333=DIRECTION('ref_axis',(0.745435741289,-0.012450351389804,0.666461209943377));
#121334=DIRECTION('center_axis',(0.,0.,-1.));
#121335=DIRECTION('ref_axis',(-0.462538290240833,-0.886599306373001,0.));
#121336=DIRECTION('center_axis',(0.449865140885107,0.893096498154832,-6.76296429840134E-17));
#121337=DIRECTION('ref_axis',(0.893096498154831,-0.449865140885107,6.47112461314111E-32));
#121338=DIRECTION('center_axis',(0.,0.,1.));
#121339=DIRECTION('ref_axis',(0.462538290240833,0.886599306373001,0.));
#121340=DIRECTION('center_axis',(0.475117626555714,0.879922292555465,-1.38914942345546E-16));
#121341=DIRECTION('ref_axis',(-0.879922292555465,0.475117626555714,-1.20794326111967E-30));
#121342=DIRECTION('center_axis',(0.,0.,-1.));
#121343=DIRECTION('ref_axis',(-0.462538290240822,-0.886599306373007,0.));
#121344=DIRECTION('center_axis',(0.,0.,1.));
#121345=DIRECTION('ref_axis',(0.462538290240822,0.886599306373007,0.));
#121346=DIRECTION('center_axis',(0.,0.,1.));
#121347=DIRECTION('ref_axis',(0.462538290240822,0.886599306373007,0.));
#121348=DIRECTION('center_axis',(0.74793464409998,0.0131407950999672,0.663642288932205));
#121349=DIRECTION('ref_axis',(0.630046475514265,-0.328694842711764,-0.703563173472533));
#121350=DIRECTION('center_axis',(0.750085764127849,0.0131785890806908,0.661209249211309));
#121351=DIRECTION('ref_axis',(0.628001877275149,-0.327628177120031,-0.705884848750767));
#121352=DIRECTION('center_axis',(-0.418327849059298,0.622739222675783,-0.661209249211308));
#121353=DIRECTION('ref_axis',(-0.628001877275143,0.327628177120045,0.705884848750767));
#121354=DIRECTION('center_axis',(-0.417128155027821,0.620953311146609,-0.663642288932184));
#121355=DIRECTION('ref_axis',(-0.630046475514251,0.32869484271175,0.703563173472552));
#121356=DIRECTION('center_axis',(0.,0.,1.));
#121357=DIRECTION('ref_axis',(0.462538290240822,0.886599306373007,0.));
#121358=DIRECTION('center_axis',(0.,0.,1.));
#121359=DIRECTION('ref_axis',(0.462538290240822,0.886599306373007,0.));
#121360=DIRECTION('center_axis',(0.,0.,1.));
#121361=DIRECTION('ref_axis',(-0.462538290240815,-0.886599306373011,0.));
#121362=DIRECTION('center_axis',(0.,0.,-1.));
#121363=DIRECTION('ref_axis',(0.462538290240833,0.886599306373001,0.));
#121364=DIRECTION('center_axis',(0.792663518646054,0.609659368998506,0.));
#121365=DIRECTION('ref_axis',(-0.609659368998506,0.792663518646054,0.));
#121366=DIRECTION('',(0.,0.,1.));
#121367=DIRECTION('center_axis',(-0.792666505425259,-0.609655485640606,
2.28597554274477E-6));
#121368=DIRECTION('ref_axis',(0.577117908749752,-0.750360342671505,0.322326349444494));
#121369=DIRECTION('',(0.,0.,-1.));
#121370=DIRECTION('center_axis',(0.081590972683001,-0.996665898471821,0.));
#121371=DIRECTION('ref_axis',(0.996665898471821,0.081590972683001,0.));
#121372=DIRECTION('center_axis',(-0.0815909726830444,0.996665898471817,
2.96721046178316E-14));
#121373=DIRECTION('ref_axis',(0.995327705513122,0.0814814229680361,-0.0518028604334566));
#121374=DIRECTION('',(0.,0.,1.));
#121375=DIRECTION('',(0.,0.,1.));
#121376=DIRECTION('center_axis',(0.,0.,1.));
#121377=DIRECTION('ref_axis',(0.40478334312238,0.914412623015818,0.));
#121378=DIRECTION('center_axis',(0.,0.,-1.));
#121379=DIRECTION('ref_axis',(-0.40478334312238,-0.914412623015818,0.));
#121380=DIRECTION('center_axis',(-0.597494048518314,-0.766398568480691,
-0.235868811452344));
#121381=DIRECTION('ref_axis',(-0.474505659308313,0.575042463570701,-0.666461209955181));
#121382=DIRECTION('center_axis',(-0.165652216491463,-0.957562137386155,
0.235868811452306));
#121383=DIRECTION('ref_axis',(0.744701860361022,0.0353354611192201,0.666461209945729));
#121384=DIRECTION('center_axis',(0.,0.,-1.));
#121385=DIRECTION('ref_axis',(-0.404783343122391,-0.914412623015814,0.));
#121386=DIRECTION('center_axis',(0.391719955604489,0.920084494153237,-6.76296429840134E-17));
#121387=DIRECTION('ref_axis',(0.920084494153237,-0.391719955604489,-7.48801562377757E-31));
#121388=DIRECTION('center_axis',(0.,0.,1.));
#121389=DIRECTION('ref_axis',(0.404783343122391,0.914412623015814,0.));
#121390=DIRECTION('center_axis',(0.417764631585787,0.908555288684179,-1.38914942345546E-16));
#121391=DIRECTION('ref_axis',(-0.908555288684179,0.417764631585787,5.7931972727168E-31));
#121392=DIRECTION('center_axis',(0.,0.,-1.));
#121393=DIRECTION('ref_axis',(-0.404783343122381,-0.914412623015818,0.));
#121394=DIRECTION('center_axis',(0.,0.,1.));
#121395=DIRECTION('ref_axis',(0.404783343122381,0.914412623015818,0.));
#121396=DIRECTION('center_axis',(0.,0.,1.));
#121397=DIRECTION('ref_axis',(0.404783343122381,0.914412623015818,0.));
#121398=DIRECTION('center_axis',(0.745555998525162,0.0610341331057705,0.663642288932205));
#121399=DIRECTION('ref_axis',(0.649811528337116,-0.287652287620733,-0.703563173472532));
#121400=DIRECTION('center_axis',(0.747700277377567,0.0612096721680979,0.661209249211309));
#121401=DIRECTION('ref_axis',(0.647702789445257,-0.286718811466814,-0.705884848750766));
#121402=DIRECTION('center_axis',(-0.457367388615341,0.594657380840936,-0.661209249211308));
#121403=DIRECTION('ref_axis',(-0.647702789445254,0.286718811466819,0.705884848750766));
#121404=DIRECTION('center_axis',(-0.456055735739378,0.592952003319043,-0.663642288932184));
#121405=DIRECTION('ref_axis',(-0.649811528337102,0.287652287620716,0.703563173472552));
#121406=DIRECTION('center_axis',(0.,0.,1.));
#121407=DIRECTION('ref_axis',(0.404783343122381,0.914412623015818,0.));
#121408=DIRECTION('center_axis',(0.,0.,1.));
#121409=DIRECTION('ref_axis',(0.404783343122381,0.914412623015818,0.));
#121410=DIRECTION('center_axis',(0.,0.,1.));
#121411=DIRECTION('ref_axis',(-0.40478334312241,-0.914412623015806,0.));
#121412=DIRECTION('center_axis',(0.,0.,-1.));
#121413=DIRECTION('ref_axis',(0.404783343122391,0.914412623015814,0.));
#121414=DIRECTION('center_axis',(0.751973896549063,0.659192884449475,0.));
#121415=DIRECTION('ref_axis',(-0.659192884449475,0.751973896549063,0.));
#121416=DIRECTION('',(0.,0.,1.));
#121417=DIRECTION('center_axis',(-0.751977125999198,-0.659189200433958,
2.28597553537158E-6));
#121418=DIRECTION('ref_axis',(0.624007910302061,-0.711842575470972,0.32232634957029));
#121419=DIRECTION('',(0.,0.,-1.));
#121420=DIRECTION('center_axis',(0.145279938641384,-0.989390589923088,0.));
#121421=DIRECTION('ref_axis',(0.989390589923088,0.145279938641384,0.));
#121422=DIRECTION('center_axis',(-0.145279938641383,0.989390589923088,1.57441884818865E-15));
#121423=DIRECTION('ref_axis',(0.988062165300268,0.145084875690857,-0.0518028604221298));
#121424=DIRECTION('',(0.,0.,1.));
#121425=DIRECTION('',(0.,0.,1.));
#121426=DIRECTION('center_axis',(0.,0.,1.));
#121427=DIRECTION('ref_axis',(0.345365054421307,0.938468422049761,0.));
#121428=DIRECTION('center_axis',(0.,0.,-1.));
#121429=DIRECTION('ref_axis',(-0.345365054421307,-0.938468422049761,0.));
#121430=DIRECTION('center_axis',(-0.547163108039054,-0.803105495551532,
-0.235868811452407));
#121431=DIRECTION('ref_axis',(-0.510373833685566,0.543459295184266,-0.666461209949176));
#121432=DIRECTION('center_axis',(-0.103960649459087,-0.96620809722756,0.235868811452349));
#121433=DIRECTION('ref_axis',(0.740907839755463,0.0829760726370221,0.666461209942956));
#121434=DIRECTION('center_axis',(0.,0.,-1.));
#121435=DIRECTION('ref_axis',(-0.345365054421305,-0.938468422049761,0.));
#121436=DIRECTION('center_axis',(0.331965109002625,0.943291665607661,-6.76296429840134E-17));
#121437=DIRECTION('ref_axis',(0.943291665607661,-0.331965109002625,6.16297582203915E-32));
#121438=DIRECTION('center_axis',(0.,0.,1.));
#121439=DIRECTION('ref_axis',(0.345365054421305,0.938468422049761,0.));
#121440=DIRECTION('center_axis',(0.358694952134443,0.933454836247191,-1.38914942345546E-16));
#121441=DIRECTION('ref_axis',(-0.933454836247191,0.358694952134442,1.17096540618744E-31));
#121442=DIRECTION('center_axis',(0.,0.,-1.));
#121443=DIRECTION('ref_axis',(-0.345365054421309,-0.93846842204976,0.));
#121444=DIRECTION('center_axis',(0.,0.,1.));
#121445=DIRECTION('ref_axis',(0.345365054421309,0.93846842204976,0.));
#121446=DIRECTION('center_axis',(0.,0.,1.));
#121447=DIRECTION('ref_axis',(0.345365054421309,0.93846842204976,0.));
#121448=DIRECTION('center_axis',(0.740113703431143,0.108676668766862,0.663642288932205));
#121449=DIRECTION('ref_axis',(0.666906366205896,-0.245427707578635,-0.703563173472534));
#121450=DIRECTION('center_axis',(0.742242329806335,0.108989231583133,0.661209249211309));
#121451=DIRECTION('ref_axis',(0.664742151921723,-0.24463125671627,-0.705884848750768));
#121452=DIRECTION('center_axis',(-0.494527507466565,0.564131964274605,-0.661209249211308));
#121453=DIRECTION('ref_axis',(-0.66474215192172,0.244631256716285,0.705884848750766));
#121454=DIRECTION('center_axis',(-0.493109285609133,0.562514128522034,-0.663642288932184));
#121455=DIRECTION('ref_axis',(-0.666906366205881,0.245427707578626,0.703563173472552));
#121456=DIRECTION('center_axis',(0.,0.,1.));
#121457=DIRECTION('ref_axis',(0.345365054421309,0.93846842204976,0.));
#121458=DIRECTION('center_axis',(0.,0.,1.));
#121459=DIRECTION('ref_axis',(0.345365054421309,0.93846842204976,0.));
#121460=DIRECTION('center_axis',(0.,0.,1.));
#121461=DIRECTION('ref_axis',(-0.345365054421273,-0.938468422049773,0.));
#121462=DIRECTION('center_axis',(0.,0.,-1.));
#121463=DIRECTION('ref_axis',(0.345365054421305,0.938468422049761,0.));
#121464=DIRECTION('center_axis',(0.708194252413257,0.706017634941811,0.));
#121465=DIRECTION('ref_axis',(-0.706017634941811,0.708194252413257,0.));
#121466=DIRECTION('',(0.,0.,1.));
#121467=DIRECTION('center_axis',(-0.708197711263846,-0.706014165407058,
2.28597556912132E-6));
#121468=DIRECTION('ref_axis',(0.668333729562862,-0.670399694507259,0.322326349424259));
#121469=DIRECTION('',(0.,0.,-1.));
#121470=DIRECTION('center_axis',(0.20837191816944,-0.978049663216745,0.));
#121471=DIRECTION('ref_axis',(0.978049663216745,0.20837191816944,0.));
#121472=DIRECTION('center_axis',(-0.208371918169327,0.978049663216769,-5.1823039677711E-14));
#121473=DIRECTION('ref_axis',(0.976736465708699,0.208092143538257,-0.0518028604667046));
#121474=DIRECTION('',(0.,0.,1.));
#121475=DIRECTION('',(0.,0.,1.));
#121476=DIRECTION('center_axis',(0.,0.,1.));
#121477=DIRECTION('ref_axis',(0.28452758663103,0.958667853036661,0.));
#121478=DIRECTION('center_axis',(0.,0.,-1.));
#121479=DIRECTION('ref_axis',(-0.28452758663103,-0.958667853036661,0.));
#121480=DIRECTION('center_axis',(-0.494583756982952,-0.836512289875464,
-0.23586881145233));
#121481=DIRECTION('ref_axis',(-0.544144772502367,0.509642935980642,-0.666461209946519));
#121482=DIRECTION('center_axis',(-0.0418418858185124,-0.970883700746492,
0.235868811452356));
#121483=DIRECTION('ref_axis',(0.734069269910053,0.130275717675065,0.66646120994246));
#121484=DIRECTION('center_axis',(0.,0.,-1.));
#121485=DIRECTION('ref_axis',(-0.28452758663103,-0.958667853036661,0.));
#121486=DIRECTION('center_axis',(0.270846146561577,0.962622649272676,-6.76296429840134E-17));
#121487=DIRECTION('ref_axis',(0.962622649272676,-0.270846146561577,-6.77927340424307E-32));
#121488=DIRECTION('center_axis',(0.,0.,1.));
#121489=DIRECTION('ref_axis',(0.28452758663103,0.958667853036661,0.));
#121490=DIRECTION('center_axis',(0.298151318184951,0.954518617662629,-1.38914942345546E-16));
#121491=DIRECTION('ref_axis',(-0.954518617662629,0.298151318184951,3.51289621856232E-31));
#121492=DIRECTION('center_axis',(0.,0.,-1.));
#121493=DIRECTION('ref_axis',(-0.284527586631029,-0.958667853036662,0.));
#121494=DIRECTION('center_axis',(0.,0.,1.));
#121495=DIRECTION('ref_axis',(0.284527586631029,0.958667853036662,0.));
#121496=DIRECTION('center_axis',(0.,0.,1.));
#121497=DIRECTION('ref_axis',(0.284527586631029,0.958667853036662,0.));
#121498=DIRECTION('center_axis',(0.731630122375834,0.155872628684918,0.663642288932205));
#121499=DIRECTION('ref_axis',(0.681260742764968,-0.202194612442027,-0.703563173472533));
#121500=DIRECTION('center_axis',(0.733734349291447,0.156320930867475,0.661209249211309));
#121501=DIRECTION('ref_axis',(0.679049946309197,-0.20153845965865,-0.705884848750768));
#121502=DIRECTION('center_axis',(-0.529655506713792,0.531288408461143,-0.661209249211308));
#121503=DIRECTION('ref_axis',(-0.679049946309192,0.20153845965867,0.705884848750768));
#121504=DIRECTION('center_axis',(-0.528136543652709,0.529764762512025,-0.663642288932184));
#121505=DIRECTION('ref_axis',(-0.681260742764954,0.202194612442015,0.703563173472551));
#121506=DIRECTION('center_axis',(0.,0.,1.));
#121507=DIRECTION('ref_axis',(0.284527586631029,0.958667853036662,0.));
#121508=DIRECTION('center_axis',(0.,0.,1.));
#121509=DIRECTION('ref_axis',(0.284527586631029,0.958667853036662,0.));
#121510=DIRECTION('center_axis',(0.,0.,1.));
#121511=DIRECTION('ref_axis',(-0.284527586631029,-0.958667853036662,0.));
#121512=DIRECTION('center_axis',(0.,0.,-1.));
#121513=DIRECTION('ref_axis',(0.28452758663103,0.958667853036661,0.));
#121514=DIRECTION('center_axis',(0.661504486187094,0.749941207531863,0.));
#121515=DIRECTION('ref_axis',(-0.749941207531863,0.661504486187094,0.));
#121516=DIRECTION('',(0.,0.,1.));
#121517=DIRECTION('center_axis',(-0.661508160224924,-0.74993796673499,2.28597553179878E-6));
#121518=DIRECTION('ref_axis',(0.709913222118179,-0.626201997342729,0.32232634950584));
#121519=DIRECTION('',(0.,0.,-1.));
#121520=DIRECTION('center_axis',(0.270607652790102,-0.962689720653249,0.));
#121521=DIRECTION('ref_axis',(0.962689720653249,0.270607652790102,0.));
#121522=DIRECTION('center_axis',(-0.27060765279011,0.962689720653247,2.92121087495402E-15));
#121523=DIRECTION('ref_axis',(0.96139714648011,0.27024431613496,-0.0518028603133916));
#121524=DIRECTION('',(0.,0.,1.));
#121525=DIRECTION('',(0.,0.,1.));
#121526=DIRECTION('center_axis',(0.,0.,1.));
#121527=DIRECTION('ref_axis',(0.222520933956302,0.974927912181827,0.));
#121528=DIRECTION('center_axis',(0.,0.,-1.));
#121529=DIRECTION('ref_axis',(-0.222520933956302,-0.974927912181827,0.));
#121530=DIRECTION('center_axis',(-0.439972055181329,-0.866481675769066,
-0.235868811452358));
#121531=DIRECTION('ref_axis',(-0.575679703722719,0.473732344632858,-0.66646120995177));
#121532=DIRECTION('center_axis',(0.0204488151059282,-0.971569734885157,
0.235868811452361));
#121533=DIRECTION('ref_axis',(0.724214251973394,0.17704003184605,0.666461209945911));
#121534=DIRECTION('center_axis',(0.,0.,-1.));
#121535=DIRECTION('ref_axis',(-0.222520933956311,-0.974927912181824,0.));
#121536=DIRECTION('center_axis',(0.208614219207991,0.977998009989918,-6.76296429840134E-17));
#121537=DIRECTION('ref_axis',(0.977998009989918,-0.208614219207991,-3.23556230657056E-32));
#121538=DIRECTION('center_axis',(0.,0.,1.));
#121539=DIRECTION('ref_axis',(0.222520933956311,0.974927912181824,0.));
#121540=DIRECTION('center_axis',(0.236382516515781,0.97166007733449,-1.38914942345546E-16));
#121541=DIRECTION('ref_axis',(-0.97166007733449,0.236382516515781,4.99201041585171E-31));
#121542=DIRECTION('center_axis',(0.,0.,-1.));
#121543=DIRECTION('ref_axis',(-0.222520933956319,-0.974927912181823,0.));
#121544=DIRECTION('center_axis',(0.,0.,1.));
#121545=DIRECTION('ref_axis',(0.222520933956319,0.974927912181823,0.));
#121546=DIRECTION('center_axis',(0.,0.,1.));
#121547=DIRECTION('ref_axis',(0.222520933956319,0.974927912181823,0.));
#121548=DIRECTION('center_axis',(0.720140116213513,0.202428074537133,0.663642288932205));
#121549=DIRECTION('ref_axis',(0.692815672802048,-0.158130656272285,-0.703563173472534));
#121550=DIRECTION('center_axis',(0.722211296949797,0.203010273916149,0.661209249211309));
#121551=DIRECTION('ref_axis',(0.690567378811531,-0.157617497840432,-0.705884848750767));
#121552=DIRECTION('center_axis',(-0.562607037873182,0.496261674616308,-0.661209249211308));
#121553=DIRECTION('ref_axis',(-0.690567378811525,0.15761749784045,0.705884848750769));
#121554=DIRECTION('center_axis',(-0.560993575353484,0.494838479458668,-0.663642288932184));
#121555=DIRECTION('ref_axis',(-0.69281567280203,0.158130656272279,0.703563173472553));
#121556=DIRECTION('center_axis',(0.,0.,1.));
#121557=DIRECTION('ref_axis',(0.222520933956319,0.974927912181823,0.));
#121558=DIRECTION('center_axis',(0.,0.,1.));
#121559=DIRECTION('ref_axis',(0.222520933956319,0.974927912181823,0.));
#121560=DIRECTION('center_axis',(0.,0.,1.));
#121561=DIRECTION('ref_axis',(-0.222520933956319,-0.974927912181823,0.));
#121562=DIRECTION('center_axis',(0.,0.,-1.));
#121563=DIRECTION('ref_axis',(0.222520933956311,0.974927912181824,0.));
#121564=DIRECTION('center_axis',(0.612096456134921,0.790783110838282,0.));
#121565=DIRECTION('ref_axis',(-0.790783110838282,0.612096456134921,0.));
#121566=DIRECTION('',(0.,0.,1.));
#121567=DIRECTION('center_axis',(-0.612100330262575,-0.790780112096416,
2.28597549873414E-6));
#121568=DIRECTION('ref_axis',(0.748575529000663,-0.579431101881055,0.322326349457012));
#121569=DIRECTION('',(0.,0.,-1.));
#121570=DIRECTION('center_axis',(0.33173140252029,-0.943373879531292,0.));
#121571=DIRECTION('ref_axis',(0.943373879531292,0.33173140252029,0.));
#121572=DIRECTION('center_axis',(-0.33173140252026,0.943373879531303,-1.39231739104898E-14));
#121573=DIRECTION('ref_axis',(0.942107240145474,0.331285996866079,-0.0518028604029466));
#121574=DIRECTION('',(0.,0.,1.));
#121575=DIRECTION('',(0.,0.,1.));
#121576=DIRECTION('center_axis',(0.,0.,1.));
#121577=DIRECTION('ref_axis',(0.159599895033352,0.987181783414455,0.));
#121578=DIRECTION('center_axis',(0.,0.,-1.));
#121579=DIRECTION('ref_axis',(-0.159599895033352,-0.987181783414455,0.));
#121580=DIRECTION('center_axis',(-0.38355241383127,-0.892890502597183,-0.235868811452375));
#121581=DIRECTION('ref_axis',(-0.604849043571402,0.43587508546863,-0.66646120994284));
#121582=DIRECTION('center_axis',(0.0826554874629293,-0.968263380582128,
0.235868811452328));
#121583=DIRECTION('ref_axis',(0.711383282337372,0.223076850549918,0.666461209943712));
#121584=DIRECTION('center_axis',(0.,0.,-1.));
#121585=DIRECTION('ref_axis',(-0.159599895033376,-0.987181783414451,0.));
#121586=DIRECTION('center_axis',(0.145525051280069,0.989354567104197,-6.76296429840134E-17));
#121587=DIRECTION('ref_axis',(0.989354567104197,-0.145525051280069,1.69481835106077E-31));
#121588=DIRECTION('center_axis',(0.,0.,1.));
#121589=DIRECTION('ref_axis',(0.159599895033376,0.987181783414451,0.));
#121590=DIRECTION('center_axis',(0.173642368382356,0.98480877732815,-1.38914942345546E-16));
#121591=DIRECTION('ref_axis',(-0.98480877732815,0.173642368382356,2.77333911991762E-31));
#121592=DIRECTION('center_axis',(0.,0.,-1.));
#121593=DIRECTION('ref_axis',(-0.159599895033363,-0.987181783414453,0.));
#121594=DIRECTION('center_axis',(0.,0.,1.));
#121595=DIRECTION('ref_axis',(0.159599895033363,0.987181783414453,0.));
#121596=DIRECTION('center_axis',(0.,0.,1.));
#121597=DIRECTION('ref_axis',(0.159599895033363,0.987181783414453,0.));
#121598=DIRECTION('center_axis',(0.705690899844101,0.24815170001039,0.663642288932205));
#121599=DIRECTION('ref_axis',(0.701523674631088,-0.113416907317004,-0.703563173472533));
#121600=DIRECTION('center_axis',(0.707720523475142,0.248865404203735,0.661209249211309));
#121601=DIRECTION('ref_axis',(0.699247121828089,-0.113048851914734,-0.705884848750767));
#121602=DIRECTION('center_axis',(-0.59324669603512,0.459195695102679,-0.661209249211308));
#121603=DIRECTION('ref_axis',(-0.699247121828083,0.113048851914757,0.70588484875077));
#121604=DIRECTION('center_axis',(-0.591545364120386,0.457878798950696,-0.663642288932184));
#121605=DIRECTION('ref_axis',(-0.701523674631068,0.113416907316999,0.703563173472553));
#121606=DIRECTION('center_axis',(0.,0.,1.));
#121607=DIRECTION('ref_axis',(0.159599895033363,0.987181783414453,0.));
#121608=DIRECTION('center_axis',(0.,0.,1.));
#121609=DIRECTION('ref_axis',(0.159599895033363,0.987181783414453,0.));
#121610=DIRECTION('center_axis',(0.,0.,1.));
#121611=DIRECTION('ref_axis',(-0.159599895033363,-0.987181783414453,0.));
#121612=DIRECTION('center_axis',(0.,0.,-1.));
#121613=DIRECTION('ref_axis',(0.159599895033376,0.987181783414451,0.));
#121614=DIRECTION('center_axis',(0.560173190450212,0.828375516719821,0.));
#121615=DIRECTION('ref_axis',(-0.828375516719821,0.560173190450212,0.));
#121616=DIRECTION('',(0.,0.,1.));
#121617=DIRECTION('center_axis',(-0.560177248748139,-0.828372772355381,
2.28597553096324E-6));
#121618=DIRECTION('ref_axis',(0.784161778430318,-0.530279199707863,0.322326349537529));
#121619=DIRECTION('',(0.,0.,-1.));
#121620=DIRECTION('center_axis',(0.39149199676136,-0.920181512785278,0.));
#121621=DIRECTION('ref_axis',(0.920181512785279,0.39149199676136,0.));
#121622=DIRECTION('center_axis',(-0.391491996761343,0.920181512785286,-5.74757724097888E-15));
#121623=DIRECTION('ref_axis',(0.918946013082694,0.390966352376137,-0.0518028604337561));
#121624=DIRECTION('',(0.,0.,1.));
#121625=DIRECTION('',(0.,0.,1.));
#121626=DIRECTION('center_axis',(0.,0.,1.));
#121627=DIRECTION('ref_axis',(0.096023025907694,0.995379112949197,0.));
#121628=DIRECTION('center_axis',(0.,0.,-1.));
#121629=DIRECTION('ref_axis',(-0.096023025907694,-0.995379112949197,0.));
#121630=DIRECTION('center_axis',(-0.325556673341238,-0.915630250825656,
-0.235868811452326));
#121631=DIRECTION('ref_axis',(-0.631532928957046,0.396226722081929,-0.666461209937341));
#121632=DIRECTION('center_axis',(0.144522510692408,-0.960978224356434,0.235868811452296));
#121633=DIRECTION('ref_axis',(-0.695629086210285,-0.268196998624628,-0.666461209934221));
#121634=DIRECTION('center_axis',(0.,0.,-1.));
#121635=DIRECTION('ref_axis',(-0.0960230259076783,-0.995379112949199,0.));
#121636=DIRECTION('center_axis',(0.0818378897014124,0.996645654086356,-6.76296429840134E-17));
#121637=DIRECTION('ref_axis',(0.996645654086356,-0.0818378897014124,-3.620748295448E-32));
#121638=DIRECTION('center_axis',(0.,0.,1.));
#121639=DIRECTION('ref_axis',(0.0960230259076783,0.995379112949198,0.));
#121640=DIRECTION('center_axis',(0.110188686511078,0.993910686814949,-1.38914942345546E-16));
#121641=DIRECTION('ref_axis',(-0.993910686814949,0.110188686511077,1.01689101063646E-31));
#121642=DIRECTION('center_axis',(0.,0.,-1.));
#121643=DIRECTION('ref_axis',(-0.096023025907693,-0.995379112949197,0.));
#121644=DIRECTION('center_axis',(0.,0.,1.));
#121645=DIRECTION('ref_axis',(0.096023025907693,0.995379112949197,0.));
#121646=DIRECTION('center_axis',(0.,0.,1.));
#121647=DIRECTION('ref_axis',(0.096023025907693,0.995379112949197,0.));
#121648=DIRECTION('center_axis',(0.688341848197006,0.292855616919931,0.663642288932205));
#121649=DIRECTION('ref_axis',(0.707348965204713,-0.0682371039617037,-0.703563173472533));
#121650=DIRECTION('center_axis',(0.690321574563952,0.293697893163985,0.661209249211309));
#121651=DIRECTION('ref_axis',(0.705053508433018,-0.0680156640076146,-0.705884848750768));
#121652=DIRECTION('center_axis',(-0.621448576272032,0.420242781980705,-0.661209249211308));
#121653=DIRECTION('ref_axis',(-0.705053508433014,0.0680156640076429,0.70588484875077));
#121654=DIRECTION('center_axis',(-0.619666366100035,0.41903759624314,-0.663642288932184));
#121655=DIRECTION('ref_axis',(-0.707348965204693,0.0682371039617002,0.703563173472553));
#121656=DIRECTION('center_axis',(0.,0.,1.));
#121657=DIRECTION('ref_axis',(0.096023025907693,0.995379112949197,0.));
#121658=DIRECTION('center_axis',(0.,0.,1.));
#121659=DIRECTION('ref_axis',(0.096023025907693,0.995379112949197,0.));
#121660=DIRECTION('center_axis',(0.,0.,1.));
#121661=DIRECTION('ref_axis',(-0.096023025907693,-0.995379112949197,0.));
#121662=DIRECTION('center_axis',(0.,0.,-1.));
#121663=DIRECTION('ref_axis',(0.0960230259076784,0.995379112949199,0.));
#121664=DIRECTION('center_axis',(0.505948052969169,0.862563949917168,0.));
#121665=DIRECTION('ref_axis',(-0.862563949917168,0.505948052969169,0.));
#121666=DIRECTION('',(0.,0.,1.));
#121667=DIRECTION('center_axis',(-0.505952278760923,-0.862561471207359,
2.2859755277705E-6));
#121668=DIRECTION('ref_axis',(0.816525738956301,-0.478948266589601,0.322326349454529));
#121669=DIRECTION('',(0.,0.,-1.));
#121670=DIRECTION('center_axis',(0.449643866412966,-0.893207922824914,0.));
#121671=DIRECTION('ref_axis',(0.893207922824915,0.449643866412966,0.));
#121672=DIRECTION('center_axis',(-0.449643866413041,0.893207922824877,3.75584255351168E-14));
#121673=DIRECTION('ref_axis',(0.892008639742985,0.449040143284211,-0.0518028603762828));
#121674=DIRECTION('',(0.,0.,1.));
#121675=DIRECTION('',(0.,0.,1.));
#121676=DIRECTION('center_axis',(0.,0.,1.));
#121677=DIRECTION('ref_axis',(0.0320515775716322,0.999486216200689,0.));
#121678=DIRECTION('center_axis',(0.,0.,-1.));
#121679=DIRECTION('ref_axis',(-0.0320515775716322,-0.999486216200689,0.));
#121680=DIRECTION('center_axis',(-0.266223150648619,-0.934607477951457,
-0.23586881145234));
#121681=DIRECTION('ref_axis',(-0.655621710048478,0.35495017810224,-0.666461209957712));
#121682=DIRECTION('center_axis',(0.205795659925439,-0.949744202477666,0.235868811452288));
#121683=DIRECTION('ref_axis',(-0.677016400948794,-0.31221506770535,-0.666461209932046));
#121684=DIRECTION('center_axis',(0.,0.,-1.));
#121685=DIRECTION('ref_axis',(-0.0320515775716516,-0.999486216200688,0.));
#121686=DIRECTION('center_axis',(0.0178144386798002,0.999841310296051,-6.76296429840134E-17));
#121687=DIRECTION('ref_axis',(0.999841310296051,-0.0178144386798002,-1.79111484828013E-32));
#121688=DIRECTION('center_axis',(0.,0.,1.));
#121689=DIRECTION('ref_axis',(0.0320515775716516,0.999486216200688,0.));
#121690=DIRECTION('center_axis',(0.0462822156915255,0.998928404096451,-1.38914942345546E-16));
#121691=DIRECTION('ref_axis',(-0.998928404096451,0.0462822156915255,1.84889274661175E-32));
#121692=DIRECTION('center_axis',(0.,0.,-1.));
#121693=DIRECTION('ref_axis',(-0.0320515775716415,-0.999486216200688,0.));
#121694=DIRECTION('center_axis',(0.,0.,1.));
#121695=DIRECTION('ref_axis',(0.0320515775716415,0.999486216200688,0.));
#121696=DIRECTION('center_axis',(0.,0.,1.));
#121697=DIRECTION('ref_axis',(0.0320515775716415,0.999486216200688,0.));
#121698=DIRECTION('center_axis',(0.668164252246806,0.336356127282215,0.663642288932205));
#121699=DIRECTION('ref_axis',(0.710267607154434,-0.0227768997094119,-0.703563173472533));
#121700=DIRECTION('center_axis',(0.670085946229365,0.337323514483224,0.661209249211309));
#121701=DIRECTION('ref_axis',(0.707962678938294,-0.0227029851477806,-0.705884848750767));
#121702=DIRECTION('center_axis',(-0.647096791008741,0.379563001125778,-0.661209249211308));
#121703=DIRECTION('ref_axis',(-0.707962678938293,0.0227029851477993,0.705884848750768));
#121704=DIRECTION('center_axis',(-0.645241026063361,0.378474478169339,-0.663642288932184));
#121705=DIRECTION('ref_axis',(-0.710267607154415,0.022776899709408,0.703563173472553));
#121706=DIRECTION('center_axis',(0.,0.,1.));
#121707=DIRECTION('ref_axis',(0.0320515775716415,0.999486216200688,0.));
#121708=DIRECTION('center_axis',(0.,0.,1.));
#121709=DIRECTION('ref_axis',(0.0320515775716415,0.999486216200688,0.));
#121710=DIRECTION('center_axis',(0.,0.,1.));
#121711=DIRECTION('ref_axis',(-0.0320515775716762,-0.999486216200687,0.));
#121712=DIRECTION('center_axis',(0.,0.,-1.));
#121713=DIRECTION('ref_axis',(0.0320515775716516,0.999486216200688,0.));
#121714=DIRECTION('center_axis',(0.44964386641296,0.893207922824918,0.));
#121715=DIRECTION('ref_axis',(-0.893207922824918,0.44964386641296,0.));
#121716=DIRECTION('',(0.,0.,1.));
#121717=DIRECTION('center_axis',(-0.449648242333896,-0.89320571995527,2.2859755482938E-6));
#121718=DIRECTION('ref_axis',(0.845534420057594,-0.425649232296221,0.322326349440293));
#121719=DIRECTION('',(0.,0.,-1.));
#121720=DIRECTION('center_axis',(0.505948052969176,-0.862563949917164,0.));
#121721=DIRECTION('ref_axis',(0.862563949917164,0.505948052969176,0.));
#121722=DIRECTION('center_axis',(-0.505948052969194,0.862563949917153,-2.04864139282425E-15));
#121723=DIRECTION('ref_axis',(0.861405811563617,0.505268731922799,-0.0518028603993475));
#121724=DIRECTION('',(0.,0.,1.));
#121725=DIRECTION('',(0.,0.,1.));
#121726=DIRECTION('center_axis',(0.,0.,1.));
#121727=DIRECTION('ref_axis',(-0.0320515775716322,0.999486216200689,0.));
#121728=DIRECTION('center_axis',(0.,0.,-1.));
#121729=DIRECTION('ref_axis',(0.0320515775716322,-0.999486216200689,0.));
#121730=DIRECTION('center_axis',(-0.205795659925178,-0.949744202477699,
-0.235868811452383));
#121731=DIRECTION('ref_axis',(-0.677016400935282,0.312215067705664,-0.666461209945624));
#121732=DIRECTION('center_axis',(0.26622315064885,-0.934607477951416,0.235868811452241));
#121733=DIRECTION('ref_axis',(-0.655621710080647,-0.354950178103372,-0.666461209925464));
#121734=DIRECTION('center_axis',(0.,0.,-1.));
#121735=DIRECTION('ref_axis',(0.0320515775716588,-0.999486216200688,0.));
#121736=DIRECTION('center_axis',(-0.0462822156915322,0.998928404096451,
-6.76296429840134E-17));
#121737=DIRECTION('ref_axis',(0.998928404096451,0.0462822156915322,-4.23704587765192E-33));
#121738=DIRECTION('center_axis',(0.,0.,1.));
#121739=DIRECTION('ref_axis',(-0.0320515775716588,0.999486216200688,0.));
#121740=DIRECTION('center_axis',(-0.0178144386798069,0.999841310296051,
-1.38914942345546E-16));
#121741=DIRECTION('ref_axis',(-0.999841310296051,-0.0178144386798069,-7.70371977754894E-33));
#121742=DIRECTION('center_axis',(0.,0.,-1.));
#121743=DIRECTION('ref_axis',(0.0320515775716415,-0.999486216200688,0.));
#121744=DIRECTION('center_axis',(0.,0.,1.));
#121745=DIRECTION('ref_axis',(-0.0320515775716415,0.999486216200688,0.));
#121746=DIRECTION('center_axis',(0.,0.,1.));
#121747=DIRECTION('ref_axis',(-0.0320515775716415,0.999486216200688,0.));
#121748=DIRECTION('center_axis',(0.645241026063342,0.378474478169334,0.663642288932205));
#121749=DIRECTION('ref_axis',(0.710267607154434,0.0227768997094152,-0.703563173472533));
#121750=DIRECTION('center_axis',(0.647096791008737,0.379563001125784,0.661209249211309));
#121751=DIRECTION('ref_axis',(0.707962678938293,0.0227029851478042,-0.705884848750767));
#121752=DIRECTION('center_axis',(-0.670085946229369,0.337323514483218,-0.661209249211308));
#121753=DIRECTION('ref_axis',(-0.707962678938293,-0.0227029851477856,0.705884848750768));
#121754=DIRECTION('center_axis',(-0.668164252246826,0.336356127282219,-0.663642288932184));
#121755=DIRECTION('ref_axis',(-0.710267607154415,-0.0227768997094186,0.703563173472553));
#121756=DIRECTION('center_axis',(0.,0.,1.));
#121757=DIRECTION('ref_axis',(-0.0320515775716415,0.999486216200688,0.));
#121758=DIRECTION('center_axis',(0.,0.,1.));
#121759=DIRECTION('ref_axis',(-0.0320515775716415,0.999486216200688,0.));
#121760=DIRECTION('center_axis',(0.,0.,1.));
#121761=DIRECTION('ref_axis',(0.0320515775716762,-0.999486216200687,0.));
#121762=DIRECTION('center_axis',(0.,0.,-1.));
#121763=DIRECTION('ref_axis',(-0.0320515775716588,0.999486216200688,0.));
#121764=DIRECTION('center_axis',(0.391491996761353,0.920181512785281,0.));
#121765=DIRECTION('ref_axis',(-0.920181512785281,0.391491996761353,0.));
#121766=DIRECTION('',(0.,0.,1.));
#121767=DIRECTION('center_axis',(-0.391496504829856,-0.920179594807873,
2.2859755625072E-6));
#121768=DIRECTION('ref_axis',(0.871068618844222,-0.370601113998325,0.322326349478321));
#121769=DIRECTION('',(0.,0.,-1.));
#121770=DIRECTION('center_axis',(0.560173190450217,-0.828375516719817,0.));
#121771=DIRECTION('ref_axis',(0.828375516719818,0.560173190450217,0.));
#121772=DIRECTION('center_axis',(-0.560173190450193,0.828375516719834,-6.33561319632668E-15));
#121773=DIRECTION('ref_axis',(0.827263282131017,0.559421062960219,-0.0518028604835341));
#121774=DIRECTION('',(0.,0.,1.));
#121775=DIRECTION('',(0.,0.,1.));
#121776=DIRECTION('center_axis',(0.,0.,1.));
#121777=DIRECTION('ref_axis',(-0.096023025907694,0.995379112949197,0.));
#121778=DIRECTION('center_axis',(0.,0.,-1.));
#121779=DIRECTION('ref_axis',(0.096023025907694,-0.995379112949197,0.));
#121780=DIRECTION('center_axis',(-0.144522510692369,-0.960978224356437,
-0.235868811452306));
#121781=DIRECTION('ref_axis',(-0.69562908620194,0.268196998625411,-0.666461209942616));
#121782=DIRECTION('center_axis',(0.325556673341202,-0.915630250825664,0.235868811452345));
#121783=DIRECTION('ref_axis',(-0.631532928959424,-0.396226722082146,-0.666461209934958));
#121784=DIRECTION('center_axis',(0.,0.,-1.));
#121785=DIRECTION('ref_axis',(0.0960230259076855,-0.995379112949198,0.));
#121786=DIRECTION('center_axis',(-0.110188686511084,0.993910686814948,-6.76296429840134E-17));
#121787=DIRECTION('ref_axis',(0.993910686814948,0.110188686511084,-1.14015052707724E-31));
#121788=DIRECTION('center_axis',(0.,0.,1.));
#121789=DIRECTION('ref_axis',(-0.0960230259076855,0.995379112949198,0.));
#121790=DIRECTION('center_axis',(-0.0818378897014191,0.996645654086355,
-1.38914942345546E-16));
#121791=DIRECTION('ref_axis',(-0.996645654086355,-0.0818378897014191,-4.46815747097839E-32));
#121792=DIRECTION('center_axis',(0.,0.,-1.));
#121793=DIRECTION('ref_axis',(0.096023025907693,-0.995379112949197,0.));
#121794=DIRECTION('center_axis',(0.,0.,1.));
#121795=DIRECTION('ref_axis',(-0.096023025907693,0.995379112949197,0.));
#121796=DIRECTION('center_axis',(0.,0.,1.));
#121797=DIRECTION('ref_axis',(-0.096023025907693,0.995379112949197,0.));
#121798=DIRECTION('center_axis',(0.619666366100017,0.419037596243134,0.663642288932205));
#121799=DIRECTION('ref_axis',(0.707348965204713,0.0682371039617049,-0.703563173472533));
#121800=DIRECTION('center_axis',(0.621448576272028,0.42024278198071,0.661209249211309));
#121801=DIRECTION('ref_axis',(0.705053508433015,0.0680156640076478,-0.705884848750769));
#121802=DIRECTION('center_axis',(-0.690321574563955,0.293697893163979,-0.661209249211308));
#121803=DIRECTION('ref_axis',(-0.705053508433017,-0.0680156640076214,0.705884848750769));
#121804=DIRECTION('center_axis',(-0.688341848197026,0.292855616919933,-0.663642288932184));
#121805=DIRECTION('ref_axis',(-0.707348965204693,-0.0682371039617086,0.703563173472553));
#121806=DIRECTION('center_axis',(0.,0.,1.));
#121807=DIRECTION('ref_axis',(-0.0960230259076933,0.995379112949197,0.));
#121808=DIRECTION('center_axis',(0.,0.,1.));
#121809=DIRECTION('ref_axis',(-0.0960230259076933,0.995379112949197,0.));
#121810=DIRECTION('center_axis',(0.,0.,1.));
#121811=DIRECTION('ref_axis',(0.0960230259076933,-0.995379112949197,0.));
#121812=DIRECTION('center_axis',(0.,0.,-1.));
#121813=DIRECTION('ref_axis',(-0.0960230259076855,0.995379112949198,0.));
#121814=DIRECTION('center_axis',(0.331731402520283,0.943373879531295,0.));
#121815=DIRECTION('ref_axis',(-0.943373879531295,0.331731402520284,0.));
#121816=DIRECTION('',(0.,0.,1.));
#121817=DIRECTION('center_axis',(-0.3317360242117,-0.943372254327521,2.28597555787171E-6));
#121818=DIRECTION('ref_axis',(0.893023409830886,-0.314030116230518,0.322326349519031));
#121819=DIRECTION('',(0.,0.,-1.));
#121820=DIRECTION('center_axis',(0.612096456134927,-0.790783110838278,0.));
#121821=DIRECTION('ref_axis',(0.790783110838278,0.612096456134927,0.));
#121822=DIRECTION('center_axis',(-0.612096456134829,0.790783110838353,-6.21041844454129E-14));
#121823=DIRECTION('ref_axis',(0.789721350430635,0.611274612858304,-0.0518028604320807));
#121824=DIRECTION('',(0.,0.,1.));
#121825=DIRECTION('',(0.,0.,1.));
#121826=DIRECTION('center_axis',(0.,0.,1.));
#121827=DIRECTION('ref_axis',(-0.159599895033413,0.987181783414445,0.));
#121828=DIRECTION('center_axis',(0.,0.,-1.));
#121829=DIRECTION('ref_axis',(0.159599895033413,-0.987181783414445,0.));
#121830=DIRECTION('center_axis',(-0.0826554874628396,-0.968263380582128,
-0.235868811452362));
#121831=DIRECTION('ref_axis',(0.71138328233753,-0.223076850549854,0.666461209943565));
#121832=DIRECTION('center_axis',(0.383552413831417,-0.89289050259713,0.235868811452339));
#121833=DIRECTION('ref_axis',(-0.604849043557018,-0.435875085466386,-0.666461209957362));
#121834=DIRECTION('center_axis',(0.,0.,-1.));
#121835=DIRECTION('ref_axis',(0.159599895033383,-0.98718178341445,0.));
#121836=DIRECTION('center_axis',(-0.173642368382363,0.984808777328149,-6.76296429840134E-17));
#121837=DIRECTION('ref_axis',(0.984808777328149,0.173642368382363,-2.77333911991762E-32));
#121838=DIRECTION('center_axis',(0.,0.,1.));
#121839=DIRECTION('ref_axis',(-0.159599895033383,0.98718178341445,0.));
#121840=DIRECTION('center_axis',(-0.145525051280076,0.989354567104196,-1.38914942345546E-16));
#121841=DIRECTION('ref_axis',(-0.989354567104196,-0.145525051280076,8.93631494195677E-32));
#121842=DIRECTION('center_axis',(0.,0.,-1.));
#121843=DIRECTION('ref_axis',(0.159599895033397,-0.987181783414447,0.));
#121844=DIRECTION('center_axis',(0.,0.,1.));
#121845=DIRECTION('ref_axis',(-0.159599895033397,0.987181783414447,0.));
#121846=DIRECTION('center_axis',(0.,0.,1.));
#121847=DIRECTION('ref_axis',(-0.159599895033397,0.987181783414447,0.));
#121848=DIRECTION('center_axis',(0.591545364120368,0.457878798950688,0.663642288932205));
#121849=DIRECTION('ref_axis',(0.701523674631087,0.113416907317007,-0.703563173472533));
#121850=DIRECTION('center_axis',(0.593246696035115,0.459195695102684,0.661209249211309));
#121851=DIRECTION('ref_axis',(0.699247121828084,0.113048851914762,-0.705884848750768));
#121852=DIRECTION('center_axis',(-0.707720523475145,0.248865404203728,-0.661209249211308));
#121853=DIRECTION('ref_axis',(-0.699247121828087,-0.113048851914738,0.705884848750768));
#121854=DIRECTION('center_axis',(-0.705690899844121,0.248151700010391,-0.663642288932184));
#121855=DIRECTION('ref_axis',(-0.701523674631068,-0.113416907317008,0.703563173472553));
#121856=DIRECTION('center_axis',(0.,0.,1.));
#121857=DIRECTION('ref_axis',(-0.159599895033397,0.987181783414447,0.));
#121858=DIRECTION('center_axis',(0.,0.,1.));
#121859=DIRECTION('ref_axis',(-0.159599895033397,0.987181783414447,0.));
#121860=DIRECTION('center_axis',(0.,0.,1.));
#121861=DIRECTION('ref_axis',(0.159599895033398,-0.987181783414447,0.));
#121862=DIRECTION('center_axis',(0.,0.,-1.));
#121863=DIRECTION('ref_axis',(-0.159599895033383,0.98718178341445,0.));
#121864=DIRECTION('center_axis',(0.270607652790095,0.962689720653251,0.));
#121865=DIRECTION('ref_axis',(-0.962689720653251,0.270607652790095,0.));
#121866=DIRECTION('',(0.,0.,1.));
#121867=DIRECTION('center_axis',(-0.270612369112877,-0.962688394901429,
2.28597555201867E-6));
#121868=DIRECTION('ref_axis',(0.911308576098357,-0.256168701364635,0.322326349482542));
#121869=DIRECTION('',(0.,0.,-1.));
#121870=DIRECTION('center_axis',(0.6615044861871,-0.749941207531858,0.));
#121871=DIRECTION('ref_axis',(0.749941207531858,0.6615044861871,0.));
#121872=DIRECTION('center_axis',(-0.661504486187023,0.749941207531925,-4.90156422134779E-14));
#121873=DIRECTION('ref_axis',(0.748934284302182,0.660616304250847,-0.0518028604879182));
#121874=DIRECTION('',(0.,0.,1.));
#121875=DIRECTION('',(0.,0.,1.));
#121876=DIRECTION('center_axis',(0.,0.,1.));
#121877=DIRECTION('ref_axis',(-0.222520933956302,0.974927912181827,0.));
#121878=DIRECTION('center_axis',(0.,0.,-1.));
#121879=DIRECTION('ref_axis',(0.222520933956302,-0.974927912181827,0.));
#121880=DIRECTION('center_axis',(-0.0204488151059326,-0.97156973488516,
-0.23586881145235));
#121881=DIRECTION('ref_axis',(0.724214251965761,-0.177040031847786,0.666461209953744));
#121882=DIRECTION('center_axis',(0.439972055181631,-0.866481675768945,0.235868811452243));
#121883=DIRECTION('ref_axis',(-0.575679703738258,-0.473732344636557,-0.666461209935718));
#121884=DIRECTION('center_axis',(0.,0.,-1.));
#121885=DIRECTION('ref_axis',(0.222520933956318,-0.974927912181823,0.));
#121886=DIRECTION('center_axis',(-0.236382516515787,0.971660077334488,-6.76296429840134E-17));
#121887=DIRECTION('ref_axis',(0.971660077334488,0.236382516515787,6.93889390390725E-14));
#121888=DIRECTION('center_axis',(0.,0.,1.));
#121889=DIRECTION('ref_axis',(-0.222520933956318,0.974927912181823,0.));
#121890=DIRECTION('center_axis',(-0.208614219207997,0.977998009989917,-1.38914942345546E-16));
#121891=DIRECTION('ref_axis',(-0.977998009989917,-0.208614219207997,-3.26637718568075E-31));
#121892=DIRECTION('center_axis',(0.,0.,-1.));
#121893=DIRECTION('ref_axis',(0.222520933956319,-0.974927912181823,0.));
#121894=DIRECTION('center_axis',(0.,0.,1.));
#121895=DIRECTION('ref_axis',(-0.222520933956319,0.974927912181823,0.));
#121896=DIRECTION('center_axis',(0.,0.,1.));
#121897=DIRECTION('ref_axis',(-0.222520933956319,0.974927912181823,0.));
#121898=DIRECTION('center_axis',(0.560993575353466,0.49483847945866,0.663642288932205));
#121899=DIRECTION('ref_axis',(0.69281567280205,0.158130656272286,-0.703563173472532));
#121900=DIRECTION('center_axis',(0.562607037873177,0.496261674616312,0.661209249211309));
#121901=DIRECTION('ref_axis',(0.690567378811527,0.157617497840452,-0.705884848750767));
#121902=DIRECTION('center_axis',(-0.722211296949799,0.203010273916143,-0.661209249211308));
#121903=DIRECTION('ref_axis',(-0.690567378811529,-0.157617497840433,0.705884848750769));
#121904=DIRECTION('center_axis',(-0.720140116213533,0.202428074537133,-0.663642288932184));
#121905=DIRECTION('ref_axis',(-0.692815672802027,-0.15813065627229,0.703563173472553));
#121906=DIRECTION('center_axis',(0.,0.,1.));
#121907=DIRECTION('ref_axis',(-0.222520933956319,0.974927912181823,0.));
#121908=DIRECTION('center_axis',(0.,0.,1.));
#121909=DIRECTION('ref_axis',(-0.222520933956319,0.974927912181823,0.));
#121910=DIRECTION('center_axis',(0.,0.,1.));
#121911=DIRECTION('ref_axis',(0.222520933956321,-0.974927912181822,0.));
#121912=DIRECTION('center_axis',(0.,0.,-1.));
#121913=DIRECTION('ref_axis',(-0.222520933956318,0.974927912181823,0.));
#121914=DIRECTION('center_axis',(0.208371918169433,0.978049663216746,0.));
#121915=DIRECTION('ref_axis',(-0.978049663216746,0.208371918169433,0.));
#121916=DIRECTION('',(0.,0.,1.));
#121917=DIRECTION('center_axis',(-0.208376709743311,-0.978048642364646,
2.28597557508953E-6));
#121918=DIRECTION('ref_axis',(0.925848979922217,-0.197254634349058,0.322326349535389));
#121919=DIRECTION('',(0.,0.,-1.));
#121920=DIRECTION('center_axis',(0.708194252413262,-0.706017634941805,0.));
#121921=DIRECTION('ref_axis',(0.706017634941806,0.708194252413262,0.));
#121922=DIRECTION('center_axis',(-0.708194252413266,0.706017634941802,-2.92121087495308E-15));
#121923=DIRECTION('ref_axis',(0.705069686558799,0.707243381552254,-0.0518028604075977));
#121924=DIRECTION('',(0.,0.,1.));
#121925=DIRECTION('',(0.,0.,1.));
#121926=DIRECTION('center_axis',(0.,0.,1.));
#121927=DIRECTION('ref_axis',(-0.28452758663103,0.958667853036661,0.));
#121928=DIRECTION('center_axis',(0.,0.,-1.));
#121929=DIRECTION('ref_axis',(0.28452758663103,-0.958667853036661,0.));
#121930=DIRECTION('center_axis',(0.0418418858184,-0.97088370074651,-0.235868811452302));
#121931=DIRECTION('ref_axis',(0.734069269914698,-0.130275717673731,0.666461209937605));
#121932=DIRECTION('center_axis',(0.494583756983124,-0.83651228987538,0.23586881145227));
#121933=DIRECTION('ref_axis',(-0.544144772508376,-0.509642935982521,-0.666461209940176));
#121934=DIRECTION('center_axis',(0.,0.,-1.));
#121935=DIRECTION('ref_axis',(0.284527586631037,-0.958667853036659,0.));
#121936=DIRECTION('center_axis',(-0.298151318184958,0.954518617662627,-6.76296429840134E-17));
#121937=DIRECTION('ref_axis',(0.954518617662627,0.298151318184958,6.93889390390724E-14));
#121938=DIRECTION('center_axis',(0.,0.,1.));
#121939=DIRECTION('ref_axis',(-0.284527586631037,0.958667853036659,0.));
#121940=DIRECTION('center_axis',(-0.270846146561583,0.962622649272674,-1.38914942345546E-16));
#121941=DIRECTION('ref_axis',(-0.962622649272674,-0.270846146561583,-3.57452597678271E-31));
#121942=DIRECTION('center_axis',(0.,0.,-1.));
#121943=DIRECTION('ref_axis',(0.284527586631029,-0.958667853036662,0.));
#121944=DIRECTION('center_axis',(0.,0.,1.));
#121945=DIRECTION('ref_axis',(-0.284527586631029,0.958667853036662,0.));
#121946=DIRECTION('center_axis',(0.,0.,1.));
#121947=DIRECTION('ref_axis',(-0.284527586631029,0.958667853036662,0.));
#121948=DIRECTION('center_axis',(0.528136543652692,0.529764762512015,0.663642288932205));
#121949=DIRECTION('ref_axis',(0.681260742764965,0.202194612442036,-0.703563173472534));
#121950=DIRECTION('center_axis',(0.529655506713787,0.531288408461147,0.661209249211309));
#121951=DIRECTION('ref_axis',(0.67904994630919,0.201538459658677,-0.705884848750768));
#121952=DIRECTION('center_axis',(-0.733734349291449,0.156320930867469,-0.661209249211308));
#121953=DIRECTION('ref_axis',(-0.679049946309195,-0.201538459658659,0.705884848750768));
#121954=DIRECTION('center_axis',(-0.731630122375853,0.155872628684916,-0.663642288932184));
#121955=DIRECTION('ref_axis',(-0.681260742764947,-0.202194612442032,0.703563173472552));
#121956=DIRECTION('center_axis',(0.,0.,1.));
#121957=DIRECTION('ref_axis',(-0.284527586631029,0.958667853036662,0.));
#121958=DIRECTION('center_axis',(0.,0.,1.));
#121959=DIRECTION('ref_axis',(-0.284527586631029,0.958667853036662,0.));
#121960=DIRECTION('center_axis',(0.,0.,1.));
#121961=DIRECTION('ref_axis',(0.284527586631029,-0.958667853036662,0.));
#121962=DIRECTION('center_axis',(0.,0.,-1.));
#121963=DIRECTION('ref_axis',(-0.284527586631037,0.958667853036659,0.));
#121964=DIRECTION('center_axis',(0.145279938641377,0.989390589923089,0.));
#121965=DIRECTION('ref_axis',(-0.989390589923089,0.145279938641377,0.));
#121966=DIRECTION('',(0.,0.,1.));
#121967=DIRECTION('center_axis',(-0.145284785776656,-0.989389878165633,
2.28597556942582E-6));
#121968=DIRECTION('ref_axis',(0.936584871683996,-0.137530005730791,0.322326349615356));
#121969=DIRECTION('',(0.,0.,-1.));
#121970=DIRECTION('center_axis',(0.751973896549068,-0.65919288444947,0.));
#121971=DIRECTION('ref_axis',(0.65919288444947,0.751973896549068,0.));
#121972=DIRECTION('center_axis',(-0.751973896549116,0.659192884449415,4.84465751599405E-14));
#121973=DIRECTION('ref_axis',(0.65830780623392,0.750964244093583,-0.0518028603885764));
#121974=DIRECTION('',(0.,0.,1.));
#121975=DIRECTION('',(0.,0.,1.));
#121976=DIRECTION('center_axis',(0.,0.,1.));
#121977=DIRECTION('ref_axis',(-0.345365054421307,0.938468422049761,0.));
#121978=DIRECTION('center_axis',(0.,0.,-1.));
#121979=DIRECTION('ref_axis',(0.345365054421307,-0.938468422049761,0.));
#121980=DIRECTION('center_axis',(0.103960649458841,-0.966208097227613,-0.235868811452239));
#121981=DIRECTION('ref_axis',(0.740907839753173,-0.0829760726379692,0.666461209945384));
#121982=DIRECTION('center_axis',(0.547163108039461,-0.803105495551311,0.235868811452214));
#121983=DIRECTION('ref_axis',(-0.510373833702409,-0.543459295190668,-0.666461209931056));
#121984=DIRECTION('center_axis',(0.,0.,-1.));
#121985=DIRECTION('ref_axis',(0.345365054421312,-0.938468422049759,0.));
#121986=DIRECTION('center_axis',(-0.358694952134449,0.933454836247189,-6.76296429840134E-17));
#121987=DIRECTION('ref_axis',(0.933454836247189,0.358694952134449,-3.75941525144388E-31));
#121988=DIRECTION('center_axis',(0.,0.,1.));
#121989=DIRECTION('ref_axis',(-0.345365054421312,0.938468422049759,0.));
#121990=DIRECTION('center_axis',(-0.331965109002631,0.943291665607659,-1.38914942345546E-16));
#121991=DIRECTION('ref_axis',(-0.943291665607659,-0.331965109002631,-1.04770588974666E-31));
#121992=DIRECTION('center_axis',(0.,0.,-1.));
#121993=DIRECTION('ref_axis',(0.345365054421309,-0.93846842204976,0.));
#121994=DIRECTION('center_axis',(0.,0.,1.));
#121995=DIRECTION('ref_axis',(-0.345365054421309,0.93846842204976,0.));
#121996=DIRECTION('center_axis',(0.,0.,1.));
#121997=DIRECTION('ref_axis',(-0.345365054421309,0.93846842204976,0.));
#121998=DIRECTION('center_axis',(0.493109285609116,0.562514128522023,0.663642288932205));
#121999=DIRECTION('ref_axis',(0.666906366205898,0.245427707578637,-0.703563173472532));
#122000=DIRECTION('center_axis',(0.49452750746656,0.564131964274609,0.661209249211309));
#122001=DIRECTION('ref_axis',(0.664742151921717,0.244631256716292,-0.705884848750766));
#122002=DIRECTION('center_axis',(-0.742242329806336,0.108989231583126,-0.661209249211308));
#122003=DIRECTION('ref_axis',(-0.66474215192172,-0.244631256716279,0.705884848750768));
#122004=DIRECTION('center_axis',(-0.740113703431162,0.108676668766859,-0.663642288932184));
#122005=DIRECTION('ref_axis',(-0.666906366205875,-0.245427707578641,0.703563173472552));
#122006=DIRECTION('center_axis',(0.,0.,1.));
#122007=DIRECTION('ref_axis',(-0.345365054421309,0.93846842204976,0.));
#122008=DIRECTION('center_axis',(0.,0.,1.));
#122009=DIRECTION('ref_axis',(-0.345365054421309,0.93846842204976,0.));
#122010=DIRECTION('center_axis',(0.,0.,1.));
#122011=DIRECTION('ref_axis',(0.345365054421309,-0.93846842204976,0.));
#122012=DIRECTION('center_axis',(0.,0.,-1.));
#122013=DIRECTION('ref_axis',(-0.345365054421312,0.938468422049759,0.));
#122014=DIRECTION('center_axis',(0.0815909726829938,0.996665898471821,0.));
#122015=DIRECTION('ref_axis',(-0.996665898471821,0.0815909726829938,0.));
#122016=DIRECTION('',(0.,0.,1.));
#122017=DIRECTION('center_axis',(-0.0815958554616844,-0.996665498733778,
2.28597552385516E-6));
#122018=DIRECTION('ref_axis',(0.943472135393123,-0.0772402368290282,0.32232634945244));
#122019=DIRECTION('',(0.,0.,-1.));
#122020=DIRECTION('center_axis',(0.792663518646059,-0.6096593689985,0.));
#122021=DIRECTION('ref_axis',(0.6096593689985,0.792663518646059,0.));
#122022=DIRECTION('center_axis',(-0.792663518646146,0.609659368998387,6.460807948113E-14));
#122023=DIRECTION('ref_axis',(0.608840797925512,0.791599233473346,-0.0518028604020782));
#122024=DIRECTION('',(0.,0.,1.));
#122025=DIRECTION('',(0.,0.,1.));
#122026=DIRECTION('center_axis',(0.,0.,1.));
#122027=DIRECTION('ref_axis',(-0.40478334312238,0.914412623015818,0.));
#122028=DIRECTION('center_axis',(0.,0.,-1.));
#122029=DIRECTION('ref_axis',(0.40478334312238,-0.914412623015818,0.));
#122030=DIRECTION('center_axis',(0.165652216491651,-0.957562137386107,-0.235868811452371));
#122031=DIRECTION('ref_axis',(0.744701860353997,-0.0353354611222299,0.666461209953419));
#122032=DIRECTION('center_axis',(0.597494048518655,-0.76639856848047,0.235868811452201));
#122033=DIRECTION('ref_axis',(-0.474505659311357,-0.575042463572249,-0.666461209951677));
#122034=DIRECTION('center_axis',(0.,0.,-1.));
#122035=DIRECTION('ref_axis',(0.404783343122398,-0.914412623015811,0.));
#122036=DIRECTION('center_axis',(-0.417764631585793,0.908555288684176,-6.76296429840134E-17));
#122037=DIRECTION('ref_axis',(0.908555288684176,0.417764631585793,-1.72563323017096E-31));
#122038=DIRECTION('center_axis',(0.,0.,1.));
#122039=DIRECTION('ref_axis',(-0.404783343122398,0.914412623015811,0.));
#122040=DIRECTION('center_axis',(-0.391719955604495,0.920084494153234,-1.38914942345546E-16));
#122041=DIRECTION('ref_axis',(-0.920084494153234,-0.391719955604495,-5.97808654737798E-31));
#122042=DIRECTION('center_axis',(0.,0.,-1.));
#122043=DIRECTION('ref_axis',(0.40478334312241,-0.914412623015806,0.));
#122044=DIRECTION('center_axis',(0.,0.,1.));
#122045=DIRECTION('ref_axis',(-0.40478334312241,0.914412623015806,0.));
#122046=DIRECTION('center_axis',(0.,0.,1.));
#122047=DIRECTION('ref_axis',(-0.40478334312241,0.914412623015806,0.));
#122048=DIRECTION('center_axis',(0.456055735739362,0.592952003319032,0.663642288932205));
#122049=DIRECTION('ref_axis',(0.64981152833712,0.287652287620727,-0.703563173472531));
#122050=DIRECTION('center_axis',(0.457367388615335,0.59465738084094,0.661209249211309));
#122051=DIRECTION('ref_axis',(0.647702789445247,0.286718811466831,-0.705884848750768));
#122052=DIRECTION('center_axis',(-0.747700277377569,0.0612096721680909,
-0.661209249211308));
#122053=DIRECTION('ref_axis',(-0.647702789445254,-0.286718811466814,0.705884848750768));
#122054=DIRECTION('center_axis',(-0.745555998525181,0.0610341331057666,
-0.663642288932184));
#122055=DIRECTION('ref_axis',(-0.649811528337097,-0.287652287620724,0.703563173472554));
#122056=DIRECTION('center_axis',(0.,0.,1.));
#122057=DIRECTION('ref_axis',(-0.40478334312241,0.914412623015806,0.));
#122058=DIRECTION('center_axis',(0.,0.,1.));
#122059=DIRECTION('ref_axis',(-0.40478334312241,0.914412623015806,0.));
#122060=DIRECTION('center_axis',(0.,0.,1.));
#122061=DIRECTION('ref_axis',(0.40478334312241,-0.914412623015806,0.));
#122062=DIRECTION('center_axis',(0.,0.,-1.));
#122063=DIRECTION('ref_axis',(-0.404783343122398,0.914412623015811,0.));
#122064=DIRECTION('center_axis',(0.0175667319166475,0.999845693059568,0.));
#122065=DIRECTION('ref_axis',(-0.999845693059568,0.0175667319166475,0.));
#122066=DIRECTION('',(0.,0.,1.));
#122067=DIRECTION('center_axis',(-0.0175716302745147,-0.999845606983533,
2.28597556281515E-6));
#122068=DIRECTION('ref_axis',(0.94648246962262,-0.0166330712173982,0.322326349588338));
#122069=DIRECTION('',(0.,0.,-1.));
#122070=DIRECTION('center_axis',(0.830095916319141,-0.557620632428791,0.));
#122071=DIRECTION('ref_axis',(0.557620632428791,0.830095916319141,0.));
#122072=DIRECTION('center_axis',(-0.830095916319178,0.557620632428737,3.49407170887273E-14));
#122073=DIRECTION('ref_axis',(0.55687193218257,0.828981371804959,-0.0518028604192842));
#122074=DIRECTION('',(0.,0.,1.));
#122075=DIRECTION('',(0.,0.,1.));
#122076=DIRECTION('center_axis',(0.,0.,1.));
#122077=DIRECTION('ref_axis',(-0.46253829024085,0.886599306372992,0.));
#122078=DIRECTION('center_axis',(0.,0.,-1.));
#122079=DIRECTION('ref_axis',(0.46253829024085,-0.886599306372992,0.));
#122080=DIRECTION('center_axis',(0.226663083033865,-0.944981349325845,-0.235868811452232));
#122081=DIRECTION('ref_axis',(0.745435741288701,0.0124503513895636,0.666461209943716));
#122082=DIRECTION('center_axis',(0.645369757790216,-0.726542345299901,0.235868811452294));
#122083=DIRECTION('ref_axis',(-0.43668763941582,-0.604262659137769,-0.666461209938876));
#122084=DIRECTION('center_axis',(0.,0.,-1.));
#122085=DIRECTION('ref_axis',(0.462538290240839,-0.886599306372998,0.));
#122086=DIRECTION('center_axis',(-0.47511762655572,0.879922292555462,-6.76296429840134E-17));
#122087=DIRECTION('ref_axis',(0.879922292555462,0.47511762655572,0.));
#122088=DIRECTION('center_axis',(0.,0.,1.));
#122089=DIRECTION('ref_axis',(-0.462538290240839,0.886599306372998,0.));
#122090=DIRECTION('center_axis',(-0.449865140885113,0.893096498154828,-1.38914942345546E-16));
#122091=DIRECTION('ref_axis',(-0.893096498154828,-0.449865140885113,-1.09700969632297E-30));
#122092=DIRECTION('center_axis',(0.,0.,-1.));
#122093=DIRECTION('ref_axis',(0.46253829024085,-0.886599306372993,0.));
#122094=DIRECTION('center_axis',(0.,0.,1.));
#122095=DIRECTION('ref_axis',(-0.46253829024085,0.886599306372993,0.));
#122096=DIRECTION('center_axis',(0.,0.,1.));
#122097=DIRECTION('ref_axis',(-0.46253829024085,0.886599306372993,0.));
#122098=DIRECTION('center_axis',(0.417128155027806,0.620953311146597,0.663642288932205));
#122099=DIRECTION('ref_axis',(0.630046475514269,0.32869484271176,-0.703563173472531));
#122100=DIRECTION('center_axis',(0.418327849059292,0.622739222675787,0.661209249211309));
#122101=DIRECTION('ref_axis',(0.628001877275144,0.327628177120047,-0.705884848750765));
#122102=DIRECTION('center_axis',(-0.75008576412785,0.0131785890806838,-0.661209249211308));
#122103=DIRECTION('ref_axis',(-0.628001877275147,-0.327628177120031,0.70588484875077));
#122104=DIRECTION('center_axis',(-0.747934644099999,0.013140795099962,-0.663642288932184));
#122105=DIRECTION('ref_axis',(-0.630046475514242,-0.328694842711771,0.70356317347255));
#122106=DIRECTION('center_axis',(0.,0.,1.));
#122107=DIRECTION('ref_axis',(-0.46253829024085,0.886599306372993,0.));
#122108=DIRECTION('center_axis',(0.,0.,1.));
#122109=DIRECTION('ref_axis',(-0.46253829024085,0.886599306372993,0.));
#122110=DIRECTION('center_axis',(0.,0.,1.));
#122111=DIRECTION('ref_axis',(0.46253829024085,-0.886599306372993,0.));
#122112=DIRECTION('center_axis',(0.,0.,-1.));
#122113=DIRECTION('ref_axis',(-0.462538290240839,0.886599306372998,0.));
#122114=DIRECTION('center_axis',(-0.0465296943191963,0.998916907228305,
0.));
#122115=DIRECTION('ref_axis',(-0.998916907228305,-0.0465296943191963,0.));
#122116=DIRECTION('',(0.,0.,1.));
#122117=DIRECTION('center_axis',(0.0465248005106162,-0.998917135167989,
2.28597555794753E-6));
#122118=DIRECTION('ref_axis',(0.945603504443602,0.0440424432494455,0.322326349491626));
#122119=DIRECTION('',(0.,0.,-1.));
#122120=DIRECTION('center_axis',(0.864117271817053,-0.503290513071182,0.));
#122121=DIRECTION('ref_axis',(0.503290513071182,0.864117271817053,0.));
#122122=DIRECTION('center_axis',(-0.864117271817065,0.503290513071162,2.12451699996577E-15));
#122123=DIRECTION('ref_axis',(0.502614760223245,0.862957047866487,-0.0518028603774638));
#122124=DIRECTION('',(0.,0.,1.));
#122125=DIRECTION('',(0.,0.,1.));
#122126=DIRECTION('center_axis',(0.,0.,1.));
#122127=DIRECTION('ref_axis',(-0.518392568310538,0.855142763005338,0.));
#122128=DIRECTION('center_axis',(0.,0.,-1.));
#122129=DIRECTION('ref_axis',(0.518392568310538,-0.855142763005338,0.));
#122130=DIRECTION('center_axis',(0.286742542349545,-0.928517430203101,-0.235868811452362));
#122131=DIRECTION('ref_axis',(0.743106466856502,0.0601850027323955,0.666461209945596));
#122132=DIRECTION('center_axis',(0.690593504295839,-0.683700603779519,0.235868811452288));
#122133=DIRECTION('ref_axis',(-0.397075176330132,-0.630999809818572,-0.666461209937473));
#122134=DIRECTION('center_axis',(0.,0.,-1.));
#122135=DIRECTION('ref_axis',(0.518392568310529,-0.855142763005344,0.));
#122136=DIRECTION('center_axis',(-0.530518261285717,0.847673506983898,-6.76296429840134E-17));
#122137=DIRECTION('ref_axis',(0.847673506983898,0.530518261285717,7.39557098644698E-32));
#122138=DIRECTION('center_axis',(0.,0.,1.));
#122139=DIRECTION('ref_axis',(-0.518392568310529,0.855142763005344,0.));
#122140=DIRECTION('center_axis',(-0.506161733806064,0.862438577076907,-1.38914942345546E-16));
#122141=DIRECTION('ref_axis',(-0.862438577076907,-0.506161733806063,-1.23259516440783E-30));
#122142=DIRECTION('center_axis',(0.,0.,-1.));
#122143=DIRECTION('ref_axis',(0.518392568310539,-0.855142763005338,0.));
#122144=DIRECTION('center_axis',(0.,0.,1.));
#122145=DIRECTION('ref_axis',(-0.518392568310539,0.855142763005338,0.));
#122146=DIRECTION('center_axis',(0.,0.,1.));
#122147=DIRECTION('ref_axis',(-0.518392568310539,0.855142763005338,0.));
#122148=DIRECTION('center_axis',(0.376486505253533,0.646402988624593,0.663642288932205));
#122149=DIRECTION('ref_axis',(0.607692426578987,0.368386720189267,-0.70356317347253));
#122150=DIRECTION('center_axis',(0.377569310640423,0.648262095467515,0.661209249211309));
#122151=DIRECTION('ref_axis',(0.605720370685325,0.367191248317467,-0.705884848750767));
#122152=DIRECTION('center_axis',(-0.749388987580438,-0.0349066476560543,
-0.661209249211308));
#122153=DIRECTION('ref_axis',(-0.605720370685332,-0.367191248317453,0.705884848750768));
#122154=DIRECTION('center_axis',(-0.747239865790733,-0.0348065412516,-0.663642288932184));
#122155=DIRECTION('ref_axis',(-0.607692426578961,-0.368386720189264,0.703563173472554));
#122156=DIRECTION('center_axis',(0.,0.,1.));
#122157=DIRECTION('ref_axis',(-0.518392568310539,0.855142763005338,0.));
#122158=DIRECTION('center_axis',(0.,0.,1.));
#122159=DIRECTION('ref_axis',(-0.518392568310539,0.855142763005338,0.));
#122160=DIRECTION('center_axis',(0.,0.,1.));
#122161=DIRECTION('ref_axis',(0.51839256831058,-0.855142763005313,0.));
#122162=DIRECTION('center_axis',(0.,0.,-1.));
#122163=DIRECTION('ref_axis',(-0.518392568310529,0.855142763005344,0.));
#122164=DIRECTION('center_axis',(-0.110434920060495,0.993883357558236,0.));
#122165=DIRECTION('ref_axis',(-0.993883357558236,-0.110434920060495,0.));
#122166=DIRECTION('',(0.,0.,1.));
#122167=DIRECTION('center_axis',(0.110430050911002,-0.993883898576976,2.28597551807898E-6));
#122168=DIRECTION('ref_axis',(0.940838851618515,0.10453697787255,0.322326349438621));
#122169=DIRECTION('',(0.,0.,-1.));
#122170=DIRECTION('center_axis',(0.894587784092495,-0.446892265039887,0.));
#122171=DIRECTION('ref_axis',(0.446892265039887,0.894587784092495,0.));
#122172=DIRECTION('center_axis',(-0.894587784092469,0.446892265039938,-2.3976691856752E-14));
#122173=DIRECTION('ref_axis',(0.446292236401057,0.893386648309996,-0.0518028604381615));
#122174=DIRECTION('',(0.,0.,1.));
#122175=DIRECTION('',(0.,0.,1.));
#122176=DIRECTION('center_axis',(0.,0.,1.));
#122177=DIRECTION('ref_axis',(-0.572116660122175,0.820172254596952,0.));
#122178=DIRECTION('center_axis',(0.,0.,-1.));
#122179=DIRECTION('ref_axis',(0.572116660122175,-0.820172254596952,0.));
#122180=DIRECTION('center_axis',(0.345643715052242,-0.908238033793422,-0.235868811452346));
#122181=DIRECTION('ref_axis',(0.737723608554744,0.107672340987873,0.666461209949355));
#122182=DIRECTION('center_axis',(0.73297945396056,-0.638049389824798,0.23586881145222));
#122183=DIRECTION('ref_axis',(-0.35583104616699,-0.655144046928193,-0.666461209942675));
#122184=DIRECTION('center_axis',(0.,0.,-1.));
#122185=DIRECTION('ref_axis',(0.572116660122174,-0.820172254596953,0.));
#122186=DIRECTION('center_axis',(-0.583738882684281,0.811941449146739,-6.76296429840134E-17));
#122187=DIRECTION('ref_axis',(0.811941449146739,0.583738882684281,1.84889274661175E-32));
#122188=DIRECTION('center_axis',(0.,0.,1.));
#122189=DIRECTION('ref_axis',(-0.572116660122174,0.820172254596953,0.));
#122190=DIRECTION('center_axis',(-0.560378399591454,0.828236710893281,-1.38914942345546E-16));
#122191=DIRECTION('ref_axis',(-0.828236710893281,-0.560378399591454,4.19082355898663E-31));
#122192=DIRECTION('center_axis',(0.,0.,-1.));
#122193=DIRECTION('ref_axis',(0.572116660122189,-0.820172254596943,0.));
#122194=DIRECTION('center_axis',(0.,0.,1.));
#122195=DIRECTION('ref_axis',(-0.572116660122189,0.820172254596943,0.));
#122196=DIRECTION('center_axis',(0.,0.,1.));
#122197=DIRECTION('ref_axis',(-0.572116660122189,0.820172254596943,0.));
#122198=DIRECTION('center_axis',(0.33429779167307,0.669196457569324,0.663642288932205));
#122199=DIRECTION('ref_axis',(0.582841239113268,0.406564817614819,-0.703563173472531));
#122200=DIRECTION('center_axis',(0.335259258935769,0.671121120257183,0.661209249211309));
#122201=DIRECTION('ref_axis',(0.580949829165752,0.405245451913269,-0.705884848750767));
#122202=DIRECTION('center_axis',(-0.745612810939625,-0.0828484454901213,
-0.661209249211308));
#122203=DIRECTION('ref_axis',(-0.580949829165763,-0.405245451913251,0.705884848750769));
#122204=DIRECTION('center_axis',(-0.743474518590484,-0.0826108500591795,
-0.663642288932184));
#122205=DIRECTION('ref_axis',(-0.582841239113243,-0.406564817614819,0.703563173472551));
#122206=DIRECTION('center_axis',(0.,0.,1.));
#122207=DIRECTION('ref_axis',(-0.572116660122189,0.820172254596943,0.));
#122208=DIRECTION('center_axis',(0.,0.,1.));
#122209=DIRECTION('ref_axis',(-0.572116660122189,0.820172254596943,0.));
#122210=DIRECTION('center_axis',(0.,0.,1.));
#122211=DIRECTION('ref_axis',(0.572116660122126,-0.820172254596987,0.));
#122212=DIRECTION('center_axis',(0.,0.,-1.));
#122213=DIRECTION('ref_axis',(-0.572116660122174,0.820172254596953,0.));
#122214=DIRECTION('center_axis',(-0.173886345027048,0.984765727984648,0.));
#122215=DIRECTION('ref_axis',(-0.984765727984648,-0.173886345027048,0.));
#122216=DIRECTION('',(0.,0.,1.));
#122217=DIRECTION('center_axis',(0.173881520544841,-0.984766579859303,2.28597557664648E-6));
#122218=DIRECTION('ref_axis',(0.932208090086838,0.164601947622779,0.322326349551875));
#122219=DIRECTION('',(0.,0.,-1.));
#122220=DIRECTION('center_axis',(0.921382243274622,-0.388657640833452,0.));
#122221=DIRECTION('ref_axis',(0.388657640833452,0.921382243274622,0.));
#122222=DIRECTION('center_axis',(-0.921382243274618,0.388657640833462,1.36576092854888E-15));
#122223=DIRECTION('ref_axis',(0.388135802051874,0.92014513138824,-0.0518028604235987));
#122224=DIRECTION('',(0.,0.,1.));
#122225=DIRECTION('',(0.,0.,1.));
#122226=DIRECTION('center_axis',(0.,0.,1.));
#122227=DIRECTION('ref_axis',(-0.623489801858719,0.781831482468041,0.));
#122228=DIRECTION('center_axis',(0.,0.,-1.));
#122229=DIRECTION('ref_axis',(0.623489801858719,-0.781831482468041,0.));
#122230=DIRECTION('center_axis',(0.403124563589518,-0.884226492486404,-0.235868811452366));
#122231=DIRECTION('ref_axis',(0.729309285709624,0.154717230502321,0.666461209946543));
#122232=DIRECTION('center_axis',(0.772353433824904,-0.589776294066584,0.235868811452398));
#122233=DIRECTION('ref_axis',(-0.313124729900363,-0.676596156612425,-0.66646120996058));
#122234=DIRECTION('center_axis',(0.,0.,-1.));
#122235=DIRECTION('ref_axis',(0.623489801858738,-0.781831482468027,0.));
#122236=DIRECTION('center_axis',(-0.634560795802298,0.772872949734142,-6.76296429840134E-17));
#122237=DIRECTION('ref_axis',(0.772872949734142,0.634560795802298,6.93889390390733E-14));
#122238=DIRECTION('center_axis',(0.,0.,1.));
#122239=DIRECTION('ref_axis',(-0.623489801858738,0.781831482468027,0.));
#122240=DIRECTION('center_axis',(-0.612292350332133,0.790631442408378,-1.38914942345546E-16));
#122241=DIRECTION('ref_axis',(-0.790631442408378,-0.612292350332133,1.38050658413677E-30));
#122242=DIRECTION('center_axis',(0.,0.,-1.));
#122243=DIRECTION('ref_axis',(0.623489801858737,-0.781831482468027,0.));
#122244=DIRECTION('center_axis',(0.,0.,1.));
#122245=DIRECTION('ref_axis',(-0.623489801858737,0.781831482468027,0.));
#122246=DIRECTION('center_axis',(0.,0.,1.));
#122247=DIRECTION('ref_axis',(-0.623489801858737,0.781831482468027,0.));
#122248=DIRECTION('center_axis',(0.290735376759972,0.689240054727713,0.663642288932205));
#122249=DIRECTION('ref_axis',(0.555595031976987,0.443072252996905,-0.70356317347253));
#122250=DIRECTION('center_axis',(0.291571555023262,0.691222364408686,0.661209249211309));
#122251=DIRECTION('ref_axis',(0.553792040184796,0.441634415022278,-0.705884848750765));
#122252=DIRECTION('center_axis',(-0.738772751325214,-0.130449801290734,
-0.661209249211308));
#122253=DIRECTION('ref_axis',(-0.553792040184805,-0.441634415022259,0.705884848750771));
#122254=DIRECTION('center_axis',(-0.736654075118562,-0.130075693163894,
-0.663642288932184));
#122255=DIRECTION('ref_axis',(-0.555595031976956,-0.443072252996913,0.70356317347255));
#122256=DIRECTION('center_axis',(0.,0.,1.));
#122257=DIRECTION('ref_axis',(-0.623489801858737,0.781831482468027,0.));
#122258=DIRECTION('center_axis',(0.,0.,1.));
#122259=DIRECTION('ref_axis',(-0.623489801858737,0.781831482468027,0.));
#122260=DIRECTION('center_axis',(0.,0.,1.));
#122261=DIRECTION('ref_axis',(0.623489801858728,-0.781831482468034,0.));
#122262=DIRECTION('center_axis',(0.,0.,-1.));
#122263=DIRECTION('ref_axis',(-0.623489801858737,0.781831482468027,0.));
#122264=DIRECTION('center_axis',(-0.236623233703382,0.971601484803186,0.));
#122265=DIRECTION('ref_axis',(-0.971601484803186,-0.236623233703382,0.));
#122266=DIRECTION('',(0.,0.,1.));
#122267=DIRECTION('center_axis',(0.236618473713326,-0.971602644033223,2.28597559089828E-6));
#122268=DIRECTION('ref_axis',(0.919746685589421,0.223990532666546,0.322326349563655));
#122269=DIRECTION('',(0.,0.,-1.));
#122270=DIRECTION('center_axis',(0.944390545183263,-0.328825939014031,0.));
#122271=DIRECTION('ref_axis',(0.328825939014031,0.944390545183263,0.));
#122272=DIRECTION('center_axis',(-0.944390545183216,0.328825939014167,-4.96985226777598E-14));
#122273=DIRECTION('ref_axis',(0.328384434435842,0.943122540746955,-0.0518028604930213));
#122274=DIRECTION('',(0.,0.,1.));
#122275=DIRECTION('',(0.,0.,1.));
#122276=DIRECTION('center_axis',(0.,0.,1.));
#122277=DIRECTION('ref_axis',(-0.672300890261307,0.740277997075324,0.));
#122278=DIRECTION('center_axis',(0.,0.,-1.));
#122279=DIRECTION('ref_axis',(0.672300890261307,-0.740277997075324,0.));
#122280=DIRECTION('center_axis',(0.458948886824949,-0.856581474855845,-0.235868811452311));
#122281=DIRECTION('ref_axis',(0.717898074564745,0.201126353722678,0.666461209954827));
#122282=DIRECTION('center_axis',(0.808553647760812,-0.539079681008988,0.235868811452327));
#122283=DIRECTION('ref_axis',(-0.269131716982949,-0.69526798758372,-0.666461209940304));
#122284=DIRECTION('center_axis',(0.,0.,-1.));
#122285=DIRECTION('ref_axis',(0.672300890261321,-0.740277997075312,0.));
#122286=DIRECTION('center_axis',(-0.682775162497499,0.73062854959036,-6.76296429840134E-17));
#122287=DIRECTION('ref_axis',(0.73062854959036,0.6827751624975,-2.28030105415449E-31));
#122288=DIRECTION('center_axis',(0.,0.,1.));
#122289=DIRECTION('ref_axis',(-0.672300890261321,0.740277997075312,0.));
#122290=DIRECTION('center_axis',(-0.661690260469,0.749777299736706,-1.38914942345546E-16));
#122291=DIRECTION('ref_axis',(-0.749777299736706,-0.661690260469,1.09700969632297E-30));
#122292=DIRECTION('center_axis',(0.,0.,-1.));
#122293=DIRECTION('ref_axis',(0.672300890261315,-0.740277997075317,0.));
#122294=DIRECTION('center_axis',(0.,0.,1.));
#122295=DIRECTION('ref_axis',(-0.672300890261315,0.740277997075317,0.));
#122296=DIRECTION('center_axis',(0.,0.,1.));
#122297=DIRECTION('ref_axis',(-0.672300890261315,0.740277997075317,0.));
#122298=DIRECTION('center_axis',(0.245978267821224,0.706451416659698,0.663642288932205));
#122299=DIRECTION('ref_axis',(0.526065765679537,0.477759009452737,-0.703563173472534));
#122300=DIRECTION('center_axis',(0.246685721049263,0.708483227598101,0.661209249211309));
#122301=DIRECTION('ref_axis',(0.524358600922691,0.476208607589683,-0.705884848750767));
#122302=DIRECTION('center_axis',(-0.728896916009349,-0.177515110876448,
-0.661209249211308));
#122303=DIRECTION('ref_axis',(-0.5243586009227,-0.476208607589672,0.705884848750767));
#122304=DIRECTION('center_axis',(-0.726806562040175,-0.17700602734425,-0.663642288932184));
#122305=DIRECTION('ref_axis',(-0.526065765679519,-0.47775900945273,0.703563173472551));
#122306=DIRECTION('center_axis',(0.,0.,1.));
#122307=DIRECTION('ref_axis',(-0.672300890261315,0.740277997075317,0.));
#122308=DIRECTION('center_axis',(0.,0.,1.));
#122309=DIRECTION('ref_axis',(-0.672300890261315,0.740277997075317,0.));
#122310=DIRECTION('center_axis',(0.,0.,1.));
#122311=DIRECTION('ref_axis',(0.672300890261315,-0.740277997075317,0.));
#122312=DIRECTION('center_axis',(0.,0.,-1.));
#122313=DIRECTION('ref_axis',(-0.672300890261321,0.740277997075312,0.));
#122314=DIRECTION('center_axis',(-0.298387786756903,0.954444722712802,0.));
#122315=DIRECTION('ref_axis',(-0.954444722712802,-0.298387786756903,0.));
#122316=DIRECTION('',(0.,0.,1.));
#122317=DIRECTION('center_axis',(0.298383110819051,-0.954446184534634,2.28597552936751E-6));
#122318=DIRECTION('ref_axis',(0.903505844692068,0.282458692570506,0.322326349525809));
#122319=DIRECTION('',(0.,0.,-1.));
#122320=DIRECTION('center_axis',(0.963518143770609,-0.267643020878258,0.));
#122321=DIRECTION('ref_axis',(0.267643020878258,0.963518143770609,0.));
#122322=DIRECTION('center_axis',(-0.963518143770608,0.267643020878261,9.48445089270243E-17));
#122323=DIRECTION('ref_axis',(0.267283664742203,0.962224457292137,-0.0518028604502678));
#122324=DIRECTION('',(0.,0.,1.));
#122325=DIRECTION('',(0.,0.,1.));
#122326=DIRECTION('center_axis',(0.,0.,1.));
#122327=DIRECTION('ref_axis',(-0.71834935009773,0.695682550603484,0.));
#122328=DIRECTION('center_axis',(0.,0.,-1.));
#122329=DIRECTION('ref_axis',(0.71834935009773,-0.695682550603484,0.));
#122330=DIRECTION('center_axis',(0.512887290640217,-0.825416580208937,-0.235868811452301));
#122331=DIRECTION('ref_axis',(0.703536866252696,0.246709005622772,0.666461209949955));
#122332=DIRECTION('center_axis',(0.84143134132397,-0.48616787390969,0.235868811452204));
#122333=DIRECTION('ref_axis',(-0.224032784092084,-0.711082813242973,-0.666461209945791));
#122334=DIRECTION('center_axis',(0.,0.,-1.));
#122335=DIRECTION('ref_axis',(0.718349350097732,-0.695682550603482,0.));
#122336=DIRECTION('center_axis',(-0.728183859595186,0.685381840016978,-6.76296429840134E-17));
#122337=DIRECTION('ref_axis',(0.685381840016978,0.728183859595186,8.81305542551599E-31));
#122338=DIRECTION('center_axis',(0.,0.,1.));
#122339=DIRECTION('ref_axis',(-0.718349350097731,0.695682550603482,0.));
#122340=DIRECTION('center_axis',(-0.708369143393485,0.705842161313689,-1.38914942345546E-16));
#122341=DIRECTION('ref_axis',(-0.705842161313689,-0.708369143393485,-6.5327543713615E-31));
#122342=DIRECTION('center_axis',(0.,0.,-1.));
#122343=DIRECTION('ref_axis',(0.718349350097735,-0.695682550603479,0.));
#122344=DIRECTION('center_axis',(0.,0.,1.));
#122345=DIRECTION('ref_axis',(-0.718349350097735,0.695682550603479,0.));
#122346=DIRECTION('center_axis',(0.,0.,1.));
#122347=DIRECTION('ref_axis',(-0.718349350097735,0.695682550603479,0.));
#122348=DIRECTION('center_axis',(0.200210381417825,0.720759818187274,0.663642288932205));
#122349=DIRECTION('ref_axis',(0.494374782310168,0.510482551659733,-0.703563173472533));
#122350=DIRECTION('center_axis',(0.20078620253355,0.72283278123614,0.661209249211309));
#122351=DIRECTION('ref_axis',(0.492770459694828,0.508825956842076,-0.705884848750768));
#122352=DIRECTION('center_axis',(-0.716025886917704,-0.223850972794698,
-0.661209249211308));
#122353=DIRECTION('ref_axis',(-0.492770459694842,-0.508825956842062,0.705884848750768));
#122354=DIRECTION('center_axis',(-0.713972444898846,-0.223209005790574,
-0.663642288932184));
#122355=DIRECTION('ref_axis',(-0.494374782310152,-0.510482551659722,0.703563173472552));
#122356=DIRECTION('center_axis',(0.,0.,1.));
#122357=DIRECTION('ref_axis',(-0.718349350097727,0.695682550603487,0.));
#122358=DIRECTION('center_axis',(0.,0.,1.));
#122359=DIRECTION('ref_axis',(-0.718349350097727,0.695682550603487,0.));
#122360=DIRECTION('center_axis',(0.,0.,1.));
#122361=DIRECTION('ref_axis',(0.718349350097761,-0.695682550603452,0.));
#122362=DIRECTION('center_axis',(0.,0.,-1.));
#122363=DIRECTION('ref_axis',(-0.718349350097731,0.695682550603482,0.));
#122364=DIRECTION('center_axis',(-0.358926200390661,0.93336594252904,0.));
#122365=DIRECTION('ref_axis',(-0.93336594252904,-0.358926200390661,0.));
#122366=DIRECTION('',(0.,0.,1.));
#122367=DIRECTION('center_axis',(0.358921627719158,-0.933367700935813,2.28597556646122E-6));
#122368=DIRECTION('ref_axis',(0.883552304442921,0.339766169107703,0.322326349595374));
#122369=DIRECTION('',(0.,0.,-1.));
#122370=DIRECTION('center_axis',(0.978686439631208,-0.205360300160449,0.));
#122371=DIRECTION('ref_axis',(0.205360300160449,0.978686439631208,0.));
#122372=DIRECTION('center_axis',(-0.978686439631198,0.205360300160498,-2.97053001959438E-14));
#122373=DIRECTION('ref_axis',(0.205084569137578,0.977372387144383,-0.0518028604359201));
#122374=DIRECTION('',(0.,0.,1.));
#122375=DIRECTION('',(0.,0.,1.));
#122376=DIRECTION('center_axis',(0.,0.,1.));
#122377=DIRECTION('ref_axis',(-0.761445958369139,0.648228395307783,0.));
#122378=DIRECTION('center_axis',(0.,0.,-1.));
#122379=DIRECTION('ref_axis',(0.761445958369139,-0.648228395307783,0.));
#122380=DIRECTION('center_axis',(0.564718130564305,-0.790859871782637,-0.235868811452275));
#122381=DIRECTION('ref_axis',(0.686284674053918,0.291277877306599,0.666461209936834));
#122382=DIRECTION('center_axis',(0.870851413018679,-0.431258298734532,0.2358688114524));
#122383=DIRECTION('ref_axis',(-0.178013252433613,-0.723975647090741,-0.666461209957151));
#122384=DIRECTION('center_axis',(0.,0.,-1.));
#122385=DIRECTION('ref_axis',(0.761445958369138,-0.648228395307784,0.));
#122386=DIRECTION('center_axis',(-0.770600293018847,0.637318749449024,-6.76296429840134E-17));
#122387=DIRECTION('ref_axis',(0.637318749449024,0.770600293018847,-9.86076131526264E-32));
#122388=DIRECTION('center_axis',(0.,0.,1.));
#122389=DIRECTION('ref_axis',(-0.761445958369138,0.648228395307784,0.));
#122390=DIRECTION('center_axis',(-0.75213718556306,0.659006566047167,-1.38914942345546E-16));
#122391=DIRECTION('ref_axis',(-0.659006566047166,-0.75213718556306,1.06003184139073E-30));
#122392=DIRECTION('center_axis',(0.,0.,-1.));
#122393=DIRECTION('ref_axis',(0.76144595836914,-0.648228395307782,0.));
#122394=DIRECTION('center_axis',(0.,0.,1.));
#122395=DIRECTION('ref_axis',(-0.76144595836914,0.648228395307782,0.));
#122396=DIRECTION('center_axis',(0.,0.,1.));
#122397=DIRECTION('ref_axis',(-0.76144595836914,0.648228395307782,0.));
#122398=DIRECTION('center_axis',(0.153619787612189,0.732106463019423,0.663642288932205));
#122399=DIRECTION('ref_axis',(0.460652306917222,0.541108411563798,-0.703563173472535));
#122400=DIRECTION('center_axis',(0.154061610443123,0.734212059928934,0.661209249211309));
#122401=DIRECTION('ref_axis',(0.459157418949153,0.539352431094974,-0.705884848750767));
#122402=DIRECTION('center_axis',(-0.700212553869644,-0.269266983049852,
-0.661209249211308));
#122403=DIRECTION('ref_axis',(-0.459157418949171,-0.539352431094955,0.70588484875077));
#122404=DIRECTION('center_axis',(-0.698204461834818,-0.268494770553923,
-0.663642288932184));
#122405=DIRECTION('ref_axis',(-0.46065230691722,-0.541108411563773,0.703563173472556));
#122406=DIRECTION('center_axis',(0.,0.,1.));
#122407=DIRECTION('ref_axis',(-0.76144595836914,0.648228395307782,0.));
#122408=DIRECTION('center_axis',(0.,0.,1.));
#122409=DIRECTION('ref_axis',(-0.76144595836914,0.648228395307782,0.));
#122410=DIRECTION('center_axis',(0.,0.,1.));
#122411=DIRECTION('ref_axis',(0.761445958369091,-0.648228395307839,0.));
#122412=DIRECTION('center_axis',(0.,0.,-1.));
#122413=DIRECTION('ref_axis',(-0.761445958369138,0.648228395307784,0.));
#122414=DIRECTION('center_axis',(-0.417989709277585,0.908451761481059,0.));
#122415=DIRECTION('ref_axis',(-0.908451761481059,-0.417989709277585,0.));
#122416=DIRECTION('',(0.,0.,1.));
#122417=DIRECTION('center_axis',(0.417985258662655,-0.908453809247057,2.28597556699346E-6));
#122418=DIRECTION('ref_axis',(0.859968058324844,0.395677473606074,0.322326349437511));
#122419=DIRECTION('',(0.,0.,-1.));
#122420=DIRECTION('center_axis',(0.98983310298378,-0.142233709919634,0.));
#122421=DIRECTION('ref_axis',(0.142233709919634,0.98983310298378,0.));
#122422=DIRECTION('center_axis',(-0.989833102983781,0.142233709919624,4.45769191956972E-15));
#122423=DIRECTION('ref_axis',(0.14204273704737,0.988504084210138,-0.0518028604612583));
#122424=DIRECTION('',(0.,0.,1.));
#122425=DIRECTION('',(0.,0.,1.));
#122426=DIRECTION('center_axis',(0.,0.,1.));
#122427=DIRECTION('ref_axis',(-0.801413621867962,0.59811053049121,0.));
#122428=DIRECTION('center_axis',(0.,0.,-1.));
#122429=DIRECTION('ref_axis',(0.801413621867962,-0.59811053049121,0.));
#122430=DIRECTION('center_axis',(0.614228422558437,-0.753053350504075,-0.235868811452385));
#122431=DIRECTION('ref_axis',(0.666212390911907,0.334649825703311,0.666461209938121));
#122432=DIRECTION('center_axis',(0.896692969460538,-0.374576590704866,0.235868811452388));
#122433=DIRECTION('ref_axis',(-0.131262226148597,-0.733893509725554,-0.666461209950904));
#122434=DIRECTION('center_axis',(0.,0.,-1.));
#122435=DIRECTION('ref_axis',(0.80141362186796,-0.598110530491212,0.));
#122436=DIRECTION('center_axis',(-0.809850164545249,0.58663677943514,-6.76296429840134E-17));
#122437=DIRECTION('ref_axis',(0.58663677943514,0.809850164545249,-5.66993775627602E-31));
#122438=DIRECTION('center_axis',(0.,0.,1.));
#122439=DIRECTION('ref_axis',(-0.80141362186796,0.598110530491212,0.));
#122440=DIRECTION('center_axis',(-0.792814534704237,0.60946297144429,-1.38914942345546E-16));
#122441=DIRECTION('ref_axis',(-0.60946297144429,-0.792814534704237,-1.23259516440783E-31));
#122442=DIRECTION('center_axis',(0.,0.,-1.));
#122443=DIRECTION('ref_axis',(0.801413621867966,-0.598110530491204,0.));
#122444=DIRECTION('center_axis',(0.,0.,1.));
#122445=DIRECTION('ref_axis',(-0.801413621867966,0.598110530491204,0.));
#122446=DIRECTION('center_axis',(0.,0.,1.));
#122447=DIRECTION('ref_axis',(-0.801413621867966,0.598110530491204,0.));
#122448=DIRECTION('center_axis',(0.106397937147913,0.740444725358681,0.663642288932205));
#122449=DIRECTION('ref_axis',(0.425036912385557,0.569510740937352,-0.703563173472533));
#122450=DIRECTION('center_axis',(0.106703946149272,0.742574303779487,0.661209249211309));
#122451=DIRECTION('ref_axis',(0.423657601880061,0.567662590517769,-0.705884848750766));
#122452=DIRECTION('center_axis',(-0.681521897242611,-0.313576517514068,
-0.661209249211308));
#122453=DIRECTION('ref_axis',(-0.423657601880075,-0.567662590517753,0.70588484875077));
#122454=DIRECTION('center_axis',(-0.679567406872724,-0.312677232713118,
-0.663642288932184));
#122455=DIRECTION('ref_axis',(-0.425036912385535,-0.569510740937347,0.70356317347255));
#122456=DIRECTION('center_axis',(0.,0.,1.));
#122457=DIRECTION('ref_axis',(-0.801413621867966,0.598110530491204,0.));
#122458=DIRECTION('center_axis',(0.,0.,1.));
#122459=DIRECTION('ref_axis',(-0.801413621867966,0.598110530491204,0.));
#122460=DIRECTION('center_axis',(0.,0.,1.));
#122461=DIRECTION('ref_axis',(0.801413621867988,-0.598110530491173,0.));
#122462=DIRECTION('center_axis',(0.,0.,-1.));
#122463=DIRECTION('ref_axis',(-0.80141362186796,0.598110530491212,0.));
#122464=DIRECTION('center_axis',(-0.475335608790577,0.879804557282861,0.));
#122465=DIRECTION('ref_axis',(-0.879804557282862,-0.475335608790577,0.));
#122466=DIRECTION('',(0.,0.,1.));
#122467=DIRECTION('center_axis',(0.475331298520703,-0.879806885993396,2.28597555931563E-6));
#122468=DIRECTION('ref_axis',(0.832850018919391,0.449962854461081,0.322326349514286));
#122469=DIRECTION('',(0.,0.,-1.));
#122470=DIRECTION('center_axis',(0.996912329797656,-0.0785226508557234,
0.));
#122471=DIRECTION('ref_axis',(0.0785226508557234,0.996912329797656,0.));
#122472=DIRECTION('center_axis',(-0.996912329797664,0.0785226508556254,
4.36901230372518E-14));
#122473=DIRECTION('ref_axis',(0.0784172208831005,0.995573805965461,-0.051802860388376));
#122474=DIRECTION('',(0.,0.,1.));
#122475=DIRECTION('',(0.,0.,1.));
#122476=DIRECTION('center_axis',(0.,0.,1.));
#122477=DIRECTION('ref_axis',(-0.83808810489185,0.545534901210534,0.));
#122478=DIRECTION('center_axis',(0.,0.,-1.));
#122479=DIRECTION('ref_axis',(0.83808810489185,-0.545534901210534,0.));
#122480=DIRECTION('center_axis',(0.661214718212524,-0.712152371479,-0.235868811452401));
#122481=DIRECTION('ref_axis',(0.643402498150284,0.376646626178607,0.66646120994567));
#122482=DIRECTION('center_axis',(0.918849822150862,-0.316355667117517,0.235868811452384));
#122483=DIRECTION('ref_axis',(-0.0839718152178504,-0.740795646506438,-0.666461209948582));
#122484=DIRECTION('center_axis',(0.,0.,-1.));
#122485=DIRECTION('ref_axis',(0.838088104891844,-0.545534901210544,0.));
#122486=DIRECTION('center_axis',(-0.84577218803322,0.533544193061362,-6.76296429840134E-17));
#122487=DIRECTION('ref_axis',(0.533544193061362,0.84577218803322,-5.54667823983524E-31));
#122488=DIRECTION('center_axis',(0.,0.,1.));
#122489=DIRECTION('ref_axis',(-0.838088104891844,0.545534901210544,0.));
#122490=DIRECTION('center_axis',(-0.83023403886413,0.557414962762352,-1.38914942345546E-16));
#122491=DIRECTION('ref_axis',(-0.557414962762352,-0.83023403886413,7.64209001932855E-31));
#122492=DIRECTION('center_axis',(0.,0.,-1.));
#122493=DIRECTION('ref_axis',(0.838088104891845,-0.545534901210541,0.));
#122494=DIRECTION('center_axis',(0.,0.,1.));
#122495=DIRECTION('ref_axis',(-0.838088104891845,0.545534901210541,0.));
#122496=DIRECTION('center_axis',(0.,0.,1.));
#122497=DIRECTION('ref_axis',(-0.838088104891845,0.545534901210541,0.));
#122498=DIRECTION('center_axis',(0.0587388747376102,0.745740341496545,0.663642288932205));
#122499=DIRECTION('ref_axis',(0.387674950010748,0.59557282851673,-0.703563173472536));
#122500=DIRECTION('center_axis',(0.0589078124527693,0.747885150534122,0.661209249211309));
#122501=DIRECTION('ref_axis',(0.386416884850565,0.593640102592886,-0.705884848750767));
#122502=DIRECTION('center_axis',(-0.660030720953819,-0.356597498805866,
-0.661209249211308));
#122503=DIRECTION('ref_axis',(-0.386416884850578,-0.593640102592876,0.705884848750768));
#122504=DIRECTION('center_axis',(-0.658137863669038,-0.355574837054039,
-0.663642288932184));
#122505=DIRECTION('ref_axis',(-0.387674950010746,-0.595572828516711,0.703563173472553));
#122506=DIRECTION('center_axis',(0.,0.,1.));
#122507=DIRECTION('ref_axis',(-0.838088104891845,0.545534901210541,0.));
#122508=DIRECTION('center_axis',(0.,0.,1.));
#122509=DIRECTION('ref_axis',(-0.838088104891845,0.545534901210541,0.));
#122510=DIRECTION('center_axis',(0.,0.,1.));
#122511=DIRECTION('ref_axis',(0.83808810489183,-0.545534901210566,0.));
#122512=DIRECTION('center_axis',(0.,0.,-1.));
#122513=DIRECTION('ref_axis',(-0.838088104891844,0.545534901210544,0.));
#122514=DIRECTION('center_axis',(-0.530728252327879,0.847542047441303,0.));
#122515=DIRECTION('ref_axis',(-0.847542047441303,-0.530728252327879,0.));
#122516=DIRECTION('',(0.,0.,1.));
#122517=DIRECTION('center_axis',(0.530724100115005,-0.847544647527133,2.28597551887765E-6));
#122518=DIRECTION('ref_axis',(0.802309620147107,0.502399241430756,0.322326349573232));
#122519=DIRECTION('',(0.,0.,-1.));
#122520=DIRECTION('center_axis',(0.999895030011369,-0.0144889253763915,
0.));
#122521=DIRECTION('ref_axis',(0.0144889253763915,0.99989503001137,0.));
#122522=DIRECTION('center_axis',(-0.999895030011369,0.0144889253764111,
-1.28134931560421E-14));
#122523=DIRECTION('ref_axis',(0.0144694715374454,0.998552501397843,-0.0518028603991841));
#122524=DIRECTION('',(0.,0.,1.));
#122525=DIRECTION('',(0.,0.,1.));
#122526=DIRECTION('center_axis',(0.,0.,1.));
#122527=DIRECTION('ref_axis',(-0.871318704123387,0.490717552003943,0.));
#122528=DIRECTION('center_axis',(0.,0.,-1.));
#122529=DIRECTION('ref_axis',(0.871318704123387,-0.490717552003943,0.));
#122530=DIRECTION('center_axis',(0.705483940759275,-0.66832500560343,-0.235868811452342));
#122531=DIRECTION('ref_axis',(0.617948726513988,0.417095704873767,0.666461209955685));
#122532=DIRECTION('center_axis',(0.93723092382929,-0.256834770235915,0.235868811452386));
#122533=DIRECTION('ref_axis',(-0.0363363460880332,-0.744653695079018,-0.666461209942586));
#122534=DIRECTION('center_axis',(0.,0.,-1.));
#122535=DIRECTION('ref_axis',(0.871318704123392,-0.490717552003933,0.));
#122536=DIRECTION('center_axis',(-0.878218752182996,0.478259159153425,-6.76296429840134E-17));
#122537=DIRECTION('ref_axis',(0.478259159153425,0.878218752182996,6.93889390390724E-14));
#122538=DIRECTION('center_axis',(0.,0.,1.));
#122539=DIRECTION('ref_axis',(-0.871318704123392,0.490717552003933,0.));
#122540=DIRECTION('center_axis',(-0.864241933273687,0.503076416433289,-1.38914942345546E-16));
#122541=DIRECTION('ref_axis',(-0.503076416433289,-0.864241933273687,-1.46678824564532E-30));
#122542=DIRECTION('center_axis',(0.,0.,-1.));
#122543=DIRECTION('ref_axis',(0.871318704123391,-0.490717552003934,0.));
#122544=DIRECTION('center_axis',(0.,0.,1.));
#122545=DIRECTION('ref_axis',(-0.871318704123391,0.490717552003934,0.));
#122546=DIRECTION('center_axis',(0.,0.,1.));
#122547=DIRECTION('ref_axis',(-0.871318704123391,0.490717552003934,0.));
#122548=DIRECTION('center_axis',(0.0108384416915616,0.747971550610398,0.663642288932205));
#122549=DIRECTION('ref_axis',(0.348719948110342,0.619187579593757,-0.703563173472536));
#122550=DIRECTION('center_axis',(0.0108696139192121,0.75012277678435,0.661209249211309));
#122551=DIRECTION('ref_axis',(0.347588297955049,0.617178220151048,-0.70588484875077));
#122552=DIRECTION('center_axis',(-0.635827336856483,-0.398153144485148,
-0.661209249211308));
#122553=DIRECTION('ref_axis',(-0.347588297955069,-0.61717822015104,0.705884848750767));
#122554=DIRECTION('center_axis',(-0.634003890813407,-0.397011308118942,
-0.663642288932184));
#122555=DIRECTION('ref_axis',(-0.34871994811034,-0.619187579593738,0.703563173472553));
#122556=DIRECTION('center_axis',(0.,0.,1.));
#122557=DIRECTION('ref_axis',(-0.871318704123391,0.490717552003934,0.));
#122558=DIRECTION('center_axis',(0.,0.,1.));
#122559=DIRECTION('ref_axis',(-0.871318704123391,0.490717552003934,0.));
#122560=DIRECTION('center_axis',(0.,0.,1.));
#122561=DIRECTION('ref_axis',(0.871318704123372,-0.490717552003968,0.));
#122562=DIRECTION('center_axis',(0.,0.,-1.));
#122563=DIRECTION('ref_axis',(-0.871318704123392,0.490717552003933,0.));
#122564=DIRECTION('center_axis',(-0.583940019635513,0.811796805529608,0.));
#122565=DIRECTION('ref_axis',(-0.811796805529608,-0.583940019635513,0.));
#122566=DIRECTION('',(0.,0.,1.));
#122567=DIRECTION('center_axis',(0.583936042541839,-0.811799666306503,2.28597554981395E-6));
#122568=DIRECTION('ref_axis',(0.768472359086984,0.552771162175832,0.322326349506313));
#122569=DIRECTION('',(0.,0.,-1.));
#122570=DIRECTION('center_axis',(0.998768947069955,0.0496043382051768,0.));
#122571=DIRECTION('ref_axis',(-0.0496043382051768,0.998768947069955,0.));
#122572=DIRECTION('center_axis',(-0.998768947069955,-0.0496043382051805,
5.96571961151145E-15));
#122573=DIRECTION('ref_axis',(0.0495377359705003,-0.997427930412718,0.0518028604183216));
#122574=DIRECTION('',(0.,0.,1.));
#122575=DIRECTION('',(0.,0.,1.));
#122576=DIRECTION('center_axis',(0.,0.,1.));
#122577=DIRECTION('ref_axis',(-0.900968867902423,0.433883739117549,0.));
#122578=DIRECTION('center_axis',(0.,0.,-1.));
#122579=DIRECTION('ref_axis',(0.900968867902423,-0.433883739117549,0.));
#122580=DIRECTION('center_axis',(0.74685417846772,-0.621751348924435,-0.235868811452366));
#122581=DIRECTION('ref_axis',(0.589955671017639,0.455830847862106,0.666461209952569));
#122582=DIRECTION('center_axis',(0.951760742606324,-0.196258484192456,0.235868811452338));
#122583=DIRECTION('ref_axis',(0.0114484368873645,-0.745451801881426,-0.666461209947415));
#122584=DIRECTION('center_axis',(0.,0.,-1.));
#122585=DIRECTION('ref_axis',(0.900968867902422,-0.433883739117553,0.));
#122586=DIRECTION('center_axis',(-0.907056527102721,0.421008855774258,-6.76296429840134E-17));
#122587=DIRECTION('ref_axis',(0.421008855774258,0.907056527102721,6.9388939039073E-14));
#122588=DIRECTION('center_axis',(0.,0.,1.));
#122589=DIRECTION('ref_axis',(-0.900968867902422,0.433883739117553,0.));
#122590=DIRECTION('center_axis',(-0.894698472200109,0.446670621199548,-1.38914942345546E-16));
#122591=DIRECTION('ref_axis',(-0.446670621199548,-0.894698472200109,3.69778549322349E-32));
#122592=DIRECTION('center_axis',(0.,0.,-1.));
#122593=DIRECTION('ref_axis',(0.900968867902425,-0.433883739117546,0.));
#122594=DIRECTION('center_axis',(0.,0.,1.));
#122595=DIRECTION('ref_axis',(-0.900968867902425,0.433883739117546,0.));
#122596=DIRECTION('center_axis',(0.,0.,1.));
#122597=DIRECTION('ref_axis',(-0.900968867902425,0.433883739117546,0.));
#122598=DIRECTION('center_axis',(-0.0371065288362363,0.747129184183398,
0.663642288932205));
#122599=DIRECTION('ref_axis',(0.308331981142967,0.640257956090912,-0.703563173472532));
#122600=DIRECTION('center_axis',(-0.037213250189464,0.749277987643941,0.661209249211309));
#122601=DIRECTION('ref_axis',(0.307331396185796,0.638180220018292,-0.705884848750768));
#122602=DIRECTION('center_axis',(-0.609011201847467,-0.438072693490158,
-0.661209249211308));
#122603=DIRECTION('ref_axis',(-0.307331396185819,-0.638180220018278,0.70588484875077));
#122604=DIRECTION('center_axis',(-0.607264659977016,-0.436816374560125,
-0.663642288932184));
#122605=DIRECTION('ref_axis',(-0.308331981142956,-0.640257956090894,0.703563173472554));
#122606=DIRECTION('center_axis',(0.,0.,1.));
#122607=DIRECTION('ref_axis',(-0.900968867902425,0.433883739117546,0.));
#122608=DIRECTION('center_axis',(0.,0.,1.));
#122609=DIRECTION('ref_axis',(-0.900968867902425,0.433883739117546,0.));
#122610=DIRECTION('center_axis',(0.,0.,1.));
#122611=DIRECTION('ref_axis',(0.900968867902412,-0.433883739117574,0.));
#122612=DIRECTION('center_axis',(0.,0.,-1.));
#122613=DIRECTION('ref_axis',(-0.900968867902422,0.433883739117553,0.));
#122614=DIRECTION('center_axis',(-0.634752252147723,0.772715716414124,0.));
#122615=DIRECTION('ref_axis',(-0.772715716414124,-0.634752252147723,0.));
#122616=DIRECTION('',(0.,0.,1.));
#122617=DIRECTION('center_axis',(0.634748466515921,-0.772718826126594,2.28597560005782E-6));
#122618=DIRECTION('ref_axis',(0.731477280229487,0.600871627619704,0.322326349574031));
#122619=DIRECTION('',(0.,0.,-1.));
#122620=DIRECTION('center_axis',(0.993538708289763,0.113493766920963,0.));
#122621=DIRECTION('ref_axis',(-0.113493766920963,0.993538708289763,0.));
#122622=DIRECTION('center_axis',(-0.993538708289748,-0.113493766921094,
5.7807728191039E-14));
#122623=DIRECTION('ref_axis',(0.113341382295553,-0.992204714114264,0.0518028604303367));
#122624=DIRECTION('',(0.,0.,1.));
#122625=DIRECTION('',(0.,0.,1.));
#122626=DIRECTION('center_axis',(0.,0.,1.));
#122627=DIRECTION('ref_axis',(-0.926916757346023,0.375267004879372,0.));
#122628=DIRECTION('center_axis',(0.,0.,-1.));
#122629=DIRECTION('ref_axis',(0.926916757346023,-0.375267004879372,0.));
#122630=DIRECTION('center_axis',(0.785155432157007,-0.572622782587642,-0.235868811452318));
#122631=DIRECTION('ref_axis',(0.559538361127005,0.492692884129434,0.666461209940628));
#122632=DIRECTION('center_axis',(0.962379572339946,-0.134875729940102,0.235868811452272));
#122633=DIRECTION('ref_axis',(0.059186175773507,-0.743186687345194,-0.666461209936621));
#122634=DIRECTION('center_axis',(0.,0.,-1.));
#122635=DIRECTION('ref_axis',(0.926916757346024,-0.375267004879368,0.));
#122636=DIRECTION('center_axis',(-0.932167012189566,0.362028536700599,-6.76296429840134E-17));
#122637=DIRECTION('ref_axis',(0.362028536700599,0.932167012189566,8.65898102996501E-31));
#122638=DIRECTION('center_axis',(0.,0.,1.));
#122639=DIRECTION('ref_axis',(-0.926916757346024,0.375267004879368,0.));
#122640=DIRECTION('center_axis',(-0.921478503192041,0.388429360572751,-1.38914942345546E-16));
#122641=DIRECTION('ref_axis',(-0.388429360572751,-0.921478503192041,5.97808654737798E-31));
#122642=DIRECTION('center_axis',(0.,0.,-1.));
#122643=DIRECTION('ref_axis',(0.92691675734602,-0.375267004879378,0.));
#122644=DIRECTION('center_axis',(0.,0.,1.));
#122645=DIRECTION('ref_axis',(-0.926916757346019,0.375267004879381,0.));
#122646=DIRECTION('center_axis',(0.,0.,1.));
#122647=DIRECTION('ref_axis',(-0.926916757346019,0.375267004879381,0.));
#122648=DIRECTION('center_axis',(-0.0848990206777204,0.743216703679881,
0.663642288932205));
#122649=DIRECTION('ref_axis',(0.266677011928053,0.658697375311593,-0.703563173472535));
#122650=DIRECTION('center_axis',(-0.0851431970708945,0.745354254532678,
0.661209249211309));
#122651=DIRECTION('ref_axis',(0.265811603787226,0.656559800472254,-0.705884848750769));
#122652=DIRECTION('center_axis',(-0.579692509177567,-0.476192107831319,
-0.661209249211308));
#122653=DIRECTION('ref_axis',(-0.265811603787247,-0.656559800472248,0.705884848750767));
#122654=DIRECTION('center_axis',(-0.578030048394918,-0.474826468821422,
-0.663642288932184));
#122655=DIRECTION('ref_axis',(-0.266677011928043,-0.658697375311579,0.703563173472551));
#122656=DIRECTION('center_axis',(0.,0.,1.));
#122657=DIRECTION('ref_axis',(-0.92691675734602,0.375267004879378,0.));
#122658=DIRECTION('center_axis',(0.,0.,1.));
#122659=DIRECTION('ref_axis',(-0.92691675734602,0.375267004879378,0.));
#122660=DIRECTION('center_axis',(0.,0.,1.));
#122661=DIRECTION('ref_axis',(0.926916757346018,-0.375267004879384,0.));
#122662=DIRECTION('center_axis',(0.,0.,-1.));
#122663=DIRECTION('ref_axis',(-0.926916757346024,0.375267004879368,0.));
#122664=DIRECTION('center_axis',(-0.682956151501928,0.730459372672893,0.));
#122665=DIRECTION('ref_axis',(-0.730459372672893,-0.682956151501928,0.));
#122666=DIRECTION('',(0.,0.,1.));
#122667=DIRECTION('center_axis',(0.682952572888172,-0.730462718542295,2.28597554966162E-6));
#122668=DIRECTION('ref_axis',(0.691476404378248,0.646502982704101,0.322326349439246));
#122669=DIRECTION('',(0.,0.,-1.));
#122670=DIRECTION('center_axis',(0.984225805843823,0.176916825404134,0.));
#122671=DIRECTION('ref_axis',(-0.176916825404134,0.984225805843823,0.));
#122672=DIRECTION('center_axis',(-0.984225805843822,-0.176916825404143,
4.89397666063556E-15));
#122673=DIRECTION('ref_axis',(0.176679284569536,-0.982904315822576,0.0518028603587719));
#122674=DIRECTION('',(0.,0.,1.));
#122675=DIRECTION('',(0.,0.,1.));
#122676=DIRECTION('center_axis',(0.,0.,1.));
#122677=DIRECTION('ref_axis',(-0.949055747010676,0.315108218023599,0.));
#122678=DIRECTION('center_axis',(0.,0.,-1.));
#122679=DIRECTION('ref_axis',(0.949055747010676,-0.315108218023599,0.));
#122680=DIRECTION('center_axis',(0.820230313760376,-0.521141186409809,-0.235868811452324));
#122681=DIRECTION('ref_axis',(0.526821788080383,0.527530339630141,0.66646120995411));
#122682=DIRECTION('center_axis',(0.969043777980972,-0.0729387423830074,
0.235868811452363));
#122683=DIRECTION('ref_axis',(0.106680705974441,-0.73786765928216,-0.66646120994268));
#122684=DIRECTION('center_axis',(0.,0.,-1.));
#122685=DIRECTION('ref_axis',(0.949055747010671,-0.315108218023615,0.));
#122686=DIRECTION('center_axis',(-0.953447023074127,0.301560564714759,-6.76296429840134E-17));
#122687=DIRECTION('ref_axis',(0.301560564714759,0.953447023074127,6.93889390390713E-14));
#122688=DIRECTION('center_axis',(0.,0.,1.));
#122689=DIRECTION('ref_axis',(-0.949055747010671,0.315108218023615,0.));
#122690=DIRECTION('center_axis',(-0.944471981357837,0.328591960385524,-1.38914942345546E-16));
#122691=DIRECTION('ref_axis',(-0.328591960385524,-0.944471981357837,1.17096540618744E-31));
#122692=DIRECTION('center_axis',(0.,0.,-1.));
#122693=DIRECTION('ref_axis',(0.949055747010673,-0.315108218023608,0.));
#122694=DIRECTION('center_axis',(0.,0.,1.));
#122695=DIRECTION('ref_axis',(-0.949055747010673,0.315108218023608,0.));
#122696=DIRECTION('center_axis',(0.,0.,1.));
#122697=DIRECTION('ref_axis',(-0.949055747010673,0.315108218023608,0.));
#122698=DIRECTION('center_axis',(-0.132342644232457,0.73625018632146,0.663642288932205));
#122699=DIRECTION('ref_axis',(0.223926209669102,0.674430065726972,-0.703563173472533));
#122700=DIRECTION('center_axis',(-0.132723272292402,0.738367700911554,0.661209249211309));
#122701=DIRECTION('ref_axis',(0.223199534492297,0.67224143587444,-0.705884848750767));
#122702=DIRECTION('center_axis',(-0.547991735643803,-0.512354746658515,
-0.661209249211308));
#122703=DIRECTION('ref_axis',(-0.223199534492311,-0.672241435874435,0.705884848750767));
#122704=DIRECTION('center_axis',(-0.546420187356908,-0.510885399272374,
-0.663642288932184));
#122705=DIRECTION('ref_axis',(-0.223926209669094,-0.674430065726953,0.703563173472554));
#122706=DIRECTION('center_axis',(0.,0.,1.));
#122707=DIRECTION('ref_axis',(-0.949055747010673,0.315108218023608,0.));
#122708=DIRECTION('center_axis',(0.,0.,1.));
#122709=DIRECTION('ref_axis',(-0.949055747010673,0.315108218023608,0.));
#122710=DIRECTION('center_axis',(0.,0.,1.));
#122711=DIRECTION('ref_axis',(0.949055747010662,-0.315108218023641,0.));
#122712=DIRECTION('center_axis',(0.,0.,-1.));
#122713=DIRECTION('ref_axis',(-0.949055747010671,0.315108218023615,0.));
#122714=DIRECTION('center_axis',(-0.728353637535975,0.685201414686305,0.));
#122715=DIRECTION('ref_axis',(-0.685201414686304,-0.728353637535975,0.));
#122716=DIRECTION('',(0.,0.,1.));
#122717=DIRECTION('center_axis',(0.728350280645412,-0.685204982963875,2.28597554837052E-6));
#122718=DIRECTION('ref_axis',(0.648634103605699,0.689477718308503,0.322326349521306));
#122719=DIRECTION('',(0.,0.,-1.));
#122720=DIRECTION('center_axis',(0.970868508445898,0.23961289470318,0.));
#122721=DIRECTION('ref_axis',(-0.23961289470318,0.970868508445898,0.));
#122722=DIRECTION('center_axis',(-0.97086850844591,-0.239612894703131,-1.78307676782824E-14));
#122723=DIRECTION('ref_axis',(0.239291173764342,-0.969564952857368,0.0518028604342702));
#122724=DIRECTION('',(0.,0.,1.));
#122725=DIRECTION('',(0.,0.,1.));
#122726=DIRECTION('center_axis',(0.,0.,1.));
#122727=DIRECTION('ref_axis',(-0.967294863039036,0.253654583909484,0.));
#122728=DIRECTION('center_axis',(0.,0.,-1.));
#122729=DIRECTION('ref_axis',(0.967294863039036,-0.253654583909484,0.));
#122730=DIRECTION('center_axis',(0.851934693065737,-0.467518109312347,-0.235868811452463));
#122731=DIRECTION('ref_axis',(0.491940391306886,0.560200059816394,0.666461209960892));
#122732=DIRECTION('center_axis',(0.971725974879099,-0.0107020338878288,
0.235868811452317));
#122733=DIRECTION('ref_axis',(0.153736862271372,-0.729516574733322,-0.666461209950222));
#122734=DIRECTION('center_axis',(0.,0.,-1.));
#122735=DIRECTION('ref_axis',(0.967294863039031,-0.253654583909501,0.));
#122736=DIRECTION('center_axis',(-0.970809115627132,0.239853415683968,-6.76296429840134E-17));
#122737=DIRECTION('ref_axis',(0.239853415683968,0.970809115627132,1.81807786750155E-31));
#122738=DIRECTION('center_axis',(0.,0.,1.));
#122739=DIRECTION('ref_axis',(-0.967294863039031,0.253654583909501,0.));
#122740=DIRECTION('center_axis',(-0.963584421563629,0.267404305350318,-1.38914942345546E-16));
#122741=DIRECTION('ref_axis',(-0.267404305350318,-0.963584421563629,9.05957445839756E-31));
#122742=DIRECTION('center_axis',(0.,0.,-1.));
#122743=DIRECTION('ref_axis',(0.967294863039032,-0.253654583909497,0.));
#122744=DIRECTION('center_axis',(0.,0.,1.));
#122745=DIRECTION('ref_axis',(-0.967294863039032,0.253654583909497,0.));
#122746=DIRECTION('center_axis',(0.,0.,1.));
#122747=DIRECTION('ref_axis',(-0.967294863039032,0.253654583909497,0.));
#122748=DIRECTION('center_axis',(-0.179242443474634,0.726258259022275,0.663642288932205));
#122749=DIRECTION('ref_axis',(0.180255246582592,0.687391378337485,-0.703563173472533));
#122750=DIRECTION('center_axis',(-0.179757959119008,0.728347036028009,0.661209249211309));
#122751=DIRECTION('ref_axis',(0.179670290433983,0.685160687021282,-0.705884848750767));
#122752=DIRECTION('center_axis',(-0.51403914652442,-0.546412009931942,-0.661209249211308));
#122753=DIRECTION('ref_axis',(-0.179670290434002,-0.685160687021275,0.705884848750769));
#122754=DIRECTION('center_axis',(-0.512564968562287,-0.544844992033141,
-0.663642288932184));
#122755=DIRECTION('ref_axis',(-0.180255246582581,-0.687391378337468,0.703563173472552));
#122756=DIRECTION('center_axis',(0.,0.,1.));
#122757=DIRECTION('ref_axis',(-0.967294863039032,0.253654583909497,0.));
#122758=DIRECTION('center_axis',(0.,0.,1.));
#122759=DIRECTION('ref_axis',(-0.967294863039032,0.253654583909497,0.));
#122760=DIRECTION('center_axis',(0.,0.,1.));
#122761=DIRECTION('ref_axis',(0.967294863039023,-0.253654583909532,0.));
#122762=DIRECTION('center_axis',(0.,0.,-1.));
#122763=DIRECTION('ref_axis',(-0.967294863039031,0.253654583909501,0.));
#122764=DIRECTION('center_axis',(-0.770758162242022,0.637127817111528,0.));
#122765=DIRECTION('ref_axis',(-0.637127817111528,-0.770758162242022,0.));
#122766=DIRECTION('',(0.,0.,1.));
#122767=DIRECTION('center_axis',(0.770755040868896,-0.637131593134385,2.28597555422295E-6));
#122768=DIRECTION('ref_axis',(0.603126426175686,0.729619242077449,0.322326349588231));
#122769=DIRECTION('',(0.,0.,-1.));
#122770=DIRECTION('center_axis',(0.953521704096127,0.301324343221085,0.));
#122771=DIRECTION('ref_axis',(-0.301324343221085,0.953521704096127,0.));
#122772=DIRECTION('center_axis',(-0.953521704096134,-0.301324343221062,
-1.04139270801893E-14));
#122773=DIRECTION('ref_axis',(0.300919764198671,-0.952241439532216,0.0518028604637758));
#122774=DIRECTION('',(0.,0.,1.));
#122775=DIRECTION('',(0.,0.,1.));
#122776=DIRECTION('center_axis',(0.,0.,1.));
#122777=DIRECTION('ref_axis',(-0.981559156991069,0.191158628701354,0.));
#122778=DIRECTION('center_axis',(0.,0.,-1.));
#122779=DIRECTION('ref_axis',(0.981559156991069,-0.191158628701354,0.));
#122780=DIRECTION('center_axis',(0.880138289977623,-0.411973900021994,-0.235868811452329));
#122781=DIRECTION('ref_axis',(0.455037505950061,0.59056779781637,0.666461209944789));
#122782=DIRECTION('center_axis',(0.970415141311856,0.0515786515599078,0.235868811452368));
#122783=DIRECTION('ref_axis',(0.200161280821526,-0.718167750109119,-0.666461209946305));
#122784=DIRECTION('center_axis',(0.,0.,-1.));
#122785=DIRECTION('ref_axis',(0.981559156991067,-0.191158628701366,0.));
#122786=DIRECTION('center_axis',(-0.984181945286122,0.177160657519735,-6.76296429840134E-17));
#122787=DIRECTION('ref_axis',(0.177160657519735,0.984181945286122,6.93889390390728E-14));
#122788=DIRECTION('center_axis',(0.,0.,1.));
#122789=DIRECTION('ref_axis',(-0.981559156991067,0.191158628701366,0.));
#122790=DIRECTION('center_axis',(-0.978737286693006,0.205117828666384,-1.38914942345546E-16));
#122791=DIRECTION('ref_axis',(-0.205117828666384,-0.978737286693006,4.74549138297015E-31));
#122792=DIRECTION('center_axis',(0.,0.,-1.));
#122793=DIRECTION('ref_axis',(0.981559156991067,-0.191158628701365,0.));
#122794=DIRECTION('center_axis',(0.,0.,1.));
#122795=DIRECTION('ref_axis',(-0.981559156991067,0.191158628701365,0.));
#122796=DIRECTION('center_axis',(0.,0.,1.));
#122797=DIRECTION('ref_axis',(-0.981559156991067,0.191158628701365,0.));
#122798=DIRECTION('center_axis',(-0.225405697069191,0.71328198075486,0.663642288932205));
#122799=DIRECTION('ref_axis',(0.135843576023242,0.697528052329421,-0.703563173472534));
#122800=DIRECTION('center_axis',(-0.226053981933632,0.715333436943476,0.661209249211309));
#122801=DIRECTION('ref_axis',(0.135402742613117,0.695264465938647,-0.705884848750767));
#122802=DIRECTION('center_axis',(-0.477974260290917,-0.57822394905155,-0.661209249211308));
#122803=DIRECTION('ref_axis',(-0.13540274261313,-0.695264465938645,0.705884848750767));
#122804=DIRECTION('center_axis',(-0.476603510367002,-0.57656569985276,-0.663642288932184));
#122805=DIRECTION('ref_axis',(-0.135843576023242,-0.6975280523294,0.703563173472554));
#122806=DIRECTION('center_axis',(0.,0.,1.));
#122807=DIRECTION('ref_axis',(-0.981559156991067,0.191158628701365,0.));
#122808=DIRECTION('center_axis',(0.,0.,1.));
#122809=DIRECTION('ref_axis',(-0.981559156991067,0.191158628701365,0.));
#122810=DIRECTION('center_axis',(0.,0.,1.));
#122811=DIRECTION('ref_axis',(0.981559156991053,-0.191158628701434,0.));
#122812=DIRECTION('center_axis',(0.,0.,-1.));
#122813=DIRECTION('ref_axis',(-0.981559156991067,0.191158628701366,0.));
#122814=DIRECTION('center_axis',(-0.80999547633231,0.586436124672751,0.));
#122815=DIRECTION('ref_axis',(-0.586436124672751,-0.80999547633231,0.));
#122816=DIRECTION('',(0.,0.,1.));
#122817=DIRECTION('center_axis',(0.80999260330302,-0.586440092924393,2.28597554479797E-6));
#122818=DIRECTION('ref_axis',(0.55514037291836,0.766762603911661,0.322326349525871));
#122819=DIRECTION('',(0.,0.,-1.));
#122820=DIRECTION('center_axis',(0.93225667453446,0.361797585378826,0.));
#122821=DIRECTION('ref_axis',(-0.361797585378826,0.932256674534461,0.));
#122822=DIRECTION('center_axis',(-0.93225667453447,-0.361797585378803,-6.98055585703023E-15));
#122823=DIRECTION('ref_axis',(0.361311810775726,-0.931004961879828,0.0518028604336393));
#122824=DIRECTION('',(0.,0.,1.));
#122825=DIRECTION('',(0.,0.,1.));
#122826=DIRECTION('center_axis',(0.,0.,1.));
#122827=DIRECTION('ref_axis',(-0.991790013823251,0.127877161684469,0.));
#122828=DIRECTION('center_axis',(0.,0.,-1.));
#122829=DIRECTION('ref_axis',(0.991790013823251,-0.127877161684469,0.));
#122830=DIRECTION('center_axis',(0.904725209867041,-0.354736801608044,-0.235868811452327));
#122831=DIRECTION('ref_axis',(0.416264773868949,0.618508766020696,0.666461209967533));
#122832=DIRECTION('center_axis',(0.965116663775578,0.113647389264953,0.235868811452381));
#122833=DIRECTION('ref_axis',(0.245763193733702,-0.703867820162628,-0.666461209932972));
#122834=DIRECTION('center_axis',(0.,0.,-1.));
#122835=DIRECTION('ref_axis',(0.991790013823247,-0.127877161684499,0.));
#122836=DIRECTION('center_axis',(-0.993510560225566,0.113739908212912,-6.76296429840134E-17));
#122837=DIRECTION('ref_axis',(0.113739908212912,0.993510560225566,-5.39260384428426E-32));
#122838=DIRECTION('center_axis',(0.,0.,1.));
#122839=DIRECTION('ref_axis',(-0.991790013823247,0.127877161684499,0.));
#122840=DIRECTION('center_axis',(-0.989868310372872,0.141988478826823,-1.38914942345546E-16));
#122841=DIRECTION('ref_axis',(-0.141988478826823,-0.989868310372872,3.05067303190938E-31));
#122842=DIRECTION('center_axis',(0.,0.,-1.));
#122843=DIRECTION('ref_axis',(0.991790013823245,-0.127877161684511,0.));
#122844=DIRECTION('center_axis',(0.,0.,1.));
#122845=DIRECTION('ref_axis',(-0.991790013823245,0.127877161684511,0.));
#122846=DIRECTION('center_axis',(0.,0.,1.));
#122847=DIRECTION('ref_axis',(-0.991790013823245,0.127877161684511,0.));
#122848=DIRECTION('center_axis',(-0.27064271030512,0.697374673830017,0.663642288932205));
#122849=DIRECTION('ref_axis',(0.0908736950716613,0.704798433935037,-0.703563173472533));
#122850=DIRECTION('center_axis',(-0.271421100448064,0.699380379328001,0.661209249211309));
#122851=DIRECTION('ref_axis',(0.0905787958790554,0.70251125403171,-0.705884848750768));
#122852=DIRECTION('center_axis',(-0.439945275296721,-0.607659841935857,
-0.661209249211308));
#122853=DIRECTION('ref_axis',(-0.0905787958790776,-0.702511254031706,0.705884848750769));
#122854=DIRECTION('center_axis',(-0.438683586116486,-0.605917175538729,
-0.663642288932184));
#122855=DIRECTION('ref_axis',(-0.0908736950716505,-0.704798433935021,0.703563173472551));
#122856=DIRECTION('center_axis',(0.,0.,1.));
#122857=DIRECTION('ref_axis',(-0.991790013823245,0.127877161684511,0.));
#122858=DIRECTION('center_axis',(0.,0.,1.));
#122859=DIRECTION('ref_axis',(-0.991790013823245,0.127877161684511,0.));
#122860=DIRECTION('center_axis',(0.,0.,1.));
#122861=DIRECTION('ref_axis',(0.991790013823245,-0.127877161684511,0.));
#122862=DIRECTION('center_axis',(0.,0.,-1.));
#122863=DIRECTION('ref_axis',(-0.991790013823247,0.127877161684499,0.));
#122864=DIRECTION('center_axis',(-0.845904345266863,0.533334640407541,0.));
#122865=DIRECTION('ref_axis',(-0.533334640407541,-0.845904345266863,0.));
#122866=DIRECTION('',(0.,0.,1.));
#122867=DIRECTION('center_axis',(0.845901732387273,-0.533338784581606,2.28597554008475E-6));
#122868=DIRECTION('ref_axis',(0.504873128786085,0.800755173732798,0.322326349481245));
#122869=DIRECTION('',(0.,0.,-1.));
#122870=DIRECTION('center_axis',(0.907160802328702,0.420784123652907,0.));
#122871=DIRECTION('ref_axis',(-0.420784123652907,0.907160802328703,0.));
#122872=DIRECTION('center_axis',(-0.907160802328718,-0.420784123652873,
-1.98035334639662E-14));
#122873=DIRECTION('ref_axis',(0.420219149621948,-0.905942785140381,0.0518028603756245));
#122874=DIRECTION('',(0.,0.,1.));
#122875=DIRECTION('',(0.,0.,1.));
#122876=DIRECTION('center_axis',(0.,0.,1.));
#122877=DIRECTION('ref_axis',(-0.997945392750336,0.0640702199807125,0.));
#122878=DIRECTION('center_axis',(0.,0.,-1.));
#122879=DIRECTION('ref_axis',(0.997945392750336,-0.0640702199807125,0.));
#122880=DIRECTION('center_axis',(0.925594419806154,-0.296042013585577,-0.235868811452269));
#122881=DIRECTION('ref_axis',(0.375781520549068,0.643908149076571,0.666461209948947));
#122882=DIRECTION('center_axis',(0.955852314850975,0.175249125470216,0.235868811452378));
#122883=DIRECTION('ref_axis',(0.290355212969804,-0.686675546343255,-0.666461209940573));
#122884=DIRECTION('center_axis',(0.,0.,-1.));
#122885=DIRECTION('ref_axis',(0.997945392750337,-0.0640702199807057,0.));
#122886=DIRECTION('center_axis',(-0.998756627165697,0.0498517772261083,
-6.76296429840134E-17));
#122887=DIRECTION('ref_axis',(0.0498517772261083,0.998756627165697,-3.73630409211124E-32));
#122888=DIRECTION('center_axis',(0.,0.,1.));
#122889=DIRECTION('ref_axis',(-0.997945392750337,0.0640702199807057,0.));
#122890=DIRECTION('center_axis',(-0.996931752839329,0.0782756678713304,
-1.38914942345546E-16));
#122891=DIRECTION('ref_axis',(-0.0782756678713304,-0.996931752839329,-1.95674482349743E-31));
#122892=DIRECTION('center_axis',(0.,0.,-1.));
#122893=DIRECTION('ref_axis',(0.997945392750337,-0.0640702199806998,0.));
#122894=DIRECTION('center_axis',(0.,0.,1.));
#122895=DIRECTION('ref_axis',(-0.997945392750337,0.0640702199806998,0.));
#122896=DIRECTION('center_axis',(0.,0.,1.));
#122897=DIRECTION('ref_axis',(-0.997945392750337,0.0640702199806997,0.));
#122898=DIRECTION('center_axis',(-0.314767594591725,0.678601704784009,0.663642288932205));
#122899=DIRECTION('ref_axis',(0.0455303946146855,0.709172647596824,-0.703563173472533));
#122900=DIRECTION('center_axis',(-0.315672891441111,0.680553417717247,0.661209249211309));
#122901=DIRECTION('ref_axis',(0.0453826414436359,0.706871272693765,-0.705884848750768));
#122902=DIRECTION('center_axis',(-0.400108460798365,-0.634598730187022,
-0.661209249211308));
#122903=DIRECTION('ref_axis',(-0.0453826414436631,-0.706871272693762,0.705884848750769));
#122904=DIRECTION('center_axis',(-0.398961016913284,-0.632778807581583,
-0.663642288932184));
#122905=DIRECTION('ref_axis',(-0.0455303946146791,-0.709172647596805,0.703563173472553));
#122906=DIRECTION('center_axis',(0.,0.,1.));
#122907=DIRECTION('ref_axis',(-0.997945392750337,0.0640702199806997,0.));
#122908=DIRECTION('center_axis',(0.,0.,1.));
#122909=DIRECTION('ref_axis',(-0.997945392750337,0.0640702199806997,0.));
#122910=DIRECTION('center_axis',(0.,0.,1.));
#122911=DIRECTION('ref_axis',(0.997945392750337,-0.0640702199806997,0.));
#122912=DIRECTION('center_axis',(0.,0.,-1.));
#122913=DIRECTION('ref_axis',(-0.997945392750337,0.0640702199807057,0.));
#122914=DIRECTION('center_axis',(-0.878337211800797,0.47804156970498,0.));
#122915=DIRECTION('ref_axis',(-0.47804156970498,-0.878337211800797,0.));
#122916=DIRECTION('',(0.,0.,1.));
#122917=DIRECTION('center_axis',(0.878334869807783,-0.478045872772184,2.28597554380844E-6));
#122918=DIRECTION('ref_axis',(0.452531252665384,0.831457268774235,0.322326349471446));
#122919=DIRECTION('',(0.,0.,-1.));
#122920=DIRECTION('center_axis',(0.878337211800797,0.47804156970498,0.));
#122921=DIRECTION('ref_axis',(-0.47804156970498,0.878337211800797,0.));
#122922=DIRECTION('center_axis',(-0.878337211800815,-0.478041569704948,
-1.94241554282581E-14));
#122923=DIRECTION('ref_axis',(0.477399717843322,-0.877157895167585,0.0518028604257383));
#122924=DIRECTION('',(0.,0.,1.));
#122925=DIRECTION('',(0.,0.,1.));
#122926=DIRECTION('center_axis',(0.,0.,1.));
#122927=DIRECTION('ref_axis',(-1.,0.,0.));
#122928=DIRECTION('center_axis',(0.,0.,-1.));
#122929=DIRECTION('ref_axis',(1.,0.,0.));
#122930=DIRECTION('center_axis',(0.942660163734981,-0.236130725428042,-0.235868811452395));
#122931=DIRECTION('ref_axis',(0.333754100353815,0.666661575414249,0.666461209946391));
#122932=DIRECTION('center_axis',(0.942660163734932,0.236130725428364,0.235868811452266));
#122933=DIRECTION('ref_axis',(0.333754100353955,-0.666661575429315,-0.66646120993125));
#122934=DIRECTION('center_axis',(0.,0.,-1.));
#122935=DIRECTION('ref_axis',(1.,0.,0.));
#122936=DIRECTION('center_axis',(-0.999898588892179,-0.0142412054064829,
-6.76296429840134E-17));
#122937=DIRECTION('ref_axis',(-0.0142412054064829,0.999898588892179,-3.2740809054583E-33));
#122938=DIRECTION('center_axis',(0.,0.,1.));
#122939=DIRECTION('ref_axis',(-1.,0.,0.));
#122940=DIRECTION('center_axis',(-0.999898588892179,0.0142412054064834,
-1.38914942345546E-16));
#122941=DIRECTION('ref_axis',(-0.0142412054064834,-0.999898588892179,3.85185988877447E-34));
#122942=DIRECTION('center_axis',(0.,0.,-1.));
#122943=DIRECTION('ref_axis',(1.,0.,0.));
#122944=DIRECTION('center_axis',(0.,0.,1.));
#122945=DIRECTION('ref_axis',(-1.,0.,0.));
#122946=DIRECTION('center_axis',(0.,0.,1.));
#122947=DIRECTION('ref_axis',(-1.,0.,0.));
#122948=DIRECTION('center_axis',(-0.357599031314712,0.657040215773436,0.663642288932205));
#122949=DIRECTION('ref_axis',(4.21884749357559E-15,0.710632718732581,-0.703563173472532));
#122950=DIRECTION('center_axis',(-0.358627514811599,0.658929916134845,0.661209249211309));
#122951=DIRECTION('ref_axis',(-9.74220704108575E-15,0.70832660567291,-0.705884848750767));
#122952=DIRECTION('center_axis',(-0.358627514811598,-0.658929916134846,
-0.661209249211308));
#122953=DIRECTION('ref_axis',(-9.24260668000443E-15,-0.708326605672909,
0.705884848750768));
#122954=DIRECTION('center_axis',(-0.35759903131472,-0.657040215773453,-0.663642288932184));
#122955=DIRECTION('ref_axis',(5.60662627435704E-15,-0.710632718732561,0.703563173472552));
#122956=DIRECTION('center_axis',(0.,0.,1.));
#122957=DIRECTION('ref_axis',(-1.,0.,0.));
#122958=DIRECTION('center_axis',(0.,0.,1.));
#122959=DIRECTION('ref_axis',(-1.,0.,0.));
#122960=DIRECTION('center_axis',(0.,0.,1.));
#122961=DIRECTION('ref_axis',(1.,0.,0.));
#122962=DIRECTION('center_axis',(0.,0.,-1.));
#122963=DIRECTION('ref_axis',(-1.,0.,0.));
#122964=DIRECTION('center_axis',(-0.907160802328708,0.420784123652894,0.));
#122965=DIRECTION('ref_axis',(-0.420784123652894,-0.907160802328709,0.));
#122966=DIRECTION('',(0.,0.,1.));
#122967=DIRECTION('center_axis',(0.907158740846047,-0.42078856793096,2.28597552685862E-6));
#122968=DIRECTION('ref_axis',(0.398329828560756,0.858742727554402,0.322326349452206));
#122969=DIRECTION('',(0.,0.,-1.));
#122970=DIRECTION('center_axis',(0.845904345266855,0.533334640407553,0.));
#122971=DIRECTION('ref_axis',(-0.533334640407553,0.845904345266855,0.));
#122972=DIRECTION('center_axis',(-0.845904345266892,-0.533334640407494,
-3.18298171959134E-14));
#122973=DIRECTION('ref_axis',(0.532618548224074,-0.844768575257462,0.0518028603955189));
#122974=DIRECTION('',(0.,0.,1.));
#122975=DIRECTION('',(0.,0.,1.));
#122976=DIRECTION('center_axis',(0.,0.,1.));
#122977=DIRECTION('ref_axis',(-0.997945392750336,-0.0640702199807127,0.));
#122978=DIRECTION('center_axis',(0.,0.,-1.));
#122979=DIRECTION('ref_axis',(0.997945392750336,0.0640702199807127,0.));
#122980=DIRECTION('center_axis',(0.955852314850978,-0.175249125470207,-0.235868811452373));
#122981=DIRECTION('ref_axis',(0.290355212971756,0.686675546312613,0.666461209971294));
#122982=DIRECTION('center_axis',(0.925594419806159,0.296042013585558,0.235868811452273));
#122983=DIRECTION('ref_axis',(0.375781520550134,-0.643908149093292,-0.66646120993219));
#122984=DIRECTION('center_axis',(0.,0.,-1.));
#122985=DIRECTION('ref_axis',(0.997945392750336,0.0640702199807201,0.));
#122986=DIRECTION('center_axis',(-0.996931752839328,-0.0782756678713443,
-6.76296429840134E-17));
#122987=DIRECTION('ref_axis',(-0.0782756678713443,0.996931752839328,2.54222752659115E-32));
#122988=DIRECTION('center_axis',(0.,0.,1.));
#122989=DIRECTION('ref_axis',(-0.997945392750336,-0.0640702199807201,0.));
#122990=DIRECTION('center_axis',(-0.998756627165696,-0.0498517772261222,
-1.38914942345546E-16));
#122991=DIRECTION('ref_axis',(0.0498517772261222,-0.998756627165696,5.39260384428426E-32));
#122992=DIRECTION('center_axis',(0.,0.,-1.));
#122993=DIRECTION('ref_axis',(0.997945392750335,0.0640702199807342,0.));
#122994=DIRECTION('center_axis',(0.,0.,1.));
#122995=DIRECTION('ref_axis',(-0.997945392750335,-0.0640702199807344,0.));
#122996=DIRECTION('center_axis',(0.,0.,1.));
#122997=DIRECTION('ref_axis',(-0.997945392750335,-0.0640702199807344,0.));
#122998=DIRECTION('center_axis',(-0.398961016913283,0.632778807581561,0.663642288932205));
#122999=DIRECTION('ref_axis',(-0.0455303946146904,0.709172647596825,-0.703563173472532));
#123000=DIRECTION('center_axis',(-0.400108460798375,0.634598730187015,0.661209249211309));
#123001=DIRECTION('ref_axis',(-0.0453826414436742,0.706871272693762,-0.705884848750769));
#123002=DIRECTION('center_axis',(-0.3156728914411,-0.680553417717253,-0.661209249211308));
#123003=DIRECTION('ref_axis',(0.0453826414436472,-0.706871272693764,0.705884848750769));
#123004=DIRECTION('center_axis',(-0.314767594591723,-0.67860170478403,-0.663642288932184));
#123005=DIRECTION('ref_axis',(0.0455303946146966,-0.709172647596804,0.703563173472552));
#123006=DIRECTION('center_axis',(0.,0.,1.));
#123007=DIRECTION('ref_axis',(-0.997945392750335,-0.0640702199807344,0.));
#123008=DIRECTION('center_axis',(0.,0.,1.));
#123009=DIRECTION('ref_axis',(-0.997945392750335,-0.0640702199807344,0.));
#123010=DIRECTION('center_axis',(0.,0.,1.));
#123011=DIRECTION('ref_axis',(0.997945392750335,0.0640702199807343,0.));
#123012=DIRECTION('center_axis',(0.,0.,-1.));
#123013=DIRECTION('ref_axis',(-0.997945392750336,-0.0640702199807201,0.));
#123014=DIRECTION('center_axis',(-0.932256674534466,0.361797585378813,0.));
#123015=DIRECTION('ref_axis',(-0.361797585378813,-0.932256674534466,0.));
#123016=DIRECTION('',(0.,0.,1.));
#123017=DIRECTION('center_axis',(0.93225490203322,-0.361802152605269,2.28597552739037E-6));
#123018=DIRECTION('ref_axis',(0.342491581739211,0.882499428244109,0.322326349507133));
#123019=DIRECTION('',(0.,0.,-1.));
#123020=DIRECTION('center_axis',(0.809995476332301,0.586436124672763,0.));
#123021=DIRECTION('ref_axis',(-0.586436124672763,0.809995476332301,0.));
#123022=DIRECTION('center_axis',(-0.809995476332275,-0.586436124672799,
3.11089989280751E-14));
#123023=DIRECTION('ref_axis',(0.585648734744481,-0.808907920069597,0.0518028603541021));
#123024=DIRECTION('',(0.,0.,1.));
#123025=DIRECTION('',(0.,0.,1.));
#123026=DIRECTION('center_axis',(0.,0.,1.));
#123027=DIRECTION('ref_axis',(-0.991790013823243,-0.127877161684531,0.));
#123028=DIRECTION('center_axis',(0.,0.,-1.));
#123029=DIRECTION('ref_axis',(0.991790013823243,0.127877161684531,0.));
#123030=DIRECTION('center_axis',(0.965116663775579,-0.113647389264971,-0.235868811452367));
#123031=DIRECTION('ref_axis',(0.245763193736745,0.703867820139019,0.666461209956784));
#123032=DIRECTION('center_axis',(0.904725209867048,0.354736801608014,0.235868811452345));
#123033=DIRECTION('ref_axis',(0.416264773870607,-0.618508766033597,-0.666461209954525));
#123034=DIRECTION('center_axis',(0.,0.,-1.));
#123035=DIRECTION('ref_axis',(0.991790013823245,0.127877161684513,0.));
#123036=DIRECTION('center_axis',(-0.98986831037287,-0.141988478826837,-6.76296429840134E-17));
#123037=DIRECTION('ref_axis',(-0.141988478826837,0.98986831037287,8.0118685686509E-32));
#123038=DIRECTION('center_axis',(0.,0.,1.));
#123039=DIRECTION('ref_axis',(-0.991790013823245,-0.127877161684513,0.));
#123040=DIRECTION('center_axis',(-0.993510560225565,-0.113739908212926,
-1.38914942345546E-16));
#123041=DIRECTION('ref_axis',(0.113739908212926,-0.993510560225564,3.08148791101958E-32));
#123042=DIRECTION('center_axis',(0.,0.,-1.));
#123043=DIRECTION('ref_axis',(0.991790013823245,0.127877161684512,0.));
#123044=DIRECTION('center_axis',(0.,0.,1.));
#123045=DIRECTION('ref_axis',(-0.991790013823245,-0.127877161684512,0.));
#123046=DIRECTION('center_axis',(0.,0.,1.));
#123047=DIRECTION('ref_axis',(-0.991790013823245,-0.127877161684512,0.));
#123048=DIRECTION('center_axis',(-0.438683586116484,0.605917175538708,0.663642288932205));
#123049=DIRECTION('ref_axis',(-0.0908736950716741,0.704798433935035,-0.703563173472534));
#123050=DIRECTION('center_axis',(-0.43994527529673,0.607659841935849,0.661209249211309));
#123051=DIRECTION('ref_axis',(-0.0905787958790902,0.702511254031705,-0.705884848750768));
#123052=DIRECTION('center_axis',(-0.271421100448053,-0.699380379328006,
-0.661209249211308));
#123053=DIRECTION('ref_axis',(0.0905787958790646,-0.702511254031708,0.705884848750769));
#123054=DIRECTION('center_axis',(-0.270642710305116,-0.697374673830039,
-0.663642288932184));
#123055=DIRECTION('ref_axis',(0.0908736950716735,-0.704798433935017,0.703563173472552));
#123056=DIRECTION('center_axis',(0.,0.,1.));
#123057=DIRECTION('ref_axis',(-0.991790013823245,-0.127877161684512,0.));
#123058=DIRECTION('center_axis',(0.,0.,1.));
#123059=DIRECTION('ref_axis',(-0.991790013823245,-0.127877161684512,0.));
#123060=DIRECTION('center_axis',(0.,0.,1.));
#123061=DIRECTION('ref_axis',(0.991790013823245,0.127877161684511,0.));
#123062=DIRECTION('center_axis',(0.,0.,-1.));
#123063=DIRECTION('ref_axis',(-0.991790013823245,-0.127877161684513,0.));
#123064=DIRECTION('center_axis',(-0.953521704096131,0.301324343221071,0.));
#123065=DIRECTION('ref_axis',(-0.301324343221071,-0.953521704096131,0.));
#123066=DIRECTION('',(0.,0.,1.));
#123067=DIRECTION('center_axis',(0.953520227859841,-0.301329014628347,2.28597558455223E-6));
#123068=DIRECTION('ref_axis',(0.285245963537521,0.902629749458501,0.322326349648977));
#123069=DIRECTION('',(0.,0.,-1.));
#123070=DIRECTION('center_axis',(0.770758162242013,0.637127817111539,0.));
#123071=DIRECTION('ref_axis',(-0.637127817111539,0.770758162242013,0.));
#123072=DIRECTION('center_axis',(-0.770758162242,-0.637127817111555,-4.55253642849831E-16));
#123073=DIRECTION('ref_axis',(0.636272364988702,-0.769723288723081,0.0518028604326862));
#123074=DIRECTION('',(0.,0.,1.));
#123075=DIRECTION('',(0.,0.,1.));
#123076=DIRECTION('center_axis',(0.,0.,1.));
#123077=DIRECTION('ref_axis',(-0.981559156991069,-0.191158628701354,0.));
#123078=DIRECTION('center_axis',(0.,0.,-1.));
#123079=DIRECTION('ref_axis',(0.981559156991069,0.191158628701354,0.));
#123080=DIRECTION('center_axis',(0.970415141311862,-0.0515786515600848,
-0.235868811452304));
#123081=DIRECTION('ref_axis',(0.200161280820835,0.718167750113079,0.666461209942244));
#123082=DIRECTION('center_axis',(0.880138289977647,0.411973900021917,0.235868811452373));
#123083=DIRECTION('ref_axis',(0.4550375059517,-0.590567797824916,-0.666461209936097));
#123084=DIRECTION('center_axis',(0.,0.,-1.));
#123085=DIRECTION('ref_axis',(0.981559156991064,0.19115862870138,0.));
#123086=DIRECTION('center_axis',(-0.978737286693004,-0.205117828666397,
-6.76296429840134E-17));
#123087=DIRECTION('ref_axis',(-0.205117828666397,0.978737286693004,-1.34044724129352E-31));
#123088=DIRECTION('center_axis',(0.,0.,1.));
#123089=DIRECTION('ref_axis',(-0.981559156991064,-0.19115862870138,0.));
#123090=DIRECTION('center_axis',(-0.98418194528612,-0.177160657519749,-1.38914942345546E-16));
#123091=DIRECTION('ref_axis',(0.177160657519749,-0.984181945286119,1.54074395550979E-31));
#123092=DIRECTION('center_axis',(0.,0.,-1.));
#123093=DIRECTION('ref_axis',(0.981559156991067,0.191158628701365,0.));
#123094=DIRECTION('center_axis',(0.,0.,1.));
#123095=DIRECTION('ref_axis',(-0.981559156991067,-0.191158628701365,0.));
#123096=DIRECTION('center_axis',(0.,0.,1.));
#123097=DIRECTION('ref_axis',(-0.981559156991067,-0.191158628701365,0.));
#123098=DIRECTION('center_axis',(-0.476603510366998,0.576565699852739,0.663642288932205));
#123099=DIRECTION('ref_axis',(-0.13584357602325,0.697528052329421,-0.703563173472532));
#123100=DIRECTION('center_axis',(-0.477974260290926,0.578223949051541,0.661209249211309));
#123101=DIRECTION('ref_axis',(-0.135402742613152,0.695264465938639,-0.705884848750769));
#123102=DIRECTION('center_axis',(-0.22605398193362,-0.715333436943481,-0.661209249211308));
#123103=DIRECTION('ref_axis',(0.135402742613124,-0.695264465938644,0.705884848750769));
#123104=DIRECTION('center_axis',(-0.225405697069186,-0.713281980754881,
-0.663642288932184));
#123105=DIRECTION('ref_axis',(0.135843576023254,-0.6975280523294,0.703563173472552));
#123106=DIRECTION('center_axis',(0.,0.,1.));
#123107=DIRECTION('ref_axis',(-0.981559156991067,-0.191158628701366,0.));
#123108=DIRECTION('center_axis',(0.,0.,1.));
#123109=DIRECTION('ref_axis',(-0.981559156991067,-0.191158628701366,0.));
#123110=DIRECTION('center_axis',(0.,0.,1.));
#123111=DIRECTION('ref_axis',(0.981559156991053,0.191158628701435,0.));
#123112=DIRECTION('center_axis',(0.,0.,-1.));
#123113=DIRECTION('ref_axis',(-0.981559156991064,-0.19115862870138,0.));
#123114=DIRECTION('center_axis',(-0.970868508445902,0.239612894703166,0.));
#123115=DIRECTION('ref_axis',(-0.239612894703166,-0.970868508445902,0.));
#123116=DIRECTION('',(0.,0.,1.));
#123117=DIRECTION('center_axis',(0.970867334540797,-0.239617651095285,2.28597557668383E-6));
#123118=DIRECTION('ref_axis',(0.226828208517194,0.919050971517716,0.322326349486391));
#123119=DIRECTION('',(0.,0.,-1.));
#123120=DIRECTION('center_axis',(0.728353637535965,0.685201414686315,0.));
#123121=DIRECTION('ref_axis',(-0.685201414686315,0.728353637535965,0.));
#123122=DIRECTION('center_axis',(-0.72835363753595,-0.685201414686332,1.04328959819753E-14));
#123123=DIRECTION('ref_axis',(0.684281415609948,-0.72737569928385,0.051802860366741));
#123124=DIRECTION('',(0.,0.,1.));
#123125=DIRECTION('',(0.,0.,1.));
#123126=DIRECTION('center_axis',(0.,0.,1.));
#123127=DIRECTION('ref_axis',(-0.967294863039035,-0.253654583909488,0.));
#123128=DIRECTION('center_axis',(0.,0.,-1.));
#123129=DIRECTION('ref_axis',(0.967294863039035,0.253654583909488,0.));
#123130=DIRECTION('center_axis',(0.971725974879087,0.0107020338879415,-0.235868811452361));
#123131=DIRECTION('ref_axis',(0.153736862271298,0.729516574733416,0.666461209950137));
#123132=DIRECTION('center_axis',(0.851934693065624,0.467518109312609,0.235868811452351));
#123133=DIRECTION('ref_axis',(0.49194039131042,-0.560200059829388,-0.666461209947361));
#123134=DIRECTION('center_axis',(0.,0.,-1.));
#123135=DIRECTION('ref_axis',(0.967294863039027,0.253654583909515,0.));
#123136=DIRECTION('center_axis',(-0.963584421563626,-0.267404305350331,
-6.76296429840134E-17));
#123137=DIRECTION('ref_axis',(-0.267404305350331,0.963584421563625,6.93889390390731E-14));
#123138=DIRECTION('center_axis',(0.,0.,1.));
#123139=DIRECTION('ref_axis',(-0.967294863039027,-0.253654583909515,0.));
#123140=DIRECTION('center_axis',(-0.970809115627128,-0.239853415683982,
-1.38914942345546E-16));
#123141=DIRECTION('ref_axis',(0.239853415683982,-0.970809115627128,-2.46519032881566E-32));
#123142=DIRECTION('center_axis',(0.,0.,-1.));
#123143=DIRECTION('ref_axis',(0.967294863039023,0.25365458390953,0.));
#123144=DIRECTION('center_axis',(0.,0.,1.));
#123145=DIRECTION('ref_axis',(-0.967294863039023,-0.25365458390953,0.));
#123146=DIRECTION('center_axis',(0.,0.,1.));
#123147=DIRECTION('ref_axis',(-0.967294863039023,-0.25365458390953,0.));
#123148=DIRECTION('center_axis',(-0.512564968562282,0.54484499203312,0.663642288932205));
#123149=DIRECTION('ref_axis',(-0.180255246582595,0.687391378337486,-0.703563173472532));
#123150=DIRECTION('center_axis',(-0.514039146524428,0.546412009931933,0.661209249211309));
#123151=DIRECTION('ref_axis',(-0.17967029043401,0.685160687021275,-0.705884848750767));
#123152=DIRECTION('center_axis',(-0.179757959118996,-0.728347036028013,
-0.661209249211308));
#123153=DIRECTION('ref_axis',(0.179670290433992,-0.685160687021278,0.705884848750768));
#123154=DIRECTION('center_axis',(-0.179242443474628,-0.726258259022296,
-0.663642288932184));
#123155=DIRECTION('ref_axis',(0.180255246582597,-0.687391378337463,0.703563173472553));
#123156=DIRECTION('center_axis',(0.,0.,1.));
#123157=DIRECTION('ref_axis',(-0.967294863039023,-0.25365458390953,0.));
#123158=DIRECTION('center_axis',(0.,0.,1.));
#123159=DIRECTION('ref_axis',(-0.967294863039023,-0.25365458390953,0.));
#123160=DIRECTION('center_axis',(0.,0.,1.));
#123161=DIRECTION('ref_axis',(0.967294863039023,0.25365458390953,0.));
#123162=DIRECTION('center_axis',(0.,0.,-1.));
#123163=DIRECTION('ref_axis',(-0.967294863039028,-0.253654583909515,0.));
#123164=DIRECTION('center_axis',(-0.984225805843826,0.17691682540412,0.));
#123165=DIRECTION('ref_axis',(-0.17691682540412,-0.984225805843826,0.));
#123166=DIRECTION('',(0.,0.,1.));
#123167=DIRECTION('center_axis',(0.984224939093727,-0.176921647236071,2.28597557197196E-6));
#123168=DIRECTION('ref_axis',(0.16747836771619,0.931695615942342,0.322326349498364));
#123169=DIRECTION('',(0.,0.,-1.));
#123170=DIRECTION('center_axis',(0.682956151501917,0.730459372672903,0.));
#123171=DIRECTION('ref_axis',(-0.730459372672903,0.682956151501917,0.));
#123172=DIRECTION('center_axis',(-0.682956151501931,-0.73045937267289,-5.27335469634203E-15));
#123173=DIRECTION('ref_axis',(0.729478607109897,-0.682039167067909,0.0518028604839242));
#123174=DIRECTION('',(0.,0.,1.));
#123175=DIRECTION('',(0.,0.,1.));
#123176=DIRECTION('center_axis',(0.,0.,1.));
#123177=DIRECTION('ref_axis',(-0.949055747010657,-0.315108218023656,0.));
#123178=DIRECTION('center_axis',(0.,0.,-1.));
#123179=DIRECTION('ref_axis',(0.949055747010657,0.315108218023656,0.));
#123180=DIRECTION('center_axis',(0.969043777980998,0.0729387423828591,-0.235868811452303));
#123181=DIRECTION('ref_axis',(0.106680705979194,0.737867659268036,0.666461209957557));
#123182=DIRECTION('center_axis',(0.820230313760368,0.521141186409817,0.235868811452335));
#123183=DIRECTION('ref_axis',(0.526821788084768,-0.527530339643292,-0.666461209940235));
#123184=DIRECTION('center_axis',(0.,0.,-1.));
#123185=DIRECTION('ref_axis',(0.949055747010666,0.315108218023628,0.));
#123186=DIRECTION('center_axis',(-0.944471981357833,-0.328591960385537,
-6.76296429840134E-17));
#123187=DIRECTION('ref_axis',(-0.328591960385537,0.944471981357833,6.93889390390723E-14));
#123188=DIRECTION('center_axis',(0.,0.,1.));
#123189=DIRECTION('ref_axis',(-0.949055747010666,-0.315108218023628,0.));
#123190=DIRECTION('center_axis',(-0.953447023074123,-0.301560564714772,
-1.38914942345546E-16));
#123191=DIRECTION('ref_axis',(0.301560564714772,-0.953447023074123,-1.10317267214501E-30));
#123192=DIRECTION('center_axis',(0.,0.,-1.));
#123193=DIRECTION('ref_axis',(0.949055747010662,0.315108218023641,0.));
#123194=DIRECTION('center_axis',(0.,0.,1.));
#123195=DIRECTION('ref_axis',(-0.949055747010662,-0.315108218023641,0.));
#123196=DIRECTION('center_axis',(0.,0.,1.));
#123197=DIRECTION('ref_axis',(-0.949055747010662,-0.315108218023641,0.));
#123198=DIRECTION('center_axis',(-0.546420187356902,0.510885399272354,0.663642288932205));
#123199=DIRECTION('ref_axis',(-0.223926209669107,0.674430065726971,-0.703563173472533));
#123200=DIRECTION('center_axis',(-0.547991735643811,0.512354746658505,0.661209249211309));
#123201=DIRECTION('ref_axis',(-0.223199534492319,0.672241435874434,-0.705884848750766));
#123202=DIRECTION('center_axis',(-0.13272327229239,-0.738367700911557,-0.661209249211308));
#123203=DIRECTION('ref_axis',(0.223199534492305,-0.672241435874436,0.705884848750769));
#123204=DIRECTION('center_axis',(-0.13234264423245,-0.736250186321481,-0.663642288932184));
#123205=DIRECTION('ref_axis',(0.223926209669108,-0.67443006572695,0.703563173472552));
#123206=DIRECTION('center_axis',(0.,0.,1.));
#123207=DIRECTION('ref_axis',(-0.949055747010662,-0.315108218023641,0.));
#123208=DIRECTION('center_axis',(0.,0.,1.));
#123209=DIRECTION('ref_axis',(-0.949055747010662,-0.315108218023641,0.));
#123210=DIRECTION('center_axis',(0.,0.,1.));
#123211=DIRECTION('ref_axis',(0.94905574701065,0.315108218023678,0.));
#123212=DIRECTION('center_axis',(0.,0.,-1.));
#123213=DIRECTION('ref_axis',(-0.949055747010666,-0.315108218023628,0.));
#123214=DIRECTION('center_axis',(-0.993538708289764,0.113493766920949,0.));
#123215=DIRECTION('ref_axis',(-0.113493766920949,-0.993538708289764,0.));
#123216=DIRECTION('',(0.,0.,1.));
#123217=DIRECTION('center_axis',(0.993538152256336,-0.113498634378743,2.28597554183348E-6));
#123218=DIRECTION('ref_axis',(0.107440322381736,0.940511723259278,0.32232634943233));
#123219=DIRECTION('',(0.,0.,-1.));
#123220=DIRECTION('center_axis',(0.634752252147712,0.772715716414133,0.));
#123221=DIRECTION('ref_axis',(-0.772715716414133,0.634752252147712,0.));
#123222=DIRECTION('center_axis',(-0.634752252147764,-0.772715716414091,
-4.12383924814779E-14));
#123223=DIRECTION('ref_axis',(0.771678214548363,-0.633899989624967,0.0518028603931937));
#123224=DIRECTION('',(0.,0.,1.));
#123225=DIRECTION('',(0.,0.,1.));
#123226=DIRECTION('center_axis',(0.,0.,1.));
#123227=DIRECTION('ref_axis',(-0.926916757346018,-0.375267004879383,0.));
#123228=DIRECTION('center_axis',(0.,0.,-1.));
#123229=DIRECTION('ref_axis',(0.926916757346018,0.375267004879383,0.));
#123230=DIRECTION('center_axis',(0.962379572339892,0.134875729940326,-0.235868811452366));
#123231=DIRECTION('ref_axis',(0.0591861757799709,0.743186687328967,0.666461209954142));
#123232=DIRECTION('center_axis',(0.785155432156967,0.572622782587701,0.235868811452306));
#123233=DIRECTION('ref_axis',(0.559538361127139,-0.492692884129657,-0.66646120994035));
#123234=DIRECTION('center_axis',(0.,0.,-1.));
#123235=DIRECTION('ref_axis',(0.926916757346019,0.375267004879382,0.));
#123236=DIRECTION('center_axis',(-0.921478503192035,-0.388429360572764,
-6.76296429840134E-17));
#123237=DIRECTION('ref_axis',(-0.388429360572764,0.921478503192035,-6.44030973403092E-31));
#123238=DIRECTION('center_axis',(0.,0.,1.));
#123239=DIRECTION('ref_axis',(-0.926916757346019,-0.375267004879382,0.));
#123240=DIRECTION('center_axis',(-0.932167012189561,-0.362028536700612,
-1.38914942345546E-16));
#123241=DIRECTION('ref_axis',(0.362028536700612,-0.932167012189561,-2.83496887813801E-31));
#123242=DIRECTION('center_axis',(0.,0.,-1.));
#123243=DIRECTION('ref_axis',(0.92691675734602,0.375267004879378,0.));
#123244=DIRECTION('center_axis',(0.,0.,1.));
#123245=DIRECTION('ref_axis',(-0.92691675734602,-0.375267004879378,0.));
#123246=DIRECTION('center_axis',(0.,0.,1.));
#123247=DIRECTION('ref_axis',(-0.92691675734602,-0.375267004879378,0.));
#123248=DIRECTION('center_axis',(-0.57803004839491,0.474826468821402,0.663642288932205));
#123249=DIRECTION('ref_axis',(-0.266677011928071,0.658697375311585,-0.703563173472535));
#123250=DIRECTION('center_axis',(-0.579692509177574,0.476192107831309,0.661209249211309));
#123251=DIRECTION('ref_axis',(-0.265811603787261,0.656559800472242,-0.705884848750767));
#123252=DIRECTION('center_axis',(-0.0851431970708823,-0.74535425453268,
-0.661209249211308));
#123253=DIRECTION('ref_axis',(0.265811603787243,-0.656559800472249,0.705884848750768));
#123254=DIRECTION('center_axis',(-0.0848990206777118,-0.743216703679901,
-0.663642288932184));
#123255=DIRECTION('ref_axis',(0.266677011928059,-0.65869737531157,0.703563173472554));
#123256=DIRECTION('center_axis',(0.,0.,1.));
#123257=DIRECTION('ref_axis',(-0.926916757346019,-0.375267004879381,0.));
#123258=DIRECTION('center_axis',(0.,0.,1.));
#123259=DIRECTION('ref_axis',(-0.926916757346019,-0.375267004879381,0.));
#123260=DIRECTION('center_axis',(0.,0.,1.));
#123261=DIRECTION('ref_axis',(0.926916757346035,0.375267004879342,0.));
#123262=DIRECTION('center_axis',(0.,0.,-1.));
#123263=DIRECTION('ref_axis',(-0.926916757346019,-0.375267004879382,0.));
#123264=DIRECTION('center_axis',(-0.998768947069956,0.0496043382051624,
0.));
#123265=DIRECTION('ref_axis',(-0.0496043382051624,-0.998768947069956,0.));
#123266=DIRECTION('',(0.,0.,1.));
#123267=DIRECTION('center_axis',(0.998768704038046,-0.0496092312874968,
2.28597557253148E-6));
#123268=DIRECTION('ref_axis',(0.0469607817114965,0.94546306611664,0.322326349512986));
#123269=DIRECTION('',(0.,0.,-1.));
#123270=DIRECTION('center_axis',(0.583940019635501,0.811796805529617,0.));
#123271=DIRECTION('ref_axis',(-0.811796805529617,0.583940019635501,0.));
#123272=DIRECTION('center_axis',(-0.583940019635481,-0.811796805529632,
5.69067053562094E-16));
#123273=DIRECTION('ref_axis',(0.810706830675423,-0.583155981150193,0.0518028603936798));
#123274=DIRECTION('',(0.,0.,1.));
#123275=DIRECTION('',(0.,0.,1.));
#123276=DIRECTION('center_axis',(0.,0.,1.));
#123277=DIRECTION('ref_axis',(-0.900968867902417,-0.433883739117562,0.));
#123278=DIRECTION('center_axis',(0.,0.,-1.));
#123279=DIRECTION('ref_axis',(0.900968867902417,0.433883739117562,0.));
#123280=DIRECTION('center_axis',(0.951760742606333,0.196258484192423,-0.235868811452327));
#123281=DIRECTION('ref_axis',(0.0114484368867947,0.745451801882648,0.666461209946058));
#123282=DIRECTION('center_axis',(0.746854178467675,0.621751348924495,0.235868811452354));
#123283=DIRECTION('ref_axis',(0.589955671020197,-0.455830847867314,-0.666461209946742));
#123284=DIRECTION('center_axis',(0.,0.,-1.));
#123285=DIRECTION('ref_axis',(0.900968867902415,0.433883739117566,0.));
#123286=DIRECTION('center_axis',(-0.894698472200103,-0.446670621199561,
-6.76296429840134E-17));
#123287=DIRECTION('ref_axis',(-0.446670621199561,0.894698472200103,1.23259516440783E-31));
#123288=DIRECTION('center_axis',(0.,0.,1.));
#123289=DIRECTION('ref_axis',(-0.900968867902415,-0.433883739117566,0.));
#123290=DIRECTION('center_axis',(-0.907056527102715,-0.421008855774271,
-1.38914942345546E-16));
#123291=DIRECTION('ref_axis',(0.421008855774271,-0.907056527102715,-2.58844984525645E-31));
#123292=DIRECTION('center_axis',(0.,0.,-1.));
#123293=DIRECTION('ref_axis',(0.900968867902412,0.433883739117574,0.));
#123294=DIRECTION('center_axis',(0.,0.,1.));
#123295=DIRECTION('ref_axis',(-0.900968867902412,-0.433883739117574,0.));
#123296=DIRECTION('center_axis',(0.,0.,1.));
#123297=DIRECTION('ref_axis',(-0.900968867902412,-0.433883739117574,0.));
#123298=DIRECTION('center_axis',(-0.607264659977007,0.436816374560105,0.663642288932205));
#123299=DIRECTION('ref_axis',(-0.308331981142968,0.640257956090913,-0.703563173472532));
#123300=DIRECTION('center_axis',(-0.609011201847474,0.438072693490148,0.661209249211309));
#123301=DIRECTION('ref_axis',(-0.307331396185831,0.638180220018272,-0.70588484875077));
#123302=DIRECTION('center_axis',(-0.0372132501894517,-0.749277987643942,
-0.661209249211308));
#123303=DIRECTION('ref_axis',(0.307331396185812,-0.638180220018285,0.705884848750767));
#123304=DIRECTION('center_axis',(-0.0371065288362263,-0.747129184183417,
-0.663642288932184));
#123305=DIRECTION('ref_axis',(0.308331981142974,-0.640257956090888,0.703563173472551));
#123306=DIRECTION('center_axis',(0.,0.,1.));
#123307=DIRECTION('ref_axis',(-0.900968867902412,-0.433883739117574,0.));
#123308=DIRECTION('center_axis',(0.,0.,1.));
#123309=DIRECTION('ref_axis',(-0.900968867902412,-0.433883739117574,0.));
#123310=DIRECTION('center_axis',(0.,0.,1.));
#123311=DIRECTION('ref_axis',(0.900968867902445,0.433883739117504,0.));
#123312=DIRECTION('center_axis',(0.,0.,-1.));
#123313=DIRECTION('ref_axis',(-0.900968867902415,-0.433883739117566,0.));
#123314=DIRECTION('center_axis',(-0.999895030011369,-0.0144889253764059,
0.));
#123315=DIRECTION('ref_axis',(0.0144889253764059,-0.999895030011369,0.));
#123316=DIRECTION('',(0.,0.,1.));
#123317=DIRECTION('center_axis',(0.999895100979656,0.0144840267763789,2.28597555049375E-6));
#123318=DIRECTION('ref_axis',(0.0137117308809598,-0.946529298470156,-0.322326349487352));
#123319=DIRECTION('',(0.,0.,-1.));
#123320=DIRECTION('center_axis',(0.530728252327867,0.84754204744131,0.));
#123321=DIRECTION('ref_axis',(-0.84754204744131,0.530728252327867,0.));
#123322=DIRECTION('center_axis',(-0.530728252327927,-0.847542047441273,
-2.31041223746203E-14));
#123323=DIRECTION('ref_axis',(0.846404078535633,-0.530015659660323,0.0518028604719626));
#123324=DIRECTION('',(0.,0.,1.));
#123325=DIRECTION('',(0.,0.,1.));
#123326=DIRECTION('center_axis',(0.,0.,1.));
#123327=DIRECTION('ref_axis',(-0.871318704123379,-0.490717552003956,0.));
#123328=DIRECTION('center_axis',(0.,0.,-1.));
#123329=DIRECTION('ref_axis',(0.871318704123379,0.490717552003956,0.));
#123330=DIRECTION('center_axis',(0.937230923829337,0.256834770235804,-0.235868811452317));
#123331=DIRECTION('ref_axis',(-0.0363363460864612,0.7446536950763,0.666461209945708));
#123332=DIRECTION('center_axis',(0.705483940759196,0.668325005603523,0.235868811452313));
#123333=DIRECTION('ref_axis',(0.61794872652725,-0.417095704897173,-0.666461209928741));
#123334=DIRECTION('center_axis',(0.,0.,-1.));
#123335=DIRECTION('ref_axis',(0.871318704123385,0.490717552003945,0.));
#123336=DIRECTION('center_axis',(-0.86424193327368,-0.503076416433301,-6.76296429840134E-17));
#123337=DIRECTION('ref_axis',(-0.503076416433301,0.86424193327368,6.93889390390714E-14));
#123338=DIRECTION('center_axis',(0.,0.,1.));
#123339=DIRECTION('ref_axis',(-0.871318704123385,-0.490717552003945,0.));
#123340=DIRECTION('center_axis',(-0.87821875218299,-0.478259159153437,-1.38914942345546E-16));
#123341=DIRECTION('ref_axis',(0.478259159153437,-0.87821875218299,6.5327543713615E-31));
#123342=DIRECTION('center_axis',(0.,0.,-1.));
#123343=DIRECTION('ref_axis',(0.871318704123391,0.490717552003934,0.));
#123344=DIRECTION('center_axis',(0.,0.,1.));
#123345=DIRECTION('ref_axis',(-0.871318704123391,-0.490717552003934,0.));
#123346=DIRECTION('center_axis',(0.,0.,1.));
#123347=DIRECTION('ref_axis',(-0.871318704123391,-0.490717552003934,0.));
#123348=DIRECTION('center_axis',(-0.634003890813397,0.397011308118922,0.663642288932205));
#123349=DIRECTION('ref_axis',(-0.348719948110368,0.619187579593742,-0.703563173472536));
#123350=DIRECTION('center_axis',(-0.635827336856489,0.398153144485137,0.661209249211309));
#123351=DIRECTION('ref_axis',(-0.34758829795508,0.617178220151034,-0.705884848750766));
#123352=DIRECTION('center_axis',(0.0108696139192246,-0.750122776784351,
-0.661209249211308));
#123353=DIRECTION('ref_axis',(0.347588297955064,-0.61717822015104,0.705884848750769));
#123354=DIRECTION('center_axis',(0.0108384416915727,-0.747971550610416,
-0.663642288932184));
#123355=DIRECTION('ref_axis',(0.34871994811035,-0.619187579593732,0.703563173472553));
#123356=DIRECTION('center_axis',(0.,0.,1.));
#123357=DIRECTION('ref_axis',(-0.871318704123391,-0.490717552003934,0.));
#123358=DIRECTION('center_axis',(0.,0.,1.));
#123359=DIRECTION('ref_axis',(-0.871318704123391,-0.490717552003934,0.));
#123360=DIRECTION('center_axis',(0.,0.,1.));
#123361=DIRECTION('ref_axis',(0.871318704123396,0.490717552003927,0.));
#123362=DIRECTION('center_axis',(0.,0.,-1.));
#123363=DIRECTION('ref_axis',(-0.871318704123385,-0.490717552003945,0.));
#123364=DIRECTION('center_axis',(-0.996912329797655,-0.0785226508557379,
0.));
#123365=DIRECTION('ref_axis',(0.0785226508557379,-0.996912329797655,0.));
#123366=DIRECTION('',(0.,0.,1.));
#123367=DIRECTION('center_axis',(0.996912714474511,0.0785177668673503,2.28597555777743E-6));
#123368=DIRECTION('ref_axis',(0.0743278990288261,-0.943706038877036,-0.322326349548056));
#123369=DIRECTION('',(0.,0.,-1.));
#123370=DIRECTION('center_axis',(0.475335608790564,0.879804557282868,0.));
#123371=DIRECTION('ref_axis',(-0.879804557282868,0.475335608790564,0.));
#123372=DIRECTION('center_axis',(-0.475335608790582,-0.879804557282858,
-1.09640252319663E-14));
#123373=DIRECTION('ref_axis',(0.878623270489444,-0.474697390140252,0.0518028604274629));
#123374=DIRECTION('',(0.,0.,1.));
#123375=DIRECTION('',(0.,0.,1.));
#123376=DIRECTION('center_axis',(0.,0.,1.));
#123377=DIRECTION('ref_axis',(-0.838088104891841,-0.545534901210548,0.));
#123378=DIRECTION('center_axis',(0.,0.,-1.));
#123379=DIRECTION('ref_axis',(0.838088104891841,0.545534901210548,0.));
#123380=DIRECTION('center_axis',(0.918849822150947,0.316355667117322,-0.235868811452313));
#123381=DIRECTION('ref_axis',(-0.0839718152198296,0.740795646509661,0.66646120994475));
#123382=DIRECTION('center_axis',(0.661214718212255,0.712152371479303,0.235868811452242));
#123383=DIRECTION('ref_axis',(0.643402498157302,-0.376646626189073,-0.66646120993298));
#123384=DIRECTION('center_axis',(0.,0.,-1.));
#123385=DIRECTION('ref_axis',(0.838088104891836,0.545534901210556,0.));
#123386=DIRECTION('center_axis',(-0.830234038864122,-0.557414962762364,
-6.76296429840134E-17));
#123387=DIRECTION('ref_axis',(-0.557414962762364,0.830234038864122,4.00593428432545E-31));
#123388=DIRECTION('center_axis',(0.,0.,1.));
#123389=DIRECTION('ref_axis',(-0.838088104891836,-0.545534901210556,0.));
#123390=DIRECTION('center_axis',(-0.845772188033212,-0.533544193061374,
-1.38914942345546E-16));
#123391=DIRECTION('ref_axis',(0.533544193061374,-0.845772188033212,7.88860905221012E-31));
#123392=DIRECTION('center_axis',(0.,0.,-1.));
#123393=DIRECTION('ref_axis',(0.83808810489183,0.545534901210566,0.));
#123394=DIRECTION('center_axis',(0.,0.,1.));
#123395=DIRECTION('ref_axis',(-0.83808810489183,-0.545534901210566,0.));
#123396=DIRECTION('center_axis',(0.,0.,1.));
#123397=DIRECTION('ref_axis',(-0.83808810489183,-0.545534901210566,0.));
#123398=DIRECTION('center_axis',(-0.658137863669027,0.355574837054021,0.663642288932205));
#123399=DIRECTION('ref_axis',(-0.387674950010773,0.595572828516714,-0.703563173472536));
#123400=DIRECTION('center_axis',(-0.660030720953824,0.356597498805855,0.661209249211309));
#123401=DIRECTION('ref_axis',(-0.386416884850581,0.593640102592878,-0.705884848750765));
#123402=DIRECTION('center_axis',(0.0589078124527818,-0.747885150534122,
-0.661209249211308));
#123403=DIRECTION('ref_axis',(0.386416884850565,-0.593640102592882,0.70588484875077));
#123404=DIRECTION('center_axis',(0.0587388747376226,-0.745740341496563,
-0.663642288932184));
#123405=DIRECTION('ref_axis',(0.387674950010756,-0.595572828516704,0.703563173472553));
#123406=DIRECTION('center_axis',(0.,0.,1.));
#123407=DIRECTION('ref_axis',(-0.83808810489183,-0.545534901210566,0.));
#123408=DIRECTION('center_axis',(0.,0.,1.));
#123409=DIRECTION('ref_axis',(-0.83808810489183,-0.545534901210566,0.));
#123410=DIRECTION('center_axis',(0.,0.,1.));
#123411=DIRECTION('ref_axis',(0.838088104891825,0.545534901210574,0.));
#123412=DIRECTION('center_axis',(0.,0.,-1.));
#123413=DIRECTION('ref_axis',(-0.838088104891836,-0.545534901210556,0.));
#123414=DIRECTION('center_axis',(-0.989833102983778,-0.142233709919647,
0.));
#123415=DIRECTION('ref_axis',(0.142233709919647,-0.989833102983778,0.));
#123416=DIRECTION('',(0.,0.,1.));
#123417=DIRECTION('center_axis',(0.989833799788485,0.14222886061227,2.28597555000455E-6));
#123418=DIRECTION('ref_axis',(0.134638637897654,-0.937004888773812,-0.32232634952644));
#123419=DIRECTION('',(0.,0.,-1.));
#123420=DIRECTION('center_axis',(0.417989709277573,0.908451761481065,0.));
#123421=DIRECTION('ref_axis',(-0.908451761481065,0.417989709277573,0.));
#123422=DIRECTION('center_axis',(-0.41798970927758,-0.908451761481062,-2.56269863120773E-14));
#123423=DIRECTION('ref_axis',(0.907232010956192,-0.417428487219462,0.0518028604814085));
#123424=DIRECTION('',(0.,0.,1.));
#123425=DIRECTION('',(0.,0.,1.));
#123426=DIRECTION('center_axis',(0.,0.,1.));
#123427=DIRECTION('ref_axis',(-0.80141362186795,-0.598110530491225,0.));
#123428=DIRECTION('center_axis',(0.,0.,-1.));
#123429=DIRECTION('ref_axis',(0.80141362186795,0.598110530491225,0.));
#123430=DIRECTION('center_axis',(0.896692969460527,0.374576590704891,-0.235868811452391));
#123431=DIRECTION('ref_axis',(-0.13126222615057,0.73389350972817,0.666461209947634));
#123432=DIRECTION('center_axis',(0.614228422558169,0.75305335050433,0.23586881145227));
#123433=DIRECTION('ref_axis',(0.666212390916414,-0.334649825709052,-0.666461209930733));
#123434=DIRECTION('center_axis',(0.,0.,-1.));
#123435=DIRECTION('ref_axis',(0.801413621867952,0.598110530491223,0.));
#123436=DIRECTION('center_axis',(-0.792814534704229,-0.609462971444301,
-6.76296429840134E-17));
#123437=DIRECTION('ref_axis',(-0.609462971444301,0.792814534704229,4.62223186652937E-31));
#123438=DIRECTION('center_axis',(0.,0.,1.));
#123439=DIRECTION('ref_axis',(-0.801413621867952,-0.598110530491223,0.));
#123440=DIRECTION('center_axis',(-0.809850164545241,-0.586636779435151,
-1.38914942345546E-16));
#123441=DIRECTION('ref_axis',(0.586636779435151,-0.809850164545241,7.02579243712464E-31));
#123442=DIRECTION('center_axis',(0.,0.,-1.));
#123443=DIRECTION('ref_axis',(0.801413621867943,0.598110530491235,0.));
#123444=DIRECTION('center_axis',(0.,0.,1.));
#123445=DIRECTION('ref_axis',(-0.801413621867943,-0.598110530491235,0.));
#123446=DIRECTION('center_axis',(0.,0.,1.));
#123447=DIRECTION('ref_axis',(-0.801413621867943,-0.598110530491235,0.));
#123448=DIRECTION('center_axis',(-0.679567406872712,0.312677232713101,0.663642288932205));
#123449=DIRECTION('ref_axis',(-0.425036912385568,0.569510740937341,-0.703563173472535));
#123450=DIRECTION('center_axis',(-0.681521897242615,0.313576517514057,0.661209249211309));
#123451=DIRECTION('ref_axis',(-0.423657601880078,0.567662590517755,-0.705884848750767));
#123452=DIRECTION('center_axis',(0.106703946149284,-0.742574303779486,-0.661209249211308));
#123453=DIRECTION('ref_axis',(0.42365760188006,-0.567662590517765,0.705884848750769));
#123454=DIRECTION('center_axis',(0.106397937147926,-0.740444725358698,-0.663642288932184));
#123455=DIRECTION('ref_axis',(0.425036912385554,-0.569510740937329,0.703563173472553));
#123456=DIRECTION('center_axis',(0.,0.,1.));
#123457=DIRECTION('ref_axis',(-0.801413621867943,-0.598110530491235,0.));
#123458=DIRECTION('center_axis',(0.,0.,1.));
#123459=DIRECTION('ref_axis',(-0.801413621867943,-0.598110530491235,0.));
#123460=DIRECTION('center_axis',(0.,0.,1.));
#123461=DIRECTION('ref_axis',(0.801413621867959,0.598110530491212,0.));
#123462=DIRECTION('center_axis',(0.,0.,-1.));
#123463=DIRECTION('ref_axis',(-0.801413621867952,-0.598110530491223,0.));
#123464=DIRECTION('center_axis',(-0.978686439631205,-0.205360300160462,
0.));
#123465=DIRECTION('ref_axis',(0.205360300160462,-0.978686439631205,0.));
#123466=DIRECTION('',(0.,0.,1.));
#123467=DIRECTION('center_axis',(0.97868744570043,0.205355505460999,2.28597553472572E-6));
#123468=DIRECTION('ref_axis',(0.194396117719157,-0.926453384570327,-0.322326349580523));
#123469=DIRECTION('',(0.,0.,-1.));
#123470=DIRECTION('center_axis',(0.358926200390648,0.933365942529045,0.));
#123471=DIRECTION('ref_axis',(-0.933365942529045,0.358926200390648,0.));
#123472=DIRECTION('center_axis',(-0.358926200390652,-0.933365942529043,
-2.20798016782112E-14));
#123473=DIRECTION('ref_axis',(0.93211274049379,-0.358444281108687,0.0518028604387188));
#123474=DIRECTION('',(0.,0.,1.));
#123475=DIRECTION('',(0.,0.,1.));
#123476=DIRECTION('center_axis',(0.,0.,1.));
#123477=DIRECTION('ref_axis',(-0.761445958369139,-0.648228395307783,0.));
#123478=DIRECTION('center_axis',(0.,0.,-1.));
#123479=DIRECTION('ref_axis',(0.761445958369139,0.648228395307783,0.));
#123480=DIRECTION('center_axis',(0.870851413018736,0.431258298734448,-0.235868811452342));
#123481=DIRECTION('ref_axis',(-0.178013252430194,0.723975647086769,0.666461209962379));
#123482=DIRECTION('center_axis',(0.564718130564361,0.790859871782578,0.235868811452335));
#123483=DIRECTION('ref_axis',(0.686284674057369,-0.291277877310675,-0.6664612099315));
#123484=DIRECTION('center_axis',(0.,0.,-1.));
#123485=DIRECTION('ref_axis',(0.761445958369129,0.648228395307795,0.));
#123486=DIRECTION('center_axis',(-0.752137185563052,-0.659006566047177,
-6.76296429840134E-17));
#123487=DIRECTION('ref_axis',(-0.659006566047177,0.752137185563051,-3.88267476788467E-31));
#123488=DIRECTION('center_axis',(0.,0.,1.));
#123489=DIRECTION('ref_axis',(-0.761445958369129,-0.648228395307795,0.));
#123490=DIRECTION('center_axis',(-0.770600293018838,-0.637318749449034,
-1.38914942345546E-16));
#123491=DIRECTION('ref_axis',(0.637318749449034,-0.770600293018838,-1.84889274661175E-31));
#123492=DIRECTION('center_axis',(0.,0.,-1.));
#123493=DIRECTION('ref_axis',(0.761445958369123,0.648228395307802,0.));
#123494=DIRECTION('center_axis',(0.,0.,1.));
#123495=DIRECTION('ref_axis',(-0.761445958369123,-0.648228395307802,0.));
#123496=DIRECTION('center_axis',(0.,0.,1.));
#123497=DIRECTION('ref_axis',(-0.761445958369123,-0.648228395307802,0.));
#123498=DIRECTION('center_axis',(-0.698204461834805,0.268494770553906,0.663642288932205));
#123499=DIRECTION('ref_axis',(-0.460652306917231,0.541108411563796,-0.703563173472531));
#123500=DIRECTION('center_axis',(-0.700212553869647,0.269266983049841,0.661209249211309));
#123501=DIRECTION('ref_axis',(-0.45915741894918,0.539352431094948,-0.705884848750769));
#123502=DIRECTION('center_axis',(0.154061610443135,-0.734212059928932,-0.661209249211308));
#123503=DIRECTION('ref_axis',(0.459157418949166,-0.539352431094964,0.705884848750767));
#123504=DIRECTION('center_axis',(0.153619787612203,-0.732106463019439,-0.663642288932184));
#123505=DIRECTION('ref_axis',(0.46065230691723,-0.54110841156377,0.703563173472551));
#123506=DIRECTION('center_axis',(0.,0.,1.));
#123507=DIRECTION('ref_axis',(-0.761445958369123,-0.648228395307802,0.));
#123508=DIRECTION('center_axis',(0.,0.,1.));
#123509=DIRECTION('ref_axis',(-0.761445958369123,-0.648228395307802,0.));
#123510=DIRECTION('center_axis',(0.,0.,1.));
#123511=DIRECTION('ref_axis',(0.761445958369147,0.648228395307773,0.));
#123512=DIRECTION('center_axis',(0.,0.,-1.));
#123513=DIRECTION('ref_axis',(-0.761445958369129,-0.648228395307795,0.));
#123514=DIRECTION('center_axis',(-0.963518143770605,-0.267643020878272,
0.));
#123515=DIRECTION('ref_axis',(0.267643020878272,-0.963518143770605,0.));
#123516=DIRECTION('',(0.,0.,1.));
#123517=DIRECTION('center_axis',(0.963519454970197,0.267638300489127,2.28597552263965E-6));
#123518=DIRECTION('ref_axis',(0.253354782218402,-0.912094884778792,-0.322326349353304));
#123519=DIRECTION('',(0.,0.,-1.));
#123520=DIRECTION('center_axis',(0.29838778675689,0.954444722712806,0.));
#123521=DIRECTION('ref_axis',(-0.954444722712806,0.29838778675689,0.));
#123522=DIRECTION('center_axis',(-0.298387786756925,-0.954444722712795,
-1.55544994640349E-14));
#123523=DIRECTION('ref_axis',(0.953163218842664,-0.297987150560371,0.051802860407533));
#123524=DIRECTION('',(0.,0.,1.));
#123525=DIRECTION('',(0.,0.,1.));
#123526=DIRECTION('center_axis',(0.,0.,1.));
#123527=DIRECTION('ref_axis',(-0.718349350097714,-0.6956825506035,0.));
#123528=DIRECTION('center_axis',(0.,0.,-1.));
#123529=DIRECTION('ref_axis',(0.718349350097714,0.6956825506035,0.));
#123530=DIRECTION('center_axis',(0.841431341323684,0.486167873910092,-0.235868811452398));
#123531=DIRECTION('ref_axis',(-0.224032784086759,0.711082813237174,0.66646120995377));
#123532=DIRECTION('center_axis',(0.512887290640309,0.825416580208867,0.235868811452346));
#123533=DIRECTION('ref_axis',(0.703536866256326,-0.246709005626589,-0.666461209944711));
#123534=DIRECTION('center_axis',(0.,0.,-1.));
#123535=DIRECTION('ref_axis',(0.718349350097721,0.695682550603493,0.));
#123536=DIRECTION('center_axis',(-0.708369143393475,-0.705842161313699,
-6.76296429840134E-17));
#123537=DIRECTION('ref_axis',(-0.705842161313699,0.708369143393475,4.00593428432545E-31));
#123538=DIRECTION('center_axis',(0.,0.,1.));
#123539=DIRECTION('ref_axis',(-0.718349350097721,-0.695682550603493,0.));
#123540=DIRECTION('center_axis',(-0.728183859595176,-0.685381840016989,
-1.38914942345546E-16));
#123541=DIRECTION('ref_axis',(0.685381840016988,-0.728183859595176,-1.3065508742723E-30));
#123542=DIRECTION('center_axis',(0.,0.,-1.));
#123543=DIRECTION('ref_axis',(0.718349350097727,0.695682550603487,0.));
#123544=DIRECTION('center_axis',(0.,0.,1.));
#123545=DIRECTION('ref_axis',(-0.718349350097727,-0.695682550603487,0.));
#123546=DIRECTION('center_axis',(0.,0.,1.));
#123547=DIRECTION('ref_axis',(-0.718349350097727,-0.695682550603487,0.));
#123548=DIRECTION('center_axis',(-0.713972444898831,0.223209005790558,0.663642288932205));
#123549=DIRECTION('ref_axis',(-0.494374782310175,0.510482551659726,-0.703563173472533));
#123550=DIRECTION('center_axis',(-0.716025886917708,0.223850972794686,0.661209249211309));
#123551=DIRECTION('ref_axis',(-0.492770459694853,0.508825956842051,-0.705884848750768));
#123552=DIRECTION('center_axis',(0.200786202533562,-0.722832781236137,-0.661209249211308));
#123553=DIRECTION('ref_axis',(0.492770459694833,-0.508825956842068,0.705884848750769));
#123554=DIRECTION('center_axis',(0.200210381417841,-0.72075981818729,-0.663642288932184));
#123555=DIRECTION('ref_axis',(0.494374782310176,-0.510482551659703,0.703563173472549));
#123556=DIRECTION('center_axis',(0.,0.,1.));
#123557=DIRECTION('ref_axis',(-0.718349350097718,-0.695682550603496,0.));
#123558=DIRECTION('center_axis',(0.,0.,1.));
#123559=DIRECTION('ref_axis',(-0.718349350097718,-0.695682550603496,0.));
#123560=DIRECTION('center_axis',(0.,0.,1.));
#123561=DIRECTION('ref_axis',(0.718349350097718,0.695682550603496,0.));
#123562=DIRECTION('center_axis',(0.,0.,-1.));
#123563=DIRECTION('ref_axis',(-0.718349350097721,-0.695682550603493,0.));
#123564=DIRECTION('center_axis',(-0.944390545183258,-0.328825939014045,
0.));
#123565=DIRECTION('ref_axis',(0.328825939014045,-0.944390545183258,0.));
#123566=DIRECTION('',(0.,0.,1.));
#123567=DIRECTION('center_axis',(0.944392156125255,0.328821312332193,2.28597556106335E-6));
#123568=DIRECTION('ref_axis',(0.311272357528953,-0.89398839130544,-0.322326349604682));
#123569=DIRECTION('',(0.,0.,-1.));
#123570=DIRECTION('center_axis',(0.236623233703368,0.971601484803189,0.));
#123571=DIRECTION('ref_axis',(-0.971601484803189,0.236623233703368,0.));
#123572=DIRECTION('center_axis',(-0.236623233703389,-0.971601484803184,
-6.58220891953721E-15));
#123573=DIRECTION('ref_axis',(0.970296945073439,-0.236305526892341,0.0518028603581309));
#123574=DIRECTION('',(0.,0.,1.));
#123575=DIRECTION('',(0.,0.,1.));
#123576=DIRECTION('center_axis',(0.,0.,1.));
#123577=DIRECTION('ref_axis',(-0.672300890261307,-0.740277997075324,0.));
#123578=DIRECTION('center_axis',(0.,0.,-1.));
#123579=DIRECTION('ref_axis',(0.672300890261307,0.740277997075324,0.));
#123580=DIRECTION('center_axis',(0.808553647760917,0.539079681008855,-0.235868811452268));
#123581=DIRECTION('ref_axis',(-0.269131716983368,0.695267987584204,0.66646120993963));
#123582=DIRECTION('center_axis',(0.458948886824981,0.85658147485582,0.235868811452339));
#123583=DIRECTION('ref_axis',(0.717898074571082,-0.201126353728443,-0.666461209946261));
#123584=DIRECTION('center_axis',(0.,0.,-1.));
#123585=DIRECTION('ref_axis',(0.67230089026131,0.740277997075322,0.));
#123586=DIRECTION('center_axis',(-0.66169026046899,-0.749777299736715,-6.76296429840134E-17));
#123587=DIRECTION('ref_axis',(-0.749777299736715,0.66169026046899,4.93038065763132E-31));
#123588=DIRECTION('center_axis',(0.,0.,1.));
#123589=DIRECTION('ref_axis',(-0.67230089026131,-0.740277997075321,0.));
#123590=DIRECTION('center_axis',(-0.682775162497489,-0.73062854959037,-1.38914942345546E-16));
#123591=DIRECTION('ref_axis',(0.73062854959037,-0.682775162497489,-2.71170936169723E-31));
#123592=DIRECTION('center_axis',(0.,0.,-1.));
#123593=DIRECTION('ref_axis',(0.672300890261315,0.740277997075317,0.));
#123594=DIRECTION('center_axis',(0.,0.,1.));
#123595=DIRECTION('ref_axis',(-0.672300890261315,-0.740277997075317,0.));
#123596=DIRECTION('center_axis',(0.,0.,1.));
#123597=DIRECTION('ref_axis',(-0.672300890261315,-0.740277997075317,0.));
#123598=DIRECTION('center_axis',(-0.726806562040159,0.177006027344235,0.663642288932205));
#123599=DIRECTION('ref_axis',(-0.526065765679541,0.477759009452735,-0.703563173472531));
#123600=DIRECTION('center_axis',(-0.728896916009352,0.177515110876435,0.661209249211309));
#123601=DIRECTION('ref_axis',(-0.524358600922711,0.47620860758966,-0.705884848750768));
#123602=DIRECTION('center_axis',(0.246685721049275,-0.708483227598097,-0.661209249211308));
#123603=DIRECTION('ref_axis',(0.524358600922702,-0.476208607589672,0.705884848750766));
#123604=DIRECTION('center_axis',(0.24597826782124,-0.706451416659712,-0.663642288932184));
#123605=DIRECTION('ref_axis',(0.526065765679537,-0.477759009452711,0.703563173472551));
#123606=DIRECTION('center_axis',(0.,0.,1.));
#123607=DIRECTION('ref_axis',(-0.672300890261315,-0.740277997075317,0.));
#123608=DIRECTION('center_axis',(0.,0.,1.));
#123609=DIRECTION('ref_axis',(-0.672300890261315,-0.740277997075317,0.));
#123610=DIRECTION('center_axis',(0.,0.,1.));
#123611=DIRECTION('ref_axis',(0.67230089026136,0.740277997075276,0.));
#123612=DIRECTION('center_axis',(0.,0.,-1.));
#123613=DIRECTION('ref_axis',(-0.67230089026131,-0.740277997075322,0.));
#123614=DIRECTION('center_axis',(-0.921382243274616,-0.388657640833466,
0.));
#123615=DIRECTION('ref_axis',(0.388657640833466,-0.921382243274617,0.));
#123616=DIRECTION('',(0.,0.,1.));
#123617=DIRECTION('center_axis',(0.921384147339249,0.38865312687112,2.28597552009451E-6));
#123618=DIRECTION('ref_axis',(0.367910847977183,-0.872208307853349,-0.322326349609068));
#123619=DIRECTION('',(0.,0.,-1.));
#123620=DIRECTION('center_axis',(0.173886345027034,0.984765727984651,0.));
#123621=DIRECTION('ref_axis',(-0.984765727984651,0.173886345027034,0.));
#123622=DIRECTION('center_axis',(-0.173886345027096,-0.98476572798464,-3.60124600396073E-14));
#123623=DIRECTION('ref_axis',(0.983443513025211,-0.173652873126014,0.0518028603815676));
#123624=DIRECTION('',(0.,0.,1.));
#123625=DIRECTION('',(0.,0.,1.));
#123626=DIRECTION('center_axis',(0.,0.,1.));
#123627=DIRECTION('ref_axis',(-0.623489801858719,-0.781831482468041,0.));
#123628=DIRECTION('center_axis',(0.,0.,-1.));
#123629=DIRECTION('ref_axis',(0.623489801858719,0.781831482468041,0.));
#123630=DIRECTION('center_axis',(0.772353433824751,0.589776294066747,-0.235868811452489));
#123631=DIRECTION('ref_axis',(-0.313124729911562,0.676596156621241,0.666461209946368));
#123632=DIRECTION('center_axis',(0.403124563589422,0.884226492486458,0.23586881145233));
#123633=DIRECTION('ref_axis',(0.729309285718661,-0.15471723050946,-0.666461209934996));
#123634=DIRECTION('center_axis',(0.,0.,-1.));
#123635=DIRECTION('ref_axis',(0.623489801858726,0.781831482468036,0.));
#123636=DIRECTION('center_axis',(-0.612292350332122,-0.790631442408387,
-6.76296429840134E-17));
#123637=DIRECTION('ref_axis',(-0.790631442408387,0.612292350332122,-3.01985815279918E-31));
#123638=DIRECTION('center_axis',(0.,0.,1.));
#123639=DIRECTION('ref_axis',(-0.623489801858726,-0.781831482468036,0.));
#123640=DIRECTION('center_axis',(-0.634560795802287,-0.772872949734151,
-1.38914942345546E-16));
#123641=DIRECTION('ref_axis',(0.772872949734151,-0.634560795802287,7.39557098644698E-32));
#123642=DIRECTION('center_axis',(0.,0.,-1.));
#123643=DIRECTION('ref_axis',(0.623489801858737,0.781831482468027,0.));
#123644=DIRECTION('center_axis',(0.,0.,1.));
#123645=DIRECTION('ref_axis',(-0.623489801858737,-0.781831482468027,0.));
#123646=DIRECTION('center_axis',(0.,0.,1.));
#123647=DIRECTION('ref_axis',(-0.623489801858737,-0.781831482468027,0.));
#123648=DIRECTION('center_axis',(-0.736654075118546,0.13007569316388,0.663642288932205));
#123649=DIRECTION('ref_axis',(-0.555595031976983,0.443072252996905,-0.703563173472533));
#123650=DIRECTION('center_axis',(-0.738772751325215,0.130449801290721,0.661209249211309));
#123651=DIRECTION('ref_axis',(-0.553792040184809,0.44163441502226,-0.705884848750767));
#123652=DIRECTION('center_axis',(0.291571555023274,-0.691222364408681,-0.661209249211308));
#123653=DIRECTION('ref_axis',(0.553792040184795,-0.441634415022275,0.705884848750769));
#123654=DIRECTION('center_axis',(0.290735376759989,-0.689240054727726,-0.663642288932184));
#123655=DIRECTION('ref_axis',(0.555595031976965,-0.443072252996894,0.703563173472555));
#123656=DIRECTION('center_axis',(0.,0.,1.));
#123657=DIRECTION('ref_axis',(-0.623489801858737,-0.781831482468027,0.));
#123658=DIRECTION('center_axis',(0.,0.,1.));
#123659=DIRECTION('ref_axis',(-0.623489801858737,-0.781831482468027,0.));
#123660=DIRECTION('center_axis',(0.,0.,1.));
#123661=DIRECTION('ref_axis',(0.623489801858737,0.781831482468027,0.));
#123662=DIRECTION('center_axis',(0.,0.,-1.));
#123663=DIRECTION('ref_axis',(-0.623489801858726,-0.781831482468036,0.));
#123664=DIRECTION('center_axis',(-0.894587784092488,-0.4468922650399,0.));
#123665=DIRECTION('ref_axis',(0.4468922650399,-0.894587784092488,0.));
#123666=DIRECTION('',(0.,0.,1.));
#123667=DIRECTION('center_axis',(0.894589973455606,0.446887882345754,2.28597555658038E-6));
#123668=DIRECTION('ref_axis',(0.423037513841325,-0.846844133390666,-0.322326349566341));
#123669=DIRECTION('',(0.,0.,-1.));
#123670=DIRECTION('center_axis',(0.11043492006048,0.993883357558238,0.));
#123671=DIRECTION('ref_axis',(-0.993883357558238,0.11043492006048,0.));
#123672=DIRECTION('center_axis',(-0.110434920060485,-0.993883357558237,
5.17851018741787E-15));
#123673=DIRECTION('ref_axis',(0.992548900635969,-0.11028664245586,0.0518028603664164));
#123674=DIRECTION('',(0.,0.,1.));
#123675=DIRECTION('',(0.,0.,1.));
#123676=DIRECTION('center_axis',(0.,0.,1.));
#123677=DIRECTION('ref_axis',(-0.572116660122161,-0.820172254596962,0.));
#123678=DIRECTION('center_axis',(0.,0.,-1.));
#123679=DIRECTION('ref_axis',(0.572116660122161,0.820172254596962,0.));
#123680=DIRECTION('center_axis',(0.732979453960397,0.638049389824958,-0.235868811452291));
#123681=DIRECTION('ref_axis',(-0.355831046164631,0.655144046926414,0.666461209945684));
#123682=DIRECTION('center_axis',(0.345643715051997,0.90823803379354,0.235868811452253));
#123683=DIRECTION('ref_axis',(0.737723608566232,-0.107672340995733,-0.666461209935369));
#123684=DIRECTION('center_axis',(0.,0.,-1.));
#123685=DIRECTION('ref_axis',(0.572116660122162,0.820172254596961,0.));
#123686=DIRECTION('center_axis',(-0.560378399591443,-0.828236710893289,
-6.76296429840134E-17));
#123687=DIRECTION('ref_axis',(-0.828236710893289,0.560378399591443,2.46519032881566E-31));
#123688=DIRECTION('center_axis',(0.,0.,1.));
#123689=DIRECTION('ref_axis',(-0.572116660122162,-0.820172254596961,0.));
#123690=DIRECTION('center_axis',(-0.58373888268427,-0.811941449146747,-1.38914942345546E-16));
#123691=DIRECTION('ref_axis',(0.811941449146747,-0.58373888268427,2.46519032881566E-32));
#123692=DIRECTION('center_axis',(0.,0.,-1.));
#123693=DIRECTION('ref_axis',(0.572116660122157,0.820172254596965,0.));
#123694=DIRECTION('center_axis',(0.,0.,1.));
#123695=DIRECTION('ref_axis',(-0.572116660122157,-0.820172254596965,0.));
#123696=DIRECTION('center_axis',(0.,0.,1.));
#123697=DIRECTION('ref_axis',(-0.572116660122157,-0.820172254596965,0.));
#123698=DIRECTION('center_axis',(-0.743474518590466,0.0826108500591668,
0.663642288932205));
#123699=DIRECTION('ref_axis',(-0.58284123911327,0.406564817614812,-0.703563173472534));
#123700=DIRECTION('center_axis',(-0.745612810939625,0.082848445490109,0.661209249211309));
#123701=DIRECTION('ref_axis',(-0.580949829165767,0.405245451913252,-0.705884848750765));
#123702=DIRECTION('center_axis',(0.33525925893578,-0.671121120257178,-0.661209249211308));
#123703=DIRECTION('ref_axis',(0.580949829165751,-0.405245451913266,0.70588484875077));
#123704=DIRECTION('center_axis',(0.334297791673088,-0.669196457569336,-0.663642288932184));
#123705=DIRECTION('ref_axis',(0.582841239113255,-0.406564817614802,0.703563173472553));
#123706=DIRECTION('center_axis',(0.,0.,1.));
#123707=DIRECTION('ref_axis',(-0.572116660122157,-0.820172254596965,0.));
#123708=DIRECTION('center_axis',(0.,0.,1.));
#123709=DIRECTION('ref_axis',(-0.572116660122157,-0.820172254596965,0.));
#123710=DIRECTION('center_axis',(0.,0.,1.));
#123711=DIRECTION('ref_axis',(0.572116660122157,0.820172254596965,0.));
#123712=DIRECTION('center_axis',(0.,0.,-1.));
#123713=DIRECTION('ref_axis',(-0.572116660122162,-0.820172254596961,0.));
#123714=DIRECTION('center_axis',(-0.864117271817046,-0.503290513071194,
0.));
#123715=DIRECTION('ref_axis',(0.503290513071194,-0.864117271817046,0.));
#123716=DIRECTION('',(0.,0.,1.));
#123717=DIRECTION('center_axis',(0.864119737482042,0.503286279654772,2.28597554434033E-6));
#123718=DIRECTION('ref_axis',(0.476425827832821,-0.81800009475483,-0.32232634945797));
#123719=DIRECTION('',(0.,0.,-1.));
#123720=DIRECTION('center_axis',(0.0465296943191825,0.998916907228306,0.));
#123721=DIRECTION('ref_axis',(-0.998916907228306,0.0465296943191825,0.));
#123722=DIRECTION('center_axis',(-0.0465296943192999,-0.9989169072283,-5.01419207570033E-14));
#123723=DIRECTION('ref_axis',(0.99757569190683,-0.0464672203152359,0.0518028604691345));
#123724=DIRECTION('',(0.,0.,1.));
#123725=DIRECTION('',(0.,0.,1.));
#123726=DIRECTION('center_axis',(0.,0.,1.));
#123727=DIRECTION('ref_axis',(-0.518392568310538,-0.855142763005338,0.));
#123728=DIRECTION('center_axis',(0.,0.,-1.));
#123729=DIRECTION('ref_axis',(0.518392568310538,0.855142763005338,0.));
#123730=DIRECTION('center_axis',(0.690593504295649,0.683700603779683,-0.235868811452367));
#123731=DIRECTION('ref_axis',(-0.397075176320611,0.630999809812658,0.666461209948745));
#123732=DIRECTION('center_axis',(0.28674254234956,0.928517430203087,0.235868811452396));
#123733=DIRECTION('ref_axis',(0.743106466862043,-0.0601850027357412,-0.666461209939115));
#123734=DIRECTION('center_axis',(0.,0.,-1.));
#123735=DIRECTION('ref_axis',(0.518392568310517,0.855142763005351,0.));
#123736=DIRECTION('center_axis',(-0.506161733806052,-0.862438577076914,
-6.76296429840134E-17));
#123737=DIRECTION('ref_axis',(-0.862438577076914,0.506161733806052,6.90253292068385E-31));
#123738=DIRECTION('center_axis',(0.,0.,1.));
#123739=DIRECTION('ref_axis',(-0.518392568310517,-0.855142763005351,0.));
#123740=DIRECTION('center_axis',(-0.530518261285706,-0.847673506983905,
-1.38914942345546E-16));
#123741=DIRECTION('ref_axis',(0.847673506983905,-0.530518261285706,-3.69778549322349E-32));
#123742=DIRECTION('center_axis',(0.,0.,-1.));
#123743=DIRECTION('ref_axis',(0.518392568310514,0.855142763005353,0.));
#123744=DIRECTION('center_axis',(0.,0.,1.));
#123745=DIRECTION('ref_axis',(-0.518392568310514,-0.855142763005353,0.));
#123746=DIRECTION('center_axis',(0.,0.,1.));
#123747=DIRECTION('ref_axis',(-0.518392568310514,-0.855142763005353,0.));
#123748=DIRECTION('center_axis',(-0.747239865790715,0.0348065412515887,
0.663642288932205));
#123749=DIRECTION('ref_axis',(-0.607692426578982,0.368386720189271,-0.703563173472532));
#123750=DIRECTION('center_axis',(-0.749388987580438,0.0349066476560422,
0.661209249211309));
#123751=DIRECTION('ref_axis',(-0.60572037068534,0.367191248317438,-0.705884848750768));
#123752=DIRECTION('center_axis',(0.377569310640434,-0.648262095467509,-0.661209249211308));
#123753=DIRECTION('ref_axis',(0.605720370685331,-0.367191248317456,0.705884848750767));
#123754=DIRECTION('center_axis',(0.376486505253551,-0.646402988624604,-0.663642288932184));
#123755=DIRECTION('ref_axis',(0.607692426578966,-0.368386720189256,0.703563173472553));
#123756=DIRECTION('center_axis',(0.,0.,1.));
#123757=DIRECTION('ref_axis',(-0.518392568310514,-0.855142763005353,0.));
#123758=DIRECTION('center_axis',(0.,0.,1.));
#123759=DIRECTION('ref_axis',(-0.518392568310514,-0.855142763005353,0.));
#123760=DIRECTION('center_axis',(0.,0.,1.));
#123761=DIRECTION('ref_axis',(0.51839256831062,0.855142763005288,0.));
#123762=DIRECTION('center_axis',(0.,0.,-1.));
#123763=DIRECTION('ref_axis',(-0.518392568310517,-0.855142763005351,0.));
#371607=CARTESIAN_POINT('',(0.,0.,0.));
#371608=CARTESIAN_POINT('Origin',(6.93889390390723E-17,9.71445146547012E-16,
-9.21875));
#371609=CARTESIAN_POINT('',(6.93889390390724E-17,-1.17524047358083,-8.9375));
#371610=CARTESIAN_POINT('',(-1.43925448419919E-16,-1.17524047358083,-9.));
#371611=CARTESIAN_POINT('',(2.82703326498063E-16,-1.17524047358083,-9.21875));
#371612=CARTESIAN_POINT('',(-0.823407874165055,-0.838564036615861,-9.));
#371613=CARTESIAN_POINT('Ctrl Pts',(-0.823407874165055,-0.838564036615862,
-9.));
#371614=CARTESIAN_POINT('Ctrl Pts',(-0.480534359260824,-1.17524047358083,
-8.96700849718747));
#371615=CARTESIAN_POINT('Ctrl Pts',(-1.43925448419919E-16,-1.17524047358083,
-8.9375));
#371616=CARTESIAN_POINT('Origin',(0.,1.84795814293585E-15,-9.));
#371617=CARTESIAN_POINT('Origin',(6.93889390390723E-17,9.71445146547012E-16,
-9.21875));
#371618=CARTESIAN_POINT('',(6.93889390390724E-17,-1.17524047358083,-8.4375));
#371619=CARTESIAN_POINT('',(6.93889390390724E-17,-1.17524047358083,-8.5));
#371620=CARTESIAN_POINT('',(2.82703326498063E-16,-1.17524047358083,-9.21875));
#371621=CARTESIAN_POINT('Ctrl Pts',(-1.43925448419919E-16,-1.17524047358083,
-8.9375));
#371622=CARTESIAN_POINT('Ctrl Pts',(0.678525403784437,-1.17524047358083,
-8.89583333333333));
#371623=CARTESIAN_POINT('Ctrl Pts',(1.01778810567666,-0.587620236790417,
-8.85416666666667));
#371624=CARTESIAN_POINT('Ctrl Pts',(1.35705080756888,2.70659426667139E-16,
-8.8125));
#371625=CARTESIAN_POINT('Ctrl Pts',(1.01778810567666,0.587620236790417,
-8.77083333333333));
#371626=CARTESIAN_POINT('Ctrl Pts',(0.678525403784439,1.17524047358083,
-8.72916666666667));
#371627=CARTESIAN_POINT('Ctrl Pts',(0.,1.17524047358083,-8.6875));
#371628=CARTESIAN_POINT('Ctrl Pts',(-0.678525403784438,1.17524047358083,
-8.64583333333334));
#371629=CARTESIAN_POINT('Ctrl Pts',(-1.01778810567666,0.587620236790418,
-8.60416666666667));
#371630=CARTESIAN_POINT('Ctrl Pts',(-1.35705080756888,6.0304101222105E-16,
-8.5625));
#371631=CARTESIAN_POINT('Ctrl Pts',(-1.01778810567666,-0.587620236790416,
-8.52083333333333));
#371632=CARTESIAN_POINT('Ctrl Pts',(-0.678525403784438,-1.17524047358083,
-8.47916666666667));
#371633=CARTESIAN_POINT('Ctrl Pts',(-1.43925448419919E-16,-1.17524047358083,
-8.4375));
#371634=CARTESIAN_POINT('Ctrl Pts',(-1.43925448419919E-16,-1.17524047358083,
-9.));
#371635=CARTESIAN_POINT('Ctrl Pts',(0.678525403784438,-1.17524047358083,
-8.95833333333334));
#371636=CARTESIAN_POINT('Ctrl Pts',(1.01778810567666,-0.587620236790417,
-8.91666666666667));
#371637=CARTESIAN_POINT('Ctrl Pts',(1.35705080756888,2.70659426667139E-16,
-8.875));
#371638=CARTESIAN_POINT('Ctrl Pts',(1.01778810567666,0.587620236790417,
-8.83333333333333));
#371639=CARTESIAN_POINT('Ctrl Pts',(0.678525403784439,1.17524047358083,
-8.79166666666667));
#371640=CARTESIAN_POINT('Ctrl Pts',(0.,1.17524047358083,-8.75));
#371641=CARTESIAN_POINT('Ctrl Pts',(-0.678525403784438,1.17524047358083,
-8.70833333333333));
#371642=CARTESIAN_POINT('Ctrl Pts',(-1.01778810567666,0.587620236790418,
-8.66666666666667));
#371643=CARTESIAN_POINT('Ctrl Pts',(-1.35705080756888,6.0304101222105E-16,
-8.625));
#371644=CARTESIAN_POINT('Ctrl Pts',(-1.01778810567666,-0.587620236790416,
-8.58333333333333));
#371645=CARTESIAN_POINT('Ctrl Pts',(-0.678525403784438,-1.17524047358083,
-8.54166666666667));
#371646=CARTESIAN_POINT('Ctrl Pts',(-1.43925448419919E-16,-1.17524047358083,
-8.5));
#371647=CARTESIAN_POINT('Origin',(6.93889390390723E-17,9.71445146547012E-16,
-9.21875));
#371648=CARTESIAN_POINT('',(6.93889390390724E-17,-1.17524047358083,-7.9375));
#371649=CARTESIAN_POINT('',(6.93889390390724E-17,-1.17524047358083,-8.));
#371650=CARTESIAN_POINT('',(2.82703326498063E-16,-1.17524047358083,-9.21875));
#371651=CARTESIAN_POINT('Ctrl Pts',(-1.43925448419919E-16,-1.17524047358083,
-8.4375));
#371652=CARTESIAN_POINT('Ctrl Pts',(0.678525403784437,-1.17524047358083,
-8.39583333333333));
#371653=CARTESIAN_POINT('Ctrl Pts',(1.01778810567666,-0.587620236790417,
-8.35416666666667));
#371654=CARTESIAN_POINT('Ctrl Pts',(1.35705080756888,2.70659426667139E-16,
-8.3125));
#371655=CARTESIAN_POINT('Ctrl Pts',(1.01778810567666,0.587620236790417,
-8.27083333333333));
#371656=CARTESIAN_POINT('Ctrl Pts',(0.678525403784439,1.17524047358083,
-8.22916666666667));
#371657=CARTESIAN_POINT('Ctrl Pts',(0.,1.17524047358083,-8.1875));
#371658=CARTESIAN_POINT('Ctrl Pts',(-0.678525403784438,1.17524047358083,
-8.14583333333333));
#371659=CARTESIAN_POINT('Ctrl Pts',(-1.01778810567666,0.587620236790418,
-8.10416666666667));
#371660=CARTESIAN_POINT('Ctrl Pts',(-1.35705080756888,6.0304101222105E-16,
-8.0625));
#371661=CARTESIAN_POINT('Ctrl Pts',(-1.01778810567666,-0.587620236790416,
-8.02083333333333));
#371662=CARTESIAN_POINT('Ctrl Pts',(-0.678525403784438,-1.17524047358083,
-7.97916666666667));
#371663=CARTESIAN_POINT('Ctrl Pts',(-1.43925448419919E-16,-1.17524047358083,
-7.9375));
#371664=CARTESIAN_POINT('Ctrl Pts',(-1.43925448419919E-16,-1.17524047358083,
-8.5));
#371665=CARTESIAN_POINT('Ctrl Pts',(0.678525403784437,-1.17524047358083,
-8.45833333333333));
#371666=CARTESIAN_POINT('Ctrl Pts',(1.01778810567666,-0.587620236790417,
-8.41666666666667));
#371667=CARTESIAN_POINT('Ctrl Pts',(1.35705080756888,2.70659426667139E-16,
-8.375));
#371668=CARTESIAN_POINT('Ctrl Pts',(1.01778810567666,0.587620236790417,
-8.33333333333334));
#371669=CARTESIAN_POINT('Ctrl Pts',(0.678525403784439,1.17524047358083,
-8.29166666666667));
#371670=CARTESIAN_POINT('Ctrl Pts',(0.,1.17524047358083,-8.25));
#371671=CARTESIAN_POINT('Ctrl Pts',(-0.678525403784438,1.17524047358083,
-8.20833333333333));
#371672=CARTESIAN_POINT('Ctrl Pts',(-1.01778810567666,0.587620236790418,
-8.16666666666667));
#371673=CARTESIAN_POINT('Ctrl Pts',(-1.35705080756888,6.0304101222105E-16,
-8.125));
#371674=CARTESIAN_POINT('Ctrl Pts',(-1.01778810567666,-0.587620236790416,
-8.08333333333333));
#371675=CARTESIAN_POINT('Ctrl Pts',(-0.678525403784438,-1.17524047358083,
-8.04166666666667));
#371676=CARTESIAN_POINT('Ctrl Pts',(-1.43925448419919E-16,-1.17524047358083,
-8.));
#371677=CARTESIAN_POINT('Origin',(6.93889390390723E-17,9.71445146547012E-16,
-9.21875));
#371678=CARTESIAN_POINT('',(6.93889390390724E-17,-1.17524047358083,-7.4375));
#371679=CARTESIAN_POINT('',(6.93889390390724E-17,-1.17524047358083,-7.5));
#371680=CARTESIAN_POINT('',(2.82703326498063E-16,-1.17524047358083,-9.21875));
#371681=CARTESIAN_POINT('Ctrl Pts',(-1.43925448419919E-16,-1.17524047358083,
-7.9375));
#371682=CARTESIAN_POINT('Ctrl Pts',(0.678525403784437,-1.17524047358083,
-7.89583333333333));
#371683=CARTESIAN_POINT('Ctrl Pts',(1.01778810567666,-0.587620236790417,
-7.85416666666667));
#371684=CARTESIAN_POINT('Ctrl Pts',(1.35705080756888,2.7065942666714E-16,
-7.8125));
#371685=CARTESIAN_POINT('Ctrl Pts',(1.01778810567666,0.587620236790417,
-7.77083333333333));
#371686=CARTESIAN_POINT('Ctrl Pts',(0.678525403784439,1.17524047358083,
-7.72916666666667));
#371687=CARTESIAN_POINT('Ctrl Pts',(0.,1.17524047358083,-7.6875));
#371688=CARTESIAN_POINT('Ctrl Pts',(-0.678525403784438,1.17524047358083,
-7.64583333333333));
#371689=CARTESIAN_POINT('Ctrl Pts',(-1.01778810567666,0.587620236790418,
-7.60416666666667));
#371690=CARTESIAN_POINT('Ctrl Pts',(-1.35705080756888,6.0304101222105E-16,
-7.5625));
#371691=CARTESIAN_POINT('Ctrl Pts',(-1.01778810567666,-0.587620236790416,
-7.52083333333333));
#371692=CARTESIAN_POINT('Ctrl Pts',(-0.678525403784438,-1.17524047358083,
-7.47916666666667));
#371693=CARTESIAN_POINT('Ctrl Pts',(-1.43925448419919E-16,-1.17524047358083,
-7.4375));
#371694=CARTESIAN_POINT('Ctrl Pts',(-1.43925448419919E-16,-1.17524047358083,
-8.));
#371695=CARTESIAN_POINT('Ctrl Pts',(0.678525403784437,-1.17524047358083,
-7.95833333333333));
#371696=CARTESIAN_POINT('Ctrl Pts',(1.01778810567666,-0.587620236790417,
-7.91666666666667));
#371697=CARTESIAN_POINT('Ctrl Pts',(1.35705080756888,2.7065942666714E-16,
-7.875));
#371698=CARTESIAN_POINT('Ctrl Pts',(1.01778810567666,0.587620236790417,
-7.83333333333333));
#371699=CARTESIAN_POINT('Ctrl Pts',(0.678525403784439,1.17524047358083,
-7.79166666666666));
#371700=CARTESIAN_POINT('Ctrl Pts',(0.,1.17524047358083,-7.75));
#371701=CARTESIAN_POINT('Ctrl Pts',(-0.678525403784438,1.17524047358083,
-7.70833333333333));
#371702=CARTESIAN_POINT('Ctrl Pts',(-1.01778810567666,0.587620236790418,
-7.66666666666667));
#371703=CARTESIAN_POINT('Ctrl Pts',(-1.35705080756888,6.0304101222105E-16,
-7.625));
#371704=CARTESIAN_POINT('Ctrl Pts',(-1.01778810567666,-0.587620236790416,
-7.58333333333333));
#371705=CARTESIAN_POINT('Ctrl Pts',(-0.678525403784438,-1.17524047358083,
-7.54166666666667));
#371706=CARTESIAN_POINT('Ctrl Pts',(-1.43925448419919E-16,-1.17524047358083,
-7.5));
#371707=CARTESIAN_POINT('Origin',(6.93889390390723E-17,9.71445146547012E-16,
-9.21875));
#371708=CARTESIAN_POINT('',(6.93889390390724E-17,-1.17524047358083,-6.9375));
#371709=CARTESIAN_POINT('',(6.93889390390724E-17,-1.17524047358083,-7.));
#371710=CARTESIAN_POINT('',(2.82703326498063E-16,-1.17524047358083,-9.21875));
#371711=CARTESIAN_POINT('Ctrl Pts',(-1.43925448419919E-16,-1.17524047358083,
-7.4375));
#371712=CARTESIAN_POINT('Ctrl Pts',(0.678525403784437,-1.17524047358083,
-7.39583333333333));
#371713=CARTESIAN_POINT('Ctrl Pts',(1.01778810567666,-0.587620236790417,
-7.35416666666667));
#371714=CARTESIAN_POINT('Ctrl Pts',(1.35705080756888,2.7065942666714E-16,
-7.3125));
#371715=CARTESIAN_POINT('Ctrl Pts',(1.01778810567666,0.587620236790417,
-7.27083333333333));
#371716=CARTESIAN_POINT('Ctrl Pts',(0.678525403784439,1.17524047358083,
-7.22916666666667));
#371717=CARTESIAN_POINT('Ctrl Pts',(0.,1.17524047358083,-7.1875));
#371718=CARTESIAN_POINT('Ctrl Pts',(-0.678525403784438,1.17524047358083,
-7.14583333333333));
#371719=CARTESIAN_POINT('Ctrl Pts',(-1.01778810567666,0.587620236790418,
-7.10416666666667));
#371720=CARTESIAN_POINT('Ctrl Pts',(-1.35705080756888,6.0304101222105E-16,
-7.0625));
#371721=CARTESIAN_POINT('Ctrl Pts',(-1.01778810567666,-0.587620236790416,
-7.02083333333333));
#371722=CARTESIAN_POINT('Ctrl Pts',(-0.678525403784438,-1.17524047358083,
-6.97916666666667));
#371723=CARTESIAN_POINT('Ctrl Pts',(-1.43925448419919E-16,-1.17524047358083,
-6.9375));
#371724=CARTESIAN_POINT('Ctrl Pts',(-1.43925448419919E-16,-1.17524047358083,
-7.5));
#371725=CARTESIAN_POINT('Ctrl Pts',(0.678525403784437,-1.17524047358083,
-7.45833333333333));
#371726=CARTESIAN_POINT('Ctrl Pts',(1.01778810567666,-0.587620236790417,
-7.41666666666667));
#371727=CARTESIAN_POINT('Ctrl Pts',(1.35705080756888,2.7065942666714E-16,
-7.375));
#371728=CARTESIAN_POINT('Ctrl Pts',(1.01778810567666,0.587620236790417,
-7.33333333333333));
#371729=CARTESIAN_POINT('Ctrl Pts',(0.678525403784439,1.17524047358083,
-7.29166666666667));
#371730=CARTESIAN_POINT('Ctrl Pts',(0.,1.17524047358083,-7.25));
#371731=CARTESIAN_POINT('Ctrl Pts',(-0.678525403784438,1.17524047358083,
-7.20833333333333));
#371732=CARTESIAN_POINT('Ctrl Pts',(-1.01778810567666,0.587620236790418,
-7.16666666666667));
#371733=CARTESIAN_POINT('Ctrl Pts',(-1.35705080756888,6.0304101222105E-16,
-7.125));
#371734=CARTESIAN_POINT('Ctrl Pts',(-1.01778810567666,-0.587620236790416,
-7.08333333333333));
#371735=CARTESIAN_POINT('Ctrl Pts',(-0.678525403784438,-1.17524047358083,
-7.04166666666667));
#371736=CARTESIAN_POINT('Ctrl Pts',(-1.43925448419919E-16,-1.17524047358083,
-7.));
#371737=CARTESIAN_POINT('Origin',(6.93889390390723E-17,9.71445146547012E-16,
-9.21875));
#371738=CARTESIAN_POINT('',(6.93889390390724E-17,-1.17524047358083,-6.4375));
#371739=CARTESIAN_POINT('',(6.93889390390724E-17,-1.17524047358083,-6.5));
#371740=CARTESIAN_POINT('',(2.82703326498063E-16,-1.17524047358083,-9.21875));
#371741=CARTESIAN_POINT('Ctrl Pts',(-1.43925448419919E-16,-1.17524047358083,
-6.9375));
#371742=CARTESIAN_POINT('Ctrl Pts',(0.678525403784437,-1.17524047358083,
-6.89583333333333));
#371743=CARTESIAN_POINT('Ctrl Pts',(1.01778810567666,-0.587620236790417,
-6.85416666666667));
#371744=CARTESIAN_POINT('Ctrl Pts',(1.35705080756888,2.7065942666714E-16,
-6.8125));
#371745=CARTESIAN_POINT('Ctrl Pts',(1.01778810567666,0.587620236790417,
-6.77083333333333));
#371746=CARTESIAN_POINT('Ctrl Pts',(0.678525403784439,1.17524047358083,
-6.72916666666667));
#371747=CARTESIAN_POINT('Ctrl Pts',(0.,1.17524047358083,-6.6875));
#371748=CARTESIAN_POINT('Ctrl Pts',(-0.678525403784438,1.17524047358083,
-6.64583333333333));
#371749=CARTESIAN_POINT('Ctrl Pts',(-1.01778810567666,0.587620236790418,
-6.60416666666667));
#371750=CARTESIAN_POINT('Ctrl Pts',(-1.35705080756888,6.0304101222105E-16,
-6.5625));
#371751=CARTESIAN_POINT('Ctrl Pts',(-1.01778810567666,-0.587620236790416,
-6.52083333333333));
#371752=CARTESIAN_POINT('Ctrl Pts',(-0.678525403784438,-1.17524047358083,
-6.47916666666667));
#371753=CARTESIAN_POINT('Ctrl Pts',(-1.43925448419919E-16,-1.17524047358083,
-6.4375));
#371754=CARTESIAN_POINT('Ctrl Pts',(-1.43925448419919E-16,-1.17524047358083,
-7.));
#371755=CARTESIAN_POINT('Ctrl Pts',(0.678525403784437,-1.17524047358083,
-6.95833333333333));
#371756=CARTESIAN_POINT('Ctrl Pts',(1.01778810567666,-0.587620236790417,
-6.91666666666667));
#371757=CARTESIAN_POINT('Ctrl Pts',(1.35705080756888,2.7065942666714E-16,
-6.875));
#371758=CARTESIAN_POINT('Ctrl Pts',(1.01778810567666,0.587620236790417,
-6.83333333333333));
#371759=CARTESIAN_POINT('Ctrl Pts',(0.678525403784439,1.17524047358083,
-6.79166666666667));
#371760=CARTESIAN_POINT('Ctrl Pts',(0.,1.17524047358083,-6.75));
#371761=CARTESIAN_POINT('Ctrl Pts',(-0.678525403784438,1.17524047358083,
-6.70833333333333));
#371762=CARTESIAN_POINT('Ctrl Pts',(-1.01778810567666,0.587620236790418,
-6.66666666666667));
#371763=CARTESIAN_POINT('Ctrl Pts',(-1.35705080756888,6.0304101222105E-16,
-6.625));
#371764=CARTESIAN_POINT('Ctrl Pts',(-1.01778810567666,-0.587620236790416,
-6.58333333333333));
#371765=CARTESIAN_POINT('Ctrl Pts',(-0.678525403784438,-1.17524047358083,
-6.54166666666667));
#371766=CARTESIAN_POINT('Ctrl Pts',(-1.43925448419919E-16,-1.17524047358083,
-6.5));
#371767=CARTESIAN_POINT('Origin',(6.93889390390723E-17,9.71445146547012E-16,
-9.21875));
#371768=CARTESIAN_POINT('',(6.93889390390724E-17,-1.17524047358083,-5.9375));
#371769=CARTESIAN_POINT('',(6.93889390390724E-17,-1.17524047358083,-6.));
#371770=CARTESIAN_POINT('',(2.82703326498063E-16,-1.17524047358083,-9.21875));
#371771=CARTESIAN_POINT('Ctrl Pts',(-1.43925448419919E-16,-1.17524047358083,
-6.4375));
#371772=CARTESIAN_POINT('Ctrl Pts',(0.678525403784437,-1.17524047358083,
-6.39583333333333));
#371773=CARTESIAN_POINT('Ctrl Pts',(1.01778810567666,-0.587620236790417,
-6.35416666666667));
#371774=CARTESIAN_POINT('Ctrl Pts',(1.35705080756888,2.7065942666714E-16,
-6.3125));
#371775=CARTESIAN_POINT('Ctrl Pts',(1.01778810567666,0.587620236790417,
-6.27083333333333));
#371776=CARTESIAN_POINT('Ctrl Pts',(0.678525403784439,1.17524047358083,
-6.22916666666667));
#371777=CARTESIAN_POINT('Ctrl Pts',(0.,1.17524047358083,-6.1875));
#371778=CARTESIAN_POINT('Ctrl Pts',(-0.678525403784438,1.17524047358083,
-6.14583333333333));
#371779=CARTESIAN_POINT('Ctrl Pts',(-1.01778810567666,0.587620236790418,
-6.10416666666667));
#371780=CARTESIAN_POINT('Ctrl Pts',(-1.35705080756888,6.0304101222105E-16,
-6.0625));
#371781=CARTESIAN_POINT('Ctrl Pts',(-1.01778810567666,-0.587620236790416,
-6.02083333333333));
#371782=CARTESIAN_POINT('Ctrl Pts',(-0.678525403784438,-1.17524047358083,
-5.97916666666667));
#371783=CARTESIAN_POINT('Ctrl Pts',(-1.43925448419919E-16,-1.17524047358083,
-5.9375));
#371784=CARTESIAN_POINT('Ctrl Pts',(-1.43925448419919E-16,-1.17524047358083,
-6.5));
#371785=CARTESIAN_POINT('Ctrl Pts',(0.678525403784437,-1.17524047358083,
-6.45833333333333));
#371786=CARTESIAN_POINT('Ctrl Pts',(1.01778810567666,-0.587620236790417,
-6.41666666666667));
#371787=CARTESIAN_POINT('Ctrl Pts',(1.35705080756888,2.7065942666714E-16,
-6.375));
#371788=CARTESIAN_POINT('Ctrl Pts',(1.01778810567666,0.587620236790417,
-6.33333333333333));
#371789=CARTESIAN_POINT('Ctrl Pts',(0.678525403784439,1.17524047358083,
-6.29166666666667));
#371790=CARTESIAN_POINT('Ctrl Pts',(0.,1.17524047358083,-6.25));
#371791=CARTESIAN_POINT('Ctrl Pts',(-0.678525403784438,1.17524047358083,
-6.20833333333333));
#371792=CARTESIAN_POINT('Ctrl Pts',(-1.01778810567666,0.587620236790418,
-6.16666666666667));
#371793=CARTESIAN_POINT('Ctrl Pts',(-1.35705080756888,6.0304101222105E-16,
-6.125));
#371794=CARTESIAN_POINT('Ctrl Pts',(-1.01778810567666,-0.587620236790416,
-6.08333333333333));
#371795=CARTESIAN_POINT('Ctrl Pts',(-0.678525403784438,-1.17524047358083,
-6.04166666666667));
#371796=CARTESIAN_POINT('Ctrl Pts',(-1.43925448419919E-16,-1.17524047358083,
-6.));
#371797=CARTESIAN_POINT('Origin',(6.93889390390723E-17,9.71445146547012E-16,
-9.21875));
#371798=CARTESIAN_POINT('',(6.93889390390724E-17,-1.17524047358083,-5.4375));
#371799=CARTESIAN_POINT('',(6.93889390390724E-17,-1.17524047358083,-5.5));
#371800=CARTESIAN_POINT('',(2.82703326498063E-16,-1.17524047358083,-9.21875));
#371801=CARTESIAN_POINT('Ctrl Pts',(-1.43925448419919E-16,-1.17524047358083,
-5.9375));
#371802=CARTESIAN_POINT('Ctrl Pts',(0.678525403784437,-1.17524047358083,
-5.89583333333333));
#371803=CARTESIAN_POINT('Ctrl Pts',(1.01778810567666,-0.587620236790417,
-5.85416666666667));
#371804=CARTESIAN_POINT('Ctrl Pts',(1.35705080756888,2.7065942666714E-16,
-5.8125));
#371805=CARTESIAN_POINT('Ctrl Pts',(1.01778810567666,0.587620236790417,
-5.77083333333333));
#371806=CARTESIAN_POINT('Ctrl Pts',(0.678525403784439,1.17524047358083,
-5.72916666666667));
#371807=CARTESIAN_POINT('Ctrl Pts',(0.,1.17524047358083,-5.6875));
#371808=CARTESIAN_POINT('Ctrl Pts',(-0.678525403784438,1.17524047358083,
-5.64583333333333));
#371809=CARTESIAN_POINT('Ctrl Pts',(-1.01778810567666,0.587620236790418,
-5.60416666666667));
#371810=CARTESIAN_POINT('Ctrl Pts',(-1.35705080756888,6.0304101222105E-16,
-5.5625));
#371811=CARTESIAN_POINT('Ctrl Pts',(-1.01778810567666,-0.587620236790416,
-5.52083333333333));
#371812=CARTESIAN_POINT('Ctrl Pts',(-0.678525403784438,-1.17524047358083,
-5.47916666666667));
#371813=CARTESIAN_POINT('Ctrl Pts',(-1.43925448419919E-16,-1.17524047358083,
-5.4375));
#371814=CARTESIAN_POINT('Ctrl Pts',(-1.43925448419919E-16,-1.17524047358083,
-6.));
#371815=CARTESIAN_POINT('Ctrl Pts',(0.678525403784437,-1.17524047358083,
-5.95833333333333));
#371816=CARTESIAN_POINT('Ctrl Pts',(1.01778810567666,-0.587620236790417,
-5.91666666666667));
#371817=CARTESIAN_POINT('Ctrl Pts',(1.35705080756888,2.7065942666714E-16,
-5.875));
#371818=CARTESIAN_POINT('Ctrl Pts',(1.01778810567666,0.587620236790417,
-5.83333333333333));
#371819=CARTESIAN_POINT('Ctrl Pts',(0.678525403784439,1.17524047358083,
-5.79166666666667));
#371820=CARTESIAN_POINT('Ctrl Pts',(0.,1.17524047358083,-5.75));
#371821=CARTESIAN_POINT('Ctrl Pts',(-0.678525403784438,1.17524047358083,
-5.70833333333333));
#371822=CARTESIAN_POINT('Ctrl Pts',(-1.01778810567666,0.587620236790418,
-5.66666666666667));
#371823=CARTESIAN_POINT('Ctrl Pts',(-1.35705080756888,6.0304101222105E-16,
-5.625));
#371824=CARTESIAN_POINT('Ctrl Pts',(-1.01778810567666,-0.587620236790416,
-5.58333333333333));
#371825=CARTESIAN_POINT('Ctrl Pts',(-0.678525403784438,-1.17524047358083,
-5.54166666666667));
#371826=CARTESIAN_POINT('Ctrl Pts',(-1.43925448419919E-16,-1.17524047358083,
-5.5));
#371827=CARTESIAN_POINT('Origin',(6.93889390390723E-17,9.71445146547012E-16,
-9.21875));
#371828=CARTESIAN_POINT('',(6.93889390390724E-17,-1.17524047358083,-4.9375));
#371829=CARTESIAN_POINT('',(6.93889390390724E-17,-1.17524047358083,-5.));
#371830=CARTESIAN_POINT('',(2.82703326498063E-16,-1.17524047358083,-9.21875));
#371831=CARTESIAN_POINT('Ctrl Pts',(-1.43925448419919E-16,-1.17524047358083,
-5.4375));
#371832=CARTESIAN_POINT('Ctrl Pts',(0.678525403784437,-1.17524047358083,
-5.39583333333333));
#371833=CARTESIAN_POINT('Ctrl Pts',(1.01778810567666,-0.587620236790417,
-5.35416666666667));
#371834=CARTESIAN_POINT('Ctrl Pts',(1.35705080756888,2.7065942666714E-16,
-5.3125));
#371835=CARTESIAN_POINT('Ctrl Pts',(1.01778810567666,0.587620236790417,
-5.27083333333333));
#371836=CARTESIAN_POINT('Ctrl Pts',(0.678525403784439,1.17524047358083,
-5.22916666666667));
#371837=CARTESIAN_POINT('Ctrl Pts',(0.,1.17524047358083,-5.1875));
#371838=CARTESIAN_POINT('Ctrl Pts',(-0.678525403784438,1.17524047358083,
-5.14583333333333));
#371839=CARTESIAN_POINT('Ctrl Pts',(-1.01778810567666,0.587620236790418,
-5.10416666666667));
#371840=CARTESIAN_POINT('Ctrl Pts',(-1.35705080756888,6.0304101222105E-16,
-5.0625));
#371841=CARTESIAN_POINT('Ctrl Pts',(-1.01778810567666,-0.587620236790416,
-5.02083333333333));
#371842=CARTESIAN_POINT('Ctrl Pts',(-0.678525403784438,-1.17524047358083,
-4.97916666666667));
#371843=CARTESIAN_POINT('Ctrl Pts',(-1.43925448419919E-16,-1.17524047358083,
-4.9375));
#371844=CARTESIAN_POINT('Ctrl Pts',(-1.43925448419919E-16,-1.17524047358083,
-5.5));
#371845=CARTESIAN_POINT('Ctrl Pts',(0.678525403784437,-1.17524047358083,
-5.45833333333333));
#371846=CARTESIAN_POINT('Ctrl Pts',(1.01778810567666,-0.587620236790417,
-5.41666666666667));
#371847=CARTESIAN_POINT('Ctrl Pts',(1.35705080756888,2.7065942666714E-16,
-5.375));
#371848=CARTESIAN_POINT('Ctrl Pts',(1.01778810567666,0.587620236790417,
-5.33333333333333));
#371849=CARTESIAN_POINT('Ctrl Pts',(0.678525403784439,1.17524047358083,
-5.29166666666667));
#371850=CARTESIAN_POINT('Ctrl Pts',(0.,1.17524047358083,-5.25));
#371851=CARTESIAN_POINT('Ctrl Pts',(-0.678525403784438,1.17524047358083,
-5.20833333333333));
#371852=CARTESIAN_POINT('Ctrl Pts',(-1.01778810567666,0.587620236790418,
-5.16666666666667));
#371853=CARTESIAN_POINT('Ctrl Pts',(-1.35705080756888,6.0304101222105E-16,
-5.125));
#371854=CARTESIAN_POINT('Ctrl Pts',(-1.01778810567666,-0.587620236790416,
-5.08333333333333));
#371855=CARTESIAN_POINT('Ctrl Pts',(-0.678525403784438,-1.17524047358083,
-5.04166666666667));
#371856=CARTESIAN_POINT('Ctrl Pts',(-1.43925448419919E-16,-1.17524047358083,
-5.));
#371857=CARTESIAN_POINT('Origin',(6.93889390390723E-17,9.71445146547012E-16,
-9.21875));
#371858=CARTESIAN_POINT('',(6.93889390390724E-17,-1.17524047358083,-4.4375));
#371859=CARTESIAN_POINT('',(6.93889390390724E-17,-1.17524047358083,-4.5));
#371860=CARTESIAN_POINT('',(2.82703326498063E-16,-1.17524047358083,-9.21875));
#371861=CARTESIAN_POINT('Ctrl Pts',(-1.43925448419919E-16,-1.17524047358083,
-4.9375));
#371862=CARTESIAN_POINT('Ctrl Pts',(0.678525403784437,-1.17524047358083,
-4.89583333333333));
#371863=CARTESIAN_POINT('Ctrl Pts',(1.01778810567666,-0.587620236790417,
-4.85416666666667));
#371864=CARTESIAN_POINT('Ctrl Pts',(1.35705080756888,2.7065942666714E-16,
-4.8125));
#371865=CARTESIAN_POINT('Ctrl Pts',(1.01778810567666,0.587620236790417,
-4.77083333333333));
#371866=CARTESIAN_POINT('Ctrl Pts',(0.678525403784439,1.17524047358083,
-4.72916666666667));
#371867=CARTESIAN_POINT('Ctrl Pts',(0.,1.17524047358083,-4.6875));
#371868=CARTESIAN_POINT('Ctrl Pts',(-0.678525403784438,1.17524047358083,
-4.64583333333333));
#371869=CARTESIAN_POINT('Ctrl Pts',(-1.01778810567666,0.587620236790418,
-4.60416666666667));
#371870=CARTESIAN_POINT('Ctrl Pts',(-1.35705080756888,6.0304101222105E-16,
-4.5625));
#371871=CARTESIAN_POINT('Ctrl Pts',(-1.01778810567666,-0.587620236790416,
-4.52083333333333));
#371872=CARTESIAN_POINT('Ctrl Pts',(-0.678525403784438,-1.17524047358083,
-4.47916666666667));
#371873=CARTESIAN_POINT('Ctrl Pts',(-1.43925448419919E-16,-1.17524047358083,
-4.4375));
#371874=CARTESIAN_POINT('Ctrl Pts',(-1.43925448419919E-16,-1.17524047358083,
-5.));
#371875=CARTESIAN_POINT('Ctrl Pts',(0.678525403784437,-1.17524047358083,
-4.95833333333333));
#371876=CARTESIAN_POINT('Ctrl Pts',(1.01778810567666,-0.587620236790417,
-4.91666666666667));
#371877=CARTESIAN_POINT('Ctrl Pts',(1.35705080756888,2.7065942666714E-16,
-4.875));
#371878=CARTESIAN_POINT('Ctrl Pts',(1.01778810567666,0.587620236790417,
-4.83333333333333));
#371879=CARTESIAN_POINT('Ctrl Pts',(0.678525403784439,1.17524047358083,
-4.79166666666667));
#371880=CARTESIAN_POINT('Ctrl Pts',(0.,1.17524047358083,-4.75));
#371881=CARTESIAN_POINT('Ctrl Pts',(-0.678525403784438,1.17524047358083,
-4.70833333333333));
#371882=CARTESIAN_POINT('Ctrl Pts',(-1.01778810567666,0.587620236790418,
-4.66666666666667));
#371883=CARTESIAN_POINT('Ctrl Pts',(-1.35705080756888,6.0304101222105E-16,
-4.625));
#371884=CARTESIAN_POINT('Ctrl Pts',(-1.01778810567666,-0.587620236790416,
-4.58333333333333));
#371885=CARTESIAN_POINT('Ctrl Pts',(-0.678525403784438,-1.17524047358083,
-4.54166666666667));
#371886=CARTESIAN_POINT('Ctrl Pts',(-1.43925448419919E-16,-1.17524047358083,
-4.5));
#371887=CARTESIAN_POINT('Origin',(6.93889390390723E-17,9.71445146547012E-16,
-9.21875));
#371888=CARTESIAN_POINT('',(6.93889390390724E-17,-1.17524047358083,-3.9375));
#371889=CARTESIAN_POINT('',(6.93889390390724E-17,-1.17524047358083,-4.));
#371890=CARTESIAN_POINT('',(2.82703326498063E-16,-1.17524047358083,-9.21875));
#371891=CARTESIAN_POINT('Ctrl Pts',(-1.43925448419919E-16,-1.17524047358083,
-4.4375));
#371892=CARTESIAN_POINT('Ctrl Pts',(0.678525403784437,-1.17524047358083,
-4.39583333333333));
#371893=CARTESIAN_POINT('Ctrl Pts',(1.01778810567666,-0.587620236790417,
-4.35416666666667));
#371894=CARTESIAN_POINT('Ctrl Pts',(1.35705080756888,2.7065942666714E-16,
-4.3125));
#371895=CARTESIAN_POINT('Ctrl Pts',(1.01778810567666,0.587620236790417,
-4.27083333333333));
#371896=CARTESIAN_POINT('Ctrl Pts',(0.678525403784439,1.17524047358083,
-4.22916666666667));
#371897=CARTESIAN_POINT('Ctrl Pts',(0.,1.17524047358083,-4.1875));
#371898=CARTESIAN_POINT('Ctrl Pts',(-0.678525403784438,1.17524047358083,
-4.14583333333333));
#371899=CARTESIAN_POINT('Ctrl Pts',(-1.01778810567666,0.587620236790418,
-4.10416666666667));
#371900=CARTESIAN_POINT('Ctrl Pts',(-1.35705080756888,6.0304101222105E-16,
-4.0625));
#371901=CARTESIAN_POINT('Ctrl Pts',(-1.01778810567666,-0.587620236790416,
-4.02083333333333));
#371902=CARTESIAN_POINT('Ctrl Pts',(-0.678525403784438,-1.17524047358083,
-3.97916666666667));
#371903=CARTESIAN_POINT('Ctrl Pts',(-1.43925448419919E-16,-1.17524047358083,
-3.9375));
#371904=CARTESIAN_POINT('Ctrl Pts',(-1.43925448419919E-16,-1.17524047358083,
-4.5));
#371905=CARTESIAN_POINT('Ctrl Pts',(0.678525403784437,-1.17524047358083,
-4.45833333333333));
#371906=CARTESIAN_POINT('Ctrl Pts',(1.01778810567666,-0.587620236790417,
-4.41666666666667));
#371907=CARTESIAN_POINT('Ctrl Pts',(1.35705080756888,2.7065942666714E-16,
-4.375));
#371908=CARTESIAN_POINT('Ctrl Pts',(1.01778810567666,0.587620236790417,
-4.33333333333333));
#371909=CARTESIAN_POINT('Ctrl Pts',(0.678525403784439,1.17524047358083,
-4.29166666666667));
#371910=CARTESIAN_POINT('Ctrl Pts',(0.,1.17524047358083,-4.25));
#371911=CARTESIAN_POINT('Ctrl Pts',(-0.678525403784438,1.17524047358083,
-4.20833333333333));
#371912=CARTESIAN_POINT('Ctrl Pts',(-1.01778810567666,0.587620236790418,
-4.16666666666667));
#371913=CARTESIAN_POINT('Ctrl Pts',(-1.35705080756888,6.0304101222105E-16,
-4.125));
#371914=CARTESIAN_POINT('Ctrl Pts',(-1.01778810567666,-0.587620236790416,
-4.08333333333333));
#371915=CARTESIAN_POINT('Ctrl Pts',(-0.678525403784438,-1.17524047358083,
-4.04166666666667));
#371916=CARTESIAN_POINT('Ctrl Pts',(-1.43925448419919E-16,-1.17524047358083,
-4.));
#371917=CARTESIAN_POINT('Origin',(6.93889390390723E-17,9.71445146547012E-16,
-9.21875));
#371918=CARTESIAN_POINT('',(6.93889390390724E-17,-1.17524047358083,-3.4375));
#371919=CARTESIAN_POINT('',(6.93889390390724E-17,-1.17524047358083,-3.5));
#371920=CARTESIAN_POINT('',(2.82703326498063E-16,-1.17524047358083,-9.21875));
#371921=CARTESIAN_POINT('Ctrl Pts',(-1.43925448419919E-16,-1.17524047358083,
-3.9375));
#371922=CARTESIAN_POINT('Ctrl Pts',(0.678525403784437,-1.17524047358083,
-3.89583333333333));
#371923=CARTESIAN_POINT('Ctrl Pts',(1.01778810567666,-0.587620236790417,
-3.85416666666667));
#371924=CARTESIAN_POINT('Ctrl Pts',(1.35705080756888,2.7065942666714E-16,
-3.8125));
#371925=CARTESIAN_POINT('Ctrl Pts',(1.01778810567666,0.587620236790417,
-3.77083333333333));
#371926=CARTESIAN_POINT('Ctrl Pts',(0.678525403784439,1.17524047358083,
-3.72916666666667));
#371927=CARTESIAN_POINT('Ctrl Pts',(0.,1.17524047358083,-3.6875));
#371928=CARTESIAN_POINT('Ctrl Pts',(-0.678525403784438,1.17524047358083,
-3.64583333333333));
#371929=CARTESIAN_POINT('Ctrl Pts',(-1.01778810567666,0.587620236790418,
-3.60416666666667));
#371930=CARTESIAN_POINT('Ctrl Pts',(-1.35705080756888,6.0304101222105E-16,
-3.5625));
#371931=CARTESIAN_POINT('Ctrl Pts',(-1.01778810567666,-0.587620236790416,
-3.52083333333333));
#371932=CARTESIAN_POINT('Ctrl Pts',(-0.678525403784438,-1.17524047358083,
-3.47916666666667));
#371933=CARTESIAN_POINT('Ctrl Pts',(-1.43925448419919E-16,-1.17524047358083,
-3.4375));
#371934=CARTESIAN_POINT('Ctrl Pts',(-1.43925448419919E-16,-1.17524047358083,
-4.));
#371935=CARTESIAN_POINT('Ctrl Pts',(0.678525403784437,-1.17524047358083,
-3.95833333333333));
#371936=CARTESIAN_POINT('Ctrl Pts',(1.01778810567666,-0.587620236790417,
-3.91666666666667));
#371937=CARTESIAN_POINT('Ctrl Pts',(1.35705080756888,2.7065942666714E-16,
-3.875));
#371938=CARTESIAN_POINT('Ctrl Pts',(1.01778810567666,0.587620236790417,
-3.83333333333333));
#371939=CARTESIAN_POINT('Ctrl Pts',(0.678525403784439,1.17524047358083,
-3.79166666666667));
#371940=CARTESIAN_POINT('Ctrl Pts',(0.,1.17524047358083,-3.75));
#371941=CARTESIAN_POINT('Ctrl Pts',(-0.678525403784438,1.17524047358083,
-3.70833333333333));
#371942=CARTESIAN_POINT('Ctrl Pts',(-1.01778810567666,0.587620236790418,
-3.66666666666667));
#371943=CARTESIAN_POINT('Ctrl Pts',(-1.35705080756888,6.0304101222105E-16,
-3.625));
#371944=CARTESIAN_POINT('Ctrl Pts',(-1.01778810567666,-0.587620236790416,
-3.58333333333333));
#371945=CARTESIAN_POINT('Ctrl Pts',(-0.678525403784438,-1.17524047358083,
-3.54166666666667));
#371946=CARTESIAN_POINT('Ctrl Pts',(-1.43925448419919E-16,-1.17524047358083,
-3.5));
#371947=CARTESIAN_POINT('Origin',(6.93889390390723E-17,9.71445146547012E-16,
-9.21875));
#371948=CARTESIAN_POINT('',(6.93889390390724E-17,-1.17524047358083,-2.9375));
#371949=CARTESIAN_POINT('',(6.93889390390724E-17,-1.17524047358083,-3.));
#371950=CARTESIAN_POINT('',(2.82703326498063E-16,-1.17524047358083,-9.21875));
#371951=CARTESIAN_POINT('Ctrl Pts',(-1.43925448419919E-16,-1.17524047358083,
-3.4375));
#371952=CARTESIAN_POINT('Ctrl Pts',(0.678525403784437,-1.17524047358083,
-3.39583333333333));
#371953=CARTESIAN_POINT('Ctrl Pts',(1.01778810567666,-0.587620236790417,
-3.35416666666667));
#371954=CARTESIAN_POINT('Ctrl Pts',(1.35705080756888,2.7065942666714E-16,
-3.3125));
#371955=CARTESIAN_POINT('Ctrl Pts',(1.01778810567666,0.587620236790417,
-3.27083333333333));
#371956=CARTESIAN_POINT('Ctrl Pts',(0.678525403784439,1.17524047358083,
-3.22916666666667));
#371957=CARTESIAN_POINT('Ctrl Pts',(0.,1.17524047358083,-3.1875));
#371958=CARTESIAN_POINT('Ctrl Pts',(-0.678525403784438,1.17524047358083,
-3.14583333333333));
#371959=CARTESIAN_POINT('Ctrl Pts',(-1.01778810567666,0.587620236790418,
-3.10416666666667));
#371960=CARTESIAN_POINT('Ctrl Pts',(-1.35705080756888,6.0304101222105E-16,
-3.0625));
#371961=CARTESIAN_POINT('Ctrl Pts',(-1.01778810567666,-0.587620236790416,
-3.02083333333333));
#371962=CARTESIAN_POINT('Ctrl Pts',(-0.678525403784438,-1.17524047358083,
-2.97916666666667));
#371963=CARTESIAN_POINT('Ctrl Pts',(-1.43925448419919E-16,-1.17524047358083,
-2.9375));
#371964=CARTESIAN_POINT('Ctrl Pts',(-1.43925448419919E-16,-1.17524047358083,
-3.5));
#371965=CARTESIAN_POINT('Ctrl Pts',(0.678525403784437,-1.17524047358083,
-3.45833333333333));
#371966=CARTESIAN_POINT('Ctrl Pts',(1.01778810567666,-0.587620236790417,
-3.41666666666667));
#371967=CARTESIAN_POINT('Ctrl Pts',(1.35705080756888,2.7065942666714E-16,
-3.375));
#371968=CARTESIAN_POINT('Ctrl Pts',(1.01778810567666,0.587620236790417,
-3.33333333333333));
#371969=CARTESIAN_POINT('Ctrl Pts',(0.678525403784439,1.17524047358083,
-3.29166666666667));
#371970=CARTESIAN_POINT('Ctrl Pts',(0.,1.17524047358083,-3.25));
#371971=CARTESIAN_POINT('Ctrl Pts',(-0.678525403784438,1.17524047358083,
-3.20833333333333));
#371972=CARTESIAN_POINT('Ctrl Pts',(-1.01778810567666,0.587620236790418,
-3.16666666666667));
#371973=CARTESIAN_POINT('Ctrl Pts',(-1.35705080756888,6.0304101222105E-16,
-3.125));
#371974=CARTESIAN_POINT('Ctrl Pts',(-1.01778810567666,-0.587620236790416,
-3.08333333333333));
#371975=CARTESIAN_POINT('Ctrl Pts',(-0.678525403784438,-1.17524047358083,
-3.04166666666667));
#371976=CARTESIAN_POINT('Ctrl Pts',(-1.43925448419919E-16,-1.17524047358083,
-3.));
#371977=CARTESIAN_POINT('Origin',(6.93889390390723E-17,9.71445146547012E-16,
-9.21875));
#371978=CARTESIAN_POINT('',(6.93889390390724E-17,-1.17524047358083,-2.4375));
#371979=CARTESIAN_POINT('',(6.93889390390724E-17,-1.17524047358083,-2.5));
#371980=CARTESIAN_POINT('',(2.82703326498063E-16,-1.17524047358083,-9.21875));
#371981=CARTESIAN_POINT('Ctrl Pts',(-1.43925448419919E-16,-1.17524047358083,
-2.9375));
#371982=CARTESIAN_POINT('Ctrl Pts',(0.678525403784437,-1.17524047358083,
-2.89583333333333));
#371983=CARTESIAN_POINT('Ctrl Pts',(1.01778810567666,-0.587620236790417,
-2.85416666666667));
#371984=CARTESIAN_POINT('Ctrl Pts',(1.35705080756888,2.7065942666714E-16,
-2.8125));
#371985=CARTESIAN_POINT('Ctrl Pts',(1.01778810567666,0.587620236790417,
-2.77083333333333));
#371986=CARTESIAN_POINT('Ctrl Pts',(0.678525403784439,1.17524047358083,
-2.72916666666667));
#371987=CARTESIAN_POINT('Ctrl Pts',(0.,1.17524047358083,-2.6875));
#371988=CARTESIAN_POINT('Ctrl Pts',(-0.678525403784438,1.17524047358083,
-2.64583333333333));
#371989=CARTESIAN_POINT('Ctrl Pts',(-1.01778810567666,0.587620236790418,
-2.60416666666667));
#371990=CARTESIAN_POINT('Ctrl Pts',(-1.35705080756888,6.03041012221051E-16,
-2.5625));
#371991=CARTESIAN_POINT('Ctrl Pts',(-1.01778810567666,-0.587620236790416,
-2.52083333333333));
#371992=CARTESIAN_POINT('Ctrl Pts',(-0.678525403784438,-1.17524047358083,
-2.47916666666667));
#371993=CARTESIAN_POINT('Ctrl Pts',(-1.43925448419919E-16,-1.17524047358083,
-2.4375));
#371994=CARTESIAN_POINT('Ctrl Pts',(-1.43925448419919E-16,-1.17524047358083,
-3.));
#371995=CARTESIAN_POINT('Ctrl Pts',(0.678525403784437,-1.17524047358083,
-2.95833333333333));
#371996=CARTESIAN_POINT('Ctrl Pts',(1.01778810567666,-0.587620236790417,
-2.91666666666667));
#371997=CARTESIAN_POINT('Ctrl Pts',(1.35705080756888,2.7065942666714E-16,
-2.875));
#371998=CARTESIAN_POINT('Ctrl Pts',(1.01778810567666,0.587620236790417,
-2.83333333333333));
#371999=CARTESIAN_POINT('Ctrl Pts',(0.678525403784439,1.17524047358083,
-2.79166666666667));
#372000=CARTESIAN_POINT('Ctrl Pts',(0.,1.17524047358083,-2.75));
#372001=CARTESIAN_POINT('Ctrl Pts',(-0.678525403784438,1.17524047358083,
-2.70833333333333));
#372002=CARTESIAN_POINT('Ctrl Pts',(-1.01778810567666,0.587620236790418,
-2.66666666666667));
#372003=CARTESIAN_POINT('Ctrl Pts',(-1.35705080756888,6.03041012221051E-16,
-2.625));
#372004=CARTESIAN_POINT('Ctrl Pts',(-1.01778810567666,-0.587620236790416,
-2.58333333333333));
#372005=CARTESIAN_POINT('Ctrl Pts',(-0.678525403784438,-1.17524047358083,
-2.54166666666667));
#372006=CARTESIAN_POINT('Ctrl Pts',(-1.43925448419919E-16,-1.17524047358083,
-2.5));
#372007=CARTESIAN_POINT('Origin',(6.93889390390723E-17,9.71445146547012E-16,
-9.21875));
#372008=CARTESIAN_POINT('',(6.93889390390724E-17,-1.17524047358083,-1.9375));
#372009=CARTESIAN_POINT('',(6.93889390390724E-17,-1.17524047358083,-2.));
#372010=CARTESIAN_POINT('',(2.82703326498063E-16,-1.17524047358083,-9.21875));
#372011=CARTESIAN_POINT('Ctrl Pts',(-1.43925448419919E-16,-1.17524047358083,
-2.4375));
#372012=CARTESIAN_POINT('Ctrl Pts',(0.678525403784437,-1.17524047358083,
-2.39583333333333));
#372013=CARTESIAN_POINT('Ctrl Pts',(1.01778810567666,-0.587620236790417,
-2.35416666666667));
#372014=CARTESIAN_POINT('Ctrl Pts',(1.35705080756888,2.7065942666714E-16,
-2.3125));
#372015=CARTESIAN_POINT('Ctrl Pts',(1.01778810567666,0.587620236790417,
-2.27083333333333));
#372016=CARTESIAN_POINT('Ctrl Pts',(0.678525403784439,1.17524047358083,
-2.22916666666667));
#372017=CARTESIAN_POINT('Ctrl Pts',(0.,1.17524047358083,-2.1875));
#372018=CARTESIAN_POINT('Ctrl Pts',(-0.678525403784438,1.17524047358083,
-2.14583333333333));
#372019=CARTESIAN_POINT('Ctrl Pts',(-1.01778810567666,0.587620236790418,
-2.10416666666667));
#372020=CARTESIAN_POINT('Ctrl Pts',(-1.35705080756888,6.03041012221051E-16,
-2.0625));
#372021=CARTESIAN_POINT('Ctrl Pts',(-1.01778810567666,-0.587620236790416,
-2.02083333333333));
#372022=CARTESIAN_POINT('Ctrl Pts',(-0.678525403784438,-1.17524047358083,
-1.97916666666667));
#372023=CARTESIAN_POINT('Ctrl Pts',(-1.43925448419919E-16,-1.17524047358083,
-1.9375));
#372024=CARTESIAN_POINT('Ctrl Pts',(-1.43925448419919E-16,-1.17524047358083,
-2.5));
#372025=CARTESIAN_POINT('Ctrl Pts',(0.678525403784437,-1.17524047358083,
-2.45833333333333));
#372026=CARTESIAN_POINT('Ctrl Pts',(1.01778810567666,-0.587620236790417,
-2.41666666666667));
#372027=CARTESIAN_POINT('Ctrl Pts',(1.35705080756888,2.7065942666714E-16,
-2.375));
#372028=CARTESIAN_POINT('Ctrl Pts',(1.01778810567666,0.587620236790417,
-2.33333333333333));
#372029=CARTESIAN_POINT('Ctrl Pts',(0.678525403784439,1.17524047358083,
-2.29166666666667));
#372030=CARTESIAN_POINT('Ctrl Pts',(0.,1.17524047358083,-2.25));
#372031=CARTESIAN_POINT('Ctrl Pts',(-0.678525403784438,1.17524047358083,
-2.20833333333333));
#372032=CARTESIAN_POINT('Ctrl Pts',(-1.01778810567666,0.587620236790418,
-2.16666666666667));
#372033=CARTESIAN_POINT('Ctrl Pts',(-1.35705080756888,6.03041012221051E-16,
-2.125));
#372034=CARTESIAN_POINT('Ctrl Pts',(-1.01778810567666,-0.587620236790416,
-2.08333333333333));
#372035=CARTESIAN_POINT('Ctrl Pts',(-0.678525403784438,-1.17524047358083,
-2.04166666666667));
#372036=CARTESIAN_POINT('Ctrl Pts',(-1.43925448419919E-16,-1.17524047358083,
-2.));
#372037=CARTESIAN_POINT('Origin',(6.93889390390723E-17,9.71445146547012E-16,
-9.21875));
#372038=CARTESIAN_POINT('',(6.93889390390724E-17,-1.17524047358083,-1.4375));
#372039=CARTESIAN_POINT('',(6.93889390390724E-17,-1.17524047358083,-1.5));
#372040=CARTESIAN_POINT('',(2.82703326498063E-16,-1.17524047358083,-9.21875));
#372041=CARTESIAN_POINT('Ctrl Pts',(-1.43925448419919E-16,-1.17524047358083,
-1.9375));
#372042=CARTESIAN_POINT('Ctrl Pts',(0.678525403784437,-1.17524047358083,
-1.89583333333333));
#372043=CARTESIAN_POINT('Ctrl Pts',(1.01778810567666,-0.587620236790417,
-1.85416666666667));
#372044=CARTESIAN_POINT('Ctrl Pts',(1.35705080756888,2.7065942666714E-16,
-1.8125));
#372045=CARTESIAN_POINT('Ctrl Pts',(1.01778810567666,0.587620236790417,
-1.77083333333333));
#372046=CARTESIAN_POINT('Ctrl Pts',(0.678525403784439,1.17524047358083,
-1.72916666666667));
#372047=CARTESIAN_POINT('Ctrl Pts',(0.,1.17524047358083,-1.6875));
#372048=CARTESIAN_POINT('Ctrl Pts',(-0.678525403784438,1.17524047358083,
-1.64583333333333));
#372049=CARTESIAN_POINT('Ctrl Pts',(-1.01778810567666,0.587620236790418,
-1.60416666666667));
#372050=CARTESIAN_POINT('Ctrl Pts',(-1.35705080756888,6.03041012221051E-16,
-1.5625));
#372051=CARTESIAN_POINT('Ctrl Pts',(-1.01778810567666,-0.587620236790416,
-1.52083333333333));
#372052=CARTESIAN_POINT('Ctrl Pts',(-0.678525403784438,-1.17524047358083,
-1.47916666666667));
#372053=CARTESIAN_POINT('Ctrl Pts',(-1.43925448419919E-16,-1.17524047358083,
-1.4375));
#372054=CARTESIAN_POINT('Ctrl Pts',(-1.43925448419919E-16,-1.17524047358083,
-2.));
#372055=CARTESIAN_POINT('Ctrl Pts',(0.678525403784437,-1.17524047358083,
-1.95833333333333));
#372056=CARTESIAN_POINT('Ctrl Pts',(1.01778810567666,-0.587620236790417,
-1.91666666666667));
#372057=CARTESIAN_POINT('Ctrl Pts',(1.35705080756888,2.7065942666714E-16,
-1.875));
#372058=CARTESIAN_POINT('Ctrl Pts',(1.01778810567666,0.587620236790417,
-1.83333333333333));
#372059=CARTESIAN_POINT('Ctrl Pts',(0.678525403784439,1.17524047358083,
-1.79166666666667));
#372060=CARTESIAN_POINT('Ctrl Pts',(0.,1.17524047358083,-1.75));
#372061=CARTESIAN_POINT('Ctrl Pts',(-0.678525403784438,1.17524047358083,
-1.70833333333333));
#372062=CARTESIAN_POINT('Ctrl Pts',(-1.01778810567666,0.587620236790418,
-1.66666666666667));
#372063=CARTESIAN_POINT('Ctrl Pts',(-1.35705080756888,6.03041012221051E-16,
-1.625));
#372064=CARTESIAN_POINT('Ctrl Pts',(-1.01778810567666,-0.587620236790416,
-1.58333333333333));
#372065=CARTESIAN_POINT('Ctrl Pts',(-0.678525403784438,-1.17524047358083,
-1.54166666666667));
#372066=CARTESIAN_POINT('Ctrl Pts',(-1.43925448419919E-16,-1.17524047358083,
-1.5));
#372067=CARTESIAN_POINT('Origin',(6.93889390390723E-17,9.71445146547012E-16,
-9.21875));
#372068=CARTESIAN_POINT('',(6.93889390390724E-17,-1.17524047358083,-0.937499999999999));
#372069=CARTESIAN_POINT('',(6.93889390390724E-17,-1.17524047358083,-0.999999999999999));
#372070=CARTESIAN_POINT('',(2.82703326498063E-16,-1.17524047358083,-9.21875));
#372071=CARTESIAN_POINT('Ctrl Pts',(-1.43925448419919E-16,-1.17524047358083,
-1.4375));
#372072=CARTESIAN_POINT('Ctrl Pts',(0.678525403784437,-1.17524047358083,
-1.39583333333333));
#372073=CARTESIAN_POINT('Ctrl Pts',(1.01778810567666,-0.587620236790417,
-1.35416666666667));
#372074=CARTESIAN_POINT('Ctrl Pts',(1.35705080756888,2.7065942666714E-16,
-1.3125));
#372075=CARTESIAN_POINT('Ctrl Pts',(1.01778810567666,0.587620236790417,
-1.27083333333333));
#372076=CARTESIAN_POINT('Ctrl Pts',(0.678525403784439,1.17524047358083,
-1.22916666666667));
#372077=CARTESIAN_POINT('Ctrl Pts',(0.,1.17524047358083,-1.1875));
#372078=CARTESIAN_POINT('Ctrl Pts',(-0.678525403784438,1.17524047358083,
-1.14583333333333));
#372079=CARTESIAN_POINT('Ctrl Pts',(-1.01778810567666,0.587620236790418,
-1.10416666666667));
#372080=CARTESIAN_POINT('Ctrl Pts',(-1.35705080756888,6.03041012221051E-16,
-1.0625));
#372081=CARTESIAN_POINT('Ctrl Pts',(-1.01778810567666,-0.587620236790416,
-1.02083333333333));
#372082=CARTESIAN_POINT('Ctrl Pts',(-0.678525403784438,-1.17524047358083,
-0.979166666666667));
#372083=CARTESIAN_POINT('Ctrl Pts',(-1.43925448419919E-16,-1.17524047358083,
-0.937499999999999));
#372084=CARTESIAN_POINT('Ctrl Pts',(-1.43925448419919E-16,-1.17524047358083,
-1.5));
#372085=CARTESIAN_POINT('Ctrl Pts',(0.678525403784437,-1.17524047358083,
-1.45833333333333));
#372086=CARTESIAN_POINT('Ctrl Pts',(1.01778810567666,-0.587620236790417,
-1.41666666666667));
#372087=CARTESIAN_POINT('Ctrl Pts',(1.35705080756888,2.7065942666714E-16,
-1.375));
#372088=CARTESIAN_POINT('Ctrl Pts',(1.01778810567666,0.587620236790417,
-1.33333333333333));
#372089=CARTESIAN_POINT('Ctrl Pts',(0.678525403784439,1.17524047358083,
-1.29166666666667));
#372090=CARTESIAN_POINT('Ctrl Pts',(0.,1.17524047358083,-1.25));
#372091=CARTESIAN_POINT('Ctrl Pts',(-0.678525403784438,1.17524047358083,
-1.20833333333333));
#372092=CARTESIAN_POINT('Ctrl Pts',(-1.01778810567666,0.587620236790418,
-1.16666666666667));
#372093=CARTESIAN_POINT('Ctrl Pts',(-1.35705080756888,6.03041012221051E-16,
-1.125));
#372094=CARTESIAN_POINT('Ctrl Pts',(-1.01778810567666,-0.587620236790416,
-1.08333333333333));
#372095=CARTESIAN_POINT('Ctrl Pts',(-0.678525403784438,-1.17524047358083,
-1.04166666666667));
#372096=CARTESIAN_POINT('Ctrl Pts',(-1.43925448419919E-16,-1.17524047358083,
-0.999999999999999));
#372097=CARTESIAN_POINT('Origin',(6.93889390390723E-17,9.71445146547012E-16,
-9.21875));
#372098=CARTESIAN_POINT('',(6.93889390390724E-17,-1.17524047358083,-0.4375));
#372099=CARTESIAN_POINT('',(6.93889390390724E-17,-1.17524047358083,-0.5));
#372100=CARTESIAN_POINT('',(2.82703326498063E-16,-1.17524047358083,-9.21875));
#372101=CARTESIAN_POINT('Ctrl Pts',(-1.43925448419919E-16,-1.17524047358083,
-0.937499999999999));
#372102=CARTESIAN_POINT('Ctrl Pts',(0.678525403784437,-1.17524047358083,
-0.895833333333333));
#372103=CARTESIAN_POINT('Ctrl Pts',(1.01778810567666,-0.587620236790417,
-0.854166666666666));
#372104=CARTESIAN_POINT('Ctrl Pts',(1.35705080756888,2.7065942666714E-16,
-0.812499999999999));
#372105=CARTESIAN_POINT('Ctrl Pts',(1.01778810567666,0.587620236790417,
-0.770833333333333));
#372106=CARTESIAN_POINT('Ctrl Pts',(0.678525403784439,1.17524047358083,
-0.729166666666666));
#372107=CARTESIAN_POINT('Ctrl Pts',(0.,1.17524047358083,-0.687500000000001));
#372108=CARTESIAN_POINT('Ctrl Pts',(-0.678525403784438,1.17524047358083,
-0.645833333333333));
#372109=CARTESIAN_POINT('Ctrl Pts',(-1.01778810567666,0.587620236790418,
-0.604166666666666));
#372110=CARTESIAN_POINT('Ctrl Pts',(-1.35705080756888,6.03041012221051E-16,
-0.5625));
#372111=CARTESIAN_POINT('Ctrl Pts',(-1.01778810567666,-0.587620236790416,
-0.520833333333333));
#372112=CARTESIAN_POINT('Ctrl Pts',(-0.678525403784438,-1.17524047358083,
-0.479166666666666));
#372113=CARTESIAN_POINT('Ctrl Pts',(-1.43925448419919E-16,-1.17524047358083,
-0.4375));
#372114=CARTESIAN_POINT('Ctrl Pts',(-1.43925448419919E-16,-1.17524047358083,
-0.999999999999999));
#372115=CARTESIAN_POINT('Ctrl Pts',(0.678525403784437,-1.17524047358083,
-0.958333333333334));
#372116=CARTESIAN_POINT('Ctrl Pts',(1.01778810567666,-0.587620236790417,
-0.916666666666666));
#372117=CARTESIAN_POINT('Ctrl Pts',(1.35705080756888,2.7065942666714E-16,
-0.874999999999999));
#372118=CARTESIAN_POINT('Ctrl Pts',(1.01778810567666,0.587620236790417,
-0.833333333333334));
#372119=CARTESIAN_POINT('Ctrl Pts',(0.678525403784439,1.17524047358083,
-0.791666666666666));
#372120=CARTESIAN_POINT('Ctrl Pts',(0.,1.17524047358083,-0.750000000000001));
#372121=CARTESIAN_POINT('Ctrl Pts',(-0.678525403784438,1.17524047358083,
-0.708333333333333));
#372122=CARTESIAN_POINT('Ctrl Pts',(-1.01778810567666,0.587620236790418,
-0.666666666666666));
#372123=CARTESIAN_POINT('Ctrl Pts',(-1.35705080756888,6.03041012221051E-16,
-0.625000000000001));
#372124=CARTESIAN_POINT('Ctrl Pts',(-1.01778810567666,-0.587620236790416,
-0.583333333333333));
#372125=CARTESIAN_POINT('Ctrl Pts',(-0.678525403784438,-1.17524047358083,
-0.541666666666666));
#372126=CARTESIAN_POINT('Ctrl Pts',(-1.43925448419919E-16,-1.17524047358083,
-0.5));
#372127=CARTESIAN_POINT('Origin',(6.93889390390723E-17,9.71445146547012E-16,
-9.21875));
#372128=CARTESIAN_POINT('',(6.93889390390724E-17,-1.17524047358083,0.0625000000000001));
#372129=CARTESIAN_POINT('',(6.93889390390724E-17,-1.17524047358083,0.));
#372130=CARTESIAN_POINT('',(2.82703326498063E-16,-1.17524047358083,-9.21875));
#372131=CARTESIAN_POINT('Ctrl Pts',(-1.43925448419919E-16,-1.17524047358083,
-0.4375));
#372132=CARTESIAN_POINT('Ctrl Pts',(0.678525403784437,-1.17524047358083,
-0.395833333333333));
#372133=CARTESIAN_POINT('Ctrl Pts',(1.01778810567666,-0.587620236790417,
-0.354166666666666));
#372134=CARTESIAN_POINT('Ctrl Pts',(1.35705080756888,2.7065942666714E-16,
-0.3125));
#372135=CARTESIAN_POINT('Ctrl Pts',(1.01778810567666,0.587620236790417,
-0.270833333333333));
#372136=CARTESIAN_POINT('Ctrl Pts',(0.678525403784439,1.17524047358083,
-0.229166666666666));
#372137=CARTESIAN_POINT('Ctrl Pts',(0.,1.17524047358083,-0.1875));
#372138=CARTESIAN_POINT('Ctrl Pts',(-0.678525403784438,1.17524047358083,
-0.145833333333333));
#372139=CARTESIAN_POINT('Ctrl Pts',(-1.01778810567666,0.587620236790418,
-0.104166666666666));
#372140=CARTESIAN_POINT('Ctrl Pts',(-1.35705080756888,6.03041012221051E-16,
-0.0625000000000001));
#372141=CARTESIAN_POINT('Ctrl Pts',(-1.01778810567666,-0.587620236790416,
-0.0208333333333328));
#372142=CARTESIAN_POINT('Ctrl Pts',(-0.678525403784438,-1.17524047358083,
0.0208333333333328));
#372143=CARTESIAN_POINT('Ctrl Pts',(-1.43925448419919E-16,-1.17524047358083,
0.0625000000000001));
#372144=CARTESIAN_POINT('Ctrl Pts',(-1.43925448419919E-16,-1.17524047358083,
-0.5));
#372145=CARTESIAN_POINT('Ctrl Pts',(0.678525403784437,-1.17524047358083,
-0.458333333333333));
#372146=CARTESIAN_POINT('Ctrl Pts',(1.01778810567666,-0.587620236790417,
-0.416666666666666));
#372147=CARTESIAN_POINT('Ctrl Pts',(1.35705080756888,2.7065942666714E-16,
-0.375));
#372148=CARTESIAN_POINT('Ctrl Pts',(1.01778810567666,0.587620236790417,
-0.333333333333333));
#372149=CARTESIAN_POINT('Ctrl Pts',(0.678525403784439,1.17524047358083,
-0.291666666666666));
#372150=CARTESIAN_POINT('Ctrl Pts',(0.,1.17524047358083,-0.25));
#372151=CARTESIAN_POINT('Ctrl Pts',(-0.678525403784438,1.17524047358083,
-0.208333333333333));
#372152=CARTESIAN_POINT('Ctrl Pts',(-1.01778810567666,0.587620236790418,
-0.166666666666666));
#372153=CARTESIAN_POINT('Ctrl Pts',(-1.35705080756888,6.03041012221051E-16,
-0.125));
#372154=CARTESIAN_POINT('Ctrl Pts',(-1.01778810567666,-0.587620236790416,
-0.0833333333333328));
#372155=CARTESIAN_POINT('Ctrl Pts',(-0.678525403784438,-1.17524047358083,
-0.0416666666666673));
#372156=CARTESIAN_POINT('Ctrl Pts',(-1.43925448419919E-16,-1.17524047358083,
0.));
#372157=CARTESIAN_POINT('Origin',(6.93889390390723E-17,9.71445146547012E-16,
-9.21875));
#372158=CARTESIAN_POINT('',(6.93889390390724E-17,-1.17524047358083,0.5625));
#372159=CARTESIAN_POINT('',(6.93889390390724E-17,-1.17524047358083,0.5));
#372160=CARTESIAN_POINT('',(2.82703326498063E-16,-1.17524047358083,-9.21875));
#372161=CARTESIAN_POINT('Ctrl Pts',(-1.43925448419919E-16,-1.17524047358083,
0.0625000000000001));
#372162=CARTESIAN_POINT('Ctrl Pts',(0.678525403784437,-1.17524047358083,
0.104166666666667));
#372163=CARTESIAN_POINT('Ctrl Pts',(1.01778810567666,-0.587620236790417,
0.145833333333333));
#372164=CARTESIAN_POINT('Ctrl Pts',(1.35705080756888,2.7065942666714E-16,
0.1875));
#372165=CARTESIAN_POINT('Ctrl Pts',(1.01778810567666,0.587620236790417,
0.229166666666667));
#372166=CARTESIAN_POINT('Ctrl Pts',(0.678525403784439,1.17524047358083,
0.270833333333333));
#372167=CARTESIAN_POINT('Ctrl Pts',(0.,1.17524047358083,0.3125));
#372168=CARTESIAN_POINT('Ctrl Pts',(-0.678525403784438,1.17524047358083,
0.354166666666668));
#372169=CARTESIAN_POINT('Ctrl Pts',(-1.01778810567666,0.587620236790418,
0.395833333333333));
#372170=CARTESIAN_POINT('Ctrl Pts',(-1.35705080756888,6.03041012221051E-16,
0.4375));
#372171=CARTESIAN_POINT('Ctrl Pts',(-1.01778810567666,-0.587620236790416,
0.479166666666668));
#372172=CARTESIAN_POINT('Ctrl Pts',(-0.678525403784438,-1.17524047358083,
0.520833333333333));
#372173=CARTESIAN_POINT('Ctrl Pts',(-1.43925448419919E-16,-1.17524047358083,
0.5625));
#372174=CARTESIAN_POINT('Ctrl Pts',(-1.43925448419919E-16,-1.17524047358083,
0.));
#372175=CARTESIAN_POINT('Ctrl Pts',(0.678525403784437,-1.17524047358083,
0.0416666666666673));
#372176=CARTESIAN_POINT('Ctrl Pts',(1.01778810567666,-0.587620236790417,
0.0833333333333328));
#372177=CARTESIAN_POINT('Ctrl Pts',(1.35705080756888,2.7065942666714E-16,
0.125));
#372178=CARTESIAN_POINT('Ctrl Pts',(1.01778810567666,0.587620236790417,
0.166666666666667));
#372179=CARTESIAN_POINT('Ctrl Pts',(0.678525403784439,1.17524047358083,
0.208333333333333));
#372180=CARTESIAN_POINT('Ctrl Pts',(0.,1.17524047358083,0.25));
#372181=CARTESIAN_POINT('Ctrl Pts',(-0.678525403784438,1.17524047358083,
0.291666666666668));
#372182=CARTESIAN_POINT('Ctrl Pts',(-1.01778810567666,0.587620236790418,
0.333333333333333));
#372183=CARTESIAN_POINT('Ctrl Pts',(-1.35705080756888,6.03041012221051E-16,
0.375));
#372184=CARTESIAN_POINT('Ctrl Pts',(-1.01778810567666,-0.587620236790416,
0.416666666666668));
#372185=CARTESIAN_POINT('Ctrl Pts',(-0.678525403784438,-1.17524047358083,
0.458333333333333));
#372186=CARTESIAN_POINT('Ctrl Pts',(-1.43925448419919E-16,-1.17524047358083,
0.5));
#372187=CARTESIAN_POINT('Origin',(6.93889390390723E-17,9.71445146547012E-16,
-9.21875));
#372188=CARTESIAN_POINT('',(6.93889390390724E-17,-1.17524047358083,1.0625));
#372189=CARTESIAN_POINT('',(6.93889390390724E-17,-1.17524047358083,1.));
#372190=CARTESIAN_POINT('',(2.82703326498063E-16,-1.17524047358083,-9.21875));
#372191=CARTESIAN_POINT('Ctrl Pts',(-1.43925448419919E-16,-1.17524047358083,
0.5625));
#372192=CARTESIAN_POINT('Ctrl Pts',(0.678525403784437,-1.17524047358083,
0.604166666666666));
#372193=CARTESIAN_POINT('Ctrl Pts',(1.01778810567666,-0.587620236790417,
0.645833333333333));
#372194=CARTESIAN_POINT('Ctrl Pts',(1.35705080756888,2.7065942666714E-16,
0.687500000000001));
#372195=CARTESIAN_POINT('Ctrl Pts',(1.01778810567666,0.587620236790417,
0.729166666666666));
#372196=CARTESIAN_POINT('Ctrl Pts',(0.678525403784439,1.17524047358083,
0.770833333333333));
#372197=CARTESIAN_POINT('Ctrl Pts',(0.,1.17524047358083,0.812500000000001));
#372198=CARTESIAN_POINT('Ctrl Pts',(-0.678525403784438,1.17524047358083,
0.854166666666666));
#372199=CARTESIAN_POINT('Ctrl Pts',(-1.01778810567666,0.587620236790418,
0.895833333333334));
#372200=CARTESIAN_POINT('Ctrl Pts',(-1.35705080756888,6.03041012221051E-16,
0.937500000000001));
#372201=CARTESIAN_POINT('Ctrl Pts',(-1.01778810567666,-0.587620236790416,
0.979166666666667));
#372202=CARTESIAN_POINT('Ctrl Pts',(-0.678525403784438,-1.17524047358083,
1.02083333333333));
#372203=CARTESIAN_POINT('Ctrl Pts',(-1.43925448419919E-16,-1.17524047358083,
1.0625));
#372204=CARTESIAN_POINT('Ctrl Pts',(-1.43925448419919E-16,-1.17524047358083,
0.5));
#372205=CARTESIAN_POINT('Ctrl Pts',(0.678525403784437,-1.17524047358083,
0.541666666666666));
#372206=CARTESIAN_POINT('Ctrl Pts',(1.01778810567666,-0.587620236790417,
0.583333333333333));
#372207=CARTESIAN_POINT('Ctrl Pts',(1.35705080756888,2.7065942666714E-16,
0.625000000000001));
#372208=CARTESIAN_POINT('Ctrl Pts',(1.01778810567666,0.587620236790417,
0.666666666666666));
#372209=CARTESIAN_POINT('Ctrl Pts',(0.678525403784439,1.17524047358083,
0.708333333333333));
#372210=CARTESIAN_POINT('Ctrl Pts',(0.,1.17524047358083,0.750000000000001));
#372211=CARTESIAN_POINT('Ctrl Pts',(-0.678525403784438,1.17524047358083,
0.791666666666666));
#372212=CARTESIAN_POINT('Ctrl Pts',(-1.01778810567666,0.587620236790418,
0.833333333333334));
#372213=CARTESIAN_POINT('Ctrl Pts',(-1.35705080756888,6.03041012221051E-16,
0.875000000000001));
#372214=CARTESIAN_POINT('Ctrl Pts',(-1.01778810567666,-0.587620236790416,
0.916666666666666));
#372215=CARTESIAN_POINT('Ctrl Pts',(-0.678525403784438,-1.17524047358083,
0.958333333333334));
#372216=CARTESIAN_POINT('Ctrl Pts',(-1.43925448419919E-16,-1.17524047358083,
1.));
#372217=CARTESIAN_POINT('Origin',(6.93889390390723E-17,9.71445146547012E-16,
-9.21875));
#372218=CARTESIAN_POINT('',(6.93889390390724E-17,-1.17524047358083,1.5625));
#372219=CARTESIAN_POINT('',(6.93889390390724E-17,-1.17524047358083,1.5));
#372220=CARTESIAN_POINT('',(2.82703326498063E-16,-1.17524047358083,-9.21875));
#372221=CARTESIAN_POINT('Ctrl Pts',(-1.43925448419919E-16,-1.17524047358083,
1.0625));
#372222=CARTESIAN_POINT('Ctrl Pts',(0.678525403784437,-1.17524047358083,
1.10416666666667));
#372223=CARTESIAN_POINT('Ctrl Pts',(1.01778810567666,-0.587620236790417,
1.14583333333333));
#372224=CARTESIAN_POINT('Ctrl Pts',(1.35705080756888,2.7065942666714E-16,
1.1875));
#372225=CARTESIAN_POINT('Ctrl Pts',(1.01778810567666,0.587620236790417,
1.22916666666667));
#372226=CARTESIAN_POINT('Ctrl Pts',(0.678525403784439,1.17524047358083,
1.27083333333333));
#372227=CARTESIAN_POINT('Ctrl Pts',(0.,1.17524047358083,1.3125));
#372228=CARTESIAN_POINT('Ctrl Pts',(-0.678525403784438,1.17524047358083,
1.35416666666667));
#372229=CARTESIAN_POINT('Ctrl Pts',(-1.01778810567666,0.587620236790418,
1.39583333333333));
#372230=CARTESIAN_POINT('Ctrl Pts',(-1.35705080756888,6.03041012221051E-16,
1.4375));
#372231=CARTESIAN_POINT('Ctrl Pts',(-1.01778810567666,-0.587620236790416,
1.47916666666667));
#372232=CARTESIAN_POINT('Ctrl Pts',(-0.678525403784438,-1.17524047358083,
1.52083333333333));
#372233=CARTESIAN_POINT('Ctrl Pts',(-1.43925448419919E-16,-1.17524047358083,
1.5625));
#372234=CARTESIAN_POINT('Ctrl Pts',(-1.43925448419919E-16,-1.17524047358083,
1.));
#372235=CARTESIAN_POINT('Ctrl Pts',(0.678525403784437,-1.17524047358083,
1.04166666666667));
#372236=CARTESIAN_POINT('Ctrl Pts',(1.01778810567666,-0.587620236790417,
1.08333333333333));
#372237=CARTESIAN_POINT('Ctrl Pts',(1.35705080756888,2.7065942666714E-16,
1.125));
#372238=CARTESIAN_POINT('Ctrl Pts',(1.01778810567666,0.587620236790417,
1.16666666666667));
#372239=CARTESIAN_POINT('Ctrl Pts',(0.678525403784439,1.17524047358083,
1.20833333333333));
#372240=CARTESIAN_POINT('Ctrl Pts',(0.,1.17524047358083,1.25));
#372241=CARTESIAN_POINT('Ctrl Pts',(-0.678525403784438,1.17524047358083,
1.29166666666667));
#372242=CARTESIAN_POINT('Ctrl Pts',(-1.01778810567666,0.587620236790418,
1.33333333333333));
#372243=CARTESIAN_POINT('Ctrl Pts',(-1.35705080756888,6.03041012221051E-16,
1.375));
#372244=CARTESIAN_POINT('Ctrl Pts',(-1.01778810567666,-0.587620236790416,
1.41666666666667));
#372245=CARTESIAN_POINT('Ctrl Pts',(-0.678525403784438,-1.17524047358083,
1.45833333333333));
#372246=CARTESIAN_POINT('Ctrl Pts',(-1.43925448419919E-16,-1.17524047358083,
1.5));
#372247=CARTESIAN_POINT('Origin',(6.93889390390723E-17,9.71445146547012E-16,
-9.21875));
#372248=CARTESIAN_POINT('',(6.93889390390724E-17,-1.17524047358083,2.0625));
#372249=CARTESIAN_POINT('',(6.93889390390724E-17,-1.17524047358083,2.));
#372250=CARTESIAN_POINT('',(2.82703326498063E-16,-1.17524047358083,-9.21875));
#372251=CARTESIAN_POINT('Ctrl Pts',(-1.43925448419919E-16,-1.17524047358083,
1.5625));
#372252=CARTESIAN_POINT('Ctrl Pts',(0.678525403784437,-1.17524047358083,
1.60416666666667));
#372253=CARTESIAN_POINT('Ctrl Pts',(1.01778810567666,-0.587620236790417,
1.64583333333333));
#372254=CARTESIAN_POINT('Ctrl Pts',(1.35705080756888,2.7065942666714E-16,
1.6875));
#372255=CARTESIAN_POINT('Ctrl Pts',(1.01778810567666,0.587620236790417,
1.72916666666667));
#372256=CARTESIAN_POINT('Ctrl Pts',(0.678525403784439,1.17524047358083,
1.77083333333333));
#372257=CARTESIAN_POINT('Ctrl Pts',(0.,1.17524047358083,1.8125));
#372258=CARTESIAN_POINT('Ctrl Pts',(-0.678525403784438,1.17524047358083,
1.85416666666667));
#372259=CARTESIAN_POINT('Ctrl Pts',(-1.01778810567666,0.587620236790418,
1.89583333333333));
#372260=CARTESIAN_POINT('Ctrl Pts',(-1.35705080756888,6.03041012221051E-16,
1.9375));
#372261=CARTESIAN_POINT('Ctrl Pts',(-1.01778810567666,-0.587620236790416,
1.97916666666667));
#372262=CARTESIAN_POINT('Ctrl Pts',(-0.678525403784438,-1.17524047358083,
2.02083333333333));
#372263=CARTESIAN_POINT('Ctrl Pts',(-1.43925448419919E-16,-1.17524047358083,
2.0625));
#372264=CARTESIAN_POINT('Ctrl Pts',(-1.43925448419919E-16,-1.17524047358083,
1.5));
#372265=CARTESIAN_POINT('Ctrl Pts',(0.678525403784437,-1.17524047358083,
1.54166666666667));
#372266=CARTESIAN_POINT('Ctrl Pts',(1.01778810567666,-0.587620236790417,
1.58333333333333));
#372267=CARTESIAN_POINT('Ctrl Pts',(1.35705080756888,2.7065942666714E-16,
1.625));
#372268=CARTESIAN_POINT('Ctrl Pts',(1.01778810567666,0.587620236790417,
1.66666666666667));
#372269=CARTESIAN_POINT('Ctrl Pts',(0.678525403784439,1.17524047358083,
1.70833333333333));
#372270=CARTESIAN_POINT('Ctrl Pts',(0.,1.17524047358083,1.75));
#372271=CARTESIAN_POINT('Ctrl Pts',(-0.678525403784438,1.17524047358083,
1.79166666666667));
#372272=CARTESIAN_POINT('Ctrl Pts',(-1.01778810567666,0.587620236790418,
1.83333333333333));
#372273=CARTESIAN_POINT('Ctrl Pts',(-1.35705080756888,6.03041012221051E-16,
1.875));
#372274=CARTESIAN_POINT('Ctrl Pts',(-1.01778810567666,-0.587620236790416,
1.91666666666667));
#372275=CARTESIAN_POINT('Ctrl Pts',(-0.678525403784438,-1.17524047358083,
1.95833333333333));
#372276=CARTESIAN_POINT('Ctrl Pts',(-1.43925448419919E-16,-1.17524047358083,
2.));
#372277=CARTESIAN_POINT('Origin',(6.93889390390723E-17,9.71445146547012E-16,
-9.21875));
#372278=CARTESIAN_POINT('',(6.93889390390724E-17,-1.17524047358083,2.5625));
#372279=CARTESIAN_POINT('',(6.93889390390724E-17,-1.17524047358083,2.5));
#372280=CARTESIAN_POINT('',(2.82703326498063E-16,-1.17524047358083,-9.21875));
#372281=CARTESIAN_POINT('Ctrl Pts',(-1.43925448419919E-16,-1.17524047358083,
2.0625));
#372282=CARTESIAN_POINT('Ctrl Pts',(0.678525403784437,-1.17524047358083,
2.10416666666667));
#372283=CARTESIAN_POINT('Ctrl Pts',(1.01778810567666,-0.587620236790417,
2.14583333333333));
#372284=CARTESIAN_POINT('Ctrl Pts',(1.35705080756888,2.7065942666714E-16,
2.1875));
#372285=CARTESIAN_POINT('Ctrl Pts',(1.01778810567666,0.587620236790417,
2.22916666666667));
#372286=CARTESIAN_POINT('Ctrl Pts',(0.678525403784439,1.17524047358083,
2.27083333333333));
#372287=CARTESIAN_POINT('Ctrl Pts',(0.,1.17524047358083,2.3125));
#372288=CARTESIAN_POINT('Ctrl Pts',(-0.678525403784438,1.17524047358083,
2.35416666666667));
#372289=CARTESIAN_POINT('Ctrl Pts',(-1.01778810567666,0.587620236790418,
2.39583333333333));
#372290=CARTESIAN_POINT('Ctrl Pts',(-1.35705080756888,6.03041012221051E-16,
2.4375));
#372291=CARTESIAN_POINT('Ctrl Pts',(-1.01778810567666,-0.587620236790416,
2.47916666666667));
#372292=CARTESIAN_POINT('Ctrl Pts',(-0.678525403784438,-1.17524047358083,
2.52083333333333));
#372293=CARTESIAN_POINT('Ctrl Pts',(-1.43925448419919E-16,-1.17524047358083,
2.5625));
#372294=CARTESIAN_POINT('Ctrl Pts',(-1.43925448419919E-16,-1.17524047358083,
2.));
#372295=CARTESIAN_POINT('Ctrl Pts',(0.678525403784437,-1.17524047358083,
2.04166666666667));
#372296=CARTESIAN_POINT('Ctrl Pts',(1.01778810567666,-0.587620236790417,
2.08333333333333));
#372297=CARTESIAN_POINT('Ctrl Pts',(1.35705080756888,2.7065942666714E-16,
2.125));
#372298=CARTESIAN_POINT('Ctrl Pts',(1.01778810567666,0.587620236790417,
2.16666666666667));
#372299=CARTESIAN_POINT('Ctrl Pts',(0.678525403784439,1.17524047358083,
2.20833333333333));
#372300=CARTESIAN_POINT('Ctrl Pts',(0.,1.17524047358083,2.25));
#372301=CARTESIAN_POINT('Ctrl Pts',(-0.678525403784438,1.17524047358083,
2.29166666666667));
#372302=CARTESIAN_POINT('Ctrl Pts',(-1.01778810567666,0.587620236790418,
2.33333333333333));
#372303=CARTESIAN_POINT('Ctrl Pts',(-1.35705080756888,6.03041012221051E-16,
2.375));
#372304=CARTESIAN_POINT('Ctrl Pts',(-1.01778810567666,-0.587620236790416,
2.41666666666667));
#372305=CARTESIAN_POINT('Ctrl Pts',(-0.678525403784438,-1.17524047358083,
2.45833333333333));
#372306=CARTESIAN_POINT('Ctrl Pts',(-1.43925448419919E-16,-1.17524047358083,
2.5));
#372307=CARTESIAN_POINT('Origin',(6.93889390390723E-17,9.71445146547012E-16,
-9.21875));
#372308=CARTESIAN_POINT('',(6.93889390390724E-17,-1.17524047358083,3.0625));
#372309=CARTESIAN_POINT('',(6.93889390390724E-17,-1.17524047358083,3.));
#372310=CARTESIAN_POINT('',(2.82703326498063E-16,-1.17524047358083,-9.21875));
#372311=CARTESIAN_POINT('Ctrl Pts',(-1.43925448419919E-16,-1.17524047358083,
2.5625));
#372312=CARTESIAN_POINT('Ctrl Pts',(0.678525403784437,-1.17524047358083,
2.60416666666667));
#372313=CARTESIAN_POINT('Ctrl Pts',(1.01778810567666,-0.587620236790417,
2.64583333333333));
#372314=CARTESIAN_POINT('Ctrl Pts',(1.35705080756888,2.7065942666714E-16,
2.6875));
#372315=CARTESIAN_POINT('Ctrl Pts',(1.01778810567666,0.587620236790417,
2.72916666666667));
#372316=CARTESIAN_POINT('Ctrl Pts',(0.678525403784439,1.17524047358083,
2.77083333333333));
#372317=CARTESIAN_POINT('Ctrl Pts',(0.,1.17524047358083,2.8125));
#372318=CARTESIAN_POINT('Ctrl Pts',(-0.678525403784438,1.17524047358083,
2.85416666666667));
#372319=CARTESIAN_POINT('Ctrl Pts',(-1.01778810567666,0.587620236790418,
2.89583333333333));
#372320=CARTESIAN_POINT('Ctrl Pts',(-1.35705080756888,6.03041012221051E-16,
2.9375));
#372321=CARTESIAN_POINT('Ctrl Pts',(-1.01778810567666,-0.587620236790416,
2.97916666666667));
#372322=CARTESIAN_POINT('Ctrl Pts',(-0.678525403784438,-1.17524047358083,
3.02083333333333));
#372323=CARTESIAN_POINT('Ctrl Pts',(-1.43925448419919E-16,-1.17524047358083,
3.0625));
#372324=CARTESIAN_POINT('Ctrl Pts',(-1.43925448419919E-16,-1.17524047358083,
2.5));
#372325=CARTESIAN_POINT('Ctrl Pts',(0.678525403784437,-1.17524047358083,
2.54166666666667));
#372326=CARTESIAN_POINT('Ctrl Pts',(1.01778810567666,-0.587620236790417,
2.58333333333333));
#372327=CARTESIAN_POINT('Ctrl Pts',(1.35705080756888,2.7065942666714E-16,
2.625));
#372328=CARTESIAN_POINT('Ctrl Pts',(1.01778810567666,0.587620236790417,
2.66666666666667));
#372329=CARTESIAN_POINT('Ctrl Pts',(0.678525403784439,1.17524047358083,
2.70833333333333));
#372330=CARTESIAN_POINT('Ctrl Pts',(0.,1.17524047358083,2.75));
#372331=CARTESIAN_POINT('Ctrl Pts',(-0.678525403784438,1.17524047358083,
2.79166666666667));
#372332=CARTESIAN_POINT('Ctrl Pts',(-1.01778810567666,0.587620236790418,
2.83333333333333));
#372333=CARTESIAN_POINT('Ctrl Pts',(-1.35705080756888,6.03041012221051E-16,
2.875));
#372334=CARTESIAN_POINT('Ctrl Pts',(-1.01778810567666,-0.587620236790416,
2.91666666666667));
#372335=CARTESIAN_POINT('Ctrl Pts',(-0.678525403784438,-1.17524047358083,
2.95833333333333));
#372336=CARTESIAN_POINT('Ctrl Pts',(-1.43925448419919E-16,-1.17524047358083,
3.));
#372337=CARTESIAN_POINT('Origin',(6.93889390390723E-17,9.71445146547012E-16,
-9.21875));
#372338=CARTESIAN_POINT('',(6.93889390390724E-17,-1.17524047358083,3.5625));
#372339=CARTESIAN_POINT('',(6.93889390390724E-17,-1.17524047358083,3.5));
#372340=CARTESIAN_POINT('',(2.82703326498063E-16,-1.17524047358083,-9.21875));
#372341=CARTESIAN_POINT('Ctrl Pts',(-1.43925448419919E-16,-1.17524047358083,
3.0625));
#372342=CARTESIAN_POINT('Ctrl Pts',(0.678525403784437,-1.17524047358083,
3.10416666666667));
#372343=CARTESIAN_POINT('Ctrl Pts',(1.01778810567666,-0.587620236790417,
3.14583333333333));
#372344=CARTESIAN_POINT('Ctrl Pts',(1.35705080756888,2.7065942666714E-16,
3.1875));
#372345=CARTESIAN_POINT('Ctrl Pts',(1.01778810567666,0.587620236790417,
3.22916666666667));
#372346=CARTESIAN_POINT('Ctrl Pts',(0.678525403784439,1.17524047358083,
3.27083333333333));
#372347=CARTESIAN_POINT('Ctrl Pts',(0.,1.17524047358083,3.3125));
#372348=CARTESIAN_POINT('Ctrl Pts',(-0.678525403784438,1.17524047358083,
3.35416666666667));
#372349=CARTESIAN_POINT('Ctrl Pts',(-1.01778810567666,0.587620236790418,
3.39583333333333));
#372350=CARTESIAN_POINT('Ctrl Pts',(-1.35705080756888,6.03041012221051E-16,
3.4375));
#372351=CARTESIAN_POINT('Ctrl Pts',(-1.01778810567666,-0.587620236790416,
3.47916666666667));
#372352=CARTESIAN_POINT('Ctrl Pts',(-0.678525403784438,-1.17524047358083,
3.52083333333333));
#372353=CARTESIAN_POINT('Ctrl Pts',(-1.43925448419919E-16,-1.17524047358083,
3.5625));
#372354=CARTESIAN_POINT('Ctrl Pts',(-1.43925448419919E-16,-1.17524047358083,
3.));
#372355=CARTESIAN_POINT('Ctrl Pts',(0.678525403784437,-1.17524047358083,
3.04166666666667));
#372356=CARTESIAN_POINT('Ctrl Pts',(1.01778810567666,-0.587620236790417,
3.08333333333333));
#372357=CARTESIAN_POINT('Ctrl Pts',(1.35705080756888,2.7065942666714E-16,
3.125));
#372358=CARTESIAN_POINT('Ctrl Pts',(1.01778810567666,0.587620236790417,
3.16666666666667));
#372359=CARTESIAN_POINT('Ctrl Pts',(0.678525403784439,1.17524047358083,
3.20833333333333));
#372360=CARTESIAN_POINT('Ctrl Pts',(0.,1.17524047358083,3.25));
#372361=CARTESIAN_POINT('Ctrl Pts',(-0.678525403784438,1.17524047358083,
3.29166666666667));
#372362=CARTESIAN_POINT('Ctrl Pts',(-1.01778810567666,0.587620236790418,
3.33333333333333));
#372363=CARTESIAN_POINT('Ctrl Pts',(-1.35705080756888,6.03041012221051E-16,
3.375));
#372364=CARTESIAN_POINT('Ctrl Pts',(-1.01778810567666,-0.587620236790416,
3.41666666666667));
#372365=CARTESIAN_POINT('Ctrl Pts',(-0.678525403784438,-1.17524047358083,
3.45833333333333));
#372366=CARTESIAN_POINT('Ctrl Pts',(-1.43925448419919E-16,-1.17524047358083,
3.5));
#372367=CARTESIAN_POINT('Origin',(6.93889390390723E-17,9.71445146547012E-16,
-9.21875));
#372368=CARTESIAN_POINT('',(6.93889390390724E-17,-1.17524047358083,4.0625));
#372369=CARTESIAN_POINT('',(6.93889390390724E-17,-1.17524047358083,4.));
#372370=CARTESIAN_POINT('',(2.82703326498063E-16,-1.17524047358083,-9.21875));
#372371=CARTESIAN_POINT('Ctrl Pts',(-1.43925448419919E-16,-1.17524047358083,
3.5625));
#372372=CARTESIAN_POINT('Ctrl Pts',(0.678525403784437,-1.17524047358083,
3.60416666666667));
#372373=CARTESIAN_POINT('Ctrl Pts',(1.01778810567666,-0.587620236790417,
3.64583333333333));
#372374=CARTESIAN_POINT('Ctrl Pts',(1.35705080756888,2.7065942666714E-16,
3.6875));
#372375=CARTESIAN_POINT('Ctrl Pts',(1.01778810567666,0.587620236790417,
3.72916666666667));
#372376=CARTESIAN_POINT('Ctrl Pts',(0.678525403784439,1.17524047358083,
3.77083333333333));
#372377=CARTESIAN_POINT('Ctrl Pts',(0.,1.17524047358083,3.8125));
#372378=CARTESIAN_POINT('Ctrl Pts',(-0.678525403784438,1.17524047358083,
3.85416666666667));
#372379=CARTESIAN_POINT('Ctrl Pts',(-1.01778810567666,0.587620236790418,
3.89583333333333));
#372380=CARTESIAN_POINT('Ctrl Pts',(-1.35705080756888,6.03041012221051E-16,
3.9375));
#372381=CARTESIAN_POINT('Ctrl Pts',(-1.01778810567666,-0.587620236790416,
3.97916666666667));
#372382=CARTESIAN_POINT('Ctrl Pts',(-0.678525403784438,-1.17524047358083,
4.02083333333333));
#372383=CARTESIAN_POINT('Ctrl Pts',(-1.43925448419919E-16,-1.17524047358083,
4.0625));
#372384=CARTESIAN_POINT('Ctrl Pts',(-1.43925448419919E-16,-1.17524047358083,
3.5));
#372385=CARTESIAN_POINT('Ctrl Pts',(0.678525403784437,-1.17524047358083,
3.54166666666667));
#372386=CARTESIAN_POINT('Ctrl Pts',(1.01778810567666,-0.587620236790417,
3.58333333333333));
#372387=CARTESIAN_POINT('Ctrl Pts',(1.35705080756888,2.7065942666714E-16,
3.625));
#372388=CARTESIAN_POINT('Ctrl Pts',(1.01778810567666,0.587620236790417,
3.66666666666667));
#372389=CARTESIAN_POINT('Ctrl Pts',(0.678525403784439,1.17524047358083,
3.70833333333333));
#372390=CARTESIAN_POINT('Ctrl Pts',(0.,1.17524047358083,3.75));
#372391=CARTESIAN_POINT('Ctrl Pts',(-0.678525403784438,1.17524047358083,
3.79166666666667));
#372392=CARTESIAN_POINT('Ctrl Pts',(-1.01778810567666,0.587620236790418,
3.83333333333333));
#372393=CARTESIAN_POINT('Ctrl Pts',(-1.35705080756888,6.03041012221051E-16,
3.875));
#372394=CARTESIAN_POINT('Ctrl Pts',(-1.01778810567666,-0.587620236790416,
3.91666666666667));
#372395=CARTESIAN_POINT('Ctrl Pts',(-0.678525403784438,-1.17524047358083,
3.95833333333333));
#372396=CARTESIAN_POINT('Ctrl Pts',(-1.43925448419919E-16,-1.17524047358083,
4.));
#372397=CARTESIAN_POINT('Origin',(6.93889390390723E-17,9.71445146547012E-16,
-9.21875));
#372398=CARTESIAN_POINT('',(6.93889390390724E-17,-1.17524047358083,4.5625));
#372399=CARTESIAN_POINT('',(6.93889390390724E-17,-1.17524047358083,4.5));
#372400=CARTESIAN_POINT('',(2.82703326498063E-16,-1.17524047358083,-9.21875));
#372401=CARTESIAN_POINT('Ctrl Pts',(-1.43925448419919E-16,-1.17524047358083,
4.0625));
#372402=CARTESIAN_POINT('Ctrl Pts',(0.678525403784437,-1.17524047358083,
4.10416666666667));
#372403=CARTESIAN_POINT('Ctrl Pts',(1.01778810567666,-0.587620236790417,
4.14583333333333));
#372404=CARTESIAN_POINT('Ctrl Pts',(1.35705080756888,2.7065942666714E-16,
4.1875));
#372405=CARTESIAN_POINT('Ctrl Pts',(1.01778810567666,0.587620236790417,
4.22916666666667));
#372406=CARTESIAN_POINT('Ctrl Pts',(0.678525403784439,1.17524047358083,
4.27083333333333));
#372407=CARTESIAN_POINT('Ctrl Pts',(0.,1.17524047358083,4.3125));
#372408=CARTESIAN_POINT('Ctrl Pts',(-0.678525403784438,1.17524047358083,
4.35416666666667));
#372409=CARTESIAN_POINT('Ctrl Pts',(-1.01778810567666,0.587620236790418,
4.39583333333333));
#372410=CARTESIAN_POINT('Ctrl Pts',(-1.35705080756888,6.03041012221051E-16,
4.4375));
#372411=CARTESIAN_POINT('Ctrl Pts',(-1.01778810567666,-0.587620236790416,
4.47916666666667));
#372412=CARTESIAN_POINT('Ctrl Pts',(-0.678525403784438,-1.17524047358083,
4.52083333333333));
#372413=CARTESIAN_POINT('Ctrl Pts',(-1.43925448419919E-16,-1.17524047358083,
4.5625));
#372414=CARTESIAN_POINT('Ctrl Pts',(-1.43925448419919E-16,-1.17524047358083,
4.));
#372415=CARTESIAN_POINT('Ctrl Pts',(0.678525403784437,-1.17524047358083,
4.04166666666667));
#372416=CARTESIAN_POINT('Ctrl Pts',(1.01778810567666,-0.587620236790417,
4.08333333333333));
#372417=CARTESIAN_POINT('Ctrl Pts',(1.35705080756888,2.7065942666714E-16,
4.125));
#372418=CARTESIAN_POINT('Ctrl Pts',(1.01778810567666,0.587620236790417,
4.16666666666667));
#372419=CARTESIAN_POINT('Ctrl Pts',(0.678525403784439,1.17524047358083,
4.20833333333333));
#372420=CARTESIAN_POINT('Ctrl Pts',(0.,1.17524047358083,4.25));
#372421=CARTESIAN_POINT('Ctrl Pts',(-0.678525403784438,1.17524047358083,
4.29166666666667));
#372422=CARTESIAN_POINT('Ctrl Pts',(-1.01778810567666,0.587620236790418,
4.33333333333333));
#372423=CARTESIAN_POINT('Ctrl Pts',(-1.35705080756888,6.03041012221051E-16,
4.375));
#372424=CARTESIAN_POINT('Ctrl Pts',(-1.01778810567666,-0.587620236790416,
4.41666666666667));
#372425=CARTESIAN_POINT('Ctrl Pts',(-0.678525403784438,-1.17524047358083,
4.45833333333333));
#372426=CARTESIAN_POINT('Ctrl Pts',(-1.43925448419919E-16,-1.17524047358083,
4.5));
#372427=CARTESIAN_POINT('Origin',(6.93889390390723E-17,9.71445146547012E-16,
-9.21875));
#372428=CARTESIAN_POINT('',(6.93889390390724E-17,-1.17524047358083,5.0625));
#372429=CARTESIAN_POINT('',(6.93889390390724E-17,-1.17524047358083,5.));
#372430=CARTESIAN_POINT('',(2.82703326498063E-16,-1.17524047358083,-9.21875));
#372431=CARTESIAN_POINT('Ctrl Pts',(-1.43925448419919E-16,-1.17524047358083,
4.5625));
#372432=CARTESIAN_POINT('Ctrl Pts',(0.678525403784437,-1.17524047358083,
4.60416666666667));
#372433=CARTESIAN_POINT('Ctrl Pts',(1.01778810567666,-0.587620236790417,
4.64583333333333));
#372434=CARTESIAN_POINT('Ctrl Pts',(1.35705080756888,2.7065942666714E-16,
4.6875));
#372435=CARTESIAN_POINT('Ctrl Pts',(1.01778810567666,0.587620236790417,
4.72916666666667));
#372436=CARTESIAN_POINT('Ctrl Pts',(0.678525403784439,1.17524047358083,
4.77083333333333));
#372437=CARTESIAN_POINT('Ctrl Pts',(0.,1.17524047358083,4.8125));
#372438=CARTESIAN_POINT('Ctrl Pts',(-0.678525403784438,1.17524047358083,
4.85416666666667));
#372439=CARTESIAN_POINT('Ctrl Pts',(-1.01778810567666,0.587620236790418,
4.89583333333333));
#372440=CARTESIAN_POINT('Ctrl Pts',(-1.35705080756888,6.03041012221051E-16,
4.9375));
#372441=CARTESIAN_POINT('Ctrl Pts',(-1.01778810567666,-0.587620236790416,
4.97916666666667));
#372442=CARTESIAN_POINT('Ctrl Pts',(-0.678525403784438,-1.17524047358083,
5.02083333333334));
#372443=CARTESIAN_POINT('Ctrl Pts',(-1.43925448419919E-16,-1.17524047358083,
5.0625));
#372444=CARTESIAN_POINT('Ctrl Pts',(-1.43925448419919E-16,-1.17524047358083,
4.5));
#372445=CARTESIAN_POINT('Ctrl Pts',(0.678525403784437,-1.17524047358083,
4.54166666666667));
#372446=CARTESIAN_POINT('Ctrl Pts',(1.01778810567666,-0.587620236790417,
4.58333333333333));
#372447=CARTESIAN_POINT('Ctrl Pts',(1.35705080756888,2.7065942666714E-16,
4.625));
#372448=CARTESIAN_POINT('Ctrl Pts',(1.01778810567666,0.587620236790417,
4.66666666666667));
#372449=CARTESIAN_POINT('Ctrl Pts',(0.678525403784439,1.17524047358083,
4.70833333333333));
#372450=CARTESIAN_POINT('Ctrl Pts',(0.,1.17524047358083,4.75));
#372451=CARTESIAN_POINT('Ctrl Pts',(-0.678525403784438,1.17524047358083,
4.79166666666667));
#372452=CARTESIAN_POINT('Ctrl Pts',(-1.01778810567666,0.587620236790418,
4.83333333333333));
#372453=CARTESIAN_POINT('Ctrl Pts',(-1.35705080756888,6.03041012221051E-16,
4.875));
#372454=CARTESIAN_POINT('Ctrl Pts',(-1.01778810567666,-0.587620236790416,
4.91666666666667));
#372455=CARTESIAN_POINT('Ctrl Pts',(-0.678525403784438,-1.17524047358083,
4.95833333333333));
#372456=CARTESIAN_POINT('Ctrl Pts',(-1.43925448419919E-16,-1.17524047358083,
5.));
#372457=CARTESIAN_POINT('Origin',(0.,2.04523456705693E-15,3.99999999999998));
#372458=CARTESIAN_POINT('',(-1.02859918696353E-15,-1.5,5.25));
#372459=CARTESIAN_POINT('',(-3.11727555887454E-14,-1.5,5.3125));
#372460=CARTESIAN_POINT('',(-1.83697019872103E-16,-1.5,3.99999999999998));
#372461=CARTESIAN_POINT('',(0.,1.5,5.5));
#372462=CARTESIAN_POINT('Ctrl Pts',(2.34187669256869E-15,-1.5,5.25));
#372463=CARTESIAN_POINT('Ctrl Pts',(0.1013142184298,-1.5,5.25487448260693));
#372464=CARTESIAN_POINT('Ctrl Pts',(0.202585377762413,-1.48973761941226,
5.26003195965966));
#372465=CARTESIAN_POINT('Ctrl Pts',(0.497494643078012,-1.42906343675683,
5.27590618226536));
#372466=CARTESIAN_POINT('Ctrl Pts',(0.682749667466072,-1.35039445539259,
5.28700451826429));
#372467=CARTESIAN_POINT('Ctrl Pts',(1.00543736318142,-1.12954128016014,
5.3086646476862));
#372468=CARTESIAN_POINT('Ctrl Pts',(1.14147220648853,-0.991881889660697,
5.31903349909473));
#372469=CARTESIAN_POINT('Ctrl Pts',(1.35790964618256,-0.667374587809761,
5.33846094198532));
#372470=CARTESIAN_POINT('Ctrl Pts',(1.43414603945203,-0.482241430142021,
5.34820880943671));
#372471=CARTESIAN_POINT('Ctrl Pts',(1.50990524563617,-0.0944424733214634,
5.36975319592674));
#372472=CARTESIAN_POINT('Ctrl Pts',(1.50925882253586,0.104265632731634,
5.38079253515191));
#372473=CARTESIAN_POINT('Ctrl Pts',(1.43263199824449,0.483378097020384,
5.40185433872351));
#372474=CARTESIAN_POINT('Ctrl Pts',(1.35997826725094,0.660697896700975,
5.41125406779552));
#372475=CARTESIAN_POINT('Ctrl Pts',(1.14752287537316,0.986274573606487,
5.43051962918385));
#372476=CARTESIAN_POINT('Ctrl Pts',(1.00682301552788,1.12952668237106,5.44126827959036));
#372477=CARTESIAN_POINT('Ctrl Pts',(0.716631896201004,1.32646655903961,
5.46070065845836));
#372478=CARTESIAN_POINT('Ctrl Pts',(0.578704042072479,1.39218522049725,
5.46916223380784));
#372479=CARTESIAN_POINT('Ctrl Pts',(0.292687271883244,1.4784772415699,5.48532022266499));
#372480=CARTESIAN_POINT('Ctrl Pts',(0.146711014173142,1.50000000000011,
5.49294136303951));
#372481=CARTESIAN_POINT('Ctrl Pts',(-1.07483466571523E-12,1.5,5.50000000000005));
#372482=CARTESIAN_POINT('',(-1.83697019872103E-16,-1.5,5.5));
#372483=CARTESIAN_POINT('Origin',(0.,1.86551418677864E-15,5.5));
#372484=CARTESIAN_POINT('',(-1.83697019872103E-16,-1.5,5.875));
#372485=CARTESIAN_POINT('',(-1.83697019872103E-16,-1.5,3.99999999999998));
#372486=CARTESIAN_POINT('Origin',(0.,1.82058409170907E-15,5.875));
#372487=CARTESIAN_POINT('',(1.05094390383306,1.07028823734363,5.5));
#372488=CARTESIAN_POINT('Origin',(0.,1.86551418677864E-15,5.5));
#372489=CARTESIAN_POINT('Ctrl Pts',(1.05094390383211,1.07028823734456,5.50000000000007));
#372490=CARTESIAN_POINT('Ctrl Pts',(1.15240189416463,0.970663993412324,
5.49235126005502));
#372491=CARTESIAN_POINT('Ctrl Pts',(1.23913482730881,0.857166793728004,
5.48512037742933));
#372492=CARTESIAN_POINT('Ctrl Pts',(1.37842494689544,0.608569005404991,
5.47130938918917));
#372493=CARTESIAN_POINT('Ctrl Pts',(1.43008604020435,0.474609193904058,
5.46386717743895));
#372494=CARTESIAN_POINT('Ctrl Pts',(1.50591325346079,0.144072283175914,
5.44550401573184));
#372495=CARTESIAN_POINT('Ctrl Pts',(1.51182377709547,-0.0540169751539241,
5.43449905693574));
#372496=CARTESIAN_POINT('Ctrl Pts',(1.44639389913366,-0.444944484987569,
5.41278086194498));
#372497=CARTESIAN_POINT('Ctrl Pts',(1.37422890585589,-0.633632259374769,
5.4026833896331));
#372498=CARTESIAN_POINT('Ctrl Pts',(1.16483810558126,-0.964245461497677,
5.38342536999877));
#372499=CARTESIAN_POINT('Ctrl Pts',(1.03247383541499,-1.1048043760253,5.3731525767887));
#372500=CARTESIAN_POINT('Ctrl Pts',(0.716072516089344,-1.33294901920865,
5.35159236001545));
#372501=CARTESIAN_POINT('Ctrl Pts',(0.533315805628695,-1.41601407028835,
5.34049211115374));
#372502=CARTESIAN_POINT('Ctrl Pts',(0.228050315786412,-1.48698613535804,
5.32383357217391));
#372503=CARTESIAN_POINT('Ctrl Pts',(0.11409269091585,-1.5,5.31798928715107));
#372504=CARTESIAN_POINT('Ctrl Pts',(-6.63705201908726E-14,-1.5,5.3125));
#372505=CARTESIAN_POINT('Origin',(0.,2.04523456705693E-15,3.99999999999998));
#372506=CARTESIAN_POINT('',(-9.30610584359856E-14,-1.5,4.74999999999999));
#372507=CARTESIAN_POINT('',(-1.24089882572763E-13,-1.5,4.81249999999999));
#372508=CARTESIAN_POINT('',(-1.83697019872103E-16,-1.5,3.99999999999998));
#372509=CARTESIAN_POINT('Ctrl Pts',(-1.86101134502792E-13,-1.5,4.74999999999999));
#372510=CARTESIAN_POINT('Ctrl Pts',(0.132337359508786,-1.50000000000001,
4.75636708417802));
#372511=CARTESIAN_POINT('Ctrl Pts',(0.264341985951988,-1.48249172459084,
4.76320450071267));
#372512=CARTESIAN_POINT('Ctrl Pts',(0.583774760997631,-1.39586701723942,
4.78097945913859));
#372513=CARTESIAN_POINT('Ctrl Pts',(0.762797992040203,-1.306664258553,4.79207057276601));
#372514=CARTESIAN_POINT('Ctrl Pts',(1.06996317836528,-1.0684234189941,4.81346686578241));
#372515=CARTESIAN_POINT('Ctrl Pts',(1.19699132836069,-0.923897060647313,
4.8235931315638));
#372516=CARTESIAN_POINT('Ctrl Pts',(1.39415333877414,-0.588066282504838,
4.84240772593883));
#372517=CARTESIAN_POINT('Ctrl Pts',(1.45974822466939,-0.398344079750572,
4.85286977334732));
#372518=CARTESIAN_POINT('Ctrl Pts',(1.51269341320913,-0.00736604210121602,
4.87459077543895));
#372519=CARTESIAN_POINT('Ctrl Pts',(1.50075352346208,0.189841157089107,
4.88554673094952));
#372520=CARTESIAN_POINT('Ctrl Pts',(1.40321020875678,0.563169765903798,
4.906287209217));
#372521=CARTESIAN_POINT('Ctrl Pts',(1.32061199135457,0.736297374579946,
4.91524806412427));
#372522=CARTESIAN_POINT('Ctrl Pts',(1.08993684967038,1.04957253614588,4.93504851487444));
#372523=CARTESIAN_POINT('Ctrl Pts',(0.941322354847056,1.18467648763986,
4.94595162063192));
#372524=CARTESIAN_POINT('Ctrl Pts',(0.60474475673763,1.38625828944633,4.96774471236585));
#372525=CARTESIAN_POINT('Ctrl Pts',(0.421081105146126,1.45262981129201,
4.97842488730767));
#372526=CARTESIAN_POINT('Ctrl Pts',(0.0389123015268975,1.51189479414534,
4.9984582419685));
#372527=CARTESIAN_POINT('Ctrl Pts',(-0.155939684676095,1.50433577026112,
5.00738221351442));
#372528=CARTESIAN_POINT('Ctrl Pts',(-0.537476109603411,1.41443190762156,
5.0282362228353));
#372529=CARTESIAN_POINT('Ctrl Pts',(-0.719934574271997,1.33085837095527,
5.03933624693928));
#372530=CARTESIAN_POINT('Ctrl Pts',(-1.03559141172507,1.10187350663975,
5.06088398428763));
#372531=CARTESIAN_POINT('Ctrl Pts',(-1.16752312838274,0.960982260328454,
5.07114519769574));
#372532=CARTESIAN_POINT('Ctrl Pts',(-1.37608593538413,0.629656626788052,
5.09038317024674));
#372533=CARTESIAN_POINT('Ctrl Pts',(-1.44776902614139,0.440547850918076,
5.10052511939358));
#372534=CARTESIAN_POINT('Ctrl Pts',(-1.51197833241709,0.0492603879786804,
5.12226331177909));
#372535=CARTESIAN_POINT('Ctrl Pts',(-1.50545082908663,-0.148747153270871,
5.1332637307374));
#372536=CARTESIAN_POINT('Ctrl Pts',(-1.41794504592827,-0.524896618648321,
5.15416092325837));
#372537=CARTESIAN_POINT('Ctrl Pts',(-1.34016456864257,-0.700019794165874,
5.16329962974384));
#372538=CARTESIAN_POINT('Ctrl Pts',(-1.11829112315409,-1.01930451755138,
5.18284354096112));
#372539=CARTESIAN_POINT('Ctrl Pts',(-0.9734531234724,-1.15841480273464,
5.1936762370583));
#372540=CARTESIAN_POINT('Ctrl Pts',(-0.642123617261976,-1.36941735503731,
5.21547851736679));
#372541=CARTESIAN_POINT('Ctrl Pts',(-0.459826381711669,-1.44090204461358,
5.22623498302315));
#372542=CARTESIAN_POINT('Ctrl Pts',(-0.18001487423605,-1.4919012135564,
5.24111406403517));
#372543=CARTESIAN_POINT('Ctrl Pts',(-0.0900013938564301,-1.5,5.24566980591913));
#372544=CARTESIAN_POINT('Ctrl Pts',(-2.74887016421606E-16,-1.5,5.25));
#372545=CARTESIAN_POINT('Ctrl Pts',(-6.21618141576187E-14,-1.5,5.3125));
#372546=CARTESIAN_POINT('Ctrl Pts',(-0.0781666029860376,-1.49999999999999,
5.30873920756036));
#372547=CARTESIAN_POINT('Ctrl Pts',(-0.156380097833171,-1.49389088525685,
5.3048064614031));
#372548=CARTESIAN_POINT('Ctrl Pts',(-0.425120326327988,-1.45145985509196,
5.29069805140434));
#372549=CARTESIAN_POINT('Ctrl Pts',(-0.608648585849205,-1.38455614161338,
5.28000960741563));
#372550=CARTESIAN_POINT('Ctrl Pts',(-0.944693493081018,-1.18198957786974,
5.25821479028525));
#372551=CARTESIAN_POINT('Ctrl Pts',(-1.09292093000477,-1.04646448570185,
5.24731860850759));
#372552=CARTESIAN_POINT('Ctrl Pts',(-1.32268404489021,-0.732560575680372,
5.22754457243236));
#372553=CARTESIAN_POINT('Ctrl Pts',(-1.4047815617659,-0.55922860385983,
5.21856825576985));
#372554=CARTESIAN_POINT('Ctrl Pts',(-1.50129034805554,-0.185605472482953,
5.19781141513781));
#372555=CARTESIAN_POINT('Ctrl Pts',(-1.51267328803592,0.0116910409612078,
5.18685049772425));
#372556=CARTESIAN_POINT('Ctrl Pts',(-1.4585882153116,0.402573071914142,
5.16513482933798));
#372557=CARTESIAN_POINT('Ctrl Pts',(-1.39244195273024,0.592110506921991,
5.15471304727201));
#372558=CARTESIAN_POINT('Ctrl Pts',(-1.19427093735495,0.927422166609085,
5.13586432708022));
#372559=CARTESIAN_POINT('Ctrl Pts',(-1.06677763582743,1.07161391255723,
5.12572497647415));
#372560=CARTESIAN_POINT('Ctrl Pts',(-0.758802919877356,1.3089975002654,
5.10431354749692));
#372561=CARTESIAN_POINT('Ctrl Pts',(-0.579449637439399,1.39767670128007,
5.093221097533));
#372562=CARTESIAN_POINT('Ctrl Pts',(-0.200110007463219,1.49926990007539,
5.07214807777638));
#372563=CARTESIAN_POINT('Ctrl Pts',(-0.00420925884862429,1.51255730384018,
5.06305133205621));
#372564=CARTESIAN_POINT('Ctrl Pts',(0.380226113100054,1.46378504761527,
5.04320039170437));
#372565=CARTESIAN_POINT('Ctrl Pts',(0.565168529376356,1.40278531907301,
5.03260790864861));
#372566=CARTESIAN_POINT('Ctrl Pts',(0.908448348456497,1.21035688739411,
5.01074661643921));
#372567=CARTESIAN_POINT('Ctrl Pts',(1.0620114849816,1.07814223110912,4.99968567724709));
#372568=CARTESIAN_POINT('Ctrl Pts',(1.30181427141735,0.769134375830037,
4.97956460876981));
#372569=CARTESIAN_POINT('Ctrl Pts',(1.38886175096562,0.597792825375605,
4.97071071252075));
#372570=CARTESIAN_POINT('Ctrl Pts',(1.49550756795418,0.227092567281358,
4.95011625373774));
#372571=CARTESIAN_POINT('Ctrl Pts',(1.51233653549556,0.0307386628157603,
4.93920770348966));
#372572=CARTESIAN_POINT('Ctrl Pts',(1.46944397407567,-0.360886484990905,
4.91745075083374));
#372573=CARTESIAN_POINT('Ctrl Pts',(1.4087453892702,-0.552238149629713,
4.90682010279825));
#372574=CARTESIAN_POINT('Ctrl Pts',(1.2204081434847,-0.892623842777975,
4.88790978651224));
#372575=CARTESIAN_POINT('Ctrl Pts',(1.09748369894562,-1.04007136398357,
4.87807850452959));
#372576=CARTESIAN_POINT('Ctrl Pts',(0.797378551679508,-1.28577242495924,
4.8568146594281));
#372577=CARTESIAN_POINT('Ctrl Pts',(0.621299834175413,-1.37949731331861,
4.84573959906122));
#372578=CARTESIAN_POINT('Ctrl Pts',(0.291688127647154,-1.47865655639298,
4.82712672501815));
#372579=CARTESIAN_POINT('Ctrl Pts',(0.146113885494368,-1.50000000000002,
4.81952990759354));
#372580=CARTESIAN_POINT('Ctrl Pts',(-2.4983487501018E-13,-1.5,4.81249999999999));
#372581=CARTESIAN_POINT('Origin',(0.,2.04523456705693E-15,3.99999999999998));
#372582=CARTESIAN_POINT('',(-9.30610584359856E-14,-1.5,4.24999999999999));
#372583=CARTESIAN_POINT('',(-3.11727555887454E-14,-1.5,4.3125));
#372584=CARTESIAN_POINT('',(-1.83697019872103E-16,-1.5,3.99999999999998));
#372585=CARTESIAN_POINT('Ctrl Pts',(-1.85858273216155E-13,-1.5,4.24999999999999));
#372586=CARTESIAN_POINT('Ctrl Pts',(0.163534910421258,-1.50000000000002,
4.25786807704614));
#372587=CARTESIAN_POINT('Ctrl Pts',(0.326190684501579,-1.47326229929913,
4.26643657053385));
#372588=CARTESIAN_POINT('Ctrl Pts',(0.667990021365253,-1.35740629940923,
4.28609962101527));
#372589=CARTESIAN_POINT('Ctrl Pts',(0.840196725402017,-1.25810649223897,
4.2971432479032));
#372590=CARTESIAN_POINT('Ctrl Pts',(1.13122312734384,-1.00320978004929,
4.31822572642256));
#372591=CARTESIAN_POINT('Ctrl Pts',(1.2490305329715,-0.852050769110481,
4.32766384616067));
#372592=CARTESIAN_POINT('Ctrl Pts',(1.42604267402587,-0.505912163077925,
4.34689376871803));
#372593=CARTESIAN_POINT('Ctrl Pts',(1.48046532813874,-0.312640018756726,
4.35763111006921));
#372594=CARTESIAN_POINT('Ctrl Pts',(1.51047312143187,0.0796059131719647,
4.37942255073191));
#372595=CARTESIAN_POINT('Ctrl Pts',(1.4874208354067,0.274691213374741,4.3902606229654));
#372596=CARTESIAN_POINT('Ctrl Pts',(1.36911846990398,0.641930210830453,
4.41066278949071));
#372597=CARTESIAN_POINT('Ctrl Pts',(1.27625099543952,0.811012624525723,
4.41945780714498));
#372598=CARTESIAN_POINT('Ctrl Pts',(1.02638328536396,1.11199346834159,4.43984015194602));
#372599=CARTESIAN_POINT('Ctrl Pts',(0.869168052732768,1.23875949404383,
4.45092545184444));
#372600=CARTESIAN_POINT('Ctrl Pts',(0.521083697970173,1.41967196683104,
4.47269801463766));
#372601=CARTESIAN_POINT('Ctrl Pts',(0.334912309122096,1.47473694490812,
4.48318477248426));
#372602=CARTESIAN_POINT('Ctrl Pts',(-0.0519432957329438,1.51189047531382,
4.50282941396224));
#372603=CARTESIAN_POINT('Ctrl Pts',(-0.249069874090919,1.49214228260642,
4.51220164983219));
#372604=CARTESIAN_POINT('Ctrl Pts',(-0.625765335375153,1.37746828716819,
4.5335108074256));
#372605=CARTESIAN_POINT('Ctrl Pts',(-0.80148385209002,1.2832077073044,4.54458341794351));
#372606=CARTESIAN_POINT('Ctrl Pts',(-1.1007294145725,1.03662777910022,4.56583031923137));
#372607=CARTESIAN_POINT('Ctrl Pts',(-1.22316683171971,0.888831648925115,
4.57562046394874));
#372608=CARTESIAN_POINT('Ctrl Pts',(-1.41043936006761,0.547898537307782,
4.59456119237192));
#372609=CARTESIAN_POINT('Ctrl Pts',(-1.47054956730788,0.356356974518528,
4.60520239030466));
#372610=CARTESIAN_POINT('Ctrl Pts',(-1.51222837316115,-0.0353448297905851,
4.62696360165516));
#372611=CARTESIAN_POINT('Ctrl Pts',(-1.49481056950729,-0.231587514103256,
4.63786597300586));
#372612=CARTESIAN_POINT('Ctrl Pts',(-1.38706553932082,-0.601965922302877,
4.65844255123917));
#372613=CARTESIAN_POINT('Ctrl Pts',(-1.29947526964824,-0.773093177466047,
4.66728711075724));
#372614=CARTESIAN_POINT('Ctrl Pts',(-1.05872747359096,-1.08135566705396,
4.68743294142861));
#372615=CARTESIAN_POINT('Ctrl Pts',(-0.904815168934766,-1.21306506743986,
4.69849664509418));
#372616=CARTESIAN_POINT('Ctrl Pts',(-0.561070447600619,-1.40442192262524,
4.72035053891));
#372617=CARTESIAN_POINT('Ctrl Pts',(-0.376005221910598,-1.46486781226288,
4.73093354622241));
#372618=CARTESIAN_POINT('Ctrl Pts',(-0.123202739728906,-1.49620944194601,
4.74396711214189));
#372619=CARTESIAN_POINT('Ctrl Pts',(-0.0615704629692202,-1.49999999999999,
4.74703768971922));
#372620=CARTESIAN_POINT('Ctrl Pts',(-1.85938419852099E-13,-1.5,4.74999999999999));
#372621=CARTESIAN_POINT('Ctrl Pts',(-2.47996068125655E-13,-1.5,4.81249999999999));
#372622=CARTESIAN_POINT('Ctrl Pts',(-0.0492637934033634,-1.49999999999999,
4.81012979463477));
#372623=CARTESIAN_POINT('Ctrl Pts',(-0.0985824301404427,-1.49757322656534,
4.80768954024514));
#372624=CARTESIAN_POINT('Ctrl Pts',(-0.339292525452773,-1.47374263063355,
4.7954464093866));
#372625=CARTESIAN_POINT('Ctrl Pts',(-0.525353669177403,-1.41810503365377,
4.78494904963034));
#372626=CARTESIAN_POINT('Ctrl Pts',(-0.872991424837885,-1.23607824286241,
4.76316702056855));
#372627=CARTESIAN_POINT('Ctrl Pts',(-1.02986284823744,-1.10878319847344,
4.75208356723598));
#372628=CARTESIAN_POINT('Ctrl Pts',(-1.27876514977376,-0.807023777370858,
4.73172604352809));
#372629=CARTESIAN_POINT('Ctrl Pts',(-1.37107046921521,-0.637726763123372,
4.72292926461787));
#372630=CARTESIAN_POINT('Ctrl Pts',(-1.48825946539048,-0.270152588186515,
4.70250847712138));
#372631=CARTESIAN_POINT('Ctrl Pts',(-1.51071949717048,-0.0749376417989757,
4.69166320232207));
#372632=CARTESIAN_POINT('Ctrl Pts',(-1.47948007658163,0.317267354827136,
4.66987403584285));
#372633=CARTESIAN_POINT('Ctrl Pts',(-1.42445466752569,0.510365031604566,
4.65914638713299));
#372634=CARTESIAN_POINT('Ctrl Pts',(-1.24635752091359,0.85595920847827,
4.63994671064001));
#372635=CARTESIAN_POINT('Ctrl Pts',(-1.12806576335496,1.00676220302361,
4.63047513926063));
#372636=CARTESIAN_POINT('Ctrl Pts',(-0.836175776888841,1.26079227363434,
4.60937518488867));
#372637=CARTESIAN_POINT('Ctrl Pts',(-0.663594441140983,1.35956972361122,
4.59832804344617));
#372638=CARTESIAN_POINT('Ctrl Pts',(-0.289247880464149,1.48509060641666,
4.57683059495905));
#372639=CARTESIAN_POINT('Ctrl Pts',(-0.0910715305443453,1.51024593205019,
4.5671662902798));
#372640=CARTESIAN_POINT('Ctrl Pts',(0.297701778274559,1.4826354295215,4.54769446733454));
#372641=CARTESIAN_POINT('Ctrl Pts',(0.484737018724916,1.43242588434229,
4.53730102054439));
#372642=CARTESIAN_POINT('Ctrl Pts',(0.836463753097666,1.26098931384478,
4.51561643318852));
#372643=CARTESIAN_POINT('Ctrl Pts',(0.996521375751348,1.13873717146129,
4.50451976438413));
#372644=CARTESIAN_POINT('Ctrl Pts',(1.25453023926176,0.84439732766198,4.48393020037851));
#372645=CARTESIAN_POINT('Ctrl Pts',(1.35217355313513,0.677110988015738,
4.4751172771119));
#372646=CARTESIAN_POINT('Ctrl Pts',(1.47982766403363,0.31272423517926,4.45487356862099));
#372647=CARTESIAN_POINT('Ctrl Pts',(1.50783339833044,0.118797860144214,
4.44409988111904));
#372648=CARTESIAN_POINT('Ctrl Pts',(1.48817173561793,-0.273638462821338,
4.42229786317651));
#372649=CARTESIAN_POINT('Ctrl Pts',(1.4388361788813,-0.468300107990309,
4.41148332733379));
#372650=CARTESIAN_POINT('Ctrl Pts',(1.27096497526889,-0.818967732484933,
4.39200179263965));
#372651=CARTESIAN_POINT('Ctrl Pts',(1.15719181702216,-0.973131571865142,
4.38281065136992));
#372652=CARTESIAN_POINT('Ctrl Pts',(0.873387965745884,-1.23521327749103,
4.36187608483048));
#372653=CARTESIAN_POINT('Ctrl Pts',(0.704364537477269,-1.338815408904,4.3508661043626));
#372654=CARTESIAN_POINT('Ctrl Pts',(0.353475962893003,-1.46855342446925,
4.33038013618092));
#372655=CARTESIAN_POINT('Ctrl Pts',(0.17734521529577,-1.5,4.32103252564921));
#372656=CARTESIAN_POINT('Ctrl Pts',(-5.98132654516803E-14,-1.5,4.3125));
#372657=CARTESIAN_POINT('Origin',(0.,2.04523456705693E-15,3.99999999999998));
#372658=CARTESIAN_POINT('',(-2.29292018146855E-16,-1.5,3.75));
#372659=CARTESIAN_POINT('',(-4.8449908341125E-15,-1.5,3.8125));
#372660=CARTESIAN_POINT('',(-1.83697019872103E-16,-1.5,3.99999999999998));
#372661=CARTESIAN_POINT('Ctrl Pts',(2.42861286636753E-15,-1.5,3.75));
#372662=CARTESIAN_POINT('Ctrl Pts',(0.193317174447722,-1.5,3.7593009768922));
#372663=CARTESIAN_POINT('Ctrl Pts',(0.384935667136526,-1.46262884767149,
3.76955831348497));
#372664=CARTESIAN_POINT('Ctrl Pts',(0.745639566529835,-1.31618466565995,
3.79098058188077));
#372665=CARTESIAN_POINT('Ctrl Pts',(0.910865964988617,-1.20774522917046,
3.80194224725221));
#372666=CARTESIAN_POINT('Ctrl Pts',(1.18629623939077,-0.937468647541969,
3.82270157533098));
#372667=CARTESIAN_POINT('Ctrl Pts',(1.29542242527005,-0.779754510200248,
3.83168030498901));
#372668=CARTESIAN_POINT('Ctrl Pts',(1.45254177348479,-0.423894276102234,
3.85145031799445));
#372669=CARTESIAN_POINT('Ctrl Pts',(1.49588111718185,-0.227782106418506,
3.86234543853244));
#372670=CARTESIAN_POINT('Ctrl Pts',(1.50345672710943,0.164529044750317,
3.88414050248626));
#372671=CARTESIAN_POINT('Ctrl Pts',(1.46971337247465,0.356943553614525,
3.89483019742316));
#372672=CARTESIAN_POINT('Ctrl Pts',(1.33112237295684,0.717914269568467,
3.91488412608726));
#372673=CARTESIAN_POINT('Ctrl Pts',(1.22776875417754,0.883105026681858,
3.92379297679183));
#372674=CARTESIAN_POINT('Ctrl Pts',(0.960169961217741,1.16944379999735,
3.94462168453532));
#372675=CARTESIAN_POINT('Ctrl Pts',(0.796899563869198,1.28626107029131,
3.95572195936514));
#372676=CARTESIAN_POINT('Ctrl Pts',(0.441174140060695,1.44636211553748,
3.97728405805476));
#372677=CARTESIAN_POINT('Ctrl Pts',(0.253275421369734,1.49079566610575,
3.98755860466638));
#372678=CARTESIAN_POINT('Ctrl Pts',(-0.137708502264893,1.50698986612346,
4.00681966635236));
#372679=CARTESIAN_POINT('Ctrl Pts',(-0.337180643988774,1.47523796094839,
4.01691044571594));
#372680=CARTESIAN_POINT('Ctrl Pts',(-0.708493892957603,1.33662597697244,
4.03862559562465));
#372681=CARTESIAN_POINT('Ctrl Pts',(-0.877146433261387,1.2325377380485,
4.04963123472341));
#372682=CARTESIAN_POINT('Ctrl Pts',(-1.16012139503677,0.969638499902146,
4.07054863053483));
#372683=CARTESIAN_POINT('Ctrl Pts',(-1.27343327571507,0.815126535815214,
4.07971519245486));
#372684=CARTESIAN_POINT('Ctrl Pts',(-1.4402476744218,0.463942020344171,
4.09922544331436));
#372685=CARTESIAN_POINT('Ctrl Pts',(-1.48899427959348,0.269128999797649,
4.11004838890027));
#372686=CARTESIAN_POINT('Ctrl Pts',(-1.50746366959263,-0.123311635354483,
4.13185064640872));
#372687=CARTESIAN_POINT('Ctrl Pts',(-1.47888959224984,-0.317096438885883,
4.14261646882713));
#372688=CARTESIAN_POINT('Ctrl Pts',(-1.35015742029248,-0.681150531106146,
4.1628416961727));
#372689=CARTESIAN_POINT('Ctrl Pts',(-1.25195759418559,-0.848229850102839,
4.17166043577936));
#372690=CARTESIAN_POINT('Ctrl Pts',(-0.993006531798035,-1.14179263176492,
4.19227374629023));
#372691=CARTESIAN_POINT('Ctrl Pts',(-0.832626718069013,-1.26351647183078,
4.20337124145558));
#372692=CARTESIAN_POINT('Ctrl Pts',(-0.4804930256072,-1.43384767725927,
4.22504470400639));
#372693=CARTESIAN_POINT('Ctrl Pts',(-0.293365512428091,-1.48349245009655,
4.23542690214965));
#372694=CARTESIAN_POINT('Ctrl Pts',(-0.0679647259223738,-1.49884641485544,
4.24669800156779));
#372695=CARTESIAN_POINT('Ctrl Pts',(-0.0339649311946905,-1.49999999999999,
4.24836586148598));
#372696=CARTESIAN_POINT('Ctrl Pts',(-1.85938419852099E-13,-1.5,4.24999999999999));
#372697=CARTESIAN_POINT('Ctrl Pts',(-6.21618141576187E-14,-1.5,4.3125));
#372698=CARTESIAN_POINT('Ctrl Pts',(-0.0220361068876159,-1.5,4.31143978731305));
#372699=CARTESIAN_POINT('Ctrl Pts',(-0.0440896866934215,-1.49951441502509,
4.31036524548832));
#372700=CARTESIAN_POINT('Ctrl Pts',(-0.257374002006283,-1.49010014052068,
4.29984209145821));
#372701=CARTESIAN_POINT('Ctrl Pts',(-0.445200616684323,-1.44513467194479,
4.28955623845232));
#372702=CARTESIAN_POINT('Ctrl Pts',(-0.800572894706048,-1.28398687415068,
4.26798205403763));
#372703=CARTESIAN_POINT('Ctrl Pts',(-0.963555031472045,-1.16666615388507,
4.25688166343012));
#372704=CARTESIAN_POINT('Ctrl Pts',(-1.23027480355594,-0.879585335516549,
4.23607463523564));
#372705=CARTESIAN_POINT('Ctrl Pts',(-1.33310063097869,-0.71420340219919,
4.22717796678877));
#372706=CARTESIAN_POINT('Ctrl Pts',(-1.4706923207297,-0.352916777050933,
4.20710648761387));
#372707=CARTESIAN_POINT('Ctrl Pts',(-1.50391414802456,-0.160357206271801,
4.19640873368169));
#372708=CARTESIAN_POINT('Ctrl Pts',(-1.49523538390863,0.231980923190581,
4.17461217093378));
#372709=CARTESIAN_POINT('Ctrl Pts',(-1.45134634220585,0.427968435029026,
4.16372397583165));
#372710=CARTESIAN_POINT('Ctrl Pts',(-1.29324177051268,0.783359016052853,
4.14398005466366));
#372711=CARTESIAN_POINT('Ctrl Pts',(-1.18369387177651,0.940746994757387,
4.13498530366013));
#372712=CARTESIAN_POINT('Ctrl Pts',(-0.907501794458939,1.21028380197535,
4.11420987261069));
#372713=CARTESIAN_POINT('Ctrl Pts',(-0.741925439127871,1.31828993756297,
4.10324340606755));
#372714=CARTESIAN_POINT('Ctrl Pts',(-0.375817827893553,1.46571065719209,
4.08153402541964));
#372715=CARTESIAN_POINT('Ctrl Pts',(-0.178470546812078,1.50254525226168,
4.07115736963867));
#372716=CARTESIAN_POINT('Ctrl Pts',(0.211061997787556,1.49728809463546,
4.05226994419216));
#372717=CARTESIAN_POINT('Ctrl Pts',(0.399615093233784,1.45832188862504,
4.04211578454639));
#372718=CARTESIAN_POINT('Ctrl Pts',(0.758793702467989,1.30901333118062,
4.02068733572334));
#372719=CARTESIAN_POINT('Ctrl Pts',(0.924938044307028,1.19740529082038,
4.00959348900624));
#372720=CARTESIAN_POINT('Ctrl Pts',(1.20152709152664,0.91876120286303,3.98854597871294));
#372721=CARTESIAN_POINT('Ctrl Pts',(1.31033315597123,0.755519761486827,
3.97947332008253));
#372722=CARTESIAN_POINT('Ctrl Pts',(1.45911184323506,0.397812888832886,
3.9596007160462));
#372723=CARTESIAN_POINT('Ctrl Pts',(1.49813742054345,0.206955371786397,
3.94899752065473));
#372724=CARTESIAN_POINT('Ctrl Pts',(1.50180400732931,-0.186695812584385,
3.92712801041191));
#372725=CARTESIAN_POINT('Ctrl Pts',(1.4633855571079,-0.385733709395978,
3.91607034947793));
#372726=CARTESIAN_POINT('Ctrl Pts',(1.31440271657819,-0.747402673668362,
3.89597762924058));
#372727=CARTESIAN_POINT('Ctrl Pts',(1.20901812608092,-0.908045177286519,
3.88711210123208));
#372728=CARTESIAN_POINT('Ctrl Pts',(0.940358863902646,-1.18484804164848,
3.86649725799934));
#372729=CARTESIAN_POINT('Ctrl Pts',(0.778280646850072,-1.29707823040083,
3.85558176090246));
#372730=CARTESIAN_POINT('Ctrl Pts',(0.417063112188425,-1.45449684338638,
3.83382993491346));
#372731=CARTESIAN_POINT('Ctrl Pts',(0.220852438302694,-1.49691451375519,
3.82321147584329));
#372732=CARTESIAN_POINT('Ctrl Pts',(0.0147017533215045,-1.49994598046505,
3.81320883897905));
#372733=CARTESIAN_POINT('Ctrl Pts',(0.00734980117470292,-1.5,3.81285361747389));
#372734=CARTESIAN_POINT('Ctrl Pts',(-1.70803542250024E-16,-1.5,3.8125));
#372735=CARTESIAN_POINT('Origin',(0.,2.04523456705693E-15,3.99999999999998));
#372736=CARTESIAN_POINT('',(3.08529632092537E-14,-1.5,3.25));
#372737=CARTESIAN_POINT('',(9.27932528099019E-14,-1.5,3.31250000000001));
#372738=CARTESIAN_POINT('',(-1.83697019872103E-16,-1.5,3.99999999999998));
#372739=CARTESIAN_POINT('Ctrl Pts',(6.18896234383795E-14,-1.5,3.25));
#372740=CARTESIAN_POINT('Ctrl Pts',(0.0236193760181181,-1.5,3.25113638775851));
#372741=CARTESIAN_POINT('Ctrl Pts',(0.0472571121222557,-1.49944213161188,
3.25228915521126));
#372742=CARTESIAN_POINT('Ctrl Pts',(0.26952666508563,-1.48892536666519,
3.26327523642389));
#372743=CARTESIAN_POINT('Ctrl Pts',(0.46428967906935,-1.44012316639196,
3.27400139297746));
#372744=CARTESIAN_POINT('Ctrl Pts',(0.819657363376108,-1.27124126752953,
3.29579019251773));
#372745=CARTESIAN_POINT('Ctrl Pts',(0.977550814569531,-1.15425150163482,
3.30663656044951));
#372746=CARTESIAN_POINT('Ctrl Pts',(1.2374143858276,-0.869097677339169,
3.32706019191482));
#372747=CARTESIAN_POINT('Ctrl Pts',(1.33794863026607,-0.704568367963706,
3.33585731289099));
#372748=CARTESIAN_POINT('Ctrl Pts',(1.47500556900581,-0.33820133932665,
3.35621103670416));
#372749=CARTESIAN_POINT('Ctrl Pts',(1.50690689687966,-0.138704427976324,
3.36729419844584));
#372750=CARTESIAN_POINT('Ctrl Pts',(1.49090952643366,0.253397825780057,
3.38907765698787));
#372751=CARTESIAN_POINT('Ctrl Pts',(1.44614680111722,0.442379325511738,
3.39957662919518));
#372752=CARTESIAN_POINT('Ctrl Pts',(1.28614841229457,0.79640059753073,3.41924447764068));
#372753=CARTESIAN_POINT('Ctrl Pts',(1.1711814584489,0.957485365441749,3.42858165484803));
#372754=CARTESIAN_POINT('Ctrl Pts',(0.884638191269975,1.22737339053452,
3.44986486380396));
#372755=CARTESIAN_POINT('Ctrl Pts',(0.715474203179367,1.33308805117331,
3.46094028832681));
#372756=CARTESIAN_POINT('Ctrl Pts',(0.352688975476681,1.47031697544214,
3.48220671529584));
#372757=CARTESIAN_POINT('Ctrl Pts',(0.16354229998072,1.50313990839815,3.49204434774589));
#372758=CARTESIAN_POINT('Ctrl Pts',(-0.22541776572076,1.49623432439379,
3.51095001941019));
#372759=CARTESIAN_POINT('Ctrl Pts',(-0.421502081379421,1.45321725354962,
3.52157904908053));
#372760=CARTESIAN_POINT('Ctrl Pts',(-0.782187844893288,1.29471707709067,
3.54333533364808));
#372761=CARTESIAN_POINT('Ctrl Pts',(-0.943880324387888,1.18203523116139,
3.55424481797074));
#372762=CARTESIAN_POINT('Ctrl Pts',(-1.21171955625412,0.904447836702659,
3.57484199997938));
#372763=CARTESIAN_POINT('Ctrl Pts',(-1.31665163765559,0.743446995699806,
3.5836973891279));
#372764=CARTESIAN_POINT('Ctrl Pts',(-1.46452924323748,0.381335799830201,
3.60381467778732));
#372765=CARTESIAN_POINT('Ctrl Pts',(-1.50234222138092,0.182246636753049,
3.61487518684716));
#372766=CARTESIAN_POINT('Ctrl Pts',(-1.49752713751633,-0.21127662527178,
3.63673759029298));
#372767=CARTESIAN_POINT('Ctrl Pts',(-1.45796575375281,-0.401967180432297,
3.64733151002412));
#372768=CARTESIAN_POINT('Ctrl Pts',(-1.30814645231051,-0.759336240874781,
3.66718534671537));
#372769=CARTESIAN_POINT('Ctrl Pts',(-1.1987759596943,-0.92237829952708,
3.67627881751247));
#372770=CARTESIAN_POINT('Ctrl Pts',(-0.92126584426853,-1.20022289459525,
3.69734843458468));
#372771=CARTESIAN_POINT('Ctrl Pts',(-0.754834825628767,-1.311291111728,
3.70844107895614));
#372772=CARTESIAN_POINT('Ctrl Pts',(-0.395318964041526,-1.45948519404714,
3.72985479619822));
#372773=CARTESIAN_POINT('Ctrl Pts',(-0.206707458644523,-1.49788856755131,
3.73999613185777));
#372774=CARTESIAN_POINT('Ctrl Pts',(-0.0106224566113999,-1.49997179727876,
3.74948814340919));
#372775=CARTESIAN_POINT('Ctrl Pts',(-0.00531062459895978,-1.5,3.74974449245485));
#372776=CARTESIAN_POINT('Ctrl Pts',(-2.74887016421606E-16,-1.5,3.75));
#372777=CARTESIAN_POINT('Ctrl Pts',(1.00613961606655E-15,-1.5,3.8125));
#372778=CARTESIAN_POINT('Ctrl Pts',(-0.182773440490596,-1.5,3.80370630874434));
#372779=CARTESIAN_POINT('Ctrl Pts',(-0.364128623411885,-1.46659527466693,
3.7940529444007));
#372780=CARTESIAN_POINT('Ctrl Pts',(-0.719708419004184,-1.33081615141452,
3.77317346119616));
#372781=CARTESIAN_POINT('Ctrl Pts',(-0.888588458717918,-1.22452674710187,
3.76209573304391));
#372782=CARTESIAN_POINT('Ctrl Pts',(-1.17417053184609,-0.953781845274569,
3.7408349674268));
#372783=CARTESIAN_POINT('Ctrl Pts',(-1.28853656997239,-0.79248842607806,
3.73152713478205));
#372784=CARTESIAN_POINT('Ctrl Pts',(-1.44745392865247,-0.438107871400596,
3.71183932618886));
#372785=CARTESIAN_POINT('Ctrl Pts',(-1.49166782250349,-0.248938403619751,
3.70132991131215));
#372786=CARTESIAN_POINT('Ctrl Pts',(-1.50648239108423,0.143329287662172,
3.67953726179648));
#372787=CARTESIAN_POINT('Ctrl Pts',(-1.47395433674677,0.342790948256581,
3.66845605843013));
#372788=CARTESIAN_POINT('Ctrl Pts',(-1.33574739983272,0.708712101293154,
3.64812710548365));
#372789=CARTESIAN_POINT('Ctrl Pts',(-1.23474837821021,0.872864648331606,
3.63932728548026));
#372790=CARTESIAN_POINT('Ctrl Pts',(-0.974041709728056,1.15722403395568,
3.61888515822173));
#372791=CARTESIAN_POINT('Ctrl Pts',(-0.815742745402805,1.27376574153387,
3.60803172609465));
#372792=CARTESIAN_POINT('Ctrl Pts',(-0.45980061970787,1.44156217831801,
3.5862454404546));
#372793=CARTESIAN_POINT('Ctrl Pts',(-0.26489011284581,1.48975679839026,
3.57552906487442));
#372794=CARTESIAN_POINT('Ctrl Pts',(0.123531837441048,1.50692421504699,
3.55636423239308));
#372795=CARTESIAN_POINT('Ctrl Pts',(0.313201827534702,1.47919447145629,
3.54685313869835));
#372796=CARTESIAN_POINT('Ctrl Pts',(0.678774778125591,1.35206517988781,
3.52573313270211));
#372797=CARTESIAN_POINT('Ctrl Pts',(0.850301629224248,1.25132059946621,
3.51468208266359));
#372798=CARTESIAN_POINT('Ctrl Pts',(1.14507492269931,0.988874219287773,
3.4932096187416));
#372799=CARTESIAN_POINT('Ctrl Pts',(1.26524264242336,0.829583920442607,
3.48358799558008));
#372800=CARTESIAN_POINT('Ctrl Pts',(1.43448023552564,0.478669870633699,
3.4640927705907));
#372801=CARTESIAN_POINT('Ctrl Pts',(1.48389686604776,0.291356187896974,
3.45368645488311));
#372802=CARTESIAN_POINT('Ctrl Pts',(1.50995189198597,-0.0991931473211767,
3.43198926959321));
#372803=CARTESIAN_POINT('Ctrl Pts',(1.48339355440948,-0.298913730684295,
3.42089368162859));
#372804=CARTESIAN_POINT('Ctrl Pts',(1.35617351730245,-0.66903123867981,
3.40033159785107));
#372805=CARTESIAN_POINT('Ctrl Pts',(1.25959301474578,-0.836800304160145,
3.39152441095101));
#372806=CARTESIAN_POINT('Ctrl Pts',(1.00689720493403,-1.12865830545299,
3.37125941143027));
#372807=CARTESIAN_POINT('Ctrl Pts',(0.852486342285255,-1.24938664153487,
3.3604767504461));
#372808=CARTESIAN_POINT('Ctrl Pts',(0.502115094222749,-1.42737944320944,
3.33867526142305));
#372809=CARTESIAN_POINT('Ctrl Pts',(0.308678900877465,-1.48130708221946,
3.32787056825897));
#372810=CARTESIAN_POINT('Ctrl Pts',(0.0735707215714186,-1.49864822341032,
3.31607722234164));
#372811=CARTESIAN_POINT('Ctrl Pts',(0.0367671122311343,-1.5,3.31426895851199));
#372812=CARTESIAN_POINT('Ctrl Pts',(1.85770202639676E-13,-1.5,3.31250000000001));
#372813=CARTESIAN_POINT('Origin',(0.,2.04523456705693E-15,3.99999999999998));
#372814=CARTESIAN_POINT('',(1.08281712706529E-13,-1.5,2.75000000000001));
#372815=CARTESIAN_POINT('',(6.17977475022196E-14,-1.5,2.8125));
#372816=CARTESIAN_POINT('',(-1.83697019872103E-16,-1.5,3.99999999999998));
#372817=CARTESIAN_POINT('Ctrl Pts',(2.16747122432931E-13,-1.5,2.75000000000001));
#372818=CARTESIAN_POINT('Ctrl Pts',(0.0522124451313231,-1.5,2.75251207243764));
#372819=CARTESIAN_POINT('Ctrl Pts',(0.10447874118418,-1.49727405122371,
2.75510245657833));
#372820=CARTESIAN_POINT('Ctrl Pts',(0.354406824394528,-1.47104006355408,
2.76785584896801));
#372821=CARTESIAN_POINT('Ctrl Pts',(0.546107038494388,-1.41113817496362,
2.77874297116893));
#372822=CARTESIAN_POINT('Ctrl Pts',(0.890309400649009,-1.22263015121861,
2.80053974903232));
#372823=CARTESIAN_POINT('Ctrl Pts',(1.04051930921944,-1.09763783034302,
2.81123873554121));
#372824=CARTESIAN_POINT('Ctrl Pts',(1.28472571765059,-0.797945454648135,
2.83131291005875));
#372825=CARTESIAN_POINT('Ctrl Pts',(1.37660375336644,-0.626260206772226,
2.84020776629049));
#372826=CARTESIAN_POINT('Ctrl Pts',(1.49202937496029,-0.251793770944039,
2.86101145716983));
#372827=CARTESIAN_POINT('Ctrl Pts',(1.5122301925727,-0.0519865643527668,
2.87211185753601));
#372828=CARTESIAN_POINT('Ctrl Pts',(1.47426865201774,0.336381921397972,
2.89368788452216));
#372829=CARTESIAN_POINT('Ctrl Pts',(1.41937297020844,0.521558431255365,
2.90397546840313));
#372830=CARTESIAN_POINT('Ctrl Pts',(1.23907502217178,0.868665674093023,
2.92325920411633));
#372831=CARTESIAN_POINT('Ctrl Pts',(1.11252577833543,1.02577158220901,2.93330056692789));
#372832=CARTESIAN_POINT('Ctrl Pts',(0.807873326352072,1.27902322098119,
2.95499293260172));
#372833=CARTESIAN_POINT('Ctrl Pts',(0.633675855472049,1.37368732240572,
2.96600357070002));
#372834=CARTESIAN_POINT('Ctrl Pts',(0.264849678828112,1.48860078663452,
2.9869407690705));
#372835=CARTESIAN_POINT('Ctrl Pts',(0.0744641039108102,1.51013733163361,
2.99613575158486));
#372836=CARTESIAN_POINT('Ctrl Pts',(-0.313170845636526,1.48036428077972,
3.01561287598095));
#372837=CARTESIAN_POINT('Ctrl Pts',(-0.506445454007791,1.4258491961316,
3.02642611281874));
#372838=CARTESIAN_POINT('Ctrl Pts',(-0.856226709513093,1.24681742407431,
3.04822807610006));
#372839=CARTESIAN_POINT('Ctrl Pts',(-1.01023130739802,1.12566531934954,
3.05900296201285));
#372840=CARTESIAN_POINT('Ctrl Pts',(-1.26209924684952,0.83303798094694,
3.07924950107758));
#372841=CARTESIAN_POINT('Ctrl Pts',(-1.35822194558857,0.664891162678306,
3.08806160207349));
#372842=CARTESIAN_POINT('Ctrl Pts',(-1.48429856811928,0.294344634871367,
3.10864752028499));
#372843=CARTESIAN_POINT('Ctrl Pts',(-1.5102380377602,0.09460703958459,3.11974405335647));
#372844=CARTESIAN_POINT('Ctrl Pts',(-1.48302106788286,-0.295745923053602,
3.14143032905859));
#372845=CARTESIAN_POINT('Ctrl Pts',(-1.43306828305171,-0.482858861267118,
3.15182549229268));
#372846=CARTESIAN_POINT('Ctrl Pts',(-1.26275751331793,-0.833407725948767,
3.17130042921943));
#372847=CARTESIAN_POINT('Ctrl Pts',(-1.14197808626569,-0.992488035128005,
3.18095899912744));
#372848=CARTESIAN_POINT('Ctrl Pts',(-0.846247312071301,-1.25405610530601,
3.20245313236201));
#372849=CARTESIAN_POINT('Ctrl Pts',(-0.674453619273247,-1.35421681136905,
3.21350080209559));
#372850=CARTESIAN_POINT('Ctrl Pts',(-0.330944750833914,-1.47246172076396,
3.23331246105066));
#372851=CARTESIAN_POINT('Ctrl Pts',(-0.165961922362418,-1.5,3.2420151532874));
#372852=CARTESIAN_POINT('Ctrl Pts',(6.6717464886068E-14,-1.5,3.25));
#372853=CARTESIAN_POINT('Ctrl Pts',(1.88425663960601E-13,-1.5,3.31250000000001));
#372854=CARTESIAN_POINT('Ctrl Pts',(-0.152607701100013,-1.5,3.30515765855747));
#372855=CARTESIAN_POINT('Ctrl Pts',(-0.304524679208517,-1.4767167661864,
3.29720179304546));
#372856=CARTESIAN_POINT('Ctrl Pts',(-0.637881204779632,-1.37174810773761,
3.27824737366289));
#372857=CARTESIAN_POINT('Ctrl Pts',(-0.811840182694752,-1.27651825179612,
3.26723249465947));
#372858=CARTESIAN_POINT('Ctrl Pts',(-1.11558185250335,-1.02240635105325,
3.2455600528476));
#372859=CARTESIAN_POINT('Ctrl Pts',(-1.24153613759052,-0.865097180051025,
3.23556095444722));
#372860=CARTESIAN_POINT('Ctrl Pts',(-1.42081536541909,-0.517635286571265,
3.21625751592057));
#372861=CARTESIAN_POINT('Ctrl Pts',(-1.47521081639495,-0.332255685912234,
3.20595864921729));
#372862=CARTESIAN_POINT('Ctrl Pts',(-1.51208229193674,0.0563280922715262,
3.18437066154042));
#372863=CARTESIAN_POINT('Ctrl Pts',(-1.49129795191174,0.2561354974193,3.17327025014332));
#372864=CARTESIAN_POINT('Ctrl Pts',(-1.37478505061458,0.630208162207134,
3.15248843543289));
#372865=CARTESIAN_POINT('Ctrl Pts',(-1.28247518031101,0.801530606296313,
3.14360504348462));
#372866=CARTESIAN_POINT('Ctrl Pts',(-1.03749078900277,1.10051002620746,
3.12351324257578));
#372867=CARTESIAN_POINT('Ctrl Pts',(-0.886892799455015,1.22511913749658,
3.11280622922291));
#372868=CARTESIAN_POINT('Ctrl Pts',(-0.542114383767811,1.4126764710966,
3.09100814403059));
#372869=CARTESIAN_POINT('Ctrl Pts',(-0.350247890791992,1.47203555681224,
3.08012809959115));
#372870=CARTESIAN_POINT('Ctrl Pts',(0.0366799443214752,1.51154513430789,
3.06041453718074));
#372871=CARTESIAN_POINT('Ctrl Pts',(0.227673498706082,1.49475418374031,
3.05140033656785));
#372872=CARTESIAN_POINT('Ctrl Pts',(0.598892177156894,1.38913607705811,
3.03060623327681));
#372873=CARTESIAN_POINT('Ctrl Pts',(0.774981653006425,1.29914199429579,
3.01963428878759));
#372874=CARTESIAN_POINT('Ctrl Pts',(1.08494916107576,1.0547200111272,2.99793147056981));
#372875=CARTESIAN_POINT('Ctrl Pts',(1.21501958033426,0.901790420280011,
2.98759946779328));
#372876=CARTESIAN_POINT('Ctrl Pts',(1.40413285092575,0.561118340799233,
2.96867324115546));
#372877=CARTESIAN_POINT('Ctrl Pts',(1.46406184662414,0.378076856399767,
2.95850426979994));
#372878=CARTESIAN_POINT('Ctrl Pts',(1.51302625577521,-0.00793947459916036,
2.93705891807778));
#372879=CARTESIAN_POINT('Ctrl Pts',(1.49873234713959,-0.207651602247236,
2.92596379987511));
#372880=CARTESIAN_POINT('Ctrl Pts',(1.39437436880055,-0.586042286108765,
2.90494209521614));
#372881=CARTESIAN_POINT('Ctrl Pts',(1.30687737144127,-0.761440127297383,
2.89589271886943));
#372882=CARTESIAN_POINT('Ctrl Pts',(1.07053769069727,-1.06828631993652,
2.87599831532686));
#372883=CARTESIAN_POINT('Ctrl Pts',(0.924283752090724,-1.19706732666361,
2.86538441923795));
#372884=CARTESIAN_POINT('Ctrl Pts',(0.584410274341166,-1.39598135855799,
2.84350685914068));
#372885=CARTESIAN_POINT('Ctrl Pts',(0.392530146371773,-1.4615871174733,
2.83245263998732));
#372886=CARTESIAN_POINT('Ctrl Pts',(0.129150917970223,-1.49583416689111,
2.81882949402433));
#372887=CARTESIAN_POINT('Ctrl Pts',(0.0645467119743484,-1.5,2.8156055051278));
#372888=CARTESIAN_POINT('Ctrl Pts',(1.23779192024311E-13,-1.5,2.8125));
#372889=CARTESIAN_POINT('Origin',(0.,2.04523456705693E-15,3.99999999999998));
#372890=CARTESIAN_POINT('',(1.53125027804872E-14,-1.5,2.25));
#372891=CARTESIAN_POINT('',(1.52431070176988E-14,-1.5,2.3125));
#372892=CARTESIAN_POINT('',(-1.83697019872103E-16,-1.5,3.99999999999998));
#372893=CARTESIAN_POINT('Ctrl Pts',(3.08087025808465E-14,-1.5,2.25));
#372894=CARTESIAN_POINT('Ctrl Pts',(0.0808582836836842,-1.5,2.25389029598758));
#372895=CARTESIAN_POINT('Ctrl Pts',(0.16175453469314,-1.49346296475911,
2.25796400299127));
#372896=CARTESIAN_POINT('Ctrl Pts',(0.43941581054574,-1.44809001830053,
2.27258334697821));
#372897=CARTESIAN_POINT('Ctrl Pts',(0.628462258701575,-1.37661598127761,
2.28366423837319));
#372898=CARTESIAN_POINT('Ctrl Pts',(0.960882035050376,-1.16779804180548,
2.30545829063843));
#372899=CARTESIAN_POINT('Ctrl Pts',(1.10266810963985,-1.03498199083381,
2.31596931108195));
#372900=CARTESIAN_POINT('Ctrl Pts',(1.33024348271686,-0.720282150838644,
2.33566019854628));
#372901=CARTESIAN_POINT('Ctrl Pts',(1.41281889958196,-0.540655708541785,
2.34496357174773));
#372902=CARTESIAN_POINT('Ctrl Pts',(1.50468845633309,-0.158024426932706,
2.36622086517045));
#372903=CARTESIAN_POINT('Ctrl Pts',(1.5123965356432,0.0413809023853515,
2.37729893902146));
#372904=CARTESIAN_POINT('Ctrl Pts',(1.45121353764186,0.424524588612146,
2.39858469936739));
#372905=CARTESIAN_POINT('Ctrl Pts',(1.38569001068393,0.605026344035973,
2.40847057894424));
#372906=CARTESIAN_POINT('Ctrl Pts',(1.18638164624256,0.939163043957149,
2.42734138209721));
#372907=CARTESIAN_POINT('Ctrl Pts',(1.05161195027867,1.08794060110316,2.43795820203822));
#372908=CARTESIAN_POINT('Ctrl Pts',(0.734778389573018,1.32220909884669,
2.45970932210568));
#372909=CARTESIAN_POINT('Ctrl Pts',(0.556575816602285,1.40654416171405,
2.47062573803046));
#372910=CARTESIAN_POINT('Ctrl Pts',(0.182569497469227,1.50097846673481,
2.4912433005891));
#372911=CARTESIAN_POINT('Ctrl Pts',(-0.00923039425979297,1.51201094511843,
2.50011046018654));
#372912=CARTESIAN_POINT('Ctrl Pts',(-0.396962349093565,1.46038094829539,
2.52019938913968));
#372913=CARTESIAN_POINT('Ctrl Pts',(-0.588583117065401,1.3942181726357,
2.53125660251669));
#372914=CARTESIAN_POINT('Ctrl Pts',(-0.927767071615718,1.19436080871201,
2.55312719158105));
#372915=CARTESIAN_POINT('Ctrl Pts',(-1.0736052072278,1.06519365227555,2.56373180871987));
#372916=CARTESIAN_POINT('Ctrl Pts',(-1.30912426207158,0.757606940798347,
2.58360729984813));
#372917=CARTESIAN_POINT('Ctrl Pts',(-1.39616247157342,0.58181724405329,
2.59267681977487));
#372918=CARTESIAN_POINT('Ctrl Pts',(-1.49935819859759,0.203023435309446,
2.61372092026064));
#372919=CARTESIAN_POINT('Ctrl Pts',(-1.51303547644827,0.00333102406007514,
2.62481494310783));
#372920=CARTESIAN_POINT('Ctrl Pts',(-1.46292579985952,-0.382421581918602,
2.64624564343997));
#372921=CARTESIAN_POINT('Ctrl Pts',(-1.4024745750708,-0.56523185884661,
2.65640176993597));
#372922=CARTESIAN_POINT('Ctrl Pts',(-1.21240661635006,-0.90529816770916,
2.67529434265056));
#372923=CARTESIAN_POINT('Ctrl Pts',(-1.08189976900056,-1.05784684540797,
2.68566504102233));
#372924=CARTESIAN_POINT('Ctrl Pts',(-0.771275797713282,-1.30133724975859,
2.70737356615202));
#372925=CARTESIAN_POINT('Ctrl Pts',(-0.594982522266591,-1.39080747307205,
2.71834076430257));
#372926=CARTESIAN_POINT('Ctrl Pts',(-0.27394416727951,-1.4811861030294,
2.73629724685739));
#372927=CARTESIAN_POINT('Ctrl Pts',(-0.13718321777196,-1.5,2.74339976935758));
#372928=CARTESIAN_POINT('Ctrl Pts',(2.12121986642444E-13,-1.5,2.75000000000001));
#372929=CARTESIAN_POINT('Ctrl Pts',(1.25732757538799E-13,-1.5,2.8125));
#372930=CARTESIAN_POINT('Ctrl Pts',(-0.125068644536108,-1.5,2.80648263203416));
#372931=CARTESIAN_POINT('Ctrl Pts',(-0.249879261089443,-1.48436218482603,
2.80004329469055));
#372932=CARTESIAN_POINT('Ctrl Pts',(-0.560819973154951,-1.40486536800048,
2.78287490779431));
#372933=CARTESIAN_POINT('Ctrl Pts',(-0.738819729590105,-1.31996381251163,
2.7719525139785));
#372934=CARTESIAN_POINT('Ctrl Pts',(-1.05497027342245,-1.08468356605574,
2.75020615144477));
#372935=CARTESIAN_POINT('Ctrl Pts',(-1.18927677596674,-0.935493387614889,
2.73960015520493));
#372936=CARTESIAN_POINT('Ctrl Pts',(-1.38757347699829,-0.600708235287357,
2.72076001316361));
#372937=CARTESIAN_POINT('Ctrl Pts',(-1.45254878301697,-0.419955776142848,
2.71083087645234));
#372938=CARTESIAN_POINT('Ctrl Pts',(-1.51253033572044,-0.0365073802504774,
2.68952818779166));
#372939=CARTESIAN_POINT('Ctrl Pts',(-1.50417280301816,0.162937666001922,
2.6784479074443));
#372940=CARTESIAN_POINT('Ctrl Pts',(-1.41106400963208,0.54515718868444,
2.6572134895175));
#372941=CARTESIAN_POINT('Ctrl Pts',(-1.32800083044783,0.724362315220717,
2.64793896098909));
#372942=CARTESIAN_POINT('Ctrl Pts',(-1.09956096666915,1.03829286473376,
2.62822784987654));
#372943=CARTESIAN_POINT('Ctrl Pts',(-0.957331683565913,1.17071965804038,
2.61770631826639));
#372944=CARTESIAN_POINT('Ctrl Pts',(-0.624168195026001,1.37857754843603,
2.59590315216156));
#372945=CARTESIAN_POINT('Ctrl Pts',(-0.434836132007832,1.44948073533607,
2.58482437606297));
#372946=CARTESIAN_POINT('Ctrl Pts',(-0.0486163057092892,1.51132307459164,
2.56452452324922));
#372947=CARTESIAN_POINT('Ctrl Pts',(0.143934424738931,1.5052396812014,2.55572049846095));
#372948=CARTESIAN_POINT('Ctrl Pts',(0.520236531724272,1.4203186948451,2.53525673860956));
#372949=CARTESIAN_POINT('Ctrl Pts',(0.700094458610885,1.34082435632475,
2.52439514399756));
#372950=CARTESIAN_POINT('Ctrl Pts',(1.02261141707528,1.11524984086218,2.50261208083574));
#372951=CARTESIAN_POINT('Ctrl Pts',(1.16127195756225,0.970045360100909,
2.49190731467214));
#372952=CARTESIAN_POINT('Ctrl Pts',(1.36916321610676,0.641468401698581,
2.4727780040985));
#372953=CARTESIAN_POINT('Ctrl Pts',(1.43933947070695,0.463059693474664,
2.46322553852634));
#372954=CARTESIAN_POINT('Ctrl Pts',(1.51063981501737,0.0825332381250036,
2.4420851798958));
#372955=CARTESIAN_POINT('Ctrl Pts',(1.50840435404898,-0.116454606961533,
2.43103029961322));
#372956=CARTESIAN_POINT('Ctrl Pts',(1.42705084815203,-0.502498436699463,
2.40958342018333));
#372957=CARTESIAN_POINT('Ctrl Pts',(1.34861280625527,-0.68571361679187,
2.40000423009386));
#372958=CARTESIAN_POINT('Ctrl Pts',(1.12832858207098,-1.00685537477425,
2.38048519602788));
#372959=CARTESIAN_POINT('Ctrl Pts',(0.990299485101312,-1.14287804995166,
2.37006586035978));
#372960=CARTESIAN_POINT('Ctrl Pts',(0.66422042262994,-1.35964487887696,
2.34835607334839));
#372961=CARTESIAN_POINT('Ctrl Pts',(0.477633199931601,-1.43586269523415,
2.33726172984523));
#372962=CARTESIAN_POINT('Ctrl Pts',(0.1885624580824,-1.49111209387676,2.32181910177559));
#372963=CARTESIAN_POINT('Ctrl Pts',(0.0942846646342436,-1.5,2.31703627304225));
#372964=CARTESIAN_POINT('Ctrl Pts',(3.06699110552697E-14,-1.5,2.3125));
#372965=CARTESIAN_POINT('Origin',(0.,2.04523456705693E-15,3.99999999999998));
#372966=CARTESIAN_POINT('',(-1.56323089387029E-14,-1.5,1.75));
#372967=CARTESIAN_POINT('',(-6.21522480643445E-14,-1.5,1.81249999999999));
#372968=CARTESIAN_POINT('',(-1.83697019872103E-16,-1.5,3.99999999999998));
#372969=CARTESIAN_POINT('Ctrl Pts',(-3.27862736959617E-14,-1.5,1.75));
#372970=CARTESIAN_POINT('Ctrl Pts',(0.110465980352864,-1.5,1.75531479695775));
#372971=CARTESIAN_POINT('Ctrl Pts',(0.220826650588412,-1.48780022182646,
1.7609634099072));
#372972=CARTESIAN_POINT('Ctrl Pts',(0.523187787936054,-1.41980742425771,
1.7773994557319));
#372973=CARTESIAN_POINT('Ctrl Pts',(0.706663478164997,-1.33798206582024,
1.78849986061712));
#372974=CARTESIAN_POINT('Ctrl Pts',(1.02486460638805,-1.11188867721038,
1.81008969144261));
#372975=CARTESIAN_POINT('Ctrl Pts',(1.15827642974689,-0.972142672853255,
1.82039030424109));
#372976=CARTESIAN_POINT('Ctrl Pts',(1.36967438783033,-0.643260876612614,
1.83969679869269));
#372977=CARTESIAN_POINT('Ctrl Pts',(1.44300442220864,-0.45559082607096,
1.84968939855165));
#372978=CARTESIAN_POINT('Ctrl Pts',(1.51138716216324,-0.0655426848016987,
1.87135873973328));
#372979=CARTESIAN_POINT('Ctrl Pts',(1.50697374411077,0.132736822001649,
1.88237426788902));
#372980=CARTESIAN_POINT('Ctrl Pts',(1.42338094597886,0.50996348712316,1.90333130484022));
#372981=CARTESIAN_POINT('Ctrl Pts',(1.34745527842838,0.685872585531904,
1.91255587728802));
#372982=CARTESIAN_POINT('Ctrl Pts',(1.12898409138924,1.00744632259985,1.93199968098273));
#372983=CARTESIAN_POINT('Ctrl Pts',(0.9856297739892,1.14807028978956,1.94280304010526));
#372984=CARTESIAN_POINT('Ctrl Pts',(0.65639193832536,1.36266393223992,1.96460443737176));
#372985=CARTESIAN_POINT('Ctrl Pts',(0.474658265785483,1.43611088421253,
1.97538829587892));
#372986=CARTESIAN_POINT('Ctrl Pts',(0.0955931180921214,1.5091936725856,
1.99565615375549));
#372987=CARTESIAN_POINT('Ctrl Pts',(-0.0979742429755275,1.50904098461822,
2.00446264950139));
#372988=CARTESIAN_POINT('Ctrl Pts',(-0.482146305565531,1.43434467581502,
2.02502103394744));
#372989=CARTESIAN_POINT('Ctrl Pts',(-0.668434095227935,1.35756902850466,
2.0361164662762));
#372990=CARTESIAN_POINT('Ctrl Pts',(-0.993748366577721,1.13987096052055,
2.05781532500923));
#372991=CARTESIAN_POINT('Ctrl Pts',(-1.13132684273033,1.00347457456687,
2.06822336102806));
#372992=CARTESIAN_POINT('Ctrl Pts',(-1.35074056268981,0.681569212981403,
2.0877217241512));
#372993=CARTESIAN_POINT('Ctrl Pts',(-1.42868159347472,0.497921452399993,
2.09733769708893));
#372994=CARTESIAN_POINT('Ctrl Pts',(-1.50877191600071,0.111477628688774,
2.11880679840622));
#372995=CARTESIAN_POINT('Ctrl Pts',(-1.51035481506967,-0.0874505114863162,
2.12985836174928));
#372996=CARTESIAN_POINT('Ctrl Pts',(-1.43784842849668,-0.467658955411782,
2.15098105307848));
#372997=CARTESIAN_POINT('Ctrl Pts',(-1.36711298429262,-0.645820324970424,
2.16049753268028));
#372998=CARTESIAN_POINT('Ctrl Pts',(-1.15819103191155,-0.973722457299709,
2.17965768736555));
#372999=CARTESIAN_POINT('Ctrl Pts',(-1.01906810208961,-1.118489200093,2.19037254085841));
#373000=CARTESIAN_POINT('Ctrl Pts',(-0.695882317517152,-1.34300659885496,
2.21215841857856));
#373001=CARTESIAN_POINT('Ctrl Pts',(-0.515833568513887,-1.42191558898578,
2.22301293444644));
#373002=CARTESIAN_POINT('Ctrl Pts',(-0.218540308087038,-1.48805180668198,
2.23915358026597));
#373003=CARTESIAN_POINT('Ctrl Pts',(-0.109320999056845,-1.5,2.24474029098054));
#373004=CARTESIAN_POINT('Ctrl Pts',(3.46944695195361E-14,-1.5,2.25));
#373005=CARTESIAN_POINT('Ctrl Pts',(3.06699110552697E-14,-1.5,2.3125));
#373006=CARTESIAN_POINT('Ctrl Pts',(-0.0965880711665686,-1.5,2.30785290425929));
#373007=CARTESIAN_POINT('Ctrl Pts',(-0.193158137690027,-1.4906725807854,
2.30294757978916));
#373008=CARTESIAN_POINT('Ctrl Pts',(-0.479015211220926,-1.43467130791224,
2.28763868401328));
#373009=CARTESIAN_POINT('Ctrl Pts',(-0.660579011765522,-1.36064740788891,
2.27684697214157));
#373010=CARTESIAN_POINT('Ctrl Pts',(-0.989193594360455,-1.14500049552058,
2.2550463036546));
#373011=CARTESIAN_POINT('Ctrl Pts',(-1.13210802585101,-1.00393400821821,
2.24425181632741));
#373012=CARTESIAN_POINT('Ctrl Pts',(-1.34957613319165,-0.681688912067382,
2.22483762446378));
#373013=CARTESIAN_POINT('Ctrl Pts',(-1.42495560561359,-0.505546483895616,
2.21558591577195));
#373014=CARTESIAN_POINT('Ctrl Pts',(-1.50739111574804,-0.128003682012438,
2.19461131566733));
#373015=CARTESIAN_POINT('Ctrl Pts',(-1.51117896410855,0.0703519564588762,
2.18359155797448));
#373016=CARTESIAN_POINT('Ctrl Pts',(-1.44156601709098,0.460030181085983,
2.16194276771742));
#373017=CARTESIAN_POINT('Ctrl Pts',(-1.36775091328919,0.647276578730561,
2.15199270819955));
#373018=CARTESIAN_POINT('Ctrl Pts',(-1.1555150408507,0.975433740479151,
2.13266602831064));
#373019=CARTESIAN_POINT('Ctrl Pts',(-1.02166635155199,1.11483732583894,
2.12235390842865));
#373020=CARTESIAN_POINT('Ctrl Pts',(-0.702715978000763,1.34006834118604,
2.10075198433335));
#373021=CARTESIAN_POINT('Ctrl Pts',(-0.518941844775744,1.42137322325474,
2.0896516782797));
#373022=CARTESIAN_POINT('Ctrl Pts',(-0.136491021717308,1.50615937001468,
2.06889583373266));
#373023=CARTESIAN_POINT('Ctrl Pts',(0.0579178943444623,1.51122112856893,
2.06002512202488));
#373024=CARTESIAN_POINT('Ctrl Pts',(0.439062286518284,1.44732779216569,
2.03991248900632));
#373025=CARTESIAN_POINT('Ctrl Pts',(0.62211066169564,1.37858561025607,2.02919606489633));
#373026=CARTESIAN_POINT('Ctrl Pts',(0.956291225897921,1.17262469136765,
2.00739665836887));
#373027=CARTESIAN_POINT('Ctrl Pts',(1.10317084007132,1.0356521579006,1.99652511704077));
#373028=CARTESIAN_POINT('Ctrl Pts',(1.32977620972735,0.71958221691235,1.97684284052687));
#373029=CARTESIAN_POINT('Ctrl Pts',(1.41014293676257,0.545538436502839,
1.9678076909168));
#373030=CARTESIAN_POINT('Ctrl Pts',(1.50306004150702,0.170899505389093,
1.94699441696604));
#373031=CARTESIAN_POINT('Ctrl Pts',(1.51250765220232,-0.0266949177684643,
1.93601694901284));
#373032=CARTESIAN_POINT('Ctrl Pts',(1.45446866407842,-0.417219669807208,
1.91432112945513));
#373033=CARTESIAN_POINT('Ctrl Pts',(1.38641298054374,-0.606104201316678,
1.90403426447937));
#373034=CARTESIAN_POINT('Ctrl Pts',(1.18475132210135,-0.939591370600925,
1.88506828093367));
#373035=CARTESIAN_POINT('Ctrl Pts',(1.05565072199852,-1.0826106135082,1.87488416866775));
#373036=CARTESIAN_POINT('Ctrl Pts',(0.744885128346205,-1.31699893814408,
1.85342166527648));
#373037=CARTESIAN_POINT('Ctrl Pts',(0.564398045291385,-1.40385240762055,
1.84232538006989));
#373038=CARTESIAN_POINT('Ctrl Pts',(0.250343776141915,-1.48430541194397,
1.82498063132477));
#373039=CARTESIAN_POINT('Ctrl Pts',(0.125295181136604,-1.5,1.81852826721312));
#373040=CARTESIAN_POINT('Ctrl Pts',(-1.25906229886397E-13,-1.49999999999999,
1.81249999999999));
#373041=CARTESIAN_POINT('Origin',(0.,2.04523456705693E-15,3.99999999999998));
#373042=CARTESIAN_POINT('',(-1.08601518864753E-13,-1.5,1.24999999999999));
#373043=CARTESIAN_POINT('',(-1.08584123502877E-13,-1.5,1.31249999999999));
#373044=CARTESIAN_POINT('',(-1.83697019872103E-16,-1.5,3.99999999999998));
#373045=CARTESIAN_POINT('Ctrl Pts',(-2.14515905039292E-13,-1.5,1.24999999999999));
#373046=CARTESIAN_POINT('Ctrl Pts',(0.142046010209568,-1.50000000000002,
1.25683419185265));
#373047=CARTESIAN_POINT('Ctrl Pts',(0.283618928461168,-1.47982853466809,
1.26420594053933));
#373048=CARTESIAN_POINT('Ctrl Pts',(0.610273392442458,-1.38443304740553,
1.28257198541148));
#373049=CARTESIAN_POINT('Ctrl Pts',(0.787232533826629,-1.29203315350746,
1.29365259979035));
#373050=CARTESIAN_POINT('Ctrl Pts',(1.08945269237421,-1.04850212355775,
1.31495792477995));
#373051=CARTESIAN_POINT('Ctrl Pts',(1.21357794911698,-0.901910093035529,
1.32489388372028));
#373052=CARTESIAN_POINT('Ctrl Pts',(1.40452842820938,-0.562873685428105,
1.34372923969847));
#373053=CARTESIAN_POINT('Ctrl Pts',(1.46666942429647,-0.371996296491918,
1.35433353908381));
#373054=CARTESIAN_POINT('Ctrl Pts',(1.51254266554068,0.0194245347427818,
1.37607914081908));
#373055=CARTESIAN_POINT('Ctrl Pts',(1.49716203510275,0.216044242038897,
1.38700245789108));
#373056=CARTESIAN_POINT('Ctrl Pts',(1.39321705231764,0.587531249040284,
1.40764062494672));
#373057=CARTESIAN_POINT('Ctrl Pts',(1.30749811300545,0.759400562987588,
1.41652076112397));
#373058=CARTESIAN_POINT('Ctrl Pts',(1.07001351269348,1.07022980169436,1.43658088980348));
#373059=CARTESIAN_POINT('Ctrl Pts',(0.917312276987485,1.20367827683049,
1.44763463351896));
#373060=CARTESIAN_POINT('Ctrl Pts',(0.575184773746649,1.39872671094257,
1.46951326275207));
#373061=CARTESIAN_POINT('Ctrl Pts',(0.390550034024555,1.46108197715838,
1.48012859653698));
#373062=CARTESIAN_POINT('Ctrl Pts',(0.00667963752372162,1.51250336222095,
1.50002594140708));
#373063=CARTESIAN_POINT('Ctrl Pts',(-0.188950779722364,1.50067134499163,
1.50907225015607));
#373064=CARTESIAN_POINT('Ctrl Pts',(-0.568861669400175,1.40204066404771,
1.53009046249537));
#373065=CARTESIAN_POINT('Ctrl Pts',(-0.749014905039891,1.31464516172283,
1.54118574192872));
#373066=CARTESIAN_POINT('Ctrl Pts',(-1.05895709623939,1.07936663988191,
1.56263335705116));
#373067=CARTESIAN_POINT('Ctrl Pts',(-1.18758289078589,0.935998387392519,
1.57280431993471));
#373068=CARTESIAN_POINT('Ctrl Pts',(-1.38821273327314,0.601967247945771,
1.59173577049441));
#373069=CARTESIAN_POINT('Ctrl Pts',(-1.45570368464549,0.412887480677177,
1.60206180662908));
#373070=CARTESIAN_POINT('Ctrl Pts',(-1.51257219096668,0.0222530178901751,
1.62376372122836));
#373071=CARTESIAN_POINT('Ctrl Pts',(-1.50255110561474,-0.175255140108835,
1.63473639667275));
#373072=CARTESIAN_POINT('Ctrl Pts',(-1.40857020455048,-0.549594300042889,
1.65553301666909));
#373073=CARTESIAN_POINT('Ctrl Pts',(-1.32769205341188,-0.723426877757731,
1.66454991067901));
#373074=CARTESIAN_POINT('Ctrl Pts',(-1.10015281575383,-1.0388579891019,
1.68425937267021));
#373075=CARTESIAN_POINT('Ctrl Pts',(-0.952873363457998,-1.17540418952279,
1.69513830863433));
#373076=CARTESIAN_POINT('Ctrl Pts',(-0.618138225247735,-1.38036373829122,
1.71693658127953));
#373077=CARTESIAN_POINT('Ctrl Pts',(-0.434946138927554,-1.44856289323058,
1.7276448356126));
#373078=CARTESIAN_POINT('Ctrl Pts',(-0.163054354521467,-1.4933575782512,
1.74197053199517));
#373079=CARTESIAN_POINT('Ctrl Pts',(-0.0815074860315138,-1.49999999999999,
1.7460784692499));
#373080=CARTESIAN_POINT('Ctrl Pts',(-3.10809208575337E-14,-1.5,1.75));
#373081=CARTESIAN_POINT('Ctrl Pts',(-1.24120799108817E-13,-1.5,1.81249999999999));
#373082=CARTESIAN_POINT('Ctrl Pts',(-0.0679352573890632,-1.49999999999999,
1.80923146340491));
#373083=CARTESIAN_POINT('Ctrl Pts',(-0.13593055666763,-1.49538533503665,
1.80583185290518));
#373084=CARTESIAN_POINT('Ctrl Pts',(-0.394898614181489,-1.45992007408125,
1.7923871002911));
#373085=CARTESIAN_POINT('Ctrl Pts',(-0.579400643834895,-1.39699345401102,
1.78176228058195));
#373086=CARTESIAN_POINT('Ctrl Pts',(-0.92103628833535,-1.20084185565978,
1.75987667246243));
#373087=CARTESIAN_POINT('Ctrl Pts',(-1.07337112290149,-1.06687452860672,
1.74882614467676));
#373088=CARTESIAN_POINT('Ctrl Pts',(-1.3098763453813,-0.755278781434875,
1.72879184443336));
#373089=CARTESIAN_POINT('Ctrl Pts',(-1.39503524027109,-0.58318558970749,
1.71989919942817));
#373090=CARTESIAN_POINT('Ctrl Pts',(-1.49783729078981,-0.211367390247104,
1.69924263279148));
#373091=CARTESIAN_POINT('Ctrl Pts',(-1.51260439447891,-0.0146384036827817,
1.68831324464902));
#373092=CARTESIAN_POINT('Ctrl Pts',(-1.46547054554408,0.376689140912213,
1.66657282550485));
#373093=CARTESIAN_POINT('Ctrl Pts',(-1.40272058491593,0.567362552788369,
1.6559798581784));
#373094=CARTESIAN_POINT('Ctrl Pts',(-1.21066545730874,0.905826170861375,
1.63717632384101));
#373095=CARTESIAN_POINT('Ctrl Pts',(-1.08603023851022,1.05205660652591,
1.62719452625359));
#373096=CARTESIAN_POINT('Ctrl Pts',(-0.782913804513272,1.29466475481155,
1.6058717147931));
#373097=CARTESIAN_POINT('Ctrl Pts',(-0.605584098510224,1.38650019717125,
1.59478895082509));
#373098=CARTESIAN_POINT('Ctrl Pts',(-0.227706574714818,1.49544911728569,
1.5735819510927));
#373099=CARTESIAN_POINT('Ctrl Pts',(-0.0311225690518228,1.51236222680461,
1.56434078049065));
#373100=CARTESIAN_POINT('Ctrl Pts',(0.354688511733669,1.47013891344908,
1.54460556639624));
#373101=CARTESIAN_POINT('Ctrl Pts',(0.540347704282607,1.41248683200107,
1.53407158762304));
#373102=CARTESIAN_POINT('Ctrl Pts',(0.886385588657729,1.22654525458887,
1.51225778833156));
#373103=CARTESIAN_POINT('Ctrl Pts',(1.04203298693861,1.09739470579444,1.50118168414592));
#373104=CARTESIAN_POINT('Ctrl Pts',(1.28752949502232,0.792903459705068,
1.48091213772451));
#373105=CARTESIAN_POINT('Ctrl Pts',(1.37785847669754,0.622845987199162,
1.47210255484438));
#373106=CARTESIAN_POINT('Ctrl Pts',(1.49111190625469,0.254094740726321,
1.45161637448478));
#373107=CARTESIAN_POINT('Ctrl Pts',(1.51147456813654,0.0584358280814496,
1.44074643489339));
#373108=CARTESIAN_POINT('Ctrl Pts',(1.47588274641145,-0.333593357307579,
1.41896703570512));
#373109=CARTESIAN_POINT('Ctrl Pts',(1.41873210864635,-0.526059065733415,
1.40827449634813));
#373110=CARTESIAN_POINT('Ctrl Pts',(1.23680525040245,-0.869720120377004,
1.38918221553459));
#373111=CARTESIAN_POINT('Ctrl Pts',(1.11679411652883,-1.01926735639925,
1.37958546652839));
#373112=CARTESIAN_POINT('Ctrl Pts',(0.821845392338527,-1.27021444053289,
1.35842398708231));
#373113=CARTESIAN_POINT('Ctrl Pts',(0.647947697679443,-1.36712826231966,
1.34736527974188));
#373114=CARTESIAN_POINT('Ctrl Pts',(0.311311645264392,-1.47566491337257,
1.32815396314479));
#373115=CARTESIAN_POINT('Ctrl Pts',(0.156016598079475,-1.50000000000002,
1.32000635207494));
#373116=CARTESIAN_POINT('Ctrl Pts',(-2.21801743638395E-13,-1.49999999999999,
1.31249999999999));
#373117=CARTESIAN_POINT('Origin',(0.,2.04523456705693E-15,3.99999999999998));
#373118=CARTESIAN_POINT('',(-6.21175810866611E-14,-1.5,0.749999999999995));
#373119=CARTESIAN_POINT('',(-1.77250281061063E-16,-1.5,0.812500000000001));
#373120=CARTESIAN_POINT('',(-1.83697019872103E-16,-1.5,3.99999999999998));
#373121=CARTESIAN_POINT('Ctrl Pts',(-1.26981758441502E-13,-1.5,0.749999999999995));
#373122=CARTESIAN_POINT('Ctrl Pts',(0.173384566787578,-1.50000000000001,
0.758341968859011));
#373123=CARTESIAN_POINT('Ctrl Pts',(0.345657063026003,-1.4699430379504,
0.767465348811296));
#373124=CARTESIAN_POINT('Ctrl Pts',(0.693992244817146,-1.34424321965294,
0.787716294678613));
#373125=CARTESIAN_POINT('Ctrl Pts',(0.863938649032978,-1.24186420207643,
0.798736706463112));
#373126=CARTESIAN_POINT('Ctrl Pts',(1.14981628665739,-0.981834134196356,
0.81971405815737));
#373127=CARTESIAN_POINT('Ctrl Pts',(1.26474494903649,-0.828538224367302,
0.828970098646288));
#373128=CARTESIAN_POINT('Ctrl Pts',(1.43525308335351,-0.479166451138578,
0.84837964160344));
#373129=CARTESIAN_POINT('Ctrl Pts',(1.48605755906629,-0.284890893244485,
0.859172728153113));
#373130=CARTESIAN_POINT('Ctrl Pts',(1.5086978727434,0.107518734382283,0.880973263021266));
#373131=CARTESIAN_POINT('Ctrl Pts',(1.48211426808514,0.301791556356168,
0.891766197575371));
#373132=CARTESIAN_POINT('Ctrl Pts',(1.35715289650818,0.667005850024354,
0.912055880556936));
#373133=CARTESIAN_POINT('Ctrl Pts',(1.26089428601025,0.83480906539487,0.920857669418136));
#373134=CARTESIAN_POINT('Ctrl Pts',(1.00523551024145,1.13107944512606,0.941387790772681));
#373135=CARTESIAN_POINT('Ctrl Pts',(0.84598771678392,1.25464405070159,0.952481953962604));
#373136=CARTESIAN_POINT('Ctrl Pts',(0.495289357898476,1.42882999593108,
0.974193435100107));
#373137=CARTESIAN_POINT('Ctrl Pts',(0.308491280707698,1.48044575440365,
0.984614532847973));
#373138=CARTESIAN_POINT('Ctrl Pts',(-0.0797322763589896,1.51082443319568,
1.00413679963482));
#373139=CARTESIAN_POINT('Ctrl Pts',(-0.27760059194994,1.48724731902885,
1.01371030584558));
#373140=CARTESIAN_POINT('Ctrl Pts',(-0.652645548149537,1.3648820972632,
1.03515369865185));
#373141=CARTESIAN_POINT('Ctrl Pts',(-0.826150819576611,1.2674080418253,
1.04620908756659));
#373142=CARTESIAN_POINT('Ctrl Pts',(-1.12018365389917,1.01553559153652,
1.06735220585628));
#373143=CARTESIAN_POINT('Ctrl Pts',(-1.23967930040037,0.865613174862536,
1.07691037917434));
#373144=CARTESIAN_POINT('Ctrl Pts',(-1.42046156818003,0.521372499608716,
1.09603486113288));
#373145=CARTESIAN_POINT('Ctrl Pts',(-1.47697743270121,0.328715277685212,
1.10673804012863));
#373146=CARTESIAN_POINT('Ctrl Pts',(-1.51126764366641,-0.0633715758174975,
1.128520643101));
#373147=CARTESIAN_POINT('Ctrl Pts',(-1.49027702721395,-0.258900036336387,
1.13938333535205));
#373148=CARTESIAN_POINT('Ctrl Pts',(-1.37584643246876,-0.62730047372594,
1.15985002631814));
#373149=CARTESIAN_POINT('Ctrl Pts',(-1.28492805400909,-0.797130166849572,
1.16865470814546));
#373150=CARTESIAN_POINT('Ctrl Pts',(-1.03841395698962,-1.10080759809765,
1.18895060736956));
#373151=CARTESIAN_POINT('Ctrl Pts',(-0.882399037793513,-1.22940552156971,
1.20002904321007));
#373152=CARTESIAN_POINT('Ctrl Pts',(-0.535879186602947,-1.41418011314842,
1.22183361486762));
#373153=CARTESIAN_POINT('Ctrl Pts',(-0.350097780224434,-1.47123122899152,
1.23235678016741));
#373154=CARTESIAN_POINT('Ctrl Pts',(-0.105814197624947,-1.49720410709341,
1.24483134835127));
#373155=CARTESIAN_POINT('Ctrl Pts',(-0.0528780712322903,-1.49999999999999,
1.24745590261165));
#373156=CARTESIAN_POINT('Ctrl Pts',(-2.17019340709635E-13,-1.5,1.24999999999999));
#373157=CARTESIAN_POINT('Ctrl Pts',(-2.16984549985882E-13,-1.5,1.31249999999999));
#373158=CARTESIAN_POINT('Ctrl Pts',(-0.0405322108119921,-1.49999999999999,
1.31054989309807));
#373159=CARTESIAN_POINT('Ctrl Pts',(-0.0811087443154879,-1.49835720581244,
1.30855202054776));
#373160=CARTESIAN_POINT('Ctrl Pts',(-0.313115738324047,-1.47948217772521,
1.29686527250828));
#373161=CARTESIAN_POINT('Ctrl Pts',(-0.499808848192362,-1.4272632921762,
1.28643247147317));
#373162=CARTESIAN_POINT('Ctrl Pts',(-0.850059522106373,-1.25189938256099,
1.26470980835596));
#373163=CARTESIAN_POINT('Ctrl Pts',(-1.00895664386298,-1.1277731486574,
1.25361691607922));
#373164=CARTESIAN_POINT('Ctrl Pts',(-1.26360571809193,-0.83067644960973,
1.23311242069832));
#373165=CARTESIAN_POINT('Ctrl Pts',(-1.35927065028476,-0.662651140882278,
1.22431395227122));
#373166=CARTESIAN_POINT('Ctrl Pts',(-1.48307334863835,-0.297082086435002,
1.20400456035748));
#373167=CARTESIAN_POINT('Ctrl Pts',(-1.50904390700285,-0.102663343036432,
1.19320351905756));
#373168=CARTESIAN_POINT('Ctrl Pts',(-1.48512163304604,0.289727796531464,
1.17140401130379));
#373169=CARTESIAN_POINT('Ctrl Pts',(-1.43368604030662,0.483833715114844,
1.16062034916027));
#373170=CARTESIAN_POINT('Ctrl Pts',(-1.26204439514748,0.832645785094674,
1.14124190082806));
#373171=CARTESIAN_POINT('Ctrl Pts',(-1.14661700524226,0.985568902270797,
1.13195638910085));
#373172=CARTESIAN_POINT('Ctrl Pts',(-0.859845498615502,1.24471185801849,
1.11096067311784));
#373173=CARTESIAN_POINT('Ctrl Pts',(-0.6895034643601,1.34656063150023,1.09993595557682));
#373174=CARTESIAN_POINT('Ctrl Pts',(-0.316872979842725,1.47960511561658,
1.07831208291712));
#373175=CARTESIAN_POINT('Ctrl Pts',(-0.117955001656985,1.50854144107688,
1.06841237491536));
#373176=CARTESIAN_POINT('Ctrl Pts',(0.272102436470558,1.48750490166672,
1.04906137935655));
#373177=CARTESIAN_POINT('Ctrl Pts',(0.459657314220201,1.44062637172882,
1.03873545970634));
#373178=CARTESIAN_POINT('Ctrl Pts',(0.81373421671715,1.27571866671084,1.0171191572083));
#373179=CARTESIAN_POINT('Ctrl Pts',(0.975666881366397,1.15659220468503,
1.00601909985821));
#373180=CARTESIAN_POINT('Ctrl Pts',(1.23921847007258,0.866851603428119,
0.985290618099559));
#373181=CARTESIAN_POINT('Ctrl Pts',(1.34014951631224,0.700779301288413,
0.976432183404897));
#373182=CARTESIAN_POINT('Ctrl Pts',(1.47413432584509,0.338358760845283,
0.956297708935835));
#373183=CARTESIAN_POINT('Ctrl Pts',(1.50546906377203,0.145287134359055,
0.945571507464378));
#373184=CARTESIAN_POINT('Ctrl Pts',(1.49280633965443,-0.247122392043873,
0.923770978219772));
#373185=CARTESIAN_POINT('Ctrl Pts',(1.446936108067,-0.442646750903302,0.912908513838693));
#373186=CARTESIAN_POINT('Ctrl Pts',(1.28528021777334,-0.796334054501323,
0.89325921919436));
#373187=CARTESIAN_POINT('Ctrl Pts',(1.17420552689302,-0.952547821731117,
0.884200994704871));
#373188=CARTESIAN_POINT('Ctrl Pts',(0.895258274487633,-1.2193995977598,
0.863367589431912));
#373189=CARTESIAN_POINT('Ctrl Pts',(0.728423672339838,-1.32582725035303,
0.85238443221042));
#373190=CARTESIAN_POINT('Ctrl Pts',(0.371751064568077,-1.46517581908719,
0.831353219792006));
#373191=CARTESIAN_POINT('Ctrl Pts',(0.186619235362833,-1.5,0.821478722147725));
#373192=CARTESIAN_POINT('Ctrl Pts',(-1.04083408558608E-16,-1.5,0.812500000000001));
#373193=CARTESIAN_POINT('Origin',(0.,2.04523456705693E-15,3.99999999999998));
#373194=CARTESIAN_POINT('',(-4.50788613606587E-8,-1.49999999999999,0.249999995662285));
#373195=CARTESIAN_POINT('',(1.52431070176988E-14,-1.5,0.312500000000002));
#373196=CARTESIAN_POINT('',(-1.83697019872103E-16,-1.5,3.99999999999998));
#373197=CARTESIAN_POINT('Ctrl Pts',(-4.51837430147789E-8,-1.49999999999999,
0.249999997826096));
#373198=CARTESIAN_POINT('Ctrl Pts',(0.00348282355345849,-1.50000000010491,
0.250167567429258));
#373199=CARTESIAN_POINT('Ctrl Pts',(0.00696619430317118,-1.49998786983704,
0.250335498128669));
#373200=CARTESIAN_POINT('Ctrl Pts',(0.209254267662016,-1.49857856147727,
0.260107235050405));
#373201=CARTESIAN_POINT('Ctrl Pts',(0.405777232132074,-1.45768418329109,
0.270698405536583));
#373202=CARTESIAN_POINT('Ctrl Pts',(0.768330064713747,-1.30301918211526,
0.292437986859785));
#373203=CARTESIAN_POINT('Ctrl Pts',(0.931381977277525,-1.19194128837559,
0.303368322708991));
#373204=CARTESIAN_POINT('Ctrl Pts',(1.20212022338398,-0.917133022467638,
0.324027785590003));
#373205=CARTESIAN_POINT('Ctrl Pts',(1.30865255207445,-0.757395376448475,
0.332922479086215));
#373206=CARTESIAN_POINT('Ctrl Pts',(1.46043143136339,-0.396851323959125,
0.352952704224513));
#373207=CARTESIAN_POINT('Ctrl Pts',(1.50038276079889,-0.197951118063682,
0.364002715663149));
#373208=CARTESIAN_POINT('Ctrl Pts',(1.49962649441611,0.196009289988444,
0.385889404999379));
#373209=CARTESIAN_POINT('Ctrl Pts',(1.46195998285909,0.387282791440873,
0.396515710635625));
#373210=CARTESIAN_POINT('Ctrl Pts',(1.31581458969238,0.745840837156813,
0.416435602064289));
#373211=CARTESIAN_POINT('Ctrl Pts',(1.20843055145291,0.909586471241854,
0.425458982186326));
#373212=CARTESIAN_POINT('Ctrl Pts',(0.934170098346782,1.19024237788855,
0.446450341795587));
#373213=CARTESIAN_POINT('Ctrl Pts',(0.768757015230046,1.3032101208217,0.457546775326919));
#373214=CARTESIAN_POINT('Ctrl Pts',(0.410444839870971,1.45532904822187,
0.479011603662826));
#373215=CARTESIAN_POINT('Ctrl Pts',(0.222046611647017,1.49571599277423,
0.489197777215388));
#373216=CARTESIAN_POINT('Ctrl Pts',(-0.167599313780493,1.50379997668454,
0.508169180651858));
#373217=CARTESIAN_POINT('Ctrl Pts',(-0.365223633275425,1.46838801912668,
0.518449940828671));
#373218=CARTESIAN_POINT('Ctrl Pts',(-0.732524358587354,1.32355716682777,
0.540144784445228));
#373219=CARTESIAN_POINT('Ctrl Pts',(-0.89897911089993,1.21664955586623,
0.551122998309901));
#373220=CARTESIAN_POINT('Ctrl Pts',(-1.1770918951988,0.948982970424738,
0.571938888812166));
#373221=CARTESIAN_POINT('Ctrl Pts',(-1.28770388209791,0.792414448668057,
0.580976975074022));
#373222=CARTESIAN_POINT('Ctrl Pts',(-1.44828613126506,0.438210499638932,
0.600654972242306));
#373223=CARTESIAN_POINT('Ctrl Pts',(-1.49355746160076,0.242543837284878,
0.611525342373087));
#373224=CARTESIAN_POINT('Ctrl Pts',(-1.50501452892094,-0.149848383426528,
0.633324910190388));
#373225=CARTESIAN_POINT('Ctrl Pts',(-1.47310810476986,-0.34276700151942,
0.644042611195548));
#373226=CARTESIAN_POINT('Ctrl Pts',(-1.33803206466294,-0.704845530579388,
0.664158085032213));
#373227=CARTESIAN_POINT('Ctrl Pts',(-1.23652944619448,-0.870708896224865,
0.673027140843388));
#373228=CARTESIAN_POINT('Ctrl Pts',(-0.972020111275437,-1.15964785062779,
0.693779434220025));
#373229=CARTESIAN_POINT('Ctrl Pts',(-0.809768461712522,-1.27822989206776,
0.704879715944881));
#373230=CARTESIAN_POINT('Ctrl Pts',(-0.455296254992094,-1.44200309956987,
0.726483523706352));
#373231=CARTESIAN_POINT('Ctrl Pts',(-0.267657278756777,-1.48830399007212,
0.736797444006965));
#373232=CARTESIAN_POINT('Ctrl Pts',(-0.0509015997152728,-1.4993528318024,
0.747533018747499));
#373233=CARTESIAN_POINT('Ctrl Pts',(-0.0254396825847984,-1.49999999999999,
0.748776032700964));
#373234=CARTESIAN_POINT('Ctrl Pts',(-1.2405146515345E-13,-1.5,0.749999999999995));
#373235=CARTESIAN_POINT('Ctrl Pts',(-1.70803542250024E-16,-1.5,0.812500000000001));
#373236=CARTESIAN_POINT('Ctrl Pts',(-0.0119425753744356,-1.5,0.811925412574397));
#373237=CARTESIAN_POINT('Ctrl Pts',(-0.0238908671823992,-1.49985737526137,
0.81134658831845));
#373238=CARTESIAN_POINT('Ctrl Pts',(-0.226821223276692,-1.49500698913326,
0.801448364060632));
#373239=CARTESIAN_POINT('Ctrl Pts',(-0.415148767636273,-1.45400207372324,
0.791248425429924));
#373240=CARTESIAN_POINT('Ctrl Pts',(-0.773077310249116,-1.30066201483827,
0.769768134314104));
#373241=CARTESIAN_POINT('Ctrl Pts',(-0.938168916315346,-1.187104171216,
0.758670776168768));
#373242=CARTESIAN_POINT('Ctrl Pts',(-1.21141488703134,-0.905575960850558,
0.737703995207406));
#373243=CARTESIAN_POINT('Ctrl Pts',(-1.31818157918045,-0.741610570018196,
0.728700587223223));
#373244=CARTESIAN_POINT('Ctrl Pts',(-1.46317859948516,-0.382682975762146,
0.70876016532011));
#373245=CARTESIAN_POINT('Ctrl Pts',(-1.50025101871615,-0.191231002705516,
0.698123944594742));
#373246=CARTESIAN_POINT('Ctrl Pts',(-1.49973635554699,0.202857738527839,
0.676230125637334));
#373247=CARTESIAN_POINT('Ctrl Pts',(-1.45911625076073,0.401694321978298,
0.665183648778974));
#373248=CARTESIAN_POINT('Ctrl Pts',(-1.30611837209093,0.761745197464029,
0.6451808223631));
#373249=CARTESIAN_POINT('Ctrl Pts',(-1.19908428845553,0.921089090541452,
0.636271828322799));
#373250=CARTESIAN_POINT('Ctrl Pts',(-0.92743766004034,1.19502329549003,
0.615592940348674));
#373251=CARTESIAN_POINT('Ctrl Pts',(-0.763962245148437,1.30559446577423,
0.604656304385748));
#373252=CARTESIAN_POINT('Ctrl Pts',(-0.400831821334879,1.45905114337201,
0.582922498235279));
#373253=CARTESIAN_POINT('Ctrl Pts',(-0.204176053948586,1.4992783205916,
0.572343471625999));
#373254=CARTESIAN_POINT('Ctrl Pts',(0.18503638089729,1.50067236949698,0.553578756042776));
#373255=CARTESIAN_POINT('Ctrl Pts',(0.373923463154697,1.46509146512387,
0.543539917466597));
#373256=CARTESIAN_POINT('Ctrl Pts',(0.735156364550241,1.32237962218791,
0.522195873535526));
#373257=CARTESIAN_POINT('Ctrl Pts',(0.902980093128755,1.21399098351906,
0.511110655111013));
#373258=CARTESIAN_POINT('Ctrl Pts',(1.18503413357111,0.940122108026969,
0.489932854999392));
#373259=CARTESIAN_POINT('Ctrl Pts',(1.29720572931344,0.778063845741863,
0.480725769207872));
#373260=CARTESIAN_POINT('Ctrl Pts',(1.45215110685594,0.42237084518817,0.460965046954891));
#373261=CARTESIAN_POINT('Ctrl Pts',(1.49434106495004,0.232523854121758,
0.450417991895646));
#373262=CARTESIAN_POINT('Ctrl Pts',(1.50479969486777,-0.16032215158135,
0.42859321380103));
#373263=CARTESIAN_POINT('Ctrl Pts',(1.46996649084184,-0.3596378809732,0.417520117723705));
#373264=CARTESIAN_POINT('Ctrl Pts',(1.3275358794875,-0.723908254097641,
0.397282874772348));
#373265=CARTESIAN_POINT('Ctrl Pts',(1.22482468313652,-0.886680660751951,
0.388466053355688));
#373266=CARTESIAN_POINT('Ctrl Pts',(0.96101225989259,-1.16810260828488,
0.367956095904041));
#373267=CARTESIAN_POINT('Ctrl Pts',(0.801227349234453,-1.28297879352365,
0.35707743566011));
#373268=CARTESIAN_POINT('Ctrl Pts',(0.443193904486032,-1.44675205425625,
0.335302286275506));
#373269=CARTESIAN_POINT('Ctrl Pts',(0.247755919662054,-1.49270029722171,
0.324622931764132));
#373270=CARTESIAN_POINT('Ctrl Pts',(0.0326763919887163,-1.49973322184082,
0.314079554146987));
#373271=CARTESIAN_POINT('Ctrl Pts',(0.0163333853167089,-1.5,0.313285840367448));
#373272=CARTESIAN_POINT('Ctrl Pts',(3.06699110552697E-14,-1.5,0.312500000000002));
#373273=CARTESIAN_POINT('Origin',(0.,2.04523456705693E-15,3.99999999999998));
#373274=CARTESIAN_POINT('',(7.73382353572088E-14,-1.5,-0.249999999999993));
#373275=CARTESIAN_POINT('',(1.08229622940747E-13,-1.5,-0.18749999999999));
#373276=CARTESIAN_POINT('',(-1.83697019872103E-16,-1.5,3.99999999999998));
#373277=CARTESIAN_POINT('Ctrl Pts',(1.5486016773429E-13,-1.5,-0.249999999999993));
#373278=CARTESIAN_POINT('Ctrl Pts',(0.032860455885365,-1.5,-0.248419000579072));
#373279=CARTESIAN_POINT('Ctrl Pts',(0.0657519915310822,-1.49892021763245,
-0.246806511877816));
#373280=CARTESIAN_POINT('Ctrl Pts',(0.297065083808075,-1.48367883097131,
-0.235254083685017));
#373281=CARTESIAN_POINT('Ctrl Pts',(0.490910090902343,-1.43127059459545,
-0.224471927088997));
#373282=CARTESIAN_POINT('Ctrl Pts',(0.842790719159963,-1.25597008082433,
-0.202672603752536));
#373283=CARTESIAN_POINT('Ctrl Pts',(0.998245550468655,-1.13634232069776,
-0.191870286357112));
#373284=CARTESIAN_POINT('Ctrl Pts',(1.25307683006948,-0.846472584804176,
-0.171557773592667));
#373285=CARTESIAN_POINT('Ctrl Pts',(1.35083608504267,-0.679675474119084,
-0.162759748562156));
#373286=CARTESIAN_POINT('Ctrl Pts',(1.48099815554993,-0.310667784306506,
-0.142259321350346));
#373287=CARTESIAN_POINT('Ctrl Pts',(1.50915093165956,-0.110999542458538,
-0.131166641247681));
#373288=CARTESIAN_POINT('Ctrl Pts',(1.48609240045633,0.280039930965759,
-0.109442226057442));
#373289=CARTESIAN_POINT('Ctrl Pts',(1.43805988182893,0.467863568677401,
-0.0990075795179057));
#373290=CARTESIAN_POINT('Ctrl Pts',(1.2715841280139,0.819713330899575,-0.0794603705055627));
#373291=CARTESIAN_POINT('Ctrl Pts',(1.15298332135301,0.979542414678213,
-0.069930091060669));
#373292=CARTESIAN_POINT('Ctrl Pts',(0.860672783550812,1.24423569732698,
-0.0485137025687251));
#373293=CARTESIAN_POINT('Ctrl Pts',(0.689840047383048,1.34647667691424,
-0.0374544815068962));
#373294=CARTESIAN_POINT('Ctrl Pts',(0.325093633437915,1.47663503667349,
-0.0162901014904864));
#373295=CARTESIAN_POINT('Ctrl Pts',(0.135586908706809,1.50589444815122,
-0.00668716285755389));
#373296=CARTESIAN_POINT('Ctrl Pts',(-0.253006716819572,1.49181979884168,
0.0124000191485191));
#373297=CARTESIAN_POINT('Ctrl Pts',(-0.44828599000737,1.44518296954627,
0.0230908650407911));
#373298=CARTESIAN_POINT('Ctrl Pts',(-0.805683809008424,1.28017481456344,
0.0448697354854288));
#373299=CARTESIAN_POINT('Ctrl Pts',(-0.965015455486543,1.1647865999199,
0.0557408110853518));
#373300=CARTESIAN_POINT('Ctrl Pts',(-1.22787773770585,0.88246416929183,
0.076230068274947));
#373301=CARTESIAN_POINT('Ctrl Pts',(-1.33006509885902,0.71927082538992,
0.0850405097005798));
#373302=CARTESIAN_POINT('Ctrl Pts',(-1.47120566569572,0.354494062141217,
0.105305885436618));
#373303=CARTESIAN_POINT('Ctrl Pts',(-1.50533426870155,0.155131010997178,
0.116381610500176));
#373304=CARTESIAN_POINT('Ctrl Pts',(-1.49354326838503,-0.23754326002992,
0.138196847779459));
#373305=CARTESIAN_POINT('Ctrl Pts',(-1.45073378385078,-0.427185465663105,
0.148732525870191));
#373306=CARTESIAN_POINT('Ctrl Pts',(-1.29457497008243,-0.782478789741982,
0.168471043874573));
#373307=CARTESIAN_POINT('Ctrl Pts',(-1.18173521246989,-0.944303668118952,
0.177707728861905));
#373308=CARTESIAN_POINT('Ctrl Pts',(-0.898603989372673,-1.21722222304294,
0.198910957154612));
#373309=CARTESIAN_POINT('Ctrl Pts',(-0.730455409049272,-1.32497165006399,
0.209994049136883));
#373310=CARTESIAN_POINT('Ctrl Pts',(-0.37209496343298,-1.46509978331248,
0.231128122261297));
#373311=CARTESIAN_POINT('Ctrl Pts',(-0.186815895788635,-1.49999999437264,
0.241011815866812));
#373312=CARTESIAN_POINT('Ctrl Pts',(-4.5183745252253E-8,-1.49999999999999,
0.249999997826096));
#373313=CARTESIAN_POINT('Ctrl Pts',(3.2682190287403E-14,-1.5,0.312500000000002));
#373314=CARTESIAN_POINT('Ctrl Pts',(-0.173451403441322,-1.5,0.304154815460988));
#373315=CARTESIAN_POINT('Ctrl Pts',(-0.345738678826419,-1.46991848495802,
0.295030042419132));
#373316=CARTESIAN_POINT('Ctrl Pts',(-0.694724820475537,-1.34397330137361,
0.274740961528629));
#373317=CARTESIAN_POINT('Ctrl Pts',(-0.865246151889541,-1.24107115352004,
0.263678357149826));
#373318=CARTESIAN_POINT('Ctrl Pts',(-1.15646444213004,-0.975386913975008,
0.242286992862745));
#373319=CARTESIAN_POINT('Ctrl Pts',(-1.27437325899852,-0.815319430751239,
0.23279552393062));
#373320=CARTESIAN_POINT('Ctrl Pts',(-1.43962337775053,-0.463056308150473,
0.2132253504528));
#373321=CARTESIAN_POINT('Ctrl Pts',(-1.48703970257091,-0.275009459948132,
0.202778303330447));
#373322=CARTESIAN_POINT('Ctrl Pts',(-1.50876566366178,0.116240468830023,
0.181042196176105));
#373323=CARTESIAN_POINT('Ctrl Pts',(-1.47990453460223,0.315881524199714,
0.169951026433344));
#373324=CARTESIAN_POINT('Ctrl Pts',(-1.34843726471597,0.684393653585345,
0.149478130356364));
#373325=CARTESIAN_POINT('Ctrl Pts',(-1.2501541581696,0.850760295813159,
0.140682506206385));
#373326=CARTESIAN_POINT('Ctrl Pts',(-0.994373222012351,1.13974345531941,
0.120348930191437));
#373327=CARTESIAN_POINT('Ctrl Pts',(-0.838455863131078,1.25887818084316,
0.109538054833435));
#373328=CARTESIAN_POINT('Ctrl Pts',(-0.485909638788608,1.43297539889288,
0.0877401328715617));
#373329=CARTESIAN_POINT('Ctrl Pts',(-0.291886496354003,1.48470586992773,
0.0769682325500131));
#373330=CARTESIAN_POINT('Ctrl Pts',(0.0961134619130744,1.50891295317755,
0.0576281568749298));
#373331=CARTESIAN_POINT('Ctrl Pts',(0.286173113423018,1.48464949424262,
0.0483050867231545));
#373332=CARTESIAN_POINT('Ctrl Pts',(0.653585225433785,1.3643677539121,0.0272868037884504));
#373333=CARTESIAN_POINT('Ctrl Pts',(0.826634636240301,1.2670229746827,0.0162569384838358));
#373334=CARTESIAN_POINT('Ctrl Pts',(1.12695650359022,1.0097041504712,-0.00534004921298362));
#373335=CARTESIAN_POINT('Ctrl Pts',(1.25068904169858,0.851635471447732,
-0.0151869182529077));
#373336=CARTESIAN_POINT('Ctrl Pts',(1.4261416971664,0.502848746380216,-0.034563958534436));
#373337=CARTESIAN_POINT('Ctrl Pts',(1.4786500184448,0.316717507606887,-0.0449045829107318));
#373338=CARTESIAN_POINT('Ctrl Pts',(1.51141470029083,-0.0726489674713217,
-0.0665360537484097));
#373339=CARTESIAN_POINT('Ctrl Pts',(1.48843464297174,-0.27244234664173,
-0.0776356859245436));
#373340=CARTESIAN_POINT('Ctrl Pts',(1.3678393689196,-0.645023521480528,
-0.0983346400822544));
#373341=CARTESIAN_POINT('Ctrl Pts',(1.27390529358518,-0.814986953888903,
-0.107181062815792));
#373342=CARTESIAN_POINT('Ctrl Pts',(1.02599149417605,-1.11127283481478,
-0.127338984410234));
#373343=CARTESIAN_POINT('Ctrl Pts',(0.873937684757876,-1.2344253143386,
-0.138075578935803));
#373344=CARTESIAN_POINT('Ctrl Pts',(0.52700932844199,-1.41837933893976,
-0.159877011278209));
#373345=CARTESIAN_POINT('Ctrl Pts',(0.334529625819275,-1.47568594816069,
-0.170729545544577));
#373346=CARTESIAN_POINT('Ctrl Pts',(0.0910182157037006,-1.49793118858919,
-0.183063417071561));
#373347=CARTESIAN_POINT('Ctrl Pts',(0.0454853740099916,-1.5,-0.185311583922599));
#373348=CARTESIAN_POINT('Ctrl Pts',(2.16642942901365E-13,-1.5,-0.18749999999999));
#373349=CARTESIAN_POINT('Origin',(0.,2.04523456705693E-15,3.99999999999998));
#373350=CARTESIAN_POINT('',(7.73382353572088E-14,-1.5,-0.749999999999992));
#373351=CARTESIAN_POINT('',(3.08182550266226E-14,-1.5,-0.687499999999998));
#373352=CARTESIAN_POINT('',(-1.83697019872103E-16,-1.5,3.99999999999998));
#373353=CARTESIAN_POINT('Ctrl Pts',(1.5486016773429E-13,-1.5,-0.749999999999992));
#373354=CARTESIAN_POINT('Ctrl Pts',(0.0605270531518406,-1.5,-0.747087890797456));
#373355=CARTESIAN_POINT('Ctrl Pts',(0.121111815912754,-1.49633682152687,
-0.744071250082467));
#373356=CARTESIAN_POINT('Ctrl Pts',(0.380907005258931,-1.46468181567999,
-0.730692542489233));
#373357=CARTESIAN_POINT('Ctrl Pts',(0.573458929788626,-1.40053904367085,
-0.719646640033961));
#373358=CARTESIAN_POINT('Ctrl Pts',(0.915125828010041,-1.20410581994117,
-0.697751705291916));
#373359=CARTESIAN_POINT('Ctrl Pts',(1.06246375204514,-1.07634209434518,
-0.687113913738957));
#373360=CARTESIAN_POINT('Ctrl Pts',(1.30094807582981,-0.771436277330007,
-0.667170225332875));
#373361=CARTESIAN_POINT('Ctrl Pts',(1.38964235735141,-0.59705846915719,
-0.658169914953168));
#373362=CARTESIAN_POINT('Ctrl Pts',(1.49703089523062,-0.219727003413118,
-0.637207055745163));
#373363=CARTESIAN_POINT('Ctrl Pts',(1.51293605277923,-0.0199721092192588,
-0.626109561623282));
#373364=CARTESIAN_POINT('Ctrl Pts',(1.46696719957355,0.366717079076811,
-0.604626828940168));
#373365=CARTESIAN_POINT('Ctrl Pts',(1.40840564943819,0.550355260220075,
-0.594424707765542));
#373366=CARTESIAN_POINT('Ctrl Pts',(1.22179400429212,0.89259639043274,-0.575411311642616));
#373367=CARTESIAN_POINT('Ctrl Pts',(1.09286815607941,1.0465149197047,-0.565177451461071));
#373368=CARTESIAN_POINT('Ctrl Pts',(0.784626975107821,1.29336119748035,
-0.543490349677642));
#373369=CARTESIAN_POINT('Ctrl Pts',(0.609076727214449,1.38472090647381,
-0.532506414743584));
#373370=CARTESIAN_POINT('Ctrl Pts',(0.238548693852844,1.4930503343714,-0.511670225651682));
#373371=CARTESIAN_POINT('Ctrl Pts',(0.0477382601695704,1.51122894014668,
-0.502608723117359));
#373372=CARTESIAN_POINT('Ctrl Pts',(-0.339405970527289,1.47457237426477,
-0.482963999692192));
#373373=CARTESIAN_POINT('Ctrl Pts',(-0.531698004873539,1.41662884683185,
-0.472102802447431));
#373374=CARTESIAN_POINT('Ctrl Pts',(-0.877963968207817,1.23155521756417,
-0.450302139372585));
#373375=CARTESIAN_POINT('Ctrl Pts',(-1.02956797170921,1.10794943345765,
-0.439574594350313));
#373376=CARTESIAN_POINT('Ctrl Pts',(-1.27657478448722,0.810828070813583,
-0.419437102345001));
#373377=CARTESIAN_POINT('Ctrl Pts',(-1.37000627001517,0.640445066970175,
-0.410580281498331));
#373378=CARTESIAN_POINT('Ctrl Pts',(-1.48933954887378,0.267400636282404,
-0.389855590904567));
#373379=CARTESIAN_POINT('Ctrl Pts',(-1.51164004661096,0.0676004233373413,
-0.378755579074287));
#373380=CARTESIAN_POINT('Ctrl Pts',(-1.4776034925801,-0.321528438969358,
-0.357137308946137));
#373381=CARTESIAN_POINT('Ctrl Pts',(-1.42451030310986,-0.507429171138638,
-0.346809490492288));
#373382=CARTESIAN_POINT('Ctrl Pts',(-1.24787445641846,-0.855807485190914,
-0.327455139711605));
#373383=CARTESIAN_POINT('Ctrl Pts',(-1.12345714577022,-1.01364197081179,
-0.317562302383004));
#373384=CARTESIAN_POINT('Ctrl Pts',(-0.822078108419088,-1.2699733049106,
-0.295941881851693));
#373385=CARTESIAN_POINT('Ctrl Pts',(-0.648745156586937,-1.36666587614998,
-0.284916491561733));
#373386=CARTESIAN_POINT('Ctrl Pts',(-0.312337813768908,-1.4754965967708,
-0.265708010161154));
#373387=CARTESIAN_POINT('Ctrl Pts',(-0.156554135230396,-1.5,-0.257532214343177));
#373388=CARTESIAN_POINT('Ctrl Pts',(1.55014889813287E-13,-1.5,-0.249999999999993));
#373389=CARTESIAN_POINT('Ctrl Pts',(2.14377127161214E-13,-1.5,-0.18749999999999));
#373390=CARTESIAN_POINT('Ctrl Pts',(-0.143866319824192,-1.5,-0.194421771539806));
#373391=CARTESIAN_POINT('Ctrl Pts',(-0.287202401435548,-1.47930819185578,
-0.201892804430179));
#373392=CARTESIAN_POINT('Ctrl Pts',(-0.613653851873503,-1.38270765947202,
-0.220282555284259));
#373393=CARTESIAN_POINT('Ctrl Pts',(-0.788957812087736,-1.29073374629065,
-0.231271701924271));
#373394=CARTESIAN_POINT('Ctrl Pts',(-1.09791823757522,-1.04158724780001,
-0.253057303395467));
#373395=CARTESIAN_POINT('Ctrl Pts',(-1.22730056572081,-0.885449105131343,
-0.26330838304826));
#373396=CARTESIAN_POINT('Ctrl Pts',(-1.41241538793125,-0.540029980306386,
-0.282498334427425));
#373397=CARTESIAN_POINT('Ctrl Pts',(-1.4696637265307,-0.355830537243378,
-0.292731636819814));
#373398=CARTESIAN_POINT('Ctrl Pts',(-1.51276028827358,0.0314809184981216,
-0.314248939916565));
#373399=CARTESIAN_POINT('Ctrl Pts',(-1.49531235561511,0.231264916379955,
-0.32534805091));
#373400=CARTESIAN_POINT('Ctrl Pts',(-1.38503041627651,0.607574273005967,
-0.346254126278111));
#373401=CARTESIAN_POINT('Ctrl Pts',(-1.29519151853042,0.780980599048122,
-0.355212307872812));
#373402=CARTESIAN_POINT('Ctrl Pts',(-1.05465300357619,1.08402094088197,
-0.375203009842583));
#373403=CARTESIAN_POINT('Ctrl Pts',(-0.906280583038949,1.21079931160738,
-0.38586320266308));
#373404=CARTESIAN_POINT('Ctrl Pts',(-0.56482212083892,1.40375369382997,
-0.407651474536063));
#373405=CARTESIAN_POINT('Ctrl Pts',(-0.373924919213404,1.46620146978531,
-0.41857068087477));
#373406=CARTESIAN_POINT('Ctrl Pts',(0.0125016797145877,1.51196053764197,
-0.438433724502437));
#373407=CARTESIAN_POINT('Ctrl Pts',(0.203910620206974,1.49820204996122,
-0.447360597345563));
#373408=CARTESIAN_POINT('Ctrl Pts',(0.576612990887898,1.39848768859079,
-0.468062091886984));
#373409=CARTESIAN_POINT('Ctrl Pts',(0.753840313387179,1.31147603597659,
-0.479005935766771));
#373410=CARTESIAN_POINT('Ctrl Pts',(1.06750320474121,1.07236929448121,-0.500738902593701));
#373411=CARTESIAN_POINT('Ctrl Pts',(1.20003911969275,0.921619379896505,
-0.511298923339085));
#373412=CARTESIAN_POINT('Ctrl Pts',(1.39455116730487,0.584424044107407,
-0.530031997549591));
#373413=CARTESIAN_POINT('Ctrl Pts',(1.4574360415234,0.402715778033152,-0.540126901220382));
#373414=CARTESIAN_POINT('Ctrl Pts',(1.51289210709091,0.0182420408411633,
-0.561486553286604));
#373415=CARTESIAN_POINT('Ctrl Pts',(1.50209794537431,-0.181333525994842,
-0.572574084777493));
#373416=CARTESIAN_POINT('Ctrl Pts',(1.4043552255257,-0.561995603514428,
-0.593721977973025));
#373417=CARTESIAN_POINT('Ctrl Pts',(1.31946718554587,-0.739628522719427,
-0.602895675512057));
#373418=CARTESIAN_POINT('Ctrl Pts',(1.08778462340069,-1.05066302556747,
-0.622682355281814));
#373419=CARTESIAN_POINT('Ctrl Pts',(0.943897572384442,-1.18161263521891,
-0.63324261340856));
#373420=CARTESIAN_POINT('Ctrl Pts',(0.607960621860351,-1.3858364241278,
-0.655078270501792));
#373421=CARTESIAN_POINT('Ctrl Pts',(0.417568947214438,-1.45458270049018,
-0.666148113006993));
#373422=CARTESIAN_POINT('Ctrl Pts',(0.146526068430488,-1.49463699899561,
-0.680301288995575));
#373423=CARTESIAN_POINT('Ctrl Pts',(0.0732374219065056,-1.5,-0.683976362895629));
#373424=CARTESIAN_POINT('Ctrl Pts',(6.18202070731173E-14,-1.5,-0.687499999999998));
#373425=CARTESIAN_POINT('Origin',(0.,2.04523456705693E-15,3.99999999999998));
#373426=CARTESIAN_POINT('',(-2.29292018146854E-16,-1.5,-1.25));
#373427=CARTESIAN_POINT('',(-1.77250281061063E-16,-1.5,-1.1875));
#373428=CARTESIAN_POINT('',(-1.83697019872103E-16,-1.5,3.99999999999998));
#373429=CARTESIAN_POINT('Ctrl Pts',(-2.74887016421606E-16,-1.5,-1.25));
#373430=CARTESIAN_POINT('Ctrl Pts',(0.0900358162878159,-1.5,-1.24566814976913));
#373431=CARTESIAN_POINT('Ctrl Pts',(0.180082196644308,-1.49189502111387,
-1.24111065297187));
#373432=CARTESIAN_POINT('Ctrl Pts',(0.465578429116048,-1.43984022717801,
-1.22592874258447));
#373433=CARTESIAN_POINT('Ctrl Pts',(0.652956059384571,-1.36511486420352,
-1.21483782761776));
#373434=CARTESIAN_POINT('Ctrl Pts',(0.981061243802619,-1.15084317520299,
-1.19309986821111));
#373435=CARTESIAN_POINT('Ctrl Pts',(1.12028672749574,-1.01582386492302,
-1.18265084260709));
#373436=CARTESIAN_POINT('Ctrl Pts',(1.342886050056,-0.696718611169778,-1.16307699288048));
#373437=CARTESIAN_POINT('Ctrl Pts',(1.42264260296975,-0.514649669801069,
-1.15359164832228));
#373438=CARTESIAN_POINT('Ctrl Pts',(1.5073476097853,-0.129677478171334,
-1.13220430434285));
#373439=CARTESIAN_POINT('Ctrl Pts',(1.5113195465766,0.0694589165068009,
-1.12114117130517));
#373440=CARTESIAN_POINT('Ctrl Pts',(1.44322862617289,0.450825439691474,
-1.09995414223936));
#373441=CARTESIAN_POINT('Ctrl Pts',(1.37453556995427,0.629894589817241,
-1.09030196817094));
#373442=CARTESIAN_POINT('Ctrl Pts',(1.1693792801673,0.960254665911306,-1.07125471279601));
#373443=CARTESIAN_POINT('Ctrl Pts',(1.03195084041089,1.1066117276265,-1.06057720996884));
#373444=CARTESIAN_POINT('Ctrl Pts',(0.711223003369554,1.33497784091084,
-1.03880268156769));
#373445=CARTESIAN_POINT('Ctrl Pts',(0.531879763453132,1.41602128727827,
-1.02792281907056));
#373446=CARTESIAN_POINT('Ctrl Pts',(0.156303877194832,1.50398228927571,
-1.00740955465126));
#373447=CARTESIAN_POINT('Ctrl Pts',(-0.0360004374524879,1.51165277426085,
-0.998591616319393));
#373448=CARTESIAN_POINT('Ctrl Pts',(-0.422715986129613,1.45308522923991,
-0.978358879558099));
#373449=CARTESIAN_POINT('Ctrl Pts',(-0.612794656082124,1.38369525968752,
-0.967286216131843));
#373450=CARTESIAN_POINT('Ctrl Pts',(-0.947909934791437,1.17838584415295,
-0.945459935447073));
#373451=CARTESIAN_POINT('Ctrl Pts',(-1.09130502719597,1.0469943407134,-0.934911071862623));
#373452=CARTESIAN_POINT('Ctrl Pts',(-1.32202372870725,0.735097289813444,
-0.915146806191128));
#373453=CARTESIAN_POINT('Ctrl Pts',(-1.40637010167788,0.556998399808634,
-0.905944355544917));
#373454=CARTESIAN_POINT('Ctrl Pts',(-1.50273781462483,0.175871277265909,
-0.884770626514766));
#373455=CARTESIAN_POINT('Ctrl Pts',(-1.51280764934617,-0.0236685359105637,
-0.873685081338296));
#373456=CARTESIAN_POINT('Ctrl Pts',(-1.45599503486762,-0.407914323054937,
-0.852338093163609));
#373457=CARTESIAN_POINT('Ctrl Pts',(-1.39246163036462,-0.589330217116489,
-0.842291224285139));
#373458=CARTESIAN_POINT('Ctrl Pts',(-1.19682557106127,-0.925814031427701,
-0.823531907373551));
#373459=CARTESIAN_POINT('Ctrl Pts',(-1.06374166172616,-1.07608073639503,
-0.812954829662284));
#373460=CARTESIAN_POINT('Ctrl Pts',(-0.749400300188114,-1.31400853300462,
-0.791221968392454));
#373461=CARTESIAN_POINT('Ctrl Pts',(-0.571941574505609,-1.40039569225495,
-0.780284338159708));
#373462=CARTESIAN_POINT('Ctrl Pts',(-0.257687088986563,-1.48336447077953,
-0.762860073883319));
#373463=CARTESIAN_POINT('Ctrl Pts',(-0.128997012608126,-1.5,-0.756206371662836));
#373464=CARTESIAN_POINT('Ctrl Pts',(1.55639390264639E-13,-1.5,-0.749999999999992));
#373465=CARTESIAN_POINT('Ctrl Pts',(6.50521303491303E-14,-1.5,-0.687499999999997));
#373466=CARTESIAN_POINT('Ctrl Pts',(-0.116639952633668,-1.5,-0.693111842337607));
#373467=CARTESIAN_POINT('Ctrl Pts',(-0.23311324418047,-1.48639868526909,
-0.69909348048802));
#373468=CARTESIAN_POINT('Ctrl Pts',(-0.536820232812539,-1.41416492733363,
-0.715712083067463));
#373469=CARTESIAN_POINT('Ctrl Pts',(-0.715940634650769,-1.332463629502,
-0.72659949791434));
#373470=CARTESIAN_POINT('Ctrl Pts',(-1.03590028118403,-1.10291468377004,
-0.748369923189322));
#373471=CARTESIAN_POINT('Ctrl Pts',(-1.17280179174001,-0.956070753908902,
-0.759035598238684));
#373472=CARTESIAN_POINT('Ctrl Pts',(-1.3767933757908,-0.624954618657059,
-0.778047818326026));
#373473=CARTESIAN_POINT('Ctrl Pts',(-1.44485502153325,-0.445602379258366,
-0.787744312263425));
#373474=CARTESIAN_POINT('Ctrl Pts',(-1.51157510457803,-0.0638798043074548,
-0.808951121982921));
#373475=CARTESIAN_POINT('Ctrl Pts',(-1.50686154990082,0.135315468900849,
-0.820017526050049));
#373476=CARTESIAN_POINT('Ctrl Pts',(-1.42072944177977,0.519826796441412,
-0.841379266468969));
#373477=CARTESIAN_POINT('Ctrl Pts',(-1.34041147848882,0.701408342574253,
-0.850826321066076));
#373478=CARTESIAN_POINT('Ctrl Pts',(-1.11301247659109,1.02506664015431,
-0.870757568913055));
#373479=CARTESIAN_POINT('Ctrl Pts',(-0.967454351703998,1.16343026506801,
-0.881604171497448));
#373480=CARTESIAN_POINT('Ctrl Pts',(-0.635115562016325,1.37266797728933,
-0.903405987644295));
#373481=CARTESIAN_POINT('Ctrl Pts',(-0.452550112791165,1.44319101552553,
-0.914148645199875));
#373482=CARTESIAN_POINT('Ctrl Pts',(-0.0721853899205506,1.51056168593121,
-0.934320358972779));
#373483=CARTESIAN_POINT('Ctrl Pts',(0.121898984874503,1.5073650006368,-0.943160284293108));
#373484=CARTESIAN_POINT('Ctrl Pts',(0.505015634751395,1.42640810437434,
-0.963841795378523));
#373485=CARTESIAN_POINT('Ctrl Pts',(0.689756384050045,1.34681347846234,
-0.974941100654235));
#373486=CARTESIAN_POINT('Ctrl Pts',(1.01114244221697,1.12442097539839,-0.996581364116831));
#373487=CARTESIAN_POINT('Ctrl Pts',(1.14641454539783,0.986147182545734,
-1.00693058490596));
#373488=CARTESIAN_POINT('Ctrl Pts',(1.36138438016108,0.660361894575678,
-1.02632291723582));
#373489=CARTESIAN_POINT('Ctrl Pts',(1.43677705693931,0.474492717363865,
-1.03613929347965));
#373490=CARTESIAN_POINT('Ctrl Pts',(1.51039363418377,0.0860327684066216,
-1.05772040175505));
#373491=CARTESIAN_POINT('Ctrl Pts',(1.50864909123881,-0.112557774460352,
-1.06875320969211));
#373492=CARTESIAN_POINT('Ctrl Pts',(1.42999222080605,-0.491124924634311,
-1.08978471803511));
#373493=CARTESIAN_POINT('Ctrl Pts',(1.35638881218185,-0.668032060615846,
-1.09913049230816));
#373494=CARTESIAN_POINT('Ctrl Pts',(1.14218573227621,-0.992451568091215,
-1.11844799578065));
#373495=CARTESIAN_POINT('Ctrl Pts',(1.00071070989974,-1.13494655346006,
-1.1292129100064));
#373496=CARTESIAN_POINT('Ctrl Pts',(0.674145277752562,-1.35400436702194,
-1.15100973595186));
#373497=CARTESIAN_POINT('Ctrl Pts',(0.493146045688107,-1.42990112156553,
-1.16182630874659));
#373498=CARTESIAN_POINT('Ctrl Pts',(0.202873194368312,-1.48970817965823,
-1.17745337498649));
#373499=CARTESIAN_POINT('Ctrl Pts',(0.101459517442463,-1.49999999999999,
-1.18261852669106));
#373500=CARTESIAN_POINT('Ctrl Pts',(-1.52655665885959E-15,-1.5,-1.1875));
#373501=CARTESIAN_POINT('Origin',(0.,2.04523456705693E-15,3.99999999999998));
#373502=CARTESIAN_POINT('',(-3.11589194069134E-14,-1.5,-1.75));
#373503=CARTESIAN_POINT('',(-7.75886181951911E-14,-1.5,-1.68750000000001));
#373504=CARTESIAN_POINT('',(-1.83697019872103E-16,-1.5,3.99999999999998));
#373505=CARTESIAN_POINT('Ctrl Pts',(-6.02989880249538E-14,-1.49999999999999,
-1.75));
#373506=CARTESIAN_POINT('Ctrl Pts',(0.118890713075185,-1.5,-1.74427986790016));
#373507=CARTESIAN_POINT('Ctrl Pts',(0.237602307351081,-1.48586871165855,
-1.7381758178703));
#373508=CARTESIAN_POINT('Ctrl Pts',(0.546666267057612,-1.41088712561192,
-1.72122314934122));
#373509=CARTESIAN_POINT('Ctrl Pts',(0.728459862929731,-1.32619188177961,
-1.71012395521974));
#373510=CARTESIAN_POINT('Ctrl Pts',(1.042461392657,-1.09535588767151,-1.68860443862946));
#373511=CARTESIAN_POINT('Ctrl Pts',(1.1734329245697,-0.953733812956441,
-1.67836912134243));
#373512=CARTESIAN_POINT('Ctrl Pts',(1.38015928113032,-0.620831811155973,
-1.65917571704723));
#373513=CARTESIAN_POINT('Ctrl Pts',(1.45077075562653,-0.4307868926055,-1.64893260514475));
#373514=CARTESIAN_POINT('Ctrl Pts',(1.51226779727029,-0.0387070076876947,
-1.62715038931598));
#373515=CARTESIAN_POINT('Ctrl Pts',(1.50437321178324,0.159112556164134,
-1.61616041354643));
#373516=CARTESIAN_POINT('Ctrl Pts',(1.41433511710263,0.534558138909894,
-1.59530232561611));
#373517=CARTESIAN_POINT('Ctrl Pts',(1.3353474978557,0.709175132572235,-1.58621429387427));
#373518=CARTESIAN_POINT('Ctrl Pts',(1.11126353645838,1.02696264563013,-1.56660561833651));
#373519=CARTESIAN_POINT('Ctrl Pts',(0.965468576997061,1.16507896747882,
-1.55575449058309));
#373520=CARTESIAN_POINT('Ctrl Pts',(0.632798716902561,1.3737330804517,-1.5339529568941));
#373521=CARTESIAN_POINT('Ctrl Pts',(0.450145830252578,1.44393850638475,
-1.52321491506744));
#373522=CARTESIAN_POINT('Ctrl Pts',(0.0696414072599108,1.51068893531618,
-1.50305370889912));
#373523=CARTESIAN_POINT('Ctrl Pts',(-0.124500319721521,1.50716026437133,
-1.49420887180708));
#373524=CARTESIAN_POINT('Ctrl Pts',(-0.50749951875255,1.42552135196551,
-1.47351406668525));
#373525=CARTESIAN_POINT('Ctrl Pts',(-0.692069231833775,1.34562133072832,
-1.46241450718991));
#373526=CARTESIAN_POINT('Ctrl Pts',(-1.0130232940995,1.122721426836,-1.44078093367235));
#373527=CARTESIAN_POINT('Ctrl Pts',(-1.14804257451774,0.984245374055827,
-1.43043825849274));
#373528=CARTESIAN_POINT('Ctrl Pts',(-1.36252636145643,0.658037569027983,
-1.41105757456481));
#373529=CARTESIAN_POINT('Ctrl Pts',(-1.43763913704559,0.47192412387742,
-1.40121800688207));
#373530=CARTESIAN_POINT('Ctrl Pts',(-1.51054509999985,0.0832463366017405,
-1.37962479647787));
#373531=CARTESIAN_POINT('Ctrl Pts',(-1.5084370634031,-0.115303956207632,
-1.36859422465513));
#373532=CARTESIAN_POINT('Ctrl Pts',(-1.42910812788447,-0.493689801146634,
-1.34757278882518));
#373533=CARTESIAN_POINT('Ctrl Pts',(-1.35518963527169,-0.670460604022503,
-1.33824435272663));
#373534=CARTESIAN_POINT('Ctrl Pts',(-1.14040697609685,-0.994495332354895,
-1.31890965254308));
#373535=CARTESIAN_POINT('Ctrl Pts',(-0.99867560474559,-1.13673807636535,
-1.30813941142593));
#373536=CARTESIAN_POINT('Ctrl Pts',(-0.67174415438103,-1.35519238150162,
-1.28634173954371));
#373537=CARTESIAN_POINT('Ctrl Pts',(-0.490643410544042,-1.4307572611263,
-1.2755295015093));
#373538=CARTESIAN_POINT('Ctrl Pts',(-0.20115025991711,-1.48988270973585,
-1.25995888223323));
#373539=CARTESIAN_POINT('Ctrl Pts',(-0.100595398491377,-1.5,-1.25483989836652));
#373540=CARTESIAN_POINT('Ctrl Pts',(-6.07153216591882E-16,-1.5,-1.25));
#373541=CARTESIAN_POINT('Ctrl Pts',(-1.70803542250024E-16,-1.5,-1.1875));
#373542=CARTESIAN_POINT('Ctrl Pts',(-0.0891224322423083,-1.5,-1.19178790502049));
#373543=CARTESIAN_POINT('Ctrl Pts',(-0.17825876817414,-1.49205861462193,
-1.1962970730207));
#373544=CARTESIAN_POINT('Ctrl Pts',(-0.462982132261434,-1.44068225222714,
-1.21142295344003));
#373545=CARTESIAN_POINT('Ctrl Pts',(-0.650528214500254,-1.36627879298293,
-1.22251303128566));
#373546=CARTESIAN_POINT('Ctrl Pts',(-0.979066611739039,-1.15254596551894,
-1.24425686527785));
#373547=CARTESIAN_POINT('Ctrl Pts',(-1.11854839282021,-1.01774373462307,
-1.25471219201281));
#373548=CARTESIAN_POINT('Ctrl Pts',(-1.34164444619969,-0.699076518440931,
-1.2742977730018));
#373549=CARTESIAN_POINT('Ctrl Pts',(-1.42168329624434,-0.51725270976017,
-1.28376373834652));
#373550=CARTESIAN_POINT('Ctrl Pts',(-1.50710590224472,-0.132511918964616,
-1.30513822672405));
#373551=CARTESIAN_POINT('Ctrl Pts',(-1.5114505885865,0.0666544100360032,
-1.31620302277964));
#373552=CARTESIAN_POINT('Ctrl Pts',(-1.44404865814611,0.448200094555797,
-1.33740000525297));
#373553=CARTESIAN_POINT('Ctrl Pts',(-1.37567310705197,0.627411452301136,
-1.34707432600766));
#373554=CARTESIAN_POINT('Ctrl Pts',(-1.17110246502015,0.958151941051232,
-1.36610397141006));
#373555=CARTESIAN_POINT('Ctrl Pts',(-1.03393881583429,1.10475411093668,
-1.37677554305525));
#373556=CARTESIAN_POINT('Ctrl Pts',(-0.713596781309212,1.33371543591048,
-1.39854804318224));
#373557=CARTESIAN_POINT('Ctrl Pts',(-0.534365319017502,1.41508980830061,
-1.40943172016541));
#373558=CARTESIAN_POINT('Ctrl Pts',(-0.158945587367972,1.50370072773037,
-1.4299555248546));
#373559=CARTESIAN_POINT('Ctrl Pts',(0.0333068351863567,1.51170981039486,
-1.43877720334395));
#373560=CARTESIAN_POINT('Ctrl Pts',(0.420126818038397,1.45384098740134,
-1.45899555575162));
#373561=CARTESIAN_POINT('Ctrl Pts',(0.610363243336896,1.3847747412201,-1.47006681686964));
#373562=CARTESIAN_POINT('Ctrl Pts',(0.945892390419239,1.18001118896129,
-1.49189784693702));
#373563=CARTESIAN_POINT('Ctrl Pts',(1.08953518990553,1.04884180942881,-1.50245245822548));
#373564=CARTESIAN_POINT('Ctrl Pts',(1.32073903794679,0.737378727795451,
-1.52222801081843));
#373565=CARTESIAN_POINT('Ctrl Pts',(1.40535812934366,0.55951452188571,-1.5314158598951));
#373566=CARTESIAN_POINT('Ctrl Pts',(1.50241818589091,0.178621252830884,
-1.55257659706482));
#373567=CARTESIAN_POINT('Ctrl Pts',(1.51285259677747,-0.0209368779816766,
-1.56366315988774));
#373568=CARTESIAN_POINT('Ctrl Pts',(1.45671497336007,-0.405351321204523,
-1.58501951784456));
#373569=CARTESIAN_POINT('Ctrl Pts',(1.39348794957596,-0.586908934735619,
-1.59509213906472));
#373570=CARTESIAN_POINT('Ctrl Pts',(1.19841716461937,-0.923752394666512,
-1.61383424935772));
#373571=CARTESIAN_POINT('Ctrl Pts',(1.06559381468328,-1.07424619729206,
-1.62440509916735));
#373572=CARTESIAN_POINT('Ctrl Pts',(0.751639208296201,-1.3127339875866,
-1.64613490805144));
#373573=CARTESIAN_POINT('Ctrl Pts',(0.574296844781584,-1.39943597200853,
-1.65707568495043));
#373574=CARTESIAN_POINT('Ctrl Pts',(0.259343809553784,-1.48314872736857,
-1.67455422423856));
#373575=CARTESIAN_POINT('Ctrl Pts',(0.129830828717176,-1.50000000000001,
-1.68125351134092));
#373576=CARTESIAN_POINT('Ctrl Pts',(-1.55327140038963E-13,-1.5,-1.68750000000001));
#373577=CARTESIAN_POINT('Origin',(0.,2.04523456705693E-15,3.99999999999998));
#373578=CARTESIAN_POINT('',(-1.24084586568037E-13,-1.5,-2.25000000000001));
#373579=CARTESIAN_POINT('',(-7.76217529874747E-14,-1.5,-2.18750000000001));
#373580=CARTESIAN_POINT('',(-1.83697019872103E-16,-1.5,3.99999999999998));
#373581=CARTESIAN_POINT('Ctrl Pts',(-2.50077736296817E-13,-1.49999999999999,
-2.25000000000001));
#373582=CARTESIAN_POINT('Ctrl Pts',(0.15137822816204,-1.50000000000002,
-2.24271681160177));
#373583=CARTESIAN_POINT('Ctrl Pts',(0.302123674236074,-1.47709065200341,
-2.23482769716825));
#373584=CARTESIAN_POINT('Ctrl Pts',(0.635500754617079,-1.37298397441661,
-2.21589623275476));
#373585=CARTESIAN_POINT('Ctrl Pts',(0.810426639220842,-1.27755733234257,
-2.20482936715013));
#373586=CARTESIAN_POINT('Ctrl Pts',(1.10779197182812,-1.02906110387188,
-2.18361969790135));
#373587=CARTESIAN_POINT('Ctrl Pts',(1.22916603383622,-0.880500500729423,
-2.17391669448497));
#373588=CARTESIAN_POINT('Ctrl Pts',(1.41410422301827,-0.538371936808744,
-2.15490955204493));
#373589=CARTESIAN_POINT('Ctrl Pts',(1.47292312942534,-0.346420806891367,
-2.14424560038285));
#373590=CARTESIAN_POINT('Ctrl Pts',(1.51194236713472,0.0454357372948264,
-2.12247579237251));
#373591=CARTESIAN_POINT('Ctrl Pts',(1.49323620480947,0.24142868694008,-2.11158729516999));
#373592=CARTESIAN_POINT('Ctrl Pts',(1.38308362845326,0.611098841720022,
-2.09105006434889));
#373593=CARTESIAN_POINT('Ctrl Pts',(1.29430022173091,0.781757708685455,
-2.08222322321111));
#373594=CARTESIAN_POINT('Ctrl Pts',(1.05147957165038,1.0883793409421,-2.06202324167436));
#373595=CARTESIAN_POINT('Ctrl Pts',(0.896805860442969,1.21897585527822,
-2.0509538183204));
#373596=CARTESIAN_POINT('Ctrl Pts',(0.552051291897144,1.40797513353587,
-2.02911682645594));
#373597=CARTESIAN_POINT('Ctrl Pts',(0.366722026935949,1.46720368714329,
-2.0185549304379));
#373598=CARTESIAN_POINT('Ctrl Pts',(-0.018444638594273,1.51251237367315,
-1.99876501597651));
#373599=CARTESIAN_POINT('Ctrl Pts',(-0.214704164387485,1.49731244788828,
-1.98959538684923));
#373600=CARTESIAN_POINT('Ctrl Pts',(-0.593279482434409,1.39183463507412,
-1.96845123412248));
#373601=CARTESIAN_POINT('Ctrl Pts',(-0.771570684384589,1.30148301662169,
-1.95736342748991));
#373602=CARTESIAN_POINT('Ctrl Pts',(-1.07694491947251,1.06136375609258,
-1.9360011232948));
#373603=CARTESIAN_POINT('Ctrl Pts',(-1.20294566781614,0.916105716146694,
-1.92590396390956));
#373604=CARTESIAN_POINT('Ctrl Pts',(-1.3978809398763,0.579142218359234,
-1.90716503909892));
#373605=CARTESIAN_POINT('Ctrl Pts',(-1.46225987747819,0.389018390923116,
-1.89661213282906));
#373606=CARTESIAN_POINT('Ctrl Pts',(-1.51269414803051,-0.00216019987483579,
-1.87487998889584));
#373607=CARTESIAN_POINT('Ctrl Pts',(-1.49952897924019,-0.199165252005918,
-1.86393526377745));
#373608=CARTESIAN_POINT('Ctrl Pts',(-1.39970813854547,-0.571842430541103,
-1.84323097608105));
#373609=CARTESIAN_POINT('Ctrl Pts',(-1.31600412169686,-0.744521148433023,
-1.834301801481));
#373610=CARTESIAN_POINT('Ctrl Pts',(-1.08331725769131,-1.05640436976061,
-1.81444322670214));
#373611=CARTESIAN_POINT('Ctrl Pts',(-0.933852575747988,-1.19057451095622,
-1.80352515547273));
#373612=CARTESIAN_POINT('Ctrl Pts',(-0.596109210807379,-1.38997725389203,
-1.78173650516906));
#373613=CARTESIAN_POINT('Ctrl Pts',(-0.412152027269476,-1.45517302032402,
-1.77107486753748));
#373614=CARTESIAN_POINT('Ctrl Pts',(-0.147590902778664,-1.49455896509157,
-1.75725211047933));
#373615=CARTESIAN_POINT('Ctrl Pts',(-0.0737683192890569,-1.49999999999999,
-1.7535491799166));
#373616=CARTESIAN_POINT('Ctrl Pts',(-6.21341417939547E-14,-1.5,-1.75));
#373617=CARTESIAN_POINT('Ctrl Pts',(-1.5499353937051E-13,-1.5,-1.68750000000001));
#373618=CARTESIAN_POINT('Ctrl Pts',(-0.0596763528147572,-1.49999999999999,
-1.69037117986349));
#373619=CARTESIAN_POINT('Ctrl Pts',(-0.119410271247936,-1.49643905972868,
-1.69334404436148));
#373620=CARTESIAN_POINT('Ctrl Pts',(-0.376383239736843,-1.46557247182356,
-1.70656506729203));
#373621=CARTESIAN_POINT('Ctrl Pts',(-0.5671766414312,-1.4028042181917,-1.7174881817119));
#373622=CARTESIAN_POINT('Ctrl Pts',(-0.908284760041371,-1.20929160666783,
-1.73927510404054));
#373623=CARTESIAN_POINT('Ctrl Pts',(-1.05642384570278,-1.08228973211698,
-1.74993027897119));
#373624=CARTESIAN_POINT('Ctrl Pts',(-1.29649837243605,-0.7788274321849,
-1.76991037835556));
#373625=CARTESIAN_POINT('Ctrl Pts',(-1.38607890643986,-0.605202148773951,
-1.77887765840131));
#373626=CARTESIAN_POINT('Ctrl Pts',(-1.49570810019784,-0.228661286203849,
-1.79979659521076));
#373627=CARTESIAN_POINT('Ctrl Pts',(-1.51280761426486,-0.0288828491712062,
-1.81089539726813));
#373628=CARTESIAN_POINT('Ctrl Pts',(-1.46906203259689,0.358289953203854,
-1.83240499740008));
#373629=CARTESIAN_POINT('Ctrl Pts',(-1.41151678854936,0.542363502300319,
-1.84263130568322));
#373630=CARTESIAN_POINT('Ctrl Pts',(-1.22579098571212,0.887567173592386,
-1.86180928742167));
#373631=CARTESIAN_POINT('Ctrl Pts',(-1.09604694951024,1.04358172875388,
-1.87208813124212));
#373632=CARTESIAN_POINT('Ctrl Pts',(-0.786539963597927,1.2922030619363,
-1.89388544118879));
#373633=CARTESIAN_POINT('Ctrl Pts',(-0.611098183816944,1.38383399431454,
-1.90487169143127));
#373634=CARTESIAN_POINT('Ctrl Pts',(-0.240708184574894,1.49270255667511,
-1.92571621531081));
#373635=CARTESIAN_POINT('Ctrl Pts',(-0.0499335931999016,1.51115673901871,
-1.93478765945971));
#373636=CARTESIAN_POINT('Ctrl Pts',(0.337252655791109,1.47506620261309,
-1.95441868144999));
#373637=CARTESIAN_POINT('Ctrl Pts',(0.52962784592717,1.41740390921588,-1.96527606747301));
#373638=CARTESIAN_POINT('Ctrl Pts',(0.876186819683551,1.23282448716524,
-1.98707710004012));
#373639=CARTESIAN_POINT('Ctrl Pts',(1.02798965381075,1.10941871911367,-1.99780865530381));
#373640=CARTESIAN_POINT('Ctrl Pts',(1.27539717593949,0.81266630562079,-2.01795517785921));
#373641=CARTESIAN_POINT('Ctrl Pts',(1.36905073696059,0.642468802256435,
-2.02680728876339));
#373642=CARTESIAN_POINT('Ctrl Pts',(1.48894178607173,0.269628878302083,
-2.04752061787197));
#373643=CARTESIAN_POINT('Ctrl Pts',(1.51154254627943,0.0698314094303458,
-2.05862047725374));
#373644=CARTESIAN_POINT('Ctrl Pts',(1.47806787363015,-0.319402952898901,
-2.08024460849425));
#373645=CARTESIAN_POINT('Ctrl Pts',(1.42523301741552,-0.505405768351132,
-2.0905780982416));
#373646=CARTESIAN_POINT('Ctrl Pts',(1.24912008159399,-0.853964715151503,
-2.10994248417496));
#373647=CARTESIAN_POINT('Ctrl Pts',(1.12500564835859,-1.01190277176006,
-2.11981488416656));
#373648=CARTESIAN_POINT('Ctrl Pts',(0.824093856174803,-1.26867097782277,
-2.14142495968661));
#373649=CARTESIAN_POINT('Ctrl Pts',(0.650885962917394,-1.36565198501259,
-2.15245234520282));
#373650=CARTESIAN_POINT('Ctrl Pts',(0.313880864981918,-1.47525183690481,
-2.17171095086744));
#373651=CARTESIAN_POINT('Ctrl Pts',(0.157333807750998,-1.50000000000001,
-2.17993027364519));
#373652=CARTESIAN_POINT('Ctrl Pts',(-1.5484141746569E-13,-1.5,-2.18750000000001));
#373653=CARTESIAN_POINT('Origin',(0.,2.04523456705693E-15,3.99999999999998));
#373654=CARTESIAN_POINT('',(-7.92750261663246E-15,-1.5,-2.75));
#373655=CARTESIAN_POINT('',(2.81886895545316E-8,-1.49999999999999,-2.68749999728754));
#373656=CARTESIAN_POINT('',(-1.83697019872103E-16,-1.5,3.99999999999998));
#373657=CARTESIAN_POINT('Ctrl Pts',(-1.57512891618694E-14,-1.49999999999999,
-2.75));
#373658=CARTESIAN_POINT('Ctrl Pts',(0.175163016033045,-1.5,-2.74157246546177));
#373659=CARTESIAN_POINT('Ctrl Pts',(0.349117234507293,-1.46932142419033,
-2.73235090656183));
#373660=CARTESIAN_POINT('Ctrl Pts',(0.699332793758691,-1.3415912281678,
-2.71195309161052));
#373661=CARTESIAN_POINT('Ctrl Pts',(0.869557542793228,-1.23806504880211,
-2.70088742234943));
#373662=CARTESIAN_POINT('Ctrl Pts',(1.15974259819827,-0.971446494831827,
-2.67951981641807));
#373663=CARTESIAN_POINT('Ctrl Pts',(1.27699845725887,-0.811153772458503,
-2.67006409846992));
#373664=CARTESIAN_POINT('Ctrl Pts',(1.44108871190044,-0.458500535932944,
-2.65047225199627));
#373665=CARTESIAN_POINT('Ctrl Pts',(1.48792081687523,-0.270244218523759,
-2.64001356769576));
#373666=CARTESIAN_POINT('Ctrl Pts',(1.50838416942693,0.121200861562273,
-2.61826661880209));
#373667=CARTESIAN_POINT('Ctrl Pts',(1.47885227826653,0.320813943583571,
-2.60717700313424));
#373668=CARTESIAN_POINT('Ctrl Pts',(1.34615009396296,0.688855334413892,
-2.58673025919923));
#373669=CARTESIAN_POINT('Ctrl Pts',(1.24737073993788,0.854815193722011,
-2.57793595288125));
#373670=CARTESIAN_POINT('Ctrl Pts',(0.99069001715621,1.14295689273815,-2.55758245976466));
#373671=CARTESIAN_POINT('Ctrl Pts',(0.834335404076568,1.26162241498806,
-2.5467635804285));
#373672=CARTESIAN_POINT('Ctrl Pts',(0.481161746154804,1.43457608369148,
-2.52496723631409));
#373673=CARTESIAN_POINT('Ctrl Pts',(0.286971912806408,1.48566319164258,
-2.51420518726898));
#373674=CARTESIAN_POINT('Ctrl Pts',(-0.101108231842388,1.5085871782716,
-2.49489689519761));
#373675=CARTESIAN_POINT('Ctrl Pts',(-0.291094986015094,1.48369344631382,
-2.48554172613075));
#373676=CARTESIAN_POINT('Ctrl Pts',(-0.658176161474092,1.36216847385968,
-2.46450483116266));
#373677=CARTESIAN_POINT('Ctrl Pts',(-0.830953964747722,1.26420474562025,
-2.45347084055351));
#373678=CARTESIAN_POINT('Ctrl Pts',(-1.13027043874279,1.0059499679797,-2.43189622616067));
#373679=CARTESIAN_POINT('Ctrl Pts',(-1.25335341632362,0.847659026260113,
-2.42209216812556));
#373680=CARTESIAN_POINT('Ctrl Pts',(-1.42768057231883,0.498484823681387,
-2.40269360131563));
#373681=CARTESIAN_POINT('Ctrl Pts',(-1.47963142692091,0.312135909405832,
-2.39234088385588));
#373682=CARTESIAN_POINT('Ctrl Pts',(-1.51118459316081,-0.0774529204248046,
-2.3706970599764));
#373683=CARTESIAN_POINT('Ctrl Pts',(-1.48755760137254,-0.27723771912035,
-2.35959790449331));
#373684=CARTESIAN_POINT('Ctrl Pts',(-1.36576210682761,-0.649376506090869,
-2.3389235274394));
#373685=CARTESIAN_POINT('Ctrl Pts',(-1.27134960904108,-0.818941361342293,
-2.33008613210933));
#373686=CARTESIAN_POINT('Ctrl Pts',(-1.01876421638275,-1.11895309720847,
-2.30959995240885));
#373687=CARTESIAN_POINT('Ctrl Pts',(-0.860805519902715,-1.24456301647905,
-2.29851099665078));
#373688=CARTESIAN_POINT('Ctrl Pts',(-0.511759732876251,-1.42304305712749,
-2.27675974448561));
#373689=CARTESIAN_POINT('Ctrl Pts',(-0.325354062737634,-1.47685928132321,
-2.26629640238298));
#373690=CARTESIAN_POINT('Ctrl Pts',(-0.0892703169527611,-1.49801001581249,
-2.25435029746548));
#373691=CARTESIAN_POINT('Ctrl Pts',(-0.0446103398246381,-1.49999999999999,
-2.25214631597553));
#373692=CARTESIAN_POINT('Ctrl Pts',(-2.47985476116201E-13,-1.5,-2.25000000000001));
#373693=CARTESIAN_POINT('Ctrl Pts',(-1.55059808955077E-13,-1.5,-2.18750000000001));
#373694=CARTESIAN_POINT('Ctrl Pts',(-0.0320907701424565,-1.49999999999999,
-2.18904396789835));
#373695=CARTESIAN_POINT('Ctrl Pts',(-0.0642115404450032,-1.49897020703486,
-2.19061798454009));
#373696=CARTESIAN_POINT('Ctrl Pts',(-0.294774887254793,-1.48413534957626,
-2.20212304810943));
#373697=CARTESIAN_POINT('Ctrl Pts',(-0.488698988986171,-1.43202683042019,
-2.21290068466963));
#373698=CARTESIAN_POINT('Ctrl Pts',(-0.840874537428373,-1.25725825310949,
-2.2346994213473));
#373699=CARTESIAN_POINT('Ctrl Pts',(-0.996534144617197,-1.13784836038626,
-2.24550553915453));
#373700=CARTESIAN_POINT('Ctrl Pts',(-1.25178559953188,-0.848370697709088,
-2.26582737669052));
#373701=CARTESIAN_POINT('Ctrl Pts',(-1.3497766463203,-0.681764192329304,
-2.27462421153712));
#373702=CARTESIAN_POINT('Ctrl Pts',(-1.48051643545944,-0.312975601528768,
-2.2951124665816));
#373703=CARTESIAN_POINT('Ctrl Pts',(-1.50898267362771,-0.113319091924842,
-2.30620449489293));
#373704=CARTESIAN_POINT('Ctrl Pts',(-1.48651373348182,0.277814066187296,
-2.32793411478806));
#373705=CARTESIAN_POINT('Ctrl Pts',(-1.438753797226,0.465736733279212,-2.33837426295983));
#373706=CARTESIAN_POINT('Ctrl Pts',(-1.27282051378257,0.81776959295667,
-2.35793164405303));
#373707=CARTESIAN_POINT('Ctrl Pts',(-1.15452623884263,0.977704243723731,
-2.36744461498256));
#373708=CARTESIAN_POINT('Ctrl Pts',(-0.862699185980956,1.2428365926044,
-2.38884993807868));
#373709=CARTESIAN_POINT('Ctrl Pts',(-0.692004024660368,1.34537042866645,
-2.39991067496967));
#373710=CARTESIAN_POINT('Ctrl Pts',(-0.327420632201285,1.47612274447825,
-2.42108371039041));
#373711=CARTESIAN_POINT('Ctrl Pts',(-0.137945278740974,1.50568186893175,
-2.43070527498944));
#373712=CARTESIAN_POINT('Ctrl Pts',(0.250680959569865,1.49221214633594,
-2.44977722255901));
#373713=CARTESIAN_POINT('Ctrl Pts',(0.446030851030766,1.44588029580342,
-2.46046299444223));
#373714=CARTESIAN_POINT('Ctrl Pts',(0.803710783288726,1.28141890135308,
-2.48224025027471));
#373715=CARTESIAN_POINT('Ctrl Pts',(0.963243425251321,1.16625730467924,
-2.49311470133078));
#373716=CARTESIAN_POINT('Ctrl Pts',(1.22652673135604,0.88433369310823,-2.51361313673437));
#373717=CARTESIAN_POINT('Ctrl Pts',(1.32894620751343,0.72132701314505,-2.52242627704736));
#373718=CARTESIAN_POINT('Ctrl Pts',(1.47065864309764,0.356774492714373,
-2.54267919484907));
#373719=CARTESIAN_POINT('Ctrl Pts',(1.50509953521437,0.157432120196595,
-2.55375377110006));
#373720=CARTESIAN_POINT('Ctrl Pts',(1.49389896064446,-0.235318813030891,
-2.57557326739048));
#373721=CARTESIAN_POINT('Ctrl Pts',(1.45136396314214,-0.425052033288715,
-2.58611400184925));
#373722=CARTESIAN_POINT('Ctrl Pts',(1.29574302933759,-0.780522660203829,
-2.6058623700112));
#373723=CARTESIAN_POINT('Ctrl Pts',(1.18319968994291,-0.942451018260852,
-2.61508580666042));
#373724=CARTESIAN_POINT('Ctrl Pts',(0.900546019732095,-1.21579125958081,
-2.63627777219017));
#373725=CARTESIAN_POINT('Ctrl Pts',(0.732541205007289,-1.32382425951471,
-2.64736182427221));
#373726=CARTESIAN_POINT('Ctrl Pts',(0.373645074360534,-1.46480484870421,
-2.66854534988637));
#373727=CARTESIAN_POINT('Ctrl Pts',(0.187602774442,-1.49999999646629,-2.67847395720811));
#373728=CARTESIAN_POINT('Ctrl Pts',(2.82541730636798E-8,-1.5,-2.68749999864062));
#373729=CARTESIAN_POINT('Origin',(0.,2.04523456705693E-15,3.99999999999998));
#373730=CARTESIAN_POINT('',(7.56010857688836E-15,-1.5,-3.25));
#373731=CARTESIAN_POINT('',(5.4022942157451E-14,-1.5,-3.18749999999999));
#373732=CARTESIAN_POINT('',(-1.83697019872103E-16,-1.5,3.99999999999998));
#373733=CARTESIAN_POINT('Ctrl Pts',(1.53039141736488E-14,-1.5,-3.25));
#373734=CARTESIAN_POINT('Ctrl Pts',(0.0154330977189969,-1.5,-3.24925747473979));
#373735=CARTESIAN_POINT('Ctrl Pts',(0.0308755078629297,-1.49976182060752,
-3.2485078853411));
#373736=CARTESIAN_POINT('Ctrl Pts',(0.237395999187744,-1.49338117750452,
-3.23839442348327));
#373737=CARTESIAN_POINT('Ctrl Pts',(0.425559701281857,-1.4510066607058,
-3.22816432323422));
#373738=CARTESIAN_POINT('Ctrl Pts',(0.782623369709154,-1.29496299027641,
-3.20665054307637));
#373739=CARTESIAN_POINT('Ctrl Pts',(0.946995122227405,-1.1801001721097,
-3.19555156960811));
#373740=CARTESIAN_POINT('Ctrl Pts',(1.21798910903121,-0.896644503164139,
-3.17463959675713));
#373741=CARTESIAN_POINT('Ctrl Pts',(1.32339002900625,-0.732190954109843,
-3.16567727522832));
#373742=CARTESIAN_POINT('Ctrl Pts',(1.4658352660189,-0.372445769911063,
-3.14569143166172));
#373743=CARTESIAN_POINT('Ctrl Pts',(1.50158458221272,-0.180603642510261,
-3.13503353569501));
#373744=CARTESIAN_POINT('Ctrl Pts',(1.49826067554571,0.211574253785341,
-3.1132458747897));
#373745=CARTESIAN_POINT('Ctrl Pts',(1.45704443977926,0.408152285478764,
-3.10232487302896));
#373746=CARTESIAN_POINT('Ctrl Pts',(1.30373031096641,0.765814626563727,
-3.08245474296868));
#373747=CARTESIAN_POINT('Ctrl Pts',(1.19622559605682,0.924790202756146,
-3.07353148074802));
#373748=CARTESIAN_POINT('Ctrl Pts',(0.92372723529977,1.19790343580508,-3.05283441855748));
#373749=CARTESIAN_POINT('Ctrl Pts',(0.759855816388863,1.30799769726818,
-3.04189197730955));
#373750=CARTESIAN_POINT('Ctrl Pts',(0.396187080606716,1.46031857135712,
-3.02016382170989));
#373751=CARTESIAN_POINT('Ctrl Pts',(0.199408818214532,1.49991927713665,
-3.00959630354133));
#373752=CARTESIAN_POINT('Ctrl Pts',(-0.189856778671457,1.50007709674746,
-2.99086336990089));
#373753=CARTESIAN_POINT('Ctrl Pts',(-0.378687652851797,1.46387523445677,
-2.98077691609773));
#373754=CARTESIAN_POINT('Ctrl Pts',(-0.739566877190839,1.31992792042753,
-2.9594155698205));
#373755=CARTESIAN_POINT('Ctrl Pts',(-0.907083090981407,1.21093924646165,
-2.94832847906098));
#373756=CARTESIAN_POINT('Ctrl Pts',(-1.18812362100217,0.936178993106713,
-2.92717468099606));
#373757=CARTESIAN_POINT('Ctrl Pts',(-1.29966801217108,0.773901223266376,
-2.91799451240369));
#373758=CARTESIAN_POINT('Ctrl Pts',(-1.45347108661435,0.41783299888567,
-2.89821294438254));
#373759=CARTESIAN_POINT('Ctrl Pts',(-1.49507687549898,0.227795003267051,
-2.88765527795928));
#373760=CARTESIAN_POINT('Ctrl Pts',(-1.50427996417078,-0.165208685895577,
-2.86582173967247));
#373761=CARTESIAN_POINT('Ctrl Pts',(-1.46878317917199,-0.364477662027525,
-2.85475124099847));
#373762=CARTESIAN_POINT('Ctrl Pts',(-1.32513837329591,-0.728269669186224,
-2.8345405739341));
#373763=CARTESIAN_POINT('Ctrl Pts',(-1.22193340796847,-0.890646368877972,
-2.82571678825526));
#373764=CARTESIAN_POINT('Ctrl Pts',(-0.957225466308382,-1.17121810923077,
-2.80518736201984));
#373765=CARTESIAN_POINT('Ctrl Pts',(-0.797014441261015,-1.28560969202727,
-2.79430166151675));
#373766=CARTESIAN_POINT('Ctrl Pts',(-0.438385311437803,-1.44821577761855,
-2.77253027375232));
#373767=CARTESIAN_POINT('Ctrl Pts',(-0.242799898516706,-1.4935139455441,
-2.76186188374332));
#373768=CARTESIAN_POINT('Ctrl Pts',(-0.0293617344802457,-1.49978458922724,
-2.75141865074141));
#373769=CARTESIAN_POINT('Ctrl Pts',(-0.0146769070534305,-1.5,-2.75070614301985));
#373770=CARTESIAN_POINT('Ctrl Pts',(-1.56713082133928E-14,-1.5,-2.75));
#373771=CARTESIAN_POINT('Ctrl Pts',(2.82541728888338E-8,-1.5,-2.68749999864062));
#373772=CARTESIAN_POINT('Ctrl Pts',(-0.0027320928716755,-1.50000000005146,
-2.687631447881));
#373773=CARTESIAN_POINT('Ctrl Pts',(-0.00546452515622478,-1.49999253561752,
-2.68776311943298));
#373774=CARTESIAN_POINT('Ctrl Pts',(-0.207001458014825,-1.49889115499487,
-2.6974901635423));
#373775=CARTESIAN_POINT('Ctrl Pts',(-0.40358363203981,-1.45829274468987,
-2.70807596141949));
#373776=CARTESIAN_POINT('Ctrl Pts',(-0.766393227447706,-1.30416358286693,
-2.72981301182346));
#373777=CARTESIAN_POINT('Ctrl Pts',(-0.92963322737301,-1.19331031809287,
-2.74074615733658));
#373778=CARTESIAN_POINT('Ctrl Pts',(-1.20077459221899,-0.918889747502195,
-2.76141424596263));
#373779=CARTESIAN_POINT('Ctrl Pts',(-1.30752956616432,-0.759326959880522,
-2.77031516889539));
#373780=CARTESIAN_POINT('Ctrl Pts',(-1.45984960981038,-0.399001644028943,
-2.79033324199826));
#373781=CARTESIAN_POINT('Ctrl Pts',(-1.50009780204417,-0.200129413280295,
-2.80138169926208));
#373782=CARTESIAN_POINT('Ctrl Pts',(-1.49990559923608,0.193888453867102,
-2.82327158077027));
#373783=CARTESIAN_POINT('Ctrl Pts',(-1.46250271323157,0.385241403380367,
-2.83390230018768));
#373784=CARTESIAN_POINT('Ctrl Pts',(-1.31686710612883,0.743963622581648,
-2.85383131236553));
#373785=CARTESIAN_POINT('Ctrl Pts',(-1.20975732903253,0.90780681842778,
-2.86284571276972));
#373786=CARTESIAN_POINT('Ctrl Pts',(-0.935947302566849,1.18885033502406,
-2.88382616816019));
#373787=CARTESIAN_POINT('Ctrl Pts',(-0.770676738163206,1.30208025119187,
-2.89492302734659));
#373788=CARTESIAN_POINT('Ctrl Pts',(-0.412534434467264,1.45474160075709,
-2.91639475001066));
#373789=CARTESIAN_POINT('Ctrl Pts',(-0.224167349469574,1.4954029972334,
-2.92658704884861));
#373790=CARTESIAN_POINT('Ctrl Pts',(0.16549812277975,1.50403330736282,-2.94557456846029));
#373791=CARTESIAN_POINT('Ctrl Pts',(0.363174829007174,1.46889642578174,
-2.95583724528012));
#373792=CARTESIAN_POINT('Ctrl Pts',(0.730704038992162,1.32456691867321,
-2.97752915561535));
#373793=CARTESIAN_POINT('Ctrl Pts',(0.897327655309507,1.21787230515505,
-2.98850957735759));
#373794=CARTESIAN_POINT('Ctrl Pts',(1.17581111208616,0.950567488669378,
-3.0093332527101));
#373795=CARTESIAN_POINT('Ctrl Pts',(1.28662860170944,0.794156643403929,
-3.01838018647743));
#373796=CARTESIAN_POINT('Ctrl Pts',(1.44768797357916,0.440182107776354,
-3.03804543845674));
#373797=CARTESIAN_POINT('Ctrl Pts',(1.49322546113538,0.244578440345993,
-3.04891230886954));
#373798=CARTESIAN_POINT('Ctrl Pts',(1.50521819068071,-0.147821929795448,
-3.07071232943296));
#373799=CARTESIAN_POINT('Ctrl Pts',(1.47356569707093,-0.340808737409749,
-3.08143381874486));
#373800=CARTESIAN_POINT('Ctrl Pts',(1.33897451148274,-0.703039340644609,
-3.1015577411468));
#373801=CARTESIAN_POINT('Ctrl Pts',(1.23772603215813,-0.868995531784903,
-3.11042197661755));
#373802=CARTESIAN_POINT('Ctrl Pts',(0.973642324634376,-1.15829099819762,
-3.13116369509797));
#373803=CARTESIAN_POINT('Ctrl Pts',(0.811532249540049,-1.27711513932012,
-3.14226389030921));
#373804=CARTESIAN_POINT('Ctrl Pts',(0.457235322458853,-1.44139275207604,
-3.16387327618216));
#373805=CARTESIAN_POINT('Ctrl Pts',(0.26963351173158,-1.48795042209609,
-3.17419254112082));
#373806=CARTESIAN_POINT('Ctrl Pts',(0.0522115465392471,-1.49931910388413,
-3.18496905701478));
#373807=CARTESIAN_POINT('Ctrl Pts',(0.0260941836402007,-1.5,-3.18624454300425));
#373808=CARTESIAN_POINT('Ctrl Pts',(1.08229581334774E-13,-1.5,-3.18749999999999));
#373809=CARTESIAN_POINT('Origin',(0.,2.04523456705693E-15,3.99999999999998));
#373810=CARTESIAN_POINT('',(1.15973386931536E-13,-1.49999999999999,-3.74999999999999));
#373811=CARTESIAN_POINT('',(1.15973386931537E-13,-1.49999999999999,-3.68749999999999));
#373812=CARTESIAN_POINT('',(-1.83697019872103E-16,-1.5,3.99999999999998));
#373813=CARTESIAN_POINT('Ctrl Pts',(2.32130470882944E-13,-1.49999999999999,
-3.74999999999999));
#373814=CARTESIAN_POINT('Ctrl Pts',(0.0420030761821631,-1.49999999999999,
-3.74797912605495));
#373815=CARTESIAN_POINT('Ctrl Pts',(0.0840524578334832,-1.49823581808009,
-3.74590701918365));
#373816=CARTESIAN_POINT('Ctrl Pts',(0.317532157721825,-1.47854786920351,
-3.73412683441645));
#373817=CARTESIAN_POINT('Ctrl Pts',(0.504123157769973,-1.42575275674287,
-3.72368293983925));
#373818=CARTESIAN_POINT('Ctrl Pts',(0.853942399427975,-1.24926412137683,
-3.70194979163417));
#373819=CARTESIAN_POINT('Ctrl Pts',(1.01250261650075,-1.12460203240067,
-3.69085822382847));
#373820=CARTESIAN_POINT('Ctrl Pts',(1.26618588593558,-0.826716944862991,
-3.67037829607211));
#373821=CARTESIAN_POINT('Ctrl Pts',(1.36128392355952,-0.658478841679479,
-3.66158215787108));
#373822=CARTESIAN_POINT('Ctrl Pts',(1.48397740638111,-0.292571139284737,
-3.64125395218248));
#373823=CARTESIAN_POINT('Ctrl Pts',(1.50936051504709,-0.0980144946652442,
-3.63044524970362));
#373824=CARTESIAN_POINT('Ctrl Pts',(1.48421097083258,0.294354999955967,
-3.60864694444689));
#373825=CARTESIAN_POINT('Ctrl Pts',(1.43217179477893,0.488296558661019,
-3.59787241340772));
#373826=CARTESIAN_POINT('Ctrl Pts',(1.25944573706426,0.836571673933364,
-3.57852379589259));
#373827=CARTESIAN_POINT('Ctrl Pts',(1.14354006376931,0.989138303288629,
-3.56920919965695));
#373828=CARTESIAN_POINT('Ctrl Pts',(0.85591204017378,1.24742962295239,-3.54819593103996));
#373829=CARTESIAN_POINT('Ctrl Pts',(0.685192166379378,1.34876859625304,
-3.53716719580178));
#373830=CARTESIAN_POINT('Ctrl Pts',(0.312269766249229,1.48055548880213,
-3.5155642114447));
#373831=CARTESIAN_POINT('Ctrl Pts',(0.113476387161101,1.50885794998208,
-3.50570568938901));
#373832=CARTESIAN_POINT('Ctrl Pts',(-0.27636898959008,1.48672502335481,
-3.48633444143745));
#373833=CARTESIAN_POINT('Ctrl Pts',(-0.463841446690415,1.43929184955474,
-3.47599708047863));
#373834=CARTESIAN_POINT('Ctrl Pts',(-0.817535381145995,1.27329545295664,
-3.45436896210629));
#373835=CARTESIAN_POINT('Ctrl Pts',(-0.979160045924644,1.15364690708048,
-3.4432692210777));
#373836=CARTESIAN_POINT('Ctrl Pts',(-1.24179108047367,0.863137736198284,
-3.42256368034533));
#373837=CARTESIAN_POINT('Ctrl Pts',(-1.34217373310823,0.696864398573333,
-3.41371468880963));
#373838=CARTESIAN_POINT('Ctrl Pts',(-1.47510896404006,0.334115757684514,
-3.39356198653803));
#373839=CARTESIAN_POINT('Ctrl Pts',(-1.50589322665991,0.140898531544399,
-3.38282769619691));
#373840=CARTESIAN_POINT('Ctrl Pts',(-1.492070616974,-0.25152412225069,-3.36102643765274));
#373841=CARTESIAN_POINT('Ctrl Pts',(-1.4456247627367,-0.446909828186021,
-3.35017167621189));
#373842=CARTESIAN_POINT('Ctrl Pts',(-1.28293685010969,-0.800099124751201,
-3.33055004862493));
#373843=CARTESIAN_POINT('Ctrl Pts',(-1.17141645804915,-0.955972075839512,
-3.32147168739789));
#373844=CARTESIAN_POINT('Ctrl Pts',(-0.89166584427233,-1.22203810273209,
-3.30062145674782));
#373845=CARTESIAN_POINT('Ctrl Pts',(-0.724466581195555,-1.32800215144422,
-3.28963363265478));
#373846=CARTESIAN_POINT('Ctrl Pts',(-0.368720817963472,-1.46575064069154,
-3.26869145971749));
#373847=CARTESIAN_POINT('Ctrl Pts',(-0.185075007272709,-1.49999999999999,
-3.2589044254391));
#373848=CARTESIAN_POINT('Ctrl Pts',(1.67227343084164E-14,-1.49999999999999,
-3.25));
#373849=CARTESIAN_POINT('Ctrl Pts',(1.05748743095546E-13,-1.5,-3.1875));
#373850=CARTESIAN_POINT('Ctrl Pts',(-0.172624793809803,-1.5,-3.19580541426457));
#373851=CARTESIAN_POINT('Ctrl Pts',(-0.344156579903346,-1.47020600738534,
-3.20488585207672));
#373852=CARTESIAN_POINT('Ctrl Pts',(-0.691996997468058,-1.34527564392206,
-3.2250916198437));
#373853=CARTESIAN_POINT('Ctrl Pts',(-0.86211954019817,-1.24313224950465,
-3.23611396100867));
#373854=CARTESIAN_POINT('Ctrl Pts',(-1.14839476463202,-0.983496554079989,
-3.25709948681679));
#373855=CARTESIAN_POINT('Ctrl Pts',(-1.26354520632856,-0.830366556260505,
-3.26636852465207));
#373856=CARTESIAN_POINT('Ctrl Pts',(-1.4345577472031,-0.48124365055675,
-3.28576424163561));
#373857=CARTESIAN_POINT('Ctrl Pts',(-1.48564309176012,-0.287043308368793,
-3.29655314953494));
#373858=CARTESIAN_POINT('Ctrl Pts',(-1.50885375884096,0.105358613817684,
-3.31835325632308));
#373859=CARTESIAN_POINT('Ctrl Pts',(-1.48254282957616,0.299696593854507,
-3.32914981076958));
#373860=CARTESIAN_POINT('Ctrl Pts',(-1.35809696534895,0.665068852552179,
-3.34944826958612));
#373861=CARTESIAN_POINT('Ctrl Pts',(-1.26210268023943,0.832970856633082,
-3.35824846916903));
#373862=CARTESIAN_POINT('Ctrl Pts',(-1.00689323710206,1.12960922700053,
-3.37876719395939));
#373863=CARTESIAN_POINT('Ctrl Pts',(-0.84780130228411,1.25342394453506,
-3.38986080595143));
#373864=CARTESIAN_POINT('Ctrl Pts',(-0.497301745488257,1.42813436872872,
-3.41157729107906));
#373865=CARTESIAN_POINT('Ctrl Pts',(-0.310550154863041,1.48001861721066,
-3.42200361029681));
#373866=CARTESIAN_POINT('Ctrl Pts',(0.0775679172145885,1.51092539479631,
-3.4415354713457));
#373867=CARTESIAN_POINT('Ctrl Pts',(0.275377779215376,1.48764844687008,
-3.45109221827783));
#373868=CARTESIAN_POINT('Ctrl Pts',(0.650554370936392,1.36588439585195,
-3.47252524521366));
#373869=CARTESIAN_POINT('Ctrl Pts',(0.824234619747844,1.26865964712896,
-3.4835821275452));
#373870=CARTESIAN_POINT('Ctrl Pts',(1.11867540841364,1.01719913638398,-3.50473343078228));
#373871=CARTESIAN_POINT('Ctrl Pts',(1.23840059250391,0.867443918796923,
-3.51430867117782));
#373872=CARTESIAN_POINT('Ctrl Pts',(1.41969290810348,0.523461335807366,
-3.53341881467724));
#373873=CARTESIAN_POINT('Ctrl Pts',(1.47649168137935,0.33088917789354,-3.54411726789468));
#373874=CARTESIAN_POINT('Ctrl Pts',(1.51136182986144,-0.061172518020671,
-3.56589847322325));
#373875=CARTESIAN_POINT('Ctrl Pts',(1.49065092451211,-0.256759346419735,
-3.57676440813431));
#373876=CARTESIAN_POINT('Ctrl Pts',(1.37674479462488,-0.625316213987474,
-3.59723978966586));
#373877=CARTESIAN_POINT('Ctrl Pts',(1.2860891936887,-0.795247355491489,
-3.60604654247091));
#373878=CARTESIAN_POINT('Ctrl Pts',(1.04002858388445,-1.09928771354101,
-3.62633070458124));
#373879=CARTESIAN_POINT('Ctrl Pts',(0.884177261008663,-1.22813210013013,
-3.63740811558783));
#373880=CARTESIAN_POINT('Ctrl Pts',(0.53787178324674,-1.41342704098718,
-3.65921682734561));
#373881=CARTESIAN_POINT('Ctrl Pts',(0.352144619071328,-1.47074607461982,
-3.669744825077));
#373882=CARTESIAN_POINT('Ctrl Pts',(0.107185427923135,-1.49713116707827,
-3.68226334889112));
#373883=CARTESIAN_POINT('Ctrl Pts',(0.0535634300530825,-1.49999999999999,
-3.68492292827002));
#373884=CARTESIAN_POINT('Ctrl Pts',(2.32130470882946E-13,-1.49999999999999,
-3.68749999999999));
#373885=CARTESIAN_POINT('Origin',(0.,2.04523456705693E-15,3.99999999999998));
#373886=CARTESIAN_POINT('',(4.6279136560691E-14,-1.5,-4.24999999999999));
#373887=CARTESIAN_POINT('',(7.56010857688827E-15,-1.5,-4.1875));
#373888=CARTESIAN_POINT('',(-1.83697019872103E-16,-1.5,3.99999999999998));
#373889=CARTESIAN_POINT('Ctrl Pts',(9.2741970141254E-14,-1.49999999999999,
-4.25));
#373890=CARTESIAN_POINT('Ctrl Pts',(0.0693232899188041,-1.49999999999999,
-4.24666468165869));
#373891=CARTESIAN_POINT('Ctrl Pts',(0.138705632270155,-1.49519485879729,
-4.24319304601137));
#373892=CARTESIAN_POINT('Ctrl Pts',(0.399009714721784,-1.45880886234304,
-4.22965843788142));
#373893=CARTESIAN_POINT('Ctrl Pts',(0.583384578401812,-1.39534188150886,
-4.21902472642679));
#373894=CARTESIAN_POINT('Ctrl Pts',(0.924551674788282,-1.19814759239858,
-4.19713269770673));
#373895=CARTESIAN_POINT('Ctrl Pts',(1.07653828060304,-1.0636902135809,-4.18608531153565));
#373896=CARTESIAN_POINT('Ctrl Pts',(1.31211599018145,-0.751370166077832,
-4.16607551682389));
#373897=CARTESIAN_POINT('Ctrl Pts',(1.39674515418371,-0.57906444187859,
-4.15717024677103));
#373898=CARTESIAN_POINT('Ctrl Pts',(1.49846374621891,-0.206933243758507,
-4.13649629131991));
#373899=CARTESIAN_POINT('Ctrl Pts',(1.51264892419061,-0.0101024249300511,
-4.12556124582944));
#373900=CARTESIAN_POINT('Ctrl Pts',(1.46432051278063,0.381132946040274,
-4.1038259474422));
#373901=CARTESIAN_POINT('Ctrl Pts',(1.40099407937911,0.571611205590939,
-4.09324382191161));
#373902=CARTESIAN_POINT('Ctrl Pts',(1.20789244880423,0.909530858192071,
-4.07447050787821));
#373903=CARTESIAN_POINT('Ctrl Pts',(1.08277279888511,1.05541873660482,-4.06444441011438));
#373904=CARTESIAN_POINT('Ctrl Pts',(0.778806050866134,1.29714949545131,
-4.0431050598303));
#373905=CARTESIAN_POINT('Ctrl Pts',(0.601126187418435,1.38844780784244,
-4.03202036918128));
#373906=CARTESIAN_POINT('Ctrl Pts',(0.222993889241262,1.49613749901354,
-4.01083609019249));
#373907=CARTESIAN_POINT('Ctrl Pts',(0.0265280057553068,1.51242862909709,
-4.00162156896913));
#373908=CARTESIAN_POINT('Ctrl Pts',(-0.359050275912133,1.46908704568924,
-3.98186649237049));
#373909=CARTESIAN_POINT('Ctrl Pts',(-0.544591484364593,1.41086374167892,
-3.97132232281638));
#373910=CARTESIAN_POINT('Ctrl Pts',(-0.89016755138681,1.22381363159918,
-3.94949995014855));
#373911=CARTESIAN_POINT('Ctrl Pts',(-1.04546374828784,1.09413852903051,
-3.93842617220901));
#373912=CARTESIAN_POINT('Ctrl Pts',(-1.28999177385172,0.78887462257984,
-3.91818175913674));
#373913=CARTESIAN_POINT('Ctrl Pts',(-1.37976064818862,0.618599897004113,
-3.90936666094467));
#373914=CARTESIAN_POINT('Ctrl Pts',(-1.49189268104597,0.249515467065523,
-3.88886197039252));
#373915=CARTESIAN_POINT('Ctrl Pts',(-1.51165667168068,0.0537341457075633,
-3.87798523031708));
#373916=CARTESIAN_POINT('Ctrl Pts',(-1.47482512978302,-0.338236073364855,
-3.85620910703528));
#373917=CARTESIAN_POINT('Ctrl Pts',(-1.41707052806472,-0.530517375765477,
-3.84552681245747));
#373918=CARTESIAN_POINT('Ctrl Pts',(-1.23405402718182,-0.873625163654692,
-3.82646526868585));
#373919=CARTESIAN_POINT('Ctrl Pts',(-1.11355085321239,-1.02281532049236,
-3.8168308703912));
#373920=CARTESIAN_POINT('Ctrl Pts',(-0.817728849491741,-1.27287830481274,
-3.79565193359227));
#373921=CARTESIAN_POINT('Ctrl Pts',(-0.643458386551141,-1.36925621168849,
-3.78459017795484));
#373922=CARTESIAN_POINT('Ctrl Pts',(-0.307993231357976,-1.47618493681224,
-3.76547986078575));
#373923=CARTESIAN_POINT('Ctrl Pts',(-0.154340990313575,-1.49999999999999,
-3.75742573435872));
#373924=CARTESIAN_POINT('Ctrl Pts',(2.21316021065121E-13,-1.49999999999999,
-3.74999999999999));
#373925=CARTESIAN_POINT('Ctrl Pts',(2.33910113500713E-13,-1.5,-3.68749999999999));
#373926=CARTESIAN_POINT('Ctrl Pts',(-0.141276695353502,-1.5,-3.69429717817437));
#373927=CARTESIAN_POINT('Ctrl Pts',(-0.282092362620038,-1.48004645163004,
-3.70162644035696));
#373928=CARTESIAN_POINT('Ctrl Pts',(-0.608182943233829,-1.38535690811647,
-3.71994574582936));
#373929=CARTESIAN_POINT('Ctrl Pts',(-0.785307562700868,-1.29320857142521,
-3.73102733407602));
#373930=CARTESIAN_POINT('Ctrl Pts',(-1.08792750627408,-1.05008895026412,
-3.75234046570973));
#373931=CARTESIAN_POINT('Ctrl Pts',(-1.21228015028828,-0.903658276744491,
-3.76229676240296));
#373932=CARTESIAN_POINT('Ctrl Pts',(-1.40372356070962,-0.564877289250618,
-3.78111792837485));
#373933=CARTESIAN_POINT('Ctrl Pts',(-1.46613635494529,-0.3740906654696,
-3.79171718525157));
#373934=CARTESIAN_POINT('Ctrl Pts',(-1.51257207849374,0.0172890465575684,
-3.81346050258642));
#373935=CARTESIAN_POINT('Ctrl Pts',(-1.49746513068593,0.213957744631522,
-3.82438654136831));
#373936=CARTESIAN_POINT('Ctrl Pts',(-1.394030070704,0.585592642461911,-3.84503292458111));
#373937=CARTESIAN_POINT('Ctrl Pts',(-1.30856115445774,0.757561799800549,
-3.8539185387629));
#373938=CARTESIAN_POINT('Ctrl Pts',(-1.07151362690525,1.06873333016387,
-3.87396714687104));
#373939=CARTESIAN_POINT('Ctrl Pts',(-0.918975741690193,1.20241353352463,
-3.8850194682775));
#373940=CARTESIAN_POINT('Ctrl Pts',(-0.577067375488448,1.3979545577994,
-3.90690123733498));
#373941=CARTESIAN_POINT('Ctrl Pts',(-0.392491661844923,1.46056490371438,
-3.91752081677356));
#373942=CARTESIAN_POINT('Ctrl Pts',(-0.00872809933920568,1.51248465847023,
-3.93742686519327));
#373943=CARTESIAN_POINT('Ctrl Pts',(0.18685186838331,1.50092573252532,-3.94646419991666));
#373944=CARTESIAN_POINT('Ctrl Pts',(0.566868952789501,1.40285153334342,
-3.96747206372549));
#373945=CARTESIAN_POINT('Ctrl Pts',(0.74717147729129,1.31569795057346,-3.97856780583493));
#373946=CARTESIAN_POINT('Ctrl Pts',(1.05748170470374,1.08081664238639,-4.00002209439531));
#373947=CARTESIAN_POINT('Ctrl Pts',(1.18631966062852,0.937604065057542,
-4.01019894058792));
#373948=CARTESIAN_POINT('Ctrl Pts',(1.3874104900289,0.603815469614292,-4.0291458330574));
#373949=CARTESIAN_POINT('Ctrl Pts',(1.45515371489895,0.414822693444069,
-4.03945429480855));
#373950=CARTESIAN_POINT('Ctrl Pts',(1.51254497872842,0.0242368175648848,
-4.06115351013518));
#373951=CARTESIAN_POINT('Ctrl Pts',(1.50277995913657,-0.173310068174655,
-4.07212833712071));
#373952=CARTESIAN_POINT('Ctrl Pts',(1.40927410874699,-0.547783208284312,
-4.09293240046014));
#373953=CARTESIAN_POINT('Ctrl Pts',(1.3286244643216,-0.721710061443943,
-4.101957360696));
#373954=CARTESIAN_POINT('Ctrl Pts',(1.10150240283646,-1.0374267303463,-4.12165468344362));
#373955=CARTESIAN_POINT('Ctrl Pts',(0.954401438343342,-1.17416356172977,
-4.13253032721384));
#373956=CARTESIAN_POINT('Ctrl Pts',(0.61991370621179,-1.37957069884262,
-4.1543291295381));
#373957=CARTESIAN_POINT('Ctrl Pts',(0.436785632905365,-1.44801250520404,
-4.16504104436089));
#373958=CARTESIAN_POINT('Ctrl Pts',(0.164305308462188,-1.49325512192942,
-4.17940749943655));
#373959=CARTESIAN_POINT('Ctrl Pts',(0.08213376367161,-1.5,-4.18354833745289));
#373960=CARTESIAN_POINT('Ctrl Pts',(1.53039141736487E-14,-1.5,-4.1875));
#373961=CARTESIAN_POINT('Origin',(0.,2.04523456705693E-15,3.99999999999998));
#373962=CARTESIAN_POINT('',(7.56010857688836E-15,-1.5,-4.75));
#373963=CARTESIAN_POINT('',(-7.92750261663254E-15,-1.5,-4.6875));
#373964=CARTESIAN_POINT('',(-1.83697019872103E-16,-1.5,3.99999999999998));
#373965=CARTESIAN_POINT('Ctrl Pts',(1.53039141736488E-14,-1.5,-4.75));
#373966=CARTESIAN_POINT('Ctrl Pts',(0.0979950813416671,-1.5,-4.74528520945068));
#373967=CARTESIAN_POINT('Ctrl Pts',(0.195964627823619,-1.49039890558719,
-4.74030495038083));
#373968=CARTESIAN_POINT('Ctrl Pts',(0.48310212608443,-1.43330761243503,
-4.72490417180033));
#373969=CARTESIAN_POINT('Ctrl Pts',(0.66450478786642,-1.35874230503128,
-4.71410517362704));
#373970=CARTESIAN_POINT('Ctrl Pts',(0.992531086681102,-1.14210808027211,
-4.69230538361246));
#373971=CARTESIAN_POINT('Ctrl Pts',(1.13503121685614,-1.00062738452671,
-4.68151932357652));
#373972=CARTESIAN_POINT('Ctrl Pts',(1.35155687454217,-0.677752945802649,
-4.66213299360489));
#373973=CARTESIAN_POINT('Ctrl Pts',(1.42642341357834,-0.501390609042993,
-4.65285503383571));
#373974=CARTESIAN_POINT('Ctrl Pts',(1.50777006032532,-0.123551390243716,
-4.63186396612464));
#373975=CARTESIAN_POINT('Ctrl Pts',(1.51096921547043,0.0748740853935728,
-4.62084032858923));
#373976=CARTESIAN_POINT('Ctrl Pts',(1.44020051357598,0.464202881123239,
-4.5992109510487));
#373977=CARTESIAN_POINT('Ctrl Pts',(1.36592984409968,0.651051461324218,
-4.58930023411752));
#373978=CARTESIAN_POINT('Ctrl Pts',(1.15290584784697,0.978526060633627,
-4.56995459567167));
#373979=CARTESIAN_POINT('Ctrl Pts',(1.01864650714161,1.11760592881781,-4.55963171045843));
#373980=CARTESIAN_POINT('Ctrl Pts',(0.698992571526539,1.34202256564563,
-4.53801855784309));
#373981=CARTESIAN_POINT('Ctrl Pts',(0.51493865994717,1.42283631721542,-4.52691843346095));
#373982=CARTESIAN_POINT('Ctrl Pts',(0.132294604949322,1.50652034927885,
-4.50618390633501));
#373983=CARTESIAN_POINT('Ctrl Pts',(-0.0620202766589267,1.51104502951983,
-4.49732285442352));
#373984=CARTESIAN_POINT('Ctrl Pts',(-0.442941434862766,1.44615212709081,
-4.47719319603141));
#373985=CARTESIAN_POINT('Ctrl Pts',(-0.625852808074851,1.37689799405716,
-4.46646914256698));
#373986=CARTESIAN_POINT('Ctrl Pts',(-0.959507530504752,1.16999394844625,
-4.44466883764907));
#373987=CARTESIAN_POINT('Ctrl Pts',(-1.10600885552506,1.03262040074767,
-4.43380435748213));
#373988=CARTESIAN_POINT('Ctrl Pts',(-1.33173288654911,0.715948899065067,
-4.41414777437365));
#373989=CARTESIAN_POINT('Ctrl Pts',(-1.41161727845045,0.541705253267488,
-4.40509473629263));
#373990=CARTESIAN_POINT('Ctrl Pts',(-1.50352918131627,0.166783910363671,
-4.38426577279797));
#373991=CARTESIAN_POINT('Ctrl Pts',(-1.51243471580371,-0.0308905016303464,
-4.37328386102053));
#373992=CARTESIAN_POINT('Ctrl Pts',(-1.45329021145476,-0.421308564944836,
-4.35159396861417));
#373993=CARTESIAN_POINT('Ctrl Pts',(-1.38470154651078,-0.610007171654256,
-4.34134350722837));
#373994=CARTESIAN_POINT('Ctrl Pts',(-1.18206653673657,-0.942977568277008,
-4.32234504809104));
#373995=CARTESIAN_POINT('Ctrl Pts',(-1.05251826643873,-1.08566569770916,
-4.31214859487936));
#373996=CARTESIAN_POINT('Ctrl Pts',(-0.740977133552966,-1.31921053196782,
-4.29067220862757));
#373997=CARTESIAN_POINT('Ctrl Pts',(-0.560176122715327,-1.40555085271442,
-4.27957507369487));
#373998=CARTESIAN_POINT('Ctrl Pts',(-0.247304238444433,-1.48468591115563,
-4.26232382207658));
#373999=CARTESIAN_POINT('Ctrl Pts',(-0.123766901248376,-1.5,-4.25595473781271));
#374000=CARTESIAN_POINT('Ctrl Pts',(8.97198981775205E-14,-1.5,-4.25));
#374001=CARTESIAN_POINT('Ctrl Pts',(1.6826817716975E-14,-1.49999999999999,
-4.1875));
#374002=CARTESIAN_POINT('Ctrl Pts',(-0.109787828417629,-1.49999999999999,
-4.19278216935755));
#374003=CARTESIAN_POINT('Ctrl Pts',(-0.219475581345938,-1.4879495279894,
-4.1983942591644));
#374004=CARTESIAN_POINT('Ctrl Pts',(-0.521290520832159,-1.4205088711852,
-4.21478868878879));
#374005=CARTESIAN_POINT('Ctrl Pts',(-0.704899784450703,-1.33891602798461,
-4.22588906147013));
#374006=CARTESIAN_POINT('Ctrl Pts',(-1.02343609181701,-1.11320780716232,
-4.24748431950447));
#374007=CARTESIAN_POINT('Ctrl Pts',(-1.15704329256801,-0.973614691781268,
-4.2577900854861));
#374008=CARTESIAN_POINT('Ctrl Pts',(-1.36881592191344,-0.645056780305522,
-4.27710560951818));
#374009=CARTESIAN_POINT('Ctrl Pts',(-1.44236294662618,-0.457576254107109,
-4.28707909699394));
#374010=CARTESIAN_POINT('Ctrl Pts',(-1.51129595325695,-0.0676933169888792,
-4.30873926016718));
#374011=CARTESIAN_POINT('Ctrl Pts',(-1.50716221617281,0.130620471611318,
-4.31975669286719));
#374012=CARTESIAN_POINT('Ctrl Pts',(-1.42408684985495,0.50798862270464,
-4.34072159015016));
#374013=CARTESIAN_POINT('Ctrl Pts',(-1.34840552196579,0.684001993990453,
-4.34995819779821));
#374014=CARTESIAN_POINT('Ctrl Pts',(-1.13038299794658,1.00587621585134,
-4.36938876198311));
#374015=CARTESIAN_POINT('Ctrl Pts',(-0.987225298387312,1.14669832783564,
-4.38018816534744));
#374016=CARTESIAN_POINT('Ctrl Pts',(-0.658265867242106,1.36176339312966,
-4.40198926294929));
#374017=CARTESIAN_POINT('Ctrl Pts',(-0.476607967494566,1.43546849574518,
-4.41277664668747));
#374018=CARTESIAN_POINT('Ctrl Pts',(-0.0976586420292757,1.50905587449095,
-4.43305294846374));
#374019=CARTESIAN_POINT('Ctrl Pts',(0.0958638183741212,1.50917093989091,
-4.44185750178158));
#374020=CARTESIAN_POINT('Ctrl Pts',(0.480126971699187,1.43502584781182,
-4.46240495725699));
#374021=CARTESIAN_POINT('Ctrl Pts',(0.666548976661914,1.35849973316441,
-4.47349991555954));
#374022=CARTESIAN_POINT('Ctrl Pts',(0.992205866389971,1.14121814093558,
-4.49520368975601));
#374023=CARTESIAN_POINT('Ctrl Pts',(1.12998615066959,1.00498883680653,-4.50561679411108));
#374024=CARTESIAN_POINT('Ctrl Pts',(1.34978962446225,0.683425221208888,
-4.52512441633016));
#374025=CARTESIAN_POINT('Ctrl Pts',(1.42795326901029,0.499971247219071,
-4.53472381959884));
#374026=CARTESIAN_POINT('Ctrl Pts',(1.50860936195778,0.113706312543667,
-4.55618298263636));
#374027=CARTESIAN_POINT('Ctrl Pts',(1.51048440759924,-0.0852488195093594,
-4.5672360455282));
#374028=CARTESIAN_POINT('Ctrl Pts',(1.43851795645481,-0.465599791205705,
-4.58836665506689));
#374029=CARTESIAN_POINT('Ctrl Pts',(1.36803298263095,-0.643871835427663,
-4.59789914452992));
#374030=CARTESIAN_POINT('Ctrl Pts',(1.15957266202618,-0.97207640577981,
-4.61704549000219));
#374031=CARTESIAN_POINT('Ctrl Pts',(1.02065669668349,-1.11703943284086,
-4.62775583825267));
#374032=CARTESIAN_POINT('Ctrl Pts',(0.697770099942208,-1.34203064007821,
-4.64954048263812));
#374033=CARTESIAN_POINT('Ctrl Pts',(0.517806603748821,-1.42120190289142,
-4.66039818213056));
#374034=CARTESIAN_POINT('Ctrl Pts',(0.219906998174013,-1.48790138370002,
-4.6765836469422));
#374035=CARTESIAN_POINT('Ctrl Pts',(0.110007116758885,-1.5,-4.68220728012721));
#374036=CARTESIAN_POINT('Ctrl Pts',(-1.65145674912992E-14,-1.5,-4.6875));
#374037=CARTESIAN_POINT('Origin',(0.,2.04523456705693E-15,3.99999999999998));
#374038=CARTESIAN_POINT('',(-6.2134141793955E-14,-1.5,-5.25000000000001));
#374039=CARTESIAN_POINT('',(-1.00853169777756E-13,-1.5,-5.18750000000001));
#374040=CARTESIAN_POINT('',(-1.83697019872103E-16,-1.5,3.99999999999998));
#374041=CARTESIAN_POINT('Ctrl Pts',(-1.24518451105615E-13,-1.49999999999999,
-5.25000000000001));
#374042=CARTESIAN_POINT('Ctrl Pts',(0.126459591807601,-1.50000000000001,
-5.24391571005236));
#374043=CARTESIAN_POINT('Ctrl Pts',(0.252644307137019,-1.4840124481302,
-5.23740054644236));
#374044=CARTESIAN_POINT('Ctrl Pts',(0.564762610399708,-1.40329255650796,
-5.22014152836333));
#374045=CARTESIAN_POINT('Ctrl Pts',(0.742572157483927,-1.31786453941667,
-5.20921366206577));
#374046=CARTESIAN_POINT('Ctrl Pts',(1.0580845573139,-1.08164511676511,-5.18747191402202));
#374047=CARTESIAN_POINT('Ctrl Pts',(1.19195911089947,-0.932072521810604,
-5.17687607725521));
#374048=CARTESIAN_POINT('Ctrl Pts',(1.38931421438151,-0.596685101977259,
-5.15806450819417));
#374049=CARTESIAN_POINT('Ctrl Pts',(1.45377925744972,-0.415698533628166,
-5.14809436297933));
#374050=CARTESIAN_POINT('Ctrl Pts',(1.51264085248949,-0.0319672768883563,
-5.12677595982711));
#374051=CARTESIAN_POINT('Ctrl Pts',(1.50367803973268,0.167512915529909,
-5.11569372691499));
#374052=CARTESIAN_POINT('Ctrl Pts',(1.40941588211803,0.549347408453337,
-5.09448069953035));
#374053=CARTESIAN_POINT('Ctrl Pts',(1.32589865595609,0.728160736685422,
-5.08523230836436));
#374054=CARTESIAN_POINT('Ctrl Pts',(1.09665318872791,1.04137334491635,-5.06550238045117));
#374055=CARTESIAN_POINT('Ctrl Pts',(0.954011352740898,1.17343566962486,
-5.05497112400887));
#374056=CARTESIAN_POINT('Ctrl Pts',(0.620156428552317,1.38039557202895,
-5.03315963530176));
#374057=CARTESIAN_POINT('Ctrl Pts',(0.430559381159025,1.45076520782745,
-5.02208293100041));
#374058=CARTESIAN_POINT('Ctrl Pts',(0.0441633336528842,1.51145122361622,
-5.00180671983615));
#374059=CARTESIAN_POINT('Ctrl Pts',(-0.148299786727769,1.50480739621165,
-4.99299846196797));
#374060=CARTESIAN_POINT('Ctrl Pts',(-0.52434652523053,1.41881411933161,
-4.97251720269054));
#374061=CARTESIAN_POINT('Ctrl Pts',(-0.70402444441196,1.33877315524592,
-4.96164908465981));
#374062=CARTESIAN_POINT('Ctrl Pts',(-1.02591325372277,1.11221258184287,
-4.93986885283989));
#374063=CARTESIAN_POINT('Ctrl Pts',(-1.16414042313644,0.96660041979913,
-4.92917361277171));
#374064=CARTESIAN_POINT('Ctrl Pts',(-1.37106782256107,0.6373938083197,-4.91007318552835));
#374065=CARTESIAN_POINT('Ctrl Pts',(-1.44072127261361,0.458753032930355,
-4.90048627960722));
#374066=CARTESIAN_POINT('Ctrl Pts',(-1.51089207521126,0.0779298891515337,
-4.87932943828618));
#374067=CARTESIAN_POINT('Ctrl Pts',(-1.50804545052884,-0.121111949225657,
-4.86827155837634));
#374068=CARTESIAN_POINT('Ctrl Pts',(-1.42551074484792,-0.506779807045686,
-4.84684556627523));
#374069=CARTESIAN_POINT('Ctrl Pts',(-1.34660798787456,-0.68959075654184,
-4.83730007489818));
#374070=CARTESIAN_POINT('Ctrl Pts',(-1.12550874088751,-1.01001651653471,
-4.81776171686236));
#374071=CARTESIAN_POINT('Ctrl Pts',(-0.987058116230062,-1.14568753259791,
-4.80733186874265));
#374072=CARTESIAN_POINT('Ctrl Pts',(-0.660264453047603,-1.36157902302987,
-4.78561201544666));
#374073=CARTESIAN_POINT('Ctrl Pts',(-0.473397980327392,-1.43727290020981,
-4.77451879038659));
#374074=CARTESIAN_POINT('Ctrl Pts',(-0.185580428376253,-1.49139155404108,
-4.75916786602213));
#374075=CARTESIAN_POINT('Ctrl Pts',(-0.0927904026472573,-1.5,-4.75446438032889));
#374076=CARTESIAN_POINT('Ctrl Pts',(1.53039141736488E-14,-1.5,-4.75));
#374077=CARTESIAN_POINT('Ctrl Pts',(-1.5671308213393E-14,-1.5,-4.6875));
#374078=CARTESIAN_POINT('Ctrl Pts',(-0.0801408922694299,-1.49999999999999,
-4.69135578047707));
#374079=CARTESIAN_POINT('Ctrl Pts',(-0.160321345391785,-1.49357843265124,
-4.69539184119727));
#374080=CARTESIAN_POINT('Ctrl Pts',(-0.437363833383036,-1.44871509963516,
-4.70996725781039));
#374081=CARTESIAN_POINT('Ctrl Pts',(-0.626538492873636,-1.37749677542739,
-4.72104721464233));
#374082=CARTESIAN_POINT('Ctrl Pts',(-0.959291920697377,-1.16910879918003,
-4.74284537629875));
#374083=CARTESIAN_POINT('Ctrl Pts',(-1.10127676354813,-1.03646702810196,
-4.75336111887653));
#374084=CARTESIAN_POINT('Ctrl Pts',(-1.32923971646631,-0.722111941960987,
-4.77306107728872));
#374085=CARTESIAN_POINT('Ctrl Pts',(-1.41203388153095,-0.542674501574207,
-4.78235141657912));
#374086=CARTESIAN_POINT('Ctrl Pts',(-1.50445922943713,-0.160227643083699,
-4.80359846427304));
#374087=CARTESIAN_POINT('Ctrl Pts',(-1.51245847028538,0.0391957489669181,
-4.81467754160918));
#374088=CARTESIAN_POINT('Ctrl Pts',(-1.45181407158714,0.422476196298371,
-4.83597089979427));
#374089=CARTESIAN_POINT('Ctrl Pts',(-1.38653641547424,0.603090284120421,
-4.84587607683253));
#374090=CARTESIAN_POINT('Ctrl Pts',(-1.18768177155032,0.937517984135334,
-4.86473313368287));
#374091=CARTESIAN_POINT('Ctrl Pts',(-1.05311969738469,1.08648082145367,
-4.87534511108691));
#374092=CARTESIAN_POINT('Ctrl Pts',(-0.736592126888934,1.32120342148533,
-4.89709412314598));
#374093=CARTESIAN_POINT('Ctrl Pts',(-0.558480316497194,1.4057926596232,
-4.90801323267833));
#374094=CARTESIAN_POINT('Ctrl Pts',(-0.184596736411954,1.50072769862936,
-4.92863879922915));
#374095=CARTESIAN_POINT('Ctrl Pts',(0.00716528927516818,1.5120192998048,
-4.93751087070187));
#374096=CARTESIAN_POINT('Ctrl Pts',(0.394973694910186,1.46092392160392,
-4.95758862737863));
#374097=CARTESIAN_POINT('Ctrl Pts',(0.586711051446983,1.39501101129075,
-4.96864450942151));
#374098=CARTESIAN_POINT('Ctrl Pts',(0.926204769872095,1.19557672223827,
-4.99051824992749));
#374099=CARTESIAN_POINT('Ctrl Pts',(1.07222963706745,1.06658270381478,-5.00112704180456));
#374100=CARTESIAN_POINT('Ctrl Pts',(1.30811708788819,0.759328293706288,
-5.02101102679895));
#374101=CARTESIAN_POINT('Ctrl Pts',(1.39536130354334,0.583714614795568,
-5.03007141028904));
#374102=CARTESIAN_POINT('Ctrl Pts',(1.49907896999085,0.205101626873878,
-5.05110546517359));
#374103=CARTESIAN_POINT('Ctrl Pts',(1.51303307166772,0.0054001348051989,
-5.06219999251074));
#374104=CARTESIAN_POINT('Ctrl Pts',(1.46343746122895,-0.380471291437901,
-5.08363729396869));
#374105=CARTESIAN_POINT('Ctrl Pts',(1.40322060533542,-0.563385559529108,
-5.09379919775153));
#374106=CARTESIAN_POINT('Ctrl Pts',(1.21358105044737,-0.90372417817919,
-5.11270689878765));
#374107=CARTESIAN_POINT('Ctrl Pts',(1.0832700197804,-1.05644402571708,-5.12306014758717));
#374108=CARTESIAN_POINT('Ctrl Pts',(0.772940467773571,-1.30035290347364,
-5.14476613172391));
#374109=CARTESIAN_POINT('Ctrl Pts',(0.596738508392062,-1.39005838763646,
-5.15573547145182));
#374110=CARTESIAN_POINT('Ctrl Pts',(0.275187786580223,-1.48101383286055,
-5.17373262791328));
#374111=CARTESIAN_POINT('Ctrl Pts',(0.137809822202473,-1.50000000000001,
-5.18086962183787));
#374112=CARTESIAN_POINT('Ctrl Pts',(-2.00776895109556E-13,-1.49999999999999,
-5.18750000000001));
#374113=CARTESIAN_POINT('Origin',(0.,2.04523456705693E-15,3.99999999999998));
#374114=CARTESIAN_POINT('',(-9.31093641809959E-14,-1.49999999999999,-5.75000000000001));
#374115=CARTESIAN_POINT('',(-3.50308222052939E-14,-1.49999999999999,-5.6875));
#374116=CARTESIAN_POINT('',(-1.83697019872103E-16,-1.5,3.99999999999998));
#374117=CARTESIAN_POINT('Ctrl Pts',(-1.85788884277116E-13,-1.49999999999999,
-5.75000000000001));
#374118=CARTESIAN_POINT('Ctrl Pts',(0.154014098631083,-1.50000000000001,
-5.7425899932247));
#374119=CARTESIAN_POINT('Ctrl Pts',(0.307309583004072,-1.4762855174169,
-5.73455582516667));
#374120=CARTESIAN_POINT('Ctrl Pts',(0.641758139830316,-1.36994648501272,
-5.71551079946263));
#374121=CARTESIAN_POINT('Ctrl Pts',(0.815495357558683,-1.274194834344,-5.70449209560319));
#374122=CARTESIAN_POINT('Ctrl Pts',(1.11839551347547,-1.01929042407315,
-5.68283812699377));
#374123=CARTESIAN_POINT('Ctrl Pts',(1.24380131179792,-0.861793831632132,
-5.67287743509064));
#374124=CARTESIAN_POINT('Ctrl Pts',(1.42213916078022,-0.514004943539909,
-5.65355583019663));
#374125=CARTESIAN_POINT('Ctrl Pts',(1.47607154328307,-0.328438783103053,
-5.64324659906125));
#374126=CARTESIAN_POINT('Ctrl Pts',(1.51193448137251,0.0603413622924671,
-5.62164770209483));
#374127=CARTESIAN_POINT('Ctrl Pts',(1.49061052871905,0.26014748319706,-5.61054736204458));
#374128=CARTESIAN_POINT('Ctrl Pts',(1.37309306628448,0.633855035717469,
-5.589785831349));
#374129=CARTESIAN_POINT('Ctrl Pts',(1.28038394458198,0.804842593549846,
-5.58091242921279));
#374130=CARTESIAN_POINT('Ctrl Pts',(1.03467992929997,1.10316165015626,-5.5608043488045));
#374131=CARTESIAN_POINT('Ctrl Pts',(0.883723504268778,1.22741493681494,
-5.5500899742339));
#374132=CARTESIAN_POINT('Ctrl Pts',(0.538414130864237,1.41409054620938,
-5.52829083566554));
#374133=CARTESIAN_POINT('Ctrl Pts',(0.346395106010818,1.47294668593921,
-5.51741742325455));
#374134=CARTESIAN_POINT('Ctrl Pts',(-0.0406105562722997,1.51144182268113,
-5.49772829529252));
#374135=CARTESIAN_POINT('Ctrl Pts',(-0.231538528745554,1.49415771958094,
-5.48869781177453));
#374136=CARTESIAN_POINT('Ctrl Pts',(-0.602512606107136,1.38757672171473,
-5.46788872988154));
#374137=CARTESIAN_POINT('Ctrl Pts',(-0.778411779409511,1.2970973463507,
-5.45691246097785));
#374138=CARTESIAN_POINT('Ctrl Pts',(-1.08776831186437,1.05181315973582,
-5.43521508824229));
#374139=CARTESIAN_POINT('Ctrl Pts',(-1.21743313452807,0.898531461080216,
-5.42491841450443));
#374140=CARTESIAN_POINT('Ctrl Pts',(-1.40565955761461,0.557300116317758,
-5.40596111757318));
#374141=CARTESIAN_POINT('Ctrl Pts',(-1.46510361883548,0.374045587193807,
-5.39578031039963));
#374142=CARTESIAN_POINT('Ctrl Pts',(-1.51300517467058,-0.0122122812649184,
-5.3743215399297));
#374143=CARTESIAN_POINT('Ctrl Pts',(-1.49813931299167,-0.211941038534931,
-5.36322549785915));
#374144=CARTESIAN_POINT('Ctrl Pts',(-1.39270451515173,-0.589956695012463,
-5.34222462805484));
#374145=CARTESIAN_POINT('Ctrl Pts',(-1.30478227037473,-0.764991809558107,
-5.33319326043181));
#374146=CARTESIAN_POINT('Ctrl Pts',(-1.06768136212527,-1.07115012178327,
-5.31328134010309));
#374147=CARTESIAN_POINT('Ctrl Pts',(-0.921042220249182,-1.19957139300912,
-5.30265890356605));
#374148=CARTESIAN_POINT('Ctrl Pts',(-0.58053074595446,-1.39760743819024,
-5.2807750363655));
#374149=CARTESIAN_POINT('Ctrl Pts',(-0.388411166202108,-1.46269511984064,
-5.26972368761799));
#374150=CARTESIAN_POINT('Ctrl Pts',(-0.126300182789163,-1.49601611959712,
-5.25618728372217));
#374151=CARTESIAN_POINT('Ctrl Pts',(-0.0631212183253676,-1.49999999999999,
-5.25303692103264));
#374152=CARTESIAN_POINT('Ctrl Pts',(-1.24084586568038E-13,-1.49999999999999,
-5.25000000000001));
#374153=CARTESIAN_POINT('Ctrl Pts',(-2.0152264253564E-13,-1.5,-5.18750000000001));
#374154=CARTESIAN_POINT('Ctrl Pts',(-0.0515794141709448,-1.49999999999999,
-5.18998161572135));
#374155=CARTESIAN_POINT('Ctrl Pts',(-0.103212185204464,-1.49733974540289,
-5.1925396945369));
#374156=CARTESIAN_POINT('Ctrl Pts',(-0.352539087313576,-1.47148866811489,
-5.20525352618786));
#374157=CARTESIAN_POINT('Ctrl Pts',(-0.5443141847556,-1.41183053316366,
-5.21613748028084));
#374158=CARTESIAN_POINT('Ctrl Pts',(-0.888775620428316,-1.22374931416049,
-5.23793486713741));
#374159=CARTESIAN_POINT('Ctrl Pts',(-1.03915996200753,-1.09892897471503,
-5.2486374687964));
#374160=CARTESIAN_POINT('Ctrl Pts',(-1.28371590709219,-0.799556796655997,
-5.26871956602526));
#374161=CARTESIAN_POINT('Ctrl Pts',(-1.37578798701838,-0.628034648928745,
-5.27760918617054));
#374162=CARTESIAN_POINT('Ctrl Pts',(-1.49170226899784,-0.253745006143942,
-5.29840305521414));
#374163=CARTESIAN_POINT('Ctrl Pts',(-1.51216527352526,-0.0539375062348138,
-5.30950347187576));
#374164=CARTESIAN_POINT('Ctrl Pts',(-1.47469344897427,0.33452809305927,
-5.33108489405877));
#374165=CARTESIAN_POINT('Ctrl Pts',(-1.42002246298498,0.519796028805142,
-5.34137755715577));
#374166=CARTESIAN_POINT('Ctrl Pts',(-1.24018233990018,0.867062757702468,
-5.36067015320562));
#374167=CARTESIAN_POINT('Ctrl Pts',(-1.11390065900744,1.02426007244313,
-5.37069243156819));
#374168=CARTESIAN_POINT('Ctrl Pts',(-0.809657539496625,1.27789866355297,
-5.3923758519003));
#374169=CARTESIAN_POINT('Ctrl Pts',(-0.635567058477546,1.37281716149636,
-5.40338840901649));
#374170=CARTESIAN_POINT('Ctrl Pts',(-0.266873761100909,1.48823898832821,
-5.42433333541366));
#374171=CARTESIAN_POINT('Ctrl Pts',(-0.0765198328215434,1.51003416255151,
-5.43353971108922));
#374172=CARTESIAN_POINT('Ctrl Pts',(0.311151008931872,1.48078997964258,
-5.45300387157364));
#374173=CARTESIAN_POINT('Ctrl Pts',(0.504498514843458,1.42653902888245,
-5.46381327864352));
#374174=CARTESIAN_POINT('Ctrl Pts',(0.854545493613196,1.24797427576227,
-5.48561505379311));
#374175=CARTESIAN_POINT('Ctrl Pts',(1.00873294315632,1.12701258997474,-5.4963934477455));
#374176=CARTESIAN_POINT('Ctrl Pts',(1.26097329689781,0.8347311900718,-5.51664829519834));
#374177=CARTESIAN_POINT('Ctrl Pts',(1.35730195217515,0.666754413238933,
-5.52545808815331));
#374178=CARTESIAN_POINT('Ctrl Pts',(1.48389311483301,0.296400750530683,
-5.54603329163711));
#374179=CARTESIAN_POINT('Ctrl Pts',(1.51011101383677,0.0966705802162286,
-5.55712941221014));
#374180=CARTESIAN_POINT('Ctrl Pts',(1.48341672623158,-0.293771154987738,
-5.57882061972147));
#374181=CARTESIAN_POINT('Ctrl Pts',(1.43370508323016,-0.48097460288667,
-5.58922081127141));
#374182=CARTESIAN_POINT('Ctrl Pts',(1.26387722187823,-0.831687904208848,
-5.60870488356709));
#374183=CARTESIAN_POINT('Ctrl Pts',(1.14337324878343,-0.990862750387745,
-5.61834672754103));
#374184=CARTESIAN_POINT('Ctrl Pts',(0.848073356367948,-1.25282640619913,
-5.63983111845616));
#374185=CARTESIAN_POINT('Ctrl Pts',(0.676399536691874,-1.35325001025456,
-5.65088032351349));
#374186=CARTESIAN_POINT('Ctrl Pts',(0.332360099323595,-1.47222341002712,
-5.67073774532188));
#374187=CARTESIAN_POINT('Ctrl Pts',(0.166678078102972,-1.5,-5.67948069722827));
#374188=CARTESIAN_POINT('Ctrl Pts',(-7.03603841856193E-14,-1.49999999999999,
-5.6875));
#374189=CARTESIAN_POINT('Origin',(0.,2.04523456705693E-15,3.99999999999998));
#374190=CARTESIAN_POINT('',(1.6836001146047E-16,-1.49999999999999,-6.25));
#374191=CARTESIAN_POINT('',(8.96943871370729E-16,-1.49999999999999,-6.1875));
#374192=CARTESIAN_POINT('',(-1.83697019872103E-16,-1.5,3.99999999999998));
#374193=CARTESIAN_POINT('Ctrl Pts',(-3.46944695195361E-16,-1.49999999999999,
-6.25));
#374194=CARTESIAN_POINT('Ctrl Pts',(0.184225546784952,-1.49999999999999,
-6.24113644424768));
#374195=CARTESIAN_POINT('Ctrl Pts',(0.366990843976295,-1.46606186050117,
-6.23140041868945));
#374196=CARTESIAN_POINT('Ctrl Pts',(0.723575025607657,-1.32872633861587,
-6.21042937864373));
#374197=CARTESIAN_POINT('Ctrl Pts',(0.892193681677509,-1.22191184689028,
-6.19934964055644));
#374198=CARTESIAN_POINT('Ctrl Pts',(1.17689583931665,-0.950384706872383,
-6.1781094810544));
#374199=CARTESIAN_POINT('Ctrl Pts',(1.29071292993964,-0.788900396449992,
-6.16882779980274));
#374200=CARTESIAN_POINT('Ctrl Pts',(1.44864026327719,-0.434191587073927,
-6.1491217548374));
#374201=CARTESIAN_POINT('Ctrl Pts',(1.49235076568262,-0.244851310904274,
-6.13860285060576));
#374202=CARTESIAN_POINT('Ctrl Pts',(1.50608106375903,0.147564878348468,
-6.11680195120283));
#374203=CARTESIAN_POINT('Ctrl Pts',(1.4729787888214,0.346992580603692,-6.10572263441087));
#374204=CARTESIAN_POINT('Ctrl Pts',(1.33371884038559,0.712504109963185,
-6.08541643833535));
#374205=CARTESIAN_POINT('Ctrl Pts',(1.23229372293241,0.876312040285589,
-6.07661342493556));
#374206=CARTESIAN_POINT('Ctrl Pts',(0.970814115657846,1.15994198807361,
-6.05615437180415));
#374207=CARTESIAN_POINT('Ctrl Pts',(0.812144175300407,1.27607139308219,
-6.04529454393355));
#374208=CARTESIAN_POINT('Ctrl Pts',(0.455677918591778,1.4428701772103,-6.02351075360213));
#374209=CARTESIAN_POINT('Ctrl Pts',(0.260633800603809,1.49050693322332,
-6.01280344587753));
#374210=CARTESIAN_POINT('Ctrl Pts',(-0.127850612998576,1.50656622384496,
-5.99366638940726));
#374211=CARTESIAN_POINT('Ctrl Pts',(-0.317461551819455,1.47828890900868,
-5.98412303810574));
#374212=CARTESIAN_POINT('Ctrl Pts',(-0.682739682995172,1.35007577555382,
-5.96298710989615));
#374213=CARTESIAN_POINT('Ctrl Pts',(-0.854019612196042,1.24879521492711,
-5.95193305155395));
#374214=CARTESIAN_POINT('Ctrl Pts',(-1.14791226642593,0.985543370965803,
-5.93048058341343));
#374215=CARTESIAN_POINT('Ctrl Pts',(-1.26751861985257,0.826060200022174,
-5.92089223333453));
#374216=CARTESIAN_POINT('Ctrl Pts',(-1.43576888205435,0.474810965013767,
-5.90137838694517));
#374217=CARTESIAN_POINT('Ctrl Pts',(-1.48469141456904,0.287313872985764,
-5.89096188183251));
#374218=CARTESIAN_POINT('Ctrl Pts',(-1.50967624051698,-0.10341320537901,
-5.86925482192336));
#374219=CARTESIAN_POINT('Ctrl Pts',(-1.48254819423185,-0.303116494536361,
-5.85816019474795));
#374220=CARTESIAN_POINT('Ctrl Pts',(-1.35427630041851,-0.672838245320214,
-5.83762009748218));
#374221=CARTESIAN_POINT('Ctrl Pts',(-1.25727455558041,-0.840259727840265,
-5.82881676893021));
#374222=CARTESIAN_POINT('Ctrl Pts',(-1.00381612065346,-1.13140836976017,
-5.80853478201853));
#374223=CARTESIAN_POINT('Ctrl Pts',(-0.849031785362385,-1.25174491652487,
-5.79774503536007));
#374224=CARTESIAN_POINT('Ctrl Pts',(-0.498119450944072,-1.42877830793129,
-5.77594416359281));
#374225=CARTESIAN_POINT('Ctrl Pts',(-0.304535941796269,-1.48216403035491,
-5.76514743593239));
#374226=CARTESIAN_POINT('Ctrl Pts',(-0.0707802209747663,-1.49874880089135,
-5.75344017050019));
#374227=CARTESIAN_POINT('Ctrl Pts',(-0.0353728198106626,-1.49999999999999,
-5.75170187558664));
#374228=CARTESIAN_POINT('Ctrl Pts',(-1.8603503134212E-13,-1.49999999999999,
-5.75000000000001));
#374229=CARTESIAN_POINT('Ctrl Pts',(-6.98779473907157E-14,-1.49999999999999,
-5.6875));
#374230=CARTESIAN_POINT('Ctrl Pts',(-0.0229199955894006,-1.49999999999999,
-5.68860273880195));
#374231=CARTESIAN_POINT('Ctrl Pts',(-0.0458574412197106,-1.49947467953825,
-5.68972090940436));
#374232=CARTESIAN_POINT('Ctrl Pts',(-0.267439001380728,-1.48930157366741,
-5.70066434346242));
#374233=CARTESIAN_POINT('Ctrl Pts',(-0.462268677088592,-1.44077292807513,
-5.71138610853854));
#374234=CARTESIAN_POINT('Ctrl Pts',(-0.817895460871673,-1.27237960162864,
-5.73317380255219));
#374235=CARTESIAN_POINT('Ctrl Pts',(-0.975971679508033,-1.15559144028853,
-5.74402336376015));
#374236=CARTESIAN_POINT('Ctrl Pts',(-1.23621500950152,-0.870795301504995,
-5.76445533066746));
#374237=CARTESIAN_POINT('Ctrl Pts',(-1.3369586063428,-0.706435810274456,
-5.7732535660958));
#374238=CARTESIAN_POINT('Ctrl Pts',(-1.47453372400099,-0.340269498138311,
-5.79359613899225));
#374239=CARTESIAN_POINT('Ctrl Pts',(-1.50671739912168,-0.140788233463958,
-5.80467843147416));
#374240=CARTESIAN_POINT('Ctrl Pts',(-1.49125281491075,0.251388985978111,
-5.8264660547765));
#374241=CARTESIAN_POINT('Ctrl Pts',(-1.44673726812926,0.440455366519274,
-5.83696974258434));
#374242=CARTESIAN_POINT('Ctrl Pts',(-1.28722595845462,0.79463863076866,
-5.8566465905982));
#374243=CARTESIAN_POINT('Ctrl Pts',(-1.1725299540558,0.955817438983461,
-5.86597044403223));
#374244=CARTESIAN_POINT('Ctrl Pts',(-0.886419821865895,1.22609190056284,
-5.88724354811813));
#374245=CARTESIAN_POINT('Ctrl Pts',(-0.717383582587183,1.33206570215302,
-5.89832002468317));
#374246=CARTESIAN_POINT('Ctrl Pts',(-0.354747129091054,1.4698244043826,
-5.91959400980432));
#374247=CARTESIAN_POINT('Ctrl Pts',(-0.165626270643064,1.50291400057419,
-5.92945035787782));
#374248=CARTESIAN_POINT('Ctrl Pts',(0.223359368904149,1.49654276868739,
-5.94834241684997));
#374249=CARTESIAN_POINT('Ctrl Pts',(0.419500896834944,1.45379593874528,
-5.95896669245532));
#374250=CARTESIAN_POINT('Ctrl Pts',(0.780426854798376,1.29578325048949,
-5.98072099204473));
#374251=CARTESIAN_POINT('Ctrl Pts',(0.942293426823095,1.18330491199423,
-5.99163319941387));
#374252=CARTESIAN_POINT('Ctrl Pts',(1.21050251090383,0.906071204019553,
-6.01223835132093));
#374253=CARTESIAN_POINT('Ctrl Pts',(1.31563867143019,0.745232081922239,
-6.02109821767093));
#374254=CARTESIAN_POINT('Ctrl Pts',(1.46401492968457,0.383320238168483,
-6.0412044312128));
#374255=CARTESIAN_POINT('Ctrl Pts',(1.50210104752628,0.184253983531882,
-6.05226366758151));
#374256=CARTESIAN_POINT('Ctrl Pts',(1.49780399834789,-0.209327391973654,
-6.07412929955404));
#374257=CARTESIAN_POINT('Ctrl Pts',(1.45848425593042,-0.400093452658332,
-6.08472741403652));
#374258=CARTESIAN_POINT('Ctrl Pts',(1.30913443149913,-0.757615020015232,
-6.10458972333413));
#374259=CARTESIAN_POINT('Ctrl Pts',(1.20001875731217,-0.920747042116454,
-6.11367371067817));
#374260=CARTESIAN_POINT('Ctrl Pts',(0.9229242446361,-1.1989526463398,-6.13473336008587));
#374261=CARTESIAN_POINT('Ctrl Pts',(0.756622398667581,-1.31026458135817,
-6.14582655957554));
#374262=CARTESIAN_POINT('Ctrl Pts',(0.397258326831598,-1.45896173369225,
-6.1672469479969));
#374263=CARTESIAN_POINT('Ctrl Pts',(0.208672976728849,-1.4976191275389,
-6.1773940813799));
#374264=CARTESIAN_POINT('Ctrl Pts',(0.0119181219976294,-1.4999644986125,
-6.18692560293834));
#374265=CARTESIAN_POINT('Ctrl Pts',(0.00595830572275474,-1.49999999999999,
-6.18721333088225));
#374266=CARTESIAN_POINT('Ctrl Pts',(-1.83697019872102E-16,-1.49999999999999,
-6.1875));
#374267=CARTESIAN_POINT('Origin',(0.,2.04523456705693E-15,3.99999999999998));
#374268=CARTESIAN_POINT('',(3.85353309639304E-14,-1.5,-6.75));
#374269=CARTESIAN_POINT('',(9.66138729396351E-14,-1.49999999999999,-6.68749999999999));
#374270=CARTESIAN_POINT('',(-1.83697019872103E-16,-1.5,3.99999999999998));
#374271=CARTESIAN_POINT('Ctrl Pts',(7.72543589477329E-14,-1.49999999999999,
-6.75));
#374272=CARTESIAN_POINT('Ctrl Pts',(0.0232667500201416,-1.49999999999999,
-6.74888057796773));
#374273=CARTESIAN_POINT('Ctrl Pts',(0.0465526615425619,-1.49945866467968,
-6.74774519693496));
#374274=CARTESIAN_POINT('Ctrl Pts',(0.26109336989109,-1.48945893012235,
-6.7371453318875));
#374275=CARTESIAN_POINT('Ctrl Pts',(0.448853229789164,-1.44401059158026,
-6.72684927756784));
#374276=CARTESIAN_POINT('Ctrl Pts',(0.803902279500261,-1.28191306194867,
-6.70526426304256));
#374277=CARTESIAN_POINT('Ctrl Pts',(0.96662140318891,-1.16413583124507,
-6.69416384581213));
#374278=CARTESIAN_POINT('Ctrl Pts',(1.23254250830526,-0.876382347002333,
-6.67337655833688));
#374279=CARTESIAN_POINT('Ctrl Pts',(1.33488958156617,-0.710826583354251,
-6.66449036574186));
#374280=CARTESIAN_POINT('Ctrl Pts',(1.4715727808645,-0.349253418196932,
-6.64440296767756));
#374281=CARTESIAN_POINT('Ctrl Pts',(1.50431998104034,-0.156563169032898,
-6.63369795383511));
#374282=CARTESIAN_POINT('Ctrl Pts',(1.49463806837838,0.235796778059404,
-6.61190017899665));
#374283=CARTESIAN_POINT('Ctrl Pts',(1.4502495785818,0.431669580882313,-6.6010183566176));
#374284=CARTESIAN_POINT('Ctrl Pts',(1.29124981480343,0.786632339865288,
-6.58129820334077));
#374285=CARTESIAN_POINT('Ctrl Pts',(1.18131804850252,0.943724119100809,
-6.57228829891116));
#374286=CARTESIAN_POINT('Ctrl Pts',(0.904432822699591,1.21258683472204,
-6.55149824350625));
#374287=CARTESIAN_POINT('Ctrl Pts',(0.73853881639193,1.32019753175719,-6.54052747837761));
#374288=CARTESIAN_POINT('Ctrl Pts',(0.37199886870174,1.4666851530346,-6.51882321633093));
#374289=CARTESIAN_POINT('Ctrl Pts',(0.174550537027293,1.5030068728719,-6.50848159087472));
#374290=CARTESIAN_POINT('Ctrl Pts',(-0.215025253801735,1.49673036131451,
-6.48956376935605));
#374291=CARTESIAN_POINT('Ctrl Pts',(-0.403523717010473,1.45725170989118,
-6.47939800361023));
#374292=CARTESIAN_POINT('Ctrl Pts',(-0.762392310665629,1.30692900901181,
-6.45795629976771));
#374293=CARTESIAN_POINT('Ctrl Pts',(-0.928274152621032,1.19483005017501,
-6.4468614459578));
#374294=CARTESIAN_POINT('Ctrl Pts',(-1.20402389510064,0.915459286317851,
-6.42583413129097));
#374295=CARTESIAN_POINT('Ctrl Pts',(-1.31231660320128,0.752036143782759,
-6.41677978576566));
#374296=CARTESIAN_POINT('Ctrl Pts',(-1.46014657514565,0.394022007304996,
-6.3968901115169));
#374297=CARTESIAN_POINT('Ctrl Pts',(-1.49868303625013,0.203013542218261,
-6.3862785301232));
#374298=CARTESIAN_POINT('Ctrl Pts',(-1.501301757405,-0.190751443848303,
-6.36440269756394));
#374299=CARTESIAN_POINT('Ctrl Pts',(-1.46233116010113,-0.389741049238268,
-6.35334771948672));
#374300=CARTESIAN_POINT('Ctrl Pts',(-1.31234084291122,-0.751005695645993,
-6.33327746135296));
#374301=CARTESIAN_POINT('Ctrl Pts',(-1.2065431930395,-0.911321883774327,
-6.32440200633597));
#374302=CARTESIAN_POINT('Ctrl Pts',(-0.937135562044617,-1.18740768650955,
-6.30377107557028));
#374303=CARTESIAN_POINT('Ctrl Pts',(-0.774706139362372,-1.2992242782468,
-6.29285016989064));
#374304=CARTESIAN_POINT('Ctrl Pts',(-0.413005804342069,-1.45565358411587,
-6.27110259591178));
#374305=CARTESIAN_POINT('Ctrl Pts',(-0.216681381152124,-1.49752351779781,
-6.26049387898363));
#374306=CARTESIAN_POINT('Ctrl Pts',(-0.0119189402414127,-1.49996449327836,
-6.25057443657752));
#374307=CARTESIAN_POINT('Ctrl Pts',(-0.00595875314440546,-1.49999999999999,
-6.25028669064433));
#374308=CARTESIAN_POINT('Ctrl Pts',(-1.83697019872102E-16,-1.49999999999999,
-6.25));
#374309=CARTESIAN_POINT('Ctrl Pts',(-5.55111512312578E-16,-1.49999999999999,
-6.1875));
#374310=CARTESIAN_POINT('Ctrl Pts',(-0.192662798346109,-1.49999999999999,
-6.19676949320733));
#374311=CARTESIAN_POINT('Ctrl Pts',(-0.383648229024422,-1.46288166459859,
-6.20698934889733));
#374312=CARTESIAN_POINT('Ctrl Pts',(-0.743963998216072,-1.3171361389242,
-6.22837353624962));
#374313=CARTESIAN_POINT('Ctrl Pts',(-0.90934848008717,-1.20889212997927,
-6.23933737886988));
#374314=CARTESIAN_POINT('Ctrl Pts',(-1.18512264087765,-0.938949350636919,
-6.2601039799045));
#374315=CARTESIAN_POINT('Ctrl Pts',(-1.29443917043375,-0.7813825258734,
-6.26908985967365));
#374316=CARTESIAN_POINT('Ctrl Pts',(-1.45200343693213,-0.425734227595574,
-6.28884809846687));
#374317=CARTESIAN_POINT('Ctrl Pts',(-1.49559102134978,-0.229678146345099,
-6.29974010298079));
#374318=CARTESIAN_POINT('Ctrl Pts',(-1.50366469040147,0.162645572469948,
-6.32153586513718));
#374319=CARTESIAN_POINT('Ctrl Pts',(-1.47015674430518,0.355125750711791,
-6.33222920837284));
#374320=CARTESIAN_POINT('Ctrl Pts',(-1.33201695307452,0.716239199926321,
-6.35229106666254));
#374321=CARTESIAN_POINT('Ctrl Pts',(-1.22890179572686,0.881516273384371,
-6.36119433126865));
#374322=CARTESIAN_POINT('Ctrl Pts',(-0.961699964356268,1.16819037229097,
-6.38201325478854));
#374323=CARTESIAN_POINT('Ctrl Pts',(-0.798559586219515,1.28523512905986,
-6.39311359313487));
#374324=CARTESIAN_POINT('Ctrl Pts',(-0.442993303102102,1.44580907279673,
-6.41468117123361));
#374325=CARTESIAN_POINT('Ctrl Pts',(-0.255126968641665,1.49048289525025,
-6.42496083397724));
#374326=CARTESIAN_POINT('Ctrl Pts',(0.135766507784468,1.50715365684147,
-6.44423078184137));
#374327=CARTESIAN_POINT('Ctrl Pts',(0.33518385049537,1.47568001957899,-6.45430209553762));
#374328=CARTESIAN_POINT('Ctrl Pts',(0.706628778545216,1.33761690521872,
-6.47600833448086));
#374329=CARTESIAN_POINT('Ctrl Pts',(0.875449082209859,1.23374816864286,
-6.48701594781064));
#374330=CARTESIAN_POINT('Ctrl Pts',(1.15879866469514,0.971218242450404,
-6.50794110890399));
#374331=CARTESIAN_POINT('Ctrl Pts',(1.27231898273961,0.816863702036046,
-6.51711868322019));
#374332=CARTESIAN_POINT('Ctrl Pts',(1.43961121071636,0.465912722300956,
-6.53661595987214));
#374333=CARTESIAN_POINT('Ctrl Pts',(1.48862412376949,0.27116790750538,-6.54743511624967));
#374334=CARTESIAN_POINT('Ctrl Pts',(1.50763248614143,-0.121271229630326,
-6.56923729053499));
#374335=CARTESIAN_POINT('Ctrl Pts',(1.47931526745495,-0.315120236426917,
-6.58000667980147));
#374336=CARTESIAN_POINT('Ctrl Pts',(1.35107045234328,-0.679324824317332,
-6.60024026801761));
#374337=CARTESIAN_POINT('Ctrl Pts',(1.25312237646632,-0.84649771413236,
-6.60905628027751));
#374338=CARTESIAN_POINT('Ctrl Pts',(0.994597339128767,-1.14041209074646,
-6.62965886017505));
#374339=CARTESIAN_POINT('Ctrl Pts',(0.834363033638614,-1.26237496255653,
-6.64075599434268));
#374340=CARTESIAN_POINT('Ctrl Pts',(0.48241297577243,-1.43320619890963,
-6.66243451151779));
#374341=CARTESIAN_POINT('Ctrl Pts',(0.29532698578952,-1.48310641479776,
-6.67282180751565));
#374342=CARTESIAN_POINT('Ctrl Pts',(0.0692686773756122,-1.49880173726729,
-6.68413402412997));
#374343=CARTESIAN_POINT('Ctrl Pts',(0.0346164231920939,-1.49999999999999,
-6.68583451656264));
#374344=CARTESIAN_POINT('Ctrl Pts',(1.93411442899142E-13,-1.49999999999999,
-6.68749999999999));
#374345=CARTESIAN_POINT('Origin',(0.,2.04523456705693E-15,3.99999999999998));
#374346=CARTESIAN_POINT('',(1.21781241129107E-13,-1.49999999999999,-7.24999999999999));
#374347=CARTESIAN_POINT('',(8.11262617461138E-14,-1.49999999999999,-7.18749999999999));
#374348=CARTESIAN_POINT('',(-1.83697019872103E-16,-1.5,3.99999999999998));
#374349=CARTESIAN_POINT('Ctrl Pts',(2.43746179278087E-13,-1.49999999999999,
-7.24999999999999));
#374350=CARTESIAN_POINT('Ctrl Pts',(0.0505804368405312,-1.49999999999999,
-7.24756644759786));
#374351=CARTESIAN_POINT('Ctrl Pts',(0.101216981078785,-1.49744178419118,
-7.245059134177));
#374352=CARTESIAN_POINT('Ctrl Pts',(0.34323090569452,-1.47283692653746,
-7.2327317655318));
#374353=CARTESIAN_POINT('Ctrl Pts',(0.529191373170625,-1.41668427876357,
-7.2222249425973));
#374354=CARTESIAN_POINT('Ctrl Pts',(0.876424344163527,-1.23365577819351,
-7.20043456347528));
#374355=CARTESIAN_POINT('Ctrl Pts',(1.03298496670605,-1.10588550053493,
-7.18935286263176));
#374356=CARTESIAN_POINT('Ctrl Pts',(1.2810179099327,-0.80342656691991,-7.16901773504191));
#374357=CARTESIAN_POINT('Ctrl Pts',(1.37281774817456,-0.633935948345838,
-7.16021866379694));
#374358=CARTESIAN_POINT('Ctrl Pts',(1.48900331988238,-0.266060519028003,
-7.13978113994595));
#374359=CARTESIAN_POINT('Ctrl Pts',(1.51092916119493,-0.0707302567385103,
-7.12892945870764));
#374360=CARTESIAN_POINT('Ctrl Pts',(1.47857984332832,0.321434519883531,
-7.10714252667309));
#374361=CARTESIAN_POINT('Ctrl Pts',(1.42301176927557,0.514373323390137,
-7.09642370425605));
#374362=CARTESIAN_POINT('Ctrl Pts',(1.24393735982193,0.85947590277909,-7.07725133873445));
#374363=CARTESIAN_POINT('Ctrl Pts',(1.125208310326,1.00995833176182,-7.06774887863388));
#374364=CARTESIAN_POINT('Ctrl Pts',(0.832539360702016,1.26320526018224,
-7.04663320032924));
#374365=CARTESIAN_POINT('Ctrl Pts',(0.659621221770886,1.36151009664086,
-7.03558298258931));
#374366=CARTESIAN_POINT('Ctrl Pts',(0.285019425604324,1.48588424625999,
-7.01410510777858));
#374367=CARTESIAN_POINT('Ctrl Pts',(0.0869552392775818,1.51046555989123,
-7.00447434589729));
#374368=CARTESIAN_POINT('Ctrl Pts',(-0.301619063180882,1.48184988803323,
-6.98498417627974));
#374369=CARTESIAN_POINT('Ctrl Pts',(-0.488569448527852,1.4311299529593,
-6.97458063458559));
#374370=CARTESIAN_POINT('Ctrl Pts',(-0.839925423151456,1.25869501755417,
-6.95288615305792));
#374371=CARTESIAN_POINT('Ctrl Pts',(-0.999690372362026,1.13596602621689,
-6.94179031970685));
#374372=CARTESIAN_POINT('Ctrl Pts',(-1.2568468840452,0.840924871256338,
-6.92122228363205));
#374373=CARTESIAN_POINT('Ctrl Pts',(-1.35398756602698,0.673450998433365,
-6.91241394435736));
#374374=CARTESIAN_POINT('Ctrl Pts',(-1.4806657203477,0.308763861472977,
-6.89215354785956));
#374375=CARTESIAN_POINT('Ctrl Pts',(-1.50815645010109,0.114710740560849,
-6.88137281892));
#374376=CARTESIAN_POINT('Ctrl Pts',(-1.48741533558303,-0.277718535298315,
-6.85957119248338));
#374377=CARTESIAN_POINT('Ctrl Pts',(-1.43754704272193,-0.472241568275601,
-6.84876435731798));
#374378=CARTESIAN_POINT('Ctrl Pts',(-1.2687196939139,-0.82244032610959,
-6.82930887077165));
#374379=CARTESIAN_POINT('Ctrl Pts',(-1.15452830518383,-0.976289341653814,
-6.82009478726942));
#374380=CARTESIAN_POINT('Ctrl Pts',(-0.869973418591145,-1.23762907166495,
-6.79914469696021));
#374381=CARTESIAN_POINT('Ctrl Pts',(-0.700614908967324,-1.34078938616193,
-6.78813086757523));
#374382=CARTESIAN_POINT('Ctrl Pts',(-0.350645763193648,-1.46906016400802,
-6.76772989203613));
#374383=CARTESIAN_POINT('Ctrl Pts',(-0.175911284893246,-1.5,-6.75846353564056));
#374384=CARTESIAN_POINT('Ctrl Pts',(7.79237785408782E-14,-1.5,-6.75));
#374385=CARTESIAN_POINT('Ctrl Pts',(1.91322652165482E-13,-1.49999999999999,
-6.68749999999999));
#374386=CARTESIAN_POINT('Ctrl Pts',(-0.162786381555151,-1.5,-6.69533206343426));
#374387=CARTESIAN_POINT('Ctrl Pts',(-0.324710088578347,-1.47350658779939,
-6.70385854953744));
#374388=CARTESIAN_POINT('Ctrl Pts',(-0.666002058072663,-1.35838692766106,
-6.72347673541294));
#374389=CARTESIAN_POINT('Ctrl Pts',(-0.838378458746723,-1.25932329927725,
-6.7345219663123));
#374390=CARTESIAN_POINT('Ctrl Pts',(-1.12979566663392,-1.00481857195472,
-6.75561235902294));
#374391=CARTESIAN_POINT('Ctrl Pts',(-1.24782220338759,-0.85382075474369,
-6.76506551362534));
#374392=CARTESIAN_POINT('Ctrl Pts',(-1.4253255584943,-0.507928449458877,
-6.78428175280783));
#374393=CARTESIAN_POINT('Ctrl Pts',(-1.48002113080588,-0.314735041226525,
-6.79501471993186));
#374394=CARTESIAN_POINT('Ctrl Pts',(-1.51058643373556,0.0774928425069627,
-6.81680515791705));
#374395=CARTESIAN_POINT('Ctrl Pts',(-1.48780216978478,0.272637047754367,
-6.82764650265302));
#374396=CARTESIAN_POINT('Ctrl Pts',(-1.3700037705473,0.640027882315319,
-6.84805710457308));
#374397=CARTESIAN_POINT('Ctrl Pts',(-1.27739092395359,0.809207407080584,
-6.8568528173796));
#374398=CARTESIAN_POINT('Ctrl Pts',(-1.02796030885468,1.11054098969522,
-6.87722393073875));
#374399=CARTESIAN_POINT('Ctrl Pts',(-0.870900564212917,1.23754669865543,
-6.88830840758607));
#374400=CARTESIAN_POINT('Ctrl Pts',(-0.523018030216007,1.41896393786654,
-6.91008528156273));
#374401=CARTESIAN_POINT('Ctrl Pts',(-0.336896352617723,1.474288258976,-6.92057685164883));
#374402=CARTESIAN_POINT('Ctrl Pts',(0.0498552654747803,1.51195041648126,
-6.94023061859191));
#374403=CARTESIAN_POINT('Ctrl Pts',(0.246926905216432,1.49248780031196,
-6.94958894847998));
#374404=CARTESIAN_POINT('Ctrl Pts',(0.623742977622026,1.37838936499508,
-6.97088792119753));
#374405=CARTESIAN_POINT('Ctrl Pts',(0.799624885290026,1.28437132678396,
-6.98196165559821));
#374406=CARTESIAN_POINT('Ctrl Pts',(1.09925996059572,1.03818943041962,-7.00321624089053));
#374407=CARTESIAN_POINT('Ctrl Pts',(1.22191799893799,0.890551336592612,
-7.01302492574487));
#374408=CARTESIAN_POINT('Ctrl Pts',(1.40967318496998,0.549866213456369,
-7.03195187703022));
#374409=CARTESIAN_POINT('Ctrl Pts',(1.47005016346408,0.358410495614678,
-7.04258830579921));
#374410=CARTESIAN_POINT('Ctrl Pts',(1.51227913759432,-0.0332570310114007,
-7.06434761283399));
#374411=CARTESIAN_POINT('Ctrl Pts',(1.49512817303511,-0.229550342745992,
-7.07525279681925));
#374412=CARTESIAN_POINT('Ctrl Pts',(1.38788135235578,-0.600074744888264,
-7.09583748582715));
#374413=CARTESIAN_POINT('Ctrl Pts',(1.30053724896104,-0.771299092575987,
-7.10468618056224));
#374414=CARTESIAN_POINT('Ctrl Pts',(1.06021787981432,-1.07989970708138,
-7.12482079089309));
#374415=CARTESIAN_POINT('Ctrl Pts',(0.9064637152035,-1.21183833271368,-7.13588325341013));
#374416=CARTESIAN_POINT('Ctrl Pts',(0.562929411680457,-1.40368124708872,
-7.15774052513845));
#374417=CARTESIAN_POINT('Ctrl Pts',(0.377919674176932,-1.46437831282019,
-7.16832783988797));
#374418=CARTESIAN_POINT('Ctrl Pts',(0.124490572931739,-1.49612975091501,
-7.18140293759819));
#374419=CARTESIAN_POINT('Ctrl Pts',(0.0622143729691964,-1.49999999999999,
-7.1845067095849));
#374420=CARTESIAN_POINT('Ctrl Pts',(1.624362205121E-13,-1.49999999999999,
-7.18749999999999));
#374421=CARTESIAN_POINT('Origin',(0.,2.04523456705693E-15,3.99999999999998));
#374422=CARTESIAN_POINT('',(5.62415717769822E-15,-1.49999999999999,-7.75));
#374423=CARTESIAN_POINT('',(1.752254379318E-15,-1.49999999999999,-7.6875));
#374424=CARTESIAN_POINT('',(-1.83697019872103E-16,-1.5,3.99999999999998));
#374425=CARTESIAN_POINT('Ctrl Pts',(1.14320113752685E-14,-1.49999999999999,
-7.75));
#374426=CARTESIAN_POINT('Ctrl Pts',(0.0793911424341125,-1.49999999999999,
-7.7461802918787));
#374427=CARTESIAN_POINT('Ctrl Pts',(0.158826622847581,-1.49369800153929,
-7.74218339503251));
#374428=CARTESIAN_POINT('Ctrl Pts',(0.428724322123408,-1.45040567746368,
-7.72799537136398));
#374429=CARTESIAN_POINT('Ctrl Pts',(0.612130401408451,-1.38302694792622,
-7.71729961088408));
#374430=CARTESIAN_POINT('Ctrl Pts',(0.94769719923993,-1.1795822442898,-7.69550340402815));
#374431=CARTESIAN_POINT('Ctrl Pts',(1.09557798558456,-1.04368206740413,
-7.68461348146432));
#374432=CARTESIAN_POINT('Ctrl Pts',(1.32452628266381,-0.729217625494919,
-7.66486307799885));
#374433=CARTESIAN_POINT('Ctrl Pts',(1.40617678145354,-0.555702613677449,
-7.65587236742646));
#374434=CARTESIAN_POINT('Ctrl Pts',(1.50176023982819,-0.181816780657192,
-7.63510093225867));
#374435=CARTESIAN_POINT('Ctrl Pts',(1.51264482580004,0.0155582913297568,
-7.62413565048162));
#374436=CARTESIAN_POINT('Ctrl Pts',(1.45754056210491,0.406351840753956,
-7.60242489773583));
#374437=CARTESIAN_POINT('Ctrl Pts',(1.39090164260854,0.59572276810637,-7.59203859847834));
#374438=CARTESIAN_POINT('Ctrl Pts',(1.19182946286311,0.930567676884839,
-7.57315948629859));
#374439=CARTESIAN_POINT('Ctrl Pts',(1.06392093210996,1.07445894599363,-7.56300850454596));
#374440=CARTESIAN_POINT('Ctrl Pts',(0.755224267438086,1.31107367371899,
-7.5415836980164));
#374441=CARTESIAN_POINT('Ctrl Pts',(0.575577084393085,1.3992836939761,-7.53049014055174));
#374442=CARTESIAN_POINT('Ctrl Pts',(0.196027137929204,1.49979221781333,
-7.50943713179834));
#374443=CARTESIAN_POINT('Ctrl Pts',(0.000225705107454212,1.51254645028954,
-7.50035937175002));
#374444=CARTESIAN_POINT('Ctrl Pts',(-0.384003545441531,1.46280504294404,
-7.48049142755418));
#374445=CARTESIAN_POINT('Ctrl Pts',(-0.568834589062393,1.40130948299218,
-7.46989052982309));
#374446=CARTESIAN_POINT('Ctrl Pts',(-0.911695294333243,1.20792225401907,
-7.44802276897806));
#374447=CARTESIAN_POINT('Ctrl Pts',(-1.06494436667421,1.07525582562551,
-7.43696439098082));
#374448=CARTESIAN_POINT('Ctrl Pts',(-1.30390007262948,0.765581267101937,
-7.41686555814758));
#374449=CARTESIAN_POINT('Ctrl Pts',(-1.39046161160093,0.594047214686918,
-7.4080026230381));
#374450=CARTESIAN_POINT('Ctrl Pts',(-1.4961212510204,0.223059015381023,
-7.38739216752111));
#374451=CARTESIAN_POINT('Ctrl Pts',(-1.51242162242496,0.0266068244045978,
-7.37647815691131));
#374452=CARTESIAN_POINT('Ctrl Pts',(-1.46844042785702,-0.364946348707522,
-7.35472520284953));
#374453=CARTESIAN_POINT('Ctrl Pts',(-1.40721461990083,-0.556126100840495,
-7.3441041055088));
#374454=CARTESIAN_POINT('Ctrl Pts',(-1.21792271522213,-0.896019815330353,
-7.32522112137048));
#374455=CARTESIAN_POINT('Ctrl Pts',(-1.09456049740161,-1.04315479321923,
-7.31535221111767));
#374456=CARTESIAN_POINT('Ctrl Pts',(-0.79368356374764,-1.28806524540754,
-7.29407319478149));
#374457=CARTESIAN_POINT('Ctrl Pts',(-0.617282604111907,-1.38130777081686,
-7.28299602950365));
#374458=CARTESIAN_POINT('Ctrl Pts',(-0.288744953791062,-1.47908794514549,
-7.26447313847911));
#374459=CARTESIAN_POINT('Ctrl Pts',(-0.144629888666687,-1.49999999999999,
-7.25695850876289));
#374460=CARTESIAN_POINT('Ctrl Pts',(2.4308680068863E-13,-1.49999999999999,
-7.24999999999999));
#374461=CARTESIAN_POINT('Ctrl Pts',(1.61641533491519E-13,-1.5,-7.18749999999999));
#374462=CARTESIAN_POINT('Ctrl Pts',(-0.131622357866343,-1.5,-7.19383268364545));
#374463=CARTESIAN_POINT('Ctrl Pts',(-0.262921317301102,-1.48268039727666,
-7.20063090785231));
#374464=CARTESIAN_POINT('Ctrl Pts',(-0.581813302325864,-1.39668966571048,
-7.21836223706774));
#374465=CARTESIAN_POINT('Ctrl Pts',(-0.760986449107481,-1.30772428277316,
-7.22945396974872));
#374466=CARTESIAN_POINT('Ctrl Pts',(-1.06851918038896,-1.06987201850085,
-7.25085715252211));
#374467=CARTESIAN_POINT('Ctrl Pts',(-1.19575846111547,-0.925497279701485,
-7.26098936468145));
#374468=CARTESIAN_POINT('Ctrl Pts',(-1.3933783893132,-0.589901638636698,
-7.27981945905066));
#374469=CARTESIAN_POINT('Ctrl Pts',(-1.45922347640908,-0.400263072301958,
-7.29026316264993));
#374470=CARTESIAN_POINT('Ctrl Pts',(-1.51268581454927,-0.00932820601693203,
-7.31198176633244));
#374471=CARTESIAN_POINT('Ctrl Pts',(-1.50099855028636,0.187919703858646,
-7.32293998354775));
#374472=CARTESIAN_POINT('Ctrl Pts',(-1.40392453846296,0.56138202670716,
-7.34368789037266));
#374473=CARTESIAN_POINT('Ctrl Pts',(-1.32155358063126,0.734602306409417,
-7.35265567666203));
#374474=CARTESIAN_POINT('Ctrl Pts',(-1.09129230738471,1.04816296412075,
-7.3724441456062));
#374475=CARTESIAN_POINT('Ctrl Pts',(-0.942853330910693,1.1834581959791,
-7.38334412007661));
#374476=CARTESIAN_POINT('Ctrl Pts',(-0.60651714013915,1.38548711548125,
-7.40513801703057));
#374477=CARTESIAN_POINT('Ctrl Pts',(-0.422914749264889,1.45210020630605,
-7.41582195481419));
#374478=CARTESIAN_POINT('Ctrl Pts',(-0.0408496404733512,1.5118368221128,
-7.43586342137066));
#374479=CARTESIAN_POINT('Ctrl Pts',(0.153956628964715,1.50453306863169,
-7.44478132319164));
#374480=CARTESIAN_POINT('Ctrl Pts',(0.535587727485882,1.41515179392173,
-7.46562537116655));
#374481=CARTESIAN_POINT('Ctrl Pts',(0.718181777986944,1.33180900745106,
-7.47672550891929));
#374482=CARTESIAN_POINT('Ctrl Pts',(1.03417691378856,1.10320535164218,-7.49827893352934));
#374483=CARTESIAN_POINT('Ctrl Pts',(1.1663051313683,0.962464837359553,-7.50854541409168));
#374484=CARTESIAN_POINT('Ctrl Pts',(1.37524402475767,0.631462669396288,
-7.52779249595254));
#374485=CARTESIAN_POINT('Ctrl Pts',(1.44714609790656,0.442545202076605,
-7.53791415544024));
#374486=CARTESIAN_POINT('Ctrl Pts',(1.51190998266283,0.05142103028195,-7.5596432760955));
#374487=CARTESIAN_POINT('Ctrl Pts',(1.50566267484778,-0.146623862090228,
-7.57064577011617));
#374488=CARTESIAN_POINT('Ctrl Pts',(1.41867570620449,-0.522916883378641,
-7.59155093796553));
#374489=CARTESIAN_POINT('Ctrl Pts',(1.34114187901499,-0.698143998507512,
-7.60070050344159));
#374490=CARTESIAN_POINT('Ctrl Pts',(1.11972047582304,-1.01773391998754,
-7.62023114348858));
#374491=CARTESIAN_POINT('Ctrl Pts',(0.975078857061156,-1.1570464511819,
-7.6310600091491));
#374492=CARTESIAN_POINT('Ctrl Pts',(0.644025265587001,-1.3685277794625,
-7.65286231383638));
#374493=CARTESIAN_POINT('Ctrl Pts',(0.461801781543798,-1.44027365666263,
-7.66362248633347));
#374494=CARTESIAN_POINT('Ctrl Pts',(0.181365339759811,-1.49177900289783,
-7.67854569499177));
#374495=CARTESIAN_POINT('Ctrl Pts',(0.0906779845837288,-1.49999999999999,
-7.68313725343258));
#374496=CARTESIAN_POINT('Ctrl Pts',(3.68820577850811E-15,-1.49999999999999,
-7.6875));
#374497=CARTESIAN_POINT('Origin',(0.,2.04523456705693E-15,3.99999999999998));
#374498=CARTESIAN_POINT('',(-4.27253208704016E-15,-1.49999999999999,-8.25));
#374499=CARTESIAN_POINT('',(-3.69667736044839E-14,-1.49999999999999,-8.1875));
#374500=CARTESIAN_POINT('',(-1.83697019872103E-16,-1.5,3.99999999999998));
#374501=CARTESIAN_POINT('Ctrl Pts',(-8.11850586757146E-15,-1.49999999999999,
-8.25));
#374502=CARTESIAN_POINT('Ctrl Pts',(0.106980697927961,-1.5,-8.2448528887711));
#374503=CARTESIAN_POINT('Ctrl Pts',(0.213877795545196,-1.48855780985152,
-8.23939196114871));
#374504=CARTESIAN_POINT('Ctrl Pts',(0.509095079291007,-1.42432975528461,
-8.22340420033518));
#374505=CARTESIAN_POINT('Ctrl Pts',(0.689431848522612,-1.34631612532873,
-8.21256069820357));
#374506=CARTESIAN_POINT('Ctrl Pts',(1.01363305676546,-1.12341811902394,
-8.19077094901311));
#374507=CARTESIAN_POINT('Ctrl Pts',(1.15345990845384,-0.979323296244408,
-8.1800408925085));
#374508=CARTESIAN_POINT('Ctrl Pts',(1.36395558444277,-0.652454566336543,
-8.16083372763366));
#374509=CARTESIAN_POINT('Ctrl Pts',(1.43554513383051,-0.474669224619041,
-8.15137051247875));
#374510=CARTESIAN_POINT('Ctrl Pts',(1.50988936886954,-0.0949478172424911,
-8.13027487873561));
#374511=CARTESIAN_POINT('Ctrl Pts',(1.50930086684915,0.103885255945463,
-8.11922859689184));
#374512=CARTESIAN_POINT('Ctrl Pts',(1.43113940933133,0.490935718138837,
-8.09772579343666));
#374513=CARTESIAN_POINT('Ctrl Pts',(1.35395742288841,0.67524459106288,-8.08805217935172));
#374514=CARTESIAN_POINT('Ctrl Pts',(1.13587079804451,0.998311822706801,
-8.06858539195381));
#374515=CARTESIAN_POINT('Ctrl Pts',(0.998980064342097,1.13527418490466,
-8.0581947233967));
#374516=CARTESIAN_POINT('Ctrl Pts',(0.6748347447419,1.35438460105627,-8.03651287398741));
#374517=CARTESIAN_POINT('Ctrl Pts',(0.489005750514352,1.43200713177716,
-8.02541599092512));
#374518=CARTESIAN_POINT('Ctrl Pts',(0.105145394201939,1.50857778172861,
-8.00482053842245));
#374519=CARTESIAN_POINT('Ctrl Pts',(-0.088574936488778,1.5096411960585,
-7.99600624738277));
#374520=CARTESIAN_POINT('Ctrl Pts',(-0.468032439517269,1.43827208746729,
-7.97576711451751));
#374521=CARTESIAN_POINT('Ctrl Pts',(-0.650020674823016,1.36570207352387,
-7.96499536774327));
#374522=CARTESIAN_POINT('Ctrl Pts',(-0.980198636604201,1.15271161612822,
-7.94319327155604));
#374523=CARTESIAN_POINT('Ctrl Pts',(-1.12421838283135,1.01276247139593,
-7.93237664204241));
#374524=CARTESIAN_POINT('Ctrl Pts',(-1.34421180483883,0.692210599243926,
-7.91288798492019));
#374525=CARTESIAN_POINT('Ctrl Pts',(-1.42096690840797,0.516654177373473,
-7.90370300985401));
#374526=CARTESIAN_POINT('Ctrl Pts',(-1.50631278814488,0.139908538316974,
-7.8827726965731));
#374527=CARTESIAN_POINT('Ctrl Pts',(-1.51167357144707,-0.058251900989222,
-7.87176378327831));
#374528=CARTESIAN_POINT('Ctrl Pts',(-1.44515794855276,-0.448857478504078,
-7.85006347341638));
#374529=CARTESIAN_POINT('Ctrl Pts',(-1.372564451948,-0.637170911603667,
-7.84000501266196));
#374530=CARTESIAN_POINT('Ctrl Pts',(-1.16243630201622,-0.967148785610963,
-7.82072916527892));
#374531=CARTESIAN_POINT('Ctrl Pts',(-1.02968703215297,-1.10741027035704,
-7.81044611070068));
#374532=CARTESIAN_POINT('Ctrl Pts',(-0.712623718683101,-1.33480374195274,
-7.78887490959674));
#374533=CARTESIAN_POINT('Ctrl Pts',(-0.529602220340034,-1.41741453994902,
-7.77777453926331));
#374534=CARTESIAN_POINT('Ctrl Pts',(-0.225399412709512,-1.48728797854404,
-7.7611976460073));
#374535=CARTESIAN_POINT('Ctrl Pts',(-0.112761604857976,-1.49999999999999,
-7.75542524524325));
#374536=CARTESIAN_POINT('Ctrl Pts',(1.13797860024079E-14,-1.49999999999999,
-7.75));
#374537=CARTESIAN_POINT('Ctrl Pts',(3.62557206479153E-15,-1.49999999999999,
-7.6875));
#374538=CARTESIAN_POINT('Ctrl Pts',(-0.100589452564642,-1.49999999999999,
-7.69233961229299));
#374539=CARTESIAN_POINT('Ctrl Pts',(-0.201140026213281,-1.48988389579456,
-7.69745835691791));
#374540=CARTESIAN_POINT('Ctrl Pts',(-0.495451818355405,-1.42977698559595,
-7.71328807601389));
#374541=CARTESIAN_POINT('Ctrl Pts',(-0.68084559408579,-1.3513596664345,
-7.72438609707316));
#374542=CARTESIAN_POINT('Ctrl Pts',(-1.00388517650595,-1.1309253649979,
-7.74605152126882));
#374543=CARTESIAN_POINT('Ctrl Pts',(-1.14012647132286,-0.993433368167938,
-7.75642565575609));
#374544=CARTESIAN_POINT('Ctrl Pts',(-1.35696148220815,-0.669272841972499,
-7.77586259414244));
#374545=CARTESIAN_POINT('Ctrl Pts',(-1.43342607099873,-0.484338668640413,
-7.7855922961867));
#374546=CARTESIAN_POINT('Ctrl Pts',(-1.50976492154754,-0.0967196035284116,
-7.80712668869292));
#374547=CARTESIAN_POINT('Ctrl Pts',(-1.50941611595624,0.102019322792505,
-7.81816774015519));
#374548=CARTESIAN_POINT('Ctrl Pts',(-1.43333942566545,0.481278957691876,
-7.83923771987182));
#374549=CARTESIAN_POINT('Ctrl Pts',(-1.36094252496436,0.658710809425312,
-7.84865247805577));
#374550=CARTESIAN_POINT('Ctrl Pts',(-1.14895997271597,0.984599762393011,
-7.86790396427189));
#374551=CARTESIAN_POINT('Ctrl Pts',(-1.008470386414,1.1280558078679,-7.87864816279645));
#374552=CARTESIAN_POINT('Ctrl Pts',(-0.683316256690496,1.34941791257009,
-7.90044109550962));
#374553=CARTESIAN_POINT('Ctrl Pts',(-0.50271108544479,1.42658382171831,
-7.91127396333894));
#374554=CARTESIAN_POINT('Ctrl Pts',(-0.125331847764131,1.50694188021935,
-7.93166279866909));
#374555=CARTESIAN_POINT('Ctrl Pts',(0.0676000990502314,1.51063252236472,
-7.94045706343858));
#374556=CARTESIAN_POINT('Ctrl Pts',(0.453053101091752,1.44385482655744,
-7.96085711564061));
#374557=CARTESIAN_POINT('Ctrl Pts',(0.641237598800616,1.37068394705898,
-7.97194367093858));
#374558=CARTESIAN_POINT('Ctrl Pts',(0.97142244740165,1.15901668018185,-7.9937093431759));
#374559=CARTESIAN_POINT('Ctrl Pts',(1.11187991864011,1.02504781595698,-8.00418846375125));
#374560=CARTESIAN_POINT('Ctrl Pts',(1.33686960467276,0.708053997096517,
-8.0238186689248));
#374561=CARTESIAN_POINT('Ctrl Pts',(1.41798274070534,0.527162031521857,
-8.03321322047106));
#374562=CARTESIAN_POINT('Ctrl Pts',(1.50613608811588,0.143308064344835,
-8.05453844086978));
#374563=CARTESIAN_POINT('Ctrl Pts',(1.5119022342726,-0.0559660969908603,
-8.06560922761065));
#374564=CARTESIAN_POINT('Ctrl Pts',(1.44712806489012,-0.438191225159822,
-8.08684395695337));
#374565=CARTESIAN_POINT('Ctrl Pts',(1.37996060665107,-0.617946335458259,
-8.09660512367491));
#374566=CARTESIAN_POINT('Ctrl Pts',(1.17761874744159,-0.950130047800848,
-8.115567626258));
#374567=CARTESIAN_POINT('Ctrl Pts',(1.04146583313214,-1.09765952383988,
-8.12621632740304));
#374568=CARTESIAN_POINT('Ctrl Pts',(0.722600625896706,-1.32887769876841,
-8.14798046392043));
#374569=CARTESIAN_POINT('Ctrl Pts',(0.54379957003011,-1.41150887834165,
-8.15887834427547));
#374570=CARTESIAN_POINT('Ctrl Pts',(0.237977572203931,-1.48582269186709,
-8.17565648460415));
#374571=CARTESIAN_POINT('Ctrl Pts',(0.119084432358742,-1.5,-8.18177054757678));
#374572=CARTESIAN_POINT('Ctrl Pts',(-7.39339145461315E-14,-1.49999999999999,
-8.1875));
#374573=CARTESIAN_POINT('Origin',(0.,-1.17768352285132E-13,1004.));
#374574=CARTESIAN_POINT('',(2.62566781617011E-12,1.22263611415546,5.22263611415551));
#374575=CARTESIAN_POINT('',(-1.22464679914734E-13,999.999999999989,1004.));
#374576=CARTESIAN_POINT('',(1.16245326511946,-0.172894699616898,5.17524047358083));
#374577=CARTESIAN_POINT('Ctrl Pts',(1.16245326511952,-0.172894699616907,
5.17524047358087));
#374578=CARTESIAN_POINT('Ctrl Pts',(1.19399906804494,-0.0751204590618667,
5.19205905165469));
#374579=CARTESIAN_POINT('Ctrl Pts',(1.21273427617106,0.0263505697178082,
5.20876352342307));
#374580=CARTESIAN_POINT('Ctrl Pts',(1.22403798349754,0.238694528089334,
5.24237097580138));
#374581=CARTESIAN_POINT('Ctrl Pts',(1.21468846965962,0.348742451219363,
5.25905662677932));
#374582=CARTESIAN_POINT('Ctrl Pts',(1.14440902939163,0.659449163520211,
5.30459309397949));
#374583=CARTESIAN_POINT('Ctrl Pts',(1.05176705868767,0.820265983472114,
5.32729141130241));
#374584=CARTESIAN_POINT('Ctrl Pts',(0.868371046406527,1.07627483107919,
5.37112509845121));
#374585=CARTESIAN_POINT('Ctrl Pts',(0.734430946342676,1.20185061729893,
5.39690248949309));
#374586=CARTESIAN_POINT('Ctrl Pts',(0.496444765757832,1.35014966254729,
5.43521886790191));
#374587=CARTESIAN_POINT('Ctrl Pts',(0.407566921813029,1.39321113075102,
5.44830739519754));
#374588=CARTESIAN_POINT('Ctrl Pts',(0.17654814223105,1.47628188585813,5.47964000519515));
#374589=CARTESIAN_POINT('Ctrl Pts',(0.0614240005287953,1.49300777123951,
5.49300777123956));
#374590=CARTESIAN_POINT('Ctrl Pts',(-3.08060338411093E-14,1.49999999999988,
5.49999999999993));
#374591=CARTESIAN_POINT('',(0.943477955795688,0.700742119235096,5.17524047358083));
#374592=CARTESIAN_POINT('Origin',(-2.08166817117217E-15,1.38777878078145E-16,
5.17524047358094));
#374593=CARTESIAN_POINT('Ctrl Pts',(0.943477955795631,0.700742119235054,
5.17524047358087));
#374594=CARTESIAN_POINT('Ctrl Pts',(0.89439950803542,0.772851645360285,
5.17883611947854));
#374595=CARTESIAN_POINT('Ctrl Pts',(0.83757969138554,0.839368825375372,
5.18257660489706));
#374596=CARTESIAN_POINT('Ctrl Pts',(0.712505185698739,0.956945420110407,
5.19008020169398));
#374597=CARTESIAN_POINT('Ctrl Pts',(0.645022284217815,1.00809919656745,
5.19381777605465));
#374598=CARTESIAN_POINT('Ctrl Pts',(0.446868995932777,1.12761359942621,
5.20401348413372));
#374599=CARTESIAN_POINT('Ctrl Pts',(0.308091646309466,1.17965824671919,
5.21034872100051));
#374600=CARTESIAN_POINT('Ctrl Pts',(0.107758738784782,1.21505485062343,
5.21851908836561));
#374601=CARTESIAN_POINT('Ctrl Pts',(0.0531588445461745,1.22064681749215,
5.2206468174922));
#374602=CARTESIAN_POINT('Ctrl Pts',(5.25148536208059E-12,1.22263611415546,
5.22263611415551));
#374603=CARTESIAN_POINT('Origin',(0.,1.84795814293585E-15,-9.));
#374604=CARTESIAN_POINT('',(-1.41298094714294,2.50437193139947E-10,-8.76225952643789));
#374605=CARTESIAN_POINT('',(-1.17524047358083,1.70403269451593E-15,-9.));
#374606=CARTESIAN_POINT('',(-1.17524047358083,1.70403269451593E-15,-9.));
#374607=CARTESIAN_POINT('Ctrl Pts',(-1.41298094714294,5.0087271136201E-10,
-8.76225952643789));
#374608=CARTESIAN_POINT('Ctrl Pts',(-1.40661633259335,0.170222827651176,
-8.76862414092715));
#374609=CARTESIAN_POINT('Ctrl Pts',(-1.36949767217021,0.337954367729962,
-8.77498443124136));
#374610=CARTESIAN_POINT('Ctrl Pts',(-1.25144210016968,0.618423802974436,
-8.78575720460891));
#374611=CARTESIAN_POINT('Ctrl Pts',(-1.16041076134757,0.786810302099258,
-8.79168857309288));
#374612=CARTESIAN_POINT('Ctrl Pts',(-0.870331100473633,1.07132672691966,
-8.80664103487819));
#374613=CARTESIAN_POINT('Ctrl Pts',(-0.718622501884707,1.17036468694909,
-8.81361329796119));
#374614=CARTESIAN_POINT('Ctrl Pts',(-0.397528466238866,1.29897691831306,
-8.82702012864551));
#374615=CARTESIAN_POINT('Ctrl Pts',(-0.232920329340296,1.33196165968486,
-8.83334360207825));
#374616=CARTESIAN_POINT('Ctrl Pts',(0.154659368267121,1.33761280872929,
-8.84697406884231));
#374617=CARTESIAN_POINT('Ctrl Pts',(0.32663216391228,1.28673458420506,-8.85349457293248));
#374618=CARTESIAN_POINT('Ctrl Pts',(0.596915603944153,1.17829870466726,
-8.86497740055058));
#374619=CARTESIAN_POINT('Ctrl Pts',(0.738687100801235,1.08684240050756,
-8.87179108117765));
#374620=CARTESIAN_POINT('Ctrl Pts',(0.983024626099762,0.852598849977181,
-8.88529312369776));
#374621=CARTESIAN_POINT('Ctrl Pts',(1.08299149273678,0.710087044469093,
-8.89149869999885));
#374622=CARTESIAN_POINT('Ctrl Pts',(1.21210093543402,0.413830143095868,
-8.90353581540508));
#374623=CARTESIAN_POINT('Ctrl Pts',(1.24700885086701,0.264141347306251,
-8.90969437811077));
#374624=CARTESIAN_POINT('Ctrl Pts',(1.26190809160109,-0.0512728550184668,
-8.92287899600932));
#374625=CARTESIAN_POINT('Ctrl Pts',(1.23765032069058,-0.2143650511596,-8.92981109575828));
#374626=CARTESIAN_POINT('Ctrl Pts',(1.1437214259834,-0.477800630596949,
-8.94119025592916));
#374627=CARTESIAN_POINT('Ctrl Pts',(1.07131936092985,-0.633771724466625,
-8.94724597180567));
#374628=CARTESIAN_POINT('Ctrl Pts',(0.833879668056824,-0.894264904214086,
-8.96158207726312));
#374629=CARTESIAN_POINT('Ctrl Pts',(0.714102016460339,-0.98463286044948,
-8.96802984706955));
#374630=CARTESIAN_POINT('Ctrl Pts',(0.493798039929723,-1.09406106811124,
-8.97884116477498));
#374631=CARTESIAN_POINT('Ctrl Pts',(0.401788558101966,-1.1265752151692,
-8.98311244451451));
#374632=CARTESIAN_POINT('Ctrl Pts',(0.20619495746093,-1.16997545830358,
-8.99170978455801));
#374633=CARTESIAN_POINT('Ctrl Pts',(0.103058272401581,-1.17925262541455,
-8.99598784816628));
#374634=CARTESIAN_POINT('Ctrl Pts',(-1.21430643318376E-16,-1.17524047358083,
-9.));
#374635=CARTESIAN_POINT('Origin',(0.,1.84795814293585E-15,-9.));
#374636=CARTESIAN_POINT('Origin',(0.,1.84795814293585E-15,-9.));
#374637=CARTESIAN_POINT('Origin',(0.,1.84795814293585E-15,-9.));
#374638=CARTESIAN_POINT('',(1.20419349529493,-0.894381364905022,-8.67524047358084));
#374639=CARTESIAN_POINT('Ctrl Pts',(1.20419349529493,-0.894381364905017,
-8.67524047358084));
#374640=CARTESIAN_POINT('Ctrl Pts',(1.13095118605837,-0.9716143545478,-8.68798858402793));
#374641=CARTESIAN_POINT('Ctrl Pts',(1.04930823985346,-1.04028664032772,
-8.70142161163385));
#374642=CARTESIAN_POINT('Ctrl Pts',(0.878046559880868,-1.15411572512553,
-8.72843423103745));
#374643=CARTESIAN_POINT('Ctrl Pts',(0.789772643293612,-1.20019602678898,
-8.74187275401195));
#374644=CARTESIAN_POINT('Ctrl Pts',(0.529623955243905,-1.30275449886039,
-8.78033713619089));
#374645=CARTESIAN_POINT('Ctrl Pts',(0.350730680924542,-1.33604442248835,
-8.8055512491075));
#374646=CARTESIAN_POINT('Ctrl Pts',(0.0206766763463416,-1.33358695022529,
-8.8497597206349));
#374647=CARTESIAN_POINT('Ctrl Pts',(-0.151348172730456,-1.30940596959337,
-8.87093339811554));
#374648=CARTESIAN_POINT('Ctrl Pts',(-0.428302486918901,-1.1896603066116,
-8.91545734281534));
#374649=CARTESIAN_POINT('Ctrl Pts',(-0.522196352027943,-1.13301202682058,
-8.93233880671145));
#374650=CARTESIAN_POINT('Ctrl Pts',(-0.688752455704374,-0.998922351205504,
-8.9663014666125));
#374651=CARTESIAN_POINT('Ctrl Pts',(-0.761425017394258,-0.922956233174634,
-8.98321102010998));
#374652=CARTESIAN_POINT('Ctrl Pts',(-0.82340787416506,-0.838564036615864,
-8.99999999999999));
#374653=CARTESIAN_POINT('',(0.243337884005315,-1.48013062741361,-8.67524047358084));
#374654=CARTESIAN_POINT('Origin',(0.,1.84795814293585E-15,-8.67524047358084));
#374655=CARTESIAN_POINT('Ctrl Pts',(0.243337884005315,-1.48013062741361,
-8.67524047358084));
#374656=CARTESIAN_POINT('Ctrl Pts',(0.101094102340477,-1.4987275388269,
-8.67996543537092));
#374657=CARTESIAN_POINT('Ctrl Pts',(-0.0426671899127046,-1.49755833949873,
-8.68419131194465));
#374658=CARTESIAN_POINT('Ctrl Pts',(-0.318529374136382,-1.45339200249797,
-8.69334244704395));
#374659=CARTESIAN_POINT('Ctrl Pts',(-0.446787711019286,-1.41439763313783,
-8.69795944692342));
#374660=CARTESIAN_POINT('Ctrl Pts',(-0.738263562285435,-1.28017117867732,
-8.70937165618806));
#374661=CARTESIAN_POINT('Ctrl Pts',(-0.891914693261224,-1.16979592346254,
-8.7161885798986));
#374662=CARTESIAN_POINT('Ctrl Pts',(-1.13959614737799,-0.907361178122547,
-8.728880211953));
#374663=CARTESIAN_POINT('Ctrl Pts',(-1.24531907020817,-0.750705326305741,
-8.73469659578812));
#374664=CARTESIAN_POINT('Ctrl Pts',(-1.38528494839894,-0.392021122233477,
-8.74772314591134));
#374665=CARTESIAN_POINT('Ctrl Pts',(-1.41799325611942,-0.206165197918358,
-8.75455854148613));
#374666=CARTESIAN_POINT('Ctrl Pts',(-1.41341885699457,-0.0128948780533315,
-8.76177751154181));
#374667=CARTESIAN_POINT('Ctrl Pts',(-1.41322194947896,-0.006445652832508,
-8.76201852410416));
#374668=CARTESIAN_POINT('Ctrl Pts',(-1.41298094714294,5.00872780991692E-10,
-8.76225952643789));
#374669=CARTESIAN_POINT('Origin',(0.,-1.17768352285132E-13,1004.));
#374670=CARTESIAN_POINT('Ctrl Pts',(5.25317636612677E-12,1.22263611415552,
5.22263611415548));
#374671=CARTESIAN_POINT('Ctrl Pts',(-0.115296684347476,1.2269507171431,
5.22695071714306));
#374672=CARTESIAN_POINT('Ctrl Pts',(-0.223766436349468,1.2148855018304,
5.23131700863417));
#374673=CARTESIAN_POINT('Ctrl Pts',(-0.478278179729571,1.15760022383143,
5.24208637023804));
#374674=CARTESIAN_POINT('Ctrl Pts',(-0.627381439373727,1.09194410272621,
5.24897616624381));
#374675=CARTESIAN_POINT('Ctrl Pts',(-0.883573773271131,0.913573132610325,
5.26199412924211));
#374676=CARTESIAN_POINT('Ctrl Pts',(-0.990681696781001,0.805713791835157,
5.26803702740709));
#374677=CARTESIAN_POINT('Ctrl Pts',(-1.15952482909877,0.559571469320968,
5.27899700986098));
#374678=CARTESIAN_POINT('Ctrl Pts',(-1.23606073166015,0.401676792848018,
5.28542047422328));
#374679=CARTESIAN_POINT('Ctrl Pts',(-1.30927486236648,0.0515901063597925,
5.29982019456112));
#374680=CARTESIAN_POINT('Ctrl Pts',(-1.3119373462125,-0.115337847574361,
5.3065789426825));
#374681=CARTESIAN_POINT('Ctrl Pts',(-1.25338969407816,-0.447917213019407,
5.31984699526509));
#374682=CARTESIAN_POINT('Ctrl Pts',(-1.19047975461417,-0.608427371489105,
5.3257816690615));
#374683=CARTESIAN_POINT('Ctrl Pts',(-1.00849050415241,-0.89486065873855,
5.3379211316854));
#374684=CARTESIAN_POINT('Ctrl Pts',(-0.893778927178617,-1.01791957302403,
5.34432830437151));
#374685=CARTESIAN_POINT('Ctrl Pts',(-0.614965052842258,-1.22385703407752,
5.35783782669075));
#374686=CARTESIAN_POINT('Ctrl Pts',(-0.450478262988456,-1.30080821357337,
5.36482096360993));
#374687=CARTESIAN_POINT('Ctrl Pts',(-0.0535197887087344,-1.39752886138873,
5.3797460760767));
#374688=CARTESIAN_POINT('Ctrl Pts',(0.138282520270641,-1.38497571780285,
5.38572569203872));
#374689=CARTESIAN_POINT('Ctrl Pts',(0.442514830477669,-1.3366523083962,
5.39679114172506));
#374690=CARTESIAN_POINT('Ctrl Pts',(0.610880602891162,-1.27592998523196,
5.40347638258105));
#374691=CARTESIAN_POINT('Ctrl Pts',(0.923558005877193,-1.0907204668723,
5.41706648777078));
#374692=CARTESIAN_POINT('Ctrl Pts',(1.06322528601953,-0.965103528812707,
5.42383292975859));
#374693=CARTESIAN_POINT('Ctrl Pts',(1.28282155738663,-0.670543286431297,
5.43610666219767));
#374694=CARTESIAN_POINT('Ctrl Pts',(1.36291448343688,-0.5044383426778,5.44192300791259));
#374695=CARTESIAN_POINT('Ctrl Pts',(1.45957001512327,-0.148199386829699,
5.45502607686382));
#374696=CARTESIAN_POINT('Ctrl Pts',(1.47330898038679,0.0407919157890449,
5.46188119746995));
#374697=CARTESIAN_POINT('Ctrl Pts',(1.43234406746629,0.381079555584754,
5.47405531723903));
#374698=CARTESIAN_POINT('Ctrl Pts',(1.38942465639446,0.531038759436448,
5.47935753809352));
#374699=CARTESIAN_POINT('Ctrl Pts',(1.25533045048584,0.817592101860293,
5.48939547357438));
#374700=CARTESIAN_POINT('Ctrl Pts',(1.16271769295252,0.952788278842525,
5.49447277254087));
#374701=CARTESIAN_POINT('Ctrl Pts',(1.0509439038327,1.07028823734397,5.50000000000003));
#374702=CARTESIAN_POINT('Origin',(0.,2.04523456705693E-15,3.99999999999998));
#374703=CARTESIAN_POINT('Ctrl Pts',(-7.37498501890957E-14,-1.49999999999999,
-8.1875));
#374704=CARTESIAN_POINT('Ctrl Pts',(-0.0707075837041045,-1.49999999999999,
-8.19090192020711));
#374705=CARTESIAN_POINT('Ctrl Pts',(-0.141469114138096,-1.49500106821859,
-8.19444529514366));
#374706=CARTESIAN_POINT('Ctrl Pts',(-0.410293528228611,-1.4566657614053,
-8.20844398543069));
#374707=CARTESIAN_POINT('Ctrl Pts',(-0.601123534669336,-1.38883044981847,
-8.2195096126071));
#374708=CARTESIAN_POINT('Ctrl Pts',(-0.938214653084433,-1.18614462758204,
-8.24135807833242));
#374709=CARTESIAN_POINT('Ctrl Pts',(-1.0827939343619,-1.05582191021027,
-8.25193422772871));
#374710=CARTESIAN_POINT('Ctrl Pts',(-1.31583506474116,-0.746005663469679,
-8.27175243119567));
#374711=CARTESIAN_POINT('Ctrl Pts',(-1.40148555690714,-0.56902757212789,
-8.28088735710405));
#374712=CARTESIAN_POINT('Ctrl Pts',(-1.50116293429005,-0.18902395801905,
-8.30199866899899));
#374713=CARTESIAN_POINT('Ctrl Pts',(-1.51297807672142,0.0105976379183958,
-8.31308875766218));
#374714=CARTESIAN_POINT('Ctrl Pts',(-1.45941370735621,0.395532893185297,
-8.33447404962145));
#374715=CARTESIAN_POINT('Ctrl Pts',(-1.39738912175206,0.577635365282228,
-8.34459085362684));
#374716=CARTESIAN_POINT('Ctrl Pts',(-1.20444714400469,0.915854641577226,
-8.363380813421));
#374717=CARTESIAN_POINT('Ctrl Pts',(-1.07262763202685,1.06724487327345,
-8.37387220325007));
#374718=CARTESIAN_POINT('Ctrl Pts',(-0.760035204662309,1.30790925908279,
-8.3955969352519));
#374719=CARTESIAN_POINT('Ctrl Pts',(-0.583135101083686,1.39579330471248,
-8.40654926894335));
#374720=CARTESIAN_POINT('Ctrl Pts',(-0.210863302817571,1.49723221581078,
-8.42727795171891));
#374721=CARTESIAN_POINT('Ctrl Pts',(-0.0195780693232269,1.51187814134585,
-8.43622810132984));
#374722=CARTESIAN_POINT('Ctrl Pts',(0.366999280241712,1.46794990166863,
-8.45604754161259));
#374723=CARTESIAN_POINT('Ctrl Pts',(0.558185703277335,1.40640519943362,
-8.46695557774176));
#374724=CARTESIAN_POINT('Ctrl Pts',(0.900625440472865,1.21502563541599,
-8.48874731627983));
#374725=CARTESIAN_POINT('Ctrl Pts',(1.0496529255059,1.08887867255185,-8.49942148679832));
#374726=CARTESIAN_POINT('Ctrl Pts',(1.29149614569776,0.787026721220456,
-8.51944195058082));
#374727=CARTESIAN_POINT('Ctrl Pts',(1.38206102761909,0.614234598378379,
-8.5283758556457));
#374728=CARTESIAN_POINT('Ctrl Pts',(1.494175951662,0.238578192797074,-8.54924565595578));
#374729=CARTESIAN_POINT('Ctrl Pts',(1.51260341881051,0.0387817213571734,
-8.56034545992466));
#374730=CARTESIAN_POINT('Ctrl Pts',(1.47133257046456,-0.348913673671884,
-8.58188409298183));
#374731=CARTESIAN_POINT('Ctrl Pts',(1.4149199778164,-0.5334643634612,-8.59213690908124));
#374732=CARTESIAN_POINT('Ctrl Pts',(1.23152121190892,-0.879487024884344,
-8.61136039027141));
#374733=CARTESIAN_POINT('Ctrl Pts',(1.10315197137068,-1.03597125398216,
-8.62153488864168));
#374734=CARTESIAN_POINT('Ctrl Pts',(0.846015702352284,-1.24559117952707,
-8.63972913886261));
#374735=CARTESIAN_POINT('Ctrl Pts',(0.733793370559806,-1.31483324275516,
-8.64705182896356));
#374736=CARTESIAN_POINT('Ctrl Pts',(0.495789405867406,-1.42161138720955,
-8.66146885962202));
#374737=CARTESIAN_POINT('Ctrl Pts',(0.371204802885295,-1.45910892507311,
-8.66850453740173));
#374738=CARTESIAN_POINT('Ctrl Pts',(0.243337884005354,-1.4801306274136,
-8.67524047358083));
#374739=CARTESIAN_POINT('Ctrl Pts',(1.20419349529492,-0.894381364905029,
-8.67524047358084));
#374740=CARTESIAN_POINT('Ctrl Pts',(1.2782414791322,-0.794683289815975,
-8.66890844732269));
#374741=CARTESIAN_POINT('Ctrl Pts',(1.33960503944486,-0.686208596444366,
-8.66312269980246));
#374742=CARTESIAN_POINT('Ctrl Pts',(1.43592702107561,-0.452405413158382,
-8.65013363406435));
#374743=CARTESIAN_POINT('Ctrl Pts',(1.46942479488015,-0.327630086744163,
-8.64320167148566));
#374744=CARTESIAN_POINT('Ctrl Pts',(1.51302216223568,-0.00378489863631561,
-8.62521027214634));
#374745=CARTESIAN_POINT('Ctrl Pts',(1.5002965148524,0.195873440965775,-8.61411814216845));
#374746=CARTESIAN_POINT('Ctrl Pts',(1.39889719309338,0.575286936544728,
-8.59303961463629));
#374747=CARTESIAN_POINT('Ctrl Pts',(1.3125677242591,0.751683001948557,-8.58393752735663));
#374748=CARTESIAN_POINT('Ctrl Pts',(1.07831502519926,1.06041034665218,-8.56409127954316));
#374749=CARTESIAN_POINT('Ctrl Pts',(0.933119620966255,1.19017001906558,
-8.55350112705509));
#374750=CARTESIAN_POINT('Ctrl Pts',(0.595003215773495,1.39147663810463,
-8.53164164339661));
#374751=CARTESIAN_POINT('Ctrl Pts',(0.403785151285716,1.4584959421497,-8.52058001264486));
#374752=CARTESIAN_POINT('Ctrl Pts',(0.0163176781344214,1.51196127815833,
-8.50045282692856));
#374753=CARTESIAN_POINT('Ctrl Pts',(-0.175613308436975,1.50181829121292,
-8.49160130884752));
#374754=CARTESIAN_POINT('Ctrl Pts',(-0.55003902760651,1.40910092939278,
-8.47101126076191));
#374755=CARTESIAN_POINT('Ctrl Pts',(-0.728550060234893,1.3256379036634,
-8.46010422731876));
#374756=CARTESIAN_POINT('Ctrl Pts',(-1.04642765622587,1.09292919435903,
-8.43834620353686));
#374757=CARTESIAN_POINT('Ctrl Pts',(-1.18190714024603,0.944789086303314,
-8.42771294082126));
#374758=CARTESIAN_POINT('Ctrl Pts',(-1.38276976512002,0.611651413680171,
-8.40879510903664));
#374759=CARTESIAN_POINT('Ctrl Pts',(-1.44913555775106,0.431533165346498,
-8.39897406474137));
#374760=CARTESIAN_POINT('Ctrl Pts',(-1.51216067476163,0.0488592118263083,
-8.37771440065692));
#374761=CARTESIAN_POINT('Ctrl Pts',(-1.50544860899612,-0.150481167469412,
-8.3666399351405));
#374762=CARTESIAN_POINT('Ctrl Pts',(-1.41548304772181,-0.533741161849835,
-8.34534771323048));
#374763=CARTESIAN_POINT('Ctrl Pts',(-1.33365689272042,-0.714015609107781,
-8.33599849691514));
#374764=CARTESIAN_POINT('Ctrl Pts',(-1.10740755095398,-1.02989318455475,
-8.31633869328833));
#374765=CARTESIAN_POINT('Ctrl Pts',(-0.966302286143343,-1.16330258406064,
-8.30584394641685));
#374766=CARTESIAN_POINT('Ctrl Pts',(-0.635026717709483,-1.37358591619412,
-8.28406423952887));
#374767=CARTESIAN_POINT('Ctrl Pts',(-0.446420881426595,-1.44593213710974,
-8.27298031975216));
#374768=CARTESIAN_POINT('Ctrl Pts',(-0.166651770674125,-1.49306059659345,
-8.25821079826063));
#374769=CARTESIAN_POINT('Ctrl Pts',(-0.0833099133578137,-1.49999999999999,
-8.25400825007527));
#374770=CARTESIAN_POINT('Ctrl Pts',(-7.92750261663253E-15,-1.49999999999999,
-8.25));
#374771=CARTESIAN_POINT('Origin',(0.,1.73472347597681E-15,5.875));
#374772=CARTESIAN_POINT('',(-1.99005104861445E-16,-1.625,6.));
#374773=CARTESIAN_POINT('Origin',(-1.99005104861445E-16,-1.625,5.875));
#374774=CARTESIAN_POINT('Origin',(0.,1.80560739335254E-15,6.));
#374775=CARTESIAN_POINT('Origin',(0.,2.35813972515597E-15,7.5));
#374776=CARTESIAN_POINT('',(0.,2.35813972515597E-15,6.77831216351297));
#374777=CARTESIAN_POINT('',(-1.25,2.54592904999812E-15,7.5));
#374778=CARTESIAN_POINT('',(-1.25,2.20505887526255E-15,7.5));
#374779=CARTESIAN_POINT('',(-0.625,-1.08253175473055,7.5));
#374780=CARTESIAN_POINT('Origin',(0.,2.35813972515597E-15,7.5));
#374781=CARTESIAN_POINT('',(0.625,-1.08253175473055,7.5));
#374782=CARTESIAN_POINT('Origin',(0.,2.35813972515597E-15,7.5));
#374783=CARTESIAN_POINT('',(1.25,1.79477175062954E-15,7.5));
#374784=CARTESIAN_POINT('Origin',(0.,2.35813972515597E-15,7.5));
#374785=CARTESIAN_POINT('',(0.625,1.08253175473055,7.5));
#374786=CARTESIAN_POINT('Origin',(0.,2.35813972515597E-15,7.5));
#374787=CARTESIAN_POINT('',(-0.625,1.08253175473055,7.5));
#374788=CARTESIAN_POINT('Origin',(0.,2.35813972515597E-15,7.5));
#374789=CARTESIAN_POINT('Origin',(0.,2.35813972515597E-15,7.5));
#374790=CARTESIAN_POINT('Origin',(0.,-7.70371977754894E-31,9.));
#374791=CARTESIAN_POINT('',(1.25,0.721687836487031,9.));
#374792=CARTESIAN_POINT('',(1.25,-0.721687836487032,9.));
#374793=CARTESIAN_POINT('Ctrl Pts',(1.25,0.721687836487026,9.));
#374794=CARTESIAN_POINT('Ctrl Pts',(1.25,-7.7715611723761E-16,8.63915608175649));
#374795=CARTESIAN_POINT('Ctrl Pts',(1.25,-0.721687836487028,9.));
#374796=CARTESIAN_POINT('Origin',(0.,-7.70371977754894E-31,9.));
#374797=CARTESIAN_POINT('Origin',(0.,1.73472347597681E-15,6.055));
#374798=CARTESIAN_POINT('',(-2.54610912703474,1.42291503670651E-15,6.01610912703474));
#374799=CARTESIAN_POINT('Origin',(0.,1.84795814293585E-15,6.01610912703474));
#374800=CARTESIAN_POINT('',(-2.50721825406948,1.42767779501581E-15,6.));
#374801=CARTESIAN_POINT('Origin',(-2.50721825406948,1.42767779501581E-15,
6.055));
#374802=CARTESIAN_POINT('Origin',(0.,1.84795814293585E-15,6.));
#374803=CARTESIAN_POINT('Origin',(0.,1.84795814293585E-15,6.01610912703474));
#374804=CARTESIAN_POINT('',(-2.73389087296526,1.51315307225634E-15,6.20389087296526));
#374805=CARTESIAN_POINT('Origin',(0.,1.84795814293585E-15,6.20389087296526));
#374806=CARTESIAN_POINT('',(-2.54610912703474,1.53614970366555E-15,6.01610912703474));
#374807=CARTESIAN_POINT('Origin',(0.,1.73472347597681E-15,6.24278174593052));
#374808=CARTESIAN_POINT('',(-2.75,1.39794560621129E-15,6.24278174593052));
#374809=CARTESIAN_POINT('Origin',(0.,1.84795814293585E-15,6.24278174593052));
#374810=CARTESIAN_POINT('Origin',(-2.695,1.4046811636066E-15,6.24278174593052));
#374811=CARTESIAN_POINT('Origin',(0.,1.84795814293585E-15,8.79610912703474));
#374812=CARTESIAN_POINT('',(-2.73365018604124,0.0362762407020289,8.79610912703474));
#374813=CARTESIAN_POINT('',(-2.73365018604124,-0.0362762407020486,8.79610912703474));
#374814=CARTESIAN_POINT('Origin',(0.,1.84795814293585E-15,8.79610912703474));
#374815=CARTESIAN_POINT('',(-2.66979042840331,-0.0685319131367817,8.85933012996512));
#374816=CARTESIAN_POINT('Ctrl Pts',(-2.73365018604124,-0.0362762407020486,
8.79610912703474));
#374817=CARTESIAN_POINT('Ctrl Pts',(-2.72808418062094,-0.0390874501823592,
8.80163734024559));
#374818=CARTESIAN_POINT('Ctrl Pts',(-2.72251616230074,-0.0418997250385102,
8.80716298614018));
#374819=CARTESIAN_POINT('Ctrl Pts',(-2.71694609217046,-0.0447130856437622,
8.8126860086129));
#374820=CARTESIAN_POINT('Ctrl Pts',(-2.70124415813737,-0.052643901881576,
8.82825531609049));
#374821=CARTESIAN_POINT('Ctrl Pts',(-2.68552590846928,-0.0605833515018367,
8.84380379913848));
#374822=CARTESIAN_POINT('Ctrl Pts',(-2.66979042840331,-0.0685319131367817,
8.85933012996512));
#374823=CARTESIAN_POINT('',(-2.66869591238441,-0.102662953079004,8.85933012996512));
#374824=CARTESIAN_POINT('Origin',(-2.67852080896312,-0.0858949510114057,
8.84999761231046));
#374825=CARTESIAN_POINT('',(-2.73035783527281,-0.138943861495087,8.79610912703474));
#374826=CARTESIAN_POINT('Ctrl Pts',(-2.66869591238441,-0.102662953079004,
8.85933012996512));
#374827=CARTESIAN_POINT('Ctrl Pts',(-2.6740857579175,-0.105834453458509,
8.8538223528706));
#374828=CARTESIAN_POINT('Ctrl Pts',(-2.67947351161323,-0.109004669736153,
8.84831178811348));
#374829=CARTESIAN_POINT('Ctrl Pts',(-2.68485921376854,-0.112173626398928,
8.84279849653635));
#374830=CARTESIAN_POINT('Ctrl Pts',(-2.7000414174675,-0.121106861876859,
8.82725662040549));
#374831=CARTESIAN_POINT('Ctrl Pts',(-2.71520733790511,-0.130030099226532,
8.81169306718667));
#374832=CARTESIAN_POINT('Ctrl Pts',(-2.73035783527281,-0.138943861495087,
8.79610912703474));
#374833=CARTESIAN_POINT('',(-2.7257093818291,-0.211347276044891,8.79610912703474));
#374834=CARTESIAN_POINT('Origin',(0.,1.84795814293585E-15,8.79610912703474));
#374835=CARTESIAN_POINT('',(-2.65991420288366,-0.23944516702142,8.85933012996512));
#374836=CARTESIAN_POINT('Ctrl Pts',(-2.7257093818291,-0.211347276044891,
8.79610912703474));
#374837=CARTESIAN_POINT('Ctrl Pts',(-2.71997469755407,-0.21379609440213,
8.80163734024559));
#374838=CARTESIAN_POINT('Ctrl Pts',(-2.714237936256,-0.216245846979342,
8.80716298614018));
#374839=CARTESIAN_POINT('Ctrl Pts',(-2.70849905779933,-0.218696551614944,
8.8126860086129));
#374840=CARTESIAN_POINT('Ctrl Pts',(-2.69232125593275,-0.225605046772597,
8.82825531609049));
#374841=CARTESIAN_POINT('Ctrl Pts',(-2.67612661881068,-0.232521112228163,
8.84380379913848));
#374842=CARTESIAN_POINT('Ctrl Pts',(-2.65991420288366,-0.23944516702142,
8.85933012996512));
#374843=CARTESIAN_POINT('',(-2.65663515242803,-0.273435955199435,8.85933012996512));
#374844=CARTESIAN_POINT('Origin',(-2.66751419228412,-0.257331888075536,
8.84999761231045));
#374845=CARTESIAN_POINT('',(-2.71584585849932,-0.313593013561955,8.79610912703474));
#374846=CARTESIAN_POINT('Ctrl Pts',(-2.65663515242803,-0.273435955199435,
8.85933012996512));
#374847=CARTESIAN_POINT('Ctrl Pts',(-2.66181072521843,-0.276946267980235,
8.8538223528706));
#374848=CARTESIAN_POINT('Ctrl Pts',(-2.66698429274206,-0.280455165273019,
8.84831178811348));
#374849=CARTESIAN_POINT('Ctrl Pts',(-2.67215589364419,-0.283962674096302,
8.84279849653635));
#374850=CARTESIAN_POINT('Ctrl Pts',(-2.68673454951515,-0.293850282414642,
8.82725662040549));
#374851=CARTESIAN_POINT('Ctrl Pts',(-2.70129759616275,-0.303726869874814,
8.81169306718667));
#374852=CARTESIAN_POINT('Ctrl Pts',(-2.71584585849932,-0.313593013561955,
8.79610912703474));
#374853=CARTESIAN_POINT('',(-2.7065680531042,-0.385549840096616,8.79610912703474));
#374854=CARTESIAN_POINT('Origin',(0.,1.84795814293585E-15,8.79610912703474));
#374855=CARTESIAN_POINT('',(-2.63910781935455,-0.40937448935394,8.85933012996512));
#374856=CARTESIAN_POINT('Ctrl Pts',(-2.7065680531042,-0.385549840096616,
8.79610912703474));
#374857=CARTESIAN_POINT('Ctrl Pts',(-2.70068825502221,-0.387626204610885,
8.80163734024559));
#374858=CARTESIAN_POINT('Ctrl Pts',(-2.69480632432897,-0.389703368350347,
8.80716298614018));
#374859=CARTESIAN_POINT('Ctrl Pts',(-2.68892221982847,-0.391781346545276,
8.8126860086129));
#374860=CARTESIAN_POINT('Ctrl Pts',(-2.67233502818641,-0.397639132134298,
8.82825531609049));
#374861=CARTESIAN_POINT('Ctrl Pts',(-2.65573055084804,-0.403503393828722,
8.84380379913848));
#374862=CARTESIAN_POINT('Ctrl Pts',(-2.63910781935455,-0.40937448935394,
8.85933012996512));
#374863=CARTESIAN_POINT('',(-2.63365770878388,-0.443085350328122,8.85933012996512));
#374864=CARTESIAN_POINT('Origin',(-2.645546187609,-0.427711393214038,8.84999761231048));
#374865=CARTESIAN_POINT('',(-2.69017388854615,-0.486953544670607,8.79610912703474));
#374866=CARTESIAN_POINT('Ctrl Pts',(-2.63365770878388,-0.443085350328122,
8.85933012996512));
#374867=CARTESIAN_POINT('Ctrl Pts',(-2.63859774129283,-0.446920050882042,
8.8538223528706));
#374868=CARTESIAN_POINT('Ctrl Pts',(-2.64353586334569,-0.450753210378334,
8.84831178811348));
#374869=CARTESIAN_POINT('Ctrl Pts',(-2.64847211177722,-0.454584858256012,
8.84279849653635));
#374870=CARTESIAN_POINT('Ctrl Pts',(-2.66238731299609,-0.465386209111295,
8.82725662040549));
#374871=CARTESIAN_POINT('Ctrl Pts',(-2.67628764317125,-0.47617556166557,
8.81169306718667));
#374872=CARTESIAN_POINT('Ctrl Pts',(-2.69017388854615,-0.486953544670607,
8.79610912703474));
#374873=CARTESIAN_POINT('',(-2.67630485569206,-0.558168097155203,8.79610912703474));
#374874=CARTESIAN_POINT('Origin',(0.,1.84795814293585E-15,8.79610912703474));
#374875=CARTESIAN_POINT('',(-2.60745677570886,-0.577621604099153,8.85933012996512));
#374876=CARTESIAN_POINT('Ctrl Pts',(-2.67630485569206,-0.558168097155203,
8.79610912703474));
#374877=CARTESIAN_POINT('Ctrl Pts',(-2.67030410515465,-0.559863475599333,
8.80163734024559));
#374878=CARTESIAN_POINT('Ctrl Pts',(-2.66430117518113,-0.56155951498969,
8.80716298614018));
#374879=CARTESIAN_POINT('Ctrl Pts',(-2.65829602368434,-0.563256227885819,
8.8126860086129));
#374880=CARTESIAN_POINT('Ctrl Pts',(-2.64136760259518,-0.568039233008733,
8.82825531609049));
#374881=CARTESIAN_POINT('Ctrl Pts',(-2.62442151639954,-0.572827593432832,
8.84380379913848));
#374882=CARTESIAN_POINT('Ctrl Pts',(-2.60745677570886,-0.577621604099153,
8.85933012996512));
#374883=CARTESIAN_POINT('',(-2.59985800069652,-0.610914012710802,8.85933012996512));
#374884=CARTESIAN_POINT('Origin',(-2.61270706618115,-0.59633334049403,8.84999761231046));
#374885=CARTESIAN_POINT('',(-2.65344741704445,-0.658313079212999,8.79610912703474));
#374886=CARTESIAN_POINT('Ctrl Pts',(-2.59985800069652,-0.610914012710802,
8.85933012996512));
#374887=CARTESIAN_POINT('Ctrl Pts',(-2.60454219327082,-0.615057343430724,
8.8538223528706));
#374888=CARTESIAN_POINT('Ctrl Pts',(-2.60922457805016,-0.619199013855944,
8.84831178811348));
#374889=CARTESIAN_POINT('Ctrl Pts',(-2.61390518990746,-0.623339055725002,
8.84279849653635));
#374890=CARTESIAN_POINT('Ctrl Pts',(-2.62709975592765,-0.63500976404968,
8.82725662040549));
#374891=CARTESIAN_POINT('Ctrl Pts',(-2.64028025019205,-0.646667545934106,
8.81169306718667));
#374892=CARTESIAN_POINT('Ctrl Pts',(-2.65344741704445,-0.658313079212999,
8.79610912703474));
#374893=CARTESIAN_POINT('',(-2.6350441475623,-0.728492721775898,8.79610912703474));
#374894=CARTESIAN_POINT('Origin',(0.,1.84795814293585E-15,8.79610912703474));
#374895=CARTESIAN_POINT('',(-2.56509113287406,-0.743495147773676,8.85933012996512));
#374896=CARTESIAN_POINT('Ctrl Pts',(-2.6350441475623,-0.728492721775898,
8.79610912703474));
#374897=CARTESIAN_POINT('Ctrl Pts',(-2.62894710294058,-0.729800147476205,
8.80163734024559));
#374898=CARTESIAN_POINT('Ctrl Pts',(-2.62284784101367,-0.731108093127803,
8.80716298614018));
#374899=CARTESIAN_POINT('Ctrl Pts',(-2.61674631897617,-0.732416568567897,
8.8126860086129));
#374900=CARTESIAN_POINT('Ctrl Pts',(-2.59954623095332,-0.736105138830703,
8.82825531609049));
#374901=CARTESIAN_POINT('Ctrl Pts',(-2.58232817100351,-0.739797921584393,
8.84380379913848));
#374902=CARTESIAN_POINT('Ctrl Pts',(-2.56509113287406,-0.743495147773676,
8.85933012996512));
#374903=CARTESIAN_POINT('',(-2.55537491841651,-0.776232298374609,8.85933012996512));
#374904=CARTESIAN_POINT('Origin',(-2.56913177099444,-0.762504826164824,
8.84999761231046));
#374905=CARTESIAN_POINT('',(-2.60581736094343,-0.826967464105193,8.79610912703474));
#374906=CARTESIAN_POINT('Ctrl Pts',(-2.55537491841651,-0.776232298374609,
8.85933012996512));
#374907=CARTESIAN_POINT('Ctrl Pts',(-2.55978402270411,-0.780667233425863,
8.8538223528706));
#374908=CARTESIAN_POINT('Ctrl Pts',(-2.5641914292865,-0.785100395767848,
8.84831178811348));
#374909=CARTESIAN_POINT('Ctrl Pts',(-2.56859717093147,-0.78953181930821,
8.84279849653635));
#374910=CARTESIAN_POINT('Ctrl Pts',(-2.58101688245097,-0.802023927658419,
8.82725662040549));
#374911=CARTESIAN_POINT('Ctrl Pts',(-2.59342337932647,-0.814502234546644,
8.81169306718667));
#374912=CARTESIAN_POINT('Ctrl Pts',(-2.60581736094343,-0.826967464105193,
8.79610912703474));
#374913=CARTESIAN_POINT('',(-2.582955477815,-0.895823813541617,8.79610912703474));
#374914=CARTESIAN_POINT('Origin',(0.,1.84795814293585E-15,8.79610912703474));
#374915=CARTESIAN_POINT('',(-2.51218498036396,-0.906313510406788,8.85933012996512));
#374916=CARTESIAN_POINT('Ctrl Pts',(-2.582955477815,-0.895823813541617,
8.79610912703474));
#374917=CARTESIAN_POINT('Ctrl Pts',(-2.57678719317314,-0.896737914005455,
8.80163734024559));
#374918=CARTESIAN_POINT('Ctrl Pts',(-2.57061666246838,-0.897652391289058,
8.80716298614018));
#374919=CARTESIAN_POINT('Ctrl Pts',(-2.56444384235301,-0.898567252466868,
8.8126860086129));
#374920=CARTESIAN_POINT('Ctrl Pts',(-2.54704276624755,-0.901146230743158,
8.82825531609049));
#374921=CARTESIAN_POINT('Ctrl Pts',(-2.52962348524517,-0.903728261390006,
8.84380379913848));
#374922=CARTESIAN_POINT('Ctrl Pts',(-2.51218498036396,-0.906313510406788,
8.85933012996512));
#374923=CARTESIAN_POINT('',(-2.50039125247053,-0.938360879023088,8.85933012996512));
#374924=CARTESIAN_POINT('Origin',(-2.51499936228368,-0.925543015948133,
8.84999761231046));
#374925=CARTESIAN_POINT('',(-2.54747944236023,-0.992223662303413,8.79610912703474));
#374926=CARTESIAN_POINT('Ctrl Pts',(-2.50039125247053,-0.938360879023088,
8.85933012996512));
#374927=CARTESIAN_POINT('Ctrl Pts',(-2.50450715051616,-0.943069194306258,
8.8538223528706));
#374928=CARTESIAN_POINT('Ctrl Pts',(-2.50862146792258,-0.947775631750034,
8.84831178811348));
#374929=CARTESIAN_POINT('Ctrl Pts',(-2.51273423521776,-0.952480227291835,
8.84279849653635));
#374930=CARTESIAN_POINT('Ctrl Pts',(-2.52432805697791,-0.965742402914816,
8.82725662040549));
#374931=CARTESIAN_POINT('Ctrl Pts',(-2.53590957550768,-0.978989958767248,
8.81169306718667));
#374932=CARTESIAN_POINT('Ctrl Pts',(-2.54747944236023,-0.992223662303413,
8.79610912703474));
#374933=CARTESIAN_POINT('',(-2.52025288996715,-1.05947377310389,8.79610912703474));
#374934=CARTESIAN_POINT('Origin',(0.,1.84795814293585E-15,8.79610912703474));
#374935=CARTESIAN_POINT('',(-2.44895572090755,-1.065407636422,8.85933012996512));
#374936=CARTESIAN_POINT('Ctrl Pts',(-2.52025288996715,-1.05947377310389,
8.79610912703474));
#374937=CARTESIAN_POINT('Ctrl Pts',(-2.51403871210983,-1.05999079209638,
8.80163734024559));
#374938=CARTESIAN_POINT('Ctrl Pts',(-2.50782226866146,-1.06050804322867,
8.80716298614018));
#374939=CARTESIAN_POINT('Ctrl Pts',(-2.50160351591014,-1.06102553078338,
8.8126860086129));
#374940=CARTESIAN_POINT('Ctrl Pts',(-2.48407295647631,-1.06248431949823,
8.82825531609049));
#374941=CARTESIAN_POINT('Ctrl Pts',(-2.46652403398342,-1.06394498792046,
8.84380379913848));
#374942=CARTESIAN_POINT('Ctrl Pts',(-2.44895572090755,-1.065407636422,8.85933012996512));
#374943=CARTESIAN_POINT('',(-2.43513294253591,-1.09663353354188,8.85933012996512));
#374944=CARTESIAN_POINT('Origin',(-2.45053228172762,-1.08477795095056,8.84999761231046));
#374945=CARTESIAN_POINT('',(-2.47867338431574,-1.15340260064192,8.79610912703474));
#374946=CARTESIAN_POINT('Ctrl Pts',(-2.43513294253591,-1.09663353354188,
8.85933012996512));
#374947=CARTESIAN_POINT('Ctrl Pts',(-2.43893872123164,-1.10159588157954,
8.8538223528706));
#374948=CARTESIAN_POINT('Ctrl Pts',(-2.44274304284934,-1.10655625436413,
8.84831178811348));
#374949=CARTESIAN_POINT('Ctrl Pts',(-2.44654593555174,-1.11151468971515,
8.84279849653635));
#374950=CARTESIAN_POINT('Ctrl Pts',(-2.45726622605206,-1.12549243548654,
8.82725662040549));
#374951=CARTESIAN_POINT('Ctrl Pts',(-2.46797517529222,-1.13945480325459,
8.81169306718667));
#374952=CARTESIAN_POINT('Ctrl Pts',(-2.47867338431574,-1.15340260064192,
8.79610912703474));
#374953=CARTESIAN_POINT('',(-2.44719404240188,-1.21877012767606,8.79610912703474));
#374954=CARTESIAN_POINT('Origin',(0.,1.84795814293585E-15,8.79610912703474));
#374955=CARTESIAN_POINT('',(-2.37566317709458,-1.22012377392993,8.85933012996512));
#374956=CARTESIAN_POINT('Ctrl Pts',(-2.44719404240188,-1.21877012767606,
8.79610912703474));
#374957=CARTESIAN_POINT('Ctrl Pts',(-2.44095950671885,-1.21888794065527,
8.80163734024559));
#374958=CARTESIAN_POINT('Ctrl Pts',(-2.43472269522642,-1.2190058401404,
8.80716298614018));
#374959=CARTESIAN_POINT('Ctrl Pts',(-2.42848356402812,-1.21912382760464,
8.8126860086129));
#374960=CARTESIAN_POINT('Ctrl Pts',(-2.41089555809493,-1.21945643228231,
8.82825531609049));
#374961=CARTESIAN_POINT('Ctrl Pts',(-2.39328910639829,-1.21978973628007,
8.84380379913848));
#374962=CARTESIAN_POINT('Ctrl Pts',(-2.37566317709458,-1.22012377392993,
8.85933012996512));
#374963=CARTESIAN_POINT('',(-2.35986814900602,-1.2503998856442,8.85933012996512));
#374964=CARTESIAN_POINT('Origin',(-2.37599543838843,-1.23955530066839,8.84999761231045));
#374965=CARTESIAN_POINT('',(-2.39968192566132,-1.30984196029031,8.79610912703474));
#374966=CARTESIAN_POINT('Ctrl Pts',(-2.35986814900602,-1.2503998856442,
8.85933012996512));
#374967=CARTESIAN_POINT('Ctrl Pts',(-2.36334816959087,-1.25559587508384,
8.8538223528706));
#374968=CARTESIAN_POINT('Ctrl Pts',(-2.36682686264629,-1.26078979997346,
8.84831178811348));
#374969=CARTESIAN_POINT('Ctrl Pts',(-2.37030425385408,-1.26598169985927,
8.84279849653635));
#374970=CARTESIAN_POINT('Ctrl Pts',(-2.38010696112141,-1.28061757822348,
8.82725662040549));
#374971=CARTESIAN_POINT('Ctrl Pts',(-2.38989933570247,-1.29523738354307,
8.81169306718667));
#374972=CARTESIAN_POINT('Ctrl Pts',(-2.39968192566132,-1.30984196029031,
8.79610912703474));
#374973=CARTESIAN_POINT('',(-2.3640791495949,-1.37305829436825,8.79610912703474));
#374974=CARTESIAN_POINT('Origin',(0.,1.84795814293585E-15,8.79610912703474));
#374975=CARTESIAN_POINT('',(-2.29260852370877,-1.36982616113506,8.85933012996512));
#374976=CARTESIAN_POINT('Ctrl Pts',(-2.3640791495949,-1.37305829436825,
8.79610912703474));
#374977=CARTESIAN_POINT('Ctrl Pts',(-2.35784987513059,-1.37277641721536,
8.80163734024559));
#374978=CARTESIAN_POINT('Ctrl Pts',(-2.35161832399032,-1.37249448057906,
8.80716298614018));
#374979=CARTESIAN_POINT('Ctrl Pts',(-2.34538445227342,-1.37221248311704,
8.8126860086129));
#374980=CARTESIAN_POINT('Ctrl Pts',(-2.32781127272986,-1.37141753701356,
8.82825531609049));
#374981=CARTESIAN_POINT('Ctrl Pts',(-2.31021964051606,-1.37062210696923,
8.84380379913848));
#374982=CARTESIAN_POINT('Ctrl Pts',(-2.29260852370877,-1.36982616113506,
8.85933012996512));
#374983=CARTESIAN_POINT('',(-2.27490615106174,-1.39902807640647,8.85933012996512));
#374984=CARTESIAN_POINT('Origin',(-2.29169512014346,-1.389239051772,8.84999761231045));
#374985=CARTESIAN_POINT('',(-2.3108296592442,-1.46089889836364,8.79610912703474));
#374986=CARTESIAN_POINT('Ctrl Pts',(-2.27490615106174,-1.39902807640647,
8.85933012996512));
#374987=CARTESIAN_POINT('Ctrl Pts',(-2.27804611338465,-1.40443635581295,
8.8538223528706));
#374988=CARTESIAN_POINT('Ctrl Pts',(-2.28118488318186,-1.40984248985614,
8.84831178811348));
#374989=CARTESIAN_POINT('Ctrl Pts',(-2.28432248354866,-1.41524651964645,
8.84279849653635));
#374990=CARTESIAN_POINT('Ctrl Pts',(-2.29316732615617,-1.43048038863989,
8.82725662040549));
#374991=CARTESIAN_POINT('Ctrl Pts',(-2.30200288711053,-1.44569755559503,
8.81169306718667));
#374992=CARTESIAN_POINT('Ctrl Pts',(-2.3108296592442,-1.46089889836364,
8.79610912703474));
#374993=CARTESIAN_POINT('',(-2.27124974846884,-1.52170427000879,8.79610912703474));
#374994=CARTESIAN_POINT('Origin',(0.,1.84795814293585E-15,8.79610912703474));
#374995=CARTESIAN_POINT('',(-2.20013305013606,-1.51389963881729,8.85933012996512));
#374996=CARTESIAN_POINT('Ctrl Pts',(-2.27124974846884,-1.52170427000879,
8.79610912703474));
#374997=CARTESIAN_POINT('Ctrl Pts',(-2.2650513326482,-1.52102386101749,
8.80163734024559));
#374998=CARTESIAN_POINT('Ctrl Pts',(-2.25885064864039,-1.52034324679787,
8.80716298614018));
#374999=CARTESIAN_POINT('Ctrl Pts',(-2.25264765272094,-1.51966242319765,
8.8126860086129));
#375000=CARTESIAN_POINT('Ctrl Pts',(-2.2351615115312,-1.51774319291709,
8.82825531609049));
#375001=CARTESIAN_POINT('Ctrl Pts',(-2.21765698659039,-1.51582229742333,
8.84380379913848));
#375002=CARTESIAN_POINT('Ctrl Pts',(-2.20013305013606,-1.51389963881729,
8.85933012996512));
#375003=CARTESIAN_POINT('',(-2.18059607577691,-1.54190736071221,8.85933012996512));
#375004=CARTESIAN_POINT('Origin',(-2.19797773508277,-1.53321412162103,8.84999761231045));
#375005=CARTESIAN_POINT('',(-2.21248169808584,-1.60595268950177,8.79610912703474));
#375006=CARTESIAN_POINT('Ctrl Pts',(-2.18059607577691,-1.54190736071221,
8.85933012996512));
#375007=CARTESIAN_POINT('Ctrl Pts',(-2.18338307705917,-1.54750570630536,
8.8538223528706));
#375008=CARTESIAN_POINT('Ctrl Pts',(-2.18616902571981,-1.55310183453774,
8.84831178811348));
#375009=CARTESIAN_POINT('Ctrl Pts',(-2.1889539421727,-1.55869578791498,
8.84279849653635));
#375010=CARTESIAN_POINT('Ctrl Pts',(-2.1968045747649,-1.5744650483023,8.82725662040549));
#375011=CARTESIAN_POINT('Ctrl Pts',(-2.20464701487737,-1.59021704628989,
8.81169306718667));
#375012=CARTESIAN_POINT('Ctrl Pts',(-2.21248169808584,-1.60595268950177,
8.79610912703474));
#375013=CARTESIAN_POINT('',(-2.16908729494479,-1.66409723639932,8.79610912703474));
#375014=CARTESIAN_POINT('Origin',(0.,1.84795814293585E-15,8.79610912703474));
#375015=CARTESIAN_POINT('',(-2.09861675793328,-1.65175217815317,8.85933012996512));
#375016=CARTESIAN_POINT('Ctrl Pts',(-2.16908729494479,-1.66409723639932,
8.79610912703474));
#375017=CARTESIAN_POINT('Ctrl Pts',(-2.16294520838798,-1.66302109151611,
8.80163734024559));
#375018=CARTESIAN_POINT('Ctrl Pts',(-2.15680087145326,-1.66194459650299,
8.80716298614018));
#375019=CARTESIAN_POINT('Ctrl Pts',(-2.15065424077203,-1.66086774441477,
8.8126860086129));
#375020=CARTESIAN_POINT('Ctrl Pts',(-2.13332699224101,-1.65783211648602,
8.82825531609049));
#375021=CARTESIAN_POINT('Ctrl Pts',(-2.1159815044209,-1.65479364891445,
8.84380379913848));
#375022=CARTESIAN_POINT('Ctrl Pts',(-2.09861675793328,-1.65175217815317,
8.85933012996512));
#375023=CARTESIAN_POINT('',(-2.07732546348032,-1.67845061693468,8.85933012996512));
#375024=CARTESIAN_POINT('Origin',(-2.09522838804386,-1.67088888577092,8.84999761231046));
#375025=CARTESIAN_POINT('',(-2.10504217505421,-1.74440727656297,8.79610912703474));
#375026=CARTESIAN_POINT('Ctrl Pts',(-2.07732546348032,-1.67845061693468,
8.85933012996512));
#375027=CARTESIAN_POINT('Ctrl Pts',(-2.07974805133586,-1.68421602391164,
8.8538223528706));
#375028=CARTESIAN_POINT('Ctrl Pts',(-2.08216973079929,-1.68997915064192,
8.84831178811348));
#375029=CARTESIAN_POINT('Ctrl Pts',(-2.08459051951921,-1.69574004085176,
8.84279849653635));
#375030=CARTESIAN_POINT('Ctrl Pts',(-2.09141468216282,-1.71197989335954,
8.82725662040549));
#375031=CARTESIAN_POINT('Ctrl Pts',(-2.09823177516478,-1.72820199404106,
8.81169306718667));
#375032=CARTESIAN_POINT('Ctrl Pts',(-2.10504217505421,-1.74440727656297,
8.79610912703474));
#375033=CARTESIAN_POINT('',(-2.05801159645804,-1.79965207029775,8.79610912703474));
#375034=CARTESIAN_POINT('Origin',(0.,1.84795814293585E-15,8.79610912703474));
#375035=CARTESIAN_POINT('',(-1.98847679932027,-1.78281731348928,8.85933012996512));
#375036=CARTESIAN_POINT('Ctrl Pts',(-2.05801159645804,-1.79965207029775,
8.79610912703474));
#375037=CARTESIAN_POINT('Ctrl Pts',(-2.0519510783162,-1.79818461163279,
8.80163734024559));
#375038=CARTESIAN_POINT('Ctrl Pts',(-2.04588833685299,-1.79671665937508,
8.80716298614018));
#375039=CARTESIAN_POINT('Ctrl Pts',(-2.03982332923389,-1.79524820381508,
8.8126860086129));
#375040=CARTESIAN_POINT('Ctrl Pts',(-2.0227261747425,-1.79110865228443,
8.82825531609049));
#375041=CARTESIAN_POINT('Ctrl Pts',(-2.00561100037312,-1.78696509835006,
8.84380379913848));
#375042=CARTESIAN_POINT('Ctrl Pts',(-1.98847679932027,-1.78281731348928,
8.85933012996512));
#375043=CARTESIAN_POINT('',(-1.96551867526937,-1.80809675954565,8.85933012996512));
#375044=CARTESIAN_POINT('Origin',(-1.98386929813342,-1.80169760908463,8.84999761231047));
#375045=CARTESIAN_POINT('',(-1.98895258219515,-1.87569371995058,8.79610912703474));
#375046=CARTESIAN_POINT('Ctrl Pts',(-1.96551867526937,-1.80809675954565,
8.85933012996512));
#375047=CARTESIAN_POINT('Ctrl Pts',(-1.96756689476505,-1.81400553661246,
8.8538223528706));
#375048=CARTESIAN_POINT('Ctrl Pts',(-1.96961435383092,-1.81991197991672,
8.84831178811348));
#375049=CARTESIAN_POINT('Ctrl Pts',(-1.97166106727775,-1.82581613422559,
8.84279849653635));
#375050=CARTESIAN_POINT('Ctrl Pts',(-1.97743071802469,-1.84245984581643,
8.82725662040549));
#375051=CARTESIAN_POINT('Ctrl Pts',(-1.98319445101873,-1.85908538910055,
8.81169306718667));
#375052=CARTESIAN_POINT('Ctrl Pts',(-1.98895258219515,-1.87569371995058,
8.79610912703474));
#375053=CARTESIAN_POINT('',(-1.93847908687934,-1.92781174781517,8.79610912703474));
#375054=CARTESIAN_POINT('Origin',(0.,1.84795814293585E-15,8.79610912703474));
#375055=CARTESIAN_POINT('',(-1.87016576301192,-1.90655647007116,8.85933012996512));
#375056=CARTESIAN_POINT('Ctrl Pts',(-1.93847908687934,-1.92781174781517,
8.79610912703474));
#375057=CARTESIAN_POINT('Ctrl Pts',(-1.93252504112149,-1.92595900547087,
8.80163734024559));
#375058=CARTESIAN_POINT('Ctrl Pts',(-1.92656880823491,-1.92410562809928,
8.80716298614018));
#375059=CARTESIAN_POINT('Ctrl Pts',(-1.9206103460952,-1.92225160326638,
8.8126860086129));
#375060=CARTESIAN_POINT('Ctrl Pts',(-1.90381354151856,-1.91702513843901,
8.82825531609049));
#375061=CARTESIAN_POINT('Ctrl Pts',(-1.88699901052261,-1.91179352489374,
8.84380379913848));
#375062=CARTESIAN_POINT('Ctrl Pts',(-1.87016576301192,-1.90655647007116,
8.85933012996512));
#375063=CARTESIAN_POINT('',(-1.84563514921931,-1.9303130447361,8.85933012996512));
#375064=CARTESIAN_POINT('Origin',(-1.86435806373832,-1.92510277045971,8.84999761231044));
#375065=CARTESIAN_POINT('',(-1.86468995654685,-1.99927253550787,8.79610912703474));
#375066=CARTESIAN_POINT('Ctrl Pts',(-1.84563514921931,-1.9303130447361,
8.85933012996512));
#375067=CARTESIAN_POINT('Ctrl Pts',(-1.84730058378188,-1.93634091146037,
8.8538223528706));
#375068=CARTESIAN_POINT('Ctrl Pts',(-1.84896540900169,-1.94236640049616,
8.84831178811348));
#375069=CARTESIAN_POINT('Ctrl Pts',(-1.85062963679087,-1.94838955746755,
8.84279849653635));
#375070=CARTESIAN_POINT('Ctrl Pts',(-1.85532106690864,-1.96536873556046,
8.82725662040549));
#375071=CARTESIAN_POINT('Ctrl Pts',(-1.86000775547958,-1.98232940352366,
8.81169306718667));
#375072=CARTESIAN_POINT('Ctrl Pts',(-1.86468995654685,-1.99927253550787,
8.79610912703474));
#375073=CARTESIAN_POINT('',(-1.8109809509302,-2.0480496333465,8.79610912703474));
#375074=CARTESIAN_POINT('Origin',(0.,1.84795814293585E-15,8.79610912703474));
#375075=CARTESIAN_POINT('',(-1.74416981443405,-2.02246117716243,8.85933012996512));
#375076=CARTESIAN_POINT('Ctrl Pts',(-1.8109809509302,-2.0480496333465,8.79610912703474));
#375077=CARTESIAN_POINT('Ctrl Pts',(-1.80515784400749,-2.04581922063857,
8.80163734024559));
#375078=CARTESIAN_POINT('Ctrl Pts',(-1.79933259513609,-2.04358803407826,
8.80716298614018));
#375079=CARTESIAN_POINT('Ctrl Pts',(-1.79350516307478,-2.04135605855819,
8.8126860086129));
#375080=CARTESIAN_POINT('Ctrl Pts',(-1.77707773008581,-2.03506415709914,
8.82825531609049));
#375081=CARTESIAN_POINT('Ctrl Pts',(-1.76063293697783,-2.02876598176521,
8.84380379913848));
#375082=CARTESIAN_POINT('Ctrl Pts',(-1.74416981443405,-2.02246117716243,
8.85933012996512));
#375083=CARTESIAN_POINT('',(-1.71816751245361,-2.04459725957488,8.85933012996512));
#375084=CARTESIAN_POINT('Origin',(-1.73718578215576,-2.0405972716177,8.84999761231045));
#375085=CARTESIAN_POINT('',(-1.73276491989237,-2.11463591137414,8.79610912703474));
#375086=CARTESIAN_POINT('Ctrl Pts',(-1.71816751245361,-2.04459725957488,
8.85933012996512));
#375087=CARTESIAN_POINT('Ctrl Pts',(-1.71944331845521,-2.05071944615927,
8.8538223528706));
#375088=CARTESIAN_POINT('Ctrl Pts',(-1.72071866870505,-2.05683922089966,
8.84831178811348));
#375089=CARTESIAN_POINT('Ctrl Pts',(-1.72199357216761,-2.06295663008962,
8.84279849653635));
#375090=CARTESIAN_POINT('Ctrl Pts',(-1.72558750356354,-2.0802015035998,
8.82725662040549));
#375091=CARTESIAN_POINT('Ctrl Pts',(-1.72917788910274,-2.09742760121936,
8.81169306718667));
#375092=CARTESIAN_POINT('Ctrl Pts',(-1.73276491989237,-2.11463591137414,
8.79610912703474));
#375093=CARTESIAN_POINT('',(-1.67604110579949,-2.15987164362913,8.79610912703474));
#375094=CARTESIAN_POINT('Origin',(0.,1.84795814293585E-15,8.79610912703474));
#375095=CARTESIAN_POINT('',(-1.61100669796542,-2.13005515746017,8.85933012996512));
#375096=CARTESIAN_POINT('Ctrl Pts',(-1.67604110579949,-2.15987164362913,
8.79610912703474));
#375097=CARTESIAN_POINT('Ctrl Pts',(-1.67037286610732,-2.15727272580181,
8.80163734024559));
#375098=CARTESIAN_POINT('Ctrl Pts',(-1.66470253844822,-2.15467289847695,
8.80716298614018));
#375099=CARTESIAN_POINT('Ctrl Pts',(-1.65903008263363,-2.15207214393587,
8.8126860086129));
#375100=CARTESIAN_POINT('Ctrl Pts',(-1.64303952507815,-2.14474066061786,
8.82825531609049));
#375101=CARTESIAN_POINT('Ctrl Pts',(-1.62703204504044,-2.13740180404866,
8.84380379913848));
#375102=CARTESIAN_POINT('Ctrl Pts',(-1.61100669796542,-2.13005515746017,
8.85933012996512));
#375103=CARTESIAN_POINT('',(-1.58363955683346,-2.15047978570934,8.85933012996512));
#375104=CARTESIAN_POINT('Origin',(-1.60287503156913,-2.14770652087987,8.84999761231047));
#375105=CARTESIAN_POINT('',(-1.59371958050514,-2.2213097946926,8.79610912703474));
#375106=CARTESIAN_POINT('Ctrl Pts',(-1.58363955683346,-2.15047978570934,
8.85933012996512));
#375107=CARTESIAN_POINT('Ctrl Pts',(-1.58452049171358,-2.15667113477596,
8.8538223528706));
#375108=CARTESIAN_POINT('Ctrl Pts',(-1.5854011263057,-2.16286004775386,
8.84831178811348));
#375109=CARTESIAN_POINT('Ctrl Pts',(-1.58628146658985,-2.16904657141585,
8.84279849653635));
#375110=CARTESIAN_POINT('Ctrl Pts',(-1.58876313102894,-2.18648627745903,
8.82725662040549));
#375111=CARTESIAN_POINT('Ctrl Pts',(-1.59124245987209,-2.20390701900485,
8.81169306718667));
#375112=CARTESIAN_POINT('Ctrl Pts',(-1.59371958050514,-2.2213097946926,
8.79610912703474));
#375113=CARTESIAN_POINT('',(-1.53421404825535,-2.26281827803708,8.79610912703474));
#375114=CARTESIAN_POINT('Origin',(0.,1.84795814293585E-15,8.79610912703474));
#375115=CARTESIAN_POINT('',(-1.471223609415,-2.22889628422052,8.85933012996512));
#375116=CARTESIAN_POINT('Ctrl Pts',(-1.53421404825535,-2.26281827803708,
8.79610912703474));
#375117=CARTESIAN_POINT('Ctrl Pts',(-1.52872396780646,-2.25986153460119,
8.80163734024559));
#375118=CARTESIAN_POINT('Ctrl Pts',(-1.52323186195229,-2.25690374975992,
8.80716298614018));
#375119=CARTESIAN_POINT('Ctrl Pts',(-1.51773769172211,-2.2539449032561,
8.8126860086129));
#375120=CARTESIAN_POINT('Ctrl Pts',(-1.50224971823107,-2.24560396471667,
8.82825531609049));
#375121=CARTESIAN_POINT('Ctrl Pts',(-1.48674532943269,-2.23725458384803,
8.84380379913848));
#375122=CARTESIAN_POINT('Ctrl Pts',(-1.471223609415,-2.22889628422052,8.85933012996512));
#375123=CARTESIAN_POINT('',(-1.44260408658466,-2.24752552912784,8.85933012996512));
#375124=CARTESIAN_POINT('Origin',(-1.46197772366218,-2.24599038336614,8.84999761231047));
#375125=CARTESIAN_POINT('',(-1.44812530550984,-2.31885583959521,8.79610912703474));
#375126=CARTESIAN_POINT('Ctrl Pts',(-1.44260408658466,-2.24752552912784,
8.85933012996512));
#375127=CARTESIAN_POINT('Ctrl Pts',(-1.44308653039291,-2.25376059909534,
8.8538223528706));
#375128=CARTESIAN_POINT('Ctrl Pts',(-1.44356883061088,-2.25999321873981,
8.84831178811348));
#375129=CARTESIAN_POINT('Ctrl Pts',(-1.44405099020956,-2.2662234351211,
8.84279849653635));
#375130=CARTESIAN_POINT('Ctrl Pts',(-1.44541019000032,-2.28378631020434,
8.82725662040549));
#375131=CARTESIAN_POINT('Ctrl Pts',(-1.44676827405338,-2.30133011011268,
8.81169306718667));
#375132=CARTESIAN_POINT('Ctrl Pts',(-1.44812530550984,-2.31885583959521,
8.79610912703474));
#375133=CARTESIAN_POINT('',(-1.38608257609906,-2.35646650676757,8.79610912703474));
#375134=CARTESIAN_POINT('Origin',(0.,1.84795814293585E-15,8.79610912703474));
#375135=CARTESIAN_POINT('',(-1.32539494747702,-2.31857839805225,8.85933012996512));
#375136=CARTESIAN_POINT('Ctrl Pts',(-1.38608257609906,-2.35646650676757,
8.79610912703474));
#375137=CARTESIAN_POINT('Ctrl Pts',(-1.38079321481162,-2.35316408761611,
8.80163734024559));
#375138=CARTESIAN_POINT('Ctrl Pts',(-1.37550189900339,-2.34986049943078,
8.80716298614018));
#375139=CARTESIAN_POINT('Ctrl Pts',(-1.37020859108158,-2.34655571949919,
8.8126860086129));
#375140=CARTESIAN_POINT('Ctrl Pts',(-1.35528684506023,-2.33723960044392,
8.82825531609049));
#375141=CARTESIAN_POINT('Ctrl Pts',(-1.34034925836043,-2.32791400467276,
8.84380379913848));
#375142=CARTESIAN_POINT('Ctrl Pts',(-1.32539494747702,-2.31857839805225,
8.85933012996512));
#375143=CARTESIAN_POINT('',(-1.29564064670648,-2.33533570805445,8.85933012996512));
#375144=CARTESIAN_POINT('Origin',(-1.31507283569547,-2.33504498960374,8.84999761231046));
#375145=CARTESIAN_POINT('',(-1.29658037301229,-2.40687320845991,8.79610912703474));
#375146=CARTESIAN_POINT('Ctrl Pts',(-1.29564064670648,-2.33533570805445,
8.85933012996512));
#375147=CARTESIAN_POINT('Ctrl Pts',(-1.29572261697777,-2.34158887768291,
8.8538223528706));
#375148=CARTESIAN_POINT('Ctrl Pts',(-1.29580460094654,-2.34783959282294,
8.84831178811348));
#375149=CARTESIAN_POINT('Ctrl Pts',(-1.29588659856254,-2.35408790062804,
8.84279849653635));
#375150=CARTESIAN_POINT('Ctrl Pts',(-1.29611774846148,-2.3717017751304,
8.82725662040549));
#375151=CARTESIAN_POINT('Ctrl Pts',(-1.29634900706577,-2.38929654216429,
8.81169306718667));
#375152=CARTESIAN_POINT('Ctrl Pts',(-1.29658037301229,-2.40687320845991,
8.79610912703474));
#375153=CARTESIAN_POINT('',(-1.23225539332379,-2.44043150916128,8.79610912703474));
#375154=CARTESIAN_POINT('Origin',(0.,1.84795814293585E-15,8.79610912703474));
#375155=CARTESIAN_POINT('',(-1.17411995340352,-2.39873297591288,8.85933012996512));
#375156=CARTESIAN_POINT('Ctrl Pts',(-1.23225539332379,-2.44043150916128,
8.79610912703474));
#375157=CARTESIAN_POINT('Ctrl Pts',(-1.2271884863179,-2.4367969846429,8.80163734024559));
#375158=CARTESIAN_POINT('Ctrl Pts',(-1.22211970370725,-2.43316116826599,
8.80716298614018));
#375159=CARTESIAN_POINT('Ctrl Pts',(-1.21704900943148,-2.42952403495622,
8.8126860086129));
#375160=CARTESIAN_POINT('Ctrl Pts',(-1.20275480753492,-2.41927101731662,
8.82825531609049));
#375161=CARTESIAN_POINT('Ctrl Pts',(-1.18844540468156,-2.4090075275163,
8.84380379913848));
#375162=CARTESIAN_POINT('Ctrl Pts',(-1.17411995340352,-2.39873297591288,
8.85933012996512));
#375163=CARTESIAN_POINT('',(-1.14335314149693,-2.41354949162872,8.85933012996512));
#375164=CARTESIAN_POINT('Origin',(-1.16276403136464,-2.4145043951135,8.84999761231045));
#375165=CARTESIAN_POINT('',(-1.13970751364642,-2.48500021903835,8.79610912703474));
#375166=CARTESIAN_POINT('Ctrl Pts',(-1.14335314149693,-2.41354949162872,
8.85933012996512));
#375167=CARTESIAN_POINT('Ctrl Pts',(-1.14303430139784,-2.41979506530284,
8.8538223528706));
#375168=CARTESIAN_POINT('Ctrl Pts',(-1.14271563222769,-2.42603819040914,
8.84831178811348));
#375169=CARTESIAN_POINT('Ctrl Pts',(-1.14239713091521,-2.43227891400102,
8.84279849653635));
#375170=CARTESIAN_POINT('Ctrl Pts',(-1.14149928107782,-2.44987140873401,
8.82725662040549));
#375171=CARTESIAN_POINT('Ctrl Pts',(-1.14060276394214,-2.46744484222164,
8.81169306718667));
#375172=CARTESIAN_POINT('Ctrl Pts',(-1.13970751364642,-2.48500021903835,
8.79610912703474));
#375173=CARTESIAN_POINT('',(-1.07336460881941,-2.51436825501292,8.79610912703474));
#375174=CARTESIAN_POINT('Origin',(0.,1.84795814293585E-15,8.79610912703474));
#375175=CARTESIAN_POINT('',(-1.01802024859356,-2.46903064544887,8.85933012996512));
#375176=CARTESIAN_POINT('Ctrl Pts',(-1.07336460881941,-2.51436825501292,
8.79610912703474));
#375177=CARTESIAN_POINT('Ctrl Pts',(-1.0685409771028,-2.51041656016848,
8.80163734024559));
#375178=CARTESIAN_POINT('Ctrl Pts',(-1.06371555640473,-2.50646345594936,
8.80716298614018));
#375179=CARTESIAN_POINT('Ctrl Pts',(-1.05888831234543,-2.50250891502235,
8.8126860086129));
#375180=CARTESIAN_POINT('Ctrl Pts',(-1.04528039251535,-2.49136113064716,
8.82825531609049));
#375181=CARTESIAN_POINT('Ctrl Pts',(-1.03165797391411,-2.48020192169879,
8.84380379913848));
#375182=CARTESIAN_POINT('Ctrl Pts',(-1.01802024859356,-2.46903064544887,
8.85933012996512));
#375183=CARTESIAN_POINT('',(-0.986367352980499,-2.48184548263714,8.85933012996512));
#375184=CARTESIAN_POINT('Origin',(-1.00567718021682,-2.48404208415414,8.84999761231045));
#375185=CARTESIAN_POINT('',(-0.978151351640474,-2.5529158306859,8.79610912703474));
#375186=CARTESIAN_POINT('Ctrl Pts',(-0.986367352980499,-2.48184548263714,
8.85933012996512));
#375187=CARTESIAN_POINT('Ctrl Pts',(-0.985649012693377,-2.48805779595503,
8.8538223528706));
#375188=CARTESIAN_POINT('Ctrl Pts',(-0.984930999864287,-2.49426767668739,
8.84831178811348));
#375189=CARTESIAN_POINT('Ctrl Pts',(-0.984213308413545,-2.50047517159418,
8.84279849653635));
#375190=CARTESIAN_POINT('Ctrl Pts',(-0.982190148297381,-2.51797399522336,
8.82725662040549));
#375191=CARTESIAN_POINT('Ctrl Pts',(-0.98016953940294,-2.53545388215705,
8.81169306718667));
#375192=CARTESIAN_POINT('Ctrl Pts',(-0.978151351640474,-2.5529158306859,
8.79610912703474));
#375193=CARTESIAN_POINT('',(-0.910063138901394,-2.57797292237442,8.79610912703474));
#375194=CARTESIAN_POINT('Origin',(0.,1.84795814293585E-15,8.79610912703474));
#375195=CARTESIAN_POINT('',(-0.857737280217463,-2.5291825384573,8.85933012996512));
#375196=CARTESIAN_POINT('Ctrl Pts',(-0.910063138901394,-2.57797292237442,
8.79610912703474));
#375197=CARTESIAN_POINT('Ctrl Pts',(-0.905502603811463,-2.57372029556567,
8.80163734024559));
#375198=CARTESIAN_POINT('Ctrl Pts',(-0.900940373714666,-2.56946614765751,
8.80716298614018));
#375199=CARTESIAN_POINT('Ctrl Pts',(-0.896376416053125,-2.56521044917018,
8.8126860086129));
#375200=CARTESIAN_POINT('Ctrl Pts',(-0.883510696150999,-2.55321370669659,
8.82825531609049));
#375201=CARTESIAN_POINT('Ctrl Pts',(-0.870631239241901,-2.54120463418337,
8.84380379913848));
#375202=CARTESIAN_POINT('Ctrl Pts',(-0.857737280217463,-2.5291825384573,
8.85933012996512));
#375203=CARTESIAN_POINT('',(-0.825328369435533,-2.53994303820322,8.85933012996512));
#375204=CARTESIAN_POINT('Origin',(-0.844457785818422,-2.54337231144563,
8.84999761231047));
#375205=CARTESIAN_POINT('',(-0.812575755917834,-2.61034096358643,8.79610912703474));
#375206=CARTESIAN_POINT('Ctrl Pts',(-0.825328369435533,-2.53994303820322,
8.85933012996512));
#375207=CARTESIAN_POINT('Ctrl Pts',(-0.824213480774706,-2.54609656343692,
8.8538223528706));
#375208=CARTESIAN_POINT('Ctrl Pts',(-0.823099074755404,-2.5522476820634,
8.84831178811348));
#375209=CARTESIAN_POINT('Ctrl Pts',(-0.821985142314512,-2.55839644035702,
8.84279849653635));
#375210=CARTESIAN_POINT('Ctrl Pts',(-0.818844985518465,-2.57572968646262,
8.82725662040549));
#375211=CARTESIAN_POINT('Ctrl Pts',(-0.815708587980628,-2.59304419823752,
8.81169306718667));
#375212=CARTESIAN_POINT('Ctrl Pts',(-0.812575755917834,-2.61034096358643,
8.79610912703474));
#375213=CARTESIAN_POINT('',(-0.743022024337704,-2.63098414602442,8.79610912703474));
#375214=CARTESIAN_POINT('Origin',(0.,1.84795814293585E-15,8.79610912703474));
#375215=CARTESIAN_POINT('',(-0.693929685372884,-2.57894147790725,8.85933012996512));
#375216=CARTESIAN_POINT('Ctrl Pts',(-0.743022024337704,-2.63098414602442,
8.79610912703474));
#375217=CARTESIAN_POINT('Ctrl Pts',(-0.738743326091364,-2.6264480622071,
8.80163734024559));
#375218=CARTESIAN_POINT('Ctrl Pts',(-0.734463033777905,-2.62191035181617,
8.80716298614018));
#375219=CARTESIAN_POINT('Ctrl Pts',(-0.730181116795117,-2.61737098334645,
8.8126860086129));
#375220=CARTESIAN_POINT('Ctrl Pts',(-0.718110464823709,-2.60457457996258,
8.82825531609049));
#375221=CARTESIAN_POINT('Ctrl Pts',(-0.706026894057835,-2.59176499173941,
8.84380379913848));
#375222=CARTESIAN_POINT('Ctrl Pts',(-0.693929685372884,-2.57894147790725,
8.85933012996512));
#375223=CARTESIAN_POINT('',(-0.660897934588176,-2.58760342300926,8.85933012996512));
#375224=CARTESIAN_POINT('Origin',(-0.679768333242473,-2.59225127635776,
8.84999761231045));
#375225=CARTESIAN_POINT('',(-0.643661112117175,-2.6570396455512,8.79610912703474));
#375226=CARTESIAN_POINT('Ctrl Pts',(-0.660897934588176,-2.58760342300926,
8.85933012996512));
#375227=CARTESIAN_POINT('Ctrl Pts',(-0.659391078870295,-2.59367287400364,
8.8538223528706));
#375228=CARTESIAN_POINT('Ctrl Pts',(-0.657884858994153,-2.59973995425839,
8.84831178811348));
#375229=CARTESIAN_POINT('Ctrl Pts',(-0.656379262950449,-2.60580470937212,
8.84279849653635));
#375230=CARTESIAN_POINT('Ctrl Pts',(-0.652135013052355,-2.62290115192791,
8.82725662040549));
#375231=CARTESIAN_POINT('Ctrl Pts',(-0.64789571500136,-2.6399791395012,
8.81169306718667));
#375232=CARTESIAN_POINT('Ctrl Pts',(-0.643661112117175,-2.6570396455512,
8.79610912703474));
#375233=CARTESIAN_POINT('',(-0.572927672898287,-2.67318409147408,8.79610912703474));
#375234=CARTESIAN_POINT('Origin',(0.,1.84795814293585E-15,8.79610912703474));
#375235=CARTESIAN_POINT('',(-0.527270584603657,-2.61810299364327,8.85933012996512));
#375236=CARTESIAN_POINT('Ctrl Pts',(-0.572927672898287,-2.67318409147408,
8.79610912703474));
#375237=CARTESIAN_POINT('Ctrl Pts',(-0.56894839358441,-2.66838319038958,
8.80163734024559));
#375238=CARTESIAN_POINT('Ctrl Pts',(-0.564967627693525,-2.66358056394121,
8.80716298614018));
#375239=CARTESIAN_POINT('Ctrl Pts',(-0.56098534670484,-2.65877617872783,
8.8126860086129));
#375240=CARTESIAN_POINT('Ctrl Pts',(-0.549759363562247,-2.64523269760001,
8.82825531609049));
#375241=CARTESIAN_POINT('Ctrl Pts',(-0.538521332923791,-2.63167523101254,
8.84380379913848));
#375242=CARTESIAN_POINT('Ctrl Pts',(-0.527270584603657,-2.61810299364327,
8.85933012996512));
#375243=CARTESIAN_POINT('',(-0.493751728365434,-2.62463079031095,8.85933012996512));
#375244=CARTESIAN_POINT('Origin',(-0.512285566775374,-2.63047812473917,
8.84999761231046));
#375245=CARTESIAN_POINT('',(-0.472101526741951,-2.69281998167918,8.79610912703474));
#375246=CARTESIAN_POINT('Ctrl Pts',(-0.493751728365434,-2.62463079031095,
8.85933012996512));
#375247=CARTESIAN_POINT('Ctrl Pts',(-0.491859097583863,-2.63059122639,8.8538223528706));
#375248=CARTESIAN_POINT('Ctrl Pts',(-0.489967253231435,-2.63654933733887,
8.84831178811348));
#375249=CARTESIAN_POINT('Ctrl Pts',(-0.488076180402012,-2.64250516789305,
8.84279849653635));
#375250=CARTESIAN_POINT('Ctrl Pts',(-0.482745277935091,-2.6592945539494,
8.82725662040549));
#375251=CARTESIAN_POINT('Ctrl Pts',(-0.477420499555957,-2.67606584020692,
8.81169306718667));
#375252=CARTESIAN_POINT('Ctrl Pts',(-0.472101526741951,-2.69281998167918,
8.79610912703474));
#375253=CARTESIAN_POINT('',(-0.40047903875833,-2.70439935009569,8.79610912703474));
#375254=CARTESIAN_POINT('Origin',(0.,1.84795814293585E-15,8.79610912703474));
#375255=CARTESIAN_POINT('',(-0.358444815903108,-2.64650616259708,8.85933012996512));
#375256=CARTESIAN_POINT('Ctrl Pts',(-0.40047903875833,-2.70439935009569,
8.79610912703474));
#375257=CARTESIAN_POINT('Ctrl Pts',(-0.396815530089169,-2.69935335967635,
8.80163734024559));
#375258=CARTESIAN_POINT('Ctrl Pts',(-0.393150648441775,-2.69430555219278,
8.80716298614018));
#375259=CARTESIAN_POINT('Ctrl Pts',(-0.389484367493974,-2.68925589248512,
8.8126860086129));
#375260=CARTESIAN_POINT('Ctrl Pts',(-0.379149183152894,-2.67502098668236,
8.82825531609049));
#375261=CARTESIAN_POINT('Ctrl Pts',(-0.3688028721203,-2.66077135226888,
8.84380379913848));
#375262=CARTESIAN_POINT('Ctrl Pts',(-0.358444815903108,-2.64650616259708,
8.85933012996512));
#375263=CARTESIAN_POINT('',(-0.324576590381425,-2.65087298671372,8.85933012996512));
#375264=CARTESIAN_POINT('Origin',(-0.342697709029489,-2.65789577427027,
8.84999761231044));
#375265=CARTESIAN_POINT('',(-0.298601974927885,-2.71753494289437,8.79610912703474));
#375266=CARTESIAN_POINT('Ctrl Pts',(-0.324576590381425,-2.65087298671372,
8.85933012996512));
#375267=CARTESIAN_POINT('Ctrl Pts',(-0.322305961762013,-2.65669991516707,
8.8538223528706));
#375268=CARTESIAN_POINT('Ctrl Pts',(-0.320036266927543,-2.66252457365416,
8.84831178811348));
#375269=CARTESIAN_POINT('Ctrl Pts',(-0.317767488136291,-2.66834700586353,
8.84279849653635));
#375270=CARTESIAN_POINT('Ctrl Pts',(-0.311371838922255,-2.68476034423181,
8.82725662040549));
#375271=CARTESIAN_POINT('Ctrl Pts',(-0.304983460871502,-2.70115601236091,
8.81169306718667));
#375272=CARTESIAN_POINT('Ctrl Pts',(-0.298601974927885,-2.71753494289437,
8.79610912703474));
#375273=CARTESIAN_POINT('',(-0.22638475034563,-2.7245016516959,8.79610912703474));
#375274=CARTESIAN_POINT('Origin',(0.,1.84795814293585E-15,8.79610912703474));
#375275=CARTESIAN_POINT('',(-0.188146120567841,-2.66403427005499,8.85933012996512));
#375276=CARTESIAN_POINT('Ctrl Pts',(-0.22638475034563,-2.7245016516959,
8.79610912703474));
#375277=CARTESIAN_POINT('Ctrl Pts',(-0.223052066464128,-2.71923130699873,
8.80163734024559));
#375278=CARTESIAN_POINT('Ctrl Pts',(-0.219718128845028,-2.71395906100366,
8.80716298614018));
#375279=CARTESIAN_POINT('Ctrl Pts',(-0.216382913472939,-2.70868487693661,
8.8126860086129));
#375280=CARTESIAN_POINT('Ctrl Pts',(-0.206980997422721,-2.69381704074023,
8.82825531609049));
#375281=CARTESIAN_POINT('Ctrl Pts',(-0.197568921207299,-2.67893379330507,
8.84380379913848));
#375282=CARTESIAN_POINT('Ctrl Pts',(-0.188146120567841,-2.66403427005499,
8.85933012996512));
#375283=CARTESIAN_POINT('',(-0.154067697566079,-2.66622217740361,8.85933012996512));
#375284=CARTESIAN_POINT('Origin',(-0.171701632888769,-2.674391559948,8.84999761231045));
#375285=CARTESIAN_POINT('',(-0.123875403548917,-2.7310829701198,8.79610912703474));
#375286=CARTESIAN_POINT('Ctrl Pts',(-0.154067697566079,-2.66622217740361,
8.85933012996512));
#375287=CARTESIAN_POINT('Ctrl Pts',(-0.151428401608871,-2.67189165413237,
8.8538223528706));
#375288=CARTESIAN_POINT('Ctrl Pts',(-0.148790182955282,-2.67755892538658,
8.84831178811348));
#375289=CARTESIAN_POINT('Ctrl Pts',(-0.146153021100905,-2.68322403362827,
8.84279849653635));
#375290=CARTESIAN_POINT('Ctrl Pts',(-0.138718906234236,-2.69919387838049,
8.82725662040549));
#375291=CARTESIAN_POINT('Ctrl Pts',(-0.131293179727579,-2.71514655506395,
8.81169306718667));
#375292=CARTESIAN_POINT('Ctrl Pts',(-0.123875403548917,-2.7310829701198,
8.79610912703474));
#375293=CARTESIAN_POINT('',(-0.0513601984344042,-2.73340839160553,8.79610912703474));
#375294=CARTESIAN_POINT('Origin',(0.,1.84795814293585E-15,8.79610912703474));
#375295=CARTESIAN_POINT('',(-0.0170742924659647,-2.67061528926368,8.85933012996512));
#375296=CARTESIAN_POINT('Ctrl Pts',(-0.0513601984344042,-2.73340839160553,
8.79610912703474));
#375297=CARTESIAN_POINT('Ctrl Pts',(-0.0483720340534879,-2.72793534960737,
8.80163734024559));
#375298=CARTESIAN_POINT('Ctrl Pts',(-0.045382740327487,-2.72246032989048,
8.80716298614018));
#375299=CARTESIAN_POINT('Ctrl Pts',(-0.0423922956464754,-2.71698329421768,
8.8126860086129));
#375300=CARTESIAN_POINT('Ctrl Pts',(-0.0339622823768732,-2.70154362275576,
8.82825531609049));
#375301=CARTESIAN_POINT('Ctrl Pts',(-0.0255231172186754,-2.68608792075508,
8.84380379913848));
#375302=CARTESIAN_POINT('Ctrl Pts',(-0.0170742924659647,-2.67061528926368,
8.85933012996512));
#375303=CARTESIAN_POINT('',(0.0170742924659647,-2.67061528926368,8.85933012996512));
#375304=CARTESIAN_POINT('Origin',(2.09135199175786E-9,-2.67989769705071,
8.84999761231045));
#375305=CARTESIAN_POINT('',(0.0513601984344042,-2.73340839160553,8.79610912703474));
#375306=CARTESIAN_POINT('Ctrl Pts',(0.0170742924659647,-2.67061528926368,
8.85933012996512));
#375307=CARTESIAN_POINT('Ctrl Pts',(0.0200714103277523,-2.67610401717189,
8.8538223528706));
#375308=CARTESIAN_POINT('Ctrl Pts',(0.0230673117941167,-2.68159061315999,
8.84831178811348));
#375309=CARTESIAN_POINT('Ctrl Pts',(0.0260620200478886,-2.68707511828909,
8.84279849653635));
#375310=CARTESIAN_POINT('Ctrl Pts',(0.0345040521945901,-2.70253584590764,
8.82725662040549));
#375311=CARTESIAN_POINT('Ctrl Pts',(0.0429366132541237,-2.71797997817513,
8.81169306718667));
#375312=CARTESIAN_POINT('Ctrl Pts',(0.0513601984344042,-2.73340839160553,
8.79610912703474));
#375313=CARTESIAN_POINT('',(0.123875403548956,-2.73108297011979,8.79610912703474));
#375314=CARTESIAN_POINT('Origin',(0.,1.84795814293585E-15,8.79610912703474));
#375315=CARTESIAN_POINT('',(0.154067697566117,-2.6662221774036,8.85933012996512));
#375316=CARTESIAN_POINT('Ctrl Pts',(0.123875403548956,-2.73108297011979,
8.79610912703474));
#375317=CARTESIAN_POINT('Ctrl Pts',(0.126506769420886,-2.72542972072417,
8.80163734024559));
#375318=CARTESIAN_POINT('Ctrl Pts',(0.129139135604666,-2.71977442531588,
8.80716298614018));
#375319=CARTESIAN_POINT('Ctrl Pts',(0.131772521215958,-2.71411704435172,
8.8126860086129));
#375320=CARTESIAN_POINT('Ctrl Pts',(0.139195990972187,-2.6981689825461,
8.82825531609049));
#375321=CARTESIAN_POINT('Ctrl Pts',(0.146627566733329,-2.68220433677466,
8.84380379913848));
#375322=CARTESIAN_POINT('Ctrl Pts',(0.154067697566117,-2.6662221774036,
8.85933012996512));
#375323=CARTESIAN_POINT('',(0.18814612056788,-2.66403427005499,8.85933012996512));
#375324=CARTESIAN_POINT('Origin',(0.171701637062919,-2.67439155968,8.84999761231045));
#375325=CARTESIAN_POINT('',(0.226384750345669,-2.7245016516959,8.79610912703474));
#375326=CARTESIAN_POINT('Ctrl Pts',(0.18814612056788,-2.66403427005499,
8.85933012996512));
#375327=CARTESIAN_POINT('Ctrl Pts',(0.191488744534073,-2.66931969478233,
8.8538223528706));
#375328=CARTESIAN_POINT('Ctrl Pts',(0.194830018011469,-2.67460306990455,
8.84831178811348));
#375329=CARTESIAN_POINT('Ctrl Pts',(0.198169966766059,-2.67988443491305,
8.84279849653635));
#375330=CARTESIAN_POINT('Ctrl Pts',(0.207585226071892,-2.69477251395182,
8.82725662040549));
#375331=CARTESIAN_POINT('Ctrl Pts',(0.216989970482129,-2.70964463855111,
8.81169306718667));
#375332=CARTESIAN_POINT('Ctrl Pts',(0.226384750345669,-2.7245016516959,
8.79610912703474));
#375333=CARTESIAN_POINT('',(0.298601974927924,-2.71753494289437,8.79610912703474));
#375334=CARTESIAN_POINT('Origin',(0.,1.84795814293585E-15,8.79610912703474));
#375335=CARTESIAN_POINT('',(0.324576590381463,-2.65087298671371,8.85933012996512));
#375336=CARTESIAN_POINT('Ctrl Pts',(0.298601974927924,-2.71753494289437,
8.79610912703474));
#375337=CARTESIAN_POINT('Ctrl Pts',(0.300865729444074,-2.71172471651568,
8.80163734024559));
#375338=CARTESIAN_POINT('Ctrl Pts',(0.303130351128344,-2.70591238423786,
8.80716298614018));
#375339=CARTESIAN_POINT('Ctrl Pts',(0.305395856523578,-2.70009790537424,
8.8126860086129));
#375340=CARTESIAN_POINT('Ctrl Pts',(0.311782278136876,-2.68370698723172,
8.82825531609049));
#375341=CARTESIAN_POINT('Ctrl Pts',(0.318175726562094,-2.6672989998434,
8.84380379913848));
#375342=CARTESIAN_POINT('Ctrl Pts',(0.324576590381463,-2.65087298671371,
8.85933012996512));
#375343=CARTESIAN_POINT('',(0.358444815903146,-2.64650616259708,8.85933012996512));
#375344=CARTESIAN_POINT('Origin',(0.342697713177886,-2.65789577373536,8.84999761231047));
#375345=CARTESIAN_POINT('',(0.400479038758368,-2.70439935009568,8.79610912703474));
#375346=CARTESIAN_POINT('Ctrl Pts',(0.358444815903146,-2.64650616259708,
8.85933012996512));
#375347=CARTESIAN_POINT('Ctrl Pts',(0.362119210414878,-2.65156656519963,
8.8538223528706));
#375348=CARTESIAN_POINT('Ctrl Pts',(0.365792125893886,-2.65662500893431,
8.84831178811348));
#375349=CARTESIAN_POINT('Ctrl Pts',(0.369463590583444,-2.66168153156055,
8.84279849653635));
#375350=CARTESIAN_POINT('Ctrl Pts',(0.379813387728354,-2.67593578370929,
8.82725662040549));
#375351=CARTESIAN_POINT('Ctrl Pts',(0.390151669377202,-2.69017478789034,
8.81169306718667));
#375352=CARTESIAN_POINT('Ctrl Pts',(0.400479038758368,-2.70439935009568,
8.79610912703474));
#375353=CARTESIAN_POINT('',(0.47210152674199,-2.69281998167918,8.79610912703474));
#375354=CARTESIAN_POINT('Origin',(0.,1.84795814293585E-15,8.79610912703474));
#375355=CARTESIAN_POINT('',(0.493751728365472,-2.62463079031094,8.85933012996512));
#375356=CARTESIAN_POINT('Ctrl Pts',(0.47210152674199,-2.69281998167918,
8.79610912703474));
#375357=CARTESIAN_POINT('Ctrl Pts',(0.473988367649479,-2.6868766537839,
8.80163734024559));
#375358=CARTESIAN_POINT('Ctrl Pts',(0.475875939017978,-2.68093116875663,
8.80716298614018));
#375359=CARTESIAN_POINT('Ctrl Pts',(0.477764254749538,-2.67498348493439,
8.8126860086129));
#375360=CARTESIAN_POINT('Ctrl Pts',(0.483087385043613,-2.65821706425346,
8.82825531609049));
#375361=CARTESIAN_POINT('Ctrl Pts',(0.488416434081935,-2.64143315918795,
8.84380379913848));
#375362=CARTESIAN_POINT('Ctrl Pts',(0.493751728365472,-2.62463079031094,
8.85933012996512));
#375363=CARTESIAN_POINT('',(0.527270584603695,-2.61810299364326,8.85933012996512));
#375364=CARTESIAN_POINT('Origin',(0.512285570880988,-2.63047812393962,8.84999761231044));
#375365=CARTESIAN_POINT('',(0.572927672898325,-2.67318409147408,8.79610912703474));
#375366=CARTESIAN_POINT('Ctrl Pts',(0.527270584603695,-2.61810299364326,
8.85933012996512));
#375367=CARTESIAN_POINT('Ctrl Pts',(0.531261650785761,-2.62291757984128,
8.8538223528706));
#375368=CARTESIAN_POINT('Ctrl Pts',(0.53525111546884,-2.62773030595808,
8.84831178811348));
#375369=CARTESIAN_POINT('Ctrl Pts',(0.53923900925743,-2.63254120786596,
8.84279849653635));
#375370=CARTESIAN_POINT('Ctrl Pts',(0.550480814704924,-2.64610305934507,
8.82725662040549));
#375371=CARTESIAN_POINT('Ctrl Pts',(0.561710151375533,-2.65965043198543,
8.81169306718667));
#375372=CARTESIAN_POINT('Ctrl Pts',(0.572927672898325,-2.67318409147408,
8.79610912703474));
#375373=CARTESIAN_POINT('',(0.643661112117213,-2.65703964555119,8.79610912703474));
#375374=CARTESIAN_POINT('Origin',(0.,1.84795814293585E-15,8.79610912703474));
#375375=CARTESIAN_POINT('',(0.660897934588214,-2.58760342300925,8.85933012996512));
#375376=CARTESIAN_POINT('Ctrl Pts',(0.643661112117213,-2.65703964555119,
8.79610912703474));
#375377=CARTESIAN_POINT('Ctrl Pts',(0.645163285982027,-2.65098763854848,
8.80163734024559));
#375378=CARTESIAN_POINT('Ctrl Pts',(0.646666050599119,-2.64493343204504,
8.80716298614018));
#375379=CARTESIAN_POINT('Ctrl Pts',(0.64816941717262,-2.63887698357279,
8.8126860086129));
#375380=CARTESIAN_POINT('Ctrl Pts',(0.652407382263286,-2.62180395717242,
8.82825531609049));
#375381=CARTESIAN_POINT('Ctrl Pts',(0.656650133709137,-2.60471310309575,
8.84380379913848));
#375382=CARTESIAN_POINT('Ctrl Pts',(0.660897934588214,-2.58760342300925,
8.85933012996512));
#375383=CARTESIAN_POINT('',(0.693929685372921,-2.57894147790724,8.85933012996512));
#375384=CARTESIAN_POINT('Origin',(0.679768337288427,-2.59225127529681,8.84999761231044));
#375385=CARTESIAN_POINT('',(0.743022024337742,-2.63098414602441,8.79610912703474));
#375386=CARTESIAN_POINT('Ctrl Pts',(0.693929685372921,-2.57894147790724,
8.85933012996512));
#375387=CARTESIAN_POINT('Ctrl Pts',(0.698221023078299,-2.58349046353331,
8.8538223528706));
#375388=CARTESIAN_POINT('Ctrl Pts',(0.702510643399328,-2.58803769550829,
8.84831178811348));
#375389=CARTESIAN_POINT('Ctrl Pts',(0.706798579175972,-2.59258320766993,
8.84279849653635));
#375390=CARTESIAN_POINT('Ctrl Pts',(0.718886197936108,-2.60539692992268,
8.82725662040549));
#375391=CARTESIAN_POINT('Ctrl Pts',(0.730960445875413,-2.61819700196228,
8.81169306718667));
#375392=CARTESIAN_POINT('Ctrl Pts',(0.743022024337742,-2.63098414602441,
8.79610912703474));
#375393=CARTESIAN_POINT('',(0.812575755917872,-2.61034096358642,8.79610912703474));
#375394=CARTESIAN_POINT('Origin',(0.,1.84795814293585E-15,8.79610912703474));
#375395=CARTESIAN_POINT('',(0.82532836943557,-2.53994303820321,8.85933012996512));
#375396=CARTESIAN_POINT('Ctrl Pts',(0.812575755917872,-2.61034096358642,
8.79610912703474));
#375397=CARTESIAN_POINT('Ctrl Pts',(0.813687089985383,-2.6042051464712,
8.80163734024559));
#375398=CARTESIAN_POINT('Ctrl Pts',(0.814798872668915,-2.59806709652474,
8.80716298614018));
#375399=CARTESIAN_POINT('Ctrl Pts',(0.815911112428636,-2.59192677064835,
8.8126860086129));
#375400=CARTESIAN_POINT('Ctrl Pts',(0.819046497608294,-2.57461729525616,
8.82825531609049));
#375401=CARTESIAN_POINT('Ctrl Pts',(0.822185517085916,-2.55728972215373,
8.84380379913848));
#375402=CARTESIAN_POINT('Ctrl Pts',(0.82532836943557,-2.53994303820321,
8.85933012996512));
#375403=CARTESIAN_POINT('',(0.857737280217499,-2.52918253845728,8.85933012996512));
#375404=CARTESIAN_POINT('Origin',(0.844457789788073,-2.5433723101276,8.84999761231049));
#375405=CARTESIAN_POINT('',(0.910063138901431,-2.57797292237441,8.79610912703474));
#375406=CARTESIAN_POINT('Ctrl Pts',(0.857737280217499,-2.52918253845728,
8.85933012996512));
#375407=CARTESIAN_POINT('Ctrl Pts',(0.862311255419068,-2.53344723075371,
8.8538223528706));
#375408=CARTESIAN_POINT('Ctrl Pts',(0.866883404408027,-2.53771028303531,
8.84831178811348));
#375409=CARTESIAN_POINT('Ctrl Pts',(0.871453762124861,-2.54197172696624,
8.84279849653635));
#375410=CARTESIAN_POINT('Ctrl Pts',(0.884337523579365,-2.55398466565934,
8.82725662040549));
#375411=CARTESIAN_POINT('Ctrl Pts',(0.897207067112666,-2.56598483885656,
8.81169306718667));
#375412=CARTESIAN_POINT('Ctrl Pts',(0.910063138901431,-2.57797292237441,
8.79610912703474));
#375413=CARTESIAN_POINT('',(0.97815135164051,-2.55291583068589,8.79610912703474));
#375414=CARTESIAN_POINT('Origin',(0.,1.84795814293585E-15,8.79610912703474));
#375415=CARTESIAN_POINT('',(0.986367352980535,-2.48184548263713,8.85933012996512));
#375416=CARTESIAN_POINT('Ctrl Pts',(0.97815135164051,-2.55291583068589,
8.79610912703474));
#375417=CARTESIAN_POINT('Ctrl Pts',(0.978867279200656,-2.54672141684682,
8.80163734024559));
#375418=CARTESIAN_POINT('Ctrl Pts',(0.979583511397104,-2.54052474602117,
8.80716298614018));
#375419=CARTESIAN_POINT('Ctrl Pts',(0.980300053911298,-2.53432577465677,
8.8126860086129));
#375420=CARTESIAN_POINT('Ctrl Pts',(0.982319975209707,-2.51685097862002,
8.82825531609049));
#375421=CARTESIAN_POINT('Ctrl Pts',(0.984342363814749,-2.49935788920645,
8.84380379913848));
#375422=CARTESIAN_POINT('Ctrl Pts',(0.986367352980535,-2.48184548263713,
8.85933012996512));
#375423=CARTESIAN_POINT('',(1.01802024859359,-2.46903064544885,8.85933012996512));
#375424=CARTESIAN_POINT('Origin',(1.00567718409387,-2.48404208258446,8.84999761231049));
#375425=CARTESIAN_POINT('',(1.07336460881944,-2.51436825501291,8.79610912703474));
#375426=CARTESIAN_POINT('Ctrl Pts',(1.01802024859359,-2.46903064544885,
8.85933012996512));
#375427=CARTESIAN_POINT('Ctrl Pts',(1.02285806584614,-2.47299351988022,
8.8538223528706));
#375428=CARTESIAN_POINT('Ctrl Pts',(1.02769395556211,-2.47695487467219,
8.84831178811348));
#375429=CARTESIAN_POINT('Ctrl Pts',(1.03252795463893,-2.48091473918521,
8.84279849653635));
#375430=CARTESIAN_POINT('Ctrl Pts',(1.04615491664843,-2.49207753057682,
8.82725662040549));
#375431=CARTESIAN_POINT('Ctrl Pts',(1.05976687206084,-2.50322849364596,
8.81169306718667));
#375432=CARTESIAN_POINT('Ctrl Pts',(1.07336460881944,-2.51436825501291,
8.79610912703474));
#375433=CARTESIAN_POINT('',(1.13970751364645,-2.48500021903834,8.79610912703474));
#375434=CARTESIAN_POINT('Origin',(0.,1.84795814293585E-15,8.79610912703474));
#375435=CARTESIAN_POINT('',(1.14335314149697,-2.4135494916287,8.85933012996512));
#375436=CARTESIAN_POINT('Ctrl Pts',(1.13970751364645,-2.48500021903834,
8.79610912703474));
#375437=CARTESIAN_POINT('Ctrl Pts',(1.14002509279932,-2.47877266265058,
8.80163734024559));
#375438=CARTESIAN_POINT('Ctrl Pts',(1.14034283135696,-2.47254283439536,
8.80716298614018));
#375439=CARTESIAN_POINT('Ctrl Pts',(1.14066073219874,-2.46631069044594,
8.8126860086129));
#375440=CARTESIAN_POINT('Ctrl Pts',(1.14155688932601,-2.44874238144989,
8.82825531609049));
#375441=CARTESIAN_POINT('Ctrl Pts',(1.14245433662989,-2.43115565858184,
8.84380379913848));
#375442=CARTESIAN_POINT('Ctrl Pts',(1.14335314149697,-2.4135494916287,8.85933012996512));
#375443=CARTESIAN_POINT('',(1.17411995340356,-2.39873297591286,8.85933012996512));
#375444=CARTESIAN_POINT('Origin',(1.16276403513316,-2.41450439329867,8.84999761231046));
#375445=CARTESIAN_POINT('',(1.23225539332383,-2.44043150916126,8.79610912703474));
#375446=CARTESIAN_POINT('Ctrl Pts',(1.17411995340356,-2.39873297591286,
8.85933012996512));
#375447=CARTESIAN_POINT('Ctrl Pts',(1.17920173307828,-2.40237774817809,
8.8538223528706));
#375448=CARTESIAN_POINT('Ctrl Pts',(1.18428149181312,-2.40602112742388,
8.84831178811348));
#375449=CARTESIAN_POINT('Ctrl Pts',(1.18935926831084,-2.40966314058634,
8.84279849653635));
#375450=CARTESIAN_POINT('Ctrl Pts',(1.20367343476546,-2.4199299143722,8.82725662040549));
#375451=CARTESIAN_POINT('Ctrl Pts',(1.21797186761244,-2.43018584561414,
8.81169306718667));
#375452=CARTESIAN_POINT('Ctrl Pts',(1.23225539332383,-2.44043150916126,
8.79610912703474));
#375453=CARTESIAN_POINT('',(1.29658037301232,-2.40687320845989,8.79610912703474));
#375454=CARTESIAN_POINT('Origin',(0.,1.84795814293585E-15,8.79610912703474));
#375455=CARTESIAN_POINT('',(1.29564064670651,-2.33533570805443,8.85933012996512));
#375456=CARTESIAN_POINT('Ctrl Pts',(1.29658037301232,-2.40687320845989,
8.79610912703474));
#375457=CARTESIAN_POINT('Ctrl Pts',(1.29649829875706,-2.40063809988845,
8.80163734024559));
#375458=CARTESIAN_POINT('Ctrl Pts',(1.29641623802,-2.39440071390423,8.80716298614018));
#375459=CARTESIAN_POINT('Ctrl Pts',(1.29633419086661,-2.3881610065861,8.8126860086129));
#375460=CARTESIAN_POINT('Ctrl Pts',(1.29610290132089,-2.37057137658079,
8.82825531609049));
#375461=CARTESIAN_POINT('Ctrl Pts',(1.29587171952014,-2.35296328787486,
8.84380379913848));
#375462=CARTESIAN_POINT('Ctrl Pts',(1.29564064670651,-2.33533570805443,
8.85933012996512));
#375463=CARTESIAN_POINT('',(1.32539494747705,-2.31857839805223,8.85933012996512));
#375464=CARTESIAN_POINT('Origin',(1.31507283933998,-2.33504498755122,8.84999761231044));
#375465=CARTESIAN_POINT('',(1.38608257609909,-2.35646650676755,8.79610912703474));
#375466=CARTESIAN_POINT('Ctrl Pts',(1.32539494747705,-2.31857839805223,
8.85933012996512));
#375467=CARTESIAN_POINT('Ctrl Pts',(1.33069980745122,-2.32189009100029,
8.8538223528706));
#375468=CARTESIAN_POINT('Ctrl Pts',(1.33600256138669,-2.32520052327308,
8.84831178811348));
#375469=CARTESIAN_POINT('Ctrl Pts',(1.3413032496325,-2.32850971927166,8.84279849653635));
#375470=CARTESIAN_POINT('Ctrl Pts',(1.3562458005519,-2.33783828707609,8.82725662040549));
#375471=CARTESIAN_POINT('Ctrl Pts',(1.37117195550587,-2.34715704266946,
8.81169306718667));
#375472=CARTESIAN_POINT('Ctrl Pts',(1.38608257609909,-2.35646650676755,
8.79610912703474));
#375473=CARTESIAN_POINT('',(1.44812530550987,-2.31885583959519,8.79610912703474));
#375474=CARTESIAN_POINT('Origin',(0.,1.84795814293585E-15,8.79610912703474));
#375475=CARTESIAN_POINT('',(1.44260408658469,-2.24752552912782,8.85933012996512));
#375476=CARTESIAN_POINT('Ctrl Pts',(1.44812530550987,-2.31885583959519,
8.79610912703474));
#375477=CARTESIAN_POINT('Ctrl Pts',(1.44764391510719,-2.31263880023861,
8.80163734024559));
#375478=CARTESIAN_POINT('Ctrl Pts',(1.4471623922806,-2.30641948728234,8.80716298614018));
#375479=CARTESIAN_POINT('Ctrl Pts',(1.4466807342814,-2.30019785689126,8.8126860086129));
#375480=CARTESIAN_POINT('Ctrl Pts',(1.44532294848104,-2.28265918543935,
8.82825531609049));
#375481=CARTESIAN_POINT('Ctrl Pts',(1.44396408755126,-2.26510208630896,
8.84380379913848));
#375482=CARTESIAN_POINT('Ctrl Pts',(1.44260408658469,-2.24752552912782,
8.85933012996512));
#375483=CARTESIAN_POINT('',(1.47122360941503,-2.2288962842205,8.85933012996512));
#375484=CARTESIAN_POINT('Origin',(1.46197772716769,-2.24599038108432,8.84999761231046));
#375485=CARTESIAN_POINT('',(1.53421404825539,-2.26281827803705,8.79610912703474));
#375486=CARTESIAN_POINT('Ctrl Pts',(1.47122360941503,-2.2288962842205,8.85933012996512));
#375487=CARTESIAN_POINT('Ctrl Pts',(1.47672975088113,-2.23186128939471,
8.8538223528706));
#375488=CARTESIAN_POINT('Ctrl Pts',(1.48223370986387,-2.2348251714182,8.84831178811348));
#375489=CARTESIAN_POINT('Ctrl Pts',(1.48773552819277,-2.23778795205674,
8.84279849653635));
#375490=CARTESIAN_POINT('Ctrl Pts',(1.50324506143006,-2.24613998079365,
8.82725662040549));
#375491=CARTESIAN_POINT('Ctrl Pts',(1.51873760371866,-2.25448326797285,
8.81169306718667));
#375492=CARTESIAN_POINT('Ctrl Pts',(1.53421404825539,-2.26281827803705,
8.79610912703474));
#375493=CARTESIAN_POINT('',(1.59371958050517,-2.22130979469258,8.79610912703474));
#375494=CARTESIAN_POINT('Origin',(0.,1.84795814293585E-15,8.79610912703474));
#375495=CARTESIAN_POINT('',(1.58363955683349,-2.15047978570931,8.85933012996512));
#375496=CARTESIAN_POINT('Ctrl Pts',(1.59371958050517,-2.22130979469258,
8.79610912703474));
#375497=CARTESIAN_POINT('Ctrl Pts',(1.5928408520915,-2.21513637169913,8.80163734024559));
#375498=CARTESIAN_POINT('Ctrl Pts',(1.59196184585596,-2.20896068826177,
8.80716298614018));
#375499=CARTESIAN_POINT('Ctrl Pts',(1.59108255624699,-2.20278270081156,
8.8126860086129));
#375500=CARTESIAN_POINT('Ctrl Pts',(1.58860385362508,-2.18536705807609,
8.82825531609049));
#375501=CARTESIAN_POINT('Ctrl Pts',(1.58612289741731,-2.16793309440754,
8.84380379913848));
#375502=CARTESIAN_POINT('Ctrl Pts',(1.58363955683349,-2.15047978570931,
8.85933012996512));
#375503=CARTESIAN_POINT('',(1.61100669796545,-2.13005515746015,8.85933012996512));
#375504=CARTESIAN_POINT('Origin',(1.60287503492125,-2.14770651837813,8.84999761231045));
#375505=CARTESIAN_POINT('',(1.67604110579952,-2.15987164362911,8.79610912703474));
#375506=CARTESIAN_POINT('Ctrl Pts',(1.61100669796545,-2.13005515746015,
8.85933012996512));
#375507=CARTESIAN_POINT('Ctrl Pts',(1.61669149500713,-2.13266129101826,
8.8538223528706));
#375508=CARTESIAN_POINT('Ctrl Pts',(1.62237404208909,-2.13526644356547,
8.84831178811348));
#375509=CARTESIAN_POINT('Ctrl Pts',(1.62805438234943,-2.1378706341428,8.84279849653635));
#375510=CARTESIAN_POINT('Ctrl Pts',(1.64406716590575,-2.1452118035346,8.82725662040549));
#375511=CARTESIAN_POINT('Ctrl Pts',(1.66006243334958,-2.15254533794299,
8.81169306718667));
#375512=CARTESIAN_POINT('Ctrl Pts',(1.67604110579952,-2.15987164362911,
8.79610912703474));
#375513=CARTESIAN_POINT('',(1.7327649198924,-2.11463591137412,8.79610912703474));
#375514=CARTESIAN_POINT('Origin',(0.,1.84795814293585E-15,8.79610912703474));
#375515=CARTESIAN_POINT('',(1.71816751245364,-2.04459725957486,8.85933012996512));
#375516=CARTESIAN_POINT('Ctrl Pts',(1.7327649198924,-2.11463591137412,8.79610912703474));
#375517=CARTESIAN_POINT('Ctrl Pts',(1.73149246435127,-2.10853147266307,
8.80163734024559));
#375518=CARTESIAN_POINT('Ctrl Pts',(1.73021958673196,-2.10242479595255,
8.80716298614018));
#375519=CARTESIAN_POINT('Ctrl Pts',(1.72894627870281,-2.09631583811882,
8.8126860086129));
#375520=CARTESIAN_POINT('Ctrl Pts',(1.72535684478011,-2.07909478871142,
8.82825531609049));
#375521=CARTESIAN_POINT('Ctrl Pts',(1.72176398807558,-2.06185560040101,
8.84380379913848));
#375522=CARTESIAN_POINT('Ctrl Pts',(1.71816751245364,-2.04459725957486,
8.85933012996512));
#375523=CARTESIAN_POINT('',(1.74416981443408,-2.0224611771624,8.85933012996512));
#375524=CARTESIAN_POINT('Origin',(1.7371857853407,-2.04059726890633,8.84999761231044));
#375525=CARTESIAN_POINT('',(1.81098095093023,-2.04804963334647,8.79610912703474));
#375526=CARTESIAN_POINT('Ctrl Pts',(1.74416981443408,-2.0224611771624,8.85933012996512));
#375527=CARTESIAN_POINT('Ctrl Pts',(1.75000990700091,-2.0246977299426,8.8538223528706));
#375528=CARTESIAN_POINT('Ctrl Pts',(1.75584769137722,-2.02693344788291,
8.84831178811348));
#375529=CARTESIAN_POINT('Ctrl Pts',(1.76168321183244,-2.02916834722135,
8.84279849653635));
#375530=CARTESIAN_POINT('Ctrl Pts',(1.77813344574543,-2.03546849082835,
8.82725662040549));
#375531=CARTESIAN_POINT('Ctrl Pts',(1.79456571035959,-2.0417621374,8.81169306718667));
#375532=CARTESIAN_POINT('Ctrl Pts',(1.81098095093023,-2.04804963334647,
8.79610912703474));
#375533=CARTESIAN_POINT('',(1.86468995654688,-1.99927253550784,8.79610912703474));
#375534=CARTESIAN_POINT('Origin',(0.,1.84795814293585E-15,8.79610912703474));
#375535=CARTESIAN_POINT('',(1.84563514921934,-1.93031304473608,8.85933012996512));
#375536=CARTESIAN_POINT('Ctrl Pts',(1.86468995654688,-1.99927253550784,
8.79610912703474));
#375537=CARTESIAN_POINT('Ctrl Pts',(1.86302900267106,-1.99326216552726,
8.80163734024559));
#375538=CARTESIAN_POINT('Ctrl Pts',(1.86136748419513,-1.98724958918806,
8.80716298614018));
#375539=CARTESIAN_POINT('Ctrl Pts',(1.85970539004164,-1.98123476398891,
8.8126860086129));
#375540=CARTESIAN_POINT('Ctrl Pts',(1.85501997457207,-1.9642790728955,8.82825531609049));
#375541=CARTESIAN_POINT('Ctrl Pts',(1.85032998118963,-1.94730549946579,
8.84380379913848));
#375542=CARTESIAN_POINT('Ctrl Pts',(1.84563514921934,-1.93031304473608,
8.85933012996512));
#375543=CARTESIAN_POINT('',(1.87016576301195,-1.90655647007113,8.85933012996512));
#375544=CARTESIAN_POINT('Origin',(1.86435806674298,-1.92510276754984,8.84999761231046));
#375545=CARTESIAN_POINT('',(1.93847908687937,-1.92781174781514,8.79610912703474));
#375546=CARTESIAN_POINT('Ctrl Pts',(1.87016576301195,-1.90655647007113,
8.85933012996512));
#375547=CARTESIAN_POINT('Ctrl Pts',(1.87613715291088,-1.90841425159831,
8.8538223528706));
#375548=CARTESIAN_POINT('Ctrl Pts',(1.88210618587333,-1.91027134788713,
8.84831178811348));
#375549=CARTESIAN_POINT('Ctrl Pts',(1.88807290711817,-1.91212777230593,
8.84279849653635));
#375550=CARTESIAN_POINT('Ctrl Pts',(1.90489299384811,-1.91736100148666,
8.82725662040549));
#375551=CARTESIAN_POINT('Ctrl Pts',(1.9216947319326,-1.92258889827782,8.81169306718667));
#375552=CARTESIAN_POINT('Ctrl Pts',(1.93847908687937,-1.92781174781514,
8.79610912703474));
#375553=CARTESIAN_POINT('',(1.98895258219517,-1.87569371995055,8.79610912703474));
#375554=CARTESIAN_POINT('Origin',(0.,1.84795814293585E-15,8.79610912703474));
#375555=CARTESIAN_POINT('',(1.9655186752694,-1.80809675954562,8.85933012996512));
#375556=CARTESIAN_POINT('Ctrl Pts',(1.98895258219517,-1.87569371995055,
8.79610912703474));
#375557=CARTESIAN_POINT('Ctrl Pts',(1.9869099552004,-1.86980211659991,8.80163734024559));
#375558=CARTESIAN_POINT('Ctrl Pts',(1.98486662340368,-1.86390834759789,
8.80716298614018));
#375559=CARTESIAN_POINT('Ctrl Pts',(1.98282257302722,-1.85801237124025,
8.8126860086129));
#375560=CARTESIAN_POINT('Ctrl Pts',(1.97706042938797,-1.84139171303252,
8.82825531609049));
#375561=CARTESIAN_POINT('Ctrl Pts',(1.97129257151643,-1.82475350253755,
8.84380379913848));
#375562=CARTESIAN_POINT('Ctrl Pts',(1.9655186752694,-1.80809675954562,8.85933012996512));
#375563=CARTESIAN_POINT('',(1.9884767993203,-1.78281731348926,8.85933012996512));
#375564=CARTESIAN_POINT('Origin',(1.98386930094547,-1.80169760598823,8.84999761231048));
#375565=CARTESIAN_POINT('',(2.05801159645807,-1.79965207029772,8.79610912703474));
#375566=CARTESIAN_POINT('Ctrl Pts',(1.9884767993203,-1.78281731348926,8.85933012996512));
#375567=CARTESIAN_POINT('Ctrl Pts',(1.99455494882937,-1.78428868974062,
8.8538223528706));
#375568=CARTESIAN_POINT('Ctrl Pts',(2.00063070234118,-1.78575953317098,
8.84831178811348));
#375569=CARTESIAN_POINT('Ctrl Pts',(2.00670410583818,-1.78722985422398,
8.84279849653635));
#375570=CARTESIAN_POINT('Ctrl Pts',(2.02382492804081,-1.79137466451721,
8.82725662040549));
#375571=CARTESIAN_POINT('Ctrl Pts',(2.04092709764987,-1.7955153289786,8.81169306718667));
#375572=CARTESIAN_POINT('Ctrl Pts',(2.05801159645807,-1.79965207029772,
8.79610912703474));
#375573=CARTESIAN_POINT('',(2.10504217505423,-1.74440727656294,8.79610912703474));
#375574=CARTESIAN_POINT('Origin',(0.,1.84795814293585E-15,8.79610912703474));
#375575=CARTESIAN_POINT('',(2.07732546348034,-1.67845061693465,8.85933012996512));
#375576=CARTESIAN_POINT('Ctrl Pts',(2.10504217505423,-1.74440727656294,
8.79610912703474));
#375577=CARTESIAN_POINT('Ctrl Pts',(2.10262626853298,-1.73865864970415,
8.80163734024559));
#375578=CARTESIAN_POINT('Ctrl Pts',(2.1002095199041,-1.73290790680036,8.80716298614018));
#375579=CARTESIAN_POINT('Ctrl Pts',(2.09779191274614,-1.72715500711575,
8.8126860086129));
#375580=CARTESIAN_POINT('Ctrl Pts',(2.09097671882138,-1.7109376796434,8.82825531609049));
#375581=CARTESIAN_POINT('Ctrl Pts',(2.08415469782594,-1.69470320205899,
8.84380379913848));
#375582=CARTESIAN_POINT('Ctrl Pts',(2.07732546348034,-1.67845061693465,
8.85933012996512));
#375583=CARTESIAN_POINT('',(2.09861675793331,-1.65175217815314,8.85933012996512));
#375584=CARTESIAN_POINT('Origin',(2.09522839065179,-1.67088888250073,8.84999761231043));
#375585=CARTESIAN_POINT('',(2.16908729494481,-1.66409723639929,8.79610912703474));
#375586=CARTESIAN_POINT('Ctrl Pts',(2.09861675793331,-1.65175217815314,
8.85933012996512));
#375587=CARTESIAN_POINT('Ctrl Pts',(2.10477669063244,-1.65283110292807,
8.8538223528706));
#375588=CARTESIAN_POINT('Ctrl Pts',(2.11093419811917,-1.6539096494888,8.84831178811348));
#375589=CARTESIAN_POINT('Ctrl Pts',(2.11708932695063,-1.65498782531142,
8.84279849653635));
#375590=CARTESIAN_POINT('Ctrl Pts',(2.1344405314951,-1.65802718480261,8.82725662040549));
#375591=CARTESIAN_POINT('Ctrl Pts',(2.1517728561454,-1.66106360205577,8.81169306718667));
#375592=CARTESIAN_POINT('Ctrl Pts',(2.16908729494481,-1.66409723639929,
8.79610912703474));
#375593=CARTESIAN_POINT('',(2.21248169808586,-1.60595268950174,8.79610912703474));
#375594=CARTESIAN_POINT('Origin',(0.,1.84795814293585E-15,8.79610912703474));
#375595=CARTESIAN_POINT('',(2.18059607577693,-1.54190736071218,8.85933012996512));
#375596=CARTESIAN_POINT('Ctrl Pts',(2.21248169808586,-1.60595268950174,
8.79610912703474));
#375597=CARTESIAN_POINT('Ctrl Pts',(2.20970243951623,-1.60037066147564,
8.80163734024559));
#375598=CARTESIAN_POINT('Ctrl Pts',(2.20692220499371,-1.59478657570621,
8.80716298614018));
#375599=CARTESIAN_POINT('Ctrl Pts',(2.20414097552062,-1.58920039259344,
8.8126860086129));
#375600=CARTESIAN_POINT('Ctrl Pts',(2.19630073640405,-1.57345303633365,
8.82825531609049));
#375601=CARTESIAN_POINT('Ctrl Pts',(2.18845258543231,-1.55768900261046,
8.84380379913848));
#375602=CARTESIAN_POINT('Ctrl Pts',(2.18059607577693,-1.54190736071218,
8.85933012996512));
#375603=CARTESIAN_POINT('',(2.20013305013608,-1.51389963881726,8.85933012996512));
#375604=CARTESIAN_POINT('Origin',(2.19797773747577,-1.53321411819045,8.84999761231047));
#375605=CARTESIAN_POINT('',(2.27124974846887,-1.52170427000876,8.79610912703474));
#375606=CARTESIAN_POINT('Ctrl Pts',(2.20013305013608,-1.51389963881726,
8.85933012996512));
#375607=CARTESIAN_POINT('Ctrl Pts',(2.20634945354051,-1.51458167858243,
8.8538223528706));
#375608=CARTESIAN_POINT('Ctrl Pts',(2.21256341248313,-1.51526349629436,
8.84831178811348));
#375609=CARTESIAN_POINT('Ctrl Pts',(2.21877497390439,-1.51594509643089,
8.84279849653635));
#375610=CARTESIAN_POINT('Ctrl Pts',(2.23628526096942,-1.51786651573993,
8.82725662040549));
#375611=CARTESIAN_POINT('Ctrl Pts',(2.2537765184212,-1.51978620849507,8.81169306718667));
#375612=CARTESIAN_POINT('Ctrl Pts',(2.27124974846887,-1.52170427000876,
8.79610912703474));
#375613=CARTESIAN_POINT('',(2.31082965924422,-1.46089889836361,8.79610912703474));
#375614=CARTESIAN_POINT('Origin',(0.,1.84795814293585E-15,8.79610912703474));
#375615=CARTESIAN_POINT('',(2.27490615106176,-1.39902807640644,8.85933012996512));
#375616=CARTESIAN_POINT('Ctrl Pts',(2.31082965924422,-1.46089889836361,
8.79610912703474));
#375617=CARTESIAN_POINT('Ctrl Pts',(2.30769846919582,-1.4555064069207,8.80163734024559));
#375618=CARTESIAN_POINT('Ctrl Pts',(2.30456617335967,-1.45011192449183,
8.80716298614018));
#375619=CARTESIAN_POINT('Ctrl Pts',(2.30143275023993,-1.44471541277554,
8.8126860086129));
#375620=CARTESIAN_POINT('Ctrl Pts',(2.29259968315581,-1.42950273699299,
8.82825531609049));
#375621=CARTESIAN_POINT('Ctrl Pts',(2.28375765194352,-1.41427392492697,
8.84380379913848));
#375622=CARTESIAN_POINT('Ctrl Pts',(2.27490615106176,-1.39902807640644,
8.85933012996512));
#375623=CARTESIAN_POINT('',(2.29260852370879,-1.36982616113503,8.85933012996512));
#375624=CARTESIAN_POINT('Origin',(2.29169512231177,-1.38923904819516,8.84999761231045));
#375625=CARTESIAN_POINT('',(2.36407914959492,-1.37305829436821,8.79610912703474));
#375626=CARTESIAN_POINT('Ctrl Pts',(2.29260852370879,-1.36982616113503,
8.85933012996512));
#375627=CARTESIAN_POINT('Ctrl Pts',(2.2988558532835,-1.37010851324274,8.8538223528706));
#375628=CARTESIAN_POINT('Ctrl Pts',(2.30510072919182,-1.37039080037066,
8.84831178811348));
#375629=CARTESIAN_POINT('Ctrl Pts',(2.31134319856465,-1.37067302397992,
8.84279849653635));
#375630=CARTESIAN_POINT('Ctrl Pts',(2.32894061462473,-1.37146860758273,
8.82725662040549));
#375631=CARTESIAN_POINT('Ctrl Pts',(2.34651892954927,-1.37226368741055,
8.81169306718667));
#375632=CARTESIAN_POINT('Ctrl Pts',(2.36407914959492,-1.37305829436821,
8.79610912703474));
#375633=CARTESIAN_POINT('',(2.39968192566134,-1.30984196029027,8.79610912703474));
#375634=CARTESIAN_POINT('Origin',(0.,1.84795814293585E-15,8.79610912703474));
#375635=CARTESIAN_POINT('',(2.35986814900604,-1.25039988564417,8.85933012996512));
#375636=CARTESIAN_POINT('Ctrl Pts',(2.39968192566134,-1.30984196029027,
8.79610912703474));
#375637=CARTESIAN_POINT('Ctrl Pts',(2.39621167086572,-1.30466116433458,
8.80163734024559));
#375638=CARTESIAN_POINT('Ctrl Pts',(2.3927401849914,-1.29947845233168,8.80716298614018));
#375639=CARTESIAN_POINT('Ctrl Pts',(2.38926744413273,-1.29429378743606,
8.8126860086129));
#375640=CARTESIAN_POINT('Ctrl Pts',(2.3794778460484,-1.27967830427864,8.82825531609049));
#375641=CARTESIAN_POINT('Ctrl Pts',(2.36967826839842,-1.26504729232515,
8.84380379913848));
#375642=CARTESIAN_POINT('Ctrl Pts',(2.35986814900604,-1.25039988564417,
8.85933012996512));
#375643=CARTESIAN_POINT('',(2.3756631770946,-1.2201237739299,8.85933012996512));
#375644=CARTESIAN_POINT('Origin',(2.37599544032312,-1.23955529695998,8.84999761231044));
#375645=CARTESIAN_POINT('',(2.44719404240189,-1.21877012767603,8.79610912703474));
#375646=CARTESIAN_POINT('Ctrl Pts',(2.3756631770946,-1.2201237739299,8.85933012996512));
#375647=CARTESIAN_POINT('Ctrl Pts',(2.38191576122233,-1.22000527813478,
8.8538223528706));
#375648=CARTESIAN_POINT('Ctrl Pts',(2.38816589256171,-1.21988687470032,
8.84831178811348));
#375649=CARTESIAN_POINT('Ctrl Pts',(2.39441361824044,-1.21976856206496,
8.84279849653635));
#375650=CARTESIAN_POINT('Ctrl Pts',(2.41202585173836,-1.21943504073788,
8.82725662040549));
#375651=CARTESIAN_POINT('Ctrl Pts',(2.42961899106908,-1.21910224048481,
8.81169306718667));
#375652=CARTESIAN_POINT('Ctrl Pts',(2.44719404240189,-1.21877012767603,
8.79610912703474));
#375653=CARTESIAN_POINT('',(2.47867338431575,-1.15340260064189,8.79610912703474));
#375654=CARTESIAN_POINT('Origin',(0.,1.84795814293585E-15,8.79610912703474));
#375655=CARTESIAN_POINT('',(2.43513294253592,-1.09663353354185,8.85933012996512));
#375656=CARTESIAN_POINT('Ctrl Pts',(2.47867338431575,-1.15340260064189,
8.79610912703474));
#375657=CARTESIAN_POINT('Ctrl Pts',(2.47487832479424,-1.14845478917526,
8.80163734024559));
#375658=CARTESIAN_POINT('Ctrl Pts',(2.47108191396185,-1.14350514447364,
8.80716298614018));
#375659=CARTESIAN_POINT('Ctrl Pts',(2.46728412560133,-1.13855363129886,
8.8126860086129));
#375660=CARTESIAN_POINT('Ctrl Pts',(2.45657822407517,-1.12459539892188,
8.82825531609049));
#375661=CARTESIAN_POINT('Ctrl Pts',(2.44586136855408,-1.11062230904737,
8.84380379913848));
#375662=CARTESIAN_POINT('Ctrl Pts',(2.43513294253592,-1.09663353354185,
8.85933012996512));
#375663=CARTESIAN_POINT('',(2.44895572090757,-1.06540763642197,8.85933012996512));
#375664=CARTESIAN_POINT('Origin',(2.45053228342073,-1.08477794712581,8.84999761231046));
#375665=CARTESIAN_POINT('',(2.52025288996717,-1.05947377310385,8.79610912703474));
#375666=CARTESIAN_POINT('Ctrl Pts',(2.44895572090757,-1.06540763642197,
8.85933012996512));
#375667=CARTESIAN_POINT('Ctrl Pts',(2.45518786637896,-1.06488877964865,
8.8538223528706));
#375668=CARTESIAN_POINT('Ctrl Pts',(2.46141757001909,-1.06437017219693,
8.84831178811348));
#375669=CARTESIAN_POINT('Ctrl Pts',(2.46764487875877,-1.06385180948896,
8.84279849653635));
#375670=CARTESIAN_POINT('Ctrl Pts',(2.48519955724927,-1.06239055374265,
8.82725662040549));
#375671=CARTESIAN_POINT('Ctrl Pts',(2.50273522700295,-1.06093124095632,
8.81169306718667));
#375672=CARTESIAN_POINT('Ctrl Pts',(2.52025288996717,-1.05947377310385,
8.79610912703474));
#375673=CARTESIAN_POINT('',(2.54747944236024,-0.992223662303376,8.79610912703474));
#375674=CARTESIAN_POINT('Origin',(0.,1.84795814293585E-15,8.79610912703474));
#375675=CARTESIAN_POINT('',(2.50039125247055,-0.938360879023052,8.85933012996512));
#375676=CARTESIAN_POINT('Ctrl Pts',(2.54747944236024,-0.992223662303376,
8.79610912703474));
#375677=CARTESIAN_POINT('Ctrl Pts',(2.54337517282645,-0.987529166944447,
8.80163734024559));
#375678=CARTESIAN_POINT('Ctrl Pts',(2.53926943730241,-0.982832928695883,
8.80716298614018));
#375679=CARTESIAN_POINT('Ctrl Pts',(2.53516220736704,-0.97813491407166,
8.8126860086129));
#375680=CARTESIAN_POINT('Ctrl Pts',(2.52358399524484,-0.964891289845987,
8.82825531609049));
#375681=CARTESIAN_POINT('Ctrl Pts',(2.51199389971073,-0.951633540473973,
8.84380379913848));
#375682=CARTESIAN_POINT('Ctrl Pts',(2.50039125247055,-0.938360879023052,
8.85933012996512));
#375683=CARTESIAN_POINT('',(2.51218498036397,-0.906313510406752,8.85933012996512));
#375684=CARTESIAN_POINT('Origin',(2.51499936372827,-0.925543012022764,8.84999761231044));
#375685=CARTESIAN_POINT('',(2.58295547781501,-0.89582381354158,8.79610912703474));
#375686=CARTESIAN_POINT('Ctrl Pts',(2.51218498036397,-0.906313510406752,
8.85933012996512));
#375687=CARTESIAN_POINT('Ctrl Pts',(2.51837107795649,-0.905396424749024,
8.8538223528706));
#375688=CARTESIAN_POINT('Ctrl Pts',(2.52455475470885,-0.904479744349289,
8.84831178811348));
#375689=CARTESIAN_POINT('Ctrl Pts',(2.53073605716211,-0.903563461632256,
8.84279849653635));
#375690=CARTESIAN_POINT('Ctrl Pts',(2.5481610447058,-0.90098047608002,8.82725662040549));
#375691=CARTESIAN_POINT('Ctrl Pts',(2.56556718705404,-0.898400647389695,
8.81169306718667));
#375692=CARTESIAN_POINT('Ctrl Pts',(2.58295547781501,-0.89582381354158,
8.79610912703474));
#375693=CARTESIAN_POINT('',(2.60581736094344,-0.826967464105156,8.79610912703474));
#375694=CARTESIAN_POINT('Origin',(0.,1.84795814293585E-15,8.79610912703474));
#375695=CARTESIAN_POINT('',(2.55537491841653,-0.776232298374573,8.85933012996512));
#375696=CARTESIAN_POINT('Ctrl Pts',(2.60581736094344,-0.826967464105156,
8.79610912703474));
#375697=CARTESIAN_POINT('Ctrl Pts',(2.60142074672124,-0.822545575542315,
8.80163734024559));
#375698=CARTESIAN_POINT('Ctrl Pts',(2.59702255785351,-0.81812204159711,
8.80716298614018));
#375699=CARTESIAN_POINT('Ctrl Pts',(2.5926227638321,-0.813696830673264,
8.8126860086129));
#375700=CARTESIAN_POINT('Ctrl Pts',(2.58021981847098,-0.80122223549159,
8.82825531609049));
#375701=CARTESIAN_POINT('Ctrl Pts',(2.56780410911246,-0.788734305558017,
8.84380379913848));
#375702=CARTESIAN_POINT('Ctrl Pts',(2.55537491841653,-0.776232298374573,
8.85933012996512));
#375703=CARTESIAN_POINT('',(2.56509113287407,-0.74349514777364,8.85933012996512));
#375704=CARTESIAN_POINT('Origin',(2.56913177218453,-0.762504822154957,8.84999761231048));
#375705=CARTESIAN_POINT('',(2.63504414756231,-0.728492721775861,8.79610912703474));
#375706=CARTESIAN_POINT('Ctrl Pts',(2.56509113287407,-0.74349514777364,
8.85933012996512));
#375707=CARTESIAN_POINT('Ctrl Pts',(2.5712057625858,-0.742183601733178,
8.8538223528706));
#375708=CARTESIAN_POINT('Ctrl Pts',(2.57731800239621,-0.740872615221825,
8.84831178811348));
#375709=CARTESIAN_POINT('Ctrl Pts',(2.5834278982654,-0.739562177697958,
8.84279849653635));
#375710=CARTESIAN_POINT('Ctrl Pts',(2.60065159185081,-0.735868076381477,
8.82725662040549));
#375711=CARTESIAN_POINT('Ctrl Pts',(2.6178566812211,-0.732178332856615,
8.81169306718667));
#375712=CARTESIAN_POINT('Ctrl Pts',(2.63504414756231,-0.728492721775861,
8.79610912703474));
#375713=CARTESIAN_POINT('',(2.65344741704446,-0.65831307921296,8.79610912703474));
#375714=CARTESIAN_POINT('Origin',(0.,1.84795814293585E-15,8.79610912703474));
#375715=CARTESIAN_POINT('',(2.59985800069653,-0.610914012710764,8.85933012996512));
#375716=CARTESIAN_POINT('Ctrl Pts',(2.65344741704446,-0.65831307921296,
8.79610912703474));
#375717=CARTESIAN_POINT('Ctrl Pts',(2.64877652476476,-0.654181967934804,
8.80163734024559));
#375718=CARTESIAN_POINT('Ctrl Pts',(2.6441039556548,-0.650049315542785,
8.80716298614018));
#375719=CARTESIAN_POINT('Ctrl Pts',(2.63942967724473,-0.645915092460206,
8.8126860086129));
#375720=CARTESIAN_POINT('Ctrl Pts',(2.62625296500761,-0.634260787109924,
8.82825531609049));
#375721=CARTESIAN_POINT('Ctrl Pts',(2.6130626606376,-0.622593992197544,
8.84380379913848));
#375722=CARTESIAN_POINT('Ctrl Pts',(2.59985800069653,-0.610914012710764,
8.85933012996512));
#375723=CARTESIAN_POINT('',(2.60745677570887,-0.577621604099114,8.85933012996512));
#375724=CARTESIAN_POINT('Origin',(2.61270706711191,-0.596333336416159,8.84999761231045));
#375725=CARTESIAN_POINT('',(2.67630485569207,-0.558168097155164,8.79610912703474));
#375726=CARTESIAN_POINT('Ctrl Pts',(2.60745677570887,-0.577621604099114,
8.85933012996512));
#375727=CARTESIAN_POINT('Ctrl Pts',(2.61347481121474,-0.575920987099925,
8.8538223528706));
#375728=CARTESIAN_POINT('Ctrl Pts',(2.61949049757874,-0.574221081601735,
8.84831178811348));
#375729=CARTESIAN_POINT('Ctrl Pts',(2.62550387999116,-0.572521874139906,
8.84279849653635));
#375730=CARTESIAN_POINT('Ctrl Pts',(2.64245550376689,-0.567731836913873,
8.82725662040549));
#375731=CARTESIAN_POINT('Ctrl Pts',(2.65938884075651,-0.562947340502065,
8.81169306718667));
#375732=CARTESIAN_POINT('Ctrl Pts',(2.67630485569207,-0.558168097155164,
8.79610912703474));
#375733=CARTESIAN_POINT('',(2.69017388854615,-0.486953544670569,8.79610912703474));
#375734=CARTESIAN_POINT('Origin',(0.,1.84795814293585E-15,8.79610912703474));
#375735=CARTESIAN_POINT('',(2.63365770878388,-0.443085350328085,8.85933012996512));
#375736=CARTESIAN_POINT('Ctrl Pts',(2.69017388854615,-0.486953544670569,
8.79610912703474));
#375737=CARTESIAN_POINT('Ctrl Pts',(2.68524791190724,-0.48313018629946,
8.80163734024559));
#375738=CARTESIAN_POINT('Ctrl Pts',(2.68032016314379,-0.479305397415756,
8.80716298614018));
#375739=CARTESIAN_POINT('Ctrl Pts',(2.67539060795768,-0.475479150583879,
8.8126860086129));
#375740=CARTESIAN_POINT('Ctrl Pts',(2.66149427478153,-0.464693025105514,
8.82825531609049));
#375741=CARTESIAN_POINT('Ctrl Pts',(2.64758357719,-0.45389530657714,8.84380379913848));
#375742=CARTESIAN_POINT('Ctrl Pts',(2.63365770878388,-0.443085350328085,
8.85933012996512));
#375743=CARTESIAN_POINT('',(2.63910781935456,-0.409374489353903,8.85933012996512));
#375744=CARTESIAN_POINT('Origin',(2.64554618827659,-0.427711389084919,8.84999761231045));
#375745=CARTESIAN_POINT('',(2.7065680531042,-0.385549840096578,8.79610912703474));
#375746=CARTESIAN_POINT('Ctrl Pts',(2.63910781935456,-0.409374489353903,
8.85933012996512));
#375747=CARTESIAN_POINT('Ctrl Pts',(2.6450045312558,-0.407291789596017,
8.8538223528706));
#375748=CARTESIAN_POINT('Ctrl Pts',(2.65089894442778,-0.40520995038731,
8.84831178811348));
#375749=CARTESIAN_POINT('Ctrl Pts',(2.65679110310522,-0.403128955395459,
8.84279849653635));
#375750=CARTESIAN_POINT('Ctrl Pts',(2.67340099921307,-0.397262665550295,
8.82725662040549));
#375751=CARTESIAN_POINT('Ctrl Pts',(2.68999300110815,-0.391403076773568,
8.81169306718667));
#375752=CARTESIAN_POINT('Ctrl Pts',(2.7065680531042,-0.385549840096578,
8.79610912703474));
#375753=CARTESIAN_POINT('',(2.71584585849932,-0.313593013561915,8.79610912703474));
#375754=CARTESIAN_POINT('Origin',(0.,1.84795814293585E-15,8.79610912703474));
#375755=CARTESIAN_POINT('',(2.65663515242804,-0.273435955199396,8.85933012996512));
#375756=CARTESIAN_POINT('Ctrl Pts',(2.71584585849932,-0.313593013561915,
8.79610912703474));
#375757=CARTESIAN_POINT('Ctrl Pts',(2.71068503939582,-0.310093119097509,
8.80163734024559));
#375758=CARTESIAN_POINT('Ctrl Pts',(2.70552236015555,-0.306591910600058,
8.80716298614018));
#375759=CARTESIAN_POINT('Ctrl Pts',(2.70035778479304,-0.303089362887842,
8.8126860086129));
#375760=CARTESIAN_POINT('Ctrl Pts',(2.68579893369164,-0.293215739784602,
8.82825531609049));
#375761=CARTESIAN_POINT('Ctrl Pts',(2.67122500491882,-0.283331467781771,
8.84380379913848));
#375762=CARTESIAN_POINT('Ctrl Pts',(2.65663515242804,-0.273435955199396,
8.85933012996512));
#375763=CARTESIAN_POINT('',(2.65991420288367,-0.239445167021381,8.85933012996512));
#375764=CARTESIAN_POINT('Origin',(2.66751419268574,-0.25733188391212,8.84999761231047));
#375765=CARTESIAN_POINT('',(2.7257093818291,-0.211347276044851,8.79610912703474));
#375766=CARTESIAN_POINT('Ctrl Pts',(2.65991420288367,-0.239445167021381,
8.85933012996512));
#375767=CARTESIAN_POINT('Ctrl Pts',(2.66566536032625,-0.236988942764841,
8.8538223528706));
#375768=CARTESIAN_POINT('Ctrl Pts',(2.67141427889812,-0.234533724569479,
8.84831178811348));
#375769=CARTESIAN_POINT('Ctrl Pts',(2.67716100169672,-0.2320794933024,8.84279849653635));
#375770=CARTESIAN_POINT('Ctrl Pts',(2.69336091651076,-0.225161056681394,
8.82725662040549));
#375771=CARTESIAN_POINT('Ctrl Pts',(2.70954340321654,-0.218250453846909,
8.81169306718667));
#375772=CARTESIAN_POINT('Ctrl Pts',(2.7257093818291,-0.211347276044851,
8.79610912703474));
#375773=CARTESIAN_POINT('',(2.73035783527281,-0.138943861495048,8.79610912703474));
#375774=CARTESIAN_POINT('Origin',(0.,1.84795814293585E-15,8.79610912703474));
#375775=CARTESIAN_POINT('',(2.66869591238441,-0.102662953078966,8.85933012996512));
#375776=CARTESIAN_POINT('Ctrl Pts',(2.73035783527281,-0.138943861495048,
8.79610912703474));
#375777=CARTESIAN_POINT('Ctrl Pts',(2.72498338061741,-0.135781812754423,
8.80163734024559));
#375778=CARTESIAN_POINT('Ctrl Pts',(2.7196069854567,-0.132618571859948,
8.80716298614018));
#375779=CARTESIAN_POINT('Ctrl Pts',(2.71422861226575,-0.129454115987237,
8.8126860086129));
#375780=CARTESIAN_POINT('Ctrl Pts',(2.69906706868114,-0.120533568094338,
8.82825531609049));
#375781=CARTESIAN_POINT('Ctrl Pts',(2.68388979612647,-0.11160335921088,
8.84380379913848));
#375782=CARTESIAN_POINT('Ctrl Pts',(2.66869591238441,-0.102662953078966,
8.85933012996512));
#375783=CARTESIAN_POINT('',(2.66979042840332,-0.0685319131367438,8.85933012996512));
#375784=CARTESIAN_POINT('Origin',(2.67852080909721,-0.0858949468308122,
8.84999761231043));
#375785=CARTESIAN_POINT('',(2.73365018604124,-0.0362762407020098,8.79610912703474));
#375786=CARTESIAN_POINT('Ctrl Pts',(2.66979042840332,-0.0685319131367438,
8.85933012996512));
#375787=CARTESIAN_POINT('Ctrl Pts',(2.67537239864768,-0.0657122575338778,
8.8538223528706));
#375788=CARTESIAN_POINT('Ctrl Pts',(2.6809521990799,-0.0628937493700682,
8.84831178811348));
#375789=CARTESIAN_POINT('Ctrl Pts',(2.68652987148302,-0.0600763667904682,
8.84279849653635));
#375790=CARTESIAN_POINT('Ctrl Pts',(2.7022532360784,-0.0521342127336968,
8.82725662040549));
#375791=CARTESIAN_POINT('Ctrl Pts',(2.71795971028587,-0.0442009929908208,
8.81169306718667));
#375792=CARTESIAN_POINT('Ctrl Pts',(2.73365018604124,-0.0362762407020098,
8.79610912703474));
#375793=CARTESIAN_POINT('',(2.73389087296526,1.51315307225634E-15,8.79610912703474));
#375794=CARTESIAN_POINT('Origin',(0.,1.84795814293585E-15,8.79610912703474));
#375795=CARTESIAN_POINT('',(2.54610912703474,1.53614970366555E-15,8.98389087296526));
#375796=CARTESIAN_POINT('',(2.73389087296526,1.51315307225634E-15,8.79610912703474));
#375797=CARTESIAN_POINT('',(-2.54610912703474,2.0465319152471E-15,8.98389087296526));
#375798=CARTESIAN_POINT('Origin',(0.,1.84795814293585E-15,8.98389087296526));
#375799=CARTESIAN_POINT('Origin',(0.,1.84795814293585E-15,8.98389087296526));
#375800=CARTESIAN_POINT('',(2.73365018604124,0.0362762407020695,8.79610912703474));
#375801=CARTESIAN_POINT('Origin',(0.,1.84795814293585E-15,8.79610912703474));
#375802=CARTESIAN_POINT('',(2.66979042840331,0.0685319131368021,8.85933012996512));
#375803=CARTESIAN_POINT('Ctrl Pts',(2.73365018604124,0.0362762407020695,
8.79610912703474));
#375804=CARTESIAN_POINT('Ctrl Pts',(2.72808418062094,0.0390874501823801,
8.80163734024559));
#375805=CARTESIAN_POINT('Ctrl Pts',(2.72251616230074,0.041899725038531,
8.80716298614018));
#375806=CARTESIAN_POINT('Ctrl Pts',(2.71694609217046,0.044713085643783,
8.8126860086129));
#375807=CARTESIAN_POINT('Ctrl Pts',(2.70124415813737,0.0526439018815967,
8.82825531609049));
#375808=CARTESIAN_POINT('Ctrl Pts',(2.68552590846928,0.0605833515018572,
8.84380379913848));
#375809=CARTESIAN_POINT('Ctrl Pts',(2.66979042840331,0.0685319131368021,
8.85933012996512));
#375810=CARTESIAN_POINT('',(2.66869591238441,0.102662953079024,8.85933012996512));
#375811=CARTESIAN_POINT('Origin',(2.67852080896314,0.0858949510114288,8.84999761231043));
#375812=CARTESIAN_POINT('',(2.7303578352728,0.138943861495108,8.79610912703474));
#375813=CARTESIAN_POINT('Ctrl Pts',(2.66869591238441,0.102662953079024,
8.85933012996512));
#375814=CARTESIAN_POINT('Ctrl Pts',(2.67408575791749,0.105834453458529,
8.8538223528706));
#375815=CARTESIAN_POINT('Ctrl Pts',(2.67947351161322,0.109004669736173,
8.84831178811348));
#375816=CARTESIAN_POINT('Ctrl Pts',(2.68485921376854,0.112173626398948,
8.84279849653635));
#375817=CARTESIAN_POINT('Ctrl Pts',(2.7000414174675,0.12110686187688,8.82725662040549));
#375818=CARTESIAN_POINT('Ctrl Pts',(2.71520733790511,0.130030099226553,
8.81169306718667));
#375819=CARTESIAN_POINT('Ctrl Pts',(2.7303578352728,0.138943861495108,8.79610912703474));
#375820=CARTESIAN_POINT('',(2.7257093818291,0.211347276044911,8.79610912703474));
#375821=CARTESIAN_POINT('Origin',(0.,1.84795814293585E-15,8.79610912703474));
#375822=CARTESIAN_POINT('',(2.65991420288366,0.239445167021439,8.85933012996512));
#375823=CARTESIAN_POINT('Ctrl Pts',(2.7257093818291,0.211347276044911,8.79610912703474));
#375824=CARTESIAN_POINT('Ctrl Pts',(2.71997469755407,0.21379609440215,8.80163734024559));
#375825=CARTESIAN_POINT('Ctrl Pts',(2.714237936256,0.216245846979362,8.80716298614018));
#375826=CARTESIAN_POINT('Ctrl Pts',(2.70849905779933,0.218696551614963,
8.8126860086129));
#375827=CARTESIAN_POINT('Ctrl Pts',(2.69232125593275,0.225605046772616,
8.82825531609049));
#375828=CARTESIAN_POINT('Ctrl Pts',(2.67612661881068,0.232521112228182,
8.84380379913848));
#375829=CARTESIAN_POINT('Ctrl Pts',(2.65991420288366,0.239445167021439,
8.85933012996512));
#375830=CARTESIAN_POINT('',(2.65663515242803,0.273435955199454,8.85933012996512));
#375831=CARTESIAN_POINT('Origin',(2.66751419228414,0.257331888075556,8.84999761231043));
#375832=CARTESIAN_POINT('',(2.71584585849932,0.313593013561975,8.79610912703474));
#375833=CARTESIAN_POINT('Ctrl Pts',(2.65663515242803,0.273435955199454,
8.85933012996512));
#375834=CARTESIAN_POINT('Ctrl Pts',(2.66181072521843,0.276946267980254,
8.8538223528706));
#375835=CARTESIAN_POINT('Ctrl Pts',(2.66698429274206,0.280455165273038,
8.84831178811348));
#375836=CARTESIAN_POINT('Ctrl Pts',(2.67215589364419,0.283962674096321,
8.84279849653635));
#375837=CARTESIAN_POINT('Ctrl Pts',(2.68673454951515,0.293850282414661,
8.82725662040549));
#375838=CARTESIAN_POINT('Ctrl Pts',(2.70129759616275,0.303726869874833,
8.81169306718667));
#375839=CARTESIAN_POINT('Ctrl Pts',(2.71584585849932,0.313593013561975,
8.79610912703474));
#375840=CARTESIAN_POINT('',(2.70656805310419,0.385549840096635,8.79610912703474));
#375841=CARTESIAN_POINT('Origin',(0.,1.84795814293585E-15,8.79610912703474));
#375842=CARTESIAN_POINT('',(2.63910781935455,0.409374489353958,8.85933012996512));
#375843=CARTESIAN_POINT('Ctrl Pts',(2.70656805310419,0.385549840096635,
8.79610912703474));
#375844=CARTESIAN_POINT('Ctrl Pts',(2.70068825502221,0.387626204610903,
8.80163734024559));
#375845=CARTESIAN_POINT('Ctrl Pts',(2.69480632432897,0.389703368350366,
8.80716298614018));
#375846=CARTESIAN_POINT('Ctrl Pts',(2.68892221982847,0.391781346545295,
8.8126860086129));
#375847=CARTESIAN_POINT('Ctrl Pts',(2.67233502818641,0.397639132134316,
8.82825531609049));
#375848=CARTESIAN_POINT('Ctrl Pts',(2.65573055084804,0.40350339382874,8.84380379913848));
#375849=CARTESIAN_POINT('Ctrl Pts',(2.63910781935455,0.409374489353958,
8.85933012996512));
#375850=CARTESIAN_POINT('',(2.63365770878388,0.44308535032814,8.85933012996512));
#375851=CARTESIAN_POINT('Origin',(2.64554618760903,0.427711393214063,8.84999761231044));
#375852=CARTESIAN_POINT('',(2.69017388854614,0.486953544670625,8.79610912703474));
#375853=CARTESIAN_POINT('Ctrl Pts',(2.63365770878388,0.44308535032814,8.85933012996512));
#375854=CARTESIAN_POINT('Ctrl Pts',(2.63859774129283,0.446920050882059,
8.8538223528706));
#375855=CARTESIAN_POINT('Ctrl Pts',(2.64353586334568,0.450753210378352,
8.84831178811348));
#375856=CARTESIAN_POINT('Ctrl Pts',(2.64847211177721,0.45458485825603,8.84279849653635));
#375857=CARTESIAN_POINT('Ctrl Pts',(2.66238731299609,0.465386209111313,
8.82725662040549));
#375858=CARTESIAN_POINT('Ctrl Pts',(2.67628764317124,0.476175561665589,
8.81169306718667));
#375859=CARTESIAN_POINT('Ctrl Pts',(2.69017388854614,0.486953544670625,
8.79610912703474));
#375860=CARTESIAN_POINT('',(2.67630485569206,0.558168097155223,8.79610912703474));
#375861=CARTESIAN_POINT('Origin',(0.,1.84795814293585E-15,8.79610912703474));
#375862=CARTESIAN_POINT('',(2.60745677570886,0.577621604099172,8.85933012996512));
#375863=CARTESIAN_POINT('Ctrl Pts',(2.67630485569206,0.558168097155223,
8.79610912703474));
#375864=CARTESIAN_POINT('Ctrl Pts',(2.67030410515465,0.559863475599352,
8.80163734024559));
#375865=CARTESIAN_POINT('Ctrl Pts',(2.66430117518113,0.561559514989709,
8.80716298614018));
#375866=CARTESIAN_POINT('Ctrl Pts',(2.65829602368433,0.563256227885838,
8.8126860086129));
#375867=CARTESIAN_POINT('Ctrl Pts',(2.64136760259518,0.568039233008752,
8.82825531609049));
#375868=CARTESIAN_POINT('Ctrl Pts',(2.62442151639954,0.572827593432851,
8.84380379913848));
#375869=CARTESIAN_POINT('Ctrl Pts',(2.60745677570886,0.577621604099172,
8.85933012996512));
#375870=CARTESIAN_POINT('',(2.59985800069652,0.610914012710821,8.85933012996512));
#375871=CARTESIAN_POINT('Origin',(2.61270706618112,0.596333340494042,8.84999761231048));
#375872=CARTESIAN_POINT('',(2.65344741704445,0.658313079213018,8.79610912703474));
#375873=CARTESIAN_POINT('Ctrl Pts',(2.59985800069652,0.610914012710821,
8.85933012996512));
#375874=CARTESIAN_POINT('Ctrl Pts',(2.60454219327082,0.615057343430743,
8.8538223528706));
#375875=CARTESIAN_POINT('Ctrl Pts',(2.60922457805015,0.619199013855962,
8.84831178811348));
#375876=CARTESIAN_POINT('Ctrl Pts',(2.61390518990746,0.623339055725021,
8.84279849653635));
#375877=CARTESIAN_POINT('Ctrl Pts',(2.62709975592764,0.635009764049699,
8.82725662040549));
#375878=CARTESIAN_POINT('Ctrl Pts',(2.64028025019204,0.646667545934124,
8.81169306718667));
#375879=CARTESIAN_POINT('Ctrl Pts',(2.65344741704445,0.658313079213018,
8.79610912703474));
#375880=CARTESIAN_POINT('',(2.63504414756229,0.728492721775916,8.79610912703474));
#375881=CARTESIAN_POINT('Origin',(0.,1.84795814293585E-15,8.79610912703474));
#375882=CARTESIAN_POINT('',(2.56509113287406,0.743495147773693,8.85933012996512));
#375883=CARTESIAN_POINT('Ctrl Pts',(2.63504414756229,0.728492721775916,
8.79610912703474));
#375884=CARTESIAN_POINT('Ctrl Pts',(2.62894710294057,0.729800147476222,
8.80163734024559));
#375885=CARTESIAN_POINT('Ctrl Pts',(2.62284784101366,0.731108093127821,
8.80716298614018));
#375886=CARTESIAN_POINT('Ctrl Pts',(2.61674631897617,0.732416568567915,
8.8126860086129));
#375887=CARTESIAN_POINT('Ctrl Pts',(2.59954623095331,0.73610513883072,8.82825531609049));
#375888=CARTESIAN_POINT('Ctrl Pts',(2.58232817100351,0.73979792158441,8.84380379913848));
#375889=CARTESIAN_POINT('Ctrl Pts',(2.56509113287406,0.743495147773693,
8.85933012996512));
#375890=CARTESIAN_POINT('',(2.55537491841651,0.776232298374626,8.85933012996512));
#375891=CARTESIAN_POINT('Origin',(2.56913177099444,0.762504826164844,8.84999761231045));
#375892=CARTESIAN_POINT('',(2.60581736094343,0.82696746410521,8.79610912703474));
#375893=CARTESIAN_POINT('Ctrl Pts',(2.55537491841651,0.776232298374626,
8.85933012996512));
#375894=CARTESIAN_POINT('Ctrl Pts',(2.55978402270411,0.78066723342588,8.8538223528706));
#375895=CARTESIAN_POINT('Ctrl Pts',(2.5641914292865,0.785100395767865,8.84831178811348));
#375896=CARTESIAN_POINT('Ctrl Pts',(2.56859717093147,0.789531819308227,
8.84279849653635));
#375897=CARTESIAN_POINT('Ctrl Pts',(2.58101688245096,0.802023927658437,
8.82725662040549));
#375898=CARTESIAN_POINT('Ctrl Pts',(2.59342337932647,0.814502234546662,
8.81169306718667));
#375899=CARTESIAN_POINT('Ctrl Pts',(2.60581736094343,0.82696746410521,8.79610912703474));
#375900=CARTESIAN_POINT('',(2.58295547781499,0.895823813541636,8.79610912703474));
#375901=CARTESIAN_POINT('Origin',(0.,1.84795814293585E-15,8.79610912703474));
#375902=CARTESIAN_POINT('',(2.51218498036395,0.906313510406806,8.85933012996512));
#375903=CARTESIAN_POINT('Ctrl Pts',(2.58295547781499,0.895823813541636,
8.79610912703474));
#375904=CARTESIAN_POINT('Ctrl Pts',(2.57678719317313,0.896737914005474,
8.80163734024559));
#375905=CARTESIAN_POINT('Ctrl Pts',(2.57061666246837,0.897652391289077,
8.80716298614018));
#375906=CARTESIAN_POINT('Ctrl Pts',(2.564443842353,0.898567252466887,8.8126860086129));
#375907=CARTESIAN_POINT('Ctrl Pts',(2.54704276624754,0.901146230743177,
8.82825531609049));
#375908=CARTESIAN_POINT('Ctrl Pts',(2.52962348524516,0.903728261390025,
8.84380379913848));
#375909=CARTESIAN_POINT('Ctrl Pts',(2.51218498036395,0.906313510406806,
8.85933012996512));
#375910=CARTESIAN_POINT('',(2.50039125247053,0.938360879023106,8.85933012996512));
#375911=CARTESIAN_POINT('Origin',(2.51499936228368,0.925543015948154,8.84999761231046));
#375912=CARTESIAN_POINT('',(2.54747944236022,0.992223662303432,8.79610912703474));
#375913=CARTESIAN_POINT('Ctrl Pts',(2.50039125247053,0.938360879023106,
8.85933012996512));
#375914=CARTESIAN_POINT('Ctrl Pts',(2.50450715051616,0.943069194306276,
8.8538223528706));
#375915=CARTESIAN_POINT('Ctrl Pts',(2.50862146792257,0.947775631750053,
8.84831178811348));
#375916=CARTESIAN_POINT('Ctrl Pts',(2.51273423521776,0.952480227291854,
8.84279849653635));
#375917=CARTESIAN_POINT('Ctrl Pts',(2.5243280569779,0.965742402914834,8.82725662040549));
#375918=CARTESIAN_POINT('Ctrl Pts',(2.53590957550767,0.978989958767267,
8.81169306718667));
#375919=CARTESIAN_POINT('Ctrl Pts',(2.54747944236022,0.992223662303432,
8.79610912703474));
#375920=CARTESIAN_POINT('',(2.52025288996714,1.05947377310391,8.79610912703474));
#375921=CARTESIAN_POINT('Origin',(0.,1.84795814293585E-15,8.79610912703474));
#375922=CARTESIAN_POINT('',(2.44895572090754,1.06540763642202,8.85933012996512));
#375923=CARTESIAN_POINT('Ctrl Pts',(2.52025288996714,1.05947377310391,8.79610912703474));
#375924=CARTESIAN_POINT('Ctrl Pts',(2.51403871210982,1.0599907920964,8.80163734024559));
#375925=CARTESIAN_POINT('Ctrl Pts',(2.50782226866145,1.06050804322869,8.80716298614018));
#375926=CARTESIAN_POINT('Ctrl Pts',(2.50160351591013,1.0610255307834,8.8126860086129));
#375927=CARTESIAN_POINT('Ctrl Pts',(2.4840729564763,1.06248431949825,8.82825531609049));
#375928=CARTESIAN_POINT('Ctrl Pts',(2.46652403398341,1.06394498792048,8.84380379913848));
#375929=CARTESIAN_POINT('Ctrl Pts',(2.44895572090754,1.06540763642202,8.85933012996512));
#375930=CARTESIAN_POINT('',(2.4351329425359,1.0966335335419,8.85933012996512));
#375931=CARTESIAN_POINT('Origin',(2.45053228172764,1.08477795095059,8.84999761231044));
#375932=CARTESIAN_POINT('',(2.47867338431573,1.15340260064194,8.79610912703474));
#375933=CARTESIAN_POINT('Ctrl Pts',(2.4351329425359,1.0966335335419,8.85933012996512));
#375934=CARTESIAN_POINT('Ctrl Pts',(2.43893872123164,1.10159588157956,8.8538223528706));
#375935=CARTESIAN_POINT('Ctrl Pts',(2.44274304284933,1.10655625436414,8.84831178811348));
#375936=CARTESIAN_POINT('Ctrl Pts',(2.44654593555173,1.11151468971517,8.84279849653635));
#375937=CARTESIAN_POINT('Ctrl Pts',(2.45726622605205,1.12549243548656,8.82725662040549));
#375938=CARTESIAN_POINT('Ctrl Pts',(2.46797517529221,1.13945480325461,8.81169306718667));
#375939=CARTESIAN_POINT('Ctrl Pts',(2.47867338431573,1.15340260064194,8.79610912703474));
#375940=CARTESIAN_POINT('',(2.44719404240187,1.21877012767608,8.79610912703474));
#375941=CARTESIAN_POINT('Origin',(0.,1.84795814293585E-15,8.79610912703474));
#375942=CARTESIAN_POINT('',(2.37566317709457,1.22012377392995,8.85933012996512));
#375943=CARTESIAN_POINT('Ctrl Pts',(2.44719404240187,1.21877012767608,8.79610912703474));
#375944=CARTESIAN_POINT('Ctrl Pts',(2.44095950671884,1.21888794065528,8.80163734024559));
#375945=CARTESIAN_POINT('Ctrl Pts',(2.43472269522642,1.21900584014042,8.80716298614018));
#375946=CARTESIAN_POINT('Ctrl Pts',(2.42848356402811,1.21912382760466,8.8126860086129));
#375947=CARTESIAN_POINT('Ctrl Pts',(2.41089555809492,1.21945643228233,8.82825531609049));
#375948=CARTESIAN_POINT('Ctrl Pts',(2.39328910639828,1.21978973628009,8.84380379913848));
#375949=CARTESIAN_POINT('Ctrl Pts',(2.37566317709457,1.22012377392995,8.85933012996512));
#375950=CARTESIAN_POINT('',(2.35986814900601,1.25039988564422,8.85933012996512));
#375951=CARTESIAN_POINT('Origin',(2.37599543838842,1.23955530066841,8.84999761231045));
#375952=CARTESIAN_POINT('',(2.39968192566131,1.30984196029033,8.79610912703474));
#375953=CARTESIAN_POINT('Ctrl Pts',(2.35986814900601,1.25039988564422,8.85933012996512));
#375954=CARTESIAN_POINT('Ctrl Pts',(2.36334816959086,1.25559587508386,8.8538223528706));
#375955=CARTESIAN_POINT('Ctrl Pts',(2.36682686264628,1.26078979997348,8.84831178811348));
#375956=CARTESIAN_POINT('Ctrl Pts',(2.37030425385407,1.26598169985929,8.84279849653635));
#375957=CARTESIAN_POINT('Ctrl Pts',(2.3801069611214,1.2806175782235,8.82725662040549));
#375958=CARTESIAN_POINT('Ctrl Pts',(2.38989933570246,1.29523738354309,8.81169306718667));
#375959=CARTESIAN_POINT('Ctrl Pts',(2.39968192566131,1.30984196029033,8.79610912703474));
#375960=CARTESIAN_POINT('',(2.36407914959489,1.37305829436826,8.79610912703474));
#375961=CARTESIAN_POINT('Origin',(0.,1.84795814293585E-15,8.79610912703474));
#375962=CARTESIAN_POINT('',(2.29260852370876,1.36982616113508,8.85933012996512));
#375963=CARTESIAN_POINT('Ctrl Pts',(2.36407914959489,1.37305829436826,8.79610912703474));
#375964=CARTESIAN_POINT('Ctrl Pts',(2.35784987513058,1.37277641721537,8.80163734024559));
#375965=CARTESIAN_POINT('Ctrl Pts',(2.35161832399031,1.37249448057907,8.80716298614018));
#375966=CARTESIAN_POINT('Ctrl Pts',(2.34538445227341,1.37221248311705,8.8126860086129));
#375967=CARTESIAN_POINT('Ctrl Pts',(2.32781127272985,1.37141753701358,8.82825531609049));
#375968=CARTESIAN_POINT('Ctrl Pts',(2.31021964051605,1.37062210696925,8.84380379913848));
#375969=CARTESIAN_POINT('Ctrl Pts',(2.29260852370876,1.36982616113508,8.85933012996512));
#375970=CARTESIAN_POINT('',(2.27490615106173,1.39902807640649,8.85933012996512));
#375971=CARTESIAN_POINT('Origin',(2.29169512014344,1.38923905177201,8.84999761231047));
#375972=CARTESIAN_POINT('',(2.31082965924419,1.46089889836366,8.79610912703474));
#375973=CARTESIAN_POINT('Ctrl Pts',(2.27490615106173,1.39902807640649,8.85933012996512));
#375974=CARTESIAN_POINT('Ctrl Pts',(2.27804611338464,1.40443635581296,8.8538223528706));
#375975=CARTESIAN_POINT('Ctrl Pts',(2.28118488318185,1.40984248985616,8.84831178811348));
#375976=CARTESIAN_POINT('Ctrl Pts',(2.28432248354865,1.41524651964647,8.84279849653635));
#375977=CARTESIAN_POINT('Ctrl Pts',(2.29316732615615,1.43048038863991,8.82725662040549));
#375978=CARTESIAN_POINT('Ctrl Pts',(2.30200288711052,1.44569755559504,8.81169306718667));
#375979=CARTESIAN_POINT('Ctrl Pts',(2.31082965924419,1.46089889836366,8.79610912703474));
#375980=CARTESIAN_POINT('',(2.27124974846883,1.5217042700088,8.79610912703474));
#375981=CARTESIAN_POINT('Origin',(0.,1.84795814293585E-15,8.79610912703474));
#375982=CARTESIAN_POINT('',(2.20013305013605,1.51389963881731,8.85933012996512));
#375983=CARTESIAN_POINT('Ctrl Pts',(2.27124974846883,1.5217042700088,8.79610912703474));
#375984=CARTESIAN_POINT('Ctrl Pts',(2.26505133264819,1.52102386101751,8.80163734024559));
#375985=CARTESIAN_POINT('Ctrl Pts',(2.25885064864038,1.52034324679789,8.80716298614018));
#375986=CARTESIAN_POINT('Ctrl Pts',(2.25264765272093,1.51966242319766,8.8126860086129));
#375987=CARTESIAN_POINT('Ctrl Pts',(2.23516151153118,1.5177431929171,8.82825531609049));
#375988=CARTESIAN_POINT('Ctrl Pts',(2.21765698659038,1.51582229742335,8.84380379913848));
#375989=CARTESIAN_POINT('Ctrl Pts',(2.20013305013605,1.51389963881731,8.85933012996512));
#375990=CARTESIAN_POINT('',(2.1805960757769,1.54190736071222,8.85933012996512));
#375991=CARTESIAN_POINT('Origin',(2.19797773508275,1.53321412162104,8.84999761231047));
#375992=CARTESIAN_POINT('',(2.21248169808583,1.60595268950179,8.79610912703474));
#375993=CARTESIAN_POINT('Ctrl Pts',(2.1805960757769,1.54190736071222,8.85933012996512));
#375994=CARTESIAN_POINT('Ctrl Pts',(2.18338307705916,1.54750570630538,8.8538223528706));
#375995=CARTESIAN_POINT('Ctrl Pts',(2.1861690257198,1.55310183453776,8.84831178811348));
#375996=CARTESIAN_POINT('Ctrl Pts',(2.18895394217269,1.55869578791499,8.84279849653635));
#375997=CARTESIAN_POINT('Ctrl Pts',(2.19680457476489,1.57446504830231,8.82725662040549));
#375998=CARTESIAN_POINT('Ctrl Pts',(2.20464701487736,1.5902170462899,8.81169306718667));
#375999=CARTESIAN_POINT('Ctrl Pts',(2.21248169808583,1.60595268950179,8.79610912703474));
#376000=CARTESIAN_POINT('',(2.16908729494478,1.66409723639934,8.79610912703474));
#376001=CARTESIAN_POINT('Origin',(0.,1.84795814293585E-15,8.79610912703474));
#376002=CARTESIAN_POINT('',(2.09861675793327,1.65175217815318,8.85933012996512));
#376003=CARTESIAN_POINT('Ctrl Pts',(2.16908729494478,1.66409723639934,8.79610912703474));
#376004=CARTESIAN_POINT('Ctrl Pts',(2.16294520838797,1.66302109151613,8.80163734024559));
#376005=CARTESIAN_POINT('Ctrl Pts',(2.15680087145325,1.661944596503,8.80716298614018));
#376006=CARTESIAN_POINT('Ctrl Pts',(2.15065424077201,1.66086774441479,8.8126860086129));
#376007=CARTESIAN_POINT('Ctrl Pts',(2.13332699224099,1.65783211648603,8.82825531609049));
#376008=CARTESIAN_POINT('Ctrl Pts',(2.11598150442088,1.65479364891447,8.84380379913848));
#376009=CARTESIAN_POINT('Ctrl Pts',(2.09861675793327,1.65175217815318,8.85933012996512));
#376010=CARTESIAN_POINT('',(2.07732546348031,1.6784506169347,8.85933012996512));
#376011=CARTESIAN_POINT('Origin',(2.09522838804386,1.67088888577093,8.84999761231045));
#376012=CARTESIAN_POINT('',(2.10504217505419,1.74440727656298,8.79610912703474));
#376013=CARTESIAN_POINT('Ctrl Pts',(2.07732546348031,1.6784506169347,8.85933012996512));
#376014=CARTESIAN_POINT('Ctrl Pts',(2.07974805133585,1.68421602391166,8.8538223528706));
#376015=CARTESIAN_POINT('Ctrl Pts',(2.08216973079928,1.68997915064194,8.84831178811348));
#376016=CARTESIAN_POINT('Ctrl Pts',(2.0845905195192,1.69574004085178,8.84279849653635));
#376017=CARTESIAN_POINT('Ctrl Pts',(2.09141468216281,1.71197989335955,8.82725662040549));
#376018=CARTESIAN_POINT('Ctrl Pts',(2.09823177516477,1.72820199404107,8.81169306718667));
#376019=CARTESIAN_POINT('Ctrl Pts',(2.10504217505419,1.74440727656298,8.79610912703474));
#376020=CARTESIAN_POINT('',(2.05801159645803,1.79965207029777,8.79610912703474));
#376021=CARTESIAN_POINT('Origin',(0.,1.84795814293585E-15,8.79610912703474));
#376022=CARTESIAN_POINT('',(1.98847679932026,1.7828173134893,8.85933012996512));
#376023=CARTESIAN_POINT('Ctrl Pts',(2.05801159645803,1.79965207029777,8.79610912703474));
#376024=CARTESIAN_POINT('Ctrl Pts',(2.05195107831618,1.7981846116328,8.80163734024559));
#376025=CARTESIAN_POINT('Ctrl Pts',(2.04588833685297,1.79671665937509,8.80716298614018));
#376026=CARTESIAN_POINT('Ctrl Pts',(2.03982332923388,1.7952482038151,8.8126860086129));
#376027=CARTESIAN_POINT('Ctrl Pts',(2.02272617474248,1.79110865228445,8.82825531609049));
#376028=CARTESIAN_POINT('Ctrl Pts',(2.00561100037311,1.78696509835008,8.84380379913848));
#376029=CARTESIAN_POINT('Ctrl Pts',(1.98847679932026,1.7828173134893,8.85933012996512));
#376030=CARTESIAN_POINT('',(1.96551867526936,1.80809675954566,8.85933012996512));
#376031=CARTESIAN_POINT('Origin',(1.9838692981334,1.80169760908465,8.84999761231047));
#376032=CARTESIAN_POINT('',(1.98895258219513,1.87569371995059,8.79610912703474));
#376033=CARTESIAN_POINT('Ctrl Pts',(1.96551867526936,1.80809675954566,8.85933012996512));
#376034=CARTESIAN_POINT('Ctrl Pts',(1.96756689476504,1.81400553661248,8.8538223528706));
#376035=CARTESIAN_POINT('Ctrl Pts',(1.9696143538309,1.81991197991674,8.84831178811348));
#376036=CARTESIAN_POINT('Ctrl Pts',(1.97166106727774,1.8258161342256,8.84279849653635));
#376037=CARTESIAN_POINT('Ctrl Pts',(1.97743071802468,1.84245984581644,8.82725662040549));
#376038=CARTESIAN_POINT('Ctrl Pts',(1.98319445101872,1.85908538910056,8.81169306718667));
#376039=CARTESIAN_POINT('Ctrl Pts',(1.98895258219513,1.87569371995059,8.79610912703474));
#376040=CARTESIAN_POINT('',(1.93847908687933,1.92781174781519,8.79610912703474));
#376041=CARTESIAN_POINT('Origin',(0.,1.84795814293585E-15,8.79610912703474));
#376042=CARTESIAN_POINT('',(1.8701657630119,1.90655647007117,8.85933012996512));
#376043=CARTESIAN_POINT('Ctrl Pts',(1.93847908687933,1.92781174781519,8.79610912703474));
#376044=CARTESIAN_POINT('Ctrl Pts',(1.93252504112147,1.92595900547089,8.80163734024559));
#376045=CARTESIAN_POINT('Ctrl Pts',(1.9265688082349,1.9241056280993,8.80716298614018));
#376046=CARTESIAN_POINT('Ctrl Pts',(1.92061034609519,1.9222516032664,8.8126860086129));
#376047=CARTESIAN_POINT('Ctrl Pts',(1.90381354151855,1.91702513843903,8.82825531609049));
#376048=CARTESIAN_POINT('Ctrl Pts',(1.88699901052259,1.91179352489375,8.84380379913848));
#376049=CARTESIAN_POINT('Ctrl Pts',(1.8701657630119,1.90655647007117,8.85933012996512));
#376050=CARTESIAN_POINT('',(1.8456351492193,1.93031304473611,8.85933012996512));
#376051=CARTESIAN_POINT('Origin',(1.86435806373829,1.92510277045971,8.84999761231047));
#376052=CARTESIAN_POINT('',(1.86468995654684,1.99927253550788,8.79610912703474));
#376053=CARTESIAN_POINT('Ctrl Pts',(1.8456351492193,1.93031304473611,8.85933012996512));
#376054=CARTESIAN_POINT('Ctrl Pts',(1.84730058378186,1.93634091146039,8.8538223528706));
#376055=CARTESIAN_POINT('Ctrl Pts',(1.84896540900168,1.94236640049617,8.84831178811348));
#376056=CARTESIAN_POINT('Ctrl Pts',(1.85062963679086,1.94838955746756,8.84279849653635));
#376057=CARTESIAN_POINT('Ctrl Pts',(1.85532106690863,1.96536873556047,8.82725662040549));
#376058=CARTESIAN_POINT('Ctrl Pts',(1.86000775547956,1.98232940352367,8.81169306718667));
#376059=CARTESIAN_POINT('Ctrl Pts',(1.86468995654684,1.99927253550788,8.79610912703474));
#376060=CARTESIAN_POINT('',(1.81098095093019,2.04804963334651,8.79610912703474));
#376061=CARTESIAN_POINT('Origin',(0.,1.84795814293585E-15,8.79610912703474));
#376062=CARTESIAN_POINT('',(1.74416981443404,2.02246117716244,8.85933012996512));
#376063=CARTESIAN_POINT('Ctrl Pts',(1.81098095093019,2.04804963334651,8.79610912703474));
#376064=CARTESIAN_POINT('Ctrl Pts',(1.80515784400747,2.04581922063858,8.80163734024559));
#376065=CARTESIAN_POINT('Ctrl Pts',(1.79933259513608,2.04358803407827,8.80716298614018));
#376066=CARTESIAN_POINT('Ctrl Pts',(1.79350516307477,2.0413560585582,8.8126860086129));
#376067=CARTESIAN_POINT('Ctrl Pts',(1.77707773008579,2.03506415709916,8.82825531609049));
#376068=CARTESIAN_POINT('Ctrl Pts',(1.76063293697782,2.02876598176522,8.84380379913848));
#376069=CARTESIAN_POINT('Ctrl Pts',(1.74416981443404,2.02246117716244,8.85933012996512));
#376070=CARTESIAN_POINT('',(1.71816751245359,2.0445972595749,8.85933012996512));
#376071=CARTESIAN_POINT('Origin',(1.73718578215574,2.0405972716177,8.84999761231047));
#376072=CARTESIAN_POINT('',(1.73276491989236,2.11463591137415,8.79610912703474));
#376073=CARTESIAN_POINT('Ctrl Pts',(1.71816751245359,2.0445972595749,8.85933012996512));
#376074=CARTESIAN_POINT('Ctrl Pts',(1.7194433184552,2.05071944615928,8.8538223528706));
#376075=CARTESIAN_POINT('Ctrl Pts',(1.72071866870503,2.05683922089967,8.84831178811348));
#376076=CARTESIAN_POINT('Ctrl Pts',(1.7219935721676,2.06295663008964,8.84279849653635));
#376077=CARTESIAN_POINT('Ctrl Pts',(1.72558750356353,2.08020150359982,8.82725662040549));
#376078=CARTESIAN_POINT('Ctrl Pts',(1.72917788910273,2.09742760121938,8.81169306718667));
#376079=CARTESIAN_POINT('Ctrl Pts',(1.73276491989236,2.11463591137415,8.79610912703474));
#376080=CARTESIAN_POINT('',(1.67604110579947,2.15987164362914,8.79610912703474));
#376081=CARTESIAN_POINT('Origin',(0.,1.84795814293585E-15,8.79610912703474));
#376082=CARTESIAN_POINT('',(1.61100669796541,2.13005515746019,8.85933012996512));
#376083=CARTESIAN_POINT('Ctrl Pts',(1.67604110579947,2.15987164362914,8.79610912703474));
#376084=CARTESIAN_POINT('Ctrl Pts',(1.6703728661073,2.15727272580182,8.80163734024559));
#376085=CARTESIAN_POINT('Ctrl Pts',(1.6647025384482,2.15467289847697,8.80716298614018));
#376086=CARTESIAN_POINT('Ctrl Pts',(1.65903008263362,2.15207214393589,8.8126860086129));
#376087=CARTESIAN_POINT('Ctrl Pts',(1.64303952507813,2.14474066061787,8.82825531609049));
#376088=CARTESIAN_POINT('Ctrl Pts',(1.62703204504042,2.13740180404867,8.84380379913848));
#376089=CARTESIAN_POINT('Ctrl Pts',(1.61100669796541,2.13005515746019,8.85933012996512));
#376090=CARTESIAN_POINT('',(1.58363955683344,2.15047978570935,8.85933012996512));
#376091=CARTESIAN_POINT('Origin',(1.60287503156912,2.14770652087988,8.84999761231047));
#376092=CARTESIAN_POINT('',(1.59371958050512,2.22130979469261,8.79610912703474));
#376093=CARTESIAN_POINT('Ctrl Pts',(1.58363955683344,2.15047978570935,8.85933012996512));
#376094=CARTESIAN_POINT('Ctrl Pts',(1.58452049171356,2.15667113477597,8.8538223528706));
#376095=CARTESIAN_POINT('Ctrl Pts',(1.58540112630568,2.16286004775387,8.84831178811348));
#376096=CARTESIAN_POINT('Ctrl Pts',(1.58628146658983,2.16904657141586,8.84279849653635));
#376097=CARTESIAN_POINT('Ctrl Pts',(1.58876313102893,2.18648627745904,8.82725662040549));
#376098=CARTESIAN_POINT('Ctrl Pts',(1.59124245987207,2.20390701900486,8.81169306718667));
#376099=CARTESIAN_POINT('Ctrl Pts',(1.59371958050512,2.22130979469261,8.79610912703474));
#376100=CARTESIAN_POINT('',(1.53421404825534,2.26281827803709,8.79610912703474));
#376101=CARTESIAN_POINT('Origin',(0.,1.84795814293585E-15,8.79610912703474));
#376102=CARTESIAN_POINT('',(1.47122360941498,2.22889628422053,8.85933012996512));
#376103=CARTESIAN_POINT('Ctrl Pts',(1.53421404825534,2.26281827803709,8.79610912703474));
#376104=CARTESIAN_POINT('Ctrl Pts',(1.52872396780644,2.2598615346012,8.80163734024559));
#376105=CARTESIAN_POINT('Ctrl Pts',(1.52323186195228,2.25690374975993,8.80716298614018));
#376106=CARTESIAN_POINT('Ctrl Pts',(1.51773769172209,2.25394490325611,8.8126860086129));
#376107=CARTESIAN_POINT('Ctrl Pts',(1.50224971823106,2.24560396471668,8.82825531609049));
#376108=CARTESIAN_POINT('Ctrl Pts',(1.48674532943268,2.23725458384804,8.84380379913848));
#376109=CARTESIAN_POINT('Ctrl Pts',(1.47122360941498,2.22889628422053,8.85933012996512));
#376110=CARTESIAN_POINT('',(1.44260408658464,2.24752552912785,8.85933012996512));
#376111=CARTESIAN_POINT('Origin',(1.46197772366217,2.24599038336617,8.84999761231045));
#376112=CARTESIAN_POINT('',(1.44812530550982,2.31885583959522,8.79610912703474));
#376113=CARTESIAN_POINT('Ctrl Pts',(1.44260408658464,2.24752552912785,8.85933012996512));
#376114=CARTESIAN_POINT('Ctrl Pts',(1.4430865303929,2.25376059909535,8.8538223528706));
#376115=CARTESIAN_POINT('Ctrl Pts',(1.44356883061086,2.25999321873982,8.84831178811348));
#376116=CARTESIAN_POINT('Ctrl Pts',(1.44405099020954,2.26622343512111,8.84279849653635));
#376117=CARTESIAN_POINT('Ctrl Pts',(1.44541019000031,2.28378631020436,8.82725662040549));
#376118=CARTESIAN_POINT('Ctrl Pts',(1.44676827405337,2.30133011011269,8.81169306718667));
#376119=CARTESIAN_POINT('Ctrl Pts',(1.44812530550982,2.31885583959522,8.79610912703474));
#376120=CARTESIAN_POINT('',(1.38608257609904,2.35646650676758,8.79610912703474));
#376121=CARTESIAN_POINT('Origin',(0.,1.84795814293585E-15,8.79610912703474));
#376122=CARTESIAN_POINT('',(1.325394947477,2.31857839805226,8.85933012996512));
#376123=CARTESIAN_POINT('Ctrl Pts',(1.38608257609904,2.35646650676758,8.79610912703474));
#376124=CARTESIAN_POINT('Ctrl Pts',(1.3807932148116,2.35316408761612,8.80163734024559));
#376125=CARTESIAN_POINT('Ctrl Pts',(1.37550189900337,2.34986049943079,8.80716298614018));
#376126=CARTESIAN_POINT('Ctrl Pts',(1.37020859108156,2.3465557194992,8.8126860086129));
#376127=CARTESIAN_POINT('Ctrl Pts',(1.35528684506022,2.33723960044393,8.82825531609049));
#376128=CARTESIAN_POINT('Ctrl Pts',(1.34034925836042,2.32791400467277,8.84380379913848));
#376129=CARTESIAN_POINT('Ctrl Pts',(1.325394947477,2.31857839805226,8.85933012996512));
#376130=CARTESIAN_POINT('',(1.29564064670646,2.33533570805445,8.85933012996512));
#376131=CARTESIAN_POINT('Origin',(1.31507283569545,2.33504498960377,8.84999761231045));
#376132=CARTESIAN_POINT('',(1.29658037301227,2.40687320845992,8.79610912703474));
#376133=CARTESIAN_POINT('Ctrl Pts',(1.29564064670646,2.33533570805445,8.85933012996512));
#376134=CARTESIAN_POINT('Ctrl Pts',(1.29572261697775,2.34158887768292,8.8538223528706));
#376135=CARTESIAN_POINT('Ctrl Pts',(1.29580460094652,2.34783959282295,8.84831178811348));
#376136=CARTESIAN_POINT('Ctrl Pts',(1.29588659856252,2.35408790062805,8.84279849653635));
#376137=CARTESIAN_POINT('Ctrl Pts',(1.29611774846146,2.37170177513041,8.82725662040549));
#376138=CARTESIAN_POINT('Ctrl Pts',(1.29634900706576,2.3892965421643,8.81169306718667));
#376139=CARTESIAN_POINT('Ctrl Pts',(1.29658037301227,2.40687320845992,8.79610912703474));
#376140=CARTESIAN_POINT('',(1.23225539332378,2.44043150916129,8.79610912703474));
#376141=CARTESIAN_POINT('Origin',(0.,1.84795814293585E-15,8.79610912703474));
#376142=CARTESIAN_POINT('',(1.17411995340351,2.39873297591288,8.85933012996512));
#376143=CARTESIAN_POINT('Ctrl Pts',(1.23225539332378,2.44043150916129,8.79610912703474));
#376144=CARTESIAN_POINT('Ctrl Pts',(1.22718848631789,2.43679698464291,8.80163734024559));
#376145=CARTESIAN_POINT('Ctrl Pts',(1.22211970370724,2.433161168266,8.80716298614018));
#376146=CARTESIAN_POINT('Ctrl Pts',(1.21704900943146,2.42952403495623,8.8126860086129));
#376147=CARTESIAN_POINT('Ctrl Pts',(1.20275480753491,2.41927101731663,8.82825531609049));
#376148=CARTESIAN_POINT('Ctrl Pts',(1.18844540468154,2.40900752751631,8.84380379913848));
#376149=CARTESIAN_POINT('Ctrl Pts',(1.17411995340351,2.39873297591288,8.85933012996512));
#376150=CARTESIAN_POINT('',(1.14335314149692,2.41354949162872,8.85933012996512));
#376151=CARTESIAN_POINT('Origin',(1.16276403136462,2.41450439511349,8.84999761231047));
#376152=CARTESIAN_POINT('',(1.1397075136464,2.48500021903836,8.79610912703474));
#376153=CARTESIAN_POINT('Ctrl Pts',(1.14335314149692,2.41354949162872,8.85933012996512));
#376154=CARTESIAN_POINT('Ctrl Pts',(1.14303430139782,2.41979506530285,8.8538223528706));
#376155=CARTESIAN_POINT('Ctrl Pts',(1.14271563222767,2.42603819040915,8.84831178811348));
#376156=CARTESIAN_POINT('Ctrl Pts',(1.1423971309152,2.43227891400103,8.84279849653635));
#376157=CARTESIAN_POINT('Ctrl Pts',(1.1414992810778,2.44987140873402,8.82725662040549));
#376158=CARTESIAN_POINT('Ctrl Pts',(1.14060276394212,2.46744484222165,8.81169306718667));
#376159=CARTESIAN_POINT('Ctrl Pts',(1.1397075136464,2.48500021903836,8.79610912703474));
#376160=CARTESIAN_POINT('',(1.07336460881939,2.51436825501293,8.79610912703474));
#376161=CARTESIAN_POINT('Origin',(0.,1.84795814293585E-15,8.79610912703474));
#376162=CARTESIAN_POINT('',(1.01802024859354,2.46903064544887,8.85933012996512));
#376163=CARTESIAN_POINT('Ctrl Pts',(1.07336460881939,2.51436825501293,8.79610912703474));
#376164=CARTESIAN_POINT('Ctrl Pts',(1.06854097710278,2.51041656016849,8.80163734024559));
#376165=CARTESIAN_POINT('Ctrl Pts',(1.06371555640471,2.50646345594937,8.80716298614018));
#376166=CARTESIAN_POINT('Ctrl Pts',(1.05888831234541,2.50250891502236,8.8126860086129));
#376167=CARTESIAN_POINT('Ctrl Pts',(1.04528039251534,2.49136113064717,8.82825531609049));
#376168=CARTESIAN_POINT('Ctrl Pts',(1.03165797391409,2.4802019216988,8.84380379913848));
#376169=CARTESIAN_POINT('Ctrl Pts',(1.01802024859354,2.46903064544887,8.85933012996512));
#376170=CARTESIAN_POINT('',(0.986367352980481,2.48184548263715,8.85933012996512));
#376171=CARTESIAN_POINT('Origin',(1.00567718021681,2.48404208415414,8.84999761231047));
#376172=CARTESIAN_POINT('',(0.978151351640454,2.55291583068591,8.79610912703474));
#376173=CARTESIAN_POINT('Ctrl Pts',(0.986367352980481,2.48184548263715,
8.85933012996512));
#376174=CARTESIAN_POINT('Ctrl Pts',(0.985649012693359,2.48805779595504,
8.8538223528706));
#376175=CARTESIAN_POINT('Ctrl Pts',(0.984930999864269,2.4942676766874,8.84831178811348));
#376176=CARTESIAN_POINT('Ctrl Pts',(0.984213308413526,2.50047517159419,
8.84279849653635));
#376177=CARTESIAN_POINT('Ctrl Pts',(0.982190148297363,2.51797399522337,
8.82725662040549));
#376178=CARTESIAN_POINT('Ctrl Pts',(0.980169539402921,2.53545388215706,
8.81169306718667));
#376179=CARTESIAN_POINT('Ctrl Pts',(0.978151351640454,2.55291583068591,
8.79610912703474));
#376180=CARTESIAN_POINT('',(0.910063138901376,2.57797292237443,8.79610912703474));
#376181=CARTESIAN_POINT('Origin',(0.,1.84795814293585E-15,8.79610912703474));
#376182=CARTESIAN_POINT('',(0.857737280217445,2.5291825384573,8.85933012996512));
#376183=CARTESIAN_POINT('Ctrl Pts',(0.910063138901376,2.57797292237443,
8.79610912703474));
#376184=CARTESIAN_POINT('Ctrl Pts',(0.905502603811445,2.57372029556567,
8.80163734024559));
#376185=CARTESIAN_POINT('Ctrl Pts',(0.900940373714648,2.56946614765751,
8.80716298614018));
#376186=CARTESIAN_POINT('Ctrl Pts',(0.896376416053107,2.56521044917019,
8.8126860086129));
#376187=CARTESIAN_POINT('Ctrl Pts',(0.883510696150981,2.5532137066966,8.82825531609049));
#376188=CARTESIAN_POINT('Ctrl Pts',(0.870631239241884,2.54120463418338,
8.84380379913848));
#376189=CARTESIAN_POINT('Ctrl Pts',(0.857737280217445,2.5291825384573,8.85933012996512));
#376190=CARTESIAN_POINT('',(0.825328369435515,2.53994303820323,8.85933012996512));
#376191=CARTESIAN_POINT('Origin',(0.844457785818413,2.54337231144565,8.84999761231045));
#376192=CARTESIAN_POINT('',(0.812575755917816,2.61034096358643,8.79610912703474));
#376193=CARTESIAN_POINT('Ctrl Pts',(0.825328369435515,2.53994303820323,
8.85933012996512));
#376194=CARTESIAN_POINT('Ctrl Pts',(0.824213480774689,2.54609656343693,
8.8538223528706));
#376195=CARTESIAN_POINT('Ctrl Pts',(0.823099074755386,2.5522476820634,8.84831178811348));
#376196=CARTESIAN_POINT('Ctrl Pts',(0.821985142314494,2.55839644035703,
8.84279849653635));
#376197=CARTESIAN_POINT('Ctrl Pts',(0.818844985518447,2.57572968646262,
8.82725662040549));
#376198=CARTESIAN_POINT('Ctrl Pts',(0.81570858798061,2.59304419823753,8.81169306718667));
#376199=CARTESIAN_POINT('Ctrl Pts',(0.812575755917816,2.61034096358643,
8.79610912703474));
#376200=CARTESIAN_POINT('',(0.743022024337684,2.63098414602443,8.79610912703474));
#376201=CARTESIAN_POINT('Origin',(0.,1.84795814293585E-15,8.79610912703474));
#376202=CARTESIAN_POINT('',(0.693929685372865,2.57894147790726,8.85933012996512));
#376203=CARTESIAN_POINT('Ctrl Pts',(0.743022024337684,2.63098414602443,
8.79610912703474));
#376204=CARTESIAN_POINT('Ctrl Pts',(0.738743326091345,2.6264480622071,8.80163734024559));
#376205=CARTESIAN_POINT('Ctrl Pts',(0.734463033777886,2.62191035181617,
8.80716298614018));
#376206=CARTESIAN_POINT('Ctrl Pts',(0.730181116795098,2.61737098334645,
8.8126860086129));
#376207=CARTESIAN_POINT('Ctrl Pts',(0.71811046482369,2.60457457996258,8.82825531609049));
#376208=CARTESIAN_POINT('Ctrl Pts',(0.706026894057816,2.59176499173941,
8.84380379913848));
#376209=CARTESIAN_POINT('Ctrl Pts',(0.693929685372865,2.57894147790726,
8.85933012996512));
#376210=CARTESIAN_POINT('',(0.660897934588157,2.58760342300926,8.85933012996512));
#376211=CARTESIAN_POINT('Origin',(0.679768333242446,2.59225127635775,8.84999761231048));
#376212=CARTESIAN_POINT('',(0.643661112117155,2.65703964555121,8.79610912703474));
#376213=CARTESIAN_POINT('Ctrl Pts',(0.660897934588157,2.58760342300926,
8.85933012996512));
#376214=CARTESIAN_POINT('Ctrl Pts',(0.659391078870276,2.59367287400365,
8.8538223528706));
#376215=CARTESIAN_POINT('Ctrl Pts',(0.657884858994133,2.5997399542584,8.84831178811348));
#376216=CARTESIAN_POINT('Ctrl Pts',(0.65637926295043,2.60580470937213,8.84279849653635));
#376217=CARTESIAN_POINT('Ctrl Pts',(0.652135013052335,2.62290115192791,
8.82725662040549));
#376218=CARTESIAN_POINT('Ctrl Pts',(0.647895715001341,2.63997913950121,
8.81169306718667));
#376219=CARTESIAN_POINT('Ctrl Pts',(0.643661112117155,2.65703964555121,
8.79610912703474));
#376220=CARTESIAN_POINT('',(0.572927672898268,2.67318409147409,8.79610912703474));
#376221=CARTESIAN_POINT('Origin',(0.,1.84795814293585E-15,8.79610912703474));
#376222=CARTESIAN_POINT('',(0.527270584603639,2.61810299364327,8.85933012996512));
#376223=CARTESIAN_POINT('Ctrl Pts',(0.572927672898268,2.67318409147409,
8.79610912703474));
#376224=CARTESIAN_POINT('Ctrl Pts',(0.568948393584391,2.66838319038958,
8.80163734024559));
#376225=CARTESIAN_POINT('Ctrl Pts',(0.564967627693506,2.66358056394121,
8.80716298614018));
#376226=CARTESIAN_POINT('Ctrl Pts',(0.560985346704822,2.65877617872783,
8.8126860086129));
#376227=CARTESIAN_POINT('Ctrl Pts',(0.549759363562228,2.64523269760001,
8.82825531609049));
#376228=CARTESIAN_POINT('Ctrl Pts',(0.538521332923773,2.63167523101254,
8.84380379913848));
#376229=CARTESIAN_POINT('Ctrl Pts',(0.527270584603639,2.61810299364327,
8.85933012996512));
#376230=CARTESIAN_POINT('',(0.493751728365416,2.62463079031095,8.85933012996512));
#376231=CARTESIAN_POINT('Origin',(0.512285566775364,2.63047812473921,8.84999761231043));
#376232=CARTESIAN_POINT('',(0.472101526741932,2.69281998167919,8.79610912703474));
#376233=CARTESIAN_POINT('Ctrl Pts',(0.493751728365416,2.62463079031095,
8.85933012996512));
#376234=CARTESIAN_POINT('Ctrl Pts',(0.491859097583844,2.63059122639,8.8538223528706));
#376235=CARTESIAN_POINT('Ctrl Pts',(0.489967253231417,2.63654933733887,
8.84831178811348));
#376236=CARTESIAN_POINT('Ctrl Pts',(0.488076180401994,2.64250516789305,
8.84279849653635));
#376237=CARTESIAN_POINT('Ctrl Pts',(0.482745277935072,2.6592945539494,8.82725662040549));
#376238=CARTESIAN_POINT('Ctrl Pts',(0.477420499555938,2.67606584020692,
8.81169306718667));
#376239=CARTESIAN_POINT('Ctrl Pts',(0.472101526741932,2.69281998167919,
8.79610912703474));
#376240=CARTESIAN_POINT('',(0.40047903875831,2.70439935009569,8.79610912703474));
#376241=CARTESIAN_POINT('Origin',(0.,1.84795814293585E-15,8.79610912703474));
#376242=CARTESIAN_POINT('',(0.358444815903088,2.64650616259708,8.85933012996512));
#376243=CARTESIAN_POINT('Ctrl Pts',(0.40047903875831,2.70439935009569,8.79610912703474));
#376244=CARTESIAN_POINT('Ctrl Pts',(0.396815530089149,2.69935335967635,
8.80163734024559));
#376245=CARTESIAN_POINT('Ctrl Pts',(0.393150648441755,2.69430555219278,
8.80716298614018));
#376246=CARTESIAN_POINT('Ctrl Pts',(0.389484367493953,2.68925589248512,
8.8126860086129));
#376247=CARTESIAN_POINT('Ctrl Pts',(0.379149183152874,2.67502098668236,
8.82825531609049));
#376248=CARTESIAN_POINT('Ctrl Pts',(0.36880287212028,2.66077135226888,8.84380379913848));
#376249=CARTESIAN_POINT('Ctrl Pts',(0.358444815903088,2.64650616259708,
8.85933012996512));
#376250=CARTESIAN_POINT('',(0.324576590381406,2.65087298671372,8.85933012996512));
#376251=CARTESIAN_POINT('Origin',(0.342697709029468,2.65789577427024,8.84999761231047));
#376252=CARTESIAN_POINT('',(0.298601974927864,2.71753494289438,8.79610912703474));
#376253=CARTESIAN_POINT('Ctrl Pts',(0.324576590381406,2.65087298671372,
8.85933012996512));
#376254=CARTESIAN_POINT('Ctrl Pts',(0.322305961761993,2.65669991516707,
8.8538223528706));
#376255=CARTESIAN_POINT('Ctrl Pts',(0.320036266927523,2.66252457365416,
8.84831178811348));
#376256=CARTESIAN_POINT('Ctrl Pts',(0.317767488136271,2.66834700586353,
8.84279849653635));
#376257=CARTESIAN_POINT('Ctrl Pts',(0.311371838922235,2.68476034423181,
8.82725662040549));
#376258=CARTESIAN_POINT('Ctrl Pts',(0.304983460871482,2.70115601236091,
8.81169306718667));
#376259=CARTESIAN_POINT('Ctrl Pts',(0.298601974927864,2.71753494289438,
8.79610912703474));
#376260=CARTESIAN_POINT('',(0.226384750345611,2.72450165169591,8.79610912703474));
#376261=CARTESIAN_POINT('Origin',(0.,1.84795814293585E-15,8.79610912703474));
#376262=CARTESIAN_POINT('',(0.188146120567823,2.66403427005499,8.85933012996512));
#376263=CARTESIAN_POINT('Ctrl Pts',(0.226384750345611,2.72450165169591,
8.79610912703474));
#376264=CARTESIAN_POINT('Ctrl Pts',(0.223052066464109,2.71923130699874,
8.80163734024559));
#376265=CARTESIAN_POINT('Ctrl Pts',(0.219718128845009,2.71395906100366,
8.80716298614018));
#376266=CARTESIAN_POINT('Ctrl Pts',(0.21638291347292,2.70868487693661,8.8126860086129));
#376267=CARTESIAN_POINT('Ctrl Pts',(0.206980997422702,2.69381704074024,
8.82825531609049));
#376268=CARTESIAN_POINT('Ctrl Pts',(0.19756892120728,2.67893379330508,8.84380379913848));
#376269=CARTESIAN_POINT('Ctrl Pts',(0.188146120567823,2.66403427005499,
8.85933012996512));
#376270=CARTESIAN_POINT('',(0.15406769756606,2.66622217740361,8.85933012996512));
#376271=CARTESIAN_POINT('Origin',(0.171701632888751,2.67439155994798,8.84999761231047));
#376272=CARTESIAN_POINT('',(0.123875403548898,2.7310829701198,8.79610912703474));
#376273=CARTESIAN_POINT('Ctrl Pts',(0.15406769756606,2.66622217740361,8.85933012996512));
#376274=CARTESIAN_POINT('Ctrl Pts',(0.151428401608852,2.67189165413237,
8.8538223528706));
#376275=CARTESIAN_POINT('Ctrl Pts',(0.148790182955263,2.67755892538658,
8.84831178811348));
#376276=CARTESIAN_POINT('Ctrl Pts',(0.146153021100887,2.68322403362827,
8.84279849653635));
#376277=CARTESIAN_POINT('Ctrl Pts',(0.138718906234218,2.69919387838049,
8.82725662040549));
#376278=CARTESIAN_POINT('Ctrl Pts',(0.13129317972756,2.71514655506395,8.81169306718667));
#376279=CARTESIAN_POINT('Ctrl Pts',(0.123875403548898,2.7310829701198,8.79610912703474));
#376280=CARTESIAN_POINT('',(0.0513601984344042,2.73340839160553,8.79610912703474));
#376281=CARTESIAN_POINT('Origin',(0.,1.84795814293585E-15,8.79610912703474));
#376282=CARTESIAN_POINT('',(0.0170742924659647,2.67061528926368,8.85933012996512));
#376283=CARTESIAN_POINT('Ctrl Pts',(0.0513601984344042,2.73340839160553,
8.79610912703474));
#376284=CARTESIAN_POINT('Ctrl Pts',(0.0483720340534879,2.72793534960737,
8.80163734024559));
#376285=CARTESIAN_POINT('Ctrl Pts',(0.045382740327487,2.72246032989048,
8.80716298614018));
#376286=CARTESIAN_POINT('Ctrl Pts',(0.0423922956464754,2.71698329421768,
8.8126860086129));
#376287=CARTESIAN_POINT('Ctrl Pts',(0.0339622823768732,2.70154362275576,
8.82825531609049));
#376288=CARTESIAN_POINT('Ctrl Pts',(0.0255231172186754,2.68608792075508,
8.84380379913848));
#376289=CARTESIAN_POINT('Ctrl Pts',(0.0170742924659647,2.67061528926368,
8.85933012996512));
#376290=CARTESIAN_POINT('',(-0.0170742924659647,2.67061528926368,8.85933012996512));
#376291=CARTESIAN_POINT('Origin',(-2.09135470009489E-9,2.6798976970507,
8.84999761231047));
#376292=CARTESIAN_POINT('',(-0.0513601984344042,2.73340839160553,8.79610912703474));
#376293=CARTESIAN_POINT('Ctrl Pts',(-0.0170742924659647,2.67061528926368,
8.85933012996512));
#376294=CARTESIAN_POINT('Ctrl Pts',(-0.0200714103277523,2.67610401717189,
8.8538223528706));
#376295=CARTESIAN_POINT('Ctrl Pts',(-0.0230673117941167,2.68159061315999,
8.84831178811348));
#376296=CARTESIAN_POINT('Ctrl Pts',(-0.0260620200478886,2.68707511828909,
8.84279849653635));
#376297=CARTESIAN_POINT('Ctrl Pts',(-0.0345040521945901,2.70253584590764,
8.82725662040549));
#376298=CARTESIAN_POINT('Ctrl Pts',(-0.0429366132541237,2.71797997817513,
8.81169306718667));
#376299=CARTESIAN_POINT('Ctrl Pts',(-0.0513601984344042,2.73340839160553,
8.79610912703474));
#376300=CARTESIAN_POINT('',(-0.123875403548937,2.73108297011979,8.79610912703474));
#376301=CARTESIAN_POINT('Origin',(0.,1.84795814293585E-15,8.79610912703474));
#376302=CARTESIAN_POINT('',(-0.154067697566098,2.66622217740361,8.85933012996512));
#376303=CARTESIAN_POINT('Ctrl Pts',(-0.123875403548937,2.73108297011979,
8.79610912703474));
#376304=CARTESIAN_POINT('Ctrl Pts',(-0.126506769420867,2.72542972072417,
8.80163734024559));
#376305=CARTESIAN_POINT('Ctrl Pts',(-0.129139135604647,2.71977442531588,
8.80716298614018));
#376306=CARTESIAN_POINT('Ctrl Pts',(-0.131772521215939,2.71411704435172,
8.8126860086129));
#376307=CARTESIAN_POINT('Ctrl Pts',(-0.139195990972168,2.6981689825461,
8.82825531609049));
#376308=CARTESIAN_POINT('Ctrl Pts',(-0.146627566733311,2.68220433677466,
8.84380379913848));
#376309=CARTESIAN_POINT('Ctrl Pts',(-0.154067697566098,2.66622217740361,
8.85933012996512));
#376310=CARTESIAN_POINT('',(-0.188146120567861,2.66403427005499,8.85933012996512));
#376311=CARTESIAN_POINT('Origin',(-0.171701637062902,2.67439155968,8.84999761231046));
#376312=CARTESIAN_POINT('',(-0.22638475034565,2.7245016516959,8.79610912703474));
#376313=CARTESIAN_POINT('Ctrl Pts',(-0.188146120567861,2.66403427005499,
8.85933012996512));
#376314=CARTESIAN_POINT('Ctrl Pts',(-0.191488744534055,2.66931969478233,
8.8538223528706));
#376315=CARTESIAN_POINT('Ctrl Pts',(-0.19483001801145,2.67460306990455,
8.84831178811348));
#376316=CARTESIAN_POINT('Ctrl Pts',(-0.19816996676604,2.67988443491305,
8.84279849653635));
#376317=CARTESIAN_POINT('Ctrl Pts',(-0.207585226071873,2.69477251395182,
8.82725662040549));
#376318=CARTESIAN_POINT('Ctrl Pts',(-0.21698997048211,2.70964463855111,
8.81169306718667));
#376319=CARTESIAN_POINT('Ctrl Pts',(-0.22638475034565,2.7245016516959,8.79610912703474));
#376320=CARTESIAN_POINT('',(-0.298601974927905,2.71753494289437,8.79610912703474));
#376321=CARTESIAN_POINT('Origin',(0.,1.84795814293585E-15,8.79610912703474));
#376322=CARTESIAN_POINT('',(-0.324576590381445,2.65087298671372,8.85933012996512));
#376323=CARTESIAN_POINT('Ctrl Pts',(-0.298601974927905,2.71753494289437,
8.79610912703474));
#376324=CARTESIAN_POINT('Ctrl Pts',(-0.300865729444055,2.71172471651568,
8.80163734024559));
#376325=CARTESIAN_POINT('Ctrl Pts',(-0.303130351128325,2.70591238423786,
8.80716298614018));
#376326=CARTESIAN_POINT('Ctrl Pts',(-0.305395856523559,2.70009790537424,
8.8126860086129));
#376327=CARTESIAN_POINT('Ctrl Pts',(-0.311782278136857,2.68370698723172,
8.82825531609049));
#376328=CARTESIAN_POINT('Ctrl Pts',(-0.318175726562075,2.6672989998434,
8.84380379913848));
#376329=CARTESIAN_POINT('Ctrl Pts',(-0.324576590381445,2.65087298671372,
8.85933012996512));
#376330=CARTESIAN_POINT('',(-0.358444815903127,2.64650616259708,8.85933012996512));
#376331=CARTESIAN_POINT('Origin',(-0.342697713177869,2.65789577373535,8.84999761231049));
#376332=CARTESIAN_POINT('',(-0.400479038758349,2.70439935009568,8.79610912703474));
#376333=CARTESIAN_POINT('Ctrl Pts',(-0.358444815903127,2.64650616259708,
8.85933012996512));
#376334=CARTESIAN_POINT('Ctrl Pts',(-0.36211921041486,2.65156656519963,
8.8538223528706));
#376335=CARTESIAN_POINT('Ctrl Pts',(-0.365792125893867,2.65662500893431,
8.84831178811348));
#376336=CARTESIAN_POINT('Ctrl Pts',(-0.369463590583425,2.66168153156055,
8.84279849653635));
#376337=CARTESIAN_POINT('Ctrl Pts',(-0.379813387728335,2.67593578370929,
8.82725662040549));
#376338=CARTESIAN_POINT('Ctrl Pts',(-0.390151669377183,2.69017478789034,
8.81169306718667));
#376339=CARTESIAN_POINT('Ctrl Pts',(-0.400479038758349,2.70439935009568,
8.79610912703474));
#376340=CARTESIAN_POINT('',(-0.472101526741971,2.69281998167918,8.79610912703474));
#376341=CARTESIAN_POINT('Origin',(0.,1.84795814293585E-15,8.79610912703474));
#376342=CARTESIAN_POINT('',(-0.493751728365454,2.62463079031095,8.85933012996512));
#376343=CARTESIAN_POINT('Ctrl Pts',(-0.472101526741971,2.69281998167918,
8.79610912703474));
#376344=CARTESIAN_POINT('Ctrl Pts',(-0.47398836764946,2.6868766537839,8.80163734024559));
#376345=CARTESIAN_POINT('Ctrl Pts',(-0.475875939017959,2.68093116875663,
8.80716298614018));
#376346=CARTESIAN_POINT('Ctrl Pts',(-0.477764254749519,2.67498348493439,
8.8126860086129));
#376347=CARTESIAN_POINT('Ctrl Pts',(-0.483087385043594,2.65821706425347,
8.82825531609049));
#376348=CARTESIAN_POINT('Ctrl Pts',(-0.488416434081916,2.64143315918795,
8.84380379913848));
#376349=CARTESIAN_POINT('Ctrl Pts',(-0.493751728365454,2.62463079031095,
8.85933012996512));
#376350=CARTESIAN_POINT('',(-0.527270584603676,2.61810299364327,8.85933012996512));
#376351=CARTESIAN_POINT('Origin',(-0.512285570880968,2.63047812393962,8.84999761231045));
#376352=CARTESIAN_POINT('',(-0.572927672898306,2.67318409147408,8.79610912703474));
#376353=CARTESIAN_POINT('Ctrl Pts',(-0.527270584603676,2.61810299364327,
8.85933012996512));
#376354=CARTESIAN_POINT('Ctrl Pts',(-0.531261650785743,2.62291757984128,
8.8538223528706));
#376355=CARTESIAN_POINT('Ctrl Pts',(-0.535251115468821,2.62773030595809,
8.84831178811348));
#376356=CARTESIAN_POINT('Ctrl Pts',(-0.539239009257411,2.63254120786596,
8.84279849653635));
#376357=CARTESIAN_POINT('Ctrl Pts',(-0.550480814704906,2.64610305934508,
8.82725662040549));
#376358=CARTESIAN_POINT('Ctrl Pts',(-0.561710151375514,2.65965043198544,
8.81169306718667));
#376359=CARTESIAN_POINT('Ctrl Pts',(-0.572927672898306,2.67318409147408,
8.79610912703474));
#376360=CARTESIAN_POINT('',(-0.643661112117194,2.6570396455512,8.79610912703474));
#376361=CARTESIAN_POINT('Origin',(0.,1.84795814293585E-15,8.79610912703474));
#376362=CARTESIAN_POINT('',(-0.660897934588195,2.58760342300925,8.85933012996512));
#376363=CARTESIAN_POINT('Ctrl Pts',(-0.643661112117194,2.6570396455512,
8.79610912703474));
#376364=CARTESIAN_POINT('Ctrl Pts',(-0.645163285982008,2.65098763854848,
8.80163734024559));
#376365=CARTESIAN_POINT('Ctrl Pts',(-0.6466660505991,2.64493343204505,8.80716298614018));
#376366=CARTESIAN_POINT('Ctrl Pts',(-0.648169417172601,2.63887698357279,
8.8126860086129));
#376367=CARTESIAN_POINT('Ctrl Pts',(-0.652407382263267,2.62180395717242,
8.82825531609049));
#376368=CARTESIAN_POINT('Ctrl Pts',(-0.656650133709119,2.60471310309576,
8.84380379913848));
#376369=CARTESIAN_POINT('Ctrl Pts',(-0.660897934588195,2.58760342300925,
8.85933012996512));
#376370=CARTESIAN_POINT('',(-0.693929685372903,2.57894147790724,8.85933012996512));
#376371=CARTESIAN_POINT('Origin',(-0.679768337288401,2.59225127529679,8.84999761231047));
#376372=CARTESIAN_POINT('',(-0.743022024337723,2.63098414602442,8.79610912703474));
#376373=CARTESIAN_POINT('Ctrl Pts',(-0.693929685372903,2.57894147790724,
8.85933012996512));
#376374=CARTESIAN_POINT('Ctrl Pts',(-0.698221023078281,2.58349046353331,
8.8538223528706));
#376375=CARTESIAN_POINT('Ctrl Pts',(-0.702510643399309,2.5880376955083,
8.84831178811348));
#376376=CARTESIAN_POINT('Ctrl Pts',(-0.706798579175954,2.59258320766994,
8.84279849653635));
#376377=CARTESIAN_POINT('Ctrl Pts',(-0.718886197936089,2.60539692992268,
8.82725662040549));
#376378=CARTESIAN_POINT('Ctrl Pts',(-0.730960445875394,2.61819700196228,
8.81169306718667));
#376379=CARTESIAN_POINT('Ctrl Pts',(-0.743022024337723,2.63098414602442,
8.79610912703474));
#376380=CARTESIAN_POINT('',(-0.812575755917853,2.61034096358642,8.79610912703474));
#376381=CARTESIAN_POINT('Origin',(0.,1.84795814293585E-15,8.79610912703474));
#376382=CARTESIAN_POINT('',(-0.825328369435551,2.53994303820322,8.85933012996512));
#376383=CARTESIAN_POINT('Ctrl Pts',(-0.812575755917853,2.61034096358642,
8.79610912703474));
#376384=CARTESIAN_POINT('Ctrl Pts',(-0.813687089985364,2.6042051464712,
8.80163734024559));
#376385=CARTESIAN_POINT('Ctrl Pts',(-0.814798872668896,2.59806709652475,
8.80716298614018));
#376386=CARTESIAN_POINT('Ctrl Pts',(-0.815911112428618,2.59192677064835,
8.8126860086129));
#376387=CARTESIAN_POINT('Ctrl Pts',(-0.819046497608276,2.57461729525617,
8.82825531609049));
#376388=CARTESIAN_POINT('Ctrl Pts',(-0.822185517085898,2.55728972215373,
8.84380379913848));
#376389=CARTESIAN_POINT('Ctrl Pts',(-0.825328369435551,2.53994303820322,
8.85933012996512));
#376390=CARTESIAN_POINT('',(-0.857737280217481,2.52918253845729,8.85933012996512));
#376391=CARTESIAN_POINT('Origin',(-0.844457789788063,2.54337231012762,8.84999761231047));
#376392=CARTESIAN_POINT('',(-0.910063138901412,2.57797292237441,8.79610912703474));
#376393=CARTESIAN_POINT('Ctrl Pts',(-0.857737280217481,2.52918253845729,
8.85933012996512));
#376394=CARTESIAN_POINT('Ctrl Pts',(-0.86231125541905,2.53344723075372,
8.8538223528706));
#376395=CARTESIAN_POINT('Ctrl Pts',(-0.866883404408009,2.53771028303531,
8.84831178811348));
#376396=CARTESIAN_POINT('Ctrl Pts',(-0.871453762124842,2.54197172696625,
8.84279849653635));
#376397=CARTESIAN_POINT('Ctrl Pts',(-0.884337523579347,2.55398466565935,
8.82725662040549));
#376398=CARTESIAN_POINT('Ctrl Pts',(-0.897207067112648,2.56598483885656,
8.81169306718667));
#376399=CARTESIAN_POINT('Ctrl Pts',(-0.910063138901412,2.57797292237441,
8.79610912703474));
#376400=CARTESIAN_POINT('',(-0.978151351640492,2.55291583068589,8.79610912703474));
#376401=CARTESIAN_POINT('Origin',(0.,1.84795814293585E-15,8.79610912703474));
#376402=CARTESIAN_POINT('',(-0.986367352980517,2.48184548263713,8.85933012996512));
#376403=CARTESIAN_POINT('Ctrl Pts',(-0.978151351640492,2.55291583068589,
8.79610912703474));
#376404=CARTESIAN_POINT('Ctrl Pts',(-0.978867279200638,2.54672141684682,
8.80163734024559));
#376405=CARTESIAN_POINT('Ctrl Pts',(-0.979583511397086,2.54052474602118,
8.80716298614018));
#376406=CARTESIAN_POINT('Ctrl Pts',(-0.98030005391128,2.53432577465677,
8.8126860086129));
#376407=CARTESIAN_POINT('Ctrl Pts',(-0.982319975209689,2.51685097862003,
8.82825531609049));
#376408=CARTESIAN_POINT('Ctrl Pts',(-0.984342363814731,2.49935788920646,
8.84380379913848));
#376409=CARTESIAN_POINT('Ctrl Pts',(-0.986367352980517,2.48184548263713,
8.85933012996512));
#376410=CARTESIAN_POINT('',(-1.01802024859358,2.46903064544886,8.85933012996512));
#376411=CARTESIAN_POINT('Origin',(-1.00567718409386,2.48404208258451,8.84999761231045));
#376412=CARTESIAN_POINT('',(-1.07336460881942,2.51436825501291,8.79610912703474));
#376413=CARTESIAN_POINT('Ctrl Pts',(-1.01802024859358,2.46903064544886,
8.85933012996512));
#376414=CARTESIAN_POINT('Ctrl Pts',(-1.02285806584612,2.47299351988022,
8.8538223528706));
#376415=CARTESIAN_POINT('Ctrl Pts',(-1.02769395556209,2.47695487467219,
8.84831178811348));
#376416=CARTESIAN_POINT('Ctrl Pts',(-1.03252795463892,2.48091473918522,
8.84279849653635));
#376417=CARTESIAN_POINT('Ctrl Pts',(-1.04615491664841,2.49207753057683,
8.82725662040549));
#376418=CARTESIAN_POINT('Ctrl Pts',(-1.05976687206082,2.50322849364597,
8.81169306718667));
#376419=CARTESIAN_POINT('Ctrl Pts',(-1.07336460881942,2.51436825501291,
8.79610912703474));
#376420=CARTESIAN_POINT('',(-1.13970751364643,2.48500021903835,8.79610912703474));
#376421=CARTESIAN_POINT('Origin',(0.,1.84795814293585E-15,8.79610912703474));
#376422=CARTESIAN_POINT('',(-1.14335314149695,2.41354949162871,8.85933012996512));
#376423=CARTESIAN_POINT('Ctrl Pts',(-1.13970751364643,2.48500021903835,
8.79610912703474));
#376424=CARTESIAN_POINT('Ctrl Pts',(-1.1400250927993,2.47877266265059,8.80163734024559));
#376425=CARTESIAN_POINT('Ctrl Pts',(-1.14034283135694,2.47254283439536,
8.80716298614018));
#376426=CARTESIAN_POINT('Ctrl Pts',(-1.14066073219872,2.46631069044595,
8.8126860086129));
#376427=CARTESIAN_POINT('Ctrl Pts',(-1.14155688932599,2.4487423814499,8.82825531609049));
#376428=CARTESIAN_POINT('Ctrl Pts',(-1.14245433662987,2.43115565858184,
8.84380379913848));
#376429=CARTESIAN_POINT('Ctrl Pts',(-1.14335314149695,2.41354949162871,
8.85933012996512));
#376430=CARTESIAN_POINT('',(-1.17411995340354,2.39873297591287,8.85933012996512));
#376431=CARTESIAN_POINT('Origin',(-1.16276403513314,2.41450439329868,8.84999761231045));
#376432=CARTESIAN_POINT('',(-1.23225539332381,2.44043150916127,8.79610912703474));
#376433=CARTESIAN_POINT('Ctrl Pts',(-1.17411995340354,2.39873297591287,
8.85933012996512));
#376434=CARTESIAN_POINT('Ctrl Pts',(-1.17920173307826,2.4023777481781,8.8538223528706));
#376435=CARTESIAN_POINT('Ctrl Pts',(-1.1842814918131,2.40602112742389,8.84831178811348));
#376436=CARTESIAN_POINT('Ctrl Pts',(-1.18935926831082,2.40966314058634,
8.84279849653635));
#376437=CARTESIAN_POINT('Ctrl Pts',(-1.20367343476545,2.41992991437221,
8.82725662040549));
#376438=CARTESIAN_POINT('Ctrl Pts',(-1.21797186761242,2.43018584561415,
8.81169306718667));
#376439=CARTESIAN_POINT('Ctrl Pts',(-1.23225539332381,2.44043150916127,
8.79610912703474));
#376440=CARTESIAN_POINT('',(-1.29658037301231,2.4068732084599,8.79610912703474));
#376441=CARTESIAN_POINT('Origin',(0.,1.84795814293585E-15,8.79610912703474));
#376442=CARTESIAN_POINT('',(-1.2956406467065,2.33533570805444,8.85933012996512));
#376443=CARTESIAN_POINT('Ctrl Pts',(-1.29658037301231,2.4068732084599,8.79610912703474));
#376444=CARTESIAN_POINT('Ctrl Pts',(-1.29649829875704,2.40063809988846,
8.80163734024559));
#376445=CARTESIAN_POINT('Ctrl Pts',(-1.29641623801998,2.39440071390424,
8.80716298614018));
#376446=CARTESIAN_POINT('Ctrl Pts',(-1.29633419086659,2.38816100658611,
8.8126860086129));
#376447=CARTESIAN_POINT('Ctrl Pts',(-1.29610290132087,2.3705713765808,8.82825531609049));
#376448=CARTESIAN_POINT('Ctrl Pts',(-1.29587171952012,2.35296328787487,
8.84380379913848));
#376449=CARTESIAN_POINT('Ctrl Pts',(-1.2956406467065,2.33533570805444,8.85933012996512));
#376450=CARTESIAN_POINT('',(-1.32539494747703,2.31857839805224,8.85933012996512));
#376451=CARTESIAN_POINT('Origin',(-1.31507283933995,2.33504498755122,8.84999761231046));
#376452=CARTESIAN_POINT('',(-1.38608257609908,2.35646650676756,8.79610912703474));
#376453=CARTESIAN_POINT('Ctrl Pts',(-1.32539494747703,2.31857839805224,
8.85933012996512));
#376454=CARTESIAN_POINT('Ctrl Pts',(-1.3306998074512,2.3218900910003,8.8538223528706));
#376455=CARTESIAN_POINT('Ctrl Pts',(-1.33600256138667,2.32520052327309,
8.84831178811348));
#376456=CARTESIAN_POINT('Ctrl Pts',(-1.34130324963248,2.32850971927167,
8.84279849653635));
#376457=CARTESIAN_POINT('Ctrl Pts',(-1.35624580055189,2.3378382870761,8.82725662040549));
#376458=CARTESIAN_POINT('Ctrl Pts',(-1.37117195550585,2.34715704266947,
8.81169306718667));
#376459=CARTESIAN_POINT('Ctrl Pts',(-1.38608257609908,2.35646650676756,
8.79610912703474));
#376460=CARTESIAN_POINT('',(-1.44812530550985,2.3188558395952,8.79610912703474));
#376461=CARTESIAN_POINT('Origin',(0.,1.84795814293585E-15,8.79610912703474));
#376462=CARTESIAN_POINT('',(-1.44260408658468,2.24752552912783,8.85933012996512));
#376463=CARTESIAN_POINT('Ctrl Pts',(-1.44812530550985,2.3188558395952,8.79610912703474));
#376464=CARTESIAN_POINT('Ctrl Pts',(-1.44764391510717,2.31263880023862,
8.80163734024559));
#376465=CARTESIAN_POINT('Ctrl Pts',(-1.44716239228058,2.30641948728235,
8.80716298614018));
#376466=CARTESIAN_POINT('Ctrl Pts',(-1.44668073428138,2.30019785689127,
8.8126860086129));
#376467=CARTESIAN_POINT('Ctrl Pts',(-1.44532294848102,2.28265918543936,
8.82825531609049));
#376468=CARTESIAN_POINT('Ctrl Pts',(-1.44396408755124,2.26510208630897,
8.84380379913848));
#376469=CARTESIAN_POINT('Ctrl Pts',(-1.44260408658468,2.24752552912783,
8.85933012996512));
#376470=CARTESIAN_POINT('',(-1.47122360941501,2.22889628422051,8.85933012996512));
#376471=CARTESIAN_POINT('Origin',(-1.46197772716767,2.24599038108432,8.84999761231047));
#376472=CARTESIAN_POINT('',(-1.53421404825537,2.26281827803707,8.79610912703474));
#376473=CARTESIAN_POINT('Ctrl Pts',(-1.47122360941501,2.22889628422051,
8.85933012996512));
#376474=CARTESIAN_POINT('Ctrl Pts',(-1.47672975088111,2.23186128939472,
8.8538223528706));
#376475=CARTESIAN_POINT('Ctrl Pts',(-1.48223370986385,2.23482517141821,
8.84831178811348));
#376476=CARTESIAN_POINT('Ctrl Pts',(-1.48773552819275,2.23778795205675,
8.84279849653635));
#376477=CARTESIAN_POINT('Ctrl Pts',(-1.50324506143004,2.24613998079366,
8.82725662040549));
#376478=CARTESIAN_POINT('Ctrl Pts',(-1.51873760371865,2.25448326797286,
8.81169306718667));
#376479=CARTESIAN_POINT('Ctrl Pts',(-1.53421404825537,2.26281827803707,
8.79610912703474));
#376480=CARTESIAN_POINT('',(-1.59371958050516,2.22130979469259,8.79610912703474));
#376481=CARTESIAN_POINT('Origin',(0.,1.84795814293585E-15,8.79610912703474));
#376482=CARTESIAN_POINT('',(-1.58363955683347,2.15047978570932,8.85933012996512));
#376483=CARTESIAN_POINT('Ctrl Pts',(-1.59371958050516,2.22130979469259,
8.79610912703474));
#376484=CARTESIAN_POINT('Ctrl Pts',(-1.59284085209148,2.21513637169914,
8.80163734024559));
#376485=CARTESIAN_POINT('Ctrl Pts',(-1.59196184585595,2.20896068826178,
8.80716298614018));
#376486=CARTESIAN_POINT('Ctrl Pts',(-1.59108255624697,2.20278270081157,
8.8126860086129));
#376487=CARTESIAN_POINT('Ctrl Pts',(-1.58860385362506,2.1853670580761,8.82825531609049));
#376488=CARTESIAN_POINT('Ctrl Pts',(-1.58612289741729,2.16793309440755,
8.84380379913848));
#376489=CARTESIAN_POINT('Ctrl Pts',(-1.58363955683347,2.15047978570932,
8.85933012996512));
#376490=CARTESIAN_POINT('',(-1.61100669796544,2.13005515746016,8.85933012996512));
#376491=CARTESIAN_POINT('Origin',(-1.60287503492123,2.14770651837814,8.84999761231046));
#376492=CARTESIAN_POINT('',(-1.6760411057995,2.15987164362912,8.79610912703474));
#376493=CARTESIAN_POINT('Ctrl Pts',(-1.61100669796544,2.13005515746016,
8.85933012996512));
#376494=CARTESIAN_POINT('Ctrl Pts',(-1.61669149500712,2.13266129101827,
8.8538223528706));
#376495=CARTESIAN_POINT('Ctrl Pts',(-1.62237404208907,2.13526644356548,
8.84831178811348));
#376496=CARTESIAN_POINT('Ctrl Pts',(-1.62805438234941,2.13787063414281,
8.84279849653635));
#376497=CARTESIAN_POINT('Ctrl Pts',(-1.64406716590573,2.14521180353462,
8.82725662040549));
#376498=CARTESIAN_POINT('Ctrl Pts',(-1.66006243334957,2.152545337943,8.81169306718667));
#376499=CARTESIAN_POINT('Ctrl Pts',(-1.6760411057995,2.15987164362912,8.79610912703474));
#376500=CARTESIAN_POINT('',(-1.73276491989239,2.11463591137413,8.79610912703474));
#376501=CARTESIAN_POINT('Origin',(0.,1.84795814293585E-15,8.79610912703474));
#376502=CARTESIAN_POINT('',(-1.71816751245362,2.04459725957487,8.85933012996512));
#376503=CARTESIAN_POINT('Ctrl Pts',(-1.73276491989239,2.11463591137413,
8.79610912703474));
#376504=CARTESIAN_POINT('Ctrl Pts',(-1.73149246435126,2.10853147266309,
8.80163734024559));
#376505=CARTESIAN_POINT('Ctrl Pts',(-1.73021958673194,2.10242479595256,
8.80716298614018));
#376506=CARTESIAN_POINT('Ctrl Pts',(-1.7289462787028,2.09631583811883,8.8126860086129));
#376507=CARTESIAN_POINT('Ctrl Pts',(-1.7253568447801,2.07909478871143,8.82825531609049));
#376508=CARTESIAN_POINT('Ctrl Pts',(-1.72176398807556,2.06185560040102,
8.84380379913848));
#376509=CARTESIAN_POINT('Ctrl Pts',(-1.71816751245362,2.04459725957487,
8.85933012996512));
#376510=CARTESIAN_POINT('',(-1.74416981443406,2.02246117716241,8.85933012996512));
#376511=CARTESIAN_POINT('Origin',(-1.73718578534068,2.04059726890635,8.84999761231045));
#376512=CARTESIAN_POINT('',(-1.81098095093021,2.04804963334648,8.79610912703474));
#376513=CARTESIAN_POINT('Ctrl Pts',(-1.74416981443406,2.02246117716241,
8.85933012996512));
#376514=CARTESIAN_POINT('Ctrl Pts',(-1.7500099070009,2.02469772994261,8.8538223528706));
#376515=CARTESIAN_POINT('Ctrl Pts',(-1.7558476913772,2.02693344788292,8.84831178811348));
#376516=CARTESIAN_POINT('Ctrl Pts',(-1.76168321183243,2.02916834722137,
8.84279849653635));
#376517=CARTESIAN_POINT('Ctrl Pts',(-1.77813344574541,2.03546849082836,
8.82725662040549));
#376518=CARTESIAN_POINT('Ctrl Pts',(-1.79456571035958,2.04176213740001,
8.81169306718667));
#376519=CARTESIAN_POINT('Ctrl Pts',(-1.81098095093021,2.04804963334648,
8.79610912703474));
#376520=CARTESIAN_POINT('',(-1.86468995654687,1.99927253550785,8.79610912703474));
#376521=CARTESIAN_POINT('Origin',(0.,1.84795814293585E-15,8.79610912703474));
#376522=CARTESIAN_POINT('',(-1.84563514921932,1.93031304473609,8.85933012996512));
#376523=CARTESIAN_POINT('Ctrl Pts',(-1.86468995654687,1.99927253550785,
8.79610912703474));
#376524=CARTESIAN_POINT('Ctrl Pts',(-1.86302900267104,1.99326216552728,
8.80163734024559));
#376525=CARTESIAN_POINT('Ctrl Pts',(-1.86136748419512,1.98724958918807,
8.80716298614018));
#376526=CARTESIAN_POINT('Ctrl Pts',(-1.85970539004162,1.98123476398892,
8.8126860086129));
#376527=CARTESIAN_POINT('Ctrl Pts',(-1.85501997457205,1.96427907289552,
8.82825531609049));
#376528=CARTESIAN_POINT('Ctrl Pts',(-1.85032998118961,1.94730549946581,
8.84380379913848));
#376529=CARTESIAN_POINT('Ctrl Pts',(-1.84563514921932,1.93031304473609,
8.85933012996512));
#376530=CARTESIAN_POINT('',(-1.87016576301193,1.90655647007114,8.85933012996512));
#376531=CARTESIAN_POINT('Origin',(-1.86435806674296,1.92510276754984,8.84999761231048));
#376532=CARTESIAN_POINT('',(-1.93847908687936,1.92781174781516,8.79610912703474));
#376533=CARTESIAN_POINT('Ctrl Pts',(-1.87016576301193,1.90655647007114,
8.85933012996512));
#376534=CARTESIAN_POINT('Ctrl Pts',(-1.87613715291086,1.90841425159832,
8.8538223528706));
#376535=CARTESIAN_POINT('Ctrl Pts',(-1.88210618587332,1.91027134788715,
8.84831178811348));
#376536=CARTESIAN_POINT('Ctrl Pts',(-1.88807290711816,1.91212777230594,
8.84279849653635));
#376537=CARTESIAN_POINT('Ctrl Pts',(-1.9048929938481,1.91736100148667,8.82725662040549));
#376538=CARTESIAN_POINT('Ctrl Pts',(-1.92169473193259,1.92258889827783,
8.81169306718667));
#376539=CARTESIAN_POINT('Ctrl Pts',(-1.93847908687936,1.92781174781516,
8.79610912703474));
#376540=CARTESIAN_POINT('',(-1.98895258219516,1.87569371995056,8.79610912703474));
#376541=CARTESIAN_POINT('Origin',(0.,1.84795814293585E-15,8.79610912703474));
#376542=CARTESIAN_POINT('',(-1.96551867526938,1.80809675954563,8.85933012996512));
#376543=CARTESIAN_POINT('Ctrl Pts',(-1.98895258219516,1.87569371995056,
8.79610912703474));
#376544=CARTESIAN_POINT('Ctrl Pts',(-1.98690995520039,1.86980211659992,
8.80163734024559));
#376545=CARTESIAN_POINT('Ctrl Pts',(-1.98486662340367,1.86390834759791,
8.80716298614018));
#376546=CARTESIAN_POINT('Ctrl Pts',(-1.98282257302721,1.85801237124026,
8.8126860086129));
#376547=CARTESIAN_POINT('Ctrl Pts',(-1.97706042938795,1.84139171303254,
8.82825531609049));
#376548=CARTESIAN_POINT('Ctrl Pts',(-1.97129257151642,1.82475350253757,
8.84380379913848));
#376549=CARTESIAN_POINT('Ctrl Pts',(-1.96551867526938,1.80809675954563,
8.85933012996512));
#376550=CARTESIAN_POINT('',(-1.98847679932028,1.78281731348927,8.85933012996512));
#376551=CARTESIAN_POINT('Origin',(-1.98386930094549,1.80169760598827,8.84999761231044));
#376552=CARTESIAN_POINT('',(-2.05801159645805,1.79965207029774,8.79610912703474));
#376553=CARTESIAN_POINT('Ctrl Pts',(-1.98847679932028,1.78281731348927,
8.85933012996512));
#376554=CARTESIAN_POINT('Ctrl Pts',(-1.99455494882936,1.78428868974064,
8.8538223528706));
#376555=CARTESIAN_POINT('Ctrl Pts',(-2.00063070234117,1.78575953317099,
8.84831178811348));
#376556=CARTESIAN_POINT('Ctrl Pts',(-2.00670410583817,1.787229854224,8.84279849653635));
#376557=CARTESIAN_POINT('Ctrl Pts',(-2.0238249280408,1.79137466451723,8.82725662040549));
#376558=CARTESIAN_POINT('Ctrl Pts',(-2.04092709764985,1.79551532897861,
8.81169306718667));
#376559=CARTESIAN_POINT('Ctrl Pts',(-2.05801159645805,1.79965207029774,
8.79610912703474));
#376560=CARTESIAN_POINT('',(-2.10504217505422,1.74440727656295,8.79610912703474));
#376561=CARTESIAN_POINT('Origin',(0.,1.84795814293585E-15,8.79610912703474));
#376562=CARTESIAN_POINT('',(-2.07732546348033,1.67845061693467,8.85933012996512));
#376563=CARTESIAN_POINT('Ctrl Pts',(-2.10504217505422,1.74440727656295,
8.79610912703474));
#376564=CARTESIAN_POINT('Ctrl Pts',(-2.10262626853296,1.73865864970416,
8.80163734024559));
#376565=CARTESIAN_POINT('Ctrl Pts',(-2.10020951990409,1.73290790680038,
8.80716298614018));
#376566=CARTESIAN_POINT('Ctrl Pts',(-2.09779191274612,1.72715500711577,
8.8126860086129));
#376567=CARTESIAN_POINT('Ctrl Pts',(-2.09097671882137,1.71093767964342,
8.82825531609049));
#376568=CARTESIAN_POINT('Ctrl Pts',(-2.08415469782593,1.694703202059,8.84380379913848));
#376569=CARTESIAN_POINT('Ctrl Pts',(-2.07732546348033,1.67845061693467,
8.85933012996512));
#376570=CARTESIAN_POINT('',(-2.0986167579333,1.65175217815315,8.85933012996512));
#376571=CARTESIAN_POINT('Origin',(-2.09522839065177,1.67088888250074,8.84999761231044));
#376572=CARTESIAN_POINT('',(-2.1690872949448,1.66409723639931,8.79610912703474));
#376573=CARTESIAN_POINT('Ctrl Pts',(-2.0986167579333,1.65175217815315,8.85933012996512));
#376574=CARTESIAN_POINT('Ctrl Pts',(-2.10477669063242,1.65283110292808,
8.8538223528706));
#376575=CARTESIAN_POINT('Ctrl Pts',(-2.11093419811916,1.65390964948881,
8.84831178811348));
#376576=CARTESIAN_POINT('Ctrl Pts',(-2.11708932695062,1.65498782531144,
8.84279849653635));
#376577=CARTESIAN_POINT('Ctrl Pts',(-2.13444053149509,1.65802718480262,
8.82725662040549));
#376578=CARTESIAN_POINT('Ctrl Pts',(-2.15177285614539,1.66106360205579,
8.81169306718667));
#376579=CARTESIAN_POINT('Ctrl Pts',(-2.1690872949448,1.66409723639931,8.79610912703474));
#376580=CARTESIAN_POINT('',(-2.21248169808585,1.60595268950176,8.79610912703474));
#376581=CARTESIAN_POINT('Origin',(0.,1.84795814293585E-15,8.79610912703474));
#376582=CARTESIAN_POINT('',(-2.18059607577692,1.54190736071219,8.85933012996512));
#376583=CARTESIAN_POINT('Ctrl Pts',(-2.21248169808585,1.60595268950176,
8.79610912703474));
#376584=CARTESIAN_POINT('Ctrl Pts',(-2.20970243951622,1.60037066147566,
8.80163734024559));
#376585=CARTESIAN_POINT('Ctrl Pts',(-2.2069222049937,1.59478657570622,8.80716298614018));
#376586=CARTESIAN_POINT('Ctrl Pts',(-2.2041409755206,1.58920039259345,8.8126860086129));
#376587=CARTESIAN_POINT('Ctrl Pts',(-2.19630073640404,1.57345303633367,
8.82825531609049));
#376588=CARTESIAN_POINT('Ctrl Pts',(-2.18845258543229,1.55768900261048,
8.84380379913848));
#376589=CARTESIAN_POINT('Ctrl Pts',(-2.18059607577692,1.54190736071219,
8.85933012996512));
#376590=CARTESIAN_POINT('',(-2.20013305013607,1.51389963881728,8.85933012996512));
#376591=CARTESIAN_POINT('Origin',(-2.19797773747577,1.53321411819047,8.84999761231046));
#376592=CARTESIAN_POINT('',(-2.27124974846885,1.52170427000877,8.79610912703474));
#376593=CARTESIAN_POINT('Ctrl Pts',(-2.20013305013607,1.51389963881728,
8.85933012996512));
#376594=CARTESIAN_POINT('Ctrl Pts',(-2.20634945354049,1.51458167858244,
8.8538223528706));
#376595=CARTESIAN_POINT('Ctrl Pts',(-2.21256341248311,1.51526349629438,
8.84831178811348));
#376596=CARTESIAN_POINT('Ctrl Pts',(-2.21877497390438,1.51594509643091,
8.84279849653635));
#376597=CARTESIAN_POINT('Ctrl Pts',(-2.23628526096941,1.51786651573995,
8.82725662040549));
#376598=CARTESIAN_POINT('Ctrl Pts',(-2.25377651842119,1.51978620849509,
8.81169306718667));
#376599=CARTESIAN_POINT('Ctrl Pts',(-2.27124974846885,1.52170427000877,
8.79610912703474));
#376600=CARTESIAN_POINT('',(-2.31082965924421,1.46089889836363,8.79610912703474));
#376601=CARTESIAN_POINT('Origin',(0.,1.84795814293585E-15,8.79610912703474));
#376602=CARTESIAN_POINT('',(-2.27490615106175,1.39902807640646,8.85933012996512));
#376603=CARTESIAN_POINT('Ctrl Pts',(-2.31082965924421,1.46089889836363,
8.79610912703474));
#376604=CARTESIAN_POINT('Ctrl Pts',(-2.30769846919581,1.45550640692072,
8.80163734024559));
#376605=CARTESIAN_POINT('Ctrl Pts',(-2.30456617335966,1.45011192449184,
8.80716298614018));
#376606=CARTESIAN_POINT('Ctrl Pts',(-2.30143275023992,1.44471541277555,
8.8126860086129));
#376607=CARTESIAN_POINT('Ctrl Pts',(-2.2925996831558,1.429502736993,8.82825531609049));
#376608=CARTESIAN_POINT('Ctrl Pts',(-2.28375765194351,1.41427392492699,
8.84380379913848));
#376609=CARTESIAN_POINT('Ctrl Pts',(-2.27490615106175,1.39902807640646,
8.85933012996512));
#376610=CARTESIAN_POINT('',(-2.29260852370878,1.36982616113504,8.85933012996512));
#376611=CARTESIAN_POINT('Origin',(-2.29169512231175,1.38923904819517,8.84999761231045));
#376612=CARTESIAN_POINT('',(-2.36407914959491,1.37305829436823,8.79610912703474));
#376613=CARTESIAN_POINT('Ctrl Pts',(-2.29260852370878,1.36982616113504,
8.85933012996512));
#376614=CARTESIAN_POINT('Ctrl Pts',(-2.29885585328349,1.37010851324275,
8.8538223528706));
#376615=CARTESIAN_POINT('Ctrl Pts',(-2.30510072919181,1.37039080037067,
8.84831178811348));
#376616=CARTESIAN_POINT('Ctrl Pts',(-2.31134319856464,1.37067302397993,
8.84279849653635));
#376617=CARTESIAN_POINT('Ctrl Pts',(-2.32894061462472,1.37146860758275,
8.82725662040549));
#376618=CARTESIAN_POINT('Ctrl Pts',(-2.34651892954926,1.37226368741056,
8.81169306718667));
#376619=CARTESIAN_POINT('Ctrl Pts',(-2.36407914959491,1.37305829436823,
8.79610912703474));
#376620=CARTESIAN_POINT('',(-2.39968192566133,1.30984196029029,8.79610912703474));
#376621=CARTESIAN_POINT('Origin',(0.,1.84795814293585E-15,8.79610912703474));
#376622=CARTESIAN_POINT('',(-2.35986814900603,1.25039988564418,8.85933012996512));
#376623=CARTESIAN_POINT('Ctrl Pts',(-2.39968192566133,1.30984196029029,
8.79610912703474));
#376624=CARTESIAN_POINT('Ctrl Pts',(-2.39621167086571,1.3046611643346,8.80163734024559));
#376625=CARTESIAN_POINT('Ctrl Pts',(-2.39274018499139,1.29947845233169,
8.80716298614018));
#376626=CARTESIAN_POINT('Ctrl Pts',(-2.38926744413272,1.29429378743607,
8.8126860086129));
#376627=CARTESIAN_POINT('Ctrl Pts',(-2.37947784604839,1.27967830427866,
8.82825531609049));
#376628=CARTESIAN_POINT('Ctrl Pts',(-2.36967826839841,1.26504729232517,
8.84380379913848));
#376629=CARTESIAN_POINT('Ctrl Pts',(-2.35986814900603,1.25039988564418,
8.85933012996512));
#376630=CARTESIAN_POINT('',(-2.37566317709459,1.22012377392992,8.85933012996512));
#376631=CARTESIAN_POINT('Origin',(-2.3759954403231,1.23955529695999,8.84999761231045));
#376632=CARTESIAN_POINT('',(-2.44719404240189,1.21877012767605,8.79610912703474));
#376633=CARTESIAN_POINT('Ctrl Pts',(-2.37566317709459,1.22012377392992,
8.85933012996512));
#376634=CARTESIAN_POINT('Ctrl Pts',(-2.38191576122232,1.2200052781348,8.8538223528706));
#376635=CARTESIAN_POINT('Ctrl Pts',(-2.3881658925617,1.21988687470034,8.84831178811348));
#376636=CARTESIAN_POINT('Ctrl Pts',(-2.39441361824043,1.21976856206498,
8.84279849653635));
#376637=CARTESIAN_POINT('Ctrl Pts',(-2.41202585173835,1.2194350407379,8.82725662040549));
#376638=CARTESIAN_POINT('Ctrl Pts',(-2.42961899106907,1.21910224048483,
8.81169306718667));
#376639=CARTESIAN_POINT('Ctrl Pts',(-2.44719404240189,1.21877012767605,
8.79610912703474));
#376640=CARTESIAN_POINT('',(-2.47867338431574,1.1534026006419,8.79610912703474));
#376641=CARTESIAN_POINT('Origin',(0.,1.84795814293585E-15,8.79610912703474));
#376642=CARTESIAN_POINT('',(-2.43513294253591,1.09663353354187,8.85933012996512));
#376643=CARTESIAN_POINT('Ctrl Pts',(-2.47867338431574,1.1534026006419,8.79610912703474));
#376644=CARTESIAN_POINT('Ctrl Pts',(-2.47487832479423,1.14845478917528,
8.80163734024559));
#376645=CARTESIAN_POINT('Ctrl Pts',(-2.47108191396184,1.14350514447366,
8.80716298614018));
#376646=CARTESIAN_POINT('Ctrl Pts',(-2.46728412560132,1.13855363129887,
8.8126860086129));
#376647=CARTESIAN_POINT('Ctrl Pts',(-2.45657822407516,1.12459539892189,
8.82825531609049));
#376648=CARTESIAN_POINT('Ctrl Pts',(-2.44586136855407,1.11062230904738,
8.84380379913848));
#376649=CARTESIAN_POINT('Ctrl Pts',(-2.43513294253591,1.09663353354187,
8.85933012996512));
#376650=CARTESIAN_POINT('',(-2.44895572090756,1.06540763642198,8.85933012996512));
#376651=CARTESIAN_POINT('Origin',(-2.4505322834207,1.08477794712582,8.84999761231048));
#376652=CARTESIAN_POINT('',(-2.52025288996716,1.05947377310387,8.79610912703474));
#376653=CARTESIAN_POINT('Ctrl Pts',(-2.44895572090756,1.06540763642198,
8.85933012996512));
#376654=CARTESIAN_POINT('Ctrl Pts',(-2.45518786637895,1.06488877964867,
8.8538223528706));
#376655=CARTESIAN_POINT('Ctrl Pts',(-2.46141757001908,1.06437017219694,
8.84831178811348));
#376656=CARTESIAN_POINT('Ctrl Pts',(-2.46764487875876,1.06385180948897,
8.84279849653635));
#376657=CARTESIAN_POINT('Ctrl Pts',(-2.48519955724926,1.06239055374266,
8.82725662040549));
#376658=CARTESIAN_POINT('Ctrl Pts',(-2.50273522700294,1.06093124095634,
8.81169306718667));
#376659=CARTESIAN_POINT('Ctrl Pts',(-2.52025288996716,1.05947377310387,
8.79610912703474));
#376660=CARTESIAN_POINT('',(-2.54747944236023,0.992223662303395,8.79610912703474));
#376661=CARTESIAN_POINT('Origin',(0.,1.84795814293585E-15,8.79610912703474));
#376662=CARTESIAN_POINT('',(-2.50039125247054,0.93836087902307,8.85933012996512));
#376663=CARTESIAN_POINT('Ctrl Pts',(-2.54747944236023,0.992223662303395,
8.79610912703474));
#376664=CARTESIAN_POINT('Ctrl Pts',(-2.54337517282644,0.987529166944465,
8.80163734024559));
#376665=CARTESIAN_POINT('Ctrl Pts',(-2.5392694373024,0.982832928695902,
8.80716298614018));
#376666=CARTESIAN_POINT('Ctrl Pts',(-2.53516220736704,0.978134914071679,
8.8126860086129));
#376667=CARTESIAN_POINT('Ctrl Pts',(-2.52358399524484,0.964891289846006,
8.82825531609049));
#376668=CARTESIAN_POINT('Ctrl Pts',(-2.51199389971072,0.951633540473991,
8.84380379913848));
#376669=CARTESIAN_POINT('Ctrl Pts',(-2.50039125247054,0.93836087902307,
8.85933012996512));
#376670=CARTESIAN_POINT('',(-2.51218498036397,0.90631351040677,8.85933012996512));
#376671=CARTESIAN_POINT('Origin',(-2.51499936372825,0.925543012022779,8.84999761231046));
#376672=CARTESIAN_POINT('',(-2.58295547781501,0.895823813541599,8.79610912703474));
#376673=CARTESIAN_POINT('Ctrl Pts',(-2.51218498036397,0.90631351040677,
8.85933012996512));
#376674=CARTESIAN_POINT('Ctrl Pts',(-2.51837107795648,0.905396424749042,
8.8538223528706));
#376675=CARTESIAN_POINT('Ctrl Pts',(-2.52455475470884,0.904479744349307,
8.84831178811348));
#376676=CARTESIAN_POINT('Ctrl Pts',(-2.53073605716211,0.903563461632275,
8.84279849653635));
#376677=CARTESIAN_POINT('Ctrl Pts',(-2.5481610447058,0.900980476080039,
8.82725662040549));
#376678=CARTESIAN_POINT('Ctrl Pts',(-2.56556718705404,0.898400647389714,
8.81169306718667));
#376679=CARTESIAN_POINT('Ctrl Pts',(-2.58295547781501,0.895823813541599,
8.79610912703474));
#376680=CARTESIAN_POINT('',(-2.60581736094344,0.826967464105174,8.79610912703474));
#376681=CARTESIAN_POINT('Origin',(0.,1.84795814293585E-15,8.79610912703474));
#376682=CARTESIAN_POINT('',(-2.55537491841652,0.77623229837459,8.85933012996512));
#376683=CARTESIAN_POINT('Ctrl Pts',(-2.60581736094344,0.826967464105174,
8.79610912703474));
#376684=CARTESIAN_POINT('Ctrl Pts',(-2.60142074672124,0.822545575542333,
8.80163734024559));
#376685=CARTESIAN_POINT('Ctrl Pts',(-2.59702255785351,0.818122041597128,
8.80716298614018));
#376686=CARTESIAN_POINT('Ctrl Pts',(-2.59262276383209,0.813696830673282,
8.8126860086129));
#376687=CARTESIAN_POINT('Ctrl Pts',(-2.58021981847098,0.801222235491608,
8.82825531609049));
#376688=CARTESIAN_POINT('Ctrl Pts',(-2.56780410911246,0.788734305558035,
8.84380379913848));
#376689=CARTESIAN_POINT('Ctrl Pts',(-2.55537491841652,0.77623229837459,
8.85933012996512));
#376690=CARTESIAN_POINT('',(-2.56509113287407,0.743495147773657,8.85933012996512));
#376691=CARTESIAN_POINT('Origin',(-2.56913177218455,0.762504822154984,8.84999761231045));
#376692=CARTESIAN_POINT('',(-2.6350441475623,0.72849272177588,8.79610912703474));
#376693=CARTESIAN_POINT('Ctrl Pts',(-2.56509113287407,0.743495147773657,
8.85933012996512));
#376694=CARTESIAN_POINT('Ctrl Pts',(-2.57120576258579,0.742183601733196,
8.8538223528706));
#376695=CARTESIAN_POINT('Ctrl Pts',(-2.5773180023962,0.740872615221843,
8.84831178811348));
#376696=CARTESIAN_POINT('Ctrl Pts',(-2.58342789826539,0.739562177697975,
8.84279849653635));
#376697=CARTESIAN_POINT('Ctrl Pts',(-2.60065159185081,0.735868076381495,
8.82725662040549));
#376698=CARTESIAN_POINT('Ctrl Pts',(-2.61785668122109,0.732178332856633,
8.81169306718667));
#376699=CARTESIAN_POINT('Ctrl Pts',(-2.6350441475623,0.72849272177588,8.79610912703474));
#376700=CARTESIAN_POINT('',(-2.65344741704446,0.65831307921298,8.79610912703474));
#376701=CARTESIAN_POINT('Origin',(0.,1.84795814293585E-15,8.79610912703474));
#376702=CARTESIAN_POINT('',(-2.59985800069653,0.610914012710784,8.85933012996512));
#376703=CARTESIAN_POINT('Ctrl Pts',(-2.65344741704446,0.65831307921298,
8.79610912703474));
#376704=CARTESIAN_POINT('Ctrl Pts',(-2.64877652476476,0.654181967934824,
8.80163734024559));
#376705=CARTESIAN_POINT('Ctrl Pts',(-2.6441039556548,0.650049315542805,
8.80716298614018));
#376706=CARTESIAN_POINT('Ctrl Pts',(-2.63942967724473,0.645915092460226,
8.8126860086129));
#376707=CARTESIAN_POINT('Ctrl Pts',(-2.62625296500761,0.634260787109944,
8.82825531609049));
#376708=CARTESIAN_POINT('Ctrl Pts',(-2.6130626606376,0.622593992197563,
8.84380379913848));
#376709=CARTESIAN_POINT('Ctrl Pts',(-2.59985800069653,0.610914012710784,
8.85933012996512));
#376710=CARTESIAN_POINT('',(-2.60745677570887,0.577621604099134,8.85933012996512));
#376711=CARTESIAN_POINT('Origin',(-2.61270706711189,0.596333336416169,8.84999761231047));
#376712=CARTESIAN_POINT('',(-2.67630485569206,0.558168097155184,8.79610912703474));
#376713=CARTESIAN_POINT('Ctrl Pts',(-2.60745677570887,0.577621604099134,
8.85933012996512));
#376714=CARTESIAN_POINT('Ctrl Pts',(-2.61347481121473,0.575920987099945,
8.8538223528706));
#376715=CARTESIAN_POINT('Ctrl Pts',(-2.61949049757874,0.574221081601754,
8.84831178811348));
#376716=CARTESIAN_POINT('Ctrl Pts',(-2.62550387999116,0.572521874139925,
8.84279849653635));
#376717=CARTESIAN_POINT('Ctrl Pts',(-2.64245550376689,0.567731836913893,
8.82725662040549));
#376718=CARTESIAN_POINT('Ctrl Pts',(-2.65938884075651,0.562947340502084,
8.81169306718667));
#376719=CARTESIAN_POINT('Ctrl Pts',(-2.67630485569206,0.558168097155184,
8.79610912703474));
#376720=CARTESIAN_POINT('',(-2.69017388854615,0.486953544670587,8.79610912703474));
#376721=CARTESIAN_POINT('Origin',(0.,1.84795814293585E-15,8.79610912703474));
#376722=CARTESIAN_POINT('',(-2.63365770878388,0.443085350328103,8.85933012996512));
#376723=CARTESIAN_POINT('Ctrl Pts',(-2.69017388854615,0.486953544670587,
8.79610912703474));
#376724=CARTESIAN_POINT('Ctrl Pts',(-2.68524791190724,0.483130186299479,
8.80163734024559));
#376725=CARTESIAN_POINT('Ctrl Pts',(-2.68032016314379,0.479305397415775,
8.80716298614018));
#376726=CARTESIAN_POINT('Ctrl Pts',(-2.67539060795767,0.475479150583897,
8.8126860086129));
#376727=CARTESIAN_POINT('Ctrl Pts',(-2.66149427478153,0.464693025105533,
8.82825531609049));
#376728=CARTESIAN_POINT('Ctrl Pts',(-2.64758357718999,0.453895306577159,
8.84380379913848));
#376729=CARTESIAN_POINT('Ctrl Pts',(-2.63365770878388,0.443085350328103,
8.85933012996512));
#376730=CARTESIAN_POINT('',(-2.63910781935455,0.409374489353921,8.85933012996512));
#376731=CARTESIAN_POINT('Origin',(-2.64554618827658,0.427711389084935,8.84999761231045));
#376732=CARTESIAN_POINT('',(-2.7065680531042,0.385549840096597,8.79610912703474));
#376733=CARTESIAN_POINT('Ctrl Pts',(-2.63910781935455,0.409374489353921,
8.85933012996512));
#376734=CARTESIAN_POINT('Ctrl Pts',(-2.6450045312558,0.407291789596035,
8.8538223528706));
#376735=CARTESIAN_POINT('Ctrl Pts',(-2.65089894442778,0.405209950387328,
8.84831178811348));
#376736=CARTESIAN_POINT('Ctrl Pts',(-2.65679110310522,0.403128955395477,
8.84279849653635));
#376737=CARTESIAN_POINT('Ctrl Pts',(-2.67340099921306,0.397262665550314,
8.82725662040549));
#376738=CARTESIAN_POINT('Ctrl Pts',(-2.68999300110814,0.391403076773586,
8.81169306718667));
#376739=CARTESIAN_POINT('Ctrl Pts',(-2.7065680531042,0.385549840096597,
8.79610912703474));
#376740=CARTESIAN_POINT('',(-2.71584585849932,0.313593013561936,8.79610912703474));
#376741=CARTESIAN_POINT('Origin',(0.,1.84795814293585E-15,8.79610912703474));
#376742=CARTESIAN_POINT('',(-2.65663515242803,0.273435955199415,8.85933012996512));
#376743=CARTESIAN_POINT('Ctrl Pts',(-2.71584585849932,0.313593013561936,
8.79610912703474));
#376744=CARTESIAN_POINT('Ctrl Pts',(-2.71068503939582,0.310093119097529,
8.80163734024559));
#376745=CARTESIAN_POINT('Ctrl Pts',(-2.70552236015554,0.306591910600078,
8.80716298614018));
#376746=CARTESIAN_POINT('Ctrl Pts',(-2.70035778479303,0.303089362887862,
8.8126860086129));
#376747=CARTESIAN_POINT('Ctrl Pts',(-2.68579893369164,0.293215739784622,
8.82825531609049));
#376748=CARTESIAN_POINT('Ctrl Pts',(-2.67122500491882,0.283331467781791,
8.84380379913848));
#376749=CARTESIAN_POINT('Ctrl Pts',(-2.65663515242803,0.273435955199415,
8.85933012996512));
#376750=CARTESIAN_POINT('',(-2.65991420288366,0.239445167021401,8.85933012996512));
#376751=CARTESIAN_POINT('Origin',(-2.66751419268574,0.257331883912138,8.84999761231047));
#376752=CARTESIAN_POINT('',(-2.7257093818291,0.211347276044871,8.79610912703474));
#376753=CARTESIAN_POINT('Ctrl Pts',(-2.65991420288366,0.239445167021401,
8.85933012996512));
#376754=CARTESIAN_POINT('Ctrl Pts',(-2.66566536032624,0.236988942764861,
8.8538223528706));
#376755=CARTESIAN_POINT('Ctrl Pts',(-2.67141427889812,0.234533724569499,
8.84831178811348));
#376756=CARTESIAN_POINT('Ctrl Pts',(-2.67716100169672,0.23207949330242,
8.84279849653635));
#376757=CARTESIAN_POINT('Ctrl Pts',(-2.69336091651076,0.225161056681414,
8.82725662040549));
#376758=CARTESIAN_POINT('Ctrl Pts',(-2.70954340321653,0.218250453846929,
8.81169306718667));
#376759=CARTESIAN_POINT('Ctrl Pts',(-2.7257093818291,0.211347276044871,
8.79610912703474));
#376760=CARTESIAN_POINT('',(-2.73035783527281,0.138943861495067,8.79610912703474));
#376761=CARTESIAN_POINT('Origin',(0.,1.84795814293585E-15,8.79610912703474));
#376762=CARTESIAN_POINT('',(-2.66869591238441,0.102662953078985,8.85933012996512));
#376763=CARTESIAN_POINT('Ctrl Pts',(-2.73035783527281,0.138943861495067,
8.79610912703474));
#376764=CARTESIAN_POINT('Ctrl Pts',(-2.72498338061741,0.135781812754442,
8.80163734024559));
#376765=CARTESIAN_POINT('Ctrl Pts',(-2.71960698545669,0.132618571859967,
8.80716298614018));
#376766=CARTESIAN_POINT('Ctrl Pts',(-2.71422861226575,0.129454115987256,
8.8126860086129));
#376767=CARTESIAN_POINT('Ctrl Pts',(-2.69906706868114,0.120533568094357,
8.82825531609049));
#376768=CARTESIAN_POINT('Ctrl Pts',(-2.68388979612647,0.111603359210898,
8.84380379913848));
#376769=CARTESIAN_POINT('Ctrl Pts',(-2.66869591238441,0.102662953078985,
8.85933012996512));
#376770=CARTESIAN_POINT('',(-2.66979042840332,0.0685319131367625,8.85933012996512));
#376771=CARTESIAN_POINT('Origin',(-2.67852080909719,0.0858949468308337,
8.84999761231045));
#376772=CARTESIAN_POINT('Ctrl Pts',(-2.66979042840332,0.0685319131367625,
8.85933012996512));
#376773=CARTESIAN_POINT('Ctrl Pts',(-2.67537239864768,0.0657122575338965,
8.8538223528706));
#376774=CARTESIAN_POINT('Ctrl Pts',(-2.6809521990799,0.0628937493700869,
8.84831178811348));
#376775=CARTESIAN_POINT('Ctrl Pts',(-2.68652987148302,0.0600763667904869,
8.84279849653635));
#376776=CARTESIAN_POINT('Ctrl Pts',(-2.7022532360784,0.0521342127337157,
8.82725662040549));
#376777=CARTESIAN_POINT('Ctrl Pts',(-2.71795971028587,0.0442009929908397,
8.81169306718667));
#376778=CARTESIAN_POINT('Ctrl Pts',(-2.73365018604124,0.0362762407020289,
8.79610912703474));
#376779=CARTESIAN_POINT('Origin',(0.,1.73472347597681E-15,8.945));
#376780=CARTESIAN_POINT('',(-2.50721825406948,1.42767779501581E-15,9.));
#376781=CARTESIAN_POINT('Origin',(0.,1.84795814293585E-15,9.));
#376782=CARTESIAN_POINT('Origin',(-2.50721825406948,1.42767779501581E-15,
8.945));
#376783=CARTESIAN_POINT('Origin',(0.,1.84795814293585E-15,9.));
#376784=CARTESIAN_POINT('',(2.74983646666349,-0.0299901084967912,8.75721825406948));
#376785=CARTESIAN_POINT('',(2.74983646666349,0.0299901084968513,8.75721825406948));
#376786=CARTESIAN_POINT('Origin',(0.,1.84795814293585E-15,8.75721825406948));
#376787=CARTESIAN_POINT('',(2.74983646666349,-0.0299901084967912,7.51860402984325));
#376788=CARTESIAN_POINT('',(2.74983646666349,-0.0299901084967912,9.));
#376789=CARTESIAN_POINT('',(2.74956360331414,-0.0489897063694301,7.49482233047033));
#376790=CARTESIAN_POINT('Origin',(2.74937751092705,-0.0583021276914146,
7.53025004711371));
#376791=CARTESIAN_POINT('',(2.74705311126524,-0.127276093151676,7.49482233047033));
#376792=CARTESIAN_POINT('Origin',(1.8470086919802E-15,-5.92299737674606E-17,
7.49482233047033));
#376793=CARTESIAN_POINT('',(2.74610810557233,-0.146254136727608,7.51860402984325));
#376794=CARTESIAN_POINT('Origin',(2.74746646844579,-0.117918295378179,7.5303083625674));
#376795=CARTESIAN_POINT('',(2.74610810557233,-0.146254136727603,8.75721825406948));
#376796=CARTESIAN_POINT('',(2.74610810557234,-0.146254136727603,9.));
#376797=CARTESIAN_POINT('',(2.74226515987506,-0.206111117932571,8.75721825406948));
#376798=CARTESIAN_POINT('Origin',(0.,1.84795814293585E-15,8.75721825406948));
#376799=CARTESIAN_POINT('',(2.74226515987506,-0.206111117932571,7.51860402984325));
#376800=CARTESIAN_POINT('',(2.74226515987506,-0.206111117932571,9.));
#376801=CARTESIAN_POINT('',(2.74077554873748,-0.225054196678863,7.49482233047033));
#376802=CARTESIAN_POINT('Origin',(2.7399931898145,-0.234335561652256,7.53025004711365));
#376803=CARTESIAN_POINT('',(2.73325438874111,-0.303018887905443,7.49482233047033));
#376804=CARTESIAN_POINT('Origin',(1.83941893708273E-15,-1.77446532635421E-16,
7.49482233047033));
#376805=CARTESIAN_POINT('',(2.73109539723704,-0.321897392332831,7.51860402984325));
#376806=CARTESIAN_POINT('Origin',(2.73426645279687,-0.293706800616635,7.53030836256733));
#376807=CARTESIAN_POINT('',(2.73109539723704,-0.321897392332826,8.75721825406948));
#376808=CARTESIAN_POINT('',(2.73109539723704,-0.321897392332826,9.));
#376809=CARTESIAN_POINT('',(2.72342529733067,-0.381385172574072,8.75721825406948));
#376810=CARTESIAN_POINT('Origin',(0.,1.84795814293585E-15,8.75721825406948));
#376811=CARTESIAN_POINT('',(2.72342529733067,-0.381385172574072,7.51860402984325));
#376812=CARTESIAN_POINT('',(2.72342529733067,-0.381385172574073,9.));
#376813=CARTESIAN_POINT('',(2.72072505953655,-0.40019389102017,7.49482233047033));
#376814=CARTESIAN_POINT('Origin',(2.7193496489583,-0.409406060525646,7.53025004711384));
#376815=CARTESIAN_POINT('',(2.70822413765242,-0.477516513051461,7.49482233047033));
#376816=CARTESIAN_POINT('Origin',(1.82427061521867E-15,-2.94933925638621E-16,
7.49482233047033));
#376817=CARTESIAN_POINT('',(2.70486003209637,-0.496217902506188,7.51860402984325));
#376818=CARTESIAN_POINT('Origin',(2.70983074979512,-0.46828840161129,7.53030836256747));
#376819=CARTESIAN_POINT('',(2.70486003209637,-0.496217902506183,8.75721825406948));
#376820=CARTESIAN_POINT('',(2.70486003209637,-0.496217902506183,9.));
#376821=CARTESIAN_POINT('',(2.69339429606666,-0.555092033734601,8.75721825406948));
#376822=CARTESIAN_POINT('Origin',(0.,1.84795814293585E-15,8.75721825406948));
#376823=CARTESIAN_POINT('',(2.69339429606666,-0.555092033734601,7.51860402984325));
#376824=CARTESIAN_POINT('',(2.69339429606666,-0.555092033734602,9.));
#376825=CARTESIAN_POINT('',(2.68949452747228,-0.573689102821954,7.49482233047033));
#376826=CARTESIAN_POINT('Origin',(2.6875317170959,-0.582794222078666,7.53025004711359));
#376827=CARTESIAN_POINT('',(2.67206521266985,-0.650051920418378,7.49482233047033));
#376828=CARTESIAN_POINT('Origin',(1.80162597409185E-15,-4.11209371878242E-16,
7.49482233047033));
#376829=CARTESIAN_POINT('',(2.66750981689316,-0.668499346879738,7.51860402984325));
#376830=CARTESIAN_POINT('Origin',(2.67425977098555,-0.640945705116414,7.53030836256731));
#376831=CARTESIAN_POINT('',(2.66750981689316,-0.668499346879733,8.75721825406948));
#376832=CARTESIAN_POINT('',(2.66750981689316,-0.668499346879733,9.));
#376833=CARTESIAN_POINT('',(2.65229555990884,-0.72651790266165,8.75721825406948));
#376834=CARTESIAN_POINT('Origin',(0.,1.84795814293585E-15,8.75721825406948));
#376835=CARTESIAN_POINT('',(2.65229555990884,-0.72651790266165,7.51860402984325));
#376836=CARTESIAN_POINT('',(2.65229555990884,-0.72651790266165,9.));
#376837=CARTESIAN_POINT('',(2.64721228549987,-0.744826903044317,7.49482233047033));
#376838=CARTESIAN_POINT('Origin',(2.64467014093421,-0.7537875571643,7.53025004711347));
#376839=CARTESIAN_POINT('',(2.62492619857224,-0.819916125008598,7.49482233047033));
#376840=CARTESIAN_POINT('Origin',(1.77157806538993E-15,-5.25795070604684E-16,
7.49482233047033));
#376841=CARTESIAN_POINT('',(2.61919823167327,-0.838033784044301,7.51860402984325));
#376842=CARTESIAN_POINT('Origin',(2.62769968515011,-0.810969225236613,7.53030836256735));
#376843=CARTESIAN_POINT('',(2.61919823167327,-0.838033784044296,8.75721825406948));
#376844=CARTESIAN_POINT('',(2.61919823167328,-0.838033784044296,9.));
#376845=CARTESIAN_POINT('',(2.60029797237974,-0.894958353689057,8.75721825406948));
#376846=CARTESIAN_POINT('Origin',(0.,1.84795814293585E-15,8.75721825406948));
#376847=CARTESIAN_POINT('',(2.60029797237974,-0.894958353689057,7.51860402984325));
#376848=CARTESIAN_POINT('',(2.60029797237974,-0.894958353689057,9.));
#376849=CARTESIAN_POINT('',(2.59405208042108,-0.912904049757199,7.49482233047033));
#376850=CARTESIAN_POINT('Origin',(2.59094104788344,-0.921683417490723,7.53025004711346));
#376851=CARTESIAN_POINT('',(2.56700079967978,-0.986411118369699,7.49482233047033));
#376852=CARTESIAN_POINT('Origin',(1.73425036241502E-15,-6.38220164603321E-16,
7.49482233047033));
#376853=CARTESIAN_POINT('',(2.56012379910318,-1.00412456063254,7.51860402984325));
#376854=CARTESIAN_POINT('Origin',(2.57034181766862,-0.977660298857871,7.53030836256752));
#376855=CARTESIAN_POINT('',(2.56012379910319,-1.00412456063254,8.75721825406948));
#376856=CARTESIAN_POINT('',(2.56012379910319,-1.00412456063254,9.));
#376857=CARTESIAN_POINT('',(2.53761520271997,-1.05972122887319,8.75721825406948));
#376858=CARTESIAN_POINT('Origin',(0.,1.84795814293585E-15,8.75721825406948));
#376859=CARTESIAN_POINT('',(2.53761520271997,-1.05972122887319,7.51860402984325));
#376860=CARTESIAN_POINT('',(2.53761520271997,-1.05972122887319,9.));
#376861=CARTESIAN_POINT('',(2.53023235892141,-1.07722987791233,7.49482233047033));
#376862=CARTESIAN_POINT('Origin',(2.52656522231176,-1.08579188295431,7.53025004711358));
#376863=CARTESIAN_POINT('',(2.4985270438815,-1.1488527368609,7.49482233047033));
#376864=CARTESIAN_POINT('Origin',(1.68979625270541E-15,-7.48022675047808E-16,
7.49482233047033));
#376865=CARTESIAN_POINT('',(2.49052926869775,-1.1660891740171,7.51860402984325));
#376866=CARTESIAN_POINT('Origin',(2.50242186432163,-1.1403339566039,7.53030836256736));
#376867=CARTESIAN_POINT('',(2.49052926869775,-1.1660891740171,8.75721825406948));
#376868=CARTESIAN_POINT('',(2.49052926869775,-1.1660891740171,9.));
#376869=CARTESIAN_POINT('',(2.46450482787546,-1.2201294822184,8.75721825406948));
#376870=CARTESIAN_POINT('Origin',(0.,1.84795814293585E-15,8.75721825406948));
#376871=CARTESIAN_POINT('',(2.46450482787546,-1.2201294822184,7.51860402984325));
#376872=CARTESIAN_POINT('',(2.46450482787547,-1.2201294822184,9.));
#376873=CARTESIAN_POINT('',(2.4560153699258,-1.23712913743403,7.49482233047033));
#376874=CARTESIAN_POINT('Origin',(2.45180719829513,-1.24543859666903,7.53025004711348));
#376875=CARTESIAN_POINT('',(2.41978630452754,-1.3065734730282,7.49482233047033));
#376876=CARTESIAN_POINT('Origin',(1.63839840773327E-15,-8.5475139987016E-16,
7.49482233047033));
#376877=CARTESIAN_POINT('',(2.41070061931038,-1.32326207686028,7.51860402984325));
#376878=CARTESIAN_POINT('Origin',(2.42421892276641,-1.29832173752123,7.53030836256741));
#376879=CARTESIAN_POINT('',(2.41070061931038,-1.32326207686027,8.75721825406948));
#376880=CARTESIAN_POINT('',(2.41070061931038,-1.32326207686027,9.));
#376881=CARTESIAN_POINT('',(2.38126727405859,-1.37552396180421,8.75721825406948));
#376882=CARTESIAN_POINT('Origin',(0.,1.84795814293585E-15,8.75721825406948));
#376883=CARTESIAN_POINT('',(2.38126727405859,-1.37552396180421,7.51860402984325));
#376884=CARTESIAN_POINT('',(2.38126727405859,-1.37552396180421,9.));
#376885=CARTESIAN_POINT('',(2.37170608696151,-1.39194476796664,7.49482233047033));
#376886=CARTESIAN_POINT('Origin',(2.36697417258961,-1.39996753604449,7.53025004711367));
#376887=CARTESIAN_POINT('',(2.33110214420574,-1.45892521853569,7.49482233047033));
#376888=CARTESIAN_POINT('Origin',(1.5802680322684E-15,-9.57967767846848E-16,
7.49482233047033));
#376889=CARTESIAN_POINT('',(2.3209658839846,-1.47499741199082,7.51860402984325));
#376890=CARTESIAN_POINT('Origin',(2.33605434566413,-1.45097443593007,7.53030836256728));
#376891=CARTESIAN_POINT('',(2.3209658839846,-1.47499741199081,8.75721825406948));
#376892=CARTESIAN_POINT('',(2.3209658839846,-1.47499741199081,9.));
#376893=CARTESIAN_POINT('',(2.28824458223239,-1.52526611838201,8.75721825406948));
#376894=CARTESIAN_POINT('Origin',(0.,1.84795814293585E-15,8.75721825406948));
#376895=CARTESIAN_POINT('',(2.28824458223239,-1.52526611838201,7.51860402984325));
#376896=CARTESIAN_POINT('',(2.28824458223239,-1.52526611838201,9.));
#376897=CARTESIAN_POINT('',(2.27765095495655,-1.54104059887647,7.49482233047033));
#376898=CARTESIAN_POINT('Origin',(2.27241474229462,-1.54874370852212,7.53025004711368));
#376899=CARTESIAN_POINT('',(2.23283898515356,-1.60528192738174,7.49482233047033));
#376900=CARTESIAN_POINT('Origin',(1.51564399649251E-15,-1.05724764078201E-15,
7.49482233047033));
#376901=CARTESIAN_POINT('',(2.22169380199591,-1.62067166636953,7.51860402984325));
#376902=CARTESIAN_POINT('Origin',(2.23829042017357,-1.59766476914842,7.53030836256744));
#376903=CARTESIAN_POINT('',(2.22169380199591,-1.62067166636952,8.75721825406948));
#376904=CARTESIAN_POINT('',(2.22169380199591,-1.62067166636952,9.));
#376905=CARTESIAN_POINT('',(2.18581900259087,-1.66874062931082,8.75721825406948));
#376906=CARTESIAN_POINT('Origin',(0.,1.84795814293585E-15,8.75721825406948));
#376907=CARTESIAN_POINT('',(2.18581900259087,-1.66874062931082,7.51860402984325));
#376908=CARTESIAN_POINT('',(2.18581900259087,-1.66874062931082,9.));
#376909=CARTESIAN_POINT('',(2.17423646662307,-1.68380396341334,7.49482233047033));
#376910=CARTESIAN_POINT('Origin',(2.16851747239208,-1.69115576089697,7.53025004711369));
#376911=CARTESIAN_POINT('',(2.12540061176892,-1.74504218845629,7.49482233047033));
#376912=CARTESIAN_POINT('Origin',(1.44479185443041E-15,-1.15218305638229E-15,
7.49482233047033));
#376913=CARTESIAN_POINT('',(2.11329230362299,-1.75968623323814,7.51860402984325));
#376914=CARTESIAN_POINT('Origin',(2.13132887923455,-1.73778995513257,7.53030836256725));
#376915=CARTESIAN_POINT('',(2.11329230362299,-1.75968623323814,8.75721825406948));
#376916=CARTESIAN_POINT('',(2.113292303623,-1.75968623323814,9.));
#376917=CARTESIAN_POINT('',(2.07441142381099,-1.80535792705005,8.75721825406948));
#376918=CARTESIAN_POINT('Origin',(0.,1.84795814293585E-15,8.75721825406948));
#376919=CARTESIAN_POINT('',(2.07441142381099,-1.80535792705005,7.51860402984325));
#376920=CARTESIAN_POINT('',(2.07441142381099,-1.80535792705005,9.));
#376921=CARTESIAN_POINT('',(2.06188757427597,-1.81964821628972,7.49482233047033));
#376922=CARTESIAN_POINT('Origin',(2.05570929904995,-1.82661849149851,7.5302500471137));
#376923=CARTESIAN_POINT('',(2.00922851137352,-1.8776316968681,7.49482233047033));
#376924=CARTESIAN_POINT('Origin',(1.36800275273158E-15,-1.24238390466141E-15,
7.49482233047033));
#376925=CARTESIAN_POINT('',(1.99620683387471,-1.89146987192287,7.51860402984325));
#376926=CARTESIAN_POINT('Origin',(2.01560925076226,-1.87077418943614,7.53030836256729));
#376927=CARTESIAN_POINT('',(1.99620683387471,-1.89146987192287,8.75721825406948));
#376928=CARTESIAN_POINT('',(1.99620683387471,-1.89146987192287,9.));
#376929=CARTESIAN_POINT('',(1.95447964353083,-1.93455662181897,8.75721825406948));
#376930=CARTESIAN_POINT('Origin',(0.,1.84795814293585E-15,8.75721825406948));
#376931=CARTESIAN_POINT('',(1.95447964353083,-1.93455662181897,7.51860402984325));
#376932=CARTESIAN_POINT('',(1.95447964353083,-1.93455662181897,9.));
#376933=CARTESIAN_POINT('',(1.94106594361268,-1.94801514433206,7.49482233047033));
#376934=CARTESIAN_POINT('Origin',(1.93445377524964,-1.95457525491017,7.53025004711394));
#376935=CARTESIAN_POINT('',(1.88480006004672,-2.00250561388673,7.49482233047033));
#376936=CARTESIAN_POINT('Origin',(1.2855922342861E-15,-1.32747953098576E-15,
7.49482233047033));
#376937=CARTESIAN_POINT('',(1.87091852206101,-2.01548105518485,7.51860402984325));
#376938=CARTESIAN_POINT('Origin',(1.89160705153173,-1.99607101131556,7.53030836256725));
#376939=CARTESIAN_POINT('',(1.87091852206101,-2.01548105518485,8.75721825406948));
#376940=CARTESIAN_POINT('',(1.87091852206102,-2.01548105518485,9.));
#376941=CARTESIAN_POINT('',(1.82651648716082,-2.05580580846774,8.75721825406948));
#376942=CARTESIAN_POINT('Origin',(0.,1.84795814293585E-15,8.75721825406948));
#376943=CARTESIAN_POINT('',(1.82651648716082,-2.05580580846774,7.51860402984325));
#376944=CARTESIAN_POINT('',(1.82651648716082,-2.05580580846774,9.));
#376945=CARTESIAN_POINT('',(1.81226805662974,-2.06837726029839,7.49482233047033));
#376946=CARTESIAN_POINT('Origin',(1.80524916594823,-2.07450024934391,7.53025004711344));
#376947=CARTESIAN_POINT('',(1.75262656098485,-2.11915080580181,7.49482233047033));
#376948=CARTESIAN_POINT('Origin',(1.19789894159128E-15,-1.40712025917382E-15,
7.49482233047033));
#376949=CARTESIAN_POINT('',(1.7379422047294,-2.13121019447175,7.51860402984325));
#376950=CARTESIAN_POINT('Origin',(1.75983183317822,-2.1131655492534,7.53030836256758));
#376951=CARTESIAN_POINT('',(1.73794220472941,-2.13121019447175,8.75721825406948));
#376952=CARTESIAN_POINT('',(1.73794220472941,-2.13121019447175,9.));
#376953=CARTESIAN_POINT('',(1.69104778275851,-2.16860724808056,8.75721825406948));
#376954=CARTESIAN_POINT('Origin',(0.,1.84795814293585E-15,8.75721825406948));
#376955=CARTESIAN_POINT('',(1.69104778275851,-2.16860724808056,7.51860402984325));
#376956=CARTESIAN_POINT('',(1.69104778275851,-2.16860724808056,9.));
#376957=CARTESIAN_POINT('',(1.67602317147183,-2.18023997043663,7.49482233047033));
#376958=CARTESIAN_POINT('Origin',(1.6686264005988,-2.18590067727457,7.53025004711363));
#376959=CARTESIAN_POINT('',(1.61325114344667,-2.22708795249942,7.49482233047033));
#376960=CARTESIAN_POINT('Origin',(1.10528322519694E-15,-1.48097882839059E-15,
7.49482233047033));
#376961=CARTESIAN_POINT('',(1.59782431009112,-2.23818173392641,7.51860402984325));
#376962=CARTESIAN_POINT('Origin',(1.62082508833912,-2.22157663667706,7.53030836256737));
#376963=CARTESIAN_POINT('',(1.59782431009113,-2.23818173392641,8.75721825406948));
#376964=CARTESIAN_POINT('',(1.59782431009113,-2.23818173392641,9.));
#376965=CARTESIAN_POINT('',(1.54863020028824,-2.27249741534621,8.75721825406948));
#376966=CARTESIAN_POINT('Origin',(0.,1.84795814293585E-15,8.75721825406948));
#376967=CARTESIAN_POINT('',(1.54863020028824,-2.27249741534621,7.51860402984325));
#376968=CARTESIAN_POINT('',(1.54863020028824,-2.27249741534621,9.));
#376969=CARTESIAN_POINT('',(1.5328911475965,-2.28314360687634,7.49482233047033));
#376970=CARTESIAN_POINT('Origin',(1.52514689145007,-2.28831877044806,7.53025004711377));
#376971=CARTESIAN_POINT('',(1.46724653091878,-2.32587351709134,7.49482233047033));
#376972=CARTESIAN_POINT('Origin',(1.00812566294775E-15,-1.54875173793254E-15,
7.49482233047033));
#376973=CARTESIAN_POINT('',(1.45114061263044,-2.33595610454789,7.51860402984325));
#376974=CARTESIAN_POINT('Origin',(1.47515802554624,-2.32085878917382,7.53030836256734));
#376975=CARTESIAN_POINT('',(1.45114061263045,-2.33595610454789,8.75721825406948));
#376976=CARTESIAN_POINT('',(1.45114061263045,-2.33595610454789,9.));
#376977=CARTESIAN_POINT('',(1.39984896414485,-2.36704940328304,8.75721825406948));
#376978=CARTESIAN_POINT('Origin',(0.,1.84795814293585E-15,8.75721825406948));
#376979=CARTESIAN_POINT('',(1.39984896414485,-2.36704940328304,7.51860402984325));
#376980=CARTESIAN_POINT('',(1.39984896414485,-2.36704940328304,9.));
#376981=CARTESIAN_POINT('',(1.38346014519158,-2.37666531650262,7.49482233047033));
#376982=CARTESIAN_POINT('Origin',(1.37540022658149,-2.38133367095087,7.53025004711378));
#376983=CARTESIAN_POINT('',(1.31521268767195,-2.41510156850322,7.49482233047033));
#376984=CARTESIAN_POINT('Origin',(9.06825496107236E-16,-1.61016049437712E-15,
7.49482233047033));
#376985=CARTESIAN_POINT('',(1.29849386712378,-2.42413153047477,7.51860402984325));
#376986=CARTESIAN_POINT('Origin',(1.3234292220059,-2.41060403508326,7.53030836256716));
#376987=CARTESIAN_POINT('',(1.29849386712378,-2.42413153047477,8.75721825406948));
#376988=CARTESIAN_POINT('',(1.29849386712378,-2.42413153047477,9.));
#376989=CARTESIAN_POINT('',(1.24531544834112,-2.45187467749128,8.75721825406948));
#376990=CARTESIAN_POINT('Origin',(0.,1.84795814293585E-15,8.75721825406948));
#376991=CARTESIAN_POINT('',(1.24531544834112,-2.45187467749128,7.51860402984325));
#376992=CARTESIAN_POINT('',(1.24531544834112,-2.45187467749128,9.));
#376993=CARTESIAN_POINT('',(1.22834420829879,-2.46042079855028,7.49482233047033));
#376994=CARTESIAN_POINT('Origin',(1.22000174715932,-2.46456316060533,7.53025004711397));
#376995=CARTESIAN_POINT('',(1.15777435337925,-2.49440544953247,7.49482233047033));
#376996=CARTESIAN_POINT('Origin',(8.01798988789759E-16,-1.66495275597196E-15,
7.49482233047033));
#376997=CARTESIAN_POINT('',(1.14051133179104,-2.50234567996835,7.51860402984325));
#376998=CARTESIAN_POINT('Origin',(1.16626216391798,-2.49044359193944,7.53030836256744));
#376999=CARTESIAN_POINT('',(1.14051133179105,-2.50234567996834,8.75721825406948));
#377000=CARTESIAN_POINT('',(1.14051133179105,-2.50234567996834,9.));
#377001=CARTESIAN_POINT('',(1.08566466424083,-2.52662467272424,8.75721825406948));
#377002=CARTESIAN_POINT('Origin',(0.,1.84795814293585E-15,8.75721825406948));
#377003=CARTESIAN_POINT('',(1.08566466424083,-2.52662467272424,7.51860402984325));
#377004=CARTESIAN_POINT('',(1.08566466424083,-2.52662467272424,9.));
#377005=CARTESIAN_POINT('',(1.0681807415751,-2.5340658837781,7.49482233047033));
#377006=CARTESIAN_POINT('Origin',(1.05959001886878,-2.5376652315856,7.53025004711381));
#377007=CARTESIAN_POINT('',(0.995578475926683,-2.5634592835213,7.49482233047033));
#377008=CARTESIAN_POINT('Origin',(6.93477717442E-16,-1.71290336956127E-15,
7.49482233047033));
#377009=CARTESIAN_POINT('',(0.977842190757062,-2.57027715431147,7.51860402984325));
#377010=CARTESIAN_POINT('Origin',(1.00430268443587,-2.56004938187796,7.53030836256745));
#377011=CARTESIAN_POINT('',(0.977842190757066,-2.57027715431146,8.75721825406948));
#377012=CARTESIAN_POINT('',(0.977842190757067,-2.57027715431146,9.));
#377013=CARTESIAN_POINT('',(0.921552651160842,-2.59099222521767,8.75721825406948));
#377014=CARTESIAN_POINT('Origin',(0.,1.84795814293585E-15,8.75721825406948));
#377015=CARTESIAN_POINT('',(0.921552651160842,-2.59099222521767,7.51860402984325));
#377016=CARTESIAN_POINT('',(0.921552651160842,-2.59099222521767,9.));
#377017=CARTESIAN_POINT('',(0.903627891060228,-2.59729794873404,7.49482233047033));
#377018=CARTESIAN_POINT('Origin',(0.894824207909509,-2.60033949180176,7.53025004711349));
#377019=CARTESIAN_POINT('',(0.829291552965625,-2.62197931345384,7.49482233047033));
#377020=CARTESIAN_POINT('Origin',(5.82306797402768E-16,-1.75381529578843E-15,
7.49482233047033));
#377021=CARTESIAN_POINT('',(0.811154886414768,-2.6276468085048,7.51860402984325));
#377022=CARTESIAN_POINT('Origin',(0.838216309801055,-2.61913537977752,7.53030836256733));
#377023=CARTESIAN_POINT('',(0.811154886414773,-2.6276468085048,8.75721825406948));
#377024=CARTESIAN_POINT('',(0.811154886414773,-2.6276468085048,9.));
#377025=CARTESIAN_POINT('',(0.753653780564806,-2.6447128348916,8.75721825406948));
#377026=CARTESIAN_POINT('Origin',(0.,1.84795814293585E-15,8.75721825406948));
#377027=CARTESIAN_POINT('',(0.753653780564806,-2.6447128348916,7.51860402984325));
#377028=CARTESIAN_POINT('',(0.753653780564806,-2.6447128348916,9.));
#377029=CARTESIAN_POINT('',(0.735361839713413,-2.64985715929997,7.49482233047033));
#377030=CARTESIAN_POINT('Origin',(0.726381372340523,-2.65232839927514,7.53025004711344));
#377031=CARTESIAN_POINT('',(0.65959689313095,-2.6697250679746,7.49482233047033));
#377032=CARTESIAN_POINT('Origin',(4.68743053828592E-16,-1.78752041877299E-15,
7.49482233047033));
#377033=CARTESIAN_POINT('',(0.641134372652019,-2.67421889833352,7.51860402984325));
#377034=CARTESIAN_POINT('Origin',(0.668685524552562,-2.66745878859875,7.53030836256735));
#377035=CARTESIAN_POINT('',(0.641134372652024,-2.67421889833351,8.75721825406948));
#377036=CARTESIAN_POINT('',(0.641134372652024,-2.67421889833351,9.));
#377037=CARTESIAN_POINT('',(0.582657984926201,-2.68756575223784,8.75721825406948));
#377038=CARTESIAN_POINT('Origin',(0.,1.84795814293585E-15,8.75721825406948));
#377039=CARTESIAN_POINT('',(0.582657984926201,-2.68756575223784,7.51860402984325));
#377040=CARTESIAN_POINT('',(0.582657984926201,-2.68756575223784,9.));
#377041=CARTESIAN_POINT('',(0.564074028832595,-2.69152753840576,7.49482233047033));
#377042=CARTESIAN_POINT('Origin',(0.554953679904234,-2.69341832043325,7.53025004711345));
#377043=CARTESIAN_POINT('',(0.487191808179311,-2.70650034953683,7.49482233047033));
#377044=CARTESIAN_POINT('Origin',(3.53253144501165E-16,-1.81388023693488E-15,
7.49482233047033));
#377045=CARTESIAN_POINT('',(0.468479300229151,-2.70980204909082,7.51860402984325));
#377046=CARTESIAN_POINT('Origin',(0.496406967050784,-2.70482103708957,7.53030836256699));
#377047=CARTESIAN_POINT('',(0.468479300229156,-2.70980204909082,8.75721825406948));
#377048=CARTESIAN_POINT('',(0.468479300229156,-2.70980204909082,9.));
#377049=CARTESIAN_POINT('',(0.409267922647788,-2.71937488542709,8.75721825406948));
#377050=CARTESIAN_POINT('Origin',(0.,1.84795814293585E-15,8.75721825406948));
#377051=CARTESIAN_POINT('',(0.409267922647788,-2.71937488542709,7.51860402984325));
#377052=CARTESIAN_POINT('',(0.409267922647788,-2.71937488542709,9.));
#377053=CARTESIAN_POINT('',(0.390468316773804,-2.72213785352539,7.49482233047033));
#377054=CARTESIAN_POINT('Origin',(0.38124556375981,-2.72344040797632,7.53025004711372));
#377055=CARTESIAN_POINT('',(0.312784747585547,-2.7321540406203,7.49482233047033));
#377056=CARTESIAN_POINT('Origin',(2.3631164223042E-16,-1.83278643212712E-15,
7.49482233047033));
#377057=CARTESIAN_POINT('',(0.293899145873147,-2.7342500419777,7.51860402984325));
#377058=CARTESIAN_POINT('Origin',(0.322088566843193,-2.73106859575657,7.53030836256759));
#377059=CARTESIAN_POINT('',(0.293899145873152,-2.7342500419777,8.75721825406948));
#377060=CARTESIAN_POINT('',(0.293899145873152,-2.7342500419777,9.));
#377061=CARTESIAN_POINT('',(0.234196090687521,-2.74000952390803,8.75721825406948));
#377062=CARTESIAN_POINT('Origin',(0.,1.84795814293585E-15,8.75721825406948));
#377063=CARTESIAN_POINT('',(0.234196090687521,-2.74000952390803,7.51860402984325));
#377064=CARTESIAN_POINT('',(0.234196090687521,-2.74000952390803,9.));
#377065=CARTESIAN_POINT('',(0.215258086646198,-2.74156232030815,7.49482233047033));
#377066=CARTESIAN_POINT('Origin',(0.205970827817083,-2.74227129470683,7.53025004711386));
#377067=CARTESIAN_POINT('',(0.137092387371836,-2.74658072470567,7.49482233047033));
#377068=CARTESIAN_POINT('Origin',(1.18399084733063E-16,-1.8441613147383E-15,
7.49482233047033));
#377069=CARTESIAN_POINT('',(0.118111296885581,-2.74746241494729,7.51860402984325));
#377070=CARTESIAN_POINT('Origin',(0.146446635625975,-2.74609360775133,7.53030836256733));
#377071=CARTESIAN_POINT('',(0.118111296885586,-2.74746241494729,8.75721825406948));
#377072=CARTESIAN_POINT('',(0.118111296885586,-2.74746241494729,9.));
#377073=CARTESIAN_POINT('',(0.058161896755696,-2.74938487552503,8.75721825406948));
#377074=CARTESIAN_POINT('Origin',(0.,1.84795814293585E-15,8.75721825406948));
#377075=CARTESIAN_POINT('',(0.058161896755696,-2.74938487552503,7.51860402984325));
#377076=CARTESIAN_POINT('',(0.058161896755696,-2.74938487552503,9.));
#377077=CARTESIAN_POINT('',(0.0391633148678293,-2.74972111945349,7.49482233047033));
#377078=CARTESIAN_POINT('Origin',(0.0298497135624777,-2.74983360047203,
7.5302500471137));
#377079=CARTESIAN_POINT('',(-0.0391633148678293,-2.74972111945349,7.49482233047033));
#377080=CARTESIAN_POINT('Origin',(0.,-1.84795814293585E-15,7.49482233047033));
#377081=CARTESIAN_POINT('',(-0.0581618967557012,-2.74938487552503,7.51860402984325));
#377082=CARTESIAN_POINT('Origin',(-0.0297970762295879,-2.74983433207657,
7.53030836256729));
#377083=CARTESIAN_POINT('',(-0.058161896755696,-2.74938487552503,8.75721825406948));
#377084=CARTESIAN_POINT('',(-0.058161896755696,-2.74938487552503,9.));
#377085=CARTESIAN_POINT('',(-0.118111296885546,-2.7474624149473,8.75721825406948));
#377086=CARTESIAN_POINT('Origin',(0.,1.84795814293585E-15,8.75721825406948));
#377087=CARTESIAN_POINT('',(-0.118111296885546,-2.7474624149473,7.51860402984325));
#377088=CARTESIAN_POINT('',(-0.118111296885546,-2.7474624149473,9.));
#377089=CARTESIAN_POINT('',(-0.137092387371797,-2.74658072470567,7.49482233047033));
#377090=CARTESIAN_POINT('Origin',(-0.146394059567869,-2.74609625013545,
7.53025004711355));
#377091=CARTESIAN_POINT('',(-0.215258086646159,-2.74156232030816,7.49482233047033));
#377092=CARTESIAN_POINT('Origin',(-1.18399084733036E-16,-1.8441613147383E-15,
7.49482233047033));
#377093=CARTESIAN_POINT('',(-0.234196090687486,-2.74000952390803,7.51860402984325));
#377094=CARTESIAN_POINT('Origin',(-0.205918345507357,-2.74227539729371,
7.53030836256732));
#377095=CARTESIAN_POINT('',(-0.234196090687482,-2.74000952390803,8.75721825406948));
#377096=CARTESIAN_POINT('',(-0.234196090687482,-2.74000952390803,9.));
#377097=CARTESIAN_POINT('',(-0.293899145873113,-2.7342500419777,8.75721825406948));
#377098=CARTESIAN_POINT('Origin',(0.,1.84795814293585E-15,8.75721825406948));
#377099=CARTESIAN_POINT('',(-0.293899145873113,-2.7342500419777,7.51860402984325));
#377100=CARTESIAN_POINT('',(-0.293899145873113,-2.7342500419777,9.));
#377101=CARTESIAN_POINT('',(-0.312784747585507,-2.73215404062031,7.49482233047033));
#377102=CARTESIAN_POINT('Origin',(-0.322036268106417,-2.73107460127124,
7.53025004711387));
#377103=CARTESIAN_POINT('',(-0.390468316773765,-2.7221378535254,7.49482233047033));
#377104=CARTESIAN_POINT('Origin',(-2.36311642230394E-16,-1.83278643212713E-15,
7.49482233047033));
#377105=CARTESIAN_POINT('',(-0.409267922647754,-2.71937488542709,7.51860402984325));
#377106=CARTESIAN_POINT('Origin',(-0.381193452134136,-2.72344786468713,
7.53030836256735));
#377107=CARTESIAN_POINT('',(-0.409267922647749,-2.71937488542709,8.75721825406948));
#377108=CARTESIAN_POINT('',(-0.409267922647749,-2.71937488542709,9.));
#377109=CARTESIAN_POINT('',(-0.468479300229117,-2.70980204909083,8.75721825406948));
#377110=CARTESIAN_POINT('Origin',(0.,1.84795814293585E-15,8.75721825406948));
#377111=CARTESIAN_POINT('',(-0.468479300229117,-2.70980204909083,7.51860402984325));
#377112=CARTESIAN_POINT('',(-0.468479300229117,-2.70980204909083,9.));
#377113=CARTESIAN_POINT('',(-0.487191808179271,-2.70650034953684,7.49482233047033));
#377114=CARTESIAN_POINT('Origin',(-0.496355160542152,-2.7048303810568,7.53025004711346));
#377115=CARTESIAN_POINT('',(-0.564074028832556,-2.69152753840577,7.49482233047033));
#377116=CARTESIAN_POINT('Origin',(-3.53253144501139E-16,-1.81388023693489E-15,
7.49482233047033));
#377117=CARTESIAN_POINT('',(-0.582657984926168,-2.68756575223785,7.51860402984325));
#377118=CARTESIAN_POINT('Origin',(-0.554902153100284,-2.69342910062684,
7.53030836256744));
#377119=CARTESIAN_POINT('',(-0.582657984926162,-2.68756575223785,8.75721825406948));
#377120=CARTESIAN_POINT('',(-0.582657984926162,-2.68756575223785,9.));
#377121=CARTESIAN_POINT('',(-0.641134372651986,-2.67421889833352,8.75721825406948));
#377122=CARTESIAN_POINT('Origin',(0.,1.84795814293585E-15,8.75721825406948));
#377123=CARTESIAN_POINT('',(-0.641134372651986,-2.67421889833352,7.51860402984325));
#377124=CARTESIAN_POINT('',(-0.641134372651986,-2.67421889833352,9.));
#377125=CARTESIAN_POINT('',(-0.659596893130912,-2.66972506797461,7.49482233047033));
#377126=CARTESIAN_POINT('Origin',(-0.668634423155866,-2.66747143262224,
7.53025004711362));
#377127=CARTESIAN_POINT('',(-0.735361839713374,-2.64985715929998,7.49482233047033));
#377128=CARTESIAN_POINT('Origin',(-4.68743053828567E-16,-1.78752041877299E-15,
7.49482233047033));
#377129=CARTESIAN_POINT('',(-0.753653780564774,-2.64471283489161,7.51860402984325));
#377130=CARTESIAN_POINT('Origin',(-0.726330642093332,-2.65234245865332,
7.53030836256738));
#377131=CARTESIAN_POINT('',(-0.753653780564768,-2.64471283489162,8.75721825406948));
#377132=CARTESIAN_POINT('',(-0.753653780564768,-2.64471283489162,9.));
#377133=CARTESIAN_POINT('',(-0.811154886414735,-2.62764680850481,8.75721825406948));
#377134=CARTESIAN_POINT('Origin',(0.,1.84795814293585E-15,8.75721825406948));
#377135=CARTESIAN_POINT('',(-0.811154886414735,-2.62764680850481,7.51860402984325));
#377136=CARTESIAN_POINT('',(-0.811154886414735,-2.62764680850481,9.));
#377137=CARTESIAN_POINT('',(-0.829291552965587,-2.62197931345385,7.49482233047033));
#377138=CARTESIAN_POINT('Origin',(-0.838166123503155,-2.6191512719002,7.53025004711377));
#377139=CARTESIAN_POINT('',(-0.903627891060191,-2.59729794873405,7.49482233047033));
#377140=CARTESIAN_POINT('Origin',(-5.82306797402743E-16,-1.75381529578843E-15,
7.49482233047033));
#377141=CARTESIAN_POINT('',(-0.92155265116081,-2.59099222521769,7.51860402984325));
#377142=CARTESIAN_POINT('Origin',(-0.894774482680656,-2.60035677259149,
7.53030836256724));
#377143=CARTESIAN_POINT('',(-0.921552651160805,-2.59099222521769,8.75721825406948));
#377144=CARTESIAN_POINT('',(-0.921552651160805,-2.59099222521769,9.));
#377145=CARTESIAN_POINT('',(-0.977842190757029,-2.57027715431148,8.75721825406948));
#377146=CARTESIAN_POINT('Origin',(0.,1.84795814293585E-15,8.75721825406948));
#377147=CARTESIAN_POINT('',(-0.977842190757029,-2.57027715431148,7.51860402984325));
#377148=CARTESIAN_POINT('',(-0.97784219075703,-2.57027715431148,9.));
#377149=CARTESIAN_POINT('',(-0.995578475926647,-2.56345928352131,7.49482233047033));
#377150=CARTESIAN_POINT('Origin',(-1.00425361946274,-2.56006845679578,7.53025004711368));
#377151=CARTESIAN_POINT('',(-1.06818074157507,-2.53406588377811,7.49482233047033));
#377152=CARTESIAN_POINT('Origin',(-6.93477717441975E-16,-1.71290336956128E-15,
7.49482233047033));
#377153=CARTESIAN_POINT('',(-1.0856646642408,-2.52662467272425,7.51860402984325));
#377154=CARTESIAN_POINT('Origin',(-1.0595415029899,-2.53768566277637,7.53030836256737));
#377155=CARTESIAN_POINT('',(-1.0856646642408,-2.52662467272425,8.75721825406948));
#377156=CARTESIAN_POINT('',(-1.0856646642408,-2.52662467272425,9.));
#377157=CARTESIAN_POINT('',(-1.14051133179101,-2.50234567996836,8.75721825406948));
#377158=CARTESIAN_POINT('Origin',(0.,1.84795814293585E-15,8.75721825406948));
#377159=CARTESIAN_POINT('',(-1.14051133179101,-2.50234567996836,7.51860402984325));
#377160=CARTESIAN_POINT('',(-1.14051133179101,-2.50234567996836,9.));
#377161=CARTESIAN_POINT('',(-1.15777435337921,-2.49440544953249,7.49482233047033));
#377162=CARTESIAN_POINT('Origin',(-1.16621442188832,-2.49046577126939,7.53025004711374));
#377163=CARTESIAN_POINT('',(-1.22834420829876,-2.4604207985503,7.49482233047033));
#377164=CARTESIAN_POINT('Origin',(-8.01798988789735E-16,-1.66495275597197E-15,
7.49482233047033));
#377165=CARTESIAN_POINT('',(-1.24531544834109,-2.4518746774913,7.51860402984325));
#377166=CARTESIAN_POINT('Origin',(-1.21995463999254,-2.464586658241,7.5303083625673));
#377167=CARTESIAN_POINT('',(-1.24531544834108,-2.4518746774913,8.75721825406948));
#377168=CARTESIAN_POINT('',(-1.24531544834108,-2.4518746774913,9.));
#377169=CARTESIAN_POINT('',(-1.29849386712375,-2.42413153047479,8.75721825406948));
#377170=CARTESIAN_POINT('Origin',(0.,1.84795814293585E-15,8.75721825406948));
#377171=CARTESIAN_POINT('',(-1.29849386712375,-2.42413153047479,7.51860402984325));
#377172=CARTESIAN_POINT('',(-1.29849386712375,-2.42413153047479,9.));
#377173=CARTESIAN_POINT('',(-1.31521268767192,-2.41510156850324,7.49482233047033));
#377174=CARTESIAN_POINT('Origin',(-1.32338299910195,-2.41062922768572,7.53025004711353));
#377175=CARTESIAN_POINT('',(-1.38346014519155,-2.37666531650264,7.49482233047033));
#377176=CARTESIAN_POINT('Origin',(-9.06825496107213E-16,-1.61016049437713E-15,
7.49482233047033));
#377177=CARTESIAN_POINT('',(-1.39984896414482,-2.36704940328306,7.51860402984325));
#377178=CARTESIAN_POINT('Origin',(-1.37535472169984,-2.38136013847482,7.53030836256751));
#377179=CARTESIAN_POINT('',(-1.39984896414481,-2.36704940328306,8.75721825406948));
#377180=CARTESIAN_POINT('',(-1.39984896414481,-2.36704940328306,9.));
#377181=CARTESIAN_POINT('',(-1.45114061263041,-2.33595610454791,8.75721825406948));
#377182=CARTESIAN_POINT('Origin',(0.,1.84795814293585E-15,8.75721825406948));
#377183=CARTESIAN_POINT('',(-1.45114061263041,-2.33595610454791,7.51860402984325));
#377184=CARTESIAN_POINT('',(-1.45114061263041,-2.33595610454791,9.));
#377185=CARTESIAN_POINT('',(-1.46724653091875,-2.32587351709136,7.49482233047033));
#377186=CARTESIAN_POINT('Origin',(-1.47511351170771,-2.32088689152705,7.53025004711358));
#377187=CARTESIAN_POINT('',(-1.53289114759647,-2.28314360687636,7.49482233047033));
#377188=CARTESIAN_POINT('Origin',(-1.00812566294773E-15,-1.54875173793256E-15,
7.49482233047033));
#377189=CARTESIAN_POINT('',(-1.54863020028821,-2.27249741534623,7.51860402984325));
#377190=CARTESIAN_POINT('Origin',(-1.52510317584316,-2.28834809909943,7.53030836256754));
#377191=CARTESIAN_POINT('',(-1.54863020028821,-2.27249741534623,8.75721825406948));
#377192=CARTESIAN_POINT('',(-1.54863020028821,-2.27249741534624,9.));
#377193=CARTESIAN_POINT('',(-1.5978243100911,-2.23818173392643,8.75721825406948));
#377194=CARTESIAN_POINT('Origin',(0.,1.84795814293585E-15,8.75721825406948));
#377195=CARTESIAN_POINT('',(-1.5978243100911,-2.23818173392643,7.51860402984325));
#377196=CARTESIAN_POINT('',(-1.5978243100911,-2.23818173392643,9.));
#377197=CARTESIAN_POINT('',(-1.61325114344663,-2.22708795249944,7.49482233047033));
#377198=CARTESIAN_POINT('Origin',(-1.62078246648316,-2.22160753330229,7.53025004711383));
#377199=CARTESIAN_POINT('',(-1.6760231714718,-2.18023997043665,7.49482233047033));
#377200=CARTESIAN_POINT('Origin',(-1.10528322519691E-15,-1.48097882839061E-15,
7.49482233047033));
#377201=CARTESIAN_POINT('',(-1.69104778275849,-2.16860724808058,7.51860402984325));
#377202=CARTESIAN_POINT('Origin',(-1.66858465390362,-2.18593274653549,7.53030836256711));
#377203=CARTESIAN_POINT('',(-1.69104778275848,-2.16860724808058,8.75721825406948));
#377204=CARTESIAN_POINT('',(-1.69104778275848,-2.16860724808058,9.));
#377205=CARTESIAN_POINT('',(-1.73794220472938,-2.13121019447177,8.75721825406948));
#377206=CARTESIAN_POINT('Origin',(0.,1.84795814293585E-15,8.75721825406948));
#377207=CARTESIAN_POINT('',(-1.73794220472938,-2.13121019447177,7.51860402984325));
#377208=CARTESIAN_POINT('',(-1.73794220472938,-2.13121019447177,9.));
#377209=CARTESIAN_POINT('',(-1.75262656098482,-2.11915080580183,7.49482233047033));
#377210=CARTESIAN_POINT('Origin',(-1.75979127844685,-2.11319911319003,7.53025004711381));
#377211=CARTESIAN_POINT('',(-1.81226805662971,-2.06837726029842,7.49482233047033));
#377212=CARTESIAN_POINT('Origin',(-1.19789894159126E-15,-1.40712025917384E-15,
7.49482233047033));
#377213=CARTESIAN_POINT('',(-1.8265164871608,-2.05580580846777,7.51860402984325));
#377214=CARTESIAN_POINT('Origin',(-1.80520955971039,-2.07453492743532,7.53030836256744));
#377215=CARTESIAN_POINT('',(-1.82651648716079,-2.05580580846777,8.75721825406948));
#377216=CARTESIAN_POINT('',(-1.82651648716079,-2.05580580846777,9.));
#377217=CARTESIAN_POINT('',(-1.87091852206099,-2.01548105518488,8.75721825406948));
#377218=CARTESIAN_POINT('Origin',(0.,1.84795814293585E-15,8.75721825406948));
#377219=CARTESIAN_POINT('',(-1.87091852206099,-2.01548105518488,7.51860402984325));
#377220=CARTESIAN_POINT('',(-1.87091852206099,-2.01548105518488,9.));
#377221=CARTESIAN_POINT('',(-1.88480006004669,-2.00250561388676,7.49482233047033));
#377222=CARTESIAN_POINT('Origin',(-1.89156873057341,-1.99610710464184,7.53025004711383));
#377223=CARTESIAN_POINT('',(-1.94106594361265,-1.94801514433209,7.49482233047033));
#377224=CARTESIAN_POINT('Origin',(-1.28559223428609E-15,-1.32747953098578E-15,
7.49482233047033));
#377225=CARTESIAN_POINT('',(-1.9544796435308,-1.934556621819,7.51860402984325));
#377226=CARTESIAN_POINT('Origin',(-1.93441647222029,-1.95461239933181,7.53030836256745));
#377227=CARTESIAN_POINT('',(-1.9544796435308,-1.934556621819,8.75721825406948));
#377228=CARTESIAN_POINT('',(-1.9544796435308,-1.934556621819,9.));
#377229=CARTESIAN_POINT('',(-1.99620683387468,-1.8914698719229,8.75721825406948));
#377230=CARTESIAN_POINT('Origin',(0.,1.84795814293585E-15,8.75721825406948));
#377231=CARTESIAN_POINT('',(-1.99620683387468,-1.8914698719229,7.51860402984325));
#377232=CARTESIAN_POINT('',(-1.99620683387468,-1.8914698719229,9.));
#377233=CARTESIAN_POINT('',(-2.00922851137349,-1.87763169686813,7.49482233047033));
#377234=CARTESIAN_POINT('Origin',(-2.01557332104574,-1.87081266383713,7.53025004711374));
#377235=CARTESIAN_POINT('',(-2.06188757427594,-1.81964821628975,7.49482233047033));
#377236=CARTESIAN_POINT('Origin',(-1.36800275273156E-15,-1.24238390466143E-15,
7.49482233047033));
#377237=CARTESIAN_POINT('',(-2.07441142381097,-1.80535792705008,7.51860402984325));
#377238=CARTESIAN_POINT('Origin',(-2.05567445251486,-1.82665794961634,7.53030836256737));
#377239=CARTESIAN_POINT('',(-2.07441142381097,-1.80535792705008,8.75721825406948));
#377240=CARTESIAN_POINT('',(-2.07441142381097,-1.80535792705008,9.));
#377241=CARTESIAN_POINT('',(-2.11329230362297,-1.75968623323817,8.75721825406948));
#377242=CARTESIAN_POINT('Origin',(0.,1.84795814293585E-15,8.75721825406948));
#377243=CARTESIAN_POINT('',(-2.11329230362297,-1.75968623323817,7.51860402984325));
#377244=CARTESIAN_POINT('',(-2.11329230362297,-1.75968623323817,9.));
#377245=CARTESIAN_POINT('',(-2.12540061176889,-1.74504218845632,7.49482233047033));
#377246=CARTESIAN_POINT('Origin',(-2.13129548840281,-1.73783065250862,7.53025004711368));
#377247=CARTESIAN_POINT('',(-2.17423646662304,-1.68380396341337,7.49482233047033));
#377248=CARTESIAN_POINT('Origin',(-1.4447918544304E-15,-1.15218305638231E-15,
7.49482233047033));
#377249=CARTESIAN_POINT('',(-2.18581900259085,-1.66874062931085,7.51860402984325));
#377250=CARTESIAN_POINT('Origin',(-2.16848522554312,-1.69119737056916,7.53030836256759));
#377251=CARTESIAN_POINT('',(-2.18581900259084,-1.66874062931085,8.75721825406948));
#377252=CARTESIAN_POINT('',(-2.18581900259084,-1.66874062931085,9.));
#377253=CARTESIAN_POINT('',(-2.22169380199589,-1.62067166636955,8.75721825406948));
#377254=CARTESIAN_POINT('Origin',(0.,1.84795814293585E-15,8.75721825406948));
#377255=CARTESIAN_POINT('',(-2.22169380199589,-1.62067166636955,7.51860402984325));
#377256=CARTESIAN_POINT('',(-2.22169380199589,-1.62067166636955,9.));
#377257=CARTESIAN_POINT('',(-2.23283898515353,-1.60528192738178,7.49482233047033));
#377258=CARTESIAN_POINT('Origin',(-2.2382597054367,-1.59770752226531,7.53025004711383));
#377259=CARTESIAN_POINT('',(-2.27765095495652,-1.5410405988765,7.49482233047033));
#377260=CARTESIAN_POINT('Origin',(-1.51564399649249E-15,-1.05724764078203E-15,
7.49482233047033));
#377261=CARTESIAN_POINT('',(-2.28824458223237,-1.52526611838204,7.51860402984325));
#377262=CARTESIAN_POINT('Origin',(-2.27238522764112,-1.54878729876548,7.53030836256757));
#377263=CARTESIAN_POINT('',(-2.28824458223237,-1.52526611838204,8.75721825406948));
#377264=CARTESIAN_POINT('',(-2.28824458223237,-1.52526611838205,9.));
#377265=CARTESIAN_POINT('',(-2.32096588398458,-1.47499741199084,8.75721825406948));
#377266=CARTESIAN_POINT('Origin',(0.,1.84795814293585E-15,8.75721825406948));
#377267=CARTESIAN_POINT('',(-2.32096588398458,-1.47499741199084,7.51860402984325));
#377268=CARTESIAN_POINT('',(-2.32096588398458,-1.47499741199084,9.));
#377269=CARTESIAN_POINT('',(-2.33110214420572,-1.45892521853572,7.49482233047033));
#377270=CARTESIAN_POINT('Origin',(-2.33602643323561,-1.45101906910599,7.53025004711374));
#377271=CARTESIAN_POINT('',(-2.37170608696149,-1.39194476796668,7.49482233047033));
#377272=CARTESIAN_POINT('Origin',(-1.58026803226839E-15,-9.5796776784687E-16,
7.49482233047033));
#377273=CARTESIAN_POINT('',(-2.38126727405858,-1.37552396180424,7.51860402984325));
#377274=CARTESIAN_POINT('Origin',(-2.36694751141368,-1.40001292773726,7.53030836256736));
#377275=CARTESIAN_POINT('',(-2.38126727405858,-1.37552396180425,8.75721825406948));
#377276=CARTESIAN_POINT('',(-2.38126727405858,-1.37552396180425,9.));
#377277=CARTESIAN_POINT('',(-2.41070061931036,-1.32326207686031,8.75721825406948));
#377278=CARTESIAN_POINT('Origin',(0.,1.84795814293585E-15,8.75721825406948));
#377279=CARTESIAN_POINT('',(-2.41070061931036,-1.32326207686031,7.51860402984325));
#377280=CARTESIAN_POINT('',(-2.41070061931036,-1.32326207686031,9.));
#377281=CARTESIAN_POINT('',(-2.41978630452752,-1.30657347302823,7.49482233047033));
#377282=CARTESIAN_POINT('Origin',(-2.42419392734421,-1.29836806734923,7.53025004711348));
#377283=CARTESIAN_POINT('',(-2.45601536992578,-1.23712913743406,7.49482233047033));
#377284=CARTESIAN_POINT('Origin',(-1.63839840773326E-15,-8.54751399870184E-16,
7.49482233047033));
#377285=CARTESIAN_POINT('',(-2.46450482787545,-1.22012948221843,7.51860402984325));
#377286=CARTESIAN_POINT('Origin',(-2.45178350015302,-1.24548560328744,7.53030836256769));
#377287=CARTESIAN_POINT('',(-2.46450482787545,-1.22012948221843,8.75721825406948));
#377288=CARTESIAN_POINT('',(-2.46450482787545,-1.22012948221843,9.));
#377289=CARTESIAN_POINT('',(-2.49052926869773,-1.16608917401713,8.75721825406948));
#377290=CARTESIAN_POINT('Origin',(0.,1.84795814293585E-15,8.75721825406948));
#377291=CARTESIAN_POINT('',(-2.49052926869773,-1.16608917401713,7.51860402984325));
#377292=CARTESIAN_POINT('',(-2.49052926869773,-1.16608917401713,9.));
#377293=CARTESIAN_POINT('',(-2.49852704388149,-1.14885273686093,7.49482233047033));
#377294=CARTESIAN_POINT('Origin',(-2.50239988861744,-1.14038179270459,7.53025004711334));
#377295=CARTESIAN_POINT('',(-2.5302323589214,-1.07722987791236,7.49482233047033));
#377296=CARTESIAN_POINT('Origin',(-1.6897962527054E-15,-7.48022675047831E-16,
7.49482233047033));
#377297=CARTESIAN_POINT('',(-2.53761520271995,-1.05972122887322,7.51860402984325));
#377298=CARTESIAN_POINT('Origin',(-2.5265445845846,-1.0858403113373,7.53030836256713));
#377299=CARTESIAN_POINT('',(-2.53761520271995,-1.05972122887323,8.75721825406948));
#377300=CARTESIAN_POINT('',(-2.53761520271995,-1.05972122887323,9.));
#377301=CARTESIAN_POINT('',(-2.56012379910317,-1.00412456063257,8.75721825406948));
#377302=CARTESIAN_POINT('Origin',(0.,1.84795814293585E-15,8.75721825406948));
#377303=CARTESIAN_POINT('',(-2.56012379910317,-1.00412456063257,7.51860402984325));
#377304=CARTESIAN_POINT('',(-2.56012379910317,-1.00412456063257,9.));
#377305=CARTESIAN_POINT('',(-2.56700079967977,-0.986411118369736,7.49482233047033));
#377306=CARTESIAN_POINT('Origin',(-2.5703229519854,-0.977709444662262,7.5302500471136));
#377307=CARTESIAN_POINT('',(-2.59405208042106,-0.912904049757236,7.49482233047033));
#377308=CARTESIAN_POINT('Origin',(-1.73425036241501E-15,-6.38220164603345E-16,
7.49482233047033));
#377309=CARTESIAN_POINT('',(-2.60029797237973,-0.89495835368909,7.51860402984325));
#377310=CARTESIAN_POINT('Origin',(-2.59092355537579,-0.921733068636329,
7.5303083625673));
#377311=CARTESIAN_POINT('',(-2.60029797237973,-0.894958353689095,8.75721825406948));
#377312=CARTESIAN_POINT('',(-2.60029797237973,-0.894958353689095,9.));
#377313=CARTESIAN_POINT('',(-2.61919823167326,-0.838033784044333,8.75721825406948));
#377314=CARTESIAN_POINT('Origin',(0.,1.84795814293585E-15,8.75721825406948));
#377315=CARTESIAN_POINT('',(-2.61919823167326,-0.838033784044333,7.51860402984325));
#377316=CARTESIAN_POINT('',(-2.61919823167326,-0.838033784044333,9.));
#377317=CARTESIAN_POINT('',(-2.62492619857223,-0.819916125008636,7.49482233047033));
#377318=CARTESIAN_POINT('Origin',(-2.62768400701105,-0.811019478793875,
7.53025004711377));
#377319=CARTESIAN_POINT('',(-2.64721228549986,-0.744826903044354,7.49482233047033));
#377320=CARTESIAN_POINT('Origin',(-1.77157806538992E-15,-5.25795070604709E-16,
7.49482233047033));
#377321=CARTESIAN_POINT('',(-2.65229555990883,-0.726517902661682,7.51860402984325));
#377322=CARTESIAN_POINT('Origin',(-2.64465586552658,-0.753838227045237,
7.53030836256741));
#377323=CARTESIAN_POINT('',(-2.65229555990883,-0.726517902661687,8.75721825406948));
#377324=CARTESIAN_POINT('',(-2.65229555990883,-0.726517902661687,9.));
#377325=CARTESIAN_POINT('',(-2.66750981689315,-0.668499346879772,8.75721825406948));
#377326=CARTESIAN_POINT('Origin',(0.,1.84795814293585E-15,8.75721825406948));
#377327=CARTESIAN_POINT('',(-2.66750981689315,-0.668499346879772,7.51860402984325));
#377328=CARTESIAN_POINT('',(-2.66750981689315,-0.668499346879772,9.));
#377329=CARTESIAN_POINT('',(-2.67206521266984,-0.650051920418417,7.49482233047033));
#377330=CARTESIAN_POINT('Origin',(-2.67424734481532,-0.640996859924407,
7.53025004711345));
#377331=CARTESIAN_POINT('',(-2.68949452747227,-0.573689102821993,7.49482233047033));
#377332=CARTESIAN_POINT('Origin',(-1.80162597409185E-15,-4.11209371878269E-16,
7.49482233047033));
#377333=CARTESIAN_POINT('',(-2.69339429606665,-0.555092033734636,7.51860402984325));
#377334=CARTESIAN_POINT('Origin',(-2.68752071744914,-0.582845702480928,
7.53030836256694));
#377335=CARTESIAN_POINT('',(-2.69339429606665,-0.555092033734641,8.75721825406948));
#377336=CARTESIAN_POINT('',(-2.69339429606665,-0.555092033734641,9.));
#377337=CARTESIAN_POINT('',(-2.70486003209636,-0.496217902506221,8.75721825406948));
#377338=CARTESIAN_POINT('Origin',(0.,1.84795814293585E-15,8.75721825406948));
#377339=CARTESIAN_POINT('',(-2.70486003209636,-0.496217902506221,7.51860402984325));
#377340=CARTESIAN_POINT('',(-2.70486003209636,-0.496217902506221,9.));
#377341=CARTESIAN_POINT('',(-2.70822413765241,-0.4775165130515,7.49482233047033));
#377342=CARTESIAN_POINT('Origin',(-2.7098216266556,-0.468340247463668,7.53025004711366));
#377343=CARTESIAN_POINT('',(-2.72072505953654,-0.400193891020209,7.49482233047033));
#377344=CARTESIAN_POINT('Origin',(-1.82427061521866E-15,-2.94933925638647E-16,
7.49482233047033));
#377345=CARTESIAN_POINT('',(-2.72342529733067,-0.381385172574106,7.51860402984325));
#377346=CARTESIAN_POINT('Origin',(-2.71934197027213,-0.409458139906076,
7.5303083625677));
#377347=CARTESIAN_POINT('',(-2.72342529733067,-0.381385172574111,8.75721825406948));
#377348=CARTESIAN_POINT('',(-2.72342529733067,-0.381385172574111,9.));
#377349=CARTESIAN_POINT('',(-2.73109539723703,-0.321897392332866,8.75721825406948));
#377350=CARTESIAN_POINT('Origin',(0.,1.84795814293585E-15,8.75721825406948));
#377351=CARTESIAN_POINT('',(-2.73109539723703,-0.321897392332866,7.51860402984325));
#377352=CARTESIAN_POINT('',(-2.73109539723703,-0.321897392332866,9.));
#377353=CARTESIAN_POINT('',(-2.73325438874111,-0.303018887905483,7.49482233047033));
#377354=CARTESIAN_POINT('Origin',(-2.734260670177,-0.293759124467549,7.53025004711372));
#377355=CARTESIAN_POINT('',(-2.74077554873748,-0.225054196678903,7.49482233047033));
#377356=CARTESIAN_POINT('Origin',(-1.83941893708273E-15,-1.77446532635447E-16,
7.49482233047033));
#377357=CARTESIAN_POINT('',(-2.74226515987506,-0.206111117932606,7.51860402984325));
#377358=CARTESIAN_POINT('Origin',(-2.73998886364241,-0.234388026004842,
7.53030836256716));
#377359=CARTESIAN_POINT('',(-2.74226515987506,-0.206111117932611,8.75721825406948));
#377360=CARTESIAN_POINT('',(-2.74226515987506,-0.206111117932611,9.));
#377361=CARTESIAN_POINT('',(-2.74610810557233,-0.146254136727642,8.75721825406948));
#377362=CARTESIAN_POINT('Origin',(0.,1.84795814293585E-15,8.75721825406948));
#377363=CARTESIAN_POINT('',(-2.74610810557233,-0.146254136727642,7.51860402984325));
#377364=CARTESIAN_POINT('',(-2.74610810557233,-0.146254136727642,9.));
#377365=CARTESIAN_POINT('',(-2.74705311126524,-0.127276093151715,7.49482233047033));
#377366=CARTESIAN_POINT('Origin',(-2.74746405010756,-0.117970882217936,
7.53025004711368));
#377367=CARTESIAN_POINT('',(-2.74956360331414,-0.0489897063694691,7.49482233047033));
#377368=CARTESIAN_POINT('Origin',(-1.8470086919802E-15,-5.92299737674868E-17,
7.49482233047033));
#377369=CARTESIAN_POINT('',(-2.74983646666349,-0.0299901084968253,7.51860402984325));
#377370=CARTESIAN_POINT('Origin',(-2.74937655504614,-0.0583547614294036,
7.53030836256751));
#377371=CARTESIAN_POINT('',(-2.74983646666349,-0.0299901084968303,8.75721825406948));
#377372=CARTESIAN_POINT('',(-2.74983646666349,-0.0299901084968303,9.));
#377373=CARTESIAN_POINT('',(-2.75,1.51118027317033E-15,8.75721825406948));
#377374=CARTESIAN_POINT('Origin',(0.,1.84795814293585E-15,8.75721825406948));
#377375=CARTESIAN_POINT('',(-2.75,1.51118027317033E-15,9.));
#377376=CARTESIAN_POINT('',(-2.74983646666349,0.0299901084968104,8.75721825406948));
#377377=CARTESIAN_POINT('Origin',(0.,1.84795814293585E-15,8.75721825406948));
#377378=CARTESIAN_POINT('',(-2.74983646666349,0.0299901084968104,7.51860402984325));
#377379=CARTESIAN_POINT('',(-2.74983646666349,0.0299901084968104,9.));
#377380=CARTESIAN_POINT('',(-2.74956360331414,0.0489897063694493,7.49482233047033));
#377381=CARTESIAN_POINT('Origin',(-2.74937751092704,0.0583021276915846,
7.5302500471139));
#377382=CARTESIAN_POINT('',(-2.74705311126524,0.127276093151695,7.49482233047033));
#377383=CARTESIAN_POINT('Origin',(-1.8470086919802E-15,5.92299737674735E-17,
7.49482233047033));
#377384=CARTESIAN_POINT('',(-2.74610810557233,0.146254136727627,7.51860402984325));
#377385=CARTESIAN_POINT('Origin',(-2.7474664684458,0.117918295377799,7.53030836256789));
#377386=CARTESIAN_POINT('',(-2.74610810557233,0.146254136727622,8.75721825406948));
#377387=CARTESIAN_POINT('',(-2.74610810557233,0.146254136727622,9.));
#377388=CARTESIAN_POINT('',(-2.74226515987506,0.206111117932592,8.75721825406948));
#377389=CARTESIAN_POINT('Origin',(0.,1.84795814293585E-15,8.75721825406948));
#377390=CARTESIAN_POINT('',(-2.74226515987506,0.206111117932592,7.51860402984325));
#377391=CARTESIAN_POINT('',(-2.74226515987506,0.206111117932592,9.));
#377392=CARTESIAN_POINT('',(-2.74077554873748,0.225054196678883,7.49482233047033));
#377393=CARTESIAN_POINT('Origin',(-2.73999318981449,0.234335561652496,7.53025004711391));
#377394=CARTESIAN_POINT('',(-2.73325438874111,0.303018887905463,7.49482233047033));
#377395=CARTESIAN_POINT('Origin',(-1.83941893708273E-15,1.77446532635434E-16,
7.49482233047033));
#377396=CARTESIAN_POINT('',(-2.73109539723704,0.321897392332852,7.51860402984325));
#377397=CARTESIAN_POINT('Origin',(-2.73426645279692,0.293706800616217,7.53030836256787));
#377398=CARTESIAN_POINT('',(-2.73109539723704,0.321897392332847,8.75721825406948));
#377399=CARTESIAN_POINT('',(-2.73109539723704,0.321897392332847,9.));
#377400=CARTESIAN_POINT('',(-2.72342529733067,0.381385172574091,8.75721825406948));
#377401=CARTESIAN_POINT('Origin',(0.,1.84795814293585E-15,8.75721825406948));
#377402=CARTESIAN_POINT('',(-2.72342529733067,0.381385172574091,7.51860402984325));
#377403=CARTESIAN_POINT('',(-2.72342529733067,0.381385172574092,9.));
#377404=CARTESIAN_POINT('',(-2.72072505953654,0.400193891020189,7.49482233047033));
#377405=CARTESIAN_POINT('Origin',(-2.71934964895829,0.409406060525678,7.53025004711383));
#377406=CARTESIAN_POINT('',(-2.70822413765242,0.47751651305148,7.49482233047033));
#377407=CARTESIAN_POINT('Origin',(-1.82427061521867E-15,2.94933925638634E-16,
7.49482233047033));
#377408=CARTESIAN_POINT('',(-2.70486003209637,0.496217902506207,7.51860402984325));
#377409=CARTESIAN_POINT('Origin',(-2.70983074979511,0.468288401611352,7.53030836256741));
#377410=CARTESIAN_POINT('',(-2.70486003209637,0.496217902506202,8.75721825406948));
#377411=CARTESIAN_POINT('',(-2.70486003209637,0.496217902506202,9.));
#377412=CARTESIAN_POINT('',(-2.69339429606665,0.555092033734621,8.75721825406948));
#377413=CARTESIAN_POINT('Origin',(0.,1.84795814293585E-15,8.75721825406948));
#377414=CARTESIAN_POINT('',(-2.69339429606665,0.555092033734621,7.51860402984325));
#377415=CARTESIAN_POINT('',(-2.69339429606665,0.555092033734622,9.));
#377416=CARTESIAN_POINT('',(-2.68949452747228,0.573689102821973,7.49482233047033));
#377417=CARTESIAN_POINT('Origin',(-2.68753171709593,0.582794222078531,7.5302500471134));
#377418=CARTESIAN_POINT('',(-2.67206521266985,0.650051920418398,7.49482233047033));
#377419=CARTESIAN_POINT('Origin',(-1.80162597409185E-15,4.11209371878256E-16,
7.49482233047033));
#377420=CARTESIAN_POINT('',(-2.66750981689315,0.668499346879758,7.51860402984325));
#377421=CARTESIAN_POINT('Origin',(-2.67425977098557,0.640945705116324,7.53030836256743));
#377422=CARTESIAN_POINT('',(-2.66750981689316,0.668499346879752,8.75721825406948));
#377423=CARTESIAN_POINT('',(-2.66750981689316,0.668499346879752,9.));
#377424=CARTESIAN_POINT('',(-2.65229555990883,0.726517902661668,8.75721825406948));
#377425=CARTESIAN_POINT('Origin',(0.,1.84795814293585E-15,8.75721825406948));
#377426=CARTESIAN_POINT('',(-2.65229555990883,0.726517902661668,7.51860402984325));
#377427=CARTESIAN_POINT('',(-2.65229555990883,0.726517902661668,9.));
#377428=CARTESIAN_POINT('',(-2.64721228549986,0.744826903044335,7.49482233047033));
#377429=CARTESIAN_POINT('Origin',(-2.64467014093422,0.753787557164282,7.53025004711341));
#377430=CARTESIAN_POINT('',(-2.62492619857223,0.819916125008616,7.49482233047033));
#377431=CARTESIAN_POINT('Origin',(-1.77157806538993E-15,5.25795070604696E-16,
7.49482233047033));
#377432=CARTESIAN_POINT('',(-2.61919823167327,0.838033784044319,7.51860402984325));
#377433=CARTESIAN_POINT('Origin',(-2.62769968515012,0.810969225236588,7.53030836256741));
#377434=CARTESIAN_POINT('',(-2.61919823167327,0.838033784044314,8.75721825406948));
#377435=CARTESIAN_POINT('',(-2.61919823167327,0.838033784044314,9.));
#377436=CARTESIAN_POINT('',(-2.60029797237973,0.894958353689077,8.75721825406948));
#377437=CARTESIAN_POINT('Origin',(0.,1.84795814293585E-15,8.75721825406948));
#377438=CARTESIAN_POINT('',(-2.60029797237973,0.894958353689077,7.51860402984325));
#377439=CARTESIAN_POINT('',(-2.60029797237973,0.894958353689077,9.));
#377440=CARTESIAN_POINT('',(-2.59405208042107,0.912904049757218,7.49482233047033));
#377441=CARTESIAN_POINT('Origin',(-2.59094104788336,0.921683417490968,7.53025004711374));
#377442=CARTESIAN_POINT('',(-2.56700079967978,0.986411118369718,7.49482233047033));
#377443=CARTESIAN_POINT('Origin',(-1.73425036241501E-15,6.38220164603333E-16,
7.49482233047033));
#377444=CARTESIAN_POINT('',(-2.56012379910318,1.00412456063256,7.51860402984325));
#377445=CARTESIAN_POINT('Origin',(-2.57034181766858,0.977660298857961,7.53030836256742));
#377446=CARTESIAN_POINT('',(-2.56012379910318,1.00412456063255,8.75721825406948));
#377447=CARTESIAN_POINT('',(-2.56012379910318,1.00412456063256,9.));
#377448=CARTESIAN_POINT('',(-2.53761520271996,1.05972122887321,8.75721825406948));
#377449=CARTESIAN_POINT('Origin',(0.,1.84795814293585E-15,8.75721825406948));
#377450=CARTESIAN_POINT('',(-2.53761520271996,1.05972122887321,7.51860402984325));
#377451=CARTESIAN_POINT('',(-2.53761520271996,1.05972122887321,9.));
#377452=CARTESIAN_POINT('',(-2.5302323589214,1.07722987791234,7.49482233047033));
#377453=CARTESIAN_POINT('Origin',(-2.52656522231168,1.08579188295449,7.53025004711381));
#377454=CARTESIAN_POINT('',(-2.49852704388149,1.14885273686092,7.49482233047033));
#377455=CARTESIAN_POINT('Origin',(-1.6897962527054E-15,7.48022675047819E-16,
7.49482233047033));
#377456=CARTESIAN_POINT('',(-2.49052926869774,1.16608917401712,7.51860402984325));
#377457=CARTESIAN_POINT('Origin',(-2.50242186432154,1.1403339566041,7.53030836256713));
#377458=CARTESIAN_POINT('',(-2.49052926869774,1.16608917401711,8.75721825406948));
#377459=CARTESIAN_POINT('',(-2.49052926869774,1.16608917401711,9.));
#377460=CARTESIAN_POINT('',(-2.46450482787546,1.22012948221842,8.75721825406948));
#377461=CARTESIAN_POINT('Origin',(0.,1.84795814293585E-15,8.75721825406948));
#377462=CARTESIAN_POINT('',(-2.46450482787546,1.22012948221842,7.51860402984325));
#377463=CARTESIAN_POINT('',(-2.46450482787546,1.22012948221842,9.));
#377464=CARTESIAN_POINT('',(-2.45601536992579,1.23712913743404,7.49482233047033));
#377465=CARTESIAN_POINT('Origin',(-2.45180719829502,1.24543859666924,7.53025004711375));
#377466=CARTESIAN_POINT('',(-2.41978630452753,1.30657347302821,7.49482233047033));
#377467=CARTESIAN_POINT('Origin',(-1.63839840773326E-15,8.54751399870172E-16,
7.49482233047033));
#377468=CARTESIAN_POINT('',(-2.41070061931037,1.3232620768603,7.51860402984325));
#377469=CARTESIAN_POINT('Origin',(-2.42421892276653,1.29832173752101,7.53030836256776));
#377470=CARTESIAN_POINT('',(-2.41070061931037,1.32326207686029,8.75721825406948));
#377471=CARTESIAN_POINT('',(-2.41070061931037,1.32326207686029,9.));
#377472=CARTESIAN_POINT('',(-2.38126727405858,1.37552396180423,8.75721825406948));
#377473=CARTESIAN_POINT('Origin',(0.,1.84795814293585E-15,8.75721825406948));
#377474=CARTESIAN_POINT('',(-2.38126727405858,1.37552396180423,7.51860402984325));
#377475=CARTESIAN_POINT('',(-2.38126727405859,1.37552396180423,9.));
#377476=CARTESIAN_POINT('',(-2.37170608696151,1.39194476796666,7.49482233047033));
#377477=CARTESIAN_POINT('Origin',(-2.36697417258968,1.39996753604437,7.53025004711349));
#377478=CARTESIAN_POINT('',(-2.33110214420573,1.45892521853571,7.49482233047033));
#377479=CARTESIAN_POINT('Origin',(-1.58026803226839E-15,9.57967767846859E-16,
7.49482233047033));
#377480=CARTESIAN_POINT('',(-2.32096588398459,1.47499741199083,7.51860402984325));
#377481=CARTESIAN_POINT('Origin',(-2.33605434566413,1.45097443593007,7.5303083625673));
#377482=CARTESIAN_POINT('',(-2.32096588398459,1.47499741199083,8.75721825406948));
#377483=CARTESIAN_POINT('',(-2.32096588398459,1.47499741199083,9.));
#377484=CARTESIAN_POINT('',(-2.28824458223238,1.52526611838203,8.75721825406948));
#377485=CARTESIAN_POINT('Origin',(0.,1.84795814293585E-15,8.75721825406948));
#377486=CARTESIAN_POINT('',(-2.28824458223238,1.52526611838203,7.51860402984325));
#377487=CARTESIAN_POINT('',(-2.28824458223238,1.52526611838203,9.));
#377488=CARTESIAN_POINT('',(-2.27765095495654,1.54104059887648,7.49482233047033));
#377489=CARTESIAN_POINT('Origin',(-2.27241474229455,1.54874370852221,7.53025004711377));
#377490=CARTESIAN_POINT('',(-2.23283898515355,1.60528192738176,7.49482233047033));
#377491=CARTESIAN_POINT('Origin',(-1.5156439964925E-15,1.05724764078202E-15,
7.49482233047033));
#377492=CARTESIAN_POINT('',(-2.2216938019959,1.62067166636954,7.51860402984325));
#377493=CARTESIAN_POINT('Origin',(-2.23829042017338,1.59766476914869,7.53030836256704));
#377494=CARTESIAN_POINT('',(-2.2216938019959,1.62067166636954,8.75721825406948));
#377495=CARTESIAN_POINT('',(-2.2216938019959,1.62067166636954,9.));
#377496=CARTESIAN_POINT('',(-2.18581900259086,1.66874062931084,8.75721825406948));
#377497=CARTESIAN_POINT('Origin',(0.,1.84795814293585E-15,8.75721825406948));
#377498=CARTESIAN_POINT('',(-2.18581900259086,1.66874062931084,7.51860402984325));
#377499=CARTESIAN_POINT('',(-2.18581900259086,1.66874062931084,9.));
#377500=CARTESIAN_POINT('',(-2.17423646662305,1.68380396341335,7.49482233047033));
#377501=CARTESIAN_POINT('Origin',(-2.16851747239199,1.69115576089708,7.53025004711385));
#377502=CARTESIAN_POINT('',(-2.1254006117689,1.74504218845631,7.49482233047033));
#377503=CARTESIAN_POINT('Origin',(-1.4447918544304E-15,1.1521830563823E-15,
7.49482233047033));
#377504=CARTESIAN_POINT('',(-2.11329230362298,1.75968623323816,7.51860402984325));
#377505=CARTESIAN_POINT('Origin',(-2.1313288792346,1.7377899551325,7.53030836256739));
#377506=CARTESIAN_POINT('',(-2.11329230362298,1.75968623323815,8.75721825406948));
#377507=CARTESIAN_POINT('',(-2.11329230362298,1.75968623323815,9.));
#377508=CARTESIAN_POINT('',(-2.07441142381098,1.80535792705007,8.75721825406948));
#377509=CARTESIAN_POINT('Origin',(0.,1.84795814293585E-15,8.75721825406948));
#377510=CARTESIAN_POINT('',(-2.07441142381098,1.80535792705007,7.51860402984325));
#377511=CARTESIAN_POINT('',(-2.07441142381098,1.80535792705007,9.));
#377512=CARTESIAN_POINT('',(-2.06188757427596,1.81964821628974,7.49482233047033));
#377513=CARTESIAN_POINT('Origin',(-2.05570929905008,1.82661849149836,7.53025004711345));
#377514=CARTESIAN_POINT('',(-2.0092285113735,1.87763169686811,7.49482233047033));
#377515=CARTESIAN_POINT('Origin',(-1.36800275273157E-15,1.24238390466142E-15,
7.49482233047033));
#377516=CARTESIAN_POINT('',(-1.9962068338747,1.89146987192289,7.51860402984325));
#377517=CARTESIAN_POINT('Origin',(-2.01560925076225,1.87077418943615,7.53030836256727));
#377518=CARTESIAN_POINT('',(-1.9962068338747,1.89146987192288,8.75721825406948));
#377519=CARTESIAN_POINT('',(-1.9962068338747,1.89146987192288,9.));
#377520=CARTESIAN_POINT('',(-1.95447964353081,1.93455662181898,8.75721825406948));
#377521=CARTESIAN_POINT('Origin',(0.,1.84795814293585E-15,8.75721825406948));
#377522=CARTESIAN_POINT('',(-1.95447964353081,1.93455662181898,7.51860402984325));
#377523=CARTESIAN_POINT('',(-1.95447964353081,1.93455662181899,9.));
#377524=CARTESIAN_POINT('',(-1.94106594361266,1.94801514433207,7.49482233047033));
#377525=CARTESIAN_POINT('Origin',(-1.93445377525002,1.95457525490979,7.53025004711328));
#377526=CARTESIAN_POINT('',(-1.88480006004671,2.00250561388675,7.49482233047033));
#377527=CARTESIAN_POINT('Origin',(-1.2855922342861E-15,1.32747953098577E-15,
7.49482233047033));
#377528=CARTESIAN_POINT('',(-1.870918522061,2.01548105518487,7.51860402984325));
#377529=CARTESIAN_POINT('Origin',(-1.89160705153176,1.99607101131553,7.5303083625673));
#377530=CARTESIAN_POINT('',(-1.870918522061,2.01548105518486,8.75721825406948));
#377531=CARTESIAN_POINT('',(-1.870918522061,2.01548105518486,9.));
#377532=CARTESIAN_POINT('',(-1.82651648716081,2.05580580846776,8.75721825406948));
#377533=CARTESIAN_POINT('Origin',(0.,1.84795814293585E-15,8.75721825406948));
#377534=CARTESIAN_POINT('',(-1.82651648716081,2.05580580846776,7.51860402984325));
#377535=CARTESIAN_POINT('',(-1.82651648716081,2.05580580846776,9.));
#377536=CARTESIAN_POINT('',(-1.81226805662972,2.0683772602984,7.49482233047033));
#377537=CARTESIAN_POINT('Origin',(-1.80524916594807,2.07450024934405,7.53025004711367));
#377538=CARTESIAN_POINT('',(-1.75262656098483,2.11915080580182,7.49482233047033));
#377539=CARTESIAN_POINT('Origin',(-1.19789894159127E-15,1.40712025917383E-15,
7.49482233047033));
#377540=CARTESIAN_POINT('',(-1.73794220472939,2.13121019447176,7.51860402984325));
#377541=CARTESIAN_POINT('Origin',(-1.75983183317789,2.11316554925368,7.53030836256706));
#377542=CARTESIAN_POINT('',(-1.73794220472939,2.13121019447176,8.75721825406948));
#377543=CARTESIAN_POINT('',(-1.73794220472939,2.13121019447176,9.));
#377544=CARTESIAN_POINT('',(-1.6910477827585,2.16860724808057,8.75721825406948));
#377545=CARTESIAN_POINT('Origin',(0.,1.84795814293585E-15,8.75721825406948));
#377546=CARTESIAN_POINT('',(-1.6910477827585,2.16860724808057,7.51860402984325));
#377547=CARTESIAN_POINT('',(-1.6910477827585,2.16860724808057,9.));
#377548=CARTESIAN_POINT('',(-1.67602317147181,2.18023997043664,7.49482233047033));
#377549=CARTESIAN_POINT('Origin',(-1.66862640059877,2.1859006772746,7.53025004711366));
#377550=CARTESIAN_POINT('',(-1.61325114344665,2.22708795249943,7.49482233047033));
#377551=CARTESIAN_POINT('Origin',(-1.10528322519692E-15,1.4809788283906E-15,
7.49482233047033));
#377552=CARTESIAN_POINT('',(-1.59782431009111,2.23818173392642,7.51860402984325));
#377553=CARTESIAN_POINT('Origin',(-1.62082508833914,2.22157663667705,7.53030836256742));
#377554=CARTESIAN_POINT('',(-1.59782431009111,2.23818173392642,8.75721825406948));
#377555=CARTESIAN_POINT('',(-1.59782431009111,2.23818173392642,9.));
#377556=CARTESIAN_POINT('',(-1.54863020028822,2.27249741534622,8.75721825406948));
#377557=CARTESIAN_POINT('Origin',(0.,1.84795814293585E-15,8.75721825406948));
#377558=CARTESIAN_POINT('',(-1.54863020028822,2.27249741534622,7.51860402984325));
#377559=CARTESIAN_POINT('',(-1.54863020028822,2.27249741534622,9.));
#377560=CARTESIAN_POINT('',(-1.53289114759649,2.28314360687635,7.49482233047033));
#377561=CARTESIAN_POINT('Origin',(-1.52514689144989,2.28831877044818,7.53025004711401));
#377562=CARTESIAN_POINT('',(-1.46724653091876,2.32587351709135,7.49482233047033));
#377563=CARTESIAN_POINT('Origin',(-1.00812566294774E-15,1.54875173793255E-15,
7.49482233047033));
#377564=CARTESIAN_POINT('',(-1.45114061263043,2.3359561045479,7.51860402984325));
#377565=CARTESIAN_POINT('Origin',(-1.47515802554598,2.32085878917399,7.53030836256696));
#377566=CARTESIAN_POINT('',(-1.45114061263043,2.3359561045479,8.75721825406948));
#377567=CARTESIAN_POINT('',(-1.45114061263043,2.3359561045479,9.));
#377568=CARTESIAN_POINT('',(-1.39984896414483,2.36704940328305,8.75721825406948));
#377569=CARTESIAN_POINT('Origin',(0.,1.84795814293585E-15,8.75721825406948));
#377570=CARTESIAN_POINT('',(-1.39984896414483,2.36704940328305,7.51860402984325));
#377571=CARTESIAN_POINT('',(-1.39984896414483,2.36704940328305,9.));
#377572=CARTESIAN_POINT('',(-1.38346014519156,2.37666531650263,7.49482233047033));
#377573=CARTESIAN_POINT('Origin',(-1.37540022658174,2.38133367095072,7.5302500471134));
#377574=CARTESIAN_POINT('',(-1.31521268767194,2.41510156850323,7.49482233047033));
#377575=CARTESIAN_POINT('Origin',(-9.06825496107225E-16,1.61016049437713E-15,
7.49482233047033));
#377576=CARTESIAN_POINT('',(-1.29849386712376,2.42413153047478,7.51860402984325));
#377577=CARTESIAN_POINT('Origin',(-1.3234292220062,2.4106040350831,7.53030836256761));
#377578=CARTESIAN_POINT('',(-1.29849386712377,2.42413153047478,8.75721825406948));
#377579=CARTESIAN_POINT('',(-1.29849386712377,2.42413153047478,9.));
#377580=CARTESIAN_POINT('',(-1.2453154483411,2.45187467749129,8.75721825406948));
#377581=CARTESIAN_POINT('Origin',(0.,1.84795814293585E-15,8.75721825406948));
#377582=CARTESIAN_POINT('',(-1.2453154483411,2.45187467749129,7.51860402984325));
#377583=CARTESIAN_POINT('',(-1.2453154483411,2.45187467749129,9.));
#377584=CARTESIAN_POINT('',(-1.22834420829878,2.46042079855029,7.49482233047033));
#377585=CARTESIAN_POINT('Origin',(-1.22000174715945,2.46456316060527,7.53025004711378));
#377586=CARTESIAN_POINT('',(-1.15777435337923,2.49440544953248,7.49482233047033));
#377587=CARTESIAN_POINT('Origin',(-8.01798988789747E-16,1.66495275597197E-15,
7.49482233047033));
#377588=CARTESIAN_POINT('',(-1.14051133179102,2.50234567996835,7.51860402984325));
#377589=CARTESIAN_POINT('Origin',(-1.16626216391795,2.49044359193945,7.53030836256741));
#377590=CARTESIAN_POINT('',(-1.14051133179103,2.50234567996835,8.75721825406948));
#377591=CARTESIAN_POINT('',(-1.14051133179103,2.50234567996835,9.));
#377592=CARTESIAN_POINT('',(-1.08566466424082,2.52662467272424,8.75721825406948));
#377593=CARTESIAN_POINT('Origin',(0.,1.84795814293585E-15,8.75721825406948));
#377594=CARTESIAN_POINT('',(-1.08566466424082,2.52662467272424,7.51860402984325));
#377595=CARTESIAN_POINT('',(-1.08566466424082,2.52662467272424,9.));
#377596=CARTESIAN_POINT('',(-1.06818074157508,2.53406588377811,7.49482233047033));
#377597=CARTESIAN_POINT('Origin',(-1.05959001886869,2.53766523158564,7.53025004711391));
#377598=CARTESIAN_POINT('',(-0.995578475926665,2.5634592835213,7.49482233047033));
#377599=CARTESIAN_POINT('Origin',(-6.93477717441988E-16,1.71290336956127E-15,
7.49482233047033));
#377600=CARTESIAN_POINT('',(-0.977842190757043,2.57027715431147,7.51860402984325));
#377601=CARTESIAN_POINT('Origin',(-1.00430268443603,2.56004938187791,7.53030836256769));
#377602=CARTESIAN_POINT('',(-0.977842190757048,2.57027715431147,8.75721825406948));
#377603=CARTESIAN_POINT('',(-0.977842190757048,2.57027715431147,9.));
#377604=CARTESIAN_POINT('',(-0.921552651160823,2.59099222521768,8.75721825406948));
#377605=CARTESIAN_POINT('Origin',(0.,1.84795814293585E-15,8.75721825406948));
#377606=CARTESIAN_POINT('',(-0.921552651160823,2.59099222521768,7.51860402984325));
#377607=CARTESIAN_POINT('',(-0.921552651160823,2.59099222521768,9.));
#377608=CARTESIAN_POINT('',(-0.90362789106021,2.59729794873405,7.49482233047033));
#377609=CARTESIAN_POINT('Origin',(-0.894824207909214,2.60033949180186,7.53025004711383));
#377610=CARTESIAN_POINT('',(-0.829291552965606,2.62197931345385,7.49482233047033));
#377611=CARTESIAN_POINT('Origin',(-5.82306797402756E-16,1.75381529578843E-15,
7.49482233047033));
#377612=CARTESIAN_POINT('',(-0.811154886414749,2.62764680850481,7.51860402984325));
#377613=CARTESIAN_POINT('Origin',(-0.838216309801102,2.61913537977751,7.5303083625674));
#377614=CARTESIAN_POINT('',(-0.811154886414754,2.6276468085048,8.75721825406948));
#377615=CARTESIAN_POINT('',(-0.811154886414754,2.6276468085048,9.));
#377616=CARTESIAN_POINT('',(-0.753653780564787,2.64471283489161,8.75721825406948));
#377617=CARTESIAN_POINT('Origin',(0.,1.84795814293585E-15,8.75721825406948));
#377618=CARTESIAN_POINT('',(-0.753653780564787,2.64471283489161,7.51860402984325));
#377619=CARTESIAN_POINT('',(-0.753653780564787,2.64471283489161,9.));
#377620=CARTESIAN_POINT('',(-0.735361839713394,2.64985715929998,7.49482233047033));
#377621=CARTESIAN_POINT('Origin',(-0.726381372340318,2.6523283992752,7.53025004711367));
#377622=CARTESIAN_POINT('',(-0.659596893130931,2.66972506797461,7.49482233047033));
#377623=CARTESIAN_POINT('Origin',(-4.6874305382858E-16,1.78752041877299E-15,
7.49482233047033));
#377624=CARTESIAN_POINT('',(-0.641134372652,2.67421889833352,7.51860402984325));
#377625=CARTESIAN_POINT('Origin',(-0.668685524552393,2.6674587885988,7.53030836256714));
#377626=CARTESIAN_POINT('',(-0.641134372652005,2.67421889833352,8.75721825406948));
#377627=CARTESIAN_POINT('',(-0.641134372652005,2.67421889833352,9.));
#377628=CARTESIAN_POINT('',(-0.582657984926182,2.68756575223785,8.75721825406948));
#377629=CARTESIAN_POINT('Origin',(0.,1.84795814293585E-15,8.75721825406948));
#377630=CARTESIAN_POINT('',(-0.582657984926182,2.68756575223785,7.51860402984325));
#377631=CARTESIAN_POINT('',(-0.582657984926182,2.68756575223785,9.));
#377632=CARTESIAN_POINT('',(-0.564074028832576,2.69152753840577,7.49482233047033));
#377633=CARTESIAN_POINT('Origin',(-0.554953679903967,2.69341832043331,7.53025004711374));
#377634=CARTESIAN_POINT('',(-0.487191808179291,2.70650034953684,7.49482233047033));
#377635=CARTESIAN_POINT('Origin',(-3.53253144501152E-16,1.81388023693489E-15,
7.49482233047033));
#377636=CARTESIAN_POINT('',(-0.468479300229132,2.70980204909083,7.51860402984325));
#377637=CARTESIAN_POINT('Origin',(-0.496406967051098,2.70482103708951,7.5303083625674));
#377638=CARTESIAN_POINT('',(-0.468479300229137,2.70980204909082,8.75721825406948));
#377639=CARTESIAN_POINT('',(-0.468479300229137,2.70980204909082,9.));
#377640=CARTESIAN_POINT('',(-0.409267922647769,2.71937488542709,8.75721825406948));
#377641=CARTESIAN_POINT('Origin',(0.,1.84795814293585E-15,8.75721825406948));
#377642=CARTESIAN_POINT('',(-0.409267922647769,2.71937488542709,7.51860402984325));
#377643=CARTESIAN_POINT('',(-0.409267922647769,2.71937488542709,9.));
#377644=CARTESIAN_POINT('',(-0.390468316773785,2.7221378535254,7.49482233047033));
#377645=CARTESIAN_POINT('Origin',(-0.381245563760008,2.72344040797629,7.53025004711346));
#377646=CARTESIAN_POINT('',(-0.312784747585528,2.73215404062031,7.49482233047033));
#377647=CARTESIAN_POINT('Origin',(-2.36311642230408E-16,1.83278643212713E-15,
7.49482233047033));
#377648=CARTESIAN_POINT('',(-0.293899145873127,2.7342500419777,7.51860402984325));
#377649=CARTESIAN_POINT('Origin',(-0.322088566843094,2.73106859575658,7.53030836256749));
#377650=CARTESIAN_POINT('',(-0.293899145873133,2.7342500419777,8.75721825406948));
#377651=CARTESIAN_POINT('',(-0.293899145873133,2.7342500419777,9.));
#377652=CARTESIAN_POINT('',(-0.234196090687502,2.74000952390803,8.75721825406948));
#377653=CARTESIAN_POINT('Origin',(0.,1.84795814293585E-15,8.75721825406948));
#377654=CARTESIAN_POINT('',(-0.234196090687502,2.74000952390803,7.51860402984325));
#377655=CARTESIAN_POINT('',(-0.234196090687502,2.74000952390803,9.));
#377656=CARTESIAN_POINT('',(-0.215258086646179,2.74156232030816,7.49482233047033));
#377657=CARTESIAN_POINT('Origin',(-0.205970827817116,2.74227129470683,7.53025004711379));
#377658=CARTESIAN_POINT('',(-0.137092387371817,2.74658072470567,7.49482233047033));
#377659=CARTESIAN_POINT('Origin',(-1.1839908473305E-16,1.8441613147383E-15,
7.49482233047033));
#377660=CARTESIAN_POINT('',(-0.118111296885561,2.7474624149473,7.51860402984325));
#377661=CARTESIAN_POINT('Origin',(-0.146446635625942,2.74609360775133,7.53030836256732));
#377662=CARTESIAN_POINT('',(-0.118111296885567,2.74746241494729,8.75721825406948));
#377663=CARTESIAN_POINT('',(-0.118111296885567,2.74746241494729,9.));
#377664=CARTESIAN_POINT('',(-0.058161896755696,2.74938487552503,8.75721825406948));
#377665=CARTESIAN_POINT('Origin',(0.,1.84795814293585E-15,8.75721825406948));
#377666=CARTESIAN_POINT('',(-0.058161896755696,2.74938487552503,7.51860402984325));
#377667=CARTESIAN_POINT('',(-0.058161896755696,2.74938487552503,9.));
#377668=CARTESIAN_POINT('',(-0.0391633148678293,2.74972111945349,7.49482233047033));
#377669=CARTESIAN_POINT('Origin',(-0.0298497135624777,2.74983360047203,
7.5302500471137));
#377670=CARTESIAN_POINT('',(0.0391633148678293,2.74972111945349,7.49482233047033));
#377671=CARTESIAN_POINT('Origin',(0.,1.84795814293585E-15,7.49482233047033));
#377672=CARTESIAN_POINT('',(0.058161896755696,2.74938487552503,7.51860402984325));
#377673=CARTESIAN_POINT('Origin',(0.0297970762297926,2.74983433207657,7.530308362567));
#377674=CARTESIAN_POINT('',(0.058161896755696,2.74938487552503,8.75721825406948));
#377675=CARTESIAN_POINT('',(0.058161896755696,2.74938487552503,9.));
#377676=CARTESIAN_POINT('',(0.118111296885527,2.7474624149473,8.75721825406948));
#377677=CARTESIAN_POINT('Origin',(0.,1.84795814293585E-15,8.75721825406948));
#377678=CARTESIAN_POINT('',(0.118111296885527,2.7474624149473,7.51860402984325));
#377679=CARTESIAN_POINT('',(0.118111296885527,2.7474624149473,9.));
#377680=CARTESIAN_POINT('',(0.137092387371777,2.74658072470567,7.49482233047033));
#377681=CARTESIAN_POINT('Origin',(0.146394059568022,2.74609625013544,7.53025004711377));
#377682=CARTESIAN_POINT('',(0.21525808664614,2.74156232030816,7.49482233047033));
#377683=CARTESIAN_POINT('Origin',(1.18399084733023E-16,1.8441613147383E-15,
7.49482233047033));
#377684=CARTESIAN_POINT('',(0.234196090687467,2.74000952390803,7.51860402984325));
#377685=CARTESIAN_POINT('Origin',(0.205918345507194,2.74227539729373,7.53030836256749));
#377686=CARTESIAN_POINT('',(0.234196090687462,2.74000952390803,8.75721825406948));
#377687=CARTESIAN_POINT('',(0.234196090687462,2.74000952390803,9.));
#377688=CARTESIAN_POINT('',(0.293899145873092,2.7342500419777,8.75721825406948));
#377689=CARTESIAN_POINT('Origin',(0.,1.84795814293585E-15,8.75721825406948));
#377690=CARTESIAN_POINT('',(0.293899145873092,2.7342500419777,7.51860402984325));
#377691=CARTESIAN_POINT('',(0.293899145873092,2.7342500419777,9.));
#377692=CARTESIAN_POINT('',(0.312784747585487,2.73215404062031,7.49482233047033));
#377693=CARTESIAN_POINT('Origin',(0.322036268106352,2.73107460127124,7.53025004711382));
#377694=CARTESIAN_POINT('',(0.390468316773744,2.7221378535254,7.49482233047033));
#377695=CARTESIAN_POINT('Origin',(2.3631164223038E-16,1.83278643212713E-15,
7.49482233047033));
#377696=CARTESIAN_POINT('',(0.409267922647734,2.71937488542709,7.51860402984325));
#377697=CARTESIAN_POINT('Origin',(0.38119345213415,2.72344786468714,7.5303083625673));
#377698=CARTESIAN_POINT('',(0.409267922647728,2.71937488542709,8.75721825406948));
#377699=CARTESIAN_POINT('',(0.409267922647728,2.71937488542709,9.));
#377700=CARTESIAN_POINT('',(0.468479300229098,2.70980204909083,8.75721825406948));
#377701=CARTESIAN_POINT('Origin',(0.,1.84795814293585E-15,8.75721825406948));
#377702=CARTESIAN_POINT('',(0.468479300229098,2.70980204909083,7.51860402984325));
#377703=CARTESIAN_POINT('',(0.468479300229098,2.70980204909083,9.));
#377704=CARTESIAN_POINT('',(0.487191808179253,2.70650034953684,7.49482233047033));
#377705=CARTESIAN_POINT('Origin',(0.496355160542298,2.70483038105678,7.53025004711366));
#377706=CARTESIAN_POINT('',(0.564074028832537,2.69152753840577,7.49482233047033));
#377707=CARTESIAN_POINT('Origin',(3.53253144501126E-16,1.81388023693489E-15,
7.49482233047033));
#377708=CARTESIAN_POINT('',(0.582657984926149,2.68756575223785,7.51860402984325));
#377709=CARTESIAN_POINT('Origin',(0.554902153100358,2.69342910062683,7.53030836256731));
#377710=CARTESIAN_POINT('',(0.582657984926143,2.68756575223785,8.75721825406948));
#377711=CARTESIAN_POINT('',(0.582657984926143,2.68756575223785,9.));
#377712=CARTESIAN_POINT('',(0.641134372651966,2.67421889833353,8.75721825406948));
#377713=CARTESIAN_POINT('Origin',(0.,1.84795814293585E-15,8.75721825406948));
#377714=CARTESIAN_POINT('',(0.641134372651966,2.67421889833353,7.51860402984325));
#377715=CARTESIAN_POINT('',(0.641134372651966,2.67421889833353,9.));
#377716=CARTESIAN_POINT('',(0.659596893130892,2.66972506797462,7.49482233047033));
#377717=CARTESIAN_POINT('Origin',(0.668634423155899,2.66747143262223,7.5302500471137));
#377718=CARTESIAN_POINT('',(0.735361839713355,2.64985715929999,7.49482233047033));
#377719=CARTESIAN_POINT('Origin',(4.68743053828553E-16,1.787520418773E-15,
7.49482233047033));
#377720=CARTESIAN_POINT('',(0.753653780564754,2.64471283489162,7.51860402984325));
#377721=CARTESIAN_POINT('Origin',(0.726330642093246,2.65234245865335,7.53030836256748));
#377722=CARTESIAN_POINT('',(0.753653780564748,2.64471283489162,8.75721825406948));
#377723=CARTESIAN_POINT('',(0.753653780564749,2.64471283489162,9.));
#377724=CARTESIAN_POINT('',(0.811154886414717,2.62764680850482,8.75721825406948));
#377725=CARTESIAN_POINT('Origin',(0.,1.84795814293585E-15,8.75721825406948));
#377726=CARTESIAN_POINT('',(0.811154886414717,2.62764680850482,7.51860402984325));
#377727=CARTESIAN_POINT('',(0.811154886414717,2.62764680850482,9.));
#377728=CARTESIAN_POINT('',(0.829291552965569,2.62197931345386,7.49482233047033));
#377729=CARTESIAN_POINT('Origin',(0.838166123502919,2.61915127190027,7.53025004711349));
#377730=CARTESIAN_POINT('',(0.903627891060173,2.59729794873406,7.49482233047033));
#377731=CARTESIAN_POINT('Origin',(5.82306797402731E-16,1.75381529578844E-15,
7.49482233047033));
#377732=CARTESIAN_POINT('',(0.921552651160791,2.59099222521769,7.51860402984325));
#377733=CARTESIAN_POINT('Origin',(0.894774482680453,2.60035677259156,7.53030836256745));
#377734=CARTESIAN_POINT('',(0.921552651160786,2.59099222521769,8.75721825406948));
#377735=CARTESIAN_POINT('',(0.921552651160786,2.5909922252177,9.));
#377736=CARTESIAN_POINT('',(0.97784219075701,2.57027715431148,8.75721825406948));
#377737=CARTESIAN_POINT('Origin',(0.,1.84795814293585E-15,8.75721825406948));
#377738=CARTESIAN_POINT('',(0.97784219075701,2.57027715431148,7.51860402984325));
#377739=CARTESIAN_POINT('',(0.97784219075701,2.57027715431149,9.));
#377740=CARTESIAN_POINT('',(0.995578475926628,2.56345928352132,7.49482233047033));
#377741=CARTESIAN_POINT('Origin',(1.00425361946275,2.56006845679578,7.53025004711372));
#377742=CARTESIAN_POINT('',(1.06818074157505,2.53406588377812,7.49482233047033));
#377743=CARTESIAN_POINT('Origin',(6.93477717441963E-16,1.71290336956128E-15,
7.49482233047033));
#377744=CARTESIAN_POINT('',(1.08566466424078,2.52662467272426,7.51860402984325));
#377745=CARTESIAN_POINT('Origin',(1.05954150299006,2.53768566277631,7.53030836256713));
#377746=CARTESIAN_POINT('',(1.08566466424078,2.52662467272426,8.75721825406948));
#377747=CARTESIAN_POINT('',(1.08566466424078,2.52662467272426,9.));
#377748=CARTESIAN_POINT('',(1.14051133179099,2.50234567996837,8.75721825406948));
#377749=CARTESIAN_POINT('Origin',(0.,1.84795814293585E-15,8.75721825406948));
#377750=CARTESIAN_POINT('',(1.14051133179099,2.50234567996837,7.51860402984325));
#377751=CARTESIAN_POINT('',(1.14051133179099,2.50234567996837,9.));
#377752=CARTESIAN_POINT('',(1.15777435337919,2.49440544953249,7.49482233047033));
#377753=CARTESIAN_POINT('Origin',(1.16621442188813,2.49046577126948,7.5302500471135));
#377754=CARTESIAN_POINT('',(1.22834420829874,2.46042079855031,7.49482233047033));
#377755=CARTESIAN_POINT('Origin',(8.01798988789723E-16,1.66495275597198E-15,
7.49482233047033));
#377756=CARTESIAN_POINT('',(1.24531544834107,2.4518746774913,7.51860402984325));
#377757=CARTESIAN_POINT('Origin',(1.21995463999246,2.46458665824104,7.53030836256742));
#377758=CARTESIAN_POINT('',(1.24531544834107,2.45187467749131,8.75721825406948));
#377759=CARTESIAN_POINT('',(1.24531544834107,2.45187467749131,9.));
#377760=CARTESIAN_POINT('',(1.29849386712373,2.4241315304748,8.75721825406948));
#377761=CARTESIAN_POINT('Origin',(0.,1.84795814293585E-15,8.75721825406948));
#377762=CARTESIAN_POINT('',(1.29849386712373,2.4241315304748,7.51860402984325));
#377763=CARTESIAN_POINT('',(1.29849386712373,2.4241315304748,9.));
#377764=CARTESIAN_POINT('',(1.3152126876719,2.41510156850325,7.49482233047033));
#377765=CARTESIAN_POINT('Origin',(1.3233829991019,2.41062922768575,7.53025004711348));
#377766=CARTESIAN_POINT('',(1.38346014519153,2.37666531650265,7.49482233047033));
#377767=CARTESIAN_POINT('Origin',(9.06825496107201E-16,1.61016049437714E-15,
7.49482233047033));
#377768=CARTESIAN_POINT('',(1.3998489641448,2.36704940328307,7.51860402984325));
#377769=CARTESIAN_POINT('Origin',(1.37535472169997,2.38136013847475,7.53030836256734));
#377770=CARTESIAN_POINT('',(1.3998489641448,2.36704940328307,8.75721825406948));
#377771=CARTESIAN_POINT('',(1.3998489641448,2.36704940328307,9.));
#377772=CARTESIAN_POINT('',(1.4511406126304,2.33595610454792,8.75721825406948));
#377773=CARTESIAN_POINT('Origin',(0.,1.84795814293585E-15,8.75721825406948));
#377774=CARTESIAN_POINT('',(1.4511406126304,2.33595610454792,7.51860402984325));
#377775=CARTESIAN_POINT('',(1.4511406126304,2.33595610454792,9.));
#377776=CARTESIAN_POINT('',(1.46724653091873,2.32587351709137,7.49482233047033));
#377777=CARTESIAN_POINT('Origin',(1.47511351170756,2.32088689152714,7.53025004711339));
#377778=CARTESIAN_POINT('',(1.53289114759645,2.28314360687637,7.49482233047033));
#377779=CARTESIAN_POINT('Origin',(1.00812566294772E-15,1.54875173793256E-15,
7.49482233047033));
#377780=CARTESIAN_POINT('',(1.5486302002882,2.27249741534624,7.51860402984325));
#377781=CARTESIAN_POINT('Origin',(1.52510317584322,2.28834809909939,7.5303083625674));
#377782=CARTESIAN_POINT('',(1.54863020028819,2.27249741534625,8.75721825406948));
#377783=CARTESIAN_POINT('',(1.54863020028819,2.27249741534625,9.));
#377784=CARTESIAN_POINT('',(1.59782431009108,2.23818173392644,8.75721825406948));
#377785=CARTESIAN_POINT('Origin',(0.,1.84795814293585E-15,8.75721825406948));
#377786=CARTESIAN_POINT('',(1.59782431009108,2.23818173392644,7.51860402984325));
#377787=CARTESIAN_POINT('',(1.59782431009108,2.23818173392644,9.));
#377788=CARTESIAN_POINT('',(1.61325114344662,2.22708795249945,7.49482233047033));
#377789=CARTESIAN_POINT('Origin',(1.62078246648304,2.22160753330238,7.53025004711372));
#377790=CARTESIAN_POINT('',(1.67602317147178,2.18023997043667,7.49482233047033));
#377791=CARTESIAN_POINT('Origin',(1.1052832251969E-15,1.48097882839062E-15,
7.49482233047033));
#377792=CARTESIAN_POINT('',(1.69104778275847,2.16860724808059,7.51860402984325));
#377793=CARTESIAN_POINT('Origin',(1.66858465390346,2.18593274653562,7.53030836256734));
#377794=CARTESIAN_POINT('',(1.69104778275847,2.16860724808059,8.75721825406948));
#377795=CARTESIAN_POINT('',(1.69104778275847,2.16860724808059,9.));
#377796=CARTESIAN_POINT('',(1.73794220472936,2.13121019447178,8.75721825406948));
#377797=CARTESIAN_POINT('Origin',(0.,1.84795814293585E-15,8.75721825406948));
#377798=CARTESIAN_POINT('',(1.73794220472936,2.13121019447178,7.51860402984325));
#377799=CARTESIAN_POINT('',(1.73794220472936,2.13121019447179,9.));
#377800=CARTESIAN_POINT('',(1.7526265609848,2.11915080580184,7.49482233047033));
#377801=CARTESIAN_POINT('Origin',(1.75979127844668,2.11319911319018,7.53025004711357));
#377802=CARTESIAN_POINT('',(1.8122680566297,2.06837726029843,7.49482233047033));
#377803=CARTESIAN_POINT('Origin',(1.19789894159125E-15,1.40712025917385E-15,
7.49482233047033));
#377804=CARTESIAN_POINT('',(1.82651648716078,2.05580580846778,7.51860402984325));
#377805=CARTESIAN_POINT('Origin',(1.80520955971042,2.0745349274353,7.53030836256737));
#377806=CARTESIAN_POINT('',(1.82651648716078,2.05580580846778,8.75721825406948));
#377807=CARTESIAN_POINT('',(1.82651648716078,2.05580580846778,9.));
#377808=CARTESIAN_POINT('',(1.87091852206097,2.01548105518489,8.75721825406948));
#377809=CARTESIAN_POINT('Origin',(0.,1.84795814293585E-15,8.75721825406948));
#377810=CARTESIAN_POINT('',(1.87091852206097,2.01548105518489,7.51860402984325));
#377811=CARTESIAN_POINT('',(1.87091852206097,2.01548105518489,9.));
#377812=CARTESIAN_POINT('',(1.88480006004668,2.00250561388678,7.49482233047033));
#377813=CARTESIAN_POINT('Origin',(1.89156873057342,1.99610710464183,7.53025004711385));
#377814=CARTESIAN_POINT('',(1.94106594361263,1.9480151443321,7.49482233047033));
#377815=CARTESIAN_POINT('Origin',(1.28559223428608E-15,1.32747953098579E-15,
7.49482233047033));
#377816=CARTESIAN_POINT('',(1.95447964353079,1.93455662181901,7.51860402984325));
#377817=CARTESIAN_POINT('Origin',(1.93441647222035,1.95461239933176,7.53030836256736));
#377818=CARTESIAN_POINT('',(1.95447964353078,1.93455662181901,8.75721825406948));
#377819=CARTESIAN_POINT('',(1.95447964353078,1.93455662181901,9.));
#377820=CARTESIAN_POINT('',(1.99620683387467,1.89146987192291,8.75721825406948));
#377821=CARTESIAN_POINT('Origin',(0.,1.84795814293585E-15,8.75721825406948));
#377822=CARTESIAN_POINT('',(1.99620683387467,1.89146987192291,7.51860402984325));
#377823=CARTESIAN_POINT('',(1.99620683387467,1.89146987192291,9.));
#377824=CARTESIAN_POINT('',(2.00922851137348,1.87763169686814,7.49482233047033));
#377825=CARTESIAN_POINT('Origin',(2.01557332104575,1.87081266383712,7.53025004711375));
#377826=CARTESIAN_POINT('',(2.06188757427593,1.81964821628977,7.49482233047033));
#377827=CARTESIAN_POINT('Origin',(1.36800275273155E-15,1.24238390466144E-15,
7.49482233047033));
#377828=CARTESIAN_POINT('',(2.07441142381096,1.80535792705009,7.51860402984325));
#377829=CARTESIAN_POINT('Origin',(2.05567445251497,1.82665794961622,7.53030836256716));
#377830=CARTESIAN_POINT('',(2.07441142381095,1.8053579270501,8.75721825406948));
#377831=CARTESIAN_POINT('',(2.07441142381095,1.8053579270501,9.));
#377832=CARTESIAN_POINT('',(2.11329230362296,1.75968623323818,8.75721825406948));
#377833=CARTESIAN_POINT('Origin',(0.,1.84795814293585E-15,8.75721825406948));
#377834=CARTESIAN_POINT('',(2.11329230362296,1.75968623323818,7.51860402984325));
#377835=CARTESIAN_POINT('',(2.11329230362296,1.75968623323818,9.));
#377836=CARTESIAN_POINT('',(2.12540061176888,1.74504218845634,7.49482233047033));
#377837=CARTESIAN_POINT('Origin',(2.13129548840287,1.73783065250855,7.5302500471138));
#377838=CARTESIAN_POINT('',(2.17423646662303,1.68380396341338,7.49482233047033));
#377839=CARTESIAN_POINT('Origin',(1.44479185443039E-15,1.15218305638232E-15,
7.49482233047033));
#377840=CARTESIAN_POINT('',(2.18581900259084,1.66874062931087,7.51860402984325));
#377841=CARTESIAN_POINT('Origin',(2.16848522554325,1.691197370569,7.53030836256729));
#377842=CARTESIAN_POINT('',(2.18581900259083,1.66874062931087,8.75721825406948));
#377843=CARTESIAN_POINT('',(2.18581900259083,1.66874062931087,9.));
#377844=CARTESIAN_POINT('',(2.22169380199588,1.62067166636957,8.75721825406948));
#377845=CARTESIAN_POINT('Origin',(0.,1.84795814293585E-15,8.75721825406948));
#377846=CARTESIAN_POINT('',(2.22169380199588,1.62067166636957,7.51860402984325));
#377847=CARTESIAN_POINT('',(2.22169380199588,1.62067166636957,9.));
#377848=CARTESIAN_POINT('',(2.23283898515352,1.60528192738179,7.49482233047033));
#377849=CARTESIAN_POINT('Origin',(2.23825970543661,1.59770752226543,7.53025004711368));
#377850=CARTESIAN_POINT('',(2.27765095495651,1.54104059887652,7.49482233047033));
#377851=CARTESIAN_POINT('Origin',(1.51564399649249E-15,1.05724764078204E-15,
7.49482233047033));
#377852=CARTESIAN_POINT('',(2.28824458223236,1.52526611838206,7.51860402984325));
#377853=CARTESIAN_POINT('Origin',(2.27238522764112,1.54878729876548,7.5303083625675));
#377854=CARTESIAN_POINT('',(2.28824458223236,1.52526611838206,8.75721825406948));
#377855=CARTESIAN_POINT('',(2.28824458223236,1.52526611838206,9.));
#377856=CARTESIAN_POINT('',(2.32096588398457,1.47499741199086,8.75721825406948));
#377857=CARTESIAN_POINT('Origin',(0.,1.84795814293585E-15,8.75721825406948));
#377858=CARTESIAN_POINT('',(2.32096588398457,1.47499741199086,7.51860402984325));
#377859=CARTESIAN_POINT('',(2.32096588398457,1.47499741199086,9.));
#377860=CARTESIAN_POINT('',(2.33110214420571,1.45892521853574,7.49482233047033));
#377861=CARTESIAN_POINT('Origin',(2.33602643323555,1.45101906910609,7.53025004711363));
#377862=CARTESIAN_POINT('',(2.37170608696149,1.39194476796669,7.49482233047033));
#377863=CARTESIAN_POINT('Origin',(1.58026803226838E-15,9.57967767846882E-16,
7.49482233047033));
#377864=CARTESIAN_POINT('',(2.38126727405857,1.37552396180426,7.51860402984325));
#377865=CARTESIAN_POINT('Origin',(2.36694751141372,1.40001292773719,7.53030836256726));
#377866=CARTESIAN_POINT('',(2.38126727405857,1.37552396180426,8.75721825406948));
#377867=CARTESIAN_POINT('',(2.38126727405857,1.37552396180426,9.));
#377868=CARTESIAN_POINT('',(2.41070061931035,1.32326207686033,8.75721825406948));
#377869=CARTESIAN_POINT('Origin',(0.,1.84795814293585E-15,8.75721825406948));
#377870=CARTESIAN_POINT('',(2.41070061931035,1.32326207686033,7.51860402984325));
#377871=CARTESIAN_POINT('',(2.41070061931035,1.32326207686033,9.));
#377872=CARTESIAN_POINT('',(2.41978630452751,1.30657347302825,7.49482233047033));
#377873=CARTESIAN_POINT('Origin',(2.42419392734427,1.29836806734912,7.53025004711366));
#377874=CARTESIAN_POINT('',(2.45601536992577,1.23712913743408,7.49482233047033));
#377875=CARTESIAN_POINT('Origin',(1.63839840773325E-15,8.54751399870196E-16,
7.49482233047033));
#377876=CARTESIAN_POINT('',(2.46450482787544,1.22012948221845,7.51860402984325));
#377877=CARTESIAN_POINT('Origin',(2.45178350015316,1.24548560328717,7.53030836256726));
#377878=CARTESIAN_POINT('',(2.46450482787544,1.22012948221845,8.75721825406948));
#377879=CARTESIAN_POINT('',(2.46450482787544,1.22012948221845,9.));
#377880=CARTESIAN_POINT('',(2.49052926869772,1.16608917401715,8.75721825406948));
#377881=CARTESIAN_POINT('Origin',(0.,1.84795814293585E-15,8.75721825406948));
#377882=CARTESIAN_POINT('',(2.49052926869772,1.16608917401715,7.51860402984325));
#377883=CARTESIAN_POINT('',(2.49052926869772,1.16608917401715,9.));
#377884=CARTESIAN_POINT('',(2.49852704388148,1.14885273686095,7.49482233047033));
#377885=CARTESIAN_POINT('Origin',(2.50239988861758,1.14038179270428,7.53025004711374));
#377886=CARTESIAN_POINT('',(2.53023235892139,1.07722987791238,7.49482233047033));
#377887=CARTESIAN_POINT('Origin',(1.68979625270539E-15,7.48022675047843E-16,
7.49482233047033));
#377888=CARTESIAN_POINT('',(2.53761520271995,1.05972122887324,7.51860402984325));
#377889=CARTESIAN_POINT('Origin',(2.52654458458447,1.08584031133761,7.53030836256753));
#377890=CARTESIAN_POINT('',(2.53761520271994,1.05972122887325,8.75721825406948));
#377891=CARTESIAN_POINT('',(2.53761520271995,1.05972122887325,9.));
#377892=CARTESIAN_POINT('',(2.56012379910316,1.00412456063259,8.75721825406948));
#377893=CARTESIAN_POINT('Origin',(0.,1.84795814293585E-15,8.75721825406948));
#377894=CARTESIAN_POINT('',(2.56012379910316,1.00412456063259,7.51860402984325));
#377895=CARTESIAN_POINT('',(2.56012379910316,1.00412456063259,9.));
#377896=CARTESIAN_POINT('',(2.56700079967976,0.986411118369754,7.49482233047033));
#377897=CARTESIAN_POINT('Origin',(2.57032295198543,0.977709444662182,7.53025004711375));
#377898=CARTESIAN_POINT('',(2.59405208042106,0.912904049757255,7.49482233047033));
#377899=CARTESIAN_POINT('Origin',(1.734250362415E-15,6.38220164603358E-16,
7.49482233047033));
#377900=CARTESIAN_POINT('',(2.60029797237972,0.894958353689109,7.51860402984325));
#377901=CARTESIAN_POINT('Origin',(2.5909235553758,0.921733068636293,7.53030836256721));
#377902=CARTESIAN_POINT('',(2.60029797237972,0.894958353689114,8.75721825406948));
#377903=CARTESIAN_POINT('',(2.60029797237972,0.894958353689114,9.));
#377904=CARTESIAN_POINT('',(2.61919823167326,0.838033784044351,8.75721825406948));
#377905=CARTESIAN_POINT('Origin',(0.,1.84795814293585E-15,8.75721825406948));
#377906=CARTESIAN_POINT('',(2.61919823167326,0.838033784044351,7.51860402984325));
#377907=CARTESIAN_POINT('',(2.61919823167326,0.838033784044351,9.));
#377908=CARTESIAN_POINT('',(2.62492619857222,0.819916125008653,7.49482233047033));
#377909=CARTESIAN_POINT('Origin',(2.62768400701103,0.81101947879393,7.53025004711372));
#377910=CARTESIAN_POINT('',(2.64721228549985,0.744826903044372,7.49482233047033));
#377911=CARTESIAN_POINT('Origin',(1.77157806538992E-15,5.25795070604721E-16,
7.49482233047033));
#377912=CARTESIAN_POINT('',(2.65229555990882,0.7265179026617,7.51860402984325));
#377913=CARTESIAN_POINT('Origin',(2.6446558655266,0.753838227045187,7.53030836256735));
#377914=CARTESIAN_POINT('',(2.65229555990882,0.726517902661705,8.75721825406948));
#377915=CARTESIAN_POINT('',(2.65229555990882,0.726517902661705,9.));
#377916=CARTESIAN_POINT('',(2.66750981689315,0.668499346879791,8.75721825406948));
#377917=CARTESIAN_POINT('Origin',(0.,1.84795814293585E-15,8.75721825406948));
#377918=CARTESIAN_POINT('',(2.66750981689315,0.668499346879791,7.51860402984325));
#377919=CARTESIAN_POINT('',(2.66750981689315,0.668499346879791,9.));
#377920=CARTESIAN_POINT('',(2.67206521266984,0.650051920418436,7.49482233047033));
#377921=CARTESIAN_POINT('Origin',(2.67424734481537,0.640996859924186,7.53025004711375));
#377922=CARTESIAN_POINT('',(2.68949452747227,0.573689102822012,7.49482233047033));
#377923=CARTESIAN_POINT('Origin',(1.80162597409184E-15,4.11209371878282E-16,
7.49482233047033));
#377924=CARTESIAN_POINT('',(2.69339429606665,0.555092033734655,7.51860402984325));
#377925=CARTESIAN_POINT('Origin',(2.68752071744906,0.582845702481334,7.53030836256744));
#377926=CARTESIAN_POINT('',(2.69339429606664,0.55509203373466,8.75721825406948));
#377927=CARTESIAN_POINT('',(2.69339429606664,0.55509203373466,9.));
#377928=CARTESIAN_POINT('',(2.70486003209636,0.49621790250624,8.75721825406948));
#377929=CARTESIAN_POINT('Origin',(0.,1.84795814293585E-15,8.75721825406948));
#377930=CARTESIAN_POINT('',(2.70486003209636,0.49621790250624,7.51860402984325));
#377931=CARTESIAN_POINT('',(2.70486003209636,0.49621790250624,9.));
#377932=CARTESIAN_POINT('',(2.70822413765241,0.477516513051518,7.49482233047033));
#377933=CARTESIAN_POINT('Origin',(2.70982162665562,0.468340247463557,7.5302500471138));
#377934=CARTESIAN_POINT('',(2.72072505953654,0.400193891020227,7.49482233047033));
#377935=CARTESIAN_POINT('Origin',(1.82427061521866E-15,2.94933925638659E-16,
7.49482233047033));
#377936=CARTESIAN_POINT('',(2.72342529733066,0.381385172574125,7.51860402984325));
#377937=CARTESIAN_POINT('Origin',(2.71934197027218,0.40945813990574,7.53030836256725));
#377938=CARTESIAN_POINT('',(2.72342529733066,0.38138517257413,8.75721825406948));
#377939=CARTESIAN_POINT('',(2.72342529733066,0.38138517257413,9.));
#377940=CARTESIAN_POINT('',(2.73109539723703,0.321897392332886,8.75721825406948));
#377941=CARTESIAN_POINT('Origin',(0.,1.84795814293585E-15,8.75721825406948));
#377942=CARTESIAN_POINT('',(2.73109539723703,0.321897392332886,7.51860402984325));
#377943=CARTESIAN_POINT('',(2.73109539723703,0.321897392332886,9.));
#377944=CARTESIAN_POINT('',(2.73325438874111,0.303018887905503,7.49482233047033));
#377945=CARTESIAN_POINT('Origin',(2.73426067017699,0.293759124467663,7.53025004711361));
#377946=CARTESIAN_POINT('',(2.74077554873748,0.225054196678923,7.49482233047033));
#377947=CARTESIAN_POINT('Origin',(1.83941893708273E-15,1.77446532635461E-16,
7.49482233047033));
#377948=CARTESIAN_POINT('',(2.74226515987506,0.206111117932626,7.51860402984325));
#377949=CARTESIAN_POINT('Origin',(2.7399888636424,0.234388026004939,7.53030836256727));
#377950=CARTESIAN_POINT('',(2.74226515987506,0.206111117932631,8.75721825406948));
#377951=CARTESIAN_POINT('',(2.74226515987506,0.206111117932631,9.));
#377952=CARTESIAN_POINT('',(2.74610810557233,0.146254136727663,8.75721825406948));
#377953=CARTESIAN_POINT('Origin',(0.,1.84795814293585E-15,8.75721825406948));
#377954=CARTESIAN_POINT('',(2.74610810557233,0.146254136727663,7.51860402984325));
#377955=CARTESIAN_POINT('',(2.74610810557233,0.146254136727663,9.));
#377956=CARTESIAN_POINT('',(2.74705311126524,0.127276093151736,7.49482233047033));
#377957=CARTESIAN_POINT('Origin',(2.74746405010757,0.117970882217837,7.53025004711382));
#377958=CARTESIAN_POINT('',(2.74956360331414,0.0489897063694902,7.49482233047033));
#377959=CARTESIAN_POINT('Origin',(1.8470086919802E-15,5.92299737675009E-17,
7.49482233047033));
#377960=CARTESIAN_POINT('',(2.74983646666349,0.029990108496846,7.51860402984325));
#377961=CARTESIAN_POINT('Origin',(2.74937655504614,0.0583547614292927,7.53030836256736));
#377962=CARTESIAN_POINT('',(2.74983646666349,0.0299901084968513,9.));
#377963=CARTESIAN_POINT('Origin',(0.,1.73472347597681E-15,8.75721825406948));
#377964=CARTESIAN_POINT('Origin',(2.69439583688069,0.0515030456391921,8.75693427654772));
#377965=CARTESIAN_POINT('Origin',(2.70228258044598,-0.048534448727824,8.76059769038453));
#377966=CARTESIAN_POINT('Origin',(0.,1.73472347597681E-15,8.75721825406948));
#377967=CARTESIAN_POINT('Origin',(2.33073265030338,-1.36834646567043,8.76059769038508));
#377968=CARTESIAN_POINT('Origin',(2.37295093746503,-1.27731176222123,8.75693427654889));
#377969=CARTESIAN_POINT('Origin',(0.,1.73472347597681E-15,8.75721825406948));
#377970=CARTESIAN_POINT('Origin',(2.28623780967396,-1.42672287677799,8.75693427654736));
#377971=CARTESIAN_POINT('Origin',(2.23827365103721,-1.51486560472308,8.7605976903849));
#377972=CARTESIAN_POINT('Origin',(0.,1.73472347597681E-15,8.75721825406948));
#377973=CARTESIAN_POINT('Origin',(2.19013004033039,-1.57027128100825,8.75693427654829));
#377974=CARTESIAN_POINT('Origin',(2.13661710522947,-1.65515983606784,8.76059769038414));
#377975=CARTESIAN_POINT('Origin',(0.,1.73472347597681E-15,8.75721825406948));
#377976=CARTESIAN_POINT('Origin',(2.08502255686731,-1.70736710371899,8.7569342765475));
#377977=CARTESIAN_POINT('Origin',(2.02618074143668,-1.78865266061642,8.76059769038484));
#377978=CARTESIAN_POINT('Origin',(0.,1.73472347597681E-15,8.75721825406948));
#377979=CARTESIAN_POINT('Origin',(1.97134726848432,-1.83744698877564,8.75693427654859));
#377980=CARTESIAN_POINT('Origin',(1.90741836636063,-1.91479552771699,8.7605976903845));
#377981=CARTESIAN_POINT('Origin',(0.,1.73472347597681E-15,8.75721825406948));
#377982=CARTESIAN_POINT('Origin',(1.84957129132088,-1.95997641002114,8.75693427654833));
#377983=CARTESIAN_POINT('Origin',(1.78081800007942,-2.0330700892728,8.76059769038499));
#377984=CARTESIAN_POINT('Origin',(0.,1.73472347597681E-15,8.75721825406948));
#377985=CARTESIAN_POINT('Origin',(1.72019502899002,-2.07445186778525,8.75693427654845));
#377986=CARTESIAN_POINT('Origin',(1.64689987064802,-2.14299032973772,8.76059769038419));
#377987=CARTESIAN_POINT('Origin',(0.,1.73472347597681E-15,8.75721825406948));
#377988=CARTESIAN_POINT('Origin',(1.5837501163042,-2.18040295785566,8.7569342765484));
#377989=CARTESIAN_POINT('Origin',(1.50621427639336,-2.24410456327018,8.76059769038494));
#377990=CARTESIAN_POINT('Origin',(0.,1.73472347597681E-15,8.75721825406948));
#377991=CARTESIAN_POINT('Origin',(1.44079723467694,-2.27739430447603,8.75693427654785));
#377992=CARTESIAN_POINT('Origin',(1.35933932459287,-2.33599728979191,8.76059769038486));
#377993=CARTESIAN_POINT('Origin',(0.,1.73472347597681E-15,8.75721825406948));
#377994=CARTESIAN_POINT('Origin',(1.29192380816251,-2.36502734939956,8.75693427654725));
#377995=CARTESIAN_POINT('Origin',(1.20687855593063,-2.41829090238031,8.76059769038491));
#377996=CARTESIAN_POINT('Origin',(0.,1.73472347597681E-15,8.75721825406948));
#377997=CARTESIAN_POINT('Origin',(1.13774158960398,-2.44294198965256,8.75693427654866));
#377998=CARTESIAN_POINT('Origin',(1.04945846440645,-2.49064723892815,8.76059769038441));
#377999=CARTESIAN_POINT('Origin',(0.,1.73472347597681E-15,8.75721825406948));
#378000=CARTESIAN_POINT('Origin',(0.978884146808586,-2.51081805725596,8.75693427654816));
#378001=CARTESIAN_POINT('Origin',(0.887725922945771,-2.55276897173096,8.76059769038499));
#378002=CARTESIAN_POINT('Origin',(0.,1.73472347597681E-15,8.75721825406948));
#378003=CARTESIAN_POINT('Origin',(0.816004259084044,-2.56837663489457,8.75693427654807));
#378004=CARTESIAN_POINT('Origin',(0.722345525249748,-2.60440082926027,8.76059769038484));
#378005=CARTESIAN_POINT('Origin',(0.,1.73472347597681E-15,8.75721825406948));
#378006=CARTESIAN_POINT('Origin',(0.649771234826351,-2.61538120202673,8.75693427654868));
#378007=CARTESIAN_POINT('Origin',(0.553996854849101,-2.6453306451417,8.76059769038543));
#378008=CARTESIAN_POINT('Origin',(0.,1.73472347597681E-15,8.75721825406948));
#378009=CARTESIAN_POINT('Origin',(0.48086816118962,-2.65163860679976,8.75693427654827));
#378010=CARTESIAN_POINT('Origin',(0.383371692537345,-2.67539022997661,8.7605976903844));
#378011=CARTESIAN_POINT('Origin',(0.,1.73472347597681E-15,8.75721825406948));
#378012=CARTESIAN_POINT('Origin',(0.309989097132222,-2.67699985976484,8.75693427654861));
#378013=CARTESIAN_POINT('Origin',(0.211171173710696,-2.69445606249166,8.76059769038521));
#378014=CARTESIAN_POINT('Origin',(0.,1.73472347597681E-15,8.75721825406948));
#378015=CARTESIAN_POINT('Origin',(0.137836221382254,-2.69136074609111,8.75693427654883));
#378016=CARTESIAN_POINT('Origin',(0.0381029072335807,-2.70244979708389,
8.76059769038479));
#378017=CARTESIAN_POINT('Origin',(0.,1.73472347597681E-15,8.75721825406948));
#378018=CARTESIAN_POINT('Origin',(-0.0348830529663535,-2.69466225381449,
8.7569342765482));
#378019=CARTESIAN_POINT('Origin',(-0.135121932261307,-2.69933858578882,
8.76059769038532));
#378020=CARTESIAN_POINT('Origin',(0.,1.73472347597681E-15,8.75721825406948));
#378021=CARTESIAN_POINT('Origin',(-0.207458985368108,-2.68689081633459,
8.75693427654791));
#378022=CARTESIAN_POINT('Origin',(-0.307791526754287,-2.68513521323456,
8.76059769038443));
#378023=CARTESIAN_POINT('Origin',(0.,1.73472347597681E-15,8.75721825406948));
#378024=CARTESIAN_POINT('Origin',(-0.379182424297982,-2.66807836815224,
8.75693427654677));
#378025=CARTESIAN_POINT('Origin',(-0.479196339841415,-2.6598980441342,8.76059769038531));
#378026=CARTESIAN_POINT('Origin',(0.,1.73472347597681E-15,8.75721825406948));
#378027=CARTESIAN_POINT('Origin',(-0.549347721314731,-2.63830221365879,
8.75693427654778));
#378028=CARTESIAN_POINT('Origin',(-0.648632032381716,-2.62373078342031,
8.76059769038475));
#378029=CARTESIAN_POINT('Origin',(0.,1.73472347597681E-15,8.75721825406948));
#378030=CARTESIAN_POINT('Origin',(-0.717255630709442,-2.59768470945429,
8.7569342765482));
#378031=CARTESIAN_POINT('Origin',(-0.815402356769413,-2.57678205013184,
8.76059769038535));
#378032=CARTESIAN_POINT('Origin',(0.,1.73472347597681E-15,8.75721825406948));
#378033=CARTESIAN_POINT('Origin',(-0.882216182865111,-2.54639276157493,
8.75693427654775));
#378034=CARTESIAN_POINT('Origin',(-0.978822017970119,-2.51924476667895,
8.76059769038503));
#378035=CARTESIAN_POINT('Origin',(0.,1.73472347597681E-15,8.75721825406948));
#378036=CARTESIAN_POINT('Origin',(-1.04355151949371,-2.48463713964208,8.75693427654898));
#378037=CARTESIAN_POINT('Origin',(-1.1382194895422,-2.45135536610346,8.76059769038475));
#378038=CARTESIAN_POINT('Origin',(0.,1.73472347597681E-15,8.75721825406948));
#378039=CARTESIAN_POINT('Origin',(-1.20059867908435,-2.41267161074603,8.75693427654834));
#378040=CARTESIAN_POINT('Origin',(-1.29293977308454,-2.37339282051633,8.76059769038498));
#378041=CARTESIAN_POINT('Origin',(0.,1.73472347597681E-15,8.75721825406948));
#378042=CARTESIAN_POINT('Origin',(-1.35271232117534,-2.33079189668547,8.75693427654807));
#378043=CARTESIAN_POINT('Origin',(-1.44234708976418,-2.28567749473594,8.76059769038434));
#378044=CARTESIAN_POINT('Origin',(0.,1.73472347597681E-15,8.75721825406948));
#378045=CARTESIAN_POINT('Origin',(-1.49926737818264,-2.23933445876821,8.75693427654765));
#378046=CARTESIAN_POINT('Origin',(-1.58582749287008,-2.18856982985657,8.76059769038499));
#378047=CARTESIAN_POINT('Origin',(0.,1.73472347597681E-15,8.75721825406948));
#378048=CARTESIAN_POINT('Origin',(-1.63966162394198,-2.13867511522477,8.75693427654776));
#378049=CARTESIAN_POINT('Origin',(-1.72279139064872,-2.08246886209855,8.76059769038511));
#378050=CARTESIAN_POINT('Origin',(0.,1.73472347597681E-15,8.75721825406948));
#378051=CARTESIAN_POINT('Origin',(-1.77331814838098,-2.02922749688787,8.75693427654726));
#378052=CARTESIAN_POINT('Origin',(-1.85267596906511,-1.96781058309659,8.76059769038474));
#378053=CARTESIAN_POINT('Origin',(0.,1.73472347597681E-15,8.75721825406948));
#378054=CARTESIAN_POINT('Origin',(-1.8996877281768,-1.91144134750023,8.75693427654833));
#378055=CARTESIAN_POINT('Origin',(-1.97494750452723,-1.84506614831579,8.76059769038486));
#378056=CARTESIAN_POINT('Origin',(0.,1.73472347597681E-15,8.75721825406948));
#378057=CARTESIAN_POINT('Origin',(-2.01825108361109,-1.78580067561075,8.75693427654771));
#378058=CARTESIAN_POINT('Origin',(-2.08910355706906,-1.71473994096737,8.7605976903854));
#378059=CARTESIAN_POINT('Origin',(0.,1.73472347597681E-15,8.75721825406948));
#378060=CARTESIAN_POINT('Origin',(-2.12852101243237,-1.65282176569325,8.75693427654811));
#378061=CARTESIAN_POINT('Origin',(-2.19467503498269,-1.57736749938913,8.76059769038525));
#378062=CARTESIAN_POINT('Origin',(0.,1.73472347597681E-15,8.75721825406948));
#378063=CARTESIAN_POINT('Origin',(-2.23004439184663,-1.51305105661106,8.7569342765483));
#378064=CARTESIAN_POINT('Origin',(-2.29122812242046,-1.43351331641059,8.76059769038468));
#378065=CARTESIAN_POINT('Origin',(0.,1.73472347597681E-15,8.75721825406948));
#378066=CARTESIAN_POINT('Origin',(-2.3224040405107,-1.3670628961886,8.75693427654811));
#378067=CARTESIAN_POINT('Origin',(-2.37836606203847,-1.28376851973026,8.7605976903854));
#378068=CARTESIAN_POINT('Origin',(0.,1.73472347597681E-15,8.75721825406948));
#378069=CARTESIAN_POINT('Origin',(-2.40522043282081,-1.21545718109189,8.75693427654895));
#378070=CARTESIAN_POINT('Origin',(-2.45573078534923,-1.12874844283407,8.76059769038575));
#378071=CARTESIAN_POINT('Origin',(0.,1.73472347597681E-15,8.75721825406948));
#378072=CARTESIAN_POINT('Origin',(-2.47815325844863,-1.05885689172298,8.75693427654761));
#378073=CARTESIAN_POINT('Origin',(-2.52300438410804,-0.969090096468077,
8.76059769038488));
#378074=CARTESIAN_POINT('Origin',(0.,1.73472347597681E-15,8.75721825406948));
#378075=CARTESIAN_POINT('Origin',(-2.54090282078107,-0.897905532262054,
8.75693427654849));
#378076=CARTESIAN_POINT('Origin',(-2.57991041667112,-0.805449551027988,
8.76059769038477));
#378077=CARTESIAN_POINT('Origin',(0.,1.73472347597681E-15,8.75721825406948));
#378078=CARTESIAN_POINT('Origin',(-2.59321126839827,-0.733264486368949,
8.7569342765483));
#378079=CARTESIAN_POINT('Origin',(-2.62621504394276,-0.638499240614201,
8.76059769038464));
#378080=CARTESIAN_POINT('Origin',(0.,1.73472347597681E-15,8.75721825406948));
#378081=CARTESIAN_POINT('Origin',(-2.63486365466874,-0.565610299417181,
8.75693427654712));
#378082=CARTESIAN_POINT('Origin',(-2.66172799027955,-0.468925199864443,
8.76059769038529));
#378083=CARTESIAN_POINT('Origin',(0.,1.73472347597681E-15,8.75721825406948));
#378084=CARTESIAN_POINT('Origin',(-2.6656888210123,-0.395631898420887,8.75693427654828));
#378085=CARTESIAN_POINT('Origin',(-2.68630332536147,-0.297424244881892,
8.76059769038425));
#378086=CARTESIAN_POINT('Origin',(0.,1.73472347597681E-15,8.75721825406948));
#378087=CARTESIAN_POINT('Origin',(-2.68556010019945,-0.224027761091513,
8.75693427654866));
#378088=CARTESIAN_POINT('Origin',(-2.69984006387362,-0.124701109882257,
8.76059769038511));
#378089=CARTESIAN_POINT('Origin',(0.,1.73472347597681E-15,8.75721825406948));
#378090=CARTESIAN_POINT('Origin',(-2.69439583688284,-0.0515030456383384,
8.75693427654858));
#378091=CARTESIAN_POINT('Origin',(-2.70228258044652,0.048534448727637,8.7605976903847));
#378092=CARTESIAN_POINT('Origin',(0.,1.73472347597681E-15,8.75721825406948));
#378093=CARTESIAN_POINT('Origin',(-2.69215972312632,0.121233306876663,8.75693427654841));
#378094=CARTESIAN_POINT('Origin',(-2.69362083825953,0.221570568876651,8.76059769038467));
#378095=CARTESIAN_POINT('Origin',(0.,1.73472347597681E-15,8.75721825406948));
#378096=CARTESIAN_POINT('Origin',(-2.67886094759852,0.293471485727828,8.75693427654727));
#378097=CARTESIAN_POINT('Origin',(-2.6738904302698,0.39369620803106,8.76059769038531));
#378098=CARTESIAN_POINT('Origin',(0.,1.73472347597681E-15,8.75721825406948));
#378099=CARTESIAN_POINT('Origin',(-2.65455415782992,0.464503727298469,8.75693427654893));
#378100=CARTESIAN_POINT('Origin',(-2.64317243295172,0.564204065019785,8.7605976903849));
#378101=CARTESIAN_POINT('Origin',(0.,1.73472347597681E-15,8.75721825406948));
#378102=CARTESIAN_POINT('Origin',(-2.61933923562136,0.633627223414736,8.75693427654828));
#378103=CARTESIAN_POINT('Origin',(-2.60159307314893,0.732393486483691,8.76059769038488));
#378104=CARTESIAN_POINT('Origin',(0.,1.73472347597681E-15,8.75721825406948));
#378105=CARTESIAN_POINT('Origin',(-2.57336088664725,0.80014700935721,8.75693427654763));
#378106=CARTESIAN_POINT('Origin',(-2.54932320936855,0.897573346013709,8.76059769038477));
#378107=CARTESIAN_POINT('Origin',(0.,1.73472347597681E-15,8.75721825406948));
#378108=CARTESIAN_POINT('Origin',(-2.51680804580947,0.963378819610446,8.75693427654892));
#378109=CARTESIAN_POINT('Origin',(-2.486577629693,1.05906488413606,8.76059769038485));
#378110=CARTESIAN_POINT('Origin',(0.,1.73472347597681E-15,8.75721825406948));
#378111=CARTESIAN_POINT('Origin',(-2.44991310085432,1.12265189964667,8.7569342765483));
#378112=CARTESIAN_POINT('Origin',(-2.41361416916817,1.21620449748084,8.76059769038502));
#378113=CARTESIAN_POINT('Origin',(0.,1.73472347597681E-15,8.75721825406948));
#378114=CARTESIAN_POINT('Origin',(-2.37295093746513,1.27731176222139,8.75693427654888));
#378115=CARTESIAN_POINT('Origin',(-2.33073265030128,1.36834646567015,8.76059769038433));
#378116=CARTESIAN_POINT('Origin',(0.,1.73472347597681E-15,8.75721825406948));
#378117=CARTESIAN_POINT('Origin',(-2.28623780967662,1.42672287678172,8.75693427654898));
#378118=CARTESIAN_POINT('Origin',(-2.23827365103789,1.51486560472324,8.76059769038512));
#378119=CARTESIAN_POINT('Origin',(0.,1.73472347597681E-15,8.75721825406948));
#378120=CARTESIAN_POINT('Origin',(-2.19013004032998,1.57027128100764,8.75693427654791));
#378121=CARTESIAN_POINT('Origin',(-2.13661710523201,1.65515983606856,8.76059769038523));
#378122=CARTESIAN_POINT('Origin',(0.,1.73472347597681E-15,8.75721825406948));
#378123=CARTESIAN_POINT('Origin',(-2.08502255686687,1.70736710371821,8.75693427654714));
#378124=CARTESIAN_POINT('Origin',(-2.02618074143595,1.78865266061619,8.76059769038451));
#378125=CARTESIAN_POINT('Origin',(0.,1.73472347597681E-15,8.75721825406948));
#378126=CARTESIAN_POINT('Origin',(-1.97134726848383,1.83744698877462,8.75693427654807));
#378127=CARTESIAN_POINT('Origin',(-1.90741836636232,1.91479552771773,8.76059769038511));
#378128=CARTESIAN_POINT('Origin',(0.,1.73472347597681E-15,8.75721825406948));
#378129=CARTESIAN_POINT('Origin',(-1.84957129132086,1.95997641002116,8.75693427654829));
#378130=CARTESIAN_POINT('Origin',(-1.78081800007809,2.03307008927213,8.76059769038453));
#378131=CARTESIAN_POINT('Origin',(0.,1.73472347597681E-15,8.75721825406948));
#378132=CARTESIAN_POINT('Origin',(-1.72019502898981,2.07445186778464,8.75693427654814));
#378133=CARTESIAN_POINT('Origin',(-1.64689987064938,2.14299032973853,8.76059769038468));
#378134=CARTESIAN_POINT('Origin',(0.,1.73472347597681E-15,8.75721825406948));
#378135=CARTESIAN_POINT('Origin',(-1.58375011630461,2.18040295785744,8.75693427654917));
#378136=CARTESIAN_POINT('Origin',(-1.50621427639386,2.24410456327052,8.76059769038516));
#378137=CARTESIAN_POINT('Origin',(0.,1.73472347597681E-15,8.75721825406948));
#378138=CARTESIAN_POINT('Origin',(-1.44079723467693,2.2773943044761,8.75693427654786));
#378139=CARTESIAN_POINT('Origin',(-1.35933932459167,2.33599728979102,8.7605976903843));
#378140=CARTESIAN_POINT('Origin',(0.,1.73472347597681E-15,8.75721825406948));
#378141=CARTESIAN_POINT('Origin',(-1.29192380816264,2.36502734940097,8.75693427654784));
#378142=CARTESIAN_POINT('Origin',(-1.20687855592903,2.41829090237895,8.76059769038412));
#378143=CARTESIAN_POINT('Origin',(0.,1.73472347597681E-15,8.75721825406948));
#378144=CARTESIAN_POINT('Origin',(-1.13774158960372,2.44294198964755,8.75693427654679));
#378145=CARTESIAN_POINT('Origin',(-1.04945846440719,2.49064723892892,8.7605976903849));
#378146=CARTESIAN_POINT('Origin',(0.,1.73472347597681E-15,8.75721825406948));
#378147=CARTESIAN_POINT('Origin',(-0.978884146808645,2.51081805725174,8.75693427654652));
#378148=CARTESIAN_POINT('Origin',(-0.887725922945521,2.55276897173071,8.76059769038493));
#378149=CARTESIAN_POINT('Origin',(0.,1.73472347597681E-15,8.75721825406948));
#378150=CARTESIAN_POINT('Origin',(-0.816004259084113,2.56837663489343,8.75693427654765));
#378151=CARTESIAN_POINT('Origin',(-0.722345525249641,2.60440082926018,8.76059769038479));
#378152=CARTESIAN_POINT('Origin',(0.,1.73472347597681E-15,8.75721825406948));
#378153=CARTESIAN_POINT('Origin',(-0.649771234826602,2.61538120202488,8.75693427654794));
#378154=CARTESIAN_POINT('Origin',(-0.55399685484881,2.64533064514131,8.76059769038531));
#378155=CARTESIAN_POINT('Origin',(0.,1.73472347597681E-15,8.75721825406948));
#378156=CARTESIAN_POINT('Origin',(-0.480868161189849,2.6516386067986,8.75693427654777));
#378157=CARTESIAN_POINT('Origin',(-0.383371692537824,2.67539022997746,8.76059769038473));
#378158=CARTESIAN_POINT('Origin',(0.,1.73472347597681E-15,8.75721825406948));
#378159=CARTESIAN_POINT('Origin',(2.4136141691684,-1.21620449748085,8.76059769038497));
#378160=CARTESIAN_POINT('Origin',(2.44991310085381,-1.1226518996461,8.75693427654797));
#378161=CARTESIAN_POINT('Origin',(0.,1.73472347597681E-15,8.75721825406948));
#378162=CARTESIAN_POINT('Origin',(2.48657762969223,-1.05906488413604,8.76059769038456));
#378163=CARTESIAN_POINT('Origin',(2.51680804580673,-0.96337881960785,8.75693427654744));
#378164=CARTESIAN_POINT('Origin',(0.,1.73472347597681E-15,8.75721825406948));
#378165=CARTESIAN_POINT('Origin',(2.5493232093696,-0.89757334601363,8.76059769038528));
#378166=CARTESIAN_POINT('Origin',(2.5733608866487,-0.800147009358387,8.75693427654833));
#378167=CARTESIAN_POINT('Origin',(0.,1.73472347597681E-15,8.75721825406948));
#378168=CARTESIAN_POINT('Origin',(2.60159307314759,-0.732393486483826,8.76059769038438));
#378169=CARTESIAN_POINT('Origin',(2.61933923561983,-0.633627223413621,8.75693427654751));
#378170=CARTESIAN_POINT('Origin',(0.,1.73472347597681E-15,8.75721825406948));
#378171=CARTESIAN_POINT('Origin',(2.64317243294954,-0.564204065020162,8.76059769038412));
#378172=CARTESIAN_POINT('Origin',(2.65455415782731,-0.464503727296811,8.75693427654779));
#378173=CARTESIAN_POINT('Origin',(0.,1.73472347597681E-15,8.75721825406948));
#378174=CARTESIAN_POINT('Origin',(2.67389043026933,-0.393696208031149,8.76059769038518));
#378175=CARTESIAN_POINT('Origin',(2.6788609475996,-0.293471485728388,8.75693427654779));
#378176=CARTESIAN_POINT('Origin',(0.,1.73472347597681E-15,8.75721825406948));
#378177=CARTESIAN_POINT('Origin',(2.69362083826087,-0.221570568876215,8.76059769038522));
#378178=CARTESIAN_POINT('Origin',(2.69215972312383,-0.121233306875485,8.75693427654745));
#378179=CARTESIAN_POINT('Origin',(0.,1.73472347597681E-15,8.75721825406948));
#378180=CARTESIAN_POINT('Origin',(2.69984006387324,0.124701109882108,8.76059769038496));
#378181=CARTESIAN_POINT('Origin',(2.68556010019784,0.224027761092042,8.75693427654803));
#378182=CARTESIAN_POINT('Origin',(0.,1.73472347597681E-15,8.75721825406948));
#378183=CARTESIAN_POINT('Origin',(2.6863033253636,0.297424244883076,8.76059769038514));
#378184=CARTESIAN_POINT('Origin',(2.66568882101331,0.39563189842066,8.75693427654874));
#378185=CARTESIAN_POINT('Origin',(0.,1.73472347597681E-15,8.75721825406948));
#378186=CARTESIAN_POINT('Origin',(2.66172799027848,0.468925199863798,8.76059769038476));
#378187=CARTESIAN_POINT('Origin',(2.63486365467144,0.565610299416714,8.75693427654806));
#378188=CARTESIAN_POINT('Origin',(0.,1.73472347597681E-15,8.75721825406948));
#378189=CARTESIAN_POINT('Origin',(2.62621504394336,0.638499240614644,8.76059769038486));
#378190=CARTESIAN_POINT('Origin',(2.59321126839706,0.733264486369107,8.7569342765479));
#378191=CARTESIAN_POINT('Origin',(0.,1.73472347597681E-15,8.75721825406948));
#378192=CARTESIAN_POINT('Origin',(2.57991041667163,0.805449551028446,8.76059769038508));
#378193=CARTESIAN_POINT('Origin',(2.54090282077683,0.897905532262281,8.75693427654695));
#378194=CARTESIAN_POINT('Origin',(0.,1.73472347597681E-15,8.75721825406948));
#378195=CARTESIAN_POINT('Origin',(2.52300438410802,0.969090096468083,8.76059769038486));
#378196=CARTESIAN_POINT('Origin',(2.4781532584484,1.05885689172299,8.75693427654758));
#378197=CARTESIAN_POINT('Origin',(0.,1.73472347597681E-15,8.75721825406948));
#378198=CARTESIAN_POINT('Origin',(2.4557307853478,1.12874844283258,8.760597690385));
#378199=CARTESIAN_POINT('Origin',(2.40522043281718,1.21545718109162,8.75693427654765));
#378200=CARTESIAN_POINT('Origin',(0.,1.73472347597681E-15,8.75721825406948));
#378201=CARTESIAN_POINT('Origin',(2.37836606203801,1.28376851972975,8.7605976903851));
#378202=CARTESIAN_POINT('Origin',(2.32240404051429,1.36706289618913,8.75693427654954));
#378203=CARTESIAN_POINT('Origin',(0.,1.73472347597681E-15,8.75721825406948));
#378204=CARTESIAN_POINT('Origin',(2.29122812242146,1.433513316412,8.76059769038528));
#378205=CARTESIAN_POINT('Origin',(2.23004439184453,1.51305105661064,8.75693427654751));
#378206=CARTESIAN_POINT('Origin',(0.,1.73472347597681E-15,8.75721825406948));
#378207=CARTESIAN_POINT('Origin',(2.19467503498184,1.57736749938779,8.76059769038468));
#378208=CARTESIAN_POINT('Origin',(2.12852101243191,1.65282176569313,8.75693427654792));
#378209=CARTESIAN_POINT('Origin',(0.,1.73472347597681E-15,8.75721825406948));
#378210=CARTESIAN_POINT('Origin',(2.08910355706757,1.71473994096463,8.76059769038429));
#378211=CARTESIAN_POINT('Origin',(2.01825108361135,1.78580067561086,8.75693427654768));
#378212=CARTESIAN_POINT('Origin',(0.,1.73472347597681E-15,8.75721825406948));
#378213=CARTESIAN_POINT('Origin',(1.9749475045275,1.8450661483164,8.76059769038504));
#378214=CARTESIAN_POINT('Origin',(1.899687728176,1.9114413474999,8.75693427654803));
#378215=CARTESIAN_POINT('Origin',(0.,1.73472347597681E-15,8.75721825406948));
#378216=CARTESIAN_POINT('Origin',(1.85267596906484,1.96781058309591,8.76059769038447));
#378217=CARTESIAN_POINT('Origin',(1.77331814838245,2.02922749688863,8.75693427654777));
#378218=CARTESIAN_POINT('Origin',(0.,1.73472347597681E-15,8.75721825406948));
#378219=CARTESIAN_POINT('Origin',(1.72279139064826,2.08246886209715,8.76059769038466));
#378220=CARTESIAN_POINT('Origin',(1.63966162394417,2.13867511522607,8.75693427654865));
#378221=CARTESIAN_POINT('Origin',(0.,1.73472347597681E-15,8.75721825406948));
#378222=CARTESIAN_POINT('Origin',(1.58582749286989,2.18856982985588,8.76059769038467));
#378223=CARTESIAN_POINT('Origin',(1.49926737818233,2.23933445876803,8.75693427654753));
#378224=CARTESIAN_POINT('Origin',(0.,1.73472347597681E-15,8.75721825406948));
#378225=CARTESIAN_POINT('Origin',(1.44234708976436,2.285677494737,8.7605976903848));
#378226=CARTESIAN_POINT('Origin',(1.35271232117604,2.33079189668602,8.75693427654834));
#378227=CARTESIAN_POINT('Origin',(0.,1.73472347597681E-15,8.75721825406948));
#378228=CARTESIAN_POINT('Origin',(1.29293977308441,2.37339282051545,8.76059769038473));
#378229=CARTESIAN_POINT('Origin',(1.20059867908477,2.41267161074641,8.75693427654861));
#378230=CARTESIAN_POINT('Origin',(0.,1.73472347597681E-15,8.75721825406948));
#378231=CARTESIAN_POINT('Origin',(1.13821948954226,2.45135536610491,8.76059769038536));
#378232=CARTESIAN_POINT('Origin',(1.04355151949228,2.48463713964067,8.75693427654822));
#378233=CARTESIAN_POINT('Origin',(0.,1.73472347597681E-15,8.75721825406948));
#378234=CARTESIAN_POINT('Origin',(0.978822017970095,2.51924476667868,8.76059769038497));
#378235=CARTESIAN_POINT('Origin',(0.882216182867039,2.54639276157716,8.75693427654885));
#378236=CARTESIAN_POINT('Origin',(0.,1.73472347597681E-15,8.75721825406948));
#378237=CARTESIAN_POINT('Origin',(0.815402356769505,2.57678205013041,8.7605976903849));
#378238=CARTESIAN_POINT('Origin',(0.717255630708937,2.59768470945367,8.75693427654799));
#378239=CARTESIAN_POINT('Origin',(0.,1.73472347597681E-15,8.75721825406948));
#378240=CARTESIAN_POINT('Origin',(0.648632032381852,2.6237307834193,8.76059769038445));
#378241=CARTESIAN_POINT('Origin',(0.549347721316237,2.63830221366104,8.75693427654871));
#378242=CARTESIAN_POINT('Origin',(0.,1.73472347597681E-15,8.75721825406948));
#378243=CARTESIAN_POINT('Origin',(0.479196339841701,2.65989804413279,8.76059769038473));
#378244=CARTESIAN_POINT('Origin',(0.379182424298648,2.66807836815341,8.75693427654746));
#378245=CARTESIAN_POINT('Origin',(0.,1.73472347597681E-15,8.75721825406948));
#378246=CARTESIAN_POINT('Origin',(0.30779152675381,2.6851352132362,8.76059769038509));
#378247=CARTESIAN_POINT('Origin',(0.207458985368901,2.68689081633622,8.75693427654862));
#378248=CARTESIAN_POINT('Origin',(0.,1.73472347597681E-15,8.75721825406948));
#378249=CARTESIAN_POINT('Origin',(0.135121932261841,2.69933858578726,8.76059769038467));
#378250=CARTESIAN_POINT('Origin',(0.0348830529663535,2.69466225381449,8.7569342765482));
#378251=CARTESIAN_POINT('Origin',(0.,1.73472347597681E-15,8.75721825406948));
#378252=CARTESIAN_POINT('Origin',(-0.30998909713224,2.67699985976471,8.75693427654847));
#378253=CARTESIAN_POINT('Origin',(-0.211171173710815,2.69445606249195,8.76059769038534));
#378254=CARTESIAN_POINT('Origin',(0.,2.67103869055211,7.5));
#378255=CARTESIAN_POINT('',(-0.00603856833113048,2.66775215476039,7.59394543036555));
#378256=CARTESIAN_POINT('',(-0.00603856833113048,2.66775215476039,8.85049129520029));
#378257=CARTESIAN_POINT('',(-0.00603856833113048,2.66775215476039,7.5));
#378258=CARTESIAN_POINT('',(0.00603856833113048,2.66775215476039,8.85049129520029));
#378259=CARTESIAN_POINT('Ctrl Pts',(-0.0060385683311304,2.66775215476039,
8.85049129520029));
#378260=CARTESIAN_POINT('Ctrl Pts',(-0.0059459900808512,2.66758205465325,
8.85097269580139));
#378261=CARTESIAN_POINT('Ctrl Pts',(-0.00584719181995321,2.66741812167859,
8.85143669361005));
#378262=CARTESIAN_POINT('Ctrl Pts',(-0.00573687539919907,2.6672532585408,
8.8519052845931));
#378263=CARTESIAN_POINT('Ctrl Pts',(-0.00552110347621796,2.66693079669851,
8.85282181883899));
#378264=CARTESIAN_POINT('Ctrl Pts',(-0.00526665369920735,2.66661318098465,
8.85372622499635));
#378265=CARTESIAN_POINT('Ctrl Pts',(-0.00495749990689061,2.66630506772301,
8.8546225773507));
#378266=CARTESIAN_POINT('Ctrl Pts',(-0.00470085140861172,2.66604928303633,
8.85536669723986));
#378267=CARTESIAN_POINT('Ctrl Pts',(-0.00440646616566121,2.66579996647417,
8.85610498449051));
#378268=CARTESIAN_POINT('Ctrl Pts',(-0.00405997820836668,2.66556586768779,
8.85681338218371));
#378269=CARTESIAN_POINT('Ctrl Pts',(-0.00374553984295258,2.66535342267149,
8.85745625420284));
#378270=CARTESIAN_POINT('Ctrl Pts',(-0.00338458256238873,2.66515034957616,
8.85808743050666));
#378271=CARTESIAN_POINT('Ctrl Pts',(-0.00295369827383558,2.66497307725867,
8.85866804508411));
#378272=CARTESIAN_POINT('Ctrl Pts',(-0.00275489760352519,2.66489128765418,
8.85893592806396));
#378273=CARTESIAN_POINT('Ctrl Pts',(-0.00254103122291519,2.6648151521707,
8.85919241173849));
#378274=CARTESIAN_POINT('Ctrl Pts',(-0.00230877295597377,2.66474750603832,
8.85943017985535));
#378275=CARTESIAN_POINT('Ctrl Pts',(-0.00199515553979517,2.66465616373421,
8.85975123720001));
#378276=CARTESIAN_POINT('Ctrl Pts',(-0.00163984270799643,2.66457859015688,
8.86004599534706));
#378277=CARTESIAN_POINT('Ctrl Pts',(-0.00124488186767327,2.66452589273075,
8.86026130871721));
#378278=CARTESIAN_POINT('Ctrl Pts',(-0.00110027556890578,2.66450659871735,
8.86034014101236));
#378279=CARTESIAN_POINT('Ctrl Pts',(-0.000948183946098822,2.66449033731455,
8.86040910639693));
#378280=CARTESIAN_POINT('Ctrl Pts',(-0.000792714888868764,2.6644778860275,
8.86046313645507));
#378281=CARTESIAN_POINT('Ctrl Pts',(-0.000550106727103745,2.66445845589833,
8.8605474499083));
#378282=CARTESIAN_POINT('Ctrl Pts',(-0.000292639848427733,2.66444792009911,
8.86059655985668));
#378283=CARTESIAN_POINT('Ctrl Pts',(-3.68383656842663E-5,2.66444666161026,
8.86059725258816));
#378284=CARTESIAN_POINT('Ctrl Pts',(0.000219554120677806,2.6644454002138,
8.86059794692011));
#378285=CARTESIAN_POINT('Ctrl Pts',(0.000477129998147651,2.66445610179498,
8.86056369958366));
#378286=CARTESIAN_POINT('Ctrl Pts',(0.000721997165140026,2.66447442282945,
8.86048590497774));
#378287=CARTESIAN_POINT('Ctrl Pts',(0.000785900205151045,2.66447920407396,
8.86046560290182));
#378288=CARTESIAN_POINT('Ctrl Pts',(0.000849762296446932,2.66448465677257,
8.86044257503091));
#378289=CARTESIAN_POINT('Ctrl Pts',(0.000911612840154663,2.66449057972519,
8.86041778462583));
#378290=CARTESIAN_POINT('Ctrl Pts',(0.00132779024918037,2.66453043384658,
8.860250975962));
#378291=CARTESIAN_POINT('Ctrl Pts',(0.0017087062830535,2.6645972575501,
8.8599848982295));
#378292=CARTESIAN_POINT('Ctrl Pts',(0.00204470696718254,2.6646807553764,
8.85968173251462));
#378293=CARTESIAN_POINT('Ctrl Pts',(0.00222243207854282,2.66472492094265,
8.85952137522077));
#378294=CARTESIAN_POINT('Ctrl Pts',(0.00239106259016765,2.6647744176014,
8.85934740853961));
#378295=CARTESIAN_POINT('Ctrl Pts',(0.00254865826271333,2.66482705571598,
8.8591675900182));
#378296=CARTESIAN_POINT('Ctrl Pts',(0.00318148680458622,2.66503842510675,
8.85844552518695));
#378297=CARTESIAN_POINT('Ctrl Pts',(0.00367310982058979,2.665309524653,
8.85759444184124));
#378298=CARTESIAN_POINT('Ctrl Pts',(0.0040540988240094,2.66556656868577,
8.85683498915139));
#378299=CARTESIAN_POINT('Ctrl Pts',(0.00409396830856038,2.66559346765924,
8.85675551444998));
#378300=CARTESIAN_POINT('Ctrl Pts',(0.00413261203991475,2.66562022675649,
8.85667699793651));
#378301=CARTESIAN_POINT('Ctrl Pts',(0.00417005525354386,2.66564677016415,
8.85659965593547));
#378302=CARTESIAN_POINT('Ctrl Pts',(0.00467546566173685,2.66600505443517,
8.85555568965886));
#378303=CARTESIAN_POINT('Ctrl Pts',(0.00510945303863149,2.66642237908077,
8.85434650606346));
#378304=CARTESIAN_POINT('Ctrl Pts',(0.00547847041769397,2.6668963274801,
8.85297329937117));
#378305=CARTESIAN_POINT('Ctrl Pts',(0.00568602020885762,2.66716289457662,
8.85220095427747));
#378306=CARTESIAN_POINT('Ctrl Pts',(0.00587285370781608,2.66744767638566,
8.85137579139183));
#378307=CARTESIAN_POINT('Ctrl Pts',(0.00603856833113047,2.66775215476039,
8.85049129520029));
#378308=CARTESIAN_POINT('',(0.00603856833113048,2.66775215476039,7.59394543036555));
#378309=CARTESIAN_POINT('',(0.00603856833113048,2.66775215476039,7.5));
#378310=CARTESIAN_POINT('Origin',(2.28698895758661E-17,2.67103869055211,
7.59394543036555));
#378311=CARTESIAN_POINT('Origin',(-0.1375,2.90929488800561,7.5));
#378312=CARTESIAN_POINT('',(-0.0469183093502055,2.74286319116668,8.75721825406948));
#378313=CARTESIAN_POINT('',(-0.0402149326548299,2.73054663635347,8.78727029226991));
#378314=CARTESIAN_POINT('Origin',(-0.0231992623667671,2.69928262639098,
8.75658640621021));
#378315=CARTESIAN_POINT('Ctrl Pts',(-0.04021493265483,2.73054663635347,
8.78727029226991));
#378316=CARTESIAN_POINT('Ctrl Pts',(-0.0288389699333486,2.7096448319675,
8.80838212259896));
#378317=CARTESIAN_POINT('Ctrl Pts',(-0.017447249324145,2.68871407457819,
8.82945686509571));
#378318=CARTESIAN_POINT('Ctrl Pts',(-0.00603856833113064,2.66775215476039,
8.85049129520029));
#378319=CARTESIAN_POINT('',(-0.0469183093502055,2.74286319116668,7.51860402984325));
#378320=CARTESIAN_POINT('Ctrl Pts',(-0.00603856833112958,2.66775215476039,
7.59394543036555));
#378321=CARTESIAN_POINT('Ctrl Pts',(-0.0144064330001523,2.68312698278351,
7.57858609112103));
#378322=CARTESIAN_POINT('Ctrl Pts',(-0.022764934078714,2.69848460646616,
7.56320440326857));
#378323=CARTESIAN_POINT('Ctrl Pts',(-0.031114562299379,2.71382592746348,
7.54780169004651));
#378324=CARTESIAN_POINT('Ctrl Pts',(-0.0363859720948704,2.72351143532608,
7.53807742314383));
#378325=CARTESIAN_POINT('Ctrl Pts',(-0.0416538495282657,2.73319045294751,
7.52834476460825));
#378326=CARTESIAN_POINT('Ctrl Pts',(-0.0469183093502052,2.74286319116668,
7.51860402984325));
#378327=CARTESIAN_POINT('',(-0.0469183093502055,2.74286319116668,7.5));
#378328=CARTESIAN_POINT('Origin',(0.00603856833113048,2.66775215476039,
7.5));
#378329=CARTESIAN_POINT('',(0.0402149326548299,2.73054663635347,8.78727029226991));
#378330=CARTESIAN_POINT('Ctrl Pts',(0.00603856833113057,2.66775215476039,
8.85049129520029));
#378331=CARTESIAN_POINT('Ctrl Pts',(0.0174472493241456,2.68871407457819,
8.82945686509571));
#378332=CARTESIAN_POINT('Ctrl Pts',(0.0288389699333437,2.70964483196749,
8.80838212259895));
#378333=CARTESIAN_POINT('Ctrl Pts',(0.0402149326548299,2.73054663635347,
8.78727029226991));
#378334=CARTESIAN_POINT('',(0.0469183093502055,2.74286319116668,8.75721825406948));
#378335=CARTESIAN_POINT('Origin',(0.0267453462054665,2.70579850156065,8.75937679713102));
#378336=CARTESIAN_POINT('',(0.0469183093502055,2.74286319116668,7.51860402984325));
#378337=CARTESIAN_POINT('',(0.0469183093502055,2.74286319116668,7.5));
#378338=CARTESIAN_POINT('Ctrl Pts',(0.0469183093502053,2.74286319116668,
7.51860402984325));
#378339=CARTESIAN_POINT('Ctrl Pts',(0.041653849528267,2.73319045294751,
7.52834476460825));
#378340=CARTESIAN_POINT('Ctrl Pts',(0.0363859720949718,2.72351143532627,
7.53807742314407));
#378341=CARTESIAN_POINT('Ctrl Pts',(0.0311145622994817,2.71382592746367,
7.54780169004674));
#378342=CARTESIAN_POINT('Ctrl Pts',(0.0227649340788154,2.69848460646635,
7.5632044032688));
#378343=CARTESIAN_POINT('Ctrl Pts',(0.0144064330001542,2.68312698278351,
7.57858609112103));
#378344=CARTESIAN_POINT('Ctrl Pts',(0.00603856833113041,2.66775215476039,
7.59394543036555));
#378345=CARTESIAN_POINT('Origin',(0.,1.25,7.5));
#378346=CARTESIAN_POINT('',(-1.25,0.721687836487033,7.5));
#378347=CARTESIAN_POINT('',(-1.25,0.721687836487033,7.5));
#378348=CARTESIAN_POINT('',(0.,1.44337567297406,7.5));
#378349=CARTESIAN_POINT('Origin',(0.,1.25,7.5));
#378350=CARTESIAN_POINT('',(0.,1.44337567297406,7.5));
#378351=CARTESIAN_POINT('',(0.,1.44337567297406,7.5));
#378352=CARTESIAN_POINT('',(1.25,0.721687836487032,7.5));
#378353=CARTESIAN_POINT('Origin',(0.,1.25,7.5));
#378354=CARTESIAN_POINT('',(1.25,0.721687836487032,7.5));
#378355=CARTESIAN_POINT('',(1.25,0.721687836487032,7.5));
#378356=CARTESIAN_POINT('',(1.25,-0.721687836487032,7.5));
#378357=CARTESIAN_POINT('Origin',(0.,1.25,7.5));
#378358=CARTESIAN_POINT('',(1.25,-0.721687836487032,7.5));
#378359=CARTESIAN_POINT('',(1.25,-0.721687836487032,7.5));
#378360=CARTESIAN_POINT('',(-2.19962454627626E-16,-1.44337567297406,7.5));
#378361=CARTESIAN_POINT('Origin',(0.,1.25,7.5));
#378362=CARTESIAN_POINT('',(-2.19962454627626E-16,-1.44337567297406,7.5));
#378363=CARTESIAN_POINT('',(-2.19962454627626E-16,-1.44337567297406,7.5));
#378364=CARTESIAN_POINT('',(-1.25,-0.721687836487031,7.5));
#378365=CARTESIAN_POINT('Origin',(0.,2.50721825406948,9.));
#378366=CARTESIAN_POINT('',(-2.16840434497101E-16,1.44337567297406,9.));
#378367=CARTESIAN_POINT('',(-1.25,0.721687836487033,9.));
#378368=CARTESIAN_POINT('Origin',(0.,-7.70371977754894E-31,9.));
#378369=CARTESIAN_POINT('Origin',(0.,-7.70371977754894E-31,9.));
#378370=CARTESIAN_POINT('',(5.42101086242752E-16,-1.44337567297406,9.));
#378371=CARTESIAN_POINT('Origin',(0.,-7.70371977754894E-31,9.));
#378372=CARTESIAN_POINT('',(-1.25,-0.721687836487032,9.));
#378373=CARTESIAN_POINT('Origin',(0.,-7.70371977754894E-31,9.));
#378374=CARTESIAN_POINT('Origin',(0.,-7.70371977754894E-31,9.));
#378375=CARTESIAN_POINT('Origin',(0.,1.73472347597681E-15,8.75721825406948));
#378376=CARTESIAN_POINT('Origin',(-0.137836221382471,2.69136074609044,8.75693427654847));
#378377=CARTESIAN_POINT('Origin',(-0.0381029072335807,2.70244979708389,
8.76059769038479));
#378378=CARTESIAN_POINT('Origin',(1.25,0.721687836487032,7.5));
#378379=CARTESIAN_POINT('',(1.25,0.721687836487032,7.5));
#378380=CARTESIAN_POINT('Ctrl Pts',(2.83368599028168E-16,1.44337567297406,
9.));
#378381=CARTESIAN_POINT('Ctrl Pts',(0.624999999999998,1.08253175473055,
8.63915608175649));
#378382=CARTESIAN_POINT('Ctrl Pts',(1.25,0.721687836487034,9.));
#378383=CARTESIAN_POINT('',(0.,1.44337567297406,7.5));
#378384=CARTESIAN_POINT('Origin',(1.25,-0.721687836487032,7.5));
#378385=CARTESIAN_POINT('',(1.25,-0.721687836487032,7.5));
#378386=CARTESIAN_POINT('Origin',(-2.19962454627626E-16,-1.44337567297406,
7.5));
#378387=CARTESIAN_POINT('',(-2.19962454627626E-16,-1.44337567297406,7.5));
#378388=CARTESIAN_POINT('Ctrl Pts',(1.25,-0.721687836487033,9.));
#378389=CARTESIAN_POINT('Ctrl Pts',(0.625,-1.08253175473055,8.63915608175649));
#378390=CARTESIAN_POINT('Ctrl Pts',(3.68379178736618E-15,-1.44337567297406,
9.));
#378391=CARTESIAN_POINT('Origin',(-1.25,-0.721687836487031,7.5));
#378392=CARTESIAN_POINT('',(-1.25,-0.721687836487031,7.5));
#378393=CARTESIAN_POINT('',(-1.25,-0.721687836487031,7.5));
#378394=CARTESIAN_POINT('Ctrl Pts',(-7.04373374727159E-15,-1.44337567297406,
8.99999999999999));
#378395=CARTESIAN_POINT('Ctrl Pts',(-0.625000000000001,-1.08253175473055,
8.63915608175649));
#378396=CARTESIAN_POINT('Ctrl Pts',(-1.25,-0.721687836487034,9.));
#378397=CARTESIAN_POINT('',(-1.25,-0.721687836487031,7.5));
#378398=CARTESIAN_POINT('Origin',(-1.25,0.721687836487033,7.5));
#378399=CARTESIAN_POINT('',(-1.25,0.721687836487033,7.5));
#378400=CARTESIAN_POINT('Ctrl Pts',(-1.25,-0.721687836487028,9.));
#378401=CARTESIAN_POINT('Ctrl Pts',(-1.25,2.4980018054066E-16,8.63915608175649));
#378402=CARTESIAN_POINT('Ctrl Pts',(-1.25,0.721687836487029,9.));
#378403=CARTESIAN_POINT('',(-1.25,0.721687836487033,7.5));
#378404=CARTESIAN_POINT('Origin',(0.,1.44337567297406,7.5));
#378405=CARTESIAN_POINT('Ctrl Pts',(-1.24999999999999,0.721687836487037,
9.));
#378406=CARTESIAN_POINT('Ctrl Pts',(-0.624999999999999,1.08253175473055,
8.63915608175649));
#378407=CARTESIAN_POINT('Ctrl Pts',(-4.49341635601809E-15,1.44337567297406,
9.));
#378408=CARTESIAN_POINT('Origin',(0.,1.25,7.5));
#378409=CARTESIAN_POINT('Origin',(0.,-7.70371977754894E-31,9.));
#378410=CARTESIAN_POINT('Origin',(0.,-7.70371977754894E-31,9.));
#378411=CARTESIAN_POINT('Origin',(0.,-7.70371977754894E-31,9.));
#378412=CARTESIAN_POINT('Origin',(0.,-7.70371977754894E-31,9.));
#378413=CARTESIAN_POINT('Origin',(0.,-7.70371977754894E-31,9.));
#378414=CARTESIAN_POINT('Origin',(2.50721825406948,1.84795814293585E-15,
6.));
#378415=CARTESIAN_POINT('Origin',(0.,1.84795814293585E-15,-9.));
#378416=CARTESIAN_POINT('Origin',(6.93889390390723E-17,9.71445146547012E-16,
-9.21875));
#378417=CARTESIAN_POINT('Ctrl Pts',(-1.43925448419919E-16,-1.17524047358083,
5.));
#378418=CARTESIAN_POINT('Ctrl Pts',(0.678525403784437,-1.17524047358083,
5.04166666666667));
#378419=CARTESIAN_POINT('Ctrl Pts',(1.01778810567666,-0.587620236790417,
5.08333333333333));
#378420=CARTESIAN_POINT('Ctrl Pts',(1.35705080756888,2.7065942666714E-16,
5.125));
#378421=CARTESIAN_POINT('Ctrl Pts',(1.01778810567666,0.587620236790417,
5.16666666666667));
#378422=CARTESIAN_POINT('Ctrl Pts',(0.983895352085429,0.646324208018836,
5.1708292169807));
#378423=CARTESIAN_POINT('Ctrl Pts',(0.943477955795688,0.700742119235096,
5.17524047358083));
#378424=CARTESIAN_POINT('Ctrl Pts',(-1.43925448419919E-16,-1.17524047358083,
5.0625));
#378425=CARTESIAN_POINT('Ctrl Pts',(0.678525403784437,-1.17524047358083,
5.10416666666667));
#378426=CARTESIAN_POINT('Ctrl Pts',(1.01778810567666,-0.587620236790417,
5.14583333333333));
#378427=CARTESIAN_POINT('Ctrl Pts',(1.12956523348519,-0.394016572301912,
5.15956128014086));
#378428=CARTESIAN_POINT('Ctrl Pts',(1.16245326511946,-0.172894699616898,
5.17524047358083));
#378429=CARTESIAN_POINT('Ctrl Pts',(0.,1.17524047358083,-9.25));
#378430=CARTESIAN_POINT('Ctrl Pts',(-0.678525403784438,1.17524047358083,
-9.20833333333333));
#378431=CARTESIAN_POINT('Ctrl Pts',(-1.01778810567666,0.587620236790418,
-9.16666666666667));
#378432=CARTESIAN_POINT('Ctrl Pts',(-1.35705080756888,6.0304101222105E-16,
-9.125));
#378433=CARTESIAN_POINT('Ctrl Pts',(-1.01778810567666,-0.587620236790416,
-9.08333333333333));
#378434=CARTESIAN_POINT('Ctrl Pts',(-0.678525403784438,-1.17524047358083,
-9.04166666666667));
#378435=CARTESIAN_POINT('Ctrl Pts',(-1.43925448419919E-16,-1.17524047358083,
-9.));
#378436=CARTESIAN_POINT('Ctrl Pts',(0.678525403784437,-1.17524047358083,
-8.95833333333333));
#378437=CARTESIAN_POINT('Ctrl Pts',(1.01778810567666,-0.587620236790417,
-8.91666666666667));
#378438=CARTESIAN_POINT('Ctrl Pts',(1.35705080756888,2.70659426667139E-16,
-8.875));
#378439=CARTESIAN_POINT('Ctrl Pts',(1.01778810567666,0.587620236790417,
-8.83333333333333));
#378440=CARTESIAN_POINT('Ctrl Pts',(0.678525403784439,1.17524047358083,
-8.79166666666667));
#378441=CARTESIAN_POINT('Ctrl Pts',(0.,1.17524047358083,-8.75));
#378442=CARTESIAN_POINT('Ctrl Pts',(-0.678525403784438,1.17524047358083,
-8.70833333333333));
#378443=CARTESIAN_POINT('Ctrl Pts',(-1.01778810567666,0.587620236790418,
-8.66666666666667));
#378444=CARTESIAN_POINT('Ctrl Pts',(-1.35705080756888,6.0304101222105E-16,
-8.625));
#378445=CARTESIAN_POINT('Ctrl Pts',(-1.01778810567666,-0.587620236790416,
-8.58333333333333));
#378446=CARTESIAN_POINT('Ctrl Pts',(-0.678525403784438,-1.17524047358083,
-8.54166666666667));
#378447=CARTESIAN_POINT('Ctrl Pts',(-1.43925448419919E-16,-1.17524047358083,
-8.5));
#378448=CARTESIAN_POINT('Ctrl Pts',(0.678525403784437,-1.17524047358083,
-8.45833333333333));
#378449=CARTESIAN_POINT('Ctrl Pts',(1.01778810567666,-0.587620236790417,
-8.41666666666667));
#378450=CARTESIAN_POINT('Ctrl Pts',(1.35705080756888,2.70659426667139E-16,
-8.375));
#378451=CARTESIAN_POINT('Ctrl Pts',(1.01778810567666,0.587620236790417,
-8.33333333333334));
#378452=CARTESIAN_POINT('Ctrl Pts',(0.678525403784439,1.17524047358083,
-8.29166666666667));
#378453=CARTESIAN_POINT('Ctrl Pts',(0.,1.17524047358083,-8.25));
#378454=CARTESIAN_POINT('Ctrl Pts',(-0.678525403784438,1.17524047358083,
-8.20833333333333));
#378455=CARTESIAN_POINT('Ctrl Pts',(-1.01778810567666,0.587620236790418,
-8.16666666666667));
#378456=CARTESIAN_POINT('Ctrl Pts',(-1.35705080756888,6.0304101222105E-16,
-8.125));
#378457=CARTESIAN_POINT('Ctrl Pts',(-1.01778810567666,-0.587620236790416,
-8.08333333333333));
#378458=CARTESIAN_POINT('Ctrl Pts',(-0.678525403784438,-1.17524047358083,
-8.04166666666667));
#378459=CARTESIAN_POINT('Ctrl Pts',(-1.43925448419919E-16,-1.17524047358083,
-8.));
#378460=CARTESIAN_POINT('Ctrl Pts',(0.678525403784437,-1.17524047358083,
-7.95833333333333));
#378461=CARTESIAN_POINT('Ctrl Pts',(1.01778810567666,-0.587620236790417,
-7.91666666666667));
#378462=CARTESIAN_POINT('Ctrl Pts',(1.35705080756888,2.7065942666714E-16,
-7.875));
#378463=CARTESIAN_POINT('Ctrl Pts',(1.01778810567666,0.587620236790417,
-7.83333333333333));
#378464=CARTESIAN_POINT('Ctrl Pts',(0.678525403784439,1.17524047358083,
-7.79166666666667));
#378465=CARTESIAN_POINT('Ctrl Pts',(0.,1.17524047358083,-7.75));
#378466=CARTESIAN_POINT('Ctrl Pts',(-0.678525403784438,1.17524047358083,
-7.70833333333333));
#378467=CARTESIAN_POINT('Ctrl Pts',(-1.01778810567666,0.587620236790418,
-7.66666666666667));
#378468=CARTESIAN_POINT('Ctrl Pts',(-1.35705080756888,6.0304101222105E-16,
-7.625));
#378469=CARTESIAN_POINT('Ctrl Pts',(-1.01778810567666,-0.587620236790416,
-7.58333333333333));
#378470=CARTESIAN_POINT('Ctrl Pts',(-0.678525403784438,-1.17524047358083,
-7.54166666666667));
#378471=CARTESIAN_POINT('Ctrl Pts',(-1.43925448419919E-16,-1.17524047358083,
-7.5));
#378472=CARTESIAN_POINT('Ctrl Pts',(0.678525403784437,-1.17524047358083,
-7.45833333333333));
#378473=CARTESIAN_POINT('Ctrl Pts',(1.01778810567666,-0.587620236790417,
-7.41666666666667));
#378474=CARTESIAN_POINT('Ctrl Pts',(1.35705080756888,2.7065942666714E-16,
-7.375));
#378475=CARTESIAN_POINT('Ctrl Pts',(1.01778810567666,0.587620236790417,
-7.33333333333333));
#378476=CARTESIAN_POINT('Ctrl Pts',(0.678525403784439,1.17524047358083,
-7.29166666666667));
#378477=CARTESIAN_POINT('Ctrl Pts',(0.,1.17524047358083,-7.25));
#378478=CARTESIAN_POINT('Ctrl Pts',(-0.678525403784438,1.17524047358083,
-7.20833333333333));
#378479=CARTESIAN_POINT('Ctrl Pts',(-1.01778810567666,0.587620236790418,
-7.16666666666667));
#378480=CARTESIAN_POINT('Ctrl Pts',(-1.35705080756888,6.0304101222105E-16,
-7.125));
#378481=CARTESIAN_POINT('Ctrl Pts',(-1.01778810567666,-0.587620236790416,
-7.08333333333333));
#378482=CARTESIAN_POINT('Ctrl Pts',(-0.678525403784438,-1.17524047358083,
-7.04166666666667));
#378483=CARTESIAN_POINT('Ctrl Pts',(-1.43925448419919E-16,-1.17524047358083,
-7.));
#378484=CARTESIAN_POINT('Ctrl Pts',(0.678525403784437,-1.17524047358083,
-6.95833333333333));
#378485=CARTESIAN_POINT('Ctrl Pts',(1.01778810567666,-0.587620236790417,
-6.91666666666667));
#378486=CARTESIAN_POINT('Ctrl Pts',(1.35705080756888,2.7065942666714E-16,
-6.875));
#378487=CARTESIAN_POINT('Ctrl Pts',(1.01778810567666,0.587620236790417,
-6.83333333333333));
#378488=CARTESIAN_POINT('Ctrl Pts',(0.678525403784439,1.17524047358083,
-6.79166666666667));
#378489=CARTESIAN_POINT('Ctrl Pts',(0.,1.17524047358083,-6.75));
#378490=CARTESIAN_POINT('Ctrl Pts',(-0.678525403784438,1.17524047358083,
-6.70833333333333));
#378491=CARTESIAN_POINT('Ctrl Pts',(-1.01778810567666,0.587620236790418,
-6.66666666666667));
#378492=CARTESIAN_POINT('Ctrl Pts',(-1.35705080756888,6.0304101222105E-16,
-6.625));
#378493=CARTESIAN_POINT('Ctrl Pts',(-1.01778810567666,-0.587620236790416,
-6.58333333333333));
#378494=CARTESIAN_POINT('Ctrl Pts',(-0.678525403784438,-1.17524047358083,
-6.54166666666667));
#378495=CARTESIAN_POINT('Ctrl Pts',(-1.43925448419919E-16,-1.17524047358083,
-6.5));
#378496=CARTESIAN_POINT('Ctrl Pts',(0.678525403784437,-1.17524047358083,
-6.45833333333333));
#378497=CARTESIAN_POINT('Ctrl Pts',(1.01778810567666,-0.587620236790417,
-6.41666666666667));
#378498=CARTESIAN_POINT('Ctrl Pts',(1.35705080756888,2.7065942666714E-16,
-6.375));
#378499=CARTESIAN_POINT('Ctrl Pts',(1.01778810567666,0.587620236790417,
-6.33333333333333));
#378500=CARTESIAN_POINT('Ctrl Pts',(0.678525403784439,1.17524047358083,
-6.29166666666667));
#378501=CARTESIAN_POINT('Ctrl Pts',(0.,1.17524047358083,-6.25));
#378502=CARTESIAN_POINT('Ctrl Pts',(-0.678525403784438,1.17524047358083,
-6.20833333333333));
#378503=CARTESIAN_POINT('Ctrl Pts',(-1.01778810567666,0.587620236790418,
-6.16666666666667));
#378504=CARTESIAN_POINT('Ctrl Pts',(-1.35705080756888,6.0304101222105E-16,
-6.125));
#378505=CARTESIAN_POINT('Ctrl Pts',(-1.01778810567666,-0.587620236790416,
-6.08333333333333));
#378506=CARTESIAN_POINT('Ctrl Pts',(-0.678525403784438,-1.17524047358083,
-6.04166666666667));
#378507=CARTESIAN_POINT('Ctrl Pts',(-1.43925448419919E-16,-1.17524047358083,
-6.));
#378508=CARTESIAN_POINT('Ctrl Pts',(0.678525403784437,-1.17524047358083,
-5.95833333333333));
#378509=CARTESIAN_POINT('Ctrl Pts',(1.01778810567666,-0.587620236790417,
-5.91666666666667));
#378510=CARTESIAN_POINT('Ctrl Pts',(1.35705080756888,2.7065942666714E-16,
-5.875));
#378511=CARTESIAN_POINT('Ctrl Pts',(1.01778810567666,0.587620236790417,
-5.83333333333333));
#378512=CARTESIAN_POINT('Ctrl Pts',(0.678525403784439,1.17524047358083,
-5.79166666666667));
#378513=CARTESIAN_POINT('Ctrl Pts',(0.,1.17524047358083,-5.75));
#378514=CARTESIAN_POINT('Ctrl Pts',(-0.678525403784438,1.17524047358083,
-5.70833333333333));
#378515=CARTESIAN_POINT('Ctrl Pts',(-1.01778810567666,0.587620236790418,
-5.66666666666667));
#378516=CARTESIAN_POINT('Ctrl Pts',(-1.35705080756888,6.0304101222105E-16,
-5.625));
#378517=CARTESIAN_POINT('Ctrl Pts',(-1.01778810567666,-0.587620236790416,
-5.58333333333333));
#378518=CARTESIAN_POINT('Ctrl Pts',(-0.678525403784438,-1.17524047358083,
-5.54166666666667));
#378519=CARTESIAN_POINT('Ctrl Pts',(-1.43925448419919E-16,-1.17524047358083,
-5.5));
#378520=CARTESIAN_POINT('Ctrl Pts',(0.678525403784437,-1.17524047358083,
-5.45833333333333));
#378521=CARTESIAN_POINT('Ctrl Pts',(1.01778810567666,-0.587620236790417,
-5.41666666666667));
#378522=CARTESIAN_POINT('Ctrl Pts',(1.35705080756888,2.7065942666714E-16,
-5.375));
#378523=CARTESIAN_POINT('Ctrl Pts',(1.01778810567666,0.587620236790417,
-5.33333333333333));
#378524=CARTESIAN_POINT('Ctrl Pts',(0.678525403784439,1.17524047358083,
-5.29166666666667));
#378525=CARTESIAN_POINT('Ctrl Pts',(0.,1.17524047358083,-5.25));
#378526=CARTESIAN_POINT('Ctrl Pts',(-0.678525403784438,1.17524047358083,
-5.20833333333333));
#378527=CARTESIAN_POINT('Ctrl Pts',(-1.01778810567666,0.587620236790418,
-5.16666666666667));
#378528=CARTESIAN_POINT('Ctrl Pts',(-1.35705080756888,6.0304101222105E-16,
-5.125));
#378529=CARTESIAN_POINT('Ctrl Pts',(-1.01778810567666,-0.587620236790416,
-5.08333333333333));
#378530=CARTESIAN_POINT('Ctrl Pts',(-0.678525403784438,-1.17524047358083,
-5.04166666666667));
#378531=CARTESIAN_POINT('Ctrl Pts',(-1.43925448419919E-16,-1.17524047358083,
-5.));
#378532=CARTESIAN_POINT('Ctrl Pts',(0.678525403784437,-1.17524047358083,
-4.95833333333333));
#378533=CARTESIAN_POINT('Ctrl Pts',(1.01778810567666,-0.587620236790417,
-4.91666666666667));
#378534=CARTESIAN_POINT('Ctrl Pts',(1.35705080756888,2.7065942666714E-16,
-4.875));
#378535=CARTESIAN_POINT('Ctrl Pts',(1.01778810567666,0.587620236790417,
-4.83333333333333));
#378536=CARTESIAN_POINT('Ctrl Pts',(0.678525403784439,1.17524047358083,
-4.79166666666667));
#378537=CARTESIAN_POINT('Ctrl Pts',(0.,1.17524047358083,-4.75));
#378538=CARTESIAN_POINT('Ctrl Pts',(-0.678525403784438,1.17524047358083,
-4.70833333333333));
#378539=CARTESIAN_POINT('Ctrl Pts',(-1.01778810567666,0.587620236790418,
-4.66666666666667));
#378540=CARTESIAN_POINT('Ctrl Pts',(-1.35705080756888,6.03041012221051E-16,
-4.625));
#378541=CARTESIAN_POINT('Ctrl Pts',(-1.01778810567666,-0.587620236790416,
-4.58333333333333));
#378542=CARTESIAN_POINT('Ctrl Pts',(-0.678525403784438,-1.17524047358083,
-4.54166666666667));
#378543=CARTESIAN_POINT('Ctrl Pts',(-1.43925448419919E-16,-1.17524047358083,
-4.5));
#378544=CARTESIAN_POINT('Ctrl Pts',(0.678525403784437,-1.17524047358083,
-4.45833333333333));
#378545=CARTESIAN_POINT('Ctrl Pts',(1.01778810567666,-0.587620236790417,
-4.41666666666667));
#378546=CARTESIAN_POINT('Ctrl Pts',(1.35705080756888,2.7065942666714E-16,
-4.375));
#378547=CARTESIAN_POINT('Ctrl Pts',(1.01778810567666,0.587620236790417,
-4.33333333333333));
#378548=CARTESIAN_POINT('Ctrl Pts',(0.678525403784439,1.17524047358083,
-4.29166666666667));
#378549=CARTESIAN_POINT('Ctrl Pts',(0.,1.17524047358083,-4.25));
#378550=CARTESIAN_POINT('Ctrl Pts',(-0.678525403784438,1.17524047358083,
-4.20833333333333));
#378551=CARTESIAN_POINT('Ctrl Pts',(-1.01778810567666,0.587620236790418,
-4.16666666666667));
#378552=CARTESIAN_POINT('Ctrl Pts',(-1.35705080756888,6.03041012221051E-16,
-4.125));
#378553=CARTESIAN_POINT('Ctrl Pts',(-1.01778810567666,-0.587620236790416,
-4.08333333333333));
#378554=CARTESIAN_POINT('Ctrl Pts',(-0.678525403784438,-1.17524047358083,
-4.04166666666667));
#378555=CARTESIAN_POINT('Ctrl Pts',(-1.43925448419919E-16,-1.17524047358083,
-4.));
#378556=CARTESIAN_POINT('Ctrl Pts',(0.678525403784437,-1.17524047358083,
-3.95833333333333));
#378557=CARTESIAN_POINT('Ctrl Pts',(1.01778810567666,-0.587620236790417,
-3.91666666666667));
#378558=CARTESIAN_POINT('Ctrl Pts',(1.35705080756888,2.7065942666714E-16,
-3.875));
#378559=CARTESIAN_POINT('Ctrl Pts',(1.01778810567666,0.587620236790417,
-3.83333333333333));
#378560=CARTESIAN_POINT('Ctrl Pts',(0.678525403784439,1.17524047358083,
-3.79166666666667));
#378561=CARTESIAN_POINT('Ctrl Pts',(0.,1.17524047358083,-3.75));
#378562=CARTESIAN_POINT('Ctrl Pts',(-0.678525403784438,1.17524047358083,
-3.70833333333333));
#378563=CARTESIAN_POINT('Ctrl Pts',(-1.01778810567666,0.587620236790418,
-3.66666666666667));
#378564=CARTESIAN_POINT('Ctrl Pts',(-1.35705080756888,6.03041012221051E-16,
-3.625));
#378565=CARTESIAN_POINT('Ctrl Pts',(-1.01778810567666,-0.587620236790416,
-3.58333333333333));
#378566=CARTESIAN_POINT('Ctrl Pts',(-0.678525403784438,-1.17524047358083,
-3.54166666666667));
#378567=CARTESIAN_POINT('Ctrl Pts',(-1.43925448419919E-16,-1.17524047358083,
-3.5));
#378568=CARTESIAN_POINT('Ctrl Pts',(0.678525403784437,-1.17524047358083,
-3.45833333333333));
#378569=CARTESIAN_POINT('Ctrl Pts',(1.01778810567666,-0.587620236790417,
-3.41666666666667));
#378570=CARTESIAN_POINT('Ctrl Pts',(1.35705080756888,2.7065942666714E-16,
-3.375));
#378571=CARTESIAN_POINT('Ctrl Pts',(1.01778810567666,0.587620236790417,
-3.33333333333333));
#378572=CARTESIAN_POINT('Ctrl Pts',(0.678525403784439,1.17524047358083,
-3.29166666666667));
#378573=CARTESIAN_POINT('Ctrl Pts',(0.,1.17524047358083,-3.25));
#378574=CARTESIAN_POINT('Ctrl Pts',(-0.678525403784438,1.17524047358083,
-3.20833333333333));
#378575=CARTESIAN_POINT('Ctrl Pts',(-1.01778810567666,0.587620236790418,
-3.16666666666667));
#378576=CARTESIAN_POINT('Ctrl Pts',(-1.35705080756888,6.03041012221051E-16,
-3.125));
#378577=CARTESIAN_POINT('Ctrl Pts',(-1.01778810567666,-0.587620236790416,
-3.08333333333333));
#378578=CARTESIAN_POINT('Ctrl Pts',(-0.678525403784438,-1.17524047358083,
-3.04166666666667));
#378579=CARTESIAN_POINT('Ctrl Pts',(-1.43925448419919E-16,-1.17524047358083,
-3.));
#378580=CARTESIAN_POINT('Ctrl Pts',(0.678525403784437,-1.17524047358083,
-2.95833333333333));
#378581=CARTESIAN_POINT('Ctrl Pts',(1.01778810567666,-0.587620236790417,
-2.91666666666667));
#378582=CARTESIAN_POINT('Ctrl Pts',(1.35705080756888,2.7065942666714E-16,
-2.875));
#378583=CARTESIAN_POINT('Ctrl Pts',(1.01778810567666,0.587620236790417,
-2.83333333333333));
#378584=CARTESIAN_POINT('Ctrl Pts',(0.678525403784439,1.17524047358083,
-2.79166666666667));
#378585=CARTESIAN_POINT('Ctrl Pts',(0.,1.17524047358083,-2.75));
#378586=CARTESIAN_POINT('Ctrl Pts',(-0.678525403784438,1.17524047358083,
-2.70833333333333));
#378587=CARTESIAN_POINT('Ctrl Pts',(-1.01778810567666,0.587620236790418,
-2.66666666666667));
#378588=CARTESIAN_POINT('Ctrl Pts',(-1.35705080756888,6.03041012221051E-16,
-2.625));
#378589=CARTESIAN_POINT('Ctrl Pts',(-1.01778810567666,-0.587620236790416,
-2.58333333333333));
#378590=CARTESIAN_POINT('Ctrl Pts',(-0.678525403784438,-1.17524047358083,
-2.54166666666667));
#378591=CARTESIAN_POINT('Ctrl Pts',(-1.43925448419919E-16,-1.17524047358083,
-2.5));
#378592=CARTESIAN_POINT('Ctrl Pts',(0.678525403784437,-1.17524047358083,
-2.45833333333333));
#378593=CARTESIAN_POINT('Ctrl Pts',(1.01778810567666,-0.587620236790417,
-2.41666666666667));
#378594=CARTESIAN_POINT('Ctrl Pts',(1.35705080756888,2.7065942666714E-16,
-2.375));
#378595=CARTESIAN_POINT('Ctrl Pts',(1.01778810567666,0.587620236790417,
-2.33333333333333));
#378596=CARTESIAN_POINT('Ctrl Pts',(0.678525403784439,1.17524047358083,
-2.29166666666667));
#378597=CARTESIAN_POINT('Ctrl Pts',(0.,1.17524047358083,-2.25));
#378598=CARTESIAN_POINT('Ctrl Pts',(-0.678525403784438,1.17524047358083,
-2.20833333333333));
#378599=CARTESIAN_POINT('Ctrl Pts',(-1.01778810567666,0.587620236790418,
-2.16666666666667));
#378600=CARTESIAN_POINT('Ctrl Pts',(-1.35705080756888,6.03041012221051E-16,
-2.125));
#378601=CARTESIAN_POINT('Ctrl Pts',(-1.01778810567666,-0.587620236790416,
-2.08333333333333));
#378602=CARTESIAN_POINT('Ctrl Pts',(-0.678525403784438,-1.17524047358083,
-2.04166666666667));
#378603=CARTESIAN_POINT('Ctrl Pts',(-1.43925448419919E-16,-1.17524047358083,
-2.));
#378604=CARTESIAN_POINT('Ctrl Pts',(0.678525403784437,-1.17524047358083,
-1.95833333333333));
#378605=CARTESIAN_POINT('Ctrl Pts',(1.01778810567666,-0.587620236790417,
-1.91666666666667));
#378606=CARTESIAN_POINT('Ctrl Pts',(1.35705080756888,2.7065942666714E-16,
-1.875));
#378607=CARTESIAN_POINT('Ctrl Pts',(1.01778810567666,0.587620236790417,
-1.83333333333333));
#378608=CARTESIAN_POINT('Ctrl Pts',(0.678525403784439,1.17524047358083,
-1.79166666666667));
#378609=CARTESIAN_POINT('Ctrl Pts',(0.,1.17524047358083,-1.75));
#378610=CARTESIAN_POINT('Ctrl Pts',(-0.678525403784438,1.17524047358083,
-1.70833333333333));
#378611=CARTESIAN_POINT('Ctrl Pts',(-1.01778810567666,0.587620236790418,
-1.66666666666667));
#378612=CARTESIAN_POINT('Ctrl Pts',(-1.35705080756888,6.03041012221051E-16,
-1.625));
#378613=CARTESIAN_POINT('Ctrl Pts',(-1.01778810567666,-0.587620236790416,
-1.58333333333333));
#378614=CARTESIAN_POINT('Ctrl Pts',(-0.678525403784438,-1.17524047358083,
-1.54166666666667));
#378615=CARTESIAN_POINT('Ctrl Pts',(-1.43925448419919E-16,-1.17524047358083,
-1.5));
#378616=CARTESIAN_POINT('Ctrl Pts',(0.678525403784437,-1.17524047358083,
-1.45833333333333));
#378617=CARTESIAN_POINT('Ctrl Pts',(1.01778810567666,-0.587620236790417,
-1.41666666666667));
#378618=CARTESIAN_POINT('Ctrl Pts',(1.35705080756888,2.7065942666714E-16,
-1.375));
#378619=CARTESIAN_POINT('Ctrl Pts',(1.01778810567666,0.587620236790417,
-1.33333333333333));
#378620=CARTESIAN_POINT('Ctrl Pts',(0.678525403784439,1.17524047358083,
-1.29166666666667));
#378621=CARTESIAN_POINT('Ctrl Pts',(0.,1.17524047358083,-1.25));
#378622=CARTESIAN_POINT('Ctrl Pts',(-0.678525403784438,1.17524047358083,
-1.20833333333333));
#378623=CARTESIAN_POINT('Ctrl Pts',(-1.01778810567666,0.587620236790418,
-1.16666666666667));
#378624=CARTESIAN_POINT('Ctrl Pts',(-1.35705080756888,6.03041012221051E-16,
-1.125));
#378625=CARTESIAN_POINT('Ctrl Pts',(-1.01778810567666,-0.587620236790416,
-1.08333333333333));
#378626=CARTESIAN_POINT('Ctrl Pts',(-0.678525403784438,-1.17524047358083,
-1.04166666666667));
#378627=CARTESIAN_POINT('Ctrl Pts',(-1.43925448419919E-16,-1.17524047358083,
-0.999999999999999));
#378628=CARTESIAN_POINT('Ctrl Pts',(0.678525403784437,-1.17524047358083,
-0.958333333333334));
#378629=CARTESIAN_POINT('Ctrl Pts',(1.01778810567666,-0.587620236790417,
-0.916666666666666));
#378630=CARTESIAN_POINT('Ctrl Pts',(1.35705080756888,2.7065942666714E-16,
-0.874999999999999));
#378631=CARTESIAN_POINT('Ctrl Pts',(1.01778810567666,0.587620236790417,
-0.833333333333334));
#378632=CARTESIAN_POINT('Ctrl Pts',(0.678525403784439,1.17524047358083,
-0.791666666666666));
#378633=CARTESIAN_POINT('Ctrl Pts',(0.,1.17524047358083,-0.750000000000001));
#378634=CARTESIAN_POINT('Ctrl Pts',(-0.678525403784438,1.17524047358083,
-0.708333333333333));
#378635=CARTESIAN_POINT('Ctrl Pts',(-1.01778810567666,0.587620236790418,
-0.666666666666666));
#378636=CARTESIAN_POINT('Ctrl Pts',(-1.35705080756888,6.03041012221051E-16,
-0.625000000000001));
#378637=CARTESIAN_POINT('Ctrl Pts',(-1.01778810567666,-0.587620236790416,
-0.583333333333333));
#378638=CARTESIAN_POINT('Ctrl Pts',(-0.678525403784438,-1.17524047358083,
-0.541666666666666));
#378639=CARTESIAN_POINT('Ctrl Pts',(-1.43925448419919E-16,-1.17524047358083,
-0.5));
#378640=CARTESIAN_POINT('Ctrl Pts',(0.678525403784437,-1.17524047358083,
-0.458333333333333));
#378641=CARTESIAN_POINT('Ctrl Pts',(1.01778810567666,-0.587620236790417,
-0.416666666666666));
#378642=CARTESIAN_POINT('Ctrl Pts',(1.35705080756888,2.7065942666714E-16,
-0.375));
#378643=CARTESIAN_POINT('Ctrl Pts',(1.01778810567666,0.587620236790417,
-0.333333333333333));
#378644=CARTESIAN_POINT('Ctrl Pts',(0.678525403784439,1.17524047358083,
-0.291666666666666));
#378645=CARTESIAN_POINT('Ctrl Pts',(0.,1.17524047358083,-0.25));
#378646=CARTESIAN_POINT('Ctrl Pts',(-0.678525403784438,1.17524047358083,
-0.208333333333333));
#378647=CARTESIAN_POINT('Ctrl Pts',(-1.01778810567666,0.587620236790418,
-0.166666666666666));
#378648=CARTESIAN_POINT('Ctrl Pts',(-1.35705080756888,6.03041012221051E-16,
-0.125));
#378649=CARTESIAN_POINT('Ctrl Pts',(-1.01778810567666,-0.587620236790416,
-0.0833333333333328));
#378650=CARTESIAN_POINT('Ctrl Pts',(-0.678525403784438,-1.17524047358083,
-0.0416666666666673));
#378651=CARTESIAN_POINT('Ctrl Pts',(-1.43925448419919E-16,-1.17524047358083,
0.));
#378652=CARTESIAN_POINT('Ctrl Pts',(0.678525403784437,-1.17524047358083,
0.0416666666666673));
#378653=CARTESIAN_POINT('Ctrl Pts',(1.01778810567666,-0.587620236790417,
0.0833333333333328));
#378654=CARTESIAN_POINT('Ctrl Pts',(1.35705080756888,2.7065942666714E-16,
0.125));
#378655=CARTESIAN_POINT('Ctrl Pts',(1.01778810567666,0.587620236790417,
0.166666666666667));
#378656=CARTESIAN_POINT('Ctrl Pts',(0.678525403784439,1.17524047358083,
0.208333333333333));
#378657=CARTESIAN_POINT('Ctrl Pts',(0.,1.17524047358083,0.25));
#378658=CARTESIAN_POINT('Ctrl Pts',(-0.678525403784438,1.17524047358083,
0.291666666666668));
#378659=CARTESIAN_POINT('Ctrl Pts',(-1.01778810567666,0.587620236790418,
0.333333333333333));
#378660=CARTESIAN_POINT('Ctrl Pts',(-1.35705080756888,6.03041012221051E-16,
0.375));
#378661=CARTESIAN_POINT('Ctrl Pts',(-1.01778810567666,-0.587620236790416,
0.416666666666668));
#378662=CARTESIAN_POINT('Ctrl Pts',(-0.678525403784438,-1.17524047358083,
0.458333333333333));
#378663=CARTESIAN_POINT('Ctrl Pts',(-1.43925448419919E-16,-1.17524047358083,
0.5));
#378664=CARTESIAN_POINT('Ctrl Pts',(0.678525403784437,-1.17524047358083,
0.541666666666666));
#378665=CARTESIAN_POINT('Ctrl Pts',(1.01778810567666,-0.587620236790417,
0.583333333333333));
#378666=CARTESIAN_POINT('Ctrl Pts',(1.35705080756888,2.7065942666714E-16,
0.625000000000001));
#378667=CARTESIAN_POINT('Ctrl Pts',(1.01778810567666,0.587620236790417,
0.666666666666666));
#378668=CARTESIAN_POINT('Ctrl Pts',(0.678525403784439,1.17524047358083,
0.708333333333333));
#378669=CARTESIAN_POINT('Ctrl Pts',(0.,1.17524047358083,0.750000000000001));
#378670=CARTESIAN_POINT('Ctrl Pts',(-0.678525403784438,1.17524047358083,
0.791666666666666));
#378671=CARTESIAN_POINT('Ctrl Pts',(-1.01778810567666,0.587620236790418,
0.833333333333334));
#378672=CARTESIAN_POINT('Ctrl Pts',(-1.35705080756888,6.03041012221051E-16,
0.875000000000001));
#378673=CARTESIAN_POINT('Ctrl Pts',(-1.01778810567666,-0.587620236790416,
0.916666666666666));
#378674=CARTESIAN_POINT('Ctrl Pts',(-0.678525403784438,-1.17524047358083,
0.958333333333334));
#378675=CARTESIAN_POINT('Ctrl Pts',(-1.43925448419919E-16,-1.17524047358083,
1.));
#378676=CARTESIAN_POINT('Ctrl Pts',(0.678525403784437,-1.17524047358083,
1.04166666666667));
#378677=CARTESIAN_POINT('Ctrl Pts',(1.01778810567666,-0.587620236790417,
1.08333333333333));
#378678=CARTESIAN_POINT('Ctrl Pts',(1.35705080756888,2.7065942666714E-16,
1.125));
#378679=CARTESIAN_POINT('Ctrl Pts',(1.01778810567666,0.587620236790417,
1.16666666666667));
#378680=CARTESIAN_POINT('Ctrl Pts',(0.678525403784439,1.17524047358083,
1.20833333333333));
#378681=CARTESIAN_POINT('Ctrl Pts',(0.,1.17524047358083,1.25));
#378682=CARTESIAN_POINT('Ctrl Pts',(-0.678525403784438,1.17524047358083,
1.29166666666667));
#378683=CARTESIAN_POINT('Ctrl Pts',(-1.01778810567666,0.587620236790418,
1.33333333333333));
#378684=CARTESIAN_POINT('Ctrl Pts',(-1.35705080756888,6.03041012221051E-16,
1.375));
#378685=CARTESIAN_POINT('Ctrl Pts',(-1.01778810567666,-0.587620236790416,
1.41666666666667));
#378686=CARTESIAN_POINT('Ctrl Pts',(-0.678525403784438,-1.17524047358083,
1.45833333333333));
#378687=CARTESIAN_POINT('Ctrl Pts',(-1.43925448419919E-16,-1.17524047358083,
1.5));
#378688=CARTESIAN_POINT('Ctrl Pts',(0.678525403784437,-1.17524047358083,
1.54166666666667));
#378689=CARTESIAN_POINT('Ctrl Pts',(1.01778810567666,-0.587620236790417,
1.58333333333333));
#378690=CARTESIAN_POINT('Ctrl Pts',(1.35705080756888,2.7065942666714E-16,
1.625));
#378691=CARTESIAN_POINT('Ctrl Pts',(1.01778810567666,0.587620236790417,
1.66666666666667));
#378692=CARTESIAN_POINT('Ctrl Pts',(0.678525403784439,1.17524047358083,
1.70833333333333));
#378693=CARTESIAN_POINT('Ctrl Pts',(0.,1.17524047358083,1.75));
#378694=CARTESIAN_POINT('Ctrl Pts',(-0.678525403784438,1.17524047358083,
1.79166666666667));
#378695=CARTESIAN_POINT('Ctrl Pts',(-1.01778810567666,0.587620236790418,
1.83333333333333));
#378696=CARTESIAN_POINT('Ctrl Pts',(-1.35705080756888,6.03041012221051E-16,
1.875));
#378697=CARTESIAN_POINT('Ctrl Pts',(-1.01778810567666,-0.587620236790416,
1.91666666666667));
#378698=CARTESIAN_POINT('Ctrl Pts',(-0.678525403784438,-1.17524047358083,
1.95833333333333));
#378699=CARTESIAN_POINT('Ctrl Pts',(-1.43925448419919E-16,-1.17524047358083,
2.));
#378700=CARTESIAN_POINT('Ctrl Pts',(0.678525403784437,-1.17524047358083,
2.04166666666667));
#378701=CARTESIAN_POINT('Ctrl Pts',(1.01778810567666,-0.587620236790417,
2.08333333333333));
#378702=CARTESIAN_POINT('Ctrl Pts',(1.35705080756888,2.7065942666714E-16,
2.125));
#378703=CARTESIAN_POINT('Ctrl Pts',(1.01778810567666,0.587620236790417,
2.16666666666667));
#378704=CARTESIAN_POINT('Ctrl Pts',(0.678525403784439,1.17524047358083,
2.20833333333333));
#378705=CARTESIAN_POINT('Ctrl Pts',(0.,1.17524047358083,2.25));
#378706=CARTESIAN_POINT('Ctrl Pts',(-0.678525403784438,1.17524047358083,
2.29166666666667));
#378707=CARTESIAN_POINT('Ctrl Pts',(-1.01778810567666,0.587620236790418,
2.33333333333333));
#378708=CARTESIAN_POINT('Ctrl Pts',(-1.35705080756888,6.03041012221051E-16,
2.375));
#378709=CARTESIAN_POINT('Ctrl Pts',(-1.01778810567666,-0.587620236790416,
2.41666666666667));
#378710=CARTESIAN_POINT('Ctrl Pts',(-0.678525403784438,-1.17524047358083,
2.45833333333333));
#378711=CARTESIAN_POINT('Ctrl Pts',(-1.43925448419919E-16,-1.17524047358083,
2.5));
#378712=CARTESIAN_POINT('Ctrl Pts',(0.678525403784437,-1.17524047358083,
2.54166666666667));
#378713=CARTESIAN_POINT('Ctrl Pts',(1.01778810567666,-0.587620236790417,
2.58333333333333));
#378714=CARTESIAN_POINT('Ctrl Pts',(1.35705080756888,2.7065942666714E-16,
2.625));
#378715=CARTESIAN_POINT('Ctrl Pts',(1.01778810567666,0.587620236790417,
2.66666666666667));
#378716=CARTESIAN_POINT('Ctrl Pts',(0.678525403784439,1.17524047358083,
2.70833333333333));
#378717=CARTESIAN_POINT('Ctrl Pts',(0.,1.17524047358083,2.75));
#378718=CARTESIAN_POINT('Ctrl Pts',(-0.678525403784438,1.17524047358083,
2.79166666666667));
#378719=CARTESIAN_POINT('Ctrl Pts',(-1.01778810567666,0.587620236790418,
2.83333333333333));
#378720=CARTESIAN_POINT('Ctrl Pts',(-1.35705080756888,6.03041012221051E-16,
2.875));
#378721=CARTESIAN_POINT('Ctrl Pts',(-1.01778810567666,-0.587620236790416,
2.91666666666667));
#378722=CARTESIAN_POINT('Ctrl Pts',(-0.678525403784438,-1.17524047358083,
2.95833333333333));
#378723=CARTESIAN_POINT('Ctrl Pts',(-1.43925448419919E-16,-1.17524047358083,
3.));
#378724=CARTESIAN_POINT('Ctrl Pts',(0.678525403784437,-1.17524047358083,
3.04166666666667));
#378725=CARTESIAN_POINT('Ctrl Pts',(1.01778810567666,-0.587620236790417,
3.08333333333333));
#378726=CARTESIAN_POINT('Ctrl Pts',(1.35705080756888,2.7065942666714E-16,
3.125));
#378727=CARTESIAN_POINT('Ctrl Pts',(1.01778810567666,0.587620236790417,
3.16666666666667));
#378728=CARTESIAN_POINT('Ctrl Pts',(0.678525403784439,1.17524047358083,
3.20833333333333));
#378729=CARTESIAN_POINT('Ctrl Pts',(0.,1.17524047358083,3.25));
#378730=CARTESIAN_POINT('Ctrl Pts',(-0.678525403784438,1.17524047358083,
3.29166666666667));
#378731=CARTESIAN_POINT('Ctrl Pts',(-1.01778810567666,0.587620236790418,
3.33333333333333));
#378732=CARTESIAN_POINT('Ctrl Pts',(-1.35705080756888,6.03041012221051E-16,
3.375));
#378733=CARTESIAN_POINT('Ctrl Pts',(-1.01778810567666,-0.587620236790416,
3.41666666666667));
#378734=CARTESIAN_POINT('Ctrl Pts',(-0.678525403784438,-1.17524047358083,
3.45833333333333));
#378735=CARTESIAN_POINT('Ctrl Pts',(-1.43925448419919E-16,-1.17524047358083,
3.5));
#378736=CARTESIAN_POINT('Ctrl Pts',(0.678525403784437,-1.17524047358083,
3.54166666666667));
#378737=CARTESIAN_POINT('Ctrl Pts',(1.01778810567666,-0.587620236790417,
3.58333333333333));
#378738=CARTESIAN_POINT('Ctrl Pts',(1.35705080756888,2.7065942666714E-16,
3.625));
#378739=CARTESIAN_POINT('Ctrl Pts',(1.01778810567666,0.587620236790417,
3.66666666666667));
#378740=CARTESIAN_POINT('Ctrl Pts',(0.678525403784439,1.17524047358083,
3.70833333333333));
#378741=CARTESIAN_POINT('Ctrl Pts',(0.,1.17524047358083,3.75));
#378742=CARTESIAN_POINT('Ctrl Pts',(-0.678525403784438,1.17524047358083,
3.79166666666667));
#378743=CARTESIAN_POINT('Ctrl Pts',(-1.01778810567666,0.587620236790418,
3.83333333333333));
#378744=CARTESIAN_POINT('Ctrl Pts',(-1.35705080756888,6.03041012221051E-16,
3.875));
#378745=CARTESIAN_POINT('Ctrl Pts',(-1.01778810567666,-0.587620236790416,
3.91666666666667));
#378746=CARTESIAN_POINT('Ctrl Pts',(-0.678525403784438,-1.17524047358083,
3.95833333333333));
#378747=CARTESIAN_POINT('Ctrl Pts',(-1.43925448419919E-16,-1.17524047358083,
4.));
#378748=CARTESIAN_POINT('Ctrl Pts',(0.678525403784437,-1.17524047358083,
4.04166666666667));
#378749=CARTESIAN_POINT('Ctrl Pts',(1.01778810567666,-0.587620236790417,
4.08333333333333));
#378750=CARTESIAN_POINT('Ctrl Pts',(1.35705080756888,2.7065942666714E-16,
4.125));
#378751=CARTESIAN_POINT('Ctrl Pts',(1.01778810567666,0.587620236790417,
4.16666666666667));
#378752=CARTESIAN_POINT('Ctrl Pts',(0.678525403784439,1.17524047358083,
4.20833333333333));
#378753=CARTESIAN_POINT('Ctrl Pts',(0.,1.17524047358083,4.25));
#378754=CARTESIAN_POINT('Ctrl Pts',(-0.678525403784438,1.17524047358083,
4.29166666666667));
#378755=CARTESIAN_POINT('Ctrl Pts',(-1.01778810567666,0.587620236790418,
4.33333333333333));
#378756=CARTESIAN_POINT('Ctrl Pts',(-1.35705080756888,6.03041012221051E-16,
4.375));
#378757=CARTESIAN_POINT('Ctrl Pts',(-1.01778810567666,-0.587620236790416,
4.41666666666667));
#378758=CARTESIAN_POINT('Ctrl Pts',(-0.678525403784438,-1.17524047358083,
4.45833333333333));
#378759=CARTESIAN_POINT('Ctrl Pts',(-1.43925448419919E-16,-1.17524047358083,
4.5));
#378760=CARTESIAN_POINT('Ctrl Pts',(0.678525403784437,-1.17524047358083,
4.54166666666667));
#378761=CARTESIAN_POINT('Ctrl Pts',(1.01778810567666,-0.587620236790417,
4.58333333333333));
#378762=CARTESIAN_POINT('Ctrl Pts',(1.35705080756888,2.7065942666714E-16,
4.625));
#378763=CARTESIAN_POINT('Ctrl Pts',(1.01778810567666,0.587620236790417,
4.66666666666667));
#378764=CARTESIAN_POINT('Ctrl Pts',(0.678525403784439,1.17524047358083,
4.70833333333333));
#378765=CARTESIAN_POINT('Ctrl Pts',(0.,1.17524047358083,4.75));
#378766=CARTESIAN_POINT('Ctrl Pts',(-0.678525403784438,1.17524047358083,
4.79166666666667));
#378767=CARTESIAN_POINT('Ctrl Pts',(-1.01778810567666,0.587620236790418,
4.83333333333333));
#378768=CARTESIAN_POINT('Ctrl Pts',(-1.35705080756888,6.03041012221051E-16,
4.875));
#378769=CARTESIAN_POINT('Ctrl Pts',(-1.01778810567666,-0.587620236790416,
4.91666666666667));
#378770=CARTESIAN_POINT('Ctrl Pts',(-0.678525403784438,-1.17524047358083,
4.95833333333333));
#378771=CARTESIAN_POINT('Ctrl Pts',(-1.43925448419919E-16,-1.17524047358083,
5.));
#378772=CARTESIAN_POINT('Ctrl Pts',(0.678525403784437,-1.17524047358083,
5.04166666666667));
#378773=CARTESIAN_POINT('Ctrl Pts',(1.01778810567666,-0.587620236790417,
5.08333333333333));
#378774=CARTESIAN_POINT('Ctrl Pts',(1.35705080756888,2.7065942666714E-16,
5.125));
#378775=CARTESIAN_POINT('Ctrl Pts',(1.01778810567666,0.587620236790417,
5.16666666666667));
#378776=CARTESIAN_POINT('Ctrl Pts',(0.678525403784439,1.17524047358083,
5.20833333333333));
#378777=CARTESIAN_POINT('Ctrl Pts',(0.,1.17524047358083,5.25));
#378778=CARTESIAN_POINT('Ctrl Pts',(-0.678525403784438,1.17524047358083,
5.29166666666667));
#378779=CARTESIAN_POINT('Ctrl Pts',(-1.01778810567666,0.587620236790418,
5.33333333333333));
#378780=CARTESIAN_POINT('Ctrl Pts',(-1.35705080756888,6.03041012221051E-16,
5.375));
#378781=CARTESIAN_POINT('Ctrl Pts',(-1.01778810567666,-0.587620236790416,
5.41666666666667));
#378782=CARTESIAN_POINT('Ctrl Pts',(-0.678525403784438,-1.17524047358083,
5.45833333333333));
#378783=CARTESIAN_POINT('Ctrl Pts',(-1.43925448419919E-16,-1.17524047358083,
5.5));
#378784=CARTESIAN_POINT('Ctrl Pts',(0.678525403784437,-1.17524047358083,
5.54166666666667));
#378785=CARTESIAN_POINT('Ctrl Pts',(1.01778810567666,-0.587620236790417,
5.58333333333333));
#378786=CARTESIAN_POINT('Ctrl Pts',(1.35705080756888,2.7065942666714E-16,
5.625));
#378787=CARTESIAN_POINT('Ctrl Pts',(1.01778810567666,0.587620236790417,
5.66666666666667));
#378788=CARTESIAN_POINT('Ctrl Pts',(0.678525403784439,1.17524047358083,
5.70833333333333));
#378789=CARTESIAN_POINT('Ctrl Pts',(0.,1.17524047358083,5.75));
#378790=CARTESIAN_POINT('Ctrl Pts',(-0.678525403784438,1.17524047358083,
5.79166666666667));
#378791=CARTESIAN_POINT('Ctrl Pts',(-1.01778810567666,0.587620236790418,
5.83333333333333));
#378792=CARTESIAN_POINT('Ctrl Pts',(-1.35705080756888,6.03041012221051E-16,
5.875));
#378793=CARTESIAN_POINT('Ctrl Pts',(-1.01778810567666,-0.587620236790416,
5.91666666666667));
#378794=CARTESIAN_POINT('Ctrl Pts',(-0.678525403784438,-1.17524047358083,
5.95833333333333));
#378795=CARTESIAN_POINT('Ctrl Pts',(-1.43925448419919E-16,-1.17524047358083,
6.));
#378796=CARTESIAN_POINT('Ctrl Pts',(0.678525403784437,-1.17524047358083,
6.04166666666667));
#378797=CARTESIAN_POINT('Ctrl Pts',(1.01778810567666,-0.587620236790417,
6.08333333333333));
#378798=CARTESIAN_POINT('Ctrl Pts',(1.35705080756888,2.7065942666714E-16,
6.125));
#378799=CARTESIAN_POINT('Ctrl Pts',(1.01778810567666,0.587620236790417,
6.16666666666667));
#378800=CARTESIAN_POINT('Ctrl Pts',(0.678525403784439,1.17524047358083,
6.20833333333333));
#378801=CARTESIAN_POINT('Ctrl Pts',(0.,1.17524047358083,6.25));
#378802=CARTESIAN_POINT('Ctrl Pts',(0.,1.52706329386826,-9.453125));
#378803=CARTESIAN_POINT('Ctrl Pts',(-0.881650403784438,1.52706329386826,
-9.41145833333334));
#378804=CARTESIAN_POINT('Ctrl Pts',(-1.32247560567666,0.763531646934132,
-9.36979166666667));
#378805=CARTESIAN_POINT('Ctrl Pts',(-1.76330080756888,6.27916650328731E-16,
-9.328125));
#378806=CARTESIAN_POINT('Ctrl Pts',(-1.32247560567666,-0.76353164693413,
-9.28645833333333));
#378807=CARTESIAN_POINT('Ctrl Pts',(-0.881650403784439,-1.52706329386826,
-9.24479166666667));
#378808=CARTESIAN_POINT('Ctrl Pts',(-1.87011317493118E-16,-1.52706329386826,
-9.203125));
#378809=CARTESIAN_POINT('Ctrl Pts',(0.881650403784437,-1.52706329386826,
-9.16145833333333));
#378810=CARTESIAN_POINT('Ctrl Pts',(1.32247560567666,-0.763531646934131,
-9.11979166666667));
#378811=CARTESIAN_POINT('Ctrl Pts',(1.76330080756888,1.96032512344098E-16,
-9.078125));
#378812=CARTESIAN_POINT('Ctrl Pts',(1.32247560567666,0.763531646934131,
-9.03645833333334));
#378813=CARTESIAN_POINT('Ctrl Pts',(0.881650403784439,1.52706329386826,
-8.99479166666667));
#378814=CARTESIAN_POINT('Ctrl Pts',(0.,1.52706329386826,-8.953125));
#378815=CARTESIAN_POINT('Ctrl Pts',(-0.881650403784438,1.52706329386826,
-8.91145833333334));
#378816=CARTESIAN_POINT('Ctrl Pts',(-1.32247560567666,0.763531646934132,
-8.86979166666667));
#378817=CARTESIAN_POINT('Ctrl Pts',(-1.76330080756888,6.27916650328731E-16,
-8.828125));
#378818=CARTESIAN_POINT('Ctrl Pts',(-1.32247560567666,-0.76353164693413,
-8.78645833333334));
#378819=CARTESIAN_POINT('Ctrl Pts',(-0.881650403784439,-1.52706329386826,
-8.74479166666667));
#378820=CARTESIAN_POINT('Ctrl Pts',(-1.87011317493118E-16,-1.52706329386826,
-8.703125));
#378821=CARTESIAN_POINT('Ctrl Pts',(0.881650403784437,-1.52706329386826,
-8.66145833333333));
#378822=CARTESIAN_POINT('Ctrl Pts',(1.32247560567666,-0.763531646934131,
-8.61979166666667));
#378823=CARTESIAN_POINT('Ctrl Pts',(1.76330080756888,1.96032512344098E-16,
-8.578125));
#378824=CARTESIAN_POINT('Ctrl Pts',(1.32247560567666,0.763531646934131,
-8.53645833333334));
#378825=CARTESIAN_POINT('Ctrl Pts',(0.881650403784439,1.52706329386826,
-8.49479166666667));
#378826=CARTESIAN_POINT('Ctrl Pts',(0.,1.52706329386826,-8.453125));
#378827=CARTESIAN_POINT('Ctrl Pts',(-0.881650403784438,1.52706329386826,
-8.41145833333334));
#378828=CARTESIAN_POINT('Ctrl Pts',(-1.32247560567666,0.763531646934132,
-8.36979166666667));
#378829=CARTESIAN_POINT('Ctrl Pts',(-1.76330080756888,6.27916650328731E-16,
-8.328125));
#378830=CARTESIAN_POINT('Ctrl Pts',(-1.32247560567666,-0.76353164693413,
-8.28645833333334));
#378831=CARTESIAN_POINT('Ctrl Pts',(-0.881650403784439,-1.52706329386826,
-8.24479166666667));
#378832=CARTESIAN_POINT('Ctrl Pts',(-1.87011317493118E-16,-1.52706329386826,
-8.203125));
#378833=CARTESIAN_POINT('Ctrl Pts',(0.881650403784437,-1.52706329386826,
-8.16145833333333));
#378834=CARTESIAN_POINT('Ctrl Pts',(1.32247560567666,-0.763531646934131,
-8.11979166666667));
#378835=CARTESIAN_POINT('Ctrl Pts',(1.76330080756888,1.96032512344098E-16,
-8.078125));
#378836=CARTESIAN_POINT('Ctrl Pts',(1.32247560567666,0.763531646934131,
-8.03645833333333));
#378837=CARTESIAN_POINT('Ctrl Pts',(0.881650403784439,1.52706329386826,
-7.99479166666667));
#378838=CARTESIAN_POINT('Ctrl Pts',(0.,1.52706329386826,-7.953125));
#378839=CARTESIAN_POINT('Ctrl Pts',(-0.881650403784438,1.52706329386826,
-7.91145833333334));
#378840=CARTESIAN_POINT('Ctrl Pts',(-1.32247560567666,0.763531646934132,
-7.86979166666667));
#378841=CARTESIAN_POINT('Ctrl Pts',(-1.76330080756888,6.27916650328731E-16,
-7.828125));
#378842=CARTESIAN_POINT('Ctrl Pts',(-1.32247560567666,-0.76353164693413,
-7.78645833333333));
#378843=CARTESIAN_POINT('Ctrl Pts',(-0.881650403784439,-1.52706329386826,
-7.74479166666667));
#378844=CARTESIAN_POINT('Ctrl Pts',(-1.87011317493118E-16,-1.52706329386826,
-7.703125));
#378845=CARTESIAN_POINT('Ctrl Pts',(0.881650403784437,-1.52706329386826,
-7.66145833333333));
#378846=CARTESIAN_POINT('Ctrl Pts',(1.32247560567666,-0.763531646934131,
-7.61979166666667));
#378847=CARTESIAN_POINT('Ctrl Pts',(1.76330080756888,1.96032512344098E-16,
-7.578125));
#378848=CARTESIAN_POINT('Ctrl Pts',(1.32247560567666,0.763531646934131,
-7.53645833333334));
#378849=CARTESIAN_POINT('Ctrl Pts',(0.881650403784439,1.52706329386826,
-7.49479166666667));
#378850=CARTESIAN_POINT('Ctrl Pts',(0.,1.52706329386826,-7.453125));
#378851=CARTESIAN_POINT('Ctrl Pts',(-0.881650403784438,1.52706329386826,
-7.41145833333334));
#378852=CARTESIAN_POINT('Ctrl Pts',(-1.32247560567666,0.763531646934132,
-7.36979166666667));
#378853=CARTESIAN_POINT('Ctrl Pts',(-1.76330080756888,6.27916650328731E-16,
-7.328125));
#378854=CARTESIAN_POINT('Ctrl Pts',(-1.32247560567666,-0.76353164693413,
-7.28645833333334));
#378855=CARTESIAN_POINT('Ctrl Pts',(-0.881650403784439,-1.52706329386826,
-7.24479166666667));
#378856=CARTESIAN_POINT('Ctrl Pts',(-1.87011317493118E-16,-1.52706329386826,
-7.203125));
#378857=CARTESIAN_POINT('Ctrl Pts',(0.881650403784437,-1.52706329386826,
-7.16145833333333));
#378858=CARTESIAN_POINT('Ctrl Pts',(1.32247560567666,-0.763531646934131,
-7.11979166666667));
#378859=CARTESIAN_POINT('Ctrl Pts',(1.76330080756888,1.96032512344098E-16,
-7.078125));
#378860=CARTESIAN_POINT('Ctrl Pts',(1.32247560567666,0.763531646934131,
-7.03645833333334));
#378861=CARTESIAN_POINT('Ctrl Pts',(0.881650403784439,1.52706329386826,
-6.99479166666667));
#378862=CARTESIAN_POINT('Ctrl Pts',(0.,1.52706329386826,-6.953125));
#378863=CARTESIAN_POINT('Ctrl Pts',(-0.881650403784438,1.52706329386826,
-6.91145833333334));
#378864=CARTESIAN_POINT('Ctrl Pts',(-1.32247560567666,0.763531646934132,
-6.86979166666667));
#378865=CARTESIAN_POINT('Ctrl Pts',(-1.76330080756888,6.27916650328731E-16,
-6.828125));
#378866=CARTESIAN_POINT('Ctrl Pts',(-1.32247560567666,-0.76353164693413,
-6.78645833333334));
#378867=CARTESIAN_POINT('Ctrl Pts',(-0.881650403784439,-1.52706329386826,
-6.74479166666667));
#378868=CARTESIAN_POINT('Ctrl Pts',(-1.87011317493118E-16,-1.52706329386826,
-6.703125));
#378869=CARTESIAN_POINT('Ctrl Pts',(0.881650403784437,-1.52706329386826,
-6.66145833333334));
#378870=CARTESIAN_POINT('Ctrl Pts',(1.32247560567666,-0.763531646934131,
-6.61979166666667));
#378871=CARTESIAN_POINT('Ctrl Pts',(1.76330080756888,1.96032512344098E-16,
-6.578125));
#378872=CARTESIAN_POINT('Ctrl Pts',(1.32247560567666,0.763531646934131,
-6.53645833333333));
#378873=CARTESIAN_POINT('Ctrl Pts',(0.881650403784439,1.52706329386826,
-6.49479166666667));
#378874=CARTESIAN_POINT('Ctrl Pts',(0.,1.52706329386826,-6.453125));
#378875=CARTESIAN_POINT('Ctrl Pts',(-0.881650403784438,1.52706329386826,
-6.41145833333334));
#378876=CARTESIAN_POINT('Ctrl Pts',(-1.32247560567666,0.763531646934132,
-6.36979166666667));
#378877=CARTESIAN_POINT('Ctrl Pts',(-1.76330080756888,6.27916650328731E-16,
-6.328125));
#378878=CARTESIAN_POINT('Ctrl Pts',(-1.32247560567666,-0.76353164693413,
-6.28645833333334));
#378879=CARTESIAN_POINT('Ctrl Pts',(-0.881650403784439,-1.52706329386826,
-6.24479166666667));
#378880=CARTESIAN_POINT('Ctrl Pts',(-1.87011317493118E-16,-1.52706329386826,
-6.203125));
#378881=CARTESIAN_POINT('Ctrl Pts',(0.881650403784437,-1.52706329386826,
-6.16145833333333));
#378882=CARTESIAN_POINT('Ctrl Pts',(1.32247560567666,-0.763531646934131,
-6.11979166666667));
#378883=CARTESIAN_POINT('Ctrl Pts',(1.76330080756888,1.96032512344098E-16,
-6.078125));
#378884=CARTESIAN_POINT('Ctrl Pts',(1.32247560567666,0.763531646934131,
-6.03645833333334));
#378885=CARTESIAN_POINT('Ctrl Pts',(0.881650403784439,1.52706329386826,
-5.99479166666667));
#378886=CARTESIAN_POINT('Ctrl Pts',(0.,1.52706329386826,-5.953125));
#378887=CARTESIAN_POINT('Ctrl Pts',(-0.881650403784438,1.52706329386826,
-5.91145833333334));
#378888=CARTESIAN_POINT('Ctrl Pts',(-1.32247560567666,0.763531646934132,
-5.86979166666667));
#378889=CARTESIAN_POINT('Ctrl Pts',(-1.76330080756888,6.27916650328731E-16,
-5.828125));
#378890=CARTESIAN_POINT('Ctrl Pts',(-1.32247560567666,-0.76353164693413,
-5.78645833333334));
#378891=CARTESIAN_POINT('Ctrl Pts',(-0.881650403784439,-1.52706329386826,
-5.74479166666667));
#378892=CARTESIAN_POINT('Ctrl Pts',(-1.87011317493118E-16,-1.52706329386826,
-5.703125));
#378893=CARTESIAN_POINT('Ctrl Pts',(0.881650403784437,-1.52706329386826,
-5.66145833333333));
#378894=CARTESIAN_POINT('Ctrl Pts',(1.32247560567666,-0.763531646934131,
-5.61979166666667));
#378895=CARTESIAN_POINT('Ctrl Pts',(1.76330080756888,1.96032512344098E-16,
-5.578125));
#378896=CARTESIAN_POINT('Ctrl Pts',(1.32247560567666,0.763531646934131,
-5.53645833333333));
#378897=CARTESIAN_POINT('Ctrl Pts',(0.881650403784439,1.52706329386826,
-5.49479166666667));
#378898=CARTESIAN_POINT('Ctrl Pts',(0.,1.52706329386826,-5.453125));
#378899=CARTESIAN_POINT('Ctrl Pts',(-0.881650403784438,1.52706329386826,
-5.41145833333334));
#378900=CARTESIAN_POINT('Ctrl Pts',(-1.32247560567666,0.763531646934132,
-5.36979166666667));
#378901=CARTESIAN_POINT('Ctrl Pts',(-1.76330080756888,6.27916650328731E-16,
-5.328125));
#378902=CARTESIAN_POINT('Ctrl Pts',(-1.32247560567666,-0.76353164693413,
-5.28645833333333));
#378903=CARTESIAN_POINT('Ctrl Pts',(-0.881650403784439,-1.52706329386826,
-5.24479166666667));
#378904=CARTESIAN_POINT('Ctrl Pts',(-1.87011317493118E-16,-1.52706329386826,
-5.203125));
#378905=CARTESIAN_POINT('Ctrl Pts',(0.881650403784437,-1.52706329386826,
-5.16145833333333));
#378906=CARTESIAN_POINT('Ctrl Pts',(1.32247560567666,-0.763531646934131,
-5.11979166666667));
#378907=CARTESIAN_POINT('Ctrl Pts',(1.76330080756888,1.96032512344098E-16,
-5.078125));
#378908=CARTESIAN_POINT('Ctrl Pts',(1.32247560567666,0.763531646934131,
-5.03645833333333));
#378909=CARTESIAN_POINT('Ctrl Pts',(0.881650403784439,1.52706329386826,
-4.99479166666667));
#378910=CARTESIAN_POINT('Ctrl Pts',(0.,1.52706329386826,-4.953125));
#378911=CARTESIAN_POINT('Ctrl Pts',(-0.881650403784438,1.52706329386826,
-4.91145833333333));
#378912=CARTESIAN_POINT('Ctrl Pts',(-1.32247560567666,0.763531646934132,
-4.86979166666667));
#378913=CARTESIAN_POINT('Ctrl Pts',(-1.76330080756888,6.27916650328731E-16,
-4.828125));
#378914=CARTESIAN_POINT('Ctrl Pts',(-1.32247560567666,-0.76353164693413,
-4.78645833333334));
#378915=CARTESIAN_POINT('Ctrl Pts',(-0.881650403784439,-1.52706329386826,
-4.74479166666667));
#378916=CARTESIAN_POINT('Ctrl Pts',(-1.87011317493118E-16,-1.52706329386826,
-4.703125));
#378917=CARTESIAN_POINT('Ctrl Pts',(0.881650403784437,-1.52706329386826,
-4.66145833333333));
#378918=CARTESIAN_POINT('Ctrl Pts',(1.32247560567666,-0.763531646934131,
-4.61979166666667));
#378919=CARTESIAN_POINT('Ctrl Pts',(1.76330080756888,1.96032512344098E-16,
-4.578125));
#378920=CARTESIAN_POINT('Ctrl Pts',(1.32247560567666,0.763531646934131,
-4.53645833333334));
#378921=CARTESIAN_POINT('Ctrl Pts',(0.881650403784439,1.52706329386826,
-4.49479166666667));
#378922=CARTESIAN_POINT('Ctrl Pts',(0.,1.52706329386826,-4.453125));
#378923=CARTESIAN_POINT('Ctrl Pts',(-0.881650403784438,1.52706329386826,
-4.41145833333333));
#378924=CARTESIAN_POINT('Ctrl Pts',(-1.32247560567666,0.763531646934132,
-4.36979166666667));
#378925=CARTESIAN_POINT('Ctrl Pts',(-1.76330080756888,6.27916650328731E-16,
-4.328125));
#378926=CARTESIAN_POINT('Ctrl Pts',(-1.32247560567666,-0.76353164693413,
-4.28645833333333));
#378927=CARTESIAN_POINT('Ctrl Pts',(-0.881650403784439,-1.52706329386826,
-4.24479166666667));
#378928=CARTESIAN_POINT('Ctrl Pts',(-1.87011317493118E-16,-1.52706329386826,
-4.203125));
#378929=CARTESIAN_POINT('Ctrl Pts',(0.881650403784437,-1.52706329386826,
-4.16145833333333));
#378930=CARTESIAN_POINT('Ctrl Pts',(1.32247560567666,-0.763531646934131,
-4.11979166666667));
#378931=CARTESIAN_POINT('Ctrl Pts',(1.76330080756888,1.96032512344098E-16,
-4.078125));
#378932=CARTESIAN_POINT('Ctrl Pts',(1.32247560567666,0.763531646934131,
-4.03645833333333));
#378933=CARTESIAN_POINT('Ctrl Pts',(0.881650403784439,1.52706329386826,
-3.99479166666667));
#378934=CARTESIAN_POINT('Ctrl Pts',(0.,1.52706329386826,-3.953125));
#378935=CARTESIAN_POINT('Ctrl Pts',(-0.881650403784438,1.52706329386826,
-3.91145833333334));
#378936=CARTESIAN_POINT('Ctrl Pts',(-1.32247560567666,0.763531646934132,
-3.86979166666667));
#378937=CARTESIAN_POINT('Ctrl Pts',(-1.76330080756888,6.27916650328731E-16,
-3.828125));
#378938=CARTESIAN_POINT('Ctrl Pts',(-1.32247560567666,-0.76353164693413,
-3.78645833333334));
#378939=CARTESIAN_POINT('Ctrl Pts',(-0.881650403784439,-1.52706329386826,
-3.74479166666667));
#378940=CARTESIAN_POINT('Ctrl Pts',(-1.87011317493118E-16,-1.52706329386826,
-3.703125));
#378941=CARTESIAN_POINT('Ctrl Pts',(0.881650403784437,-1.52706329386826,
-3.66145833333334));
#378942=CARTESIAN_POINT('Ctrl Pts',(1.32247560567666,-0.763531646934131,
-3.61979166666667));
#378943=CARTESIAN_POINT('Ctrl Pts',(1.76330080756888,1.96032512344098E-16,
-3.578125));
#378944=CARTESIAN_POINT('Ctrl Pts',(1.32247560567666,0.763531646934131,
-3.53645833333333));
#378945=CARTESIAN_POINT('Ctrl Pts',(0.881650403784439,1.52706329386826,
-3.49479166666667));
#378946=CARTESIAN_POINT('Ctrl Pts',(0.,1.52706329386826,-3.453125));
#378947=CARTESIAN_POINT('Ctrl Pts',(-0.881650403784438,1.52706329386826,
-3.41145833333334));
#378948=CARTESIAN_POINT('Ctrl Pts',(-1.32247560567666,0.763531646934132,
-3.36979166666667));
#378949=CARTESIAN_POINT('Ctrl Pts',(-1.76330080756888,6.27916650328731E-16,
-3.328125));
#378950=CARTESIAN_POINT('Ctrl Pts',(-1.32247560567666,-0.76353164693413,
-3.28645833333334));
#378951=CARTESIAN_POINT('Ctrl Pts',(-0.881650403784439,-1.52706329386826,
-3.24479166666667));
#378952=CARTESIAN_POINT('Ctrl Pts',(-1.87011317493118E-16,-1.52706329386826,
-3.203125));
#378953=CARTESIAN_POINT('Ctrl Pts',(0.881650403784437,-1.52706329386826,
-3.16145833333334));
#378954=CARTESIAN_POINT('Ctrl Pts',(1.32247560567666,-0.763531646934131,
-3.11979166666667));
#378955=CARTESIAN_POINT('Ctrl Pts',(1.76330080756888,1.96032512344098E-16,
-3.078125));
#378956=CARTESIAN_POINT('Ctrl Pts',(1.32247560567666,0.763531646934131,
-3.03645833333333));
#378957=CARTESIAN_POINT('Ctrl Pts',(0.881650403784439,1.52706329386826,
-2.99479166666667));
#378958=CARTESIAN_POINT('Ctrl Pts',(0.,1.52706329386826,-2.953125));
#378959=CARTESIAN_POINT('Ctrl Pts',(-0.881650403784438,1.52706329386826,
-2.91145833333334));
#378960=CARTESIAN_POINT('Ctrl Pts',(-1.32247560567666,0.763531646934132,
-2.86979166666667));
#378961=CARTESIAN_POINT('Ctrl Pts',(-1.76330080756888,6.27916650328731E-16,
-2.828125));
#378962=CARTESIAN_POINT('Ctrl Pts',(-1.32247560567666,-0.76353164693413,
-2.78645833333334));
#378963=CARTESIAN_POINT('Ctrl Pts',(-0.881650403784439,-1.52706329386826,
-2.74479166666667));
#378964=CARTESIAN_POINT('Ctrl Pts',(-1.87011317493118E-16,-1.52706329386826,
-2.703125));
#378965=CARTESIAN_POINT('Ctrl Pts',(0.881650403784437,-1.52706329386826,
-2.66145833333334));
#378966=CARTESIAN_POINT('Ctrl Pts',(1.32247560567666,-0.763531646934131,
-2.61979166666667));
#378967=CARTESIAN_POINT('Ctrl Pts',(1.76330080756888,1.96032512344098E-16,
-2.578125));
#378968=CARTESIAN_POINT('Ctrl Pts',(1.32247560567666,0.763531646934131,
-2.53645833333334));
#378969=CARTESIAN_POINT('Ctrl Pts',(0.881650403784439,1.52706329386826,
-2.49479166666667));
#378970=CARTESIAN_POINT('Ctrl Pts',(0.,1.52706329386826,-2.453125));
#378971=CARTESIAN_POINT('Ctrl Pts',(-0.881650403784438,1.52706329386826,
-2.41145833333334));
#378972=CARTESIAN_POINT('Ctrl Pts',(-1.32247560567666,0.763531646934132,
-2.36979166666667));
#378973=CARTESIAN_POINT('Ctrl Pts',(-1.76330080756888,6.27916650328731E-16,
-2.328125));
#378974=CARTESIAN_POINT('Ctrl Pts',(-1.32247560567666,-0.76353164693413,
-2.28645833333333));
#378975=CARTESIAN_POINT('Ctrl Pts',(-0.881650403784439,-1.52706329386826,
-2.24479166666667));
#378976=CARTESIAN_POINT('Ctrl Pts',(-1.87011317493118E-16,-1.52706329386826,
-2.203125));
#378977=CARTESIAN_POINT('Ctrl Pts',(0.881650403784437,-1.52706329386826,
-2.16145833333333));
#378978=CARTESIAN_POINT('Ctrl Pts',(1.32247560567666,-0.763531646934131,
-2.11979166666667));
#378979=CARTESIAN_POINT('Ctrl Pts',(1.76330080756888,1.96032512344098E-16,
-2.078125));
#378980=CARTESIAN_POINT('Ctrl Pts',(1.32247560567666,0.763531646934131,
-2.03645833333334));
#378981=CARTESIAN_POINT('Ctrl Pts',(0.881650403784439,1.52706329386826,
-1.99479166666667));
#378982=CARTESIAN_POINT('Ctrl Pts',(0.,1.52706329386826,-1.953125));
#378983=CARTESIAN_POINT('Ctrl Pts',(-0.881650403784438,1.52706329386826,
-1.91145833333334));
#378984=CARTESIAN_POINT('Ctrl Pts',(-1.32247560567666,0.763531646934132,
-1.86979166666667));
#378985=CARTESIAN_POINT('Ctrl Pts',(-1.76330080756888,6.27916650328731E-16,
-1.828125));
#378986=CARTESIAN_POINT('Ctrl Pts',(-1.32247560567666,-0.76353164693413,
-1.78645833333334));
#378987=CARTESIAN_POINT('Ctrl Pts',(-0.881650403784439,-1.52706329386826,
-1.74479166666667));
#378988=CARTESIAN_POINT('Ctrl Pts',(-1.87011317493118E-16,-1.52706329386826,
-1.703125));
#378989=CARTESIAN_POINT('Ctrl Pts',(0.881650403784437,-1.52706329386826,
-1.66145833333334));
#378990=CARTESIAN_POINT('Ctrl Pts',(1.32247560567666,-0.763531646934131,
-1.61979166666667));
#378991=CARTESIAN_POINT('Ctrl Pts',(1.76330080756888,1.96032512344098E-16,
-1.578125));
#378992=CARTESIAN_POINT('Ctrl Pts',(1.32247560567666,0.763531646934131,
-1.53645833333334));
#378993=CARTESIAN_POINT('Ctrl Pts',(0.881650403784439,1.52706329386826,
-1.49479166666667));
#378994=CARTESIAN_POINT('Ctrl Pts',(0.,1.52706329386826,-1.453125));
#378995=CARTESIAN_POINT('Ctrl Pts',(-0.881650403784438,1.52706329386826,
-1.41145833333334));
#378996=CARTESIAN_POINT('Ctrl Pts',(-1.32247560567666,0.763531646934132,
-1.36979166666667));
#378997=CARTESIAN_POINT('Ctrl Pts',(-1.76330080756888,6.27916650328731E-16,
-1.328125));
#378998=CARTESIAN_POINT('Ctrl Pts',(-1.32247560567666,-0.76353164693413,
-1.28645833333334));
#378999=CARTESIAN_POINT('Ctrl Pts',(-0.881650403784439,-1.52706329386826,
-1.24479166666667));
#379000=CARTESIAN_POINT('Ctrl Pts',(-1.87011317493118E-16,-1.52706329386826,
-1.203125));
#379001=CARTESIAN_POINT('Ctrl Pts',(0.881650403784437,-1.52706329386826,
-1.16145833333334));
#379002=CARTESIAN_POINT('Ctrl Pts',(1.32247560567666,-0.763531646934131,
-1.11979166666667));
#379003=CARTESIAN_POINT('Ctrl Pts',(1.76330080756888,1.96032512344098E-16,
-1.078125));
#379004=CARTESIAN_POINT('Ctrl Pts',(1.32247560567666,0.763531646934131,
-1.03645833333334));
#379005=CARTESIAN_POINT('Ctrl Pts',(0.881650403784439,1.52706329386826,
-0.994791666666668));
#379006=CARTESIAN_POINT('Ctrl Pts',(0.,1.52706329386826,-0.953125000000003));
#379007=CARTESIAN_POINT('Ctrl Pts',(-0.881650403784438,1.52706329386826,
-0.911458333333335));
#379008=CARTESIAN_POINT('Ctrl Pts',(-1.32247560567666,0.763531646934132,
-0.869791666666668));
#379009=CARTESIAN_POINT('Ctrl Pts',(-1.76330080756888,6.27916650328731E-16,
-0.828125000000002));
#379010=CARTESIAN_POINT('Ctrl Pts',(-1.32247560567666,-0.76353164693413,
-0.786458333333335));
#379011=CARTESIAN_POINT('Ctrl Pts',(-0.881650403784439,-1.52706329386826,
-0.744791666666668));
#379012=CARTESIAN_POINT('Ctrl Pts',(-1.87011317493118E-16,-1.52706329386826,
-0.703125000000002));
#379013=CARTESIAN_POINT('Ctrl Pts',(0.881650403784437,-1.52706329386826,
-0.661458333333335));
#379014=CARTESIAN_POINT('Ctrl Pts',(1.32247560567666,-0.763531646934131,
-0.619791666666668));
#379015=CARTESIAN_POINT('Ctrl Pts',(1.76330080756888,1.96032512344098E-16,
-0.578125000000002));
#379016=CARTESIAN_POINT('Ctrl Pts',(1.32247560567666,0.763531646934131,
-0.536458333333335));
#379017=CARTESIAN_POINT('Ctrl Pts',(0.881650403784439,1.52706329386826,
-0.494791666666668));
#379018=CARTESIAN_POINT('Ctrl Pts',(0.,1.52706329386826,-0.453125000000002));
#379019=CARTESIAN_POINT('Ctrl Pts',(-0.881650403784438,1.52706329386826,
-0.411458333333335));
#379020=CARTESIAN_POINT('Ctrl Pts',(-1.32247560567666,0.763531646934132,
-0.369791666666668));
#379021=CARTESIAN_POINT('Ctrl Pts',(-1.76330080756888,6.27916650328731E-16,
-0.328125000000002));
#379022=CARTESIAN_POINT('Ctrl Pts',(-1.32247560567666,-0.76353164693413,
-0.286458333333335));
#379023=CARTESIAN_POINT('Ctrl Pts',(-0.881650403784439,-1.52706329386826,
-0.244791666666669));
#379024=CARTESIAN_POINT('Ctrl Pts',(-1.87011317493118E-16,-1.52706329386826,
-0.203125000000002));
#379025=CARTESIAN_POINT('Ctrl Pts',(0.881650403784437,-1.52706329386826,
-0.161458333333335));
#379026=CARTESIAN_POINT('Ctrl Pts',(1.32247560567666,-0.763531646934131,
-0.119791666666669));
#379027=CARTESIAN_POINT('Ctrl Pts',(1.76330080756888,1.96032512344098E-16,
-0.0781250000000018));
#379028=CARTESIAN_POINT('Ctrl Pts',(1.32247560567666,0.763531646934131,
-0.0364583333333345));
#379029=CARTESIAN_POINT('Ctrl Pts',(0.881650403784439,1.52706329386826,
0.00520833333333102));
#379030=CARTESIAN_POINT('Ctrl Pts',(0.,1.52706329386826,0.0468749999999983));
#379031=CARTESIAN_POINT('Ctrl Pts',(-0.881650403784438,1.52706329386826,
0.0885416666666656));
#379032=CARTESIAN_POINT('Ctrl Pts',(-1.32247560567666,0.763531646934132,
0.130208333333331));
#379033=CARTESIAN_POINT('Ctrl Pts',(-1.76330080756888,6.27916650328731E-16,
0.171874999999998));
#379034=CARTESIAN_POINT('Ctrl Pts',(-1.32247560567666,-0.76353164693413,
0.213541666666666));
#379035=CARTESIAN_POINT('Ctrl Pts',(-0.881650403784439,-1.52706329386826,
0.255208333333331));
#379036=CARTESIAN_POINT('Ctrl Pts',(-1.87011317493118E-16,-1.52706329386826,
0.296874999999999));
#379037=CARTESIAN_POINT('Ctrl Pts',(0.881650403784437,-1.52706329386826,
0.338541666666664));
#379038=CARTESIAN_POINT('Ctrl Pts',(1.32247560567666,-0.763531646934131,
0.380208333333331));
#379039=CARTESIAN_POINT('Ctrl Pts',(1.76330080756888,1.96032512344098E-16,
0.421874999999999));
#379040=CARTESIAN_POINT('Ctrl Pts',(1.32247560567666,0.763531646934131,
0.463541666666664));
#379041=CARTESIAN_POINT('Ctrl Pts',(0.881650403784439,1.52706329386826,
0.505208333333331));
#379042=CARTESIAN_POINT('Ctrl Pts',(0.,1.52706329386826,0.546874999999999));
#379043=CARTESIAN_POINT('Ctrl Pts',(-0.881650403784438,1.52706329386826,
0.588541666666664));
#379044=CARTESIAN_POINT('Ctrl Pts',(-1.32247560567666,0.763531646934132,
0.630208333333332));
#379045=CARTESIAN_POINT('Ctrl Pts',(-1.76330080756888,6.27916650328732E-16,
0.671874999999999));
#379046=CARTESIAN_POINT('Ctrl Pts',(-1.32247560567666,-0.76353164693413,
0.713541666666664));
#379047=CARTESIAN_POINT('Ctrl Pts',(-0.881650403784439,-1.52706329386826,
0.755208333333332));
#379048=CARTESIAN_POINT('Ctrl Pts',(-1.87011317493118E-16,-1.52706329386826,
0.796874999999999));
#379049=CARTESIAN_POINT('Ctrl Pts',(0.881650403784437,-1.52706329386826,
0.838541666666665));
#379050=CARTESIAN_POINT('Ctrl Pts',(1.32247560567666,-0.763531646934131,
0.880208333333332));
#379051=CARTESIAN_POINT('Ctrl Pts',(1.76330080756888,1.96032512344098E-16,
0.921874999999997));
#379052=CARTESIAN_POINT('Ctrl Pts',(1.32247560567666,0.763531646934131,
0.963541666666665));
#379053=CARTESIAN_POINT('Ctrl Pts',(0.881650403784439,1.52706329386826,
1.00520833333333));
#379054=CARTESIAN_POINT('Ctrl Pts',(0.,1.52706329386826,1.046875));
#379055=CARTESIAN_POINT('Ctrl Pts',(-0.881650403784438,1.52706329386826,
1.08854166666666));
#379056=CARTESIAN_POINT('Ctrl Pts',(-1.32247560567666,0.763531646934132,
1.13020833333333));
#379057=CARTESIAN_POINT('Ctrl Pts',(-1.76330080756888,6.27916650328732E-16,
1.171875));
#379058=CARTESIAN_POINT('Ctrl Pts',(-1.32247560567666,-0.76353164693413,
1.21354166666666));
#379059=CARTESIAN_POINT('Ctrl Pts',(-0.881650403784439,-1.52706329386826,
1.25520833333333));
#379060=CARTESIAN_POINT('Ctrl Pts',(-1.87011317493118E-16,-1.52706329386826,
1.296875));
#379061=CARTESIAN_POINT('Ctrl Pts',(0.881650403784437,-1.52706329386826,
1.33854166666667));
#379062=CARTESIAN_POINT('Ctrl Pts',(1.32247560567666,-0.763531646934131,
1.38020833333333));
#379063=CARTESIAN_POINT('Ctrl Pts',(1.76330080756888,1.96032512344098E-16,
1.421875));
#379064=CARTESIAN_POINT('Ctrl Pts',(1.32247560567666,0.763531646934131,
1.46354166666667));
#379065=CARTESIAN_POINT('Ctrl Pts',(0.881650403784439,1.52706329386826,
1.50520833333333));
#379066=CARTESIAN_POINT('Ctrl Pts',(0.,1.52706329386826,1.546875));
#379067=CARTESIAN_POINT('Ctrl Pts',(-0.881650403784438,1.52706329386826,
1.58854166666667));
#379068=CARTESIAN_POINT('Ctrl Pts',(-1.32247560567666,0.763531646934132,
1.63020833333333));
#379069=CARTESIAN_POINT('Ctrl Pts',(-1.76330080756888,6.27916650328732E-16,
1.671875));
#379070=CARTESIAN_POINT('Ctrl Pts',(-1.32247560567666,-0.76353164693413,
1.71354166666667));
#379071=CARTESIAN_POINT('Ctrl Pts',(-0.881650403784439,-1.52706329386826,
1.75520833333333));
#379072=CARTESIAN_POINT('Ctrl Pts',(-1.87011317493118E-16,-1.52706329386826,
1.796875));
#379073=CARTESIAN_POINT('Ctrl Pts',(0.881650403784437,-1.52706329386826,
1.83854166666667));
#379074=CARTESIAN_POINT('Ctrl Pts',(1.32247560567666,-0.763531646934131,
1.88020833333333));
#379075=CARTESIAN_POINT('Ctrl Pts',(1.76330080756888,1.96032512344098E-16,
1.921875));
#379076=CARTESIAN_POINT('Ctrl Pts',(1.32247560567666,0.763531646934131,
1.96354166666667));
#379077=CARTESIAN_POINT('Ctrl Pts',(0.881650403784439,1.52706329386826,
2.00520833333333));
#379078=CARTESIAN_POINT('Ctrl Pts',(0.,1.52706329386826,2.046875));
#379079=CARTESIAN_POINT('Ctrl Pts',(-0.881650403784438,1.52706329386826,
2.08854166666667));
#379080=CARTESIAN_POINT('Ctrl Pts',(-1.32247560567666,0.763531646934132,
2.13020833333333));
#379081=CARTESIAN_POINT('Ctrl Pts',(-1.76330080756888,6.27916650328732E-16,
2.171875));
#379082=CARTESIAN_POINT('Ctrl Pts',(-1.32247560567666,-0.76353164693413,
2.21354166666666));
#379083=CARTESIAN_POINT('Ctrl Pts',(-0.881650403784439,-1.52706329386826,
2.25520833333333));
#379084=CARTESIAN_POINT('Ctrl Pts',(-1.87011317493118E-16,-1.52706329386826,
2.296875));
#379085=CARTESIAN_POINT('Ctrl Pts',(0.881650403784437,-1.52706329386826,
2.33854166666666));
#379086=CARTESIAN_POINT('Ctrl Pts',(1.32247560567666,-0.763531646934131,
2.38020833333333));
#379087=CARTESIAN_POINT('Ctrl Pts',(1.76330080756888,1.96032512344098E-16,
2.421875));
#379088=CARTESIAN_POINT('Ctrl Pts',(1.32247560567666,0.763531646934131,
2.46354166666666));
#379089=CARTESIAN_POINT('Ctrl Pts',(0.881650403784439,1.52706329386826,
2.50520833333333));
#379090=CARTESIAN_POINT('Ctrl Pts',(0.,1.52706329386826,2.546875));
#379091=CARTESIAN_POINT('Ctrl Pts',(-0.881650403784438,1.52706329386826,
2.58854166666666));
#379092=CARTESIAN_POINT('Ctrl Pts',(-1.32247560567666,0.763531646934132,
2.63020833333333));
#379093=CARTESIAN_POINT('Ctrl Pts',(-1.76330080756888,6.27916650328732E-16,
2.671875));
#379094=CARTESIAN_POINT('Ctrl Pts',(-1.32247560567666,-0.76353164693413,
2.71354166666666));
#379095=CARTESIAN_POINT('Ctrl Pts',(-0.881650403784439,-1.52706329386826,
2.75520833333333));
#379096=CARTESIAN_POINT('Ctrl Pts',(-1.87011317493118E-16,-1.52706329386826,
2.796875));
#379097=CARTESIAN_POINT('Ctrl Pts',(0.881650403784437,-1.52706329386826,
2.83854166666666));
#379098=CARTESIAN_POINT('Ctrl Pts',(1.32247560567666,-0.763531646934131,
2.88020833333333));
#379099=CARTESIAN_POINT('Ctrl Pts',(1.76330080756888,1.96032512344098E-16,
2.921875));
#379100=CARTESIAN_POINT('Ctrl Pts',(1.32247560567666,0.763531646934131,
2.96354166666666));
#379101=CARTESIAN_POINT('Ctrl Pts',(0.881650403784439,1.52706329386826,
3.00520833333333));
#379102=CARTESIAN_POINT('Ctrl Pts',(0.,1.52706329386826,3.046875));
#379103=CARTESIAN_POINT('Ctrl Pts',(-0.881650403784438,1.52706329386826,
3.08854166666666));
#379104=CARTESIAN_POINT('Ctrl Pts',(-1.32247560567666,0.763531646934132,
3.13020833333333));
#379105=CARTESIAN_POINT('Ctrl Pts',(-1.76330080756888,6.27916650328732E-16,
3.171875));
#379106=CARTESIAN_POINT('Ctrl Pts',(-1.32247560567666,-0.76353164693413,
3.21354166666667));
#379107=CARTESIAN_POINT('Ctrl Pts',(-0.881650403784439,-1.52706329386826,
3.25520833333333));
#379108=CARTESIAN_POINT('Ctrl Pts',(-1.87011317493118E-16,-1.52706329386826,
3.296875));
#379109=CARTESIAN_POINT('Ctrl Pts',(0.881650403784437,-1.52706329386826,
3.33854166666667));
#379110=CARTESIAN_POINT('Ctrl Pts',(1.32247560567666,-0.763531646934131,
3.38020833333333));
#379111=CARTESIAN_POINT('Ctrl Pts',(1.76330080756888,1.96032512344098E-16,
3.421875));
#379112=CARTESIAN_POINT('Ctrl Pts',(1.32247560567666,0.763531646934131,
3.46354166666667));
#379113=CARTESIAN_POINT('Ctrl Pts',(0.881650403784439,1.52706329386826,
3.50520833333333));
#379114=CARTESIAN_POINT('Ctrl Pts',(0.,1.52706329386826,3.546875));
#379115=CARTESIAN_POINT('Ctrl Pts',(-0.881650403784438,1.52706329386826,
3.58854166666667));
#379116=CARTESIAN_POINT('Ctrl Pts',(-1.32247560567666,0.763531646934132,
3.63020833333333));
#379117=CARTESIAN_POINT('Ctrl Pts',(-1.76330080756888,6.27916650328732E-16,
3.671875));
#379118=CARTESIAN_POINT('Ctrl Pts',(-1.32247560567666,-0.76353164693413,
3.71354166666667));
#379119=CARTESIAN_POINT('Ctrl Pts',(-0.881650403784439,-1.52706329386826,
3.75520833333333));
#379120=CARTESIAN_POINT('Ctrl Pts',(-1.87011317493118E-16,-1.52706329386826,
3.796875));
#379121=CARTESIAN_POINT('Ctrl Pts',(0.881650403784437,-1.52706329386826,
3.83854166666667));
#379122=CARTESIAN_POINT('Ctrl Pts',(1.32247560567666,-0.763531646934131,
3.88020833333333));
#379123=CARTESIAN_POINT('Ctrl Pts',(1.76330080756888,1.96032512344098E-16,
3.921875));
#379124=CARTESIAN_POINT('Ctrl Pts',(1.32247560567666,0.763531646934131,
3.96354166666667));
#379125=CARTESIAN_POINT('Ctrl Pts',(0.881650403784439,1.52706329386826,
4.00520833333333));
#379126=CARTESIAN_POINT('Ctrl Pts',(0.,1.52706329386826,4.046875));
#379127=CARTESIAN_POINT('Ctrl Pts',(-0.881650403784438,1.52706329386826,
4.08854166666666));
#379128=CARTESIAN_POINT('Ctrl Pts',(-1.32247560567666,0.763531646934132,
4.13020833333333));
#379129=CARTESIAN_POINT('Ctrl Pts',(-1.76330080756888,6.27916650328732E-16,
4.171875));
#379130=CARTESIAN_POINT('Ctrl Pts',(-1.32247560567666,-0.76353164693413,
4.21354166666666));
#379131=CARTESIAN_POINT('Ctrl Pts',(-0.881650403784439,-1.52706329386826,
4.25520833333333));
#379132=CARTESIAN_POINT('Ctrl Pts',(-1.87011317493118E-16,-1.52706329386826,
4.296875));
#379133=CARTESIAN_POINT('Ctrl Pts',(0.881650403784437,-1.52706329386826,
4.33854166666666));
#379134=CARTESIAN_POINT('Ctrl Pts',(1.32247560567666,-0.763531646934131,
4.38020833333333));
#379135=CARTESIAN_POINT('Ctrl Pts',(1.76330080756888,1.96032512344098E-16,
4.421875));
#379136=CARTESIAN_POINT('Ctrl Pts',(1.32247560567666,0.763531646934131,
4.46354166666666));
#379137=CARTESIAN_POINT('Ctrl Pts',(0.881650403784439,1.52706329386826,
4.50520833333333));
#379138=CARTESIAN_POINT('Ctrl Pts',(0.,1.52706329386826,4.546875));
#379139=CARTESIAN_POINT('Ctrl Pts',(-0.881650403784438,1.52706329386826,
4.58854166666666));
#379140=CARTESIAN_POINT('Ctrl Pts',(-1.32247560567666,0.763531646934132,
4.63020833333333));
#379141=CARTESIAN_POINT('Ctrl Pts',(-1.76330080756888,6.27916650328732E-16,
4.671875));
#379142=CARTESIAN_POINT('Ctrl Pts',(-1.32247560567666,-0.76353164693413,
4.71354166666666));
#379143=CARTESIAN_POINT('Ctrl Pts',(-0.881650403784439,-1.52706329386826,
4.75520833333333));
#379144=CARTESIAN_POINT('Ctrl Pts',(-1.87011317493118E-16,-1.52706329386826,
4.796875));
#379145=CARTESIAN_POINT('Ctrl Pts',(0.881650403784437,-1.52706329386826,
4.83854166666667));
#379146=CARTESIAN_POINT('Ctrl Pts',(1.32247560567666,-0.763531646934131,
4.88020833333333));
#379147=CARTESIAN_POINT('Ctrl Pts',(1.76330080756888,1.96032512344098E-16,
4.921875));
#379148=CARTESIAN_POINT('Ctrl Pts',(1.32247560567666,0.763531646934131,
4.96354166666666));
#379149=CARTESIAN_POINT('Ctrl Pts',(0.881650403784439,1.52706329386826,
5.00520833333333));
#379150=CARTESIAN_POINT('Ctrl Pts',(0.,1.52706329386826,5.046875));
#379151=CARTESIAN_POINT('Ctrl Pts',(-0.881650403784438,1.52706329386826,
5.08854166666667));
#379152=CARTESIAN_POINT('Ctrl Pts',(-1.32247560567666,0.763531646934132,
5.13020833333333));
#379153=CARTESIAN_POINT('Ctrl Pts',(-1.76330080756888,6.27916650328732E-16,
5.171875));
#379154=CARTESIAN_POINT('Ctrl Pts',(-1.32247560567666,-0.76353164693413,
5.21354166666667));
#379155=CARTESIAN_POINT('Ctrl Pts',(-0.881650403784439,-1.52706329386826,
5.25520833333333));
#379156=CARTESIAN_POINT('Ctrl Pts',(-1.87011317493118E-16,-1.52706329386826,
5.296875));
#379157=CARTESIAN_POINT('Ctrl Pts',(0.881650403784437,-1.52706329386826,
5.33854166666667));
#379158=CARTESIAN_POINT('Ctrl Pts',(1.32247560567666,-0.763531646934131,
5.38020833333333));
#379159=CARTESIAN_POINT('Ctrl Pts',(1.76330080756888,1.96032512344098E-16,
5.421875));
#379160=CARTESIAN_POINT('Ctrl Pts',(1.32247560567666,0.763531646934131,
5.46354166666667));
#379161=CARTESIAN_POINT('Ctrl Pts',(0.881650403784439,1.52706329386826,
5.50520833333333));
#379162=CARTESIAN_POINT('Ctrl Pts',(0.,1.52706329386826,5.546875));
#379163=CARTESIAN_POINT('Ctrl Pts',(-0.881650403784438,1.52706329386826,
5.58854166666667));
#379164=CARTESIAN_POINT('Ctrl Pts',(-1.32247560567666,0.763531646934132,
5.63020833333333));
#379165=CARTESIAN_POINT('Ctrl Pts',(-1.76330080756888,6.27916650328732E-16,
5.671875));
#379166=CARTESIAN_POINT('Ctrl Pts',(-1.32247560567666,-0.76353164693413,
5.71354166666667));
#379167=CARTESIAN_POINT('Ctrl Pts',(-0.881650403784439,-1.52706329386826,
5.75520833333333));
#379168=CARTESIAN_POINT('Ctrl Pts',(-1.87011317493118E-16,-1.52706329386826,
5.796875));
#379169=CARTESIAN_POINT('Ctrl Pts',(0.881650403784437,-1.52706329386826,
5.83854166666667));
#379170=CARTESIAN_POINT('Ctrl Pts',(1.32247560567666,-0.763531646934131,
5.88020833333333));
#379171=CARTESIAN_POINT('Ctrl Pts',(1.76330080756888,1.96032512344098E-16,
5.921875));
#379172=CARTESIAN_POINT('Ctrl Pts',(1.32247560567666,0.763531646934131,
5.96354166666666));
#379173=CARTESIAN_POINT('Ctrl Pts',(0.881650403784439,1.52706329386826,
6.00520833333333));
#379174=CARTESIAN_POINT('Ctrl Pts',(0.,1.52706329386826,6.046875));
#379175=CARTESIAN_POINT('Ctrl Pts',(0.,1.52706329386826,-8.984375));
#379176=CARTESIAN_POINT('Ctrl Pts',(-0.881650403784438,1.52706329386826,
-8.94270833333333));
#379177=CARTESIAN_POINT('Ctrl Pts',(-1.32247560567666,0.763531646934132,
-8.90104166666666));
#379178=CARTESIAN_POINT('Ctrl Pts',(-1.76330080756888,6.27916650328731E-16,
-8.859375));
#379179=CARTESIAN_POINT('Ctrl Pts',(-1.32247560567666,-0.76353164693413,
-8.81770833333333));
#379180=CARTESIAN_POINT('Ctrl Pts',(-0.881650403784439,-1.52706329386826,
-8.77604166666666));
#379181=CARTESIAN_POINT('Ctrl Pts',(-1.87011317493118E-16,-1.52706329386826,
-8.734375));
#379182=CARTESIAN_POINT('Ctrl Pts',(0.881650403784437,-1.52706329386826,
-8.69270833333333));
#379183=CARTESIAN_POINT('Ctrl Pts',(1.32247560567666,-0.763531646934131,
-8.65104166666666));
#379184=CARTESIAN_POINT('Ctrl Pts',(1.76330080756888,1.96032512344098E-16,
-8.609375));
#379185=CARTESIAN_POINT('Ctrl Pts',(1.32247560567666,0.763531646934131,
-8.56770833333333));
#379186=CARTESIAN_POINT('Ctrl Pts',(0.881650403784439,1.52706329386826,
-8.52604166666666));
#379187=CARTESIAN_POINT('Ctrl Pts',(0.,1.52706329386826,-8.484375));
#379188=CARTESIAN_POINT('Ctrl Pts',(-0.881650403784438,1.52706329386826,
-8.44270833333333));
#379189=CARTESIAN_POINT('Ctrl Pts',(-1.32247560567666,0.763531646934132,
-8.40104166666666));
#379190=CARTESIAN_POINT('Ctrl Pts',(-1.76330080756888,6.27916650328731E-16,
-8.359375));
#379191=CARTESIAN_POINT('Ctrl Pts',(-1.32247560567666,-0.76353164693413,
-8.31770833333333));
#379192=CARTESIAN_POINT('Ctrl Pts',(-0.881650403784439,-1.52706329386826,
-8.27604166666666));
#379193=CARTESIAN_POINT('Ctrl Pts',(-1.87011317493118E-16,-1.52706329386826,
-8.234375));
#379194=CARTESIAN_POINT('Ctrl Pts',(0.881650403784437,-1.52706329386826,
-8.19270833333333));
#379195=CARTESIAN_POINT('Ctrl Pts',(1.32247560567666,-0.763531646934131,
-8.15104166666666));
#379196=CARTESIAN_POINT('Ctrl Pts',(1.76330080756888,1.96032512344098E-16,
-8.109375));
#379197=CARTESIAN_POINT('Ctrl Pts',(1.32247560567666,0.763531646934131,
-8.06770833333333));
#379198=CARTESIAN_POINT('Ctrl Pts',(0.881650403784439,1.52706329386826,
-8.02604166666666));
#379199=CARTESIAN_POINT('Ctrl Pts',(0.,1.52706329386826,-7.984375));
#379200=CARTESIAN_POINT('Ctrl Pts',(-0.881650403784438,1.52706329386826,
-7.94270833333333));
#379201=CARTESIAN_POINT('Ctrl Pts',(-1.32247560567666,0.763531646934132,
-7.90104166666667));
#379202=CARTESIAN_POINT('Ctrl Pts',(-1.76330080756888,6.27916650328731E-16,
-7.859375));
#379203=CARTESIAN_POINT('Ctrl Pts',(-1.32247560567666,-0.76353164693413,
-7.81770833333333));
#379204=CARTESIAN_POINT('Ctrl Pts',(-0.881650403784439,-1.52706329386826,
-7.77604166666666));
#379205=CARTESIAN_POINT('Ctrl Pts',(-1.87011317493118E-16,-1.52706329386826,
-7.734375));
#379206=CARTESIAN_POINT('Ctrl Pts',(0.881650403784437,-1.52706329386826,
-7.69270833333333));
#379207=CARTESIAN_POINT('Ctrl Pts',(1.32247560567666,-0.763531646934131,
-7.65104166666666));
#379208=CARTESIAN_POINT('Ctrl Pts',(1.76330080756888,1.96032512344098E-16,
-7.609375));
#379209=CARTESIAN_POINT('Ctrl Pts',(1.32247560567666,0.763531646934131,
-7.56770833333333));
#379210=CARTESIAN_POINT('Ctrl Pts',(0.881650403784439,1.52706329386826,
-7.52604166666667));
#379211=CARTESIAN_POINT('Ctrl Pts',(0.,1.52706329386826,-7.484375));
#379212=CARTESIAN_POINT('Ctrl Pts',(-0.881650403784438,1.52706329386826,
-7.44270833333333));
#379213=CARTESIAN_POINT('Ctrl Pts',(-1.32247560567666,0.763531646934132,
-7.40104166666666));
#379214=CARTESIAN_POINT('Ctrl Pts',(-1.76330080756888,6.27916650328731E-16,
-7.359375));
#379215=CARTESIAN_POINT('Ctrl Pts',(-1.32247560567666,-0.76353164693413,
-7.31770833333333));
#379216=CARTESIAN_POINT('Ctrl Pts',(-0.881650403784439,-1.52706329386826,
-7.27604166666667));
#379217=CARTESIAN_POINT('Ctrl Pts',(-1.87011317493118E-16,-1.52706329386826,
-7.234375));
#379218=CARTESIAN_POINT('Ctrl Pts',(0.881650403784437,-1.52706329386826,
-7.19270833333333));
#379219=CARTESIAN_POINT('Ctrl Pts',(1.32247560567666,-0.763531646934131,
-7.15104166666666));
#379220=CARTESIAN_POINT('Ctrl Pts',(1.76330080756888,1.96032512344098E-16,
-7.109375));
#379221=CARTESIAN_POINT('Ctrl Pts',(1.32247560567666,0.763531646934131,
-7.06770833333333));
#379222=CARTESIAN_POINT('Ctrl Pts',(0.881650403784439,1.52706329386826,
-7.02604166666667));
#379223=CARTESIAN_POINT('Ctrl Pts',(0.,1.52706329386826,-6.984375));
#379224=CARTESIAN_POINT('Ctrl Pts',(-0.881650403784438,1.52706329386826,
-6.94270833333333));
#379225=CARTESIAN_POINT('Ctrl Pts',(-1.32247560567666,0.763531646934132,
-6.90104166666667));
#379226=CARTESIAN_POINT('Ctrl Pts',(-1.76330080756888,6.27916650328731E-16,
-6.859375));
#379227=CARTESIAN_POINT('Ctrl Pts',(-1.32247560567666,-0.76353164693413,
-6.81770833333333));
#379228=CARTESIAN_POINT('Ctrl Pts',(-0.881650403784439,-1.52706329386826,
-6.77604166666667));
#379229=CARTESIAN_POINT('Ctrl Pts',(-1.87011317493118E-16,-1.52706329386826,
-6.734375));
#379230=CARTESIAN_POINT('Ctrl Pts',(0.881650403784437,-1.52706329386826,
-6.69270833333333));
#379231=CARTESIAN_POINT('Ctrl Pts',(1.32247560567666,-0.763531646934131,
-6.65104166666667));
#379232=CARTESIAN_POINT('Ctrl Pts',(1.76330080756888,1.96032512344098E-16,
-6.609375));
#379233=CARTESIAN_POINT('Ctrl Pts',(1.32247560567666,0.763531646934131,
-6.56770833333333));
#379234=CARTESIAN_POINT('Ctrl Pts',(0.881650403784439,1.52706329386826,
-6.52604166666666));
#379235=CARTESIAN_POINT('Ctrl Pts',(0.,1.52706329386826,-6.484375));
#379236=CARTESIAN_POINT('Ctrl Pts',(-0.881650403784438,1.52706329386826,
-6.44270833333333));
#379237=CARTESIAN_POINT('Ctrl Pts',(-1.32247560567666,0.763531646934132,
-6.40104166666666));
#379238=CARTESIAN_POINT('Ctrl Pts',(-1.76330080756888,6.27916650328731E-16,
-6.359375));
#379239=CARTESIAN_POINT('Ctrl Pts',(-1.32247560567666,-0.76353164693413,
-6.31770833333333));
#379240=CARTESIAN_POINT('Ctrl Pts',(-0.881650403784439,-1.52706329386826,
-6.27604166666667));
#379241=CARTESIAN_POINT('Ctrl Pts',(-1.87011317493118E-16,-1.52706329386826,
-6.234375));
#379242=CARTESIAN_POINT('Ctrl Pts',(0.881650403784437,-1.52706329386826,
-6.19270833333333));
#379243=CARTESIAN_POINT('Ctrl Pts',(1.32247560567666,-0.763531646934131,
-6.15104166666666));
#379244=CARTESIAN_POINT('Ctrl Pts',(1.76330080756888,1.96032512344098E-16,
-6.109375));
#379245=CARTESIAN_POINT('Ctrl Pts',(1.32247560567666,0.763531646934131,
-6.06770833333333));
#379246=CARTESIAN_POINT('Ctrl Pts',(0.881650403784439,1.52706329386826,
-6.02604166666666));
#379247=CARTESIAN_POINT('Ctrl Pts',(0.,1.52706329386826,-5.984375));
#379248=CARTESIAN_POINT('Ctrl Pts',(-0.881650403784438,1.52706329386826,
-5.94270833333333));
#379249=CARTESIAN_POINT('Ctrl Pts',(-1.32247560567666,0.763531646934132,
-5.90104166666666));
#379250=CARTESIAN_POINT('Ctrl Pts',(-1.76330080756888,6.27916650328731E-16,
-5.859375));
#379251=CARTESIAN_POINT('Ctrl Pts',(-1.32247560567666,-0.76353164693413,
-5.81770833333333));
#379252=CARTESIAN_POINT('Ctrl Pts',(-0.881650403784439,-1.52706329386826,
-5.77604166666666));
#379253=CARTESIAN_POINT('Ctrl Pts',(-1.87011317493118E-16,-1.52706329386826,
-5.734375));
#379254=CARTESIAN_POINT('Ctrl Pts',(0.881650403784437,-1.52706329386826,
-5.69270833333333));
#379255=CARTESIAN_POINT('Ctrl Pts',(1.32247560567666,-0.763531646934131,
-5.65104166666666));
#379256=CARTESIAN_POINT('Ctrl Pts',(1.76330080756888,1.96032512344098E-16,
-5.609375));
#379257=CARTESIAN_POINT('Ctrl Pts',(1.32247560567666,0.763531646934131,
-5.56770833333333));
#379258=CARTESIAN_POINT('Ctrl Pts',(0.881650403784439,1.52706329386826,
-5.52604166666666));
#379259=CARTESIAN_POINT('Ctrl Pts',(0.,1.52706329386826,-5.484375));
#379260=CARTESIAN_POINT('Ctrl Pts',(-0.881650403784438,1.52706329386826,
-5.44270833333333));
#379261=CARTESIAN_POINT('Ctrl Pts',(-1.32247560567666,0.763531646934132,
-5.40104166666667));
#379262=CARTESIAN_POINT('Ctrl Pts',(-1.76330080756888,6.27916650328731E-16,
-5.359375));
#379263=CARTESIAN_POINT('Ctrl Pts',(-1.32247560567666,-0.76353164693413,
-5.31770833333333));
#379264=CARTESIAN_POINT('Ctrl Pts',(-0.881650403784439,-1.52706329386826,
-5.27604166666666));
#379265=CARTESIAN_POINT('Ctrl Pts',(-1.87011317493118E-16,-1.52706329386826,
-5.234375));
#379266=CARTESIAN_POINT('Ctrl Pts',(0.881650403784437,-1.52706329386826,
-5.19270833333333));
#379267=CARTESIAN_POINT('Ctrl Pts',(1.32247560567666,-0.763531646934131,
-5.15104166666667));
#379268=CARTESIAN_POINT('Ctrl Pts',(1.76330080756888,1.96032512344098E-16,
-5.109375));
#379269=CARTESIAN_POINT('Ctrl Pts',(1.32247560567666,0.763531646934131,
-5.06770833333333));
#379270=CARTESIAN_POINT('Ctrl Pts',(0.881650403784439,1.52706329386826,
-5.02604166666667));
#379271=CARTESIAN_POINT('Ctrl Pts',(0.,1.52706329386826,-4.984375));
#379272=CARTESIAN_POINT('Ctrl Pts',(-0.881650403784438,1.52706329386826,
-4.94270833333333));
#379273=CARTESIAN_POINT('Ctrl Pts',(-1.32247560567666,0.763531646934132,
-4.90104166666666));
#379274=CARTESIAN_POINT('Ctrl Pts',(-1.76330080756888,6.27916650328731E-16,
-4.859375));
#379275=CARTESIAN_POINT('Ctrl Pts',(-1.32247560567666,-0.76353164693413,
-4.81770833333333));
#379276=CARTESIAN_POINT('Ctrl Pts',(-0.881650403784439,-1.52706329386826,
-4.77604166666667));
#379277=CARTESIAN_POINT('Ctrl Pts',(-1.87011317493118E-16,-1.52706329386826,
-4.734375));
#379278=CARTESIAN_POINT('Ctrl Pts',(0.881650403784437,-1.52706329386826,
-4.69270833333333));
#379279=CARTESIAN_POINT('Ctrl Pts',(1.32247560567666,-0.763531646934131,
-4.65104166666666));
#379280=CARTESIAN_POINT('Ctrl Pts',(1.76330080756888,1.96032512344098E-16,
-4.609375));
#379281=CARTESIAN_POINT('Ctrl Pts',(1.32247560567666,0.763531646934131,
-4.56770833333333));
#379282=CARTESIAN_POINT('Ctrl Pts',(0.881650403784439,1.52706329386826,
-4.52604166666666));
#379283=CARTESIAN_POINT('Ctrl Pts',(0.,1.52706329386826,-4.484375));
#379284=CARTESIAN_POINT('Ctrl Pts',(-0.881650403784438,1.52706329386826,
-4.44270833333333));
#379285=CARTESIAN_POINT('Ctrl Pts',(-1.32247560567666,0.763531646934132,
-4.40104166666666));
#379286=CARTESIAN_POINT('Ctrl Pts',(-1.76330080756888,6.27916650328731E-16,
-4.359375));
#379287=CARTESIAN_POINT('Ctrl Pts',(-1.32247560567666,-0.76353164693413,
-4.31770833333333));
#379288=CARTESIAN_POINT('Ctrl Pts',(-0.881650403784439,-1.52706329386826,
-4.27604166666666));
#379289=CARTESIAN_POINT('Ctrl Pts',(-1.87011317493118E-16,-1.52706329386826,
-4.234375));
#379290=CARTESIAN_POINT('Ctrl Pts',(0.881650403784437,-1.52706329386826,
-4.19270833333333));
#379291=CARTESIAN_POINT('Ctrl Pts',(1.32247560567666,-0.763531646934131,
-4.15104166666666));
#379292=CARTESIAN_POINT('Ctrl Pts',(1.76330080756888,1.96032512344098E-16,
-4.109375));
#379293=CARTESIAN_POINT('Ctrl Pts',(1.32247560567666,0.763531646934131,
-4.06770833333333));
#379294=CARTESIAN_POINT('Ctrl Pts',(0.881650403784439,1.52706329386826,
-4.02604166666666));
#379295=CARTESIAN_POINT('Ctrl Pts',(0.,1.52706329386826,-3.984375));
#379296=CARTESIAN_POINT('Ctrl Pts',(-0.881650403784438,1.52706329386826,
-3.94270833333333));
#379297=CARTESIAN_POINT('Ctrl Pts',(-1.32247560567666,0.763531646934132,
-3.90104166666666));
#379298=CARTESIAN_POINT('Ctrl Pts',(-1.76330080756888,6.27916650328731E-16,
-3.859375));
#379299=CARTESIAN_POINT('Ctrl Pts',(-1.32247560567666,-0.76353164693413,
-3.81770833333333));
#379300=CARTESIAN_POINT('Ctrl Pts',(-0.881650403784439,-1.52706329386826,
-3.77604166666667));
#379301=CARTESIAN_POINT('Ctrl Pts',(-1.87011317493118E-16,-1.52706329386826,
-3.734375));
#379302=CARTESIAN_POINT('Ctrl Pts',(0.881650403784437,-1.52706329386826,
-3.69270833333333));
#379303=CARTESIAN_POINT('Ctrl Pts',(1.32247560567666,-0.763531646934131,
-3.65104166666666));
#379304=CARTESIAN_POINT('Ctrl Pts',(1.76330080756888,1.96032512344098E-16,
-3.609375));
#379305=CARTESIAN_POINT('Ctrl Pts',(1.32247560567666,0.763531646934131,
-3.56770833333333));
#379306=CARTESIAN_POINT('Ctrl Pts',(0.881650403784439,1.52706329386826,
-3.52604166666666));
#379307=CARTESIAN_POINT('Ctrl Pts',(0.,1.52706329386826,-3.484375));
#379308=CARTESIAN_POINT('Ctrl Pts',(-0.881650403784438,1.52706329386826,
-3.44270833333333));
#379309=CARTESIAN_POINT('Ctrl Pts',(-1.32247560567666,0.763531646934132,
-3.40104166666666));
#379310=CARTESIAN_POINT('Ctrl Pts',(-1.76330080756888,6.27916650328731E-16,
-3.359375));
#379311=CARTESIAN_POINT('Ctrl Pts',(-1.32247560567666,-0.76353164693413,
-3.31770833333333));
#379312=CARTESIAN_POINT('Ctrl Pts',(-0.881650403784439,-1.52706329386826,
-3.27604166666666));
#379313=CARTESIAN_POINT('Ctrl Pts',(-1.87011317493118E-16,-1.52706329386826,
-3.234375));
#379314=CARTESIAN_POINT('Ctrl Pts',(0.881650403784437,-1.52706329386826,
-3.19270833333333));
#379315=CARTESIAN_POINT('Ctrl Pts',(1.32247560567666,-0.763531646934131,
-3.15104166666667));
#379316=CARTESIAN_POINT('Ctrl Pts',(1.76330080756888,1.96032512344098E-16,
-3.109375));
#379317=CARTESIAN_POINT('Ctrl Pts',(1.32247560567666,0.763531646934131,
-3.06770833333333));
#379318=CARTESIAN_POINT('Ctrl Pts',(0.881650403784439,1.52706329386826,
-3.02604166666667));
#379319=CARTESIAN_POINT('Ctrl Pts',(0.,1.52706329386826,-2.984375));
#379320=CARTESIAN_POINT('Ctrl Pts',(-0.881650403784438,1.52706329386826,
-2.94270833333333));
#379321=CARTESIAN_POINT('Ctrl Pts',(-1.32247560567666,0.763531646934132,
-2.90104166666667));
#379322=CARTESIAN_POINT('Ctrl Pts',(-1.76330080756888,6.27916650328731E-16,
-2.859375));
#379323=CARTESIAN_POINT('Ctrl Pts',(-1.32247560567666,-0.76353164693413,
-2.81770833333333));
#379324=CARTESIAN_POINT('Ctrl Pts',(-0.881650403784439,-1.52706329386826,
-2.77604166666666));
#379325=CARTESIAN_POINT('Ctrl Pts',(-1.87011317493118E-16,-1.52706329386826,
-2.734375));
#379326=CARTESIAN_POINT('Ctrl Pts',(0.881650403784437,-1.52706329386826,
-2.69270833333333));
#379327=CARTESIAN_POINT('Ctrl Pts',(1.32247560567666,-0.763531646934131,
-2.65104166666666));
#379328=CARTESIAN_POINT('Ctrl Pts',(1.76330080756888,1.96032512344098E-16,
-2.609375));
#379329=CARTESIAN_POINT('Ctrl Pts',(1.32247560567666,0.763531646934131,
-2.56770833333333));
#379330=CARTESIAN_POINT('Ctrl Pts',(0.881650403784439,1.52706329386826,
-2.52604166666666));
#379331=CARTESIAN_POINT('Ctrl Pts',(0.,1.52706329386826,-2.484375));
#379332=CARTESIAN_POINT('Ctrl Pts',(-0.881650403784438,1.52706329386826,
-2.44270833333333));
#379333=CARTESIAN_POINT('Ctrl Pts',(-1.32247560567666,0.763531646934132,
-2.40104166666666));
#379334=CARTESIAN_POINT('Ctrl Pts',(-1.76330080756888,6.27916650328731E-16,
-2.359375));
#379335=CARTESIAN_POINT('Ctrl Pts',(-1.32247560567666,-0.76353164693413,
-2.31770833333333));
#379336=CARTESIAN_POINT('Ctrl Pts',(-0.881650403784439,-1.52706329386826,
-2.27604166666666));
#379337=CARTESIAN_POINT('Ctrl Pts',(-1.87011317493118E-16,-1.52706329386826,
-2.234375));
#379338=CARTESIAN_POINT('Ctrl Pts',(0.881650403784437,-1.52706329386826,
-2.19270833333333));
#379339=CARTESIAN_POINT('Ctrl Pts',(1.32247560567666,-0.763531646934131,
-2.15104166666666));
#379340=CARTESIAN_POINT('Ctrl Pts',(1.76330080756888,1.96032512344098E-16,
-2.109375));
#379341=CARTESIAN_POINT('Ctrl Pts',(1.32247560567666,0.763531646934131,
-2.06770833333333));
#379342=CARTESIAN_POINT('Ctrl Pts',(0.881650403784439,1.52706329386826,
-2.02604166666666));
#379343=CARTESIAN_POINT('Ctrl Pts',(0.,1.52706329386826,-1.984375));
#379344=CARTESIAN_POINT('Ctrl Pts',(-0.881650403784438,1.52706329386826,
-1.94270833333333));
#379345=CARTESIAN_POINT('Ctrl Pts',(-1.32247560567666,0.763531646934132,
-1.90104166666666));
#379346=CARTESIAN_POINT('Ctrl Pts',(-1.76330080756888,6.27916650328731E-16,
-1.859375));
#379347=CARTESIAN_POINT('Ctrl Pts',(-1.32247560567666,-0.76353164693413,
-1.81770833333333));
#379348=CARTESIAN_POINT('Ctrl Pts',(-0.881650403784439,-1.52706329386826,
-1.77604166666666));
#379349=CARTESIAN_POINT('Ctrl Pts',(-1.87011317493118E-16,-1.52706329386826,
-1.734375));
#379350=CARTESIAN_POINT('Ctrl Pts',(0.881650403784437,-1.52706329386826,
-1.69270833333333));
#379351=CARTESIAN_POINT('Ctrl Pts',(1.32247560567666,-0.763531646934131,
-1.65104166666666));
#379352=CARTESIAN_POINT('Ctrl Pts',(1.76330080756888,1.96032512344098E-16,
-1.609375));
#379353=CARTESIAN_POINT('Ctrl Pts',(1.32247560567666,0.763531646934131,
-1.56770833333333));
#379354=CARTESIAN_POINT('Ctrl Pts',(0.881650403784439,1.52706329386826,
-1.52604166666666));
#379355=CARTESIAN_POINT('Ctrl Pts',(0.,1.52706329386826,-1.484375));
#379356=CARTESIAN_POINT('Ctrl Pts',(-0.881650403784438,1.52706329386826,
-1.44270833333333));
#379357=CARTESIAN_POINT('Ctrl Pts',(-1.32247560567666,0.763531646934132,
-1.40104166666666));
#379358=CARTESIAN_POINT('Ctrl Pts',(-1.76330080756888,6.27916650328731E-16,
-1.359375));
#379359=CARTESIAN_POINT('Ctrl Pts',(-1.32247560567666,-0.76353164693413,
-1.31770833333333));
#379360=CARTESIAN_POINT('Ctrl Pts',(-0.881650403784439,-1.52706329386826,
-1.27604166666666));
#379361=CARTESIAN_POINT('Ctrl Pts',(-1.87011317493118E-16,-1.52706329386826,
-1.234375));
#379362=CARTESIAN_POINT('Ctrl Pts',(0.881650403784437,-1.52706329386826,
-1.19270833333333));
#379363=CARTESIAN_POINT('Ctrl Pts',(1.32247560567666,-0.763531646934131,
-1.15104166666666));
#379364=CARTESIAN_POINT('Ctrl Pts',(1.76330080756888,1.96032512344098E-16,
-1.109375));
#379365=CARTESIAN_POINT('Ctrl Pts',(1.32247560567666,0.763531646934131,
-1.06770833333333));
#379366=CARTESIAN_POINT('Ctrl Pts',(0.881650403784439,1.52706329386826,
-1.02604166666666));
#379367=CARTESIAN_POINT('Ctrl Pts',(0.,1.52706329386826,-0.984374999999997));
#379368=CARTESIAN_POINT('Ctrl Pts',(-0.881650403784438,1.52706329386826,
-0.942708333333332));
#379369=CARTESIAN_POINT('Ctrl Pts',(-1.32247560567666,0.763531646934132,
-0.901041666666665));
#379370=CARTESIAN_POINT('Ctrl Pts',(-1.76330080756888,6.27916650328731E-16,
-0.859374999999997));
#379371=CARTESIAN_POINT('Ctrl Pts',(-1.32247560567666,-0.76353164693413,
-0.817708333333332));
#379372=CARTESIAN_POINT('Ctrl Pts',(-0.881650403784439,-1.52706329386826,
-0.776041666666665));
#379373=CARTESIAN_POINT('Ctrl Pts',(-1.87011317493118E-16,-1.52706329386826,
-0.734374999999997));
#379374=CARTESIAN_POINT('Ctrl Pts',(0.881650403784437,-1.52706329386826,
-0.692708333333332));
#379375=CARTESIAN_POINT('Ctrl Pts',(1.32247560567666,-0.763531646934131,
-0.651041666666664));
#379376=CARTESIAN_POINT('Ctrl Pts',(1.76330080756888,1.96032512344098E-16,
-0.609374999999997));
#379377=CARTESIAN_POINT('Ctrl Pts',(1.32247560567666,0.763531646934131,
-0.567708333333331));
#379378=CARTESIAN_POINT('Ctrl Pts',(0.881650403784439,1.52706329386826,
-0.526041666666664));
#379379=CARTESIAN_POINT('Ctrl Pts',(0.,1.52706329386826,-0.484374999999999));
#379380=CARTESIAN_POINT('Ctrl Pts',(-0.881650403784438,1.52706329386826,
-0.442708333333331));
#379381=CARTESIAN_POINT('Ctrl Pts',(-1.32247560567666,0.763531646934132,
-0.401041666666664));
#379382=CARTESIAN_POINT('Ctrl Pts',(-1.76330080756888,6.27916650328731E-16,
-0.359374999999999));
#379383=CARTESIAN_POINT('Ctrl Pts',(-1.32247560567666,-0.76353164693413,
-0.317708333333331));
#379384=CARTESIAN_POINT('Ctrl Pts',(-0.881650403784439,-1.52706329386826,
-0.276041666666664));
#379385=CARTESIAN_POINT('Ctrl Pts',(-1.87011317493118E-16,-1.52706329386826,
-0.234374999999998));
#379386=CARTESIAN_POINT('Ctrl Pts',(0.881650403784437,-1.52706329386826,
-0.192708333333331));
#379387=CARTESIAN_POINT('Ctrl Pts',(1.32247560567666,-0.763531646934131,
-0.151041666666664));
#379388=CARTESIAN_POINT('Ctrl Pts',(1.76330080756888,1.96032512344098E-16,
-0.109374999999998));
#379389=CARTESIAN_POINT('Ctrl Pts',(1.32247560567666,0.763531646934131,
-0.0677083333333311));
#379390=CARTESIAN_POINT('Ctrl Pts',(0.881650403784439,1.52706329386826,
-0.0260416666666638));
#379391=CARTESIAN_POINT('Ctrl Pts',(0.,1.52706329386826,0.0156250000000017));
#379392=CARTESIAN_POINT('Ctrl Pts',(-0.881650403784438,1.52706329386826,
0.057291666666669));
#379393=CARTESIAN_POINT('Ctrl Pts',(-1.32247560567666,0.763531646934132,
0.0989583333333363));
#379394=CARTESIAN_POINT('Ctrl Pts',(-1.76330080756888,6.27916650328731E-16,
0.140625000000002));
#379395=CARTESIAN_POINT('Ctrl Pts',(-1.32247560567666,-0.76353164693413,
0.182291666666669));
#379396=CARTESIAN_POINT('Ctrl Pts',(-0.881650403784439,-1.52706329386826,
0.223958333333335));
#379397=CARTESIAN_POINT('Ctrl Pts',(-1.87011317493118E-16,-1.52706329386826,
0.265625000000002));
#379398=CARTESIAN_POINT('Ctrl Pts',(0.881650403784437,-1.52706329386826,
0.307291666666669));
#379399=CARTESIAN_POINT('Ctrl Pts',(1.32247560567666,-0.763531646934131,
0.348958333333335));
#379400=CARTESIAN_POINT('Ctrl Pts',(1.76330080756888,1.96032512344098E-16,
0.390625000000002));
#379401=CARTESIAN_POINT('Ctrl Pts',(1.32247560567666,0.763531646934131,
0.432291666666669));
#379402=CARTESIAN_POINT('Ctrl Pts',(0.881650403784439,1.52706329386826,
0.473958333333335));
#379403=CARTESIAN_POINT('Ctrl Pts',(0.,1.52706329386826,0.515625000000002));
#379404=CARTESIAN_POINT('Ctrl Pts',(-0.881650403784438,1.52706329386826,
0.55729166666667));
#379405=CARTESIAN_POINT('Ctrl Pts',(-1.32247560567666,0.763531646934132,
0.598958333333335));
#379406=CARTESIAN_POINT('Ctrl Pts',(-1.76330080756888,6.27916650328731E-16,
0.640625000000002));
#379407=CARTESIAN_POINT('Ctrl Pts',(-1.32247560567666,-0.76353164693413,
0.68229166666667));
#379408=CARTESIAN_POINT('Ctrl Pts',(-0.881650403784439,-1.52706329386826,
0.723958333333335));
#379409=CARTESIAN_POINT('Ctrl Pts',(-1.87011317493118E-16,-1.52706329386826,
0.765625000000003));
#379410=CARTESIAN_POINT('Ctrl Pts',(0.881650403784437,-1.52706329386826,
0.807291666666668));
#379411=CARTESIAN_POINT('Ctrl Pts',(1.32247560567666,-0.763531646934131,
0.848958333333335));
#379412=CARTESIAN_POINT('Ctrl Pts',(1.76330080756888,1.96032512344098E-16,
0.890625000000003));
#379413=CARTESIAN_POINT('Ctrl Pts',(1.32247560567666,0.763531646934131,
0.932291666666668));
#379414=CARTESIAN_POINT('Ctrl Pts',(0.881650403784439,1.52706329386826,
0.973958333333336));
#379415=CARTESIAN_POINT('Ctrl Pts',(0.,1.52706329386826,1.015625));
#379416=CARTESIAN_POINT('Ctrl Pts',(-0.881650403784438,1.52706329386826,
1.05729166666667));
#379417=CARTESIAN_POINT('Ctrl Pts',(-1.32247560567666,0.763531646934132,
1.09895833333334));
#379418=CARTESIAN_POINT('Ctrl Pts',(-1.76330080756888,6.27916650328732E-16,
1.140625));
#379419=CARTESIAN_POINT('Ctrl Pts',(-1.32247560567666,-0.76353164693413,
1.18229166666667));
#379420=CARTESIAN_POINT('Ctrl Pts',(-0.881650403784439,-1.52706329386826,
1.22395833333334));
#379421=CARTESIAN_POINT('Ctrl Pts',(-1.87011317493118E-16,-1.52706329386826,
1.265625));
#379422=CARTESIAN_POINT('Ctrl Pts',(0.881650403784437,-1.52706329386826,
1.30729166666667));
#379423=CARTESIAN_POINT('Ctrl Pts',(1.32247560567666,-0.763531646934131,
1.34895833333334));
#379424=CARTESIAN_POINT('Ctrl Pts',(1.76330080756888,1.96032512344098E-16,
1.390625));
#379425=CARTESIAN_POINT('Ctrl Pts',(1.32247560567666,0.763531646934131,
1.43229166666667));
#379426=CARTESIAN_POINT('Ctrl Pts',(0.881650403784439,1.52706329386826,
1.47395833333334));
#379427=CARTESIAN_POINT('Ctrl Pts',(0.,1.52706329386826,1.515625));
#379428=CARTESIAN_POINT('Ctrl Pts',(-0.881650403784438,1.52706329386826,
1.55729166666667));
#379429=CARTESIAN_POINT('Ctrl Pts',(-1.32247560567666,0.763531646934132,
1.59895833333334));
#379430=CARTESIAN_POINT('Ctrl Pts',(-1.76330080756888,6.27916650328732E-16,
1.640625));
#379431=CARTESIAN_POINT('Ctrl Pts',(-1.32247560567666,-0.76353164693413,
1.68229166666667));
#379432=CARTESIAN_POINT('Ctrl Pts',(-0.881650403784439,-1.52706329386826,
1.72395833333334));
#379433=CARTESIAN_POINT('Ctrl Pts',(-1.87011317493118E-16,-1.52706329386826,
1.765625));
#379434=CARTESIAN_POINT('Ctrl Pts',(0.881650403784437,-1.52706329386826,
1.80729166666667));
#379435=CARTESIAN_POINT('Ctrl Pts',(1.32247560567666,-0.763531646934131,
1.84895833333334));
#379436=CARTESIAN_POINT('Ctrl Pts',(1.76330080756888,1.96032512344098E-16,
1.890625));
#379437=CARTESIAN_POINT('Ctrl Pts',(1.32247560567666,0.763531646934131,
1.93229166666667));
#379438=CARTESIAN_POINT('Ctrl Pts',(0.881650403784439,1.52706329386826,
1.97395833333334));
#379439=CARTESIAN_POINT('Ctrl Pts',(0.,1.52706329386826,2.015625));
#379440=CARTESIAN_POINT('Ctrl Pts',(-0.881650403784438,1.52706329386826,
2.05729166666667));
#379441=CARTESIAN_POINT('Ctrl Pts',(-1.32247560567666,0.763531646934132,
2.09895833333333));
#379442=CARTESIAN_POINT('Ctrl Pts',(-1.76330080756888,6.27916650328732E-16,
2.140625));
#379443=CARTESIAN_POINT('Ctrl Pts',(-1.32247560567666,-0.76353164693413,
2.18229166666667));
#379444=CARTESIAN_POINT('Ctrl Pts',(-0.881650403784439,-1.52706329386826,
2.22395833333333));
#379445=CARTESIAN_POINT('Ctrl Pts',(-1.87011317493118E-16,-1.52706329386826,
2.265625));
#379446=CARTESIAN_POINT('Ctrl Pts',(0.881650403784437,-1.52706329386826,
2.30729166666667));
#379447=CARTESIAN_POINT('Ctrl Pts',(1.32247560567666,-0.763531646934131,
2.34895833333333));
#379448=CARTESIAN_POINT('Ctrl Pts',(1.76330080756888,1.96032512344098E-16,
2.390625));
#379449=CARTESIAN_POINT('Ctrl Pts',(1.32247560567666,0.763531646934131,
2.43229166666667));
#379450=CARTESIAN_POINT('Ctrl Pts',(0.881650403784439,1.52706329386826,
2.47395833333333));
#379451=CARTESIAN_POINT('Ctrl Pts',(0.,1.52706329386826,2.515625));
#379452=CARTESIAN_POINT('Ctrl Pts',(-0.881650403784438,1.52706329386826,
2.55729166666667));
#379453=CARTESIAN_POINT('Ctrl Pts',(-1.32247560567666,0.763531646934132,
2.59895833333334));
#379454=CARTESIAN_POINT('Ctrl Pts',(-1.76330080756888,6.27916650328732E-16,
2.640625));
#379455=CARTESIAN_POINT('Ctrl Pts',(-1.32247560567666,-0.76353164693413,
2.68229166666667));
#379456=CARTESIAN_POINT('Ctrl Pts',(-0.881650403784439,-1.52706329386826,
2.72395833333334));
#379457=CARTESIAN_POINT('Ctrl Pts',(-1.87011317493118E-16,-1.52706329386826,
2.765625));
#379458=CARTESIAN_POINT('Ctrl Pts',(0.881650403784437,-1.52706329386826,
2.80729166666667));
#379459=CARTESIAN_POINT('Ctrl Pts',(1.32247560567666,-0.763531646934131,
2.84895833333334));
#379460=CARTESIAN_POINT('Ctrl Pts',(1.76330080756888,1.96032512344098E-16,
2.890625));
#379461=CARTESIAN_POINT('Ctrl Pts',(1.32247560567666,0.763531646934131,
2.93229166666667));
#379462=CARTESIAN_POINT('Ctrl Pts',(0.881650403784439,1.52706329386826,
2.97395833333334));
#379463=CARTESIAN_POINT('Ctrl Pts',(0.,1.52706329386826,3.015625));
#379464=CARTESIAN_POINT('Ctrl Pts',(-0.881650403784438,1.52706329386826,
3.05729166666667));
#379465=CARTESIAN_POINT('Ctrl Pts',(-1.32247560567666,0.763531646934132,
3.09895833333334));
#379466=CARTESIAN_POINT('Ctrl Pts',(-1.76330080756888,6.27916650328732E-16,
3.140625));
#379467=CARTESIAN_POINT('Ctrl Pts',(-1.32247560567666,-0.76353164693413,
3.18229166666667));
#379468=CARTESIAN_POINT('Ctrl Pts',(-0.881650403784439,-1.52706329386826,
3.22395833333334));
#379469=CARTESIAN_POINT('Ctrl Pts',(-1.87011317493118E-16,-1.52706329386826,
3.265625));
#379470=CARTESIAN_POINT('Ctrl Pts',(0.881650403784437,-1.52706329386826,
3.30729166666667));
#379471=CARTESIAN_POINT('Ctrl Pts',(1.32247560567666,-0.763531646934131,
3.34895833333334));
#379472=CARTESIAN_POINT('Ctrl Pts',(1.76330080756888,1.96032512344098E-16,
3.390625));
#379473=CARTESIAN_POINT('Ctrl Pts',(1.32247560567666,0.763531646934131,
3.43229166666667));
#379474=CARTESIAN_POINT('Ctrl Pts',(0.881650403784439,1.52706329386826,
3.47395833333334));
#379475=CARTESIAN_POINT('Ctrl Pts',(0.,1.52706329386826,3.515625));
#379476=CARTESIAN_POINT('Ctrl Pts',(-0.881650403784438,1.52706329386826,
3.55729166666667));
#379477=CARTESIAN_POINT('Ctrl Pts',(-1.32247560567666,0.763531646934132,
3.59895833333334));
#379478=CARTESIAN_POINT('Ctrl Pts',(-1.76330080756888,6.27916650328732E-16,
3.640625));
#379479=CARTESIAN_POINT('Ctrl Pts',(-1.32247560567666,-0.76353164693413,
3.68229166666667));
#379480=CARTESIAN_POINT('Ctrl Pts',(-0.881650403784439,-1.52706329386826,
3.72395833333334));
#379481=CARTESIAN_POINT('Ctrl Pts',(-1.87011317493118E-16,-1.52706329386826,
3.765625));
#379482=CARTESIAN_POINT('Ctrl Pts',(0.881650403784437,-1.52706329386826,
3.80729166666667));
#379483=CARTESIAN_POINT('Ctrl Pts',(1.32247560567666,-0.763531646934131,
3.84895833333334));
#379484=CARTESIAN_POINT('Ctrl Pts',(1.76330080756888,1.96032512344098E-16,
3.890625));
#379485=CARTESIAN_POINT('Ctrl Pts',(1.32247560567666,0.763531646934131,
3.93229166666667));
#379486=CARTESIAN_POINT('Ctrl Pts',(0.881650403784439,1.52706329386826,
3.97395833333333));
#379487=CARTESIAN_POINT('Ctrl Pts',(0.,1.52706329386826,4.015625));
#379488=CARTESIAN_POINT('Ctrl Pts',(-0.881650403784438,1.52706329386826,
4.05729166666667));
#379489=CARTESIAN_POINT('Ctrl Pts',(-1.32247560567666,0.763531646934132,
4.09895833333333));
#379490=CARTESIAN_POINT('Ctrl Pts',(-1.76330080756888,6.27916650328732E-16,
4.140625));
#379491=CARTESIAN_POINT('Ctrl Pts',(-1.32247560567666,-0.76353164693413,
4.18229166666667));
#379492=CARTESIAN_POINT('Ctrl Pts',(-0.881650403784439,-1.52706329386826,
4.22395833333334));
#379493=CARTESIAN_POINT('Ctrl Pts',(-1.87011317493118E-16,-1.52706329386826,
4.265625));
#379494=CARTESIAN_POINT('Ctrl Pts',(0.881650403784437,-1.52706329386826,
4.30729166666667));
#379495=CARTESIAN_POINT('Ctrl Pts',(1.32247560567666,-0.763531646934131,
4.34895833333333));
#379496=CARTESIAN_POINT('Ctrl Pts',(1.76330080756888,1.96032512344098E-16,
4.390625));
#379497=CARTESIAN_POINT('Ctrl Pts',(1.32247560567666,0.763531646934131,
4.43229166666667));
#379498=CARTESIAN_POINT('Ctrl Pts',(0.881650403784439,1.52706329386826,
4.47395833333333));
#379499=CARTESIAN_POINT('Ctrl Pts',(0.,1.52706329386826,4.515625));
#379500=CARTESIAN_POINT('Ctrl Pts',(-0.881650403784438,1.52706329386826,
4.55729166666667));
#379501=CARTESIAN_POINT('Ctrl Pts',(-1.32247560567666,0.763531646934132,
4.59895833333333));
#379502=CARTESIAN_POINT('Ctrl Pts',(-1.76330080756888,6.27916650328732E-16,
4.640625));
#379503=CARTESIAN_POINT('Ctrl Pts',(-1.32247560567666,-0.76353164693413,
4.68229166666667));
#379504=CARTESIAN_POINT('Ctrl Pts',(-0.881650403784439,-1.52706329386826,
4.72395833333334));
#379505=CARTESIAN_POINT('Ctrl Pts',(-1.87011317493118E-16,-1.52706329386826,
4.765625));
#379506=CARTESIAN_POINT('Ctrl Pts',(0.881650403784437,-1.52706329386826,
4.80729166666667));
#379507=CARTESIAN_POINT('Ctrl Pts',(1.32247560567666,-0.763531646934131,
4.84895833333334));
#379508=CARTESIAN_POINT('Ctrl Pts',(1.76330080756888,1.96032512344098E-16,
4.890625));
#379509=CARTESIAN_POINT('Ctrl Pts',(1.32247560567666,0.763531646934131,
4.93229166666667));
#379510=CARTESIAN_POINT('Ctrl Pts',(0.881650403784439,1.52706329386826,
4.97395833333334));
#379511=CARTESIAN_POINT('Ctrl Pts',(0.,1.52706329386826,5.015625));
#379512=CARTESIAN_POINT('Ctrl Pts',(-0.881650403784438,1.52706329386826,
5.05729166666667));
#379513=CARTESIAN_POINT('Ctrl Pts',(-1.32247560567666,0.763531646934132,
5.09895833333334));
#379514=CARTESIAN_POINT('Ctrl Pts',(-1.76330080756888,6.27916650328732E-16,
5.140625));
#379515=CARTESIAN_POINT('Ctrl Pts',(-1.32247560567666,-0.76353164693413,
5.18229166666667));
#379516=CARTESIAN_POINT('Ctrl Pts',(-0.881650403784439,-1.52706329386826,
5.22395833333334));
#379517=CARTESIAN_POINT('Ctrl Pts',(-1.87011317493118E-16,-1.52706329386826,
5.265625));
#379518=CARTESIAN_POINT('Ctrl Pts',(0.881650403784437,-1.52706329386826,
5.30729166666667));
#379519=CARTESIAN_POINT('Ctrl Pts',(1.32247560567666,-0.763531646934131,
5.34895833333334));
#379520=CARTESIAN_POINT('Ctrl Pts',(1.76330080756888,1.96032512344098E-16,
5.390625));
#379521=CARTESIAN_POINT('Ctrl Pts',(1.32247560567666,0.763531646934131,
5.43229166666667));
#379522=CARTESIAN_POINT('Ctrl Pts',(0.881650403784439,1.52706329386826,
5.47395833333334));
#379523=CARTESIAN_POINT('Ctrl Pts',(0.,1.52706329386826,5.515625));
#379524=CARTESIAN_POINT('Ctrl Pts',(-0.881650403784438,1.52706329386826,
5.55729166666667));
#379525=CARTESIAN_POINT('Ctrl Pts',(-1.32247560567666,0.763531646934132,
5.59895833333334));
#379526=CARTESIAN_POINT('Ctrl Pts',(-1.76330080756888,6.27916650328732E-16,
5.640625));
#379527=CARTESIAN_POINT('Ctrl Pts',(-1.32247560567666,-0.76353164693413,
5.68229166666667));
#379528=CARTESIAN_POINT('Ctrl Pts',(-0.881650403784439,-1.52706329386826,
5.72395833333334));
#379529=CARTESIAN_POINT('Ctrl Pts',(-1.87011317493118E-16,-1.52706329386826,
5.765625));
#379530=CARTESIAN_POINT('Ctrl Pts',(0.881650403784437,-1.52706329386826,
5.80729166666667));
#379531=CARTESIAN_POINT('Ctrl Pts',(1.32247560567666,-0.763531646934131,
5.84895833333333));
#379532=CARTESIAN_POINT('Ctrl Pts',(1.76330080756888,1.96032512344098E-16,
5.890625));
#379533=CARTESIAN_POINT('Ctrl Pts',(1.32247560567666,0.763531646934131,
5.93229166666667));
#379534=CARTESIAN_POINT('Ctrl Pts',(0.881650403784439,1.52706329386826,
5.97395833333333));
#379535=CARTESIAN_POINT('Ctrl Pts',(0.,1.52706329386826,6.015625));
#379536=CARTESIAN_POINT('Ctrl Pts',(-0.881650403784438,1.52706329386826,
6.05729166666667));
#379537=CARTESIAN_POINT('Ctrl Pts',(-1.32247560567666,0.763531646934132,
6.09895833333334));
#379538=CARTESIAN_POINT('Ctrl Pts',(-1.76330080756888,6.27916650328732E-16,
6.140625));
#379539=CARTESIAN_POINT('Ctrl Pts',(-1.32247560567666,-0.76353164693413,
6.18229166666667));
#379540=CARTESIAN_POINT('Ctrl Pts',(-0.881650403784439,-1.52706329386826,
6.22395833333333));
#379541=CARTESIAN_POINT('Ctrl Pts',(-1.87011317493118E-16,-1.52706329386826,
6.265625));
#379542=CARTESIAN_POINT('Ctrl Pts',(0.881650403784437,-1.52706329386826,
6.30729166666667));
#379543=CARTESIAN_POINT('Ctrl Pts',(1.32247560567666,-0.763531646934131,
6.34895833333334));
#379544=CARTESIAN_POINT('Ctrl Pts',(1.76330080756888,1.96032512344098E-16,
6.390625));
#379545=CARTESIAN_POINT('Ctrl Pts',(1.32247560567666,0.763531646934131,
6.43229166666667));
#379546=CARTESIAN_POINT('Ctrl Pts',(0.881650403784439,1.52706329386826,
6.47395833333333));
#379547=CARTESIAN_POINT('Ctrl Pts',(0.,1.52706329386826,6.515625));
#379548=CARTESIAN_POINT('Ctrl Pts',(0.,1.17523182375213,-9.18750499398093));
#379549=CARTESIAN_POINT('Ctrl Pts',(-0.678520409803505,1.17523182375213,
-9.14583832731426));
#379550=CARTESIAN_POINT('Ctrl Pts',(-1.01778061470526,0.587615911876064,
-9.1041716606476));
#379551=CARTESIAN_POINT('Ctrl Pts',(-1.35704081960701,6.03040400634774E-16,
-9.06250499398093));
#379552=CARTESIAN_POINT('Ctrl Pts',(-1.01778061470526,-0.587615911876062,
-9.02083832731427));
#379553=CARTESIAN_POINT('Ctrl Pts',(-0.678520409803505,-1.17523182375213,
-8.9791716606476));
#379554=CARTESIAN_POINT('Ctrl Pts',(-1.43924389121415E-16,-1.17523182375213,
-8.93750499398093));
#379555=CARTESIAN_POINT('Ctrl Pts',(0.678520409803504,-1.17523182375213,
-8.89583832731427));
#379556=CARTESIAN_POINT('Ctrl Pts',(1.01778061470526,-0.587615911876063,
-8.8541716606476));
#379557=CARTESIAN_POINT('Ctrl Pts',(1.35704081960701,2.70661261425969E-16,
-8.81250499398093));
#379558=CARTESIAN_POINT('Ctrl Pts',(1.01778061470526,0.587615911876063,
-8.77083832731427));
#379559=CARTESIAN_POINT('Ctrl Pts',(0.678520409803506,1.17523182375213,
-8.7291716606476));
#379560=CARTESIAN_POINT('Ctrl Pts',(0.,1.17523182375213,-8.68750499398093));
#379561=CARTESIAN_POINT('Ctrl Pts',(-0.678520409803505,1.17523182375213,
-8.64583832731427));
#379562=CARTESIAN_POINT('Ctrl Pts',(-1.01778061470526,0.587615911876064,
-8.6041716606476));
#379563=CARTESIAN_POINT('Ctrl Pts',(-1.35704081960701,6.03040400634774E-16,
-8.56250499398093));
#379564=CARTESIAN_POINT('Ctrl Pts',(-1.01778061470526,-0.587615911876062,
-8.52083832731427));
#379565=CARTESIAN_POINT('Ctrl Pts',(-0.678520409803505,-1.17523182375213,
-8.4791716606476));
#379566=CARTESIAN_POINT('Ctrl Pts',(-1.43924389121415E-16,-1.17523182375213,
-8.43750499398093));
#379567=CARTESIAN_POINT('Ctrl Pts',(0.678520409803504,-1.17523182375213,
-8.39583832731427));
#379568=CARTESIAN_POINT('Ctrl Pts',(1.01778061470526,-0.587615911876063,
-8.3541716606476));
#379569=CARTESIAN_POINT('Ctrl Pts',(1.35704081960701,2.70661261425969E-16,
-8.31250499398093));
#379570=CARTESIAN_POINT('Ctrl Pts',(1.01778061470526,0.587615911876063,
-8.27083832731427));
#379571=CARTESIAN_POINT('Ctrl Pts',(0.678520409803506,1.17523182375213,
-8.2291716606476));
#379572=CARTESIAN_POINT('Ctrl Pts',(0.,1.17523182375213,-8.18750499398093));
#379573=CARTESIAN_POINT('Ctrl Pts',(-0.678520409803505,1.17523182375213,
-8.14583832731427));
#379574=CARTESIAN_POINT('Ctrl Pts',(-1.01778061470526,0.587615911876064,
-8.1041716606476));
#379575=CARTESIAN_POINT('Ctrl Pts',(-1.35704081960701,6.03040400634774E-16,
-8.06250499398093));
#379576=CARTESIAN_POINT('Ctrl Pts',(-1.01778061470526,-0.587615911876062,
-8.02083832731427));
#379577=CARTESIAN_POINT('Ctrl Pts',(-0.678520409803505,-1.17523182375213,
-7.9791716606476));
#379578=CARTESIAN_POINT('Ctrl Pts',(-1.43924389121415E-16,-1.17523182375213,
-7.93750499398093));
#379579=CARTESIAN_POINT('Ctrl Pts',(0.678520409803504,-1.17523182375213,
-7.89583832731427));
#379580=CARTESIAN_POINT('Ctrl Pts',(1.01778061470526,-0.587615911876063,
-7.8541716606476));
#379581=CARTESIAN_POINT('Ctrl Pts',(1.35704081960701,2.70661261425969E-16,
-7.81250499398093));
#379582=CARTESIAN_POINT('Ctrl Pts',(1.01778061470526,0.587615911876063,
-7.77083832731427));
#379583=CARTESIAN_POINT('Ctrl Pts',(0.678520409803506,1.17523182375213,
-7.7291716606476));
#379584=CARTESIAN_POINT('Ctrl Pts',(0.,1.17523182375213,-7.68750499398093));
#379585=CARTESIAN_POINT('Ctrl Pts',(-0.678520409803505,1.17523182375213,
-7.64583832731426));
#379586=CARTESIAN_POINT('Ctrl Pts',(-1.01778061470526,0.587615911876064,
-7.6041716606476));
#379587=CARTESIAN_POINT('Ctrl Pts',(-1.35704081960701,6.03040400634774E-16,
-7.56250499398093));
#379588=CARTESIAN_POINT('Ctrl Pts',(-1.01778061470526,-0.587615911876062,
-7.52083832731427));
#379589=CARTESIAN_POINT('Ctrl Pts',(-0.678520409803505,-1.17523182375213,
-7.4791716606476));
#379590=CARTESIAN_POINT('Ctrl Pts',(-1.43924389121415E-16,-1.17523182375213,
-7.43750499398093));
#379591=CARTESIAN_POINT('Ctrl Pts',(0.678520409803504,-1.17523182375213,
-7.39583832731426));
#379592=CARTESIAN_POINT('Ctrl Pts',(1.01778061470526,-0.587615911876063,
-7.3541716606476));
#379593=CARTESIAN_POINT('Ctrl Pts',(1.35704081960701,2.70661261425969E-16,
-7.31250499398093));
#379594=CARTESIAN_POINT('Ctrl Pts',(1.01778061470526,0.587615911876063,
-7.27083832731427));
#379595=CARTESIAN_POINT('Ctrl Pts',(0.678520409803506,1.17523182375213,
-7.2291716606476));
#379596=CARTESIAN_POINT('Ctrl Pts',(0.,1.17523182375213,-7.18750499398093));
#379597=CARTESIAN_POINT('Ctrl Pts',(-0.678520409803505,1.17523182375213,
-7.14583832731427));
#379598=CARTESIAN_POINT('Ctrl Pts',(-1.01778061470526,0.587615911876064,
-7.1041716606476));
#379599=CARTESIAN_POINT('Ctrl Pts',(-1.35704081960701,6.03040400634774E-16,
-7.06250499398093));
#379600=CARTESIAN_POINT('Ctrl Pts',(-1.01778061470526,-0.587615911876062,
-7.02083832731427));
#379601=CARTESIAN_POINT('Ctrl Pts',(-0.678520409803505,-1.17523182375213,
-6.9791716606476));
#379602=CARTESIAN_POINT('Ctrl Pts',(-1.43924389121415E-16,-1.17523182375213,
-6.93750499398093));
#379603=CARTESIAN_POINT('Ctrl Pts',(0.678520409803504,-1.17523182375213,
-6.89583832731427));
#379604=CARTESIAN_POINT('Ctrl Pts',(1.01778061470526,-0.587615911876063,
-6.8541716606476));
#379605=CARTESIAN_POINT('Ctrl Pts',(1.35704081960701,2.70661261425969E-16,
-6.81250499398093));
#379606=CARTESIAN_POINT('Ctrl Pts',(1.01778061470526,0.587615911876063,
-6.77083832731427));
#379607=CARTESIAN_POINT('Ctrl Pts',(0.678520409803506,1.17523182375213,
-6.7291716606476));
#379608=CARTESIAN_POINT('Ctrl Pts',(0.,1.17523182375213,-6.68750499398093));
#379609=CARTESIAN_POINT('Ctrl Pts',(-0.678520409803505,1.17523182375213,
-6.64583832731427));
#379610=CARTESIAN_POINT('Ctrl Pts',(-1.01778061470526,0.587615911876064,
-6.6041716606476));
#379611=CARTESIAN_POINT('Ctrl Pts',(-1.35704081960701,6.03040400634774E-16,
-6.56250499398093));
#379612=CARTESIAN_POINT('Ctrl Pts',(-1.01778061470526,-0.587615911876062,
-6.52083832731427));
#379613=CARTESIAN_POINT('Ctrl Pts',(-0.678520409803505,-1.17523182375213,
-6.4791716606476));
#379614=CARTESIAN_POINT('Ctrl Pts',(-1.43924389121415E-16,-1.17523182375213,
-6.43750499398093));
#379615=CARTESIAN_POINT('Ctrl Pts',(0.678520409803504,-1.17523182375213,
-6.39583832731427));
#379616=CARTESIAN_POINT('Ctrl Pts',(1.01778061470526,-0.587615911876063,
-6.3541716606476));
#379617=CARTESIAN_POINT('Ctrl Pts',(1.35704081960701,2.70661261425969E-16,
-6.31250499398093));
#379618=CARTESIAN_POINT('Ctrl Pts',(1.01778061470526,0.587615911876063,
-6.27083832731427));
#379619=CARTESIAN_POINT('Ctrl Pts',(0.678520409803506,1.17523182375213,
-6.2291716606476));
#379620=CARTESIAN_POINT('Ctrl Pts',(0.,1.17523182375213,-6.18750499398093));
#379621=CARTESIAN_POINT('Ctrl Pts',(-0.678520409803505,1.17523182375213,
-6.14583832731427));
#379622=CARTESIAN_POINT('Ctrl Pts',(-1.01778061470526,0.587615911876064,
-6.1041716606476));
#379623=CARTESIAN_POINT('Ctrl Pts',(-1.35704081960701,6.03040400634774E-16,
-6.06250499398093));
#379624=CARTESIAN_POINT('Ctrl Pts',(-1.01778061470526,-0.587615911876062,
-6.02083832731427));
#379625=CARTESIAN_POINT('Ctrl Pts',(-0.678520409803505,-1.17523182375213,
-5.9791716606476));
#379626=CARTESIAN_POINT('Ctrl Pts',(-1.43924389121415E-16,-1.17523182375213,
-5.93750499398093));
#379627=CARTESIAN_POINT('Ctrl Pts',(0.678520409803504,-1.17523182375213,
-5.89583832731427));
#379628=CARTESIAN_POINT('Ctrl Pts',(1.01778061470526,-0.587615911876063,
-5.8541716606476));
#379629=CARTESIAN_POINT('Ctrl Pts',(1.35704081960701,2.70661261425969E-16,
-5.81250499398093));
#379630=CARTESIAN_POINT('Ctrl Pts',(1.01778061470526,0.587615911876063,
-5.77083832731426));
#379631=CARTESIAN_POINT('Ctrl Pts',(0.678520409803506,1.17523182375213,
-5.7291716606476));
#379632=CARTESIAN_POINT('Ctrl Pts',(0.,1.17523182375213,-5.68750499398093));
#379633=CARTESIAN_POINT('Ctrl Pts',(-0.678520409803505,1.17523182375213,
-5.64583832731427));
#379634=CARTESIAN_POINT('Ctrl Pts',(-1.01778061470526,0.587615911876064,
-5.6041716606476));
#379635=CARTESIAN_POINT('Ctrl Pts',(-1.35704081960701,6.03040400634774E-16,
-5.56250499398093));
#379636=CARTESIAN_POINT('Ctrl Pts',(-1.01778061470526,-0.587615911876062,
-5.52083832731427));
#379637=CARTESIAN_POINT('Ctrl Pts',(-0.678520409803505,-1.17523182375213,
-5.4791716606476));
#379638=CARTESIAN_POINT('Ctrl Pts',(-1.43924389121415E-16,-1.17523182375213,
-5.43750499398093));
#379639=CARTESIAN_POINT('Ctrl Pts',(0.678520409803504,-1.17523182375213,
-5.39583832731426));
#379640=CARTESIAN_POINT('Ctrl Pts',(1.01778061470526,-0.587615911876063,
-5.3541716606476));
#379641=CARTESIAN_POINT('Ctrl Pts',(1.35704081960701,2.70661261425969E-16,
-5.31250499398093));
#379642=CARTESIAN_POINT('Ctrl Pts',(1.01778061470526,0.587615911876063,
-5.27083832731427));
#379643=CARTESIAN_POINT('Ctrl Pts',(0.678520409803506,1.17523182375213,
-5.2291716606476));
#379644=CARTESIAN_POINT('Ctrl Pts',(0.,1.17523182375213,-5.18750499398093));
#379645=CARTESIAN_POINT('Ctrl Pts',(-0.678520409803505,1.17523182375213,
-5.14583832731427));
#379646=CARTESIAN_POINT('Ctrl Pts',(-1.01778061470526,0.587615911876064,
-5.1041716606476));
#379647=CARTESIAN_POINT('Ctrl Pts',(-1.35704081960701,6.03040400634774E-16,
-5.06250499398093));
#379648=CARTESIAN_POINT('Ctrl Pts',(-1.01778061470526,-0.587615911876062,
-5.02083832731427));
#379649=CARTESIAN_POINT('Ctrl Pts',(-0.678520409803505,-1.17523182375213,
-4.9791716606476));
#379650=CARTESIAN_POINT('Ctrl Pts',(-1.43924389121415E-16,-1.17523182375213,
-4.93750499398093));
#379651=CARTESIAN_POINT('Ctrl Pts',(0.678520409803504,-1.17523182375213,
-4.89583832731427));
#379652=CARTESIAN_POINT('Ctrl Pts',(1.01778061470526,-0.587615911876063,
-4.8541716606476));
#379653=CARTESIAN_POINT('Ctrl Pts',(1.35704081960701,2.70661261425969E-16,
-4.81250499398093));
#379654=CARTESIAN_POINT('Ctrl Pts',(1.01778061470526,0.587615911876063,
-4.77083832731427));
#379655=CARTESIAN_POINT('Ctrl Pts',(0.678520409803506,1.17523182375213,
-4.7291716606476));
#379656=CARTESIAN_POINT('Ctrl Pts',(0.,1.17523182375213,-4.68750499398093));
#379657=CARTESIAN_POINT('Ctrl Pts',(-0.678520409803505,1.17523182375213,
-4.64583832731427));
#379658=CARTESIAN_POINT('Ctrl Pts',(-1.01778061470526,0.587615911876064,
-4.6041716606476));
#379659=CARTESIAN_POINT('Ctrl Pts',(-1.35704081960701,6.03040400634774E-16,
-4.56250499398093));
#379660=CARTESIAN_POINT('Ctrl Pts',(-1.01778061470526,-0.587615911876062,
-4.52083832731427));
#379661=CARTESIAN_POINT('Ctrl Pts',(-0.678520409803505,-1.17523182375213,
-4.4791716606476));
#379662=CARTESIAN_POINT('Ctrl Pts',(-1.43924389121415E-16,-1.17523182375213,
-4.43750499398093));
#379663=CARTESIAN_POINT('Ctrl Pts',(0.678520409803504,-1.17523182375213,
-4.39583832731427));
#379664=CARTESIAN_POINT('Ctrl Pts',(1.01778061470526,-0.587615911876063,
-4.3541716606476));
#379665=CARTESIAN_POINT('Ctrl Pts',(1.35704081960701,2.70661261425969E-16,
-4.31250499398093));
#379666=CARTESIAN_POINT('Ctrl Pts',(1.01778061470526,0.587615911876063,
-4.27083832731427));
#379667=CARTESIAN_POINT('Ctrl Pts',(0.678520409803506,1.17523182375213,
-4.2291716606476));
#379668=CARTESIAN_POINT('Ctrl Pts',(0.,1.17523182375213,-4.18750499398093));
#379669=CARTESIAN_POINT('Ctrl Pts',(-0.678520409803505,1.17523182375213,
-4.14583832731427));
#379670=CARTESIAN_POINT('Ctrl Pts',(-1.01778061470526,0.587615911876064,
-4.1041716606476));
#379671=CARTESIAN_POINT('Ctrl Pts',(-1.35704081960701,6.03040400634774E-16,
-4.06250499398093));
#379672=CARTESIAN_POINT('Ctrl Pts',(-1.01778061470526,-0.587615911876062,
-4.02083832731427));
#379673=CARTESIAN_POINT('Ctrl Pts',(-0.678520409803505,-1.17523182375213,
-3.9791716606476));
#379674=CARTESIAN_POINT('Ctrl Pts',(-1.43924389121415E-16,-1.17523182375213,
-3.93750499398093));
#379675=CARTESIAN_POINT('Ctrl Pts',(0.678520409803504,-1.17523182375213,
-3.89583832731427));
#379676=CARTESIAN_POINT('Ctrl Pts',(1.01778061470526,-0.587615911876063,
-3.8541716606476));
#379677=CARTESIAN_POINT('Ctrl Pts',(1.35704081960701,2.70661261425969E-16,
-3.81250499398093));
#379678=CARTESIAN_POINT('Ctrl Pts',(1.01778061470526,0.587615911876063,
-3.77083832731427));
#379679=CARTESIAN_POINT('Ctrl Pts',(0.678520409803506,1.17523182375213,
-3.7291716606476));
#379680=CARTESIAN_POINT('Ctrl Pts',(0.,1.17523182375213,-3.68750499398093));
#379681=CARTESIAN_POINT('Ctrl Pts',(-0.678520409803505,1.17523182375213,
-3.64583832731427));
#379682=CARTESIAN_POINT('Ctrl Pts',(-1.01778061470526,0.587615911876064,
-3.6041716606476));
#379683=CARTESIAN_POINT('Ctrl Pts',(-1.35704081960701,6.03040400634774E-16,
-3.56250499398093));
#379684=CARTESIAN_POINT('Ctrl Pts',(-1.01778061470526,-0.587615911876062,
-3.52083832731427));
#379685=CARTESIAN_POINT('Ctrl Pts',(-0.678520409803505,-1.17523182375213,
-3.4791716606476));
#379686=CARTESIAN_POINT('Ctrl Pts',(-1.43924389121415E-16,-1.17523182375213,
-3.43750499398093));
#379687=CARTESIAN_POINT('Ctrl Pts',(0.678520409803504,-1.17523182375213,
-3.39583832731427));
#379688=CARTESIAN_POINT('Ctrl Pts',(1.01778061470526,-0.587615911876063,
-3.3541716606476));
#379689=CARTESIAN_POINT('Ctrl Pts',(1.35704081960701,2.70661261425969E-16,
-3.31250499398093));
#379690=CARTESIAN_POINT('Ctrl Pts',(1.01778061470526,0.587615911876063,
-3.27083832731427));
#379691=CARTESIAN_POINT('Ctrl Pts',(0.678520409803506,1.17523182375213,
-3.2291716606476));
#379692=CARTESIAN_POINT('Ctrl Pts',(0.,1.17523182375213,-3.18750499398093));
#379693=CARTESIAN_POINT('Ctrl Pts',(-0.678520409803505,1.17523182375213,
-3.14583832731427));
#379694=CARTESIAN_POINT('Ctrl Pts',(-1.01778061470526,0.587615911876064,
-3.1041716606476));
#379695=CARTESIAN_POINT('Ctrl Pts',(-1.35704081960701,6.03040400634774E-16,
-3.06250499398093));
#379696=CARTESIAN_POINT('Ctrl Pts',(-1.01778061470526,-0.587615911876062,
-3.02083832731427));
#379697=CARTESIAN_POINT('Ctrl Pts',(-0.678520409803505,-1.17523182375213,
-2.9791716606476));
#379698=CARTESIAN_POINT('Ctrl Pts',(-1.43924389121415E-16,-1.17523182375213,
-2.93750499398093));
#379699=CARTESIAN_POINT('Ctrl Pts',(0.678520409803504,-1.17523182375213,
-2.89583832731427));
#379700=CARTESIAN_POINT('Ctrl Pts',(1.01778061470526,-0.587615911876063,
-2.8541716606476));
#379701=CARTESIAN_POINT('Ctrl Pts',(1.35704081960701,2.70661261425969E-16,
-2.81250499398093));
#379702=CARTESIAN_POINT('Ctrl Pts',(1.01778061470526,0.587615911876063,
-2.77083832731427));
#379703=CARTESIAN_POINT('Ctrl Pts',(0.678520409803506,1.17523182375213,
-2.7291716606476));
#379704=CARTESIAN_POINT('Ctrl Pts',(0.,1.17523182375213,-2.68750499398093));
#379705=CARTESIAN_POINT('Ctrl Pts',(-0.678520409803505,1.17523182375213,
-2.64583832731427));
#379706=CARTESIAN_POINT('Ctrl Pts',(-1.01778061470526,0.587615911876064,
-2.6041716606476));
#379707=CARTESIAN_POINT('Ctrl Pts',(-1.35704081960701,6.03040400634774E-16,
-2.56250499398093));
#379708=CARTESIAN_POINT('Ctrl Pts',(-1.01778061470526,-0.587615911876062,
-2.52083832731427));
#379709=CARTESIAN_POINT('Ctrl Pts',(-0.678520409803505,-1.17523182375213,
-2.4791716606476));
#379710=CARTESIAN_POINT('Ctrl Pts',(-1.43924389121415E-16,-1.17523182375213,
-2.43750499398093));
#379711=CARTESIAN_POINT('Ctrl Pts',(0.678520409803504,-1.17523182375213,
-2.39583832731427));
#379712=CARTESIAN_POINT('Ctrl Pts',(1.01778061470526,-0.587615911876063,
-2.3541716606476));
#379713=CARTESIAN_POINT('Ctrl Pts',(1.35704081960701,2.70661261425969E-16,
-2.31250499398093));
#379714=CARTESIAN_POINT('Ctrl Pts',(1.01778061470526,0.587615911876063,
-2.27083832731427));
#379715=CARTESIAN_POINT('Ctrl Pts',(0.678520409803506,1.17523182375213,
-2.2291716606476));
#379716=CARTESIAN_POINT('Ctrl Pts',(0.,1.17523182375213,-2.18750499398093));
#379717=CARTESIAN_POINT('Ctrl Pts',(-0.678520409803505,1.17523182375213,
-2.14583832731427));
#379718=CARTESIAN_POINT('Ctrl Pts',(-1.01778061470526,0.587615911876064,
-2.1041716606476));
#379719=CARTESIAN_POINT('Ctrl Pts',(-1.35704081960701,6.03040400634774E-16,
-2.06250499398093));
#379720=CARTESIAN_POINT('Ctrl Pts',(-1.01778061470526,-0.587615911876062,
-2.02083832731427));
#379721=CARTESIAN_POINT('Ctrl Pts',(-0.678520409803505,-1.17523182375213,
-1.9791716606476));
#379722=CARTESIAN_POINT('Ctrl Pts',(-1.43924389121415E-16,-1.17523182375213,
-1.93750499398093));
#379723=CARTESIAN_POINT('Ctrl Pts',(0.678520409803504,-1.17523182375213,
-1.89583832731427));
#379724=CARTESIAN_POINT('Ctrl Pts',(1.01778061470526,-0.587615911876063,
-1.8541716606476));
#379725=CARTESIAN_POINT('Ctrl Pts',(1.35704081960701,2.70661261425969E-16,
-1.81250499398093));
#379726=CARTESIAN_POINT('Ctrl Pts',(1.01778061470526,0.587615911876063,
-1.77083832731427));
#379727=CARTESIAN_POINT('Ctrl Pts',(0.678520409803506,1.17523182375213,
-1.7291716606476));
#379728=CARTESIAN_POINT('Ctrl Pts',(0.,1.17523182375213,-1.68750499398093));
#379729=CARTESIAN_POINT('Ctrl Pts',(-0.678520409803505,1.17523182375213,
-1.64583832731427));
#379730=CARTESIAN_POINT('Ctrl Pts',(-1.01778061470526,0.587615911876064,
-1.6041716606476));
#379731=CARTESIAN_POINT('Ctrl Pts',(-1.35704081960701,6.03040400634774E-16,
-1.56250499398093));
#379732=CARTESIAN_POINT('Ctrl Pts',(-1.01778061470526,-0.587615911876062,
-1.52083832731427));
#379733=CARTESIAN_POINT('Ctrl Pts',(-0.678520409803505,-1.17523182375213,
-1.4791716606476));
#379734=CARTESIAN_POINT('Ctrl Pts',(-1.43924389121415E-16,-1.17523182375213,
-1.43750499398093));
#379735=CARTESIAN_POINT('Ctrl Pts',(0.678520409803504,-1.17523182375213,
-1.39583832731427));
#379736=CARTESIAN_POINT('Ctrl Pts',(1.01778061470526,-0.587615911876063,
-1.3541716606476));
#379737=CARTESIAN_POINT('Ctrl Pts',(1.35704081960701,2.70661261425969E-16,
-1.31250499398093));
#379738=CARTESIAN_POINT('Ctrl Pts',(1.01778061470526,0.587615911876063,
-1.27083832731427));
#379739=CARTESIAN_POINT('Ctrl Pts',(0.678520409803506,1.17523182375213,
-1.2291716606476));
#379740=CARTESIAN_POINT('Ctrl Pts',(0.,1.17523182375213,-1.18750499398093));
#379741=CARTESIAN_POINT('Ctrl Pts',(-0.678520409803505,1.17523182375213,
-1.14583832731427));
#379742=CARTESIAN_POINT('Ctrl Pts',(-1.01778061470526,0.587615911876064,
-1.1041716606476));
#379743=CARTESIAN_POINT('Ctrl Pts',(-1.35704081960701,6.03040400634774E-16,
-1.06250499398093));
#379744=CARTESIAN_POINT('Ctrl Pts',(-1.01778061470526,-0.587615911876062,
-1.02083832731427));
#379745=CARTESIAN_POINT('Ctrl Pts',(-0.678520409803505,-1.17523182375213,
-0.9791716606476));
#379746=CARTESIAN_POINT('Ctrl Pts',(-1.43924389121415E-16,-1.17523182375213,
-0.937504993980932));
#379747=CARTESIAN_POINT('Ctrl Pts',(0.678520409803504,-1.17523182375213,
-0.895838327314267));
#379748=CARTESIAN_POINT('Ctrl Pts',(1.01778061470526,-0.587615911876063,
-0.854171660647599));
#379749=CARTESIAN_POINT('Ctrl Pts',(1.35704081960701,2.70661261425969E-16,
-0.812504993980932));
#379750=CARTESIAN_POINT('Ctrl Pts',(1.01778061470526,0.587615911876063,
-0.770838327314266));
#379751=CARTESIAN_POINT('Ctrl Pts',(0.678520409803506,1.17523182375213,
-0.729171660647599));
#379752=CARTESIAN_POINT('Ctrl Pts',(0.,1.17523182375213,-0.687504993980934));
#379753=CARTESIAN_POINT('Ctrl Pts',(-0.678520409803505,1.17523182375213,
-0.645838327314266));
#379754=CARTESIAN_POINT('Ctrl Pts',(-1.01778061470526,0.587615911876064,
-0.604171660647599));
#379755=CARTESIAN_POINT('Ctrl Pts',(-1.35704081960701,6.03040400634774E-16,
-0.562504993980934));
#379756=CARTESIAN_POINT('Ctrl Pts',(-1.01778061470526,-0.587615911876062,
-0.520838327314266));
#379757=CARTESIAN_POINT('Ctrl Pts',(-0.678520409803505,-1.17523182375213,
-0.479171660647599));
#379758=CARTESIAN_POINT('Ctrl Pts',(-1.43924389121415E-16,-1.17523182375213,
-0.437504993980933));
#379759=CARTESIAN_POINT('Ctrl Pts',(0.678520409803504,-1.17523182375213,
-0.395838327314266));
#379760=CARTESIAN_POINT('Ctrl Pts',(1.01778061470526,-0.587615911876063,
-0.354171660647599));
#379761=CARTESIAN_POINT('Ctrl Pts',(1.35704081960701,2.70661261425969E-16,
-0.312504993980933));
#379762=CARTESIAN_POINT('Ctrl Pts',(1.01778061470526,0.587615911876063,
-0.270838327314266));
#379763=CARTESIAN_POINT('Ctrl Pts',(0.678520409803506,1.17523182375213,
-0.229171660647599));
#379764=CARTESIAN_POINT('Ctrl Pts',(0.,1.17523182375213,-0.187504993980933));
#379765=CARTESIAN_POINT('Ctrl Pts',(-0.678520409803505,1.17523182375213,
-0.145838327314266));
#379766=CARTESIAN_POINT('Ctrl Pts',(-1.01778061470526,0.587615911876064,
-0.104171660647599));
#379767=CARTESIAN_POINT('Ctrl Pts',(-1.35704081960701,6.03040400634774E-16,
-0.0625049939809331));
#379768=CARTESIAN_POINT('Ctrl Pts',(-1.01778061470526,-0.587615911876062,
-0.0208383273142658));
#379769=CARTESIAN_POINT('Ctrl Pts',(-0.678520409803505,-1.17523182375213,
0.0208283393523997));
#379770=CARTESIAN_POINT('Ctrl Pts',(-1.43924389121415E-16,-1.17523182375213,
0.062495006019067));
#379771=CARTESIAN_POINT('Ctrl Pts',(0.678520409803504,-1.17523182375213,
0.104161672685734));
#379772=CARTESIAN_POINT('Ctrl Pts',(1.01778061470526,-0.587615911876063,
0.1458283393524));
#379773=CARTESIAN_POINT('Ctrl Pts',(1.35704081960701,2.70661261425969E-16,
0.187495006019067));
#379774=CARTESIAN_POINT('Ctrl Pts',(1.01778061470526,0.587615911876063,
0.229161672685734));
#379775=CARTESIAN_POINT('Ctrl Pts',(0.678520409803506,1.17523182375213,
0.2708283393524));
#379776=CARTESIAN_POINT('Ctrl Pts',(0.,1.17523182375213,0.312495006019067));
#379777=CARTESIAN_POINT('Ctrl Pts',(-0.678520409803505,1.17523182375213,
0.354161672685734));
#379778=CARTESIAN_POINT('Ctrl Pts',(-1.01778061470526,0.587615911876064,
0.3958283393524));
#379779=CARTESIAN_POINT('Ctrl Pts',(-1.35704081960701,6.03040400634774E-16,
0.437495006019067));
#379780=CARTESIAN_POINT('Ctrl Pts',(-1.01778061470526,-0.587615911876062,
0.479161672685735));
#379781=CARTESIAN_POINT('Ctrl Pts',(-0.678520409803505,-1.17523182375213,
0.5208283393524));
#379782=CARTESIAN_POINT('Ctrl Pts',(-1.43924389121415E-16,-1.17523182375213,
0.562495006019067));
#379783=CARTESIAN_POINT('Ctrl Pts',(0.678520409803504,-1.17523182375213,
0.604161672685733));
#379784=CARTESIAN_POINT('Ctrl Pts',(1.01778061470526,-0.587615911876063,
0.6458283393524));
#379785=CARTESIAN_POINT('Ctrl Pts',(1.35704081960701,2.70661261425969E-16,
0.687495006019068));
#379786=CARTESIAN_POINT('Ctrl Pts',(1.01778061470526,0.587615911876063,
0.729161672685733));
#379787=CARTESIAN_POINT('Ctrl Pts',(0.678520409803506,1.17523182375213,
0.770828339352401));
#379788=CARTESIAN_POINT('Ctrl Pts',(0.,1.17523182375213,0.812495006019068));
#379789=CARTESIAN_POINT('Ctrl Pts',(-0.678520409803505,1.17523182375213,
0.854161672685734));
#379790=CARTESIAN_POINT('Ctrl Pts',(-1.01778061470526,0.587615911876064,
0.8958283393524));
#379791=CARTESIAN_POINT('Ctrl Pts',(-1.35704081960701,6.03040400634774E-16,
0.937495006019068));
#379792=CARTESIAN_POINT('Ctrl Pts',(-1.01778061470526,-0.587615911876062,
0.979161672685733));
#379793=CARTESIAN_POINT('Ctrl Pts',(-0.678520409803505,-1.17523182375213,
1.0208283393524));
#379794=CARTESIAN_POINT('Ctrl Pts',(-1.43924389121415E-16,-1.17523182375213,
1.06249500601907));
#379795=CARTESIAN_POINT('Ctrl Pts',(0.678520409803504,-1.17523182375213,
1.10416167268573));
#379796=CARTESIAN_POINT('Ctrl Pts',(1.01778061470526,-0.587615911876063,
1.1458283393524));
#379797=CARTESIAN_POINT('Ctrl Pts',(1.35704081960701,2.70661261425969E-16,
1.18749500601907));
#379798=CARTESIAN_POINT('Ctrl Pts',(1.01778061470526,0.587615911876063,
1.22916167268573));
#379799=CARTESIAN_POINT('Ctrl Pts',(0.678520409803506,1.17523182375213,
1.2708283393524));
#379800=CARTESIAN_POINT('Ctrl Pts',(0.,1.17523182375213,1.31249500601907));
#379801=CARTESIAN_POINT('Ctrl Pts',(-0.678520409803505,1.17523182375213,
1.35416167268573));
#379802=CARTESIAN_POINT('Ctrl Pts',(-1.01778061470526,0.587615911876064,
1.3958283393524));
#379803=CARTESIAN_POINT('Ctrl Pts',(-1.35704081960701,6.03040400634774E-16,
1.43749500601907));
#379804=CARTESIAN_POINT('Ctrl Pts',(-1.01778061470526,-0.587615911876062,
1.47916167268573));
#379805=CARTESIAN_POINT('Ctrl Pts',(-0.678520409803505,-1.17523182375213,
1.5208283393524));
#379806=CARTESIAN_POINT('Ctrl Pts',(-1.43924389121415E-16,-1.17523182375213,
1.56249500601907));
#379807=CARTESIAN_POINT('Ctrl Pts',(0.678520409803504,-1.17523182375213,
1.60416167268573));
#379808=CARTESIAN_POINT('Ctrl Pts',(1.01778061470526,-0.587615911876063,
1.6458283393524));
#379809=CARTESIAN_POINT('Ctrl Pts',(1.35704081960701,2.70661261425969E-16,
1.68749500601907));
#379810=CARTESIAN_POINT('Ctrl Pts',(1.01778061470526,0.587615911876063,
1.72916167268573));
#379811=CARTESIAN_POINT('Ctrl Pts',(0.678520409803506,1.17523182375213,
1.7708283393524));
#379812=CARTESIAN_POINT('Ctrl Pts',(0.,1.17523182375213,1.81249500601907));
#379813=CARTESIAN_POINT('Ctrl Pts',(-0.678520409803505,1.17523182375213,
1.85416167268573));
#379814=CARTESIAN_POINT('Ctrl Pts',(-1.01778061470526,0.587615911876064,
1.8958283393524));
#379815=CARTESIAN_POINT('Ctrl Pts',(-1.35704081960701,6.03040400634774E-16,
1.93749500601907));
#379816=CARTESIAN_POINT('Ctrl Pts',(-1.01778061470526,-0.587615911876062,
1.97916167268573));
#379817=CARTESIAN_POINT('Ctrl Pts',(-0.678520409803505,-1.17523182375213,
2.0208283393524));
#379818=CARTESIAN_POINT('Ctrl Pts',(-1.43924389121415E-16,-1.17523182375213,
2.06249500601907));
#379819=CARTESIAN_POINT('Ctrl Pts',(0.678520409803504,-1.17523182375213,
2.10416167268574));
#379820=CARTESIAN_POINT('Ctrl Pts',(1.01778061470526,-0.587615911876063,
2.1458283393524));
#379821=CARTESIAN_POINT('Ctrl Pts',(1.35704081960701,2.70661261425969E-16,
2.18749500601907));
#379822=CARTESIAN_POINT('Ctrl Pts',(1.01778061470526,0.587615911876063,
2.22916167268573));
#379823=CARTESIAN_POINT('Ctrl Pts',(0.678520409803506,1.17523182375213,
2.2708283393524));
#379824=CARTESIAN_POINT('Ctrl Pts',(0.,1.17523182375213,2.31249500601907));
#379825=CARTESIAN_POINT('Ctrl Pts',(-0.678520409803505,1.17523182375213,
2.35416167268573));
#379826=CARTESIAN_POINT('Ctrl Pts',(-1.01778061470526,0.587615911876064,
2.3958283393524));
#379827=CARTESIAN_POINT('Ctrl Pts',(-1.35704081960701,6.03040400634774E-16,
2.43749500601907));
#379828=CARTESIAN_POINT('Ctrl Pts',(-1.01778061470526,-0.587615911876062,
2.47916167268573));
#379829=CARTESIAN_POINT('Ctrl Pts',(-0.678520409803505,-1.17523182375213,
2.5208283393524));
#379830=CARTESIAN_POINT('Ctrl Pts',(-1.43924389121415E-16,-1.17523182375213,
2.56249500601907));
#379831=CARTESIAN_POINT('Ctrl Pts',(0.678520409803504,-1.17523182375213,
2.60416167268573));
#379832=CARTESIAN_POINT('Ctrl Pts',(1.01778061470526,-0.587615911876063,
2.6458283393524));
#379833=CARTESIAN_POINT('Ctrl Pts',(1.35704081960701,2.70661261425969E-16,
2.68749500601907));
#379834=CARTESIAN_POINT('Ctrl Pts',(1.01778061470526,0.587615911876063,
2.72916167268573));
#379835=CARTESIAN_POINT('Ctrl Pts',(0.678520409803506,1.17523182375213,
2.7708283393524));
#379836=CARTESIAN_POINT('Ctrl Pts',(0.,1.17523182375213,2.81249500601907));
#379837=CARTESIAN_POINT('Ctrl Pts',(-0.678520409803505,1.17523182375213,
2.85416167268573));
#379838=CARTESIAN_POINT('Ctrl Pts',(-1.01778061470526,0.587615911876064,
2.8958283393524));
#379839=CARTESIAN_POINT('Ctrl Pts',(-1.35704081960701,6.03040400634774E-16,
2.93749500601907));
#379840=CARTESIAN_POINT('Ctrl Pts',(-1.01778061470526,-0.587615911876062,
2.97916167268573));
#379841=CARTESIAN_POINT('Ctrl Pts',(-0.678520409803505,-1.17523182375213,
3.0208283393524));
#379842=CARTESIAN_POINT('Ctrl Pts',(-1.43924389121415E-16,-1.17523182375213,
3.06249500601907));
#379843=CARTESIAN_POINT('Ctrl Pts',(0.678520409803504,-1.17523182375213,
3.10416167268573));
#379844=CARTESIAN_POINT('Ctrl Pts',(1.01778061470526,-0.587615911876063,
3.1458283393524));
#379845=CARTESIAN_POINT('Ctrl Pts',(1.35704081960701,2.70661261425969E-16,
3.18749500601907));
#379846=CARTESIAN_POINT('Ctrl Pts',(1.01778061470526,0.587615911876063,
3.22916167268573));
#379847=CARTESIAN_POINT('Ctrl Pts',(0.678520409803506,1.17523182375213,
3.2708283393524));
#379848=CARTESIAN_POINT('Ctrl Pts',(0.,1.17523182375213,3.31249500601907));
#379849=CARTESIAN_POINT('Ctrl Pts',(-0.678520409803505,1.17523182375213,
3.35416167268573));
#379850=CARTESIAN_POINT('Ctrl Pts',(-1.01778061470526,0.587615911876064,
3.3958283393524));
#379851=CARTESIAN_POINT('Ctrl Pts',(-1.35704081960701,6.03040400634774E-16,
3.43749500601907));
#379852=CARTESIAN_POINT('Ctrl Pts',(-1.01778061470526,-0.587615911876062,
3.47916167268573));
#379853=CARTESIAN_POINT('Ctrl Pts',(-0.678520409803505,-1.17523182375213,
3.5208283393524));
#379854=CARTESIAN_POINT('Ctrl Pts',(-1.43924389121415E-16,-1.17523182375213,
3.56249500601907));
#379855=CARTESIAN_POINT('Ctrl Pts',(0.678520409803504,-1.17523182375213,
3.60416167268574));
#379856=CARTESIAN_POINT('Ctrl Pts',(1.01778061470526,-0.587615911876063,
3.6458283393524));
#379857=CARTESIAN_POINT('Ctrl Pts',(1.35704081960701,2.7066126142597E-16,
3.68749500601907));
#379858=CARTESIAN_POINT('Ctrl Pts',(1.01778061470526,0.587615911876063,
3.72916167268573));
#379859=CARTESIAN_POINT('Ctrl Pts',(0.678520409803506,1.17523182375213,
3.7708283393524));
#379860=CARTESIAN_POINT('Ctrl Pts',(0.,1.17523182375213,3.81249500601907));
#379861=CARTESIAN_POINT('Ctrl Pts',(-0.678520409803505,1.17523182375213,
3.85416167268573));
#379862=CARTESIAN_POINT('Ctrl Pts',(-1.01778061470526,0.587615911876064,
3.8958283393524));
#379863=CARTESIAN_POINT('Ctrl Pts',(-1.35704081960701,6.03040400634774E-16,
3.93749500601907));
#379864=CARTESIAN_POINT('Ctrl Pts',(-1.01778061470526,-0.587615911876062,
3.97916167268573));
#379865=CARTESIAN_POINT('Ctrl Pts',(-0.678520409803505,-1.17523182375213,
4.0208283393524));
#379866=CARTESIAN_POINT('Ctrl Pts',(-1.43924389121415E-16,-1.17523182375213,
4.06249500601907));
#379867=CARTESIAN_POINT('Ctrl Pts',(0.678520409803504,-1.17523182375213,
4.10416167268574));
#379868=CARTESIAN_POINT('Ctrl Pts',(1.01778061470526,-0.587615911876063,
4.1458283393524));
#379869=CARTESIAN_POINT('Ctrl Pts',(1.35704081960701,2.7066126142597E-16,
4.18749500601907));
#379870=CARTESIAN_POINT('Ctrl Pts',(1.01778061470526,0.587615911876063,
4.22916167268574));
#379871=CARTESIAN_POINT('Ctrl Pts',(0.678520409803506,1.17523182375213,
4.2708283393524));
#379872=CARTESIAN_POINT('Ctrl Pts',(0.,1.17523182375213,4.31249500601907));
#379873=CARTESIAN_POINT('Ctrl Pts',(-0.678520409803505,1.17523182375213,
4.35416167268573));
#379874=CARTESIAN_POINT('Ctrl Pts',(-1.01778061470526,0.587615911876064,
4.3958283393524));
#379875=CARTESIAN_POINT('Ctrl Pts',(-1.35704081960701,6.03040400634775E-16,
4.43749500601907));
#379876=CARTESIAN_POINT('Ctrl Pts',(-1.01778061470526,-0.587615911876062,
4.47916167268573));
#379877=CARTESIAN_POINT('Ctrl Pts',(-0.678520409803505,-1.17523182375213,
4.5208283393524));
#379878=CARTESIAN_POINT('Ctrl Pts',(-1.43924389121415E-16,-1.17523182375213,
4.56249500601907));
#379879=CARTESIAN_POINT('Ctrl Pts',(0.678520409803504,-1.17523182375213,
4.60416167268573));
#379880=CARTESIAN_POINT('Ctrl Pts',(1.01778061470526,-0.587615911876063,
4.6458283393524));
#379881=CARTESIAN_POINT('Ctrl Pts',(1.35704081960701,2.7066126142597E-16,
4.68749500601907));
#379882=CARTESIAN_POINT('Ctrl Pts',(1.01778061470526,0.587615911876063,
4.72916167268573));
#379883=CARTESIAN_POINT('Ctrl Pts',(0.678520409803506,1.17523182375213,
4.7708283393524));
#379884=CARTESIAN_POINT('Ctrl Pts',(0.,1.17523182375213,4.81249500601907));
#379885=CARTESIAN_POINT('Ctrl Pts',(-0.678520409803505,1.17523182375213,
4.85416167268573));
#379886=CARTESIAN_POINT('Ctrl Pts',(-1.01778061470526,0.587615911876064,
4.8958283393524));
#379887=CARTESIAN_POINT('Ctrl Pts',(-1.35704081960701,6.03040400634775E-16,
4.93749500601907));
#379888=CARTESIAN_POINT('Ctrl Pts',(-1.01778061470526,-0.587615911876062,
4.97916167268573));
#379889=CARTESIAN_POINT('Ctrl Pts',(-0.678520409803505,-1.17523182375213,
5.0208283393524));
#379890=CARTESIAN_POINT('Ctrl Pts',(-1.43924389121415E-16,-1.17523182375213,
5.06249500601907));
#379891=CARTESIAN_POINT('Ctrl Pts',(0.678520409803504,-1.17523182375213,
5.10416167268573));
#379892=CARTESIAN_POINT('Ctrl Pts',(1.01778061470526,-0.587615911876063,
5.1458283393524));
#379893=CARTESIAN_POINT('Ctrl Pts',(1.35704081960701,2.7066126142597E-16,
5.18749500601907));
#379894=CARTESIAN_POINT('Ctrl Pts',(1.01778061470526,0.587615911876063,
5.22916167268573));
#379895=CARTESIAN_POINT('Ctrl Pts',(0.678520409803506,1.17523182375213,
5.2708283393524));
#379896=CARTESIAN_POINT('Ctrl Pts',(0.,1.17523182375213,5.31249500601907));
#379897=CARTESIAN_POINT('Ctrl Pts',(-0.678520409803505,1.17523182375213,
5.35416167268573));
#379898=CARTESIAN_POINT('Ctrl Pts',(-1.01778061470526,0.587615911876064,
5.3958283393524));
#379899=CARTESIAN_POINT('Ctrl Pts',(-1.35704081960701,6.03040400634775E-16,
5.43749500601907));
#379900=CARTESIAN_POINT('Ctrl Pts',(-1.01778061470526,-0.587615911876062,
5.47916167268573));
#379901=CARTESIAN_POINT('Ctrl Pts',(-0.678520409803505,-1.17523182375213,
5.5208283393524));
#379902=CARTESIAN_POINT('Ctrl Pts',(-1.43924389121415E-16,-1.17523182375213,
5.56249500601907));
#379903=CARTESIAN_POINT('Ctrl Pts',(0.678520409803504,-1.17523182375213,
5.60416167268573));
#379904=CARTESIAN_POINT('Ctrl Pts',(1.01778061470526,-0.587615911876063,
5.6458283393524));
#379905=CARTESIAN_POINT('Ctrl Pts',(1.35704081960701,2.7066126142597E-16,
5.68749500601907));
#379906=CARTESIAN_POINT('Ctrl Pts',(1.01778061470526,0.587615911876063,
5.72916167268573));
#379907=CARTESIAN_POINT('Ctrl Pts',(0.678520409803506,1.17523182375213,
5.7708283393524));
#379908=CARTESIAN_POINT('Ctrl Pts',(0.,1.17523182375213,5.81249500601907));
#379909=CARTESIAN_POINT('Ctrl Pts',(-0.678520409803505,1.17523182375213,
5.85416167268574));
#379910=CARTESIAN_POINT('Ctrl Pts',(-1.01778061470526,0.587615911876064,
5.8958283393524));
#379911=CARTESIAN_POINT('Ctrl Pts',(-1.35704081960701,6.03040400634775E-16,
5.93749500601907));
#379912=CARTESIAN_POINT('Ctrl Pts',(-1.01778061470526,-0.587615911876062,
5.97916167268573));
#379913=CARTESIAN_POINT('Ctrl Pts',(-0.678520409803505,-1.17523182375213,
6.0208283393524));
#379914=CARTESIAN_POINT('Ctrl Pts',(-1.43924389121415E-16,-1.17523182375213,
6.06249500601907));
#379915=CARTESIAN_POINT('Ctrl Pts',(0.678520409803504,-1.17523182375213,
6.10416167268574));
#379916=CARTESIAN_POINT('Ctrl Pts',(1.01778061470526,-0.587615911876063,
6.1458283393524));
#379917=CARTESIAN_POINT('Ctrl Pts',(1.35704081960701,2.7066126142597E-16,
6.18749500601907));
#379918=CARTESIAN_POINT('Ctrl Pts',(1.01778061470526,0.587615911876063,
6.22916167268573));
#379919=CARTESIAN_POINT('Ctrl Pts',(0.678520409803506,1.17523182375213,
6.2708283393524));
#379920=CARTESIAN_POINT('Ctrl Pts',(0.,1.17523182375213,6.31249500601907));
#379921=CARTESIAN_POINT('Origin',(0.,0.,7.5));
#379922=CARTESIAN_POINT('',(-0.0391111754616882,2.74606032550115,7.50366116523517));
#379923=CARTESIAN_POINT('',(1.95335088339909E-13,2.67396661573471,7.57603338622103));
#379924=CARTESIAN_POINT('Ctrl Pts',(-0.039111175493625,2.74606032554878,
7.50366116529969));
#379925=CARTESIAN_POINT('Ctrl Pts',(-0.0260946561062611,2.72206870155541,
7.52783573079709));
#379926=CARTESIAN_POINT('Ctrl Pts',(-0.0130581974131689,2.69803860815066,
7.55196141284069));
#379927=CARTESIAN_POINT('Ctrl Pts',(-8.83381775932182E-10,2.67396661662181,
7.57603338728831));
#379928=CARTESIAN_POINT('',(0.0391111754616882,2.74606032550115,7.50366116523517));
#379929=CARTESIAN_POINT('Ctrl Pts',(8.84014432836477E-10,2.673966616623,
7.57603338728985));
#379930=CARTESIAN_POINT('Ctrl Pts',(0.0130581974166911,2.69803860815728,
7.55196141284922));
#379931=CARTESIAN_POINT('Ctrl Pts',(0.0260946561203838,2.72206870158194,
7.52783573083105));
#379932=CARTESIAN_POINT('Ctrl Pts',(0.0391111754945677,2.74606032555036,
7.50366116530176));
#379933=CARTESIAN_POINT('Origin',(0.,0.,7.50366116523517));
#379934=CARTESIAN_POINT('Ctrl Pts',(-0.00576978243959104,2.66725829676663,
7.59443877723642));
#379935=CARTESIAN_POINT('Ctrl Pts',(-0.00300154637558126,2.66217203460837,
7.58783886950016));
#379936=CARTESIAN_POINT('Ctrl Pts',(0.00519220816616302,2.66439499840616,
7.58559994247159));
#379937=CARTESIAN_POINT('Ctrl Pts',(-0.02088150189643,2.69502405266403,
7.56670252222137));
#379938=CARTESIAN_POINT('Ctrl Pts',(-0.0181172667194093,2.68994514159859,
7.56004874999026));
#379939=CARTESIAN_POINT('Ctrl Pts',(-0.00986936707313795,2.69216065704217,
7.55786368756704));
#379940=CARTESIAN_POINT('Ctrl Pts',(-0.0359650017270119,2.72273795878639,
7.53888913333556));
#379941=CARTESIAN_POINT('Ctrl Pts',(-0.0331843385650257,2.71762886350384,
7.53222002137276));
#379942=CARTESIAN_POINT('Ctrl Pts',(-0.0249043752016816,2.71987489365092,
7.53005029815326));
#379943=CARTESIAN_POINT('Ctrl Pts',(-0.0510195993927981,2.75039876106078,
7.51101258149734));
#379944=CARTESIAN_POINT('Ctrl Pts',(-0.0482052295407062,2.74522773425994,
7.5043616886572));
#379945=CARTESIAN_POINT('Ctrl Pts',(-0.0399120007351545,2.74753637834759,
7.50217374673251));
#379946=CARTESIAN_POINT('Ctrl Pts',(-0.0469183093502058,2.74286319116668,
7.51860402984325));
#379947=CARTESIAN_POINT('Ctrl Pts',(-0.047129417868931,2.74325107473053,
7.51734760759494));
#379948=CARTESIAN_POINT('Ctrl Pts',(-0.0472679263427277,2.74363002494186,
7.51608817408573));
#379949=CARTESIAN_POINT('Ctrl Pts',(-0.0473209740766783,2.74400375441725,
7.5148100591312));
#379950=CARTESIAN_POINT('Ctrl Pts',(-0.0473690259817077,2.74434228750662,
7.51365231206384));
#379951=CARTESIAN_POINT('Ctrl Pts',(-0.0473472713218901,2.74467697892738,
7.51247773061043));
#379952=CARTESIAN_POINT('Ctrl Pts',(-0.0472192392491731,2.74499964227536,
7.51129758471022));
#379953=CARTESIAN_POINT('Ctrl Pts',(-0.047060110004601,2.74540067596735,
7.50983079813402));
#379954=CARTESIAN_POINT('Ctrl Pts',(-0.0467297792999064,2.74576552647934,
7.50839324291155));
#379955=CARTESIAN_POINT('Ctrl Pts',(-0.0461647233399476,2.7460415258142,
7.50715379678855));
#379956=CARTESIAN_POINT('Ctrl Pts',(-0.045903683768143,2.74616902955418,
7.50658120839351));
#379957=CARTESIAN_POINT('Ctrl Pts',(-0.0455512704078027,2.74628715902903,
7.50598221009429));
#379958=CARTESIAN_POINT('Ctrl Pts',(-0.045108640875781,2.74637153582515,
7.50545747549611));
#379959=CARTESIAN_POINT('Ctrl Pts',(-0.0448724400568288,2.74641656189527,
7.50517746087247));
#379960=CARTESIAN_POINT('Ctrl Pts',(-0.0446080257594691,2.74645266364665,
7.50491486231392));
#379961=CARTESIAN_POINT('Ctrl Pts',(-0.0443221744710907,2.74647723236113,
7.50468370960992));
#379962=CARTESIAN_POINT('Ctrl Pts',(-0.043894736628288,2.74651397033903,
7.50433806340447));
#379963=CARTESIAN_POINT('Ctrl Pts',(-0.0434065014443661,2.74652546781193,
7.50405484070984));
#379964=CARTESIAN_POINT('Ctrl Pts',(-0.042890333785409,2.74651023424991,
7.50385766036131));
#379965=CARTESIAN_POINT('Ctrl Pts',(-0.0428351376773461,2.74650860525723,
7.50383657498791));
#379966=CARTESIAN_POINT('Ctrl Pts',(-0.0427796461468639,2.7465066857332,
7.50381643264937));
#379967=CARTESIAN_POINT('Ctrl Pts',(-0.0427239166342629,2.74650448512403,
7.50379723213559));
#379968=CARTESIAN_POINT('Ctrl Pts',(-0.0423519039072553,2.74648979533795,
7.50366906242519));
#379969=CARTESIAN_POINT('Ctrl Pts',(-0.041961222930374,2.74646154237284,
7.50358235568538));
#379970=CARTESIAN_POINT('Ctrl Pts',(-0.041585309161405,2.74642525806308,
7.5035341175365));
#379971=CARTESIAN_POINT('Ctrl Pts',(-0.0410216690100585,2.74637085384718,
7.50346178989176));
#379972=CARTESIAN_POINT('Ctrl Pts',(-0.0404176336735107,2.74628836196342,
7.50346967198527));
#379973=CARTESIAN_POINT('Ctrl Pts',(-0.0398271499193936,2.74618913461648,
7.50354272648692));
#379974=CARTESIAN_POINT('Ctrl Pts',(-0.0395842717290364,2.74614832035481,
7.50357277531559));
#379975=CARTESIAN_POINT('Ctrl Pts',(-0.0393439854661266,2.74610486877363,
7.50361331098761));
#379976=CARTESIAN_POINT('Ctrl Pts',(-0.0391111754617084,2.74606032550257,
7.50366116523658));
#379977=CARTESIAN_POINT('Origin',(2.85317610332501E-6,2.68280355420138,
7.58486873427628));
#379978=CARTESIAN_POINT('Origin',(-0.0578975244977156,2.73688767154537,
9.));
#379979=CARTESIAN_POINT('Origin',(-0.0578975244977155,2.73688767154537,
8.75721825406948));
#379980=CARTESIAN_POINT('Origin',(-0.0578975244977156,2.73688767154537,
7.51860402984325));
#379981=CARTESIAN_POINT('Ctrl Pts',(-0.00637576431677354,2.66873949177856,
7.59639677331371));
#379982=CARTESIAN_POINT('Ctrl Pts',(-0.000286090908296224,2.6515061579884,
7.59959882295465));
#379983=CARTESIAN_POINT('Ctrl Pts',(0.00631291894862653,2.66856962426893,
7.59642833564546));
#379984=CARTESIAN_POINT('Ctrl Pts',(-0.00568422544926916,2.66490062761342,
7.58707626057423));
#379985=CARTESIAN_POINT('Ctrl Pts',(-9.68314384630046E-5,2.66106744105337,
7.58809943920598));
#379986=CARTESIAN_POINT('Ctrl Pts',(0.0055389809656482,2.66480268125159,
7.58710240504252));
#379987=CARTESIAN_POINT('Ctrl Pts',(-0.00215341460009478,2.66984623243071,
7.58015376756929));
#379988=CARTESIAN_POINT('Ctrl Pts',(-3.20712293815052E-5,2.66794119340239,
7.58205880659761));
#379989=CARTESIAN_POINT('Ctrl Pts',(0.00209070701379044,2.66979075755872,
7.58020924244128));
#379990=CARTESIAN_POINT('Ctrl Pts',(-7.55734230502141E-15,2.67396661490714,
7.57603338509286));
#379991=CARTESIAN_POINT('Ctrl Pts',(-7.55734230502141E-15,2.67396661490714,
7.57603338509286));
#379992=CARTESIAN_POINT('Ctrl Pts',(-7.55734230502141E-15,2.67396661490714,
7.57603338509286));
#379993=CARTESIAN_POINT('Origin',(-2.85317609963331E-6,2.68280355420132,
7.58486873427623));
#379994=CARTESIAN_POINT('Ctrl Pts',(-0.0469178037552555,2.74286226211022,
7.51860402984325));
#379995=CARTESIAN_POINT('Ctrl Pts',(-0.0505546378370145,2.74954580337902,
7.51860402984325));
#379996=CARTESIAN_POINT('Ctrl Pts',(-0.0581618967556967,2.74938487552503,
7.51860402984325));
#379997=CARTESIAN_POINT('Ctrl Pts',(-0.0482681861850447,2.74534390598683,
7.51041458714366));
#379998=CARTESIAN_POINT('Ctrl Pts',(-0.0523568843976852,2.74950766782993,
7.51004642900442));
#379999=CARTESIAN_POINT('Ctrl Pts',(-0.0581639947473825,2.74938483114304,
7.50729136483008));
#380000=CARTESIAN_POINT('Ctrl Pts',(-0.0464115390694411,2.74745970339853,
7.50215815450138));
#380001=CARTESIAN_POINT('Ctrl Pts',(-0.0486873335340281,2.74958545597972,
7.49877163671531));
#380002=CARTESIAN_POINT('Ctrl Pts',(-0.0521371901874483,2.74953633709117,
7.49481588533172));
#380003=CARTESIAN_POINT('Ctrl Pts',(-0.0391111676211739,2.74605977503896,
7.50366171572174));
#380004=CARTESIAN_POINT('Ctrl Pts',(-0.0391633148674429,2.7497211194535,
7.50000045605858));
#380005=CARTESIAN_POINT('Ctrl Pts',(-0.0391633148675675,2.7497211194535,
7.49482233047317));
#380006=CARTESIAN_POINT('Origin',(-0.0389852998002483,2.73722238709234,
7.49482233047033));
#380007=CARTESIAN_POINT('Ctrl Pts',(-0.0389349646546055,2.72819480378047,
8.78942910404912));
#380008=CARTESIAN_POINT('Ctrl Pts',(-0.0415810698404549,2.73309894040653,
8.7967269950169));
#380009=CARTESIAN_POINT('Ctrl Pts',(-0.0500812990341607,2.73037504803777,
8.79893251111267));
#380010=CARTESIAN_POINT('Ctrl Pts',(-0.0441907101996744,2.7378515401601,
8.78111911759583));
#380011=CARTESIAN_POINT('Ctrl Pts',(-0.0473342496199769,2.74366191622698,
8.78644465894812));
#380012=CARTESIAN_POINT('Ctrl Pts',(-0.0554049987396861,2.74290131092718,
8.78817647674132));
#380013=CARTESIAN_POINT('Ctrl Pts',(-0.047466216212685,2.7438698485916,
8.76780923932029));
#380014=CARTESIAN_POINT('Ctrl Pts',(-0.0511815136631339,2.75072632739817,
8.76988516158374));
#380015=CARTESIAN_POINT('Ctrl Pts',(-0.0587403725670999,2.75072062947551,
8.77093053738833));
#380016=CARTESIAN_POINT('Ctrl Pts',(-0.0468275373701205,2.74269636081296,
8.75371302330492));
#380017=CARTESIAN_POINT('Ctrl Pts',(-0.0504509795361613,2.74938492330704,
8.75300828287559));
#380018=CARTESIAN_POINT('Ctrl Pts',(-0.0580902600704512,2.74919536526138,
8.75267964240738));
#380019=CARTESIAN_POINT('Origin',(-0.0511941478023398,2.72457111673216,
8.78727029226991));
#380020=CARTESIAN_POINT('Ctrl Pts',(0.0510325618244046,2.75042257778878,
7.51098857897448));
#380021=CARTESIAN_POINT('Ctrl Pts',(0.0482181791375388,2.74525152740576,
7.50433767179956));
#380022=CARTESIAN_POINT('Ctrl Pts',(0.0399249227228591,2.74756019566318,
7.50214974420965));
#380023=CARTESIAN_POINT('Ctrl Pts',(0.0359736340692041,2.72275381955636,
7.53887321589169));
#380024=CARTESIAN_POINT('Ctrl Pts',(0.0331929726815447,2.71764472753391,
7.53220407452065));
#380025=CARTESIAN_POINT('Ctrl Pts',(0.0249129797891101,2.71989075460921,
7.53003438070911));
#380026=CARTESIAN_POINT('Ctrl Pts',(0.0208857876177118,2.69503192710157,
7.56669465659234));
#380027=CARTESIAN_POINT('Ctrl Pts',(0.0181215594219111,2.68995302886307,
7.56004085833303));
#380028=CARTESIAN_POINT('Ctrl Pts',(0.00987363856813336,2.6921685314508,
7.55785582193789));
#380029=CARTESIAN_POINT('Ctrl Pts',(0.00576970483280572,2.66725815417458,
7.59443891967696));
#380030=CARTESIAN_POINT('Ctrl Pts',(0.00300146885025822,2.66217189216599,
7.58783901202978));
#380031=CARTESIAN_POINT('Ctrl Pts',(-0.00519228551543038,2.66439485581461,
7.58560008491213));
#380032=CARTESIAN_POINT('Ctrl Pts',(0.0391111754616935,2.74606032550152,
7.50366116523554));
#380033=CARTESIAN_POINT('Ctrl Pts',(0.0398554269668709,2.74620254791117,
7.50350835821027));
#380034=CARTESIAN_POINT('Ctrl Pts',(0.0405442017937646,2.74630907137797,
7.50345484956));
#380035=CARTESIAN_POINT('Ctrl Pts',(0.0411978859975111,2.74638365637749,
7.50349758195598));
#380036=CARTESIAN_POINT('Ctrl Pts',(0.0415332744725173,2.74642192401361,
7.50351950684424));
#380037=CARTESIAN_POINT('Ctrl Pts',(0.0418924680760451,2.74645568442726,
7.50357029184312));
#380038=CARTESIAN_POINT('Ctrl Pts',(0.0422397292057554,2.74647871828665,
7.50365515313923));
#380039=CARTESIAN_POINT('Ctrl Pts',(0.0427739574431695,2.74651415368973,
7.50378570417639));
#380040=CARTESIAN_POINT('Ctrl Pts',(0.0432956039785114,2.74652558920171,
7.50400001621911));
#380041=CARTESIAN_POINT('Ctrl Pts',(0.0437650136951304,2.7465098845443,
7.50428903009635));
#380042=CARTESIAN_POINT('Ctrl Pts',(0.0438171145622515,2.74650814144815,
7.50432110841318));
#380043=CARTESIAN_POINT('Ctrl Pts',(0.04386859742804,2.7465060803685,7.50435406373354));
#380044=CARTESIAN_POINT('Ctrl Pts',(0.0439194270703296,2.7465037088339,
7.50438785222352));
#380045=CARTESIAN_POINT('Ctrl Pts',(0.0442297664683503,2.74648922947526,
7.50459414719561));
#380046=CARTESIAN_POINT('Ctrl Pts',(0.0445206726054137,2.74646243160482,
7.50483629897752));
#380047=CARTESIAN_POINT('Ctrl Pts',(0.0447811216729627,2.74642565232408,
7.5050991045531));
#380048=CARTESIAN_POINT('Ctrl Pts',(0.0453556984756082,2.74634451353664,
7.50567888004914));
#380049=CARTESIAN_POINT('Ctrl Pts',(0.0458047587608243,2.74621211426885,
7.50637912803144));
#380050=CARTESIAN_POINT('Ctrl Pts',(0.0461444808270324,2.74605479234556,
7.50710440483569));
#380051=CARTESIAN_POINT('Ctrl Pts',(0.0462277874220944,2.74601621388668,
7.50728225710685));
#380052=CARTESIAN_POINT('Ctrl Pts',(0.0463062389178228,2.74597550121701,
7.50746498566954));
#380053=CARTESIAN_POINT('Ctrl Pts',(0.0463781958941233,2.74593397446876,
7.50764697238949));
#380054=CARTESIAN_POINT('Ctrl Pts',(0.0467650167956208,2.74571073809862,
7.50862528291182));
#380055=CARTESIAN_POINT('Ctrl Pts',(0.047001339897482,2.74544729614725,
7.50965856837422));
#380056=CARTESIAN_POINT('Ctrl Pts',(0.0471465970325937,2.74517302978349,
7.51067959873202));
#380057=CARTESIAN_POINT('Ctrl Pts',(0.0472265322172639,2.74502210065757,
7.51124147302579));
#380058=CARTESIAN_POINT('Ctrl Pts',(0.0472785253772168,2.74486765340863,
7.51180065547253));
#380059=CARTESIAN_POINT('Ctrl Pts',(0.0473100357766603,2.74471340164584,
7.51235175716501));
#380060=CARTESIAN_POINT('Ctrl Pts',(0.0474189167589901,2.7441804003588,
7.51425603304535));
#380061=CARTESIAN_POINT('Ctrl Pts',(0.0472902783286506,2.74358496893378,
7.51626900505179));
#380062=CARTESIAN_POINT('Ctrl Pts',(0.0469717238008028,2.74296420982058,
7.51827788969242));
#380063=CARTESIAN_POINT('Ctrl Pts',(0.0469544830277703,2.7429306131643,
7.51838661432544));
#380064=CARTESIAN_POINT('Ctrl Pts',(0.0469366766840814,2.74289693867703,
7.51849533314856));
#380065=CARTESIAN_POINT('Ctrl Pts',(0.0469183093502092,2.74286319116668,
7.51860402984325));
#380066=CARTESIAN_POINT('Origin',(0.,9.23979071467924E-16,7.49482233047033));
#380067=CARTESIAN_POINT('Origin',(0.0389852998002483,2.73722238709234,7.49482233047033));
#380068=CARTESIAN_POINT('Ctrl Pts',(-0.00603856833113048,2.66775215476039,
8.85049129520029));
#380069=CARTESIAN_POINT('Ctrl Pts',(-0.00883014741545966,2.67288130658491,
8.85711686593484));
#380070=CARTESIAN_POINT('Ctrl Pts',(-0.0170742924659647,2.67061528926368,
8.85933012996512));
#380071=CARTESIAN_POINT('Ctrl Pts',(-0.0174472646350165,2.68871410270986,
8.82945683644723));
#380072=CARTESIAN_POINT('Ctrl Pts',(-0.0202620155135629,2.69388582959568,
8.8360746990239));
#380073=CARTESIAN_POINT('Ctrl Pts',(-0.0285204257242725,2.69157699801036,
8.8382956714852));
#380074=CARTESIAN_POINT('Ctrl Pts',(-0.0288389553570734,2.70964480518555,
8.80838214965002));
#380075=CARTESIAN_POINT('Ctrl Pts',(-0.0316648145567818,2.71483694212032,
8.81501364461994));
#380076=CARTESIAN_POINT('Ctrl Pts',(-0.0399486090321783,2.71250722933019,
8.81722098428721));
#380077=CARTESIAN_POINT('Ctrl Pts',(-0.04021493265483,2.73054663635347,
8.78727029226991));
#380078=CARTESIAN_POINT('Ctrl Pts',(-0.0430412612390256,2.73573963571921,
8.79393457792714));
#380079=CARTESIAN_POINT('Ctrl Pts',(-0.0513601984344042,2.73340839160553,
8.79610912703474));
#380080=CARTESIAN_POINT('Origin',(-0.0170177834786405,2.66177663513908,
8.85049129520029));
#380081=CARTESIAN_POINT('Ctrl Pts',(0.0391111642587046,2.74605953891717,
7.50366195182966));
#380082=CARTESIAN_POINT('Ctrl Pts',(0.0391633148679688,2.74972111945349,
7.50000065167735));
#380083=CARTESIAN_POINT('Ctrl Pts',(0.0391633148680856,2.74972111945349,
7.49482233047108));
#380084=CARTESIAN_POINT('Ctrl Pts',(0.0464182127131564,2.74745983977445,
7.50215800491337));
#380085=CARTESIAN_POINT('Ctrl Pts',(0.0486957095368234,2.74958532922222,
7.49877273257267));
#380086=CARTESIAN_POINT('Ctrl Pts',(0.0521474832453746,2.74953619049074,
7.49481816995647));
#380087=CARTESIAN_POINT('Ctrl Pts',(0.0482654124422666,2.74533902165334,
7.51043025814041));
#380088=CARTESIAN_POINT('Ctrl Pts',(0.0523537600593804,2.74950773497384,
7.51006209594513));
#380089=CARTESIAN_POINT('Ctrl Pts',(0.0581644280551635,2.74938482197663,
7.50731281821699));
#380090=CARTESIAN_POINT('Ctrl Pts',(0.0469175869148853,2.74286186359761,
7.51860402984325));
#380091=CARTESIAN_POINT('Ctrl Pts',(0.0505543270057753,2.74954580995451,
7.51860402984325));
#380092=CARTESIAN_POINT('Ctrl Pts',(0.0581618967557014,2.74938487552503,
7.51860402984325));
#380093=CARTESIAN_POINT('Origin',(0.0578975244977155,2.73688767154537,7.51860402984325));
#380094=CARTESIAN_POINT('Ctrl Pts',(0.00603856833113047,2.66775215476039,
8.85049129520029));
#380095=CARTESIAN_POINT('Ctrl Pts',(0.00883014741545964,2.67288130658491,
8.85711686593484));
#380096=CARTESIAN_POINT('Ctrl Pts',(0.0170742924659647,2.67061528926368,
8.85933012996512));
#380097=CARTESIAN_POINT('Ctrl Pts',(0.0035688986120927,2.66321446818132,
8.86332496987232));
#380098=CARTESIAN_POINT('Ctrl Pts',(0.00818107962988514,2.66349674576787,
8.86648636486738));
#380099=CARTESIAN_POINT('Ctrl Pts',(0.0101502424853851,2.65792911615186,
8.87206031107457));
#380100=CARTESIAN_POINT('Ctrl Pts',(-0.00355211642776816,2.66318363317047,
8.86341338519876));
#380101=CARTESIAN_POINT('Ctrl Pts',(-0.0081791237408215,2.6634371562646,
8.86654584966058));
#380102=CARTESIAN_POINT('Ctrl Pts',(-0.0100991546002723,2.65783022891655,
8.87215952290714));
#380103=CARTESIAN_POINT('Ctrl Pts',(-0.0060385683311304,2.66775215476039,
8.85049129520029));
#380104=CARTESIAN_POINT('Ctrl Pts',(-0.00883014741545944,2.67288130658491,
8.85711686593484));
#380105=CARTESIAN_POINT('Ctrl Pts',(-0.0170742924659645,2.67061528926368,
8.85933012996512));
#380106=CARTESIAN_POINT('Origin',(0.0170177834786405,2.66177663513908,8.85049129520029));
#380107=CARTESIAN_POINT('Origin',(0.0578975244977156,2.73688767154537,9.));
#380108=CARTESIAN_POINT('Origin',(0.0578975244977156,2.73688767154537,8.75721825406948));
#380109=CARTESIAN_POINT('Ctrl Pts',(0.0402149326548301,2.73054663635347,
8.78727029226991));
#380110=CARTESIAN_POINT('Ctrl Pts',(0.0430412612390258,2.73573963571921,
8.79393457792714));
#380111=CARTESIAN_POINT('Ctrl Pts',(0.0513601984344043,2.73340839160553,
8.79610912703474));
#380112=CARTESIAN_POINT('Ctrl Pts',(0.0288389553570644,2.70964480518553,
8.80838214965001));
#380113=CARTESIAN_POINT('Ctrl Pts',(0.0316648145567926,2.71483694212031,
8.81501364461994));
#380114=CARTESIAN_POINT('Ctrl Pts',(0.0399486090321813,2.71250722933019,
8.81722098428722));
#380115=CARTESIAN_POINT('Ctrl Pts',(0.0174472646350206,2.68871410270986,
8.82945683644722));
#380116=CARTESIAN_POINT('Ctrl Pts',(0.0202620155135602,2.69388582959568,
8.8360746990239));
#380117=CARTESIAN_POINT('Ctrl Pts',(0.0285204257242735,2.69157699801037,
8.83829567148519));
#380118=CARTESIAN_POINT('Ctrl Pts',(0.00603856833113056,2.66775215476039,
8.85049129520029));
#380119=CARTESIAN_POINT('Ctrl Pts',(0.00883014741545973,2.67288130658491,
8.85711686593484));
#380120=CARTESIAN_POINT('Ctrl Pts',(0.0170742924659648,2.67061528926368,
8.85933012996512));
#380121=CARTESIAN_POINT('Origin',(0.05119414780234,2.72457111673216,8.78727029226991));
#380122=CARTESIAN_POINT('Ctrl Pts',(0.0468298108357679,2.74270054843764,
8.75374538247848));
#380123=CARTESIAN_POINT('Ctrl Pts',(0.0504509039511556,2.74938127167972,
8.75304829418601));
#380124=CARTESIAN_POINT('Ctrl Pts',(0.0580822141425596,2.74919756546978,
8.75272238421917));
#380125=CARTESIAN_POINT('Ctrl Pts',(0.0474608175312104,2.7438599394262,
8.7676940844502));
#380126=CARTESIAN_POINT('Ctrl Pts',(0.0511736401317078,2.75070845045484,
8.76974318093969));
#380127=CARTESIAN_POINT('Ctrl Pts',(0.0587246898268686,2.7507060460072,
8.77077869880429));
#380128=CARTESIAN_POINT('Ctrl Pts',(0.0442266366581527,2.73791756168736,
8.78108014887991));
#380129=CARTESIAN_POINT('Ctrl Pts',(0.0473697799404577,2.74372323887499,
8.78639403366324));
#380130=CARTESIAN_POINT('Ctrl Pts',(0.0554304751827418,2.74298346327396,
8.78812224174742));
#380131=CARTESIAN_POINT('Ctrl Pts',(0.0389265281907873,2.72817931634984,
8.78944554828685));
#380132=CARTESIAN_POINT('Ctrl Pts',(0.041570530208704,2.73307479088723,
8.79673892988686));
#380133=CARTESIAN_POINT('Ctrl Pts',(0.0500624819120103,2.73035627831871,
8.79894799272499));
#380134=CARTESIAN_POINT('Origin',(-0.16489730596466,2.66265786424426,7.5));
#380135=CARTESIAN_POINT('',(-0.16489730596466,2.66265786424426,7.59394543036555));
#380136=CARTESIAN_POINT('',(-0.16489730596466,2.66265786424426,8.85049129520029));
#380137=CARTESIAN_POINT('',(-0.16489730596466,2.66265786424426,7.5));
#380138=CARTESIAN_POINT('',(-0.13481441689611,2.72751301502058,8.78727029226991));
#380139=CARTESIAN_POINT('Ctrl Pts',(-0.16489730596466,2.66265786424426,
8.85049129520029));
#380140=CARTESIAN_POINT('Ctrl Pts',(-0.154855100144266,2.68430767225054,
8.82945686509571));
#380141=CARTESIAN_POINT('Ctrl Pts',(-0.144827823277113,2.70592529519936,
8.80838212259895));
#380142=CARTESIAN_POINT('Ctrl Pts',(-0.13481441689611,2.72751301502058,
8.78727029226991));
#380143=CARTESIAN_POINT('',(-0.128913937383377,2.74023375097047,8.75721825406948));
#380144=CARTESIAN_POINT('Origin',(-0.146670710194622,2.70195272855935,8.75937679713156));
#380145=CARTESIAN_POINT('',(-0.128913937383377,2.74023375097047,7.51860402984325));
#380146=CARTESIAN_POINT('',(-0.128913937383377,2.74023375097047,7.5));
#380147=CARTESIAN_POINT('Ctrl Pts',(-0.128913937383377,2.74023375097047,
7.51860402984325));
#380148=CARTESIAN_POINT('Ctrl Pts',(-0.133547846342482,2.73024359133049,
7.52834476460825));
#380149=CARTESIAN_POINT('Ctrl Pts',(-0.138184763568422,2.72024694622305,
7.53807742314407));
#380150=CARTESIAN_POINT('Ctrl Pts',(-0.142824790067749,2.71024359788991,
7.54780169004674));
#380151=CARTESIAN_POINT('Ctrl Pts',(-0.150174341270648,2.69439883476507,
7.5632044032688));
#380152=CARTESIAN_POINT('Ctrl Pts',(-0.157531702584656,2.67853723396437,
7.57858609112103));
#380153=CARTESIAN_POINT('Ctrl Pts',(-0.16489730596466,2.66265786424426,
7.59394543036555));
#380154=CARTESIAN_POINT('Origin',(-0.323616654966455,2.89450777438995,7.5));
#380155=CARTESIAN_POINT('',(-0.222557758686723,2.73422161816809,8.75721825406948));
#380156=CARTESIAN_POINT('',(-0.215079030421415,2.72235985585717,8.78727029226991));
#380157=CARTESIAN_POINT('Origin',(-0.196095228656818,2.69225027889422,8.75658640621001));
#380158=CARTESIAN_POINT('',(-0.176949628854379,2.66188407944157,8.85049129520029));
#380159=CARTESIAN_POINT('Ctrl Pts',(-0.215079030421415,2.72235985585717,
8.78727029226991));
#380160=CARTESIAN_POINT('Ctrl Pts',(-0.202387257630408,2.70222985690407,
8.80838212259895));
#380161=CARTESIAN_POINT('Ctrl Pts',(-0.189677904302661,2.68207197404603,
8.82945686509571));
#380162=CARTESIAN_POINT('Ctrl Pts',(-0.176949628854379,2.66188407944157,
8.85049129520029));
#380163=CARTESIAN_POINT('',(-0.176949628854379,2.66188407944157,7.59394543036555));
#380164=CARTESIAN_POINT('',(-0.176949628854379,2.66188407944157,7.5));
#380165=CARTESIAN_POINT('',(-0.222557758686723,2.73422161816809,7.51860402984325));
#380166=CARTESIAN_POINT('Ctrl Pts',(-0.176949628854379,2.66188407944157,
7.59394543036555));
#380167=CARTESIAN_POINT('Ctrl Pts',(-0.186285369461595,2.67669118730146,
7.57858609112103));
#380168=CARTESIAN_POINT('Ctrl Pts',(-0.195610663430972,2.69148172609634,
7.56320440326857));
#380169=CARTESIAN_POINT('Ctrl Pts',(-0.204926058256057,2.70625656418747,
7.54780169004651));
#380170=CARTESIAN_POINT('Ctrl Pts',(-0.210807189994148,2.71558443175019,
7.53807742314383));
#380171=CARTESIAN_POINT('Ctrl Pts',(-0.216684380796579,2.72490604872585,
7.52834476460825));
#380172=CARTESIAN_POINT('Ctrl Pts',(-0.222557758686721,2.73422161816808,
7.51860402984324));
#380173=CARTESIAN_POINT('',(-0.222557758686723,2.73422161816809,7.5));
#380174=CARTESIAN_POINT('Origin',(-0.17113403648067,2.66555075509437,7.5));
#380175=CARTESIAN_POINT('Ctrl Pts',(-0.176949628854379,2.66188407944157,
8.85049129520029));
#380176=CARTESIAN_POINT('Ctrl Pts',(-0.176846342464761,2.6617202603322,
8.85097269580138));
#380177=CARTESIAN_POINT('Ctrl Pts',(-0.176737243973737,2.66156299420173,
8.85143669361005));
#380178=CARTESIAN_POINT('Ctrl Pts',(-0.176616591392395,2.66140553779028,
8.8519052845931));
#380179=CARTESIAN_POINT('Ctrl Pts',(-0.1763806025948,2.66109756303501,8.85282181883899));
#380180=CARTESIAN_POINT('Ctrl Pts',(-0.176106325903489,2.66079690254988,
8.85372622499636));
#380181=CARTESIAN_POINT('Ctrl Pts',(-0.175778066416341,2.66050922989146,
8.85462257735071));
#380182=CARTESIAN_POINT('Ctrl Pts',(-0.175505557048785,2.6602704142676,
8.85536669723986));
#380183=CARTESIAN_POINT('Ctrl Pts',(-0.175195802884907,2.66004047128033,
8.85610498449051));
#380184=CARTESIAN_POINT('Ctrl Pts',(-0.174835028063543,2.65982905303466,
8.85681338218371));
#380185=CARTESIAN_POINT('Ctrl Pts',(-0.174507624346547,2.65963719064467,
8.85745625420284));
#380186=CARTESIAN_POINT('Ctrl Pts',(-0.174134397753541,2.65945766139716,
8.85808743050666));
#380187=CARTESIAN_POINT('Ctrl Pts',(-0.173693040886597,2.65930836015582,
8.8586680450841));
#380188=CARTESIAN_POINT('Ctrl Pts',(-0.17348940839563,2.65923947579952,
8.85893592806395));
#380189=CARTESIAN_POINT('Ctrl Pts',(-0.17327110340926,2.65917719921061,
8.85919241173848));
#380190=CARTESIAN_POINT('Ctrl Pts',(-0.173034988239252,2.65912457290272,
8.85943017985534));
#380191=CARTESIAN_POINT('Ctrl Pts',(-0.172716162862172,2.65905351180801,
8.8597512372));
#380192=CARTESIAN_POINT('Ctrl Pts',(-0.172356609902529,2.65899886258521,
8.86004599534706));
#380193=CARTESIAN_POINT('Ctrl Pts',(-0.171959084215928,2.65897157865952,
8.86026130871721));
#380194=CARTESIAN_POINT('Ctrl Pts',(-0.171813538854627,2.65896158924511,
8.86034014101235));
#380195=CARTESIAN_POINT('Ctrl Pts',(-0.171660717848717,2.65895510579684,
8.86040910639693));
#380196=CARTESIAN_POINT('Ctrl Pts',(-0.171504770462638,2.65895264102899,
8.86046313645507));
#380197=CARTESIAN_POINT('Ctrl Pts',(-0.171261415872711,2.6589487947794,
8.8605474499083));
#380198=CARTESIAN_POINT('Ctrl Pts',(-0.171003802956377,2.65895477658666,
8.86059655985669));
#380199=CARTESIAN_POINT('Ctrl Pts',(-0.170748446413557,2.65896990994078,
8.86059725258816));
#380200=CARTESIAN_POINT('Ctrl Pts',(-0.170492499895108,2.658985078259,8.86059794692011));
#380201=CARTESIAN_POINT('Ctrl Pts',(-0.170236138887563,2.65901226079576,
8.86056369958366));
#380202=CARTESIAN_POINT('Ctrl Pts',(-0.169992948659137,2.65904623288096,
8.86048590497774));
#380203=CARTESIAN_POINT('Ctrl Pts',(-0.169929483250163,2.65905509858373,
8.86046560290182));
#380204=CARTESIAN_POINT('Ctrl Pts',(-0.169866101725982,2.65906463173742,
8.86044257503091));
#380205=CARTESIAN_POINT('Ctrl Pts',(-0.169804757745728,2.65907450529864,
8.86041778462583));
#380206=CARTESIAN_POINT('Ctrl Pts',(-0.169391988880148,2.65914094211361,
8.86025097596201));
#380207=CARTESIAN_POINT('Ctrl Pts',(-0.169016136888504,2.65923203389475,
8.8599848982295));
#380208=CARTESIAN_POINT('Ctrl Pts',(-0.168686176277915,2.65933688780355,
8.85968173251461));
#380209=CARTESIAN_POINT('Ctrl Pts',(-0.168511646019403,2.65939234951389,
8.85952137522076));
#380210=CARTESIAN_POINT('Ctrl Pts',(-0.168346533239064,2.65945254867042,
8.85934740853961));
#380211=CARTESIAN_POINT('Ctrl Pts',(-0.16819263389931,2.65951517582375,
8.8591675900182));
#380212=CARTESIAN_POINT('Ctrl Pts',(-0.16757464805491,2.65976665639733,
8.85844552518695));
#380213=CARTESIAN_POINT('Ctrl Pts',(-0.167101404538683,2.66006869733527,
8.85759444184124));
#380214=CARTESIAN_POINT('Ctrl Pts',(-0.166737667185756,2.66034962329277,
8.85683498915138));
#380215=CARTESIAN_POINT('Ctrl Pts',(-0.166699603040485,2.66037902144606,
8.85675551444998));
#380216=CARTESIAN_POINT('Ctrl Pts',(-0.166662753168069,2.66040820147624,
8.85667699793651));
#380217=CARTESIAN_POINT('Ctrl Pts',(-0.166627087527507,2.66043708934255,
8.85659965593547));
#380218=CARTESIAN_POINT('Ctrl Pts',(-0.166145670891262,2.66082701923615,
8.85555568965886));
#380219=CARTESIAN_POINT('Ctrl Pts',(-0.165739313269825,2.66127129211021,
8.85434650606346));
#380220=CARTESIAN_POINT('Ctrl Pts',(-0.165401420054749,2.66176790975638,
8.85297329937117));
#380221=CARTESIAN_POINT('Ctrl Pts',(-0.165211375709405,2.66204722692299,
8.85220095427747));
#380222=CARTESIAN_POINT('Ctrl Pts',(-0.165043172113059,2.66234339408063,
8.85137579139183));
#380223=CARTESIAN_POINT('Ctrl Pts',(-0.16489730596466,2.66265786424426,
8.85049129520029));
#380224=CARTESIAN_POINT('Origin',(-0.171134036480669,2.66555075509437,7.59394543036555));
#380225=CARTESIAN_POINT('Ctrl Pts',(-0.176649753621982,2.66140845730323,
7.59443877723642));
#380226=CARTESIAN_POINT('Ctrl Pts',(-0.173561327260499,2.65651000690965,
7.58783886950016));
#380227=CARTESIAN_POINT('Ctrl Pts',(-0.165526833445772,2.65925337904586,
7.58559994247159));
#380228=CARTESIAN_POINT('Ctrl Pts',(-0.193509382518731,2.68814895428735,
7.56670252222133));
#380229=CARTESIAN_POINT('Ctrl Pts',(-0.190425419810154,2.68325758354529,
7.56004874999026));
#380230=CARTESIAN_POINT('Ctrl Pts',(-0.18233641492009,2.68599699171951,
7.55786368756704));
#380231=CARTESIAN_POINT('Ctrl Pts',(-0.210337527743017,2.71483951606509,
7.53888913333558));
#380232=CARTESIAN_POINT('Ctrl Pts',(-0.207235236893081,2.70991907566721,
7.53222002137277));
#380233=CARTESIAN_POINT('Ctrl Pts',(-0.199116189248093,2.7126909901786,
7.53005029815326));
#380234=CARTESIAN_POINT('Ctrl Pts',(-0.227133427809856,2.74147893487042,
7.51101258149734));
#380235=CARTESIAN_POINT('Ctrl Pts',(-0.223993531557809,2.73649884979426,
7.5043616886572));
#380236=CARTESIAN_POINT('Ctrl Pts',(-0.215865257414837,2.73933409951895,
7.50217374673251));
#380237=CARTESIAN_POINT('',(-0.214971506492209,2.73791238843283,7.50366116523517));
#380238=CARTESIAN_POINT('Ctrl Pts',(-0.222557758686723,2.73422161816808,
7.51860402984325));
#380239=CARTESIAN_POINT('Ctrl Pts',(-0.222793285245618,2.73459517901432,
7.51734760759493));
#380240=CARTESIAN_POINT('Ctrl Pts',(-0.222955788562301,2.7349644763634,
7.51608817408572));
#380241=CARTESIAN_POINT('Ctrl Pts',(-0.223032672233694,2.73533403919153,
7.51481005913119));
#380242=CARTESIAN_POINT('Ctrl Pts',(-0.223102315300436,2.73566879803223,
7.51365231206383));
#380243=CARTESIAN_POINT('Ctrl Pts',(-0.223102049090854,2.73600419561941,
7.51247773061042));
#380244=CARTESIAN_POINT('Ctrl Pts',(-0.222994953185447,2.736334399064,7.51129758471022));
#380245=CARTESIAN_POINT('Ctrl Pts',(-0.222861845205841,2.73674480423496,
7.50983079813402));
#380246=CARTESIAN_POINT('Ctrl Pts',(-0.222555569253571,2.73713006948336,
7.50839324291155));
#380247=CARTESIAN_POINT('Ctrl Pts',(-0.222009357599783,2.73744170500765,
7.50715379678855));
#380248=CARTESIAN_POINT('Ctrl Pts',(-0.221757023554444,2.73758567164031,
7.50658120839351));
#380249=CARTESIAN_POINT('Ctrl Pts',(-0.221412902846589,2.73772613760701,
7.50598221009429));
#380250=CARTESIAN_POINT('Ctrl Pts',(-0.220976588784301,2.73783870041343,
7.50545747549611));
#380251=CARTESIAN_POINT('Ctrl Pts',(-0.220743758095481,2.73789876741109,
7.50517746087247));
#380252=CARTESIAN_POINT('Ctrl Pts',(-0.220482200112806,2.73795173606974,
7.50491486231392));
#380253=CARTESIAN_POINT('Ctrl Pts',(-0.220198510259498,2.73799456886009,
7.50468370960992));
#380254=CARTESIAN_POINT('Ctrl Pts',(-0.219774304443913,2.7380586173925,
7.50433806340446));
#380255=CARTESIAN_POINT('Ctrl Pts',(-0.219287809037159,2.73810137257825,
7.50405484070984));
#380256=CARTESIAN_POINT('Ctrl Pts',(-0.218771725882347,2.73811924129067,
7.50385766036131));
#380257=CARTESIAN_POINT('Ctrl Pts',(-0.218716538810688,2.73812115207172,
7.50383657498791));
#380258=CARTESIAN_POINT('Ctrl Pts',(-0.218661038309179,2.73812279184612,
7.50381643264937));
#380259=CARTESIAN_POINT('Ctrl Pts',(-0.218605282305324,2.73812416636047,
7.50379723213559));
#380260=CARTESIAN_POINT('Ctrl Pts',(-0.218233092740536,2.73813334169338,
7.50366906242519));
#380261=CARTESIAN_POINT('Ctrl Pts',(-0.217841404285933,2.73813017779315,
7.50358235568538));
#380262=CARTESIAN_POINT('Ctrl Pts',(-0.217463938128411,2.73811805291127,
7.5035341175365));
#380263=CARTESIAN_POINT('Ctrl Pts',(-0.216897970346127,2.73809987302315,
7.50346178989176));
#380264=CARTESIAN_POINT('Ctrl Pts',(-0.216289890791823,2.7380562513047,
7.50346967198527));
#380265=CARTESIAN_POINT('Ctrl Pts',(-0.215694262731964,2.73799506025502,
7.50354272648692));
#380266=CARTESIAN_POINT('Ctrl Pts',(-0.215449268582172,2.7379698911097,
7.50357277531559));
#380267=CARTESIAN_POINT('Ctrl Pts',(-0.215206692060793,2.73794192399818,
7.50361331098761));
#380268=CARTESIAN_POINT('Ctrl Pts',(-0.21497150649232,2.73791238843424,
7.50366116523659));
#380269=CARTESIAN_POINT('',(-0.171321629291009,2.66847266454068,7.57603338622103));
#380270=CARTESIAN_POINT('Origin',(-0.171884966568795,2.677291629373,7.58486873427628));
#380271=CARTESIAN_POINT('Ctrl Pts',(-0.214971506527132,2.73791238847831,
7.50366116529969));
#380272=CARTESIAN_POINT('Ctrl Pts',(-0.200444582347927,2.71480402911006,
7.52783573079709));
#380273=CARTESIAN_POINT('Ctrl Pts',(-0.185895295086754,2.69165855688567,
7.55196141284068));
#380274=CARTESIAN_POINT('Ctrl Pts',(-0.171321630229604,2.66847266536934,
7.57603338728831));
#380275=CARTESIAN_POINT('Ctrl Pts',(-0.177349390934668,2.662847783649,7.59639677331371));
#380276=CARTESIAN_POINT('Ctrl Pts',(-0.170168085926414,2.64604002430609,
7.59959882295466));
#380277=CARTESIAN_POINT('Ctrl Pts',(-0.16467589448117,2.66349123187844,
7.59642833564546));
#380278=CARTESIAN_POINT('Ctrl Pts',(-0.176413316036416,2.65906111388935,
7.58707626057422));
#380279=CARTESIAN_POINT('Ctrl Pts',(-0.170591808819725,2.65559378858556,
7.58809943920599));
#380280=CARTESIAN_POINT('Ctrl Pts',(-0.165206893457788,2.65968244207271,
7.58710240504253));
#380281=CARTESIAN_POINT('Ctrl Pts',(-0.173206625605347,2.66422277725894,
7.5801537675693));
#380282=CARTESIAN_POINT('Ctrl Pts',(-0.170967584492428,2.66245756727403,
7.58205880659761));
#380283=CARTESIAN_POINT('Ctrl Pts',(-0.168967669707232,2.66443933817145,
7.58020924244127));
#380284=CARTESIAN_POINT('Ctrl Pts',(-0.171321629238191,2.66847266371479,
7.57603338509286));
#380285=CARTESIAN_POINT('Ctrl Pts',(-0.171321629238191,2.66847266371479,
7.57603338509286));
#380286=CARTESIAN_POINT('Ctrl Pts',(-0.171321629238191,2.6684726637148,
7.57603338509286));
#380287=CARTESIAN_POINT('Origin',(-0.171890661196598,2.67729126376561,7.58486873427622));
#380288=CARTESIAN_POINT('Ctrl Pts',(-0.125292469645935,2.74804120708308,
7.51098857897448));
#380289=CARTESIAN_POINT('Ctrl Pts',(-0.127769759546158,2.74270046305981,
7.50433767179957));
#380290=CARTESIAN_POINT('Ctrl Pts',(-0.1361938934592,2.74447303714785,7.50214974420965));
#380291=CARTESIAN_POINT('Ctrl Pts',(-0.138547713792453,2.71946446846797,
7.53887321589168));
#380292=CARTESIAN_POINT('Ctrl Pts',(-0.140995321363277,2.71418771603619,
7.5322040745206));
#380293=CARTESIAN_POINT('Ctrl Pts',(-0.149402205571103,2.71589862744196,
7.53003438070911));
#380294=CARTESIAN_POINT('Ctrl Pts',(-0.151828412897386,2.6908328519732,
7.56669465659235));
#380295=CARTESIAN_POINT('Ctrl Pts',(-0.154261555562458,2.68558728416726,
7.56004085833303));
#380296=CARTESIAN_POINT('Ctrl Pts',(-0.162634477916442,2.68726978866384,
7.55785582193789));
#380297=CARTESIAN_POINT('Ctrl Pts',(-0.165133966327888,2.66214765249215,
7.59443891967696));
#380298=CARTESIAN_POINT('Ctrl Pts',(-0.167570636746948,2.656894479266,7.58783901202978));
#380299=CARTESIAN_POINT('Ctrl Pts',(-0.17588998193549,2.65858789995271,
7.58560008491213));
#380300=CARTESIAN_POINT('',(-0.136909871778125,2.74292411166389,7.50366116523517));
#380301=CARTESIAN_POINT('Ctrl Pts',(-0.136909871778144,2.74292411166427,
7.50366116523554));
#380302=CARTESIAN_POINT('Ctrl Pts',(-0.136176261638576,2.74311372622038,
7.50350835821027));
#380303=CARTESIAN_POINT('Ctrl Pts',(-0.135495726955387,2.74326416077797,
7.50345484956));
#380304=CARTESIAN_POINT('Ctrl Pts',(-0.134848164493271,2.74338047422534,
7.50349758195598));
#380305=CARTESIAN_POINT('Ctrl Pts',(-0.134515916925721,2.74344015164987,
7.50351950684424));
#380306=CARTESIAN_POINT('Ctrl Pts',(-0.134159624361105,2.74349685631232,
7.50357029184312));
#380307=CARTESIAN_POINT('Ctrl Pts',(-0.133814552501067,2.74354209194315,
7.50365515313923));
#380308=CARTESIAN_POINT('Ctrl Pts',(-0.133283692246939,2.74361168266108,
7.50378570417639));
#380309=CARTESIAN_POINT('Ctrl Pts',(-0.132763850166124,2.74365651668585,
7.50400001621911));
#380310=CARTESIAN_POINT('Ctrl Pts',(-0.132294398701261,2.74367091947915,
7.50428903009634));
#380311=CARTESIAN_POINT('Ctrl Pts',(-0.1322422932004,2.74367251807839,7.50432110841318));
#380312=CARTESIAN_POINT('Ctrl Pts',(-0.132190784057849,2.74367375975199,
7.50435406373354));
#380313=CARTESIAN_POINT('Ctrl Pts',(-0.132139906905762,2.74367464975632,
7.50438785222352));
#380314=CARTESIAN_POINT('Ctrl Pts',(-0.131829277437625,2.74368008366058,
7.50459414719561));
#380315=CARTESIAN_POINT('Ctrl Pts',(-0.131537252052967,2.74367197926943,
7.50483629897752));
#380316=CARTESIAN_POINT('Ctrl Pts',(-0.131274981649352,2.74365196258472,
7.5050991045531));
#380317=CARTESIAN_POINT('Ctrl Pts',(-0.130696386796411,2.74360780376776,
7.50567888004914));
#380318=CARTESIAN_POINT('Ctrl Pts',(-0.130239766303498,2.74350444791973,
7.50637912803145));
#380319=CARTESIAN_POINT('Ctrl Pts',(-0.129890662582477,2.74336921529871,
7.50710440483569));
#380320=CARTESIAN_POINT('Ctrl Pts',(-0.129805055419403,2.74333605357529,
7.50728225710685));
#380321=CARTESIAN_POINT('Ctrl Pts',(-0.129724156640984,2.74330045095875,
7.50746498566955));
#380322=CARTESIAN_POINT('Ctrl Pts',(-0.129649686880113,2.74326361983096,
7.50764697238949));
#380323=CARTESIAN_POINT('Ctrl Pts',(-0.129249357940303,2.74306562582414,
7.50862528291182));
#380324=CARTESIAN_POINT('Ctrl Pts',(-0.128996641605824,2.74281786641564,
7.50965856837422));
#380325=CARTESIAN_POINT('Ctrl Pts',(-0.128834110610815,2.74255347021813,
7.51067959873202));
#380326=CARTESIAN_POINT('Ctrl Pts',(-0.128744669599255,2.74240797265715,
7.51124147302578));
#380327=CARTESIAN_POINT('Ctrl Pts',(-0.128682887795611,2.74225717394985,
7.51180065547253));
#380328=CARTESIAN_POINT('Ctrl Pts',(-0.128641559193288,2.74210525799208,
7.51235175716501));
#380329=CARTESIAN_POINT('Ctrl Pts',(-0.128498752408904,2.74158032784183,
7.51425603304536));
#380330=CARTESIAN_POINT('Ctrl Pts',(-0.128588977115408,2.74097787790201,
7.5162690050518));
#380331=CARTESIAN_POINT('Ctrl Pts',(-0.128867104965876,2.7403379843463,
7.51827788969243));
#380332=CARTESIAN_POINT('Ctrl Pts',(-0.128882157770732,2.74030335209784,
7.51838661432545));
#380333=CARTESIAN_POINT('Ctrl Pts',(-0.128897769997571,2.74026860594206,
7.51849533314856));
#380334=CARTESIAN_POINT('Ctrl Pts',(-0.128913937383373,2.74023375097047,
7.51860402984325));
#380335=CARTESIAN_POINT('Ctrl Pts',(-0.171321628465918,2.66847266548377,
7.57603338728985));
#380336=CARTESIAN_POINT('Ctrl Pts',(-0.159832559191475,2.69333184005413,
7.55196141284922));
#380337=CARTESIAN_POINT('Ctrl Pts',(-0.148362498662232,2.71814780985154,
7.52783573083104));
#380338=CARTESIAN_POINT('Ctrl Pts',(-0.136909871748466,2.74292411171511,
7.50366116530176));
#380339=CARTESIAN_POINT('Origin',(-5.91995423665249E-17,9.22080657369149E-16,
7.49482233047033));
#380340=CARTESIAN_POINT('Origin',(-0.214279640797787,2.72910067339766,7.49482233047033));
#380341=CARTESIAN_POINT('Origin',(0.,0.,7.50366116523517));
#380342=CARTESIAN_POINT('Origin',(-0.13646924015649,2.7340962668661,7.49482233047033));
#380343=CARTESIAN_POINT('Ctrl Pts',(-0.222557194605718,2.73422072341404,
7.51860402984325));
#380344=CARTESIAN_POINT('Ctrl Pts',(-0.226614772381148,2.74065751987086,
7.51860402984325));
#380345=CARTESIAN_POINT('Ctrl Pts',(-0.234196090687502,2.74000952390803,
7.51860402984325));
#380346=CARTESIAN_POINT('Ctrl Pts',(-0.224063801999056,2.73661074918781,
7.51041458714366));
#380347=CARTESIAN_POINT('Ctrl Pts',(-0.228410872679949,2.74050399234172,
7.51004642900444));
#380348=CARTESIAN_POINT('Ctrl Pts',(-0.234198181525068,2.74000934519844,
7.50729136483011));
#380349=CARTESIAN_POINT('Ctrl Pts',(-0.22234652916969,2.73884115525596,
7.50215815450137));
#380350=CARTESIAN_POINT('Ctrl Pts',(-0.224753845205969,2.74081672959849,
7.49877163671527));
#380351=CARTESIAN_POINT('Ctrl Pts',(-0.228193466700913,2.74054667855528,
7.49481588533168));
#380352=CARTESIAN_POINT('Ctrl Pts',(-0.21497146339957,2.73791183960396,
7.50366171572174));
#380353=CARTESIAN_POINT('Ctrl Pts',(-0.215258086645794,2.74156232030819,
7.50000045605858));
#380354=CARTESIAN_POINT('Ctrl Pts',(-0.215258086645918,2.74156232030818,
7.49482233047317));
#380355=CARTESIAN_POINT('Origin',(-0.233131563002558,2.72755493516299,7.51860402984325));
#380356=CARTESIAN_POINT('Origin',(-0.233131563002558,2.72755493516299,9.));
#380357=CARTESIAN_POINT('Origin',(-0.233131563002558,2.72755493516299,8.75721825406948));
#380358=CARTESIAN_POINT('Ctrl Pts',(-0.213651009822412,2.72009486320776,
8.78942910404912));
#380359=CARTESIAN_POINT('Ctrl Pts',(-0.21660588741381,2.7248193872178,8.7967269950169));
#380360=CARTESIAN_POINT('Ctrl Pts',(-0.22491413159172,2.72155647982373,
8.79893251111266));
#380361=CARTESIAN_POINT('Ctrl Pts',(-0.219514666098731,2.7293950220136,
8.78111911759582));
#380362=CARTESIAN_POINT('Ctrl Pts',(-0.223024018852928,2.73499205277751,
8.78644465894816));
#380363=CARTESIAN_POINT('Ctrl Pts',(-0.231029453604107,2.73371591555135,
8.78817647674133));
#380364=CARTESIAN_POINT('Ctrl Pts',(-0.223169036578443,2.73519110279414,
8.76780923932031));
#380365=CARTESIAN_POINT('Ctrl Pts',(-0.227315996657256,2.74179545430471,
8.76988516158372));
#380366=CARTESIAN_POINT('Ctrl Pts',(-0.23485896000775,2.74130547033627,
8.77093053738832));
#380367=CARTESIAN_POINT('Ctrl Pts',(-0.222456484349946,2.73406094636595,
8.75371302330492));
#380368=CARTESIAN_POINT('Ctrl Pts',(-0.226501019435791,2.74050361175437,
8.7530082828756));
#380369=CARTESIAN_POINT('Ctrl Pts',(-0.23411245922323,2.73982499279172,
8.75267964240738));
#380370=CARTESIAN_POINT('Origin',(-0.225652834737251,2.71569317285207,8.78727029226991));
#380371=CARTESIAN_POINT('Ctrl Pts',(-0.176949628854379,2.66188407944157,
8.85049129520029));
#380372=CARTESIAN_POINT('Ctrl Pts',(-0.180064098225795,2.66682383578754,
8.85711686593484));
#380373=CARTESIAN_POINT('Ctrl Pts',(-0.188146120567861,2.66403427005499,
8.85933012996512));
#380374=CARTESIAN_POINT('Ctrl Pts',(-0.18967792138448,2.68207200113893,
8.82945683644722));
#380375=CARTESIAN_POINT('Ctrl Pts',(-0.192818242734717,2.68705276044922,
8.83607469902389));
#380376=CARTESIAN_POINT('Ctrl Pts',(-0.200911757808369,2.68421955444711,
8.8382956714852));
#380377=CARTESIAN_POINT('Ctrl Pts',(-0.202387241368152,2.70222983111105,
8.80838214965002));
#380378=CARTESIAN_POINT('Ctrl Pts',(-0.205539955892616,2.70723024682303,
8.81501364461987));
#380379=CARTESIAN_POINT('Ctrl Pts',(-0.213657465212923,2.70437457614343,
8.81722098428721));
#380380=CARTESIAN_POINT('Ctrl Pts',(-0.215079030421415,2.72235985585717,
8.78727029226991));
#380381=CARTESIAN_POINT('Ctrl Pts',(-0.218232268622135,2.72736110215464,
8.79393457792714));
#380382=CARTESIAN_POINT('Ctrl Pts',(-0.22638475034565,2.7245016516959,8.79610912703474));
#380383=CARTESIAN_POINT('Origin',(-0.187523433170215,2.65521739643647,8.85049129520029));
#380384=CARTESIAN_POINT('Ctrl Pts',(-0.16489730596466,2.66265786424426,
8.85049129520029));
#380385=CARTESIAN_POINT('Ctrl Pts',(-0.162440088364667,2.66795533476228,
8.85711686593484));
#380386=CARTESIAN_POINT('Ctrl Pts',(-0.154067697566098,2.66622217740361,
8.85933012996512));
#380387=CARTESIAN_POINT('Ctrl Pts',(-0.167071170905058,2.65797126854676,
8.86332496987231));
#380388=CARTESIAN_POINT('Ctrl Pts',(-0.162486551694886,2.65854846961614,
8.86648636486737));
#380389=CARTESIAN_POINT('Ctrl Pts',(-0.160164715441403,2.65311844398962,
8.87206031107457));
#380390=CARTESIAN_POINT('Ctrl Pts',(-0.174175579449871,2.65748425188965,
8.86341338519877));
#380391=CARTESIAN_POINT('Ctrl Pts',(-0.178809323360565,2.65744080071697,
8.86654584966058));
#380392=CARTESIAN_POINT('Ctrl Pts',(-0.180366172242092,2.65172237660299,
8.87215952290714));
#380393=CARTESIAN_POINT('Ctrl Pts',(-0.176949628854379,2.66188407944157,
8.85049129520029));
#380394=CARTESIAN_POINT('Ctrl Pts',(-0.180064098225795,2.66682383578754,
8.85711686593484));
#380395=CARTESIAN_POINT('Ctrl Pts',(-0.188146120567861,2.66403427005499,
8.85933012996512));
#380396=CARTESIAN_POINT('Origin',(-0.153557795935551,2.6573980626986,8.85049129520029));
#380397=CARTESIAN_POINT('Ctrl Pts',(-0.13481441689611,2.72751301502058,
8.78727029226991));
#380398=CARTESIAN_POINT('Ctrl Pts',(-0.132326611918836,2.7328764283063,
8.79393457792714));
#380399=CARTESIAN_POINT('Ctrl Pts',(-0.123875403548937,2.73108297011979,
8.79610912703474));
#380400=CARTESIAN_POINT('Ctrl Pts',(-0.144827836107518,2.70592526753853,
8.80838214965002));
#380401=CARTESIAN_POINT('Ctrl Pts',(-0.142340444294179,2.71128779009166,
8.81501364461991));
#380402=CARTESIAN_POINT('Ctrl Pts',(-0.133924404552004,2.70949360848066,
8.81722098428721));
#380403=CARTESIAN_POINT('Ctrl Pts',(-0.154855086667246,2.6843077013054,
8.82945683644723));
#380404=CARTESIAN_POINT('Ctrl Pts',(-0.152377472675517,2.68964914403163,
8.8360746990239));
#380405=CARTESIAN_POINT('Ctrl Pts',(-0.143988102906735,2.68787417434732,
8.8382956714852));
#380406=CARTESIAN_POINT('Ctrl Pts',(-0.16489730596466,2.66265786424426,
8.85049129520029));
#380407=CARTESIAN_POINT('Ctrl Pts',(-0.162440088364667,2.66795533476228,
8.85711686593484));
#380408=CARTESIAN_POINT('Ctrl Pts',(-0.154067697566098,2.66622217740361,
8.85933012996512));
#380409=CARTESIAN_POINT('Origin',(-0.123474906867001,2.72225321347492,8.78727029226991));
#380410=CARTESIAN_POINT('Ctrl Pts',(-0.128991833512702,2.74006577228906,
8.75374538247847));
#380411=CARTESIAN_POINT('Ctrl Pts',(-0.125806215729227,2.74696477350121,
8.75304829418601));
#380412=CARTESIAN_POINT('Ctrl Pts',(-0.118178814785787,2.74727038445809,
8.75272238421917));
#380413=CARTESIAN_POINT('Ctrl Pts',(-0.128436405723859,2.7412632099223,
8.76769408445022));
#380414=CARTESIAN_POINT('Ctrl Pts',(-0.125169997123756,2.74833553131128,
8.7697431809397));
#380415=CARTESIAN_POINT('Ctrl Pts',(-0.117634307816532,2.74881692921888,
8.7707786988043));
#380416=CARTESIAN_POINT('Ctrl Pts',(-0.131283212176532,2.73512582675581,
8.78108014887987));
#380417=CARTESIAN_POINT('Ctrl Pts',(-0.128518497833744,2.74112095743854,
8.78639403366324));
#380418=CARTESIAN_POINT('Ctrl Pts',(-0.120426966568854,2.74089915230321,
8.78812224174741));
#380419=CARTESIAN_POINT('Ctrl Pts',(-0.135948499481602,2.72506801057236,
8.78944554828685));
#380420=CARTESIAN_POINT('Ctrl Pts',(-0.133623583979923,2.7301228286232,
8.79673892988686));
#380421=CARTESIAN_POINT('Ctrl Pts',(-0.12497490420386,2.72795398274399,
8.79894799272499));
#380422=CARTESIAN_POINT('Origin',(-0.117574427354269,2.73497394942481,8.75721825406948));
#380423=CARTESIAN_POINT('Origin',(-0.117574427354269,2.73497394942481,9.));
#380424=CARTESIAN_POINT('Origin',(-0.117574427354269,2.73497394942481,7.51860402984325));
#380425=CARTESIAN_POINT('Ctrl Pts',(-0.136909832561483,2.74292332597826,
7.50366195182966));
#380426=CARTESIAN_POINT('Ctrl Pts',(-0.137092387371678,2.74658072470567,
7.50000065167735));
#380427=CARTESIAN_POINT('Ctrl Pts',(-0.137092387371561,2.74658072470568,
7.49482233047108));
#380428=CARTESIAN_POINT('Ctrl Pts',(-0.129707514805723,2.74478891396913,
7.50215800491337));
#380429=CARTESIAN_POINT('Ctrl Pts',(-0.127570877920018,2.74705595609337,
7.49877273257264));
#380430=CARTESIAN_POINT('Ctrl Pts',(-0.124123047921427,2.74722807422352,
7.49481816995647));
#380431=CARTESIAN_POINT('Ctrl Pts',(-0.127728229063016,2.74279080378929,
7.51043025814042));
#380432=CARTESIAN_POINT('Ctrl Pts',(-0.123915371774049,2.74721289337236,
7.51006209594515));
#380433=CARTESIAN_POINT('Ctrl Pts',(-0.118108767356067,2.74746252368982,
7.50731281821699));
#380434=CARTESIAN_POINT('Ctrl Pts',(-0.128914573276736,2.74023237984244,
7.51860402984325));
#380435=CARTESIAN_POINT('Ctrl Pts',(-0.125713547171829,2.74713560005233,
7.51860402984325));
#380436=CARTESIAN_POINT('Ctrl Pts',(-0.118111296885561,2.7474624149473,
7.51860402984325));
#380437=CARTESIAN_POINT('Origin',(0.,0.,7.5));
#380438=CARTESIAN_POINT('Origin',(0.176949628854341,2.66188407944157,7.5));
#380439=CARTESIAN_POINT('',(0.176949628854341,2.66188407944157,7.59394543036555));
#380440=CARTESIAN_POINT('',(0.176949628854341,2.66188407944157,8.85049129520029));
#380441=CARTESIAN_POINT('',(0.176949628854341,2.66188407944157,7.5));
#380442=CARTESIAN_POINT('',(0.215079030421376,2.72235985585717,8.78727029226991));
#380443=CARTESIAN_POINT('Ctrl Pts',(0.176949628854341,2.66188407944157,
8.85049129520029));
#380444=CARTESIAN_POINT('Ctrl Pts',(0.189677904302623,2.68207197404603,
8.82945686509571));
#380445=CARTESIAN_POINT('Ctrl Pts',(0.202387257630373,2.70222985690408,
8.80838212259896));
#380446=CARTESIAN_POINT('Ctrl Pts',(0.215079030421377,2.72235985585717,
8.78727029226991));
#380447=CARTESIAN_POINT('',(0.222557758686683,2.73422161816809,8.75721825406948));
#380448=CARTESIAN_POINT('Origin',(0.200051500241714,2.6985255681284,8.75937679713107));
#380449=CARTESIAN_POINT('',(0.222557758686683,2.73422161816809,7.51860402984325));
#380450=CARTESIAN_POINT('',(0.222557758686684,2.73422161816809,7.5));
#380451=CARTESIAN_POINT('Ctrl Pts',(0.222557758686683,2.73422161816809,
7.51860402984325));
#380452=CARTESIAN_POINT('Ctrl Pts',(0.216684380796542,2.72490604872586,
7.52834476460825));
#380453=CARTESIAN_POINT('Ctrl Pts',(0.210807189994223,2.71558443175037,
7.53807742314407));
#380454=CARTESIAN_POINT('Ctrl Pts',(0.204926058256133,2.70625656418765,
7.54780169004674));
#380455=CARTESIAN_POINT('Ctrl Pts',(0.195610663431048,2.69148172609652,
7.5632044032688));
#380456=CARTESIAN_POINT('Ctrl Pts',(0.186285369461558,2.67669118730146,
7.57858609112103));
#380457=CARTESIAN_POINT('Ctrl Pts',(0.176949628854341,2.66188407944157,
7.59394543036555));
#380458=CARTESIAN_POINT('Origin',(0.0491816719600702,2.91212708488465,7.5));
#380459=CARTESIAN_POINT('',(0.128913937383338,2.74023375097047,8.75721825406948));
#380460=CARTESIAN_POINT('',(0.134814416896071,2.72751301502058,8.78727029226991));
#380461=CARTESIAN_POINT('Origin',(0.149792034669353,2.69522304258,8.75658640620967));
#380462=CARTESIAN_POINT('',(0.164897305964621,2.66265786424426,8.85049129520029));
#380463=CARTESIAN_POINT('Ctrl Pts',(0.134814416896071,2.72751301502058,
8.78727029226991));
#380464=CARTESIAN_POINT('Ctrl Pts',(0.144827823277063,2.70592529519939,
8.80838212259898));
#380465=CARTESIAN_POINT('Ctrl Pts',(0.154855100144228,2.68430767225054,
8.82945686509571));
#380466=CARTESIAN_POINT('Ctrl Pts',(0.164897305964621,2.66265786424426,
8.85049129520029));
#380467=CARTESIAN_POINT('',(0.164897305964621,2.66265786424426,7.59394543036555));
#380468=CARTESIAN_POINT('',(0.164897305964621,2.66265786424426,7.5));
#380469=CARTESIAN_POINT('',(0.128913937383338,2.74023375097047,7.51860402984325));
#380470=CARTESIAN_POINT('Ctrl Pts',(0.164897305964622,2.66265786424426,
7.59394543036555));
#380471=CARTESIAN_POINT('Ctrl Pts',(0.157531702584619,2.67853723396437,
7.57858609112103));
#380472=CARTESIAN_POINT('Ctrl Pts',(0.150174341270698,2.69439883476488,
7.56320440326857));
#380473=CARTESIAN_POINT('Ctrl Pts',(0.1428247900678,2.71024359788972,7.54780169004651));
#380474=CARTESIAN_POINT('Ctrl Pts',(0.138184763568473,2.72024694622285,
7.53807742314383));
#380475=CARTESIAN_POINT('Ctrl Pts',(0.133547846342444,2.73024359133049,
7.52834476460825));
#380476=CARTESIAN_POINT('Ctrl Pts',(0.128913937383338,2.74023375097047,
7.51860402984325));
#380477=CARTESIAN_POINT('',(0.128913937383338,2.74023375097047,7.5));
#380478=CARTESIAN_POINT('Origin',(0.171134036480631,2.66555075509437,7.5));
#380479=CARTESIAN_POINT('Ctrl Pts',(0.164897305964622,2.66265786424426,
8.85049129520029));
#380480=CARTESIAN_POINT('Ctrl Pts',(0.164978795651674,2.66248218211717,
8.85097269580138));
#380481=CARTESIAN_POINT('Ctrl Pts',(0.1650668876992,2.66231225593408,8.85143669361005));
#380482=CARTESIAN_POINT('Ctrl Pts',(0.165166414645531,2.66214066352794,
8.8519052845931));
#380483=CARTESIAN_POINT('Ctrl Pts',(0.165361083040785,2.66180503966352,
8.85282181883899));
#380484=CARTESIAN_POINT('Ctrl Pts',(0.165594660314783,2.66147177387202,
8.85372622499636));
#380485=CARTESIAN_POINT('Ctrl Pts',(0.165883438033025,2.66114448611063,
8.85462257735071));
#380486=CARTESIAN_POINT('Ctrl Pts',(0.166123171038294,2.66087278343529,
8.85536669723986));
#380487=CARTESIAN_POINT('Ctrl Pts',(0.166400977668207,2.66060511779347,
8.85610498449051));
#380488=CARTESIAN_POINT('Ctrl Pts',(0.16673175496809,2.66034930042851,8.85681338218371));
#380489=CARTESIAN_POINT('Ctrl Pts',(0.167031935887229,2.66011714576804,
8.85745625420285));
#380490=CARTESIAN_POINT('Ctrl Pts',(0.167379140604456,2.65989136329579,
8.85808743050666));
#380491=CARTESIAN_POINT('Ctrl Pts',(0.167797781718648,2.65968684835214,
8.85866804508411));
#380492=CARTESIAN_POINT('Ctrl Pts',(0.167990933653708,2.65959248959048,
8.85893592806396));
#380493=CARTESIAN_POINT('Ctrl Pts',(0.168199482605728,2.65950280806947,
8.85919241173848));
#380494=CARTESIAN_POINT('Ctrl Pts',(0.168426929570569,2.65942042008506,
8.85943017985534));
#380495=CARTESIAN_POINT('Ctrl Pts',(0.168734050304612,2.65930917191666,
8.8597512372));
#380496=CARTESIAN_POINT('Ctrl Pts',(0.169083662951928,2.65920899275127,
8.86004599534706));
#380497=CARTESIAN_POINT('Ctrl Pts',(0.169474435967161,2.65913109836974,
8.86026130871721));
#380498=CARTESIAN_POINT('Ctrl Pts',(0.169617508985096,2.65910257904058,
8.86034014101236));
#380499=CARTESIAN_POINT('Ctrl Pts',(0.169768246247698,2.65907660650484,
8.86040910639692));
#380500=CARTESIAN_POINT('Ctrl Pts',(0.169922598120376,2.6590542198636,8.86046313645507));
#380501=CARTESIAN_POINT('Ctrl Pts',(0.170163462925003,2.65901928569743,
8.8605474499083));
#380502=CARTESIAN_POINT('Ctrl Pts',(0.17041972577939,2.65899227558558,8.86059655985669));
#380503=CARTESIAN_POINT('Ctrl Pts',(0.170674921058896,2.65897463042516,
8.86059725258816));
#380504=CARTESIAN_POINT('Ctrl Pts',(0.170930705941449,2.65895694449737,
8.86059794692012));
#380505=CARTESIAN_POINT('Ctrl Pts',(0.171188438254314,2.65895112114787,
8.86056369958366));
#380506=CARTESIAN_POINT('Ctrl Pts',(0.171433976148159,2.65895371584656,
8.86048590497774));
#380507=CARTESIAN_POINT('Ctrl Pts',(0.171498054227909,2.65895439298566,
8.86046560290182));
#380508=CARTESIAN_POINT('Ctrl Pts',(0.171562134463288,2.65895574282288,
8.86044257503091));
#380509=CARTESIAN_POINT('Ctrl Pts',(0.171624237413298,2.65895769082822,
8.86041778462583));
#380510=CARTESIAN_POINT('Ctrl Pts',(0.172042113203527,2.65897079848689,
8.86025097596201));
#380511=CARTESIAN_POINT('Ctrl Pts',(0.17242652801394,2.65901307951986,8.8599848982295));
#380512=CARTESIAN_POINT('Ctrl Pts',(0.172767188072727,2.65907487815317,
8.85968173251462));
#380513=CARTESIAN_POINT('Ctrl Pts',(0.17294737772633,2.65910756608955,8.85952137522077));
#380514=CARTESIAN_POINT('Ctrl Pts',(0.173118833030298,2.65914615685814,
8.85934740853961));
#380515=CARTESIAN_POINT('Ctrl Pts',(0.173279477441213,2.65918858963265,
8.85916759001821));
#380516=CARTESIAN_POINT('Ctrl Pts',(0.173924548252338,2.65935897927845,
8.85844552518696));
#380517=CARTESIAN_POINT('Ctrl Pts',(0.174432530583691,2.65959802342683,
8.85759444184125));
#380518=CARTESIAN_POINT('Ctrl Pts',(0.174829205672066,2.65983012928581,
8.8568349891514));
#380519=CARTESIAN_POINT('Ctrl Pts',(0.174870716663634,2.6598544185458,8.85675551444999));
#380520=CARTESIAN_POINT('Ctrl Pts',(0.174910995458546,2.65987864675125,
8.85667699793651));
#380521=CARTESIAN_POINT('Ctrl Pts',(0.174950062383047,2.6599027366277,8.85659965593547));
#380522=CARTESIAN_POINT('Ctrl Pts',(0.17547738972341,2.66022790300923,8.85555568965886));
#380523=CARTESIAN_POINT('Ctrl Pts',(0.17593722350854,2.66061656454988,8.85434650606346));
#380524=CARTESIAN_POINT('Ctrl Pts',(0.176335848680025,2.66106589614674,
8.85297329937117));
#380525=CARTESIAN_POINT('Ctrl Pts',(0.176560051050397,2.6613186177918,8.85220095427747));
#380526=CARTESIAN_POINT('Ctrl Pts',(0.176764746713045,2.66159084402269,
8.85137579139183));
#380527=CARTESIAN_POINT('Ctrl Pts',(0.176949628854341,2.66188407944157,
8.85049129520029));
#380528=CARTESIAN_POINT('Origin',(0.171134036480631,2.66555075509437,7.59394543036555));
#380529=CARTESIAN_POINT('Ctrl Pts',(0.16513389801642,2.66214779976352,7.59443877723642));
#380530=CARTESIAN_POINT('Ctrl Pts',(0.167570568507185,2.65689462638278,
7.58783886950016));
#380531=CARTESIAN_POINT('Ctrl Pts',(0.175889913880979,2.65858804720708,
7.58559994247159));
#380532=CARTESIAN_POINT('Ctrl Pts',(0.151832185296215,2.69082471912743,
7.56670252222135));
#380533=CARTESIAN_POINT('Ctrl Pts',(0.154265334106333,2.68557913807364,
7.56004874999028));
#380534=CARTESIAN_POINT('Ctrl Pts',(0.162638236120083,2.68726165675841,
7.55786368756704));
#380535=CARTESIAN_POINT('Ctrl Pts',(0.138555312195495,2.71944808720963,
7.53888913333562));
#380536=CARTESIAN_POINT('Ctrl Pts',(0.141002921328123,2.71417133141078,
7.5322200213728));
#380537=CARTESIAN_POINT('Ctrl Pts',(0.149409776264335,2.7158822477739,7.53005029815327));
#380538=CARTESIAN_POINT('Ctrl Pts',(0.125303879501795,2.74801660878327,
7.51101258149734));
#380539=CARTESIAN_POINT('Ctrl Pts',(0.127781158104529,2.74267588911605,
7.5043616886572));
#380540=CARTESIAN_POINT('Ctrl Pts',(0.136205262916607,2.74444844085289,
7.50217374673251));
#380541=CARTESIAN_POINT('',(0.136909871778086,2.7429241116639,7.50366116523517));
#380542=CARTESIAN_POINT('Ctrl Pts',(0.128913937383338,2.74023375097047,
7.51860402984325));
#380543=CARTESIAN_POINT('Ctrl Pts',(0.128728114394968,2.74063436335517,
7.51734760759493));
#380544=CARTESIAN_POINT('Ctrl Pts',(0.128614169925088,2.74102140924103,
7.51608817408572));
#380545=CARTESIAN_POINT('Ctrl Pts',(0.128585176113098,2.74139776962912,
7.51481005913119));
#380546=CARTESIAN_POINT('Ctrl Pts',(0.128558912825369,2.74173868586207,
7.51365231206383));
#380547=CARTESIAN_POINT('Ctrl Pts',(0.128602066540858,2.74207129579757,
7.51247773061042));
#380548=CARTESIAN_POINT('Ctrl Pts',(0.128750508669634,2.74238509315603,
7.51129758471022));
#380549=CARTESIAN_POINT('Ctrl Pts',(0.128935005282971,2.74277510743559,
7.50983079813402));
#380550=CARTESIAN_POINT('Ctrl Pts',(0.129288033340368,2.74311804396216,
7.50839324291155));
#380551=CARTESIAN_POINT('Ctrl Pts',(0.129869611670354,2.74335727296713,
7.50715379678855));
#380552=CARTESIAN_POINT('Ctrl Pts',(0.13013828410103,2.74346778987421,7.50658120839351));
#380553=CARTESIAN_POINT('Ctrl Pts',(0.130497541971766,2.74356309743786,
7.50598221009429));
#380554=CARTESIAN_POINT('Ctrl Pts',(0.130944668113831,2.74361894150132,
7.50545747549611));
#380555=CARTESIAN_POINT('Ctrl Pts',(0.131183268463085,2.74364874162212,
7.50517746087247));
#380556=CARTESIAN_POINT('Ctrl Pts',(0.131449452540065,2.74366782811638,
7.50491486231392));
#380557=CARTESIAN_POINT('Ctrl Pts',(0.131736290639255,2.74367403179687,
7.50468370960992));
#380558=CARTESIAN_POINT('Ctrl Pts',(0.132165204075493,2.74368330825604,
7.50433806340447));
#380559=CARTESIAN_POINT('Ctrl Pts',(0.132653172773484,2.74366350077052,
7.50405484070984));
#380560=CARTESIAN_POINT('Ctrl Pts',(0.133167303892957,2.74361522753202,
7.50385766036131));
#380561=CARTESIAN_POINT('Ctrl Pts',(0.133222282224778,2.7436100654595,7.50383657498791));
#380562=CARTESIAN_POINT('Ctrl Pts',(0.133277536757632,2.74360459452477,
7.50381643264937));
#380563=CARTESIAN_POINT('Ctrl Pts',(0.13333301077446,2.74359882783486,7.50379723213559));
#380564=CARTESIAN_POINT('Ctrl Pts',(0.133703317983596,2.74356033329326,
7.50366906242519));
#380565=CARTESIAN_POINT('Ctrl Pts',(0.13409138609082,2.74350710736077,7.50358235568538));
#380566=CARTESIAN_POINT('Ctrl Pts',(0.134464202760926,2.74344681272314,
7.5035341175365));
#380567=CARTESIAN_POINT('Ctrl Pts',(0.13502319916305,2.74335640773805,7.50346178989176));
#380568=CARTESIAN_POINT('Ctrl Pts',(0.135620708171075,2.74323538466582,
7.50346967198527));
#380569=CARTESIAN_POINT('Ctrl Pts',(0.136203621195044,2.7430985287681,7.50354272648692));
#380570=CARTESIAN_POINT('Ctrl Pts',(0.136443385387387,2.74304223710461,
7.50357277531559));
#380571=CARTESIAN_POINT('Ctrl Pts',(0.136680394004036,2.74298347960564,
7.50361331098761));
#380572=CARTESIAN_POINT('Ctrl Pts',(0.136909871778157,2.74292411166531,
7.50366116523658));
#380573=CARTESIAN_POINT('',(0.171321629291362,2.66847266454066,7.57603338622103));
#380574=CARTESIAN_POINT('Origin',(0.17189066119661,2.67729126376579,7.58486873427626));
#380575=CARTESIAN_POINT('Ctrl Pts',(0.136909871749266,2.74292411171347,
7.50366116529968));
#380576=CARTESIAN_POINT('Ctrl Pts',(0.148362498674568,2.71814780982416,
7.52783573079709));
#380577=CARTESIAN_POINT('Ctrl Pts',(0.159832559194538,2.6933318400473,7.55196141284068));
#380578=CARTESIAN_POINT('Ctrl Pts',(0.171321628466439,2.66847266548254,
7.57603338728831));
#380579=CARTESIAN_POINT('Ctrl Pts',(0.164624061684221,2.6636647768937,7.5963967733137));
#380580=CARTESIAN_POINT('Ctrl Pts',(0.169597079718486,2.64607668412072,
7.59959882295472));
#380581=CARTESIAN_POINT('Ctrl Pts',(0.177275791240311,2.66268229166692,
7.59642833564546));
#380582=CARTESIAN_POINT('Ctrl Pts',(0.165068222839356,2.6597894930393,7.5870762605742));
#380583=CARTESIAN_POINT('Ctrl Pts',(0.170398543843799,2.65560619660867,
7.58809943920599));
#380584=CARTESIAN_POINT('Ctrl Pts',(0.176262094528132,2.65897267461483,
7.58710240504253));
#380585=CARTESIAN_POINT('Ctrl Pts',(0.168908645247665,2.66449871675321,
7.58015376756929));
#380586=CARTESIAN_POINT('Ctrl Pts',(0.170903573821348,2.66246167689546,
7.58205880659762));
#380587=CARTESIAN_POINT('Ctrl Pts',(0.173140492571299,2.66417143405488,
7.58020924244126));
#380588=CARTESIAN_POINT('Ctrl Pts',(0.171321629238138,2.6684726637148,7.57603338509286));
#380589=CARTESIAN_POINT('Ctrl Pts',(0.171321629238138,2.6684726637148,7.57603338509286));
#380590=CARTESIAN_POINT('Ctrl Pts',(0.171321629238137,2.6684726637148,7.57603338509286));
#380591=CARTESIAN_POINT('Origin',(0.171884966568783,2.6772916293728,7.58486873427623));
#380592=CARTESIAN_POINT('Ctrl Pts',(0.227147889551719,2.74150187215855,
7.51098857897448));
#380593=CARTESIAN_POINT('Ctrl Pts',(0.224007978980353,2.73652176437099,
7.50433767179956));
#380594=CARTESIAN_POINT('Ctrl Pts',(0.215879678833542,2.73935703998472,
7.50214974420965));
#380595=CARTESIAN_POINT('Ctrl Pts',(0.210347158552135,2.71485479117137,
7.53887321589173));
#380596=CARTESIAN_POINT('Ctrl Pts',(0.207244869681733,2.70993435391323,
7.53220407452068));
#380597=CARTESIAN_POINT('Ctrl Pts',(0.199125792371518,2.71270626725104,
7.53003438070911));
#380598=CARTESIAN_POINT('Ctrl Pts',(0.193514163951452,2.68815653795892,
7.56669465659233));
#380599=CARTESIAN_POINT('Ctrl Pts',(0.19043020903154,2.68326517957014,7.560040858333));
#380600=CARTESIAN_POINT('Ctrl Pts',(0.182341182153904,2.6860045762737,7.55785582193789));
#380601=CARTESIAN_POINT('Ctrl Pts',(0.176649667038706,2.66140831997643,
7.59443891967696));
#380602=CARTESIAN_POINT('Ctrl Pts',(0.173561240768107,2.656509869727,7.58783901202978));
#380603=CARTESIAN_POINT('Ctrl Pts',(0.165526747119516,2.65925324170307,
7.58560008491213));
#380604=CARTESIAN_POINT('',(0.21497150649217,2.73791238843283,7.50366116523517));
#380605=CARTESIAN_POINT('Ctrl Pts',(0.214971506492199,2.7379123884332,7.50366116523554));
#380606=CARTESIAN_POINT('Ctrl Pts',(0.21572334107391,2.73800663427399,7.50350835821027));
#380607=CARTESIAN_POINT('Ctrl Pts',(0.216417525721002,2.73806880892224,
7.50345484956));
#380608=CARTESIAN_POINT('Ctrl Pts',(0.217074645537771,2.73810135898814,
7.50349758195598));
#380609=CARTESIAN_POINT('Ctrl Pts',(0.21741179673705,2.73811805958593,7.50351950684424));
#380610=CARTESIAN_POINT('Ctrl Pts',(0.217772415375925,2.73812873702199,
7.50357029184312));
#380611=CARTESIAN_POINT('Ctrl Pts',(0.218120438804839,2.73812947445888,
7.50365515313923));
#380612=CARTESIAN_POINT('Ctrl Pts',(0.218655839767117,2.73813060893543,
7.50378570417639));
#380613=CARTESIAN_POINT('Ctrl Pts',(0.219177147199477,2.73810859894365,
7.50400001621911));
#380614=CARTESIAN_POINT('Ctrl Pts',(0.219644586262636,2.73806285136934,
7.50428903009635));
#380615=CARTESIAN_POINT('Ctrl Pts',(0.219696468402382,2.73805777374055,
7.50432110841318));
#380616=CARTESIAN_POINT('Ctrl Pts',(0.219747713437272,2.73805241837707,
7.50435406373354));
#380617=CARTESIAN_POINT('Ctrl Pts',(0.219798286699864,2.73804679504868,
7.50438785222351));
#380618=CARTESIAN_POINT('Ctrl Pts',(0.220107060776615,2.73801246192593,
7.50459414719561));
#380619=CARTESIAN_POINT('Ctrl Pts',(0.220395652270365,2.7379670806944,7.50483629897752));
#380620=CARTESIAN_POINT('Ctrl Pts',(0.220653209760764,2.73791368995158,
7.50509910455309));
#380621=CARTESIAN_POINT('Ctrl Pts',(0.221221407453785,2.73779590461034,
7.50567888004914));
#380622=CARTESIAN_POINT('Ctrl Pts',(0.221661062246274,2.73763500597979,
7.50637912803144));
#380623=CARTESIAN_POINT('Ctrl Pts',(0.221990006666829,2.73745624122374,
7.50710440483569));
#380624=CARTESIAN_POINT('Ctrl Pts',(0.22207067036921,2.73741240455658,7.50728225710685));
#380625=CARTESIAN_POINT('Ctrl Pts',(0.222146352208224,2.73736674913086,
7.50746498566954));
#380626=CARTESIAN_POINT('Ctrl Pts',(0.222215500713304,2.73732069740447,
7.50764697238949));
#380627=CARTESIAN_POINT('Ctrl Pts',(0.222587224046429,2.73707313599715,
7.50862528291181));
#380628=CARTESIAN_POINT('Ctrl Pts',(0.222806182813355,2.7367950940424,7.50965856837421));
#380629=CARTESIAN_POINT('Ctrl Pts',(0.222933569195844,2.7365120845317,7.51067959873201));
#380630=CARTESIAN_POINT('Ctrl Pts',(0.223003670082806,2.73635634404099,
7.51124147302577));
#380631=CARTESIAN_POINT('Ctrl Pts',(0.223045660948021,2.73619888290729,
7.51180065547252));
#380632=CARTESIAN_POINT('Ctrl Pts',(0.223067223661595,2.73604292919307,
7.512351757165));
#380633=CARTESIAN_POINT('Ctrl Pts',(0.223141731426557,2.73550404698585,
7.51425603304534));
#380634=CARTESIAN_POINT('Ctrl Pts',(0.222975207875285,2.73491808083108,
7.51626900505178));
#380635=CARTESIAN_POINT('Ctrl Pts',(0.222617535678944,2.73431900699274,
7.5182778896924));
#380636=CARTESIAN_POINT('Ctrl Pts',(0.222598177783769,2.73428658398451,
7.51838661432543));
#380637=CARTESIAN_POINT('Ctrl Pts',(0.222578250493315,2.73425411954144,
7.51849533314855));
#380638=CARTESIAN_POINT('Ctrl Pts',(0.222557758686687,2.73422161816809,
7.51860402984325));
#380639=CARTESIAN_POINT('Ctrl Pts',(0.171321630230276,2.66847266537049,
7.57603338728985));
#380640=CARTESIAN_POINT('Ctrl Pts',(0.18589529509066,2.69165855689206,7.55196141284922));
#380641=CARTESIAN_POINT('Ctrl Pts',(0.20044458236368,2.71480402913563,7.52783573083105));
#380642=CARTESIAN_POINT('Ctrl Pts',(0.214971506528135,2.73791238847983,
7.50366116530176));
#380643=CARTESIAN_POINT('Origin',(5.91995423665117E-17,9.2208065736915E-16,
7.49482233047033));
#380644=CARTESIAN_POINT('Origin',(0.136469240156451,2.7340962668661,7.49482233047033));
#380645=CARTESIAN_POINT('Origin',(0.,0.,7.50366116523517));
#380646=CARTESIAN_POINT('Origin',(0.214279640797748,2.72910067339767,7.49482233047033));
#380647=CARTESIAN_POINT('Ctrl Pts',(0.128914382414638,2.74023279142927,
7.51860402984325));
#380648=CARTESIAN_POINT('Ctrl Pts',(0.125713236557893,2.74713561340539,
7.51860402984325));
#380649=CARTESIAN_POINT('Ctrl Pts',(0.118111296885526,2.7474624149473,7.51860402984325));
#380650=CARTESIAN_POINT('Ctrl Pts',(0.127725773959473,2.7427958558017,7.51041458714366));
#380651=CARTESIAN_POINT('Ctrl Pts',(0.123912249553058,2.74721302654345,
7.51004642900442));
#380652=CARTESIAN_POINT('Ctrl Pts',(0.118109200360832,2.74746250507528,
7.5072913648301));
#380653=CARTESIAN_POINT('Ctrl Pts',(0.129714166000048,2.7447883502916,7.50215815450137));
#380654=CARTESIAN_POINT('Ctrl Pts',(0.127579244834765,2.7470555459381,7.49877163671529));
#380655=CARTESIAN_POINT('Ctrl Pts',(0.124133329223839,2.74722756104425,
7.4948158853317));
#380656=CARTESIAN_POINT('Ctrl Pts',(0.136909844334258,2.74292356183035,
7.50366171572174));
#380657=CARTESIAN_POINT('Ctrl Pts',(0.137092387372164,2.74658072470565,
7.50000045605858));
#380658=CARTESIAN_POINT('Ctrl Pts',(0.137092387372039,2.74658072470566,
7.49482233047317));
#380659=CARTESIAN_POINT('Origin',(0.117574427354229,2.73497394942481,7.51860402984325));
#380660=CARTESIAN_POINT('Origin',(0.117574427354229,2.73497394942481,9.));
#380661=CARTESIAN_POINT('Origin',(0.117574427354229,2.73497394942481,8.75721825406948));
#380662=CARTESIAN_POINT('Ctrl Pts',(0.135941072634455,2.72508400670848,
8.78942910404913));
#380663=CARTESIAN_POINT('Ctrl Pts',(0.13361461326795,2.73014760380123,8.79672699501692));
#380664=CARTESIAN_POINT('Ctrl Pts',(0.124957328323498,2.72797391951581,
8.79893251111267));
#380665=CARTESIAN_POINT('Ctrl Pts',(0.131314834806412,2.7350576390608,8.78111911759581));
#380666=CARTESIAN_POINT('Ctrl Pts',(0.128550026197774,2.74105748434908,
8.78644465894811));
#380667=CARTESIAN_POINT('Ctrl Pts',(0.120447127148838,2.74081553646592,
8.78817647674132));
#380668=CARTESIAN_POINT('Ctrl Pts',(0.128431653016943,2.74127344462292,
8.76780923932031));
#380669=CARTESIAN_POINT('Ctrl Pts',(0.125163285148986,2.74835387598335,
8.76988516158376));
#380670=CARTESIAN_POINT('Ctrl Pts',(0.117619591664174,2.74883248752051,
8.77093053738832));
#380671=CARTESIAN_POINT('Ctrl Pts',(0.128993834005189,2.74006144760687,
8.75371302330492));
#380672=CARTESIAN_POINT('Ctrl Pts',(0.125806374260045,2.74696842246863,
8.75300828287559));
#380673=CARTESIAN_POINT('Ctrl Pts',(0.118170644421235,2.74726870427462,
8.75267964240737));
#380674=CARTESIAN_POINT('Origin',(0.123474906866962,2.72225321347492,8.78727029226991));
#380675=CARTESIAN_POINT('Ctrl Pts',(0.164897305964621,2.66265786424426,
8.85049129520029));
#380676=CARTESIAN_POINT('Ctrl Pts',(0.162440088364629,2.66795533476229,
8.85711686593484));
#380677=CARTESIAN_POINT('Ctrl Pts',(0.15406769756606,2.66622217740361,8.85933012996512));
#380678=CARTESIAN_POINT('Ctrl Pts',(0.154855086667218,2.68430770130538,
8.82945683644722));
#380679=CARTESIAN_POINT('Ctrl Pts',(0.152377472675456,2.68964914403161,
8.83607469902389));
#380680=CARTESIAN_POINT('Ctrl Pts',(0.143988102906681,2.68787417434732,
8.8382956714852));
#380681=CARTESIAN_POINT('Ctrl Pts',(0.144827836107466,2.70592526753856,
8.80838214965004));
#380682=CARTESIAN_POINT('Ctrl Pts',(0.142340444294155,2.71128779009166,
8.8150136446199));
#380683=CARTESIAN_POINT('Ctrl Pts',(0.13392440455196,2.70949360848066,8.81722098428721));
#380684=CARTESIAN_POINT('Ctrl Pts',(0.134814416896071,2.72751301502058,
8.78727029226991));
#380685=CARTESIAN_POINT('Ctrl Pts',(0.132326611918797,2.7328764283063,8.79393457792714));
#380686=CARTESIAN_POINT('Ctrl Pts',(0.123875403548898,2.7310829701198,8.79610912703474));
#380687=CARTESIAN_POINT('Origin',(0.153557795935513,2.6573980626986,8.85049129520029));
#380688=CARTESIAN_POINT('Ctrl Pts',(0.176949628854341,2.66188407944157,
8.85049129520029));
#380689=CARTESIAN_POINT('Ctrl Pts',(0.180064098225757,2.66682383578755,
8.85711686593484));
#380690=CARTESIAN_POINT('Ctrl Pts',(0.188146120567823,2.66403427005499,
8.85933012996512));
#380691=CARTESIAN_POINT('Ctrl Pts',(0.174194302759283,2.65751394830841,
8.86332496987232));
#380692=CARTESIAN_POINT('Ctrl Pts',(0.178815093143597,2.65750014247301,
8.86648636486738));
#380693=CARTESIAN_POINT('Ctrl Pts',(0.180423490888535,2.65181778745183,
8.87206031107457));
#380694=CARTESIAN_POINT('Ctrl Pts',(0.167085943002636,2.65793942165148,
8.86341338519874));
#380695=CARTESIAN_POINT('Ctrl Pts',(0.162484685652754,2.6584888772316,8.86654584966055));
#380696=CARTESIAN_POINT('Ctrl Pts',(0.160209362634033,2.65301648671671,
8.87215952290714));
#380697=CARTESIAN_POINT('Ctrl Pts',(0.164897305964622,2.66265786424426,
8.85049129520029));
#380698=CARTESIAN_POINT('Ctrl Pts',(0.162440088364629,2.66795533476229,
8.85711686593484));
#380699=CARTESIAN_POINT('Ctrl Pts',(0.15406769756606,2.66622217740361,8.85933012996512));
#380700=CARTESIAN_POINT('Origin',(0.187523433170177,2.65521739643648,8.85049129520029));
#380701=CARTESIAN_POINT('Ctrl Pts',(0.215079030421377,2.72235985585717,
8.78727029226991));
#380702=CARTESIAN_POINT('Ctrl Pts',(0.218232268622096,2.72736110215464,
8.79393457792714));
#380703=CARTESIAN_POINT('Ctrl Pts',(0.226384750345611,2.72450165169591,
8.79610912703474));
#380704=CARTESIAN_POINT('Ctrl Pts',(0.202387241368117,2.70222983111106,
8.80838214965003));
#380705=CARTESIAN_POINT('Ctrl Pts',(0.205539955892618,2.70723024682311,
8.81501364461995));
#380706=CARTESIAN_POINT('Ctrl Pts',(0.213657465212887,2.70437457614343,
8.81722098428721));
#380707=CARTESIAN_POINT('Ctrl Pts',(0.189677921384441,2.68207200113894,
8.82945683644722));
#380708=CARTESIAN_POINT('Ctrl Pts',(0.192818242734668,2.68705276044921,
8.83607469902389));
#380709=CARTESIAN_POINT('Ctrl Pts',(0.200911757808326,2.68421955444713,
8.8382956714852));
#380710=CARTESIAN_POINT('Ctrl Pts',(0.176949628854341,2.66188407944157,
8.85049129520029));
#380711=CARTESIAN_POINT('Ctrl Pts',(0.180064098225757,2.66682383578755,
8.85711686593484));
#380712=CARTESIAN_POINT('Ctrl Pts',(0.188146120567823,2.66403427005499,
8.85933012996512));
#380713=CARTESIAN_POINT('Origin',(0.225652834737212,2.71569317285208,8.78727029226991));
#380714=CARTESIAN_POINT('Ctrl Pts',(0.222459021446504,2.73406497972526,
8.75374538247847));
#380715=CARTESIAN_POINT('Ctrl Pts',(0.226500710045474,2.74049997247247,
8.75304829418603));
#380716=CARTESIAN_POINT('Ctrl Pts',(0.234104570794356,2.73982770398394,
8.75272238421917));
#380717=CARTESIAN_POINT('Ctrl Pts',(0.2231630141067,2.73518155988291,8.76769408445022));
#380718=CARTESIAN_POINT('Ctrl Pts',(0.227306993923109,2.74177811855038,
8.76974318093965));
#380719=CARTESIAN_POINT('Ctrl Pts',(0.234842375123338,2.74129192162787,
8.77077869880429));
#380720=CARTESIAN_POINT('Ctrl Pts',(0.219554748756163,2.72945860607643,
8.78108014887987));
#380721=CARTESIAN_POINT('Ctrl Pts',(0.223063405128047,2.73505097299612,
8.78639403366329));
#380722=CARTESIAN_POINT('Ctrl Pts',(0.231060141221959,2.73379626682602,
8.78812224174742));
#380723=CARTESIAN_POINT('Ctrl Pts',(0.21364159840909,2.72007994812382,8.78944554828686));
#380724=CARTESIAN_POINT('Ctrl Pts',(0.216593822171808,2.72479596259282,
8.79673892988685));
#380725=CARTESIAN_POINT('Ctrl Pts',(0.2248941505513,2.72153895428624,8.79894799272499));
#380726=CARTESIAN_POINT('Origin',(0.233131563002519,2.727554935163,8.75721825406948));
#380727=CARTESIAN_POINT('Origin',(0.233131563002519,2.727554935163,9.));
#380728=CARTESIAN_POINT('Origin',(0.233131563002519,2.727554935163,7.51860402984325));
#380729=CARTESIAN_POINT('Ctrl Pts',(0.214971444915595,2.73791160418275,
7.50366195182965));
#380730=CARTESIAN_POINT('Ctrl Pts',(0.215258086646279,2.74156232030815,
7.50000065167735));
#380731=CARTESIAN_POINT('Ctrl Pts',(0.215258086646395,2.74156232030814,
7.49482233047108));
#380732=CARTESIAN_POINT('Ctrl Pts',(0.222353197839296,2.73884086376983,
7.50215800491338));
#380733=CARTESIAN_POINT('Ctrl Pts',(0.224762195877964,2.74081606644905,
7.49877273257268));
#380734=CARTESIAN_POINT('Ctrl Pts',(0.228203729217893,2.74054587277758,
7.49481816995649));
#380735=CARTESIAN_POINT('Ctrl Pts',(0.224060721014884,2.73660605260403,
7.51043025814041));
#380736=CARTESIAN_POINT('Ctrl Pts',(0.228407759062819,2.74050425952474,
7.51006209594512));
#380737=CARTESIAN_POINT('Ctrl Pts',(0.234198613355249,2.74000930828873,
7.50731281821699));
#380738=CARTESIAN_POINT('Ctrl Pts',(0.222556952678043,2.73422033961324,
7.51860402984326));
#380739=CARTESIAN_POINT('Ctrl Pts',(0.226614462609803,2.74065754634786,
7.51860402984326));
#380740=CARTESIAN_POINT('Ctrl Pts',(0.234196090687468,2.74000952390803,
7.51860402984327));
#380741=CARTESIAN_POINT('Origin',(0.,0.,7.5));
#380742=CARTESIAN_POINT('Origin',(0.34713356539705,2.64507775146798,7.5));
#380743=CARTESIAN_POINT('',(0.34713356539705,2.64507775146798,7.59394543036555));
#380744=CARTESIAN_POINT('',(0.34713356539705,2.64507775146798,8.85049129520029));
#380745=CARTESIAN_POINT('',(0.34713356539705,2.64507775146798,7.5));
#380746=CARTESIAN_POINT('',(0.389059322317652,2.7029863147688,8.78727029226991));
#380747=CARTESIAN_POINT('Ctrl Pts',(0.34713356539705,2.64507775146798,8.85049129520029));
#380748=CARTESIAN_POINT('Ctrl Pts',(0.361129132086575,2.66440866446989,
8.82945686509571));
#380749=CARTESIAN_POINT('Ctrl Pts',(0.375103892673901,2.68371083973216,
8.80838212259896));
#380750=CARTESIAN_POINT('Ctrl Pts',(0.389059322317652,2.7029863147688,8.78727029226991));
#380751=CARTESIAN_POINT('',(0.397282670454267,2.71434454205174,8.75721825406948));
#380752=CARTESIAN_POINT('Origin',(0.372535599753802,2.68016381430646,8.75937679713185));
#380753=CARTESIAN_POINT('',(0.397282670454267,2.71434454205174,7.51860402984325));
#380754=CARTESIAN_POINT('',(0.397282670454267,2.71434454205174,7.5));
#380755=CARTESIAN_POINT('Ctrl Pts',(0.397282670454266,2.71434454205174,
7.51860402984325));
#380756=CARTESIAN_POINT('Ctrl Pts',(0.390824509465509,2.70542442105947,
7.52834476460825));
#380757=CARTESIAN_POINT('Ctrl Pts',(0.384362155931824,2.69649850925338,
7.53807742314407));
#380758=CARTESIAN_POINT('Ctrl Pts',(0.377895469082945,2.68756661219917,
7.54780169004674));
#380759=CARTESIAN_POINT('Ctrl Pts',(0.367652586608923,2.67341896999315,
7.5632044032688));
#380760=CARTESIAN_POINT('Ctrl Pts',(0.357398819381796,2.65925629358233,
7.57858609112103));
#380761=CARTESIAN_POINT('Ctrl Pts',(0.34713356539705,2.64507775146798,7.59394543036555));
#380762=CARTESIAN_POINT('Origin',(0.235661245880662,2.9029927269226,7.5));
#380763=CARTESIAN_POINT('',(0.304216449096259,2.72634410251322,8.75721825406948));
#380764=CARTESIAN_POINT('',(0.309289785090383,2.71327145765926,8.78727029226991));
#380765=CARTESIAN_POINT('Origin',(0.322167804103539,2.68008820916626,8.75658640621033));
#380766=CARTESIAN_POINT('',(0.335155581859841,2.64662214142563,8.85049129520029));
#380767=CARTESIAN_POINT('Ctrl Pts',(0.309289785090383,2.71327145765926,
8.78727029226991));
#380768=CARTESIAN_POINT('Ctrl Pts',(0.317899487896211,2.69108653097412,
8.80838212259896));
#380769=CARTESIAN_POINT('Ctrl Pts',(0.326521116789831,2.66887087391543,
8.82945686509571));
#380770=CARTESIAN_POINT('Ctrl Pts',(0.335155581859841,2.64662214142563,
8.85049129520029));
#380771=CARTESIAN_POINT('',(0.335155581859841,2.64662214142563,7.59394543036555));
#380772=CARTESIAN_POINT('',(0.335155581859841,2.64662214142563,7.5));
#380773=CARTESIAN_POINT('',(0.304216449096259,2.72634410251322,7.51860402984325));
#380774=CARTESIAN_POINT('Ctrl Pts',(0.335155581859841,2.64662214142563,
7.59394543036555));
#380775=CARTESIAN_POINT('Ctrl Pts',(0.328822506613063,2.66294080110644,
7.57858609112103));
#380776=CARTESIAN_POINT('Ctrl Pts',(0.322496518039572,2.67924120030481,
7.56320440326857));
#380777=CARTESIAN_POINT('Ctrl Pts',(0.316177244736808,2.69552429602679,
7.54780169004651));
#380778=CARTESIAN_POINT('Ctrl Pts',(0.312187668397812,2.70580437892645,
7.53807742314383));
#380779=CARTESIAN_POINT('Ctrl Pts',(0.308200765466647,2.71607757316129,
7.52834476460825));
#380780=CARTESIAN_POINT('Ctrl Pts',(0.304216449096259,2.72634410251322,
7.51860402984325));
#380781=CARTESIAN_POINT('',(0.304216449096259,2.72634410251322,7.5));
#380782=CARTESIAN_POINT('Origin',(0.341564846497265,2.64910949982511,7.5));
#380783=CARTESIAN_POINT('Ctrl Pts',(0.335155581859841,2.64662214142563,
8.85049129520029));
#380784=CARTESIAN_POINT('Ctrl Pts',(0.335225648125062,2.64644159919414,
8.85097269580138));
#380785=CARTESIAN_POINT('Ctrl Pts',(0.335302671970097,2.64626637806575,
8.85143669361005));
#380786=CARTESIAN_POINT('Ctrl Pts',(0.335391000464435,2.64608876150127,
8.8519052845931));
#380787=CARTESIAN_POINT('Ctrl Pts',(0.335563765397768,2.64574135476517,
8.85282181883899));
#380788=CARTESIAN_POINT('Ctrl Pts',(0.335775510349633,2.64539380835665,
8.85372622499636));
#380789=CARTESIAN_POINT('Ctrl Pts',(0.336042725344213,2.64504869099114,
8.85462257735071));
#380790=CARTESIAN_POINT('Ctrl Pts',(0.336264557742135,2.6447621868117,8.85536669723986));
#380791=CARTESIAN_POINT('Ctrl Pts',(0.33652464419198,2.64447727198576,8.85610498449051));
#380792=CARTESIAN_POINT('Ctrl Pts',(0.336838351599578,2.64420078725064,
8.85681338218371));
#380793=CARTESIAN_POINT('Ctrl Pts',(0.337123041564658,2.64394987691929,
8.85745625420284));
#380794=CARTESIAN_POINT('Ctrl Pts',(0.337455066979889,2.64370231285874,
8.85808743050665));
#380795=CARTESIAN_POINT('Ctrl Pts',(0.33785974463358,2.6434713956847,8.85866804508409));
#380796=CARTESIAN_POINT('Ctrl Pts',(0.338046454130659,2.64336485550627,
8.85893592806395));
#380797=CARTESIAN_POINT('Ctrl Pts',(0.338248828681714,2.64326199646833,
8.85919241173848));
#380798=CARTESIAN_POINT('Ctrl Pts',(0.33847052971609,2.6431652051818,8.85943017985534));
#380799=CARTESIAN_POINT('Ctrl Pts',(0.338769891743025,2.6430345082917,8.8597512372));
#380800=CARTESIAN_POINT('Ctrl Pts',(0.339112367572496,2.64291213519593,
8.86004599534705));
#380801=CARTESIAN_POINT('Ctrl Pts',(0.339497346992498,2.64280936394371,
8.86026130871721));
#380802=CARTESIAN_POINT('Ctrl Pts',(0.339638298811881,2.64277173649084,
8.86034014101235));
#380803=CARTESIAN_POINT('Ctrl Pts',(0.339787062302531,2.64273615954889,
8.86040910639692));
#380804=CARTESIAN_POINT('Ctrl Pts',(0.339939662725702,2.64270392954497,
8.86046313645506));
#380805=CARTESIAN_POINT('Ctrl Pts',(0.340177794408044,2.64265363489377,
8.86054744990829));
#380806=CARTESIAN_POINT('Ctrl Pts',(0.340431800199104,2.64261026145964,
8.86059655985669));
#380807=CARTESIAN_POINT('Ctrl Pts',(0.340685340623228,2.6425763021354,8.86059725258816));
#380808=CARTESIAN_POINT('Ctrl Pts',(0.340939466827023,2.64254226435155,
8.86059794692011));
#380809=CARTESIAN_POINT('Ctrl Pts',(0.341196296497925,2.64251994000076,
8.86056369958366));
#380810=CARTESIAN_POINT('Ctrl Pts',(0.341441496150749,2.64250679770149,
8.86048590497774));
#380811=CARTESIAN_POINT('Ctrl Pts',(0.341505485959662,2.64250336795268,
8.86046560290182));
#380812=CARTESIAN_POINT('Ctrl Pts',(0.341569521019693,2.64250060938173,
8.86044257503091));
#380813=CARTESIAN_POINT('Ctrl Pts',(0.341631621181662,2.64249857443501,
8.86041778462583));
#380814=CARTESIAN_POINT('Ctrl Pts',(0.342049478211836,2.64248488176879,
8.86025097596201));
#380815=CARTESIAN_POINT('Ctrl Pts',(0.342435812155876,2.64250244638938,
8.8599848982295));
#380816=CARTESIAN_POINT('Ctrl Pts',(0.342779731744066,2.64254229188586,
8.85968173251461));
#380817=CARTESIAN_POINT('Ctrl Pts',(0.342961645501975,2.64256336787063,
8.85952137522076));
#380818=CARTESIAN_POINT('Ctrl Pts',(0.343135221051665,2.6425908941713,8.85934740853961));
#380819=CARTESIAN_POINT('Ctrl Pts',(0.343298254078606,2.64262294724038,
8.8591675900182));
#380820=CARTESIAN_POINT('Ctrl Pts',(0.343952916424662,2.64275165697361,
8.85844552518695));
#380821=CARTESIAN_POINT('Ctrl Pts',(0.344475170663011,2.64295766344042,
8.85759444184123));
#380822=CARTESIAN_POINT('Ctrl Pts',(0.34488590181332,2.64316387735285,8.85683498915137));
#380823=CARTESIAN_POINT('Ctrl Pts',(0.34492888373433,2.6431854570896,8.85675551444997));
#380824=CARTESIAN_POINT('Ctrl Pts',(0.344970632078586,2.64320705484434,
8.85667699793651));
#380825=CARTESIAN_POINT('Ctrl Pts',(0.345011162179579,2.64322859219911,
8.85659965593547));
#380826=CARTESIAN_POINT('Ctrl Pts',(0.345558239550962,2.64351930451273,
8.85555568965886));
#380827=CARTESIAN_POINT('Ctrl Pts',(0.346042030188672,2.64387770585479,
8.85434650606346));
#380828=CARTESIAN_POINT('Ctrl Pts',(0.346468625116245,2.64430057424927,
8.85297329937117));
#380829=CARTESIAN_POINT('Ctrl Pts',(0.346708558770194,2.64453841195541,
8.85220095427747));
#380830=CARTESIAN_POINT('Ctrl Pts',(0.346930275458148,2.64479696397218,
8.85137579139184));
#380831=CARTESIAN_POINT('Ctrl Pts',(0.34713356539705,2.64507775146798,8.85049129520029));
#380832=CARTESIAN_POINT('Origin',(0.341564846497265,2.64910949982511,7.59394543036555));
#380833=CARTESIAN_POINT('Ctrl Pts',(0.335359007864409,2.64609796642226,
7.59443877723642));
#380834=CARTESIAN_POINT('Ctrl Pts',(0.337454099980217,2.64069946823527,
7.58783886950016));
#380835=CARTESIAN_POINT('Ctrl Pts',(0.345864850211427,2.64185638745667,
7.58559994247159));
#380836=CARTESIAN_POINT('Ctrl Pts',(0.323921961471611,2.67556820963984,
7.56670252222135));
#380837=CARTESIAN_POINT('Ctrl Pts',(0.326014025584496,2.67017751381545,
7.56004874999031));
#380838=CARTESIAN_POINT('Ctrl Pts',(0.334477523915324,2.67132012191119,
7.55786368756705));
#380839=CARTESIAN_POINT('Ctrl Pts',(0.312506272620235,2.70498342012269,
7.53888913333558));
#380840=CARTESIAN_POINT('Ctrl Pts',(0.314610769972604,2.69956068712902,
7.53222002137279));
#380841=CARTESIAN_POINT('Ctrl Pts',(0.323109970911448,2.70072945918588,
7.53005029815326));
#380842=CARTESIAN_POINT('Ctrl Pts',(0.301112457877955,2.73434226681255,
7.51101258149734));
#380843=CARTESIAN_POINT('Ctrl Pts',(0.303242465562179,2.72885380044164,
7.5043616886572));
#380844=CARTESIAN_POINT('Ctrl Pts',(0.311762829927145,2.73008297603239,
7.50217374673251));
#380845=CARTESIAN_POINT('',(0.312368326987687,2.72851663429644,7.50366116523517));
#380846=CARTESIAN_POINT('Ctrl Pts',(0.304216449096259,2.72634410251322,
7.51860402984325));
#380847=CARTESIAN_POINT('Ctrl Pts',(0.304056675224763,2.72675579751655,
7.51734760759493));
#380848=CARTESIAN_POINT('Ctrl Pts',(0.303967762981066,2.72714934862238,
7.51608817408573));
#380849=CARTESIAN_POINT('Ctrl Pts',(0.30396294223283,2.7275267933776,7.5148100591312));
#380850=CARTESIAN_POINT('Ctrl Pts',(0.303958575483881,2.72786869185621,
7.51365231206384));
#380851=CARTESIAN_POINT('Ctrl Pts',(0.30402295092717,2.72819785354088,7.51247773061043));
#380852=CARTESIAN_POINT('Ctrl Pts',(0.304191193131457,2.72850149544917,
7.51129758471022));
#380853=CARTESIAN_POINT('Ctrl Pts',(0.304400298977402,2.72887888766396,
7.50983079813402));
#380854=CARTESIAN_POINT('Ctrl Pts',(0.30477457371949,2.72919850100536,7.50839324291155));
#380855=CARTESIAN_POINT('Ctrl Pts',(0.305370284589398,2.72939997663714,
7.50715379678855));
#380856=CARTESIAN_POINT('Ctrl Pts',(0.305645485846298,2.72949305257365,
7.50658120839351));
#380857=CARTESIAN_POINT('Ctrl Pts',(0.306010111959777,2.72956514658689,
7.50598221009429));
#380858=CARTESIAN_POINT('Ctrl Pts',(0.306459897374659,2.72959222844244,
7.50545747549611));
#380859=CARTESIAN_POINT('Ctrl Pts',(0.306699916794201,2.72960668015883,
7.50517746087247));
#380860=CARTESIAN_POINT('Ctrl Pts',(0.306966776843333,2.72960867296547,
7.50491486231392));
#380861=CARTESIAN_POINT('Ctrl Pts',(0.307253423074059,2.72959648611972,
7.50468370960993));
#380862=CARTESIAN_POINT('Ctrl Pts',(0.307682049606423,2.72957826294121,
7.50433806340447));
#380863=CARTESIAN_POINT('Ctrl Pts',(0.308167746650436,2.72952723189046,
7.50405484070984));
#380864=CARTESIAN_POINT('Ctrl Pts',(0.308677728555375,2.72944611734059,
7.50385766036131));
#380865=CARTESIAN_POINT('Ctrl Pts',(0.308732263193193,2.72943744340029,
7.50383657498791));
#380866=CARTESIAN_POINT('Ctrl Pts',(0.308787053675691,2.7294284435361,7.50381643264937));
#380867=CARTESIAN_POINT('Ctrl Pts',(0.308842044242109,2.72941913446201,
7.50379723213559));
#380868=CARTESIAN_POINT('Ctrl Pts',(0.30920912426162,2.72935699334723,7.50366906242519));
#380869=CARTESIAN_POINT('Ctrl Pts',(0.309592984844094,2.72927901316413,
7.50358235568538));
#380870=CARTESIAN_POINT('Ctrl Pts',(0.30996117243167,2.72919495596223,7.5035341175365));
#380871=CARTESIAN_POINT('Ctrl Pts',(0.310513228048452,2.72906892170143,
7.50346178989176));
#380872=CARTESIAN_POINT('Ctrl Pts',(0.311101755435278,2.72890986475049,
7.50346967198527));
#380873=CARTESIAN_POINT('Ctrl Pts',(0.311674702414449,2.72873594267221,
7.50354272648692));
#380874=CARTESIAN_POINT('Ctrl Pts',(0.311910367366282,2.72866440492144,
7.50357277531559));
#380875=CARTESIAN_POINT('Ctrl Pts',(0.312143124417423,2.72859058295185,
7.50361331098761));
#380876=CARTESIAN_POINT('Ctrl Pts',(0.312368326987848,2.72851663429785,
7.50366116523659));
#380877=CARTESIAN_POINT('',(0.341939261259435,2.65201338678241,7.57603338622103));
#380878=CARTESIAN_POINT('Origin',(0.343072133619939,2.66077740925045,7.58486873427624));
#380879=CARTESIAN_POINT('Ctrl Pts',(0.312368326962103,2.72851663434776,
7.50366116529969));
#380880=CARTESIAN_POINT('Ctrl Pts',(0.32221000012475,2.70305746570147,7.52783573079709));
#380881=CARTESIAN_POINT('Ctrl Pts',(0.332066529532574,2.67755759369531,
7.55196141284068));
#380882=CARTESIAN_POINT('Ctrl Pts',(0.341939260496553,2.65201338777521,
7.57603338728831));
#380883=CARTESIAN_POINT('Ctrl Pts',(0.334947412104083,2.64764449208613,
7.59639677331371));
#380884=CARTESIAN_POINT('Ctrl Pts',(0.338963550211397,2.62893435951653,
7.59974925422225));
#380885=CARTESIAN_POINT('Ctrl Pts',(0.347594250863814,2.64601386279729,
7.59639677331372));
#380886=CARTESIAN_POINT('Ctrl Pts',(0.3351423703935,2.64374871291513,7.58707626057423));
#380887=CARTESIAN_POINT('Ctrl Pts',(0.340281256478474,2.63915422911306,
7.58811717123965));
#380888=CARTESIAN_POINT('Ctrl Pts',(0.346417486467306,2.64229494768145,
7.58707626057423));
#380889=CARTESIAN_POINT('Ctrl Pts',(0.339276623241288,2.64820220431539,
7.58015376756929));
#380890=CARTESIAN_POINT('Ctrl Pts',(0.341165064355264,2.6460088684777,7.58208760766041));
#380891=CARTESIAN_POINT('Ctrl Pts',(0.343548093433272,2.64765145922139,
7.5801537675693));
#380892=CARTESIAN_POINT('Ctrl Pts',(0.341939261153406,2.65201338596166,
7.57603338509286));
#380893=CARTESIAN_POINT('Ctrl Pts',(0.341939261153406,2.65201338596166,
7.57603338509286));
#380894=CARTESIAN_POINT('Ctrl Pts',(0.341939261153406,2.65201338596166,
7.57603338509286));
#380895=CARTESIAN_POINT('Origin',(0.343066474116786,2.6607781389623,7.58486873427623));
#380896=CARTESIAN_POINT('Ctrl Pts',(0.402329817877834,2.72131574728531,
7.51098857897448));
#380897=CARTESIAN_POINT('Ctrl Pts',(0.398877281988015,2.71654704642435,
7.50433767179956));
#380898=CARTESIAN_POINT('Ctrl Pts',(0.390947339037891,2.71989727863872,
7.50214974420965));
#380899=CARTESIAN_POINT('Ctrl Pts',(0.383856321441241,2.69579984211485,
7.53887321589168));
#380900=CARTESIAN_POINT('Ctrl Pts',(0.380445153058535,2.69108827875312,
7.53220407452063));
#380901=CARTESIAN_POINT('Ctrl Pts',(0.372520354360726,2.69437468796706,
7.53003438070911));
#380902=CARTESIAN_POINT('Ctrl Pts',(0.365347349076903,2.67023493699404,
7.56669465659233));
#380903=CARTESIAN_POINT('Ctrl Pts',(0.361956340065153,2.6655512180958,7.560040858333));
#380904=CARTESIAN_POINT('Ctrl Pts',(0.354059446710206,2.66880325214652,
7.55785582193789));
#380905=CARTESIAN_POINT('Ctrl Pts',(0.346803737871547,2.6446221881212,7.59443891967696));
#380906=CARTESIAN_POINT('Ctrl Pts',(0.343407812318908,2.63993167841372,
7.58783901202978));
#380907=CARTESIAN_POINT('Ctrl Pts',(0.33556559484521,2.64318418561333,7.58560008491213));
#380908=CARTESIAN_POINT('',(0.389948473491269,2.71851378208007,7.50366116523517));
#380909=CARTESIAN_POINT('Ctrl Pts',(0.389948473491322,2.71851378208044,
7.50366116523554));
#380910=CARTESIAN_POINT('Ctrl Pts',(0.390704801700004,2.71855966407601,
7.50350835821027));
#380911=CARTESIAN_POINT('Ctrl Pts',(0.391401543613678,2.71857723441672,
7.50345484956));
#380912=CARTESIAN_POINT('Ctrl Pts',(0.39205939879719,2.71856761579381,7.50349758195599));
#380913=CARTESIAN_POINT('Ctrl Pts',(0.392396927294144,2.71856268072692,
7.50351950684424));
#380914=CARTESIAN_POINT('Ctrl Pts',(0.392757489109026,2.71855023130953,
7.50357029184312));
#380915=CARTESIAN_POINT('Ctrl Pts',(0.393104844734224,2.71852866929362,
7.50365515313924));
#380916=CARTESIAN_POINT('Ctrl Pts',(0.393639218343962,2.71849549818184,
7.50378570417639));
#380917=CARTESIAN_POINT('Ctrl Pts',(0.394158044509274,2.71844013313008,
7.50400001621911));
#380918=CARTESIAN_POINT('Ctrl Pts',(0.394621592111593,2.71836453062546,
7.50428903009635));
#380919=CARTESIAN_POINT('Ctrl Pts',(0.394673042329127,2.7183561393291,7.50432110841318));
#380920=CARTESIAN_POINT('Ctrl Pts',(0.394723838956284,2.71834751168814,
7.50435406373355));
#380921=CARTESIAN_POINT('Ctrl Pts',(0.3947739480228,2.71833865967342,7.50438785222352));
#380922=CARTESIAN_POINT('Ctrl Pts',(0.395079887959366,2.71828461386873,
7.50459414719562));
#380923=CARTESIAN_POINT('Ctrl Pts',(0.395364978925454,2.71822083575731,
7.50483629897752));
#380924=CARTESIAN_POINT('Ctrl Pts',(0.395618586479729,2.71815105294644,
7.5050991045531));
#380925=CARTESIAN_POINT('Ctrl Pts',(0.396178070216927,2.71799710505663,
7.50567888004914));
#380926=CARTESIAN_POINT('Ctrl Pts',(0.396606512880836,2.7178083682303,7.50637912803145));
#380927=CARTESIAN_POINT('Ctrl Pts',(0.396923327952554,2.71760889522423,
7.50710440483569));
#380928=CARTESIAN_POINT('Ctrl Pts',(0.3970010172978,2.71755998048305,7.50728225710686));
#380929=CARTESIAN_POINT('Ctrl Pts',(0.39707361848719,2.71750956990922,7.50746498566955));
#380930=CARTESIAN_POINT('Ctrl Pts',(0.397139674375009,2.71745918244111,
7.50764697238949));
#380931=CARTESIAN_POINT('Ctrl Pts',(0.397494772648854,2.71718831327952,
7.50862528291182));
#380932=CARTESIAN_POINT('Ctrl Pts',(0.397695467332306,2.71689681385543,
7.50965856837422));
#380933=CARTESIAN_POINT('Ctrl Pts',(0.397804459504203,2.71660622414456,
7.51067959873202));
#380934=CARTESIAN_POINT('Ctrl Pts',(0.397864438033874,2.71644631226014,
7.51124147302578));
#380935=CARTESIAN_POINT('Ctrl Pts',(0.397896254054879,2.71628648428327,
7.51180065547253));
#380936=CARTESIAN_POINT('Ctrl Pts',(0.397907780476768,2.71612946946488,
7.51235175716501));
#380937=CARTESIAN_POINT('Ctrl Pts',(0.397947608855977,2.71558692072005,
7.51425603304536));
#380938=CARTESIAN_POINT('Ctrl Pts',(0.397743884464762,2.71501282769615,
7.51626900505181));
#380939=CARTESIAN_POINT('Ctrl Pts',(0.397348564351696,2.71443790085555,
7.51827788969244));
#380940=CARTESIAN_POINT('Ctrl Pts',(0.397327168880126,2.71440678472847,
7.51838661432546));
#380941=CARTESIAN_POINT('Ctrl Pts',(0.397305202528421,2.71437566373297,
7.51849533314857));
#380942=CARTESIAN_POINT('Ctrl Pts',(0.39728267045427,2.71434454205174,7.51860402984325));
#380943=CARTESIAN_POINT('Ctrl Pts',(0.341939262249588,2.65201338755038,
7.57603338728985));
#380944=CARTESIAN_POINT('Ctrl Pts',(0.357968509122732,2.67421790325761,
7.55196141284922));
#380945=CARTESIAN_POINT('Ctrl Pts',(0.373970838822828,2.69638364460998,
7.52783573083104));
#380946=CARTESIAN_POINT('Ctrl Pts',(0.389948473530171,2.71851378212467,
7.50366116530176));
#380947=CARTESIAN_POINT('Origin',(1.1815582111519E-16,9.16393216063564E-16,
7.49482233047033));
#380948=CARTESIAN_POINT('Origin',(0.311362998732826,2.71973515861749,7.49482233047033));
#380949=CARTESIAN_POINT('Origin',(0.,0.,7.50366116523517));
#380950=CARTESIAN_POINT('Origin',(0.388693460788409,2.70976449964574,7.49482233047033));
#380951=CARTESIAN_POINT('Ctrl Pts',(0.304216831735178,2.72634311643025,
7.51860402984325));
#380952=CARTESIAN_POINT('Ctrl Pts',(0.301464528298415,2.73343685393752,
7.51860402984325));
#380953=CARTESIAN_POINT('Ctrl Pts',(0.293899145873092,2.73425004197771,
7.51860402984325));
#380954=CARTESIAN_POINT('Ctrl Pts',(0.303194881501727,2.72897706911724,
7.51041458714366));
#380955=CARTESIAN_POINT('Ctrl Pts',(0.299672201491318,2.73362949765557,
7.51004642900443));
#380956=CARTESIAN_POINT('Ctrl Pts',(0.29389705943045,2.73425026624531,7.5072913648301));
#380957=CARTESIAN_POINT('Ctrl Pts',(0.305306847737879,2.73083807309806,
7.50215815450138));
#380958=CARTESIAN_POINT('Ctrl Pts',(0.303321572720914,2.73323739541665,
7.49877163671529));
#380959=CARTESIAN_POINT('Ctrl Pts',(0.299893758158875,2.73362983767055,
7.4948158853317));
#380960=CARTESIAN_POINT('Ctrl Pts',(0.312368264372289,2.72851608735092,
7.50366171572174));
#380961=CARTESIAN_POINT('Ctrl Pts',(0.312784747585871,2.73215404062027,
7.50000045605858));
#380962=CARTESIAN_POINT('Ctrl Pts',(0.312784747585747,2.73215404062028,
7.49482233047317));
#380963=CARTESIAN_POINT('Origin',(0.292563240664578,2.72182163269599,7.51860402984325));
#380964=CARTESIAN_POINT('Origin',(0.292563240664578,2.72182163269599,9.));
#380965=CARTESIAN_POINT('Origin',(0.292563240664578,2.72182163269599,8.75721825406948));
#380966=CARTESIAN_POINT('Ctrl Pts',(0.310258498896826,2.71077525492426,
8.78942910404912));
#380967=CARTESIAN_POINT('Ctrl Pts',(0.308261245270224,2.71597750507709,
8.79672699501689));
#380968=CARTESIAN_POINT('Ctrl Pts',(0.299482479215855,2.71436296100999,
8.79893251111267));
#380969=CARTESIAN_POINT('Ctrl Pts',(0.306280778989386,2.72102479945456,
8.78111911759584));
#380970=CARTESIAN_POINT('Ctrl Pts',(0.303906062384031,2.72718945931294,
8.78644465894816));
#380971=CARTESIAN_POINT('Ctrl Pts',(0.295804309956124,2.72746716306224,
8.78817647674132));
#380972=CARTESIAN_POINT('Ctrl Pts',(0.303801769035835,2.72741256006903,
8.76780923932029));
#380973=CARTESIAN_POINT('Ctrl Pts',(0.300993761175014,2.73468784897217,
8.76988516158371));
#380974=CARTESIAN_POINT('Ctrl Pts',(0.293496231764001,2.73564880325158,
8.77093053738832));
#380975=CARTESIAN_POINT('Ctrl Pts',(0.304285142047523,2.72616703417123,
8.75371302330492));
#380976=CARTESIAN_POINT('Ctrl Pts',(0.301546762679073,2.7332640391594,8.7530082828756));
#380977=CARTESIAN_POINT('Ctrl Pts',(0.293945960387518,2.73405292689471,
8.75267964240738));
#380978=CARTESIAN_POINT('Origin',(0.297636576658702,2.70874898784203,8.78727029226991));
#380979=CARTESIAN_POINT('Ctrl Pts',(0.335155581859841,2.64662214142563,
8.85049129520029));
#380980=CARTESIAN_POINT('Ctrl Pts',(0.333042822978375,2.6520661621945,8.85711686593484));
#380981=CARTESIAN_POINT('Ctrl Pts',(0.324576590381406,2.65087298671372,
8.85933012996512));
#380982=CARTESIAN_POINT('Ctrl Pts',(0.326521105202062,2.66887090377405,
8.82945683644721));
#380983=CARTESIAN_POINT('Ctrl Pts',(0.324390809144477,2.67436011320681,
8.83607469902387));
#380984=CARTESIAN_POINT('Ctrl Pts',(0.315904953537504,2.67312629915468,
8.8382956714852));
#380985=CARTESIAN_POINT('Ctrl Pts',(0.317899498928018,2.69108650254807,
8.80838214965002));
#380986=CARTESIAN_POINT('Ctrl Pts',(0.31576079572757,2.69659737496415,8.81501364461992));
#380987=CARTESIAN_POINT('Ctrl Pts',(0.307247094031156,2.69534609720933,
8.81722098428721));
#380988=CARTESIAN_POINT('Ctrl Pts',(0.309289785090383,2.71327145765926,
8.78727029226991));
#380989=CARTESIAN_POINT('Ctrl Pts',(0.307150726644314,2.71878324544933,
8.79393457792714));
#380990=CARTESIAN_POINT('Ctrl Pts',(0.298601974927864,2.71753494289438,
8.79610912703474));
#380991=CARTESIAN_POINT('Origin',(0.32350237342816,2.64209967160839,8.85049129520029));
#380992=CARTESIAN_POINT('Ctrl Pts',(0.34713356539705,2.64507775146798,8.85049129520029));
#380993=CARTESIAN_POINT('Ctrl Pts',(0.350558127032854,2.64980781381701,
8.85711686593484));
#380994=CARTESIAN_POINT('Ctrl Pts',(0.358444815903088,2.64650616259708,
8.85933012996512));
#380995=CARTESIAN_POINT('Ctrl Pts',(0.344103905151925,2.64089313358697,
8.86332496987232));
#380996=CARTESIAN_POINT('Ctrl Pts',(0.34871431708389,2.64058330106072,8.86648636486737));
#380997=CARTESIAN_POINT('Ctrl Pts',(0.349955340466956,2.63480957065002,
8.87206031107457));
#380998=CARTESIAN_POINT('Ctrl Pts',(0.33703741045343,2.64177316692275,8.86341338519876));
#380999=CARTESIAN_POINT('Ctrl Pts',(0.332480810620154,2.64261629715804,
8.86654584966058));
#381000=CARTESIAN_POINT('Ctrl Pts',(0.329859545232487,2.6373009307027,8.87215952290714));
#381001=CARTESIAN_POINT('Ctrl Pts',(0.335155581859841,2.64662214142563,
8.85049129520029));
#381002=CARTESIAN_POINT('Ctrl Pts',(0.333042822978374,2.6520661621945,8.85711686593484));
#381003=CARTESIAN_POINT('Ctrl Pts',(0.324576590381406,2.65087298671372,
8.85933012996512));
#381004=CARTESIAN_POINT('Origin',(0.357258508851204,2.63774729990957,8.85049129520029));
#381005=CARTESIAN_POINT('Ctrl Pts',(0.389059322317652,2.7029863147688,8.78727029226991));
#381006=CARTESIAN_POINT('Ctrl Pts',(0.392526512802761,2.7077752568042,8.79393457792714));
#381007=CARTESIAN_POINT('Ctrl Pts',(0.40047903875831,2.70439935009569,8.79610912703474));
#381008=CARTESIAN_POINT('Ctrl Pts',(0.375103874792494,2.68371081503406,
8.80838214965003));
#381009=CARTESIAN_POINT('Ctrl Pts',(0.378570489461518,2.68849896174254,
8.81501364461987));
#381010=CARTESIAN_POINT('Ctrl Pts',(0.38648835703967,2.68512906773677,8.81722098428722));
#381011=CARTESIAN_POINT('Ctrl Pts',(0.361129150869144,2.66440869041269,
8.82945683644722));
#381012=CARTESIAN_POINT('Ctrl Pts',(0.364582138437037,2.66917801513908,
8.83607469902391));
#381013=CARTESIAN_POINT('Ctrl Pts',(0.372477500384153,2.66583207697138,
8.8382956714852));
#381014=CARTESIAN_POINT('Ctrl Pts',(0.34713356539705,2.64507775146798,8.85049129520029));
#381015=CARTESIAN_POINT('Ctrl Pts',(0.350558127032854,2.64980781381701,
8.85711686593484));
#381016=CARTESIAN_POINT('Ctrl Pts',(0.358444815903088,2.64650616259708,
8.85933012996512));
#381017=CARTESIAN_POINT('Origin',(0.399184265771806,2.69565586321039,8.78727029226991));
#381018=CARTESIAN_POINT('Ctrl Pts',(0.397174100220844,2.71419455155609,
8.75374538247847));
#381019=CARTESIAN_POINT('Ctrl Pts',(0.401619776138006,2.72035737104292,
8.75304829418601));
#381020=CARTESIAN_POINT('Ctrl Pts',(0.409164941549523,2.71919930277122,
8.75272238421917));
#381021=CARTESIAN_POINT('Ctrl Pts',(0.397948185988952,2.71526373261546,
8.76769408445021));
#381022=CARTESIAN_POINT('Ctrl Pts',(0.402506294519329,2.72158123224723,
8.76974318093972));
#381023=CARTESIAN_POINT('Ctrl Pts',(0.409995042726933,2.7206132407373,8.7707786988043));
#381024=CARTESIAN_POINT('Ctrl Pts',(0.393980663297225,2.70978371958609,
8.78108014887987));
#381025=CARTESIAN_POINT('Ctrl Pts',(0.397840414937049,2.71513979600258,
8.78639403366322));
#381026=CARTESIAN_POINT('Ctrl Pts',(0.405740331578681,2.71337531512024,
8.78812224174741));
#381027=CARTESIAN_POINT('Ctrl Pts',(0.387478769473589,2.70080318793564,
8.78944554828686));
#381028=CARTESIAN_POINT('Ctrl Pts',(0.390727083660423,2.70532036322122,
8.79673892988687));
#381029=CARTESIAN_POINT('Ctrl Pts',(0.398801680886371,2.70153824292232,
8.79894799272499));
#381030=CARTESIAN_POINT('Origin',(0.407407613908421,2.70701409049334,8.75721825406948));
#381031=CARTESIAN_POINT('Origin',(0.407407613908421,2.70701409049334,9.));
#381032=CARTESIAN_POINT('Origin',(0.40740761390842,2.70701409049334,7.51860402984325));
#381033=CARTESIAN_POINT('Ctrl Pts',(0.389948361794135,2.71851300338654,
7.50366195182966));
#381034=CARTESIAN_POINT('Ctrl Pts',(0.390468316773883,2.72213785352538,
7.50000065167736));
#381035=CARTESIAN_POINT('Ctrl Pts',(0.390468316773998,2.72213785352537,
7.49482233047108));
#381036=CARTESIAN_POINT('Ctrl Pts',(0.397374485980921,2.7189674031765,7.50215800491337));
#381037=CARTESIAN_POINT('Ctrl Pts',(0.399905086144918,2.7207842025557,7.49877273257266));
#381038=CARTESIAN_POINT('Ctrl Pts',(0.403322237117531,2.72029406422793,
7.49481816995647));
#381039=CARTESIAN_POINT('Ctrl Pts',(0.398935316024003,2.71662778228441,
7.51043025814043));
#381040=CARTESIAN_POINT('Ctrl Pts',(0.403523181590999,2.72023946423693,
7.51006209594515));
#381041=CARTESIAN_POINT('Ctrl Pts',(0.409270426317654,2.71937450862293,
7.50731281821701));
#381042=CARTESIAN_POINT('Ctrl Pts',(0.397281784184358,2.71434331776496,
7.51860402984326));
#381043=CARTESIAN_POINT('Ctrl Pts',(0.401743390778344,2.72050733301407,
7.51860402984326));
#381044=CARTESIAN_POINT('Ctrl Pts',(0.409267922647734,2.71937488542709,
7.51860402984327));
#381045=CARTESIAN_POINT('Origin',(0.,0.,7.5));
#381046=CARTESIAN_POINT('Origin',(0.515891055659628,2.61740223164621,7.5));
#381047=CARTESIAN_POINT('',(0.515891055659628,2.61740223164621,7.59394543036555));
#381048=CARTESIAN_POINT('',(0.515891055659628,2.61740223164621,8.85049129520029));
#381049=CARTESIAN_POINT('',(0.515891055659628,2.61740223164621,7.5));
#381050=CARTESIAN_POINT('',(0.561440886005564,2.67250562312429,8.78727029226991));
#381051=CARTESIAN_POINT('Ctrl Pts',(0.515891055659628,2.61740223164621,
8.85049129520029));
#381052=CARTESIAN_POINT('Ctrl Pts',(0.531096402804831,2.63579672817757,
8.82945686509571));
#381053=CARTESIAN_POINT('Ctrl Pts',(0.546279145362893,2.6541638790656,8.80838212259895));
#381054=CARTESIAN_POINT('Ctrl Pts',(0.561440886005564,2.67250562312429,
8.78727029226991));
#381055=CARTESIAN_POINT('',(0.57037506251209,2.68331364198703,8.75721825406948));
#381056=CARTESIAN_POINT('Origin',(0.543488870575911,2.65078869247541,8.75937679713127));
#381057=CARTESIAN_POINT('',(0.57037506251209,2.68331364198703,7.51860402984325));
#381058=CARTESIAN_POINT('',(0.57037506251209,2.68331364198703,7.5));
#381059=CARTESIAN_POINT('Ctrl Pts',(0.57037506251209,2.68331364198703,7.51860402984325));
#381060=CARTESIAN_POINT('Ctrl Pts',(0.563358656393491,2.67482562413524,
7.52834476460825));
#381061=CARTESIAN_POINT('Ctrl Pts',(0.556337695325281,2.66633209598475,
7.53807742314407));
#381062=CARTESIAN_POINT('Ctrl Pts',(0.549312026368974,2.65783287251993,
7.54780169004674));
#381063=CARTESIAN_POINT('Ctrl Pts',(0.538183746447192,2.6443705618955,7.5632044032688));
#381064=CARTESIAN_POINT('Ctrl Pts',(0.52704364089139,2.63089394534418,7.57858609112103));
#381065=CARTESIAN_POINT('Ctrl Pts',(0.515891055659629,2.61740223164621,
7.59394543036555));
#381066=CARTESIAN_POINT('Origin',(0.421172437192753,2.88192934915565,7.5));
#381067=CARTESIAN_POINT('',(0.478268870165622,2.70125132133977,8.75721825406948));
#381068=CARTESIAN_POINT('',(0.482494215215309,2.68788048588352,8.78727029226991));
#381069=CARTESIAN_POINT('Origin',(0.493219716926182,2.65394031842374,8.75658640621087));
#381070=CARTESIAN_POINT('',(0.504036631578554,2.61971088052921,8.85049129520029));
#381071=CARTESIAN_POINT('Ctrl Pts',(0.482494215215309,2.68788048588352,
8.78727029226991));
#381072=CARTESIAN_POINT('Ctrl Pts',(0.489664835330364,2.66518951495684,
8.80838212259895));
#381073=CARTESIAN_POINT('Ctrl Pts',(0.496845388127988,2.6424671126884,8.82945686509571));
#381074=CARTESIAN_POINT('Ctrl Pts',(0.504036631578554,2.61971088052921,
8.85049129520029));
#381075=CARTESIAN_POINT('',(0.504036631578554,2.61971088052921,7.59394543036555));
#381076=CARTESIAN_POINT('',(0.504036631578554,2.61971088052921,7.5));
#381077=CARTESIAN_POINT('',(0.478268870165622,2.70125132133977,7.51860402984325));
#381078=CARTESIAN_POINT('Ctrl Pts',(0.504036631578554,2.61971088052921,
7.59394543036555));
#381079=CARTESIAN_POINT('Ctrl Pts',(0.498762108429631,2.63640177329775,
7.57858609112103));
#381080=CARTESIAN_POINT('Ctrl Pts',(0.493493487440537,2.65307398905726,
7.56320440326857));
#381081=CARTESIAN_POINT('Ctrl Pts',(0.488230459287388,2.66972850664335,
7.54780169004651));
#381082=CARTESIAN_POINT('Ctrl Pts',(0.484907727133662,2.68024308104383,
7.53807742314383));
#381083=CARTESIAN_POINT('Ctrl Pts',(0.481587221536694,2.69075060964715,
7.52834476460825));
#381084=CARTESIAN_POINT('Ctrl Pts',(0.478268870165622,2.70125132133977,
7.51860402984325));
#381085=CARTESIAN_POINT('',(0.478268870165622,2.70125132133977,7.5));
#381086=CARTESIAN_POINT('Origin',(0.510592093294214,2.62178248538886,7.5));
#381087=CARTESIAN_POINT('Ctrl Pts',(0.504036631578554,2.61971088052921,
8.85049129520029));
#381088=CARTESIAN_POINT('Ctrl Pts',(0.504094986504631,2.61952622008007,
8.85097269580138));
#381089=CARTESIAN_POINT('Ctrl Pts',(0.504160625639675,2.61934642402759,
8.85143669361005));
#381090=CARTESIAN_POINT('Ctrl Pts',(0.504237392721289,2.61916351316932,
8.8519052845931));
#381091=CARTESIAN_POINT('Ctrl Pts',(0.504387544264533,2.61880575113034,
8.85282181883899));
#381092=CARTESIAN_POINT('Ctrl Pts',(0.504576586788838,2.61844535224755,
8.85372622499636));
#381093=CARTESIAN_POINT('Ctrl Pts',(0.504821141016025,2.61808382343919,
8.85462257735071));
#381094=CARTESIAN_POINT('Ctrl Pts',(0.505024161249691,2.61778369506278,
8.85536669723986));
#381095=CARTESIAN_POINT('Ctrl Pts',(0.505265458768457,2.61748270182885,
8.85610498449051));
#381096=CARTESIAN_POINT('Ctrl Pts',(0.50556080719274,2.61718668585866,8.85681338218371));
#381097=CARTESIAN_POINT('Ctrl Pts',(0.50582883635163,2.61691805090081,8.85745625420285));
#381098=CARTESIAN_POINT('Ctrl Pts',(0.506144318101219,2.61664972254578,
8.85808743050666));
#381099=CARTESIAN_POINT('Ctrl Pts',(0.506533369387132,2.61639335202954,
8.8586680450841));
#381100=CARTESIAN_POINT('Ctrl Pts',(0.506712869216856,2.61627506823078,
8.85893592806395));
#381101=CARTESIAN_POINT('Ctrl Pts',(0.506908237766501,2.61615945434576,
8.85919241173848));
#381102=CARTESIAN_POINT('Ctrl Pts',(0.507123281853302,2.61604865749327,
8.85943017985534));
#381103=CARTESIAN_POINT('Ctrl Pts',(0.507413655030347,2.61589904894304,
8.8597512372));
#381104=CARTESIAN_POINT('Ctrl Pts',(0.507747586735331,2.61575498477418,
8.86004599534705));
#381105=CARTESIAN_POINT('Ctrl Pts',(0.508125190597089,2.61562775896039,
8.86026130871721));
#381106=CARTESIAN_POINT('Ctrl Pts',(0.508263442016658,2.61558117800309,
8.86034014101235));
#381107=CARTESIAN_POINT('Ctrl Pts',(0.508409620434265,2.61553614284821,
8.86040910639692));
#381108=CARTESIAN_POINT('Ctrl Pts',(0.50855984234006,2.6154942019216,8.86046313645506));
#381109=CARTESIAN_POINT('Ctrl Pts',(0.508794262365954,2.61542875345688,
8.86054744990829));
#381110=CARTESIAN_POINT('Ctrl Pts',(0.509044967329408,2.61536919493122,
8.86059655985668));
#381111=CARTESIAN_POINT('Ctrl Pts',(0.509295811046165,2.6153190609893,8.86059725258815));
#381112=CARTESIAN_POINT('Ctrl Pts',(0.50954723431212,2.61526881121795,8.86059794692011));
#381113=CARTESIAN_POINT('Ctrl Pts',(0.509802105972853,2.61523007760143,
8.86056369958366));
#381114=CARTESIAN_POINT('Ctrl Pts',(0.510045959806687,2.61520125230873,
8.86048590497774));
#381115=CARTESIAN_POINT('Ctrl Pts',(0.510109598396914,2.61519372976556,
8.86046560290182));
#381116=CARTESIAN_POINT('Ctrl Pts',(0.510173325147798,2.61518687412201,
8.86044257503091));
#381117=CARTESIAN_POINT('Ctrl Pts',(0.510235167338841,2.61518086458528,
8.86041778462583));
#381118=CARTESIAN_POINT('Ctrl Pts',(0.510651288544795,2.61514042786026,
8.860250975962));
#381119=CARTESIAN_POINT('Ctrl Pts',(0.511037954093418,2.61513320389167,
8.8599848982295));
#381120=CARTESIAN_POINT('Ctrl Pts',(0.511383719971653,2.61515093251764,
8.85968173251461));
#381121=CARTESIAN_POINT('Ctrl Pts',(0.511566610311217,2.61516030994504,
8.85952137522076));
#381122=CARTESIAN_POINT('Ctrl Pts',(0.511741592847463,2.61517665866632,
8.85934740853961));
#381123=CARTESIAN_POINT('Ctrl Pts',(0.511906344552753,2.61519820031704,
8.8591675900182));
#381124=CARTESIAN_POINT('Ctrl Pts',(0.512567908285739,2.61528470124179,
8.85844552518694));
#381125=CARTESIAN_POINT('Ctrl Pts',(0.513102288376397,2.6154568235023,8.8575944418412));
#381126=CARTESIAN_POINT('Ctrl Pts',(0.513525387806243,2.61563629809098,
8.85683498915133));
#381127=CARTESIAN_POINT('Ctrl Pts',(0.513569664034758,2.6156550796287,8.85675551444994));
#381128=CARTESIAN_POINT('Ctrl Pts',(0.513612710375454,2.61567395818294,
8.85667699793649));
#381129=CARTESIAN_POINT('Ctrl Pts',(0.513654537106058,2.61569285451441,
8.85659965593547));
#381130=CARTESIAN_POINT('Ctrl Pts',(0.514219116450193,2.61594791816087,
8.85555568965886));
#381131=CARTESIAN_POINT('Ctrl Pts',(0.514724875940979,2.61627458655636,
8.85434650606346));
#381132=CARTESIAN_POINT('Ctrl Pts',(0.515177687654578,2.61666925409151,
8.85297329937117));
#381133=CARTESIAN_POINT('Ctrl Pts',(0.515432366653254,2.61689123053259,
8.85220095427747));
#381134=CARTESIAN_POINT('Ctrl Pts',(0.515670193285084,2.61713504588954,
8.85137579139183));
#381135=CARTESIAN_POINT('Ctrl Pts',(0.515891055659628,2.61740223164621,
8.85049129520029));
#381136=CARTESIAN_POINT('Origin',(0.510592093294214,2.62178248538886,7.59394543036555));
#381137=CARTESIAN_POINT('Ctrl Pts',(0.504206055614804,2.61917474895075,
7.59443877723642));
#381138=CARTESIAN_POINT('Ctrl Pts',(0.505950960172756,2.61365310954453,
7.58783886950015));
#381139=CARTESIAN_POINT('Ctrl Pts',(0.514418553684581,2.61426877313379,
7.58559994247159));
#381140=CARTESIAN_POINT('Ctrl Pts',(0.494680672826266,2.6493172164713,7.56670252222138));
#381141=CARTESIAN_POINT('Ctrl Pts',(0.496423055501803,2.64380355740166,
7.56004874999028));
#381142=CARTESIAN_POINT('Ctrl Pts',(0.504942371819573,2.64440155968669,
7.55786368756704));
#381143=CARTESIAN_POINT('Ctrl Pts',(0.485173077738388,2.67940339594535,
7.53888913333558));
#381144=CARTESIAN_POINT('Ctrl Pts',(0.486925815479428,2.67385696892987,
7.53222002137275));
#381145=CARTESIAN_POINT('Ctrl Pts',(0.495482437381201,2.67447879394539,
7.53005029815327));
#381146=CARTESIAN_POINT('Ctrl Pts',(0.475683700576278,2.70943192595292,
7.51101258149734));
#381147=CARTESIAN_POINT('Ctrl Pts',(0.477457684683531,2.70381826616392,
7.5043616886572));
#381148=CARTESIAN_POINT('Ctrl Pts',(0.486039296596597,2.70449901466241,
7.50217374673251));
#381149=CARTESIAN_POINT('',(0.486543193738902,2.70289709681368,7.50366116523517));
#381150=CARTESIAN_POINT('Ctrl Pts',(0.478268870165621,2.70125132133977,
7.51860402984325));
#381151=CARTESIAN_POINT('Ctrl Pts',(0.478135801956109,2.70167240721866,
7.51734760759494));
#381152=CARTESIAN_POINT('Ctrl Pts',(0.478072287298077,2.70207084635854,
7.51608817408573));
#381153=CARTESIAN_POINT('Ctrl Pts',(0.478091659423082,2.70244782447943,
7.5148100591312));
#381154=CARTESIAN_POINT('Ctrl Pts',(0.478109207156824,2.70278930026952,
7.51365231206384));
#381155=CARTESIAN_POINT('Ctrl Pts',(0.478194539795407,2.70311366110739,
7.51247773061043));
#381156=CARTESIAN_POINT('Ctrl Pts',(0.478381890731902,2.70340589983578,
7.51129758471022));
#381157=CARTESIAN_POINT('Ctrl Pts',(0.47861474654968,2.70376911920024,7.50983079813402));
#381158=CARTESIAN_POINT('Ctrl Pts',(0.479008730001262,2.70406409599669,
7.50839324291155));
#381159=CARTESIAN_POINT('Ctrl Pts',(0.479616125507346,2.7042269903487,7.50715379678855));
#381160=CARTESIAN_POINT('Ctrl Pts',(0.479896724729476,2.70430224284564,
7.50658120839351));
#381161=CARTESIAN_POINT('Ctrl Pts',(0.480265220758786,2.7043508270587,7.50598221009429));
#381162=CARTESIAN_POINT('Ctrl Pts',(0.480715817181737,2.7043490354212,7.50545747549611));
#381163=CARTESIAN_POINT('Ctrl Pts',(0.480956269380287,2.70434807934798,
7.50517746087247));
#381164=CARTESIAN_POINT('Ctrl Pts',(0.481222708816388,2.70433297027813,
7.50491486231392));
#381165=CARTESIAN_POINT('Ctrl Pts',(0.481507985287802,2.70430244298451,
7.50468370960993));
#381166=CARTESIAN_POINT('Ctrl Pts',(0.481934563597929,2.70425679505125,
7.50433806340447));
#381167=CARTESIAN_POINT('Ctrl Pts',(0.482415993154627,2.70417475013281,
7.50405484070984));
#381168=CARTESIAN_POINT('Ctrl Pts',(0.482919730219993,2.70406112758865,
7.50385766036131));
#381169=CARTESIAN_POINT('Ctrl Pts',(0.482973597069285,2.70404897742364,
7.50383657498791));
#381170=CARTESIAN_POINT('Ctrl Pts',(0.483027698355582,2.70403648561238,
7.50381643264937));
#381171=CARTESIAN_POINT('Ctrl Pts',(0.483081979503558,2.70402367240709,
7.50379723213559));
#381172=CARTESIAN_POINT('Ctrl Pts',(0.483444323922905,2.70393814007029,
7.50366906242519));
#381173=CARTESIAN_POINT('Ctrl Pts',(0.483822399615159,2.70383572607388,
7.50358235568538));
#381174=CARTESIAN_POINT('Ctrl Pts',(0.484184445158432,2.70372825171679,
7.5035341175365));
#381175=CARTESIAN_POINT('Ctrl Pts',(0.484727291474926,2.70356710608208,
7.50346178989176));
#381176=CARTESIAN_POINT('Ctrl Pts',(0.485304418855281,2.70337066885157,
7.50346967198527));
#381177=CARTESIAN_POINT('Ctrl Pts',(0.48586504542762,2.70316039527586,7.50354272648692));
#381178=CARTESIAN_POINT('Ctrl Pts',(0.486095642741106,2.70307390540177,
7.50357277531559));
#381179=CARTESIAN_POINT('Ctrl Pts',(0.486323191778091,2.70298532231186,
7.50361331098761));
#381180=CARTESIAN_POINT('Ctrl Pts',(0.486543193739153,2.70289709681507,
7.50366116523659));
#381181=CARTESIAN_POINT('',(0.511151791457249,2.62465641716279,7.57603338622103));
#381182=CARTESIAN_POINT('Origin',(0.512843849057291,2.63332984962507,7.58486873427626));
#381183=CARTESIAN_POINT('Ctrl Pts',(0.486543193716658,2.70289709686654,
7.50366116529969));
#381184=CARTESIAN_POINT('Ctrl Pts',(0.494733471570576,2.67685967864821,
7.52783573079709));
#381185=CARTESIAN_POINT('Ctrl Pts',(0.502935967272698,2.65078068885653,
7.55196141284069));
#381186=CARTESIAN_POINT('Ctrl Pts',(0.511151790759542,2.62465641820243,
7.57603338728831));
#381187=CARTESIAN_POINT('Ctrl Pts',(0.503894391761599,2.62074446814269,
7.59639677331371));
#381188=CARTESIAN_POINT('Ctrl Pts',(0.506703515972806,2.60181546269511,
7.59974925422224));
#381189=CARTESIAN_POINT('Ctrl Pts',(0.516410771457479,2.61830690341518,
7.59639677331372));
#381190=CARTESIAN_POINT('Ctrl Pts',(0.503839346059811,2.61684420224733,
7.58707626057421));
#381191=CARTESIAN_POINT('Ctrl Pts',(0.508673304164263,2.61192990874306,
7.58811717123965));
#381192=CARTESIAN_POINT('Ctrl Pts',(0.514998153140065,2.61467102476307,
7.58707626057424));
#381193=CARTESIAN_POINT('Ctrl Pts',(0.508250440815437,2.62102366098245,
7.58015376756929));
#381194=CARTESIAN_POINT('Ctrl Pts',(0.509994474415054,2.61871383875087,
7.5820876076604));
#381195=CARTESIAN_POINT('Ctrl Pts',(0.512477848454474,2.62020037341847,
7.5801537675693));
#381196=CARTESIAN_POINT('Ctrl Pts',(0.511151791298856,2.62465641635052,
7.57603338509286));
#381197=CARTESIAN_POINT('Ctrl Pts',(0.511151791298856,2.62465641635052,
7.57603338509286));
#381198=CARTESIAN_POINT('Ctrl Pts',(0.511151791298856,2.62465641635052,
7.57603338509286));
#381199=CARTESIAN_POINT('Origin',(0.512838247935124,2.63333094044375,7.58486873427622));
#381200=CARTESIAN_POINT('Ctrl Pts',(0.575858486682816,2.68994715228608,
7.51098857897448));
#381201=CARTESIAN_POINT('Ctrl Pts',(0.572107512685082,2.68540945396643,
7.50433767179956));
#381202=CARTESIAN_POINT('Ctrl Pts',(0.564408512768194,2.68926087595866,
7.50214974420965));
#381203=CARTESIAN_POINT('Ctrl Pts',(0.555788136368668,2.6656672732599,7.53887321589171));
#381204=CARTESIAN_POINT('Ctrl Pts',(0.552082105696194,2.66118394461906,
7.53220407452063));
#381205=CARTESIAN_POINT('Ctrl Pts',(0.544384150308548,2.66497134514866,
7.53003438070911));
#381206=CARTESIAN_POINT('Ctrl Pts',(0.535679243578228,2.64134076790945,
7.56669465659231));
#381207=CARTESIAN_POINT('Ctrl Pts',(0.531995114858024,2.63688393490738,
7.56004085833299));
#381208=CARTESIAN_POINT('Ctrl Pts',(0.524322805054424,2.64063524299977,
7.55785582193788));
#381209=CARTESIAN_POINT('Ctrl Pts',(0.515532717756307,2.61696873642531,
7.59443891967696));
#381210=CARTESIAN_POINT('Ctrl Pts',(0.511843247508148,2.61250544157026,
7.58783901202978));
#381211=CARTESIAN_POINT('Ctrl Pts',(0.504225531563093,2.61625371874368,
7.58560008491213));
#381212=CARTESIAN_POINT('',(0.563323058569111,2.68794421947737,7.50366116523517));
#381213=CARTESIAN_POINT('Ctrl Pts',(0.563323058569187,2.68794421947773,
7.50366116523554));
#381214=CARTESIAN_POINT('Ctrl Pts',(0.564080772489997,2.68794154908911,
7.50350835821027));
#381215=CARTESIAN_POINT('Ctrl Pts',(0.564777208608279,2.687914442922,7.50345484956));
#381216=CARTESIAN_POINT('Ctrl Pts',(0.565433095890476,2.68786269513526,
7.50349758195598));
#381217=CARTESIAN_POINT('Ctrl Pts',(0.565769614708112,2.68783614468294,
7.50351950684424));
#381218=CARTESIAN_POINT('Ctrl Pts',(0.566128638073164,2.68780061956941,
7.50357029184312));
#381219=CARTESIAN_POINT('Ctrl Pts',(0.566473898535874,2.68775684670367,
7.50365515313924));
#381220=CARTESIAN_POINT('Ctrl Pts',(0.56700504893729,2.68768950631076,7.50378570417639));
#381221=CARTESIAN_POINT('Ctrl Pts',(0.567519261867555,2.6876010137059,7.50400001621911));
#381222=CARTESIAN_POINT('Ctrl Pts',(0.567977013192507,2.68749586693788,
7.50428903009635));
#381223=CARTESIAN_POINT('Ctrl Pts',(0.568027820067849,2.68748419645558,
7.50432110841318));
#381224=CARTESIAN_POINT('Ctrl Pts',(0.568077959553033,2.68747233198995,
7.50435406373354));
#381225=CARTESIAN_POINT('Ctrl Pts',(0.568127398514568,2.68746028766373,
7.50438785222352));
#381226=CARTESIAN_POINT('Ctrl Pts',(0.568429247138127,2.68738675126291,
7.50459414719561));
#381227=CARTESIAN_POINT('Ctrl Pts',(0.568709666076621,2.68730483834955,
7.50483629897752));
#381228=CARTESIAN_POINT('Ctrl Pts',(0.568958281566933,2.68721895022316,
7.5050991045531));
#381229=CARTESIAN_POINT('Ctrl Pts',(0.569506752309622,2.68702947238968,
7.50567888004914));
#381230=CARTESIAN_POINT('Ctrl Pts',(0.569922222282148,2.68681367292768,
7.50637912803145));
#381231=CARTESIAN_POINT('Ctrl Pts',(0.570225606143944,2.68659431134895,
7.50710440483569));
#381232=CARTESIAN_POINT('Ctrl Pts',(0.570300001889869,2.68654051953491,
7.50728225710685));
#381233=CARTESIAN_POINT('Ctrl Pts',(0.570369224095775,2.68648556096084,
7.50746498566954));
#381234=CARTESIAN_POINT('Ctrl Pts',(0.570431915928522,2.68643104480392,
7.50764697238949));
#381235=CARTESIAN_POINT('Ctrl Pts',(0.570768929968109,2.68613798094756,
7.50862528291181));
#381236=CARTESIAN_POINT('Ctrl Pts',(0.570950535870584,2.68583422188778,
7.50965856837421));
#381237=CARTESIAN_POINT('Ctrl Pts',(0.571040685959675,2.68553724607221,
7.51067959873201));
#381238=CARTESIAN_POINT('Ctrl Pts',(0.571090295667412,2.68537381990632,
7.51124147302578));
#381239=CARTESIAN_POINT('Ctrl Pts',(0.571111806105353,2.6852122818537,7.51180065547252));
#381240=CARTESIAN_POINT('Ctrl Pts',(0.571113248871017,2.6850548511387,7.51235175716501));
#381241=CARTESIAN_POINT('Ctrl Pts',(0.571118234201117,2.68451086530544,
7.51425603304536));
#381242=CARTESIAN_POINT('Ctrl Pts',(0.570878146117182,2.68395100448379,
7.51626900505181));
#381243=CARTESIAN_POINT('Ctrl Pts',(0.570446802542537,2.68340258713866,
7.51827788969244));
#381244=CARTESIAN_POINT('Ctrl Pts',(0.570423457413152,2.68337290575557,
7.51838661432546));
#381245=CARTESIAN_POINT('Ctrl Pts',(0.570399542264644,2.68334325609048,
7.51849533314857));
#381246=CARTESIAN_POINT('Ctrl Pts',(0.570375062512093,2.68331364198703,
7.51860402984325));
#381247=CARTESIAN_POINT('Ctrl Pts',(0.511151792494568,2.62465641786575,
7.57603338728984));
#381248=CARTESIAN_POINT('Ctrl Pts',(0.528570753766796,2.64578831464074,
7.55196141284921));
#381249=CARTESIAN_POINT('Ctrl Pts',(0.545960368888797,2.66688324131613,
7.52783573083105));
#381250=CARTESIAN_POINT('Ctrl Pts',(0.563323058610791,2.68794421951938,
7.50366116530176));
#381251=CARTESIAN_POINT('Origin',(1.76626572250563E-16,9.06940118467445E-16,
7.49482233047033));
#381252=CARTESIAN_POINT('Origin',(0.484977299960256,2.69419807522076,7.49482233047033));
#381253=CARTESIAN_POINT('Origin',(0.,0.,7.50366116523517));
#381254=CARTESIAN_POINT('Origin',(0.561510055974207,2.67929332232211,7.49482233047033));
#381255=CARTESIAN_POINT('Ctrl Pts',(0.478269188839816,2.70125031276705,
7.51860402984325));
#381256=CARTESIAN_POINT('Ctrl Pts',(0.475977037628223,2.70850581611646,
7.51860402984325));
#381257=CARTESIAN_POINT('Ctrl Pts',(0.468479300229098,2.70980204909083,
7.51860402984325));
#381258=CARTESIAN_POINT('Ctrl Pts',(0.477418096240793,2.70394433029203,
7.51041458714366));
#381259=CARTESIAN_POINT('Ctrl Pts',(0.474200736074164,2.70881289880015,
7.5100464290044));
#381260=CARTESIAN_POINT('Ctrl Pts',(0.468477232442144,2.7098024065765,7.50729136483009));
#381261=CARTESIAN_POINT('Ctrl Pts',(0.47964495815025,2.70566619649923,7.50215815450137));
#381262=CARTESIAN_POINT('Ctrl Pts',(0.477817487202485,2.70818778615986,
7.49877163671533));
#381263=CARTESIAN_POINT('Ctrl Pts',(0.474421859314631,2.70879904293209,
7.49481588533172));
#381264=CARTESIAN_POINT('Ctrl Pts',(0.486543096209234,2.7028965550037,7.50366171572174));
#381265=CARTESIAN_POINT('Ctrl Pts',(0.487191808179633,2.70650034953677,
7.50000045605858));
#381266=CARTESIAN_POINT('Ctrl Pts',(0.48719180817951,2.7065003495368,7.49482233047317));
#381267=CARTESIAN_POINT('Origin',(0.466349848864421,2.69748476704951,7.51860402984325));
#381268=CARTESIAN_POINT('Origin',(0.466349848864421,2.69748476704951,9.));
#381269=CARTESIAN_POINT('Origin',(0.466349848864421,2.69748476704951,8.75721825406948));
#381270=CARTESIAN_POINT('Ctrl Pts',(0.483301006436993,2.68532734615808,
8.78942910404912));
#381271=CARTESIAN_POINT('Ctrl Pts',(0.481641165693858,2.69064687220925,
8.7967269950169));
#381272=CARTESIAN_POINT('Ctrl Pts',(0.472776992362322,2.68959810286835,
8.79893251111267));
#381273=CARTESIAN_POINT('Ctrl Pts',(0.479988149754479,2.69581068528935,
8.78111911759585));
#381274=CARTESIAN_POINT('Ctrl Pts',(0.478013283372308,2.70211482780821,
8.78644465894814));
#381275=CARTESIAN_POINT('Ctrl Pts',(0.46994596940398,2.70291104204566,8.78817647674132));
#381276=CARTESIAN_POINT('Ctrl Pts',(0.477923498420489,2.70234415227765,
8.76780923932028));
#381277=CARTESIAN_POINT('Ctrl Pts',(0.475587389273433,2.7097844030008,8.76988516158372));
#381278=CARTESIAN_POINT('Ctrl Pts',(0.468166832892768,2.71122375125526,
8.77093053738833));
#381279=CARTESIAN_POINT('Ctrl Pts',(0.478326077172229,2.70107021563117,
8.75371302330493));
#381280=CARTESIAN_POINT('Ctrl Pts',(0.476048030768675,2.70832808762997,
8.75300828287559));
#381281=CARTESIAN_POINT('Ctrl Pts',(0.468513389351356,2.70960233958568,
8.75267964240738));
#381282=CARTESIAN_POINT('Origin',(0.470575193914108,2.68411393159326,8.78727029226991));
#381283=CARTESIAN_POINT('Ctrl Pts',(0.504036631578554,2.61971088052921,
8.85049129520029));
#381284=CARTESIAN_POINT('Ctrl Pts',(0.502277013195043,2.62527908089984,
8.85711686593484));
#381285=CARTESIAN_POINT('Ctrl Pts',(0.493751728365416,2.62463079031095,
8.85933012996512));
#381286=CARTESIAN_POINT('Ctrl Pts',(0.496845378477071,2.64246714322811,
8.82945683644722));
#381287=CARTESIAN_POINT('Ctrl Pts',(0.495071154197079,2.64808156302842,
8.83607469902389));
#381288=CARTESIAN_POINT('Ctrl Pts',(0.486523682952831,2.64739397461503,
8.8382956714852));
#381289=CARTESIAN_POINT('Ctrl Pts',(0.489664844518242,2.66518948588238,
8.80838214965002));
#381290=CARTESIAN_POINT('Ctrl Pts',(0.48788361832088,2.67082606280458,8.81501364461995));
#381291=CARTESIAN_POINT('Ctrl Pts',(0.479307239296681,2.67012283067464,
8.81722098428721));
#381292=CARTESIAN_POINT('Ctrl Pts',(0.482494215215309,2.68788048588352,
8.78727029226991));
#381293=CARTESIAN_POINT('Ctrl Pts',(0.480712693150428,2.69351799905963,
8.79393457792714));
#381294=CARTESIAN_POINT('Ctrl Pts',(0.472101526741932,2.69281998167919,
8.79610912703474));
#381295=CARTESIAN_POINT('Origin',(0.492117610277352,2.61594432623895,8.85049129520029));
#381296=CARTESIAN_POINT('Ctrl Pts',(0.515891055659628,2.61740223164621,
8.85049129520029));
#381297=CARTESIAN_POINT('Ctrl Pts',(0.519611637301493,2.6219031631575,8.85711686593484));
#381298=CARTESIAN_POINT('Ctrl Pts',(0.527270584603639,2.61810299364327,
8.85933012996512));
#381299=CARTESIAN_POINT('Ctrl Pts',(0.512599510788232,2.61342032250981,
8.86332496987232));
#381300=CARTESIAN_POINT('Ctrl Pts',(0.517180599096309,2.61281573646103,
8.86648636486738));
#381301=CARTESIAN_POINT('Ctrl Pts',(0.518049148486212,2.60697435615754,
8.87206031107457));
#381302=CARTESIAN_POINT('Ctrl Pts',(0.505603918890392,2.61475129959255,
8.86341338519876));
#381303=CARTESIAN_POINT('Ctrl Pts',(0.501110700619808,2.61588463988004,
8.86654584966058));
#381304=CARTESIAN_POINT('Ctrl Pts',(0.498154264204941,2.61074813946514,
8.87215952290714));
#381305=CARTESIAN_POINT('Ctrl Pts',(0.504036631578554,2.61971088052921,
8.85049129520029));
#381306=CARTESIAN_POINT('Ctrl Pts',(0.502277013195043,2.62527908089984,
8.85711686593484));
#381307=CARTESIAN_POINT('Ctrl Pts',(0.493751728365416,2.62463079031095,
8.85933012996512));
#381308=CARTESIAN_POINT('Origin',(0.525525532687654,2.60943813393232,8.85049129520029));
#381309=CARTESIAN_POINT('Ctrl Pts',(0.561440886005564,2.67250562312429,
8.78727029226991));
#381310=CARTESIAN_POINT('Ctrl Pts',(0.565207781345649,2.67706258210757,
8.79393457792714));
#381311=CARTESIAN_POINT('Ctrl Pts',(0.572927672898268,2.67318409147409,
8.79610912703474));
#381312=CARTESIAN_POINT('Ctrl Pts',(0.546279125935812,2.65416385556391,
8.80838214965001));
#381313=CARTESIAN_POINT('Ctrl Pts',(0.550045395686141,2.65872005774707,
8.81501364461993));
#381314=CARTESIAN_POINT('Ctrl Pts',(0.557731085305871,2.6548497880324,8.81722098428722));
#381315=CARTESIAN_POINT('Ctrl Pts',(0.531096423210977,2.63579675286367,
8.82945683644723));
#381316=CARTESIAN_POINT('Ctrl Pts',(0.534847887929955,2.64033504482784,
8.8360746990239));
#381317=CARTESIAN_POINT('Ctrl Pts',(0.542512653014727,2.63649012367217,
8.83829567148519));
#381318=CARTESIAN_POINT('Ctrl Pts',(0.515891055659628,2.61740223164621,
8.85049129520029));
#381319=CARTESIAN_POINT('Ctrl Pts',(0.519611637301494,2.6219031631575,8.85711686593484));
#381320=CARTESIAN_POINT('Ctrl Pts',(0.527270584603639,2.61810299364327,
8.85933012996512));
#381321=CARTESIAN_POINT('Origin',(0.57107536303359,2.6645415254104,8.78727029226991));
#381322=CARTESIAN_POINT('Ctrl Pts',(0.570257105423809,2.68317091578168,
8.75374538247848));
#381323=CARTESIAN_POINT('Ctrl Pts',(0.575088500423227,2.68903623766094,
8.75304829418602));
#381324=CARTESIAN_POINT('Ctrl Pts',(0.582543965794262,2.68739712835699,
8.75272238421917));
#381325=CARTESIAN_POINT('Ctrl Pts',(0.571098103415353,2.68418830424844,
8.76769408445019));
#381326=CARTESIAN_POINT('Ctrl Pts',(0.576051610414024,2.69020078488341,
8.76974318093968));
#381327=CARTESIAN_POINT('Ctrl Pts',(0.583462952756301,2.68875497647084,
8.7707786988043));
#381328=CARTESIAN_POINT('Ctrl Pts',(0.566787626784243,2.67897375054523,
8.78108014887991));
#381329=CARTESIAN_POINT('Ctrl Pts',(0.570982613144604,2.68407152719165,
8.78639403366325));
#381330=CARTESIAN_POINT('Ctrl Pts',(0.578753247881939,2.68180452222744,
8.78812224174741));
#381331=CARTESIAN_POINT('Ctrl Pts',(0.559723707160385,2.67042824812776,
8.78944554828685));
#381332=CARTESIAN_POINT('Ctrl Pts',(0.563254763751582,2.67472802218773,
8.79673892988685));
#381333=CARTESIAN_POINT('Ctrl Pts',(0.571070449571984,2.6704363314401,8.79894799272499));
#381334=CARTESIAN_POINT('Origin',(0.580009539540115,2.67534954427314,8.75721825406948));
#381335=CARTESIAN_POINT('Origin',(0.580009539540115,2.67534954427314,9.));
#381336=CARTESIAN_POINT('Origin',(0.580009539540115,2.67534954427314,7.51860402984325));
#381337=CARTESIAN_POINT('Ctrl Pts',(0.563322897210404,2.68794344954021,
7.50366195182966));
#381338=CARTESIAN_POINT('Ctrl Pts',(0.564074028832674,2.69152753840575,
7.50000065167736));
#381339=CARTESIAN_POINT('Ctrl Pts',(0.564074028832788,2.69152753840572,
7.49482233047108));
#381340=CARTESIAN_POINT('Ctrl Pts',(0.5707628771231,2.68792112230681,7.50215800491337));
#381341=CARTESIAN_POINT('Ctrl Pts',(0.57340468063354,2.68957205276766,7.49877273257266));
#381342=CARTESIAN_POINT('Ctrl Pts',(0.576783407432508,2.68886398386711,
7.49481816995649));
#381343=CARTESIAN_POINT('Ctrl Pts',(0.572170600248225,2.68548630569255,
7.51043025814042));
#381344=CARTESIAN_POINT('Ctrl Pts',(0.576980440810566,2.68879662150103,
7.51006209594513));
#381345=CARTESIAN_POINT('Ctrl Pts',(0.58266045931007,2.68756521579719,7.50731281821697));
#381346=CARTESIAN_POINT('Ctrl Pts',(0.570374099622798,2.68331247699919,
7.51860402984325));
#381347=CARTESIAN_POINT('Ctrl Pts',(0.575221469180506,2.68917797150193,
7.51860402984324));
#381348=CARTESIAN_POINT('Ctrl Pts',(0.582657984926149,2.68756575223785,
7.51860402984325));
#381349=CARTESIAN_POINT('Origin',(0.,0.,7.5));
#381350=CARTESIAN_POINT('Origin',(0.682528638916215,2.57897124462359,7.5));
#381351=CARTESIAN_POINT('',(0.682528638916215,2.57897124462359,7.59394543036555));
#381352=CARTESIAN_POINT('',(0.682528638916215,2.57897124462359,8.85049129520029));
#381353=CARTESIAN_POINT('',(0.682528638916215,2.57897124462359,7.5));
#381354=CARTESIAN_POINT('',(0.731515368664185,2.63104303262371,8.78727029226991));
#381355=CARTESIAN_POINT('Ctrl Pts',(0.682528638916215,2.57897124462359,
8.85049129520029));
#381356=CARTESIAN_POINT('Ctrl Pts',(0.698881284484137,2.59635373775255,
8.82945686509571));
#381357=CARTESIAN_POINT('Ctrl Pts',(0.715209619867097,2.61371038970361,
8.80838212259897));
#381358=CARTESIAN_POINT('Ctrl Pts',(0.731515368664185,2.63104303262371,
8.78727029226991));
#381359=CARTESIAN_POINT('',(0.741123661092981,2.64125643059842,8.75721825406948));
#381360=CARTESIAN_POINT('Origin',(0.712208829051163,2.61052091131519,8.75937679713107));
#381361=CARTESIAN_POINT('',(0.741123661092981,2.64125643059842,7.51860402984325));
#381362=CARTESIAN_POINT('',(0.741123661092981,2.64125643059842,7.5));
#381363=CARTESIAN_POINT('Ctrl Pts',(0.741123661092982,2.64125643059842,
7.51860402984325));
#381364=CARTESIAN_POINT('Ctrl Pts',(0.733577841762296,2.63323539497314,
7.52834476460825));
#381365=CARTESIAN_POINT('Ctrl Pts',(0.726027123794582,2.62520915220727,
7.53807742314407));
#381366=CARTESIAN_POINT('Ctrl Pts',(0.718471342711591,2.61717752746415,
7.54780169004674));
#381367=CARTESIAN_POINT('Ctrl Pts',(0.706503393831256,2.60445586794331,
7.5632044032688));
#381368=CARTESIAN_POINT('Ctrl Pts',(0.694522727030052,2.59172068955964,
7.57858609112103));
#381369=CARTESIAN_POINT('Ctrl Pts',(0.682528638916215,2.57897124462359,
7.59394543036555));
#381370=CARTESIAN_POINT('Origin',(0.604952940619213,2.8490235055211,7.5));
#381371=CARTESIAN_POINT('',(0.650355981859121,2.66505851907035,8.75721825406948));
#381372=CARTESIAN_POINT('',(0.653715973115229,2.65144443664273,8.78727029226991));
#381373=CARTESIAN_POINT('Origin',(0.66224488413743,2.6168868176421,8.75658640621054));
#381374=CARTESIAN_POINT('',(0.670846486662589,2.58203466569848,8.85049129520029));
#381375=CARTESIAN_POINT('Ctrl Pts',(0.653715973115229,2.65144443664273,
8.78727029226991));
#381376=CARTESIAN_POINT('Ctrl Pts',(0.659418044923361,2.62834066354125,
8.80838212259896));
#381377=CARTESIAN_POINT('Ctrl Pts',(0.665128015193322,2.60520488728791,
8.82945686509571));
#381378=CARTESIAN_POINT('Ctrl Pts',(0.670846486662589,2.58203466569848,
8.85049129520029));
#381379=CARTESIAN_POINT('',(0.670846486662589,2.58203466569848,7.59394543036555));
#381380=CARTESIAN_POINT('',(0.670846486662589,2.58203466569848,7.5));
#381381=CARTESIAN_POINT('',(0.650355981859121,2.66505851907035,7.51860402984325));
#381382=CARTESIAN_POINT('Ctrl Pts',(0.670846486662589,2.58203466569848,
7.59394543036555));
#381383=CARTESIAN_POINT('Ctrl Pts',(0.666652189758522,2.59902920509618,
7.57858609112103));
#381384=CARTESIAN_POINT('Ctrl Pts',(0.662462586247585,2.61600472770608,
7.56320440326857));
#381385=CARTESIAN_POINT('Ctrl Pts',(0.658277430155648,2.63296223017114,
7.54780169004651));
#381386=CARTESIAN_POINT('Ctrl Pts',(0.655635196006337,2.64366808943085,
7.53807742314383));
#381387=CARTESIAN_POINT('Ctrl Pts',(0.652994732413309,2.65436677471377,
7.52834476460825));
#381388=CARTESIAN_POINT('Ctrl Pts',(0.650355981859121,2.66505851907035,
7.51860402984325));
#381389=CARTESIAN_POINT('',(0.650355981859121,2.66505851907035,7.5));
#381390=CARTESIAN_POINT('Origin',(0.677521207658155,2.58368200434956,7.5));
#381391=CARTESIAN_POINT('Ctrl Pts',(0.670846486662589,2.58203466569848,
8.85049129520029));
#381392=CARTESIAN_POINT('Ctrl Pts',(0.670892890456614,2.58184664584109,
8.85097269580138));
#381393=CARTESIAN_POINT('Ctrl Pts',(0.670946875156382,2.58166301368506,
8.85143669361005));
#381394=CARTESIAN_POINT('Ctrl Pts',(0.671011765372867,2.58147556015296,
8.8519052845931));
#381395=CARTESIAN_POINT('Ctrl Pts',(0.671138686521124,2.58110891293205,
8.85282181883899));
#381396=CARTESIAN_POINT('Ctrl Pts',(0.671304249801585,2.5807371425313,8.85372622499636));
#381397=CARTESIAN_POINT('Ctrl Pts',(0.671525138335603,2.58036068787951,
8.85462257735071));
#381398=CARTESIAN_POINT('Ctrl Pts',(0.671708512151326,2.58004816859801,
8.85536669723986));
#381399=CARTESIAN_POINT('Ctrl Pts',(0.67193002919575,2.57973233380186,8.85610498449051));
#381400=CARTESIAN_POINT('Ctrl Pts',(0.67220580498669,2.57941800298971,8.85681338218371));
#381401=CARTESIAN_POINT('Ctrl Pts',(0.672456071950082,2.57913274728402,
8.85745625420284));
#381402=CARTESIAN_POINT('Ctrl Pts',(0.672753713651846,2.57884475725327,
8.85808743050665));
#381403=CARTESIAN_POINT('Ctrl Pts',(0.673125539874794,2.57856398687628,
8.85866804508409));
#381404=CARTESIAN_POINT('Ctrl Pts',(0.67329709243386,2.5784344455107,8.85893592806395));
#381405=CARTESIAN_POINT('Ctrl Pts',(0.673484652170822,2.57830655186085,
8.85919241173848));
#381406=CARTESIAN_POINT('Ctrl Pts',(0.673692155647773,2.57818220473043,
8.85943017985534));
#381407=CARTESIAN_POINT('Ctrl Pts',(0.673972346769258,2.57801429929367,
8.8597512372));
#381408=CARTESIAN_POINT('Ctrl Pts',(0.67429636215275,2.57784913604231,8.86004599534706));
#381409=CARTESIAN_POINT('Ctrl Pts',(0.674665038801,2.57769797846511,8.86026130871721));
#381410=CARTESIAN_POINT('Ctrl Pts',(0.674800021716019,2.57764263541452,
8.86034014101236));
#381411=CARTESIAN_POINT('Ctrl Pts',(0.67494301438211,2.57758832710582,8.86040910639693));
#381412=CARTESIAN_POINT('Ctrl Pts',(0.675090240476494,2.57753684760079,
8.86046313645507));
#381413=CARTESIAN_POINT('Ctrl Pts',(0.675319985563772,2.57745651426434,
8.8605474499083));
#381414=CARTESIAN_POINT('Ctrl Pts',(0.67556635949915,2.57738101538589,8.86059655985669));
#381415=CARTESIAN_POINT('Ctrl Pts',(0.6758134757379,2.57731491283742,8.86059725258816));
#381416=CARTESIAN_POINT('Ctrl Pts',(0.676061162913886,2.57724865756566,
8.86059794692012));
#381417=CARTESIAN_POINT('Ctrl Pts',(0.676313029242126,2.57719367384813,
8.86056369958366));
#381418=CARTESIAN_POINT('Ctrl Pts',(0.676554535209261,2.57714928401131,
8.86048590497774));
#381419=CARTESIAN_POINT('Ctrl Pts',(0.676617561076184,2.57713769958554,
8.86046560290182));
#381420=CARTESIAN_POINT('Ctrl Pts',(0.676680717651033,2.5771267750407,8.86044257503091));
#381421=CARTESIAN_POINT('Ctrl Pts',(0.676742047748321,2.57711681560842,
8.86041778462584));
#381422=CARTESIAN_POINT('Ctrl Pts',(0.677154723198763,2.57704980098779,
8.86025097596201));
#381423=CARTESIAN_POINT('Ctrl Pts',(0.67754013146029,2.57701781811486,8.8599848982295));
#381424=CARTESIAN_POINT('Ctrl Pts',(0.677886322802411,2.57701335701958,
8.85968173251461));
#381425=CARTESIAN_POINT('Ctrl Pts',(0.678069438187994,2.57701099735577,
8.85952137522076));
#381426=CARTESIAN_POINT('Ctrl Pts',(0.678245108670022,2.57701610131726,
8.85934740853961));
#381427=CARTESIAN_POINT('Ctrl Pts',(0.678410902053563,2.57702704303034,
8.85916759001821));
#381428=CARTESIAN_POINT('Ctrl Pts',(0.679076648666176,2.57707097969576,
8.85844552518695));
#381429=CARTESIAN_POINT('Ctrl Pts',(0.679620958726714,2.57720851046266,
8.85759444184122));
#381430=CARTESIAN_POINT('Ctrl Pts',(0.680054687829779,2.577360508228,8.85683498915136));
#381431=CARTESIAN_POINT('Ctrl Pts',(0.680100076425294,2.57737641438934,
8.85675551444996));
#381432=CARTESIAN_POINT('Ctrl Pts',(0.680144243875795,2.57739249616705,
8.8566769979365));
#381433=CARTESIAN_POINT('Ctrl Pts',(0.680187195361015,2.57740867382615,
8.85659965593547));
#381434=CARTESIAN_POINT('Ctrl Pts',(0.680766956700275,2.57762704069423,
8.85555568965886));
#381435=CARTESIAN_POINT('Ctrl Pts',(0.681292606769904,2.57792063379263,
8.85434650606346));
#381436=CARTESIAN_POINT('Ctrl Pts',(0.68176977456907,2.5782854786949,8.85297329937117));
#381437=CARTESIAN_POINT('Ctrl Pts',(0.682038152381839,2.57849068172211,
8.85220095427747));
#381438=CARTESIAN_POINT('Ctrl Pts',(0.682291111676902,2.57871875852964,
8.85137579139183));
#381439=CARTESIAN_POINT('Ctrl Pts',(0.682528638916215,2.57897124462359,
8.85049129520029));
#381440=CARTESIAN_POINT('Origin',(0.677521207658155,2.58368200434956,7.59394543036555));
#381441=CARTESIAN_POINT('Ctrl Pts',(0.670981212530816,2.58148878062457,
7.59443877723642));
#381442=CARTESIAN_POINT('Ctrl Pts',(0.672368759343803,2.57586668959983,
7.58783886950016));
#381443=CARTESIAN_POINT('Ctrl Pts',(0.680858400978209,2.57593856766321,
7.58559994247159));
#381444=CARTESIAN_POINT('Ctrl Pts',(0.663406635187616,2.61217961058349,
7.56670252222136));
#381445=CARTESIAN_POINT('Ctrl Pts',(0.664792176601528,2.60656564507644,
7.5600487499903));
#381446=CARTESIAN_POINT('Ctrl Pts',(0.673332303208251,2.60661658423106,
7.55786368756705));
#381447=CARTESIAN_POINT('Ctrl Pts',(0.655846202610808,2.64281312848387,
7.53888913333561));
#381448=CARTESIAN_POINT('Ctrl Pts',(0.657239978365199,2.63716579890492,
7.53222002137279));
#381449=CARTESIAN_POINT('Ctrl Pts',(0.6658188602351,2.63723812166669,7.53005029815326));
#381450=CARTESIAN_POINT('Ctrl Pts',(0.648300256915097,2.67338794813823,
7.51101258149734));
#381451=CARTESIAN_POINT('Ctrl Pts',(0.649710927764165,2.66767216266333,
7.5043616886572));
#381452=CARTESIAN_POINT('Ctrl Pts',(0.658318523541229,2.66780168672796,
7.50217374673251));
#381453=CARTESIAN_POINT('',(0.658718750143853,2.6661707753905,7.50366116523517));
#381454=CARTESIAN_POINT('Ctrl Pts',(0.650355981859121,2.66505851907035,
7.51860402984325));
#381455=CARTESIAN_POINT('Ctrl Pts',(0.650250166117407,2.66548726549259,
7.51734760759493));
#381456=CARTESIAN_POINT('Ctrl Pts',(0.650212310040393,2.66588895539464,
7.51608817408573));
#381457=CARTESIAN_POINT('Ctrl Pts',(0.650255795434424,2.66626391779724,
7.51481005913119));
#381458=CARTESIAN_POINT('Ctrl Pts',(0.650295185543453,2.66660356770153,
7.51365231206383));
#381459=CARTESIAN_POINT('Ctrl Pts',(0.650401124727213,2.66692179482435,
7.51247773061042));
#381460=CARTESIAN_POINT('Ctrl Pts',(0.65060681453073,2.66720142950121,7.51129758471022));
#381461=CARTESIAN_POINT('Ctrl Pts',(0.650862463465839,2.66754898346906,
7.50983079813402));
#381462=CARTESIAN_POINT('Ctrl Pts',(0.651274536664403,2.66781811159763,
7.50839324291155));
#381463=CARTESIAN_POINT('Ctrl Pts',(0.651891120888244,2.66794175530204,
7.50715379678855));
#381464=CARTESIAN_POINT('Ctrl Pts',(0.652175965033211,2.66799887513076,
7.50658120839351));
#381465=CARTESIAN_POINT('Ctrl Pts',(0.652546816749126,2.66802374990068,
7.50598221009429));
#381466=CARTESIAN_POINT('Ctrl Pts',(0.652996372582791,2.66799309213236,
7.50545747549611));
#381467=CARTESIAN_POINT('Ctrl Pts',(0.653236269490689,2.66797673219823,
7.50517746087247));
#381468=CARTESIAN_POINT('Ctrl Pts',(0.653501193456964,2.66794458333831,
7.50491486231392));
#381469=CARTESIAN_POINT('Ctrl Pts',(0.653783927906854,2.66789584104001,
7.50468370960993));
#381470=CARTESIAN_POINT('Ctrl Pts',(0.654206705092963,2.66782295592915,
7.50433806340447));
#381471=CARTESIAN_POINT('Ctrl Pts',(0.654681888865027,2.6677102342832,7.50405484070984));
#381472=CARTESIAN_POINT('Ctrl Pts',(0.655177311127163,2.66756457064415,
7.50385766036131));
#381473=CARTESIAN_POINT('Ctrl Pts',(0.655230288837496,2.66754899418208,
7.50383657498791));
#381474=CARTESIAN_POINT('Ctrl Pts',(0.655283478613807,2.66753306175527,
7.50381643264937));
#381475=CARTESIAN_POINT('Ctrl Pts',(0.655336827290465,2.66751679707099,
7.50379723213559));
#381476=CARTESIAN_POINT('Ctrl Pts',(0.655692947158707,2.66740822498289,
7.50366906242519));
#381477=CARTESIAN_POINT('Ctrl Pts',(0.656063684366623,2.66728179801425,
7.50358235568538));
#381478=CARTESIAN_POINT('Ctrl Pts',(0.656418100142797,2.66715134813715,
7.5035341175365));
#381479=CARTESIAN_POINT('Ctrl Pts',(0.656949506487048,2.66695575331052,
7.50346178989176));
#381480=CARTESIAN_POINT('Ctrl Pts',(0.657512862320731,2.66672274300315,
7.50346967198527));
#381481=CARTESIAN_POINT('Ctrl Pts',(0.658058864751397,2.66647698198924,
7.50354272648692));
#381482=CARTESIAN_POINT('Ctrl Pts',(0.658283446852712,2.66637589539727,
7.50357277531559));
#381483=CARTESIAN_POINT('Ctrl Pts',(0.658504852827741,2.66627291519396,
7.50361331098761));
#381484=CARTESIAN_POINT('Ctrl Pts',(0.658718750144193,2.66617077539188,
7.50366116523658));
#381485=CARTESIAN_POINT('',(0.678263889302254,2.58651417133801,7.57603338622103));
#381486=CARTESIAN_POINT('Origin',(0.680508179114277,2.59506137280035,7.58486873427628));
#381487=CARTESIAN_POINT('Ctrl Pts',(0.658718750125042,2.66617077544467,
7.50366116529969));
#381488=CARTESIAN_POINT('Ctrl Pts',(0.665223977061721,2.63966210099077,
7.52783573079709));
#381489=CARTESIAN_POINT('Ctrl Pts',(0.671738733243894,2.61311115757656,
7.55196141284069));
#381490=CARTESIAN_POINT('Ctrl Pts',(0.678263888672591,2.58651417242021,
7.57603338728831));
#381491=CARTESIAN_POINT('Ctrl Pts',(0.67077076127836,2.58307524303169,7.59639677331372));
#381492=CARTESIAN_POINT('Ctrl Pts',(0.672289956972022,2.5648608542088,7.59959882295464));
#381493=CARTESIAN_POINT('Ctrl Pts',(0.683001371747239,2.57969238838817,
7.59642833564546));
#381494=CARTESIAN_POINT('Ctrl Pts',(0.670465937779987,2.57918651744114,
7.58707626057422));
#381495=CARTESIAN_POINT('Ctrl Pts',(0.674898289962463,2.57406142766957,
7.58809943920599));
#381496=CARTESIAN_POINT('Ctrl Pts',(0.681297243148316,2.57624495667518,
7.58710240504253));
#381497=CARTESIAN_POINT('Ctrl Pts',(0.675135748308881,2.58307476921871,
7.58015376756929));
#381498=CARTESIAN_POINT('Ctrl Pts',(0.676704490972113,2.5806939462827,7.5820588065976));
#381499=CARTESIAN_POINT('Ctrl Pts',(0.67922699388854,2.58194456775798,7.58020924244128));
#381500=CARTESIAN_POINT('Ctrl Pts',(0.678263889092142,2.58651417053755,
7.57603338509286));
#381501=CARTESIAN_POINT('Ctrl Pts',(0.678263889092142,2.58651417053755,
7.57603338509286));
#381502=CARTESIAN_POINT('Ctrl Pts',(0.678263889092142,2.58651417053755,
7.57603338509286));
#381503=CARTESIAN_POINT('Origin',(0.680502659389257,2.59506282024303,7.58486873427621));
#381504=CARTESIAN_POINT('Ctrl Pts',(0.747020829444758,2.64752498744625,
7.51098857897448));
#381505=CARTESIAN_POINT('Ctrl Pts',(0.742986830895846,2.64323693804364,
7.50433767179956));
#381506=CARTESIAN_POINT('Ctrl Pts',(0.735550410854283,2.64757372349463,
7.50214974420965));
#381507=CARTESIAN_POINT('Ctrl Pts',(0.725436098627537,2.62458090579523,
7.53887321589168));
#381508=CARTESIAN_POINT('Ctrl Pts',(0.721450434540296,2.62034423483437,
7.53220407452061));
#381509=CARTESIAN_POINT('Ctrl Pts',(0.714010955012692,2.62461706343849,
7.53003438070911));
#381510=CARTESIAN_POINT('Ctrl Pts',(0.703809917164866,2.60159276304372,
7.56669465659231));
#381511=CARTESIAN_POINT('Ctrl Pts',(0.699847807611444,2.59738113002056,
7.56004085833304));
#381512=CARTESIAN_POINT('Ctrl Pts',(0.692431608525831,2.60161629722504,
7.55785582193789));
#381513=CARTESIAN_POINT('Ctrl Pts',(0.682143263122383,2.5785615988534,7.59443891967696));
#381514=CARTESIAN_POINT('Ctrl Pts',(0.678175409003342,2.57434385948674,
7.58783901202978));
#381515=CARTESIAN_POINT('Ctrl Pts',(0.670813497415743,2.57857250415905,
7.58560008491213));
#381516=CARTESIAN_POINT('',(0.734382828366872,2.64632931751461,7.50366116523517));
#381517=CARTESIAN_POINT('Ctrl Pts',(0.734382828366971,2.64632931751497,
7.50366116523554));
#381518=CARTESIAN_POINT('Ctrl Pts',(0.73513881439088,2.64627810571536,7.50350835821027));
#381519=CARTESIAN_POINT('Ctrl Pts',(0.735832082908374,2.64620643442547,
7.50345484956));
#381520=CARTESIAN_POINT('Ctrl Pts',(0.736483307107726,2.64611277011765,
7.50349758195598));
#381521=CARTESIAN_POINT('Ctrl Pts',(0.73681743341804,2.64606471338142,7.50351950684424));
#381522=CARTESIAN_POINT('Ctrl Pts',(0.737173443029245,2.64600625855207,
7.50357029184312));
#381523=CARTESIAN_POINT('Ctrl Pts',(0.737515189580167,2.64594045470857,
7.50365515313924));
#381524=CARTESIAN_POINT('Ctrl Pts',(0.738040934162335,2.64583922175066,
7.50378570417639));
#381525=CARTESIAN_POINT('Ctrl Pts',(0.738548420846329,2.64571796522779,
7.50400001621911));
#381526=CARTESIAN_POINT('Ctrl Pts',(0.738998494895536,2.64558370626699,
7.50428903009635));
#381527=CARTESIAN_POINT('Ctrl Pts',(0.739048449652331,2.64556880455527,
7.50432110841318));
#381528=CARTESIAN_POINT('Ctrl Pts',(0.739097725961639,2.64555375201862,
7.50435406373354));
#381529=CARTESIAN_POINT('Ctrl Pts',(0.739146291662892,2.64553856487362,
7.50438785222351));
#381530=CARTESIAN_POINT('Ctrl Pts',(0.739442808612704,2.6454458400535,7.50459414719561));
#381531=CARTESIAN_POINT('Ctrl Pts',(0.739717403222036,2.64534612893594,
7.50483629897752));
#381532=CARTESIAN_POINT('Ctrl Pts',(0.739960005034007,2.64524448842675,
7.5050991045531));
#381533=CARTESIAN_POINT('Ctrl Pts',(0.74049520899826,2.64502025925467,7.50567888004914));
#381534=CARTESIAN_POINT('Ctrl Pts',(0.740895999024166,2.64477828392327,
7.50637912803144));
#381535=CARTESIAN_POINT('Ctrl Pts',(0.741184705006676,2.64453993517567,
7.50710440483569));
#381536=CARTESIAN_POINT('Ctrl Pts',(0.741255501445204,2.64448148733087,
7.50728225710685));
#381537=CARTESIAN_POINT('Ctrl Pts',(0.741321060218732,2.64442220659313,
7.50746498566954));
#381538=CARTESIAN_POINT('Ctrl Pts',(0.741380130382219,2.64436378576598,
7.50764697238949));
#381539=CARTESIAN_POINT('Ctrl Pts',(0.741697675324574,2.64404973147709,
7.50862528291182));
#381540=CARTESIAN_POINT('Ctrl Pts',(0.741859446188464,2.64373496099275,
7.50965856837422));
#381541=CARTESIAN_POINT('Ctrl Pts',(0.741930383748696,2.64343281940981,
7.51067959873203));
#381542=CARTESIAN_POINT('Ctrl Pts',(0.741969420777567,2.64326655051562,
7.51124147302579));
#381543=CARTESIAN_POINT('Ctrl Pts',(0.741980537241439,2.64310396618176,
7.51180065547253));
#381544=CARTESIAN_POINT('Ctrl Pts',(0.741971890422245,2.64294676648674,
7.51235175716501));
#381545=CARTESIAN_POINT('Ctrl Pts',(0.741942012217447,2.64240357891953,
7.51425603304535));
#381546=CARTESIAN_POINT('Ctrl Pts',(0.74166654701423,2.64186025088833,7.51626900505179));
#381547=CARTESIAN_POINT('Ctrl Pts',(0.741200952461279,2.64134059660317,
7.51827788969242));
#381548=CARTESIAN_POINT('Ctrl Pts',(0.74117575360422,2.64131247193124,7.51838661432544));
#381549=CARTESIAN_POINT('Ctrl Pts',(0.741149987931383,2.64128441543339,
7.51849533314856));
#381550=CARTESIAN_POINT('Ctrl Pts',(0.741123661092985,2.64125643059842,
7.51860402984325));
#381551=CARTESIAN_POINT('Ctrl Pts',(0.678263890382482,2.58651417197306,
7.57603338728985));
#381552=CARTESIAN_POINT('Ctrl Pts',(0.697000987805591,2.60648661431919,
7.55196141284922));
#381553=CARTESIAN_POINT('Ctrl Pts',(0.715706430690848,2.62642404273906,
7.52783573083105));
#381554=CARTESIAN_POINT('Ctrl Pts',(0.734382828411158,2.64632931755387,
7.50366116530176));
#381555=CARTESIAN_POINT('Origin',(2.34371526914277E-16,8.93760209386499E-16,
7.49482233047033));
#381556=CARTESIAN_POINT('Origin',(0.656598725434842,2.65758995402928,7.49482233047033));
#381557=CARTESIAN_POINT('Origin',(0.,0.,7.50366116523517));
#381558=CARTESIAN_POINT('Origin',(0.732019285896476,2.63781235403044,7.49482233047033));
#381559=CARTESIAN_POINT('Ctrl Pts',(0.65035623525909,2.66505749215232,7.51860402984325));
#381560=CARTESIAN_POINT('Ctrl Pts',(0.648533655213662,2.6724449469243,7.51860402984325));
#381561=CARTESIAN_POINT('Ctrl Pts',(0.641134372651965,2.67421889833353,
7.51860402984325));
#381562=CARTESIAN_POINT('Ctrl Pts',(0.649679497616552,2.6678005042194,7.51041458714366));
#381563=CARTESIAN_POINT('Ctrl Pts',(0.646780678116749,2.67286520670502,
7.51004642900441));
#381564=CARTESIAN_POINT('Ctrl Pts',(0.64113233201769,2.67421938756826,7.5072913648301));
#381565=CARTESIAN_POINT('Ctrl Pts',(0.652012104546052,2.66937615713541,
7.50215815450137));
#381566=CARTESIAN_POINT('Ctrl Pts',(0.650349947137605,2.67200965238525,
7.49877163671531));
#381567=CARTESIAN_POINT('Ctrl Pts',(0.647000459287285,2.67283721189065,
7.49481588533171));
#381568=CARTESIAN_POINT('Ctrl Pts',(0.658718618100686,2.66617024094247,
7.50366171572174));
#381569=CARTESIAN_POINT('Ctrl Pts',(0.659596893131267,2.66972506797453,
7.50000045605858));
#381570=CARTESIAN_POINT('Ctrl Pts',(0.659596893131146,2.66972506797456,
7.49482233047317));
#381571=CARTESIAN_POINT('Origin',(0.638220125503548,2.66206335788656,7.51860402984325));
#381572=CARTESIAN_POINT('Origin',(0.638220125503548,2.66206335788656,9.));
#381573=CARTESIAN_POINT('Origin',(0.638220125503548,2.66206335788656,8.75721825406948));
#381574=CARTESIAN_POINT('Ctrl Pts',(0.654357526473971,2.64884485132562,
8.78942910404912));
#381575=CARTESIAN_POINT('Ctrl Pts',(0.653041919255957,2.65425979420155,
8.7967269950169));
#381576=CARTESIAN_POINT('Ctrl Pts',(0.64412876343682,2.65378110920504,8.79893251111267));
#381577=CARTESIAN_POINT('Ctrl Pts',(0.651723146255084,2.65951890676874,
8.78111911759583));
#381578=CARTESIAN_POINT('Ctrl Pts',(0.650156245245669,2.6659366268742,8.78644465894814));
#381579=CARTESIAN_POINT('Ctrl Pts',(0.642156520060452,2.66724807978472,
8.78817647674132));
#381580=CARTESIAN_POINT('Ctrl Pts',(0.650081337635878,2.66617123271352,
8.76780923932029));
#381581=CARTESIAN_POINT('Ctrl Pts',(0.648226726776164,2.67374587167056,
8.76988516158373));
#381582=CARTESIAN_POINT('Ctrl Pts',(0.640913636083721,2.67565769930935,
8.77093053738833));
#381583=CARTESIAN_POINT('Ctrl Pts',(0.650401467845208,2.66487412019735,
8.75371302330493));
#381584=CARTESIAN_POINT('Ctrl Pts',(0.648593115387865,2.67226303505393,
8.75300828287559));
#381585=CARTESIAN_POINT('Ctrl Pts',(0.641155596302533,2.67401741505541,
8.75267964240738));
#381586=CARTESIAN_POINT('Origin',(0.641580116759656,2.64844927545894,8.78727029226991));
#381587=CARTESIAN_POINT('Ctrl Pts',(0.670846486662589,2.58203466569848,
8.85049129520029));
#381588=CARTESIAN_POINT('Ctrl Pts',(0.669447239426409,2.58770416474117,
8.85711686593484));
#381589=CARTESIAN_POINT('Ctrl Pts',(0.660897934588157,2.58760342300926,
8.85933012996512));
#381590=CARTESIAN_POINT('Ctrl Pts',(0.665128007518924,2.60520491838319,
8.82945683644722));
#381591=CARTESIAN_POINT('Ctrl Pts',(0.663717145684686,2.6109214776958,8.83607469902388));
#381592=CARTESIAN_POINT('Ctrl Pts',(0.655143182195917,2.61078294036945,
8.8382956714852));
#381593=CARTESIAN_POINT('Ctrl Pts',(0.659418052229554,2.62834063393786,
8.80838214965002));
#381594=CARTESIAN_POINT('Ctrl Pts',(0.658001622475789,2.63407975346251,
8.81501364461989));
#381595=CARTESIAN_POINT('Ctrl Pts',(0.649397808304859,2.63392745668916,
8.81722098428721));
#381596=CARTESIAN_POINT('Ctrl Pts',(0.653715973115229,2.65144443664273,
8.78727029226991));
#381597=CARTESIAN_POINT('Ctrl Pts',(0.652299308087835,2.65718450945399,
8.79393457792714));
#381598=CARTESIAN_POINT('Ctrl Pts',(0.643661112117155,2.6570396455512,8.79610912703474));
#381599=CARTESIAN_POINT('Origin',(0.658710630307015,2.57903950451469,8.85049129520029));
#381600=CARTESIAN_POINT('Ctrl Pts',(0.682528638916215,2.57897124462359,
8.85049129520029));
#381601=CARTESIAN_POINT('Ctrl Pts',(0.686529951896112,2.58322455000412,
8.85711686593484));
#381602=CARTESIAN_POINT('Ctrl Pts',(0.693929685372865,2.57894147790726,
8.85933012996512));
#381603=CARTESIAN_POINT('Ctrl Pts',(0.678988735082457,2.57520840675055,
8.86332496987231));
#381604=CARTESIAN_POINT('Ctrl Pts',(0.683521675092151,2.574311551553,8.86648636486737));
#381605=CARTESIAN_POINT('Ctrl Pts',(0.684014181433137,2.56842652484136,
8.87206031107457));
#381606=CARTESIAN_POINT('Ctrl Pts',(0.672092792372933,2.57698485830991,
8.86341338519876));
#381607=CARTESIAN_POINT('Ctrl Pts',(0.667681419262718,2.57840375151122,
8.86654584966056));
#381608=CARTESIAN_POINT('Ctrl Pts',(0.66440196045203,2.57346722411881,8.87215952290714));
#381609=CARTESIAN_POINT('Ctrl Pts',(0.670846486662589,2.58203466569848,
8.85049129520029));
#381610=CARTESIAN_POINT('Ctrl Pts',(0.669447239426409,2.58770416474117,
8.85711686593484));
#381611=CARTESIAN_POINT('Ctrl Pts',(0.660897934588157,2.58760342300926,
8.85933012996512));
#381612=CARTESIAN_POINT('Origin',(0.691633059385415,2.57040622694002,8.85049129520029));
#381613=CARTESIAN_POINT('Ctrl Pts',(0.731515368664185,2.63104303262371,
8.78727029226991));
#381614=CARTESIAN_POINT('Ctrl Pts',(0.735566489878297,2.63534928303294,
8.79393457792714));
#381615=CARTESIAN_POINT('Ctrl Pts',(0.743022024337685,2.63098414602443,
8.79610912703474));
#381616=CARTESIAN_POINT('Ctrl Pts',(0.715209598974175,2.61371036749491,
8.80838214965003));
#381617=CARTESIAN_POINT('Ctrl Pts',(0.719260047395476,2.61801590274056,
8.81501364461988));
#381618=CARTESIAN_POINT('Ctrl Pts',(0.726681976909626,2.61366116108552,
8.81722098428721));
#381619=CARTESIAN_POINT('Ctrl Pts',(0.698881306429992,2.59635376108049,
8.82945683644723));
#381620=CARTESIAN_POINT('Ctrl Pts',(0.702915832726861,2.60064237146729,
8.83607469902389));
#381621=CARTESIAN_POINT('Ctrl Pts',(0.710318504785448,2.59631426692943,
8.8382956714852));
#381622=CARTESIAN_POINT('Ctrl Pts',(0.682528638916215,2.57897124462359,
8.85049129520029));
#381623=CARTESIAN_POINT('Ctrl Pts',(0.686529951896112,2.58322455000412,
8.85711686593484));
#381624=CARTESIAN_POINT('Ctrl Pts',(0.693929685372865,2.57894147790726,
8.85933012996512));
#381625=CARTESIAN_POINT('Origin',(0.740619789133384,2.62247801494013,8.78727029226991));
#381626=CARTESIAN_POINT('Ctrl Pts',(0.740996801860814,2.64112155517596,
8.75374538247849));
#381627=CARTESIAN_POINT('Ctrl Pts',(0.7461940627041,2.64666527758192,8.75304829418602));
#381628=CARTESIAN_POINT('Ctrl Pts',(0.753529191928262,2.64455186269746,
8.75272238421917));
#381629=CARTESIAN_POINT('Ctrl Pts',(0.741901256234672,2.64208297038269,
8.76769408445017));
#381630=CARTESIAN_POINT('Ctrl Pts',(0.747229806678867,2.64776572544832,
8.76974318093968));
#381631=CARTESIAN_POINT('Ctrl Pts',(0.754533288360377,2.64584804126992,
8.77077869880429));
#381632=CARTESIAN_POINT('Ctrl Pts',(0.737265538337212,2.63715530372528,
8.78108014887992));
#381633=CARTESIAN_POINT('Ctrl Pts',(0.741778521319331,2.64197383274391,
8.78639403366327));
#381634=CARTESIAN_POINT('Ctrl Pts',(0.749387942947455,2.63921361930754,
8.78812224174741));
#381635=CARTESIAN_POINT('Ctrl Pts',(0.729668620074102,2.62907994584327,
8.78944554828685));
#381636=CARTESIAN_POINT('Ctrl Pts',(0.733467909200717,2.63314464998372,
8.79673892988685));
#381637=CARTESIAN_POINT('Ctrl Pts',(0.740992567286079,2.62836102426519,
8.79894799272499));
#381638=CARTESIAN_POINT('Origin',(0.750228081562181,2.63269141291484,8.75721825406948));
#381639=CARTESIAN_POINT('Origin',(0.750228081562181,2.63269141291484,9.));
#381640=CARTESIAN_POINT('Origin',(0.750228081562181,2.63269141291484,7.51860402984325));
#381641=CARTESIAN_POINT('Ctrl Pts',(0.734382618009651,2.64632855949765,
7.50366195182966));
#381642=CARTESIAN_POINT('Ctrl Pts',(0.735361839713489,2.64985715929995,
7.50000065167735));
#381643=CARTESIAN_POINT('Ctrl Pts',(0.735361839713602,2.64985715929992,
7.49482233047108));
#381644=CARTESIAN_POINT('Ctrl Pts',(0.741805881174924,2.64582959698829,
7.50215800491337));
#381645=CARTESIAN_POINT('Ctrl Pts',(0.744548032294523,2.6473078745034,7.49877273257265));
#381646=CARTESIAN_POINT('Ctrl Pts',(0.747874451006687,2.64638478463708,
7.49481816995647));
#381647=CARTESIAN_POINT('Ctrl Pts',(0.743054712745831,2.64330958983561,
7.51043025814041));
#381648=CARTESIAN_POINT('Ctrl Pts',(0.74806676363693,2.64630493670232,7.51006209594514));
#381649=CARTESIAN_POINT('Ctrl Pts',(0.753656215494924,2.64471214101881,
7.50731281821699));
#381650=CARTESIAN_POINT('Ctrl Pts',(0.741122625541025,2.6412553296967,7.51860402984325));
#381651=CARTESIAN_POINT('Ctrl Pts',(0.746335839181183,2.64679820087802,
7.51860402984325));
#381652=CARTESIAN_POINT('Ctrl Pts',(0.753653780564754,2.64471283489162,
7.51860402984325));
#381653=CARTESIAN_POINT('Origin',(0.,0.,7.5));
#381654=CARTESIAN_POINT('Origin',(0.846361565593563,2.52994271156922,7.5));
#381655=CARTESIAN_POINT('',(0.846361565593563,2.52994271156922,7.59394543036555));
#381656=CARTESIAN_POINT('',(0.846361565593563,2.52994271156922,8.85049129520029));
#381657=CARTESIAN_POINT('',(0.846361565593563,2.52994271156922,7.5));
#381658=CARTESIAN_POINT('',(0.898583897763412,2.57876892194512,8.78727029226991));
#381659=CARTESIAN_POINT('Ctrl Pts',(0.846361565593563,2.52994271156922,
8.85049129520029));
#381660=CARTESIAN_POINT('Ctrl Pts',(0.863794313055935,2.54624177290297,
8.82945686509571));
#381661=CARTESIAN_POINT('Ctrl Pts',(0.881201144631272,2.56251660371119,
8.80838212259896));
#381662=CARTESIAN_POINT('Ctrl Pts',(0.898583897763412,2.57876892194512,
8.78727029226991));
#381663=CARTESIAN_POINT('',(0.908826823579918,2.58834572998875,8.75721825406948));
#381664=CARTESIAN_POINT('Origin',(0.878002168680578,2.55952593977649,8.75937679713143));
#381665=CARTESIAN_POINT('',(0.908826823579918,2.58834572998875,7.51860402984325));
#381666=CARTESIAN_POINT('',(0.908826823579918,2.58834572998875,7.5));
#381667=CARTESIAN_POINT('Ctrl Pts',(0.908826823579918,2.58834572998875,
7.51860402984325));
#381668=CARTESIAN_POINT('Ctrl Pts',(0.900782598427349,2.58082463674587,
7.52834476460825));
#381669=CARTESIAN_POINT('Ctrl Pts',(0.892733151079883,2.57329866091778,
7.53807742314407));
#381670=CARTESIAN_POINT('Ctrl Pts',(0.884678306195387,2.56576763856519,
7.54780169004674));
#381671=CARTESIAN_POINT('Ctrl Pts',(0.871919867225566,2.55383890617572,
7.5632044032688));
#381672=CARTESIAN_POINT('Ctrl Pts',(0.859147870308693,2.54189749753934,
7.57858609112102));
#381673=CARTESIAN_POINT('Ctrl Pts',(0.846361565593563,2.52994271156922,
7.59394543036555));
#381674=CARTESIAN_POINT('Origin',(0.786247562650672,2.80441041318874,7.5));
#381675=CARTESIAN_POINT('',(0.819770641322243,2.6179144196928,8.75721825406948));
#381676=CARTESIAN_POINT('',(0.822251471859985,2.60411303347873,8.78727029226991));
#381677=CARTESIAN_POINT('Origin',(0.828548745068344,2.56907996760748,8.75658640621073));
#381678=CARTESIAN_POINT('',(0.83489968963681,2.53374831658169,8.85049129520029));
#381679=CARTESIAN_POINT('Ctrl Pts',(0.822251471859985,2.60411303347873,
8.78727029226991));
#381680=CARTESIAN_POINT('Ctrl Pts',(0.826461564325047,2.58069139656185,
8.80838212259895));
#381681=CARTESIAN_POINT('Ctrl Pts',(0.830677488574718,2.55723731619086,
8.82945686509571));
#381682=CARTESIAN_POINT('Ctrl Pts',(0.834899689636811,2.53374831658169,
8.85049129520029));
#381683=CARTESIAN_POINT('',(0.83489968963681,2.53374831658169,7.59394543036555));
#381684=CARTESIAN_POINT('',(0.83489968963681,2.53374831658169,7.5));
#381685=CARTESIAN_POINT('',(0.819770641322243,2.6179144196928,7.51860402984325));
#381686=CARTESIAN_POINT('Ctrl Pts',(0.834899689636811,2.53374831658169,
7.59394543036555));
#381687=CARTESIAN_POINT('Ctrl Pts',(0.831802854243252,2.55097666840085,
7.57858609112103));
#381688=CARTESIAN_POINT('Ctrl Pts',(0.828709484189966,2.56818574179751,
7.56320440326857));
#381689=CARTESIAN_POINT('Ctrl Pts',(0.825619397863336,2.58537654712653,
7.54780169004651));
#381690=CARTESIAN_POINT('Ctrl Pts',(0.823668519225315,2.59622969857338,
7.53807742314383));
#381691=CARTESIAN_POINT('Ctrl Pts',(0.82171894786751,2.60707557734321,7.52834476460825));
#381692=CARTESIAN_POINT('Ctrl Pts',(0.819770641322244,2.6179144196928,7.51860402984325));
#381693=CARTESIAN_POINT('',(0.819770641322243,2.6179144196928,7.5));
#381694=CARTESIAN_POINT('Origin',(0.841666242051987,2.53496461975634,7.5));
#381695=CARTESIAN_POINT('Ctrl Pts',(0.83489968963681,2.53374831658169,8.85049129520029));
#381696=CARTESIAN_POINT('Ctrl Pts',(0.83493395161564,2.53355770992997,8.85097269580138));
#381697=CARTESIAN_POINT('Ctrl Pts',(0.83497606004542,2.53337099625431,8.85143669361005));
#381698=CARTESIAN_POINT('Ctrl Pts',(0.835028806748958,2.53317977033515,
8.8519052845931));
#381699=CARTESIAN_POINT('Ctrl Pts',(0.835131975956005,2.53280574456439,
8.85282181883899));
#381700=CARTESIAN_POINT('Ctrl Pts',(0.835273379657592,2.53242413033,8.85372622499635));
#381701=CARTESIAN_POINT('Ctrl Pts',(0.835469694820074,2.53203429676771,
8.85462257735071));
#381702=CARTESIAN_POINT('Ctrl Pts',(0.835632668695512,2.53171067078987,
8.85536669723986));
#381703=CARTESIAN_POINT('Ctrl Pts',(0.835833495004543,2.53138129226441,
8.85610498449051));
#381704=CARTESIAN_POINT('Ctrl Pts',(0.836088564940264,2.53104993826304,
8.85681338218371));
#381705=CARTESIAN_POINT('Ctrl Pts',(0.836320041307526,2.53074923398639,
8.85745625420284));
#381706=CARTESIAN_POINT('Ctrl Pts',(0.836598619887871,2.53044276569274,
8.85808743050666));
#381707=CARTESIAN_POINT('Ctrl Pts',(0.83695169313415,2.53013874920071,8.85866804508411));
#381708=CARTESIAN_POINT('Ctrl Pts',(0.837114593476293,2.52999848258155,
8.85893592806396));
#381709=CARTESIAN_POINT('Ctrl Pts',(0.837293573677378,2.52985883470932,
8.85919241173848));
#381710=CARTESIAN_POINT('Ctrl Pts',(0.837492683868179,2.52972144827001,
8.85943017985534));
#381711=CARTESIAN_POINT('Ctrl Pts',(0.837761541568687,2.52953593590619,
8.8597512372));
#381712=CARTESIAN_POINT('Ctrl Pts',(0.838074309181975,2.52935035226354,
8.86004599534706));
#381713=CARTESIAN_POINT('Ctrl Pts',(0.838432543645287,2.52917588406184,
8.86026130871721));
#381714=CARTESIAN_POINT('Ctrl Pts',(0.838563703382005,2.52911200633442,
8.86034014101235));
#381715=CARTESIAN_POINT('Ctrl Pts',(0.838702922709042,2.52904864803639,
8.86040910639693));
#381716=CARTESIAN_POINT('Ctrl Pts',(0.838846548008413,2.52898784149328,
8.86046313645507));
#381717=CARTESIAN_POINT('Ctrl Pts',(0.839070674085231,2.528892953392,8.8605474499083));
#381718=CARTESIAN_POINT('Ctrl Pts',(0.839311704589184,2.52880182440186,
8.86059655985668));
#381719=CARTESIAN_POINT('Ctrl Pts',(0.839554077896298,2.52872002487639,
8.86059725258816));
#381720=CARTESIAN_POINT('Ctrl Pts',(0.839797011182579,2.52863803636134,
8.86059794692011));
#381721=CARTESIAN_POINT('Ctrl Pts',(0.840044837205558,2.5285670284827,8.86056369958366));
#381722=CARTESIAN_POINT('Ctrl Pts',(0.840283002906171,2.52850725650911,
8.86048590497774));
#381723=CARTESIAN_POINT('Ctrl Pts',(0.840345157062984,2.52849165780363,
8.86046560290182));
#381724=CARTESIAN_POINT('Ctrl Pts',(0.840407483937885,2.52847670924879,
8.86044257503091));
#381725=CARTESIAN_POINT('Ctrl Pts',(0.840468049922893,2.52846284084641,
8.86041778462583));
#381726=CARTESIAN_POINT('Ctrl Pts',(0.840875583845876,2.52836952370761,
8.860250975962));
#381727=CARTESIAN_POINT('Ctrl Pts',(0.841258151095091,2.52831291335483,
8.8599848982295));
#381728=CARTESIAN_POINT('Ctrl Pts',(0.841603345326615,2.5282862808699,8.85968173251461));
#381729=CARTESIAN_POINT('Ctrl Pts',(0.841785933297819,2.52827219381124,
8.85952137522076));
#381730=CARTESIAN_POINT('Ctrl Pts',(0.841961569857936,2.52826603203966,
8.85934740853961));
#381731=CARTESIAN_POINT('Ctrl Pts',(0.842127723639154,2.52826632885327,
8.85916759001821));
#381732=CARTESIAN_POINT('Ctrl Pts',(0.842794917435776,2.52826752071418,
8.85844552518694));
#381733=CARTESIAN_POINT('Ctrl Pts',(0.843346920779412,2.52836989484405,
8.8575944418412));
#381734=CARTESIAN_POINT('Ctrl Pts',(0.843789497269782,2.52849379119464,
8.85683498915133));
#381735=CARTESIAN_POINT('Ctrl Pts',(0.84383581172081,2.52850675661776,8.85675551444995));
#381736=CARTESIAN_POINT('Ctrl Pts',(0.843880918787578,2.52851997553546,
8.85667699793649));
#381737=CARTESIAN_POINT('Ctrl Pts',(0.843924818530538,2.52853336804472,
8.85659965593547));
#381738=CARTESIAN_POINT('Ctrl Pts',(0.844517379501221,2.5287141408181,8.85555568965886));
#381739=CARTESIAN_POINT('Ctrl Pts',(0.845060760140805,2.5289734521824,8.85434650606345));
#381740=CARTESIAN_POINT('Ctrl Pts',(0.8455603232407,2.52930697522583,8.85297329937117));
#381741=CARTESIAN_POINT('Ctrl Pts',(0.845841297045563,2.52949456161591,
8.85220095427747));
#381742=CARTESIAN_POINT('Ctrl Pts',(0.846108349539856,2.52970596265749,
8.85137579139183));
#381743=CARTESIAN_POINT('Ctrl Pts',(0.846361565593563,2.52994271156922,
8.85049129520029));
#381744=CARTESIAN_POINT('Origin',(0.841666242051987,2.53496461975634,7.59394543036555));
#381745=CARTESIAN_POINT('Ctrl Pts',(0.834999163719523,2.5331949211712,7.59443877723642));
#381746=CARTESIAN_POINT('Ctrl Pts',(0.836023651060061,2.52749548090589,
7.58783886950016));
#381747=CARTESIAN_POINT('Ctrl Pts',(0.844500455058551,2.52702327808101,
7.58559994247159));
#381748=CARTESIAN_POINT('Ctrl Pts',(0.829406517384706,2.56430799836501,
7.56670252222135));
#381749=CARTESIAN_POINT('Ctrl Pts',(0.830429524050183,2.55861679540903,
7.5600487499903));
#381750=CARTESIAN_POINT('Ctrl Pts',(0.838955367733707,2.55812046211334,
7.55786368756704));
#381751=CARTESIAN_POINT('Ctrl Pts',(0.823824314758139,2.59536297499579,
7.53888913333561));
#381752=CARTESIAN_POINT('Ctrl Pts',(0.824853401202298,2.58963794894194,
7.53222002137279));
#381753=CARTESIAN_POINT('Ctrl Pts',(0.833419290574609,2.58916047226025,
7.53005029815327));
#381754=CARTESIAN_POINT('Ctrl Pts',(0.818252808438286,2.62635844580471,
7.51101258149734));
#381755=CARTESIAN_POINT('Ctrl Pts',(0.81929436928006,2.62056402203247,7.5043616886572));
#381756=CARTESIAN_POINT('Ctrl Pts',(0.827892578463753,2.62014178942108,
7.50217374673251));
#381757=CARTESIAN_POINT('',(0.828187489909737,2.61848858635941,7.50366116523517));
#381758=CARTESIAN_POINT('Ctrl Pts',(0.819770641322243,2.6179144196928,7.51860402984325));
#381759=CARTESIAN_POINT('Ctrl Pts',(0.819692512867909,2.61834906484739,
7.51734760759493));
#381760=CARTESIAN_POINT('Ctrl Pts',(0.819680470930653,2.61875235488163,
7.51608817408572));
#381761=CARTESIAN_POINT('Ctrl Pts',(0.819747890902897,2.619123760765,7.51481005913119));
#381762=CARTESIAN_POINT('Ctrl Pts',(0.819808961524808,2.61946018908918,
7.51365231206383));
#381763=CARTESIAN_POINT('Ctrl Pts',(0.819935071926916,2.61977097483344,
7.51247773061042));
#381764=CARTESIAN_POINT('Ctrl Pts',(0.820158255373932,2.62003685637991,
7.51129758471022));
#381765=CARTESIAN_POINT('Ctrl Pts',(0.820435646910061,2.62036731677735,
7.50983079813402));
#381766=CARTESIAN_POINT('Ctrl Pts',(0.820864116558444,2.62060949033284,
7.50839324291155));
#381767=CARTESIAN_POINT('Ctrl Pts',(0.82148735582321,2.62069337531113,7.50715379678855));
#381768=CARTESIAN_POINT('Ctrl Pts',(0.821775274405323,2.62073212775402,
7.50658120839351));
#381769=CARTESIAN_POINT('Ctrl Pts',(0.822146957898595,2.62073319086503,
7.50598221009429));
#381770=CARTESIAN_POINT('Ctrl Pts',(0.822593625821624,2.62067379294523,
7.50545747549611));
#381771=CARTESIAN_POINT('Ctrl Pts',(0.822831981651018,2.62064209637668,
7.50517746087247));
#381772=CARTESIAN_POINT('Ctrl Pts',(0.823094301518063,2.62059303983324,
7.50491486231392));
#381773=CARTESIAN_POINT('Ctrl Pts',(0.823373332129928,2.62052628282281,
7.50468370960993));
#381774=CARTESIAN_POINT('Ctrl Pts',(0.823790570909882,2.62042646003492,
7.50433806340447));
#381775=CARTESIAN_POINT('Ctrl Pts',(0.824257556265273,2.62028352485887,
7.50405484070984));
#381776=CARTESIAN_POINT('Ctrl Pts',(0.824742627927844,2.62010641868807,
7.50385766036131));
#381777=CARTESIAN_POINT('Ctrl Pts',(0.824794498802434,2.62008747993595,
7.50383657498791));
#381778=CARTESIAN_POINT('Ctrl Pts',(0.824846558500551,2.62006817236335,
7.50381643264937));
#381779=CARTESIAN_POINT('Ctrl Pts',(0.824898755484729,2.62004852303516,
7.50379723213559));
#381780=CARTESIAN_POINT('Ctrl Pts',(0.82524718742894,2.61991735734177,7.50366906242519));
#381781=CARTESIAN_POINT('Ctrl Pts',(0.825609062713809,2.61976743691642,
7.50358235568538));
#381782=CARTESIAN_POINT('Ctrl Pts',(0.825954392352437,2.61961454756585,
7.5035341175365));
#381783=CARTESIAN_POINT('Ctrl Pts',(0.826472175061791,2.61938530728839,
7.50346178989176));
#381784=CARTESIAN_POINT('Ctrl Pts',(0.827019444398843,2.6191166813935,7.50346967198527));
#381785=CARTESIAN_POINT('Ctrl Pts',(0.827548579046732,2.61883644282611,
7.50354272648692));
#381786=CARTESIAN_POINT('Ctrl Pts',(0.827766223079849,2.61872117490274,
7.50357277531559));
#381787=CARTESIAN_POINT('Ctrl Pts',(0.827980576188277,2.61860422075378,
7.50361331098761));
#381788=CARTESIAN_POINT('Ctrl Pts',(0.828187489910165,2.61848858636076,
7.50366116523658));
#381789=CARTESIAN_POINT('',(0.842588855338968,2.53774338397765,7.57603338622103));
#381790=CARTESIAN_POINT('Origin',(0.845376155095215,2.54612923215661,7.58486873427626));
#381791=CARTESIAN_POINT('Ctrl Pts',(0.828187489894435,2.61848858641467,
7.50366116529969));
#381792=CARTESIAN_POINT('Ctrl Pts',(0.832980934541032,2.59161758555463,
7.52783573079709));
#381793=CARTESIAN_POINT('Ctrl Pts',(0.83778118067268,2.56470379203953,7.55196141284068));
#381794=CARTESIAN_POINT('Ctrl Pts',(0.842588854779936,2.53774338509797,
7.57603338728831));
#381795=CARTESIAN_POINT('Ctrl Pts',(0.83489078985715,2.53479160767929,7.5963967733137));
#381796=CARTESIAN_POINT('Ctrl Pts',(0.83525626370703,2.51565878627385,7.59974925422225));
#381797=CARTESIAN_POINT('Ctrl Pts',(0.846992701389922,2.53077349621429,
7.59639677331373));
#381798=CARTESIAN_POINT('Ctrl Pts',(0.834337441147242,2.53093040200112,
7.5870762605742));
#381799=CARTESIAN_POINT('Ctrl Pts',(0.838503286617428,2.52543830193646,
7.58811717123965));
#381800=CARTESIAN_POINT('Ctrl Pts',(0.845126734807065,2.52734810969667,
7.58707626057426));
#381801=CARTESIAN_POINT('Ctrl Pts',(0.839246778196414,2.53451146916045,
7.58015376756929));
#381802=CARTESIAN_POINT('Ctrl Pts',(0.840681119793326,2.53199758847086,
7.58208760766041));
#381803=CARTESIAN_POINT('Ctrl Pts',(0.843334199200238,2.53315435188583,
7.58015376756931));
#381804=CARTESIAN_POINT('Ctrl Pts',(0.842588855078002,2.5377433831923,7.57603338509286));
#381805=CARTESIAN_POINT('Ctrl Pts',(0.842588855078001,2.5377433831923,7.57603338509286));
#381806=CARTESIAN_POINT('Ctrl Pts',(0.842588855078001,2.5377433831923,7.57603338509286));
#381807=CARTESIAN_POINT('Origin',(0.845370739448622,2.54613103027501,7.5848687342762));
#381808=CARTESIAN_POINT('Ctrl Pts',(0.915113503383049,2.59422357454068,
7.51098857897448));
#381809=CARTESIAN_POINT('Ctrl Pts',(0.910813056848287,2.59020279456989,
7.50433767179956));
#381810=CARTESIAN_POINT('Ctrl Pts',(0.903669774527107,2.59500712269798,
7.50214974420965));
#381811=CARTESIAN_POINT('Ctrl Pts',(0.89210308835161,2.57270957241784,7.53887321589169));
#381812=CARTESIAN_POINT('Ctrl Pts',(0.887854168798255,2.56873696852669,
7.53220407452062));
#381813=CARTESIAN_POINT('Ctrl Pts',(0.880703735547808,2.57347766723606,
7.53003438070911));
#381814=CARTESIAN_POINT('Ctrl Pts',(0.869048484835129,2.55115425547475,
7.56669465659233));
#381815=CARTESIAN_POINT('Ctrl Pts',(0.864824675606408,2.547205128934,7.56004085833301));
#381816=CARTESIAN_POINT('Ctrl Pts',(0.857695061991681,2.55190675204007,
7.55785582193789));
#381817=CARTESIAN_POINT('Ctrl Pts',(0.845950735501021,2.52955859857208,
7.59443891967696));
#381818=CARTESIAN_POINT('Ctrl Pts',(0.841720802274774,2.52560374628956,
7.58783901202978));
#381819=CARTESIAN_POINT('Ctrl Pts',(0.83464494671847,2.53029538205277,7.58560008491213));
#381820=CARTESIAN_POINT('',(0.902424861598253,2.59384008075032,7.50366116523517));
#381821=CARTESIAN_POINT('Ctrl Pts',(0.902424861598376,2.59384008075068,
7.50366116523554));
#381822=CARTESIAN_POINT('Ctrl Pts',(0.903176013216653,2.59374053798035,
7.50350835821027));
#381823=CARTESIAN_POINT('Ctrl Pts',(0.903863265344316,2.59362459608039,
7.50345484956));
#381824=CARTESIAN_POINT('Ctrl Pts',(0.904507150440901,2.59348940013823,
7.50349758195598));
#381825=CARTESIAN_POINT('Ctrl Pts',(0.904837511247212,2.59342003459351,
7.50351950684424));
#381826=CARTESIAN_POINT('Ctrl Pts',(0.905189044184713,2.59333889025177,
7.50357029184312));
#381827=CARTESIAN_POINT('Ctrl Pts',(0.905525872513966,2.59325132583263,
7.50365515313924));
#381828=CARTESIAN_POINT('Ctrl Pts',(0.906044050879611,2.59311661629766,
7.50378570417639));
#381829=CARTESIAN_POINT('Ctrl Pts',(0.906542725945682,2.59296309412584,
7.50400001621911));
#381830=CARTESIAN_POINT('Ctrl Pts',(0.906983273268325,2.59280027467114,
7.50428903009634));
#381831=CARTESIAN_POINT('Ctrl Pts',(0.907032170631776,2.59278220296433,
7.50432110841318));
#381832=CARTESIAN_POINT('Ctrl Pts',(0.907080381278296,2.59276402421074,
7.50435406373354));
#381833=CARTESIAN_POINT('Ctrl Pts',(0.907127874152393,2.59274575665419,
7.50438785222352));
#381834=CARTESIAN_POINT('Ctrl Pts',(0.907417840976708,2.59263422444096,
7.50459414719561));
#381835=CARTESIAN_POINT('Ctrl Pts',(0.907685482888729,2.59251712485356,
7.50483629897752));
#381836=CARTESIAN_POINT('Ctrl Pts',(0.907921074119476,2.59240014962424,
7.5050991045531));
#381837=CARTESIAN_POINT('Ctrl Pts',(0.908440812037402,2.59214209051931,
7.50567888004914));
#381838=CARTESIAN_POINT('Ctrl Pts',(0.908825275184502,2.59187493364706,
7.50637912803145));
#381839=CARTESIAN_POINT('Ctrl Pts',(0.909098116932917,2.59161857715672,
7.50710440483569));
#381840=CARTESIAN_POINT('Ctrl Pts',(0.909165023146295,2.5915557134559,7.50728225710685));
#381841=CARTESIAN_POINT('Ctrl Pts',(0.909226649092385,2.59149235415174,
7.50746498566955));
#381842=CARTESIAN_POINT('Ctrl Pts',(0.909281854854638,2.59143026871808,
7.50764697238949));
#381843=CARTESIAN_POINT('Ctrl Pts',(0.909578625839476,2.5910965145131,7.50862528291182));
#381844=CARTESIAN_POINT('Ctrl Pts',(0.909719896913601,2.59077202606365,
7.50965856837421));
#381845=CARTESIAN_POINT('Ctrl Pts',(0.909771330447324,2.5904659602779,7.51067959873202));
#381846=CARTESIAN_POINT('Ctrl Pts',(0.909799634385806,2.59029753188996,
7.51124147302578));
#381847=CARTESIAN_POINT('Ctrl Pts',(0.909800311195675,2.59013456936877,
7.51180065547253));
#381848=CARTESIAN_POINT('Ctrl Pts',(0.909781610323258,2.58997824666099,
7.512351757165));
#381849=CARTESIAN_POINT('Ctrl Pts',(0.909716991359514,2.58943808943404,
7.51425603304535));
#381850=CARTESIAN_POINT('Ctrl Pts',(0.90940728098262,2.58891352684472,7.51626900505179));
#381851=CARTESIAN_POINT('Ctrl Pts',(0.908909348679248,2.58842477099045,
7.51827788969242));
#381852=CARTESIAN_POINT('Ctrl Pts',(0.908882399642027,2.58839831859999,
7.51838661432544));
#381853=CARTESIAN_POINT('Ctrl Pts',(0.908854889321539,2.58837197055955,
7.51849533314856));
#381854=CARTESIAN_POINT('Ctrl Pts',(0.908826823579921,2.58834572998875,
7.51860402984325));
#381855=CARTESIAN_POINT('Ctrl Pts',(0.842588856457665,2.53774338454218,
7.57603338728985));
#381856=CARTESIAN_POINT('Ctrl Pts',(0.862567095279239,2.55647430140978,
7.55196141284922));
#381857=CARTESIAN_POINT('Ctrl Pts',(0.882511501250637,2.57517230440419,
7.52783573083105));
#381858=CARTESIAN_POINT('Ctrl Pts',(0.902424861644963,2.59384008078666,
7.50366116530176));
#381859=CARTESIAN_POINT('Origin',(2.91153398701365E-16,8.76907647894219E-16,
7.49482233047033));
#381860=CARTESIAN_POINT('Origin',(0.825522045906634,2.61006122566543,7.49482233047033));
#381861=CARTESIAN_POINT('Origin',(0.,0.,7.50366116523517));
#381862=CARTESIAN_POINT('Origin',(0.899520491555354,2.58549204896709,7.49482233047033));
#381863=CARTESIAN_POINT('Ctrl Pts',(0.819770828406711,2.61791337864929,
7.51860402984325));
#381864=CARTESIAN_POINT('Ctrl Pts',(0.818425308899797,2.62540242820759,
7.51860402984325));
#381865=CARTESIAN_POINT('Ctrl Pts',(0.811154886414717,2.62764680850482,
7.51860402984325));
#381866=CARTESIAN_POINT('Ctrl Pts',(0.819271226580787,2.62069411363351,
7.51041458714367));
#381867=CARTESIAN_POINT('Ctrl Pts',(0.816702859618942,2.62593413814772,
7.51004642900443));
#381868=CARTESIAN_POINT('Ctrl Pts',(0.811152881318522,2.62764742747825,
7.50729136483011));
#381869=CARTESIAN_POINT('Ctrl Pts',(0.821699993348124,2.62211707856253,
7.50215815450136));
#381870=CARTESIAN_POINT('Ctrl Pts',(0.820209979640308,2.62485165780475,
7.49877163671529));
#381871=CARTESIAN_POINT('Ctrl Pts',(0.816920395591568,2.62589211942377,
7.49481588533168));
#381872=CARTESIAN_POINT('Ctrl Pts',(0.828187323895664,2.61848806146949,
7.50366171572174));
#381873=CARTESIAN_POINT('Ctrl Pts',(0.829291552965938,2.62197931345374,
7.50000045605858));
#381874=CARTESIAN_POINT('Ctrl Pts',(0.829291552965819,2.62197931345378,
7.49482233047317));
#381875=CARTESIAN_POINT('Origin',(0.807467818749196,2.61570295937525,7.51860402984325));
#381876=CARTESIAN_POINT('Origin',(0.807467818749196,2.61570295937525,9.));
#381877=CARTESIAN_POINT('Origin',(0.807467818749196,2.61570295937525,8.75721825406948));
#381878=CARTESIAN_POINT('Ctrl Pts',(0.822725151075418,2.60147768482363,
8.78942910404913));
#381879=CARTESIAN_POINT('Ctrl Pts',(0.82175918349478,2.60696579336254,8.79672699501691));
#381880=CARTESIAN_POINT('Ctrl Pts',(0.812833671257172,2.60705915972975,
8.79893251111267));
#381881=CARTESIAN_POINT('Ctrl Pts',(0.820780072553557,2.61229859459517,
8.78111911759577));
#381882=CARTESIAN_POINT('Ctrl Pts',(0.819627575649247,2.61880352049876,
8.78644465894812));
#381883=CARTESIAN_POINT('Ctrl Pts',(0.811728311833866,2.62062482304101,
8.78817647674132));
#381884=CARTESIAN_POINT('Ctrl Pts',(0.819567853192906,2.61904244366226,
8.76780923932034));
#381885=CARTESIAN_POINT('Ctrl Pts',(0.818202361614361,2.62672034503694,
8.76988516158374));
#381886=CARTESIAN_POINT('Ctrl Pts',(0.81102678766845,2.62909679595021,8.77093053738833));
#381887=CARTESIAN_POINT('Ctrl Pts',(0.819804219376137,2.61772748538993,
8.75371302330491));
#381888=CARTESIAN_POINT('Ctrl Pts',(0.818472991773145,2.62521708046822,
8.75300828287559));
#381889=CARTESIAN_POINT('Ctrl Pts',(0.811163157381067,2.62744437939174,
8.75267964240737));
#381890=CARTESIAN_POINT('Origin',(0.809948649286937,2.60190157316117,8.78727029226991));
#381891=CARTESIAN_POINT('Ctrl Pts',(0.834899689636811,2.53374831658169,
8.85049129520029));
#381892=CARTESIAN_POINT('Ctrl Pts',(0.833866563354992,2.53949581710878,
8.85711686593484));
#381893=CARTESIAN_POINT('Ctrl Pts',(0.825328369435516,2.53994303820323,
8.85933012996512));
#381894=CARTESIAN_POINT('Ctrl Pts',(0.830677482908367,2.55723734771397,
8.82945683644722));
#381895=CARTESIAN_POINT('Ctrl Pts',(0.829635781053761,2.56303255597043,
8.83607469902389));
#381896=CARTESIAN_POINT('Ctrl Pts',(0.821070557575562,2.56344363901072,
8.83829567148519));
#381897=CARTESIAN_POINT('Ctrl Pts',(0.826461569719534,2.58069136655117,
8.80838214965001));
#381898=CARTESIAN_POINT('Ctrl Pts',(0.825415756823051,2.58650944540522,
8.81501364461994));
#381899=CARTESIAN_POINT('Ctrl Pts',(0.816819862423319,2.58690870980847,
8.81722098428721));
#381900=CARTESIAN_POINT('Ctrl Pts',(0.822251471859985,2.60411303347873,
8.78727029226991));
#381901=CARTESIAN_POINT('Ctrl Pts',(0.82120548525055,2.60993207873472,8.79393457792714));
#381902=CARTESIAN_POINT('Ctrl Pts',(0.812575755917816,2.61034096358643,
8.79610912703474));
#381903=CARTESIAN_POINT('Origin',(0.822596867063763,2.53153685626414,8.85049129520029));
#381904=CARTESIAN_POINT('Ctrl Pts',(0.846361565593563,2.52994271156922,
8.85049129520029));
#381905=CARTESIAN_POINT('Ctrl Pts',(0.850627167658178,2.53393091307484,
8.85711686593484));
#381906=CARTESIAN_POINT('Ctrl Pts',(0.857737280217445,2.5291825384573,8.85933012996512));
#381907=CARTESIAN_POINT('Ctrl Pts',(0.842587849021616,2.52641440726749,
8.86332496987231));
#381908=CARTESIAN_POINT('Ctrl Pts',(0.84705401391008,2.52522896829157,8.86648636486737));
#381909=CARTESIAN_POINT('Ctrl Pts',(0.847168453387979,2.51932447800885,
8.87206031107457));
#381910=CARTESIAN_POINT('Ctrl Pts',(0.835819892408161,2.52862903348297,
8.86341338519877));
#381911=CARTESIAN_POINT('Ctrl Pts',(0.831508491736653,2.53032764906163,
8.86654584966059));
#381912=CARTESIAN_POINT('Ctrl Pts',(0.827919486529833,2.52561137994158,
8.87215952290715));
#381913=CARTESIAN_POINT('Ctrl Pts',(0.83489968963681,2.53374831658169,8.85049129520029));
#381914=CARTESIAN_POINT('Ctrl Pts',(0.833866563354992,2.53949581710878,
8.85711686593484));
#381915=CARTESIAN_POINT('Ctrl Pts',(0.825328369435516,2.53994303820323,
8.85933012996512));
#381916=CARTESIAN_POINT('Origin',(0.854898517487337,2.52081196941081,8.85049129520029));
#381917=CARTESIAN_POINT('Ctrl Pts',(0.898583897763412,2.57876892194512,
8.78727029226991));
#381918=CARTESIAN_POINT('Ctrl Pts',(0.90290259792552,2.58280676847368,8.79393457792714));
#381919=CARTESIAN_POINT('Ctrl Pts',(0.910063138901376,2.57797292237443,
8.79610912703474));
#381920=CARTESIAN_POINT('Ctrl Pts',(0.881201122358356,2.56251658288673,
8.80838214965003));
#381921=CARTESIAN_POINT('Ctrl Pts',(0.885519105289311,2.5665537588271,8.81501364461989));
#381922=CARTESIAN_POINT('Ctrl Pts',(0.892646776397471,2.56173243979916,
8.81722098428722));
#381923=CARTESIAN_POINT('Ctrl Pts',(0.86379433645133,2.54624179477691,8.82945683644722));
#381924=CARTESIAN_POINT('Ctrl Pts',(0.868095345592108,2.55026310076635,
8.83607469902389));
#381925=CARTESIAN_POINT('Ctrl Pts',(0.87520550545719,2.54546959795622,8.83829567148519));
#381926=CARTESIAN_POINT('Ctrl Pts',(0.846361565593563,2.52994271156922,
8.85049129520029));
#381927=CARTESIAN_POINT('Ctrl Pts',(0.850627167658178,2.53393091307484,
8.85711686593484));
#381928=CARTESIAN_POINT('Ctrl Pts',(0.857737280217445,2.5291825384573,8.85933012996512));
#381929=CARTESIAN_POINT('Origin',(0.907120849657186,2.56963817978671,8.78727029226991));
#381930=CARTESIAN_POINT('Ctrl Pts',(0.908691583495659,2.58821925958122,
8.75374538247847));
#381931=CARTESIAN_POINT('Ctrl Pts',(0.9142333535232,2.59341860216942,8.75304829418601));
#381932=CARTESIAN_POINT('Ctrl Pts',(0.921418004981125,2.59083956617952,
8.75272238421917));
#381933=CARTESIAN_POINT('Ctrl Pts',(0.90965577765479,2.5891207508666,8.76769408445022));
#381934=CARTESIAN_POINT('Ctrl Pts',(0.915337475387768,2.59445042870331,
8.76974318093972));
#381935=CARTESIAN_POINT('Ctrl Pts',(0.922503084835704,2.5920687489348,8.77077869880429));
#381936=CARTESIAN_POINT('Ctrl Pts',(0.904713867650191,2.58450022009428,
8.78108014887987));
#381937=CARTESIAN_POINT('Ctrl Pts',(0.90952630243896,2.58901970111584,8.78639403366323));
#381938=CARTESIAN_POINT('Ctrl Pts',(0.916943242212184,2.58577762151637,
8.78812224174741));
#381939=CARTESIAN_POINT('Ctrl Pts',(0.896615168114507,2.57692819012542,
8.78944554828686));
#381940=CARTESIAN_POINT('Ctrl Pts',(0.900667077682575,2.58074112160516,
8.79673892988686));
#381941=CARTESIAN_POINT('Ctrl Pts',(0.907869787598794,2.57548521785991,
8.79894799272499));
#381942=CARTESIAN_POINT('Origin',(0.917363775473692,2.57921498783034,8.75721825406948));
#381943=CARTESIAN_POINT('Origin',(0.917363775473692,2.57921498783034,9.));
#381944=CARTESIAN_POINT('Origin',(0.917363775473692,2.57921498783034,7.51860402984325));
#381945=CARTESIAN_POINT('Ctrl Pts',(0.902424603106922,2.59383933776843,
7.50366195182966));
#381946=CARTESIAN_POINT('Ctrl Pts',(0.903627891060305,2.59729794873402,
7.50000065167735));
#381947=CARTESIAN_POINT('Ctrl Pts',(0.903627891060415,2.59729794873398,
7.49482233047108));
#381948=CARTESIAN_POINT('Ctrl Pts',(0.909800645744139,2.59286579032708,
7.50215800491337));
#381949=CARTESIAN_POINT('Ctrl Pts',(0.912631876385749,2.59416534033702,
7.49877273257265));
#381950=CARTESIAN_POINT('Ctrl Pts',(0.915892318043124,2.59303102267921,
7.49481816995647));
#381951=CARTESIAN_POINT('Ctrl Pts',(0.910885454044027,2.5902709478859,7.51043025814041));
#381952=CARTESIAN_POINT('Ctrl Pts',(0.916079119671698,2.59293901728806,
7.51006209594514));
#381953=CARTESIAN_POINT('Ctrl Pts',(0.921555036631549,2.59099137676401,
7.50731281821699));
#381954=CARTESIAN_POINT('Ctrl Pts',(0.9088257196206,2.588344697697,7.51860402984325));
#381955=CARTESIAN_POINT('Ctrl Pts',(0.91438335513013,2.59354216871027,7.51860402984325));
#381956=CARTESIAN_POINT('Ctrl Pts',(0.921552651160791,2.59099222521769,
7.51860402984325));
#381957=CARTESIAN_POINT('Origin',(0.,0.,7.5));
#381958=CARTESIAN_POINT('Origin',(1.0067166110539,2.47051810124199,7.5));
#381959=CARTESIAN_POINT('',(1.0067166110539,2.47051810124199,7.59394543036555));
#381960=CARTESIAN_POINT('',(1.0067166110539,2.47051810124199,8.85049129520029));
#381961=CARTESIAN_POINT('',(1.0067166110539,2.47051810124199,7.5));
#381962=CARTESIAN_POINT('',(1.06195995288109,2.51589809662206,8.78727029226991));
#381963=CARTESIAN_POINT('Ctrl Pts',(1.0067166110539,2.47051810124199,8.85049129520029));
#381964=CARTESIAN_POINT('Ctrl Pts',(1.02515782551208,2.48566675444138,8.82945686509571));
#381965=CARTESIAN_POINT('Ctrl Pts',(1.0435716248751,2.50079288733604,8.80838212259895));
#381966=CARTESIAN_POINT('Ctrl Pts',(1.06195995288109,2.51589809662206,8.78727029226991));
#381967=CARTESIAN_POINT('',(1.07279542170602,2.52479896157614,8.75721825406948));
#381968=CARTESIAN_POINT('Origin',(1.04018760906799,2.49801332713449,8.75937679713162));
#381969=CARTESIAN_POINT('',(1.07279542170602,2.52479896157614,7.51860402984325));
#381970=CARTESIAN_POINT('',(1.07279542170602,2.52479896157614,7.5));
#381971=CARTESIAN_POINT('Ctrl Pts',(1.07279542170602,2.52479896157614,7.51860402984325));
#381972=CARTESIAN_POINT('Ctrl Pts',(1.0642858461782,2.51780871650106,7.52834476460825));
#381973=CARTESIAN_POINT('Ctrl Pts',(1.05577074635674,2.51081393345975,7.53807742314407));
#381974=CARTESIAN_POINT('Ctrl Pts',(1.04724993675612,2.50381446008394,7.54780169004674));
#381975=CARTESIAN_POINT('Ctrl Pts',(1.03375343485922,2.49272767254592,7.5632044032688));
#381976=CARTESIAN_POINT('Ctrl Pts',(1.02024259070159,2.48162910346636,7.57858609112103));
#381977=CARTESIAN_POINT('Ctrl Pts',(1.0067166110539,2.47051810124199,7.59394543036555));
#381978=CARTESIAN_POINT('Origin',(0.964311324797623,2.74827339692444,7.5));
#381979=CARTESIAN_POINT('',(0.985816687379919,2.56001274842385,8.75721825406948));
#381980=CARTESIAN_POINT('',(0.987408162934477,2.54608077127966,8.78727029226991));
#381981=CARTESIAN_POINT('Origin',(0.99144792148259,2.51071621692061,8.75658640621085));
#381982=CARTESIAN_POINT('',(0.99552211070089,2.47505025214476,8.85049129520029));
#381983=CARTESIAN_POINT('Ctrl Pts',(0.987408162934478,2.54608077127966,
8.78727029226991));
#381984=CARTESIAN_POINT('Ctrl Pts',(0.990108975883465,2.52243751507743,
8.80838212259896));
#381985=CARTESIAN_POINT('Ctrl Pts',(0.992813529975795,2.49876150843589,
8.82945686509571));
#381986=CARTESIAN_POINT('Ctrl Pts',(0.99552211070089,2.47505025214476,8.85049129520029));
#381987=CARTESIAN_POINT('',(0.99552211070089,2.47505025214476,7.59394543036555));
#381988=CARTESIAN_POINT('',(0.99552211070089,2.47505025214476,7.5));
#381989=CARTESIAN_POINT('',(0.985816687379919,2.56001274842385,7.51860402984325));
#381990=CARTESIAN_POINT('Ctrl Pts',(0.99552211070089,2.47505025214476,7.59394543036555));
#381991=CARTESIAN_POINT('Ctrl Pts',(0.99353546237874,2.49244162139228,7.57858609112103));
#381992=CARTESIAN_POINT('Ctrl Pts',(0.99155103710418,2.50981352980178,7.56320440326857));
#381993=CARTESIAN_POINT('Ctrl Pts',(0.989568718370395,2.52716699728825,
7.54780169004651));
#381994=CARTESIAN_POINT('Ctrl Pts',(0.98831721182245,2.53812284299494,7.53807742314383));
#381995=CARTESIAN_POINT('Ctrl Pts',(0.987066543906758,2.54907134720939,
7.52834476460825));
#381996=CARTESIAN_POINT('Ctrl Pts',(0.985816687379919,2.56001274842385,
7.51860402984325));
#381997=CARTESIAN_POINT('',(0.985816687379919,2.56001274842385,7.5));
#381998=CARTESIAN_POINT('Origin',(1.00235268932038,2.47583052179234,7.5));
#381999=CARTESIAN_POINT('Ctrl Pts',(0.99552211070089,2.47505025214476,8.85049129520029));
#382000=CARTESIAN_POINT('Ctrl Pts',(0.995544090074704,2.47485784194233,
8.85097269580138));
#382001=CARTESIAN_POINT('Ctrl Pts',(0.995574149201926,2.47466881399358,
8.85143669361005));
#382002=CARTESIAN_POINT('Ctrl Pts',(0.995614535644998,2.47447460147568,
8.8519052845931));
#382003=CARTESIAN_POINT('Ctrl Pts',(0.995693528966433,2.47409473410719,
8.85282181883899));
#382004=CARTESIAN_POINT('Ctrl Pts',(0.995810192031005,2.4737048441739,8.85372622499636));
#382005=CARTESIAN_POINT('Ctrl Pts',(0.99598112712084,2.47330323361083,8.85462257735071));
#382006=CARTESIAN_POINT('Ctrl Pts',(0.99612303136138,2.47296983078523,8.85536669723987));
#382007=CARTESIAN_POINT('Ctrl Pts',(0.996302341696638,2.47262826201748,
8.85610498449051));
#382008=CARTESIAN_POINT('Ctrl Pts',(0.996535657640059,2.47228124643155,
8.85681338218371));
#382009=CARTESIAN_POINT('Ctrl Pts',(0.996747392225142,2.47196632924232,
8.85745625420284));
#382010=CARTESIAN_POINT('Ctrl Pts',(0.997005762944923,2.47164264202972,
8.85808743050664));
#382011=CARTESIAN_POINT('Ctrl Pts',(0.997338632360824,2.47131662869162,
8.85866804508408));
#382012=CARTESIAN_POINT('Ctrl Pts',(0.9974922110936,2.47116621320452,8.85893592806394));
#382013=CARTESIAN_POINT('Ctrl Pts',(0.997661876290776,2.47101538495296,
8.85919241173847));
#382014=CARTESIAN_POINT('Ctrl Pts',(0.99785177500895,2.47086552375509,8.85943017985534));
#382015=CARTESIAN_POINT('Ctrl Pts',(0.998108194494517,2.4706631667743,8.8597512372));
#382016=CARTESIAN_POINT('Ctrl Pts',(0.998408429108391,2.47045792534337,
8.86004599534706));
#382017=CARTESIAN_POINT('Ctrl Pts',(0.998754749324516,2.47026086344443,
8.86026130871721));
#382018=CARTESIAN_POINT('Ctrl Pts',(0.99888154691944,2.47018871352747,8.86034014101235));
#382019=CARTESIAN_POINT('Ctrl Pts',(0.999016420825345,2.47011656559295,
8.86040910639693));
#382020=CARTESIAN_POINT('Ctrl Pts',(0.999155855142542,2.47004668187887,
8.86046313645507));
#382021=CARTESIAN_POINT('Ctrl Pts',(0.999373441226775,2.46993762892833,
8.8605474499083));
#382022=CARTESIAN_POINT('Ctrl Pts',(0.999608137853262,2.46983124429506,
8.86059655985668));
#382023=CARTESIAN_POINT('Ctrl Pts',(0.99984477226483,2.46973408392439,8.86059725258816));
#382024=CARTESIAN_POINT('Ctrl Pts',(1.00008195339643,2.46963669907444,8.86059794692011));
#382025=CARTESIAN_POINT('Ctrl Pts',(1.00032472074386,2.46954995882129,8.86056369958366));
#382026=CARTESIAN_POINT('Ctrl Pts',(1.000558567504,2.46947505032681,8.86048590497774));
#382027=CARTESIAN_POINT('Ctrl Pts',(1.00061959454594,2.46945550144004,8.86046560290182));
#382028=CARTESIAN_POINT('Ctrl Pts',(1.00068083560639,2.46943659030203,8.86044257503091));
#382029=CARTESIAN_POINT('Ctrl Pts',(1.0007403886005,2.46941886991778,8.86041778462583));
#382030=CARTESIAN_POINT('Ctrl Pts',(1.00114110635172,2.46929963372096,8.860250975962));
#382031=CARTESIAN_POINT('Ctrl Pts',(1.00151926053773,2.4692186285124,8.8599848982295));
#382032=CARTESIAN_POINT('Ctrl Pts',(1.00186203918152,2.46916993407642,8.85968173251462));
#382033=CARTESIAN_POINT('Ctrl Pts',(1.0020433494452,2.46914417750965,8.85952137522077));
#382034=CARTESIAN_POINT('Ctrl Pts',(1.00221823035511,2.46912677532505,8.85934740853961));
#382035=CARTESIAN_POINT('Ctrl Pts',(1.00238406177248,2.46911642601951,8.8591675900182));
#382036=CARTESIAN_POINT('Ctrl Pts',(1.00304996111067,2.46907486817829,8.85844552518694));
#382037=CARTESIAN_POINT('Ctrl Pts',(1.00360738943725,2.46914166499387,8.85759444184123));
#382038=CARTESIAN_POINT('Ctrl Pts',(1.00405699467319,2.46923695081303,8.85683498915136));
#382039=CARTESIAN_POINT('Ctrl Pts',(1.00410404466373,2.46924692222023,8.85675551444997));
#382040=CARTESIAN_POINT('Ctrl Pts',(1.00414990599216,2.46925722395856,8.85667699793651));
#382041=CARTESIAN_POINT('Ctrl Pts',(1.00419457359941,2.46926777628528,8.85659965593547));
#382042=CARTESIAN_POINT('Ctrl Pts',(1.00479749924139,2.46941021212987,8.85555568965886));
#382043=CARTESIAN_POINT('Ctrl Pts',(1.00535637758332,2.46963417619405,8.85434650606346));
#382044=CARTESIAN_POINT('Ctrl Pts',(1.00587628317201,2.46993500686091,8.85297329937118));
#382045=CARTESIAN_POINT('Ctrl Pts',(1.00616869838734,2.47010420578114,8.85220095427748));
#382046=CARTESIAN_POINT('Ctrl Pts',(1.00644874670488,2.47029806236456,8.85137579139183));
#382047=CARTESIAN_POINT('Ctrl Pts',(1.0067166110539,2.47051810124199,8.85049129520029));
#382048=CARTESIAN_POINT('Origin',(1.00235268932038,2.47583052179234,7.59394543036555));
#382049=CARTESIAN_POINT('Ctrl Pts',(0.995585924237744,2.47449162041813,
7.59443877723642));
#382050=CARTESIAN_POINT('Ctrl Pts',(0.9962431422676,2.46873825113483,7.58783886950016));
#382051=CARTESIAN_POINT('Ctrl Pts',(1.00467227562428,2.46772390780438,7.58559994247159));
#382052=CARTESIAN_POINT('Ctrl Pts',(0.991998190294714,2.50589909453895,
7.56670252222137));
#382053=CARTESIAN_POINT('Ctrl Pts',(0.992654458457978,2.50015404050766,
7.56004874999027));
#382054=CARTESIAN_POINT('Ctrl Pts',(1.00113098469779,2.49911247430167,7.55786368756704));
#382055=CARTESIAN_POINT('Ctrl Pts',(0.988417156086367,2.53724791833982,
7.53888913333559));
#382056=CARTESIAN_POINT('Ctrl Pts',(0.989077324483416,2.53146872117116,
7.53222002137277));
#382057=CARTESIAN_POINT('Ctrl Pts',(0.997595022281273,2.53044340710011,
7.53005029815327));
#382058=CARTESIAN_POINT('Ctrl Pts',(0.984842983656921,2.56853667326527,
7.51101258149734));
#382059=CARTESIAN_POINT('Ctrl Pts',(0.985511154494491,2.56268742172587,
7.5043616886572));
#382060=CARTESIAN_POINT('Ctrl Pts',(0.994064645198965,2.56171516748282,
7.50217374673251));
#382061=CARTESIAN_POINT('',(0.99425302963392,2.56004646606292,7.50366116523517));
#382062=CARTESIAN_POINT('Ctrl Pts',(0.985816687379918,2.56001274842385,
7.51860402984325));
#382063=CARTESIAN_POINT('Ctrl Pts',(0.98576656725954,2.56045150626061,7.51734760759493));
#382064=CARTESIAN_POINT('Ctrl Pts',(0.985780388944946,2.5608547392218,7.51608817408572));
#382065=CARTESIAN_POINT('Ctrl Pts',(0.985871466452276,2.56122106239949,
7.51481005913119));
#382066=CARTESIAN_POINT('Ctrl Pts',(0.985953966634782,2.56155288668742,
7.51365231206383));
#382067=CARTESIAN_POINT('Ctrl Pts',(0.986099730040545,2.56185495396783,
7.51247773061042));
#382068=CARTESIAN_POINT('Ctrl Pts',(0.986339490022403,2.5621059898196,7.51129758471022));
#382069=CARTESIAN_POINT('Ctrl Pts',(0.98663748429823,2.56241799871397,7.50983079813402));
#382070=CARTESIAN_POINT('Ctrl Pts',(0.987080589722741,2.56263222255329,
7.50839324291155));
#382071=CARTESIAN_POINT('Ctrl Pts',(0.987707923004607,2.5626760041041,7.50715379678855));
#382072=CARTESIAN_POINT('Ctrl Pts',(0.987997732904655,2.56269622991905,
7.50658120839351));
#382073=CARTESIAN_POINT('Ctrl Pts',(0.988368720848084,2.56267347700261,
7.50598221009429));
#382074=CARTESIAN_POINT('Ctrl Pts',(0.988810665406172,2.56258558301011,
7.50545747549611));
#382075=CARTESIAN_POINT('Ctrl Pts',(0.989046500701831,2.56253868005514,
7.50517746087247));
#382076=CARTESIAN_POINT('Ctrl Pts',(0.989305138541046,2.56247291741205,
7.50491486231392));
#382077=CARTESIAN_POINT('Ctrl Pts',(0.98957931871825,2.56238842000837,7.50468370960993));
#382078=CARTESIAN_POINT('Ctrl Pts',(0.989989304568402,2.56226206973669,
7.50433806340447));
#382079=CARTESIAN_POINT('Ctrl Pts',(0.990446172564123,2.56208950838184,
7.50405484070984));
#382080=CARTESIAN_POINT('Ctrl Pts',(0.990918900363615,2.56188168744653,
7.50385766036131));
#382081=CARTESIAN_POINT('Ctrl Pts',(0.990969451253917,2.56185946422777,
7.50383657498791));
#382082=CARTESIAN_POINT('Ctrl Pts',(0.991020166949378,2.56183686084834,
7.50381643264937));
#382083=CARTESIAN_POINT('Ctrl Pts',(0.991070997752475,2.56181390761954,
7.50379723213559));
#382084=CARTESIAN_POINT('Ctrl Pts',(0.991410309991058,2.56166068730882,
7.50366906242519));
#382085=CARTESIAN_POINT('Ctrl Pts',(0.991761836329712,2.56148788948196,
7.50358235568538));
#382086=CARTESIAN_POINT('Ctrl Pts',(0.992096660797237,2.56131318891304,
7.5035341175365));
#382087=CARTESIAN_POINT('Ctrl Pts',(0.992598692191478,2.56105124518222,
7.50346178989176));
#382088=CARTESIAN_POINT('Ctrl Pts',(0.993127626184805,2.56074810754123,
7.50346967198527));
#382089=CARTESIAN_POINT('Ctrl Pts',(0.99363771872215,2.56043454298074,7.50354272648692));
#382090=CARTESIAN_POINT('Ctrl Pts',(0.993847530341052,2.56030556738661,
7.50357277531559));
#382091=CARTESIAN_POINT('Ctrl Pts',(0.994053949759978,2.56017511988168,
7.50361331098761));
#382092=CARTESIAN_POINT('Ctrl Pts',(0.994253029634434,2.56004646606424,
7.50366116523659));
#382093=CARTESIAN_POINT('',(1.00345144303435,2.47854446470828,7.57603338622103));
#382094=CARTESIAN_POINT('Origin',(1.00677029912172,2.48673450035404,7.58486873427626));
#382095=CARTESIAN_POINT('Ctrl Pts',(0.994253029622191,2.56004646611905,
7.50366116529969));
#382096=CARTESIAN_POINT('Ctrl Pts',(0.997314994686469,2.53292355755921,
7.52783573079709));
#382097=CARTESIAN_POINT('Ctrl Pts',(1.00038100552659,2.50575750849376,7.55196141284068));
#382098=CARTESIAN_POINT('Ctrl Pts',(1.00345144254825,2.47854446586212,7.57603338728831));
#382099=CARTESIAN_POINT('Ctrl Pts',(0.995580073096902,2.47609196989964,
7.59639677331372));
#382100=CARTESIAN_POINT('Ctrl Pts',(0.994718951965599,2.45697504293773,
7.59974925422226));
#382101=CARTESIAN_POINT('Ctrl Pts',(1.00739967866912,2.4713067419417,7.5963967733137));
#382102=CARTESIAN_POINT('Ctrl Pts',(0.994780473004155,2.47227415065622,
7.58707626057422));
#382103=CARTESIAN_POINT('Ctrl Pts',(0.998585879238804,2.46652642806453,
7.58811717123965));
#382104=CARTESIAN_POINT('Ctrl Pts',(1.00531808064709,2.46800794613741,7.58707626057424));
#382105=CARTESIAN_POINT('Ctrl Pts',(0.999909163054375,2.47553331782442,
7.5801537675693));
#382106=CARTESIAN_POINT('Ctrl Pts',(1.00117949275383,2.47293270359069,7.58208760766041));
#382107=CARTESIAN_POINT('Ctrl Pts',(1.00390123521105,2.47391710692994,7.58015376756929));
#382108=CARTESIAN_POINT('Ctrl Pts',(1.0034514427236,2.47854446394126,7.57603338509286));
#382109=CARTESIAN_POINT('Ctrl Pts',(1.0034514427236,2.47854446394126,7.57603338509286));
#382110=CARTESIAN_POINT('Ctrl Pts',(1.0034514427236,2.47854446394126,7.57603338509286));
#382111=CARTESIAN_POINT('Origin',(1.0067650098081,2.48673664175957,7.58486873427622));
#382112=CARTESIAN_POINT('Ctrl Pts',(1.07944577964471,2.53026194050811,7.51098857897448));
#382113=CARTESIAN_POINT('Ctrl Pts',(1.07489655658135,2.52652495221649,7.50433767179956));
#382114=CARTESIAN_POINT('Ctrl Pts',(1.06807576525984,2.53177708100688,7.50214974420965));
#382115=CARTESIAN_POINT('Ctrl Pts',(1.0551042351301,2.51026642356289,7.53887321589164));
#382116=CARTESIAN_POINT('Ctrl Pts',(1.05060951983246,2.50657421102296,7.53220407452058));
#382117=CARTESIAN_POINT('Ctrl Pts',(1.04377751552321,2.51176329928973,7.53003438070911));
#382118=CARTESIAN_POINT('Ctrl Pts',(1.03071594587084,2.49023250784912,7.56669465659229));
#382119=CARTESIAN_POINT('Ctrl Pts',(1.02624779350493,2.48656211559886,7.56004085833293));
#382120=CARTESIAN_POINT('Ctrl Pts',(1.01943406247276,2.4917108746287,7.55785582193788));
#382121=CARTESIAN_POINT('Ctrl Pts',(1.00628201485162,2.47016109942061,7.59443891967696));
#382122=CARTESIAN_POINT('Ctrl Pts',(1.00180738422111,2.46648538555857,7.58783901202978));
#382123=CARTESIAN_POINT('Ctrl Pts',(0.99504666090435,2.47162073347497,7.58560008491213));
#382124=CARTESIAN_POINT('',(1.0667586375038,2.53069219871728,7.50366116523517));
#382125=CARTESIAN_POINT('Ctrl Pts',(1.06675863750394,2.53069219871762,7.50366116523554));
#382126=CARTESIAN_POINT('Ctrl Pts',(1.06750186807347,2.53054473401917,7.50350835821027));
#382127=CARTESIAN_POINT('Ctrl Pts',(1.06818027974489,2.53038499793928,7.50345484955999));
#382128=CARTESIAN_POINT('Ctrl Pts',(1.06881417987673,2.5302088259119,7.50349758195598));
#382129=CARTESIAN_POINT('Ctrl Pts',(1.06913941765563,2.5301184365966,7.50351950684424));
#382130=CARTESIAN_POINT('Ctrl Pts',(1.06948502939518,2.53001493618197,7.50357029184312));
#382131=CARTESIAN_POINT('Ctrl Pts',(1.06981555540291,2.52990597100817,7.50365515313923));
#382132=CARTESIAN_POINT('Ctrl Pts',(1.070324038246,2.52973833844652,7.50378570417639));
#382133=CARTESIAN_POINT('Ctrl Pts',(1.07081185253134,2.52955318148128,7.50400001621911));
#382134=CARTESIAN_POINT('Ctrl Pts',(1.07124106282399,2.52936247059274,7.50428903009634));
#382135=CARTESIAN_POINT('Ctrl Pts',(1.07128870186433,2.52934130315135,7.50432110841318));
#382136=CARTESIAN_POINT('Ctrl Pts',(1.07133564874016,2.52932007288124,7.50435406373354));
#382137=CARTESIAN_POINT('Ctrl Pts',(1.07138187362868,2.52929879997845,7.50438785222352));
#382138=CARTESIAN_POINT('Ctrl Pts',(1.07166409879162,2.5291689186819,7.50459414719561));
#382139=CARTESIAN_POINT('Ctrl Pts',(1.0719236882083,2.52903491181198,7.50483629897752));
#382140=CARTESIAN_POINT('Ctrl Pts',(1.07215130076292,2.52890308253883,7.5050991045531));
#382141=CARTESIAN_POINT('Ctrl Pts',(1.07265343691994,2.52861225392128,7.50567888004914));
#382142=CARTESIAN_POINT('Ctrl Pts',(1.07301999334669,2.52832101331307,7.50637912803144));
#382143=CARTESIAN_POINT('Ctrl Pts',(1.07327584969574,2.52804770250378,7.50710440483569));
#382144=CARTESIAN_POINT('Ctrl Pts',(1.07333859075199,2.52798068126737,7.50728225710685));
#382145=CARTESIAN_POINT('Ctrl Pts',(1.07339603063641,2.52791350375378,7.50746498566954));
#382146=CARTESIAN_POINT('Ctrl Pts',(1.07344714514511,2.52784800883597,7.50764697238949));
#382147=CARTESIAN_POINT('Ctrl Pts',(1.0737219226768,2.52749592618251,7.50862528291181));
#382148=CARTESIAN_POINT('Ctrl Pts',(1.07384211344801,2.52716305316058,7.50965856837422));
#382149=CARTESIAN_POINT('Ctrl Pts',(1.0738738316038,2.526854320862,7.51067959873202));
#382150=CARTESIAN_POINT('Ctrl Pts',(1.07389128614494,2.52668442508868,7.51124147302578));
#382151=CARTESIAN_POINT('Ctrl Pts',(1.07388152051965,2.52652175402811,7.51180065547253));
#382152=CARTESIAN_POINT('Ctrl Pts',(1.07385284243991,2.52636695067111,7.51235175716501));
#382153=CARTESIAN_POINT('Ctrl Pts',(1.0737537482504,2.52583204340633,7.51425603304536));
#382154=CARTESIAN_POINT('Ctrl Pts',(1.0734110653662,2.52532840179909,7.5162690050518));
#382155=CARTESIAN_POINT('Ctrl Pts',(1.07288284142304,2.52487255277835,7.51827788969244));
#382156=CARTESIAN_POINT('Ctrl Pts',(1.07285425294504,2.52484788136791,7.51838661432545));
#382157=CARTESIAN_POINT('Ctrl Pts',(1.07282511102271,2.52482335005463,7.51849533314857));
#382158=CARTESIAN_POINT('Ctrl Pts',(1.07279542170602,2.52479896157614,7.51860402984325));
#382159=CARTESIAN_POINT('Ctrl Pts',(1.00345144418691,2.47854446519998,7.57603338728984));
#382160=CARTESIAN_POINT('Ctrl Pts',(1.0245887295383,2.49595688723387,7.55196141284921));
#382161=CARTESIAN_POINT('Ctrl Pts',(1.04569014275367,2.51333863069779,7.52783573083105));
#382162=CARTESIAN_POINT('Ctrl Pts',(1.06675863755274,2.53069219875055,7.50366116530176));
#382163=CARTESIAN_POINT('Origin',(3.46738858720981E-16,8.56451684780641E-16,
7.49482233047033));
#382164=CARTESIAN_POINT('Origin',(0.99105311921787,2.55180719586895,7.49482233047033));
#382165=CARTESIAN_POINT('Origin',(0.,0.,7.50366116523517));
#382166=CARTESIAN_POINT('Origin',(1.06332537456789,2.52254740248822,7.49482233047033));
#382167=CARTESIAN_POINT('Ctrl Pts',(0.985816807380114,2.56001169753274,
7.51860402984325));
#382168=CARTESIAN_POINT('Ctrl Pts',(0.98495387743998,2.56757156776632,7.51860402984325));
#382169=CARTESIAN_POINT('Ctrl Pts',(0.97784219075701,2.57027715431148,7.51860402984325));
#382170=CARTESIAN_POINT('Ctrl Pts',(0.985496394341871,2.56281872879759,
7.51041458714366));
#382171=CARTESIAN_POINT('Ctrl Pts',(0.983269033888734,2.56821254295569,
7.51004642900443));
#382172=CARTESIAN_POINT('Ctrl Pts',(0.977840229438259,2.57027790048013,
7.5072913648301));
#382173=CARTESIAN_POINT('Ctrl Pts',(0.988011340623422,2.56408315847148,
7.50215815450137));
#382174=CARTESIAN_POINT('Ctrl Pts',(0.986699593402179,2.5669075847334,7.4987716367153));
#382175=CARTESIAN_POINT('Ctrl Pts',(0.983483430761492,2.56815667298609,
7.49481588533169));
#382176=CARTESIAN_POINT('Ctrl Pts',(0.994252830331128,2.56004595288801,
7.50366171572174));
#382177=CARTESIAN_POINT('Ctrl Pts',(0.995578475926988,2.56345928352118,
7.50000045605858));
#382178=CARTESIAN_POINT('Ctrl Pts',(0.995578475926872,2.56345928352122,
7.49482233047317));
#382179=CARTESIAN_POINT('Origin',(0.973397453526297,2.55859407633734,7.51860402984325));
#382180=CARTESIAN_POINT('Origin',(0.973397453526297,2.55859407633734,9.));
#382181=CARTESIAN_POINT('Origin',(0.973397453526297,2.55859407633734,8.75721825406948));
#382182=CARTESIAN_POINT('Ctrl Pts',(0.987712021557103,2.54342048849949,
8.78942910404912));
#382183=CARTESIAN_POINT('Ctrl Pts',(0.987099662981816,2.54895921088619,
8.79672699501691));
#382184=CARTESIAN_POINT('Ctrl Pts',(0.978198471170056,2.54962424495469,
8.79893251111267));
#382185=CARTESIAN_POINT('Ctrl Pts',(0.986464237477126,2.55434378716015,
8.78111911759583));
#382186=CARTESIAN_POINT('Ctrl Pts',(0.985730880534924,2.560909188726,8.78644465894813));
#382187=CARTESIAN_POINT('Ctrl Pts',(0.977964537858769,2.56323285677718,
8.78817647674132));
#382188=CARTESIAN_POINT('Ctrl Pts',(0.985686588644408,2.56115144742715,
8.76780923932029));
#382189=CARTESIAN_POINT('Ctrl Pts',(0.984815827444813,2.56890106107581,
8.76988516158374));
#382190=CARTESIAN_POINT('Ctrl Pts',(0.977807256217952,2.57173236991702,
8.77093053738833));
#382191=CARTESIAN_POINT('Ctrl Pts',(0.985838219522192,2.55982404684426,
8.75371302330492));
#382192=CARTESIAN_POINT('Ctrl Pts',(0.984989587073317,2.56738354579158,
8.75300828287559));
#382193=CARTESIAN_POINT('Ctrl Pts',(0.97783747505197,2.5700746111881,8.75267964240738));
#382194=CARTESIAN_POINT('Origin',(0.974988929080856,2.54466209919315,8.78727029226991));
#382195=CARTESIAN_POINT('Ctrl Pts',(0.99552211070089,2.47505025214476,8.85049129520029));
#382196=CARTESIAN_POINT('Ctrl Pts',(0.99485935071093,2.48085213644374,8.85711686593484));
#382197=CARTESIAN_POINT('Ctrl Pts',(0.986367352980481,2.48184548263715,
8.85933012996512));
#382198=CARTESIAN_POINT('Ctrl Pts',(0.992813526340779,2.49876154025728,
8.82945683644722));
#382199=CARTESIAN_POINT('Ctrl Pts',(0.992145265042191,2.50461158370381,
8.83607469902387));
#382200=CARTESIAN_POINT('Ctrl Pts',(0.98362397791506,2.50557059788235,8.83829567148519));
#382201=CARTESIAN_POINT('Ctrl Pts',(0.990108979344078,2.52243748478279,
8.80838214965003));
#382202=CARTESIAN_POINT('Ctrl Pts',(0.989438080774401,2.52831061523211,
8.81501364461989));
#382203=CARTESIAN_POINT('Ctrl Pts',(0.980885428519758,2.529259800149,8.81722098428721));
#382204=CARTESIAN_POINT('Ctrl Pts',(0.987408162934478,2.54608077127966,
8.78727029226991));
#382205=CARTESIAN_POINT('Ctrl Pts',(0.986737152926342,2.55195487727525,
8.79393457792714));
#382206=CARTESIAN_POINT('Ctrl Pts',(0.978151351640454,2.55291583068591,
8.79610912703474));
#382207=CARTESIAN_POINT('Origin',(0.983102876847268,2.47363158005825,8.85049129520029));
#382208=CARTESIAN_POINT('Ctrl Pts',(1.0067166110539,2.47051810124199,8.85049129520029));
#382209=CARTESIAN_POINT('Ctrl Pts',(1.01122897392938,2.47422481049726,8.85711686593484));
#382210=CARTESIAN_POINT('Ctrl Pts',(1.01802024859354,2.46903064544887,8.85933012996512));
#382211=CARTESIAN_POINT('Ctrl Pts',(1.00272458875461,2.46723882907078,8.86332496987232));
#382212=CARTESIAN_POINT('Ctrl Pts',(1.00710562609236,2.46576967753949,8.86648636486738));
#382213=CARTESIAN_POINT('Ctrl Pts',(1.00684152845079,2.45986998650278,8.87206031107457));
#382214=CARTESIAN_POINT('Ctrl Pts',(0.996112429222676,2.46988252956821,
8.86341338519875));
#382215=CARTESIAN_POINT('Ctrl Pts',(0.991918717460033,2.47185388754846,
8.86654584966059));
#382216=CARTESIAN_POINT('Ctrl Pts',(0.988034913849316,2.46737725686224,
8.87215952290715));
#382217=CARTESIAN_POINT('Ctrl Pts',(0.99552211070089,2.47505025214476,8.85049129520029));
#382218=CARTESIAN_POINT('Ctrl Pts',(0.99485935071093,2.48085213644374,8.85711686593484));
#382219=CARTESIAN_POINT('Ctrl Pts',(0.986367352980481,2.48184548263715,
8.85933012996512));
#382220=CARTESIAN_POINT('Origin',(1.01465101420574,2.46085915478682,8.85049129520029));
#382221=CARTESIAN_POINT('Ctrl Pts',(1.06195995288109,2.51589809662206,8.78727029226991));
#382222=CARTESIAN_POINT('Ctrl Pts',(1.06652848552586,2.51965094689245,8.79393457792714));
#382223=CARTESIAN_POINT('Ctrl Pts',(1.07336460881939,2.51436825501293,8.79610912703474));
#382224=CARTESIAN_POINT('Ctrl Pts',(1.04357160131372,2.50079286798139,8.80838214965002));
#382225=CARTESIAN_POINT('Ctrl Pts',(1.04813937523626,2.5045450949946,8.81501364461995));
#382226=CARTESIAN_POINT('Ctrl Pts',(1.05494349880895,2.4992770104278,8.81722098428721));
#382227=CARTESIAN_POINT('Ctrl Pts',(1.02515785026088,2.48566677477144,8.82945683644722));
#382228=CARTESIAN_POINT('Ctrl Pts',(1.02970766847646,2.48940425195465,8.83607469902389));
#382229=CARTESIAN_POINT('Ctrl Pts',(1.036496098976,2.48416504840349,8.83829567148519));
#382230=CARTESIAN_POINT('Ctrl Pts',(1.0067166110539,2.47051810124199,8.85049129520029));
#382231=CARTESIAN_POINT('Ctrl Pts',(1.01122897392938,2.47422481049726,8.85711686593484));
#382232=CARTESIAN_POINT('Ctrl Pts',(1.01802024859354,2.46903064544887,8.85933012996512));
#382233=CARTESIAN_POINT('Origin',(1.06989435603293,2.50623915016688,8.78727029226991));
#382234=CARTESIAN_POINT('Ctrl Pts',(1.07265235650019,2.52468141587758,8.75374538247849));
#382235=CARTESIAN_POINT('Ctrl Pts',(1.07851586339024,2.52951501343406,8.75304829418602));
#382236=CARTESIAN_POINT('Ctrl Pts',(1.08552051380797,2.52648095415081,8.75272238421917));
#382237=CARTESIAN_POINT('Ctrl Pts',(1.07367232836398,2.52551927882055,8.76769408445016));
#382238=CARTESIAN_POINT('Ctrl Pts',(1.07968382607103,2.53047397863891,8.76974318093967));
#382239=CARTESIAN_POINT('Ctrl Pts',(1.08668211825915,2.5276380901133,8.7707786988043));
#382240=CARTESIAN_POINT('Ctrl Pts',(1.0684445336205,2.52122487068539,8.78108014887994));
#382241=CARTESIAN_POINT('Ctrl Pts',(1.07353664488911,2.52542673219291,8.78639403366327));
#382242=CARTESIAN_POINT('Ctrl Pts',(1.08073062501097,2.52171610883081,8.78812224174741));
#382243=CARTESIAN_POINT('Ctrl Pts',(1.05987733210578,2.51418728372499,8.78944554828685));
#382244=CARTESIAN_POINT('Ctrl Pts',(1.06416521194975,2.51773277439069,8.79673892988685));
#382245=CARTESIAN_POINT('Ctrl Pts',(1.0710163762168,2.5120261902546,8.79894799272499));
#382246=CARTESIAN_POINT('Origin',(1.08072982485787,2.51514001512097,8.75721825406948));
#382247=CARTESIAN_POINT('Origin',(1.08072982485787,2.51514001512097,9.));
#382248=CARTESIAN_POINT('Origin',(1.08072982485787,2.51514001512097,7.51860402984325));
#382249=CARTESIAN_POINT('Ctrl Pts',(1.06675833194055,2.53069147382352,7.50366195182966));
#382250=CARTESIAN_POINT('Ctrl Pts',(1.06818074157518,2.53406588377807,7.50000065167735));
#382251=CARTESIAN_POINT('Ctrl Pts',(1.06818074157528,2.53406588377802,7.49482233047108));
#382252=CARTESIAN_POINT('Ctrl Pts',(1.07405684430837,2.52924734196545,7.50215800491337));
#382253=CARTESIAN_POINT('Ctrl Pts',(1.07696552033799,2.5303628243405,7.49877273257266));
#382254=CARTESIAN_POINT('Ctrl Pts',(1.08014658708643,2.52902194004574,7.49481816995649));
#382255=CARTESIAN_POINT('Ctrl Pts',(1.07497317162722,2.52658832699994,7.51043025814042));
#382256=CARTESIAN_POINT('Ctrl Pts',(1.08032711010537,2.52891815526811,7.51006209594513));
#382257=CARTESIAN_POINT('Ctrl Pts',(1.08566699044973,2.52662367317617,7.50731281821698));
#382258=CARTESIAN_POINT('Ctrl Pts',(1.07279425387574,2.52479800213626,7.51860402984325));
#382259=CARTESIAN_POINT('Ctrl Pts',(1.07867347373823,2.52962871545824,7.51860402984325));
#382260=CARTESIAN_POINT('Ctrl Pts',(1.08566466424078,2.52662467272426,7.51860402984325));
#382261=CARTESIAN_POINT('Origin',(0.,0.,7.5));
#382262=CARTESIAN_POINT('Origin',(1.16293484201938,2.40094160211229,7.5));
#382263=CARTESIAN_POINT('',(1.16293484201938,2.40094160211229,7.59394543036555));
#382264=CARTESIAN_POINT('',(1.16293484201938,2.40094160211229,8.85049129520029));
#382265=CARTESIAN_POINT('',(1.16293484201938,2.40094160211229,7.5));
#382266=CARTESIAN_POINT('',(1.22097218676268,2.44268890636152,8.78727029226991));
#382267=CARTESIAN_POINT('Ctrl Pts',(1.16293484201938,2.40094160211229,8.85049129520029));
#382268=CARTESIAN_POINT('Ctrl Pts',(1.18230874456754,2.41487759811195,8.82945686509571));
#382269=CARTESIAN_POINT('Ctrl Pts',(1.20165384546692,2.42879287656844,8.80838212259896));
#382270=CARTESIAN_POINT('Ctrl Pts',(1.22097218676268,2.44268890636152,8.78727029226991));
#382271=CARTESIAN_POINT('',(1.23235567333044,2.45087725266274,8.75721825406948));
#382272=CARTESIAN_POINT('Origin',(1.19809869544952,2.42623584190851,8.75937679713156));
#382273=CARTESIAN_POINT('',(1.23235567333044,2.45087725266274,7.51860402984325));
#382274=CARTESIAN_POINT('',(1.23235567333044,2.45087725266274,7.5));
#382275=CARTESIAN_POINT('Ctrl Pts',(1.23235567333044,2.45087725266274,7.51860402984325));
#382276=CARTESIAN_POINT('Ctrl Pts',(1.22341571509851,2.44444658017187,7.52834476460825));
#382277=CARTESIAN_POINT('Ctrl Pts',(1.2144699531747,2.43801173298123,7.53807742314407));
#382278=CARTESIAN_POINT('Ctrl Pts',(1.20551819269233,2.43157257091969,7.54780169004674));
#382279=CARTESIAN_POINT('Ctrl Pts',(1.19133908788962,2.42137328622122,7.5632044032688));
#382280=CARTESIAN_POINT('Ctrl Pts',(1.17714491544795,2.41116316309945,7.57858609112103));
#382281=CARTESIAN_POINT('Ctrl Pts',(1.16293484201938,2.40094160211229,7.59394543036555));
#382282=CARTESIAN_POINT('Origin',(1.13841252486685,2.68084313576939,7.5));
#382283=CARTESIAN_POINT('',(1.14781180121214,2.49159143565062,8.75721825406948));
#382284=CARTESIAN_POINT('',(1.14850738206909,2.4775861170588,8.78727029226991));
#382285=CARTESIAN_POINT('Origin',(1.15027302572293,2.4420353947459,8.75658640620927));
#382286=CARTESIAN_POINT('',(1.15205371787328,2.40618167532515,8.85049129520029));
#382287=CARTESIAN_POINT('Ctrl Pts',(1.14850738206909,2.4775861170588,8.78727029226991));
#382288=CARTESIAN_POINT('Ctrl Pts',(1.14968781728227,2.45381839678239,8.80838212259896));
#382289=CARTESIAN_POINT('Ctrl Pts',(1.15086988762437,2.4300177536601,8.82945686509571));
#382290=CARTESIAN_POINT('Ctrl Pts',(1.15205371787328,2.40618167532515,8.85049129520029));
#382291=CARTESIAN_POINT('',(1.15205371787328,2.40618167532515,7.59394543036555));
#382292=CARTESIAN_POINT('',(1.15205371787328,2.40618167532515,7.5));
#382293=CARTESIAN_POINT('',(1.14781180121214,2.49159143565062,7.51860402984325));
#382294=CARTESIAN_POINT('Ctrl Pts',(1.15205371787328,2.40618167532515,7.59394543036555));
#382295=CARTESIAN_POINT('Ctrl Pts',(1.15118542018663,2.42366459713436,7.57858609112103));
#382296=CARTESIAN_POINT('Ctrl Pts',(1.15031809411991,2.44112795565877,7.56320440326857));
#382297=CARTESIAN_POINT('Ctrl Pts',(1.14945168875185,2.45857277618248,7.54780169004651));
#382298=CARTESIAN_POINT('Ctrl Pts',(1.14890469700283,2.469586296229,7.53807742314383));
#382299=CARTESIAN_POINT('Ctrl Pts',(1.14835807179199,2.4805924361358,7.52834476460825));
#382300=CARTESIAN_POINT('Ctrl Pts',(1.14781180121214,2.49159143565062,7.51860402984325));
#382301=CARTESIAN_POINT('',(1.14781180121214,2.49159143565062,7.5));
#382302=CARTESIAN_POINT('Origin',(1.15892025438438,2.40652270515031,7.5));
#382303=CARTESIAN_POINT('Ctrl Pts',(1.15205371787328,2.40618167532515,8.85049129520029));
#382304=CARTESIAN_POINT('Ctrl Pts',(1.15206332432412,2.4059882522268,8.85097269580138));
#382305=CARTESIAN_POINT('Ctrl Pts',(1.15208121062938,2.40579768676135,8.85143669361005));
#382306=CARTESIAN_POINT('Ctrl Pts',(1.15210907085543,2.40560128570561,8.8519052845931));
#382307=CARTESIAN_POINT('Ctrl Pts',(1.15216356369075,2.40521713769589,8.85282181883899));
#382308=CARTESIAN_POINT('Ctrl Pts',(1.15225500672475,2.40482057420507,8.85372622499636));
#382309=CARTESIAN_POINT('Ctrl Pts',(1.15239985933298,2.40440883694516,8.85462257735071));
#382310=CARTESIAN_POINT('Ctrl Pts',(1.15252011082366,2.40406702729552,8.85536669723986));
#382311=CARTESIAN_POINT('Ctrl Pts',(1.15267716836052,2.40371467186481,8.85610498449051));
#382312=CARTESIAN_POINT('Ctrl Pts',(1.15288777156639,2.40335342065579,8.8568133821837));
#382313=CARTESIAN_POINT('Ctrl Pts',(1.15307889430647,2.40302558461626,8.85745625420285));
#382314=CARTESIAN_POINT('Ctrl Pts',(1.15331599546498,2.4026860085849,8.85808743050666));
#382315=CARTESIAN_POINT('Ctrl Pts',(1.15362729321869,2.40233933805946,8.85866804508411));
#382316=CARTESIAN_POINT('Ctrl Pts',(1.15377091925414,2.40217939179392,8.85893592806396));
#382317=CARTESIAN_POINT('Ctrl Pts',(1.15393057225671,2.40201800294868,8.85919241173849));
#382318=CARTESIAN_POINT('Ctrl Pts',(1.15411047916768,2.40185628280407,8.85943017985534));
#382319=CARTESIAN_POINT('Ctrl Pts',(1.15435340675564,2.40163791273455,8.8597512372));
#382320=CARTESIAN_POINT('Ctrl Pts',(1.15463987464167,2.40141385689639,8.86004599534705));
#382321=CARTESIAN_POINT('Ctrl Pts',(1.15497285750655,2.40119501106983,8.86026130871721));
#382322=CARTESIAN_POINT('Ctrl Pts',(1.15509477192116,2.40111488544281,8.86034014101235));
#382323=CARTESIAN_POINT('Ctrl Pts',(1.15522474618013,2.40103424434314,8.86040910639692));
#382324=CARTESIAN_POINT('Ctrl Pts',(1.15535941654963,2.40095557062528,8.86046313645507));
#382325=CARTESIAN_POINT('Ctrl Pts',(1.15556956853339,2.40083280094743,8.8605474499083));
#382326=CARTESIAN_POINT('Ctrl Pts',(1.15579696686363,2.40071159782832,8.86059655985668));
#382327=CARTESIAN_POINT('Ctrl Pts',(1.1560268899981,2.40059947586524,8.86059725258816));
#382328=CARTESIAN_POINT('Ctrl Pts',(1.15625734434686,2.40048709485563,8.86059794692011));
#382329=CARTESIAN_POINT('Ctrl Pts',(1.15649405543564,2.40038497866229,8.86056369958366));
#382330=CARTESIAN_POINT('Ctrl Pts',(1.15672262232881,2.40029524146198,8.86048590497774));
#382331=CARTESIAN_POINT('Ctrl Pts',(1.15678227148268,2.40027182272449,8.86046560290182));
#382332=CARTESIAN_POINT('Ctrl Pts',(1.15684217507603,2.40024902671322,8.86044257503091));
#382333=CARTESIAN_POINT('Ctrl Pts',(1.15690047036321,2.40022752716397,8.86041778462583));
#382334=CARTESIAN_POINT('Ctrl Pts',(1.15729272530747,2.40008286187624,8.86025097596201));
#382335=CARTESIAN_POINT('Ctrl Pts',(1.15766491251362,2.39997779467968,8.8599848982295));
#382336=CARTESIAN_POINT('Ctrl Pts',(1.15800386701869,2.39990723838853,8.85968173251461));
#382337=CARTESIAN_POINT('Ctrl Pts',(1.1581831545321,2.39986991815291,8.85952137522076));
#382338=CARTESIAN_POINT('Ctrl Pts',(1.15835656116863,2.3998413470646,8.85934740853961));
#382339=CARTESIAN_POINT('Ctrl Pts',(1.15852138878528,2.39982039416742,8.8591675900182));
#382340=CARTESIAN_POINT('Ctrl Pts',(1.15918325734183,2.39973625739416,8.85844552518695));
#382341=CARTESIAN_POINT('Ctrl Pts',(1.15974382005879,2.39976720241302,8.85759444184125));
#382342=CARTESIAN_POINT('Ctrl Pts',(1.16019860651594,2.39983348615086,8.85683498915139));
#382343=CARTESIAN_POINT('Ctrl Pts',(1.16024619870749,2.3998404225675,8.85675551444999));
#382344=CARTESIAN_POINT('Ctrl Pts',(1.16029262584355,2.3998477647944,8.85667699793652));
#382345=CARTESIAN_POINT('Ctrl Pts',(1.16033787776631,2.39985543357681,8.85659965593547));
#382346=CARTESIAN_POINT('Ctrl Pts',(1.16094869052878,2.39995894719317,8.85555568965886));
#382347=CARTESIAN_POINT('Ctrl Pts',(1.16152077002208,2.40014664364084,8.85434650606346));
#382348=CARTESIAN_POINT('Ctrl Pts',(1.16205888169598,2.40041354575341,8.85297329937118));
#382349=CARTESIAN_POINT('Ctrl Pts',(1.16236153672493,2.40056366192914,8.85220095427747));
#382350=CARTESIAN_POINT('Ctrl Pts',(1.16265343008711,2.4007391774561,8.85137579139184));
#382351=CARTESIAN_POINT('Ctrl Pts',(1.16293484201938,2.40094160211229,8.85049129520029));
#382352=CARTESIAN_POINT('Origin',(1.15892025438438,2.40652270515031,7.59394543036555));
#382353=CARTESIAN_POINT('Ctrl Pts',(1.15208160864076,2.40562010281997,7.59443877723642));
#382354=CARTESIAN_POINT('Ctrl Pts',(1.15236885671008,2.39983644634717,7.58783886950016));
#382355=CARTESIAN_POINT('Ctrl Pts',(1.16071568230793,2.39828413066547,7.58559994247159));
#382356=CARTESIAN_POINT('Ctrl Pts',(1.15051352985786,2.43719291381974,7.56670252222138));
#382357=CARTESIAN_POINT('Ctrl Pts',(1.1508003627722,2.43141761637252,7.56004874999025));
#382358=CARTESIAN_POINT('Ctrl Pts',(1.15919273970381,2.42983509727515,7.55786368756704));
#382359=CARTESIAN_POINT('Ctrl Pts',(1.14894837930542,2.46870676574945,7.5388891333356));
#382360=CARTESIAN_POINT('Ctrl Pts',(1.14923691688177,2.46289714542676,7.53222002137278));
#382361=CARTESIAN_POINT('Ctrl Pts',(1.15767142205791,2.4613282072018,7.53005029815327));
#382362=CARTESIAN_POINT('Ctrl Pts',(1.14738622780756,2.50016023258599,7.51101258149734));
#382363=CARTESIAN_POINT('Ctrl Pts',(1.14767826298363,2.49428018910866,7.5043616886572));
#382364=CARTESIAN_POINT('Ctrl Pts',(1.15615188708086,2.49276190843519,7.50217374673251));
#382365=CARTESIAN_POINT('',(1.15623297039273,2.49108456570913,7.50366116523517));
#382366=CARTESIAN_POINT('Ctrl Pts',(1.14781180121214,2.49159143565062,7.51860402984325));
#382367=CARTESIAN_POINT('Ctrl Pts',(1.14778989538004,2.49203250321948,7.51734760759494));
#382368=CARTESIAN_POINT('Ctrl Pts',(1.14782952389184,2.49243402213688,7.51608817408573));
#382369=CARTESIAN_POINT('Ctrl Pts',(1.14794388467724,2.49279375730838,7.51481005913121));
#382370=CARTESIAN_POINT('Ctrl Pts',(1.14804747540939,2.49311961402289,7.51365231206384));
#382371=CARTESIAN_POINT('Ctrl Pts',(1.14821229284571,2.4934117215802,7.51247773061043));
#382372=CARTESIAN_POINT('Ctrl Pts',(1.14846764413722,2.49364688017711,7.51129758471022));
#382373=CARTESIAN_POINT('Ctrl Pts',(1.14878501663034,2.49393915545694,7.50983079813402));
#382374=CARTESIAN_POINT('Ctrl Pts',(1.14924093701575,2.49412454928838,7.50839324291155));
#382375=CARTESIAN_POINT('Ctrl Pts',(1.1498697864677,2.49412804750393,7.50715379678855));
#382376=CARTESIAN_POINT('Ctrl Pts',(1.15016029679463,2.49412966357872,7.50658120839351));
#382377=CARTESIAN_POINT('Ctrl Pts',(1.15052906471918,2.49408318813145,7.50598221009429));
#382378=CARTESIAN_POINT('Ctrl Pts',(1.15096446986735,2.49396715924153,7.50545747549611));
#382379=CARTESIAN_POINT('Ctrl Pts',(1.15119681553145,2.49390524263443,7.50517746087247));
#382380=CARTESIAN_POINT('Ctrl Pts',(1.15145070854448,2.49382304412449,7.50491486231392));
#382381=CARTESIAN_POINT('Ctrl Pts',(1.15171891162186,2.49372115354553,7.50468370960992));
#382382=CARTESIAN_POINT('Ctrl Pts',(1.15211995982241,2.49356879499042,7.50433806340447));
#382383=CARTESIAN_POINT('Ctrl Pts',(1.15256483308987,2.49336731654839,7.50405484070984));
#382384=CARTESIAN_POINT('Ctrl Pts',(1.15302327448635,2.49312963482938,7.50385766036131));
#382385=CARTESIAN_POINT('Ctrl Pts',(1.15307229766792,2.49310421846394,7.50383657498791));
#382386=CARTESIAN_POINT('Ctrl Pts',(1.15312146095905,2.49307841215981,7.50381643264937));
#382387=CARTESIAN_POINT('Ctrl Pts',(1.1531707167064,2.49305224935015,7.50379723213559));
#382388=CARTESIAN_POINT('Ctrl Pts',(1.15349951493258,2.49287760403722,7.50366906242519));
#382389=CARTESIAN_POINT('Ctrl Pts',(1.15383924782789,2.49268263887218,7.50358235568538));
#382390=CARTESIAN_POINT('Ctrl Pts',(1.15416219125876,2.49248684496703,7.5035341175365));
#382391=CARTESIAN_POINT('Ctrl Pts',(1.1546464083832,2.49219327416583,7.50346178989176));
#382392=CARTESIAN_POINT('Ctrl Pts',(1.15515483352957,2.49185687043633,7.50346967198527));
#382393=CARTESIAN_POINT('Ctrl Pts',(1.15564378787672,2.49151126838678,7.50354272648693));
#382394=CARTESIAN_POINT('Ctrl Pts',(1.15584490492046,2.49136911511026,7.50357277531559));
#382395=CARTESIAN_POINT('Ctrl Pts',(1.15604254242821,2.49122571028614,7.50361331098761));
#382396=CARTESIAN_POINT('Ctrl Pts',(1.15623297039333,2.49108456571042,7.50366116523659));
#382397=CARTESIAN_POINT('',(1.16019063351064,2.4091606745873,7.57603338622103));
#382398=CARTESIAN_POINT('Origin',(1.16402740803766,2.4171212430868,7.58486873427629));
#382399=CARTESIAN_POINT('Ctrl Pts',(1.15623297038463,2.4910845657659,7.50366116529968));
#382400=CARTESIAN_POINT('Ctrl Pts',(1.15755087359533,2.46382120335538,7.52783573079709));
#382401=CARTESIAN_POINT('Ctrl Pts',(1.15887005024772,2.4365145298623,7.55196141284069));
#382402=CARTESIAN_POINT('Ctrl Pts',(1.16019063309946,2.40916067576991,7.57603338728831));
#382403=CARTESIAN_POINT('Ctrl Pts',(1.15205371787328,2.40618167532515,7.59394543036555));
#382404=CARTESIAN_POINT('Ctrl Pts',(1.152680314397,2.39356533625318,7.59394543036555));
#382405=CARTESIAN_POINT('Ctrl Pts',(1.16293484201938,2.40094160211229,7.59394543036555));
#382406=CARTESIAN_POINT('Ctrl Pts',(1.15216945057637,2.40385143095157,7.58587155981959));
#382407=CARTESIAN_POINT('Ctrl Pts',(1.15521804482293,2.39883498778136,7.58685956158229));
#382408=CARTESIAN_POINT('Ctrl Pts',(1.16104082544615,2.39957920198036,7.58587155981959));
#382409=CARTESIAN_POINT('Ctrl Pts',(1.15683108903169,2.40656504321341,7.57982961904597));
#382410=CARTESIAN_POINT('Ctrl Pts',(1.15782736055642,2.40425328773227,7.58148017275035));
#382411=CARTESIAN_POINT('Ctrl Pts',(1.16025592890684,2.40491572725606,7.57982961904597));
#382412=CARTESIAN_POINT('Ctrl Pts',(1.16019063315139,2.40916067384177,7.57603338509286));
#382413=CARTESIAN_POINT('Ctrl Pts',(1.16019063315139,2.40916067384177,7.57603338509286));
#382414=CARTESIAN_POINT('Ctrl Pts',(1.16019063315139,2.40916067384177,7.57603338509286));
#382415=CARTESIAN_POINT('Origin',(1.16402226679187,2.4171237189801,7.5848687342762));
#382416=CARTESIAN_POINT('Ctrl Pts',(1.23934238165741,2.4559029174225,7.51098857897448));
#382417=CARTESIAN_POINT('Ctrl Pts',(1.23456307579883,2.45246507689653,7.50433767179957));
#382418=CARTESIAN_POINT('Ctrl Pts',(1.22809280357158,2.45814342422545,7.50214974420965));
#382419=CARTESIAN_POINT('Ctrl Pts',(1.21376973228735,2.4375080515231,7.53887321589168));
#382420=CARTESIAN_POINT('Ctrl Pts',(1.20904769099469,2.4341114024277,7.53220407452062));
#382421=CARTESIAN_POINT('Ctrl Pts',(1.20256218979777,2.43972755717507,7.53003438070911));
#382422=CARTESIAN_POINT('Ctrl Pts',(1.18814797399715,2.41907786069558,7.56669465659231));
#382423=CARTESIAN_POINT('Ctrl Pts',(1.18345383909063,2.41570128516482,7.56004085833298));
#382424=CARTESIAN_POINT('Ctrl Pts',(1.17698398972326,2.42127602276314,7.55785582193789));
#382425=CARTESIAN_POINT('Ctrl Pts',(1.16247826555638,2.40061317846372,7.59443891967696));
#382426=CARTESIAN_POINT('Ctrl Pts',(1.15777732473868,2.39723170731886,7.58783901202978));
#382427=CARTESIAN_POINT('Ctrl Pts',(1.15135951492374,2.40278966514234,7.58560008491213));
#382428=CARTESIAN_POINT('',(1.22670887334883,2.45714515960793,7.50366116523517));
#382429=CARTESIAN_POINT('Ctrl Pts',(1.226708873349,2.45714515960827,7.50366116523554));
#382430=CARTESIAN_POINT('Ctrl Pts',(1.22744112877594,2.45695037894577,7.50350835821027));
#382431=CARTESIAN_POINT('Ctrl Pts',(1.22810791225205,2.45674750507576,7.50345484956));
#382432=CARTESIAN_POINT('Ctrl Pts',(1.22872922258754,2.45653108089181,7.50349758195598));
#382433=CARTESIAN_POINT('Ctrl Pts',(1.22904800086722,2.45642003923501,7.50351950684424));
#382434=CARTESIAN_POINT('Ctrl Pts',(1.22938627121605,2.45629460805291,7.50357029184312));
#382435=CARTESIAN_POINT('Ctrl Pts',(1.22970913669999,2.45616468988572,7.50365515313923));
#382436=CARTESIAN_POINT('Ctrl Pts',(1.23020583455544,2.45596482313552,7.50378570417639));
#382437=CARTESIAN_POINT('Ctrl Pts',(1.23068078352653,2.45574879222656,7.50400001621911));
#382438=CARTESIAN_POINT('Ctrl Pts',(1.23109689307202,2.45553097357612,7.50428903009635));
#382439=CARTESIAN_POINT('Ctrl Pts',(1.23114307803021,2.45550679738172,7.50432110841318));
#382440=CARTESIAN_POINT('Ctrl Pts',(1.23118856822057,2.45548260283481,7.50435406373354));
#382441=CARTESIAN_POINT('Ctrl Pts',(1.23123333517554,2.45545841200072,7.50438785222351));
#382442=CARTESIAN_POINT('Ctrl Pts',(1.23150665895337,2.45531071533094,7.50459414719561));
#382443=CARTESIAN_POINT('Ctrl Pts',(1.23175712916612,2.45516035184147,7.50483629897752));
#382444=CARTESIAN_POINT('Ctrl Pts',(1.23197582773581,2.45501421023926,7.5050991045531));
#382445=CARTESIAN_POINT('Ctrl Pts',(1.23245829874673,2.45469180718626,7.50567888004914));
#382446=CARTESIAN_POINT('Ctrl Pts',(1.23280544219416,2.45437767961221,7.50637912803144));
#382447=CARTESIAN_POINT('Ctrl Pts',(1.23304326177522,2.45408853757673,7.50710440483569));
#382448=CARTESIAN_POINT('Ctrl Pts',(1.23310157985788,2.45401763420936,7.50728225710685));
#382449=CARTESIAN_POINT('Ctrl Pts',(1.23315459764782,2.45394691453315,7.50746498566954));
#382450=CARTESIAN_POINT('Ctrl Pts',(1.23320141086249,2.45387827926385,7.50764697238949));
#382451=CARTESIAN_POINT('Ctrl Pts',(1.23345306582122,2.45350931494506,7.50862528291182));
#382452=CARTESIAN_POINT('Ctrl Pts',(1.23355168239986,2.45316942519731,7.50965856837422));
#382453=CARTESIAN_POINT('Ctrl Pts',(1.23356355484101,2.45285929503312,7.51067959873204));
#382454=CARTESIAN_POINT('Ctrl Pts',(1.23357008826035,2.4526886300126,7.51124147302579));
#382455=CARTESIAN_POINT('Ctrl Pts',(1.23354992032895,2.45252691886293,7.51180065547253));
#382456=CARTESIAN_POINT('Ctrl Pts',(1.23351138288626,2.45237427097691,7.51235175716501));
#382457=CARTESIAN_POINT('Ctrl Pts',(1.23337822067027,2.451846811723,7.51425603304535));
#382458=CARTESIAN_POINT('Ctrl Pts',(1.23300397343624,2.45136616066923,7.51626900505179));
#382459=CARTESIAN_POINT('Ctrl Pts',(1.23244762843879,2.45094509166343,7.51827788969242));
#382460=CARTESIAN_POINT('Ctrl Pts',(1.23241751799618,2.45092230261312,7.51838661432544));
#382461=CARTESIAN_POINT('Ctrl Pts',(1.23238686422242,2.45089968883143,7.51849533314856));
#382462=CARTESIAN_POINT('Ctrl Pts',(1.23235567333044,2.45087725266274,7.51860402984325));
#382463=CARTESIAN_POINT('Ctrl Pts',(1.16019063469235,2.40916067500414,7.57603338728985));
#382464=CARTESIAN_POINT('Ctrl Pts',(1.18240010893414,2.42518305082722,7.55196141284922));
#382465=CARTESIAN_POINT('Ctrl Pts',(1.2045718191603,2.4411771094484,7.52783573083105));
#382466=CARTESIAN_POINT('Ctrl Pts',(1.22670887339981,2.457145159638,7.50366116530176));
#382467=CARTESIAN_POINT('Origin',(4.00899494394862E-16,8.32476377985989E-16,
7.49482233047033));
#382468=CARTESIAN_POINT('Origin',(1.15251174268201,2.48306724294371,7.49482233047033));
#382469=CARTESIAN_POINT('Origin',(0.,0.,7.50366116523517));
#382470=CARTESIAN_POINT('Origin',(1.22276082553375,2.44923706764781,7.49482233047033));
#382471=CARTESIAN_POINT('Ctrl Pts',(1.14781185363495,2.49159037923024,7.51860402984325));
#382472=CARTESIAN_POINT('Ctrl Pts',(1.14743505922582,2.49919000501072,7.51860402984325));
#382473=CARTESIAN_POINT('Ctrl Pts',(1.14051133179099,2.50234567996837,7.51860402984325));
#382474=CARTESIAN_POINT('Ctrl Pts',(1.14767194603029,2.49441217208217,7.51041458714365));
#382475=CARTESIAN_POINT('Ctrl Pts',(1.14579474478773,2.49993761154478,7.51004642900441));
#382476=CARTESIAN_POINT('Ctrl Pts',(1.14050942230917,2.50234655026605,7.50729136483008));
#382477=CARTESIAN_POINT('Ctrl Pts',(1.15026273737233,2.49551287068814,7.50215815450139));
#382478=CARTESIAN_POINT('Ctrl Pts',(1.14913464688836,2.49841553779643,7.49877163671531));
#382479=CARTESIAN_POINT('Ctrl Pts',(1.14600512155788,2.49986811991122,7.49481588533172));
#382480=CARTESIAN_POINT('Ctrl Pts',(1.1562327386202,2.49108406635797,7.50366171572174));
#382481=CARTESIAN_POINT('Ctrl Pts',(1.15777435337954,2.49440544953233,7.50000045605858));
#382482=CARTESIAN_POINT('Ctrl Pts',(1.15777435337943,2.49440544953238,7.49482233047317));
#382483=CARTESIAN_POINT('Origin',(1.13532718937376,2.49097138142306,7.51860402984325));
#382484=CARTESIAN_POINT('Origin',(1.13532718937376,2.49097138142306,9.));
#382485=CARTESIAN_POINT('Origin',(1.13532718937376,2.49097138142306,8.75721825406948));
#382486=CARTESIAN_POINT('Ctrl Pts',(1.14864017147865,2.47491183182611,8.78942910404913));
#382487=CARTESIAN_POINT('Ctrl Pts',(1.14838393822146,2.48047840826227,8.79672699501689));
#382488=CARTESIAN_POINT('Ctrl Pts',(1.13954364374199,2.48171237726442,8.79893251111266));
#382489=CARTESIAN_POINT('Ctrl Pts',(1.14809480925299,2.48589263319866,8.78111911759583));
#382490=CARTESIAN_POINT('Ctrl Pts',(1.14778360579385,2.49249153178346,8.78644465894816));
#382491=CARTESIAN_POINT('Ctrl Pts',(1.14018209782487,2.49530801689312,8.78817647674132));
#382492=CARTESIAN_POINT('Ctrl Pts',(1.14775492647406,2.49273613052929,8.76780923932029));
#382493=CARTESIAN_POINT('Ctrl Pts',(1.14738247379799,2.50052561162719,8.76988516158371));
#382494=CARTESIAN_POINT('Ctrl Pts',(1.14056970501266,2.50380014394097,8.77093053738833));
#382495=CARTESIAN_POINT('Ctrl Pts',(1.1478211989626,2.49140174220957,8.75371302330492));
#382496=CARTESIAN_POINT('Ctrl Pts',(1.1474586488806,2.49900008142322,8.75300828287559));
#382497=CARTESIAN_POINT('Ctrl Pts',(1.1404936487924,2.50214385512782,8.75267964240738));
#382498=CARTESIAN_POINT('Origin',(1.13602277023071,2.47696606283123,8.78727029226991));
#382499=CARTESIAN_POINT('Ctrl Pts',(1.15205371787328,2.40618167532515,8.85049129520029));
#382500=CARTESIAN_POINT('Ctrl Pts',(1.15176404759814,2.41201410220894,8.85711686593484));
#382501=CARTESIAN_POINT('Ctrl Pts',(1.14335314149692,2.41354949162872,8.85933012996512));
#382502=CARTESIAN_POINT('Ctrl Pts',(1.15086988603562,2.43001778564904,8.82945683644728));
#382503=CARTESIAN_POINT('Ctrl Pts',(1.15057781132205,2.43589862520232,8.83607469902393));
#382504=CARTESIAN_POINT('Ctrl Pts',(1.1421354763426,2.43740162972408,8.8382956714852));
#382505=CARTESIAN_POINT('Ctrl Pts',(1.14968781879479,2.45381836632828,8.80838214965002));
#382506=CARTESIAN_POINT('Ctrl Pts',(1.14939459141804,2.45972241442014,8.81501364461988));
#382507=CARTESIAN_POINT('Ctrl Pts',(1.14092032599117,2.46121761944619,8.81722098428721));
#382508=CARTESIAN_POINT('Ctrl Pts',(1.14850738206909,2.4775861170588,8.78727029226991));
#382509=CARTESIAN_POINT('Ctrl Pts',(1.14821410598631,2.48349114583245,8.79393457792714));
#382510=CARTESIAN_POINT('Ctrl Pts',(1.1397075136464,2.48500021903836,8.79610912703474));
#382511=CARTESIAN_POINT('Origin',(1.1395691060349,2.40556162109758,8.85049129520029));
#382512=CARTESIAN_POINT('Ctrl Pts',(1.16293484201938,2.40094160211229,8.85049129520029));
#382513=CARTESIAN_POINT('Ctrl Pts',(1.16767542343877,2.40435158745379,8.85711686593484));
#382514=CARTESIAN_POINT('Ctrl Pts',(1.17411995340351,2.39873297591288,8.85933012996512));
#382515=CARTESIAN_POINT('Ctrl Pts',(1.15874091806866,2.39792483730434,8.86332496987231));
#382516=CARTESIAN_POINT('Ctrl Pts',(1.16301882523354,2.39617801027645,8.86648636486737));
#382517=CARTESIAN_POINT('Ctrl Pts',(1.16237727570635,2.39030736158172,8.87206031107457));
#382518=CARTESIAN_POINT('Ctrl Pts',(1.15231172640007,2.40098674855133,8.86341338519877));
#382519=CARTESIAN_POINT('Ctrl Pts',(1.14825293640748,2.40322274820032,8.86654584966058));
#382520=CARTESIAN_POINT('Ctrl Pts',(1.14409029377498,2.39900415138368,8.87215952290714));
#382521=CARTESIAN_POINT('Ctrl Pts',(1.15205371787328,2.40618167532515,8.85049129520029));
#382522=CARTESIAN_POINT('Ctrl Pts',(1.15176404759814,2.41201410220894,8.85711686593484));
#382523=CARTESIAN_POINT('Ctrl Pts',(1.14335314149692,2.41354949162872,8.85933012996512));
#382524=CARTESIAN_POINT('Origin',(1.17023409226482,2.39079414204317,8.85049129520029));
#382525=CARTESIAN_POINT('Ctrl Pts',(1.22097218676268,2.44268890636152,8.78727029226991));
#382526=CARTESIAN_POINT('Ctrl Pts',(1.22577177880954,2.446141339107,8.79393457792714));
#382527=CARTESIAN_POINT('Ctrl Pts',(1.23225539332378,2.44043150916129,8.79610912703474));
#382528=CARTESIAN_POINT('Ctrl Pts',(1.20165382071389,2.42879285876314,8.80838214965003));
#382529=CARTESIAN_POINT('Ctrl Pts',(1.20645261566514,2.43224471814344,8.8150136446199));
#382530=CARTESIAN_POINT('Ctrl Pts',(1.21290523209917,2.42655151572733,8.81722098428721));
#382531=CARTESIAN_POINT('Ctrl Pts',(1.18230877056804,2.41487761681457,8.82945683644722));
#382532=CARTESIAN_POINT('Ctrl Pts',(1.18708870167942,2.4183159070961,8.83607469902387));
#382533=CARTESIAN_POINT('Ctrl Pts',(1.1935275076964,2.41265253181514,8.83829567148519));
#382534=CARTESIAN_POINT('Ctrl Pts',(1.16293484201938,2.40094160211229,8.85049129520029));
#382535=CARTESIAN_POINT('Ctrl Pts',(1.16767542343877,2.40435158745379,8.85711686593484));
#382536=CARTESIAN_POINT('Ctrl Pts',(1.17411995340351,2.39873297591288,8.85933012996512));
#382537=CARTESIAN_POINT('Origin',(1.22827143700812,2.4325414462924,8.78727029226991));
#382538=CARTESIAN_POINT('Ctrl Pts',(1.23220537088866,2.45076911469363,8.75374538247848));
#382539=CARTESIAN_POINT('Ctrl Pts',(1.23836652023368,2.45521710492923,8.75304829418602));
#382540=CARTESIAN_POINT('Ctrl Pts',(1.24516238600017,2.45174048995302,8.75272238421917));
#382541=CARTESIAN_POINT('Ctrl Pts',(1.23327692917391,2.45153990633562,8.7676940844502));
#382542=CARTESIAN_POINT('Ctrl Pts',(1.23959352432148,2.45609926821131,8.76974318093968));
#382543=CARTESIAN_POINT('Ctrl Pts',(1.24639574176609,2.45282082420285,8.7707786988043));
#382544=CARTESIAN_POINT('Ctrl Pts',(1.22778473182154,2.4475892674818,8.78108014887991));
#382545=CARTESIAN_POINT('Ctrl Pts',(1.23313559499254,2.45145624312506,8.78639403366326));
#382546=CARTESIAN_POINT('Ctrl Pts',(1.24007705385559,2.44729232374766,8.78812224174741));
#382547=CARTESIAN_POINT('Ctrl Pts',(1.21878423279645,2.44111504248424,8.78944554828685));
#382548=CARTESIAN_POINT('Ctrl Pts',(1.2232904630983,2.44437852315427,8.79673892988685));
#382549=CARTESIAN_POINT('Ctrl Pts',(1.22976192881264,2.4382447082056,8.79894799272499));
#382550=CARTESIAN_POINT('Origin',(1.23965492357588,2.44072979259362,8.75721825406948));
#382551=CARTESIAN_POINT('Origin',(1.23965492357588,2.44072979259362,9.));
#382552=CARTESIAN_POINT('Origin',(1.23965492357588,2.44072979259362,7.51860402984325));
#382553=CARTESIAN_POINT('Ctrl Pts',(1.2267085219693,2.45714445578105,7.50366195182966));
#382554=CARTESIAN_POINT('Ctrl Pts',(1.22834420829887,2.46042079855025,7.50000065167735));
#382555=CARTESIAN_POINT('Ctrl Pts',(1.22834420829897,2.4604207985502,7.49482233047108));
#382556=CARTESIAN_POINT('Ctrl Pts',(1.23389951291486,2.45523567375382,7.50215800491337));
#382557=CARTESIAN_POINT('Ctrl Pts',(1.23687368195879,2.45616250473763,7.49877273257264));
#382558=CARTESIAN_POINT('Ctrl Pts',(1.23996230211268,2.45462056378712,7.49481816995647));
#382559=CARTESIAN_POINT('Ctrl Pts',(1.23464359386721,2.45252341272686,7.51043025814041));
#382560=CARTESIAN_POINT('Ctrl Pts',(1.24013580471419,2.45450542609693,7.51006209594514));
#382561=CARTESIAN_POINT('Ctrl Pts',(1.2453177057293,2.45187353095618,7.50731281821699));
#382562=CARTESIAN_POINT('Ctrl Pts',(1.23235444642807,2.45087637001727,7.51860402984325));
#382563=CARTESIAN_POINT('Ctrl Pts',(1.23853109166801,2.45532047521073,7.51860402984325));
#382564=CARTESIAN_POINT('Ctrl Pts',(1.24531544834107,2.4518746774913,7.51860402984325));
#382565=CARTESIAN_POINT('Origin',(0.,0.,7.5));
#382566=CARTESIAN_POINT('Origin',(1.31437432427026,2.32149911893916,7.5));
#382567=CARTESIAN_POINT('',(1.31437432427026,2.32149911893916,7.59394543036555));
#382568=CARTESIAN_POINT('',(1.31437432427026,2.32149911893916,8.85049129520029));
#382569=CARTESIAN_POINT('',(1.31437432427026,2.32149911893916,7.5));
#382570=CARTESIAN_POINT('',(1.37496718403115,2.35944218342962,8.78727029226991));
#382571=CARTESIAN_POINT('Ctrl Pts',(1.31437432427026,2.32149911893916,8.85049129520029));
#382572=CARTESIAN_POINT('Ctrl Pts',(1.33460130338714,2.33416519174225,8.82945686509571));
#382573=CARTESIAN_POINT('Ctrl Pts',(1.35479821265376,2.34681243489657,8.80838212259895));
#382574=CARTESIAN_POINT('Ctrl Pts',(1.37496718403115,2.35944218342962,8.78727029226991));
#382575=CARTESIAN_POINT('',(1.38685191115367,2.36688436340662,8.75721825406948));
#382576=CARTESIAN_POINT('Origin',(1.35108653730003,2.34448843318217,8.75937679713155));
#382577=CARTESIAN_POINT('',(1.38685191115367,2.36688436340662,7.51860402984325));
#382578=CARTESIAN_POINT('',(1.38685191115367,2.36688436340662,7.5));
#382579=CARTESIAN_POINT('Ctrl Pts',(1.38685191115367,2.36688436340662,7.51860402984325));
#382580=CARTESIAN_POINT('Ctrl Pts',(1.37751830642363,2.36103968851261,7.52834476460825));
#382581=CARTESIAN_POINT('Ctrl Pts',(1.36817864245207,2.35519121934001,7.53807742314407));
#382582=CARTESIAN_POINT('Ctrl Pts',(1.35883271579191,2.34933882849084,7.54780169004674));
#382583=CARTESIAN_POINT('Ctrl Pts',(1.34402927306645,2.3400689576805,7.5632044032688));
#382584=CARTESIAN_POINT('Ctrl Pts',(1.32921009923994,2.3307892361025,7.57858609112103));
#382585=CARTESIAN_POINT('Ctrl Pts',(1.31437432427026,2.32149911893916,7.59394543036555));
#382586=CARTESIAN_POINT('Origin',(1.30783574368268,2.60239671513041,7.5));
#382587=CARTESIAN_POINT('',(1.30509031014831,2.41293163922361,8.75721825406948));
#382588=CARTESIAN_POINT('',(1.30488713801671,2.39891053004238,8.78727029226991));
#382589=CARTESIAN_POINT('Origin',(1.30437141136732,2.36331972532997,8.75658640621135));
#382590=CARTESIAN_POINT('',(1.30385128920418,2.32742558187728,8.85049129520029));
#382591=CARTESIAN_POINT('Ctrl Pts',(1.30488713801671,2.39891053004238,8.78727029226991));
#382592=CARTESIAN_POINT('Ctrl Pts',(1.3045423448326,2.37511601235258,8.80838212259895));
#382593=CARTESIAN_POINT('Ctrl Pts',(1.30419707404388,2.35128853469735,8.82945686509571));
#382594=CARTESIAN_POINT('Ctrl Pts',(1.30385128920418,2.32742558187728,8.85049129520029));
#382595=CARTESIAN_POINT('',(1.30385128920418,2.32742558187728,7.59394543036555));
#382596=CARTESIAN_POINT('',(1.30385128920418,2.32742558187728,7.5));
#382597=CARTESIAN_POINT('',(1.30509031014831,2.41293163922361,7.51860402984325));
#382598=CARTESIAN_POINT('Ctrl Pts',(1.30385128920418,2.32742558187728,7.59394543036555));
#382599=CARTESIAN_POINT('Ctrl Pts',(1.30410491017447,2.34492821517239,7.57858609112103));
#382600=CARTESIAN_POINT('Ctrl Pts',(1.30435824734443,2.36241126312566,7.56320440326857));
#382601=CARTESIAN_POINT('Ctrl Pts',(1.3046113155876,2.37987575217718,7.54780169004651));
#382602=CARTESIAN_POINT('Ctrl Pts',(1.30477108634394,2.39090168964725,7.53807742314383));
#382603=CARTESIAN_POINT('Ctrl Pts',(1.30493075003819,2.40192023865671,7.52834476460825));
#382604=CARTESIAN_POINT('Ctrl Pts',(1.30509031014831,2.41293163922361,7.51860402984325));
#382605=CARTESIAN_POINT('',(1.30509031014831,2.41293163922361,7.5));
#382606=CARTESIAN_POINT('Origin',(1.3107255675355,2.32732597051532,7.5));
#382607=CARTESIAN_POINT('Ctrl Pts',(1.30385128920418,2.32742558187728,8.85049129520029));
#382608=CARTESIAN_POINT('Ctrl Pts',(1.30384848325707,2.32723194070001,8.85097269580138));
#382609=CARTESIAN_POINT('Ctrl Pts',(1.30385412324171,2.32704062079224,8.85143669361005));
#382610=CARTESIAN_POINT('Ctrl Pts',(1.30386934276709,2.32684283825272,8.8519052845931));
#382611=CARTESIAN_POINT('Ctrl Pts',(1.30389911119355,2.32645598814833,8.85282181883899));
#382612=CARTESIAN_POINT('Ctrl Pts',(1.30396495843793,2.32605438066444,8.85372622499636));
#382613=CARTESIAN_POINT('Ctrl Pts',(1.30408313333414,2.32563420862442,8.85462257735071));
#382614=CARTESIAN_POINT('Ctrl Pts',(1.30418123793579,2.32528539671989,8.85536669723987));
#382615=CARTESIAN_POINT('Ctrl Pts',(1.30431539729113,2.32492370253027,8.85610498449051));
#382616=CARTESIAN_POINT('Ctrl Pts',(1.30450242234569,2.32454970015688,8.85681338218371));
#382617=CARTESIAN_POINT('Ctrl Pts',(1.30467214787644,2.32421029241565,8.85745625420284));
#382618=CARTESIAN_POINT('Ctrl Pts',(1.30488700517416,2.32385622295629,8.85808743050665));
#382619=CARTESIAN_POINT('Ctrl Pts',(1.30517545207641,2.32349031978707,8.85866804508409));
#382620=CARTESIAN_POINT('Ctrl Pts',(1.30530853522435,2.3233214999966,8.85893592806395));
#382621=CARTESIAN_POINT('Ctrl Pts',(1.30545751998389,2.32315021373905,8.85919241173848));
#382622=CARTESIAN_POINT('Ctrl Pts',(1.30562669581158,2.32297729919045,8.85943017985534));
#382623=CARTESIAN_POINT('Ctrl Pts',(1.30585513326037,2.32274381336167,8.8597512372));
#382624=CARTESIAN_POINT('Ctrl Pts',(1.30612665726056,2.32250186380978,8.86004599534705));
#382625=CARTESIAN_POINT('Ctrl Pts',(1.30644493447619,2.32226213334004,8.86026130871721));
#382626=CARTESIAN_POINT('Ctrl Pts',(1.30656146473801,2.32217436125635,8.86034014101235));
#382627=CARTESIAN_POINT('Ctrl Pts',(1.30668600525793,2.3220855583631,8.86040910639693));
#382628=CARTESIAN_POINT('Ctrl Pts',(1.3068153582903,2.32199841792863,8.86046313645507));
#382629=CARTESIAN_POINT('Ctrl Pts',(1.307017212614,2.32186243601043,8.8605474499083));
#382630=CARTESIAN_POINT('Ctrl Pts',(1.30723637821948,2.32172691245507,8.86059655985668));
#382631=CARTESIAN_POINT('Ctrl Pts',(1.30745864527337,2.32160028963279,8.86059725258816));
#382632=CARTESIAN_POINT('Ctrl Pts',(1.30768142585295,2.3214733742612,8.86059794692011));
#382633=CARTESIAN_POINT('Ctrl Pts',(1.30791110798644,2.321356301745,8.86056369958366));
#382634=CARTESIAN_POINT('Ctrl Pts',(1.30813345578225,2.32125210458826,8.86048590497774));
#382635=CARTESIAN_POINT('Ctrl Pts',(1.30819148193687,2.32122491223268,8.86046560290182));
#382636=CARTESIAN_POINT('Ctrl Pts',(1.30824980190641,2.32119832502185,8.86044257503091));
#382637=CARTESIAN_POINT('Ctrl Pts',(1.30830659993882,2.32117313465386,8.86041778462584));
#382638=CARTESIAN_POINT('Ctrl Pts',(1.30868878021642,2.3210036347359,8.86025097596201));
#382639=CARTESIAN_POINT('Ctrl Pts',(1.30905347104564,2.320874937295,8.8599848982295));
#382640=CARTESIAN_POINT('Ctrl Pts',(1.30938720857524,2.32078280907962,8.85968173251461));
#382641=CARTESIAN_POINT('Ctrl Pts',(1.30956373660751,2.32073407853199,8.85952137522076));
#382642=CARTESIAN_POINT('Ctrl Pts',(1.30973495640559,2.3206944559447,8.85934740853961));
#382643=CARTESIAN_POINT('Ctrl Pts',(1.3098981029095,2.32066298555584,8.8591675900182));
#382644=CARTESIAN_POINT('Ctrl Pts',(1.31055322092454,2.32053661558659,8.85844552518695));
#382645=CARTESIAN_POINT('Ctrl Pts',(1.31111461455945,2.320531581649,8.85759444184123));
#382646=CARTESIAN_POINT('Ctrl Pts',(1.31157271342272,2.32056859093144,8.85683498915138));
#382647=CARTESIAN_POINT('Ctrl Pts',(1.31162065224874,2.32057246385428,8.85675551444997));
#382648=CARTESIAN_POINT('Ctrl Pts',(1.31166745441336,2.32057681639897,8.85667699793651));
#382649=CARTESIAN_POINT('Ctrl Pts',(1.31171310470176,2.3205815701244,8.85659965593547));
#382650=CARTESIAN_POINT('Ctrl Pts',(1.31232929462408,2.32064573615287,8.85555568965886));
#382651=CARTESIAN_POINT('Ctrl Pts',(1.3129122244714,2.32079639369908,8.85434650606346));
#382652=CARTESIAN_POINT('Ctrl Pts',(1.31346633101422,2.32102827049931,8.85297329937117));
#382653=CARTESIAN_POINT('Ctrl Pts',(1.31377798218235,2.32115868707097,8.85220095427747));
#382654=CARTESIAN_POINT('Ctrl Pts',(1.31408052113673,2.32131514031054,8.85137579139183));
#382655=CARTESIAN_POINT('Ctrl Pts',(1.31437432427026,2.32149911893916,8.85049129520029));
#382656=CARTESIAN_POINT('Origin',(1.3107255675355,2.32732597051532,7.59394543036555));
#382657=CARTESIAN_POINT('Ctrl Pts',(1.30384314259315,2.32686337621543,7.59443877723642));
#382658=CARTESIAN_POINT('Ctrl Pts',(1.30375924033799,2.32107319883816,7.58783886950015));
#382659=CARTESIAN_POINT('Ctrl Pts',(1.31198945928026,2.31898928960332,7.58559994247159));
#382660=CARTESIAN_POINT('Ctrl Pts',(1.30430116254244,2.35847178464138,7.56670252222136));
#382661=CARTESIAN_POINT('Ctrl Pts',(1.30421738154988,2.35268997571431,7.56004874999032));
#382662=CARTESIAN_POINT('Ctrl Pts',(1.31249112309633,2.35057300663594,7.55786368756704));
#382663=CARTESIAN_POINT('Ctrl Pts',(1.30475832718525,2.39002116752267,7.53888913333559));
#382664=CARTESIAN_POINT('Ctrl Pts',(1.30467404827812,2.38420499702201,7.53222002137277));
#382665=CARTESIAN_POINT('Ctrl Pts',(1.31299070164157,2.38209888174684,7.53005029815327));
#382666=CARTESIAN_POINT('Ctrl Pts',(1.30521461583455,2.42151009722833,7.51101258149734));
#382667=CARTESIAN_POINT('Ctrl Pts',(1.30512931531394,2.41562342417298,7.5043616886572));
#382668=CARTESIAN_POINT('Ctrl Pts',(1.31348825286493,2.41356535601004,7.50217374673251));
#382669=CARTESIAN_POINT('',(1.31346170186501,2.41188626453889,7.50366116523517));
#382670=CARTESIAN_POINT('Ctrl Pts',(1.30509031014831,2.41293163922361,7.51860402984325));
#382671=CARTESIAN_POINT('Ctrl Pts',(1.30509670862026,2.41337320408333,7.51734760759493));
#382672=CARTESIAN_POINT('Ctrl Pts',(1.30516198111639,2.41377135902958,7.51608817408572));
#382673=CARTESIAN_POINT('Ctrl Pts',(1.30529915524687,2.41412302796592,7.51481005913119));
#382674=CARTESIAN_POINT('Ctrl Pts',(1.30542341085214,2.41444157809186,7.51365231206383));
#382675=CARTESIAN_POINT('Ctrl Pts',(1.30560660504881,2.41472252559346,7.51247773061043));
#382676=CARTESIAN_POINT('Ctrl Pts',(1.30587649835674,2.41494084061839,7.51129758471022));
#382677=CARTESIAN_POINT('Ctrl Pts',(1.30621194491551,2.41521218126186,7.50983079813402));
#382678=CARTESIAN_POINT('Ctrl Pts',(1.30667880678715,2.41536798326241,7.50839324291155));
#382679=CARTESIAN_POINT('Ctrl Pts',(1.30730658833189,2.41533118376778,7.50715379678855));
#382680=CARTESIAN_POINT('Ctrl Pts',(1.30759660531648,2.41531418346162,7.50658120839351));
#382681=CARTESIAN_POINT('Ctrl Pts',(1.30796163787564,2.41524417646109,7.50598221009429));
#382682=CARTESIAN_POINT('Ctrl Pts',(1.30838871444073,2.41510048946134,7.50545747549611));
#382683=CARTESIAN_POINT('Ctrl Pts',(1.30861661571512,2.41502381363075,7.50517746087247));
#382684=CARTESIAN_POINT('Ctrl Pts',(1.3088647206011,2.41492551702526,7.50491486231392));
#382685=CARTESIAN_POINT('Ctrl Pts',(1.30912584447469,2.41480665196125,7.50468370960993));
#382686=CARTESIAN_POINT('Ctrl Pts',(1.30951630703256,2.4146289111967,7.50433806340447));
#382687=CARTESIAN_POINT('Ctrl Pts',(1.30994735749208,2.41439934358563,7.50405484070984));
#382688=CARTESIAN_POINT('Ctrl Pts',(1.31038962865153,2.41413277776808,7.50385766036131));
#382689=CARTESIAN_POINT('Ctrl Pts',(1.31043692267758,2.41410427269727,7.50383657498791));
#382690=CARTESIAN_POINT('Ctrl Pts',(1.31048433154187,2.41407536951208,7.50381643264937));
#382691=CARTESIAN_POINT('Ctrl Pts',(1.31053180983103,2.41404610463015,7.50379723213559));
#382692=CARTESIAN_POINT('Ctrl Pts',(1.31084874294237,2.41385075197006,7.50366906242519));
#382693=CARTESIAN_POINT('Ctrl Pts',(1.311175286359,2.41363442062053,7.50358235568538));
#382694=CARTESIAN_POINT('Ctrl Pts',(1.31148502170938,2.4134183379383,7.5035341175365));
#382695=CARTESIAN_POINT('Ctrl Pts',(1.311949434812,2.41309434641212,7.50346178989176));
#382696=CARTESIAN_POINT('Ctrl Pts',(1.31243526188342,2.41272605894919,7.50346967198527));
#382697=CARTESIAN_POINT('Ctrl Pts',(1.31290106882208,2.41234983956353,7.50354272648692));
#382698=CARTESIAN_POINT('Ctrl Pts',(1.31309266485759,2.41219509274292,7.50357277531559));
#382699=CARTESIAN_POINT('Ctrl Pts',(1.31328070831926,2.4120393198808,7.50361331098761));
#382700=CARTESIAN_POINT('Ctrl Pts',(1.31346170186569,2.41188626454013,7.50366116523659));
#382701=CARTESIAN_POINT('',(1.31216235181373,2.3298771264911,7.57603338622103));
#382702=CARTESIAN_POINT('Origin',(1.31650127865085,2.3375755161608,7.58486873427629));
#382703=CARTESIAN_POINT('Ctrl Pts',(1.31346170186055,2.41188626459606,7.50366116529968));
#382704=CARTESIAN_POINT('Ctrl Pts',(1.31303012767071,2.38459447933897,7.52783573079709));
#382705=CARTESIAN_POINT('Ctrl Pts',(1.31259704935554,2.3572593903969,7.55196141284069));
#382706=CARTESIAN_POINT('Ctrl Pts',(1.31216235147917,2.32987712769763,7.57603338728831));
#382707=CARTESIAN_POINT('Ctrl Pts',(1.3040419876395,2.32845133507715,7.59639677331371));
#382708=CARTESIAN_POINT('Ctrl Pts',(1.30089133461177,2.31044729938369,7.59959882295468));
#382709=CARTESIAN_POINT('Ctrl Pts',(1.31501451773084,2.32207676674859,7.59642833564546));
#382710=CARTESIAN_POINT('Ctrl Pts',(1.30276074036375,2.32476711066729,7.58707626057421));
#382711=CARTESIAN_POINT('Ctrl Pts',(1.30574812934753,2.31868535121003,7.58809943920599));
#382712=CARTESIAN_POINT('Ctrl Pts',(1.31249166603443,2.31917434379263,7.58710240504253));
#382713=CARTESIAN_POINT('Ctrl Pts',(1.30826409698653,2.32734367779126,7.58015376756929));
#382714=CARTESIAN_POINT('Ctrl Pts',(1.30917762705492,2.32464280122792,7.58205880659761));
#382715=CARTESIAN_POINT('Ctrl Pts',(1.31193485703792,2.32521267652891,7.58020924244127));
#382716=CARTESIAN_POINT('Ctrl Pts',(1.31216235140745,2.32987712577012,7.57603338509286));
#382717=CARTESIAN_POINT('Ctrl Pts',(1.31216235140745,2.32987712577012,7.57603338509286));
#382718=CARTESIAN_POINT('Ctrl Pts',(1.31216235140745,2.32987712577012,7.57603338509286));
#382719=CARTESIAN_POINT('Origin',(1.31649630659926,2.33757831636739,7.58486873427623));
#382720=CARTESIAN_POINT('Ctrl Pts',(1.39414625998577,2.37145206245969,7.51098857897448));
#382721=CARTESIAN_POINT('Ctrl Pts',(1.3891565105249,2.3683274965235,7.50433767179956));
#382722=CARTESIAN_POINT('Ctrl Pts',(1.38306334512837,2.37440872884376,7.50214974420965));
#382723=CARTESIAN_POINT('Ctrl Pts',(1.36744758926183,2.35473343605575,7.53887321589169));
#382724=CARTESIAN_POINT('Ctrl Pts',(1.36251762585468,2.3516463079646,7.53220407452062));
#382725=CARTESIAN_POINT('Ctrl Pts',(1.35640527808564,2.35766645120807,7.53003438070911));
#382726=CARTESIAN_POINT('Ctrl Pts',(1.34069764724135,2.33798270372187,7.56669465659232));
#382727=CARTESIAN_POINT('Ctrl Pts',(1.33579681900139,2.33491381998374,7.56004085833298));
#382728=CARTESIAN_POINT('Ctrl Pts',(1.32969743729769,2.34089162835799,7.55785582193789));
#382729=CARTESIAN_POINT('Ctrl Pts',(1.31389764371716,2.32120062302662,7.59443891967696));
#382730=CARTESIAN_POINT('Ctrl Pts',(1.30898970988643,2.31812728978919,7.58783901202978));
#382731=CARTESIAN_POINT('Ctrl Pts',(1.30294118573046,2.32408501867887,7.58560008491213));
#382732=CARTESIAN_POINT('',(1.38161829930505,2.37350118398178,7.50366116523517));
#382733=CARTESIAN_POINT('Ctrl Pts',(1.38161829930524,2.3735011839821,7.50366116523554));
#382734=CARTESIAN_POINT('Ctrl Pts',(1.38233657059497,2.37325988775107,7.50350835821027));
#382735=CARTESIAN_POINT('Ctrl Pts',(1.38298898591943,2.37301470974319,7.50345484956));
#382736=CARTESIAN_POINT('Ctrl Pts',(1.38359515336113,2.37275892273607,7.50349758195598));
#382737=CARTESIAN_POINT('Ctrl Pts',(1.38390616221327,2.37262768503176,7.50351950684424));
#382738=CARTESIAN_POINT('Ctrl Pts',(1.38423570114596,2.37248083850581,7.50357029184312));
#382739=CARTESIAN_POINT('Ctrl Pts',(1.38454957938259,2.37233050120685,7.50365515313923));
#382740=CARTESIAN_POINT('Ctrl Pts',(1.38503245121237,2.37209922156347,7.50378570417639));
#382741=CARTESIAN_POINT('Ctrl Pts',(1.385492583202,2.37185320442812,7.50400001621911));
#382742=CARTESIAN_POINT('Ctrl Pts',(1.38589388211694,2.37160917307934,7.50428903009634));
#382743=CARTESIAN_POINT('Ctrl Pts',(1.38593842320909,2.37158208747709,7.50432110841318));
#382744=CARTESIAN_POINT('Ctrl Pts',(1.38598226978504,2.37155502807398,7.50435406373354));
#382745=CARTESIAN_POINT('Ctrl Pts',(1.38602539484944,2.37152801871389,7.50438785222351));
#382746=CARTESIAN_POINT('Ctrl Pts',(1.38628869409613,2.37136311358819,7.50459414719561));
#382747=CARTESIAN_POINT('Ctrl Pts',(1.38652901586912,2.371197011355,7.50483629897752));
#382748=CARTESIAN_POINT('Ctrl Pts',(1.38673790177454,2.37103715795092,7.50509910455309));
#382749=CARTESIAN_POINT('Ctrl Pts',(1.38719872506249,2.37068450528576,7.50567888004914));
#382750=CARTESIAN_POINT('Ctrl Pts',(1.38752502904371,2.37034878156346,7.50637912803144));
#382751=CARTESIAN_POINT('Ctrl Pts',(1.38774383460512,2.37004499644843,7.50710440483569));
#382752=CARTESIAN_POINT('Ctrl Pts',(1.38779749007268,2.36997050230725,7.50728225710685));
#382753=CARTESIAN_POINT('Ctrl Pts',(1.38784586790667,2.36989653107073,7.50746498566954));
#382754=CARTESIAN_POINT('Ctrl Pts',(1.38788818746177,2.369825037487,7.50764697238949));
#382755=CARTESIAN_POINT('Ctrl Pts',(1.38811568574332,2.36944070765641,7.50862528291181));
#382756=CARTESIAN_POINT('Ctrl Pts',(1.38819232289272,2.36909519786271,7.50965856837421));
#382757=CARTESIAN_POINT('Ctrl Pts',(1.38818430083282,2.36878494422429,7.51067959873202));
#382758=CARTESIAN_POINT('Ctrl Pts',(1.38817988628315,2.36861421125574,7.51124147302578));
#382759=CARTESIAN_POINT('Ctrl Pts',(1.38814939891999,2.36845412452277,7.51180065547252));
#382760=CARTESIAN_POINT('Ctrl Pts',(1.38810116047297,2.36830425937063,7.512351757165));
#382761=CARTESIAN_POINT('Ctrl Pts',(1.3879344774226,2.3677864155708,7.51425603304535));
#382762=CARTESIAN_POINT('Ctrl Pts',(1.38753020370091,2.36733073016879,7.51626900505179));
#382763=CARTESIAN_POINT('Ctrl Pts',(1.3869480237901,2.36694617144079,7.51827788969241));
#382764=CARTESIAN_POINT('Ctrl Pts',(1.38691651511316,2.36692535839572,7.51838661432544));
#382765=CARTESIAN_POINT('Ctrl Pts',(1.38688447545089,2.36690475507049,7.51849533314856));
#382766=CARTESIAN_POINT('Ctrl Pts',(1.38685191115368,2.36688436340662,7.51860402984325));
#382767=CARTESIAN_POINT('Ctrl Pts',(1.31216235301971,2.32987712683138,7.57603338728984));
#382768=CARTESIAN_POINT('Ctrl Pts',(1.33535275265831,2.34444361706461,7.55196141284921));
#382769=CARTESIAN_POINT('Ctrl Pts',(1.35850365158215,2.35898426782545,7.52783573083105));
#382770=CARTESIAN_POINT('Ctrl Pts',(1.38161829935784,2.37350118400852,7.50366116530176));
#382771=CARTESIAN_POINT('Origin',(4.53412748053601E-16,8.0508024718857E-16,
7.49482233047033));
#382772=CARTESIAN_POINT('Origin',(1.30923444818248,2.40412383410096,7.49482233047033));
#382773=CARTESIAN_POINT('Origin',(0.,0.,7.50366116523517));
#382774=CARTESIAN_POINT('Origin',(1.37717168998611,2.36586229233673,7.49482233047033));
#382775=CARTESIAN_POINT('Ctrl Pts',(1.30509029477833,2.41293058161502,7.51860402984325));
#382776=CARTESIAN_POINT('Ctrl Pts',(1.30520118422925,2.42053873444996,7.51860402984325));
#382777=CARTESIAN_POINT('Ctrl Pts',(1.29849386712373,2.4241315304748,7.51860402984325));
#382778=CARTESIAN_POINT('Ctrl Pts',(1.30513146751761,2.41575554070189,7.51041458714366));
#382779=CARTESIAN_POINT('Ctrl Pts',(1.30361213930819,2.42138990025307,7.51004642900444));
#382780=CARTESIAN_POINT('Ctrl Pts',(1.29849201732532,2.42413252132528,7.50729136483011));
#382781=CARTESIAN_POINT('Ctrl Pts',(1.30778745780281,2.41668798523335,7.50215815450137));
#382782=CARTESIAN_POINT('Ctrl Pts',(1.30684765962187,2.41965696550621,7.49877163671527));
#382783=CARTESIAN_POINT('Ctrl Pts',(1.30381763149245,2.42130707251161,7.49481588533168));
#382784=CARTESIAN_POINT('Ctrl Pts',(1.31346143857514,2.41188578106341,7.50366171572174));
#382785=CARTESIAN_POINT('Ctrl Pts',(1.31521268767224,2.41510156850307,7.50000045605858));
#382786=CARTESIAN_POINT('Ctrl Pts',(1.31521268767213,2.41510156850313,7.49482233047317));
#382787=CARTESIAN_POINT('Origin',(1.29259162227317,2.41311275079082,7.51860402984325));
#382788=CARTESIAN_POINT('Origin',(1.29259162227317,2.41311275079082,9.));
#382789=CARTESIAN_POINT('Origin',(1.29259162227317,2.41311275079082,8.75721825406948));
#382790=CARTESIAN_POINT('Ctrl Pts',(1.30484831255304,2.39623323156884,8.78942910404913));
#382791=CARTESIAN_POINT('Ctrl Pts',(1.30494925753137,2.40180478779785,8.79672699501691));
#382792=CARTESIAN_POINT('Ctrl Pts',(1.29620618705044,2.40360262109034,8.79893251111266));
#382793=CARTESIAN_POINT('Ctrl Pts',(1.30500761319207,2.40722641318505,8.78111911759576));
#382794=CARTESIAN_POINT('Ctrl Pts',(1.30511984201778,2.41383169249909,8.78644465894811));
#382795=CARTESIAN_POINT('Ctrl Pts',(1.29771440498272,2.41712942112576,8.78817647674131));
#382796=CARTESIAN_POINT('Ctrl Pts',(1.30510689311817,2.41407762618082,8.76780923932035));
#382797=CARTESIAN_POINT('Ctrl Pts',(1.30523427945354,2.42187496607927,8.76988516158375));
#382798=CARTESIAN_POINT('Ctrl Pts',(1.29864530823804,2.42557926611001,8.77093053738834));
#382799=CARTESIAN_POINT('Ctrl Pts',(1.30508753488959,2.41274173341214,8.75371302330491));
#382800=CARTESIAN_POINT('Ctrl Pts',(1.30521255697053,2.42034768968648,8.75300828287559));
#382801=CARTESIAN_POINT('Ctrl Pts',(1.29846328949482,2.42393125325864,8.75267964240737));
#382802=CARTESIAN_POINT('Origin',(1.29238845014157,2.39909164160959,8.78727029226991));
#382803=CARTESIAN_POINT('Ctrl Pts',(1.30385128920418,2.32742558187728,8.85049129520029));
#382804=CARTESIAN_POINT('Ctrl Pts',(1.30393589896115,2.33326458465276,8.85711686593484));
#382805=CARTESIAN_POINT('Ctrl Pts',(1.29564064670646,2.33533570805445,8.85933012996512));
#382806=CARTESIAN_POINT('Ctrl Pts',(1.30419707450793,2.35128856672232,8.82945683644724));
#382807=CARTESIAN_POINT('Ctrl Pts',(1.30428238657705,2.35717603675118,8.8360746990239));
#382808=CARTESIAN_POINT('Ctrl Pts',(1.29595369511061,2.35921685544825,8.83829567148519));
#382809=CARTESIAN_POINT('Ctrl Pts',(1.30454234439081,2.37511598186413,8.80838214965001));
#382810=CARTESIAN_POINT('Ctrl Pts',(1.30462799314117,2.38102668659857,8.81501364461995));
#382811=CARTESIAN_POINT('Ctrl Pts',(1.29626693711641,2.38306176761556,8.81722098428721));
#382812=CARTESIAN_POINT('Ctrl Pts',(1.30488713801671,2.39891053004238,8.78727029226991));
#382813=CARTESIAN_POINT('Ctrl Pts',(1.30497280099362,2.40482221656425,8.79393457792714));
#382814=CARTESIAN_POINT('Ctrl Pts',(1.29658037301227,2.40687320845992,8.79610912703474));
#382815=CARTESIAN_POINT('Origin',(1.29135260132903,2.32760669344449,8.85049129520029));
#382816=CARTESIAN_POINT('Ctrl Pts',(1.31437432427026,2.32149911893916,8.85049129520029));
#382817=CARTESIAN_POINT('Ctrl Pts',(1.31932364416766,2.32459836800567,8.85711686593484));
#382818=CARTESIAN_POINT('Ctrl Pts',(1.325394947477,2.31857839805226,8.85933012996512));
#382819=CARTESIAN_POINT('Ctrl Pts',(1.30999573240122,2.31875725802815,8.86332496987232));
#382820=CARTESIAN_POINT('Ctrl Pts',(1.31415293055507,2.31673993359065,8.86648636486738));
#382821=CARTESIAN_POINT('Ctrl Pts',(1.31313656540689,2.31092245099262,8.87206031107457));
#382822=CARTESIAN_POINT('Ctrl Pts',(1.3037759275236,2.32222479797461,8.86341338519876));
#382823=CARTESIAN_POINT('Ctrl Pts',(1.29986873773974,2.32471625109016,8.86654584966054));
#382824=CARTESIAN_POINT('Ctrl Pts',(1.29544436127692,2.32077302326231,8.87215952290714));
#382825=CARTESIAN_POINT('Ctrl Pts',(1.30385128920418,2.32742558187728,8.85049129520029));
#382826=CARTESIAN_POINT('Ctrl Pts',(1.30393589896115,2.33326458465277,8.85711686593484));
#382827=CARTESIAN_POINT('Ctrl Pts',(1.29564064670646,2.33533570805445,8.85933012996512));
#382828=CARTESIAN_POINT('Origin',(1.32100842742436,2.31090484334614,8.85049129520029));
#382829=CARTESIAN_POINT('Ctrl Pts',(1.37496718403115,2.35944218342962,8.78727029226991));
#382830=CARTESIAN_POINT('Ctrl Pts',(1.37997811292687,2.3625800118635,8.79393457792714));
#382831=CARTESIAN_POINT('Ctrl Pts',(1.38608257609904,2.35646650676758,8.79610912703474));
#382832=CARTESIAN_POINT('Ctrl Pts',(1.3547981868108,2.34681241871379,8.80838214965002));
#382833=CARTESIAN_POINT('Ctrl Pts',(1.35980828351299,2.34994972603061,8.81501364461989));
#382834=CARTESIAN_POINT('Ctrl Pts',(1.36588287762333,2.34385480035508,8.81722098428721));
#382835=CARTESIAN_POINT('Ctrl Pts',(1.3346013305325,2.33416520874059,8.82945683644723));
#382836=CARTESIAN_POINT('Ctrl Pts',(1.33959173277748,2.33729018344821,8.8360746990239));
#382837=CARTESIAN_POINT('Ctrl Pts',(1.34565445587684,2.3312259084612,8.8382956714852));
#382838=CARTESIAN_POINT('Ctrl Pts',(1.31437432427026,2.32149911893916,8.85049129520029));
#382839=CARTESIAN_POINT('Ctrl Pts',(1.31932364416766,2.32459836800567,8.85711686593484));
#382840=CARTESIAN_POINT('Ctrl Pts',(1.325394947477,2.31857839805226,8.85933012996512));
#382841=CARTESIAN_POINT('Origin',(1.38160128718524,2.34884790783661,8.78727029226991));
#382842=CARTESIAN_POINT('Ctrl Pts',(1.38669498910091,2.36678607752908,8.75374538247848));
#382843=CARTESIAN_POINT('Ctrl Pts',(1.39312846341669,2.37083018269781,8.75304829418602));
#382844=CARTESIAN_POINT('Ctrl Pts',(1.3996876188618,2.36692529818532,8.75272238421917));
#382845=CARTESIAN_POINT('Ctrl Pts',(1.3878137305448,2.36748663052192,8.76769408445021));
#382846=CARTESIAN_POINT('Ctrl Pts',(1.39440946688854,2.37163191905903,8.76974318093966));
#382847=CARTESIAN_POINT('Ctrl Pts',(1.40098765781904,2.36792439139735,8.77077869880429));
#382848=CARTESIAN_POINT('Ctrl Pts',(1.38207969920048,2.36389599497185,8.78108014887988));
#382849=CARTESIAN_POINT('Ctrl Pts',(1.38766732642936,2.36741219451847,8.78639403366328));
#382850=CARTESIAN_POINT('Ctrl Pts',(1.39432774009022,2.36281208956368,8.78812224174742));
#382851=CARTESIAN_POINT('Ctrl Pts',(1.37268288764616,2.3580117359164,8.78944554828686));
#382852=CARTESIAN_POINT('Ctrl Pts',(1.37738895133899,2.36097979624867,8.79673892988685));
#382853=CARTESIAN_POINT('Ctrl Pts',(1.38345412585988,2.35444395564874,8.79894799272499));
#382854=CARTESIAN_POINT('Origin',(1.39348601430777,2.35629008781361,8.75721825406948));
#382855=CARTESIAN_POINT('Origin',(1.39348601430777,2.35629008781361,9.));
#382856=CARTESIAN_POINT('Origin',(1.39348601430777,2.35629008781361,7.51860402984325));
#382857=CARTESIAN_POINT('Ctrl Pts',(1.38161790355312,2.37350050411394,7.50366195182966));
#382858=CARTESIAN_POINT('Ctrl Pts',(1.38346014519165,2.37666531650258,7.50000065167735));
#382859=CARTESIAN_POINT('Ctrl Pts',(1.38346014519175,2.37666531650252,7.49482233047108));
#382860=CARTESIAN_POINT('Ctrl Pts',(1.38867182375217,2.37113491551234,7.50215800491338));
#382861=CARTESIAN_POINT('Ctrl Pts',(1.39169926431183,2.37186928655758,7.49877273257264));
#382862=CARTESIAN_POINT('Ctrl Pts',(1.39468274606847,2.37013262511744,7.49481816995647));
#382863=CARTESIAN_POINT('Ctrl Pts',(1.38924060074975,2.36838055368624,7.5104302581404));
#382864=CARTESIAN_POINT('Ctrl Pts',(1.39484851529313,2.37000660764011,7.51006209594515));
#382865=CARTESIAN_POINT('Ctrl Pts',(1.39985114343623,2.36704811447227,7.50731281821699));
#382866=CARTESIAN_POINT('Ctrl Pts',(1.38685063022082,2.36688356118255,7.51860402984325));
#382867=CARTESIAN_POINT('Ctrl Pts',(1.39329931967803,2.370922796466,7.51860402984324));
#382868=CARTESIAN_POINT('Ctrl Pts',(1.3998489641448,2.36704940328307,7.51860402984325));
#382869=CARTESIAN_POINT('Origin',(0.,0.,7.5));
#382870=CARTESIAN_POINT('Origin',(1.46041276049031,2.2325170979263,7.5));
#382871=CARTESIAN_POINT('',(1.46041276049031,2.2325170979263,7.59394543036555));
#382872=CARTESIAN_POINT('',(1.46041276049031,2.2325170979263,8.85049129520029));
#382873=CARTESIAN_POINT('',(1.46041276049031,2.2325170979263,7.5));
#382874=CARTESIAN_POINT('',(1.5233121462109,2.26650000646725,8.78727029226991));
#382875=CARTESIAN_POINT('Ctrl Pts',(1.46041276049031,2.2325170979263,8.85049129520029));
#382876=CARTESIAN_POINT('Ctrl Pts',(1.48140969918004,2.24386119992283,8.82945686509571));
#382877=CARTESIAN_POINT('Ctrl Pts',(1.50237542338151,2.25518843754003,8.80838212259896));
#382878=CARTESIAN_POINT('Ctrl Pts',(1.5233121462109,2.26650000646725,8.78727029226991));
#382879=CARTESIAN_POINT('',(1.53564927699518,2.27316543860616,8.75721825406948));
#382880=CARTESIAN_POINT('Origin',(1.49852247476168,2.25310701859276,8.75937679713152));
#382881=CARTESIAN_POINT('',(1.53564927699518,2.27316543860616,7.51860402984325));
#382882=CARTESIAN_POINT('',(1.53564927699518,2.27316543860616,7.5));
#382883=CARTESIAN_POINT('Ctrl Pts',(1.53564927699518,2.27316543860616,7.51860402984325));
#382884=CARTESIAN_POINT('Ctrl Pts',(1.5259603795509,2.26793077833183,7.52834476460825));
#382885=CARTESIAN_POINT('Ctrl Pts',(1.51626519221421,2.26269271979159,7.53807742314407));
#382886=CARTESIAN_POINT('Ctrl Pts',(1.50656350379361,2.25745114888413,7.54780169004675));
#382887=CARTESIAN_POINT('Ctrl Pts',(1.49119655366688,2.24914878384945,7.5632044032688));
#382888=CARTESIAN_POINT('Ctrl Pts',(1.47581327361948,2.24083759618168,7.57858609112103));
#382889=CARTESIAN_POINT('Ctrl Pts',(1.46041276049031,2.2325170979263,7.59394543036555));
#382890=CARTESIAN_POINT('Origin',(1.47188478489783,2.51325648817661,7.5));
#382891=CARTESIAN_POINT('',(1.45700592305909,2.32435658911882,8.75721825406948));
#382892=CARTESIAN_POINT('',(1.45590483281682,2.31037730509333,8.78727029226991));
#382893=CARTESIAN_POINT('Origin',(1.45310985509558,2.27489266822179,8.75658640620982));
#382894=CARTESIAN_POINT('',(1.45029105591251,2.23910559748226,8.85049129520029));
#382895=CARTESIAN_POINT('Ctrl Pts',(1.45590483281682,2.31037730509333,8.78727029226991));
#382896=CARTESIAN_POINT('Ctrl Pts',(1.45403622806456,2.28665376676723,8.80838212259896));
#382897=CARTESIAN_POINT('Ctrl Pts',(1.45216503493675,2.26289736679571,8.82945686509571));
#382898=CARTESIAN_POINT('Ctrl Pts',(1.45029105591251,2.23910559748226,8.85049129520029));
#382899=CARTESIAN_POINT('',(1.45029105591251,2.23910559748226,7.59394543036555));
#382900=CARTESIAN_POINT('',(1.45029105591251,2.23910559748226,7.5));
#382901=CARTESIAN_POINT('',(1.45700592305909,2.32435658911882,7.51860402984325));
#382902=CARTESIAN_POINT('Ctrl Pts',(1.45029105591251,2.23910559748225,7.59394543036555));
#382903=CARTESIAN_POINT('Ctrl Pts',(1.45166555335678,2.25655602018875,7.57858609112103));
#382904=CARTESIAN_POINT('Ctrl Pts',(1.45303851274666,2.27398691597674,7.56320440326857));
#382905=CARTESIAN_POINT('Ctrl Pts',(1.45441001468936,2.29139930822443,7.54780169004651));
#382906=CARTESIAN_POINT('Ctrl Pts',(1.45527589141875,2.30239235517594,7.53807742314383));
#382907=CARTESIAN_POINT('Ctrl Pts',(1.45614118792571,2.31337803570671,7.52834476460825));
#382908=CARTESIAN_POINT('Ctrl Pts',(1.4570059230591,2.32435658911882,7.51860402984325));
#382909=CARTESIAN_POINT('',(1.45700592305909,2.32435658911882,7.5));
#382910=CARTESIAN_POINT('Origin',(1.45714482817987,2.23856575425762,7.5));
#382911=CARTESIAN_POINT('Ctrl Pts',(1.45029105591251,2.23910559748225,8.85049129520029));
#382912=CARTESIAN_POINT('Ctrl Pts',(1.4502758490977,2.2389125339392,8.85097269580138));
#382913=CARTESIAN_POINT('Ctrl Pts',(1.45026921958581,2.23872124576364,8.85143669361005));
#382914=CARTESIAN_POINT('Ctrl Pts',(1.45027173587022,2.23852289447122,8.8519052845931));
#382915=CARTESIAN_POINT('Ctrl Pts',(1.45027665756297,2.23813493192223,8.85282181883899));
#382916=CARTESIAN_POINT('Ctrl Pts',(1.45031663843729,2.23772993073655,8.85372622499635));
#382917=CARTESIAN_POINT('Ctrl Pts',(1.45040765001546,2.23730305049346,8.8546225773507));
#382918=CARTESIAN_POINT('Ctrl Pts',(1.45048320459523,2.23694866967699,8.85536669723986));
#382919=CARTESIAN_POINT('Ctrl Pts',(1.4505939144795,2.23657912300746,8.85610498449051));
#382920=CARTESIAN_POINT('Ctrl Pts',(1.45075659285669,2.23619390632567,8.85681338218371));
#382921=CARTESIAN_POINT('Ctrl Pts',(1.45090422373948,2.23584432158196,8.85745625420284));
#382922=CARTESIAN_POINT('Ctrl Pts',(1.4510959542817,2.23547721364194,8.85808743050665));
#382923=CARTESIAN_POINT('Ctrl Pts',(1.45136036504231,2.23509358140355,8.85866804508409));
#382924=CARTESIAN_POINT('Ctrl Pts',(1.45148235843553,2.23491658180487,8.85893592806395));
#382925=CARTESIAN_POINT('Ctrl Pts',(1.4516200627417,2.234736101987,8.85919241173848));
#382926=CARTESIAN_POINT('Ctrl Pts',(1.45177781230635,2.23455270357739,8.85943017985534));
#382927=CARTESIAN_POINT('Ctrl Pts',(1.45199082091748,2.23430506143268,8.8597512372));
#382928=CARTESIAN_POINT('Ctrl Pts',(1.45224628528148,2.23404621238968,8.86004599534705));
#382929=CARTESIAN_POINT('Ctrl Pts',(1.4525485489785,2.23378658238068,8.86026130871721));
#382930=CARTESIAN_POINT('Ctrl Pts',(1.4526592162397,2.23369152451464,8.86034014101235));
#382931=CARTESIAN_POINT('Ctrl Pts',(1.45277781125685,2.23359492473796,8.86040910639692));
#382932=CARTESIAN_POINT('Ctrl Pts',(1.45290131541274,2.23349967566561,8.86046313645506));
#382933=CARTESIAN_POINT('Ctrl Pts',(1.45309404261367,2.23335104028592,8.86054744990829));
#382934=CARTESIAN_POINT('Ctrl Pts',(1.45330407489591,2.23320175318969,8.86059655985668));
#382935=CARTESIAN_POINT('Ctrl Pts',(1.45351777252622,2.23306114982854,8.86059725258816));
#382936=CARTESIAN_POINT('Ctrl Pts',(1.45373196388343,2.23292022161745,8.86059794692011));
#382937=CARTESIAN_POINT('Ctrl Pts',(1.45395367324847,2.23278867385447,8.86056369958366));
#382938=CARTESIAN_POINT('Ctrl Pts',(1.45416888827214,2.23267044490978,8.86048590497774));
#382939=CARTESIAN_POINT('Ctrl Pts',(1.45422505298559,2.23263959067531,8.86046560290182));
#382940=CARTESIAN_POINT('Ctrl Pts',(1.45428154968206,2.23260932151749,8.86044257503091));
#382941=CARTESIAN_POINT('Ctrl Pts',(1.45433661706439,2.23258054384337,8.86041778462584));
#382942=CARTESIAN_POINT('Ctrl Pts',(1.4547071522146,2.23238690580672,8.86025097596201));
#382943=CARTESIAN_POINT('Ctrl Pts',(1.45506284807405,2.23223510696686,8.8599848982295));
#382944=CARTESIAN_POINT('Ctrl Pts',(1.45538999722907,2.23212178540184,8.85968173251461));
#382945=CARTESIAN_POINT('Ctrl Pts',(1.45556304038866,2.23206184478649,8.85952137522076));
#382946=CARTESIAN_POINT('Ctrl Pts',(1.45573136976942,2.23201133351792,8.85934740853961));
#382947=CARTESIAN_POINT('Ctrl Pts',(1.4558921647566,2.23196947495596,8.8591675900182));
#382948=CARTESIAN_POINT('Ctrl Pts',(1.45653784020969,2.23180139107203,8.85844552518695));
#382949=CARTESIAN_POINT('Ctrl Pts',(1.45709775787567,2.23176039886351,8.85759444184125));
#382950=CARTESIAN_POINT('Ctrl Pts',(1.45755728671856,2.23176798161147,8.8568349891514));
#382951=CARTESIAN_POINT('Ctrl Pts',(1.45760537518814,2.23176877512585,8.85675551444999));
#382952=CARTESIAN_POINT('Ctrl Pts',(1.45765236006119,2.23177012010279,8.85667699793651));
#382953=CARTESIAN_POINT('Ctrl Pts',(1.45769822112842,2.23177193923716,8.85659965593547));
#382954=CARTESIAN_POINT('Ctrl Pts',(1.45831725615402,2.23179649400577,8.85555568965886));
#382955=CARTESIAN_POINT('Ctrl Pts',(1.45890864097158,2.23190949356634,8.85434650606346));
#382956=CARTESIAN_POINT('Ctrl Pts',(1.45947646544067,2.23210539222272,8.85297329937117));
#382957=CARTESIAN_POINT('Ctrl Pts',(1.45979583210649,2.23221557328066,8.85220095427747));
#382958=CARTESIAN_POINT('Ctrl Pts',(1.46010777345562,2.2323523213329,8.85137579139183));
#382959=CARTESIAN_POINT('Ctrl Pts',(1.46041276049031,2.2325170979263,8.85049129520029));
#382960=CARTESIAN_POINT('Origin',(1.45714482817987,2.23856575425762,7.59394543036555));
#382961=CARTESIAN_POINT('Ctrl Pts',(1.45024690539914,2.2385450688874,7.59443877723642));
#382962=CARTESIAN_POINT('Ctrl Pts',(1.44979219759188,2.23277216368648,7.58783886950015));
#382963=CARTESIAN_POINT('Ctrl Pts',(1.45787199014354,2.23016522412854,7.58559994247159));
#382964=CARTESIAN_POINT('Ctrl Pts',(1.45272914197842,2.27005918900933,7.56670252222137));
#382965=CARTESIAN_POINT('Ctrl Pts',(1.45227509135303,2.26429462729542,7.56004874999031));
#382966=CARTESIAN_POINT('Ctrl Pts',(1.46039619893559,2.26165190731612,7.55786368756704));
#382967=CARTESIAN_POINT('Ctrl Pts',(1.45520674322889,2.30151445966059,7.53888913333558));
#382968=CARTESIAN_POINT('Ctrl Pts',(1.4547499941584,2.29571563887413,7.53222002137277));
#382969=CARTESIAN_POINT('Ctrl Pts',(1.46291462079657,2.29308100102818,7.53005029815327));
#382970=CARTESIAN_POINT('Ctrl Pts',(1.45767959703743,2.33290945746887,7.51101258149734));
#382971=CARTESIAN_POINT('Ctrl Pts',(1.45721731133828,2.32704034443777,7.5043616886572));
#382972=CARTESIAN_POINT('Ctrl Pts',(1.46542721367564,2.32445094582891,7.50217374673251));
#382973=CARTESIAN_POINT('',(1.46529313746767,2.32277700535967,7.50366116523517));
#382974=CARTESIAN_POINT('Ctrl Pts',(1.45700592305909,2.32435658911882,7.51860402984325));
#382975=CARTESIAN_POINT('Ctrl Pts',(1.45704059954239,2.32479683678467,7.51734760759494));
#382976=CARTESIAN_POINT('Ctrl Pts',(1.45713124780418,2.3251899916557,7.51608817408573));
#382977=CARTESIAN_POINT('Ctrl Pts',(1.4572906716018,2.32553214927377,7.5148100591312));
#382978=CARTESIAN_POINT('Ctrl Pts',(1.45743508148724,2.32584208382035,7.51365231206384));
#382979=CARTESIAN_POINT('Ctrl Pts',(1.45763589966002,2.3261107167927,7.51247773061043));
#382980=CARTESIAN_POINT('Ctrl Pts',(1.45791922593487,2.32631129114239,7.51129758471022));
#382981=CARTESIAN_POINT('Ctrl Pts',(1.45827136813743,2.32656058215259,7.50983079813402));
#382982=CARTESIAN_POINT('Ctrl Pts',(1.45874725305973,2.3266861520984,7.50839324291155));
#382983=CARTESIAN_POINT('Ctrl Pts',(1.45937138700825,2.32660920611061,7.50715379678855));
#382984=CARTESIAN_POINT('Ctrl Pts',(1.45965971890848,2.3265736592814,7.50658120839351));
#382985=CARTESIAN_POINT('Ctrl Pts',(1.46001951610518,2.32648040840139,7.50598221009429));
#382986=CARTESIAN_POINT('Ctrl Pts',(1.46043650913798,2.32630965373253,7.50545747549611));
#382987=CARTESIAN_POINT('Ctrl Pts',(1.46065902952742,2.32621853375587,7.50517746087247));
#382988=CARTESIAN_POINT('Ctrl Pts',(1.46090032677017,2.32610454297667,7.50491486231392));
#382989=CARTESIAN_POINT('Ctrl Pts',(1.46115329842596,2.32596919186967,7.50468370960992));
#382990=CARTESIAN_POINT('Ctrl Pts',(1.46153157084674,2.3257667992706,7.50433806340446));
#382991=CARTESIAN_POINT('Ctrl Pts',(1.46194702721951,2.32551008583305,7.50405484070984));
#382992=CARTESIAN_POINT('Ctrl Pts',(1.46237131075486,2.32521573129308,7.50385766036131));
#382993=CARTESIAN_POINT('Ctrl Pts',(1.46241668128411,2.32518425465034,7.50383657498791));
#382994=CARTESIAN_POINT('Ctrl Pts',(1.46246214090838,2.32515237335348,7.50381643264937));
#382995=CARTESIAN_POINT('Ctrl Pts',(1.46250764664087,2.32512012665496,7.50379723213559));
#382996=CARTESIAN_POINT('Ctrl Pts',(1.46281141229124,2.3249048693937,7.50366906242519));
#382997=CARTESIAN_POINT('Ctrl Pts',(1.46312342439225,2.32466806081159,7.50358235568538));
#382998=CARTESIAN_POINT('Ctrl Pts',(1.46341867889314,2.32443257728237,7.5035341175365));
#382999=CARTESIAN_POINT('Ctrl Pts',(1.46386137960088,2.32407949638188,7.50346178989176));
#383000=CARTESIAN_POINT('Ctrl Pts',(1.46432261222972,2.3236808385577,7.50346967198527));
#383001=CARTESIAN_POINT('Ctrl Pts',(1.46476335765927,2.32327554780209,7.50354272648692));
#383002=CARTESIAN_POINT('Ctrl Pts',(1.46494464537733,2.32310884332528,7.50357277531559));
#383003=CARTESIAN_POINT('Ctrl Pts',(1.465122322082,2.32294134252926,7.50361331098761));
#383004=CARTESIAN_POINT('Ctrl Pts',(1.46529313746842,2.32277700536087,7.50366116523658));
#383005=CARTESIAN_POINT('',(1.45874211355528,2.24101961352507,7.57603338622103));
#383006=CARTESIAN_POINT('Origin',(1.4635653631209,2.24842419003007,7.5848687342763));
#383007=CARTESIAN_POINT('Ctrl Pts',(1.46529313746688,2.32277700541701,7.50366116529968));
#383008=CARTESIAN_POINT('Ctrl Pts',(1.46311385930741,2.29556894511304,7.52783573079709));
#383009=CARTESIAN_POINT('Ctrl Pts',(1.46093030563638,2.26831776646581,7.55196141284069));
#383010=CARTESIAN_POINT('Ctrl Pts',(1.4587421132987,2.24101961475055,7.57603338728831));
#383011=CARTESIAN_POINT('Ctrl Pts',(1.45054708277063,2.24011702507157,7.59639677331369));
#383012=CARTESIAN_POINT('Ctrl Pts',(1.44604747589547,2.22151724109334,7.59974925422225));
#383013=CARTESIAN_POINT('Ctrl Pts',(1.46123398723744,2.23316062115794,7.59639677331374));
#383014=CARTESIAN_POINT('Ctrl Pts',(1.44903241888635,2.2365224600907,7.58707626057419));
#383015=CARTESIAN_POINT('Ctrl Pts',(1.45166892345315,2.23015329411148,7.58811717123965));
#383016=CARTESIAN_POINT('Ctrl Pts',(1.45856018235537,2.2303205733527,7.58707626057427));
#383017=CARTESIAN_POINT('Ctrl Pts',(1.45468954949523,2.23874113211159,7.58015376756928));
#383018=CARTESIAN_POINT('Ctrl Pts',(1.4554393233935,2.23594564091327,7.58208760766041));
#383019=CARTESIAN_POINT('Ctrl Pts',(1.4582990518177,2.23639160646932,7.58015376756931));
#383020=CARTESIAN_POINT('Ctrl Pts',(1.45874211310364,2.2410196128316,7.57603338509286));
#383021=CARTESIAN_POINT('Ctrl Pts',(1.45874211310364,2.2410196128316,7.57603338509286));
#383022=CARTESIAN_POINT('Ctrl Pts',(1.45874211310364,2.2410196128316,7.57603338509286));
#383023=CARTESIAN_POINT('Origin',(1.46356058069556,2.24842730304488,7.58486873427623));
#383024=CARTESIAN_POINT('Ctrl Pts',(1.54322129228843,2.27725640229735,7.51098857897448));
#383025=CARTESIAN_POINT('Ctrl Pts',(1.53804160317609,2.27445795046259,7.50433767179956));
#383026=CARTESIAN_POINT('Ctrl Pts',(1.53235058273387,2.28091707868618,7.50214974420965));
#383027=CARTESIAN_POINT('Ctrl Pts',(1.51550631077543,2.2622827158109,7.53887321589169));
#383028=CARTESIAN_POINT('Ctrl Pts',(1.51038868353094,2.25951779439551,7.53220407452062));
#383029=CARTESIAN_POINT('Ctrl Pts',(1.50467460613785,2.26591718807518,7.53003438070911));
#383030=CARTESIAN_POINT('Ctrl Pts',(1.4877381062743,2.24728027432284,7.56669465659234));
#383031=CARTESIAN_POINT('Ctrl Pts',(1.48265072325537,2.24453169307895,7.56004085833301));
#383032=CARTESIAN_POINT('Ctrl Pts',(1.47694687288308,2.25088800813224,7.55785582193788));
#383033=CARTESIAN_POINT('Ctrl Pts',(1.45991793462975,2.23224975633353,7.59443891967696));
#383034=CARTESIAN_POINT('Ctrl Pts',(1.45482317553885,2.22949718998903,7.58783901202978));
#383035=CARTESIAN_POINT('Ctrl Pts',(1.449168791725,2.23583020835897,7.58560008491213));
#383036=CARTESIAN_POINT('',(1.53085035931323,2.28010398287623,7.50366116523517));
#383037=CARTESIAN_POINT('Ctrl Pts',(1.53085035931343,2.28010398287654,7.50366116523554));
#383038=CARTESIAN_POINT('Ctrl Pts',(1.53155169493517,2.27981716261496,7.50350835821027));
#383039=CARTESIAN_POINT('Ctrl Pts',(1.53218706119348,2.27953068795824,7.50345484956));
#383040=CARTESIAN_POINT('Ctrl Pts',(1.53277559486934,2.27923658921162,7.50349758195598));
#383041=CARTESIAN_POINT('Ctrl Pts',(1.53307755629185,2.27908569474368,7.50351950684424));
#383042=CARTESIAN_POINT('Ctrl Pts',(1.53339700966224,2.27891803629775,7.50357029184312));
#383043=CARTESIAN_POINT('Ctrl Pts',(1.53370061085855,2.27874789763523,7.50365515313924));
#383044=CARTESIAN_POINT('Ctrl Pts',(1.53416767243874,2.27848615547632,7.50378570417639));
#383045=CARTESIAN_POINT('Ctrl Pts',(1.53461109666587,2.27821116305176,7.50400001621911));
#383046=CARTESIAN_POINT('Ctrl Pts',(1.53499593592695,2.27794192178181,7.50428903009635));
#383047=CARTESIAN_POINT('Ctrl Pts',(1.53503865012416,2.27791203807227,7.50432110841318));
#383048=CARTESIAN_POINT('Ctrl Pts',(1.5350806729107,2.27788222500583,7.50435406373354));
#383049=CARTESIAN_POINT('Ctrl Pts',(1.53512197887439,2.277852508107,7.50438785222352));
#383050=CARTESIAN_POINT('Ctrl Pts',(1.53537417163686,2.27767107215592,7.50459414719561));
#383051=CARTESIAN_POINT('Ctrl Pts',(1.53560335743637,2.27748991372872,7.50483629897752));
#383052=CARTESIAN_POINT('Ctrl Pts',(1.53580157232053,2.27731700539469,7.5050991045531));
#383053=CARTESIAN_POINT('Ctrl Pts',(1.53623885426378,2.27693555224282,7.50567888004914));
#383054=CARTESIAN_POINT('Ctrl Pts',(1.53654297792573,2.27657961193306,7.50637912803145));
#383055=CARTESIAN_POINT('Ctrl Pts',(1.5367418703485,2.27626243205668,7.50710440483569));
#383056=CARTESIAN_POINT('Ctrl Pts',(1.53679064271913,2.27618465325409,7.50728225710685));
#383057=CARTESIAN_POINT('Ctrl Pts',(1.53683418180228,2.27610773442094,7.50746498566955));
#383058=CARTESIAN_POINT('Ctrl Pts',(1.53687183379768,2.27603367630524,7.50764697238949));
#383059=CARTESIAN_POINT('Ctrl Pts',(1.53707424056282,2.27563556025657,7.50862528291182));
#383060=CARTESIAN_POINT('Ctrl Pts',(1.53712858336449,2.27528585019077,7.50965856837421));
#383061=CARTESIAN_POINT('Ctrl Pts',(1.53710069976791,2.27497674797687,7.51067959873202));
#383062=CARTESIAN_POINT('Ctrl Pts',(1.53708535538955,2.27480664863868,7.51124147302578));
#383063=CARTESIAN_POINT('Ctrl Pts',(1.53704467387375,2.27464884415314,7.51180065547253));
#383064=CARTESIAN_POINT('Ctrl Pts',(1.53698693264453,2.27450237756294,7.51235175716501));
#383065=CARTESIAN_POINT('Ctrl Pts',(1.5367874136962,2.27399627714843,7.51425603304537));
#383066=CARTESIAN_POINT('Ctrl Pts',(1.53635477473427,2.27356742990723,7.51626900505183));
#383067=CARTESIAN_POINT('Ctrl Pts',(1.53574915221222,2.27322096169133,7.51827788969247));
#383068=CARTESIAN_POINT('Ctrl Pts',(1.53571637477686,2.27320221017675,7.51838661432547));
#383069=CARTESIAN_POINT('Ctrl Pts',(1.53568308088394,2.27318370197148,7.51849533314857));
#383070=CARTESIAN_POINT('Ctrl Pts',(1.53564927699518,2.27316543860616,7.51860402984325));
#383071=CARTESIAN_POINT('Ctrl Pts',(1.45874211478058,2.24101961378738,7.57603338728984));
#383072=CARTESIAN_POINT('Ctrl Pts',(1.48281814548955,2.25407036159789,7.55196141284921));
#383073=CARTESIAN_POINT('Ctrl Pts',(1.50685310110153,2.26709785384546,7.52783573083104));
#383074=CARTESIAN_POINT('Ctrl Pts',(1.53085035936762,2.28010398289953,7.50366116530176));
#383075=CARTESIAN_POINT('Origin',(5.04062831473859E-16,7.74375868966282E-16,
7.49482233047033));
#383076=CARTESIAN_POINT('Origin',(1.46057722850546,2.31530136474095,7.49482233047033));
#383077=CARTESIAN_POINT('Origin',(0.,0.,7.50366116523517));
#383078=CARTESIAN_POINT('Origin',(1.52592346056192,2.27276568139057,7.49482233047033));
#383079=CARTESIAN_POINT('Ctrl Pts',(1.45700583995948,2.32435553466796,7.51860402984325));
#383080=CARTESIAN_POINT('Ctrl Pts',(1.45760395760191,2.33194095102541,7.51860402984325));
#383081=CARTESIAN_POINT('Ctrl Pts',(1.4511406126304,2.33595610454792,7.51860402984325));
#383082=CARTESIAN_POINT('Ctrl Pts',(1.45722792385509,2.32717205162695,7.51041458714365));
#383083=CARTESIAN_POINT('Ctrl Pts',(1.45607271192432,2.33289217847477,7.51004642900443));
#383084=CARTESIAN_POINT('Ctrl Pts',(1.4511388301166,2.33595721187959,7.5072913648301));
#383085=CARTESIAN_POINT('Ctrl Pts',(1.45993819904963,2.32793241046927,7.50215815450138));
#383086=CARTESIAN_POINT('Ctrl Pts',(1.45919055500405,2.33095550372991,7.49877163671529));
#383087=CARTESIAN_POINT('Ctrl Pts',(1.45627247511123,2.33279635498231,7.4948158853317));
#383088=CARTESIAN_POINT('Ctrl Pts',(1.46529284374238,2.32277653974658,7.50366171572174));
#383089=CARTESIAN_POINT('Ctrl Pts',(1.46724653091906,2.32587351709116,7.50000045605858));
#383090=CARTESIAN_POINT('Ctrl Pts',(1.46724653091895,2.32587351709123,7.49482233047317));
#383091=CARTESIAN_POINT('Origin',(1.44454451893662,2.32533812225452,7.51860402984325));
#383092=CARTESIAN_POINT('Origin',(1.44454451893662,2.32533812225452,9.));
#383093=CARTESIAN_POINT('Origin',(1.44454451893662,2.32533812225452,8.75721825406948));
#383094=CARTESIAN_POINT('Ctrl Pts',(1.45569455202207,2.30770799497264,8.78942910404913));
#383095=CARTESIAN_POINT('Ctrl Pts',(1.45615226043134,2.31326163627486,8.79672699501691));
#383096=CARTESIAN_POINT('Ctrl Pts',(1.44754234110094,2.31561594617506,8.79893251111267));
#383097=CARTESIAN_POINT('Ctrl Pts',(1.45655786092529,2.31866838349121,8.78111911759576));
#383098=CARTESIAN_POINT('Ctrl Pts',(1.45709306086352,2.32525290102493,8.78644465894812));
#383099=CARTESIAN_POINT('Ctrl Pts',(1.44991412529163,2.32901832209436,8.78817647674131));
#383100=CARTESIAN_POINT('Ctrl Pts',(1.45709589559391,2.3254991590484,8.76780923932034));
#383101=CARTESIAN_POINT('Ctrl Pts',(1.45772259748296,2.33327231680525,8.76988516158375));
#383102=CARTESIAN_POINT('Ctrl Pts',(1.45138449933332,2.3373911627895,8.77093053738833));
#383103=CARTESIAN_POINT('Ctrl Pts',(1.45699098619532,2.32416725130065,8.75371302330491));
#383104=CARTESIAN_POINT('Ctrl Pts',(1.45760306669665,2.33174957012985,8.75300828287559));
#383105=CARTESIAN_POINT('Ctrl Pts',(1.45109726602121,2.33575819793819,8.75267964240738));
#383106=CARTESIAN_POINT('Origin',(1.44344342869435,2.31135883822903,8.78727029226991));
#383107=CARTESIAN_POINT('Ctrl Pts',(1.45029105591251,2.23910559748226,8.85049129520029));
#383108=CARTESIAN_POINT('Ctrl Pts',(1.45074959802196,2.24492718243456,8.85711686593484));
#383109=CARTESIAN_POINT('Ctrl Pts',(1.44260408658464,2.24752552912785,8.85933012996512));
#383110=CARTESIAN_POINT('Ctrl Pts',(1.45216503745169,2.26289739872515,8.82945683644722));
#383111=CARTESIAN_POINT('Ctrl Pts',(1.45262738573788,2.26876730635237,8.83607469902389));
#383112=CARTESIAN_POINT('Ctrl Pts',(1.44444656216418,2.27133755306296,8.8382956714852));
#383113=CARTESIAN_POINT('Ctrl Pts',(1.45403622567028,2.28665373636973,8.80838214965002));
#383114=CARTESIAN_POINT('Ctrl Pts',(1.45450039859867,2.2925468093931,8.81501364461996));
#383115=CARTESIAN_POINT('Ctrl Pts',(1.44628690934866,2.29511340381665,8.81722098428721));
#383116=CARTESIAN_POINT('Ctrl Pts',(1.45590483281682,2.31037730509333,8.78727029226991));
#383117=CARTESIAN_POINT('Ctrl Pts',(1.45636908284586,2.31627135697544,8.79393457792714));
#383118=CARTESIAN_POINT('Ctrl Pts',(1.44812530550982,2.31885583959522,8.79610912703474));
#383119=CARTESIAN_POINT('Origin',(1.43782965179004,2.24008713061795,8.85049129520029));
#383120=CARTESIAN_POINT('Ctrl Pts',(1.46041276049031,2.2325170979263,8.85049129520029));
#383121=CARTESIAN_POINT('Ctrl Pts',(1.46555048104863,2.23529287523863,8.85711686593484));
#383122=CARTESIAN_POINT('Ctrl Pts',(1.47122360941498,2.22889628422053,8.85933012996512));
#383123=CARTESIAN_POINT('Ctrl Pts',(1.45586749327613,2.23006140780685,8.86332496987232));
#383124=CARTESIAN_POINT('Ctrl Pts',(1.45988689960006,2.22778187557852,8.86648636486736));
#383125=CARTESIAN_POINT('Ctrl Pts',(1.45849989529328,2.22204146436105,8.87206031107457));
#383126=CARTESIAN_POINT('Ctrl Pts',(1.44988263370187,2.23392032758735,8.86341338519876));
#383127=CARTESIAN_POINT('Ctrl Pts',(1.44614309960763,2.23665699625423,8.86654584966054));
#383128=CARTESIAN_POINT('Ctrl Pts',(1.44147517002643,2.23300534098411,8.87215952290714));
#383129=CARTESIAN_POINT('Ctrl Pts',(1.45029105591251,2.23910559748225,8.85049129520029));
#383130=CARTESIAN_POINT('Ctrl Pts',(1.45074959802196,2.24492718243456,8.85711686593484));
#383131=CARTESIAN_POINT('Ctrl Pts',(1.44260408658464,2.24752552912785,8.85933012996512));
#383132=CARTESIAN_POINT('Origin',(1.46635445560019,2.22151954096027,8.85049129520029));
#383133=CARTESIAN_POINT('Ctrl Pts',(1.5233121462109,2.26650000646725,8.78727029226991));
#383134=CARTESIAN_POINT('Ctrl Pts',(1.5285138209738,2.26931033657942,8.79393457792714));
#383135=CARTESIAN_POINT('Ctrl Pts',(1.53421404825534,2.26281827803709,8.79610912703474));
#383136=CARTESIAN_POINT('Ctrl Pts',(1.50237539655482,2.25518842304626,8.80838214965003));
#383137=CARTESIAN_POINT('Ctrl Pts',(1.50757620744593,2.25799828643089,8.81501364461988));
#383138=CARTESIAN_POINT('Ctrl Pts',(1.51324781742237,2.2515266828529,8.81722098428721));
#383139=CARTESIAN_POINT('Ctrl Pts',(1.48140972735871,2.24386121514703,8.82945683644723));
#383140=CARTESIAN_POINT('Ctrl Pts',(1.486590094104,2.24666003308934,8.8360746990239));
#383141=CARTESIAN_POINT('Ctrl Pts',(1.4922518212561,2.24021977780303,8.83829567148519));
#383142=CARTESIAN_POINT('Ctrl Pts',(1.46041276049031,2.2325170979263,8.85049129520029));
#383143=CARTESIAN_POINT('Ctrl Pts',(1.46555048104863,2.23529287523863,8.85711686593484));
#383144=CARTESIAN_POINT('Ctrl Pts',(1.47122360941498,2.22889628422053,8.85933012996512));
#383145=CARTESIAN_POINT('Origin',(1.52925384132078,2.25550244950121,8.78727029226991));
#383146=CARTESIAN_POINT('Ctrl Pts',(1.53548638015781,2.27307740869794,8.75374538247848));
#383147=CARTESIAN_POINT('Ctrl Pts',(1.5421657429184,2.27670101070422,8.75304829418601));
#383148=CARTESIAN_POINT('Ctrl Pts',(1.54846123506547,2.2723839026635,8.75272238421917));
#383149=CARTESIAN_POINT('Ctrl Pts',(1.53664770761177,2.2737048443191,8.76769408445021));
#383150=CARTESIAN_POINT('Ctrl Pts',(1.54349548185627,2.27741902563786,8.76974318093969));
#383151=CARTESIAN_POINT('Ctrl Pts',(1.54982261507513,2.2732976493494,8.7707786988043));
#383152=CARTESIAN_POINT('Ctrl Pts',(1.53069540464027,2.27048896676448,8.78108014887988));
#383153=CARTESIAN_POINT('Ctrl Pts',(1.53649683516816,2.27363994139629,8.78639403366325));
#383154=CARTESIAN_POINT('Ctrl Pts',(1.54284883455845,2.26862255368209,8.78812224174741));
#383155=CARTESIAN_POINT('Ctrl Pts',(1.52094089407098,2.26521885333375,8.78944554828685));
#383156=CARTESIAN_POINT('Ctrl Pts',(1.52582745292964,2.26787929693169,8.79673892988686));
#383157=CARTESIAN_POINT('Ctrl Pts',(1.53146141315399,2.26096828785146,8.79894799272499));
#383158=CARTESIAN_POINT('Origin',(1.54159097210506,2.26216788164013,8.75721825406948));
#383159=CARTESIAN_POINT('Origin',(1.54159097210506,2.26216788164013,9.));
#383160=CARTESIAN_POINT('Origin',(1.54159097210506,2.26216788164013,7.51860402984325));
#383161=CARTESIAN_POINT('Ctrl Pts',(1.53084992081512,2.28010332976117,7.50366195182967));
#383162=CARTESIAN_POINT('Ctrl Pts',(1.53289114759657,2.28314360687629,7.50000065167736));
#383163=CARTESIAN_POINT('Ctrl Pts',(1.53289114759667,2.28314360687623,7.49482233047108));
#383164=CARTESIAN_POINT('Ctrl Pts',(1.53773778419651,2.2772906552962,7.50215800491336));
#383165=CARTESIAN_POINT('Ctrl Pts',(1.54080605586926,2.2778295487147,7.49877273257261));
#383166=CARTESIAN_POINT('Ctrl Pts',(1.54367213946216,2.2759053030993,7.49481816995645));
#383167=CARTESIAN_POINT('Ctrl Pts',(1.53812892001263,2.2745055109345,7.51043025814043));
#383168=CARTESIAN_POINT('Ctrl Pts',(1.54382949412868,2.27576892366773,7.51006209594518));
#383169=CARTESIAN_POINT('Ctrl Pts',(1.54863229252764,2.27249598955576,7.50731281821701));
#383170=CARTESIAN_POINT('Ctrl Pts',(1.53564794729546,2.27316472009999,7.51860402984324));
#383171=CARTESIAN_POINT('Ctrl Pts',(1.54234218192173,2.27678248738924,7.51860402984324));
#383172=CARTESIAN_POINT('Ctrl Pts',(1.5486302002882,2.27249741534624,7.51860402984325));
#383173=CARTESIAN_POINT('Origin',(0.,0.,7.5));
#383174=CARTESIAN_POINT('Origin',(1.60045004741994,2.13436118528465,7.5));
#383175=CARTESIAN_POINT('',(1.60045004741994,2.13436118528465,7.59394543036555));
#383176=CARTESIAN_POINT('',(1.60045004741994,2.13436118528465,8.85049129520029));
#383177=CARTESIAN_POINT('',(1.60045004741994,2.13436118528465,7.5));
#383178=CARTESIAN_POINT('',(1.66539749203243,2.16424429481557,8.78727029226991));
#383179=CARTESIAN_POINT('Ctrl Pts',(1.60045004741994,2.13436118528465,8.85049129520029));
#383180=CARTESIAN_POINT('Ctrl Pts',(1.62213066475763,2.1443367011262,8.82945686509571));
#383181=CARTESIAN_POINT('Ctrl Pts',(1.64377905123605,2.15429738715723,8.80838212259895));
#383182=CARTESIAN_POINT('Ctrl Pts',(1.66539749203243,2.16424429481557,8.78727029226991));
#383183=CARTESIAN_POINT('',(1.67813633056178,2.17010558942601,8.75721825406948));
#383184=CARTESIAN_POINT('Origin',(1.6398006619417,2.15246710397366,8.75937679713116));
#383185=CARTESIAN_POINT('',(1.67813633056178,2.17010558942601,7.51860402984325));
#383186=CARTESIAN_POINT('',(1.67813633056178,2.17010558942601,7.5));
#383187=CARTESIAN_POINT('Ctrl Pts',(1.67813633056178,2.17010558942601,7.51860402984325));
#383188=CARTESIAN_POINT('Ctrl Pts',(1.66813195416113,2.16550245411326,7.52834476460825));
#383189=CARTESIAN_POINT('Ctrl Pts',(1.65812108306368,2.16089633051148,7.53807742314407));
#383190=CARTESIAN_POINT('Ctrl Pts',(1.64810349920135,2.1562871182849,7.54780169004674));
#383191=CARTESIAN_POINT('Ctrl Pts',(1.63223618776763,2.14898637522467,7.5632044032688));
#383192=CARTESIAN_POINT('Ctrl Pts',(1.61635201469676,2.14167787391999,7.57858609112103));
#383193=CARTESIAN_POINT('Ctrl Pts',(1.60045004741994,2.13436118528465,7.59394543036555));
#383194=CARTESIAN_POINT('Origin',(1.62988553581354,2.41378875122107,7.5));
#383195=CARTESIAN_POINT('',(1.60293438610524,2.22623025921642,8.75721825406948));
#383196=CARTESIAN_POINT('',(1.60093990236827,2.21235024422327,8.78727029226991));
#383197=CARTESIAN_POINT('Origin',(1.59587715873839,2.17711758918247,8.75658640621021));
#383198=CARTESIAN_POINT('',(1.59077126558564,2.14158464790053,8.85049129520029));
#383199=CARTESIAN_POINT('Ctrl Pts',(1.60093990236827,2.21235024422327,8.78727029226991));
#383200=CARTESIAN_POINT('Ctrl Pts',(1.59755516454561,2.18879517036853,8.80838212259895));
#383201=CARTESIAN_POINT('Ctrl Pts',(1.59416573821263,2.16520746822395,8.82945686509571));
#383202=CARTESIAN_POINT('Ctrl Pts',(1.59077126558564,2.14158464790053,8.85049129520029));
#383203=CARTESIAN_POINT('',(1.59077126558564,2.14158464790053,7.59394543036555));
#383204=CARTESIAN_POINT('',(1.59077126558564,2.14158464790053,7.5));
#383205=CARTESIAN_POINT('',(1.60293438610524,2.22623025921642,7.51860402984325));
#383206=CARTESIAN_POINT('Ctrl Pts',(1.59077126558564,2.14158464790053,7.59394543036555));
#383207=CARTESIAN_POINT('Ctrl Pts',(1.59326099139906,2.1589111524884,7.57858609112103));
#383208=CARTESIAN_POINT('Ctrl Pts',(1.59574793122422,2.17621826882141,7.56320440326857));
#383209=CARTESIAN_POINT('Ctrl Pts',(1.59823223107079,2.19350701301058,7.54780169004651));
#383210=CARTESIAN_POINT('Ctrl Pts',(1.59980065570001,2.2044219966556,7.53807742314383));
#383211=CARTESIAN_POINT('Ctrl Pts',(1.60136802933074,2.21532966618996,7.52834476460825));
#383212=CARTESIAN_POINT('Ctrl Pts',(1.60293438610524,2.22623025921642,7.51860402984325));
#383213=CARTESIAN_POINT('',(1.60293438610524,2.22623025921642,7.5));
#383214=CARTESIAN_POINT('Origin',(1.59757636816866,2.14060679114483,7.5));
#383215=CARTESIAN_POINT('Ctrl Pts',(1.59077126558564,2.14158464790053,8.85049129520029));
#383216=CARTESIAN_POINT('Ctrl Pts',(1.59074372039119,2.1413929553312,8.85097269580138));
#383217=CARTESIAN_POINT('Ctrl Pts',(1.59072484862485,2.141202484932,8.85143669361005));
#383218=CARTESIAN_POINT('Ctrl Pts',(1.59071465132835,2.14100437995469,8.8519052845931));
#383219=CARTESIAN_POINT('Ctrl Pts',(1.5906947060631,2.14061689918243,8.85282181883899));
#383220=CARTESIAN_POINT('Ctrl Pts',(1.59070865627737,2.14021016853171,8.85372622499635));
#383221=CARTESIAN_POINT('Ctrl Pts',(1.59077213055141,2.13977833422802,8.8546225773507));
#383222=CARTESIAN_POINT('Ctrl Pts',(1.59082482463932,2.1394198407264,8.85536669723986));
#383223=CARTESIAN_POINT('Ctrl Pts',(1.59091163012185,2.1390439601235,8.85610498449051));
#383224=CARTESIAN_POINT('Ctrl Pts',(1.59104929334132,2.13864911207128,8.8568133821837));
#383225=CARTESIAN_POINT('Ctrl Pts',(1.5911742229292,2.13829078684378,8.85745625420284));
#383226=CARTESIAN_POINT('Ctrl Pts',(1.59134203885398,2.13791214894838,8.85808743050666));
#383227=CARTESIAN_POINT('Ctrl Pts',(1.59158132695242,2.13751236406796,8.8586680450841));
#383228=CARTESIAN_POINT('Ctrl Pts',(1.59169172929391,2.13732791199041,8.85893592806395));
#383229=CARTESIAN_POINT('Ctrl Pts',(1.59181758729019,2.13713898024249,8.85919241173848));
#383230=CARTESIAN_POINT('Ctrl Pts',(1.59196326236498,2.13694585159528,8.85943017985534));
#383231=CARTESIAN_POINT('Ctrl Pts',(1.59215996684039,2.13668507074934,8.8597512372));
#383232=CARTESIAN_POINT('Ctrl Pts',(1.59239832181033,2.13641038588146,8.86004599534705));
#383233=CARTESIAN_POINT('Ctrl Pts',(1.59268332992238,2.1361319232086,8.86026130871721));
#383234=CARTESIAN_POINT('Ctrl Pts',(1.59278767942742,2.13602997017337,8.86034014101235));
#383235=CARTESIAN_POINT('Ctrl Pts',(1.59289984160946,2.13592597046245,8.86040910639693));
#383236=CARTESIAN_POINT('Ctrl Pts',(1.5930169893838,2.1358230041511,8.86046313645507));
#383237=CARTESIAN_POINT('Ctrl Pts',(1.59319979750455,2.13566232608458,8.8605474499083));
#383238=CARTESIAN_POINT('Ctrl Pts',(1.59339983339584,2.13549988890018,8.86059655985668));
#383239=CARTESIAN_POINT('Ctrl Pts',(1.59360408347317,2.13534588276953,8.86059725258816));
#383240=CARTESIAN_POINT('Ctrl Pts',(1.59380880544978,2.13519152082319,8.86059794692011));
#383241=CARTESIAN_POINT('Ctrl Pts',(1.59402163099504,2.13504603837141,8.86056369958366));
#383242=CARTESIAN_POINT('Ctrl Pts',(1.59422882888186,2.13491426346685,8.86048590497774));
#383243=CARTESIAN_POINT('Ctrl Pts',(1.5942829013613,2.13487987414017,8.86046560290182));
#383244=CARTESIAN_POINT('Ctrl Pts',(1.59433734262764,2.13484604741781,8.86044257503091));
#383245=CARTESIAN_POINT('Ctrl Pts',(1.59439045307622,2.13481380069121,8.86041778462583));
#383246=CARTESIAN_POINT('Ctrl Pts',(1.59474782049062,2.13459682023609,8.860250975962));
#383247=CARTESIAN_POINT('Ctrl Pts',(1.59509305974972,2.13442254377126,8.8599848982295));
#383248=CARTESIAN_POINT('Ctrl Pts',(1.59541227620411,2.13428849451922,8.85968173251462));
#383249=CARTESIAN_POINT('Ctrl Pts',(1.59558112341956,2.134217590145,8.85952137522077));
#383250=CARTESIAN_POINT('Ctrl Pts',(1.59574587068147,2.13415639775679,8.85934740853961));
#383251=CARTESIAN_POINT('Ctrl Pts',(1.59590365341083,2.13410432302753,8.8591675900182));
#383252=CARTESIAN_POINT('Ctrl Pts',(1.59653723308303,2.13389521592165,8.85844552518695));
#383253=CARTESIAN_POINT('Ctrl Pts',(1.5970933739583,2.133818433888,8.85759444184124));
#383254=CARTESIAN_POINT('Ctrl Pts',(1.59755244447823,2.13379655894234,8.85683498915138));
#383255=CARTESIAN_POINT('Ctrl Pts',(1.59760048498554,2.13379426978753,8.85675551444998));
#383256=CARTESIAN_POINT('Ctrl Pts',(1.59764745949609,2.13379260166991,8.85667699793651));
#383257=CARTESIAN_POINT('Ctrl Pts',(1.59769334288918,2.13379147873802,8.85659965593547));
#383258=CARTESIAN_POINT('Ctrl Pts',(1.59831267927035,2.13377632134596,8.85555568965886));
#383259=CARTESIAN_POINT('Ctrl Pts',(1.59891008893107,2.13385119858146,8.85434650606346));
#383260=CARTESIAN_POINT('Ctrl Pts',(1.59948929801391,2.13401031410439,8.85297329937117));
#383261=CARTESIAN_POINT('Ctrl Pts',(1.59981506783128,2.13409980689099,8.85220095427747));
#383262=CARTESIAN_POINT('Ctrl Pts',(1.60013512974124,2.13421628782884,8.85137579139183));
#383263=CARTESIAN_POINT('Ctrl Pts',(1.60045004741994,2.13436118528465,8.85049129520029));
#383264=CARTESIAN_POINT('Origin',(1.59757636816866,2.14060679114483,7.59394543036555));
#383265=CARTESIAN_POINT('Ctrl Pts',(1.59069129259386,2.14102809970489,7.59443877723642));
#383266=CARTESIAN_POINT('Ctrl Pts',(1.5898676477264,2.13529618878609,7.58783886950016));
#383267=CARTESIAN_POINT('Ctrl Pts',(1.59776381228676,2.13217693137888,7.58559994247159));
#383268=CARTESIAN_POINT('Ctrl Pts',(1.59518754576058,2.17231843324348,7.56670252222136));
#383269=CARTESIAN_POINT('Ctrl Pts',(1.59436509129383,2.16659480656326,7.56004874999026));
#383270=CARTESIAN_POINT('Ctrl Pts',(1.60230019353944,2.16343719518632,7.55786368756704));
#383271=CARTESIAN_POINT('Ctrl Pts',(1.59967540262374,2.20355033521047,7.53888913333559));
#383272=CARTESIAN_POINT('Ctrl Pts',(1.59884806026979,2.19779269273671,7.53222002137282));
#383273=CARTESIAN_POINT('Ctrl Pts',(1.6068271099805,2.19464035861197,7.53005029815327));
#383274=CARTESIAN_POINT('Ctrl Pts',(1.60415466010479,2.23472239234116,7.51101258149734));
#383275=CARTESIAN_POINT('Ctrl Pts',(1.60331728885819,2.22889495677869,7.5043616886572));
#383276=CARTESIAN_POINT('Ctrl Pts',(1.6113444197322,2.2257848681182,7.50217374673251));
#383277=CARTESIAN_POINT('',(1.61110336926408,2.22412295723132,7.50366116523517));
#383278=CARTESIAN_POINT('Ctrl Pts',(1.60293438610524,2.22623025921642,7.51860402984325));
#383279=CARTESIAN_POINT('Ctrl Pts',(1.60299719810678,2.22666738061631,7.51734760759494));
#383280=CARTESIAN_POINT('Ctrl Pts',(1.60311284964106,2.22705391985441,7.51608817408573));
#383281=CARTESIAN_POINT('Ctrl Pts',(1.60329386799925,2.22738516015518,7.5148100591312));
#383282=CARTESIAN_POINT('Ctrl Pts',(1.60345783875367,2.22768520553486,7.51365231206384));
#383283=CARTESIAN_POINT('Ctrl Pts',(1.60367545569761,2.22794042010746,7.51247773061043));
#383284=CARTESIAN_POINT('Ctrl Pts',(1.60397105069095,2.22812242957887,7.51129758471022));
#383285=CARTESIAN_POINT('Ctrl Pts',(1.60433844150945,2.22834864656558,7.50983079813401));
#383286=CARTESIAN_POINT('Ctrl Pts',(1.60482139396919,2.22844346846281,7.50839324291155));
#383287=CARTESIAN_POINT('Ctrl Pts',(1.60543931562121,2.22832669216943,7.50715379678855));
#383288=CARTESIAN_POINT('Ctrl Pts',(1.60572477761946,2.22827274488671,7.50658120839351));
#383289=CARTESIAN_POINT('Ctrl Pts',(1.60607786096983,2.2281566333151,7.50598221009429));
#383290=CARTESIAN_POINT('Ctrl Pts',(1.60648305695653,2.22795951264467,7.50545747549611));
#383291=CARTESIAN_POINT('Ctrl Pts',(1.60669928207701,2.22785432295347,7.50517746087247));
#383292=CARTESIAN_POINT('Ctrl Pts',(1.6069327801344,2.22772510641314,7.50491486231392));
#383293=CARTESIAN_POINT('Ctrl Pts',(1.60717656005759,2.22757382544986,7.50468370960992));
#383294=CARTESIAN_POINT('Ctrl Pts',(1.60754108793877,2.22734761269088,7.50433806340446));
#383295=CARTESIAN_POINT('Ctrl Pts',(1.60793924302545,2.22706480831742,7.50405484070984));
#383296=CARTESIAN_POINT('Ctrl Pts',(1.60834379546465,2.22674387462099,7.50385766036131));
#383297=CARTESIAN_POINT('Ctrl Pts',(1.60838705605985,2.22670955575059,7.50383657498791));
#383298=CARTESIAN_POINT('Ctrl Pts',(1.60843037964074,2.22667482734915,7.50381643264937));
#383299=CARTESIAN_POINT('Ctrl Pts',(1.60847372582376,2.22663973134264,7.50379723213559));
#383300=CARTESIAN_POINT('Ctrl Pts',(1.60876307577494,2.22640545401847,7.50366906242519));
#383301=CARTESIAN_POINT('Ctrl Pts',(1.60905927443567,2.22614914130104,7.50358235568538));
#383302=CARTESIAN_POINT('Ctrl Pts',(1.60933883482301,2.22589522457716,7.5035341175365));
#383303=CARTESIAN_POINT('Ctrl Pts',(1.6097580039837,2.22551450518752,7.50346178989176));
#383304=CARTESIAN_POINT('Ctrl Pts',(1.61019274686614,2.2250871151726,7.50346967198527));
#383305=CARTESIAN_POINT('Ctrl Pts',(1.61060661966907,2.22465441847369,7.50354272648693));
#383306=CARTESIAN_POINT('Ctrl Pts',(1.61077685411957,2.22447644136514,7.50357277531559));
#383307=CARTESIAN_POINT('Ctrl Pts',(1.61094343395555,2.22429790093191,7.50361331098761));
#383308=CARTESIAN_POINT('Ctrl Pts',(1.61110336926491,2.22412295723247,7.50366116523659));
#383309=CARTESIAN_POINT('',(1.59932759105302,2.14295327026986,7.57603338622103));
#383310=CARTESIAN_POINT('Origin',(1.60461534358149,2.15003360661828,7.58486873427626));
#383311=CARTESIAN_POINT('Ctrl Pts',(1.61110336926697,2.22412295728859,7.50366116529968));
#383312=CARTESIAN_POINT('Ctrl Pts',(1.60718534225927,2.19711042569366,7.5278357307971));
#383313=CARTESIAN_POINT('Ctrl Pts',(1.6032602859228,2.17005513827967,7.55196141284068));
#383314=CARTESIAN_POINT('Ctrl Pts',(1.59932759087549,2.14295327150927,7.57603338728831));
#383315=CARTESIAN_POINT('Ctrl Pts',(1.59109156879722,2.1425775937061,7.59639677331372));
#383316=CARTESIAN_POINT('Ctrl Pts',(1.58540951459636,2.12430431578102,7.59974925422225));
#383317=CARTESIAN_POINT('Ctrl Pts',(1.6013108175438,2.13495077015054,7.59639677331371));
#383318=CARTESIAN_POINT('Ctrl Pts',(1.5893497123834,2.13908745899276,7.58707626057423));
#383319=CARTESIAN_POINT('Ctrl Pts',(1.59157272610353,2.13256245772059,7.58811717123966));
#383320=CARTESIAN_POINT('Ctrl Pts',(1.59846054379304,2.13228786879498,7.58707626057422));
#383321=CARTESIAN_POINT('Ctrl Pts',(1.59513737061503,2.14093911891167,7.5801537675693));
#383322=CARTESIAN_POINT('Ctrl Pts',(1.59570649628631,2.13810133317129,7.58208760766041));
#383323=CARTESIAN_POINT('Ctrl Pts',(1.59858892220311,2.138363159014,7.5801537675693));
#383324=CARTESIAN_POINT('Ctrl Pts',(1.59932759055788,2.14295326960676,7.57603338509286));
#383325=CARTESIAN_POINT('Ctrl Pts',(1.59932759055788,2.14295326960676,7.57603338509286));
#383326=CARTESIAN_POINT('Ctrl Pts',(1.59932759055788,2.14295326960676,7.57603338509286));
#383327=CARTESIAN_POINT('Origin',(1.60461077043304,2.15003701964786,7.5848687342762));
#383328=CARTESIAN_POINT('Ctrl Pts',(1.68595489728113,2.17370300710801,7.51098857897448));
#383329=CARTESIAN_POINT('Ctrl Pts',(1.68060655297094,2.17124216881354,7.50433767179956));
#383330=CARTESIAN_POINT('Ctrl Pts',(1.67534106310675,2.17805265099709,7.50214974420965));
#383331=CARTESIAN_POINT('Ctrl Pts',(1.65733749178292,2.16053579062865,7.53887321589164));
#383332=CARTESIAN_POINT('Ctrl Pts',(1.65205323012916,2.15810443754413,7.53220407452056));
#383333=CARTESIAN_POINT('Ctrl Pts',(1.64676090348175,2.16485678517878,7.53003438070911));
#383334=CARTESIAN_POINT('Ctrl Pts',(1.62866513030971,2.1473432882365,7.56669465659232));
#383335=CARTESIAN_POINT('Ctrl Pts',(1.62341209765988,2.1449263039967,7.56004085833299));
#383336=CARTESIAN_POINT('Ctrl Pts',(1.61812721696367,2.1516350062671,7.55785582193789));
#383337=CARTESIAN_POINT('Ctrl Pts',(1.59993910959752,2.13412609657559,7.59443891967696));
#383338=CARTESIAN_POINT('Ctrl Pts',(1.59467846070439,2.13170560800956,7.58783901202978));
#383339=CARTESIAN_POINT('Ctrl Pts',(1.58944145230862,2.13838789212886,7.58560008491213));
#383340=CARTESIAN_POINT('',(1.67379182682861,2.17733734542427,7.50366116523517));
#383341=CARTESIAN_POINT('Ctrl Pts',(1.67379182682884,2.17733734542457,7.50366116523554));
#383342=CARTESIAN_POINT('Ctrl Pts',(1.67447334484406,2.17700617973841,7.50350835821027));
#383343=CARTESIAN_POINT('Ctrl Pts',(1.67508905117998,2.17667958561866,7.50345484955999));
#383344=CARTESIAN_POINT('Ctrl Pts',(1.67565753267889,2.17634838364738,7.50349758195598));
#383345=CARTESIAN_POINT('Ctrl Pts',(1.67594920584752,2.17617845247354,7.50351950684424));
#383346=CARTESIAN_POINT('Ctrl Pts',(1.67625726095318,2.17599067105216,7.50357029184312));
#383347=CARTESIAN_POINT('Ctrl Pts',(1.67654933754674,2.17580143016233,7.50365515313924));
#383348=CARTESIAN_POINT('Ctrl Pts',(1.67699866962112,2.17551030104257,7.50378570417639));
#383349=CARTESIAN_POINT('Ctrl Pts',(1.67742356396048,2.17520746333167,7.50400001621911));
#383350=CARTESIAN_POINT('Ctrl Pts',(1.67779036218063,2.17491411851067,7.50428903009634));
#383351=CARTESIAN_POINT('Ctrl Pts',(1.6778310739611,2.1748815594924,7.50432110841318));
#383352=CARTESIAN_POINT('Ctrl Pts',(1.6778711002776,2.17484911527092,7.50435406373354));
#383353=CARTESIAN_POINT('Ctrl Pts',(1.67791041740551,2.17481681294647,7.50438785222352));
#383354=CARTESIAN_POINT('Ctrl Pts',(1.6781504673696,2.17461959172923,7.50459414719561));
#383355=CARTESIAN_POINT('Ctrl Pts',(1.67836757542203,2.17442412152687,7.50483629897752));
#383356=CARTESIAN_POINT('Ctrl Pts',(1.67855430477745,2.17423886878032,7.5050991045531));
#383357=CARTESIAN_POINT('Ctrl Pts',(1.6789662484907,2.17383018261457,7.50567888004914));
#383358=CARTESIAN_POINT('Ctrl Pts',(1.67924694212402,2.17345548835242,7.50637912803144));
#383359=CARTESIAN_POINT('Ctrl Pts',(1.67942510411653,2.17312621707483,7.50710440483569));
#383360=CARTESIAN_POINT('Ctrl Pts',(1.6794687929741,2.17304547322062,7.50728225710685));
#383361=CARTESIAN_POINT('Ctrl Pts',(1.67950731439497,2.17296592286683,7.50746498566954));
#383362=CARTESIAN_POINT('Ctrl Pts',(1.67954014411054,2.17288960453984,7.50764697238949));
#383363=CARTESIAN_POINT('Ctrl Pts',(1.67971662762646,2.17247933821732,7.50862528291182));
#383364=CARTESIAN_POINT('Ctrl Pts',(1.67974845277417,2.1721268649131,7.50965856837423));
#383365=CARTESIAN_POINT('Ctrl Pts',(1.67970082222059,2.17182018429101,7.51067959873204));
#383366=CARTESIAN_POINT('Ctrl Pts',(1.67967461106688,2.17165141755786,7.5112414730258));
#383367=CARTESIAN_POINT('Ctrl Pts',(1.67962390256752,2.17149654377222,7.51180065547253));
#383368=CARTESIAN_POINT('Ctrl Pts',(1.67955689582719,2.1713540776066,7.51235175716501));
#383369=CARTESIAN_POINT('Ctrl Pts',(1.67932536084705,2.17086180025259,7.51425603304536));
#383370=CARTESIAN_POINT('Ctrl Pts',(1.67886613445119,2.1704615533975,7.5162690050518));
#383371=CARTESIAN_POINT('Ctrl Pts',(1.67823955795076,2.17015459940593,7.51827788969243));
#383372=CARTESIAN_POINT('Ctrl Pts',(1.67820564644649,2.17013798647584,7.51838661432545));
#383373=CARTESIAN_POINT('Ctrl Pts',(1.67817123513466,2.1701216494447,7.51849533314856));
#383374=CARTESIAN_POINT('Ctrl Pts',(1.67813633056178,2.17010558942601,7.51860402984325));
#383375=CARTESIAN_POINT('Ctrl Pts',(1.59932759229262,2.14295327045313,7.57603338728985));
#383376=CARTESIAN_POINT('Ctrl Pts',(1.62419032049748,2.15443464751878,7.55196141284922));
#383377=CARTESIAN_POINT('Ctrl Pts',(1.64901056800951,2.16589544849306,7.52783573083105));
#383378=CARTESIAN_POINT('Ctrl Pts',(1.67379182688439,2.17733734544404,7.50366116530176));
#383379=CARTESIAN_POINT('Origin',(5.52641612598452E-16,7.40489414195308E-16,
7.49482233047033));
#383380=CARTESIAN_POINT('Origin',(1.60591818370368,2.21696482544263,7.49482233047033));
#383381=CARTESIAN_POINT('Origin',(0.,0.,7.50366116523517));
#383382=CARTESIAN_POINT('Origin',(1.66840488432873,2.17032978875286,7.49482233047033));
#383383=CARTESIAN_POINT('Ctrl Pts',(1.60293423561746,2.22622921225625,7.51860402984325));
#383384=CARTESIAN_POINT('Ctrl Pts',(1.60401712365771,2.23376072203333,7.51860402984325));
#383385=CARTESIAN_POINT('Ctrl Pts',(1.59782431009108,2.23818173392644,7.51860402984325));
#383386=CARTESIAN_POINT('Ctrl Pts',(1.60333631807902,2.22902571341502,7.51041458714365));
#383387=CARTESIAN_POINT('Ctrl Pts',(1.60254996944052,2.23480810233128,7.5100464290044));
#383388=CARTESIAN_POINT('Ctrl Pts',(1.59782260218663,2.23818295318903,7.50729136483009));
#383389=CARTESIAN_POINT('Ctrl Pts',(1.60608974108079,2.22961086209063,7.50215815450138));
#383390=CARTESIAN_POINT('Ctrl Pts',(1.60553732340033,2.23267564580042,7.49877163671533));
#383391=CARTESIAN_POINT('Ctrl Pts',(1.6027431827603,2.23469967684714,7.49481588533172));
#383392=CARTESIAN_POINT('Ctrl Pts',(1.61110304631034,2.22412251139393,7.50366171572174));
#383393=CARTESIAN_POINT('Ctrl Pts',(1.61325114344693,2.22708795249922,7.50000045605858));
#383394=CARTESIAN_POINT('Ctrl Pts',(1.61325114344683,2.2270879524993,7.49482233047317));
#383395=CARTESIAN_POINT('Origin',(1.59056147231794,2.22800818059041,7.51860402984325));
#383396=CARTESIAN_POINT('Origin',(1.59056147231794,2.22800818059041,9.));
#383397=CARTESIAN_POINT('Origin',(1.59056147231794,2.22800818059041,8.75721825406948));
#383398=CARTESIAN_POINT('Ctrl Pts',(1.60055903033134,2.20969989122328,8.78942910404912));
#383399=CARTESIAN_POINT('Ctrl Pts',(1.60137162134951,2.21521279649536,8.79672699501691));
#383400=CARTESIAN_POINT('Ctrl Pts',(1.592930233175,2.21811390863888,8.79893251111267));
#383401=CARTESIAN_POINT('Ctrl Pts',(1.60212279997728,2.22058244805681,8.78111911759583));
#383402=CARTESIAN_POINT('Ctrl Pts',(1.60307877177669,2.22711914661526,8.78644465894814));
#383403=CARTESIAN_POINT('Ctrl Pts',(1.59615583745411,2.2313367872046,8.78817647674132));
#383404=CARTESIAN_POINT('Ctrl Pts',(1.60309737848857,2.22736471705347,8.76780923932029));
#383405=CARTESIAN_POINT('Ctrl Pts',(1.60422082067878,2.23508175109614,8.76988516158372));
#383406=CARTESIAN_POINT('Ctrl Pts',(1.59815964019983,2.23959821781225,8.77093053738833));
#383407=CARTESIAN_POINT('Ctrl Pts',(1.60290734901519,2.22604226742124,8.75371302330492));
#383408=CARTESIAN_POINT('Ctrl Pts',(1.60400397276683,2.23356979143084,8.75300828287559));
#383409=CARTESIAN_POINT('Ctrl Pts',(1.59776837262213,2.23798701116386,8.75267964240738));
#383410=CARTESIAN_POINT('Origin',(1.58856698858097,2.21412816559727,8.78727029226991));
#383411=CARTESIAN_POINT('Ctrl Pts',(1.59077126558564,2.14158464790053,8.85049129520029));
#383412=CARTESIAN_POINT('Ctrl Pts',(1.59160185579968,2.14736489288837,8.85711686593484));
#383413=CARTESIAN_POINT('Ctrl Pts',(1.58363955683344,2.15047978570935,8.85933012996512));
#383414=CARTESIAN_POINT('Ctrl Pts',(1.59416574276814,2.16520749992665,8.82945683644721));
#383415=CARTESIAN_POINT('Ctrl Pts',(1.59500322738313,2.17103572444269,8.83607469902388));
#383416=CARTESIAN_POINT('Ctrl Pts',(1.58700388846101,2.17412483747177,8.83829567148519));
#383417=CARTESIAN_POINT('Ctrl Pts',(1.59755516020867,2.18879514018688,8.80838214965002));
#383418=CARTESIAN_POINT('Ctrl Pts',(1.59839594992895,2.19464636559807,8.81501364461995));
#383419=CARTESIAN_POINT('Ctrl Pts',(1.59036377844284,2.19773392674117,8.81722098428721));
#383420=CARTESIAN_POINT('Ctrl Pts',(1.60093990236827,2.21235024422327,8.78727029226991));
#383421=CARTESIAN_POINT('Ctrl Pts',(1.6017808317465,2.21820244154216,8.79393457792714));
#383422=CARTESIAN_POINT('Ctrl Pts',(1.59371958050512,2.22130979469261,8.79610912703474));
#383423=CARTESIAN_POINT('Origin',(1.57839835179835,2.14336256927453,8.85049129520029));
#383424=CARTESIAN_POINT('Ctrl Pts',(1.60045004741994,2.13436118528465,8.85049129520029));
#383425=CARTESIAN_POINT('Ctrl Pts',(1.60575505664338,2.13680208457842,8.85711686593484));
#383426=CARTESIAN_POINT('Ctrl Pts',(1.61100669796541,2.13005515746019,8.85933012996512));
#383427=CARTESIAN_POINT('Ctrl Pts',(1.59575678233858,2.13220175691421,8.86332496987232));
#383428=CARTESIAN_POINT('Ctrl Pts',(1.59962188022982,2.12966938398193,8.86648636486737));
#383429=CARTESIAN_POINT('Ctrl Pts',(1.59786993626266,2.12402963272603,8.87206031107457));
#383430=CARTESIAN_POINT('Ctrl Pts',(1.59003146113941,2.13643619939961,8.86341338519876));
#383431=CARTESIAN_POINT('Ctrl Pts',(1.58647494928256,2.13940683805928,8.86654584966057));
#383432=CARTESIAN_POINT('Ctrl Pts',(1.58158264810683,2.13606176078166,8.87215952290715));
#383433=CARTESIAN_POINT('Ctrl Pts',(1.59077126558564,2.14158464790053,8.85049129520029));
#383434=CARTESIAN_POINT('Ctrl Pts',(1.59160185579968,2.14736489288837,8.85711686593484));
#383435=CARTESIAN_POINT('Ctrl Pts',(1.58363955683344,2.15047978570935,8.85933012996512));
#383436=CARTESIAN_POINT('Origin',(1.60567491878591,2.12300553826614,8.85049129520029));
#383437=CARTESIAN_POINT('Ctrl Pts',(1.66539749203243,2.16424429481557,8.78727029226991));
#383438=CARTESIAN_POINT('Ctrl Pts',(1.67076853786517,2.16671557835679,8.79393457792714));
#383439=CARTESIAN_POINT('Ctrl Pts',(1.67604110579947,2.15987164362914,8.79610912703474));
#383440=CARTESIAN_POINT('Ctrl Pts',(1.64377902353585,2.15429737441203,8.80838214965001));
#383441=CARTESIAN_POINT('Ctrl Pts',(1.64914917736843,2.15676824753312,8.81501364461993));
#383442=CARTESIAN_POINT('Ctrl Pts',(1.65439449734899,2.14994655925992,8.81722098428721));
#383443=CARTESIAN_POINT('Ctrl Pts',(1.62213069385382,2.14433671451371,8.82945683644722));
#383444=CARTESIAN_POINT('Ctrl Pts',(1.6274797378613,2.1467978747474,8.8360746990239));
#383445=CARTESIAN_POINT('Ctrl Pts',(1.63271720381481,2.1400081035522,8.8382956714852));
#383446=CARTESIAN_POINT('Ctrl Pts',(1.60045004741994,2.13436118528465,8.85049129520029));
#383447=CARTESIAN_POINT('Ctrl Pts',(1.60575505664338,2.13680208457842,8.85711686593484));
#383448=CARTESIAN_POINT('Ctrl Pts',(1.61100669796541,2.13005515746019,8.85933012996512));
#383449=CARTESIAN_POINT('Origin',(1.6706223633984,2.15288864779706,8.78727029226991));
#383450=CARTESIAN_POINT('Ctrl Pts',(1.67796812831783,2.17002817722088,8.75374538247848));
#383451=CARTESIAN_POINT('Ctrl Pts',(1.68486593258895,2.17321638590681,8.75304829418601));
#383452=CARTESIAN_POINT('Ctrl Pts',(1.69087189191036,2.16850479426082,8.75272238421917));
#383453=CARTESIAN_POINT('Ctrl Pts',(1.67916726963829,2.17057991720283,8.76769408445022));
#383454=CARTESIAN_POINT('Ctrl Pts',(1.6862389428103,2.1738477289355,8.76974318093972));
#383455=CARTESIAN_POINT('Ctrl Pts',(1.69228901876996,2.16932943963945,8.7707786988043));
#383456=CARTESIAN_POINT('Ctrl Pts',(1.67302115432923,2.16775201237431,8.78108014887987));
#383457=CARTESIAN_POINT('Ctrl Pts',(1.67901254883373,2.17052481406067,8.78639403366322));
#383458=CARTESIAN_POINT('Ctrl Pts',(1.68503003222545,2.1651107611094,8.78812224174741));
#383459=CARTESIAN_POINT('Ctrl Pts',(1.66294902812127,2.16311770059482,8.78944554828685));
#383460=CARTESIAN_POINT('Ctrl Pts',(1.66799600222723,2.16545959512505,8.79673892988687));
#383461=CARTESIAN_POINT('Ctrl Pts',(1.673175597004,2.15820181638323,8.79894799272499));
#383462=CARTESIAN_POINT('Origin',(1.68336120192775,2.1587499424075,8.75721825406948));
#383463=CARTESIAN_POINT('Origin',(1.68336120192775,2.1587499424075,9.));
#383464=CARTESIAN_POINT('Origin',(1.68336120192775,2.1587499424075,7.51860402984325));
#383465=CARTESIAN_POINT('Ctrl Pts',(1.67379134738622,2.17733672174578,7.50366195182966));
#383466=CARTESIAN_POINT('Ctrl Pts',(1.67602317147189,2.18023997043658,7.50000065167735));
#383467=CARTESIAN_POINT('Ctrl Pts',(1.67602317147199,2.18023997043651,7.49482233047108));
#383468=CARTESIAN_POINT('Ctrl Pts',(1.68048485024187,2.1740885193001,7.50215800491337));
#383469=CARTESIAN_POINT('Ctrl Pts',(1.68358134484128,2.17442972066327,7.49877273257265));
#383470=CARTESIAN_POINT('Ctrl Pts',(1.68631825291817,2.17232579801056,7.49481816995649));
#383471=CARTESIAN_POINT('Ctrl Pts',(1.68069673761558,2.17128403715843,7.51043025814042));
#383472=CARTESIAN_POINT('Ctrl Pts',(1.68646654642245,2.17217961703705,7.51006209594514));
#383473=CARTESIAN_POINT('Ctrl Pts',(1.69104977934847,2.16860569116931,7.50731281821698));
#383474=CARTESIAN_POINT('Ctrl Pts',(1.67813495755922,2.17010495759025,7.51860402984325));
#383475=CARTESIAN_POINT('Ctrl Pts',(1.68504722930856,2.17328639070348,7.51860402984324));
#383476=CARTESIAN_POINT('Ctrl Pts',(1.69104778275847,2.16860724808059,7.51860402984325));
#383477=CARTESIAN_POINT('Origin',(0.,0.,7.5));
#383478=CARTESIAN_POINT('Origin',(1.73391074180927,2.02743472471363,7.5));
#383479=CARTESIAN_POINT('',(1.73391074180927,2.02743472471363,7.59394543036555));
#383480=CARTESIAN_POINT('',(1.73391074180927,2.02743472471363,8.85049129520029));
#383481=CARTESIAN_POINT('',(1.73391074180927,2.02743472471363,7.5));
#383482=CARTESIAN_POINT('',(1.80063936233257,2.05309523912755,8.78727029226991));
#383483=CARTESIAN_POINT('Ctrl Pts',(1.73391074180927,2.02743472471362,8.85049129520029));
#383484=CARTESIAN_POINT('Ctrl Pts',(1.75618594748779,2.03600066286586,8.82945686509571));
#383485=CARTESIAN_POINT('Ctrl Pts',(1.77842803837959,2.04455386671526,8.80838212259896));
#383486=CARTESIAN_POINT('Ctrl Pts',(1.80063936233257,2.05309523912756,8.78727029226991));
#383487=CARTESIAN_POINT('',(1.81372756198698,2.05812831089272,8.75721825406948));
#383488=CARTESIAN_POINT('Origin',(1.77434055646696,2.04298224032222,8.75937679713133));
#383489=CARTESIAN_POINT('',(1.81372756198698,2.05812831089272,7.51860402984325));
#383490=CARTESIAN_POINT('',(1.81372756198698,2.05812831089272,7.5));
#383491=CARTESIAN_POINT('Ctrl Pts',(1.81372756198698,2.05812831089272,7.51860402984325));
#383492=CARTESIAN_POINT('Ctrl Pts',(1.80344881675852,2.05417561581191,7.52834476460825));
#383493=CARTESIAN_POINT('Ctrl Pts',(1.79316339871698,2.0502203546985,7.53807742314407));
#383494=CARTESIAN_POINT('Ctrl Pts',(1.78287108381379,2.04626244139451,7.54780169004674));
#383495=CARTESIAN_POINT('Ctrl Pts',(1.76656861325928,2.03999332062795,7.5632044032688));
#383496=CARTESIAN_POINT('Ctrl Pts',(1.75024881863924,2.0337175378859,7.57858609112103));
#383497=CARTESIAN_POINT('Ctrl Pts',(1.73391074180927,2.02743472471363,7.59394543036555));
#383498=CARTESIAN_POINT('Origin',(1.78118873745324,2.3044022385307,7.5));
#383499=CARTESIAN_POINT('',(1.74227604793053,2.118955871654,8.75721825406948));
#383500=CARTESIAN_POINT('',(1.73939636646036,2.10523216165206,8.78727029226991));
#383501=CARTESIAN_POINT('Origin',(1.7320866608215,2.07039626697888,8.75658640621061));
#383502=CARTESIAN_POINT('',(1.72471465490912,2.03526346763212,8.85049129520029));
#383503=CARTESIAN_POINT('Ctrl Pts',(1.73939636646036,2.10523216165206,8.78727029226991));
#383504=CARTESIAN_POINT('Ctrl Pts',(1.73450940418103,2.0819423451197,8.80838212259894));
#383505=CARTESIAN_POINT('Ctrl Pts',(1.72961567252273,2.05862026772972,8.82945686509571));
#383506=CARTESIAN_POINT('Ctrl Pts',(1.72471465490912,2.03526346763212,8.85049129520029));
#383507=CARTESIAN_POINT('',(1.72471465490912,2.03526346763212,7.59394543036555));
#383508=CARTESIAN_POINT('',(1.72471465490912,2.03526346763212,7.5));
#383509=CARTESIAN_POINT('',(1.74227604793053,2.118955871654,7.51860402984325));
#383510=CARTESIAN_POINT('Ctrl Pts',(1.72471465490912,2.03526346763212,7.59394543036555));
#383511=CARTESIAN_POINT('Ctrl Pts',(1.72830937827427,2.05239485577749,7.57858609112103));
#383512=CARTESIAN_POINT('Ctrl Pts',(1.73190007916553,2.06950707400214,7.56320440326857));
#383513=CARTESIAN_POINT('Ctrl Pts',(1.73548696839501,2.08660112697449,7.54780169004651));
#383514=CARTESIAN_POINT('Ctrl Pts',(1.73775149593084,2.09739319530396,7.53807742314383));
#383515=CARTESIAN_POINT('Ctrl Pts',(1.74001450601089,2.10817803188811,7.52834476460825));
#383516=CARTESIAN_POINT('Ctrl Pts',(1.74227604793053,2.118955871654,7.51860402984325));
#383517=CARTESIAN_POINT('',(1.74227604793053,2.118955871654,7.5));
#383518=CARTESIAN_POINT('Origin',(1.73144312418159,2.03385161556851,7.5));
#383519=CARTESIAN_POINT('Ctrl Pts',(1.72471465490912,2.03526346763211,8.85049129520029));
#383520=CARTESIAN_POINT('Ctrl Pts',(1.72467488452414,2.0350739337424,8.85097269580138));
#383521=CARTESIAN_POINT('Ctrl Pts',(1.72464384805149,2.03488506380328,8.85143669361005));
#383522=CARTESIAN_POINT('Ctrl Pts',(1.72462097907696,2.03468801919692,8.8519052845931));
#383523=CARTESIAN_POINT('Ctrl Pts',(1.72457624881307,2.034302612443,8.85282181883899));
#383524=CARTESIAN_POINT('Ctrl Pts',(1.72456411104286,2.03389582367072,8.85372622499635));
#383525=CARTESIAN_POINT('Ctrl Pts',(1.72459978718337,2.03346080980622,8.85462257735071));
#383526=CARTESIAN_POINT('Ctrl Pts',(1.72462940424812,2.03309967674615,8.85536669723986));
#383527=CARTESIAN_POINT('Ctrl Pts',(1.72469194862655,2.0327190067839,8.85610498449051));
#383528=CARTESIAN_POINT('Ctrl Pts',(1.72480403100062,2.0323161498766,8.85681338218371));
#383529=CARTESIAN_POINT('Ctrl Pts',(1.72490574593111,2.03195055660052,8.85745625420285));
#383530=CARTESIAN_POINT('Ctrl Pts',(1.72504895764682,2.03156194465407,8.85808743050666));
#383531=CARTESIAN_POINT('Ctrl Pts',(1.72526213979697,2.03114764993346,8.85866804508411));
#383532=CARTESIAN_POINT('Ctrl Pts',(1.72536049741983,2.03095650333018,8.85893592806396));
#383533=CARTESIAN_POINT('Ctrl Pts',(1.72547399192869,2.03075989601329,8.85919241173849));
#383534=CARTESIAN_POINT('Ctrl Pts',(1.72560699390351,2.03055783073551,8.85943017985534));
#383535=CARTESIAN_POINT('Ctrl Pts',(1.72578658594231,2.03028498279279,8.8597512372));
#383536=CARTESIAN_POINT('Ctrl Pts',(1.72600685206649,2.02999559083907,8.86004599534705));
#383537=CARTESIAN_POINT('Ctrl Pts',(1.7262734334341,2.02969943976519,8.86026130871721));
#383538=CARTESIAN_POINT('Ctrl Pts',(1.7263710363885,2.02959101050767,8.86034014101235));
#383539=CARTESIAN_POINT('Ctrl Pts',(1.72647630483695,2.02948003821963,8.86040910639692));
#383540=CARTESIAN_POINT('Ctrl Pts',(1.7265866148444,2.02936977777994,8.86046313645507));
#383541=CARTESIAN_POINT('Ctrl Pts',(1.72675875268719,2.02919771728723,8.8605474499083));
#383542=CARTESIAN_POINT('Ctrl Pts',(1.72694797019715,2.02902279750388,8.86059655985668));
#383543=CARTESIAN_POINT('Ctrl Pts',(1.72714193341413,2.02885602144796,8.86059725258816));
#383544=CARTESIAN_POINT('Ctrl Pts',(1.72733634476362,2.02868886007272,8.86059794692011));
#383545=CARTESIAN_POINT('Ctrl Pts',(1.72753941194329,2.02853004075074,8.86056369958366));
#383546=CARTESIAN_POINT('Ctrl Pts',(1.72773774127271,2.02838526137767,8.86048590497774));
#383547=CARTESIAN_POINT('Ctrl Pts',(1.72778949932271,2.0283474782719,8.86046560290182));
#383548=CARTESIAN_POINT('Ctrl Pts',(1.72784166144809,2.02831023298625,8.86044257503091));
#383549=CARTESIAN_POINT('Ctrl Pts',(1.72789259672069,2.02827464971589,8.86041778462583));
#383550=CARTESIAN_POINT('Ctrl Pts',(1.72823532789991,2.02803521846153,8.86025097596201));
#383551=CARTESIAN_POINT('Ctrl Pts',(1.72856869189649,2.02783918051111,8.8599848982295));
#383552=CARTESIAN_POINT('Ctrl Pts',(1.72887866392137,2.02768495440918,8.85968173251461));
#383553=CARTESIAN_POINT('Ctrl Pts',(1.72904262136326,2.02760337763736,8.85952137522076));
#383554=CARTESIAN_POINT('Ctrl Pts',(1.72920310952447,2.02753175558217,8.85934740853961));
#383555=CARTESIAN_POINT('Ctrl Pts',(1.72935723163293,2.02746967867185,8.8591675900182));
#383556=CARTESIAN_POINT('Ctrl Pts',(1.72997611200948,2.02722040760997,8.85844552518695));
#383557=CARTESIAN_POINT('Ctrl Pts',(1.7305261907919,2.02710815126501,8.85759444184122));
#383558=CARTESIAN_POINT('Ctrl Pts',(1.73098291656963,2.02705690851458,8.85683498915136));
#383559=CARTESIAN_POINT('Ctrl Pts',(1.7310307117059,2.02705154609722,8.85675551444996));
#383560=CARTESIAN_POINT('Ctrl Pts',(1.73107748282562,2.0270468717397,8.8566769979365));
#383561=CARTESIAN_POINT('Ctrl Pts',(1.73112319999986,2.0270428113559,8.85659965593547));
#383562=CARTESIAN_POINT('Ctrl Pts',(1.73174029275056,2.02698800408814,8.85555568965886));
#383563=CARTESIAN_POINT('Ctrl Pts',(1.73234127237002,2.02702445131195,8.85434650606346));
#383564=CARTESIAN_POINT('Ctrl Pts',(1.73292948597223,2.02714612986163,8.85297329937117));
#383565=CARTESIAN_POINT('Ctrl Pts',(1.73326032028309,2.02721456663184,8.85220095427747));
#383566=CARTESIAN_POINT('Ctrl Pts',(1.73358718755085,2.02731030181013,8.85137579139183));
#383567=CARTESIAN_POINT('Ctrl Pts',(1.73391074180927,2.02743472471362,8.85049129520029));
#383568=CARTESIAN_POINT('Origin',(1.73144312418159,2.03385161556851,7.59394543036555));
#383569=CARTESIAN_POINT('Ctrl Pts',(1.7245991880651,2.03471318681161,7.59443877723642));
#383570=CARTESIAN_POINT('Ctrl Pts',(1.72340999067088,2.02904582382638,7.58783886950016));
#383571=CARTESIAN_POINT('Ctrl Pts',(1.73109008020603,2.02542706626767,7.58559994247159));
#383572=CARTESIAN_POINT('Ctrl Pts',(1.73109098175055,2.06565115507456,7.56670252222133));
#383573=CARTESIAN_POINT('Ctrl Pts',(1.72990350308422,2.05999198303783,7.56004874999025));
#383574=CARTESIAN_POINT('Ctrl Pts',(1.73761999295571,2.05633245556569,7.55786368756704));
#383575=CARTESIAN_POINT('Ctrl Pts',(1.73757065265992,2.09653134977293,7.53888913333561));
#383576=CARTESIAN_POINT('Ctrl Pts',(1.73637611674972,2.09083854499971,7.53222002137279));
#383577=CARTESIAN_POINT('Ctrl Pts',(1.7441368019062,2.08718146821334,7.53005029815327));
#383578=CARTESIAN_POINT('Ctrl Pts',(1.74403790758368,2.12735237355687,7.51101258149734));
#383579=CARTESIAN_POINT('Ctrl Pts',(1.7428288917277,2.12159056164572,7.5043616886572));
#383580=CARTESIAN_POINT('Ctrl Pts',(1.75064026593579,2.11797256295503,7.50217374673251));
#383581=CARTESIAN_POINT('',(1.7502932317356,2.11632951079883,7.50366116523517));
#383582=CARTESIAN_POINT('Ctrl Pts',(1.74227604793053,2.118955871654,7.51860402984325));
#383583=CARTESIAN_POINT('Ctrl Pts',(1.74236673734232,2.11938807056234,7.51734760759493));
#383584=CARTESIAN_POINT('Ctrl Pts',(1.74250691691214,2.11976640579488,7.51608817408573));
#383585=CARTESIAN_POINT('Ctrl Pts',(1.74270878598764,2.12008536764089,7.51481005913119));
#383586=CARTESIAN_POINT('Ctrl Pts',(1.74289164382004,2.12037429090285,7.51365231206383));
#383587=CARTESIAN_POINT('Ctrl Pts',(1.74312516530044,2.12061503834427,7.51247773061042));
#383588=CARTESIAN_POINT('Ctrl Pts',(1.74343181434903,2.12077773502146,7.51129758471022));
#383589=CARTESIAN_POINT('Ctrl Pts',(1.7438129440958,2.12097994841054,7.50983079813402));
#383590=CARTESIAN_POINT('Ctrl Pts',(1.74430097953773,2.12104363261568,7.50839324291155));
#383591=CARTESIAN_POINT('Ctrl Pts',(1.74491014972063,2.12088750587554,7.50715379678855));
#383592=CARTESIAN_POINT('Ctrl Pts',(1.74519156879232,2.12081537982028,7.50658120839351));
#383593=CARTESIAN_POINT('Ctrl Pts',(1.74553648740115,2.12067688468441,7.50598221009429));
#383594=CARTESIAN_POINT('Ctrl Pts',(1.74592822130451,2.12045420802354,7.50545747549611));
#383595=CARTESIAN_POINT('Ctrl Pts',(1.74613726264064,2.12033538086481,7.50517746087247));
#383596=CARTESIAN_POINT('Ctrl Pts',(1.74636200201907,2.12019146954181,7.50491486231392));
#383597=CARTESIAN_POINT('Ctrl Pts',(1.74659558846566,2.12002488036819,7.50468370960992));
#383598=CARTESIAN_POINT('Ctrl Pts',(1.74694487388399,2.11977577700606,7.50433806340446));
#383599=CARTESIAN_POINT('Ctrl Pts',(1.74732409157993,2.11946804380052,7.50405484070983));
#383600=CARTESIAN_POINT('Ctrl Pts',(1.74770725053022,2.119121849733,7.5038576603613));
#383601=CARTESIAN_POINT('Ctrl Pts',(1.74774822342431,2.11908482965856,7.5038365749879));
#383602=CARTESIAN_POINT('Ctrl Pts',(1.74778923293593,2.11904739685899,7.50381643264937));
#383603=CARTESIAN_POINT('Ctrl Pts',(1.74783024145071,2.11900959576151,7.50379723213559));
#383604=CARTESIAN_POINT('Ctrl Pts',(1.74810398670169,2.1187572610702,7.50366906242519));
#383605=CARTESIAN_POINT('Ctrl Pts',(1.74838315477832,2.11848249746139,7.50358235568538));
#383606=CARTESIAN_POINT('Ctrl Pts',(1.7486458722785,2.11821119094114,7.5035341175365));
#383607=CARTESIAN_POINT('Ctrl Pts',(1.74903978743615,2.11780439751998,7.50346178989176));
#383608=CARTESIAN_POINT('Ctrl Pts',(1.74944625412043,2.11735003155157,7.50346967198527));
#383609=CARTESIAN_POINT('Ctrl Pts',(1.74983155360462,2.11689170695291,7.50354272648692));
#383610=CARTESIAN_POINT('Ctrl Pts',(1.74999003525769,2.11670318855872,7.50357277531559));
#383611=CARTESIAN_POINT('Ctrl Pts',(1.75014483371269,2.11651434214922,7.50361331098761));
#383612=CARTESIAN_POINT('Ctrl Pts',(1.7502932317365,2.11632951079992,7.50366116523659));
#383613=CARTESIAN_POINT('',(1.73334108842444,2.03608107236508,7.57603338622103));
#383614=CARTESIAN_POINT('Origin',(1.73907161540509,2.04280807393504,7.58486873427629));
#383615=CARTESIAN_POINT('Ctrl Pts',(1.75029323174215,2.1163295108558,7.50366116529969));
#383616=CARTESIAN_POINT('Ctrl Pts',(1.74465255589963,2.08962350825639,7.5278357307971));
#383617=CARTESIAN_POINT('Ctrl Pts',(1.73900212579611,2.06287528805497,7.55196141284068));
#383618=CARTESIAN_POINT('Ctrl Pts',(1.73334108832669,2.03608107361332,7.57603338728831));
#383619=CARTESIAN_POINT('Ctrl Pts',(1.72471465490912,2.03526346763212,7.59394543036555));
#383620=CARTESIAN_POINT('Ctrl Pts',(1.72212056626995,2.02290080857694,7.59394543036555));
#383621=CARTESIAN_POINT('Ctrl Pts',(1.73391074180927,2.02743472471363,7.59394543036555));
#383622=CARTESIAN_POINT('Ctrl Pts',(1.72423552539132,2.03298007808928,7.58587155981959));
#383623=CARTESIAN_POINT('Ctrl Pts',(1.72591197114046,2.02735440847488,7.58685956158229));
#383624=CARTESIAN_POINT('Ctrl Pts',(1.7317330902689,2.0265973080504,7.58587155981959));
#383625=CARTESIAN_POINT('Ctrl Pts',(1.72943302451169,2.03442249532769,7.57982961904598));
#383626=CARTESIAN_POINT('Ctrl Pts',(1.72981032546514,2.03193363728709,7.58148017275035));
#383627=CARTESIAN_POINT('Ctrl Pts',(1.73232749797677,2.03195839414114,7.57982961904596));
#383628=CARTESIAN_POINT('Ctrl Pts',(1.73334108788783,2.03608107173507,7.57603338509286));
#383629=CARTESIAN_POINT('Ctrl Pts',(1.73334108788783,2.03608107173507,7.57603338509286));
#383630=CARTESIAN_POINT('Ctrl Pts',(1.73334108788783,2.03608107173507,7.57603338509286));
#383631=CARTESIAN_POINT('Origin',(1.73906727032654,2.04281177295477,7.58486873427624));
#383632=CARTESIAN_POINT('Ctrl Pts',(1.82176055196472,2.06121740000463,7.51098857897448));
#383633=CARTESIAN_POINT('Ctrl Pts',(1.81626552995066,2.05910428736284,7.50433767179956));
#383634=CARTESIAN_POINT('Ctrl Pts',(1.81144720769179,2.06623813777423,7.50214974420965));
#383635=CARTESIAN_POINT('Ctrl Pts',(1.79235831753899,2.04991076044927,7.53887321589168));
#383636=CARTESIAN_POINT('Ctrl Pts',(1.78692913564057,2.04782296664701,7.53220407452062));
#383637=CARTESIAN_POINT('Ctrl Pts',(1.78208030704416,2.05490052139172,7.53003438070912));
#383638=CARTESIAN_POINT('Ctrl Pts',(1.76289961997714,2.03858240797512,7.56669465659235));
#383639=CARTESIAN_POINT('Ctrl Pts',(1.75750252353437,2.03650695264608,7.56004085833302));
#383640=CARTESIAN_POINT('Ctrl Pts',(1.75265832922257,2.04354047463692,7.55785582193789));
#383641=CARTESIAN_POINT('Ctrl Pts',(1.7333857915781,2.02723285491821,7.59443891967696));
#383642=CARTESIAN_POINT('Ctrl Pts',(1.72798087001744,2.02515439043736,7.58783901202978));
#383643=CARTESIAN_POINT('Ctrl Pts',(1.72318275703058,2.03215848136722,7.58560008491213));
#383644=CARTESIAN_POINT('',(1.80985532470034,2.06562356178257,7.50366116523517));
#383645=CARTESIAN_POINT('Ctrl Pts',(1.80985532470058,2.06562356178285,7.50366116523554));
#383646=CARTESIAN_POINT('Ctrl Pts',(1.81051422460559,2.06524941150296,7.50350835821027));
#383647=CARTESIAN_POINT('Ctrl Pts',(1.81110774094971,2.06488403996546,7.50345484956));
#383648=CARTESIAN_POINT('Ctrl Pts',(1.81165383425925,2.06451709574947,7.50349758195598));
#383649=CARTESIAN_POINT('Ctrl Pts',(1.81193402062638,2.06432882615337,7.50351950684424));
#383650=CARTESIAN_POINT('Ctrl Pts',(1.81222941160282,2.06412169339068,7.50357029184312));
#383651=CARTESIAN_POINT('Ctrl Pts',(1.81250876338825,2.06391412790495,7.50365515313923));
#383652=CARTESIAN_POINT('Ctrl Pts',(1.81293851955495,2.06359480813634,7.50378570417639));
#383653=CARTESIAN_POINT('Ctrl Pts',(1.81334313802456,2.0632653695642,7.50400001621911));
#383654=CARTESIAN_POINT('Ctrl Pts',(1.81369038795123,2.06294912660894,7.50428903009634));
#383655=CARTESIAN_POINT('Ctrl Pts',(1.81372893002151,2.06291402607393,7.50432110841318));
#383656=CARTESIAN_POINT('Ctrl Pts',(1.81376679539123,2.06287908401769,7.50435406373354));
#383657=CARTESIAN_POINT('Ctrl Pts',(1.81380396212085,2.06284432900479,7.50438785222351));
#383658=CARTESIAN_POINT('Ctrl Pts',(1.81403088286978,2.0626321329457,7.50459414719561));
#383659=CARTESIAN_POINT('Ctrl Pts',(1.81423502103156,2.06242315419715,7.50483629897752));
#383660=CARTESIAN_POINT('Ctrl Pts',(1.81440949754727,2.06222631828136,7.50509910455309));
#383661=CARTESIAN_POINT('Ctrl Pts',(1.81479441026544,2.06179207848083,7.50567888004914));
#383662=CARTESIAN_POINT('Ctrl Pts',(1.81505052043979,2.0614001699654,7.50637912803144));
#383663=CARTESIAN_POINT('Ctrl Pts',(1.81520721989618,2.06106016033292,7.50710440483569));
#383664=CARTESIAN_POINT('Ctrl Pts',(1.81524564571381,2.06097678322089,7.50728225710685));
#383665=CARTESIAN_POINT('Ctrl Pts',(1.81527899117963,2.06089492823593,7.50746498566954));
#383666=CARTESIAN_POINT('Ctrl Pts',(1.81530686371103,2.06081666330603,7.50764697238949));
#383667=CARTESIAN_POINT('Ctrl Pts',(1.8154566987691,2.06039593258198,7.50862528291182));
#383668=CARTESIAN_POINT('Ctrl Pts',(1.81546587548649,2.06004214442775,7.50965856837422));
#383669=CARTESIAN_POINT('Ctrl Pts',(1.81539869370007,2.05973914561394,7.51067959873203));
#383670=CARTESIAN_POINT('Ctrl Pts',(1.81536172347827,2.05957240498452,7.51124147302579));
#383671=CARTESIAN_POINT('Ctrl Pts',(1.81530119636744,2.0594210983084,7.51180065547253));
#383672=CARTESIAN_POINT('Ctrl Pts',(1.81522519946108,2.05928321799139,7.51235175716501));
#383673=CARTESIAN_POINT('Ctrl Pts',(1.81496259987602,2.05880678657111,7.51425603304535));
#383674=CARTESIAN_POINT('Ctrl Pts',(1.81447867310599,2.05843678480232,7.51626900505178));
#383675=CARTESIAN_POINT('Ctrl Pts',(1.81383371736442,2.05817060637486,7.51827788969241));
#383676=CARTESIAN_POINT('Ctrl Pts',(1.81379881114089,2.05815620029535,7.51838661432543));
#383677=CARTESIAN_POINT('Ctrl Pts',(1.81376342381361,2.05814210157072,7.51849533314856));
#383678=CARTESIAN_POINT('Ctrl Pts',(1.81372756198698,2.05812831089272,7.51860402984325));
#383679=CARTESIAN_POINT('Ctrl Pts',(1.73334108967323,2.03608107246855,7.57603338728985));
#383680=CARTESIAN_POINT('Ctrl Pts',(1.75888834909077,2.04594589934822,7.55196141284923));
#383681=CARTESIAN_POINT('Ctrl Pts',(1.78439189678191,2.05579291415965,7.52783573083105));
#383682=CARTESIAN_POINT('Ctrl Pts',(1.80985532475727,2.06562356179872,7.50366116530176));
#383683=CARTESIAN_POINT('Origin',(5.98949470795624E-16,7.03560129586924E-16,
7.49482233047033));
#383684=CARTESIAN_POINT('Origin',(1.74466007661669,2.10951830213911,7.49482233047033));
#383685=CARTESIAN_POINT('Origin',(0.,0.,7.50366116523517));
#383686=CARTESIAN_POINT('Origin',(1.80403047455411,2.05897554547889,7.49482233047033));
#383687=CARTESIAN_POINT('Ctrl Pts',(1.74227583067298,2.1189548364867,7.51860402984325));
#383688=CARTESIAN_POINT('Ctrl Pts',(1.74383903929182,2.12640149109425,7.51860402984325));
#383689=CARTESIAN_POINT('Ctrl Pts',(1.73794220472936,2.13121019447179,7.51860402984325));
#383690=CARTESIAN_POINT('Ctrl Pts',(1.74285625945742,2.12171983042216,7.51041458714366));
#383691=CARTESIAN_POINT('Ctrl Pts',(1.74244200538641,2.12754072033047,7.51004642900443));
#383692=CARTESIAN_POINT('Ctrl Pts',(1.73794057845241,2.13121152065508,7.5072913648301));
#383693=CARTESIAN_POINT('Ctrl Pts',(1.7456415158607,2.12212736442965,7.50215815450137));
#383694=CARTESIAN_POINT('Ctrl Pts',(1.74528659454809,2.12522124473493,7.49877163671529));
#383695=CARTESIAN_POINT('Ctrl Pts',(1.74262787488407,2.12742013839824,7.49481588533169));
#383696=CARTESIAN_POINT('Ctrl Pts',(1.75029288088051,2.11632908656918,7.50366171572174));
#383697=CARTESIAN_POINT('Ctrl Pts',(1.7526265609851,2.1191508058016,7.50000045605858));
#383698=CARTESIAN_POINT('Ctrl Pts',(1.752626560985,2.11915080580168,7.49482233047317));
#383699=CARTESIAN_POINT('Origin',(1.73004246743514,2.121522875406,7.51860402984325));
#383700=CARTESIAN_POINT('Origin',(1.73004246743514,2.121522875406,9.));
#383701=CARTESIAN_POINT('Origin',(1.73004246743514,2.121522875406,8.75721825406948));
#383702=CARTESIAN_POINT('Ctrl Pts',(1.73884646826614,2.10261165664175,8.78942910404913));
#383703=CARTESIAN_POINT('Ctrl Pts',(1.74001060278244,2.10806117217339,8.79672699501691));
#383704=CARTESIAN_POINT('Ctrl Pts',(1.73177243323848,2.11149716526816,8.79893251111267));
#383705=CARTESIAN_POINT('Ctrl Pts',(1.74110427278991,2.11337166302988,8.78111911759576));
#383706=CARTESIAN_POINT('Ctrl Pts',(1.74247708815731,2.11983368191662,8.78644465894812));
#383707=CARTESIAN_POINT('Ctrl Pts',(1.73583860290615,2.12448621083598,8.78817647674132));
#383708=CARTESIAN_POINT('Ctrl Pts',(1.7425113903917,2.12007755566787,8.76780923932034));
#383709=CARTESIAN_POINT('Ctrl Pts',(1.74412695641817,2.1277067550482,8.76988516158375));
#383710=CARTESIAN_POINT('Ctrl Pts',(1.73836760030061,2.1326022833657,8.77093053738832));
#383711=CARTESIAN_POINT('Ctrl Pts',(1.74223702171541,2.11876999838043,8.75371302330491));
#383712=CARTESIAN_POINT('Ctrl Pts',(1.74381368245515,2.12621179535963,8.75300828287559));
#383713=CARTESIAN_POINT('Ctrl Pts',(1.7378739062597,2.13101945571394,8.75267964240738));
#383714=CARTESIAN_POINT('Origin',(1.72716278596497,2.10779916540406,8.78727029226991));
#383715=CARTESIAN_POINT('Ctrl Pts',(1.72471465490912,2.03526346763212,8.85049129520029));
#383716=CARTESIAN_POINT('Ctrl Pts',(1.72591388015439,2.04097862038897,8.85711686593484));
#383717=CARTESIAN_POINT('Ctrl Pts',(1.71816751245359,2.0445972595749,8.85933012996512));
#383718=CARTESIAN_POINT('Ctrl Pts',(1.72961567910008,2.05862029907541,8.82945683644722));
#383719=CARTESIAN_POINT('Ctrl Pts',(1.73082485863995,2.06438289105559,8.83607469902389));
#383720=CARTESIAN_POINT('Ctrl Pts',(1.72303987536886,2.06797817657509,8.8382956714852));
#383721=CARTESIAN_POINT('Ctrl Pts',(1.73450939791925,2.08194231527792,8.80838214965001));
#383722=CARTESIAN_POINT('Ctrl Pts',(1.73572334944616,2.08772764913661,8.81501364461993));
#383723=CARTESIAN_POINT('Ctrl Pts',(1.72790550163944,2.09132348954826,8.81722098428721));
#383724=CARTESIAN_POINT('Ctrl Pts',(1.73939636646036,2.10523216165206,8.78727029226991));
#383725=CARTESIAN_POINT('Ctrl Pts',(1.74061051962858,2.11101845647366,8.79393457792714));
#383726=CARTESIAN_POINT('Ctrl Pts',(1.73276491989236,2.11463591137415,8.79610912703474));
#383727=CARTESIAN_POINT('Origin',(1.71248107441373,2.03783047138412,8.85049129520029));
#383728=CARTESIAN_POINT('Ctrl Pts',(1.73391074180927,2.02743472471362,8.85049129520029));
#383729=CARTESIAN_POINT('Ctrl Pts',(1.739361240277,2.02953071581006,8.85711686593484));
#383730=CARTESIAN_POINT('Ctrl Pts',(1.74416981443404,2.02246117716244,8.85933012996512));
#383731=CARTESIAN_POINT('Ctrl Pts',(1.72908876449365,2.02558043164656,8.86332496987232));
#383732=CARTESIAN_POINT('Ctrl Pts',(1.73278367143587,2.02280562407395,8.86648636486738));
#383733=CARTESIAN_POINT('Ctrl Pts',(1.7306739869219,2.01728970772722,8.87206031107457));
#383734=CARTESIAN_POINT('Ctrl Pts',(1.72364650824246,2.03017299660443,8.86341338519876));
#383735=CARTESIAN_POINT('Ctrl Pts',(1.72028763309304,2.03336539826537,8.86654584966054));
#383736=CARTESIAN_POINT('Ctrl Pts',(1.71519106383777,2.03034064462034,8.87215952290714));
#383737=CARTESIAN_POINT('Ctrl Pts',(1.72471465490912,2.03526346763211,8.85049129520029));
#383738=CARTESIAN_POINT('Ctrl Pts',(1.72591388015439,2.04097862038897,8.85711686593484));
#383739=CARTESIAN_POINT('Ctrl Pts',(1.71816751245359,2.0445972595749,8.85933012996512));
#383740=CARTESIAN_POINT('Origin',(1.73839731931416,2.01576765043201,8.85049129520029));
#383741=CARTESIAN_POINT('Ctrl Pts',(1.80063936233257,2.05309523912756,8.78727029226991));
#383742=CARTESIAN_POINT('Ctrl Pts',(1.80615770845572,2.05521732106367,8.79393457792714));
#383743=CARTESIAN_POINT('Ctrl Pts',(1.81098095093019,2.04804963334651,8.79610912703474));
#383744=CARTESIAN_POINT('Ctrl Pts',(1.77842800991972,2.04455385577101,8.80838214965003));
#383745=CARTESIAN_POINT('Ctrl Pts',(1.78394543957967,2.04667558528085,8.81501364461987));
#383746=CARTESIAN_POINT('Ctrl Pts',(1.78874291541949,2.03953184409283,8.81722098428722));
#383747=CARTESIAN_POINT('Ctrl Pts',(1.75618597738195,2.03600067436167,8.82945683644723));
#383748=CARTESIAN_POINT('Ctrl Pts',(1.76168171828239,2.03811406345147,8.8360746990239));
#383749=CARTESIAN_POINT('Ctrl Pts',(1.7664734011663,2.0310026769736,8.83829567148519));
#383750=CARTESIAN_POINT('Ctrl Pts',(1.73391074180927,2.02743472471362,8.85049129520029));
#383751=CARTESIAN_POINT('Ctrl Pts',(1.739361240277,2.02953071581006,8.85711686593484));
#383752=CARTESIAN_POINT('Ctrl Pts',(1.74416981443404,2.02246117716244,8.85933012996512));
#383753=CARTESIAN_POINT('Origin',(1.80512593983745,2.04142816484594,8.78727029226991));
#383754=CARTESIAN_POINT('Ctrl Pts',(1.81355474551558,2.05806183449404,8.75374538247848));
#383755=CARTESIAN_POINT('Ctrl Pts',(1.82064264673988,2.06080154882625,8.75304829418602));
#383756=CARTESIAN_POINT('Ctrl Pts',(1.82633439346051,2.0557148345157,8.75272238421917));
#383757=CARTESIAN_POINT('Ctrl Pts',(1.81478677317359,2.05853561161883,8.7676940844502));
#383758=CARTESIAN_POINT('Ctrl Pts',(1.82205328625122,2.06134362562606,8.7697431809397));
#383759=CARTESIAN_POINT('Ctrl Pts',(1.82780144389181,2.05644698994232,8.77077869880429));
#383760=CARTESIAN_POINT('Ctrl Pts',(1.80847210123317,2.05610729998395,8.78108014887988));
#383761=CARTESIAN_POINT('Ctrl Pts',(1.81462883978908,2.05849053468798,8.78639403366325));
#383762=CARTESIAN_POINT('Ctrl Pts',(1.82028708005223,2.0527020640045,8.78812224174742));
#383763=CARTESIAN_POINT('Ctrl Pts',(1.79812374791355,2.05212783323686,8.78944554828686));
#383764=CARTESIAN_POINT('Ctrl Pts',(1.80331039816766,2.05414155535239,8.79673892988686));
#383765=CARTESIAN_POINT('Ctrl Pts',(1.80801434343089,2.04656683071865,8.79894799272499));
#383766=CARTESIAN_POINT('Origin',(1.81821413949186,2.04646123661111,8.75721825406948));
#383767=CARTESIAN_POINT('Origin',(1.81821413949186,2.04646123661111,9.));
#383768=CARTESIAN_POINT('Origin',(1.81821413949186,2.04646123661111,7.51860402984325));
#383769=CARTESIAN_POINT('Ctrl Pts',(1.8098548062838,2.06562297010347,7.50366195182966));
#383770=CARTESIAN_POINT('Ctrl Pts',(1.8122680566298,2.06837726029834,7.50000065167735));
#383771=CARTESIAN_POINT('Ctrl Pts',(1.81226805662989,2.06837726029826,7.49482233047108));
#383772=CARTESIAN_POINT('Ctrl Pts',(1.81632644357471,2.06195258723767,7.50215800491338));
#383773=CARTESIAN_POINT('Ctrl Pts',(1.81943843694025,2.06209469447589,7.49877273257267));
#383774=CARTESIAN_POINT('Ctrl Pts',(1.8220349229588,2.05981974025537,7.49481816995647));
#383775=CARTESIAN_POINT('Ctrl Pts',(1.81635821181535,2.05914029153471,7.5104302581404));
#383776=CARTESIAN_POINT('Ctrl Pts',(1.82217354593104,2.05966435842891,7.51006209594513));
#383777=CARTESIAN_POINT('Ctrl Pts',(1.82651837989692,2.05580412683338,7.50731281821699));
#383778=CARTESIAN_POINT('Ctrl Pts',(1.81372615132356,2.05812776832371,7.51860402984325));
#383779=CARTESIAN_POINT('Ctrl Pts',(1.82082805618866,2.06085979406985,7.51860402984324));
#383780=CARTESIAN_POINT('Ctrl Pts',(1.82651648716078,2.05580580846778,7.51860402984325));
#383781=CARTESIAN_POINT('Origin',(0.,0.,7.5));
#383782=CARTESIAN_POINT('Origin',(1.86024642503782,1.91217709997537,7.5));
#383783=CARTESIAN_POINT('',(1.86024642503782,1.91217709997537,7.59394543036555));
#383784=CARTESIAN_POINT('',(1.86024642503782,1.91217709997537,8.85049129520029));
#383785=CARTESIAN_POINT('',(1.86024642503782,1.91217709997537,7.5));
#383786=CARTESIAN_POINT('',(1.92848201925695,1.93350957471442,8.78727029226991));
#383787=CARTESIAN_POINT('Ctrl Pts',(1.86024642503782,1.91217709997537,8.85049129520029));
#383788=CARTESIAN_POINT('Ctrl Pts',(1.88302468545901,1.91929826116104,8.82945686509571));
#383789=CARTESIAN_POINT('Ctrl Pts',(1.9057690832418,1.92640883587954,8.80838212259897));
#383790=CARTESIAN_POINT('Ctrl Pts',(1.92848201925695,1.93350957471442,8.78727029226991));
#383791=CARTESIAN_POINT('',(1.94186579781664,1.93769374166284,8.75721825406948));
#383792=CARTESIAN_POINT('Origin',(1.90158930505073,1.92510232442688,8.75937679713145));
#383793=CARTESIAN_POINT('',(1.94186579781664,1.93769374166284,7.51860402984325));
#383794=CARTESIAN_POINT('',(1.94186579781664,1.93769374166284,7.5));
#383795=CARTESIAN_POINT('Ctrl Pts',(1.94186579781664,1.93769374166284,7.51860402984325));
#383796=CARTESIAN_POINT('Ctrl Pts',(1.9313549213293,1.93440772928591,7.52834476460825));
#383797=CARTESIAN_POINT('Ctrl Pts',(1.92083722133262,1.93111958367716,7.53807742314407));
#383798=CARTESIAN_POINT('Ctrl Pts',(1.91031246871818,1.9278292332105,7.54780169004674));
#383799=CARTESIAN_POINT('Ctrl Pts',(1.89364182939126,1.92261749589957,7.5632044032688));
#383800=CARTESIAN_POINT('Ctrl Pts',(1.87695347475873,1.91740022025759,7.57858609112103));
#383801=CARTESIAN_POINT('Ctrl Pts',(1.86024642503782,1.91217709997537,7.59394543036555));
#383802=CARTESIAN_POINT('Origin',(1.92517265250696,2.18554644274947,7.5));
#383803=CARTESIAN_POINT('',(1.87445832375783,2.00297423990034,8.75721825406948));
#383804=CARTESIAN_POINT('',(1.87070527778331,1.98946322855773,8.78727029226991));
#383805=CARTESIAN_POINT('Origin',(1.86117864728403,1.95516724241569,8.75658640621101));
#383806=CARTESIAN_POINT('',(1.85157082176544,1.92057895321256,8.85049129520029));
#383807=CARTESIAN_POINT('Ctrl Pts',(1.87070527778331,1.98946322855773,8.78727029226991));
#383808=CARTESIAN_POINT('Ctrl Pts',(1.86433617262357,1.96653437219954,8.80838212259895));
#383809=CARTESIAN_POINT('Ctrl Pts',(1.85795824503303,1.94357375498271,8.82945686509571));
#383810=CARTESIAN_POINT('Ctrl Pts',(1.85157082176544,1.92057895321256,8.85049129520029));
#383811=CARTESIAN_POINT('',(1.85157082176544,1.92057895321256,7.59394543036555));
#383812=CARTESIAN_POINT('',(1.85157082176544,1.92057895321256,7.5));
#383813=CARTESIAN_POINT('',(1.87445832375783,2.00297423990034,7.51860402984325));
#383814=CARTESIAN_POINT('Ctrl Pts',(1.85157082176544,1.92057895321256,7.59394543036555));
#383815=CARTESIAN_POINT('Ctrl Pts',(1.85625577119296,1.93744482836688,7.57858609112103));
#383816=CARTESIAN_POINT('Ctrl Pts',(1.86093547819014,1.95429183070791,7.56320440326857));
#383817=CARTESIAN_POINT('Ctrl Pts',(1.86561021750531,1.97112094933312,7.54780169004651));
#383818=CARTESIAN_POINT('Ctrl Pts',(1.86856154251836,1.98174575542339,7.53807742314383));
#383819=CARTESIAN_POINT('Ctrl Pts',(1.8715108898539,1.99236344185046,7.52834476460825));
#383820=CARTESIAN_POINT('Ctrl Pts',(1.87445832375783,2.00297423990034,7.51860402984325));
#383821=CARTESIAN_POINT('',(1.87445832375783,2.00297423990034,7.5));
#383822=CARTESIAN_POINT('Origin',(1.85819500900386,1.91873890744402,7.5));
#383823=CARTESIAN_POINT('Ctrl Pts',(1.85157082176544,1.92057895321256,8.85049129520029));
#383824=CARTESIAN_POINT('Ctrl Pts',(1.85151898961497,1.92039235683786,8.85097269580138));
#383825=CARTESIAN_POINT('Ctrl Pts',(1.85147591597154,1.92020586346591,8.85143669361005));
#383826=CARTESIAN_POINT('Ctrl Pts',(1.85144046929249,1.92001068892906,8.8519052845931));
#383827=CARTESIAN_POINT('Ctrl Pts',(1.85137113783622,1.91962893991249,8.85282181883899));
#383828=CARTESIAN_POINT('Ctrl Pts',(1.85133296195824,1.91922376460099,8.85372622499636));
#383829=CARTESIAN_POINT('Ctrl Pts',(1.85134069336429,1.91878735874096,8.85462257735071));
#383830=CARTESIAN_POINT('Ctrl Pts',(1.85134711170301,1.91842507009563,8.85536669723986));
#383831=CARTESIAN_POINT('Ctrl Pts',(1.85138513796909,1.91804117502856,8.85610498449051));
#383832=CARTESIAN_POINT('Ctrl Pts',(1.85147117892722,1.91763196469162,8.85681338218371));
#383833=CARTESIAN_POINT('Ctrl Pts',(1.85154926123186,1.91726060566817,8.85745625420284));
#383834=CARTESIAN_POINT('Ctrl Pts',(1.85166728025085,1.91686361656052,8.85808743050666));
#383835=CARTESIAN_POINT('Ctrl Pts',(1.85185348044152,1.91643651442559,8.8586680450841));
#383836=CARTESIAN_POINT('Ctrl Pts',(1.85193938917317,1.91623945875897,8.85893592806395));
#383837=CARTESIAN_POINT('Ctrl Pts',(1.85204005382135,1.91603598377475,8.85919241173848));
#383838=CARTESIAN_POINT('Ctrl Pts',(1.85215983616255,1.91582581219597,8.85943017985534));
#383839=CARTESIAN_POINT('Ctrl Pts',(1.85232157778254,1.91554201834717,8.8597512372));
#383840=CARTESIAN_POINT('Ctrl Pts',(1.85252284994021,1.91523910848123,8.86004599534705));
#383841=CARTESIAN_POINT('Ctrl Pts',(1.85276990912335,1.91492648595463,8.86026130871721));
#383842=CARTESIAN_POINT('Ctrl Pts',(1.85286036445564,1.91481202603389,8.86034014101235));
#383843=CARTESIAN_POINT('Ctrl Pts',(1.85295830659985,1.91469453717767,8.86040910639692));
#383844=CARTESIAN_POINT('Ctrl Pts',(1.85306132555294,1.91457743569343,8.86046313645506));
#383845=CARTESIAN_POINT('Ctrl Pts',(1.85322208576646,1.914394699808,8.86054744990829));
#383846=CARTESIAN_POINT('Ctrl Pts',(1.85339970735975,1.91420801620862,8.86059655985668));
#383847=CARTESIAN_POINT('Ctrl Pts',(1.8535825866799,1.91402915554602,8.86059725258816));
#383848=CARTESIAN_POINT('Ctrl Pts',(1.85376588852434,1.91384988164382,8.86059794692011));
#383849=CARTESIAN_POINT('Ctrl Pts',(1.85395836289181,1.91367837807429,8.86056369958366));
#383850=CARTESIAN_POINT('Ctrl Pts',(1.85414700868607,1.91352118916221,8.86048590497774));
#383851=CARTESIAN_POINT('Ctrl Pts',(1.85419623962171,1.91348016753623,8.86046560290182));
#383852=CARTESIAN_POINT('Ctrl Pts',(1.85424590826076,1.91343965673617,8.86044257503091));
#383853=CARTESIAN_POINT('Ctrl Pts',(1.85429445905343,1.91340088314134,8.86041778462583));
#383854=CARTESIAN_POINT('Ctrl Pts',(1.85462114564155,1.91313998496212,8.86025097596201));
#383855=CARTESIAN_POINT('Ctrl Pts',(1.85494126451143,1.91292299108811,8.8599848982295));
#383856=CARTESIAN_POINT('Ctrl Pts',(1.85524071836527,1.91274922188442,8.85968173251461));
#383857=CARTESIAN_POINT('Ctrl Pts',(1.85539911229729,1.91265730793145,8.85952137522076));
#383858=CARTESIAN_POINT('Ctrl Pts',(1.85555468187753,1.91257555051966,8.8593474085396));
#383859=CARTESIAN_POINT('Ctrl Pts',(1.85570451004429,1.91250372651562,8.8591675900182));
#383860=CARTESIAN_POINT('Ctrl Pts',(1.85630614801294,1.91221531580601,8.85844552518696));
#383861=CARTESIAN_POINT('Ctrl Pts',(1.85684790431078,1.91206804643516,8.85759444184128));
#383862=CARTESIAN_POINT('Ctrl Pts',(1.85730040856211,1.9119876464474,8.85683498915144));
#383863=CARTESIAN_POINT('Ctrl Pts',(1.8573477619269,1.9119792328028,8.85675551445002));
#383864=CARTESIAN_POINT('Ctrl Pts',(1.85739413746324,1.91197157141332,8.85667699793653));
#383865=CARTESIAN_POINT('Ctrl Pts',(1.85743950055697,1.9119645902626,8.85659965593547));
#383866=CARTESIAN_POINT('Ctrl Pts',(1.85805181391074,1.91187035833397,8.85555568965886));
#383867=CARTESIAN_POINT('Ctrl Pts',(1.85865389393476,1.91186822577663,8.85434650606346));
#383868=CARTESIAN_POINT('Ctrl Pts',(1.85924869496048,1.91195196734978,8.85297329937117));
#383869=CARTESIAN_POINT('Ctrl Pts',(1.85958323429569,1.91199906688223,8.85220095427747));
#383870=CARTESIAN_POINT('Ctrl Pts',(1.85991556375352,1.91207366290458,8.85137579139183));
#383871=CARTESIAN_POINT('Ctrl Pts',(1.86024642503782,1.91217709997537,8.85049129520029));
#383872=CARTESIAN_POINT('Origin',(1.85819500900386,1.91873890744402,7.59394543036555));
#383873=CARTESIAN_POINT('Ctrl Pts',(1.85142033554721,1.92003720098911,7.59443877723642));
#383874=CARTESIAN_POINT('Ctrl Pts',(1.84987047229341,1.91445767434761,7.58783886950016));
#383875=CARTESIAN_POINT('Ctrl Pts',(1.85730292766808,1.91035428688842,7.58559994247159));
#383876=CARTESIAN_POINT('Ctrl Pts',(1.85988099357867,1.95049567322872,7.56670252222138));
#383877=CARTESIAN_POINT('Ctrl Pts',(1.85833337031732,1.94492421058726,7.56004874999029));
#383878=CARTESIAN_POINT('Ctrl Pts',(1.86579953910258,1.94077780480322,7.55786368756704));
#383879=CARTESIAN_POINT('Ctrl Pts',(1.86832585217657,1.98089726731458,7.5388891333356));
#383880=CARTESIAN_POINT('Ctrl Pts',(1.86676903131436,1.97529269319786,7.53222002137279));
#383881=CARTESIAN_POINT('Ctrl Pts',(1.8742794615967,1.97114590146279,7.53005029815327));
#383882=CARTESIAN_POINT('Ctrl Pts',(1.87675452920535,2.01124060755398,7.51101258149734));
#383883=CARTESIAN_POINT('Ctrl Pts',(1.87517883684548,2.00556809581521,7.5043616886572));
#383884=CARTESIAN_POINT('Ctrl Pts',(1.88274235577549,2.001457054227,7.50217374673251));
#383885=CARTESIAN_POINT('',(1.88229076388119,1.99983961245521,7.50366116523517));
#383886=CARTESIAN_POINT('Ctrl Pts',(1.87445832375783,2.00297423990034,7.51860402984325));
#383887=CARTESIAN_POINT('Ctrl Pts',(1.87457651791763,2.00339974031911,7.51734760759494));
#383888=CARTESIAN_POINT('Ctrl Pts',(1.87474064949507,2.00376831688546,7.51608817408573));
#383889=CARTESIAN_POINT('Ctrl Pts',(1.87496253976454,2.00407368959408,7.5148100591312));
#383890=CARTESIAN_POINT('Ctrl Pts',(1.87516353327286,2.00435030349067,7.51365231206384));
#383891=CARTESIAN_POINT('Ctrl Pts',(1.87541199969986,2.00457559451803,7.51247773061043));
#383892=CARTESIAN_POINT('Ctrl Pts',(1.875728442717,2.00471830984544,7.51129758471022));
#383893=CARTESIAN_POINT('Ctrl Pts',(1.87612174524814,2.00489568869871,7.50983079813402));
#383894=CARTESIAN_POINT('Ctrl Pts',(1.87661285822995,2.0049279735197,7.50839324291155));
#383895=CARTESIAN_POINT('Ctrl Pts',(1.87721077373279,2.00473313789107,7.50715379678855));
#383896=CARTESIAN_POINT('Ctrl Pts',(1.87748699346659,2.00464312944469,7.50658120839351));
#383897=CARTESIAN_POINT('Ctrl Pts',(1.87782232998932,2.00448281985079,7.50598221009429));
#383898=CARTESIAN_POINT('Ctrl Pts',(1.87819899209072,2.00423550222564,7.50545747549611));
#383899=CARTESIAN_POINT('Ctrl Pts',(1.87839999064681,2.00410352588566,7.50517746087247));
#383900=CARTESIAN_POINT('Ctrl Pts',(1.87861504784395,2.0039455111425,7.50491486231392));
#383901=CARTESIAN_POINT('Ctrl Pts',(1.87883748095714,2.00376429830918,7.50468370960993));
#383902=CARTESIAN_POINT('Ctrl Pts',(1.8791700886239,2.00349332796303,7.50433806340447));
#383903=CARTESIAN_POINT('Ctrl Pts',(1.87952881064224,2.00316193046717,7.50405484070983));
#383904=CARTESIAN_POINT('Ctrl Pts',(1.87988900162131,2.00279189861427,7.50385766036131));
#383905=CARTESIAN_POINT('Ctrl Pts',(1.87992751844788,2.0027523294592,7.50383657498791));
#383906=CARTESIAN_POINT('Ctrl Pts',(1.87996604537337,2.0027123460809,7.50381643264937));
#383907=CARTESIAN_POINT('Ctrl Pts',(1.88000454770712,2.00267199522526,7.50379723213559));
#383908=CARTESIAN_POINT('Ctrl Pts',(1.88026156337995,2.00240264006419,7.50366906242519));
#383909=CARTESIAN_POINT('Ctrl Pts',(1.88052255371096,2.0021105546266,7.50358235568538));
#383910=CARTESIAN_POINT('Ctrl Pts',(1.88076734876143,2.00182297316666,7.5035341175365));
#383911=CARTESIAN_POINT('Ctrl Pts',(1.88113439123415,2.00139177731542,7.50346178989176));
#383912=CARTESIAN_POINT('Ctrl Pts',(1.8815109114615,2.00091230248074,7.50346967198527));
#383913=CARTESIAN_POINT('Ctrl Pts',(1.88186605434871,2.00043023333641,7.50354272648692));
#383914=CARTESIAN_POINT('Ctrl Pts',(1.88201213196924,2.0002319483191,7.50357277531559));
#383915=CARTESIAN_POINT('Ctrl Pts',(1.88215451294322,2.00003357194374,7.50361331098761));
#383916=CARTESIAN_POINT('Ctrl Pts',(1.88229076388216,1.99983961245625,7.50366116523659));
#383917=CARTESIAN_POINT('',(1.86023191546302,1.92084218059594,7.57603338622103));
#383918=CARTESIAN_POINT('Origin',(1.86638166893215,1.92718820469566,7.58486873427626));
#383919=CARTESIAN_POINT('Ctrl Pts',(1.88229076389138,1.99983961251165,7.50366116529968));
#383920=CARTESIAN_POINT('Ctrl Pts',(1.87495061796099,1.97354987960085,7.52783573079709));
#383921=CARTESIAN_POINT('Ctrl Pts',(1.86759803291971,1.9472186407863,7.55196141284068));
#383922=CARTESIAN_POINT('Ctrl Pts',(1.86023191544544,1.92084218184787,7.57603338728831));
#383923=CARTESIAN_POINT('Ctrl Pts',(1.85201547038342,1.92152278748126,7.59639677331371));
#383924=CARTESIAN_POINT('Ctrl Pts',(1.84404333085312,1.90412613787916,7.59974925422226));
#383925=CARTESIAN_POINT('Ctrl Pts',(1.86117552269004,1.91265177151733,7.59639677331372));
#383926=CARTESIAN_POINT('Ctrl Pts',(1.8498416060656,1.91828405037994,7.58707626057423));
#383927=CARTESIAN_POINT('Ctrl Pts',(1.85121197023113,1.91152834659309,7.58811717123965));
#383928=CARTESIAN_POINT('Ctrl Pts',(1.85800812538016,1.9103752174624,7.58707626057424));
#383929=CARTESIAN_POINT('Ctrl Pts',(1.85581853271803,1.91938039888898,7.58015376756929));
#383930=CARTESIAN_POINT('Ctrl Pts',(1.85602009788945,1.91649313315482,7.58208760766041));
#383931=CARTESIAN_POINT('Ctrl Pts',(1.85891234067495,1.91638421296597,7.5801537675693));
#383932=CARTESIAN_POINT('Ctrl Pts',(1.86023191488714,1.9208421800016,7.57603338509286));
#383933=CARTESIAN_POINT('Ctrl Pts',(1.86023191488714,1.9208421800016,7.57603338509286));
#383934=CARTESIAN_POINT('Ctrl Pts',(1.86023191488714,1.9208421800016,7.57603338509286));
#383935=CARTESIAN_POINT('Origin',(1.86637756977751,1.92719217450502,7.58486873427621));
#383936=CARTESIAN_POINT('Ctrl Pts',(1.95008020177387,1.94026180847488,7.51098857897448));
#383937=CARTESIAN_POINT('Ctrl Pts',(1.94446108228008,1.93850510471889,7.50433767179956));
#383938=CARTESIAN_POINT('Ctrl Pts',(1.94010972714622,1.94593300883657,7.50214974420965));
#383939=CARTESIAN_POINT('Ctrl Pts',(1.9200139585086,1.9308622072507,7.53887321589169));
#383940=CARTESIAN_POINT('Ctrl Pts',(1.91446216603848,1.92912655192328,7.53220407452063));
#383941=CARTESIAN_POINT('Ctrl Pts',(1.91007676036986,1.93650023058754,7.53003438070912));
#383942=CARTESIAN_POINT('Ctrl Pts',(1.88988997696529,1.92144455532481,7.56669465659235));
#383943=CARTESIAN_POINT('Ctrl Pts',(1.88437099455651,1.91971915739766,7.56004085833303));
#383944=CARTESIAN_POINT('Ctrl Pts',(1.87998739246264,1.92704859685844,7.55785582193789));
#383945=CARTESIAN_POINT('Ctrl Pts',(1.859709619531,1.91200927861988,7.59443891967696));
#383946=CARTESIAN_POINT('Ctrl Pts',(1.85418263528485,1.9102813790806,7.58783901202978));
#383947=CARTESIAN_POINT('Ctrl Pts',(1.84984313418236,1.91757849550901,7.58560008491213));
#383948=CARTESIAN_POINT('',(1.93848173883012,1.94542168785064,7.50366116523517));
#383949=CARTESIAN_POINT('Ctrl Pts',(1.93848173883038,1.9454216878509,7.50366116523554));
#383950=CARTESIAN_POINT('Ctrl Pts',(1.93911531306413,1.94500609044103,7.50350835821027));
#383951=CARTESIAN_POINT('Ctrl Pts',(1.93968420053048,1.94460344287582,7.50345484956));
#383952=CARTESIAN_POINT('Ctrl Pts',(1.94020566163611,1.9442022642676,7.50349758195598));
#383953=CARTESIAN_POINT('Ctrl Pts',(1.94047320985586,1.9439964298894,7.50351950684424));
#383954=CARTESIAN_POINT('Ctrl Pts',(1.94075472287819,1.94377079693834,7.50357029184312));
#383955=CARTESIAN_POINT('Ctrl Pts',(1.94102020193909,1.94354575978782,7.50365515313923));
#383956=CARTESIAN_POINT('Ctrl Pts',(1.94142861623783,1.94319956152378,7.50378570417639));
#383957=CARTESIAN_POINT('Ctrl Pts',(1.94181129617362,1.94284487582416,7.50400001621911));
#383958=CARTESIAN_POINT('Ctrl Pts',(1.94213757088235,1.94250703424478,7.50428903009635));
#383959=CARTESIAN_POINT('Ctrl Pts',(1.94217378486482,1.94246953642867,7.50432110841318));
#383960=CARTESIAN_POINT('Ctrl Pts',(1.94220933369085,1.94243224012206,7.50435406373354));
#383961=CARTESIAN_POINT('Ctrl Pts',(1.94224419729612,1.94239517523653,7.50438785222352));
#383962=CARTESIAN_POINT('Ctrl Pts',(1.94245705636384,1.94216887629469,7.50459414719561));
#383963=CARTESIAN_POINT('Ctrl Pts',(1.94264738578748,1.94194724773846,7.50483629897752));
#383964=CARTESIAN_POINT('Ctrl Pts',(1.94280889250206,1.94173963749442,7.5050991045531));
#383965=CARTESIAN_POINT('Ctrl Pts',(1.94316519253622,1.94128162844362,7.50567888004914));
#383966=CARTESIAN_POINT('Ctrl Pts',(1.94339566683995,1.94087411611105,7.50637912803144));
#383967=CARTESIAN_POINT('Ctrl Pts',(1.94353025984855,1.94052476529618,7.50710440483569));
#383968=CARTESIAN_POINT('Ctrl Pts',(1.94356326472631,1.94043909754079,7.50728225710685));
#383969=CARTESIAN_POINT('Ctrl Pts',(1.9435912972134,1.94035527428434,7.50746498566954));
#383970=CARTESIAN_POINT('Ctrl Pts',(1.94361409802642,1.94027538435891,7.50764697238949));
#383971=CARTESIAN_POINT('Ctrl Pts',(1.94373666892225,1.93984591810613,7.50862528291181));
#383972=CARTESIAN_POINT('Ctrl Pts',(1.94372315950022,1.93949226889331,7.50965856837422));
#383973=CARTESIAN_POINT('Ctrl Pts',(1.94363670254534,1.93919419697489,7.51067959873202));
#383974=CARTESIAN_POINT('Ctrl Pts',(1.94358912517401,1.93903016762222,7.51124147302579));
#383975=CARTESIAN_POINT('Ctrl Pts',(1.9435190281706,1.9388830498072,7.51180065547253));
#383976=CARTESIAN_POINT('Ctrl Pts',(1.94343435338579,1.93875032191859,7.51235175716501));
#383977=CARTESIAN_POINT('Ctrl Pts',(1.94314176827384,1.93829169419094,7.51425603304536));
#383978=CARTESIAN_POINT('Ctrl Pts',(1.94263512968854,1.93795345792508,7.5162690050518));
#383979=CARTESIAN_POINT('Ctrl Pts',(1.94197444496731,1.93772914884598,7.51827788969243));
#383980=CARTESIAN_POINT('Ctrl Pts',(1.94193868746167,1.93771700881473,7.51838661432545));
#383981=CARTESIAN_POINT('Ctrl Pts',(1.94190246953306,1.93770520633128,7.51849533314857));
#383982=CARTESIAN_POINT('Ctrl Pts',(1.94186579781664,1.93769374166283,7.51860402984325));
#383983=CARTESIAN_POINT('Ctrl Pts',(1.86023191671587,1.92084218061918,7.57603338728985));
#383984=CARTESIAN_POINT('Ctrl Pts',(1.88635872817725,1.92904992062325,7.55196141284922));
#383985=CARTESIAN_POINT('Ctrl Pts',(1.91244077649953,1.93724268577581,7.52783573083105));
#383986=CARTESIAN_POINT('Ctrl Pts',(1.93848173888797,1.94542168786311,7.50366116530176));
#383987=CARTESIAN_POINT('Origin',(6.42796117143038E-16,6.63739765492893E-16,
7.49482233047033));
#383988=CARTESIAN_POINT('Origin',(1.87623278704646,1.99340331564184,7.49482233047033));
#383989=CARTESIAN_POINT('Origin',(0.,0.,7.50366116523517));
#383990=CARTESIAN_POINT('Origin',(1.93224291659621,1.93916053003968,7.49482233047033));
#383991=CARTESIAN_POINT('Ctrl Pts',(1.87445804062326,2.00297322077965,7.51860402984325));
#383992=CARTESIAN_POINT('Ctrl Pts',(1.87649514626116,2.01030442031657,7.51860402984325));
#383993=CARTESIAN_POINT('Ctrl Pts',(1.87091852206097,2.01548105518489,7.51860402984325));
#383994=CARTESIAN_POINT('Ctrl Pts',(1.8752144306242,2.00569534553863,7.51041458714365));
#383995=CARTESIAN_POINT('Ctrl Pts',(1.87517397337952,2.0115308171538,7.51004642900439));
#383996=CARTESIAN_POINT('Ctrl Pts',(1.87091698409424,2.01548248283932,7.50729136483008));
#383997=CARTESIAN_POINT('Ctrl Pts',(1.87802007521299,2.00592359023331,7.50215815450138));
#383998=CARTESIAN_POINT('Ctrl Pts',(1.87786410871603,2.00903385371625,7.49877163671532));
#383999=CARTESIAN_POINT('Ctrl Pts',(1.87535173527745,2.01139857427046,7.49481588533172));
#384000=CARTESIAN_POINT('Ctrl Pts',(1.88229038656648,1.99983921157655,7.50366171572174));
#384001=CARTESIAN_POINT('Ctrl Pts',(1.88480006004696,2.00250561388651,7.50000045605858));
#384002=CARTESIAN_POINT('Ctrl Pts',(1.88480006004687,2.0025056138866,7.49482233047317));
#384003=CARTESIAN_POINT('Origin',(1.86241434696069,2.00631977766132,7.51860402984325));
#384004=CARTESIAN_POINT('Origin',(1.86241434696069,2.00631977766132,9.));
#384005=CARTESIAN_POINT('Origin',(1.86241434696069,2.00631977766132,8.75721825406948));
#384006=CARTESIAN_POINT('Ctrl Pts',(1.86998861308143,1.98688333975429,8.78942910404913));
#384007=CARTESIAN_POINT('Ctrl Pts',(1.87149950741741,1.99224707231727,8.79672699501689));
#384008=CARTESIAN_POINT('Ctrl Pts',(1.86349840890978,1.99620382713063,8.79893251111267));
#384009=CARTESIAN_POINT('Ctrl Pts',(1.87293117467995,1.9974765805228,8.78111911759583));
#384010=CARTESIAN_POINT('Ctrl Pts',(1.87471519242254,2.0038373659161,8.78644465894818));
#384011=CARTESIAN_POINT('Ctrl Pts',(1.86838843520261,2.00890566492618,8.78817647674132));
#384012=CARTESIAN_POINT('Ctrl Pts',(1.8747650492242,2.00407854085087,8.7678092393203));
#384013=CARTESIAN_POINT('Ctrl Pts',(1.87686610037956,2.01158855555213,8.7698851615837));
#384014=CARTESIAN_POINT('Ctrl Pts',(1.87143223505306,2.01684302869505,8.77093053738832));
#384015=CARTESIAN_POINT('Ctrl Pts',(1.87440746878473,2.00279124894155,8.75371302330492));
#384016=CARTESIAN_POINT('Ctrl Pts',(1.87645768767539,2.01011673895028,8.7530082828756));
#384017=CARTESIAN_POINT('Ctrl Pts',(1.87083814324368,2.01529508421825,8.75267964240738));
#384018=CARTESIAN_POINT('Origin',(1.85866130098617,1.99280876631871,8.78727029226991));
#384019=CARTESIAN_POINT('Ctrl Pts',(1.85157082176544,1.92057895321256,8.85049129520029));
#384020=CARTESIAN_POINT('Ctrl Pts',(1.85313375416819,1.92620552894985,8.85711686593484));
#384021=CARTESIAN_POINT('Ctrl Pts',(1.8456351492193,1.93031304473611,8.85933012996512));
#384022=CARTESIAN_POINT('Ctrl Pts',(1.85795825360519,1.9435737858426,8.82945683644724));
#384023=CARTESIAN_POINT('Ctrl Pts',(1.85953415929185,1.94924706556041,8.83607469902391));
#384024=CARTESIAN_POINT('Ctrl Pts',(1.85199552183796,1.95333374977092,8.8382956714852));
#384025=CARTESIAN_POINT('Ctrl Pts',(1.86433616446269,1.96653434282029,8.80838214965001));
#384026=CARTESIAN_POINT('Ctrl Pts',(1.86591828940897,1.97223001194863,8.81501364461985));
#384027=CARTESIAN_POINT('Ctrl Pts',(1.85834689049523,1.97631935554933,8.81722098428721));
#384028=CARTESIAN_POINT('Ctrl Pts',(1.87070527778331,1.98946322855773,8.78727029226991));
#384029=CARTESIAN_POINT('Ctrl Pts',(1.87228766552573,1.99515984375547,8.79393457792714));
#384030=CARTESIAN_POINT('Ctrl Pts',(1.86468995654684,1.99927253550788,8.79610912703474));
#384031=CARTESIAN_POINT('Origin',(1.83952684496831,1.92392449097353,8.85049129520029));
#384032=CARTESIAN_POINT('Ctrl Pts',(1.86024642503782,1.91217709997537,8.85049129520029));
#384033=CARTESIAN_POINT('Ctrl Pts',(1.86582001548251,1.91391956999747,8.85711686593484));
#384034=CARTESIAN_POINT('Ctrl Pts',(1.8701657630119,1.90655647007117,8.85933012996512));
#384035=CARTESIAN_POINT('Ctrl Pts',(1.85531555002703,1.91063556189963,8.86332496987232));
#384036=CARTESIAN_POINT('Ctrl Pts',(1.85882508285508,1.90762972196619,8.86648636486737));
#384037=CARTESIAN_POINT('Ctrl Pts',(1.85636632694048,1.90226030661207,8.87206031107457));
#384038=CARTESIAN_POINT('Ctrl Pts',(1.85017872212211,1.91556737749546,8.86341338519876));
#384039=CARTESIAN_POINT('Ctrl Pts',(1.84703128601863,1.91896842389455,8.86654584966059));
#384040=CARTESIAN_POINT('Ctrl Pts',(1.84175139158005,1.91627642324358,8.87215952290715));
#384041=CARTESIAN_POINT('Ctrl Pts',(1.85157082176544,1.92057895321256,8.85049129520029));
#384042=CARTESIAN_POINT('Ctrl Pts',(1.85313375416819,1.92620552894985,8.85711686593484));
#384043=CARTESIAN_POINT('Ctrl Pts',(1.8456351492193,1.93031304473611,8.85933012996512));
#384044=CARTESIAN_POINT('Origin',(1.86397627237228,1.90024654094146,8.85049129520029));
#384045=CARTESIAN_POINT('Ctrl Pts',(1.92848201925695,1.93350957471442,8.78727029226991));
#384046=CARTESIAN_POINT('Ctrl Pts',(1.93412498960261,1.93527373495556,8.79393457792714));
#384047=CARTESIAN_POINT('Ctrl Pts',(1.93847908687933,1.92781174781519,8.79610912703474));
#384048=CARTESIAN_POINT('Ctrl Pts',(1.9057690541392,1.9264088267812,8.80838214965004));
#384049=CARTESIAN_POINT('Ctrl Pts',(1.91141108732461,1.92817269403821,8.81501364461989));
#384050=CARTESIAN_POINT('Ctrl Pts',(1.91574100516638,1.92073625510017,8.81722098428722));
#384051=CARTESIAN_POINT('Ctrl Pts',(1.88302471602829,1.91929827071791,8.82945683644723));
#384052=CARTESIAN_POINT('Ctrl Pts',(1.88864457064353,1.92105520429471,8.8360746990239));
#384053=CARTESIAN_POINT('Ctrl Pts',(1.89297078040504,1.9136514247466,8.83829567148519));
#384054=CARTESIAN_POINT('Ctrl Pts',(1.86024642503782,1.91217709997537,8.85049129520029));
#384055=CARTESIAN_POINT('Ctrl Pts',(1.86582001548251,1.91391956999747,8.85711686593484));
#384056=CARTESIAN_POINT('Ctrl Pts',(1.8701657630119,1.90655647007117,8.85933012996512));
#384057=CARTESIAN_POINT('Origin',(1.93221186659141,1.92157901568051,8.78727029226991));
#384058=CARTESIAN_POINT('Ctrl Pts',(1.94168907725773,1.93763847423638,8.75374538247848));
#384059=CARTESIAN_POINT('Ctrl Pts',(1.94893794972874,1.93991843614102,8.75304829418601));
#384060=CARTESIAN_POINT('Ctrl Pts',(1.95429209524043,1.93447750156611,8.75272238421917));
#384061=CARTESIAN_POINT('Ctrl Pts',(1.94294892858739,1.93803234165219,8.76769408445018));
#384062=CARTESIAN_POINT('Ctrl Pts',(1.95038042190972,1.9403690192021,8.7697431809397));
#384063=CARTESIAN_POINT('Ctrl Pts',(1.95580304081852,1.93511415845703,8.77077869880429));
#384064=CARTESIAN_POINT('Ctrl Pts',(1.9364916483571,1.93601360166434,8.78108014887992));
#384065=CARTESIAN_POINT('Ctrl Pts',(1.94278843160509,1.93799747616341,8.78639403366325));
#384066=CARTESIAN_POINT('Ctrl Pts',(1.94806417781672,1.9318583738154,8.78812224174741));
#384067=CARTESIAN_POINT('Ctrl Pts',(1.92590959152933,1.93270533243209,8.78944554828686));
#384068=CARTESIAN_POINT('Ctrl Pts',(1.93121460487314,1.93438260731682,8.79673892988685));
#384069=CARTESIAN_POINT('Ctrl Pts',(1.93542357110275,1.92652206295943,8.79894799272499));
#384070=CARTESIAN_POINT('Origin',(1.9455956451511,1.92576318262893,8.75721825406948));
#384071=CARTESIAN_POINT('Origin',(1.9455956451511,1.92576318262893,9.));
#384072=CARTESIAN_POINT('Origin',(1.9455956451511,1.92576318262893,7.51860402984325));
#384073=CARTESIAN_POINT('Ctrl Pts',(1.93848118356971,1.94542113060227,7.50366195182966));
#384074=CARTESIAN_POINT('Ctrl Pts',(1.94106594361273,1.948015144332,7.50000065167735));
#384075=CARTESIAN_POINT('Ctrl Pts',(1.94106594361282,1.94801514433192,7.49482233047108));
#384076=CARTESIAN_POINT('Ctrl Pts',(1.94470436195011,1.94134364970687,7.50215800491337));
#384077=CARTESIAN_POINT('Ctrl Pts',(1.94781906623354,1.94128607887102,7.49877273257265));
#384078=CARTESIAN_POINT('Ctrl Pts',(1.95026446067572,1.93884944135754,7.49481816995649));
#384079=CARTESIAN_POINT('Ctrl Pts',(1.94455588051514,1.93853509676886,7.51043025814042));
#384080=CARTESIAN_POINT('Ctrl Pts',(1.95039284348441,1.93868549717537,7.51006209594514));
#384081=CARTESIAN_POINT('Ctrl Pts',(1.95448142463542,1.93455482237168,7.50731281821698));
#384082=CARTESIAN_POINT('Ctrl Pts',(1.94186435528905,1.9376932905901,7.51860402984325));
#384083=CARTESIAN_POINT('Ctrl Pts',(1.94912671001948,1.93996468248936,7.51860402984324));
#384084=CARTESIAN_POINT('Ctrl Pts',(1.95447964353079,1.93455662181901,7.51860402984325));
#384085=CARTESIAN_POINT('Origin',(0.,0.,7.5));
#384086=CARTESIAN_POINT('Origin',(1.97893795668428,1.78906192937261,7.5));
#384087=CARTESIAN_POINT('',(1.97893795668428,1.78906192937261,7.59394543036555));
#384088=CARTESIAN_POINT('',(1.97893795668428,1.78906192937261,8.85049129520029));
#384089=CARTESIAN_POINT('',(1.97893795668428,1.78906192937261,7.5));
#384090=CARTESIAN_POINT('',(2.0484001299061,1.80597870472227,8.78727029226991));
#384091=CARTESIAN_POINT('Ctrl Pts',(1.97893795668428,1.78906192937261,8.85049129520029));
#384092=CARTESIAN_POINT('Ctrl Pts',(2.00212567109016,1.79470905121292,8.82945686509571));
#384093=CARTESIAN_POINT('Ctrl Pts',(2.02527891415477,1.80034777792378,8.80838212259896));
#384094=CARTESIAN_POINT('Ctrl Pts',(2.0484001299061,1.80597870472227,8.78727029226991));
#384095=CARTESIAN_POINT('',(2.06202449055416,1.80929677321445,8.75721825406948));
#384096=CARTESIAN_POINT('Origin',(2.02102401528965,1.79931175014709,8.75937679713129));
#384097=CARTESIAN_POINT('',(2.06202449055416,1.80929677321445,7.51860402984325));
#384098=CARTESIAN_POINT('',(2.06202449055416,1.80929677321445,7.5));
#384099=CARTESIAN_POINT('Ctrl Pts',(2.06202449055416,1.80929677321445,7.51860402984325));
#384100=CARTESIAN_POINT('Ctrl Pts',(2.051324674254,1.80669094647111,7.52834476460825));
#384101=CARTESIAN_POINT('Ctrl Pts',(2.0406179117875,1.80408342806265,7.53807742314407));
#384102=CARTESIAN_POINT('Ctrl Pts',(2.02990396992788,1.80147416118916,7.54780169004674));
#384103=CARTESIAN_POINT('Ctrl Pts',(2.01293366506138,1.79734122348039,7.5632044032688));
#384104=CARTESIAN_POINT('Ctrl Pts',(1.99594532644518,1.79320389384319,7.57858609112103));
#384105=CARTESIAN_POINT('Ctrl Pts',(1.97893795668428,1.78906192937261,7.59394543036555));
#384106=CARTESIAN_POINT('Origin',(2.06124562018329,2.05770976783675,7.5));
#384107=CARTESIAN_POINT('',(1.99893804826276,1.87876195735831,8.75721825406948));
#384108=CARTESIAN_POINT('',(1.99432705985482,1.86551916431874,8.78727029226991));
#384109=CARTESIAN_POINT('Origin',(1.98262265146286,1.83190401626966,8.75658640621077));
#384110=CARTESIAN_POINT('',(1.97081848695443,1.79800236791135,8.85049129520029));
#384111=CARTESIAN_POINT('Ctrl Pts',(1.99432705985482,1.86551916431874,8.78727029226991));
#384112=CARTESIAN_POINT('Ctrl Pts',(1.98650198383395,1.84304548772372,8.80838212259896));
#384113=CARTESIAN_POINT('Ctrl Pts',(1.97866606858369,1.82054068078122,8.82945686509571));
#384114=CARTESIAN_POINT('Ctrl Pts',(1.97081848695443,1.79800236791135,8.85049129520029));
#384115=CARTESIAN_POINT('',(1.97081848695443,1.79800236791135,7.59394543036555));
#384116=CARTESIAN_POINT('',(1.97081848695443,1.79800236791135,7.5));
#384117=CARTESIAN_POINT('',(1.99893804826276,1.87876195735831,7.51860402984325));
#384118=CARTESIAN_POINT('Ctrl Pts',(1.97081848695443,1.79800236791135,7.59394543036555));
#384119=CARTESIAN_POINT('Ctrl Pts',(1.97657441098219,1.81453342457589,7.57858609112103));
#384120=CARTESIAN_POINT('Ctrl Pts',(1.98232389416546,1.83104598308703,7.56320440326857));
#384121=CARTESIAN_POINT('Ctrl Pts',(1.98806727405974,1.84754101290683,7.54780169004651));
#384122=CARTESIAN_POINT('Ctrl Pts',(1.99169326892248,1.85795489715066,7.53807742314383));
#384123=CARTESIAN_POINT('Ctrl Pts',(1.99531683401267,1.86836180306963,7.52834476460825));
#384124=CARTESIAN_POINT('Ctrl Pts',(1.99893804826276,1.87876195735831,7.51860402984324));
#384125=CARTESIAN_POINT('',(1.99893804826276,1.87876195735831,7.5));
#384126=CARTESIAN_POINT('Origin',(1.97731117195257,1.79574168958063,7.5));
#384127=CARTESIAN_POINT('Ctrl Pts',(1.97081848695443,1.79800236791135,8.85049129520029));
#384128=CARTESIAN_POINT('Ctrl Pts',(1.9707548060279,1.7978194758162,8.85097269580138));
#384129=CARTESIAN_POINT('Ctrl Pts',(1.97069987221252,1.7976361253527,8.85143669361005));
#384130=CARTESIAN_POINT('Ctrl Pts',(1.97065199348697,1.79744362289939,8.8519052845931));
#384131=CARTESIAN_POINT('Ctrl Pts',(1.97055834573614,1.79706710030878,8.85282181883899));
#384132=CARTESIAN_POINT('Ctrl Pts',(1.97049428862326,1.7966652034103,8.85372622499636));
#384133=CARTESIAN_POINT('Ctrl Pts',(1.97047404352485,1.79622919884003,8.85462257735071));
#384134=CARTESIAN_POINT('Ctrl Pts',(1.9704572367632,1.79586724333121,8.85536669723986));
#384135=CARTESIAN_POINT('Ctrl Pts',(1.97047058865884,1.79548170066649,8.85610498449051));
#384136=CARTESIAN_POINT('Ctrl Pts',(1.9705302346403,1.79506781843297,8.85681338218371));
#384137=CARTESIAN_POINT('Ctrl Pts',(1.97058436346214,1.79469221965602,8.85745625420285));
#384138=CARTESIAN_POINT('Ctrl Pts',(1.97067670481894,1.79428848470056,8.85808743050666));
#384139=CARTESIAN_POINT('Ctrl Pts',(1.97083515791361,1.79385033020559,8.85866804508411));
#384140=CARTESIAN_POINT('Ctrl Pts',(1.97090826473664,1.79364817521964,8.85893592806396));
#384141=CARTESIAN_POINT('Ctrl Pts',(1.97099568587151,1.79343866869044,8.85919241173848));
#384142=CARTESIAN_POINT('Ctrl Pts',(1.97110175636776,1.79322125445076,8.85943017985534));
#384143=CARTESIAN_POINT('Ctrl Pts',(1.97124498293792,1.79292768086569,8.8597512372));
#384144=CARTESIAN_POINT('Ctrl Pts',(1.97142643405861,1.79261249780914,8.86004599534705));
#384145=CARTESIAN_POINT('Ctrl Pts',(1.97165295583811,1.79228468846284,8.86026130871721));
#384146=CARTESIAN_POINT('Ctrl Pts',(1.97173589184792,1.79216466821924,8.86034014101235));
#384147=CARTESIAN_POINT('Ctrl Pts',(1.97182610522263,1.79204114558175,8.86040910639692));
#384148=CARTESIAN_POINT('Ctrl Pts',(1.97192140979438,1.79191768424809,8.86046313645506));
#384149=CARTESIAN_POINT('Ctrl Pts',(1.97207013178041,1.79172502387089,8.86054744990829));
#384150=CARTESIAN_POINT('Ctrl Pts',(1.97223542757181,1.79152734357843,8.86059655985668));
#384151=CARTESIAN_POINT('Ctrl Pts',(1.97240647150479,1.79133713328596,8.86059725258816));
#384152=CARTESIAN_POINT('Ctrl Pts',(1.97257791061758,1.79114648353173,8.86059794692011));
#384153=CARTESIAN_POINT('Ctrl Pts',(1.97275900125439,1.79096300045962,8.86056369958366));
#384154=CARTESIAN_POINT('Ctrl Pts',(1.97293718832746,1.79079404793147,8.86048590497774));
#384155=CARTESIAN_POINT('Ctrl Pts',(1.97298368984827,1.79074995635195,8.86046560290182));
#384156=CARTESIAN_POINT('Ctrl Pts',(1.9730306609019,1.79070634650504,8.86044257503091));
#384157=CARTESIAN_POINT('Ctrl Pts',(1.973076627709,1.79066454191475,8.86041778462583));
#384158=CARTESIAN_POINT('Ctrl Pts',(1.97338592728075,1.79038324889726,8.86025097596201));
#384159=CARTESIAN_POINT('Ctrl Pts',(1.97369148558684,1.79014619077402,8.8599848982295));
#384160=CARTESIAN_POINT('Ctrl Pts',(1.97397919074952,1.78995359252351,8.85968173251461));
#384161=CARTESIAN_POINT('Ctrl Pts',(1.97413137029703,1.78985171908355,8.85952137522076));
#384162=CARTESIAN_POINT('Ctrl Pts',(1.97428138202753,1.7897601622739,8.85934740853961));
#384163=CARTESIAN_POINT('Ctrl Pts',(1.97442630057651,1.78967888631637,8.8591675900182));
#384164=CARTESIAN_POINT('Ctrl Pts',(1.97500822387783,1.7893525211005,8.85844552518696));
#384165=CARTESIAN_POINT('Ctrl Pts',(1.97553943149826,1.78917084386518,8.85759444184126));
#384166=CARTESIAN_POINT('Ctrl Pts',(1.97598585478618,1.7890616170209,8.85683498915141));
#384167=CARTESIAN_POINT('Ctrl Pts',(1.97603257179434,1.78905018672254,8.85675551444999));
#384168=CARTESIAN_POINT('Ctrl Pts',(1.97607836118025,1.78903956978339,8.85667699793652));
#384169=CARTESIAN_POINT('Ctrl Pts',(1.97612318378677,1.7890296965528,8.85659965593547));
#384170=CARTESIAN_POINT('Ctrl Pts',(1.97672820161668,1.7888964271825,8.85555568965886));
#384171=CARTESIAN_POINT('Ctrl Pts',(1.97732890796931,1.78885572360714,8.85434650606346));
#384172=CARTESIAN_POINT('Ctrl Pts',(1.97792785225354,1.78890118409168,8.85297329937118));
#384173=CARTESIAN_POINT('Ctrl Pts',(1.97826472191922,1.7889267528443,8.85220095427748));
#384174=CARTESIAN_POINT('Ctrl Pts',(1.9786011479541,1.78897990317965,8.85137579139184));
#384175=CARTESIAN_POINT('Ctrl Pts',(1.97893795668428,1.78906192937261,8.85049129520029));
#384176=CARTESIAN_POINT('Origin',(1.97731117195257,1.79574168958063,7.59394543036555));
#384177=CARTESIAN_POINT('Ctrl Pts',(1.97063359974215,1.79747137046106,7.59443877723642));
#384178=CARTESIAN_POINT('Ctrl Pts',(1.96872943934931,1.79200260763506,7.58783886950016));
#384179=CARTESIAN_POINT('Ctrl Pts',(1.97588371901011,1.78743145197464,7.58559994247159));
#384180=CARTESIAN_POINT('Ctrl Pts',(1.98102835546094,1.82732518628152,7.56670252222135));
#384181=CARTESIAN_POINT('Ctrl Pts',(1.97912694712045,1.82186432737043,7.56004874999029));
#384182=CARTESIAN_POINT('Ctrl Pts',(1.98631211473056,1.81724808174526,7.55786368756704));
#384183=CARTESIAN_POINT('Ctrl Pts',(1.99140370001199,1.85712325308371,7.5388891333356));
#384184=CARTESIAN_POINT('Ctrl Pts',(1.98949099150865,1.85162994002072,7.53222002137279));
#384185=CARTESIAN_POINT('Ctrl Pts',(1.99672030494779,1.84701047339368,7.53005029815327));
#384186=CARTESIAN_POINT('Ctrl Pts',(2.00175916390393,1.8868642224849,7.51101258149734));
#384187=CARTESIAN_POINT('Ctrl Pts',(1.99982326989806,1.88130432048599,7.5043616886572));
#384188=CARTESIAN_POINT('Ctrl Pts',(2.00710785342834,1.87671712915195,7.50217374673251));
#384189=CARTESIAN_POINT('',(2.00655355952789,1.87513194417977,7.50366116523517));
#384190=CARTESIAN_POINT('Ctrl Pts',(1.99893804826276,1.87876195735831,7.51860402984325));
#384191=CARTESIAN_POINT('Ctrl Pts',(1.99908326148542,1.87917901081501,7.51734760759493));
#384192=CARTESIAN_POINT('Ctrl Pts',(1.99927067061861,1.87953631415501,7.51608817408572));
#384193=CARTESIAN_POINT('Ctrl Pts',(1.99951167028734,1.87982684288428,7.51481005913119));
#384194=CARTESIAN_POINT('Ctrl Pts',(1.99972997354615,1.88009001074965,7.51365231206383));
#384195=CARTESIAN_POINT('Ctrl Pts',(1.99999236391792,1.88029891959379,7.51247773061042));
#384196=CARTESIAN_POINT('Ctrl Pts',(2.00031730057136,1.88042106712354,7.51129758471022));
#384197=CARTESIAN_POINT('Ctrl Pts',(2.00072115972242,1.88057288255325,7.50983079813402));
#384198=CARTESIAN_POINT('Ctrl Pts',(2.00121333215551,1.88057363532483,7.50839324291155));
#384199=CARTESIAN_POINT('Ctrl Pts',(2.00179753601525,1.88034089142909,7.50715379678855));
#384200=CARTESIAN_POINT('Ctrl Pts',(2.00206742136501,1.88023337045562,7.50658120839351));
#384201=CARTESIAN_POINT('Ctrl Pts',(2.00239179783195,1.88005190515019,7.50598221009429));
#384202=CARTESIAN_POINT('Ctrl Pts',(2.00275184034601,1.87978096284193,7.50545747549612));
#384203=CARTESIAN_POINT('Ctrl Pts',(2.00294397017588,1.87963637963979,7.50517746087247));
#384204=CARTESIAN_POINT('Ctrl Pts',(2.00314846147559,1.87946491079294,7.50491486231392));
#384205=CARTESIAN_POINT('Ctrl Pts',(2.00335882723,1.87926981894233,7.50468370960993));
#384206=CARTESIAN_POINT('Ctrl Pts',(2.00367339038895,1.87897809508744,7.50433806340447));
#384207=CARTESIAN_POINT('Ctrl Pts',(2.00401014266396,1.87862439508465,7.50405484070984));
#384208=CARTESIAN_POINT('Ctrl Pts',(2.00434588556982,1.87823204598661,7.50385766036131));
#384209=CARTESIAN_POINT('Ctrl Pts',(2.00438178805498,1.87819009034906,7.50383657498791));
#384210=CARTESIAN_POINT('Ctrl Pts',(2.00441767407892,1.87814772069231,7.50381643264937));
#384211=CARTESIAN_POINT('Ctrl Pts',(2.0044535120173,1.87810498588884,7.50379723213559));
#384212=CARTESIAN_POINT('Ctrl Pts',(2.00469274197944,1.87781971709614,7.50366906242519));
#384213=CARTESIAN_POINT('Ctrl Pts',(2.00493448209958,1.87751151007149,7.50358235568538));
#384214=CARTESIAN_POINT('Ctrl Pts',(2.00516034878496,1.87720883540576,7.5035341175365));
#384215=CARTESIAN_POINT('Ctrl Pts',(2.00549901031652,1.87675500900067,7.50346178989176));
#384216=CARTESIAN_POINT('Ctrl Pts',(2.00584403688454,1.87625239556468,7.50346967198527));
#384217=CARTESIAN_POINT('Ctrl Pts',(2.00616756381648,1.8757485628002,7.50354272648692));
#384218=CARTESIAN_POINT('Ctrl Pts',(2.0063006371402,1.87554132595544,7.50357277531559));
#384219=CARTESIAN_POINT('Ctrl Pts',(2.00643001555918,1.8753342347853,7.50361331098761));
#384220=CARTESIAN_POINT('Ctrl Pts',(2.00655355952893,1.87513194418074,7.50366116523658));
#384221=CARTESIAN_POINT('',(1.97947865054246,1.79771013628737,7.57603338622103));
#384222=CARTESIAN_POINT('Origin',(1.98602235984314,1.80364910574213,7.58486873427626));
#384223=CARTESIAN_POINT('Ctrl Pts',(2.00655355954168,1.87513194423543,7.50366116529969));
#384224=CARTESIAN_POINT('Ctrl Pts',(1.99754410575749,1.84936651116493,7.5278357307971));
#384225=CARTESIAN_POINT('Ctrl Pts',(1.98851957912755,1.82356045444555,7.55196141284068));
#384226=CARTESIAN_POINT('Ctrl Pts',(1.97947865060514,1.79771013753785,7.57603338728831));
#384227=CARTESIAN_POINT('Ctrl Pts',(1.97132269366338,1.7989157742366,7.5963967733137));
#384228=CARTESIAN_POINT('Ctrl Pts',(1.96225232658171,1.7820656446504,7.59974925422226));
#384229=CARTESIAN_POINT('Ctrl Pts',(1.97989555771579,1.78947609816001,7.59639677331373));
#384230=CARTESIAN_POINT('Ctrl Pts',(1.96894578918438,1.79582297143307,7.58707626057422));
#384231=CARTESIAN_POINT('Ctrl Pts',(1.96988049836197,1.78899334843065,7.58811717123965));
#384232=CARTESIAN_POINT('Ctrl Pts',(1.97658880884429,1.78740715737198,7.58707626057425));
#384233=CARTESIAN_POINT('Ctrl Pts',(1.97498067889015,1.79653412437102,7.58015376756929));
#384234=CARTESIAN_POINT('Ctrl Pts',(1.97499684217358,1.79363987650909,7.58208760766041));
#384235=CARTESIAN_POINT('Ctrl Pts',(1.97787616399562,1.79334587347695,7.58015376756931));
#384236=CARTESIAN_POINT('Ctrl Pts',(1.97947864992969,1.79771013573114,7.57603338509286));
#384237=CARTESIAN_POINT('Ctrl Pts',(1.97947864992969,1.79771013573114,7.57603338509286));
#384238=CARTESIAN_POINT('Ctrl Pts',(1.97947864992969,1.79771013573114,7.57603338509286));
#384239=CARTESIAN_POINT('Origin',(1.98601852345785,1.80365333002931,7.58486873427623));
#384240=CARTESIAN_POINT('Ctrl Pts',(2.07038655374304,1.81133326498926,7.51098857897448));
#384241=CARTESIAN_POINT('Ctrl Pts',(2.06466642693681,1.8099401887916,7.50433767179956));
#384242=CARTESIAN_POINT('Ctrl Pts',(2.06079991957957,1.81763162376428,7.50214974420965));
#384243=CARTESIAN_POINT('Ctrl Pts',(2.03977985028099,1.8038793270739,7.53887321589169));
#384244=CARTESIAN_POINT('Ctrl Pts',(2.03412826074528,1.80250294240137,7.53220407452062));
#384245=CARTESIAN_POINT('Ctrl Pts',(2.03022429857703,1.81014244495787,7.53003438070911));
#384246=CARTESIAN_POINT('Ctrl Pts',(2.00911437065793,1.7964110748481,7.56669465659233));
#384247=CARTESIAN_POINT('Ctrl Pts',(2.00349618096567,1.79504282435304,7.56004085833301));
#384248=CARTESIAN_POINT('Ctrl Pts',(1.99959118425104,1.80263806304485,7.55785582193789));
#384249=CARTESIAN_POINT('Ctrl Pts',(1.97839150175078,1.78892884607101,7.59443891967696));
#384250=CARTESIAN_POINT('Ctrl Pts',(1.97276516638294,1.78755861178312,7.58783901202978));
#384251=CARTESIAN_POINT('Ctrl Pts',(1.96890210910568,1.79511876829347,7.58560008491213));
#384252=CARTESIAN_POINT('',(2.05914251569201,1.81722565891169,7.50366116523517));
#384253=CARTESIAN_POINT('Ctrl Pts',(2.0591425156923,1.81722565891194,7.50366116523554));
#384254=CARTESIAN_POINT('Ctrl Pts',(2.05974816076236,1.81677032215098,7.50350835821027));
#384255=CARTESIAN_POINT('Ctrl Pts',(2.06029008167032,1.81633205312326,7.50345484956));
#384256=CARTESIAN_POINT('Ctrl Pts',(2.0607847677765,1.81589828865177,7.50349758195598));
#384257=CARTESIAN_POINT('Ctrl Pts',(2.06103857843585,1.81567573530908,7.50351950684424));
#384258=CARTESIAN_POINT('Ctrl Pts',(2.06130505670667,1.81543252934385,7.50357029184312));
#384259=CARTESIAN_POINT('Ctrl Pts',(2.06155557213263,1.81519094525446,7.50365515313924));
#384260=CARTESIAN_POINT('Ctrl Pts',(2.06194096630146,1.81481929109793,7.50378570417639));
#384261=CARTESIAN_POINT('Ctrl Pts',(2.06230013518947,1.81444081575045,7.50400001621911));
#384262=CARTESIAN_POINT('Ctrl Pts',(2.06260409394752,1.81408276381047,7.50428903009635));
#384263=CARTESIAN_POINT('Ctrl Pts',(2.06263783103114,1.81404302279981,7.50432110841318));
#384264=CARTESIAN_POINT('Ctrl Pts',(2.06267091723573,1.81400352550136,7.50435406373355));
#384265=CARTESIAN_POINT('Ctrl Pts',(2.06270333445461,1.81396430305075,7.50438785222352));
#384266=CARTESIAN_POINT('Ctrl Pts',(2.06290125715757,1.81372483113706,7.50459414719562));
#384267=CARTESIAN_POINT('Ctrl Pts',(2.06307699573865,1.81349146349243,7.50483629897752));
#384268=CARTESIAN_POINT('Ctrl Pts',(2.06322486898635,1.81327393203518,7.5050991045531));
#384269=CARTESIAN_POINT('Ctrl Pts',(2.06355109222324,1.81279403579152,7.50567888004914));
#384270=CARTESIAN_POINT('Ctrl Pts',(2.063754983588,1.81237259419741,7.50637912803144));
#384271=CARTESIAN_POINT('Ctrl Pts',(2.06386691707728,1.81201533775758,7.50710440483569));
#384272=CARTESIAN_POINT('Ctrl Pts',(2.06389436539104,1.811927731386,7.50728225710685));
#384273=CARTESIAN_POINT('Ctrl Pts',(2.06391696970789,1.81184228430581,7.50746498566954));
#384274=CARTESIAN_POINT('Ctrl Pts',(2.0639346051091,1.8117610976697,7.50764697238949));
#384275=CARTESIAN_POINT('Ctrl Pts',(2.06402940817259,1.81132466065713,7.50862528291182));
#384276=CARTESIAN_POINT('Ctrl Pts',(2.06399326812426,1.81097260360619,7.50965856837422));
#384277=CARTESIAN_POINT('Ctrl Pts',(2.06388789127108,1.81068068342462,7.51067959873203));
#384278=CARTESIAN_POINT('Ctrl Pts',(2.06382990225586,1.81052003938049,7.51124147302579));
#384279=CARTESIAN_POINT('Ctrl Pts',(2.06375052340349,1.81037771496522,7.51180065547253));
#384280=CARTESIAN_POINT('Ctrl Pts',(2.06365751868708,1.81025068491239,7.512351757165));
#384281=CARTESIAN_POINT('Ctrl Pts',(2.06333615034322,1.80981174547708,7.51425603304536));
#384282=CARTESIAN_POINT('Ctrl Pts',(2.06280888182927,1.80950666459951,7.5162690050518));
#384283=CARTESIAN_POINT('Ctrl Pts',(2.06213518302361,1.8093251466029,7.51827788969244));
#384284=CARTESIAN_POINT('Ctrl Pts',(2.06209872117114,1.8093153225059,7.51838661432545));
#384285=CARTESIAN_POINT('Ctrl Pts',(2.06206182146844,1.80930586476257,7.51849533314857));
#384286=CARTESIAN_POINT('Ctrl Pts',(2.06202449055416,1.80929677321445,7.51860402984325));
#384287=CARTESIAN_POINT('Ctrl Pts',(1.97947865179423,1.79771013623029,7.57603338728985));
#384288=CARTESIAN_POINT('Ctrl Pts',(2.00607765462697,1.80422706199454,7.55196141284922));
#384289=CARTESIAN_POINT('Ctrl Pts',(2.03263102684925,1.81073191165887,7.52783573083104));
#384290=CARTESIAN_POINT('Ctrl Pts',(2.05914251575055,1.81722565892043,7.50366116530176));
#384291=CARTESIAN_POINT('Origin',(6.84001376365777E-16,6.21191952330719E-16,
7.49482233047033));
#384292=CARTESIAN_POINT('Origin',(2.0000956545036,1.86909700733692,7.49482233047033));
#384293=CARTESIAN_POINT('Origin',(0.,0.,7.50366116523517));
#384294=CARTESIAN_POINT('Origin',(2.05251535802922,1.81137708803391,7.49482233047033));
#384295=CARTESIAN_POINT('Ctrl Pts',(1.99893770041463,1.878760958472,7.51860402984325));
#384296=CARTESIAN_POINT('Ctrl Pts',(2.00144033216758,1.88594657746686,7.51860402984325));
#384297=CARTESIAN_POINT('Ctrl Pts',(1.99620683387467,1.89146987192291,7.51860402984325));
#384298=CARTESIAN_POINT('Ctrl Pts',(1.99986694346332,1.88142902825996,7.51041458714367));
#384299=CARTESIAN_POINT('Ctrl Pts',(2.00020044929247,1.88725510237742,7.51004642900443));
#384300=CARTESIAN_POINT('Ctrl Pts',(1.99620539053798,1.89147139518194,7.50729136483011));
#384301=CARTESIAN_POINT('Ctrl Pts',(2.00268144724221,1.88147704573546,7.50215815450137));
#384302=CARTESIAN_POINT('Ctrl Pts',(2.00272507646069,1.88459091165628,7.49877163671529));
#384303=CARTESIAN_POINT('Ctrl Pts',(2.00036937312888,1.88711174195736,7.49481588533168));
#384304=CARTESIAN_POINT('Ctrl Pts',(2.00655315730403,1.87513156829939,7.50366171572174));
#384305=CARTESIAN_POINT('Ctrl Pts',(2.00922851137374,1.87763169686786,7.50000045605858));
#384306=CARTESIAN_POINT('Ctrl Pts',(2.00922851137366,1.87763169686795,7.49482233047317));
#384307=CARTESIAN_POINT('Origin',(1.98713316644797,1.88287228159599,7.51860402984325));
#384308=CARTESIAN_POINT('Origin',(1.98713316644797,1.88287228159599,9.));
#384309=CARTESIAN_POINT('Origin',(1.98713316644797,1.88287228159599,8.75721825406948));
#384310=CARTESIAN_POINT('Ctrl Pts',(1.99344657357428,1.86299049303864,8.78942910404913));
#384311=CARTESIAN_POINT('Ctrl Pts',(1.99529801914104,1.86824640190533,8.7967269950169));
#384312=CARTESIAN_POINT('Ctrl Pts',(1.98756686989969,1.87270765928304,8.79893251111266));
#384313=CARTESIAN_POINT('Ctrl Pts',(1.99706180063074,1.87337343828892,8.78111911759577));
#384314=CARTESIAN_POINT('Ctrl Pts',(1.99924968983695,1.87960685235723,8.78644465894813));
#384315=CARTESIAN_POINT('Ctrl Pts',(1.99326065865079,1.88507009473028,8.78817647674132));
#384316=CARTESIAN_POINT('Ctrl Pts',(1.99931489633358,1.87984433743599,8.76780923932033));
#384317=CARTESIAN_POINT('Ctrl Pts',(2.00189279894798,1.88720430719688,8.76988516158374));
#384318=CARTESIAN_POINT('Ctrl Pts',(1.99680675333071,1.89279613340802,8.77093053738833));
#384319=CARTESIAN_POINT('Ctrl Pts',(1.99887557350567,1.87858260066337,8.75371302330491));
#384320=CARTESIAN_POINT('Ctrl Pts',(2.00139092575807,1.8857616816919,8.75300828287559));
#384321=CARTESIAN_POINT('Ctrl Pts',(1.99611470500354,1.89128943294207,8.75267964240738));
#384322=CARTESIAN_POINT('Origin',(1.98252217804003,1.86962948855642,8.78727029226991));
#384323=CARTESIAN_POINT('Ctrl Pts',(1.97081848695443,1.79800236791135,8.85049129520029));
#384324=CARTESIAN_POINT('Ctrl Pts',(1.97273870409016,1.80351724582249,8.85711686593484));
#384325=CARTESIAN_POINT('Ctrl Pts',(1.96551867526936,1.80809675954566,8.85933012996512));
#384326=CARTESIAN_POINT('Ctrl Pts',(1.97866607911544,1.82054071102848,8.82945683644722));
#384327=CARTESIAN_POINT('Ctrl Pts',(1.98060223521436,1.82610136576063,8.83607469902389));
#384328=CARTESIAN_POINT('Ctrl Pts',(1.97334092145601,1.83066265560018,8.8382956714852));
#384329=CARTESIAN_POINT('Ctrl Pts',(1.9865019738075,1.84304545892769,8.80838214965003));
#384330=CARTESIAN_POINT('Ctrl Pts',(1.98844577088237,1.84862805859969,8.81501364461993));
#384331=CARTESIAN_POINT('Ctrl Pts',(1.98115193336379,1.85319410139927,8.81722098428722));
#384332=CARTESIAN_POINT('Ctrl Pts',(1.99432705985482,1.86551916431874,8.78727029226991));
#384333=CARTESIAN_POINT('Ctrl Pts',(1.99627117980078,1.87110269127884,8.79393457792714));
#384334=CARTESIAN_POINT('Ctrl Pts',(1.98895258219513,1.87569371995059,8.79610912703474));
#384335=CARTESIAN_POINT('Origin',(1.95901360513964,1.80211269214903,8.85049129520029));
#384336=CARTESIAN_POINT('Ctrl Pts',(1.97893795668428,1.78906192937261,8.85049129520029));
#384337=CARTESIAN_POINT('Ctrl Pts',(1.98461173602726,1.7904437181373,8.85711686593484));
#384338=CARTESIAN_POINT('Ctrl Pts',(1.98847679932026,1.7828173134893,8.85933012996512));
#384339=CARTESIAN_POINT('Ctrl Pts',(1.97391844600142,1.78783948079882,8.86332496987232));
#384340=CARTESIAN_POINT('Ctrl Pts',(1.9772281832921,1.78461496014557,8.86648636486737));
#384341=CARTESIAN_POINT('Ctrl Pts',(1.97443045953233,1.77941410986349,8.87206031107457));
#384342=CARTESIAN_POINT('Ctrl Pts',(1.96910815477048,1.79309028114443,8.86341338519876));
#384343=CARTESIAN_POINT('Ctrl Pts',(1.966185091203,1.79668599665246,8.86654584966058));
#384344=CARTESIAN_POINT('Ctrl Pts',(1.9607435677999,1.79433781100371,8.87215952290714));
#384345=CARTESIAN_POINT('Ctrl Pts',(1.97081848695443,1.79800236791135,8.85049129520029));
#384346=CARTESIAN_POINT('Ctrl Pts',(1.97273870409016,1.80351724582249,8.85711686593484));
#384347=CARTESIAN_POINT('Ctrl Pts',(1.96551867526936,1.80809675954566,8.85933012996512));
#384348=CARTESIAN_POINT('Origin',(1.98189574710557,1.77691691081257,8.85049129520029));
#384349=CARTESIAN_POINT('Ctrl Pts',(2.0484001299061,1.80597870472227,8.78727029226991));
#384350=CARTESIAN_POINT('Ctrl Pts',(2.05414453629871,1.8073776939556,8.79393457792714));
#384351=CARTESIAN_POINT('Ctrl Pts',(2.05801159645803,1.79965207029777,8.79610912703474));
#384352=CARTESIAN_POINT('Ctrl Pts',(2.02527888452904,1.80034777070874,8.80838214965003));
#384353=CARTESIAN_POINT('Ctrl Pts',(2.0310223369153,1.80174652760397,8.81501364461988));
#384354=CARTESIAN_POINT('Ctrl Pts',(2.03486690419788,1.79404794883869,8.81722098428721));
#384355=CARTESIAN_POINT('Ctrl Pts',(2.00212570220894,1.79470905879157,8.82945683644723));
#384356=CARTESIAN_POINT('Ctrl Pts',(2.00784657735089,1.79610231723846,8.83607469902389));
#384357=CARTESIAN_POINT('Ctrl Pts',(2.01168953666614,1.78843656833838,8.8382956714852));
#384358=CARTESIAN_POINT('Ctrl Pts',(1.97893795668428,1.78906192937261,8.85049129520029));
#384359=CARTESIAN_POINT('Ctrl Pts',(1.98461173602726,1.7904437181373,8.85711686593484));
#384360=CARTESIAN_POINT('Ctrl Pts',(1.98847679932026,1.7828173134893,8.85933012996512));
#384361=CARTESIAN_POINT('Origin',(2.0513579203274,1.79383368616223,8.78727029226991));
#384362=CARTESIAN_POINT('Ctrl Pts',(2.06184459209041,1.80925294186594,8.75374538247847));
#384363=CARTESIAN_POINT('Ctrl Pts',(2.06922464863628,1.8110637824905,8.75304829418601));
#384364=CARTESIAN_POINT('Ctrl Pts',(2.07421919160667,1.80529098561845,8.75272238421917));
#384365=CARTESIAN_POINT('Ctrl Pts',(2.06312709009236,1.80956528108706,8.76769408445022));
#384366=CARTESIAN_POINT('Ctrl Pts',(2.07069302605927,1.81142102027039,8.76974318093972));
#384367=CARTESIAN_POINT('Ctrl Pts',(2.07576782353207,1.80582952781395,8.7707786988043));
#384368=CARTESIAN_POINT('Ctrl Pts',(2.05655373592174,1.80796440818185,8.78108014887987));
#384369=CARTESIAN_POINT('Ctrl Pts',(2.0629646890288,1.80954077031014,8.78639403366321));
#384370=CARTESIAN_POINT('Ctrl Pts',(2.0678362620161,1.80307626318599,8.78812224174741));
#384371=CARTESIAN_POINT('Ctrl Pts',(2.04578145952719,1.80534093085236,8.78944554828686));
#384372=CARTESIAN_POINT('Ctrl Pts',(2.05118303652296,1.80667486622402,8.79673892988686));
#384373=CARTESIAN_POINT('Ctrl Pts',(2.0548797281739,1.79856080280582,8.79894799272499));
#384374=CARTESIAN_POINT('Origin',(2.06498228097545,1.79715175465441,8.75721825406948));
#384375=CARTESIAN_POINT('Origin',(2.06498228097545,1.79715175465441,9.));
#384376=CARTESIAN_POINT('Origin',(2.06498228097545,1.79715175465441,7.51860402984325));
#384377=CARTESIAN_POINT('Ctrl Pts',(2.05914192586943,1.8172251383839,7.50366195182966));
#384378=CARTESIAN_POINT('Ctrl Pts',(2.06188757427602,1.81964821628966,7.50000065167735));
#384379=CARTESIAN_POINT('Ctrl Pts',(2.0618875742761,1.81964821628958,7.49482233047108));
#384380=CARTESIAN_POINT('Ctrl Pts',(2.06509107296447,1.8127573147025,7.50215800491337));
#384381=CARTESIAN_POINT('Ctrl Pts',(2.06819568917778,1.81250030236349,7.49877273257264));
#384382=CARTESIAN_POINT('Ctrl Pts',(2.07047994339331,1.80991199422326,7.49481816995649));
#384383=CARTESIAN_POINT('Ctrl Pts',(2.06476295199597,1.80996404547592,7.51043025814042));
#384384=CARTESIAN_POINT('Ctrl Pts',(2.07059755848593,1.8097401613672,7.51006209594515));
#384385=CARTESIAN_POINT('Ctrl Pts',(2.07441308596513,1.80535601718416,7.50731281821698));
#384386=CARTESIAN_POINT('Ctrl Pts',(2.06202302209007,1.80929641549156,7.51860402984325));
#384387=CARTESIAN_POINT('Ctrl Pts',(2.06941598411247,1.81109783990739,7.51860402984324));
#384388=CARTESIAN_POINT('Ctrl Pts',(2.07441142381096,1.80535792705009,7.51860402984325));
#384389=CARTESIAN_POINT('Origin',(0.,0.,7.5));
#384390=CARTESIAN_POINT('Origin',(2.08949760778586,1.65859511954948,7.5));
#384391=CARTESIAN_POINT('',(2.08949760778586,1.65859511954948,7.59394543036555));
#384392=CARTESIAN_POINT('',(2.08949760778586,1.65859511954948,8.85049129520029));
#384393=CARTESIAN_POINT('',(2.08949760778586,1.65859511954948,7.5));
#384394=CARTESIAN_POINT('',(2.15990092504103,1.6710266808512,8.78727029226991));
#384395=CARTESIAN_POINT('Ctrl Pts',(2.08949760778586,1.65859511954948,8.85049129520029));
#384396=CARTESIAN_POINT('Ctrl Pts',(2.11299949288419,1.66274499680948,8.82945686509571));
#384397=CARTESIAN_POINT('Ctrl Pts',(2.1364664395885,1.66688870477514,8.80838212259894));
#384398=CARTESIAN_POINT('Ctrl Pts',(2.15990092504103,1.67102668085121,8.78727029226991));
#384399=CARTESIAN_POINT('',(2.17370988235713,1.67346501623199,8.75721825406948));
#384400=CARTESIAN_POINT('Origin',(2.13215390434319,1.66612741793514,8.75937679713173));
#384401=CARTESIAN_POINT('',(2.17370988235713,1.67346501623199,7.51860402984325));
#384402=CARTESIAN_POINT('',(2.17370988235713,1.67346501623199,7.5));
#384403=CARTESIAN_POINT('Ctrl Pts',(2.17370988235713,1.67346501623199,7.51860402984325));
#384404=CARTESIAN_POINT('Ctrl Pts',(2.16286509408443,1.67155008302327,7.52834476460825));
#384405=CARTESIAN_POINT('Ctrl Pts',(2.15201326553168,1.66963390666755,7.53807742314407));
#384406=CARTESIAN_POINT('Ctrl Pts',(2.14115416031211,1.6677164454245,7.54780169004674));
#384407=CARTESIAN_POINT('Ctrl Pts',(2.12395392452885,1.66467929044544,7.5632044032688));
#384408=CARTESIAN_POINT('Ctrl Pts',(2.10673541065634,1.66163890798795,7.57858609112103));
#384409=CARTESIAN_POINT('Ctrl Pts',(2.08949760778586,1.65859511954948,7.59394543036555));
#384410=CARTESIAN_POINT('Origin',(2.18884848747049,1.92141752211062,7.5));
#384411=CARTESIAN_POINT('',(2.11520370755651,1.74682943894032,8.75721825406948));
#384412=CARTESIAN_POINT('',(2.10975372425558,1.73390928168096,8.78727029226991));
#384413=CARTESIAN_POINT('Origin',(2.09591963389567,1.70111310357894,8.75658640621063));
#384414=CARTESIAN_POINT('',(2.08196763624129,1.6680374052101,8.85049129520029));
#384415=CARTESIAN_POINT('Ctrl Pts',(2.10975372425558,1.73390928168096,8.78727029226991));
#384416=CARTESIAN_POINT('Ctrl Pts',(2.10050483228941,1.71198313400682,8.80838212259895));
#384417=CARTESIAN_POINT('Ctrl Pts',(2.09124312883601,1.69002661441765,8.82945686509571));
#384418=CARTESIAN_POINT('Ctrl Pts',(2.08196763624129,1.6680374052101,8.85049129520029));
#384419=CARTESIAN_POINT('',(2.08196763624129,1.6680374052101,7.59394543036555));
#384420=CARTESIAN_POINT('',(2.08196763624129,1.6680374052101,7.5));
#384421=CARTESIAN_POINT('',(2.11520370755651,1.74682943894032,7.51860402984325));
#384422=CARTESIAN_POINT('Ctrl Pts',(2.08196763624129,1.6680374052101,7.59394543036555));
#384423=CARTESIAN_POINT('Ctrl Pts',(2.08877088254282,1.68416571372712,7.57858609112103));
#384424=CARTESIAN_POINT('Ctrl Pts',(2.09556651605251,1.7002759747635,7.56320440326857));
#384425=CARTESIAN_POINT('Ctrl Pts',(2.10235493574597,1.71636913416219,7.54780169004651));
#384426=CARTESIAN_POINT('Ctrl Pts',(2.10664070046774,1.72652930367545,7.53807742314383));
#384427=CARTESIAN_POINT('Ctrl Pts',(2.11092359330636,1.73668266487763,7.52834476460825));
#384428=CARTESIAN_POINT('Ctrl Pts',(2.11520370755651,1.74682943894032,7.51860402984325));
#384429=CARTESIAN_POINT('',(2.11520370755651,1.74682943894032,7.5));
#384430=CARTESIAN_POINT('Origin',(2.0883021391638,1.66536538392937,7.5));
#384431=CARTESIAN_POINT('Ctrl Pts',(2.08196763624129,1.6680374052101,8.85049129520029));
#384432=CARTESIAN_POINT('Ctrl Pts',(2.08189236821728,1.66785896893735,8.85097269580138));
#384433=CARTESIAN_POINT('Ctrl Pts',(2.08182579996479,1.66767951480867,8.85143669361005));
#384434=CARTESIAN_POINT('Ctrl Pts',(2.08176568593668,1.66749047547278,8.8519052845931));
#384435=CARTESIAN_POINT('Ctrl Pts',(2.08164810670999,1.6671207265202,8.85282181883899));
#384436=CARTESIAN_POINT('Ctrl Pts',(2.08155843158662,1.66672375951533,8.85372622499636));
#384437=CARTESIAN_POINT('Ctrl Pts',(2.08151029317522,1.66628994787111,8.85462257735071));
#384438=CARTESIAN_POINT('Ctrl Pts',(2.08147033037578,1.66592981285162,8.85536669723987));
#384439=CARTESIAN_POINT('Ctrl Pts',(2.08145895303518,1.66554420686677,8.85610498449051));
#384440=CARTESIAN_POINT('Ctrl Pts',(2.08149195894182,1.66512735346752,8.85681338218371));
#384441=CARTESIAN_POINT('Ctrl Pts',(2.08152191185393,1.66474905835303,8.85745625420284));
#384442=CARTESIAN_POINT('Ctrl Pts',(2.0815881960981,1.66434023658329,8.85808743050666));
#384443=CARTESIAN_POINT('Ctrl Pts',(2.08171825097901,1.6638928301991,8.8586680450841));
#384444=CARTESIAN_POINT('Ctrl Pts',(2.08177825548182,1.66368640659201,8.85893592806395));
#384445=CARTESIAN_POINT('Ctrl Pts',(2.08185207387118,1.6634717294251,8.85919241173848));
#384446=CARTESIAN_POINT('Ctrl Pts',(2.08194399665605,1.66324796592627,8.85943017985534));
#384447=CARTESIAN_POINT('Ctrl Pts',(2.08206811962769,1.66294581896175,8.8597512372));
#384448=CARTESIAN_POINT('Ctrl Pts',(2.08222900408982,1.66261965786937,8.86004599534706));
#384449=CARTESIAN_POINT('Ctrl Pts',(2.08243405763911,1.66227800874229,8.86026130871721));
#384450=CARTESIAN_POINT('Ctrl Pts',(2.08250913352457,1.66215292136476,8.86034014101235));
#384451=CARTESIAN_POINT('Ctrl Pts',(2.08259124742368,1.66202387252702,8.86040910639692));
#384452=CARTESIAN_POINT('Ctrl Pts',(2.08267844598715,1.66189455867303,8.86046313645506));
#384453=CARTESIAN_POINT('Ctrl Pts',(2.08281451861517,1.66169276548687,8.86054744990829));
#384454=CARTESIAN_POINT('Ctrl Pts',(2.08296680936882,1.66148490081206,8.86059655985668));
#384455=CARTESIAN_POINT('Ctrl Pts',(2.08312531505841,1.66128412250463,8.86059725258816));
#384456=CARTESIAN_POINT('Ctrl Pts',(2.08328418695946,1.66108288031909,8.86059794692011));
#384457=CARTESIAN_POINT('Ctrl Pts',(2.08345314972534,1.66088817171569,8.86056369958366));
#384458=CARTESIAN_POINT('Ctrl Pts',(2.08362014586832,1.66070814983367,8.86048590497774));
#384459=CARTESIAN_POINT('Ctrl Pts',(2.08366372688956,1.66066116948236,8.86046560290182));
#384460=CARTESIAN_POINT('Ctrl Pts',(2.08370780734364,1.66061463979082,8.86044257503091));
#384461=CARTESIAN_POINT('Ctrl Pts',(2.08375100127771,1.6605699759891,8.86041778462583));
#384462=CARTESIAN_POINT('Ctrl Pts',(2.08404164285481,1.66026944402668,8.86025097596201));
#384463=CARTESIAN_POINT('Ctrl Pts',(2.08433138499248,1.66001329577689,8.8599848982295));
#384464=CARTESIAN_POINT('Ctrl Pts',(2.08460615922177,1.65980265990707,8.85968173251461));
#384465=CARTESIAN_POINT('Ctrl Pts',(2.08475149904637,1.65969124559994,8.85952137522076));
#384466=CARTESIAN_POINT('Ctrl Pts',(2.08489533649674,1.65959026561901,8.8593474085396));
#384467=CARTESIAN_POINT('Ctrl Pts',(2.08503474992654,1.65949987168834,8.8591675900182));
#384468=CARTESIAN_POINT('Ctrl Pts',(2.08559456731286,1.65913689307087,8.85844552518695));
#384469=CARTESIAN_POINT('Ctrl Pts',(2.08611304340984,1.65892155452182,8.85759444184124));
#384470=CARTESIAN_POINT('Ctrl Pts',(2.0865515512853,1.65878394965754,8.85683498915139));
#384471=CARTESIAN_POINT('Ctrl Pts',(2.08659743996662,1.65876954967496,8.85675551444998));
#384472=CARTESIAN_POINT('Ctrl Pts',(2.0866424550437,1.65875602081343,8.85667699793651));
#384473=CARTESIAN_POINT('Ctrl Pts',(2.0866865529773,1.65874329607419,8.85659965593547));
#384474=CARTESIAN_POINT('Ctrl Pts',(2.08728178913532,1.65857153689465,8.85555568965886));
#384475=CARTESIAN_POINT('Ctrl Pts',(2.08787865338529,1.65849242956099,8.85434650606346));
#384476=CARTESIAN_POINT('Ctrl Pts',(2.0884792797375,1.65849942215005,8.85297329937117));
#384477=CARTESIAN_POINT('Ctrl Pts',(2.08881709546393,1.65850335505533,8.85220095427747));
#384478=CARTESIAN_POINT('Ctrl Pts',(2.08915623562911,1.65853484129756,8.85137579139184));
#384479=CARTESIAN_POINT('Ctrl Pts',(2.08949760778586,1.65859511954948,8.85049129520029));
#384480=CARTESIAN_POINT('Origin',(2.0883021391638,1.66536538392937,7.59394543036555));
#384481=CARTESIAN_POINT('Ctrl Pts',(2.08174910777616,1.66751934451538,7.59443877723642));
#384482=CARTESIAN_POINT('Ctrl Pts',(2.07949847484779,1.66218381782438,7.58783886950016));
#384483=CARTESIAN_POINT('Ctrl Pts',(2.086345180325,1.65716367782185,7.58559994247159));
#384484=CARTESIAN_POINT('Ctrl Pts',(2.09403524690138,1.69664582818389,7.56670252222138));
#384485=CARTESIAN_POINT('Ctrl Pts',(2.09178786677661,1.69131801284371,7.56004874999029));
#384486=CARTESIAN_POINT('Ctrl Pts',(2.09866250781646,1.68625089652094,7.55786368756705));
#384487=CARTESIAN_POINT('Ctrl Pts',(2.1062984428893,1.72571792105421,7.53888913333558));
#384488=CARTESIAN_POINT('Ctrl Pts',(2.10403770647439,1.72035844224661,7.53222002137275));
#384489=CARTESIAN_POINT('Ctrl Pts',(2.11095619627073,1.71528528310687,7.53005029815327));
#384490=CARTESIAN_POINT('Ctrl Pts',(2.11853814082204,1.75473430759452,7.51101258149734));
#384491=CARTESIAN_POINT('Ctrl Pts',(2.11625000017389,1.74930986216538,7.5043616886572));
#384492=CARTESIAN_POINT('Ctrl Pts',(2.12322571438817,1.74426537083866,7.50217374673251));
#384493=CARTESIAN_POINT('',(2.12257099619411,1.74271895653114,7.50366116523517));
#384494=CARTESIAN_POINT('Ctrl Pts',(2.11520370755651,1.74682943894032,7.51860402984325));
#384495=CARTESIAN_POINT('Ctrl Pts',(2.11537534312975,1.74723633167284,7.51734760759494));
#384496=CARTESIAN_POINT('Ctrl Pts',(2.11558525971437,1.74758089355042,7.51608817408573));
#384497=CARTESIAN_POINT('Ctrl Pts',(2.11584437846302,1.74785538445546,7.5148100591312));
#384498=CARTESIAN_POINT('Ctrl Pts',(2.1160790944174,1.74810402487641,7.51365231206384));
#384499=CARTESIAN_POINT('Ctrl Pts',(2.11635433051561,1.74829569308609,7.51247773061043));
#384500=CARTESIAN_POINT('Ctrl Pts',(2.11668642557094,1.74839677088778,7.51129758471022));
#384501=CARTESIAN_POINT('Ctrl Pts',(2.11709918179804,1.74852239905175,7.50983079813402));
#384502=CARTESIAN_POINT('Ctrl Pts',(2.11759039124033,1.74849161668062,7.50839324291155));
#384503=CARTESIAN_POINT('Ctrl Pts',(2.11815848283798,1.74822192091238,7.50715379678855));
#384504=CARTESIAN_POINT('Ctrl Pts',(2.11842092478693,1.74809732923854,7.50658120839351));
#384505=CARTESIAN_POINT('Ctrl Pts',(2.11873300826559,1.74789545390146,7.50598221009429));
#384506=CARTESIAN_POINT('Ctrl Pts',(2.1190749517004,1.74760200027015,7.50545747549611));
#384507=CARTESIAN_POINT('Ctrl Pts',(2.11925742330135,1.74744540432924,7.50517746087247));
#384508=CARTESIAN_POINT('Ctrl Pts',(2.11945050840502,1.74726118598096,7.50491486231392));
#384509=CARTESIAN_POINT('Ctrl Pts',(2.11964794236264,1.74705301678733,7.50468370960992));
#384510=CARTESIAN_POINT('Ctrl Pts',(2.11994316840629,1.74674173817959,7.50433806340447));
#384511=CARTESIAN_POINT('Ctrl Pts',(2.12025656715065,1.74636718909905,7.50405484070984));
#384512=CARTESIAN_POINT('Ctrl Pts',(2.12056648234368,1.74595413500248,7.50385766036131));
#384513=CARTESIAN_POINT('Ctrl Pts',(2.1205996229564,1.74590996528717,7.50383657498791));
#384514=CARTESIAN_POINT('Ctrl Pts',(2.12063272061543,1.74586538345797,7.50381643264937));
#384515=CARTESIAN_POINT('Ctrl Pts',(2.12066574689267,1.74582044031314,7.50379723213559));
#384516=CARTESIAN_POINT('Ctrl Pts',(2.12088620809689,1.74552043011947,7.50366906242519));
#384517=CARTESIAN_POINT('Ctrl Pts',(2.12110770464416,1.74519736799653,7.50358235568538));
#384518=CARTESIAN_POINT('Ctrl Pts',(2.1213137148298,1.74488084388015,7.5035341175365));
#384519=CARTESIAN_POINT('Ctrl Pts',(2.12162260378731,1.74440625179125,7.50346178989176));
#384520=CARTESIAN_POINT('Ctrl Pts',(2.12193471890784,1.74388256510035,7.50346967198527));
#384521=CARTESIAN_POINT('Ctrl Pts',(2.12222530044294,1.74335903907262,7.50354272648692));
#384522=CARTESIAN_POINT('Ctrl Pts',(2.12234482264301,1.74314370198107,7.50357277531559));
#384523=CARTESIAN_POINT('Ctrl Pts',(2.12246066686333,1.74292874699818,7.50361331098761));
#384524=CARTESIAN_POINT('Ctrl Pts',(2.12257099619521,1.74271895653205,7.50366116523659));
#384525=CARTESIAN_POINT('',(2.09059128324999,1.66719091542118,7.57603338622103));
#384526=CARTESIAN_POINT('Origin',(2.09750205887771,1.67269842573194,7.58486873427627));
#384527=CARTESIAN_POINT('Ctrl Pts',(2.12257099621144,1.74271895658581,7.50366116529969));
#384528=CARTESIAN_POINT('Ctrl Pts',(2.11192925635159,1.71758369904673,7.52783573079709));
#384529=CARTESIAN_POINT('Ctrl Pts',(2.10126987184861,1.692408867045,7.55196141284069));
#384530=CARTESIAN_POINT('Ctrl Pts',(2.09059128339265,1.66719091666508,7.57603338728831));
#384531=CARTESIAN_POINT('Ctrl Pts',(2.08252932914759,1.66891663020922,7.59639677331372));
#384532=CARTESIAN_POINT('Ctrl Pts',(2.07239800659894,1.65268226143543,7.59974925422224));
#384533=CARTESIAN_POINT('Ctrl Pts',(2.0904797772088,1.65894708367398,7.59639677331371));
#384534=CARTESIAN_POINT('Ctrl Pts',(2.07995915171788,1.66598247069355,7.58707626057424));
#384535=CARTESIAN_POINT('Ctrl Pts',(2.08045436498717,1.65910699286144,7.58811717123965));
#384536=CARTESIAN_POINT('Ctrl Pts',(2.0870472649161,1.65709425787422,7.58707626057421));
#384537=CARTESIAN_POINT('Ctrl Pts',(2.08602720582062,1.66630550578071,7.5801537675693));
#384538=CARTESIAN_POINT('Ctrl Pts',(2.0858579007976,1.66341616887639,7.58208760766041));
#384539=CARTESIAN_POINT('Ctrl Pts',(2.08871246990528,1.66293829112239,7.5801537675693));
#384540=CARTESIAN_POINT('Ctrl Pts',(2.09059128260285,1.66719091490535,7.57603338509286));
#384541=CARTESIAN_POINT('Ctrl Pts',(2.09059128260285,1.66719091490535,7.57603338509286));
#384542=CARTESIAN_POINT('Ctrl Pts',(2.09059128260285,1.66719091490535,7.57603338509286));
#384543=CARTESIAN_POINT('Origin',(2.09749850102576,1.67270288713816,7.58486873427622));
#384544=CARTESIAN_POINT('Ctrl Pts',(2.18218524326636,1.67496156458802,7.51098857897448));
#384545=CARTESIAN_POINT('Ctrl Pts',(2.1763876143757,1.67393784039762,7.50433767179956));
#384546=CARTESIAN_POINT('Ctrl Pts',(2.17302184310317,1.68186120046917,7.50214974420965));
#384547=CARTESIAN_POINT('Ctrl Pts',(2.15116384911715,1.66948391981124,7.53887321589167));
#384548=CARTESIAN_POINT('Ctrl Pts',(2.14543568610953,1.66847246165342,7.5322040745206));
#384549=CARTESIAN_POINT('Ctrl Pts',(2.14202920965962,1.6763463957475,7.53003438070911));
#384550=CARTESIAN_POINT('Ctrl Pts',(2.12008288244789,1.66399575593587,7.56669465659234));
#384551=CARTESIAN_POINT('Ctrl Pts',(2.11438857181863,1.66299027530768,7.56004085833295));
#384552=CARTESIAN_POINT('Ctrl Pts',(2.1109782269524,1.67082010276554,7.55785582193789));
#384553=CARTESIAN_POINT('Ctrl Pts',(2.08894374892622,1.65849732116959,7.59443891967696));
#384554=CARTESIAN_POINT('Ctrl Pts',(2.08324118225557,1.65749038271971,7.58783901202978));
#384555=CARTESIAN_POINT('Ctrl Pts',(2.0798704429345,1.66528251300723,7.58560008491213));
#384556=CARTESIAN_POINT('',(2.17134183427225,1.68156225994659,7.50366116523517));
#384557=CARTESIAN_POINT('Ctrl Pts',(2.17134183427255,1.68156225994682,7.50366116523554));
#384558=CARTESIAN_POINT('Ctrl Pts',(2.17191706145342,1.6810690549112,7.50350835821027));
#384559=CARTESIAN_POINT('Ctrl Pts',(2.17242978893373,1.68059696536242,7.50345484956));
#384560=CARTESIAN_POINT('Ctrl Pts',(2.17289566726915,1.68013239745891,7.50349758195598));
#384561=CARTESIAN_POINT('Ctrl Pts',(2.17313469740565,1.67989403967115,7.50351950684424));
#384562=CARTESIAN_POINT('Ctrl Pts',(2.1733850459086,1.67963426007723,7.50357029184312));
#384563=CARTESIAN_POINT('Ctrl Pts',(2.17361956827799,1.67937712176982,7.50365515313924));
#384564=CARTESIAN_POINT('Ctrl Pts',(2.1739803586496,1.67898153892743,7.50378570417639));
#384565=CARTESIAN_POINT('Ctrl Pts',(2.17431454058785,1.67858082916848,7.50400001621911));
#384566=CARTESIAN_POINT('Ctrl Pts',(2.17459493436346,1.67820403818011,7.50428903009635));
#384567=CARTESIAN_POINT('Ctrl Pts',(2.17462605591534,1.67816221727926,7.50432110841318));
#384568=CARTESIAN_POINT('Ctrl Pts',(2.17465654354017,1.67812068129183,7.50435406373354));
#384569=CARTESIAN_POINT('Ctrl Pts',(2.17468638116336,1.67807946244961,7.50438785222352));
#384570=CARTESIAN_POINT('Ctrl Pts',(2.17486855419471,1.67782780160553,7.50459414719561));
#384571=CARTESIAN_POINT('Ctrl Pts',(2.17502897978569,1.67758365383021,7.50483629897752));
#384572=CARTESIAN_POINT('Ctrl Pts',(2.17516261192363,1.67735709504316,7.5050991045531));
#384573=CARTESIAN_POINT('Ctrl Pts',(2.17545741784199,1.67685728360325,7.50567888004914));
#384574=CARTESIAN_POINT('Ctrl Pts',(2.17563388843443,1.6764236445415,7.50637912803144));
#384575=CARTESIAN_POINT('Ctrl Pts',(2.17572270244566,1.67605995052007,7.50710440483569));
#384576=CARTESIAN_POINT('Ctrl Pts',(2.17574448140442,1.67597076552567,7.50728225710685));
#384577=CARTESIAN_POINT('Ctrl Pts',(2.17576156466506,1.67588404574211,7.50746498566954));
#384578=CARTESIAN_POINT('Ctrl Pts',(2.17577396218681,1.67580189600862,7.50764697238949));
#384579=CARTESIAN_POINT('Ctrl Pts',(2.17584060785183,1.67536028164957,7.50862528291181));
#384580=CARTESIAN_POINT('Ctrl Pts',(2.17578198568441,1.67501126343844,7.50965856837421));
#384581=CARTESIAN_POINT('Ctrl Pts',(2.17565812194902,1.67472669455636,7.51067959873201));
#384582=CARTESIAN_POINT('Ctrl Pts',(2.17558995957921,1.67457009594161,7.51124147302578));
#384583=CARTESIAN_POINT('Ctrl Pts',(2.17550162506261,1.67443314976765,7.51180065547252));
#384584=CARTESIAN_POINT('Ctrl Pts',(2.17540067259094,1.67431233954432,7.51235175716501));
#384585=CARTESIAN_POINT('Ctrl Pts',(2.17505184158663,1.67389489209765,7.51425603304535));
#384586=CARTESIAN_POINT('Ctrl Pts',(2.17450610980346,1.67362422025114,7.5162690050518));
#384587=CARTESIAN_POINT('Ctrl Pts',(2.17382216528628,1.6734862392334,7.51827788969243));
#384588=CARTESIAN_POINT('Ctrl Pts',(2.17378514891653,1.67347877143997,7.51838661432545));
#384589=CARTESIAN_POINT('Ctrl Pts',(2.17374771906853,1.67347169730066,7.51849533314856));
#384590=CARTESIAN_POINT('Ctrl Pts',(2.17370988235713,1.67346501623199,7.51860402984325));
#384591=CARTESIAN_POINT('Ctrl Pts',(2.09059128449553,1.66719091528402,7.57603338728984));
#384592=CARTESIAN_POINT('Ctrl Pts',(2.11755317769153,1.67199024736258,7.55196141284922));
#384593=CARTESIAN_POINT('Ctrl Pts',(2.14446876031168,1.67678045171611,7.52783573083105));
#384594=CARTESIAN_POINT('Ctrl Pts',(2.17134183433122,1.68156225995156,7.50366116530176));
#384595=CARTESIAN_POINT('Origin',(7.22395927215194E-16,5.76091528191162E-16,
7.49482233047033));
#384596=CARTESIAN_POINT('Origin',(2.1157396998972,1.73711017850881,7.49482233047033));
#384597=CARTESIAN_POINT('Origin',(0.,0.,7.50366116523517));
#384598=CARTESIAN_POINT('Origin',(2.16435357359292,1.67615030903423,7.49482233047033));
#384599=CARTESIAN_POINT('Ctrl Pts',(2.11520329642422,1.74682846439304,7.51860402984325));
#384600=CARTESIAN_POINT('Ctrl Pts',(2.11816117044151,1.75383897559608,7.51860402984325));
#384601=CARTESIAN_POINT('Ctrl Pts',(2.11329230362296,1.75968623323819,7.51860402984325));
#384602=CARTESIAN_POINT('Ctrl Pts',(2.11630157406164,1.74943151553893,7.51041458714365));
#384603=CARTESIAN_POINT('Ctrl Pts',(2.1170076725176,1.75522425157044,7.5100464290044));
#384604=CARTESIAN_POINT('Ctrl Pts',(2.1132909608473,1.75968784584242,7.50729136483009));
#384605=CARTESIAN_POINT('Ctrl Pts',(2.11911337163085,1.74929910848111,7.50215815450139));
#384606=CARTESIAN_POINT('Ctrl Pts',(2.11935641728298,1.75240378129679,7.49877163671533));
#384607=CARTESIAN_POINT('Ctrl Pts',(2.11716706414824,1.75507036271236,7.49481588533172));
#384608=CARTESIAN_POINT('Ctrl Pts',(2.12257057071393,1.74271860719363,7.50366171572174));
#384609=CARTESIAN_POINT('Ctrl Pts',(2.12540061176913,1.74504218845604,7.50000045605858));
#384610=CARTESIAN_POINT('Ctrl Pts',(2.12540061176905,1.74504218845613,7.49482233047317));
#384611=CARTESIAN_POINT('Origin',(2.10368642951558,1.75168765945074,7.51860402984325));
#384612=CARTESIAN_POINT('Origin',(2.10368642951558,1.75168765945074,9.));
#384613=CARTESIAN_POINT('Origin',(2.10368642951558,1.75168765945074,8.75721825406948));
#384614=CARTESIAN_POINT('Ctrl Pts',(2.10871303450336,1.73144221877688,8.78942910404912));
#384615=CARTESIAN_POINT('Ctrl Pts',(2.11089742331392,1.73656870629038,8.79672699501691));
#384616=CARTESIAN_POINT('Ctrl Pts',(2.10346799228943,1.74151613396893,8.79893251111267));
#384617=CARTESIAN_POINT('Ctrl Pts',(2.11298607127434,1.74157220275981,8.78111911759583));
#384618=CARTESIAN_POINT('Ctrl Pts',(2.1155688414381,1.74765263106764,8.78644465894813));
#384619=CARTESIAN_POINT('Ctrl Pts',(2.10994214649949,1.75348836716887,8.78817647674131));
#384620=CARTESIAN_POINT('Ctrl Pts',(2.11564912968224,1.74788545041325,8.76780923932029));
#384621=CARTESIAN_POINT('Ctrl Pts',(2.11869329060088,1.75506513153933,8.76988516158374));
#384622=CARTESIAN_POINT('Ctrl Pts',(2.11397596434524,1.7609713328053,8.77093053738833));
#384623=CARTESIAN_POINT('Ctrl Pts',(2.11512986973762,1.74665445352438,8.75371302330492));
#384624=CARTESIAN_POINT('Ctrl Pts',(2.11810001922979,1.75365762518884,8.75300828287559));
#384625=CARTESIAN_POINT('Ctrl Pts',(2.11318880327527,1.75951206770563,8.75267964240738));
#384626=CARTESIAN_POINT('Origin',(2.09823644621465,1.73876750219138,8.78727029226991));
#384627=CARTESIAN_POINT('Ctrl Pts',(2.08196763624129,1.6680374052101,8.85049129520029));
#384628=CARTESIAN_POINT('Ctrl Pts',(2.0842372475259,1.67341792347881,8.85711686593484));
#384629=CARTESIAN_POINT('Ctrl Pts',(2.07732546348031,1.6784506169347,8.85933012996512));
#384630=CARTESIAN_POINT('Ctrl Pts',(2.09124314128407,1.690026643928,8.82945683644723));
#384631=CARTESIAN_POINT('Ctrl Pts',(2.09353159171458,1.69545182375145,8.83607469902391));
#384632=CARTESIAN_POINT('Ctrl Pts',(2.08657743994751,1.70046897590166,8.8382956714852));
#384633=CARTESIAN_POINT('Ctrl Pts',(2.10050482043859,1.71198310591235,8.80838214965002));
#384634=CARTESIAN_POINT('Ctrl Pts',(2.10280230216297,1.7174296960284,8.81501364461992));
#384635=CARTESIAN_POINT('Ctrl Pts',(2.09581599798245,1.72245367517765,8.81722098428721));
#384636=CARTESIAN_POINT('Ctrl Pts',(2.10975372425558,1.73390928168096,8.78727029226991));
#384637=CARTESIAN_POINT('Ctrl Pts',(2.11205158759921,1.73935677649348,8.79393457792714));
#384638=CARTESIAN_POINT('Ctrl Pts',(2.10504217505419,1.74440727656298,8.79610912703474));
#384639=CARTESIAN_POINT('Origin',(2.07045035820036,1.67289562572052,8.85049129520029));
#384640=CARTESIAN_POINT('Ctrl Pts',(2.08949760778586,1.65859511954948,8.85049129520029));
#384641=CARTESIAN_POINT('Ctrl Pts',(2.09524826125079,1.65961054899033,8.85711686593484));
#384642=CARTESIAN_POINT('Ctrl Pts',(2.09861675793327,1.65175217815318,8.85933012996512));
#384643=CARTESIAN_POINT('Ctrl Pts',(2.084410087677,1.65769678378104,8.86332496987232));
#384644=CARTESIAN_POINT('Ctrl Pts',(2.08750642900989,1.654266832655,8.86648636486737));
#384645=CARTESIAN_POINT('Ctrl Pts',(2.08438123385196,1.64925591885436,8.87206031107456));
#384646=CARTESIAN_POINT('Ctrl Pts',(2.07994609963852,1.66324499221154,8.86341338519877));
#384647=CARTESIAN_POINT('Ctrl Pts',(2.07725942010221,1.6670206012622,8.86654584966059));
#384648=CARTESIAN_POINT('Ctrl Pts',(2.07167862812148,1.66502587981416,8.87215952290715));
#384649=CARTESIAN_POINT('Ctrl Pts',(2.08196763624129,1.6680374052101,8.85049129520029));
#384650=CARTESIAN_POINT('Ctrl Pts',(2.0842372475259,1.67341792347881,8.85711686593484));
#384651=CARTESIAN_POINT('Ctrl Pts',(2.07732546348031,1.6784506169347,8.85933012996512));
#384652=CARTESIAN_POINT('Origin',(2.0916711870987,1.64628554794967,8.85049129520029));
#384653=CARTESIAN_POINT('Ctrl Pts',(2.15990092504103,1.67102668085121,8.78727029226991));
#384654=CARTESIAN_POINT('Ctrl Pts',(2.16572316248255,1.67205475032988,8.79393457792714));
#384655=CARTESIAN_POINT('Ctrl Pts',(2.16908729494478,1.66409723639934,8.79610912703474));
#384656=CARTESIAN_POINT('Ctrl Pts',(2.13646640956136,1.66688869947306,8.80838214965001));
#384657=CARTESIAN_POINT('Ctrl Pts',(2.14228768007071,1.66791659821439,8.81501364461984));
#384658=CARTESIAN_POINT('Ctrl Pts',(2.14563109864245,1.65998751473334,8.81722098428721));
#384659=CARTESIAN_POINT('Ctrl Pts',(2.1129995244246,1.66274500237877,8.82945683644722));
#384660=CARTESIAN_POINT('Ctrl Pts',(2.1187979117902,1.66376886049793,8.83607469902389));
#384661=CARTESIAN_POINT('Ctrl Pts',(2.12214182911501,1.65587264245243,8.83829567148519));
#384662=CARTESIAN_POINT('Ctrl Pts',(2.08949760778586,1.65859511954948,8.85049129520029));
#384663=CARTESIAN_POINT('Ctrl Pts',(2.0952482612508,1.65961054899033,8.85711686593484));
#384664=CARTESIAN_POINT('Ctrl Pts',(2.09861675793327,1.65175217815318,8.85933012996512));
#384665=CARTESIAN_POINT('Origin',(2.16207450435387,1.6587171092514,8.78727029226991));
#384666=CARTESIAN_POINT('Ctrl Pts',(2.17352754522994,1.67343280107383,8.75374538247848));
#384667=CARTESIAN_POINT('Ctrl Pts',(2.18100845961528,1.67476707928574,8.75304829418602));
#384668=CARTESIAN_POINT('Ctrl Pts',(2.18562287639598,1.66868614177719,8.75272238421917));
#384669=CARTESIAN_POINT('Ctrl Pts',(2.17482741984481,1.67366232863142,8.76769408445018));
#384670=CARTESIAN_POINT('Ctrl Pts',(2.18249670840253,1.6750295038178,8.76974318093969));
#384671=CARTESIAN_POINT('Ctrl Pts',(2.18720283100793,1.66912435629186,8.7707786988043));
#384672=CARTESIAN_POINT('Ctrl Pts',(2.16816500305613,1.67248590113901,8.78108014887992));
#384673=CARTESIAN_POINT('Ctrl Pts',(2.17466378204077,1.67364827328636,8.78639403366325));
#384674=CARTESIAN_POINT('Ctrl Pts',(2.17911116346538,1.66688492543247,8.78812224174741));
#384675=CARTESIAN_POINT('Ctrl Pts',(2.15724677268912,1.67055799614335,8.78944554828685));
#384676=CARTESIAN_POINT('Ctrl Pts',(2.16272271709833,1.67154311057535,8.79673892988686));
#384677=CARTESIAN_POINT('Ctrl Pts',(2.16589194367167,1.66320887052341,8.79894799272499));
#384678=CARTESIAN_POINT('Origin',(2.17588346166996,1.66115544463218,8.75721825406948));
#384679=CARTESIAN_POINT('Origin',(2.17588346166996,1.66115544463218,9.));
#384680=CARTESIAN_POINT('Origin',(2.17588346166996,1.66115544463218,7.51860402984325));
#384681=CARTESIAN_POINT('Ctrl Pts',(2.17134121231119,1.68156177827834,7.50366195182966));
#384682=CARTESIAN_POINT('Ctrl Pts',(2.17423646662311,1.68380396341327,7.50000065167735));
#384683=CARTESIAN_POINT('Ctrl Pts',(2.17423646662319,1.68380396341318,7.49482233047108));
#384684=CARTESIAN_POINT('Ctrl Pts',(2.17699188179938,1.67672197105678,7.50215800491337));
#384685=CARTESIAN_POINT('Ctrl Pts',(2.18007365240861,1.67626657333344,7.49877273257267));
#384686=CARTESIAN_POINT('Ctrl Pts',(2.18218737990695,1.6735372304798,7.49481816995647));
#384687=CARTESIAN_POINT('Ctrl Pts',(2.17648546961679,1.67395546368404,7.51043025814042));
#384688=CARTESIAN_POINT('Ctrl Pts',(2.18229374397787,1.67335821504792,7.51006209594515));
#384689=CARTESIAN_POINT('Ctrl Pts',(2.18582053896441,1.66873861687436,7.507312818217));
#384690=CARTESIAN_POINT('Ctrl Pts',(2.17370839399077,1.67346475332889,7.51860402984326));
#384691=CARTESIAN_POINT('Ctrl Pts',(2.1812015840384,1.67478880782198,7.51860402984326));
#384692=CARTESIAN_POINT('Ctrl Pts',(2.18581900259084,1.66874062931087,7.51860402984327));
#384693=CARTESIAN_POINT('Origin',(0.,0.,7.5));
#384694=CARTESIAN_POINT('Origin',(2.19147106502122,1.52131278661258,7.5));
#384695=CARTESIAN_POINT('',(2.19147106502122,1.52131278661258,7.59394543036555));
#384696=CARTESIAN_POINT('',(2.19147106502122,1.52131278661258,8.85049129520029));
#384697=CARTESIAN_POINT('',(2.19147106502122,1.52131278661258,7.5));
#384698=CARTESIAN_POINT('',(2.26252622397766,1.52920804991442,8.78727029226991));
#384699=CARTESIAN_POINT('Ctrl Pts',(2.19147106502122,1.52131278661258,8.85049129520029));
#384700=CARTESIAN_POINT('Ctrl Pts',(2.21519054652499,1.52394836655647,8.82945686509571));
#384701=CARTESIAN_POINT('Ctrl Pts',(2.2388747661514,1.52658002839208,8.80838212259897));
#384702=CARTESIAN_POINT('Ctrl Pts',(2.26252622397766,1.52920804991442,8.78727029226991));
#384703=CARTESIAN_POINT('',(2.27646303399418,1.53075663254071,8.75721825406948));
#384704=CARTESIAN_POINT('Origin',(2.23452231565462,1.52609661077913,8.75937679713095));
#384705=CARTESIAN_POINT('',(2.27646303399418,1.53075663254071,7.51860402984325));
#384706=CARTESIAN_POINT('',(2.27646303399418,1.53075663254071,7.5));
#384707=CARTESIAN_POINT('Ctrl Pts',(2.27646303399418,1.53075663254071,7.51860402984325));
#384708=CARTESIAN_POINT('Ctrl Pts',(2.26551783731016,1.52954046173792,7.52834476460825));
#384709=CARTESIAN_POINT('Ctrl Pts',(2.2545655351624,1.5283235014146,7.53807742314407));
#384710=CARTESIAN_POINT('Ctrl Pts',(2.24360588897548,1.52710572506153,7.54780169004674));
#384711=CARTESIAN_POINT('Ctrl Pts',(2.22624640173374,1.52517683313347,7.5632044032688));
#384712=CARTESIAN_POINT('Ctrl Pts',(2.20886846717178,1.52324589143937,7.57858609112103));
#384713=CARTESIAN_POINT('Ctrl Pts',(2.19147106502122,1.52131278661258,7.59394543036555));
#384714=CARTESIAN_POINT('Origin',(2.30745690681614,1.77722975964338,7.5));
#384715=CARTESIAN_POINT('',(2.22277754110614,1.60771882366398,8.75721825406948));
#384716=CARTESIAN_POINT('',(2.21651095806262,1.59517439388238,8.78727029226991));
#384717=CARTESIAN_POINT('Origin',(2.20060403297873,1.56333195225666,8.75658640621012));
#384718=CARTESIAN_POINT('',(2.18456153393017,1.53121811901794,8.85049129520029));
#384719=CARTESIAN_POINT('Ctrl Pts',(2.21651095806262,1.59517439388238,8.78727029226991));
#384720=CARTESIAN_POINT('Ctrl Pts',(2.20587625583212,1.57388587437305,8.80838212259895));
#384721=CARTESIAN_POINT('Ctrl Pts',(2.19522682250169,1.55256786618587,8.82945686509571));
#384722=CARTESIAN_POINT('Ctrl Pts',(2.18456153393017,1.53121811901794,8.85049129520029));
#384723=CARTESIAN_POINT('',(2.18456153393017,1.53121811901794,7.59394543036555));
#384724=CARTESIAN_POINT('',(2.18456153393017,1.53121811901794,7.5));
#384725=CARTESIAN_POINT('',(2.22277754110614,1.60771882366398,7.51860402984325));
#384726=CARTESIAN_POINT('Ctrl Pts',(2.18456153393017,1.53121811901794,7.59394543036555));
#384727=CARTESIAN_POINT('Ctrl Pts',(2.19238414650714,1.54687740470824,7.57858609112103));
#384728=CARTESIAN_POINT('Ctrl Pts',(2.20019800562749,1.56251916775162,7.56320440326857));
#384729=CARTESIAN_POINT('Ctrl Pts',(2.20800357004749,1.57814432648526,7.54780169004651));
#384730=CARTESIAN_POINT('Ctrl Pts',(2.21293149350175,1.58800903095208,7.53807742314383));
#384731=CARTESIAN_POINT('Ctrl Pts',(2.21785611476347,1.5978671250984,7.52834476460825));
#384732=CARTESIAN_POINT('Ctrl Pts',(2.22277754110614,1.60771882366398,7.51860402984324));
#384733=CARTESIAN_POINT('',(2.22277754110614,1.60771882366398,7.5));
#384734=CARTESIAN_POINT('Origin',(2.19071182494581,1.52814573469579,7.5));
#384735=CARTESIAN_POINT('Ctrl Pts',(2.18456153393017,1.53121811901794,8.85049129520029));
#384736=CARTESIAN_POINT('Ctrl Pts',(2.18447498810114,1.5310448718005,8.85097269580138));
#384737=CARTESIAN_POINT('Ctrl Pts',(2.18439705895476,1.53087005142217,8.85143669361005));
#384738=CARTESIAN_POINT('Ctrl Pts',(2.18432495664554,1.53068525200686,8.8519052845931));
#384739=CARTESIAN_POINT('Ctrl Pts',(2.18418392910125,1.53032379607009,8.85282181883899));
#384740=CARTESIAN_POINT('Ctrl Pts',(2.18406900446171,1.52993339018138,8.85372622499635));
#384741=CARTESIAN_POINT('Ctrl Pts',(2.18399317054836,1.52950355408832,8.8546225773507));
#384742=CARTESIAN_POINT('Ctrl Pts',(2.18393021592686,1.5291467194302,8.85536669723986));
#384743=CARTESIAN_POINT('Ctrl Pts',(2.18389415610195,1.52876263466292,8.85610498449051));
#384744=CARTESIAN_POINT('Ctrl Pts',(2.18390038630543,1.52834452303799,8.85681338218371));
#384745=CARTESIAN_POINT('Ctrl Pts',(2.18390604022486,1.52796508608171,8.85745625420285));
#384746=CARTESIAN_POINT('Ctrl Pts',(2.18394599498022,1.52755285743403,8.85808743050667));
#384747=CARTESIAN_POINT('Ctrl Pts',(2.18404711722398,1.5270980376494,8.85866804508412));
#384748=CARTESIAN_POINT('Ctrl Pts',(2.18409377283519,1.52688819366007,8.85893592806397));
#384749=CARTESIAN_POINT('Ctrl Pts',(2.18415368514344,1.52666922800998,8.85919241173849));
#384750=CARTESIAN_POINT('Ctrl Pts',(2.18423108248649,1.52644003474421,8.85943017985534));
#384751=CARTESIAN_POINT('Ctrl Pts',(2.18433559181169,1.52613055598694,8.8597512372));
#384752=CARTESIAN_POINT('Ctrl Pts',(2.1844752485065,1.52579475712462,8.86004599534705));
#384753=CARTESIAN_POINT('Ctrl Pts',(2.18465799121655,1.52544067212631,8.86026130871721));
#384754=CARTESIAN_POINT('Ctrl Pts',(2.18472489847476,1.52531103162571,8.86034014101235));
#384755=CARTESIAN_POINT('Ctrl Pts',(2.18479857547463,1.52517698687706,8.86040910639693));
#384756=CARTESIAN_POINT('Ctrl Pts',(2.18487730971223,1.52504235188111,8.86046313645507));
#384757=CARTESIAN_POINT('Ctrl Pts',(2.18500017383062,1.52483225509749,8.8605474499083));
#384758=CARTESIAN_POINT('Ctrl Pts',(2.18513883375113,1.52461506020086,8.86059655985669));
#384759=CARTESIAN_POINT('Ctrl Pts',(2.18528414986346,1.52440453891959,8.86059725258816));
#384760=CARTESIAN_POINT('Ctrl Pts',(2.18542980171406,1.52419353125006,8.86059794692012));
#384761=CARTESIAN_POINT('Ctrl Pts',(2.18558594230477,1.52398839721479,8.86056369958366));
#384762=CARTESIAN_POINT('Ctrl Pts',(2.18574106129467,1.52379804572741,8.86048590497774));
#384763=CARTESIAN_POINT('Ctrl Pts',(2.18578154273259,1.52374836965665,8.86046560290182));
#384764=CARTESIAN_POINT('Ctrl Pts',(2.18582255145108,1.52369911132097,8.86044257503091));
#384765=CARTESIAN_POINT('Ctrl Pts',(2.18586279501898,1.52365177184096,8.86041778462583));
#384766=CARTESIAN_POINT('Ctrl Pts',(2.18613358429284,1.52333323588391,8.860250975962));
#384767=CARTESIAN_POINT('Ctrl Pts',(2.18640631964951,1.52305905007567,8.8599848982295));
#384768=CARTESIAN_POINT('Ctrl Pts',(2.18666703383915,1.52283124213453,8.85968173251461));
#384769=CARTESIAN_POINT('Ctrl Pts',(2.18680493670833,1.5227107447855,8.85952137522076));
#384770=CARTESIAN_POINT('Ctrl Pts',(2.18694200881964,1.52260075658168,8.85934740853961));
#384771=CARTESIAN_POINT('Ctrl Pts',(2.18707534425058,1.52250161612592,8.8591675900182));
#384772=CARTESIAN_POINT('Ctrl Pts',(2.18761075531216,1.52210351566387,8.85844552518697));
#384773=CARTESIAN_POINT('Ctrl Pts',(2.18811436935617,1.52185540067338,8.85759444184127));
#384774=CARTESIAN_POINT('Ctrl Pts',(2.18854315989624,1.52168998323701,8.85683498915143));
#384775=CARTESIAN_POINT('Ctrl Pts',(2.1885880316843,1.52167267274283,8.85675551445001));
#384776=CARTESIAN_POINT('Ctrl Pts',(2.18863208747595,1.5216562875519,8.85667699793653));
#384777=CARTESIAN_POINT('Ctrl Pts',(2.18867527952879,1.52164076359269,8.85659965593547));
#384778=CARTESIAN_POINT('Ctrl Pts',(2.18925828806186,1.52143122039922,8.85555568965886));
#384779=CARTESIAN_POINT('Ctrl Pts',(2.18984885756595,1.52131403437627,8.85434650606346));
#384780=CARTESIAN_POINT('Ctrl Pts',(2.19044869788362,1.5212825303358,8.85297329937117));
#384781=CARTESIAN_POINT('Ctrl Pts',(2.19078607151351,1.5212648112326,8.85220095427747));
#384782=CARTESIAN_POINT('Ctrl Pts',(2.19112653220932,1.52127450399798,8.85137579139184));
#384783=CARTESIAN_POINT('Ctrl Pts',(2.19147106502122,1.52131278661258,8.85049129520029));
#384784=CARTESIAN_POINT('Origin',(2.19071182494581,1.52814573469579,7.59394543036555));
#384785=CARTESIAN_POINT('Ctrl Pts',(2.18431026219254,1.53071512390131,7.59443877723642));
#384786=CARTESIAN_POINT('Ctrl Pts',(2.18172240506209,1.52553475816895,7.58783886950016));
#384787=CARTESIAN_POINT('Ctrl Pts',(2.1882334017743,1.52008626265639,7.58559994247159));
#384788=CARTESIAN_POINT('Ctrl Pts',(2.19843729834314,1.55899458844884,7.56670252222137));
#384789=CARTESIAN_POINT('Ctrl Pts',(2.19585318140098,1.55382170981567,7.56004874999025));
#384790=CARTESIAN_POINT('Ctrl Pts',(2.20238904649608,1.54832454466312,7.55786368756705));
#384791=CARTESIAN_POINT('Ctrl Pts',(2.21253795366518,1.58722124392178,7.53888913333555));
#384792=CARTESIAN_POINT('Ctrl Pts',(2.20993847918948,1.58201762261761,7.53222002137274));
#384793=CARTESIAN_POINT('Ctrl Pts',(2.2165177157845,1.57651161766423,7.53005029815326));
#384794=CARTESIAN_POINT('Ctrl Pts',(2.2266115900945,1.6153938130449,7.51101258149734));
#384795=CARTESIAN_POINT('Ctrl Pts',(2.2239806052648,1.61012711439534,7.5043616886572));
#384796=CARTESIAN_POINT('Ctrl Pts',(2.23061878545708,1.60464605197284,7.50217374673251));
#384797=CARTESIAN_POINT('',(2.22986633334691,1.60314476287809,7.50366116523517));
#384798=CARTESIAN_POINT('Ctrl Pts',(2.22277754110614,1.60771882366398,7.51860402984325));
#384799=CARTESIAN_POINT('Ctrl Pts',(2.22297489374257,1.60811388366282,7.51734760759493));
#384800=CARTESIAN_POINT('Ctrl Pts',(2.22320645518634,1.60844428819931,7.51608817408572));
#384801=CARTESIAN_POINT('Ctrl Pts',(2.22348262824041,1.60870161333811,7.51481005913119));
#384802=CARTESIAN_POINT('Ctrl Pts',(2.22373279239216,1.60893470459783,7.51365231206383));
#384803=CARTESIAN_POINT('Ctrl Pts',(2.22401974321264,1.60910834456725,7.51247773061042));
#384804=CARTESIAN_POINT('Ctrl Pts',(2.22435763202005,1.6091879372905,7.51129758471022));
#384805=CARTESIAN_POINT('Ctrl Pts',(2.22477758921932,1.60928686195567,7.50983079813402));
#384806=CARTESIAN_POINT('Ctrl Pts',(2.22526581718583,1.6092246709332,7.50839324291155));
#384807=CARTESIAN_POINT('Ctrl Pts',(2.22581546211117,1.60891913153021,7.50715379678855));
#384808=CARTESIAN_POINT('Ctrl Pts',(2.22606938222903,1.60877798112993,7.50658120839351));
#384809=CARTESIAN_POINT('Ctrl Pts',(2.22636789030146,1.60855652531024,7.50598221009429));
#384810=CARTESIAN_POINT('Ctrl Pts',(2.2266903295381,1.6082417662198,7.50545747549611));
#384811=CARTESIAN_POINT('Ctrl Pts',(2.2268623930952,1.60807380102644,7.50517746087247));
#384812=CARTESIAN_POINT('Ctrl Pts',(2.22704327857472,1.60787759016945,7.50491486231392));
#384813=CARTESIAN_POINT('Ctrl Pts',(2.22722696943706,1.60765719904465,7.50468370960993));
#384814=CARTESIAN_POINT('Ctrl Pts',(2.22750164521827,1.60732764479464,7.50433806340447));
#384815=CARTESIAN_POINT('Ctrl Pts',(2.22779040260931,1.60693378573887,7.50405484070984));
#384816=CARTESIAN_POINT('Ctrl Pts',(2.22807321658151,1.60650172397165,7.50385766036131));
#384817=CARTESIAN_POINT('Ctrl Pts',(2.22810345913991,1.6064555216814,7.50383657498791));
#384818=CARTESIAN_POINT('Ctrl Pts',(2.22813363242864,1.60640891087605,7.50381643264937));
#384819=CARTESIAN_POINT('Ctrl Pts',(2.22816371133268,1.60636194407088,7.50379723213559));
#384820=CARTESIAN_POINT('Ctrl Pts',(2.2283644978566,1.60604842528248,7.50366906242519));
#384821=CARTESIAN_POINT('Ctrl Pts',(2.22856484065418,1.60571183559281,7.50358235568538));
#384822=CARTESIAN_POINT('Ctrl Pts',(2.22875014780003,1.60538276269127,7.5035341175365));
#384823=CARTESIAN_POINT('Ctrl Pts',(2.22902799489252,1.60488935511926,7.50346178989176));
#384824=CARTESIAN_POINT('Ctrl Pts',(2.22930591601756,1.6043467471144,7.50346967198527));
#384825=CARTESIAN_POINT('Ctrl Pts',(2.22956235809398,1.60380567910417,7.50354272648692));
#384826=CARTESIAN_POINT('Ctrl Pts',(2.22966783802804,1.60358312663211,7.50357277531559));
#384827=CARTESIAN_POINT('Ctrl Pts',(2.22976967202095,1.60336119113261,7.50361331098761));
#384828=CARTESIAN_POINT('Ctrl Pts',(2.22986633334807,1.60314476287892,7.50366116523658));
#384829=CARTESIAN_POINT('',(2.19311322794422,1.52982084947219,7.57603338622103));
#384830=CARTESIAN_POINT('Origin',(2.2003626720401,1.5348742690979,7.58486873427626));
#384831=CARTESIAN_POINT('Ctrl Pts',(2.22986633336771,1.60314476293154,7.50366116529969));
#384832=CARTESIAN_POINT('Ctrl Pts',(2.21763603662394,1.5787429670886,7.52783573079709));
#384833=CARTESIAN_POINT('Ctrl Pts',(2.2053855959453,1.55430280858918,7.55196141284069));
#384834=CARTESIAN_POINT('Ctrl Pts',(2.19311322816629,1.5298208507044,7.57603338728831));
#384835=CARTESIAN_POINT('Ctrl Pts',(2.18456153393017,1.53121811901794,7.59394543036555));
#384836=CARTESIAN_POINT('Ctrl Pts',(2.17891644017658,1.51991778489476,7.59394543036555));
#384837=CARTESIAN_POINT('Ctrl Pts',(2.19147106502122,1.52131278661258,7.59394543036555));
#384838=CARTESIAN_POINT('Ctrl Pts',(2.18351888218448,1.52913094144132,7.58587155981958));
#384839=CARTESIAN_POINT('Ctrl Pts',(2.18371352266054,1.52326402197321,7.58685956158229));
#384840=CARTESIAN_POINT('Ctrl Pts',(2.18915221929746,1.52105512907139,7.5858715598196));
#384841=CARTESIAN_POINT('Ctrl Pts',(2.1889122721287,1.52920781474962,7.57982961904599));
#384842=CARTESIAN_POINT('Ctrl Pts',(2.18864592315211,1.52670465103575,7.58148017275035));
#384843=CARTESIAN_POINT('Ctrl Pts',(2.19108705088151,1.52609010586745,7.57982961904595));
#384844=CARTESIAN_POINT('Ctrl Pts',(2.19311322726536,1.52982084899889,7.57603338509286));
#384845=CARTESIAN_POINT('Ctrl Pts',(2.19311322726536,1.52982084899889,7.57603338509286));
#384846=CARTESIAN_POINT('Ctrl Pts',(2.19311322726536,1.52982084899889,7.57603338509286));
#384847=CARTESIAN_POINT('Origin',(2.20035940734063,1.53487894928969,7.58486873427622));
#384848=CARTESIAN_POINT('Ctrl Pts',(2.28501686554783,1.53170708783977,7.51098857897448));
#384849=CARTESIAN_POINT('Ctrl Pts',(2.27916555827344,1.5310569223589,7.50433767179956));
#384850=CARTESIAN_POINT('Ctrl Pts',(2.27631435376174,1.53917964874325,7.50214974420965));
#384851=CARTESIAN_POINT('Ctrl Pts',(2.25370825427413,1.52822824501891,7.53887321589169));
#384852=CARTESIAN_POINT('Ctrl Pts',(2.24792705604506,1.52758586967435,7.53220407452061));
#384853=CARTESIAN_POINT('Ctrl Pts',(2.24503206325587,1.53566187962185,7.53003438070912));
#384854=CARTESIAN_POINT('Ctrl Pts',(2.22233951891749,1.52474272153654,7.56669465659231));
#384855=CARTESIAN_POINT('Ctrl Pts',(2.21659248649519,1.52410414251075,7.56004085833303));
#384856=CARTESIAN_POINT('Ctrl Pts',(2.21369080731581,1.53213638429418,7.55785582193789));
#384857=CARTESIAN_POINT('Ctrl Pts',(2.1909120781603,1.52125067502893,7.59443891967696));
#384858=CARTESIAN_POINT('Ctrl Pts',(2.18515671325648,1.52061117014313,7.58783901202978));
#384859=CARTESIAN_POINT('Ctrl Pts',(2.18229214298249,1.52860325467307,7.58560008491213));
#384860=CARTESIAN_POINT('',(2.2746186435041,1.53898896096139,7.50366116523517));
#384861=CARTESIAN_POINT('Ctrl Pts',(2.27461864350441,1.5389889609616,7.50366116523554));
#384862=CARTESIAN_POINT('Ctrl Pts',(2.27516108906422,1.53845991433661,7.50350835821027));
#384863=CARTESIAN_POINT('Ctrl Pts',(2.27564251620969,1.53795594418399,7.50345484956));
#384864=CARTESIAN_POINT('Ctrl Pts',(2.27607767238033,1.53746248185762,7.50349758195598));
#384865=CARTESIAN_POINT('Ctrl Pts',(2.27630093976789,1.53720929908808,7.50351950684424));
#384866=CARTESIAN_POINT('Ctrl Pts',(2.27653412976725,1.53693401335554,7.50357029184312));
#384867=CARTESIAN_POINT('Ctrl Pts',(2.27675169537736,1.53666237746656,7.50365515313923));
#384868=CARTESIAN_POINT('Ctrl Pts',(2.27708639938673,1.53624449147307,7.50378570417639));
#384869=CARTESIAN_POINT('Ctrl Pts',(2.27739422114994,1.53582319390499,7.50400001621911));
#384870=CARTESIAN_POINT('Ctrl Pts',(2.27764989774496,1.53542921218324,7.50428903009635));
#384871=CARTESIAN_POINT('Ctrl Pts',(2.27767827587995,1.53538548324324,7.50432110841318));
#384872=CARTESIAN_POINT('Ctrl Pts',(2.27770603964484,1.53534207924713,7.50435406373354));
#384873=CARTESIAN_POINT('Ctrl Pts',(2.27773317506314,1.53529903339035,7.50438785222352));
#384874=CARTESIAN_POINT('Ctrl Pts',(2.27789884983481,1.53503621774428,7.50459414719561));
#384875=CARTESIAN_POINT('Ctrl Pts',(2.27804330321255,1.53478229309384,7.50483629897752));
#384876=CARTESIAN_POINT('Ctrl Pts',(2.2781621451176,1.53454763795564,7.5050991045531));
#384877=CARTESIAN_POINT('Ctrl Pts',(2.27842432229668,1.53402996515189,7.50567888004914));
#384878=CARTESIAN_POINT('Ctrl Pts',(2.27857264696128,1.53358591053843,7.50637912803144));
#384879=CARTESIAN_POINT('Ctrl Pts',(2.27863797653864,1.53321727343213,7.50710440483569));
#384880=CARTESIAN_POINT('Ctrl Pts',(2.27865399664798,1.53312687629519,7.50728225710685));
#384881=CARTESIAN_POINT('Ctrl Pts',(2.27866548865362,1.53303924015847,7.50746498566954));
#384882=CARTESIAN_POINT('Ctrl Pts',(2.27867259735184,1.53295646489846,7.50764697238949));
#384883=CARTESIAN_POINT('Ctrl Pts',(2.27871081175707,1.53251148788106,7.50862528291181));
#384884=CARTESIAN_POINT('Ctrl Pts',(2.2786299483616,1.53216694270045,7.5096585683742));
#384885=CARTESIAN_POINT('Ctrl Pts',(2.27848810672668,1.53189089447242,7.510679598732));
#384886=CARTESIAN_POINT('Ctrl Pts',(2.27841005109606,1.53173898478435,7.51124147302577));
#384887=CARTESIAN_POINT('Ctrl Pts',(2.27831312390071,1.5316079795929,7.51180065547252));
#384888=CARTESIAN_POINT('Ctrl Pts',(2.27820463850914,1.5314938856342,7.512351757165));
#384889=CARTESIAN_POINT('Ctrl Pts',(2.2778297782658,1.53109964555726,7.51425603304536));
#384890=CARTESIAN_POINT('Ctrl Pts',(2.27726782574235,1.53086449499048,7.51626900505182));
#384891=CARTESIAN_POINT('Ctrl Pts',(2.27657644598837,1.53077061794521,7.51827788969245));
#384892=CARTESIAN_POINT('Ctrl Pts',(2.27653902720956,1.53076553714212,7.51838661432546));
#384893=CARTESIAN_POINT('Ctrl Pts',(2.27650122102354,1.53076087567598,7.51849533314857));
#384894=CARTESIAN_POINT('Ctrl Pts',(2.27646303399418,1.53075663254071,7.51860402984325));
#384895=CARTESIAN_POINT('Ctrl Pts',(2.19311322917842,1.52982084925552,7.57603338728985));
#384896=CARTESIAN_POINT('Ctrl Pts',(2.22032722053522,1.53288286616343,7.55196141284922));
#384897=CARTESIAN_POINT('Ctrl Pts',(2.24749441165088,1.53593874122898,7.52783573083105));
#384898=CARTESIAN_POINT('Ctrl Pts',(2.27461864356327,1.53898896096258,7.50366116530176));
#384899=CARTESIAN_POINT('Origin',(7.57821998246243E-16,5.28623820391022E-16,
7.49482233047033));
#384900=CARTESIAN_POINT('Origin',(2.22268971703919,1.59798519134824,7.49482233047033));
#384901=CARTESIAN_POINT('Origin',(0.,0.,7.50366116523517));
#384902=CARTESIAN_POINT('Origin',(2.26729799607035,1.53403586888162,7.49482233047033));
#384903=CARTESIAN_POINT('Ctrl Pts',(2.2227770683791,1.60771787746035,7.51860402984325));
#384904=CARTESIAN_POINT('Ctrl Pts',(2.22617803012196,1.61452447317728,7.51860402984325));
#384905=CARTESIAN_POINT('Ctrl Pts',(2.22169380199588,1.62067166636957,7.51860402984325));
#384906=CARTESIAN_POINT('Ctrl Pts',(2.22403986754686,1.61024521346864,7.51041458714367));
#384907=CARTESIAN_POINT('Ctrl Pts',(2.22511565711968,1.61598080781929,7.51004642900443));
#384908=CARTESIAN_POINT('Ctrl Pts',(2.22169256529901,1.62067336169246,7.50729136483011));
#384909=CARTESIAN_POINT('Ctrl Pts',(2.22683740462711,1.60993292596655,7.50215815450136));
#384910=CARTESIAN_POINT('Ctrl Pts',(2.22727886798611,1.61301564791056,7.49877163671529));
#384911=CARTESIAN_POINT('Ctrl Pts',(2.2252648615701,1.61581702288556,7.49481588533168));
#384912=CARTESIAN_POINT('Ctrl Pts',(2.22986588635879,1.60314444151893,7.50366171572174));
#384913=CARTESIAN_POINT('Ctrl Pts',(2.23283898515375,1.60528192738148,7.50000045605858));
#384914=CARTESIAN_POINT('Ctrl Pts',(2.23283898515367,1.60528192738158,7.49482233047317));
#384915=CARTESIAN_POINT('Origin',(2.21159519380499,1.61330497697698,7.51860402984325));
#384916=CARTESIAN_POINT('Origin',(2.21159519380499,1.61330497697698,9.));
#384917=CARTESIAN_POINT('Origin',(2.21159519380499,1.61330497697698,8.75721825406948));
#384918=CARTESIAN_POINT('Ctrl Pts',(2.21531434125614,1.59277907704499,8.78942910404912));
#384919=CARTESIAN_POINT('Ctrl Pts',(2.21782269718832,1.59775507736846,8.7967269950169));
#384920=CARTESIAN_POINT('Ctrl Pts',(2.21072551350638,1.6031683453063,8.79893251111267));
#384921=CARTESIAN_POINT('Ctrl Pts',(2.22022762891697,1.60261447348346,8.78111911759584));
#384922=CARTESIAN_POINT('Ctrl Pts',(2.2231946668817,1.60851693024665,8.78644465894815));
#384923=CARTESIAN_POINT('Ctrl Pts',(2.21795342948706,1.61470117978467,8.78817647674132));
#384924=CARTESIAN_POINT('Ctrl Pts',(2.22328970695173,1.60874412715453,8.76780923932029));
#384925=CARTESIAN_POINT('Ctrl Pts',(2.2267876170644,1.61571401679599,8.76988516158372));
#384926=CARTESIAN_POINT('Ctrl Pts',(2.22245839467584,1.62191032326894,8.77093053738833));
#384927=CARTESIAN_POINT('Ctrl Pts',(2.22269264364087,1.60754892857964,8.75371302330492));
#384928=CARTESIAN_POINT('Ctrl Pts',(2.22610538539147,1.61434741334549,8.7530082828756));
#384929=CARTESIAN_POINT('Ctrl Pts',(2.22157935547677,1.62050448996882,8.75267964240738));
#384930=CARTESIAN_POINT('Origin',(2.20532861076146,1.60076054719537,8.78727029226991));
#384931=CARTESIAN_POINT('Ctrl Pts',(2.18456153393017,1.53121811901794,8.85049129520029));
#384932=CARTESIAN_POINT('Ctrl Pts',(2.18717121304407,1.53644216794053,8.85711686593484));
#384933=CARTESIAN_POINT('Ctrl Pts',(2.1805960757769,1.54190736071222,8.85933012996512));
#384934=CARTESIAN_POINT('Ctrl Pts',(2.1952268368149,1.55256789483802,8.82945683644723));
#384935=CARTESIAN_POINT('Ctrl Pts',(2.19785817784331,1.55783530652517,8.83607469902391));
#384936=CARTESIAN_POINT('Ctrl Pts',(2.19123976416882,1.5632877044317,8.8382956714852));
#384937=CARTESIAN_POINT('Ctrl Pts',(2.20587624220564,1.57388584709559,8.80838214965001));
#384938=CARTESIAN_POINT('Ctrl Pts',(2.20851796773429,1.57917404644857,8.81501364461986));
#384939=CARTESIAN_POINT('Ctrl Pts',(2.20186790511425,1.5846353173396,8.81722098428721));
#384940=CARTESIAN_POINT('Ctrl Pts',(2.21651095806262,1.59517439388238,8.78727029226991));
#384941=CARTESIAN_POINT('Ctrl Pts',(2.21915312239054,1.60046347162265,8.79393457792714));
#384942=CARTESIAN_POINT('Ctrl Pts',(2.21248169808583,1.60595268950179,8.79610912703474));
#384943=CARTESIAN_POINT('Origin',(2.17337918662901,1.53680427233094,8.85049129520029));
#384944=CARTESIAN_POINT('Ctrl Pts',(2.19147106502122,1.52131278661258,8.85049129520029));
#384945=CARTESIAN_POINT('Ctrl Pts',(2.19727496193951,1.52195768411221,8.85711686593484));
#384946=CARTESIAN_POINT('Ctrl Pts',(2.20013305013605,1.51389963881731,8.85933012996512));
#384947=CARTESIAN_POINT('Ctrl Pts',(2.18633644119775,1.52074225510386,8.86332496987232));
#384948=CARTESIAN_POINT('Ctrl Pts',(2.18920666304212,1.51712096790994,8.86648636486738));
#384949=CARTESIAN_POINT('Ctrl Pts',(2.1857668385833,1.51232058151036,8.87206031107458));
#384950=CARTESIAN_POINT('Ctrl Pts',(2.1822370998361,1.5265650728407,8.86341338519875));
#384951=CARTESIAN_POINT('Ctrl Pts',(2.17979784447348,1.53050506064651,8.86654584966054));
#384952=CARTESIAN_POINT('Ctrl Pts',(2.17410071658646,1.52887200013753,8.87215952290714));
#384953=CARTESIAN_POINT('Ctrl Pts',(2.18456153393017,1.53121811901794,8.85049129520029));
#384954=CARTESIAN_POINT('Ctrl Pts',(2.18717121304407,1.53644216794053,8.85711686593484));
#384955=CARTESIAN_POINT('Ctrl Pts',(2.1805960757769,1.54190736071222,8.85933012996512));
#384956=CARTESIAN_POINT('Origin',(2.19285150152198,1.5088892446431,8.85049129520029));
#384957=CARTESIAN_POINT('Ctrl Pts',(2.26252622397766,1.52920804991442,8.78727029226991));
#384958=CARTESIAN_POINT('Ctrl Pts',(2.26840236764558,1.52986097508044,8.79393457792714));
#384959=CARTESIAN_POINT('Ctrl Pts',(2.27124974846883,1.5217042700088,8.79610912703474));
#384960=CARTESIAN_POINT('Ctrl Pts',(2.23887473584625,1.52658002502474,8.80838214965003));
#384961=CARTESIAN_POINT('Ctrl Pts',(2.24474990362954,1.52723284175577,8.81501364461996));
#384962=CARTESIAN_POINT('Ctrl Pts',(2.24757843466629,1.51910583586372,8.81722098428721));
#384963=CARTESIAN_POINT('Ctrl Pts',(2.21519057835741,1.52394837009352,8.82945683644722));
#384964=CARTESIAN_POINT('Ctrl Pts',(2.22104265112922,1.52459862063229,8.83607469902388));
#384965=CARTESIAN_POINT('Ctrl Pts',(2.22387378559008,1.51650438069503,8.8382956714852));
#384966=CARTESIAN_POINT('Ctrl Pts',(2.19147106502122,1.52131278661258,8.85049129520029));
#384967=CARTESIAN_POINT('Ctrl Pts',(2.19727496193951,1.52195768411221,8.85711686593484));
#384968=CARTESIAN_POINT('Ctrl Pts',(2.20013305013605,1.51389963881731,8.85933012996512));
#384969=CARTESIAN_POINT('Origin',(2.26390666047842,1.51678450794494,8.78727029226991));
#384970=CARTESIAN_POINT('Ctrl Pts',(2.27627900746589,1.53073616595189,8.75374538247848));
#384971=CARTESIAN_POINT('Ctrl Pts',(2.28383003900886,1.5315883989158,8.75304829418602));
#384972=CARTESIAN_POINT('Ctrl Pts',(2.28804536797154,1.52522430864732,8.75272238421917));
#384973=CARTESIAN_POINT('Ctrl Pts',(2.27759091723008,1.53088193866798,8.76769408445019));
#384974=CARTESIAN_POINT('Ctrl Pts',(2.28533204362688,1.53175493184133,8.76974318093969));
#384975=CARTESIAN_POINT('Ctrl Pts',(2.28965015289764,1.52556039476371,8.77077869880429));
#384976=CARTESIAN_POINT('Ctrl Pts',(2.27086681512296,1.53013479078127,8.78108014887989));
#384977=CARTESIAN_POINT('Ctrl Pts',(2.2774267151084,1.53087839651125,8.78639403366324));
#384978=CARTESIAN_POINT('Ctrl Pts',(2.28143162972609,1.52384399997467,8.78812224174741));
#384979=CARTESIAN_POINT('Ctrl Pts',(2.25984749613408,1.52891038029461,8.78944554828685));
#384980=CARTESIAN_POINT('Ctrl Pts',(2.26537530612658,1.52954262574047,8.79673892988685));
#384981=CARTESIAN_POINT('Ctrl Pts',(2.26800404459052,1.52102245623483,8.79894799272499));
#384982=CARTESIAN_POINT('Origin',(2.27784347049494,1.51833309057123,8.75721825406948));
#384983=CARTESIAN_POINT('Origin',(2.27784347049494,1.51833309057123,9.));
#384984=CARTESIAN_POINT('Origin',(2.27784347049494,1.51833309057123,7.51860402984325));
#384985=CARTESIAN_POINT('Ctrl Pts',(2.27461799196033,1.53898852013197,7.50366195182966));
#384986=CARTESIAN_POINT('Ctrl Pts',(2.27765095495659,1.5410405988764,7.50000065167735));
#384987=CARTESIAN_POINT('Ctrl Pts',(2.27765095495666,1.5410405988763,7.49482233047108));
#384988=CARTESIAN_POINT('Ctrl Pts',(2.27994696402869,1.53379661717627,7.50215800491336));
#384989=CARTESIAN_POINT('Ctrl Pts',(2.28299322537737,1.53314470539553,7.49877273257267));
#384990=CARTESIAN_POINT('Ctrl Pts',(2.28492774039883,1.5302855432837,7.49481816995647));
#384991=CARTESIAN_POINT('Ctrl Pts',(2.27926434158826,1.53106823982957,7.51043025814043));
#384992=CARTESIAN_POINT('Ctrl Pts',(2.28502241637524,1.53010008088881,7.51006209594514));
#384993=CARTESIAN_POINT('Ctrl Pts',(2.28824598651204,1.52526401164453,7.50731281821701));
#384994=CARTESIAN_POINT('Ctrl Pts',(2.27646153184156,1.53075646553773,7.51860402984326));
#384995=CARTESIAN_POINT('Ctrl Pts',(2.28402415878925,1.53159770928416,7.51860402984326));
#384996=CARTESIAN_POINT('Ctrl Pts',(2.28824458223236,1.52526611838206,7.51860402984327));
#384997=CARTESIAN_POINT('Origin',(0.,0.,7.5));
#384998=CARTESIAN_POINT('Origin',(2.28443929758134,1.37777905311492,7.5));
#384999=CARTESIAN_POINT('',(2.28443929758134,1.37777905311492,7.59394543036555));
#385000=CARTESIAN_POINT('',(2.28443929758134,1.37777905311492,8.85049129520029));
#385001=CARTESIAN_POINT('',(2.28443929758134,1.37777905311492,7.5));
#385002=CARTESIAN_POINT('',(2.35585431734962,1.38110557508644,8.78727029226991));
#385003=CARTESIAN_POINT('Ctrl Pts',(2.28443929758134,1.37777905311492,8.85049129520029));
#385004=CARTESIAN_POINT('Ctrl Pts',(2.30827890705323,1.37888950557938,8.82945686509571));
#385005=CARTESIAN_POINT('Ctrl Pts',(2.332083076063,1.37999830722197,8.80838212259896));
#385006=CARTESIAN_POINT('Ctrl Pts',(2.35585431734962,1.38110557508644,8.78727029226991));
#385007=CARTESIAN_POINT('',(2.36986171072476,1.38175804150005,8.75721825406948));
#385008=CARTESIAN_POINT('Origin',(2.32770859547085,1.37979474530318,8.75937679713124));
#385009=CARTESIAN_POINT('',(2.36986171072476,1.38175804150005,7.51860402984325));
#385010=CARTESIAN_POINT('',(2.36986171072476,1.38175804150005,7.5));
#385011=CARTESIAN_POINT('Ctrl Pts',(2.36986171072476,1.38175804150005,7.51860402984325));
#385012=CARTESIAN_POINT('Ctrl Pts',(2.35886108179033,1.38124563060989,7.52834476460825));
#385013=CARTESIAN_POINT('Ctrl Pts',(2.34785331140634,1.38073288706997,7.53807742314407));
#385014=CARTESIAN_POINT('Ctrl Pts',(2.3368381597891,1.38021979971113,7.54780169004674));
#385015=CARTESIAN_POINT('Ctrl Pts',(2.31939075494555,1.37940709706474,7.5632044032688));
#385016=CARTESIAN_POINT('Ctrl Pts',(2.30192480935482,1.37859353078764,7.57858609112103));
#385017=CARTESIAN_POINT('Ctrl Pts',(2.28443929758134,1.37777905311492,7.59394543036555));
#385018=CARTESIAN_POINT('Origin',(2.41658349078373,1.62573897887917,7.5));
#385019=CARTESIAN_POINT('',(2.32121750495508,1.4620017468866,8.75721825406948));
#385020=CARTESIAN_POINT('',(2.31416007290287,1.44988459233549,8.78727029226991));
#385021=CARTESIAN_POINT('Origin',(2.29624567806382,1.41912673461211,8.75658640621071));
#385022=CARTESIAN_POINT('',(2.27817859968916,1.38810672912948,8.85049129520029));
#385023=CARTESIAN_POINT('Ctrl Pts',(2.31416007290287,1.44988459233549,8.78727029226991));
#385024=CARTESIAN_POINT('Ctrl Pts',(2.30218326068065,1.42932118008403,8.80838212259896));
#385025=CARTESIAN_POINT('Ctrl Pts',(2.29018985827904,1.40872928356716,8.82945686509571));
#385026=CARTESIAN_POINT('Ctrl Pts',(2.27817859968916,1.38810672912948,8.85049129520029));
#385027=CARTESIAN_POINT('',(2.27817859968916,1.38810672912948,7.59394543036555));
#385028=CARTESIAN_POINT('',(2.27817859968916,1.38810672912948,7.5));
#385029=CARTESIAN_POINT('',(2.32121750495508,1.4620017468866,7.51860402984325));
#385030=CARTESIAN_POINT('Ctrl Pts',(2.27817859968916,1.38810672912948,7.59394543036555));
#385031=CARTESIAN_POINT('Ctrl Pts',(2.28698843374853,1.40323264462924,7.57858609112103));
#385032=CARTESIAN_POINT('Ctrl Pts',(2.29578840965636,1.41834163432014,7.56320440326857));
#385033=CARTESIAN_POINT('Ctrl Pts',(2.30457904406442,1.43343458525991,7.54780169004651));
#385034=CARTESIAN_POINT('Ctrl Pts',(2.31012887635665,1.44296328849364,7.53807742314383));
#385035=CARTESIAN_POINT('Ctrl Pts',(2.31567498971637,1.4524856065607,7.52834476460825));
#385036=CARTESIAN_POINT('Ctrl Pts',(2.32121750495508,1.4620017468866,7.51860402984325));
#385037=CARTESIAN_POINT('',(2.32121750495508,1.4620017468866,7.5));
#385038=CARTESIAN_POINT('Origin',(2.2841194059329,1.38464660685212,7.5));
#385039=CARTESIAN_POINT('Ctrl Pts',(2.27817859968916,1.38810672912948,8.85049129520029));
#385040=CARTESIAN_POINT('Ctrl Pts',(2.27808113169048,1.38793938287733,8.85097269580138));
#385041=CARTESIAN_POINT('Ctrl Pts',(2.27799216187779,1.38776991462376,8.85143669361005));
#385042=CARTESIAN_POINT('Ctrl Pts',(2.2779083675713,1.3875901145095,8.8519052845931));
#385043=CARTESIAN_POINT('Ctrl Pts',(2.27774447122185,1.38723843688849,8.852821818839));
#385044=CARTESIAN_POINT('Ctrl Pts',(2.27760476931614,1.38685619637749,8.85372622499636));
#385045=CARTESIAN_POINT('Ctrl Pts',(2.27750155151866,1.38643210212429,8.85462257735071));
#385046=CARTESIAN_POINT('Ctrl Pts',(2.27741586376914,1.3860800341377,8.85536669723987));
#385047=CARTESIAN_POINT('Ctrl Pts',(2.27735526963748,1.38569904887468,8.85610498449051));
#385048=CARTESIAN_POINT('Ctrl Pts',(2.27733469853654,1.38528139713442,8.85681338218371));
#385049=CARTESIAN_POINT('Ctrl Pts',(2.27731603023014,1.3849023775242,8.85745625420284));
#385050=CARTESIAN_POINT('Ctrl Pts',(2.27732949131403,1.38448843593453,8.85808743050666));
#385051=CARTESIAN_POINT('Ctrl Pts',(2.27740126538764,1.38402807170153,8.8586680450841));
#385052=CARTESIAN_POINT('Ctrl Pts',(2.27743438038933,1.3838156696239,8.85893592806395));
#385053=CARTESIAN_POINT('Ctrl Pts',(2.27748014042395,1.38359331526745,8.85919241173848));
#385054=CARTESIAN_POINT('Ctrl Pts',(2.27754269428291,1.38335963403902,8.85943017985534));
#385055=CARTESIAN_POINT('Ctrl Pts',(2.27762716051043,1.3830440952036,8.8597512372));
#385056=CARTESIAN_POINT('Ctrl Pts',(2.2777450155586,1.3827000384409,8.86004599534705));
#385057=CARTESIAN_POINT('Ctrl Pts',(2.27790469650042,1.38233497258256,8.86026130871721));
#385058=CARTESIAN_POINT('Ctrl Pts',(2.27796316019511,1.38220131167952,8.86034014101235));
#385059=CARTESIAN_POINT('Ctrl Pts',(2.27802809754115,1.3820628218386,8.86040910639693));
#385060=CARTESIAN_POINT('Ctrl Pts',(2.278098043917,1.38192341894476,8.86046313645507));
#385061=CARTESIAN_POINT('Ctrl Pts',(2.27820719465073,1.38170588189642,8.8605474499083));
#385062=CARTESIAN_POINT('Ctrl Pts',(2.27833165395477,1.38148024927839,8.86059655985668));
#385063=CARTESIAN_POINT('Ctrl Pts',(2.27846318335475,1.38126085010039,8.86059725258816));
#385064=CARTESIAN_POINT('Ctrl Pts',(2.2785950166402,1.38104094402264,8.86059794692011));
#385065=CARTESIAN_POINT('Ctrl Pts',(2.27873769344055,1.38082622749525,8.86056369958366));
#385066=CARTESIAN_POINT('Ctrl Pts',(2.27888029786019,1.38062632859761,8.86048590497774));
#385067=CARTESIAN_POINT('Ctrl Pts',(2.27891751336787,1.38057416093704,8.86046560290182));
#385068=CARTESIAN_POINT('Ctrl Pts',(2.27895528183714,1.38052237637027,8.86044257503091));
#385069=CARTESIAN_POINT('Ctrl Pts',(2.27899240966942,1.38047255574005,8.86041778462583));
#385070=CARTESIAN_POINT('Ctrl Pts',(2.27924223390883,1.38013732472094,8.860250975962));
#385071=CARTESIAN_POINT('Ctrl Pts',(2.27949684175641,1.37984622804255,8.8599848982295));
#385072=CARTESIAN_POINT('Ctrl Pts',(2.27974242457589,1.37960218414178,8.85968173251461));
#385073=CARTESIAN_POINT('Ctrl Pts',(2.27987232381717,1.37947309890031,8.85952137522076));
#385074=CARTESIAN_POINT('Ctrl Pts',(2.28000206733072,1.37935455443873,8.85934740853961));
#385075=CARTESIAN_POINT('Ctrl Pts',(2.2801287768589,1.37924707484728,8.8591675900182));
#385076=CARTESIAN_POINT('Ctrl Pts',(2.28063758147686,1.37881548842082,8.85844552518696));
#385077=CARTESIAN_POINT('Ctrl Pts',(2.28112426400979,1.3785356165466,8.85759444184125));
#385078=CARTESIAN_POINT('Ctrl Pts',(2.28154157522217,1.37834306627386,8.8568349891514));
#385079=CARTESIAN_POINT('Ctrl Pts',(2.28158524572916,1.37832291640062,8.85675551444999));
#385080=CARTESIAN_POINT('Ctrl Pts',(2.28162816120066,1.37830374221057,8.85667699793652));
#385081=CARTESIAN_POINT('Ctrl Pts',(2.28167026988731,1.37828548282268,8.85659965593547));
#385082=CARTESIAN_POINT('Ctrl Pts',(2.28223865508833,1.3780390166732,8.85555568965886));
#385083=CARTESIAN_POINT('Ctrl Pts',(2.28282050306976,1.37788423350347,8.85434650606346));
#385084=CARTESIAN_POINT('Ctrl Pts',(2.28341709248037,1.37781436229031,8.85297329937118));
#385085=CARTESIAN_POINT('Ctrl Pts',(2.28375263767311,1.37777506399023,8.85220095427747));
#385086=CARTESIAN_POINT('Ctrl Pts',(2.28409301987351,1.3777629234491,8.85137579139184));
#385087=CARTESIAN_POINT('Ctrl Pts',(2.28443929758134,1.37777905311492,8.85049129520029));
#385088=CARTESIAN_POINT('Origin',(2.2841194059329,1.38464660685212,7.59394543036555));
#385089=CARTESIAN_POINT('Ctrl Pts',(2.27789561720848,1.38762086650577,7.59443877723642));
#385090=CARTESIAN_POINT('Ctrl Pts',(2.27498116993601,1.38261694896602,7.58783886950016));
#385091=CARTESIAN_POINT('Ctrl Pts',(2.28112970280111,1.3767624869802,7.58559994247159));
#385092=CARTESIAN_POINT('Ctrl Pts',(2.29380549936271,1.41493710554661,7.5667025222214));
#385093=CARTESIAN_POINT('Ctrl Pts',(2.29089526429404,1.40994042008829,7.56004874999031));
#385094=CARTESIAN_POINT('Ctrl Pts',(2.29706549617269,1.40403579513669,7.55786368756704));
#385095=CARTESIAN_POINT('Ctrl Pts',(2.30968567140157,1.44220233424022,7.5388891333356));
#385096=CARTESIAN_POINT('Ctrl Pts',(2.3067581406633,1.43717595323564,7.5322200213728));
#385097=CARTESIAN_POINT('Ctrl Pts',(2.31297108856251,1.43125972782396,7.53005029815327));
#385098=CARTESIAN_POINT('Ctrl Pts',(2.32553541473658,1.4694153188166,7.51101258149734));
#385099=CARTESIAN_POINT('Ctrl Pts',(2.32257239700633,1.46432800894107,7.5043616886572));
#385100=CARTESIAN_POINT('Ctrl Pts',(2.32884576547033,1.45843289828396,7.50217374673251));
#385101=CARTESIAN_POINT('',(2.32799867143117,1.4569829035209,7.50366116523517));
#385102=CARTESIAN_POINT('Ctrl Pts',(2.32121750495508,1.4620017468866,7.51860402984325));
#385103=CARTESIAN_POINT('Ctrl Pts',(2.32143976369038,1.46238335076547,7.51734760759494));
#385104=CARTESIAN_POINT('Ctrl Pts',(2.32169201845767,1.46269824025776,7.51608817408573));
#385105=CARTESIAN_POINT('Ctrl Pts',(2.32198411096283,1.46293734222614,7.5148100591312));
#385106=CARTESIAN_POINT('Ctrl Pts',(2.32224869533378,1.46315392650263,7.51365231206384));
#385107=CARTESIAN_POINT('Ctrl Pts',(2.32254618173406,1.46330882470793,7.51247773061043));
#385108=CARTESIAN_POINT('Ctrl Pts',(2.32288847583597,1.46336660528917,7.51129758471022));
#385109=CARTESIAN_POINT('Ctrl Pts',(2.32331390831319,1.46343841995286,7.50983079813402));
#385110=CARTESIAN_POINT('Ctrl Pts',(2.32379714857049,1.46334507583531,7.50839324291155));
#385111=CARTESIAN_POINT('Ctrl Pts',(2.32432608821462,1.46300494832451,7.50715379678855));
#385112=CARTESIAN_POINT('Ctrl Pts',(2.32457044308917,1.46284781921505,7.50658120839351));
#385113=CARTESIAN_POINT('Ctrl Pts',(2.32485414912167,1.46260769292224,7.50598221009429));
#385114=CARTESIAN_POINT('Ctrl Pts',(2.32515575918815,1.46227292178528,7.50545747549611));
#385115=CARTESIAN_POINT('Ctrl Pts',(2.32531670765533,1.46209427754447,7.50517746087247));
#385116=CARTESIAN_POINT('Ctrl Pts',(2.32548465021346,1.46188688045126,7.50491486231392));
#385117=CARTESIAN_POINT('Ctrl Pts',(2.32565384315538,1.46165517302971,7.50468370960993));
#385118=CARTESIAN_POINT('Ctrl Pts',(2.32590683997244,1.46130869734652,7.50433806340447));
#385119=CARTESIAN_POINT('Ctrl Pts',(2.32616976944411,1.46089714676686,7.50405484070984));
#385120=CARTESIAN_POINT('Ctrl Pts',(2.3264243200522,1.46044785276346,7.50385766036131));
#385121=CARTESIAN_POINT('Ctrl Pts',(2.32645154028312,1.46039980775341,7.50383657498791));
#385122=CARTESIAN_POINT('Ctrl Pts',(2.32647866521304,1.46035135950571,7.50381643264937));
#385123=CARTESIAN_POINT('Ctrl Pts',(2.3265056731432,1.46030256203688,7.50379723213559));
#385124=CARTESIAN_POINT('Ctrl Pts',(2.32668595991194,1.4599768229697,7.50366906242519));
#385125=CARTESIAN_POINT('Ctrl Pts',(2.32686432570829,1.45962808883253,7.50358235568538));
#385126=CARTESIAN_POINT('Ctrl Pts',(2.32702816834755,1.45928781937696,7.5035341175365));
#385127=CARTESIAN_POINT('Ctrl Pts',(2.3272738318417,1.45877762383939,7.50346178989177));
#385128=CARTESIAN_POINT('Ctrl Pts',(2.32751641693376,1.45821832421325,7.50346967198527));
#385129=CARTESIAN_POINT('Ctrl Pts',(2.32773766577598,1.45766193758503,7.50354272648692));
#385130=CARTESIAN_POINT('Ctrl Pts',(2.32782867000437,1.45743308424832,7.50357277531559));
#385131=CARTESIAN_POINT('Ctrl Pts',(2.32791607531214,1.45720508021277,7.50361331098761));
#385132=CARTESIAN_POINT('Ctrl Pts',(2.32799867143237,1.45698290352165,7.50366116523659));
#385133=CARTESIAN_POINT('',(2.28662319996352,1.38616442150718,7.57603338622103));
#385134=CARTESIAN_POINT('Origin',(2.29418152300578,1.39074298486225,7.5848687342763));
#385135=CARTESIAN_POINT('Ctrl Pts',(2.32799867145534,1.4569829035729,7.50366116529969));
#385136=CARTESIAN_POINT('Ctrl Pts',(2.31423007474033,1.43341484163944,7.5278357307971));
#385137=CARTESIAN_POINT('Ctrl Pts',(2.30043891757453,1.40980978649596,7.55196141284068));
#385138=CARTESIAN_POINT('Ctrl Pts',(2.28662320026408,1.38616442272263,7.57603338728831));
#385139=CARTESIAN_POINT('Ctrl Pts',(2.27884811390189,1.38890690800898,7.59639677331371));
#385140=CARTESIAN_POINT('Ctrl Pts',(2.26672396437058,1.37410138795021,7.59974925422225));
#385141=CARTESIAN_POINT('Ctrl Pts',(2.28545841158006,1.37800253058071,7.59639677331372));
#385142=CARTESIAN_POINT('Ctrl Pts',(2.2759238256025,1.38632550489715,7.58707626057422));
#385143=CARTESIAN_POINT('Ctrl Pts',(2.27553575658722,1.37944314817572,7.58811717123965));
#385144=CARTESIAN_POINT('Ctrl Pts',(2.28181714606147,1.37660385638466,7.58707626057424));
#385145=CARTESIAN_POINT('Ctrl Pts',(2.28198336987503,1.38586992233497,7.58015376756929));
#385146=CARTESIAN_POINT('Ctrl Pts',(2.28144597464152,1.38302595709235,7.5820876076604));
#385147=CARTESIAN_POINT('Ctrl Pts',(2.28421599812537,1.38218696851293,7.5801537675693));
#385148=CARTESIAN_POINT('Ctrl Pts',(2.28662319925573,1.38616442107835,7.57603338509286));
#385149=CARTESIAN_POINT('Ctrl Pts',(2.28662319925573,1.38616442107835,7.57603338509286));
#385150=CARTESIAN_POINT('Ctrl Pts',(2.28662319925573,1.38616442107835,7.57603338509286));
#385151=CARTESIAN_POINT('Origin',(2.29417856487513,1.3907478646081,7.58486873427623));
#385152=CARTESIAN_POINT('Ctrl Pts',(2.37845886339418,1.38215849811745,7.51098857897448));
#385153=CARTESIAN_POINT('Ctrl Pts',(2.37257792201276,1.38188456301553,7.50433767179956));
#385154=CARTESIAN_POINT('Ctrl Pts',(2.37025300047281,1.39017327768763,7.50214974420965));
#385155=CARTESIAN_POINT('Ctrl Pts',(2.34699168879536,1.38069275256386,7.53887321589168));
#385156=CARTESIAN_POINT('Ctrl Pts',(2.34118121152847,1.38042209969057,7.53220407452061));
#385157=CARTESIAN_POINT('Ctrl Pts',(2.33880959854635,1.38866699943437,7.53003438070912));
#385158=CARTESIAN_POINT('Ctrl Pts',(2.31546408561356,1.37922419223812,7.56669465659234));
#385159=CARTESIAN_POINT('Ctrl Pts',(2.30968794718703,1.37895513887304,7.56004085833298));
#385160=CARTESIAN_POINT('Ctrl Pts',(2.30730685731678,1.38715678877751,7.55785582193789));
#385161=CARTESIAN_POINT('Ctrl Pts',(2.28387747971605,1.37775288355733,7.59443891967696));
#385162=CARTESIAN_POINT('Ctrl Pts',(2.27809296660797,1.37748344009836,7.58783901202978));
#385163=CARTESIAN_POINT('Ctrl Pts',(2.27574633651477,1.38564263768109,7.58560008491213));
#385164=CARTESIAN_POINT('',(2.36854855682562,1.39009162622351,7.50366116523517));
#385165=CARTESIAN_POINT('Ctrl Pts',(2.36854855682595,1.3900916262237,7.50366116523554));
#385166=CARTESIAN_POINT('Ctrl Pts',(2.36905599173953,1.3895289119754,7.50350835821027));
#385167=CARTESIAN_POINT('Ctrl Pts',(2.36950414026276,1.38899513214038,7.50345484956));
#385168=CARTESIAN_POINT('Ctrl Pts',(2.36990678611857,1.38847480313371,7.50349758195598));
#385169=CARTESIAN_POINT('Ctrl Pts',(2.3701133733036,1.38820783576469,7.50351950684424));
#385170=CARTESIAN_POINT('Ctrl Pts',(2.37032844657166,1.38791817510165,7.50357029184312));
#385171=CARTESIAN_POINT('Ctrl Pts',(2.37052816139873,1.38763315784124,7.50365515313923));
#385172=CARTESIAN_POINT('Ctrl Pts',(2.37083540367528,1.38719468587983,7.50378570417639));
#385173=CARTESIAN_POINT('Ctrl Pts',(2.37111560035779,1.38675453170472,7.50400001621911));
#385174=CARTESIAN_POINT('Ctrl Pts',(2.37134550914225,1.38634497820498,7.50428903009634));
#385175=CARTESIAN_POINT('Ctrl Pts',(2.37137102724851,1.38629952091742,7.50432110841318));
#385176=CARTESIAN_POINT('Ctrl Pts',(2.37139595306619,1.38625442726895,7.50435406373354));
#385177=CARTESIAN_POINT('Ctrl Pts',(2.37142027477435,1.38620973128228,7.50438785222352));
#385178=CARTESIAN_POINT('Ctrl Pts',(2.37156877049318,1.38593684080007,7.50459414719561));
#385179=CARTESIAN_POINT('Ctrl Pts',(2.37169665806774,1.38567418270537,7.50483629897752));
#385180=CARTESIAN_POINT('Ctrl Pts',(2.37180022139303,1.38543239546432,7.5050991045531));
#385181=CARTESIAN_POINT('Ctrl Pts',(2.37202869249057,1.38489898852534,7.50567888004914));
#385182=CARTESIAN_POINT('Ctrl Pts',(2.37214826172947,1.38444634307581,7.50637912803144));
#385183=CARTESIAN_POINT('Ctrl Pts',(2.37218983841972,1.38407427769359,7.50710440483569));
#385184=CARTESIAN_POINT('Ctrl Pts',(2.37220003384958,1.38398303987534,7.50728225710685));
#385185=CARTESIAN_POINT('Ctrl Pts',(2.3722058873771,1.38389484750112,7.50746498566954));
#385186=CARTESIAN_POINT('Ctrl Pts',(2.37220767804061,1.38381178685591,7.50764697238949));
#385187=CARTESIAN_POINT('Ctrl Pts',(2.37221730415485,1.38336527568616,7.50862528291181));
#385188=CARTESIAN_POINT('Ctrl Pts',(2.37211453181639,1.3830266193461,7.50965856837421));
#385189=CARTESIAN_POINT('Ctrl Pts',(2.37195529513962,1.38276022611353,7.51067959873201));
#385190=CARTESIAN_POINT('Ctrl Pts',(2.37186766699554,1.38261362958163,7.51124147302578));
#385191=CARTESIAN_POINT('Ctrl Pts',(2.37176254541607,1.38248910370112,7.51180065547252));
#385192=CARTESIAN_POINT('Ctrl Pts',(2.37164697289434,1.3823821948436,7.51235175716501));
#385193=CARTESIAN_POINT('Ctrl Pts',(2.37124762379312,1.38201278215343,7.51425603304536));
#385194=CARTESIAN_POINT('Ctrl Pts',(2.37067175971286,1.38181411915051,7.5162690050518));
#385195=CARTESIAN_POINT('Ctrl Pts',(2.3699757857498,1.38176473183863,7.51827788969243));
#385196=CARTESIAN_POINT('Ctrl Pts',(2.36993811832371,1.38176205890398,7.51838661432545));
#385197=CARTESIAN_POINT('Ctrl Pts',(2.36990009115339,1.38175982926598,7.51849533314856));
#385198=CARTESIAN_POINT('Ctrl Pts',(2.36986171072477,1.38175804150005,7.51860402984325));
#385199=CARTESIAN_POINT('Ctrl Pts',(2.2866232011813,1.38616442121187,7.57603338728985));
#385200=CARTESIAN_POINT('Ctrl Pts',(2.31397746257105,1.38747654046485,7.55196141284922));
#385201=CARTESIAN_POINT('Ctrl Pts',(2.34128462636657,1.38878552899631,7.52783573083105));
#385202=CARTESIAN_POINT('Ctrl Pts',(2.36854855688475,1.3900916262209,7.50366116530176));
#385203=CARTESIAN_POINT('Origin',(7.90134016134189E-16,4.78983883923441E-16,
7.49482233047033));
#385204=CARTESIAN_POINT('Origin',(2.32050622536841,1.45229374026967,7.49482233047033));
#385205=CARTESIAN_POINT('Origin',(0.,0.,7.50366116523517));
#385206=CARTESIAN_POINT('Origin',(2.36092560474802,1.38561774629412,7.49482233047033));
#385207=CARTESIAN_POINT('Ctrl Pts',(2.32121697257583,1.46200083291477,7.51860402984325));
#385208=CARTESIAN_POINT('Ctrl Pts',(2.32504704676294,1.46857554338378,7.51860402984325));
#385209=CARTESIAN_POINT('Ctrl Pts',(2.32096588398457,1.47499741199086,7.51860402984325));
#385210=CARTESIAN_POINT('Ctrl Pts',(2.32263910416129,1.46444206841972,7.51041458714366));
#385211=CARTESIAN_POINT('Ctrl Pts',(2.32408016420081,1.47009695230205,7.51004642900443));
#385212=CARTESIAN_POINT('Ctrl Pts',(2.32096475844833,1.47499918306597,7.5072913648301));
#385213=CARTESIAN_POINT('Ctrl Pts',(2.3254108850726,1.46395118372964,7.50215815450137));
#385214=CARTESIAN_POINT('Ctrl Pts',(2.32604895207089,1.46699928723627,7.49877163671528));
#385215=CARTESIAN_POINT('Ctrl Pts',(2.32421856835796,1.46992394432006,7.4948158853317));
#385216=CARTESIAN_POINT('Ctrl Pts',(2.32799820477188,1.45698261146063,7.50366171572174));
#385217=CARTESIAN_POINT('Ctrl Pts',(2.33110214420591,1.45892521853541,7.50000045605858));
#385218=CARTESIAN_POINT('Ctrl Pts',(2.33110214420585,1.45892521853552,7.49482233047317));
#385219=CARTESIAN_POINT('Origin',(2.31041603905737,1.46829287829999,7.51860402984325));
#385220=CARTESIAN_POINT('Origin',(2.31041603905737,1.46829287829999,9.));
#385221=CARTESIAN_POINT('Origin',(2.31041603905737,1.46829287829999,8.75721825406948));
#385222=CARTESIAN_POINT('Ctrl Pts',(2.31281244619726,1.44757086443546,8.78942910404912));
#385223=CARTESIAN_POINT('Ctrl Pts',(2.31563446187851,1.45237593011623,8.79672699501691));
#385224=CARTESIAN_POINT('Ctrl Pts',(2.30889868938921,1.45823279403427,8.79893251111267));
#385225=CARTESIAN_POINT('Ctrl Pts',(2.31834579499506,1.45707125757588,8.78111911759583));
#385226=CARTESIAN_POINT('Ctrl Pts',(2.32168490856531,1.46277148833352,8.78644465894813));
#385227=CARTESIAN_POINT('Ctrl Pts',(2.31685066608332,1.46927883890044,8.78817647674132));
#385228=CARTESIAN_POINT('Ctrl Pts',(2.32179430992118,1.46299212920275,8.7678092393203));
#385229=CARTESIAN_POINT('Ctrl Pts',(2.32573159556495,1.46972358658803,8.76988516158374));
#385230=CARTESIAN_POINT('Ctrl Pts',(2.3218082667469,1.47618453631557,8.77093053738833));
#385231=CARTESIAN_POINT('Ctrl Pts',(2.32112189670533,1.46183764026921,8.75371302330492));
#385232=CARTESIAN_POINT('Ctrl Pts',(2.32496320702647,1.46840350170427,8.75300828287559));
#385233=CARTESIAN_POINT('Ctrl Pts',(2.32084096157934,1.47483791168561,8.75267964240738));
#385234=CARTESIAN_POINT('Origin',(2.30335860700516,1.45617572374888,8.78727029226991));
#385235=CARTESIAN_POINT('Ctrl Pts',(2.27817859968916,1.38810672912948,8.85049129520029));
#385236=CARTESIAN_POINT('Ctrl Pts',(2.28111762290109,1.39315284196837,8.85711686593484));
#385237=CARTESIAN_POINT('Ctrl Pts',(2.27490615106173,1.39902807640649,8.85933012996512));
#385238=CARTESIAN_POINT('Ctrl Pts',(2.29018987439859,1.40872931124339,8.82945683644723));
#385239=CARTESIAN_POINT('Ctrl Pts',(2.29315329328014,1.41381730986979,8.83607469902389));
#385240=CARTESIAN_POINT('Ctrl Pts',(2.28689781417967,1.4196825484601,8.8382956714852));
#385241=CARTESIAN_POINT('Ctrl Pts',(2.30218324533449,1.42932115373567,8.80838214965002));
#385242=CARTESIAN_POINT('Ctrl Pts',(2.30515835925054,1.43442923198018,8.81501364461988));
#385243=CARTESIAN_POINT('Ctrl Pts',(2.29887186472475,1.44030535307938,8.81722098428721));
#385244=CARTESIAN_POINT('Ctrl Pts',(2.31416007290287,1.44988459233549,8.78727029226991));
#385245=CARTESIAN_POINT('Ctrl Pts',(2.31713568099512,1.45499351904858,8.79393457792714));
#385246=CARTESIAN_POINT('Ctrl Pts',(2.31082965924419,1.46089889836366,8.79610912703474));
#385247=CARTESIAN_POINT('Origin',(2.26737713379144,1.39439786054287,8.85049129520029));
#385248=CARTESIAN_POINT('Ctrl Pts',(2.28443929758134,1.37777905311492,8.85049129520029));
#385249=CARTESIAN_POINT('Ctrl Pts',(2.29027258849561,1.37805076865117,8.85711686593484));
#385250=CARTESIAN_POINT('Ctrl Pts',(2.29260852370876,1.36982616113508,8.85933012996512));
#385251=CARTESIAN_POINT('Ctrl Pts',(2.27927866931394,1.37753867030226,8.86332496987232));
#385252=CARTESIAN_POINT('Ctrl Pts',(2.28191097731257,1.3737409276863,8.86648636486737));
#385253=CARTESIAN_POINT('Ctrl Pts',(2.27817065852941,1.36917079450518,8.87206031107458));
#385254=CARTESIAN_POINT('Ctrl Pts',(2.27556081970207,1.38361217013839,8.86341338519876));
#385255=CARTESIAN_POINT('Ctrl Pts',(2.27337901193666,1.3877003464444,8.86654584966059));
#385256=CARTESIAN_POINT('Ctrl Pts',(2.26758895886382,1.38643565747033,8.87215952290713));
#385257=CARTESIAN_POINT('Ctrl Pts',(2.27817859968916,1.38810672912948,8.85049129520029));
#385258=CARTESIAN_POINT('Ctrl Pts',(2.28111762290109,1.39315284196837,8.85711686593484));
#385259=CARTESIAN_POINT('Ctrl Pts',(2.27490615106173,1.39902807640649,8.85933012996512));
#385260=CARTESIAN_POINT('Origin',(2.28502091876033,1.36529259177457,8.85049129520029));
#385261=CARTESIAN_POINT('Ctrl Pts',(2.35585431734962,1.38110557508644,8.78727029226991));
#385262=CARTESIAN_POINT('Ctrl Pts',(2.36176022090917,1.38138067293023,8.79393457792714));
#385263=CARTESIAN_POINT('Ctrl Pts',(2.36407914959489,1.37305829436826,8.79610912703474));
#385264=CARTESIAN_POINT('Ctrl Pts',(2.33208304560438,1.3799983058032,8.80838214965002));
#385265=CARTESIAN_POINT('Ctrl Pts',(2.33798796833692,1.38027335795994,8.81501364461995));
#385266=CARTESIAN_POINT('Ctrl Pts',(2.340289988798,1.37198182526738,8.81722098428721));
#385267=CARTESIAN_POINT('Ctrl Pts',(2.30827893904692,1.37888950706965,8.82945683644729));
#385268=CARTESIAN_POINT('Ctrl Pts',(2.31416064980264,1.37916347800914,8.83607469902394));
#385269=CARTESIAN_POINT('Ctrl Pts',(2.31646736766072,1.37090447714819,8.8382956714852));
#385270=CARTESIAN_POINT('Ctrl Pts',(2.28443929758134,1.37777905311492,8.85049129520029));
#385271=CARTESIAN_POINT('Ctrl Pts',(2.29027258849561,1.37805076865117,8.85711686593484));
#385272=CARTESIAN_POINT('Ctrl Pts',(2.29260852370876,1.36982616113508,8.85933012996512));
#385273=CARTESIAN_POINT('Origin',(2.35643593852861,1.36861911374609,8.78727029226991));
#385274=CARTESIAN_POINT('Ctrl Pts',(2.36967675099987,1.38174940758219,8.75374538247849));
#385275=CARTESIAN_POINT('Ctrl Pts',(2.37726687089215,1.38211609329003,8.75304829418603));
#385276=CARTESIAN_POINT('Ctrl Pts',(2.38106579034591,1.37549500167362,8.75272238421917));
#385277=CARTESIAN_POINT('Ctrl Pts',(2.37099530499473,1.38181082644541,8.76769408445016));
#385278=CARTESIAN_POINT('Ctrl Pts',(2.37877645928179,1.38218605028951,8.76974318093965));
#385279=CARTESIAN_POINT('Ctrl Pts',(2.38268881118068,1.3757275783418,8.7707786988043));
#385280=CARTESIAN_POINT('Ctrl Pts',(2.3642371483471,1.38149602835534,8.78108014887993));
#385281=CARTESIAN_POINT('Ctrl Pts',(2.37083121329715,1.38181781203247,8.78639403366329));
#385282=CARTESIAN_POINT('Ctrl Pts',(2.37437720405471,1.37454127265745,8.78812224174741));
#385283=CARTESIAN_POINT('Ctrl Pts',(2.35316202148166,1.380980143743,8.78944554828684));
#385284=CARTESIAN_POINT('Ctrl Pts',(2.35871898210047,1.38125692217054,8.79673892988684));
#385285=CARTESIAN_POINT('Ctrl Pts',(2.36079643040481,1.37258583441529,8.79894799272499));
#385286=CARTESIAN_POINT('Origin',(2.37044333190375,1.3692715801597,8.75721825406948));
#385287=CARTESIAN_POINT('Origin',(2.37044333190375,1.3692715801597,9.));
#385288=CARTESIAN_POINT('Origin',(2.37044333190375,1.3692715801597,7.51860402984325));
#385289=CARTESIAN_POINT('Ctrl Pts',(2.36854787837648,1.39009122804437,7.50366195182966));
#385290=CARTESIAN_POINT('Ctrl Pts',(2.37170608696156,1.39194476796657,7.50000065167735));
#385291=CARTESIAN_POINT('Ctrl Pts',(2.37170608696162,1.39194476796647,7.49482233047108));
#385292=CARTESIAN_POINT('Ctrl Pts',(2.37353325513569,1.38456856399743,7.50215800491337));
#385293=CARTESIAN_POINT('Ctrl Pts',(2.37653148948252,1.38372281700464,7.49877273257267));
#385294=CARTESIAN_POINT('Ctrl Pts',(2.37827884268993,1.38074558454504,7.49481816995647));
#385295=CARTESIAN_POINT('Ctrl Pts',(2.37267722747951,1.38188952816453,7.51043025814041));
#385296=CARTESIAN_POINT('Ctrl Pts',(2.37836144152797,1.38055443729187,7.51006209594513));
#385297=CARTESIAN_POINT('Ctrl Pts',(2.38126854047387,1.37552176942275,7.507312818217));
#385298=CARTESIAN_POINT('Ctrl Pts',(2.36986020095857,1.38175797108345,7.51860402984325));
#385299=CARTESIAN_POINT('Ctrl Pts',(2.37746118834999,1.3821129472322,7.51860402984324));
#385300=CARTESIAN_POINT('Ctrl Pts',(2.38126727405857,1.37552396180426,7.51860402984325));
#385301=CARTESIAN_POINT('Origin',(0.,0.,7.5));
#385302=CARTESIAN_POINT('Origin',(2.36802027905701,1.22858372995534,7.5));
#385303=CARTESIAN_POINT('',(2.36802027905701,1.22858372995534,7.59394543036555));
#385304=CARTESIAN_POINT('',(2.36802027905701,1.22858372995534,8.85049129520029));
#385305=CARTESIAN_POINT('',(2.36802027905701,1.22858372995534,7.5));
#385306=CARTESIAN_POINT('',(2.43950170000241,1.22732784120422,8.78727029226991));
#385307=CARTESIAN_POINT('Ctrl Pts',(2.36802027905701,1.22858372995534,8.85049129520029));
#385308=CARTESIAN_POINT('Ctrl Pts',(2.39188205442812,1.22816449185299,8.82945686509571));
#385309=CARTESIAN_POINT('Ctrl Pts',(2.41570835638483,1.22774587699877,8.80838212259895));
#385310=CARTESIAN_POINT('Ctrl Pts',(2.43950170000242,1.22732784120422,8.78727029226991));
#385311=CARTESIAN_POINT('',(2.45352211735224,1.2270815102807,8.75721825406948));
#385312=CARTESIAN_POINT('Origin',(2.41132982137661,1.2278230072536,8.75937679713168));
#385313=CARTESIAN_POINT('',(2.45352211735224,1.2270815102807,7.51860402984325));
#385314=CARTESIAN_POINT('',(2.45352211735224,1.2270815102807,7.5));
#385315=CARTESIAN_POINT('Ctrl Pts',(2.45352211735224,1.2270815102807,7.51860402984325));
#385316=CARTESIAN_POINT('Ctrl Pts',(2.44251126011131,1.22727496490942,7.52834476460825));
#385317=CARTESIAN_POINT('Ctrl Pts',(2.43149325478075,1.2274685451261,7.53807742314407));
#385318=CARTESIAN_POINT('Ctrl Pts',(2.42046786135393,1.2276622551475,7.54780169004674));
#385319=CARTESIAN_POINT('Ctrl Pts',(2.40300423403753,1.22796908135228,7.5632044032688));
#385320=CARTESIAN_POINT('Ctrl Pts',(2.38552204873489,1.22827623361052,7.57858609112103));
#385321=CARTESIAN_POINT('Ctrl Pts',(2.36802027905701,1.22858372995534,7.59394543036555));
#385322=CARTESIAN_POINT('Origin',(2.51577981483215,1.46756768793083,7.5));
#385323=CARTESIAN_POINT('',(2.41011908817656,1.31027699133287,8.75721825406948));
#385324=CARTESIAN_POINT('',(2.40229980761778,1.29863690399944,8.78727029226991));
#385325=CARTESIAN_POINT('Origin',(2.38245155711292,1.26909002081042,8.75658640621015));
#385326=CARTESIAN_POINT('',(2.36243414091424,1.23929131094307,8.85049129520029));
#385327=CARTESIAN_POINT('Ctrl Pts',(2.40229980761778,1.29863690399944,8.78727029226991));
#385328=CARTESIAN_POINT('Ctrl Pts',(2.38903010069427,1.27888309847761,8.80838212259896));
#385329=CARTESIAN_POINT('Ctrl Pts',(2.37574201268453,1.2591019301508,8.82945686509571));
#385330=CARTESIAN_POINT('Ctrl Pts',(2.36243414091424,1.23929131094307,8.85049129520029));
#385331=CARTESIAN_POINT('',(2.36243414091424,1.23929131094307,7.59394543036555));
#385332=CARTESIAN_POINT('',(2.36243414091424,1.23929131094307,7.5));
#385333=CARTESIAN_POINT('',(2.41011908817656,1.31027699133287,7.51860402984325));
#385334=CARTESIAN_POINT('Ctrl Pts',(2.36243414091424,1.23929131094307,7.59394543036555));
#385335=CARTESIAN_POINT('Ctrl Pts',(2.37219499495816,1.25382170062101,7.57858609112103));
#385336=CARTESIAN_POINT('Ctrl Pts',(2.38194492666489,1.26833583087991,7.56320440326857));
#385337=CARTESIAN_POINT('Ctrl Pts',(2.39168450845862,1.28283455385297,7.54780169004651));
#385338=CARTESIAN_POINT('Ctrl Pts',(2.39783344413751,1.29198810036814,7.53807742314383));
#385339=CARTESIAN_POINT('Ctrl Pts',(2.4039782594258,1.30113551310847,7.52834476460825));
#385340=CARTESIAN_POINT('Ctrl Pts',(2.41011908817656,1.31027699133287,7.51860402984325));
#385341=CARTESIAN_POINT('',(2.41011908817656,1.31027699133287,7.5));
#385342=CARTESIAN_POINT('Origin',(2.36814105033893,1.23545766909512,7.5));
#385343=CARTESIAN_POINT('Ctrl Pts',(2.36243414091424,1.23929131094307,8.85049129520029));
#385344=CARTESIAN_POINT('Ctrl Pts',(2.36232615126283,1.23913055331786,8.85097269580138));
#385345=CARTESIAN_POINT('Ctrl Pts',(2.36222650637988,1.23896713357046,8.85143669361005));
#385346=CARTESIAN_POINT('Ctrl Pts',(2.36213136440491,1.23879307159446,8.8519052845931));
#385347=CARTESIAN_POINT('Ctrl Pts',(2.36194527273555,1.23845261740801,8.85282181883899));
#385348=CARTESIAN_POINT('Ctrl Pts',(2.36178136762875,1.23808011298297,8.85372622499636));
#385349=CARTESIAN_POINT('Ctrl Pts',(2.36165119009121,1.23766350326389,8.85462257735071));
#385350=CARTESIAN_POINT('Ctrl Pts',(2.36154312132302,1.23731764867169,8.85536669723986));
#385351=CARTESIAN_POINT('Ctrl Pts',(2.36145824187889,1.2369413284631,8.85610498449051));
#385352=CARTESIAN_POINT('Ctrl Pts',(2.36141095400461,1.23652585282809,8.85681338218371));
#385353=CARTESIAN_POINT('Ctrl Pts',(2.36136804018444,1.23614880803681,8.85745625420284));
#385354=CARTESIAN_POINT('Ctrl Pts',(2.36135495228238,1.23573485447993,8.85808743050665));
#385355=CARTESIAN_POINT('Ctrl Pts',(2.36139708325078,1.23527083753394,8.8586680450841));
#385356=CARTESIAN_POINT('Ctrl Pts',(2.36141652156631,1.23505675017371,8.85893592806395));
#385357=CARTESIAN_POINT('Ctrl Pts',(2.3614479412895,1.23483192081265,8.85919241173848));
#385358=CARTESIAN_POINT('Ctrl Pts',(2.36149539461713,1.23459471186786,8.85943017985534));
#385359=CARTESIAN_POINT('Ctrl Pts',(2.36155947065713,1.23427440957104,8.8597512372));
#385360=CARTESIAN_POINT('Ctrl Pts',(2.361655039767,1.233923508711,8.86004599534706));
#385361=CARTESIAN_POINT('Ctrl Pts',(2.36179100277735,1.23354896212654,8.86026130871721));
#385362=CARTESIAN_POINT('Ctrl Pts',(2.36184078266864,1.23341183006239,8.86034014101235));
#385363=CARTESIAN_POINT('Ctrl Pts',(2.36189671351936,1.23326946421365,8.86040910639692));
#385364=CARTESIAN_POINT('Ctrl Pts',(2.36195758460882,1.23312586625832,8.86046313645506));
#385365=CARTESIAN_POINT('Ctrl Pts',(2.36205257343412,1.23290178285166,8.86054744990829));
#385366=CARTESIAN_POINT('Ctrl Pts',(2.36216232069169,1.23266863968505,8.86059655985668));
#385367=CARTESIAN_POINT('Ctrl Pts',(2.36227952289682,1.2324412641686,8.86059725258816));
#385368=CARTESIAN_POINT('Ctrl Pts',(2.36239699588587,1.23221336332387,8.86059794692011));
#385369=CARTESIAN_POINT('Ctrl Pts',(2.36252562260629,1.23198994662063,8.86056369958366));
#385370=CARTESIAN_POINT('Ctrl Pts',(2.3626551264635,1.23178132174018,8.86048590497774));
#385371=CARTESIAN_POINT('Ctrl Pts',(2.36268892311444,1.2317268768579,8.86046560290182));
#385372=CARTESIAN_POINT('Ctrl Pts',(2.36272329613576,1.23167277885394,8.86044257503091));
#385373=CARTESIAN_POINT('Ctrl Pts',(2.36275715566618,1.23162068179717,8.86041778462583));
#385374=CARTESIAN_POINT('Ctrl Pts',(2.36298498828977,1.23127013325217,8.86025097596201));
#385375=CARTESIAN_POINT('Ctrl Pts',(2.36322042238999,1.23096332188232,8.8599848982295));
#385376=CARTESIAN_POINT('Ctrl Pts',(2.36344986468682,1.23070404485065,8.85968173251461));
#385377=CARTESIAN_POINT('Ctrl Pts',(2.36357122651637,1.23056690215569,8.85952137522076));
#385378=CARTESIAN_POINT('Ctrl Pts',(2.36369310828822,1.23044028856096,8.85934740853961));
#385379=CARTESIAN_POINT('Ctrl Pts',(2.36381267123702,1.23032491149051,8.8591675900182));
#385380=CARTESIAN_POINT('Ctrl Pts',(2.36429277862403,1.22986161258086,8.85844552518697));
#385381=CARTESIAN_POINT('Ctrl Pts',(2.36476052976295,1.22955113387649,8.85759444184128));
#385382=CARTESIAN_POINT('Ctrl Pts',(2.36516464682635,1.22933224199776,8.85683498915144));
#385383=CARTESIAN_POINT('Ctrl Pts',(2.36520693660079,1.2293093355456,8.85675551445001));
#385384=CARTESIAN_POINT('Ctrl Pts',(2.36524853540329,1.22928745114727,8.85667699793653));
#385385=CARTESIAN_POINT('Ctrl Pts',(2.36528938769013,1.22926653136243,8.85659965593547));
#385386=CARTESIAN_POINT('Ctrl Pts',(2.36584081394238,1.22898415503923,8.85555568965886));
#385387=CARTESIAN_POINT('Ctrl Pts',(2.36641154946299,1.22879241075995,8.85434650606346));
#385388=CARTESIAN_POINT('Ctrl Pts',(2.36700243645268,1.22868445948992,8.85297329937117));
#385389=CARTESIAN_POINT('Ctrl Pts',(2.3673347743811,1.2286237434781,8.85220095427747));
#385390=CARTESIAN_POINT('Ctrl Pts',(2.36767367938263,1.22858981951856,8.85137579139183));
#385391=CARTESIAN_POINT('Ctrl Pts',(2.36802027905701,1.22858372995534,8.85049129520029));
#385392=CARTESIAN_POINT('Origin',(2.36814105033893,1.23545766909512,7.59394543036555));
#385393=CARTESIAN_POINT('Ctrl Pts',(2.36212061052624,1.23882457732601,7.59443877723642));
#385394=CARTESIAN_POINT('Ctrl Pts',(2.35889154920072,1.23401767014939,7.58783886950016));
#385395=CARTESIAN_POINT('Ctrl Pts',(2.36465235257833,1.22778129893038,7.58559994247159));
#385396=CARTESIAN_POINT('Ctrl Pts',(2.37974796156564,1.26506534257459,7.56670252222138));
#385397=CARTESIAN_POINT('Ctrl Pts',(2.37652356715048,1.26026538274351,7.56004874999027));
#385398=CARTESIAN_POINT('Ctrl Pts',(2.38230281100646,1.25397756136337,7.55786368756705));
#385399=CARTESIAN_POINT('Ctrl Pts',(2.39734239528812,1.29125710581579,7.53888913333557));
#385400=CARTESIAN_POINT('Ctrl Pts',(2.3940988381391,1.28642861958841,7.53222002137274));
#385401=CARTESIAN_POINT('Ctrl Pts',(2.39991996700693,1.28012648475776,7.53005029815326));
#385402=CARTESIAN_POINT('Ctrl Pts',(2.41490311553372,1.31739868185468,7.51101258149734));
#385403=CARTESIAN_POINT('Ctrl Pts',(2.41162024057834,1.31251166560068,7.5043616886572));
#385404=CARTESIAN_POINT('Ctrl Pts',(2.41750301869741,1.30622673098317,7.50217374673251));
#385405=CARTESIAN_POINT('',(2.41656476362036,1.30483398889129,7.50366116523517));
#385406=CARTESIAN_POINT('Ctrl Pts',(2.41011908817656,1.31027699133287,7.51860402984325));
#385407=CARTESIAN_POINT('Ctrl Pts',(2.41036533970192,1.31064357099958,7.51734760759493));
#385408=CARTESIAN_POINT('Ctrl Pts',(2.41063725122378,1.31094165149921,7.51608817408572));
#385409=CARTESIAN_POINT('Ctrl Pts',(2.41094406290927,1.31116154777589,7.51481005913119));
#385410=CARTESIAN_POINT('Ctrl Pts',(2.41122198026549,1.31136073507791,7.51365231206383));
#385411=CARTESIAN_POINT('Ctrl Pts',(2.41152877981015,1.31149625500912,7.51247773061042));
#385412=CARTESIAN_POINT('Ctrl Pts',(2.41187407264667,1.31153198601555,7.51129758471022));
#385413=CARTESIAN_POINT('Ctrl Pts',(2.41230323220853,1.31157639557592,7.50983079813402));
#385414=CARTESIAN_POINT('Ctrl Pts',(2.41277949901876,1.31145228193427,7.50839324291155));
#385415=CARTESIAN_POINT('Ctrl Pts',(2.41328555985521,1.31107896397256,7.50715379678855));
#385416=CARTESIAN_POINT('Ctrl Pts',(2.41351934537986,1.31090650183115,7.50658120839351));
#385417=CARTESIAN_POINT('Ctrl Pts',(2.41378708356348,1.31064869179565,7.50598221009429));
#385418=CARTESIAN_POINT('Ctrl Pts',(2.41406662507935,1.31029528425859,7.50545747549612));
#385419=CARTESIAN_POINT('Ctrl Pts',(2.41421579708483,1.31010669505783,7.50517746087247));
#385420=CARTESIAN_POINT('Ctrl Pts',(2.41437010660958,1.30988896396755,7.50491486231392));
#385421=CARTESIAN_POINT('Ctrl Pts',(2.41452410638098,1.30964689238474,7.50468370960993));
#385422=CARTESIAN_POINT('Ctrl Pts',(2.41475438461571,1.30928491901128,7.50433806340446));
#385423=CARTESIAN_POINT('Ctrl Pts',(2.41499040573442,1.30885736805732,7.50405484070983));
#385424=CARTESIAN_POINT('Ctrl Pts',(2.41521564697535,1.30839268806317,7.5038576603613));
#385425=CARTESIAN_POINT('Ctrl Pts',(2.41523973302502,1.30834299776057,7.50383657498791));
#385426=CARTESIAN_POINT('Ctrl Pts',(2.41526369813397,1.30829291115477,7.50381643264937));
#385427=CARTESIAN_POINT('Ctrl Pts',(2.41528752410888,1.30824248354156,7.50379723213559));
#385428=CARTESIAN_POINT('Ctrl Pts',(2.41544657028543,1.30790586272729,7.50366906242519));
#385429=CARTESIAN_POINT('Ctrl Pts',(2.41560222613724,1.307546417166,7.50358235568538));
#385430=CARTESIAN_POINT('Ctrl Pts',(2.41574393100535,1.30719634939658,7.5035341175365));
#385431=CARTESIAN_POINT('Ctrl Pts',(2.41595640141718,1.30667146239635,7.50346178989176));
#385432=CARTESIAN_POINT('Ctrl Pts',(2.41616265364206,1.30609776943107,7.50346967198527));
#385433=CARTESIAN_POINT('Ctrl Pts',(2.41634780009115,1.30552835049685,7.50354272648692));
#385434=CARTESIAN_POINT('Ctrl Pts',(2.41642395465796,1.30529413670293,7.50357277531559));
#385435=CARTESIAN_POINT('Ctrl Pts',(2.41649657211344,1.30506100104883,7.50361331098761));
#385436=CARTESIAN_POINT('Ctrl Pts',(2.41656476362161,1.30483398889196,7.50366116523658));
#385437=CARTESIAN_POINT('',(2.37073694677503,1.23681194660286,7.57603338622103));
#385438=CARTESIAN_POINT('Origin',(2.37857308999266,1.2408968393883,7.58486873427628));
#385439=CARTESIAN_POINT('Ctrl Pts',(2.41656476364781,1.30483398894163,7.50366116529969));
#385440=CARTESIAN_POINT('Ctrl Pts',(2.40131444507885,1.28219650713941,7.52783573079709));
#385441=CARTESIAN_POINT('Ctrl Pts',(2.3860392422488,1.25952355358682,7.55196141284069));
#385442=CARTESIAN_POINT('Ctrl Pts',(2.37073694715283,1.23681194779657,7.57603338728831));
#385443=CARTESIAN_POINT('Ctrl Pts',(2.36315354717505,1.24004694984635,7.59639677331371));
#385444=CARTESIAN_POINT('Ctrl Pts',(2.35069119251653,1.22667677287986,7.59959882295466));
#385445=CARTESIAN_POINT('Ctrl Pts',(2.36887194462181,1.22871860183697,7.59642833564546));
#385446=CARTESIAN_POINT('Ctrl Pts',(2.36006987607436,1.23765821029868,7.58707626057422));
#385447=CARTESIAN_POINT('Ctrl Pts',(2.35925575920167,1.2309314350866,7.58809943920598));
#385448=CARTESIAN_POINT('Ctrl Pts',(2.36517419960408,1.22766241933318,7.58710240504253));
#385449=CARTESIAN_POINT('Ctrl Pts',(2.36608778108832,1.23681532744523,7.58015376756929));
#385450=CARTESIAN_POINT('Ctrl Pts',(2.36537997734291,1.23405339238916,7.58205880659762));
#385451=CARTESIAN_POINT('Ctrl Pts',(2.36800166586016,1.23302683291375,7.58020924244128));
#385452=CARTESIAN_POINT('Ctrl Pts',(2.37073694604121,1.23681194622026,7.57603338509286));
#385453=CARTESIAN_POINT('Ctrl Pts',(2.37073694604121,1.23681194622026,7.57603338509286));
#385454=CARTESIAN_POINT('Ctrl Pts',(2.37073694604121,1.23681194622026,7.57603338509286));
#385455=CARTESIAN_POINT('Origin',(2.37857045058671,1.24090189863631,7.58486873427622));
#385456=CARTESIAN_POINT('Ctrl Pts',(2.46212726359302,1.22693032265429,7.51098857897448));
#385457=CARTESIAN_POINT('Ctrl Pts',(2.45624085415415,1.22703374358942,7.50433767179956));
#385458=CARTESIAN_POINT('Ctrl Pts',(2.45445176918725,1.23545438644277,7.50214974420965));
#385459=CARTESIAN_POINT('Ctrl Pts',(2.43063083103921,1.22748369743086,7.53887321589169));
#385460=CARTESIAN_POINT('Ctrl Pts',(2.42481495123189,1.22758587919964,7.53220407452061));
#385461=CARTESIAN_POINT('Ctrl Pts',(2.42297646352331,1.23596578867811,7.53003438070911));
#385462=CARTESIAN_POINT('Ctrl Pts',(2.39907391371632,1.22803813489113,7.5666946565923));
#385463=CARTESIAN_POINT('Ctrl Pts',(2.39329240467737,1.22813971278464,7.56004085833293));
#385464=CARTESIAN_POINT('Ctrl Pts',(2.39144168852525,1.23647706847158,7.55785582193789));
#385465=CARTESIAN_POINT('Ctrl Pts',(2.36745793881746,1.22859360996012,7.59443891967696));
#385466=CARTESIAN_POINT('Ctrl Pts',(2.36166804731026,1.22869533512896,7.58783901202978));
#385467=CARTESIAN_POINT('Ctrl Pts',(2.35984900020426,1.23698811787147,7.58560008491213));
#385468=CARTESIAN_POINT('',(2.45274559607508,1.23548210681976,7.50366116523517));
#385469=CARTESIAN_POINT('Ctrl Pts',(2.45274559607541,1.23548210681992,7.50366116523554));
#385470=CARTESIAN_POINT('Ctrl Pts',(2.45321593518387,1.23488803726186,7.50350835821027));
#385471=CARTESIAN_POINT('Ctrl Pts',(2.45362896354644,1.2343266411603,7.50345484956));
#385472=CARTESIAN_POINT('Ctrl Pts',(2.45399744452924,1.23378158361682,7.50349758195598));
#385473=CARTESIAN_POINT('Ctrl Pts',(2.45418650260067,1.2335019286745,7.50351950684424));
#385474=CARTESIAN_POINT('Ctrl Pts',(2.45438257535524,1.23319908335876,7.50357029184312));
#385475=CARTESIAN_POINT('Ctrl Pts',(2.4545636187282,1.23290185592397,7.50365515313924));
#385476=CARTESIAN_POINT('Ctrl Pts',(2.45484213674752,1.23244459976999,7.50378570417639));
#385477=CARTESIAN_POINT('Ctrl Pts',(2.45509355696108,1.23198739767575,7.50400001621911));
#385478=CARTESIAN_POINT('Ctrl Pts',(2.45529675319046,1.2315639553412,7.50428903009635));
#385479=CARTESIAN_POINT('Ctrl Pts',(2.45531930640862,1.23151695649984,7.50432110841318));
#385480=CARTESIAN_POINT('Ctrl Pts',(2.45534129185355,1.23147035849848,7.50435406373354));
#385481=CARTESIAN_POINT('Ctrl Pts',(2.45536269990846,1.23142419604732,7.50438785222352));
#385482=CARTESIAN_POINT('Ctrl Pts',(2.45549340637369,1.2311423520945,7.50459414719561));
#385483=CARTESIAN_POINT('Ctrl Pts',(2.4556042026276,1.23087203987399,7.50483629897752));
#385484=CARTESIAN_POINT('Ctrl Pts',(2.45569206180921,1.23062411408573,7.5050991045531));
#385485=CARTESIAN_POINT('Ctrl Pts',(2.45588588798845,1.23007716489503,7.50567888004914));
#385486=CARTESIAN_POINT('Ctrl Pts',(2.45597621046601,1.22961778862668,7.50637912803145));
#385487=CARTESIAN_POINT('Ctrl Pts',(2.45599386342159,1.229243823865,7.50710440483569));
#385488=CARTESIAN_POINT('Ctrl Pts',(2.45599819227676,1.2291521202812,7.50728225710685));
#385489=CARTESIAN_POINT('Ctrl Pts',(2.45599838327277,1.22906373407088,7.50746498566954));
#385490=CARTESIAN_POINT('Ctrl Pts',(2.45599484854336,1.22898072935447,7.50764697238949));
#385491=CARTESIAN_POINT('Ctrl Pts',(2.45597584681085,1.22853451884255,7.50862528291181));
#385492=CARTESIAN_POINT('Ctrl Pts',(2.45585158784298,1.2282031429546,7.50965856837421));
#385493=CARTESIAN_POINT('Ctrl Pts',(2.45567561046202,1.22794749938439,7.51067959873201));
#385494=CARTESIAN_POINT('Ctrl Pts',(2.45557876988732,1.22780681840526,7.51124147302578));
#385495=CARTESIAN_POINT('Ctrl Pts',(2.45546588589085,1.22768928353925,7.51180065547252));
#385496=CARTESIAN_POINT('Ctrl Pts',(2.45534370115124,1.22758999909434,7.512351757165));
#385497=CARTESIAN_POINT('Ctrl Pts',(2.45492150420325,1.22724693178692,7.51425603304536));
#385498=CARTESIAN_POINT('Ctrl Pts',(2.45433409491521,1.22708557269675,7.5162690050518));
#385499=CARTESIAN_POINT('Ctrl Pts',(2.45363638664936,1.22708087806131,7.51827788969244));
#385500=CARTESIAN_POINT('Ctrl Pts',(2.45359862535953,1.22708062397877,7.51838661432545));
#385501=CARTESIAN_POINT('Ctrl Pts',(2.45356053346671,1.22708083533097,7.51849533314857));
#385502=CARTESIAN_POINT('Ctrl Pts',(2.45352211735224,1.2270815102807,7.51860402984325));
#385503=CARTESIAN_POINT('Ctrl Pts',(2.37073694797139,1.23681194623013,7.57603338728985));
#385504=CARTESIAN_POINT('Ctrl Pts',(2.39811907486655,1.23636877604874,7.55196141284922));
#385505=CARTESIAN_POINT('Ctrl Pts',(2.42545400034853,1.23592549913145,7.52783573083105));
#385506=CARTESIAN_POINT('Ctrl Pts',(2.45274559613391,1.23548210681337,7.50366116530176));
#385507=CARTESIAN_POINT('Origin',(8.19199203866625E-16,4.27375699935098E-16,
7.49482233047033));
#385508=CARTESIAN_POINT('Origin',(2.40878727587057,1.3006345026963,7.49482233047033));
#385509=CARTESIAN_POINT('Origin',(0.,0.,7.50366116523517));
#385510=CARTESIAN_POINT('Origin',(2.44485166369884,1.23150582317302,7.49482233047033));
#385511=CARTESIAN_POINT('Ctrl Pts',(2.41011849833277,1.31027611334855,7.51860402984325));
#385512=CARTESIAN_POINT('Ctrl Pts',(2.41436194636775,1.31659192167406,7.51860402984325));
#385513=CARTESIAN_POINT('Ctrl Pts',(2.41070061931035,1.32326207686033,7.51860402984325));
#385514=CARTESIAN_POINT('Ctrl Pts',(2.41169411849219,1.31262121678981,7.51041458714367));
#385515=CARTESIAN_POINT('Ctrl Pts',(2.41349452737361,1.31817215307298,7.51004642900444));
#385516=CARTESIAN_POINT('Ctrl Pts',(2.41069960955982,1.32326391640993,7.50729136483011));
#385517=CARTESIAN_POINT('Ctrl Pts',(2.41442875339228,1.31195375206225,7.50215815450137));
#385518=CARTESIAN_POINT('Ctrl Pts',(2.41526080207567,1.31495471182038,7.49877163671528));
#385519=CARTESIAN_POINT('Ctrl Pts',(2.41362156250511,1.31799063296965,7.49481588533168));
#385520=CARTESIAN_POINT('Ctrl Pts',(2.4165642792075,1.30483372733005,7.50366171572174));
#385521=CARTESIAN_POINT('Ctrl Pts',(2.4197863045277,1.30657347302791,7.50000045605858));
#385522=CARTESIAN_POINT('Ctrl Pts',(2.41978630452764,1.30657347302802,7.49482233047317));
#385523=CARTESIAN_POINT('Origin',(2.39974288922258,1.31724724923823,7.51860402984325));
#385524=CARTESIAN_POINT('Origin',(2.39974288922258,1.31724724923823,9.));
#385525=CARTESIAN_POINT('Origin',(2.39974288922258,1.31724724923823,8.75721825406948));
#385526=CARTESIAN_POINT('Ctrl Pts',(2.40080670870024,1.29641427264101,8.78942910404912));
#385527=CARTESIAN_POINT('Ctrl Pts',(2.4039307878628,1.3010286586335,8.7967269950169));
#385528=CARTESIAN_POINT('Ctrl Pts',(2.39758410530011,1.30730505142161,8.79893251111267));
#385529=CARTESIAN_POINT('Ctrl Pts',(2.4069373809179,1.3055406233301,8.78111911759584));
#385530=CARTESIAN_POINT('Ctrl Pts',(2.4106348489598,1.31101520461131,8.78644465894814));
#385531=CARTESIAN_POINT('Ctrl Pts',(2.40622746632976,1.31781891610784,8.78817647674132));
#385532=CARTESIAN_POINT('Ctrl Pts',(2.41075816204786,1.31122838278128,8.7678092393203));
#385533=CARTESIAN_POINT('Ctrl Pts',(2.41511864407147,1.31769374690809,8.76988516158373));
#385534=CARTESIAN_POINT('Ctrl Pts',(2.41161733062358,1.3243927904619,8.77093053738833));
#385535=CARTESIAN_POINT('Ctrl Pts',(2.41001316201714,1.31011934753173,8.75371302330492));
#385536=CARTESIAN_POINT('Ctrl Pts',(2.41426725614075,1.316425605103,8.75300828287559));
#385537=CARTESIAN_POINT('Ctrl Pts',(2.41056573435195,1.32311090807155,8.75267964240738));
#385538=CARTESIAN_POINT('Origin',(2.39192360866379,1.3056071619048,8.78727029226991));
#385539=CARTESIAN_POINT('Ctrl Pts',(2.36243414091424,1.23929131094307,8.85049129520029));
#385540=CARTESIAN_POINT('Ctrl Pts',(2.36569043114741,1.24413875213822,8.85711686593484));
#385541=CARTESIAN_POINT('Ctrl Pts',(2.35986814900601,1.25039988564422,8.85933012996512));
#385542=CARTESIAN_POINT('Ctrl Pts',(2.3757420305442,1.2591019567374,8.82945683644723));
#385543=CARTESIAN_POINT('Ctrl Pts',(2.37902534995512,1.26398963462527,8.83607469902391));
#385544=CARTESIAN_POINT('Ctrl Pts',(2.37315851053407,1.27024361237588,8.83829567148519));
#385545=CARTESIAN_POINT('Ctrl Pts',(2.3890300836915,1.27888307316661,8.80838214965003));
#385546=CARTESIAN_POINT('Ctrl Pts',(2.39232636061372,1.28379004011345,8.81501364461987));
#385547=CARTESIAN_POINT('Ctrl Pts',(2.38642926673663,1.29005686517883,8.81722098428721));
#385548=CARTESIAN_POINT('Ctrl Pts',(2.40229980761778,1.29863690399944,8.78727029226991));
#385549=CARTESIAN_POINT('Ctrl Pts',(2.40559663206245,1.30354468600962,8.79393457792714));
#385550=CARTESIAN_POINT('Ctrl Pts',(2.39968192566131,1.30984196029033,8.79610912703474));
#385551=CARTESIAN_POINT('Origin',(2.35205794196025,1.24626156884843,8.85049129520029));
#385552=CARTESIAN_POINT('Ctrl Pts',(2.36802027905701,1.22858372995534,8.85049129520029));
#385553=CARTESIAN_POINT('Ctrl Pts',(2.37385899372365,1.22848114699079,8.85711686593484));
#385554=CARTESIAN_POINT('Ctrl Pts',(2.37566317709457,1.22012377392995,8.85933012996512));
#385555=CARTESIAN_POINT('Ctrl Pts',(2.36285485247416,1.22867448362327,8.86332496987231));
#385556=CARTESIAN_POINT('Ctrl Pts',(2.36523842990887,1.22471589132429,8.86648636486738));
#385557=CARTESIAN_POINT('Ctrl Pts',(2.36121298657354,1.22039479101918,8.87206031107457));
#385558=CARTESIAN_POINT('Ctrl Pts',(2.35953377205362,1.23497370824509,8.86341338519876));
#385559=CARTESIAN_POINT('Ctrl Pts',(2.3576183774015,1.23919327385792,8.86654584966059));
#385560=CARTESIAN_POINT('Ctrl Pts',(2.35175919171291,1.23830215329706,8.87215952290714));
#385561=CARTESIAN_POINT('Ctrl Pts',(2.36243414091424,1.23929131094307,8.85049129520029));
#385562=CARTESIAN_POINT('Ctrl Pts',(2.36569043114741,1.24413875213822,8.85711686593484));
#385563=CARTESIAN_POINT('Ctrl Pts',(2.35986814900601,1.25039988564422,8.85933012996512));
#385564=CARTESIAN_POINT('Origin',(2.36780069490805,1.21608565879209,8.85049129520029));
#385565=CARTESIAN_POINT('Ctrl Pts',(2.43950170000242,1.22732784120422,8.78727029226991));
#385566=CARTESIAN_POINT('Ctrl Pts',(2.44541309482907,1.22722398128974,8.79393457792714));
#385567=CARTESIAN_POINT('Ctrl Pts',(2.44719404240187,1.21877012767608,8.79610912703474));
#385568=CARTESIAN_POINT('Ctrl Pts',(2.41570832589787,1.22774587753441,8.80838214965002));
#385569=CARTESIAN_POINT('Ctrl Pts',(2.4216187389855,1.22764203486855,8.81501364461988));
#385570=CARTESIAN_POINT('Ctrl Pts',(2.42338478937513,1.21922004706182,8.81722098428721));
#385571=CARTESIAN_POINT('Ctrl Pts',(2.39188208645151,1.22816449129036,8.82945683644721));
#385572=CARTESIAN_POINT('Ctrl Pts',(2.39776926598005,1.22806105682517,8.83607469902391));
#385573=CARTESIAN_POINT('Ctrl Pts',(2.39954208843694,1.2196712330467,8.83829567148519));
#385574=CARTESIAN_POINT('Ctrl Pts',(2.36802027905701,1.22858372995534,8.85049129520029));
#385575=CARTESIAN_POINT('Ctrl Pts',(2.37385899372365,1.22848114699079,8.85711686593484));
#385576=CARTESIAN_POINT('Ctrl Pts',(2.37566317709457,1.22012377392995,8.85933012996512));
#385577=CARTESIAN_POINT('Origin',(2.43928211585346,1.21482977004097,8.78727029226991));
#385578=CARTESIAN_POINT('Ctrl Pts',(2.45333698446993,1.22708474451241,8.75374538247848));
#385579=CARTESIAN_POINT('Ctrl Pts',(2.46093500328082,1.22696437617396,8.75304829418601));
#385580=CARTESIAN_POINT('Ctrl Pts',(2.46430190265074,1.22011349069529,8.75272238421917));
#385581=CARTESIAN_POINT('Ctrl Pts',(2.45465676447423,1.22706155713948,8.76769408445019));
#385582=CARTESIAN_POINT('Ctrl Pts',(2.46244597221949,1.22693746977907,8.76974318093971));
#385583=CARTESIAN_POINT('Ctrl Pts',(2.46593649005342,1.22024160220786,8.77077869880429));
#385584=CARTESIAN_POINT('Ctrl Pts',(2.44789232400142,1.22718040241893,8.78108014887992));
#385585=CARTESIAN_POINT('Ctrl Pts',(2.4544934574888,1.22707904176507,8.78639403366324));
#385586=CARTESIAN_POINT('Ctrl Pts',(2.45756595314955,1.21959026041271,8.78812224174742));
#385587=CARTESIAN_POINT('Ctrl Pts',(2.4368068993313,1.22737516356144,8.78944554828686));
#385588=CARTESIAN_POINT('Ctrl Pts',(2.44237017583327,1.22729533762874,8.79673892988686));
#385589=CARTESIAN_POINT('Ctrl Pts',(2.44388779729732,1.2185089629834,8.79894799272499));
#385590=CARTESIAN_POINT('Origin',(2.45330253320328,1.21458343911746,8.75721825406948));
#385591=CARTESIAN_POINT('Origin',(2.45330253320328,1.21458343911746,9.));
#385592=CARTESIAN_POINT('Origin',(2.45330253320328,1.21458343911746,7.51860402984325));
#385593=CARTESIAN_POINT('Ctrl Pts',(2.45274489350846,1.2354817529271,7.50366195182966));
#385594=CARTESIAN_POINT('Ctrl Pts',(2.45601536992583,1.23712913743396,7.50000065167735));
#385595=CARTESIAN_POINT('Ctrl Pts',(2.45601536992589,1.23712913743385,7.49482233047108));
#385596=CARTESIAN_POINT('Ctrl Pts',(2.45736618897607,1.2296510216001,7.50215800491337));
#385597=CARTESIAN_POINT('Ctrl Pts',(2.46030407593302,1.22861491475105,7.49877273257265));
#385598=CARTESIAN_POINT('Ctrl Pts',(2.46185708707723,1.22553184603046,7.49481816995647));
#385599=CARTESIAN_POINT('Ctrl Pts',(2.45634027370536,1.22703233601389,7.51043025814043));
#385600=CARTESIAN_POINT('Ctrl Pts',(2.46192726936052,1.22533579938413,7.51006209594516));
#385601=CARTESIAN_POINT('Ctrl Pts',(2.46450595122239,1.22012721320191,7.50731281821701));
#385602=CARTESIAN_POINT('Ctrl Pts',(2.45352060617641,1.22708153673983,7.51860402984326));
#385603=CARTESIAN_POINT('Ctrl Pts',(2.46112871992397,1.22694878661777,7.51860402984326));
#385604=CARTESIAN_POINT('Ctrl Pts',(2.46450482787544,1.22012948221845,7.51860402984327));
#385605=CARTESIAN_POINT('Origin',(0.,0.,7.5));
#385606=CARTESIAN_POINT('Origin',(2.44187055726727,1.07433989271898,7.5));
#385607=CARTESIAN_POINT('',(2.44187055726727,1.07433989271898,7.59394543036555));
#385608=CARTESIAN_POINT('',(2.44187055726727,1.07433989271898,8.85049129520029));
#385609=CARTESIAN_POINT('',(2.44187055726727,1.07433989271898,7.5));
#385610=CARTESIAN_POINT('',(2.51312464689843,1.06850675396149,8.78727029226991));
#385611=CARTESIAN_POINT('Ctrl Pts',(2.44187055726727,1.07433989271898,8.85049129520029));
#385612=CARTESIAN_POINT('Ctrl Pts',(2.46565644538428,1.07239268678912,8.82945686509571));
#385613=CARTESIAN_POINT('Ctrl Pts',(2.48940697290245,1.07044837561632,8.80838212259895));
#385614=CARTESIAN_POINT('Ctrl Pts',(2.51312464689843,1.06850675396149,8.78727029226991));
#385615=CARTESIAN_POINT('',(2.52710047532066,1.06736263792745,8.75721825406948));
#385616=CARTESIAN_POINT('Origin',(2.48504237581485,1.07080588110006,8.75937679713113));
#385617=CARTESIAN_POINT('',(2.52710047532066,1.06736263792745,7.51860402984325));
#385618=CARTESIAN_POINT('',(2.52710047532066,1.06736263792745,7.5));
#385619=CARTESIAN_POINT('Ctrl Pts',(2.52710047532066,1.06736263792745,7.51860402984325));
#385620=CARTESIAN_POINT('Ctrl Pts',(2.51612463574747,1.06826116312848,7.52834476460825));
#385621=CARTESIAN_POINT('Ctrl Pts',(2.50514167081761,1.06916027163912,7.53807742314407));
#385622=CARTESIAN_POINT('Ctrl Pts',(2.49415134128774,1.07005998304475,7.54780169004674));
#385623=CARTESIAN_POINT('Ctrl Pts',(2.47674325328906,1.071485077286,7.5632044032688));
#385624=CARTESIAN_POINT('Ctrl Pts',(2.45931666632383,1.07291168592507,7.57858609112103));
#385625=CARTESIAN_POINT('Ctrl Pts',(2.44187055726727,1.07433989271898,7.59394543036555));
#385626=CARTESIAN_POINT('Origin',(2.60463825998836,1.3033658465605,7.5));
#385627=CARTESIAN_POINT('',(2.48911697509581,1.15316802656823,8.75721825406948));
#385628=CARTESIAN_POINT('',(2.4805679771315,1.1420528380681,8.78727029226991));
#385629=CARTESIAN_POINT('Origin',(2.4588674316814,1.11383834389691,8.75658640621072));
#385630=CARTESIAN_POINT('',(2.43698193351377,1.08538337893284,8.85049129520029));
#385631=CARTESIAN_POINT('Ctrl Pts',(2.4805679771315,1.1420528380681,8.78727029226991));
#385632=CARTESIAN_POINT('Ctrl Pts',(2.4660599035788,1.12318981189998,8.80838212259896));
#385633=CARTESIAN_POINT('Ctrl Pts',(2.45153173356484,1.10430065682692,8.82945686509571));
#385634=CARTESIAN_POINT('Ctrl Pts',(2.43698193351377,1.08538337893284,8.85049129520029));
#385635=CARTESIAN_POINT('',(2.43698193351377,1.08538337893284,7.59394543036555));
#385636=CARTESIAN_POINT('',(2.43698193351377,1.08538337893284,7.5));
#385637=CARTESIAN_POINT('',(2.48911697509581,1.15316802656823,7.51860402984325));
#385638=CARTESIAN_POINT('Ctrl Pts',(2.43698193351377,1.08538337893284,7.59394543036555));
#385639=CARTESIAN_POINT('Ctrl Pts',(2.44765369809929,1.09925853430101,7.57858609112103));
#385640=CARTESIAN_POINT('Ctrl Pts',(2.45831352104416,1.11311816345342,7.56320440326857));
#385641=CARTESIAN_POINT('Ctrl Pts',(2.46896202819286,1.12696308009709,7.54780169004651));
#385642=CARTESIAN_POINT('Ctrl Pts',(2.47568479996275,1.13570385600764,7.53807742314383));
#385643=CARTESIAN_POINT('Ctrl Pts',(2.48240306681553,1.14443877474018,7.52834476460825));
#385644=CARTESIAN_POINT('Ctrl Pts',(2.48911697509581,1.15316802656823,7.51860402984325));
#385645=CARTESIAN_POINT('',(2.48911697509581,1.15316802656823,7.5));
#385646=CARTESIAN_POINT('Origin',(2.44243149520446,1.08119197077097,7.5));
#385647=CARTESIAN_POINT('Ctrl Pts',(2.43698193351377,1.08538337893284,8.85049129520029));
#385648=CARTESIAN_POINT('Ctrl Pts',(2.43686386596228,1.08522987052213,8.85097269580138));
#385649=CARTESIAN_POINT('Ctrl Pts',(2.43675395547126,1.0850731708077,8.85143669361005));
#385650=CARTESIAN_POINT('Ctrl Pts',(2.43664785678659,1.08490556222797,8.8519052845931));
#385651=CARTESIAN_POINT('Ctrl Pts',(2.4364403344879,1.08457773047535,8.85282181883899));
#385652=CARTESIAN_POINT('Ctrl Pts',(2.43625289970127,1.08421649283684,8.85372622499635));
#385653=CARTESIAN_POINT('Ctrl Pts',(2.43609629735109,1.08380907959058,8.8546225773507));
#385654=CARTESIAN_POINT('Ctrl Pts',(2.43596629164197,1.08347085958349,8.85536669723986));
#385655=CARTESIAN_POINT('Ctrl Pts',(2.43585747567321,1.08310075080978,8.85610498449051));
#385656=CARTESIAN_POINT('Ctrl Pts',(2.43578366534162,1.08268915855854,8.85681338218371));
#385657=CARTESIAN_POINT('Ctrl Pts',(2.43571668234977,1.08231563794411,8.85745625420284));
#385658=CARTESIAN_POINT('Ctrl Pts',(2.43567709924276,1.08190337344397,8.85808743050666));
#385659=CARTESIAN_POINT('Ctrl Pts',(2.43568941398076,1.08143761053014,8.85866804508411));
#385660=CARTESIAN_POINT('Ctrl Pts',(2.43569509573392,1.0812227176182,8.85893592806396));
#385661=CARTESIAN_POINT('Ctrl Pts',(2.4357120460353,1.08099633712461,8.85919241173848));
#385662=CARTESIAN_POINT('Ctrl Pts',(2.43574420383571,1.0807565752059,8.85943017985534));
#385663=CARTESIAN_POINT('Ctrl Pts',(2.43578762638599,1.08043282563852,8.8597512372));
#385664=CARTESIAN_POINT('Ctrl Pts',(2.43586051684358,1.08007652260804,8.86004599534706));
#385665=CARTESIAN_POINT('Ctrl Pts',(2.43597220322128,1.07969403438973,8.86026130871721));
#385666=CARTESIAN_POINT('Ctrl Pts',(2.43601309475293,1.07955399466952,8.86034014101235));
#385667=CARTESIAN_POINT('Ctrl Pts',(2.43605978927648,1.07940833782478,8.86040910639692));
#385668=CARTESIAN_POINT('Ctrl Pts',(2.43611133494716,1.07926113488276,8.86046313645506));
#385669=CARTESIAN_POINT('Ctrl Pts',(2.43619177153458,1.07903142592456,8.86054744990829));
#385670=CARTESIAN_POINT('Ctrl Pts',(2.43628635577067,1.07879173024466,8.86059655985668));
#385671=CARTESIAN_POINT('Ctrl Pts',(2.43638874917194,1.07855731272453,8.86059725258816));
#385672=CARTESIAN_POINT('Ctrl Pts',(2.43649137914287,1.07832235360627,8.86059794692011));
#385673=CARTESIAN_POINT('Ctrl Pts',(2.43660542722858,1.07809115479434,8.86056369958366));
#385674=CARTESIAN_POINT('Ctrl Pts',(2.43672129836424,1.07787466121546,8.86048590497774));
#385675=CARTESIAN_POINT('Ctrl Pts',(2.43675153728075,1.07781816283716,8.86046560290182));
#385676=CARTESIAN_POINT('Ctrl Pts',(2.436782373608,1.07776197369632,8.86044257503091));
#385677=CARTESIAN_POINT('Ctrl Pts',(2.4368128257005,1.07770781429098,8.86041778462583));
#385678=CARTESIAN_POINT('Ctrl Pts',(2.43701773049513,1.07734338869924,8.86025097596201));
#385679=CARTESIAN_POINT('Ctrl Pts',(2.43723302339879,1.07702212339167,8.8599848982295));
#385680=CARTESIAN_POINT('Ctrl Pts',(2.43744538234536,1.07674867865403,8.85968173251461));
#385681=CARTESIAN_POINT('Ctrl Pts',(2.43755770806138,1.07660404205434,8.85952137522076));
#385682=CARTESIAN_POINT('Ctrl Pts',(2.43767122725319,1.07646987960889,8.85934740853961));
#385683=CARTESIAN_POINT('Ctrl Pts',(2.4377831523128,1.07634707916857,8.8591675900182));
#385684=CARTESIAN_POINT('Ctrl Pts',(2.43823258960464,1.07585397157031,8.85844552518695));
#385685=CARTESIAN_POINT('Ctrl Pts',(2.4386794872598,1.07551416185936,8.85759444184124));
#385686=CARTESIAN_POINT('Ctrl Pts',(2.43906874957054,1.07526982784832,8.85683498915138));
#385687=CARTESIAN_POINT('Ctrl Pts',(2.43910948483467,1.07524425894478,8.85675551444998));
#385688=CARTESIAN_POINT('Ctrl Pts',(2.43914959602974,1.07521975426587,8.85667699793651));
#385689=CARTESIAN_POINT('Ctrl Pts',(2.43918902404595,1.07519626004797,8.85659965593547));
#385690=CARTESIAN_POINT('Ctrl Pts',(2.43972122542068,1.07487913389593,8.85555568965886));
#385691=CARTESIAN_POINT('Ctrl Pts',(2.4402785032058,1.07465121642548,8.85434650606346));
#385692=CARTESIAN_POINT('Ctrl Pts',(2.44086125969317,1.0745056286935,8.85297329937118));
#385693=CARTESIAN_POINT('Ctrl Pts',(2.44118902470945,1.07442374446505,8.85220095427747));
#385694=CARTESIAN_POINT('Ctrl Pts',(2.44152505987875,1.07436817648792,8.85137579139184));
#385695=CARTESIAN_POINT('Ctrl Pts',(2.44187055726727,1.07433989271898,8.85049129520029));
#385696=CARTESIAN_POINT('Origin',(2.44243149520446,1.08119197077097,7.59394543036555));
#385697=CARTESIAN_POINT('Ctrl Pts',(2.43663914358207,1.08493769223099,7.59443877723642));
#385698=CARTESIAN_POINT('Ctrl Pts',(2.43310873710912,1.08034754803015,7.58783886950016));
#385699=CARTESIAN_POINT('Ctrl Pts',(2.43845813862246,1.07375489416499,7.58559994247159));
#385700=CARTESIAN_POINT('Ctrl Pts',(2.45591152894015,1.10999515475426,7.56670252222136));
#385701=CARTESIAN_POINT('Ctrl Pts',(2.45238622490691,1.10541164461491,7.56004874999027));
#385702=CARTESIAN_POINT('Ctrl Pts',(2.45775073258753,1.09876646481299,7.55786368756704));
#385703=CARTESIAN_POINT('Ctrl Pts',(2.4751479250441,1.13500582496978,7.53888913333557));
#385704=CARTESIAN_POINT('Ctrl Pts',(2.47160166995631,1.13039507480532,7.53222002137274));
#385705=CARTESIAN_POINT('Ctrl Pts',(2.47700705952566,1.12373292737947,7.53005029815327));
#385706=CARTESIAN_POINT('Ctrl Pts',(2.49434746143404,1.15996857112789,7.51101258149734));
#385707=CARTESIAN_POINT('Ctrl Pts',(2.4907582192909,1.15530193029348,7.5043616886572));
#385708=CARTESIAN_POINT('Ctrl Pts',(2.49622623346789,1.14865299786,7.50217374673251));
#385709=CARTESIAN_POINT('',(2.49520067284432,1.14732323151531,7.50366116523517));
#385710=CARTESIAN_POINT('Ctrl Pts',(2.48911697509581,1.15316802656823,7.51860402984325));
#385711=CARTESIAN_POINT('Ctrl Pts',(2.48938620751088,1.15351807566829,7.51734760759493));
#385712=CARTESIAN_POINT('Ctrl Pts',(2.48967665844453,1.15379812229854,7.51608817408573));
#385713=CARTESIAN_POINT('Ctrl Pts',(2.48999692855533,1.15399790928256,7.5148100591312));
#385714=CARTESIAN_POINT('Ctrl Pts',(2.4902870368748,1.15417888110675,7.51365231206384));
#385715=CARTESIAN_POINT('Ctrl Pts',(2.49060188885869,1.15429446588341,7.51247773061043));
#385716=CARTESIAN_POINT('Ctrl Pts',(2.49094876154749,1.15430800048867,7.51129758471022));
#385717=CARTESIAN_POINT('Ctrl Pts',(2.49137988468531,1.15432482245729,7.50983079813402));
#385718=CARTESIAN_POINT('Ctrl Pts',(2.49184722096597,1.15417044930113,7.50839324291155));
#385719=CARTESIAN_POINT('Ctrl Pts',(2.49232832348223,1.1537654749321,7.50715379678855));
#385720=CARTESIAN_POINT('Ctrl Pts',(2.49255057898211,1.15357838844267,7.50658120839351));
#385721=CARTESIAN_POINT('Ctrl Pts',(2.49280124912323,1.1533039540612,7.50598221009429));
#385722=CARTESIAN_POINT('Ctrl Pts',(2.49305757339242,1.15293336235142,7.50545747549611));
#385723=CARTESIAN_POINT('Ctrl Pts',(2.49319435595644,1.15273560314419,7.50517746087247));
#385724=CARTESIAN_POINT('Ctrl Pts',(2.49333439835687,1.15250843276059,7.50491486231392));
#385725=CARTESIAN_POINT('Ctrl Pts',(2.49347257213967,1.15225699174058,7.50468370960992));
#385726=CARTESIAN_POINT('Ctrl Pts',(2.4936791855294,1.15188100810308,7.50433806340446));
#385727=CARTESIAN_POINT('Ctrl Pts',(2.49388732843373,1.15143921367341,7.50405484070983));
#385728=CARTESIAN_POINT('Ctrl Pts',(2.49408233474293,1.1509610571583,7.5038576603613));
#385729=CARTESIAN_POINT('Ctrl Pts',(2.49410318763662,1.15090992575125,7.50383657498791));
#385730=CARTESIAN_POINT('Ctrl Pts',(2.49412389444683,1.15085840660396,7.50381643264937));
#385731=CARTESIAN_POINT('Ctrl Pts',(2.49414444056045,1.15080655606423,7.50379723213559));
#385732=CARTESIAN_POINT('Ctrl Pts',(2.49428159258994,1.15046043675001,7.50366906242519));
#385733=CARTESIAN_POINT('Ctrl Pts',(2.49441389887393,1.15009175680351,7.50358235568538));
#385734=CARTESIAN_POINT('Ctrl Pts',(2.49453288367519,1.14973332922379,7.5035341175365));
#385735=CARTESIAN_POINT('Ctrl Pts',(2.49471128791821,1.14919590763417,7.50346178989176));
#385736=CARTESIAN_POINT('Ctrl Pts',(2.49488035974129,1.14861017875719,7.50346967198527));
#385737=CARTESIAN_POINT('Ctrl Pts',(2.49502864299076,1.14803006738152,7.50354272648692));
#385738=CARTESIAN_POINT('Ctrl Pts',(2.49508963496055,1.14779145556511,7.50357277531559));
#385739=CARTESIAN_POINT('Ctrl Pts',(2.49514716616304,1.14755414629688,7.50361331098761));
#385740=CARTESIAN_POINT('Ctrl Pts',(2.49520067284561,1.1473232315159,7.50366116523659));
#385741=CARTESIAN_POINT('',(2.44510882695076,1.08237714611462,7.57603338622103));
#385742=CARTESIAN_POINT('Origin',(2.45319058995184,1.0859515826301,7.58486873427627));
#385743=CARTESIAN_POINT('Ctrl Pts',(2.49520067287494,1.14732323156379,7.50366116529969));
#385744=CARTESIAN_POINT('Ctrl Pts',(2.47853129928219,1.12570935216129,7.52783573079709));
#385745=CARTESIAN_POINT('Ctrl Pts',(2.46183481987291,1.10406166822897,7.55196141284068));
#385746=CARTESIAN_POINT('Ctrl Pts',(2.44510882740428,1.08237714728166,7.57603338728831));
#385747=CARTESIAN_POINT('Ctrl Pts',(2.43774827562801,1.08609137277755,7.59639677331371));
#385748=CARTESIAN_POINT('Ctrl Pts',(2.42383037731441,1.07295780766365,7.59974925422225));
#385749=CARTESIAN_POINT('Ctrl Pts',(2.4429098820182,1.07443121403228,7.59639677331372));
#385750=CARTESIAN_POINT('Ctrl Pts',(2.43451789319204,1.08390511263724,7.58707626057422));
#385751=CARTESIAN_POINT('Ctrl Pts',(2.4332529139748,1.07712888513356,7.58811717123965));
#385752=CARTESIAN_POINT('Ctrl Pts',(2.43911965275286,1.07350965763148,7.58707626057424));
#385753=CARTESIAN_POINT('Ctrl Pts',(2.44046943008489,1.08267839307897,7.5801537675693));
#385754=CARTESIAN_POINT('Ctrl Pts',(2.43957276865562,1.07992649732891,7.58208760766041));
#385755=CARTESIAN_POINT('Ctrl Pts',(2.44221276280679,1.07874017409314,7.5801537675693));
#385756=CARTESIAN_POINT('Ctrl Pts',(2.44510882619394,1.08237714577982,7.57603338509286));
#385757=CARTESIAN_POINT('Ctrl Pts',(2.44510882619394,1.08237714577982,7.57603338509286));
#385758=CARTESIAN_POINT('Ctrl Pts',(2.44510882619394,1.08237714577982,7.57603338509286));
#385759=CARTESIAN_POINT('Origin',(2.45318828011531,1.08595680059061,7.5848687342762));
#385760=CARTESIAN_POINT('Ctrl Pts',(2.53567825474112,1.06666042731961,7.51098857897448));
#385761=CARTESIAN_POINT('Ctrl Pts',(2.52981056576382,1.06714077931299,7.50433767179956));
#385762=CARTESIAN_POINT('Ctrl Pts',(2.52856466910386,1.07565874811988,7.50214974420965));
#385763=CARTESIAN_POINT('Ctrl Pts',(2.50428198982965,1.06923064849069,7.53887321589171));
#385764=CARTESIAN_POINT('Ctrl Pts',(2.49848460617955,1.06970524501469,7.53220407452063));
#385765=CARTESIAN_POINT('Ctrl Pts',(2.49718679848483,1.07818572938232,7.53003438070912));
#385766=CARTESIAN_POINT('Ctrl Pts',(2.4728254325079,1.07180580543453,7.5666946565923));
#385767=CARTESIAN_POINT('Ctrl Pts',(2.46706231031734,1.07227759718128,7.56004085833297));
#385768=CARTESIAN_POINT('Ctrl Pts',(2.46574957287294,1.0807163986678,7.55785582193789));
#385769=CARTESIAN_POINT('Ctrl Pts',(2.44131000543014,1.07438578168709,7.59443891967696));
#385770=CARTESIAN_POINT('Ctrl Pts',(2.43553852742995,1.07485825747318,7.58783901202978));
#385771=CARTESIAN_POINT('Ctrl Pts',(2.43425453816588,1.08325054855239,7.58560008491213));
#385772=CARTESIAN_POINT('',(2.52686377755798,1.075795726429,7.50366116523517));
#385773=CARTESIAN_POINT('Ctrl Pts',(2.52686377755832,1.07579572642914,7.50366116523554));
#385774=CARTESIAN_POINT('Ctrl Pts',(2.52729508813737,1.07517274272056,7.50350835821027));
#385775=CARTESIAN_POINT('Ctrl Pts',(2.52767129911715,1.07458603724944,7.50345484956));
#385776=CARTESIAN_POINT('Ctrl Pts',(2.52800410105954,1.07401849092752,7.50349758195598));
#385777=CARTESIAN_POINT('Ctrl Pts',(2.52817485313721,1.07372729757405,7.50351950684424));
#385778=CARTESIAN_POINT('Ctrl Pts',(2.52835111967327,1.07341251206197,7.50357029184312));
#385779=CARTESIAN_POINT('Ctrl Pts',(2.52851274764608,1.07310429582409,7.50365515313923));
#385780=CARTESIAN_POINT('Ctrl Pts',(2.52876139691789,1.07263013444116,7.50378570417639));
#385781=CARTESIAN_POINT('Ctrl Pts',(2.5289830075229,1.07215776316926,7.50400001621911));
#385782=CARTESIAN_POINT('Ctrl Pts',(2.52915865622031,1.07172217201528,7.50428903009634));
#385783=CARTESIAN_POINT('Ctrl Pts',(2.52917815187436,1.07167382474843,7.50432110841318));
#385784=CARTESIAN_POINT('Ctrl Pts',(2.52919710660364,1.07162591387537,7.50435406373354));
#385785=CARTESIAN_POINT('Ctrl Pts',(2.529215513035,1.07157847465114,7.50438785222351));
#385786=CARTESIAN_POINT('Ctrl Pts',(2.52932789314572,1.07128883538497,7.50459414719561));
#385787=CARTESIAN_POINT('Ctrl Pts',(2.52942114279341,1.07101197980954,7.50483629897752));
#385788=CARTESIAN_POINT('Ctrl Pts',(2.52949293679912,1.07075893425431,7.5050991045531));
#385789=CARTESIAN_POINT('Ctrl Pts',(2.52965132158672,1.07020069034344,7.50567888004914));
#385790=CARTESIAN_POINT('Ctrl Pts',(2.52971202614849,1.0697364709319,7.50637912803144));
#385791=CARTESIAN_POINT('Ctrl Pts',(2.52970568282964,1.06936214349218,7.50710440483569));
#385792=CARTESIAN_POINT('Ctrl Pts',(2.52970412732193,1.06927035097252,7.50728225710685));
#385793=CARTESIAN_POINT('Ctrl Pts',(2.52969865500157,1.069182134124,7.50746498566954));
#385794=CARTESIAN_POINT('Ctrl Pts',(2.52968980940421,1.06909952642057,7.50764697238949));
#385795=CARTESIAN_POINT('Ctrl Pts',(2.52964225790714,1.06865545014118,7.50862528291182));
#385796=CARTESIAN_POINT('Ctrl Pts',(2.5294970229166,1.06833271639993,7.50965856837422));
#385797=CARTESIAN_POINT('Ctrl Pts',(2.52930502796027,1.06808887298637,7.51067959873202));
#385798=CARTESIAN_POINT('Ctrl Pts',(2.52919937289363,1.06795468564832,7.51124147302579));
#385799=CARTESIAN_POINT('Ctrl Pts',(2.52907919034472,1.06784462477279,7.51180065547253));
#385800=CARTESIAN_POINT('Ctrl Pts',(2.52895089547053,1.06775337272156,7.51235175716501));
#385801=CARTESIAN_POINT('Ctrl Pts',(2.52850758557361,1.06743806053406,7.51425603304536));
#385802=CARTESIAN_POINT('Ctrl Pts',(2.52791104486854,1.06731466841575,7.5162690050518));
#385803=CARTESIAN_POINT('Ctrl Pts',(2.52721446933283,1.06735468574801,7.51827788969243));
#385804=CARTESIAN_POINT('Ctrl Pts',(2.52717676934849,1.06735685156166,7.51838661432545));
#385805=CARTESIAN_POINT('Ctrl Pts',(2.52713876926093,1.06735950303556,7.51849533314856));
#385806=CARTESIAN_POINT('Ctrl Pts',(2.52710047532066,1.06736263792744,7.51860402984325));
#385807=CARTESIAN_POINT('Ctrl Pts',(2.44510882812078,1.08237714566601,7.57603338728985));
#385808=CARTESIAN_POINT('Ctrl Pts',(2.4724063014885,1.08018050713157,7.55196141284922));
#385809=CARTESIAN_POINT('Ctrl Pts',(2.49965666358481,1.07798678628545,7.52783573083105));
#385810=CARTESIAN_POINT('Ctrl Pts',(2.52686377761628,1.07579572641885,7.50366116530176));
#385811=CARTESIAN_POINT('Origin',(8.44898126352695E-16,3.74011337523921E-16,
7.49482233047033));
#385812=CARTESIAN_POINT('Origin',(2.48717010277292,1.14363067896613,7.49482233047033));
#385813=CARTESIAN_POINT('Origin',(0.,0.,7.50366116523517));
#385814=CARTESIAN_POINT('Origin',(2.51873130274447,1.07233337846732,7.49482233047033));
#385815=CARTESIAN_POINT('Ctrl Pts',(2.48911633021126,1.15316718817924,7.51860402984325));
#385816=CARTESIAN_POINT('Ctrl Pts',(2.49375571485591,1.1591981413501,7.51860402984325));
#385817=CARTESIAN_POINT('Ctrl Pts',(2.49052926869772,1.16608917401715,7.51860402984325));
#385818=CARTESIAN_POINT('Ctrl Pts',(2.49083896438344,1.15540652302375,7.51041458714366));
#385819=CARTESIAN_POINT('Ctrl Pts',(2.49299132384047,1.1608307017199,7.5100464290044));
#385820=CARTESIAN_POINT('Ctrl Pts',(2.49052837888218,1.16609107448214,7.50729136483008));
#385821=CARTESIAN_POINT('Ctrl Pts',(2.4935252160709,1.15456522101444,7.50215815450138));
#385822=CARTESIAN_POINT('Ctrl Pts',(2.49454782737291,1.1575067054367,7.49877163671533));
#385823=CARTESIAN_POINT('Ctrl Pts',(2.49310646793173,1.16064141540027,7.49481588533172));
#385824=CARTESIAN_POINT('Ctrl Pts',(2.49520017266846,1.14732300152792,7.50366171572174));
#385825=CARTESIAN_POINT('Ctrl Pts',(2.49852704388164,1.1488527368606,7.50000045605858));
#385826=CARTESIAN_POINT('Ctrl Pts',(2.49852704388159,1.14885273686071,7.49482233047317));
#385827=CARTESIAN_POINT('Origin',(2.47920868111273,1.16078876868071,7.51860402984325));
#385828=CARTESIAN_POINT('Origin',(2.47920868111273,1.16078876868071,9.));
#385829=CARTESIAN_POINT('Origin',(2.47920868111273,1.16078876868071,8.75721825406948));
#385830=CARTESIAN_POINT('Ctrl Pts',(2.47893554146575,1.13993043652028,8.78942910404912));
#385831=CARTESIAN_POINT('Ctrl Pts',(2.48234884659823,1.14433518132267,8.7967269950169));
#385832=CARTESIAN_POINT('Ctrl Pts',(2.47641733384217,1.15100531193659,8.79893251111267));
#385833=CARTESIAN_POINT('Ctrl Pts',(2.48563834485609,1.14864524262545,8.78111911759584));
#385834=CARTESIAN_POINT('Ctrl Pts',(2.48967897368032,1.15387167820146,8.78644465894814));
#385835=CARTESIAN_POINT('Ctrl Pts',(2.48571656178288,1.16094379271768,8.78817647674132));
#385836=CARTESIAN_POINT('Ctrl Pts',(2.48981569178069,1.15407651767735,8.76780923932029));
#385837=CARTESIAN_POINT('Ctrl Pts',(2.49458145202819,1.16024922097768,8.76988516158373));
#385838=CARTESIAN_POINT('Ctrl Pts',(2.49151654159843,1.16715883055087,8.77093053738833));
#385839=CARTESIAN_POINT('Ctrl Pts',(2.48900116630002,1.15301749337551,8.75371302330492));
#385840=CARTESIAN_POINT('Ctrl Pts',(2.49365056324085,1.15903823331794,8.75300828287559));
#385841=CARTESIAN_POINT('Ctrl Pts',(2.49038497545739,1.16594695792981,8.75267964240738));
#385842=CARTESIAN_POINT('Origin',(2.47065968314843,1.14967358018058,8.78727029226991));
#385843=CARTESIAN_POINT('Ctrl Pts',(2.43698193351377,1.08538337893284,8.85049129520029));
#385844=CARTESIAN_POINT('Ctrl Pts',(2.44054210997314,1.09001222930861,8.85711686593484));
#385845=CARTESIAN_POINT('Ctrl Pts',(2.4351329425359,1.0966335335419,8.85933012996512));
#385846=CARTESIAN_POINT('Ctrl Pts',(2.45153175309122,1.10430068221462,8.82945683644724));
#385847=CARTESIAN_POINT('Ctrl Pts',(2.45512148116771,1.10896795484717,8.8360746990239));
#385848=CARTESIAN_POINT('Ctrl Pts',(2.44966738952773,1.11558497282205,8.83829567148519));
#385849=CARTESIAN_POINT('Ctrl Pts',(2.46605988498928,1.12318978773036,8.80838214965002));
#385850=CARTESIAN_POINT('Ctrl Pts',(2.46966377980879,1.12787547959984,8.81501364461992));
#385851=CARTESIAN_POINT('Ctrl Pts',(2.46418031900403,1.13450725690291,8.81722098428721));
#385852=CARTESIAN_POINT('Ctrl Pts',(2.4805679771315,1.1420528380681,8.78727029226991));
#385853=CARTESIAN_POINT('Ctrl Pts',(2.48417247056978,1.14673930824638,8.79393457792714));
#385854=CARTESIAN_POINT('Ctrl Pts',(2.47867338431573,1.15340260064194,8.79610912703474));
#385855=CARTESIAN_POINT('Origin',(2.4270736395307,1.09300412104532,8.85049129520029));
#385856=CARTESIAN_POINT('Ctrl Pts',(2.44187055726727,1.07433989271898,8.85049129520029));
#385857=CARTESIAN_POINT('Ctrl Pts',(2.44769070315532,1.07386343278904,8.85711686593484));
#385858=CARTESIAN_POINT('Ctrl Pts',(2.44895572090754,1.06540763642202,8.85933012996512));
#385859=CARTESIAN_POINT('Ctrl Pts',(2.43672155821481,1.07476140994123,8.86332496987232));
#385860=CARTESIAN_POINT('Ctrl Pts',(2.43884661045462,1.0706582346641,8.86648636486738));
#385861=CARTESIAN_POINT('Ctrl Pts',(2.43455258397725,1.06660392356302,8.87206031107457));
#385862=CARTESIAN_POINT('Ctrl Pts',(2.43381089401739,1.08126047448359,8.86341338519876));
#385863=CARTESIAN_POINT('Ctrl Pts',(2.43216978324604,1.08559409030303,8.86654584966059));
#385864=CARTESIAN_POINT('Ctrl Pts',(2.42626554159248,1.08508019996091,8.87215952290714));
#385865=CARTESIAN_POINT('Ctrl Pts',(2.43698193351377,1.08538337893284,8.85049129520029));
#385866=CARTESIAN_POINT('Ctrl Pts',(2.44054210997314,1.09001222930861,8.85711686593484));
#385867=CARTESIAN_POINT('Ctrl Pts',(2.4351329425359,1.0966335335419,8.85933012996512));
#385868=CARTESIAN_POINT('Origin',(2.44085067010873,1.06188156898808,8.85049129520029));
#385869=CARTESIAN_POINT('Ctrl Pts',(2.51312464689843,1.06850675396149,8.78727029226991));
#385870=CARTESIAN_POINT('Ctrl Pts',(2.51901724180285,1.0680243630714,8.79393457792714));
#385871=CARTESIAN_POINT('Ctrl Pts',(2.52025288996714,1.05947377310391,8.79610912703474));
#385872=CARTESIAN_POINT('Ctrl Pts',(2.48940694251246,1.07044837810417,8.80838214965001));
#385873=CARTESIAN_POINT('Ctrl Pts',(2.49529855880009,1.0699660673275,8.81501364461992));
#385874=CARTESIAN_POINT('Ctrl Pts',(2.4965213820383,1.06144823216102,8.81722098428721));
#385875=CARTESIAN_POINT('Ctrl Pts',(2.46565647730582,1.07239268417589,8.82945683644723));
#385876=CARTESIAN_POINT('Ctrl Pts',(2.47152493392368,1.07191226934046,8.8360746990239));
#385877=CARTESIAN_POINT('Ctrl Pts',(2.47275657607161,1.06342609822994,8.8382956714852));
#385878=CARTESIAN_POINT('Ctrl Pts',(2.44187055726727,1.07433989271898,8.85049129520029));
#385879=CARTESIAN_POINT('Ctrl Pts',(2.44769070315532,1.07386343278904,8.85711686593484));
#385880=CARTESIAN_POINT('Ctrl Pts',(2.44895572090754,1.06540763642202,8.85933012996512));
#385881=CARTESIAN_POINT('Origin',(2.51210475973989,1.05604843023059,8.78727029226991));
#385882=CARTESIAN_POINT('Ctrl Pts',(2.52691593003165,1.06737772701857,8.75374538247848));
#385883=CARTESIAN_POINT('Ctrl Pts',(2.53449062587208,1.06677079925315,8.75304829418602));
#385884=CARTESIAN_POINT('Ctrl Pts',(2.53741166984647,1.05971827167017,8.75272238421917));
#385885=CARTESIAN_POINT('Ctrl Pts',(2.52823151278633,1.06727002869138,8.76769408445018));
#385886=CARTESIAN_POINT('Ctrl Pts',(2.53599676646445,1.06664714002805,8.76974318093966));
#385887=CARTESIAN_POINT('Ctrl Pts',(2.53905110694683,1.05974139158941,8.7707786988043));
#385888=CARTESIAN_POINT('Ctrl Pts',(2.52148858502512,1.0678220289796,8.78108014887992));
#385889=CARTESIAN_POINT('Ctrl Pts',(2.52806966157637,1.06729794050742,8.78639403366329));
#385890=CARTESIAN_POINT('Ctrl Pts',(2.53065603659667,1.05962769018665,8.78812224174741));
#385891=CARTESIAN_POINT('Ctrl Pts',(2.51043841493815,1.06872663556165,8.78944554828686));
#385892=CARTESIAN_POINT('Ctrl Pts',(2.51598514662683,1.0682905332906,8.79673892988685));
#385893=CARTESIAN_POINT('Ctrl Pts',(2.51693670501844,1.05942497685325,8.79894799272499));
#385894=CARTESIAN_POINT('Origin',(2.52608058816213,1.05490431419655,8.75721825406948));
#385895=CARTESIAN_POINT('Origin',(2.52608058816213,1.05490431419655,9.));
#385896=CARTESIAN_POINT('Origin',(2.52608058816213,1.05490431419655,7.51860402984325));
#385897=CARTESIAN_POINT('Ctrl Pts',(2.52686305376087,1.07579541827706,7.50366195182966));
#385898=CARTESIAN_POINT('Ctrl Pts',(2.53023235892144,1.07722987791225,7.50000065167736));
#385899=CARTESIAN_POINT('Ctrl Pts',(2.53023235892149,1.07722987791214,7.49482233047108));
#385900=CARTESIAN_POINT('Ctrl Pts',(2.53110127804255,1.0696805793957,7.50215800491337));
#385901=CARTESIAN_POINT('Ctrl Pts',(2.53396674520192,1.06845837027569,7.49877273257265));
#385902=CARTESIAN_POINT('Ctrl Pts',(2.53531903262702,1.0652821342848,7.49481816995649));
#385903=CARTESIAN_POINT('Ctrl Pts',(2.52990969086322,1.06713300479696,7.51043025814042));
#385904=CARTESIAN_POINT('Ctrl Pts',(2.53537650996154,1.065081993843,7.51006209594516));
#385905=CARTESIAN_POINT('Ctrl Pts',(2.53761617838247,1.05971889254556,7.50731281821699));
#385906=CARTESIAN_POINT('Ctrl Pts',(2.52709896894495,1.06736276115358,7.51860402984326));
#385907=CARTESIAN_POINT('Ctrl Pts',(2.53468294567732,1.06674283025944,7.51860402984327));
#385908=CARTESIAN_POINT('Ctrl Pts',(2.53761520271995,1.05972122887324,7.51860402984327));
#385909=CARTESIAN_POINT('Origin',(0.,0.,7.5));
#385910=CARTESIAN_POINT('Origin',(2.50568666557813,0.915681362418256,7.5));
#385911=CARTESIAN_POINT('',(2.50568666557813,0.915681362418256,7.59394543036555));
#385912=CARTESIAN_POINT('',(2.50568666557813,0.915681362418256,8.85049129520029));
#385913=CARTESIAN_POINT('',(2.50568666557813,0.915681362418256,7.5));
#385914=CARTESIAN_POINT('',(2.57642062555679,0.905294943272749,8.78727029226991));
#385915=CARTESIAN_POINT('Ctrl Pts',(2.50568666557813,0.915681362418256,
8.85049129520029));
#385916=CARTESIAN_POINT('Ctrl Pts',(2.5292989251247,0.912214190147721,8.82945686509571));
#385917=CARTESIAN_POINT('Ctrl Pts',(2.55287608219231,0.908752172248009,
8.80838212259897));
#385918=CARTESIAN_POINT('Ctrl Pts',(2.5764206255568,0.905294943272749,8.78727029226991));
#385919=CARTESIAN_POINT('',(2.59029443537465,0.903257743546384,8.75721825406948));
#385920=CARTESIAN_POINT('Origin',(2.54854335809215,0.909388583893973,8.75937679713106));
#385921=CARTESIAN_POINT('',(2.59029443537465,0.903257743546384,7.51860402984325));
#385922=CARTESIAN_POINT('',(2.59029443537465,0.903257743546384,7.5));
#385923=CARTESIAN_POINT('Ctrl Pts',(2.59029443537465,0.903257743546384,
7.51860402984325));
#385924=CARTESIAN_POINT('Ctrl Pts',(2.5793987155483,0.904857647086956,7.52834476460825));
#385925=CARTESIAN_POINT('Ctrl Pts',(2.56849592237787,0.906458589261826,
7.53807742314407));
#385926=CARTESIAN_POINT('Ctrl Pts',(2.5575858183664,0.908060604944513,7.54780169004674));
#385927=CARTESIAN_POINT('Ctrl Pts',(2.54030480325306,0.910598111204327,
7.5632044032688));
#385928=CARTESIAN_POINT('Ctrl Pts',(2.52300542420908,0.913138313983315,
7.57858609112103));
#385929=CARTESIAN_POINT('Ctrl Pts',(2.50568666557813,0.915681362418256,
7.59394543036555));
#385930=CARTESIAN_POINT('Origin',(2.68279368784111,1.13380819535556,7.5));
#385931=CARTESIAN_POINT('',(2.55788654645047,0.991320447028643,8.75721825406948));
#385932=CARTESIAN_POINT('',(2.54864296074702,0.98077583205558,8.78727029226991));
#385933=CARTESIAN_POINT('Origin',(2.5251792925462,0.954009666308747,8.75658640621048));
#385934=CARTESIAN_POINT('',(2.50151564461751,0.927015373804568,8.85049129520029));
#385935=CARTESIAN_POINT('Ctrl Pts',(2.54864296074703,0.98077583205558,8.78727029226991));
#385936=CARTESIAN_POINT('Ctrl Pts',(2.53295613735133,0.962881097461795,
8.80838212259897));
#385937=CARTESIAN_POINT('Ctrl Pts',(2.51724758470003,0.9449615752324,8.82945686509571));
#385938=CARTESIAN_POINT('Ctrl Pts',(2.50151564461751,0.927015373804568,
8.85049129520029));
#385939=CARTESIAN_POINT('',(2.50151564461751,0.927015373804568,7.59394543036555));
#385940=CARTESIAN_POINT('',(2.50151564461751,0.927015373804568,7.5));
#385941=CARTESIAN_POINT('',(2.55788654645047,0.991320447028643,7.51860402984325));
#385942=CARTESIAN_POINT('Ctrl Pts',(2.50151564461751,0.927015373804568,
7.59394543036555));
#385943=CARTESIAN_POINT('Ctrl Pts',(2.51305446717485,0.940178278873355,
7.57858609112103));
#385944=CARTESIAN_POINT('Ctrl Pts',(2.52458037785886,0.953326454730193,
7.56320440326857));
#385945=CARTESIAN_POINT('Ctrl Pts',(2.53609405336255,0.966460673312278,
7.54780169004651));
#385946=CARTESIAN_POINT('Ctrl Pts',(2.54336303591222,0.974752760895097,
7.53807742314383));
#385947=CARTESIAN_POINT('Ctrl Pts',(2.55062714752992,0.983039291965133,
7.52834476460825));
#385948=CARTESIAN_POINT('Ctrl Pts',(2.55788654645047,0.991320447028641,
7.51860402984325));
#385949=CARTESIAN_POINT('',(2.55788654645047,0.991320447028643,7.5));
#385950=CARTESIAN_POINT('Origin',(2.50668546515629,0.922483422723978,7.5));
#385951=CARTESIAN_POINT('Ctrl Pts',(2.50151564461751,0.927015373804568,
8.85049129520029));
#385952=CARTESIAN_POINT('Ctrl Pts',(2.50138798433082,0.926869745407353,
8.85097269580138));
#385953=CARTESIAN_POINT('Ctrl Pts',(2.50126825987752,0.926720409638632,
8.85143669361005));
#385954=CARTESIAN_POINT('Ctrl Pts',(2.5011516404654,0.926559943194764,8.8519052845931));
#385955=CARTESIAN_POINT('Ctrl Pts',(2.50092354029102,0.92624608100697,8.85282181883899));
#385956=CARTESIAN_POINT('Ctrl Pts',(2.5007133460343,0.925897594557944,8.85372622499636));
#385957=CARTESIAN_POINT('Ctrl Pts',(2.50053096238414,0.925501051932918,
8.85462257735071));
#385958=CARTESIAN_POINT('Ctrl Pts',(2.50037955395543,0.925171856329486,
8.85536669723987));
#385959=CARTESIAN_POINT('Ctrl Pts',(2.5002472486102,0.924809479847003,8.85610498449051));
#385960=CARTESIAN_POINT('Ctrl Pts',(2.50014721912377,0.924403462300365,
8.85681338218371));
#385961=CARTESIAN_POINT('Ctrl Pts',(2.50005644220773,0.924035000739128,
8.85745625420284));
#385962=CARTESIAN_POINT('Ctrl Pts',(2.49999052655124,0.923626119378991,
8.85808743050666));
#385963=CARTESIAN_POINT('Ctrl Pts',(2.49997297445494,0.923160524417053,
8.8586680450841));
#385964=CARTESIAN_POINT('Ctrl Pts',(2.49996487629819,0.922945708994476,
8.85893592806395));
#385965=CARTESIAN_POINT('Ctrl Pts',(2.49996728752533,0.92271870761434,8.85919241173848));
#385966=CARTESIAN_POINT('Ctrl Pts',(2.49998401765522,0.922477377954862,
8.85943017985535));
#385967=CARTESIAN_POINT('Ctrl Pts',(2.50000660828322,0.922151511473342,
8.85975123720001));
#385968=CARTESIAN_POINT('Ctrl Pts',(2.500056520566,0.921791270397994,8.86004599534705));
#385969=CARTESIAN_POINT('Ctrl Pts',(2.50014347136777,0.921402412271963,
8.86026130871721));
#385970=CARTESIAN_POINT('Ctrl Pts',(2.50017530650771,0.921260040348952,
8.86034014101235));
#385971=CARTESIAN_POINT('Ctrl Pts',(2.50021257282626,0.921111691043425,
8.86040910639692));
#385972=CARTESIAN_POINT('Ctrl Pts',(2.50025458126596,0.920961488003178,
8.86046313645506));
#385973=CARTESIAN_POINT('Ctrl Pts',(2.50032013508429,0.920727097416814,
8.86054744990829));
#385974=CARTESIAN_POINT('Ctrl Pts',(2.50039916763199,0.92048183418458,8.86059655985669));
#385975=CARTESIAN_POINT('Ctrl Pts',(2.50048633147295,0.920241337932643,
8.86059725258816));
#385976=CARTESIAN_POINT('Ctrl Pts',(2.50057369669721,0.920000286038284,
8.86059794692011));
#385977=CARTESIAN_POINT('Ctrl Pts',(2.50067269750015,0.919762255163163,
8.86056369958366));
#385978=CARTESIAN_POINT('Ctrl Pts',(2.50077445977492,0.919538782504412,
8.86048590497774));
#385979=CARTESIAN_POINT('Ctrl Pts',(2.50080101669881,0.91948046279406,8.86046560290182));
#385980=CARTESIAN_POINT('Ctrl Pts',(2.5008281896189,0.919422413409564,8.86044257503091));
#385981=CARTESIAN_POINT('Ctrl Pts',(2.5008551091393,0.919366414208263,8.86041778462584));
#385982=CARTESIAN_POINT('Ctrl Pts',(2.50103624410722,0.918989609072723,
8.86025097596201));
#385983=CARTESIAN_POINT('Ctrl Pts',(2.50123051112959,0.918655209975485,
8.85998489822951));
#385984=CARTESIAN_POINT('Ctrl Pts',(2.50142491409744,0.918368721174964,
8.85968173251462));
#385985=CARTESIAN_POINT('Ctrl Pts',(2.50152774212946,0.918217185013339,
8.85952137522077));
#385986=CARTESIAN_POINT('Ctrl Pts',(2.50163243226652,0.91807602501943,8.85934740853961));
#385987=CARTESIAN_POINT('Ctrl Pts',(2.50173625951288,0.917946305822599,
8.8591675900182));
#385988=CARTESIAN_POINT('Ctrl Pts',(2.5021531798753,0.917425415820627,8.85844552518695));
#385989=CARTESIAN_POINT('Ctrl Pts',(2.50257738764837,0.917057671454099,
8.85759444184125));
#385990=CARTESIAN_POINT('Ctrl Pts',(2.5029501956441,0.91678889933161,8.85683498915139));
#385991=CARTESIAN_POINT('Ctrl Pts',(2.50298920900799,0.916760773044789,
8.85675551444998));
#385992=CARTESIAN_POINT('Ctrl Pts',(2.50302766777014,0.91673374878028,8.85667699793651));
#385993=CARTESIAN_POINT('Ctrl Pts',(2.50306550949756,0.916707776672099,
8.85659965593547));
#385994=CARTESIAN_POINT('Ctrl Pts',(2.50357629906516,0.916357203830595,
8.85555568965886));
#385995=CARTESIAN_POINT('Ctrl Pts',(2.50411782914084,0.916094049730749,
8.85434650606346));
#385996=CARTESIAN_POINT('Ctrl Pts',(2.50469006045449,0.915911423788039,
8.85297329937117));
#385997=CARTESIAN_POINT('Ctrl Pts',(2.50501190570186,0.915808707822827,
8.85220095427747));
#385998=CARTESIAN_POINT('Ctrl Pts',(2.50534369019835,0.91573172416885,8.85137579139183));
#385999=CARTESIAN_POINT('Ctrl Pts',(2.50568666557813,0.915681362418256,
8.85049129520029));
#386000=CARTESIAN_POINT('Origin',(2.50668546515629,0.922483422723978,7.59394543036555));
#386001=CARTESIAN_POINT('Ctrl Pts',(2.50114500373946,0.926592565440176,
7.59443877723642));
#386002=CARTESIAN_POINT('Ctrl Pts',(2.49732775931655,0.922238046102233,
7.58783886950016));
#386003=CARTESIAN_POINT('Ctrl Pts',(2.50224377712737,0.91531620021978,7.58559994247159));
#386004=CARTESIAN_POINT('Ctrl Pts',(2.52198322905087,0.950363758749822,
7.56670252222133));
#386005=CARTESIAN_POINT('Ctrl Pts',(2.51817150162988,0.946015532928613,
7.56004874999025));
#386006=CARTESIAN_POINT('Ctrl Pts',(2.5230992292225,0.939040301174041,7.55786368756704));
#386007=CARTESIAN_POINT('Ctrl Pts',(2.54278254105854,0.974090561731036,
7.53888913333559));
#386008=CARTESIAN_POINT('Ctrl Pts',(2.53894816035486,0.969716494190849,
7.53222002137277));
#386009=CARTESIAN_POINT('Ctrl Pts',(2.54391559872046,0.96272171036261,7.53005029815327));
#386010=CARTESIAN_POINT('Ctrl Pts',(2.56354199857947,0.997771900729855,
7.51101258149734));
#386011=CARTESIAN_POINT('Ctrl Pts',(2.55966113821443,0.99334481154321,7.5043616886572));
#386012=CARTESIAN_POINT('Ctrl Pts',(2.5646919192062,0.986359203183337,7.50217374673251));
#386013=CARTESIAN_POINT('',(2.56358326728469,0.98509787688097,7.50366116523517));
#386014=CARTESIAN_POINT('Ctrl Pts',(2.55788654645047,0.991320447028644,
7.51860402984325));
#386015=CARTESIAN_POINT('Ctrl Pts',(2.55817765342151,0.99165252713523,7.51734760759493));
#386016=CARTESIAN_POINT('Ctrl Pts',(2.55848545024178,0.991913389124431,
7.51608817408572));
#386017=CARTESIAN_POINT('Ctrl Pts',(2.5588178627193,0.992092245848213,7.51481005913119));
#386018=CARTESIAN_POINT('Ctrl Pts',(2.5591189698847,0.992254258542534,7.51365231206383));
#386019=CARTESIAN_POINT('Ctrl Pts',(2.55944058051348,0.992349433202007,
7.51247773061042));
#386020=CARTESIAN_POINT('Ctrl Pts',(2.55978760768028,0.992340715789489,
7.51129758471022));
#386021=CARTESIAN_POINT('Ctrl Pts',(2.5602189228166,0.992329881041294,7.50983079813402));
#386022=CARTESIAN_POINT('Ctrl Pts',(2.56067540818268,0.992145882723034,
7.50839324291155));
#386023=CARTESIAN_POINT('Ctrl Pts',(2.56112957542531,0.991710916073226,
7.50715379678855));
#386024=CARTESIAN_POINT('Ctrl Pts',(2.5613393876049,0.991509974014278,7.50658120839351));
#386025=CARTESIAN_POINT('Ctrl Pts',(2.56157195964613,0.991220042996603,
7.50598221009429));
#386026=CARTESIAN_POINT('Ctrl Pts',(2.56180401337726,0.990833789954918,
7.50545747549612));
#386027=CARTESIAN_POINT('Ctrl Pts',(2.56192784443093,0.990627673376225,
7.50517746087247));
#386028=CARTESIAN_POINT('Ctrl Pts',(2.56205304424277,0.990391997191143,
7.50491486231392));
#386029=CARTESIAN_POINT('Ctrl Pts',(2.56217482425125,0.990132219959011,
7.50468370960992));
#386030=CARTESIAN_POINT('Ctrl Pts',(2.56235692377725,0.989743771054887,
7.50433806340446));
#386031=CARTESIAN_POINT('Ctrl Pts',(2.56253633316337,0.989289548577592,
7.50405484070983));
#386032=CARTESIAN_POINT('Ctrl Pts',(2.56270030321808,0.988799880389195,
7.5038576603613));
#386033=CARTESIAN_POINT('Ctrl Pts',(2.56271783726676,0.988747517987619,
7.50383657498791));
#386034=CARTESIAN_POINT('Ctrl Pts',(2.56273520068951,0.988694778002053,
7.50381643264937));
#386035=CARTESIAN_POINT('Ctrl Pts',(2.56275238251344,0.988641717600799,
7.50379723213559));
#386036=CARTESIAN_POINT('Ctrl Pts',(2.56286707680879,0.988287522065131,
7.50366906242519));
#386037=CARTESIAN_POINT('Ctrl Pts',(2.56297548985005,0.987911122718402,
7.50358235568538));
#386038=CARTESIAN_POINT('Ctrl Pts',(2.5630712656504,0.987545808184195,7.5035341175365));
#386039=CARTESIAN_POINT('Ctrl Pts',(2.56321487062329,0.986998060385773,
7.50346178989177));
#386040=CARTESIAN_POINT('Ctrl Pts',(2.56334606729218,0.986402702482696,
7.50346967198527));
#386041=CARTESIAN_POINT('Ctrl Pts',(2.56345687801436,0.985814282467652,
7.50354272648693));
#386042=CARTESIAN_POINT('Ctrl Pts',(2.56350245675804,0.985572253135891,
7.50357277531559));
#386043=CARTESIAN_POINT('Ctrl Pts',(2.56354466529948,0.985331745408197,
7.50361331098761));
#386044=CARTESIAN_POINT('Ctrl Pts',(2.56358326728602,0.985097876881478,
7.50366116523659));
#386045=CARTESIAN_POINT('',(2.50943323048235,0.923494625763825,7.57603338622103));
#386046=CARTESIAN_POINT('Origin',(2.51772740356821,0.926543917882798,7.58486873427629));
#386047=CARTESIAN_POINT('Ctrl Pts',(2.56358326731836,0.985097876927392,
7.50366116529969));
#386048=CARTESIAN_POINT('Ctrl Pts',(2.54556333673348,0.964596415991244,
7.5278357307971));
#386049=CARTESIAN_POINT('Ctrl Pts',(2.52751419016024,0.944062956655914,
7.55196141284068));
#386050=CARTESIAN_POINT('Ctrl Pts',(2.50943323100971,0.923494626899403,
7.57603338728831));
#386051=CARTESIAN_POINT('Ctrl Pts',(2.50232577352107,0.927672813292166,
7.59639677331371));
#386052=CARTESIAN_POINT('Ctrl Pts',(2.48825599434034,0.916006055835398,
7.59959882295466));
#386053=CARTESIAN_POINT('Ctrl Pts',(2.50654858601383,0.915706218428471,
7.59642833564546));
#386054=CARTESIAN_POINT('Ctrl Pts',(2.49896195408414,0.925698016371091,
7.58707626057422));
#386055=CARTESIAN_POINT('Ctrl Pts',(2.49729432017831,0.919130574845469,
7.58809943920598));
#386056=CARTESIAN_POINT('Ctrl Pts',(2.50274613781078,0.915131564305941,
7.58710240504253));
#386057=CARTESIAN_POINT('Ctrl Pts',(2.50482266671419,0.924092500961746,
7.5801537675693));
#386058=CARTESIAN_POINT('Ctrl Pts',(2.50376748561201,0.921443753288322,
7.58205880659761));
#386059=CARTESIAN_POINT('Ctrl Pts',(2.50623637659076,0.920090367765581,
7.58020924244128));
#386060=CARTESIAN_POINT('Ctrl Pts',(2.50943322970563,0.923494625478202,
7.57603338509286));
#386061=CARTESIAN_POINT('Ctrl Pts',(2.50943322970563,0.923494625478202,
7.57603338509286));
#386062=CARTESIAN_POINT('Ctrl Pts',(2.50943322970563,0.923494625478202,
7.57603338509286));
#386063=CARTESIAN_POINT('Origin',(2.51772543279328,0.926549273113992,7.58486873427622));
#386064=CARTESIAN_POINT('Ctrl Pts',(2.5988096000392,0.902007395491139,7.51098857897448));
#386065=CARTESIAN_POINT('Ctrl Pts',(2.5929847431161,0.902862704673379,7.50433767179956));
#386066=CARTESIAN_POINT('Ctrl Pts',(2.59228715441969,0.911442997272883,
7.50214974420965));
#386067=CARTESIAN_POINT('Ctrl Pts',(2.56764251675708,0.90658390146661,7.53887321589171));
#386068=CARTESIAN_POINT('Ctrl Pts',(2.56188745195716,0.907428962526944,
7.53220407452065));
#386069=CARTESIAN_POINT('Ctrl Pts',(2.56113565724649,0.915975173654399,
7.53003438070911));
#386070=CARTESIAN_POINT('Ctrl Pts',(2.53641558117792,0.911169196021767,
7.56669465659233));
#386071=CARTESIAN_POINT('Ctrl Pts',(2.53069452774099,0.912009262928332,
7.56004085833297));
#386072=CARTESIAN_POINT('Ctrl Pts',(2.52992516332406,0.920514833368955,
7.55785582193789));
#386073=CARTESIAN_POINT('Ctrl Pts',(2.50513020557114,0.915763071782075,
7.59443891967696));
#386074=CARTESIAN_POINT('Ctrl Pts',(2.49940085731905,0.91660435668108,7.58783901202978));
#386075=CARTESIAN_POINT('Ctrl Pts',(2.49865720208422,0.925061670372792,
7.58560008491213));
#386076=CARTESIAN_POINT('',(2.59059853376831,0.911688670640886,7.50366116523517));
#386077=CARTESIAN_POINT('Ctrl Pts',(2.59059853376866,0.91168867064101,7.50366116523554));
#386078=CARTESIAN_POINT('Ctrl Pts',(2.59098904347061,0.911039332755585,
7.50350835821027));
#386079=CARTESIAN_POINT('Ctrl Pts',(2.59132689113599,0.910429728813554,
7.50345484956));
#386080=CARTESIAN_POINT('Ctrl Pts',(2.5916226464834,0.909842025882762,7.50349758195598));
#386081=CARTESIAN_POINT('Ctrl Pts',(2.59177439091041,0.909540490694081,
7.50351950684424));
#386082=CARTESIAN_POINT('Ctrl Pts',(2.59193012691096,0.909215058506864,
7.50357029184312));
#386083=CARTESIAN_POINT('Ctrl Pts',(2.5920716753196,0.908897119992529,7.50365515313924));
#386084=CARTESIAN_POINT('Ctrl Pts',(2.5922894340907,0.908408001811463,7.50378570417639));
#386085=CARTESIAN_POINT('Ctrl Pts',(2.59248032444165,0.907922402436793,
7.50400001621911));
#386086=CARTESIAN_POINT('Ctrl Pts',(2.59262770382891,0.907476452400882,
7.50428903009635));
#386087=CARTESIAN_POINT('Ctrl Pts',(2.59264406180703,0.907426955377829,
7.50432110841318));
#386088=CARTESIAN_POINT('Ctrl Pts',(2.59265990793161,0.907377928509123,
7.50435406373355));
#386089=CARTESIAN_POINT('Ctrl Pts',(2.59267523710345,0.907329407449752,
7.50438785222352));
#386090=CARTESIAN_POINT('Ctrl Pts',(2.59276882906568,0.907033163060106,
7.50459414719562));
#386091=CARTESIAN_POINT('Ctrl Pts',(2.59284414892436,0.90675090178871,7.50483629897752));
#386092=CARTESIAN_POINT('Ctrl Pts',(2.59289958273718,0.906493776284968,
7.5050991045531));
#386093=CARTESIAN_POINT('Ctrl Pts',(2.59302187529608,0.905926531597902,
7.50567888004914));
#386094=CARTESIAN_POINT('Ctrl Pts',(2.593052712494,0.905459376620307,7.50637912803144));
#386095=CARTESIAN_POINT('Ctrl Pts',(2.59302239896678,0.905086224694295,
7.50710440483569));
#386096=CARTESIAN_POINT('Ctrl Pts',(2.59301496548809,0.904994720433934,
7.50728225710685));
#386097=CARTESIAN_POINT('Ctrl Pts',(2.59300385233831,0.904907035449151,
7.50746498566954));
#386098=CARTESIAN_POINT('Ctrl Pts',(2.59298973222145,0.904825164211477,
7.50764697238949));
#386099=CARTESIAN_POINT('Ctrl Pts',(2.59291382635912,0.904385046969313,
7.50862528291182));
#386100=CARTESIAN_POINT('Ctrl Pts',(2.59274821214765,0.904072281556945,
7.50965856837421));
#386101=CARTESIAN_POINT('Ctrl Pts',(2.5925409885644,0.903841240304918,7.51067959873202));
#386102=CARTESIAN_POINT('Ctrl Pts',(2.59242695316516,0.903714098012506,
7.51124147302578));
#386103=CARTESIAN_POINT('Ctrl Pts',(2.59229996591968,0.903611963391194,
7.51180065547253));
#386104=CARTESIAN_POINT('Ctrl Pts',(2.59216608810208,0.9035291187079,7.51235175716501));
#386105=CARTESIAN_POINT('Ctrl Pts',(2.59170348691166,0.903242857325715,
7.51425603304536));
#386106=CARTESIAN_POINT('Ctrl Pts',(2.59110026610329,0.903157939223945,
7.5162690050518));
#386107=CARTESIAN_POINT('Ctrl Pts',(2.590407685676,0.903242504084119,7.51827788969243));
#386108=CARTESIAN_POINT('Ctrl Pts',(2.59037020191448,0.903247080894157,
7.51838661432545));
#386109=CARTESIAN_POINT('Ctrl Pts',(2.59033244978269,0.903252161594292,
7.51849533314856));
#386110=CARTESIAN_POINT('Ctrl Pts',(2.59029443537465,0.90325774354638,7.51860402984325));
#386111=CARTESIAN_POINT('Ctrl Pts',(2.50943323162122,0.923494625241175,
7.57603338728985));
#386112=CARTESIAN_POINT('Ctrl Pts',(2.53653388028815,0.91955354481261,7.55196141284922));
#386113=CARTESIAN_POINT('Ctrl Pts',(2.56358770141575,0.915618394507179,
7.52783573083105));
#386114=CARTESIAN_POINT('Ctrl Pts',(2.59059853382585,0.911688670627024,
7.50366116530176));
#386115=CARTESIAN_POINT('Origin',(8.67125181207502E-16,3.19110082301679E-16,
7.49482233047033));
#386116=CARTESIAN_POINT('Origin',(2.55533261422667,0.981927431468074,7.49482233047033));
#386117=CARTESIAN_POINT('Origin',(0.,0.,7.50366116523517));
#386118=CARTESIAN_POINT('Origin',(2.58226093460096,0.908754485894723,7.49482233047033));
#386119=CARTESIAN_POINT('Ctrl Pts',(2.55788584917514,0.99131965168011,7.51860402984325));
#386120=CARTESIAN_POINT('Ctrl Pts',(2.56290210620281,0.997040967216104,
7.51860402984325));
#386121=CARTESIAN_POINT('Ctrl Pts',(2.56012379910316,1.00412456063259,7.51860402984325));
#386122=CARTESIAN_POINT('Ctrl Pts',(2.55974841868675,0.993444016020654,
7.51041458714366));
#386123=CARTESIAN_POINT('Ctrl Pts',(2.56224388421272,0.998719148016046,
7.51004642900443));
#386124=CARTESIAN_POINT('Ctrl Pts',(2.56012303287905,1.00412651420355,7.5072913648301));
#386125=CARTESIAN_POINT('Ctrl Pts',(2.56237524877722,0.992432333820012,
7.50215815450138));
#386126=CARTESIAN_POINT('Ctrl Pts',(2.56358422056863,0.99530225571599,7.49877163671529));
#386127=CARTESIAN_POINT('Ctrl Pts',(2.56234666411195,0.998522873298203,
7.4948158853317));
#386128=CARTESIAN_POINT('Ctrl Pts',(2.56358275340116,0.985097679412492,
7.50366171572174));
#386129=CARTESIAN_POINT('Ctrl Pts',(2.5670007996799,0.986411118369394,7.50000045605858));
#386130=CARTESIAN_POINT('Ctrl Pts',(2.56700079967986,0.986411118369511,
7.49482233047317));
#386131=CARTESIAN_POINT('Origin',(2.5484868727436,0.999560358084262,7.51860402984325));
#386132=CARTESIAN_POINT('Origin',(2.5484868727436,0.999560358084262,9.));
#386133=CARTESIAN_POINT('Origin',(2.5484868727436,0.999560358084262,8.75721825406948));
#386134=CARTESIAN_POINT('Ctrl Pts',(2.54687789636137,0.97876238172157,8.78942910404913));
#386135=CARTESIAN_POINT('Ctrl Pts',(2.55056640146082,0.982939385292657,
8.79672699501689));
#386136=CARTESIAN_POINT('Ctrl Pts',(2.54507443236962,0.989975844734957,
8.79893251111266));
#386137=CARTESIAN_POINT('Ctrl Pts',(2.55412528766752,0.987029832235237,
8.78111911759583));
#386138=CARTESIAN_POINT('Ctrl Pts',(2.55849247346355,0.991986645561208,
8.78644465894816));
#386139=CARTESIAN_POINT('Ctrl Pts',(2.55499131469909,0.999298102261577,
8.78817647674132));
#386140=CARTESIAN_POINT('Ctrl Pts',(2.55864203477219,0.992182304613644,
8.7678092393203));
#386141=CARTESIAN_POINT('Ctrl Pts',(2.56379348971243,0.998036982125591,
8.76988516158372));
#386142=CARTESIAN_POINT('Ctrl Pts',(2.56117757667523,1.00512876465032,8.77093053738832));
#386143=CARTESIAN_POINT('Ctrl Pts',(2.5577613309015,0.991177643017536,8.75371302330492));
#386144=CARTESIAN_POINT('Ctrl Pts',(2.56278692529023,0.996888124819248,
8.75300828287559));
#386145=CARTESIAN_POINT('Ctrl Pts',(2.55997069051277,1.0039918816431,8.75267964240738));
#386146=CARTESIAN_POINT('Origin',(2.53924328704016,0.989015743111198,8.78727029226991));
#386147=CARTESIAN_POINT('Ctrl Pts',(2.50151564461751,0.927015373804568,
8.85049129520029));
#386148=CARTESIAN_POINT('Ctrl Pts',(2.50536507777435,0.931406612421877,
8.85711686593484));
#386149=CARTESIAN_POINT('Ctrl Pts',(2.50039125247053,0.938360879023106,
8.85933012996512));
#386150=CARTESIAN_POINT('Ctrl Pts',(2.51724760581287,0.94496159931686,8.82945683644722));
#386151=CARTESIAN_POINT('Ctrl Pts',(2.52112899159229,0.94938928786971,8.83607469902387));
#386152=CARTESIAN_POINT('Ctrl Pts',(2.51611005976582,0.956342155322669,
8.8382956714852));
#386153=CARTESIAN_POINT('Ctrl Pts',(2.53295611725146,0.96288107453287,8.80838214965003));
#386154=CARTESIAN_POINT('Ctrl Pts',(2.53685282079135,0.967326236811966,
8.81501364461989));
#386155=CARTESIAN_POINT('Ctrl Pts',(2.5318055257756,0.974295714957373,8.81722098428721));
#386156=CARTESIAN_POINT('Ctrl Pts',(2.54864296074703,0.98077583205558,8.78727029226991));
#386157=CARTESIAN_POINT('Ctrl Pts',(2.5525403115422,0.985221732690743,8.79393457792714));
#386158=CARTESIAN_POINT('Ctrl Pts',(2.54747944236022,0.992223662303431,
8.79610912703474));
#386159=CARTESIAN_POINT('Origin',(2.49211597091065,0.935255284860186,8.85049129520029));
#386160=CARTESIAN_POINT('Ctrl Pts',(2.50568666557813,0.915681362418256,
8.85049129520029));
#386161=CARTESIAN_POINT('Ctrl Pts',(2.51146432645972,0.914832983398971,
8.85711686593484));
#386162=CARTESIAN_POINT('Ctrl Pts',(2.51218498036395,0.906313510406806,
8.85933012996512));
#386163=CARTESIAN_POINT('Ctrl Pts',(2.50057525239759,0.916431911090139,
8.86332496987232));
#386164=CARTESIAN_POINT('Ctrl Pts',(2.50243304714704,0.912201013662211,
8.86648636486736));
#386165=CARTESIAN_POINT('Ctrl Pts',(2.4978880826035,0.908430151799111,8.87206031107457));
#386166=CARTESIAN_POINT('Ctrl Pts',(2.49808696496685,0.923104109502799,
8.86341338519875));
#386167=CARTESIAN_POINT('Ctrl Pts',(2.49672688175244,0.927533967771879,
8.86654584966058));
#386168=CARTESIAN_POINT('Ctrl Pts',(2.49080184592933,0.927399419334149,
8.87215952290715));
#386169=CARTESIAN_POINT('Ctrl Pts',(2.50151564461751,0.927015373804567,
8.85049129520029));
#386170=CARTESIAN_POINT('Ctrl Pts',(2.50536507777435,0.931406612421877,
8.85711686593484));
#386171=CARTESIAN_POINT('Ctrl Pts',(2.50039125247053,0.938360879023106,
8.85933012996512));
#386172=CARTESIAN_POINT('Origin',(2.50387066634511,0.903313980044218,8.85049129520029));
#386173=CARTESIAN_POINT('Ctrl Pts',(2.5764206255568,0.905294943272749,8.78727029226991));
#386174=CARTESIAN_POINT('Ctrl Pts',(2.58227020660256,0.904436003654703,
8.79393457792714));
#386175=CARTESIAN_POINT('Ctrl Pts',(2.58295547781499,0.895823813541636,
8.79610912703474));
#386176=CARTESIAN_POINT('Ctrl Pts',(2.55287605202415,0.908752176677835,
8.80838214965003));
#386177=CARTESIAN_POINT('Ctrl Pts',(2.55872466159671,0.907893379708777,
8.81501364461997));
#386178=CARTESIAN_POINT('Ctrl Pts',(2.55939923284052,0.899314698794315,
8.81722098428721));
#386179=CARTESIAN_POINT('Ctrl Pts',(2.52929895681322,0.912214185494648,
8.82945683644722));
#386180=CARTESIAN_POINT('Ctrl Pts',(2.53512457577336,0.911358764416574,
8.83607469902387));
#386181=CARTESIAN_POINT('Ctrl Pts',(2.53580997653059,0.902811117471385,
8.83829567148519));
#386182=CARTESIAN_POINT('Ctrl Pts',(2.50568666557813,0.915681362418256,
8.85049129520029));
#386183=CARTESIAN_POINT('Ctrl Pts',(2.51146432645972,0.914832983398971,
8.85711686593484));
#386184=CARTESIAN_POINT('Ctrl Pts',(2.51218498036395,0.906313510406806,
8.85933012996512));
#386185=CARTESIAN_POINT('Origin',(2.57460462632378,0.892927560898711,8.78727029226991));
#386186=CARTESIAN_POINT('Ctrl Pts',(2.59011123601511,0.903284625492616,
8.75374538247848));
#386187=CARTESIAN_POINT('Ctrl Pts',(2.59763148283512,0.902193632296599,
8.75304829418601));
#386188=CARTESIAN_POINT('Ctrl Pts',(2.60009466821772,0.894968442957906,
8.75272238421917));
#386189=CARTESIAN_POINT('Ctrl Pts',(2.5914172155084,0.903092858766698,8.76769408445019));
#386190=CARTESIAN_POINT('Ctrl Pts',(2.59912660602631,0.901973728383564,
8.7697431809397));
#386191=CARTESIAN_POINT('Ctrl Pts',(2.60173221821703,0.894886476279139,
8.7707786988043));
#386192=CARTESIAN_POINT('Ctrl Pts',(2.58472350859536,0.904075745776096,
8.78108014887991));
#386193=CARTESIAN_POINT('Ctrl Pts',(2.59125748515533,0.903131083077539,
8.78639403366325));
#386194=CARTESIAN_POINT('Ctrl Pts',(2.59334711156538,0.895310882492175,
8.78812224174741));
#386195=CARTESIAN_POINT('Ctrl Pts',(2.57375400061066,0.905686480575195,
8.78944554828685));
#386196=CARTESIAN_POINT('Ctrl Pts',(2.57926139477576,0.904895894003568,
8.79673892988685));
#386197=CARTESIAN_POINT('Ctrl Pts',(2.57964297993741,0.895987586247271,
8.79894799272499));
#386198=CARTESIAN_POINT('Origin',(2.58847843614163,0.890890361172345,8.75721825406948));
#386199=CARTESIAN_POINT('Origin',(2.58847843614163,0.890890361172345,9.));
#386200=CARTESIAN_POINT('Origin',(2.58847843614163,0.890890361172345,7.51860402984325));
#386201=CARTESIAN_POINT('Ctrl Pts',(2.59059779171497,0.911688409495914,
7.50366195182966));
#386202=CARTESIAN_POINT('Ctrl Pts',(2.5940520804211,0.912904049757124,7.50000065167735));
#386203=CARTESIAN_POINT('Ctrl Pts',(2.59405208042114,0.912904049757014,
7.49482233047108));
#386204=CARTESIAN_POINT('Ctrl Pts',(2.59443552903803,0.905314590244799,
7.50215800491337));
#386205=CARTESIAN_POINT('Ctrl Pts',(2.5972168015806,0.903911301173251,7.49877273257264));
#386206=CARTESIAN_POINT('Ctrl Pts',(2.59836280844753,0.900654949747057,
7.49481816995649));
#386207=CARTESIAN_POINT('Ctrl Pts',(2.59308316643741,0.902848595164,7.51043025814043));
#386208=CARTESIAN_POINT('Ctrl Pts',(2.59840734464655,0.900451537929794,
7.51006209594516));
#386209=CARTESIAN_POINT('Ctrl Pts',(2.60029879634861,0.894955959650746,
7.50731281821699));
#386210=CARTESIAN_POINT('Ctrl Pts',(2.59029293998907,0.903257963033155,
7.51860402984326));
#386211=CARTESIAN_POINT('Ctrl Pts',(2.59782161551911,0.902153398795956,
7.51860402984326));
#386212=CARTESIAN_POINT('Ctrl Pts',(2.60029797237972,0.894958353689109,
7.51860402984327));
#386213=CARTESIAN_POINT('Origin',(0.,0.,7.5));
#386214=CARTESIAN_POINT('Origin',(2.55920636991202,0.753260100986319,7.5));
#386215=CARTESIAN_POINT('',(2.55920636991202,0.753260100986319,7.59394543036555));
#386216=CARTESIAN_POINT('',(2.55920636991202,0.753260100986319,8.85049129520029));
#386217=CARTESIAN_POINT('',(2.55920636991202,0.753260100986319,7.5));
#386218=CARTESIAN_POINT('',(2.62912953922426,0.738363081476946,8.78727029226991));
#386219=CARTESIAN_POINT('Ctrl Pts',(2.55920636991202,0.753260100986318,
8.85049129520029));
#386220=CARTESIAN_POINT('Ctrl Pts',(2.58254797304886,0.748287209729676,
8.82945686509571));
#386221=CARTESIAN_POINT('Ctrl Pts',(2.60585487607021,0.7433217112772,8.80838212259895));
#386222=CARTESIAN_POINT('Ctrl Pts',(2.62912953922426,0.738363081476946,
8.78727029226991));
#386223=CARTESIAN_POINT('',(2.64284431997726,0.735441169348907,8.75721825406948));
#386224=CARTESIAN_POINT('Origin',(2.60157182905073,0.744234413933357,8.75937679713113));
#386225=CARTESIAN_POINT('',(2.64284431997726,0.735441169348907,7.51860402984325));
#386226=CARTESIAN_POINT('',(2.64284431997726,0.735441169348907,7.5));
#386227=CARTESIAN_POINT('Ctrl Pts',(2.64284431997726,0.735441169348907,
7.51860402984325));
#386228=CARTESIAN_POINT('Ctrl Pts',(2.63207349274765,0.737735876882188,
7.52834476460825));
#386229=CARTESIAN_POINT('Ctrl Pts',(2.62129567325243,0.740032074106494,
7.53807742314407));
#386230=CARTESIAN_POINT('Ctrl Pts',(2.61051062671697,0.742329811040171,
7.54780169004674));
#386231=CARTESIAN_POINT('Ctrl Pts',(2.59342769588682,0.74596930216103,7.5632044032688));
#386232=CARTESIAN_POINT('Ctrl Pts',(2.57632661162329,0.74961266084185,7.57858609112103));
#386233=CARTESIAN_POINT('Ctrl Pts',(2.55920636991202,0.753260100986319,
7.59394543036555));
#386234=CARTESIAN_POINT('Origin',(2.74992494097309,0.959591483074807,7.5));
#386235=CARTESIAN_POINT('',(2.61614521332082,0.825399319134649,8.75721825406948));
#386236=CARTESIAN_POINT('',(2.60624502375464,0.815468607773385,8.78727029226991));
#386237=CARTESIAN_POINT('Origin',(2.58111465004893,0.790260758367688,8.75658640621043));
#386238=CARTESIAN_POINT('',(2.5557700913641,0.764838063661159,8.85049129520029));
#386239=CARTESIAN_POINT('Ctrl Pts',(2.60624502375464,0.815468607773385,
8.78727029226991));
#386240=CARTESIAN_POINT('Ctrl Pts',(2.58944391103809,0.798615698056782,
8.80838212259896));
#386241=CARTESIAN_POINT('Ctrl Pts',(2.57261952556176,0.781739443831623,
8.82945686509571));
#386242=CARTESIAN_POINT('Ctrl Pts',(2.5557700913641,0.764838063661159,8.85049129520029));
#386243=CARTESIAN_POINT('',(2.5557700913641,0.764838063661159,7.59394543036555));
#386244=CARTESIAN_POINT('',(2.5557700913641,0.764838063661159,7.5));
#386245=CARTESIAN_POINT('',(2.61614521332082,0.825399319134649,7.51860402984325));
#386246=CARTESIAN_POINT('Ctrl Pts',(2.5557700913641,0.764838063661158,7.59394543036555));
#386247=CARTESIAN_POINT('Ctrl Pts',(2.56812855639629,0.777234629230197,
7.57858609112103));
#386248=CARTESIAN_POINT('Ctrl Pts',(2.58047319238015,0.789617323116598,
7.56320440326857));
#386249=CARTESIAN_POINT('Ctrl Pts',(2.59280472407651,0.801986872315658,
7.54780169004651));
#386250=CARTESIAN_POINT('Ctrl Pts',(2.60059004759746,0.80979619760422,7.53807742314383));
#386251=CARTESIAN_POINT('Ctrl Pts',(2.60837015418731,0.817600289878136,
7.52834476460825));
#386252=CARTESIAN_POINT('Ctrl Pts',(2.61614521332082,0.825399319134647,
7.51860402984325));
#386253=CARTESIAN_POINT('',(2.61614521332082,0.825399319134649,7.5));
#386254=CARTESIAN_POINT('Origin',(2.56063892684944,0.759984192420934,7.5));
#386255=CARTESIAN_POINT('Ctrl Pts',(2.5557700913641,0.764838063661158,8.85049129520029));
#386256=CARTESIAN_POINT('Ctrl Pts',(2.55563336292571,0.764700913695755,
8.85097269580138));
#386257=CARTESIAN_POINT('Ctrl Pts',(2.55550431648359,0.764559555525447,
8.85143669361005));
#386258=CARTESIAN_POINT('Ctrl Pts',(2.5553776555582,0.764406890608487,8.8519052845931));
#386259=CARTESIAN_POINT('Ctrl Pts',(2.55512991482068,0.764108287712571,
8.85282181883899));
#386260=CARTESIAN_POINT('Ctrl Pts',(2.55489782482715,0.763773984458597,
8.85372622499635));
#386261=CARTESIAN_POINT('Ctrl Pts',(2.55469040933054,0.763389941933513,
8.8546225773507));
#386262=CARTESIAN_POINT('Ctrl Pts',(2.55451822035196,0.763071123469087,
8.85536669723986));
#386263=CARTESIAN_POINT('Ctrl Pts',(2.5543629693013,0.762717968360524,8.8561049844905));
#386264=CARTESIAN_POINT('Ctrl Pts',(2.55423713170265,0.762319193931679,
8.8568133821837));
#386265=CARTESIAN_POINT('Ctrl Pts',(2.55412293388424,0.761957305511216,
8.85745625420284));
#386266=CARTESIAN_POINT('Ctrl Pts',(2.55403095653984,0.761553487472297,
8.85808743050666));
#386267=CARTESIAN_POINT('Ctrl Pts',(2.55398360973458,0.761089973691814,
8.8586680450841));
#386268=CARTESIAN_POINT('Ctrl Pts',(2.55396176494498,0.760876118481245,
8.85893592806396));
#386269=CARTESIAN_POINT('Ctrl Pts',(2.55394962718963,0.760649429011939,
8.85919241173848));
#386270=CARTESIAN_POINT('Ctrl Pts',(2.5539508609013,0.760407523287027,8.85943017985534));
#386271=CARTESIAN_POINT('Ctrl Pts',(2.55395252677728,0.760080878946637,
8.8597512372));
#386272=CARTESIAN_POINT('Ctrl Pts',(2.55397925578498,0.759718180134276,
8.86004599534705));
#386273=CARTESIAN_POINT('Ctrl Pts',(2.55404111371133,0.759324550001974,
8.86026130871721));
#386274=CARTESIAN_POINT('Ctrl Pts',(2.55406376164212,0.759180430912929,
8.86034014101235));
#386275=CARTESIAN_POINT('Ctrl Pts',(2.55409144662039,0.759029998745733,
8.86040910639693));
#386276=CARTESIAN_POINT('Ctrl Pts',(2.55412374520742,0.758877412823769,
8.86046313645507));
#386277=CARTESIAN_POINT('Ctrl Pts',(2.55417414688197,0.758639303770441,
8.8605474499083));
#386278=CARTESIAN_POINT('Ctrl Pts',(2.55423730297957,0.758389480825107,
8.86059655985669));
#386279=CARTESIAN_POINT('Ctrl Pts',(2.55430887908532,0.758143894092047,
8.86059725258816));
#386280=CARTESIAN_POINT('Ctrl Pts',(2.55438062056045,0.757897739955521,
8.86059794692012));
#386281=CARTESIAN_POINT('Ctrl Pts',(2.55446416726509,0.757653855137138,
8.86056369958366));
#386282=CARTESIAN_POINT('Ctrl Pts',(2.55455140251595,0.757424321695602,
8.86048590497774));
#386283=CARTESIAN_POINT('Ctrl Pts',(2.55457416831912,0.757364420301395,
8.86046560290182));
#386284=CARTESIAN_POINT('Ctrl Pts',(2.55459756617269,0.757304749210617,
8.86044257503091));
#386285=CARTESIAN_POINT('Ctrl Pts',(2.5546208425029,0.757247140326087,8.86041778462584));
#386286=CARTESIAN_POINT('Ctrl Pts',(2.55477746332169,0.756859504019869,
8.86025097596201));
#386287=CARTESIAN_POINT('Ctrl Pts',(2.5549499061779,0.756513345250583,8.8599848982295));
#386288=CARTESIAN_POINT('Ctrl Pts',(2.55512555432353,0.756214989631114,
8.85968173251461));
#386289=CARTESIAN_POINT('Ctrl Pts',(2.55521846212913,0.756057176602153,
8.85952137522076));
#386290=CARTESIAN_POINT('Ctrl Pts',(2.55531389301721,0.755909599116478,
8.85934740853961));
#386291=CARTESIAN_POINT('Ctrl Pts',(2.55540919580187,0.755773494207136,
8.8591675900182));
#386292=CARTESIAN_POINT('Ctrl Pts',(2.55579188601969,0.755226962250202,
8.85844552518695));
#386293=CARTESIAN_POINT('Ctrl Pts',(2.55619166074993,0.754832794368578,
8.85759444184124));
#386294=CARTESIAN_POINT('Ctrl Pts',(2.55654648248264,0.754540688576943,
8.85683498915139));
#386295=CARTESIAN_POINT('Ctrl Pts',(2.556583613632,0.75451012048379,8.85675551444998));
#386296=CARTESIAN_POINT('Ctrl Pts',(2.55662026192593,0.754480687682179,
8.85667699793651));
#386297=CARTESIAN_POINT('Ctrl Pts',(2.55665636186477,0.754452344408681,
8.85659965593547));
#386298=CARTESIAN_POINT('Ctrl Pts',(2.55714364068135,0.754069765456718,
8.85555568965886));
#386299=CARTESIAN_POINT('Ctrl Pts',(2.55766719778434,0.753772456084119,
8.85434650606346));
#386300=CARTESIAN_POINT('Ctrl Pts',(2.55822655250307,0.753553542379849,
8.85297329937117));
#386301=CARTESIAN_POINT('Ctrl Pts',(2.55854115545037,0.753430416759805,
8.85220095427747));
#386302=CARTESIAN_POINT('Ctrl Pts',(2.55886732590038,0.753332333771325,
8.85137579139183));
#386303=CARTESIAN_POINT('Ctrl Pts',(2.55920636991202,0.753260100986319,
8.85049129520029));
#386304=CARTESIAN_POINT('Origin',(2.56063892684944,0.759984192420934,7.59394543036555));
#386305=CARTESIAN_POINT('Ctrl Pts',(2.55537312258256,0.764439871044488,
7.59443877723642));
#386306=CARTESIAN_POINT('Ctrl Pts',(2.55128472608583,0.760338870223441,
7.58783886950016));
#386307=CARTESIAN_POINT('Ctrl Pts',(2.55574715922245,0.753116275673151,
7.58559994247159));
#386308=CARTESIAN_POINT('Ctrl Pts',(2.57769155910976,0.786827114208349,
7.56670252222139));
#386309=CARTESIAN_POINT('Ctrl Pts',(2.57360907150672,0.782732040497738,
7.56004874999029));
#386310=CARTESIAN_POINT('Ctrl Pts',(2.57807976992147,0.775455419514101,
7.55786368756705));
#386311=CARTESIAN_POINT('Ctrl Pts',(2.59996831818662,0.809172551432348,
7.5388891333356));
#386312=CARTESIAN_POINT('Ctrl Pts',(2.59586156815985,0.805053140498195,
7.53222002137279));
#386313=CARTESIAN_POINT('Ctrl Pts',(2.60037064305195,0.797754463334677,
7.53005029815326));
#386314=CARTESIAN_POINT('Ctrl Pts',(2.62220239177471,0.83147517157032,7.51101258149734));
#386315=CARTESIAN_POINT('Ctrl Pts',(2.61804586047545,0.827305825890515,
7.5043616886572));
#386316=CARTESIAN_POINT('Ctrl Pts',(2.6226187357238,0.820012246967404,7.50217374673251));
#386317=CARTESIAN_POINT('',(2.62143154819291,0.818824543767695,7.50366116523517));
#386318=CARTESIAN_POINT('Ctrl Pts',(2.61614521332082,0.82539931913465,7.51860402984325));
#386319=CARTESIAN_POINT('Ctrl Pts',(2.61645699862685,0.825712065659369,
7.51734760759494));
#386320=CARTESIAN_POINT('Ctrl Pts',(2.61678087653057,0.825952671069652,
7.51608817408572));
#386321=CARTESIAN_POINT('Ctrl Pts',(2.61712406542064,0.826109862572553,
7.51481005913119));
#386322=CARTESIAN_POINT('Ctrl Pts',(2.61743493411804,0.826252250392093,
7.51365231206383));
#386323=CARTESIAN_POINT('Ctrl Pts',(2.61776198182467,0.826326623841287,
7.51247773061043));
#386324=CARTESIAN_POINT('Ctrl Pts',(2.61810773746039,0.826295690232712,
7.51129758471022));
#386325=CARTESIAN_POINT('Ctrl Pts',(2.61853747222881,0.826257243290004,
7.50983079813402));
#386326=CARTESIAN_POINT('Ctrl Pts',(2.61898123088401,0.8260443758982,7.50839324291155));
#386327=CARTESIAN_POINT('Ctrl Pts',(2.6194065965824,0.825581204338881,7.50715379678855));
#386328=CARTESIAN_POINT('Ctrl Pts',(2.61960310327844,0.825367232424444,
7.50658120839351));
#386329=CARTESIAN_POINT('Ctrl Pts',(2.61981662153139,0.825062996159295,
7.50598221009429));
#386330=CARTESIAN_POINT('Ctrl Pts',(2.62002345116589,0.824662668982309,
7.50545747549611));
#386331=CARTESIAN_POINT('Ctrl Pts',(2.62013382186084,0.824449042009384,
7.50517746087247));
#386332=CARTESIAN_POINT('Ctrl Pts',(2.62024366461122,0.824205828466814,
7.50491486231392));
#386333=CARTESIAN_POINT('Ctrl Pts',(2.6203485504252,0.823938782502934,7.50468370960992));
#386334=CARTESIAN_POINT('Ctrl Pts',(2.62050538780146,0.823539464552062,
7.50433806340447));
#386335=CARTESIAN_POINT('Ctrl Pts',(2.6206553264377,0.823074680524733,7.50405484070984));
#386336=CARTESIAN_POINT('Ctrl Pts',(2.62078758644981,0.822575512814678,
7.50385766036131));
#386337=CARTESIAN_POINT('Ctrl Pts',(2.62080172960231,0.822522134586908,
7.50383657498791));
#386338=CARTESIAN_POINT('Ctrl Pts',(2.62081567828758,0.822468390482977,
7.50381643264937));
#386339=CARTESIAN_POINT('Ctrl Pts',(2.62082942521803,0.822414338256762,
7.50379723213559));
#386340=CARTESIAN_POINT('Ctrl Pts',(2.62092119047576,0.822053521965076,
7.50366906242519));
#386341=CARTESIAN_POINT('Ctrl Pts',(2.62100526478185,0.821670949923771,
7.50358235568538));
#386342=CARTESIAN_POINT('Ctrl Pts',(2.62107743801798,0.821300249590857,
7.5035341175365));
#386343=CARTESIAN_POINT('Ctrl Pts',(2.62118565361712,0.820744426396829,
7.50346178989176));
#386344=CARTESIAN_POINT('Ctrl Pts',(2.62127843601656,0.820141885920979,
7.50346967198526));
#386345=CARTESIAN_POINT('Ctrl Pts',(2.62135131886642,0.819547575210617,
7.50354272648692));
#386346=CARTESIAN_POINT('Ctrl Pts',(2.62138129709116,0.819303122913942,
7.50357277531559));
#386347=CARTESIAN_POINT('Ctrl Pts',(2.6214080095276,0.819060405024635,7.50361331098761));
#386348=CARTESIAN_POINT('Ctrl Pts',(2.62143154819427,0.818824543768117,
7.50366116523658));
#386349=CARTESIAN_POINT('',(2.56344583459815,0.76081726790679,7.57603338622103));
#386350=CARTESIAN_POINT('Origin',(2.57191833523268,0.763328885433888,7.58486873427624));
#386351=CARTESIAN_POINT('Ctrl Pts',(2.62143154822949,0.818824543811863,
7.50366116529968));
#386352=CARTESIAN_POINT('Ctrl Pts',(2.60213510841253,0.799519746242575,
7.52783573079709));
#386353=CARTESIAN_POINT('Ctrl Pts',(2.58280746249008,0.780184887893108,
7.55196141284069));
#386354=CARTESIAN_POINT('Ctrl Pts',(2.56344583519718,0.760817269006253,
7.57603338728831));
#386355=CARTESIAN_POINT('Ctrl Pts',(2.55662067806349,0.765442247231722,
7.59639677331372));
#386356=CARTESIAN_POINT('Ctrl Pts',(2.54113756247318,0.754196289838712,
7.59974925422225));
#386357=CARTESIAN_POINT('Ctrl Pts',(2.5602488397315,0.753217766653679,7.59639677331371));
#386358=CARTESIAN_POINT('Ctrl Pts',(2.55313724428124,0.76368702839399,7.58707626057424));
#386359=CARTESIAN_POINT('Ctrl Pts',(2.55101612578581,0.757128195576313,
7.58811717123966));
#386360=CARTESIAN_POINT('Ctrl Pts',(2.55637188217917,0.752788459978747,
7.58707626057422));
#386361=CARTESIAN_POINT('Ctrl Pts',(2.55888304972317,0.761709314540876,
7.58015376756929));
#386362=CARTESIAN_POINT('Ctrl Pts',(2.55764184525409,0.759094674335489,
7.5820876076604));
#386363=CARTESIAN_POINT('Ctrl Pts',(2.56010846144153,0.757580495838136,
7.5801537675693));
#386364=CARTESIAN_POINT('Ctrl Pts',(2.56344583380473,0.760817267671516,
7.57603338509286));
#386365=CARTESIAN_POINT('Ctrl Pts',(2.56344583380473,0.760817267671516,
7.57603338509286));
#386366=CARTESIAN_POINT('Ctrl Pts',(2.56344583380473,0.760817267671516,
7.57603338509286));
#386367=CARTESIAN_POINT('Origin',(2.57191671161825,0.763334355930457,7.58486873427622));
#386368=CARTESIAN_POINT('Ctrl Pts',(2.65126187924781,0.733647821794611,
7.51098857897448));
#386369=CARTESIAN_POINT('Ctrl Pts',(2.64550378996543,0.734874573516824,
7.50433767179956));
#386370=CARTESIAN_POINT('Ctrl Pts',(2.64535737577417,0.743481931646183,
7.50214974420965));
#386371=CARTESIAN_POINT('Ctrl Pts',(2.62045204982553,0.740211806729772,
7.5388732158917));
#386372=CARTESIAN_POINT('Ctrl Pts',(2.61476295267152,0.741423859789251,
7.53220407452065));
#386373=CARTESIAN_POINT('Ctrl Pts',(2.61456026023065,0.750000679461852,
7.53003438070912));
#386374=CARTESIAN_POINT('Ctrl Pts',(2.58958305416543,0.746788396937374,
7.56669465659231));
#386375=CARTESIAN_POINT('Ctrl Pts',(2.58392757851788,0.747993286988592,
7.56004085833299));
#386376=CARTESIAN_POINT('Ctrl Pts',(2.58370474861185,0.75653067516997,7.55785582193789));
#386377=CARTESIAN_POINT('Ctrl Pts',(2.55865628834872,0.753377294984544,
7.59443891967696));
#386378=CARTESIAN_POINT('Ctrl Pts',(2.55299261296562,0.754583931976354,
7.58783901202978));
#386379=CARTESIAN_POINT('Ctrl Pts',(2.5527923475989,0.763071515364528,7.58560008491213));
#386380=CARTESIAN_POINT('',(2.64368796492175,0.743835290548502,7.50366116523517));
#386381=CARTESIAN_POINT('Ctrl Pts',(2.64368796492211,0.743835290548603,
7.50366116523554));
#386382=CARTESIAN_POINT('Ctrl Pts',(2.64403606905883,0.743162266754996,
7.50350835821027));
#386383=CARTESIAN_POINT('Ctrl Pts',(2.64433416512128,0.742532269335402,
7.50345484956));
#386384=CARTESIAN_POINT('Ctrl Pts',(2.64459165855155,0.741926824793144,
7.50349758195598));
#386385=CARTESIAN_POINT('Ctrl Pts',(2.64472377177749,0.741616186842028,
7.50351950684424));
#386386=CARTESIAN_POINT('Ctrl Pts',(2.6448583372899,0.741281445250328,7.50357029184312));
#386387=CARTESIAN_POINT('Ctrl Pts',(2.6449792244816,0.74095509093709,7.50365515313923));
#386388=CARTESIAN_POINT('Ctrl Pts',(2.64516519793449,0.740453025849417,
7.50378570417639));
#386389=CARTESIAN_POINT('Ctrl Pts',(2.64532458362198,0.739956193803965,
7.50400001621911));
#386390=CARTESIAN_POINT('Ctrl Pts',(2.64544308808559,0.739501717390469,
7.50428903009634));
#386391=CARTESIAN_POINT('Ctrl Pts',(2.64545624116933,0.739451274005102,
7.50432110841318));
#386392=CARTESIAN_POINT('Ctrl Pts',(2.64546891357409,0.739401332602668,
7.50435406373354));
#386393=CARTESIAN_POINT('Ctrl Pts',(2.64548110249555,0.739351929091606,
7.50438785222352));
#386394=CARTESIAN_POINT('Ctrl Pts',(2.64555552171984,0.739050296910222,
7.50459414719561));
#386395=CARTESIAN_POINT('Ctrl Pts',(2.64561260228404,0.738763789814967,
7.50483629897752));
#386396=CARTESIAN_POINT('Ctrl Pts',(2.64565144811457,0.738503640946567,
7.5050991045531));
#386397=CARTESIAN_POINT('Ctrl Pts',(2.6457371459184,0.737929726413397,7.50567888004914));
#386398=CARTESIAN_POINT('Ctrl Pts',(2.64573798903582,0.737461555509749,
7.50637912803144));
#386399=CARTESIAN_POINT('Ctrl Pts',(2.645683829865,0.737091112458748,7.50710440483569));
#386400=CARTESIAN_POINT('Ctrl Pts',(2.6456705489611,0.737000272468318,7.50728225710685));
#386401=CARTESIAN_POINT('Ctrl Pts',(2.64565384064822,0.736913479663692,
7.50746498566954));
#386402=CARTESIAN_POINT('Ctrl Pts',(2.64563450403443,0.73683268131825,7.50764697238949));
#386403=CARTESIAN_POINT('Ctrl Pts',(2.64553055572032,0.736398331649459,
7.50862528291182));
#386404=CARTESIAN_POINT('Ctrl Pts',(2.64534524283224,0.736096819786135,
7.50965856837421));
#386405=CARTESIAN_POINT('Ctrl Pts',(2.64512364214822,0.735879530093703,
7.51067959873202));
#386406=CARTESIAN_POINT('Ctrl Pts',(2.64500169501229,0.735759955301882,
7.51124147302578));
#386407=CARTESIAN_POINT('Ctrl Pts',(2.64486842488808,0.735666166627857,
7.51180065547253));
#386408=CARTESIAN_POINT('Ctrl Pts',(2.64472951425972,0.735592069739074,
7.512351757165));
#386409=CARTESIAN_POINT('Ctrl Pts',(2.64424952270334,0.735336035471634,
7.51425603304536));
#386410=CARTESIAN_POINT('Ctrl Pts',(2.64364210055535,0.735289940333101,
7.5162690050518));
#386411=CARTESIAN_POINT('Ctrl Pts',(2.64295636119802,0.735418705226031,
7.51827788969244));
#386412=CARTESIAN_POINT('Ctrl Pts',(2.64291924768814,0.735425674225368,
7.51838661432545));
#386413=CARTESIAN_POINT('Ctrl Pts',(2.64288189864373,0.735433163274049,
7.51849533314857));
#386414=CARTESIAN_POINT('Ctrl Pts',(2.64284431997726,0.735441169348903,
7.51860402984325));
#386415=CARTESIAN_POINT('Ctrl Pts',(2.56344583570119,0.760817267312242,
7.57603338728985));
#386416=CARTESIAN_POINT('Ctrl Pts',(2.59023829728888,0.755147939734382,
7.55196141284922));
#386417=CARTESIAN_POINT('Ctrl Pts',(2.61698440749374,0.749487530346329,
7.52783573083105));
#386418=CARTESIAN_POINT('Ctrl Pts',(2.64368796497828,0.743835290530981,
7.50366116530176));
#386419=CARTESIAN_POINT('Origin',(8.85789032694959E-16,2.62897535302361E-16,
7.49482233047033));
#386420=CARTESIAN_POINT('Origin',(2.61299471585144,0.816189233531341,7.49482233047033));
#386421=CARTESIAN_POINT('Origin',(0.,0.,7.50366116523517));
#386422=CARTESIAN_POINT('Origin',(2.63517950238394,0.741441326212352,7.49482233047033));
#386423=CARTESIAN_POINT('Ctrl Pts',(2.61614446651996,0.825398570094828,
7.51860402984325));
#386424=CARTESIAN_POINT('Ctrl Pts',(2.62151698305455,0.830786737883201,
7.51860402984325));
#386425=CARTESIAN_POINT('Ctrl Pts',(2.61919823167326,0.838033784044352,
7.51860402984325));
#386426=CARTESIAN_POINT('Ctrl Pts',(2.61813931767337,0.827399234462656,
7.51041458714366));
#386427=CARTESIAN_POINT('Ctrl Pts',(2.62096763486515,0.832503643108405,
7.51004642900443));
#386428=CARTESIAN_POINT('Ctrl Pts',(2.61919759218916,0.838035782693636,
7.5072913648301));
#386429=CARTESIAN_POINT('Ctrl Pts',(2.62069593195854,0.826221329289853,
7.50215815450137));
#386430=CARTESIAN_POINT('Ctrl Pts',(2.62208629631496,0.829007895534876,
7.49877163671529));
#386431=CARTESIAN_POINT('Ctrl Pts',(2.62105762822771,0.832301186527272,
7.4948158853317));
#386432=CARTESIAN_POINT('Ctrl Pts',(2.62143102271335,0.818824379629568,
7.50366171572174));
#386433=CARTESIAN_POINT('Ctrl Pts',(2.62492619857234,0.819916125008284,
7.50000045605858));
#386434=CARTESIAN_POINT('Ctrl Pts',(2.6249261985723,0.819916125008403,7.49482233047317));
#386435=CARTESIAN_POINT('Origin',(2.60729278516565,0.834224539571422,7.51860402984325));
#386436=CARTESIAN_POINT('Origin',(2.60729278516565,0.834224539571422,9.));
#386437=CARTESIAN_POINT('Origin',(2.60729278516565,0.834224539571422,8.75721825406948));
#386438=CARTESIAN_POINT('Ctrl Pts',(2.60435458367724,0.813572382352496,
8.78942910404913));
#386439=CARTESIAN_POINT('Ctrl Pts',(2.60830313188505,0.817504480488642,
8.79672699501691));
#386440=CARTESIAN_POINT('Ctrl Pts',(2.60327327413769,0.824878354438172,
8.79893251111266));
#386441=CARTESIAN_POINT('Ctrl Pts',(2.61211678181375,0.821358504547112,
8.78111911759577));
#386442=CARTESIAN_POINT('Ctrl Pts',(2.61679257887839,0.826025327013849,
8.78644465894811));
#386443=CARTESIAN_POINT('Ctrl Pts',(2.61376706025929,0.83354608155451,8.78817647674132));
#386444=CARTESIAN_POINT('Ctrl Pts',(2.61695436881582,0.826211001637836,
8.76780923932034));
#386445=CARTESIAN_POINT('Ctrl Pts',(2.62247035001552,0.831723595235669,
8.76988516158376));
#386446=CARTESIAN_POINT('Ctrl Pts',(2.62031418371861,0.838968409056361,
8.77093053738832));
#386447=CARTESIAN_POINT('Ctrl Pts',(2.61601110555621,0.82526483111746,8.75371302330491));
#386448=CARTESIAN_POINT('Ctrl Pts',(2.62139224614752,0.830641589183852,
8.75300828287559));
#386449=CARTESIAN_POINT('Ctrl Pts',(2.61903693688884,0.837911187359152,
8.75267964240738));
#386450=CARTESIAN_POINT('Origin',(2.59739259559947,0.824293828210157,8.78727029226991));
#386451=CARTESIAN_POINT('Ctrl Pts',(2.5557700913641,0.764838063661159,8.85049129520029));
#386452=CARTESIAN_POINT('Ctrl Pts',(2.55989296307186,0.768973645978611,
8.85711686593484));
#386453=CARTESIAN_POINT('Ctrl Pts',(2.55537491841651,0.776232298374626,
8.85933012996512));
#386454=CARTESIAN_POINT('Ctrl Pts',(2.57261954817433,0.781739466513905,
8.82945683644723));
#386455=CARTESIAN_POINT('Ctrl Pts',(2.57677664221,0.785909376665029,8.8360746990239));
#386456=CARTESIAN_POINT('Ctrl Pts',(2.57221349406443,0.793169522772296,
8.83829567148519));
#386457=CARTESIAN_POINT('Ctrl Pts',(2.58944388951045,0.798615676462769,
8.80838214965002));
#386458=CARTESIAN_POINT('Ctrl Pts',(2.59361738938009,0.802802043026221,
8.81501364461988));
#386459=CARTESIAN_POINT('Ctrl Pts',(2.58902700057119,0.810080582933261,
8.81722098428722));
#386460=CARTESIAN_POINT('Ctrl Pts',(2.60624502375464,0.815468607773385,
8.78727029226991));
#386461=CARTESIAN_POINT('Ctrl Pts',(2.61041921685633,0.819655669706082,
8.79393457792714));
#386462=CARTESIAN_POINT('Ctrl Pts',(2.60581736094343,0.82696746410521,8.79610912703474));
#386463=CARTESIAN_POINT('Origin',(2.54691766320893,0.773663284097931,8.85049129520029));
#386464=CARTESIAN_POINT('Ctrl Pts',(2.55920636991202,0.753260100986319,
8.85049129520029));
#386465=CARTESIAN_POINT('Ctrl Pts',(2.56491780413929,0.752043289049059,
8.85711686593484));
#386466=CARTESIAN_POINT('Ctrl Pts',(2.56509113287406,0.743495147773693,
8.85933012996512));
#386467=CARTESIAN_POINT('Ctrl Pts',(2.55415354649658,0.754336596942347,
8.86332496987232));
#386468=CARTESIAN_POINT('Ctrl Pts',(2.55573644967854,0.749995363028666,
8.86648636486736));
#386469=CARTESIAN_POINT('Ctrl Pts',(2.55095922330301,0.746523445683803,
8.87206031107457));
#386470=CARTESIAN_POINT('Ctrl Pts',(2.55209786073928,0.761154511730837,
8.86341338519876));
#386471=CARTESIAN_POINT('Ctrl Pts',(2.55102439395549,0.765662409211744,
8.86654584966058));
#386472=CARTESIAN_POINT('Ctrl Pts',(2.54510291120593,0.765907755566788,
8.87215952290714));
#386473=CARTESIAN_POINT('Ctrl Pts',(2.5557700913641,0.764838063661158,8.85049129520029));
#386474=CARTESIAN_POINT('Ctrl Pts',(2.55989296307186,0.768973645978611,
8.85711686593484));
#386475=CARTESIAN_POINT('Ctrl Pts',(2.55537491841651,0.776232298374626,
8.85933012996512));
#386476=CARTESIAN_POINT('Origin',(2.55660172093491,0.741034480196109,8.85049129520029));
#386477=CARTESIAN_POINT('Ctrl Pts',(2.62912953922426,0.738363081476945,
8.78727029226991));
#386478=CARTESIAN_POINT('Ctrl Pts',(2.63491206922812,0.737131122698069,
8.79393457792714));
#386479=CARTESIAN_POINT('Ctrl Pts',(2.63504414756229,0.728492721775916,
8.79610912703474));
#386480=CARTESIAN_POINT('Ctrl Pts',(2.60585484624786,0.743321717630804,
8.80838214965002));
#386481=CARTESIAN_POINT('Ctrl Pts',(2.61163641591401,0.74208996345033,8.8150136446199));
#386482=CARTESIAN_POINT('Ctrl Pts',(2.61175996320558,0.733485688427888,
8.81722098428721));
#386483=CARTESIAN_POINT('Ctrl Pts',(2.58254800437416,0.748287203055872,
8.82945683644723));
#386484=CARTESIAN_POINT('Ctrl Pts',(2.58830684695872,0.747060290843834,
8.83607469902389));
#386485=CARTESIAN_POINT('Ctrl Pts',(2.58844318986646,0.738486292178741,
8.83829567148519));
#386486=CARTESIAN_POINT('Ctrl Pts',(2.55920636991202,0.753260100986318,
8.85049129520029));
#386487=CARTESIAN_POINT('Ctrl Pts',(2.56491780413929,0.752043289049059,
8.85711686593484));
#386488=CARTESIAN_POINT('Ctrl Pts',(2.56509113287406,0.743495147773693,
8.85933012996512));
#386489=CARTESIAN_POINT('Origin',(2.62652489024714,0.726137460686736,8.78727029226991));
#386490=CARTESIAN_POINT('Ctrl Pts',(2.64266321935266,0.735479733686564,
8.75374538247849));
#386491=CARTESIAN_POINT('Ctrl Pts',(2.65009811484497,0.733909158185006,
8.75304829418602));
#386492=CARTESIAN_POINT('Ctrl Pts',(2.65209331987869,0.726540996943395,
8.75272238421917));
#386493=CARTESIAN_POINT('Ctrl Pts',(2.64395422903473,0.73520468657252,8.76769408445017));
#386494=CARTESIAN_POINT('Ctrl Pts',(2.65157607685313,0.733593913216396,
8.76974318093968));
#386495=CARTESIAN_POINT('Ctrl Pts',(2.65372225373277,0.726354280485274,
8.7707786988043));
#386496=CARTESIAN_POINT('Ctrl Pts',(2.63733724884731,0.736614421409556,
8.78108014887994));
#386497=CARTESIAN_POINT('Ctrl Pts',(2.64379727590478,0.735253066306277,
8.78639403366326));
#386498=CARTESIAN_POINT('Ctrl Pts',(2.64538156698146,0.727315050337962,
8.78812224174741));
#386499=CARTESIAN_POINT('Ctrl Pts',(2.62649347902617,0.738924665570915,
8.78944554828685));
#386500=CARTESIAN_POINT('Ctrl Pts',(2.63193890460373,0.737782843388512,
8.79673892988685));
#386501=CARTESIAN_POINT('Ctrl Pts',(2.63174894852014,0.728868390460666,
8.79894799272499));
#386502=CARTESIAN_POINT('Origin',(2.64023967100014,0.723215548558698,8.75721825406948));
#386503=CARTESIAN_POINT('Origin',(2.64023967100014,0.723215548558698,9.));
#386504=CARTESIAN_POINT('Origin',(2.64023967100014,0.723215548558698,7.51860402984325));
#386505=CARTESIAN_POINT('Ctrl Pts',(2.64368720766141,0.7438350774836,7.50366195182966));
#386506=CARTESIAN_POINT('Ctrl Pts',(2.64721228549989,0.744826903044238,
7.50000065167735));
#386507=CARTESIAN_POINT('Ctrl Pts',(2.64721228549992,0.744826903044126,
7.49482233047108));
#386508=CARTESIAN_POINT('Ctrl Pts',(2.64710868794002,0.737228469253212,
7.50215800491336));
#386509=CARTESIAN_POINT('Ctrl Pts',(2.64979433702035,0.735649866645935,
7.49877273257264));
#386510=CARTESIAN_POINT('Ctrl Pts',(2.65072935414104,0.732326780830922,
7.49481816995649));
#386511=CARTESIAN_POINT('Ctrl Pts',(2.64560110706609,0.7348541869931,7.51043025814043));
#386512=CARTESIAN_POINT('Ctrl Pts',(2.65076076619579,0.732120933500987,
7.51006209594517));
#386513=CARTESIAN_POINT('Ctrl Pts',(2.65229622879822,0.726515460750279,
7.507312818217));
#386514=CARTESIAN_POINT('Ctrl Pts',(2.64284284172668,0.735441484194402,
7.51860402984326));
#386515=CARTESIAN_POINT('Ctrl Pts',(2.65028527911173,0.733856825505522,
7.51860402984326));
#386516=CARTESIAN_POINT('Ctrl Pts',(2.65229555990882,0.7265179026617,7.51860402984327));
#386517=CARTESIAN_POINT('Origin',(0.,0.,7.5));
#386518=CARTESIAN_POINT('Origin',(2.6022097463239,0.587743532225645,7.5));
#386519=CARTESIAN_POINT('',(2.6022097463239,0.587743532225645,7.59394543036555));
#386520=CARTESIAN_POINT('',(2.6022097463239,0.587743532225645,8.85049129520029));
#386521=CARTESIAN_POINT('',(2.6022097463239,0.587743532225645,7.5));
#386522=CARTESIAN_POINT('',(2.67103479566853,0.568397127400971,8.78727029226991));
#386523=CARTESIAN_POINT('Ctrl Pts',(2.6022097463239,0.587743532225645,8.85049129520029));
#386524=CARTESIAN_POINT('Ctrl Pts',(2.62518477739697,0.58128535665975,8.82945686509571));
#386525=CARTESIAN_POINT('Ctrl Pts',(2.64812565330824,0.574836781952744,
8.80838212259896));
#386526=CARTESIAN_POINT('Ctrl Pts',(2.67103479566853,0.568397127400971,
8.78727029226991));
#386527=CARTESIAN_POINT('',(2.68453419038076,0.564602509634941,8.75721825406948));
#386528=CARTESIAN_POINT('Origin',(2.64390988332938,0.576022025127795,8.75937679713151));
#386529=CARTESIAN_POINT('',(2.68453419038076,0.564602509634941,7.51860402984325));
#386530=CARTESIAN_POINT('',(2.68453419038076,0.564602509634941,7.5));
#386531=CARTESIAN_POINT('Ctrl Pts',(2.68453419038076,0.564602509634941,
7.51860402984325));
#386532=CARTESIAN_POINT('Ctrl Pts',(2.67393251538731,0.567582591715464,
7.52834476460825));
#386533=CARTESIAN_POINT('Ctrl Pts',(2.66332395793944,0.570564608422277,
7.53807742314407));
#386534=CARTESIAN_POINT('Ctrl Pts',(2.65270828694957,0.573548624713022,
7.54780169004674));
#386535=CARTESIAN_POINT('Ctrl Pts',(2.63589363782969,0.578275145245242,
7.5632044032688));
#386536=CARTESIAN_POINT('Ctrl Pts',(2.61906112037001,0.583006688485576,
7.57858609112103));
#386537=CARTESIAN_POINT('Ctrl Pts',(2.6022097463239,0.587743532225645,7.59394543036555));
#386538=CARTESIAN_POINT('Origin',(2.80575616266556,0.781431603558372,7.5));
#386539=CARTESIAN_POINT('',(2.66365357834824,0.656086448390735,8.75721825406948));
#386540=CARTESIAN_POINT('',(2.65313746692184,0.646810448064383,8.78727029226991));
#386541=CARTESIAN_POINT('Origin',(2.62644365380812,0.623264499460921,8.75658640621069));
#386542=CARTESIAN_POINT('',(2.5995223305943,0.599517869856918,8.85049129520029));
#386543=CARTESIAN_POINT('Ctrl Pts',(2.65313746692184,0.646810448064383,
8.78727029226991));
#386544=CARTESIAN_POINT('Ctrl Pts',(2.63529110426043,0.631068615445932,
8.80838212259896));
#386545=CARTESIAN_POINT('Ctrl Pts',(2.61742002096781,0.61530497737356,8.82945686509571));
#386546=CARTESIAN_POINT('Ctrl Pts',(2.5995223305943,0.599517869856918,8.85049129520029));
#386547=CARTESIAN_POINT('',(2.5995223305943,0.599517869856918,7.59394543036555));
#386548=CARTESIAN_POINT('',(2.5995223305943,0.599517869856918,7.5));
#386549=CARTESIAN_POINT('',(2.66365357834824,0.656086448390735,7.51860402984325));
#386550=CARTESIAN_POINT('Ctrl Pts',(2.5995223305943,0.599517869856917,7.59394543036555));
#386551=CARTESIAN_POINT('Ctrl Pts',(2.61264965451766,0.61109715577923,7.57858609112103));
#386552=CARTESIAN_POINT('Ctrl Pts',(2.62576228904419,0.622663484549934,
7.56320440326857));
#386553=CARTESIAN_POINT('Ctrl Pts',(2.63886100402437,0.63421753523505,7.54780169004651));
#386554=CARTESIAN_POINT('Ctrl Pts',(2.64713067695232,0.641512008036651,
7.53807742314383));
#386555=CARTESIAN_POINT('Ctrl Pts',(2.65539480838749,0.648801592825318,
7.52834476460825));
#386556=CARTESIAN_POINT('Ctrl Pts',(2.66365357834824,0.656086448390733,
7.51860402984325));
#386557=CARTESIAN_POINT('',(2.66365357834824,0.656086448390735,7.5));
#386558=CARTESIAN_POINT('Origin',(2.60407017393683,0.594362024055136,7.5));
#386559=CARTESIAN_POINT('Ctrl Pts',(2.5995223305943,0.599517869856918,8.85049129520029));
#386560=CARTESIAN_POINT('Ctrl Pts',(2.5993770958507,0.599389761901953,8.85097269580138));
#386561=CARTESIAN_POINT('Ctrl Pts',(2.59923925769927,0.5992569622011,8.85143669361005));
#386562=CARTESIAN_POINT('Ctrl Pts',(2.59910307573752,0.599112726143938,
8.8519052845931));
#386563=CARTESIAN_POINT('Ctrl Pts',(2.59883671245668,0.598830609563248,
8.85282181883899));
#386564=CARTESIAN_POINT('Ctrl Pts',(2.59858368043392,0.598511863228102,
8.85372622499636));
#386565=CARTESIAN_POINT('Ctrl Pts',(2.59835208540563,0.598141898916068,
8.85462257735071));
#386566=CARTESIAN_POINT('Ctrl Pts',(2.59815982343862,0.597834767684107,
8.85536669723986));
#386567=CARTESIAN_POINT('Ctrl Pts',(2.5979822646424,0.597492285139559,8.85610498449051));
#386568=CARTESIAN_POINT('Ctrl Pts',(2.59783113602521,0.597102392478176,
8.85681338218371));
#386569=CARTESIAN_POINT('Ctrl Pts',(2.59769398656776,0.596748564275631,
8.85745625420285));
#386570=CARTESIAN_POINT('Ctrl Pts',(2.5975763254901,0.59635146893287,8.85808743050666));
#386571=CARTESIAN_POINT('Ctrl Pts',(2.59749937853404,0.595891941011388,
8.85866804508411));
#386572=CARTESIAN_POINT('Ctrl Pts',(2.59746387687652,0.595679924789762,
8.85893592806396));
#386573=CARTESIAN_POINT('Ctrl Pts',(2.59743724001533,0.595454478746938,
8.85919241173848));
#386574=CARTESIAN_POINT('Ctrl Pts',(2.5974229722392,0.595212990999105,8.85943017985534));
#386575=CARTESIAN_POINT('Ctrl Pts',(2.59740370651771,0.594886911051505,
8.8597512372));
#386576=CARTESIAN_POINT('Ctrl Pts',(2.5974071424151,0.594523244909351,8.86004599534706));
#386577=CARTESIAN_POINT('Ctrl Pts',(2.59744365327854,0.594126460281423,
8.86026130871721));
#386578=CARTESIAN_POINT('Ctrl Pts',(2.597457020935,0.593981186242596,8.86034014101236));
#386579=CARTESIAN_POINT('Ctrl Pts',(2.59747501080946,0.593829289371773,
8.86040910639692));
#386580=CARTESIAN_POINT('Ctrl Pts',(2.59749746682199,0.593674947576375,
8.86046313645506));
#386581=CARTESIAN_POINT('Ctrl Pts',(2.59753250924147,0.593434098497258,
8.86054744990829));
#386582=CARTESIAN_POINT('Ctrl Pts',(2.59757952936704,0.593180742414891,
8.86059655985668));
#386583=CARTESIAN_POINT('Ctrl Pts',(2.59763522361598,0.592931074369274,
8.86059725258816));
#386584=CARTESIAN_POINT('Ctrl Pts',(2.59769104654089,0.592680829490728,
8.86059794692011));
#386585=CARTESIAN_POINT('Ctrl Pts',(2.5977587958359,0.592432092904116,8.86056369958366));
#386586=CARTESIAN_POINT('Ctrl Pts',(2.59783114559448,0.592197441881941,
8.86048590497774));
#386587=CARTESIAN_POINT('Ctrl Pts',(2.59785002672736,0.592136204951556,
8.86046560290182));
#386588=CARTESIAN_POINT('Ctrl Pts',(2.59786955336763,0.592075157355808,
8.86044257503091));
#386589=CARTESIAN_POINT('Ctrl Pts',(2.59788909086021,0.592016175515313,
8.86041778462584));
#386590=CARTESIAN_POINT('Ctrl Pts',(2.59802055394132,0.591619300919147,
8.86025097596201));
#386591=CARTESIAN_POINT('Ctrl Pts',(2.5981704640267,0.591262804918446,8.8599848982295));
#386592=CARTESIAN_POINT('Ctrl Pts',(2.59832663557419,0.590953808487266,
8.85968173251461));
#386593=CARTESIAN_POINT('Ctrl Pts',(2.59840924137526,0.590790367078556,
8.85952137522076));
#386594=CARTESIAN_POINT('Ctrl Pts',(2.59849502086838,0.590636978528661,
8.85934740853961));
#386595=CARTESIAN_POINT('Ctrl Pts',(2.59858140757177,0.590495047191074,
8.8591675900182));
#386596=CARTESIAN_POINT('Ctrl Pts',(2.59892829508878,0.589925119096225,
8.85844552518696));
#386597=CARTESIAN_POINT('Ctrl Pts',(2.59930199401607,0.589506147419881,
8.85759444184125));
#386598=CARTESIAN_POINT('Ctrl Pts',(2.59963737144715,0.589191908284455,
8.8568349891514));
#386599=CARTESIAN_POINT('Ctrl Pts',(2.59967246780213,0.589159023995817,
8.85675551444999));
#386600=CARTESIAN_POINT('Ctrl Pts',(2.59970715503213,0.589127303602798,
8.85667699793652));
#386601=CARTESIAN_POINT('Ctrl Pts',(2.59974136484002,0.58909670563257,8.85659965593547));
#386602=CARTESIAN_POINT('Ctrl Pts',(2.60020313057239,0.588683692669124,
8.85555568965886));
#386603=CARTESIAN_POINT('Ctrl Pts',(2.60070656329426,0.588353449731756,
8.85434650606346));
#386604=CARTESIAN_POINT('Ctrl Pts',(2.60125074290954,0.588099147829294,
8.85297329937117));
#386605=CARTESIAN_POINT('Ctrl Pts',(2.60155681078578,0.587956118504001,
8.85220095427747));
#386606=CARTESIAN_POINT('Ctrl Pts',(2.60187602688497,0.587837339225057,
8.85137579139183));
#386607=CARTESIAN_POINT('Ctrl Pts',(2.6022097463239,0.587743532225645,8.85049129520029));
#386608=CARTESIAN_POINT('Origin',(2.60407017393683,0.594362024055136,7.59394543036555));
#386609=CARTESIAN_POINT('Ctrl Pts',(2.59910066513915,0.599145929246844,
7.59443877723642));
#386610=CARTESIAN_POINT('Ctrl Pts',(2.59475791666676,0.595315298834728,
7.58783886950016));
#386611=CARTESIAN_POINT('Ctrl Pts',(2.59874842803423,0.587821634806851,
7.58559994247159));
#386612=CARTESIAN_POINT('Ctrl Pts',(2.62280760163913,0.620057228280669,
7.56670252222137));
#386613=CARTESIAN_POINT('Ctrl Pts',(2.61847112967123,0.616232134217035,
7.5600487499903));
#386614=CARTESIAN_POINT('Ctrl Pts',(2.6224664278495,0.608684025200656,7.55786368756704));
#386615=CARTESIAN_POINT('Ctrl Pts',(2.64647026780379,0.640929477552829,
7.53888913333558));
#386616=CARTESIAN_POINT('Ctrl Pts',(2.64210802397063,0.637081650767913,
7.53222002137278));
#386617=CARTESIAN_POINT('Ctrl Pts',(2.64614020663337,0.629509072099142,
7.53005029815326));
#386618=CARTESIAN_POINT('Ctrl Pts',(2.6700875928815,0.66176173257994,7.51101258149734));
#386619=CARTESIAN_POINT('Ctrl Pts',(2.6656724707267,0.657867263142695,7.5043616886572));
#386620=CARTESIAN_POINT('Ctrl Pts',(2.66976864930636,0.650295684536609,
7.50217374673251));
#386621=CARTESIAN_POINT('',(2.6685078045743,0.649186484966767,7.50366116523517));
#386622=CARTESIAN_POINT('Ctrl Pts',(2.66365357834824,0.656086448390735,
7.51860402984325));
#386623=CARTESIAN_POINT('Ctrl Pts',(2.66398476079656,0.656378576191033,
7.51734760759493));
#386624=CARTESIAN_POINT('Ctrl Pts',(2.66432338889996,0.656597936323158,
7.51608817408572));
#386625=CARTESIAN_POINT('Ctrl Pts',(2.66467594396582,0.656732816671575,
7.51481005913119));
#386626=CARTESIAN_POINT('Ctrl Pts',(2.66499529676906,0.656854994514241,
7.51365231206383));
#386627=CARTESIAN_POINT('Ctrl Pts',(2.66532643764435,0.656908261136698,
7.51247773061042));
#386628=CARTESIAN_POINT('Ctrl Pts',(2.66566950096493,0.656855238444899,
7.51129758471022));
#386629=CARTESIAN_POINT('Ctrl Pts',(2.6660958894931,0.656789337294412,7.50983079813402));
#386630=CARTESIAN_POINT('Ctrl Pts',(2.66652509793794,0.656548475546837,
7.50839324291155));
#386631=CARTESIAN_POINT('Ctrl Pts',(2.66691991417319,0.656059002349293,
7.50715379678855));
#386632=CARTESIAN_POINT('Ctrl Pts',(2.66710230789751,0.65583287983586,7.50658120839351));
#386633=CARTESIAN_POINT('Ctrl Pts',(2.66729589496988,0.655515588495312,
7.50598221009429));
#386634=CARTESIAN_POINT('Ctrl Pts',(2.66747665060042,0.655102832213265,
7.50545747549611));
#386635=CARTESIAN_POINT('Ctrl Pts',(2.66757310739979,0.654882572685162,
7.50517746087247));
#386636=CARTESIAN_POINT('Ctrl Pts',(2.66766714172128,0.654632821201721,
7.50491486231392));
#386637=CARTESIAN_POINT('Ctrl Pts',(2.66775470234246,0.65435960385524,7.50468370960993));
#386638=CARTESIAN_POINT('Ctrl Pts',(2.66788563309054,0.653951057740731,
7.50433806340447));
#386639=CARTESIAN_POINT('Ctrl Pts',(2.66800548484691,0.653477622060633,
7.50405484070985));
#386640=CARTESIAN_POINT('Ctrl Pts',(2.66810549133164,0.65297100601611,7.50385766036132));
#386641=CARTESIAN_POINT('Ctrl Pts',(2.66811618547073,0.652916831304736,
7.50383657498792));
#386642=CARTESIAN_POINT('Ctrl Pts',(2.66812666210036,0.652862303928491,
7.50381643264937));
#386643=CARTESIAN_POINT('Ctrl Pts',(2.66813691764825,0.652807481989508,
7.50379723213559));
#386644=CARTESIAN_POINT('Ctrl Pts',(2.66820537678523,0.652441527613342,
7.50366906242519));
#386645=CARTESIAN_POINT('Ctrl Pts',(2.6682647668768,0.652054354948041,7.50358235568538));
#386646=CARTESIAN_POINT('Ctrl Pts',(2.6683130409734,0.651679792103603,7.5035341175365));
#386647=CARTESIAN_POINT('Ctrl Pts',(2.66838542251767,0.651118177510698,
7.50346178989176));
#386648=CARTESIAN_POINT('Ctrl Pts',(2.66843940938489,0.650510930430136,
7.50346967198527));
#386649=CARTESIAN_POINT('Ctrl Pts',(2.66847406487117,0.649913171174646,
7.50354272648692));
#386650=CARTESIAN_POINT('Ctrl Pts',(2.66848831939,0.649667300419978,7.50357277531559));
#386651=CARTESIAN_POINT('Ctrl Pts',(2.66849942595432,0.649423369748924,
7.50361331098761));
#386652=CARTESIAN_POINT('Ctrl Pts',(2.66850780457568,0.649186484967102,
7.50366116523659));
#386653=CARTESIAN_POINT('',(2.60692468992218,0.595013548701134,7.57603338622103));
#386654=CARTESIAN_POINT('Origin',(2.61554070278251,0.596977170861226,7.58486873427627));
#386655=CARTESIAN_POINT('Ctrl Pts',(2.66850780461363,0.649186485008502,
7.50366116529969));
#386656=CARTESIAN_POINT('Ctrl Pts',(2.64801414877486,0.631157678360177,
7.52783573079709));
#386657=CARTESIAN_POINT('Ctrl Pts',(2.62748742494611,0.613100872076781,
7.55196141284068));
#386658=CARTESIAN_POINT('Ctrl Pts',(2.60692469059042,0.595013549759952,
7.57603338728831));
#386659=CARTESIAN_POINT('Ctrl Pts',(2.60040987984641,0.60006631479062,7.59639677331371));
#386660=CARTESIAN_POINT('Ctrl Pts',(2.58423804501348,0.589835470045181,
7.59974925422225));
#386661=CARTESIAN_POINT('Ctrl Pts',(2.60324736190728,0.58763449360278,7.59639677331372));
#386662=CARTESIAN_POINT('Ctrl Pts',(2.59682114589539,0.598537886606984,
7.58707626057423));
#386663=CARTESIAN_POINT('Ctrl Pts',(2.59428415960392,0.592128430143389,
7.58811717123965));
#386664=CARTESIAN_POINT('Ctrl Pts',(2.59935086420695,0.587454466507722,
7.58707626057423));
#386665=CARTESIAN_POINT('Ctrl Pts',(2.60242843340217,0.596196101160384,
7.5801537675693));
#386666=CARTESIAN_POINT('Ctrl Pts',(2.60102225854765,0.593666357257041,
7.58208760766041));
#386667=CARTESIAN_POINT('Ctrl Pts',(2.60338679305817,0.591997253160117,
7.5801537675693));
#386668=CARTESIAN_POINT('Ctrl Pts',(2.60692468911531,0.595013548517179,
7.57603338509286));
#386669=CARTESIAN_POINT('Ctrl Pts',(2.60692468911531,0.595013548517179,
7.57603338509286));
#386670=CARTESIAN_POINT('Ctrl Pts',(2.60692468911531,0.595013548517179,
7.57603338509286));
#386671=CARTESIAN_POINT('Origin',(2.61553943299981,0.59698273414312,7.58486873427623));
#386672=CARTESIAN_POINT('Ctrl Pts',(2.69281955470071,0.562273531831367,
7.51098857897448));
#386673=CARTESIAN_POINT('Ctrl Pts',(2.68715189428301,0.563866685107589,
7.50433767179956));
#386674=CARTESIAN_POINT('Ctrl Pts',(2.68755725624421,0.572465739285978,
7.50214974420965));
#386675=CARTESIAN_POINT('Ctrl Pts',(2.66249358333604,0.570798022904151,
7.53887321589168));
#386676=CARTESIAN_POINT('Ctrl Pts',(2.65689383154843,0.572372087376793,
7.53220407452062));
#386677=CARTESIAN_POINT('Ctrl Pts',(2.6572410742841,0.580944271602793,7.53003438070911));
#386678=CARTESIAN_POINT('Ctrl Pts',(2.63210937491955,0.579338884144357,
7.56669465659231));
#386679=CARTESIAN_POINT('Ctrl Pts',(2.62654271662392,0.580903646188594,
7.560040858333));
#386680=CARTESIAN_POINT('Ctrl Pts',(2.62686733688466,0.589437770151413,
7.55785582193789));
#386681=CARTESIAN_POINT('Ctrl Pts',(2.60166830360741,0.587895729283,7.59443891967696));
#386682=CARTESIAN_POINT('Ctrl Pts',(2.59609357435032,0.589462760037394,
7.58783901202978));
#386683=CARTESIAN_POINT('Ctrl Pts',(2.59643752178506,0.597945735821307,
7.58560008491213));
#386684=CARTESIAN_POINT('',(2.68591391515803,0.572925331695086,7.50366116523517));
#386685=CARTESIAN_POINT('Ctrl Pts',(2.6859139151584,0.572925331695164,7.50366116523554));
#386686=CARTESIAN_POINT('Ctrl Pts',(2.68621818329533,0.572231387592507,
7.50350835821027));
#386687=CARTESIAN_POINT('Ctrl Pts',(2.68647530281419,0.571583585489882,
7.50345484956));
#386688=CARTESIAN_POINT('Ctrl Pts',(2.68669347623158,0.570962887237649,
7.50349758195598));
#386689=CARTESIAN_POINT('Ctrl Pts',(2.68680541537486,0.570644423002071,
7.50351950684424));
#386690=CARTESIAN_POINT('Ctrl Pts',(2.68691825744058,0.57030174753089,7.50357029184312));
#386691=CARTESIAN_POINT('Ctrl Pts',(2.68701798666393,0.569968318478625,
7.50365515313924));
#386692=CARTESIAN_POINT('Ctrl Pts',(2.68717141059381,0.569455369577485,
7.50378570417639));
#386693=CARTESIAN_POINT('Ctrl Pts',(2.68729863666787,0.568949346450696,
7.50400001621911));
#386694=CARTESIAN_POINT('Ctrl Pts',(2.68738777924756,0.568488211200682,
7.50428903009634));
#386695=CARTESIAN_POINT('Ctrl Pts',(2.68739767338808,0.568437028735691,
7.50432110841318));
#386696=CARTESIAN_POINT('Ctrl Pts',(2.68740711999938,0.568386378019464,
7.50435406373354));
#386697=CARTESIAN_POINT('Ctrl Pts',(2.68741611858358,0.568336295066333,
7.50438785222352));
#386698=CARTESIAN_POINT('Ctrl Pts',(2.68747105926538,0.568030514564544,
7.50459414719561));
#386699=CARTESIAN_POINT('Ctrl Pts',(2.68750966597882,0.567740938964541,
7.50483629897752));
#386700=CARTESIAN_POINT('Ctrl Pts',(2.68753176420119,0.567478835738985,
7.5050991045531));
#386701=CARTESIAN_POINT('Ctrl Pts',(2.68758051509931,0.566900609697632,
7.50567888004914));
#386702=CARTESIAN_POINT('Ctrl Pts',(2.68755136067166,0.566433346682598,
7.50637912803144));
#386703=CARTESIAN_POINT('Ctrl Pts',(2.6874735784089,0.566067134736563,7.50710440483569));
#386704=CARTESIAN_POINT('Ctrl Pts',(2.68745450465387,0.56597733229707,7.50728225710685));
#386705=CARTESIAN_POINT('Ctrl Pts',(2.68743226983592,0.565891788322851,
7.50746498566954));
#386706=CARTESIAN_POINT('Ctrl Pts',(2.68740779618352,0.565812394887375,
7.50764697238949));
#386707=CARTESIAN_POINT('Ctrl Pts',(2.68727623256354,0.565385597627915,
7.50862528291181));
#386708=CARTESIAN_POINT('Ctrl Pts',(2.68707198248925,0.565096578290556,
7.50965856837421));
#386709=CARTESIAN_POINT('Ctrl Pts',(2.68683691530922,0.564893933047675,
7.51067959873201));
#386710=CARTESIAN_POINT('Ctrl Pts',(2.68670755754354,0.564782417114912,
7.51124147302578));
#386711=CARTESIAN_POINT('Ctrl Pts',(2.68656855217611,0.564697359785952,
7.51180065547253));
#386712=CARTESIAN_POINT('Ctrl Pts',(2.68642517955058,0.56463231517169,7.51235175716501));
#386713=CARTESIAN_POINT('Ctrl Pts',(2.68592977001648,0.564407560118717,
7.51425603304536));
#386714=CARTESIAN_POINT('Ctrl Pts',(2.68532064255678,0.564400477358233,
7.51626900505182));
#386715=CARTESIAN_POINT('Ctrl Pts',(2.68464456211952,0.564572913161355,
7.51827788969245));
#386716=CARTESIAN_POINT('Ctrl Pts',(2.68460797136864,0.564582245712878,
7.51838661432546));
#386717=CARTESIAN_POINT('Ctrl Pts',(2.68457117888685,0.564592112335995,
7.51849533314857));
#386718=CARTESIAN_POINT('Ctrl Pts',(2.68453419038076,0.564602509634937,
7.51860402984325));
#386719=CARTESIAN_POINT('Ctrl Pts',(2.60692469098486,0.59501354803714,7.57603338728985));
#386720=CARTESIAN_POINT('Ctrl Pts',(2.63329886952168,0.587639269793085,
7.55196141284922));
#386721=CARTESIAN_POINT('Ctrl Pts',(2.65962736329994,0.580276861158748,
7.52783573083105));
#386722=CARTESIAN_POINT('Ctrl Pts',(2.68591391521332,0.57292533167398,7.50366116530176));
#386723=CARTESIAN_POINT('Origin',(9.00812987045921E-16,2.05604685939141E-16,
7.49482233047033));
#386724=CARTESIAN_POINT('Origin',(2.65991946170316,0.647097138961989,7.49482233047033));
#386725=CARTESIAN_POINT('Origin',(0.,0.,7.50366116523517));
#386726=CARTESIAN_POINT('Origin',(2.6772695523474,0.571081425081912,7.49482233047033));
#386727=CARTESIAN_POINT('Ctrl Pts',(2.66365278509062,0.656085748737588,
7.51860402984325));
#386728=CARTESIAN_POINT('Ctrl Pts',(2.66935948430929,0.661118627641139,
7.51860402984325));
#386729=CARTESIAN_POINT('Ctrl Pts',(2.66750981689315,0.668499346879792,
7.51860402984325));
#386730=CARTESIAN_POINT('Ctrl Pts',(2.66577172061454,0.657954491973673,
7.51041458714367));
#386731=CARTESIAN_POINT('Ctrl Pts',(2.66892126731012,0.66286720215976,7.51004642900444));
#386732=CARTESIAN_POINT('Ctrl Pts',(2.66750930677684,0.668501382394517,
7.50729136483012));
#386733=CARTESIAN_POINT('Ctrl Pts',(2.66824761341795,0.656615204093723,
7.50215815450136));
#386734=CARTESIAN_POINT('Ctrl Pts',(2.66981365703399,0.659306964089372,
7.49877163671527));
#386735=CARTESIAN_POINT('Ctrl Pts',(2.66899810433397,0.66265939565286,7.49481588533168));
#386736=CARTESIAN_POINT('Ctrl Pts',(2.66850726965803,0.64918635483347,7.50366171572174));
#386737=CARTESIAN_POINT('Ctrl Pts',(2.67206521266993,0.650051920418061,
7.50000045605858));
#386738=CARTESIAN_POINT('Ctrl Pts',(2.6720652126699,0.650051920418182,7.49482233047317));
#386739=CARTESIAN_POINT('Origin',(2.6553847722709,0.665460713484883,7.51860402984325));
#386740=CARTESIAN_POINT('Origin',(2.6553847722709,0.665460713484883,9.));
#386741=CARTESIAN_POINT('Origin',(2.6553847722709,0.665460713484883,8.75721825406948));
#386742=CARTESIAN_POINT('Ctrl Pts',(2.65112941937648,0.645039239553609,
8.78942910404912));
#386743=CARTESIAN_POINT('Ctrl Pts',(2.65532178526108,0.648710274420148,
8.79672699501691));
#386744=CARTESIAN_POINT('Ctrl Pts',(2.65077470762197,0.656391262047141,
8.79893251111267));
#386745=CARTESIAN_POINT('Ctrl Pts',(2.65937452780626,0.652312038583003,
8.78111911759583));
#386746=CARTESIAN_POINT('Ctrl Pts',(2.6643397222864,0.656669693215929,8.78644465894813));
#386747=CARTESIAN_POINT('Ctrl Pts',(2.66180227631761,0.664368841203266,
8.78817647674132));
#386748=CARTESIAN_POINT('Ctrl Pts',(2.66451307602303,0.656844620434605,
8.76780923932029));
#386749=CARTESIAN_POINT('Ctrl Pts',(2.67037091713223,0.661992477688804,
8.76988516158374));
#386750=CARTESIAN_POINT('Ctrl Pts',(2.66868335772545,0.669360552311447,
8.77093053738833));
#386751=CARTESIAN_POINT('Ctrl Pts',(2.66351112944559,0.655960829007586,
8.75371302330492));
#386752=CARTESIAN_POINT('Ctrl Pts',(2.66922570397851,0.660981769086442,
8.75300828287559));
#386753=CARTESIAN_POINT('Ctrl Pts',(2.66734099870957,0.668387336274949,
8.75267964240738));
#386754=CARTESIAN_POINT('Origin',(2.6448686608445,0.656184713158531,8.78727029226991));
#386755=CARTESIAN_POINT('Ctrl Pts',(2.5995223305943,0.599517869856918,8.85049129520029));
#386756=CARTESIAN_POINT('Ctrl Pts',(2.60390169908879,0.60338080187969,8.85711686593484));
#386757=CARTESIAN_POINT('Ctrl Pts',(2.59985800069652,0.610914012710821,
8.85933012996512));
#386758=CARTESIAN_POINT('Ctrl Pts',(2.61742004498717,0.615304998560444,
8.82945683644722));
#386759=CARTESIAN_POINT('Ctrl Pts',(2.62183576488798,0.619199995254582,
8.83607469902389));
#386760=CARTESIAN_POINT('Ctrl Pts',(2.61774715137786,0.626737586518525,
8.8382956714852));
#386761=CARTESIAN_POINT('Ctrl Pts',(2.63529108139348,0.631068595275567,
8.80838214965002));
#386762=CARTESIAN_POINT('Ctrl Pts',(2.63972422778672,0.634978963445221,
8.81501364461994));
#386763=CARTESIAN_POINT('Ctrl Pts',(2.63560960807689,0.642536656032147,
8.81722098428721));
#386764=CARTESIAN_POINT('Ctrl Pts',(2.65313746692184,0.646810448064383,
8.78727029226991));
#386765=CARTESIAN_POINT('Ctrl Pts',(2.65757134967522,0.650721465759011,
8.79393457792714));
#386766=CARTESIAN_POINT('Ctrl Pts',(2.65344741704445,0.658313079213018,
8.79610912703474));
#386767=CARTESIAN_POINT('Origin',(2.59125352451696,0.608892134951066,8.85049129520029));
#386768=CARTESIAN_POINT('Ctrl Pts',(2.6022097463239,0.587743532225645,8.85049129520029));
#386769=CARTESIAN_POINT('Ctrl Pts',(2.60783148438851,0.586163287511667,
8.85711686593484));
#386770=CARTESIAN_POINT('Ctrl Pts',(2.60745677570886,0.577621604099172,
8.85933012996512));
#386771=CARTESIAN_POINT('Ctrl Pts',(2.5972362758088,0.589141551913027,8.86332496987232));
#386772=CARTESIAN_POINT('Ctrl Pts',(2.59853778293458,0.584707820574949,
8.86648636486737));
#386773=CARTESIAN_POINT('Ctrl Pts',(2.59354792537494,0.581549114601405,
8.87206031107456));
#386774=CARTESIAN_POINT('Ctrl Pts',(2.59562163897866,0.596077166803049,
8.86341338519876));
#386775=CARTESIAN_POINT('Ctrl Pts',(2.59483919973077,0.600644579578093,
8.86654584966058));
#386776=CARTESIAN_POINT('Ctrl Pts',(2.58894560269752,0.601268812545118,
8.87215952290715));
#386777=CARTESIAN_POINT('Ctrl Pts',(2.5995223305943,0.599517869856918,8.85049129520029));
#386778=CARTESIAN_POINT('Ctrl Pts',(2.60390169908879,0.60338080187969,8.85711686593484));
#386779=CARTESIAN_POINT('Ctrl Pts',(2.59985800069652,0.610914012710821,
8.85933012996512));
#386780=CARTESIAN_POINT('Origin',(2.59882715066403,0.575709910717479,8.85049129520029));
#386781=CARTESIAN_POINT('Ctrl Pts',(2.67103479566853,0.568397127400971,
8.78727029226991));
#386782=CARTESIAN_POINT('Ctrl Pts',(2.67672651297435,0.56679721184414,8.79393457792714));
#386783=CARTESIAN_POINT('Ctrl Pts',(2.67630485569206,0.558168097155223,
8.79610912703474));
#386784=CARTESIAN_POINT('Ctrl Pts',(2.64812562395424,0.574836790204019,
8.80838214965003));
#386785=CARTESIAN_POINT('Ctrl Pts',(2.65381639600417,0.573237140354268,
8.81501364461993));
#386786=CARTESIAN_POINT('Ctrl Pts',(2.65338841166109,0.564642628035515,
8.81722098428721));
#386787=CARTESIAN_POINT('Ctrl Pts',(2.6251848082303,0.581285347992641,8.82945683644722));
#386788=CARTESIAN_POINT('Ctrl Pts',(2.63085321011981,0.579691986292097,
8.83607469902389));
#386789=CARTESIAN_POINT('Ctrl Pts',(2.63043993491584,0.57112686830673,8.8382956714852));
#386790=CARTESIAN_POINT('Ctrl Pts',(2.6022097463239,0.587743532225645,8.85049129520029));
#386791=CARTESIAN_POINT('Ctrl Pts',(2.60783148438851,0.586163287511667,
8.85711686593484));
#386792=CARTESIAN_POINT('Ctrl Pts',(2.60745677570886,0.577621604099171,
8.85933012996512));
#386793=CARTESIAN_POINT('Origin',(2.66765220000865,0.556363505892805,8.78727029226991));
#386794=CARTESIAN_POINT('Ctrl Pts',(2.68435593267242,0.564652597894885,
8.75374538247847));
#386795=CARTESIAN_POINT('Ctrl Pts',(2.69167492525666,0.562608893919413,
8.75304829418602));
#386796=CARTESIAN_POINT('Ctrl Pts',(2.69319395121605,0.555128038129891,
8.75272238421917));
#386797=CARTESIAN_POINT('Ctrl Pts',(2.68562666750752,0.564295400620314,
8.7676940844502));
#386798=CARTESIAN_POINT('Ctrl Pts',(2.6931296528189,0.56219960330441,8.76974318093968));
#386799=CARTESIAN_POINT('Ctrl Pts',(2.69480757528628,0.554837339150392,
8.7707786988043));
#386800=CARTESIAN_POINT('Ctrl Pts',(2.67911360463672,0.566126190382139,
8.78108014887992));
#386801=CARTESIAN_POINT('Ctrl Pts',(2.6854731365548,0.564353736974275,8.78639403366327));
#386802=CARTESIAN_POINT('Ctrl Pts',(2.68654558210626,0.55633052463332,8.78812224174741));
#386803=CARTESIAN_POINT('Ctrl Pts',(2.66844013235527,0.569126450616964,
8.78944554828686));
#386804=CARTESIAN_POINT('Ctrl Pts',(2.67380121292356,0.567638084816047,
8.79673892988686));
#386805=CARTESIAN_POINT('Ctrl Pts',(2.67304049616502,0.558754118115881,
8.79894799272499));
#386806=CARTESIAN_POINT('Origin',(2.68115159472089,0.552568888126775,8.75721825406948));
#386807=CARTESIAN_POINT('Origin',(2.68115159472089,0.552568888126775,9.));
#386808=CARTESIAN_POINT('Origin',(2.68115159472089,0.552568888126776,7.51860402984325));
#386809=CARTESIAN_POINT('Ctrl Pts',(2.68591314580245,0.572925167585785,
7.50366195182966));
#386810=CARTESIAN_POINT('Ctrl Pts',(2.6894945274723,0.573689102821876,7.50000065167735));
#386811=CARTESIAN_POINT('Ctrl Pts',(2.68949452747232,0.573689102821761,
7.49482233047108));
#386812=CARTESIAN_POINT('Ctrl Pts',(2.68890430944023,0.566112918346452,
7.50215800491336));
#386813=CARTESIAN_POINT('Ctrl Pts',(2.69148329915018,0.56436548902017,7.49877273257265));
#386814=CARTESIAN_POINT('Ctrl Pts',(2.69220348433873,0.560989324088758,
7.49481816995649));
#386815=CARTESIAN_POINT('Ctrl Pts',(2.68724770526619,0.563840105342118,
7.51043025814043));
#386816=CARTESIAN_POINT('Ctrl Pts',(2.69222164317034,0.560781887116979,
7.51006209594516));
#386817=CARTESIAN_POINT('Ctrl Pts',(2.69339480712793,0.555089553984509,
7.507312818217));
#386818=CARTESIAN_POINT('Ctrl Pts',(2.68453273533962,0.564602918545393,
7.51860402984326));
#386819=CARTESIAN_POINT('Ctrl Pts',(2.69185835200808,0.562544677107289,
7.51860402984327));
#386820=CARTESIAN_POINT('Ctrl Pts',(2.69339429606665,0.555092033734655,
7.51860402984327));
#386821=CARTESIAN_POINT('Origin',(0.,0.,7.5));
#386822=CARTESIAN_POINT('Origin',(2.6345200847159,0.419811799220462,7.5));
#386823=CARTESIAN_POINT('',(2.6345200847159,0.419811799220462,7.59394543036555));
#386824=CARTESIAN_POINT('',(2.6345200847159,0.419811799220462,8.85049129520029));
#386825=CARTESIAN_POINT('',(2.6345200847159,0.419811799220462,7.5));
#386826=CARTESIAN_POINT('',(2.70196419720223,0.396095507607702,8.78727029226991));
#386827=CARTESIAN_POINT('Ctrl Pts',(2.6345200847159,0.419811799220462,8.85049129520029));
#386828=CARTESIAN_POINT('Ctrl Pts',(2.65703413439438,0.41189487737399,8.82945686509571));
#386829=CARTESIAN_POINT('Ctrl Pts',(2.67951471421565,0.403989724989143,
8.80838212259895));
#386830=CARTESIAN_POINT('Ctrl Pts',(2.70196419720223,0.396095507607702,
8.78727029226991));
#386831=CARTESIAN_POINT('',(2.71519273396521,0.391443777102025,8.75721825406948));
#386832=CARTESIAN_POINT('Origin',(2.67538354477845,0.405442638265208,8.75937679713132));
#386833=CARTESIAN_POINT('',(2.71519273396521,0.391443777102025,7.51860402984325));
#386834=CARTESIAN_POINT('',(2.71519273396521,0.391443777102025,7.5));
#386835=CARTESIAN_POINT('Ctrl Pts',(2.71519273396521,0.391443777102025,
7.51860402984325));
#386836=CARTESIAN_POINT('Ctrl Pts',(2.70480377576452,0.395096987933295,
7.52834476460825));
#386837=CARTESIAN_POINT('Ctrl Pts',(2.69440807320208,0.398752570376327,
7.53807742314407));
#386838=CARTESIAN_POINT('Ctrl Pts',(2.68400539982696,0.402410604061131,
7.54780169004674));
#386839=CARTESIAN_POINT('Ctrl Pts',(2.6675281274173,0.40820473171801,7.5632044032688));
#386840=CARTESIAN_POINT('Ctrl Pts',(2.65103334518628,0.414005016591771,
7.57858609112103));
#386841=CARTESIAN_POINT('Ctrl Pts',(2.6345200847159,0.419811799220462,7.59394543036555));
#386842=CARTESIAN_POINT('Origin',(2.85005793045282,0.60006065396636,7.5));
#386843=CARTESIAN_POINT('',(2.70021641947034,0.484077577700278,8.75721825406948));
#386844=CARTESIAN_POINT('',(2.68912759914126,0.475494405483876,8.78727029226991));
#386845=CARTESIAN_POINT('Origin',(2.66098003722313,0.453707113035681,8.75658640621088));
#386846=CARTESIAN_POINT('',(2.6325925749723,0.431734128529253,8.85049129520029));
#386847=CARTESIAN_POINT('Ctrl Pts',(2.68912759914126,0.475494405483876,
8.78727029226991));
#386848=CARTESIAN_POINT('Ctrl Pts',(2.67030932106718,0.460928336530414,
8.80838212259895));
#386849=CARTESIAN_POINT('Ctrl Pts',(2.65146497607287,0.446342090780963,
8.82945686509571));
#386850=CARTESIAN_POINT('Ctrl Pts',(2.6325925749723,0.431734128529253,8.85049129520029));
#386851=CARTESIAN_POINT('',(2.6325925749723,0.431734128529253,7.59394543036555));
#386852=CARTESIAN_POINT('',(2.6325925749723,0.431734128529253,7.5));
#386853=CARTESIAN_POINT('',(2.70021641947034,0.484077577700278,7.51860402984325));
#386854=CARTESIAN_POINT('Ctrl Pts',(2.6325925749723,0.431734128529252,7.59394543036555));
#386855=CARTESIAN_POINT('Ctrl Pts',(2.64643481479702,0.442448553035235,
7.57858609112103));
#386856=CARTESIAN_POINT('Ctrl Pts',(2.6602615652383,0.453150988164354,7.56320440326857));
#386857=CARTESIAN_POINT('Ctrl Pts',(2.67407363807278,0.463842062262924,
7.54780169004651));
#386858=CARTESIAN_POINT('Ctrl Pts',(2.68279367854782,0.470591708024162,
7.53807742314383));
#386859=CARTESIAN_POINT('Ctrl Pts',(2.69150787573962,0.477336830860077,
7.52834476460825));
#386860=CARTESIAN_POINT('Ctrl Pts',(2.70021641947034,0.484077577700278,
7.51860402984325));
#386861=CARTESIAN_POINT('',(2.70021641947034,0.484077577700278,7.5));
#386862=CARTESIAN_POINT('Origin',(2.63680073810823,0.42629749464224,7.5));
#386863=CARTESIAN_POINT('Ctrl Pts',(2.6325925749723,0.431734128529253,8.85049129520029));
#386864=CARTESIAN_POINT('Ctrl Pts',(2.6324394307242,0.431615589007792,8.85097269580138));
#386865=CARTESIAN_POINT('Ctrl Pts',(2.63229336726998,0.431491893478853,
8.85143669361005));
#386866=CARTESIAN_POINT('Ctrl Pts',(2.63214822387277,0.431356678978386,
8.8519052845931));
#386867=CARTESIAN_POINT('Ctrl Pts',(2.63186433259248,0.431092207990465,
8.85282181883899));
#386868=CARTESIAN_POINT('Ctrl Pts',(2.63159139830333,0.430790328371211,
8.85372622499636));
#386869=CARTESIAN_POINT('Ctrl Pts',(2.63133657541701,0.430435962534942,
8.85462257735071));
#386870=CARTESIAN_POINT('Ctrl Pts',(2.63112503050723,0.430141780603558,
8.85536669723987));
#386871=CARTESIAN_POINT('Ctrl Pts',(2.63092589359264,0.429811377957262,
8.85610498449051));
#386872=CARTESIAN_POINT('Ctrl Pts',(2.63075009497682,0.429431969215917,
8.85681338218371));
#386873=CARTESIAN_POINT('Ctrl Pts',(2.63059055745687,0.429087655187274,
8.85745625420284));
#386874=CARTESIAN_POINT('Ctrl Pts',(2.63044769614054,0.428698914290614,
8.85808743050665));
#386875=CARTESIAN_POINT('Ctrl Pts',(2.63034146522524,0.428245260526937,
8.85866804508409));
#386876=CARTESIAN_POINT('Ctrl Pts',(2.63029245258373,0.428035954514381,
8.85893592806395));
#386877=CARTESIAN_POINT('Ctrl Pts',(2.63025142607327,0.427812678304184,
8.85919241173848));
#386878=CARTESIAN_POINT('Ctrl Pts',(2.63022171543869,0.42757260085838,8.85943017985534));
#386879=CARTESIAN_POINT('Ctrl Pts',(2.63018159728671,0.427248425236019,
8.8597512372));
#386880=CARTESIAN_POINT('Ctrl Pts',(2.63016172595496,0.426885286146255,
8.86004599534705));
#386881=CARTESIAN_POINT('Ctrl Pts',(2.63017273972451,0.426486977495848,
8.86026130871721));
#386882=CARTESIAN_POINT('Ctrl Pts',(2.63017677217606,0.426341145469424,
8.86034014101235));
#386883=CARTESIAN_POINT('Ctrl Pts',(2.63018499302247,0.426188408071798,
8.86040910639693));
#386884=CARTESIAN_POINT('Ctrl Pts',(2.63019751418393,0.42603294462651,8.86046313645507));
#386885=CARTESIAN_POINT('Ctrl Pts',(2.63021705335152,0.425790345222132,
8.8605474499083));
#386886=CARTESIAN_POINT('Ctrl Pts',(2.63024774428927,0.425534497097221,
8.86059655985668));
#386887=CARTESIAN_POINT('Ctrl Pts',(2.6302873278218,0.425281773678598,8.86059725258816));
#386888=CARTESIAN_POINT('Ctrl Pts',(2.6303270028081,0.425028466367915,8.86059794692011));
#386889=CARTESIAN_POINT('Ctrl Pts',(2.6303786762971,0.424775900125062,8.86056369958366));
#386890=CARTESIAN_POINT('Ctrl Pts',(2.63043584326273,0.42453709575363,8.86048590497774));
#386891=CARTESIAN_POINT('Ctrl Pts',(2.6304507621387,0.424474774922749,8.86046560290182));
#386892=CARTESIAN_POINT('Ctrl Pts',(2.6304663373265,0.424412601679696,8.86044257503091));
#386893=CARTESIAN_POINT('Ctrl Pts',(2.63048205569772,0.424352489252271,
8.86041778462584));
#386894=CARTESIAN_POINT('Ctrl Pts',(2.63058782083114,0.423948007209002,
8.86025097596201));
#386895=CARTESIAN_POINT('Ctrl Pts',(2.63071458213298,0.42358263889542,8.8599848982295));
#386896=CARTESIAN_POINT('Ctrl Pts',(2.63085063533997,0.423264271385145,
8.85968173251462));
#386897=CARTESIAN_POINT('Ctrl Pts',(2.63092259969155,0.423095873212493,
8.85952137522077));
#386898=CARTESIAN_POINT('Ctrl Pts',(2.63099837530336,0.42293730390483,8.85934740853961));
#386899=CARTESIAN_POINT('Ctrl Pts',(2.63107549094398,0.422790129365309,
8.8591675900182));
#386900=CARTESIAN_POINT('Ctrl Pts',(2.63138515032498,0.422199147089328,
8.85844552518695));
#386901=CARTESIAN_POINT('Ctrl Pts',(2.63173123784028,0.421757093262747,
8.85759444184125));
#386902=CARTESIAN_POINT('Ctrl Pts',(2.63204579283192,0.42142201205954,8.85683498915139));
#386903=CARTESIAN_POINT('Ctrl Pts',(2.63207871017407,0.421386946704019,
8.85675551444998));
#386904=CARTESIAN_POINT('Ctrl Pts',(2.63211129380288,0.421353069065494,
8.85667699793651));
#386905=CARTESIAN_POINT('Ctrl Pts',(2.63214347290436,0.421320342132163,
8.85659965593547));
#386906=CARTESIAN_POINT('Ctrl Pts',(2.63257782805809,0.420878592316094,
8.85555568965886));
#386907=CARTESIAN_POINT('Ctrl Pts',(2.63305906768579,0.420516772853024,
8.85434650606346));
#386908=CARTESIAN_POINT('Ctrl Pts',(2.63358583604685,0.420228127733434,
8.85297329937117));
#386909=CARTESIAN_POINT('Ctrl Pts',(2.63388211115348,0.42006578244107,8.85220095427747));
#386910=CARTESIAN_POINT('Ctrl Pts',(2.63419306117444,0.419926794961197,
8.85137579139183));
#386911=CARTESIAN_POINT('Ctrl Pts',(2.6345200847159,0.419811799220462,8.85049129520029));
#386912=CARTESIAN_POINT('Origin',(2.63680073810823,0.42629749464224,7.59394543036555));
#386913=CARTESIAN_POINT('Ctrl Pts',(2.63214794555735,0.431389968309522,
7.59443877723642));
#386914=CARTESIAN_POINT('Ctrl Pts',(2.62756869039428,0.427845449188369,
7.58783886950016));
#386915=CARTESIAN_POINT('Ctrl Pts',(2.63107088212544,0.42011150875578,7.58559994247159));
#386916=CARTESIAN_POINT('Ctrl Pts',(2.65714596514289,0.45073939420012,7.56670252222134));
#386917=CARTESIAN_POINT('Ctrl Pts',(2.65257332830363,0.447199997915403,
7.56004874999029));
#386918=CARTESIAN_POINT('Ctrl Pts',(2.65607680870819,0.439411417665382,
7.55786368756704));
#386919=CARTESIAN_POINT('Ctrl Pts',(2.68209730342447,0.47005268697112,7.53888913333559));
#386920=CARTESIAN_POINT('Ctrl Pts',(2.67749749118058,0.466492255880997,
7.53222002137278));
#386921=CARTESIAN_POINT('Ctrl Pts',(2.68103621251043,0.458676893057078,
7.53005029815327));
#386922=CARTESIAN_POINT('Ctrl Pts',(2.70700083133714,0.48932897268294,7.51101258149734));
#386923=CARTESIAN_POINT('Ctrl Pts',(2.70234526101077,0.485725382698534,
7.5043616886572));
#386924=CARTESIAN_POINT('Ctrl Pts',(2.70594791084534,0.477906917650063,
7.50217374673251));
#386925=CARTESIAN_POINT('',(2.70461858999357,0.476880779649044,7.50366116523517));
#386926=CARTESIAN_POINT('Ctrl Pts',(2.70021641947034,0.484077577700279,
7.51860402984325));
#386927=CARTESIAN_POINT('Ctrl Pts',(2.70056563816122,0.484347886360363,
7.51734760759493));
#386928=CARTESIAN_POINT('Ctrl Pts',(2.70091762496878,0.484545099816493,
7.51608817408572));
#386929=CARTESIAN_POINT('Ctrl Pts',(2.70127809748605,0.484657114758144,
7.51481005913119));
#386930=CARTESIAN_POINT('Ctrl Pts',(2.70160462210596,0.484758580568974,
7.51365231206383));
#386931=CARTESIAN_POINT('Ctrl Pts',(2.70193849542102,0.484790521480719,
7.51247773061042));
#386932=CARTESIAN_POINT('Ctrl Pts',(2.70227745670569,0.48471562758731,7.51129758471022));
#386933=CARTESIAN_POINT('Ctrl Pts',(2.70269874687169,0.484622543031008,
7.50983079813402));
#386934=CARTESIAN_POINT('Ctrl Pts',(2.70311164139659,0.484354676680247,
7.50839324291155));
#386935=CARTESIAN_POINT('Ctrl Pts',(2.7034742857841,0.48384091319484,7.50715379678855));
#386936=CARTESIAN_POINT('Ctrl Pts',(2.70364181704178,0.483603569268321,
7.50658120839351));
#386937=CARTESIAN_POINT('Ctrl Pts',(2.70381467744276,0.483274526670549,
7.50598221009429));
#386938=CARTESIAN_POINT('Ctrl Pts',(2.70396861630568,0.482851037387539,
7.50545747549611));
#386939=CARTESIAN_POINT('Ctrl Pts',(2.70405076284779,0.482625050397906,
7.50517746087247));
#386940=CARTESIAN_POINT('Ctrl Pts',(2.7041286023332,0.482369787256009,7.50491486231392));
#386941=CARTESIAN_POINT('Ctrl Pts',(2.7041984779562,0.482091521235608,7.50468370960993));
#386942=CARTESIAN_POINT('Ctrl Pts',(2.70430296405359,0.481675425761071,
7.50433806340447));
#386943=CARTESIAN_POINT('Ctrl Pts',(2.7043922364335,0.481195283876951,7.50405484070984));
#386944=CARTESIAN_POINT('Ctrl Pts',(2.70445957844276,0.480683301291942,
7.50385766036131));
#386945=CARTESIAN_POINT('Ctrl Pts',(2.70446677962392,0.480628552712486,
7.50383657498791));
#386946=CARTESIAN_POINT('Ctrl Pts',(2.70447374114721,0.480573466128624,
7.50381643264937));
#386947=CARTESIAN_POINT('Ctrl Pts',(2.70448046317028,0.480518099751992,
7.50379723213559));
#386948=CARTESIAN_POINT('Ctrl Pts',(2.70452533487324,0.480148511076374,
7.50366906242519));
#386949=CARTESIAN_POINT('Ctrl Pts',(2.70455979670366,0.479758328762606,
7.50358235568538));
#386950=CARTESIAN_POINT('Ctrl Pts',(2.70458397329211,0.479381442565715,
7.5035341175365));
#386951=CARTESIAN_POINT('Ctrl Pts',(2.70462022335022,0.47881634436876,7.50346178989176));
#386952=CARTESIAN_POINT('Ctrl Pts',(2.7046351928416,0.478206885991993,7.50346967198527));
#386953=CARTESIAN_POINT('Ctrl Pts',(2.70463147855747,0.477608134512373,
7.50354272648692));
#386954=CARTESIAN_POINT('Ctrl Pts',(2.70462995079553,0.477361855635383,
7.50357277531559));
#386955=CARTESIAN_POINT('Ctrl Pts',(2.70462540584846,0.477117714546036,
7.50361331098761));
#386956=CARTESIAN_POINT('Ctrl Pts',(2.70461858999496,0.47688077964929,7.50366116523658));
#386957=CARTESIAN_POINT('',(2.63969113251172,0.426764791193857,7.57603338622103));
#386958=CARTESIAN_POINT('Origin',(2.64841525255361,0.428172349042287,7.5848687342763));
#386959=CARTESIAN_POINT('Ctrl Pts',(2.70461859003549,0.476880779688174,
7.50366116529968));
#386960=CARTESIAN_POINT('Ctrl Pts',(2.68301193100262,0.460202048194502,
7.52783573079709));
#386961=CARTESIAN_POINT('Ctrl Pts',(2.66137047797874,0.44349749326739,7.55196141284069));
#386962=CARTESIAN_POINT('Ctrl Pts',(2.63969113324643,0.426764792207688,
7.57603338728831));
#386963=CARTESIAN_POINT('Ctrl Pts',(2.63351343964686,0.432224581148209,
7.59639677331371));
#386964=CARTESIAN_POINT('Ctrl Pts',(2.6174729176982,0.423462528228453,7.59959882295468));
#386965=CARTESIAN_POINT('Ctrl Pts',(2.63537086205299,0.419671433336357,
7.59642833564546));
#386966=CARTESIAN_POINT('Ctrl Pts',(2.62983415240467,0.430929224257913,
7.58707626057421));
#386967=CARTESIAN_POINT('Ctrl Pts',(2.62694184795774,0.424801674501049,
7.58809943920599));
#386968=CARTESIAN_POINT('Ctrl Pts',(2.63152868410626,0.419834247104491,
7.58710240504252));
#386969=CARTESIAN_POINT('Ctrl Pts',(2.63527988042916,0.428232990116564,
7.58015376756929));
#386970=CARTESIAN_POINT('Ctrl Pts',(2.63373782678302,0.425834794555615,
7.58205880659761));
#386971=CARTESIAN_POINT('Ctrl Pts',(2.6359024780102,0.424034416788969,7.58020924244127));
#386972=CARTESIAN_POINT('Ctrl Pts',(2.63969113169473,0.426764791061976,
7.57603338509286));
#386973=CARTESIAN_POINT('Ctrl Pts',(2.63969113169473,0.426764791061976,
7.57603338509286));
#386974=CARTESIAN_POINT('Ctrl Pts',(2.63969113169473,0.426764791061976,
7.57603338509286));
#386975=CARTESIAN_POINT('Origin',(2.64841434182079,0.428177982249355,7.58486873427618));
#386976=CARTESIAN_POINT('Ctrl Pts',(2.72331185699535,0.388588739318531,
7.51098857897448));
#386977=CARTESIAN_POINT('Ctrl Pts',(2.71775791507471,0.39054174754022,7.50433767179956));
#386978=CARTESIAN_POINT('Ctrl Pts',(2.71871338746911,0.399097162409528,
7.50214974420965));
#386979=CARTESIAN_POINT('Ctrl Pts',(2.69359435960956,0.399038707566622,
7.53887321589169));
#386980=CARTESIAN_POINT('Ctrl Pts',(2.6881069637696,0.400968315283842,7.53220407452063));
#386981=CARTESIAN_POINT('Ctrl Pts',(2.68900271478691,0.409500639119538,
7.53003438070911));
#386982=CARTESIAN_POINT('Ctrl Pts',(2.66381979366645,0.409508743608587,
7.56669465659231));
#386983=CARTESIAN_POINT('Ctrl Pts',(2.65836482731568,0.411426947702931,
7.56004085833299));
#386984=CARTESIAN_POINT('Ctrl Pts',(2.65923556380893,0.419922738901277,
7.55785582193789));
#386985=CARTESIAN_POINT('Ctrl Pts',(2.63398950575049,0.419998373926593,
7.59443891967696));
#386986=CARTESIAN_POINT('Ctrl Pts',(2.62852663037769,0.421919359178073,
7.58783901202978));
#386987=CARTESIAN_POINT('Ctrl Pts',(2.6294133772601,0.430362868990635,7.58560008491213));
#386988=CARTESIAN_POINT('',(2.7171028689902,0.399661099761635,7.50366116523517));
#386989=CARTESIAN_POINT('Ctrl Pts',(2.71710286899057,0.399661099761689,
7.50366116523554));
#386990=CARTESIAN_POINT('Ctrl Pts',(2.71736205082467,0.39894908691515,7.50350835821027));
#386991=CARTESIAN_POINT('Ctrl Pts',(2.71757713724068,0.398286142087287,
7.50345484956));
#386992=CARTESIAN_POINT('Ctrl Pts',(2.71775509412383,0.397652740707336,
7.50349758195598));
#386993=CARTESIAN_POINT('Ctrl Pts',(2.71784639920251,0.397327758825151,
7.50351950684424));
#386994=CARTESIAN_POINT('Ctrl Pts',(2.71793705412928,0.396978557601504,
7.50357029184312));
#386995=CARTESIAN_POINT('Ctrl Pts',(2.71801521557552,0.396639423941707,
7.50365515313923));
#386996=CARTESIAN_POINT('Ctrl Pts',(2.71813545953054,0.39611769904416,7.50378570417639));
#386997=CARTESIAN_POINT('Ctrl Pts',(2.71823000319194,0.395604564193603,
7.50400001621911));
#386998=CARTESIAN_POINT('Ctrl Pts',(2.71828941758173,0.395138665010726,
7.50428903009634));
#386999=CARTESIAN_POINT('Ctrl Pts',(2.71829601212189,0.395086953785839,
7.50432110841318));
#387000=CARTESIAN_POINT('Ctrl Pts',(2.71830219412158,0.395035801890477,
7.50435406373354));
#387001=CARTESIAN_POINT('Ctrl Pts',(2.7183079653914,0.394985245296876,7.50438785222351));
#387002=CARTESIAN_POINT('Ctrl Pts',(2.71834320176766,0.394676572992355,
7.50459414719561));
#387003=CARTESIAN_POINT('Ctrl Pts',(2.71836317598707,0.394385118815853,
7.50483629897752));
#387004=CARTESIAN_POINT('Ctrl Pts',(2.71836843579496,0.394122138271516,
7.50509910455309));
#387005=CARTESIAN_POINT('Ctrl Pts',(2.71838003945946,0.393541976776812,
7.50567888004914));
#387006=CARTESIAN_POINT('Ctrl Pts',(2.71832100728855,0.393077541734351,
7.50637912803144));
#387007=CARTESIAN_POINT('Ctrl Pts',(2.71821992155784,0.392717065736721,
7.50710440483569));
#387008=CARTESIAN_POINT('Ctrl Pts',(2.71819513332984,0.392628669865651,
7.50728225710685));
#387009=CARTESIAN_POINT('Ctrl Pts',(2.71816746337446,0.392544726240379,
7.50746498566954));
#387010=CARTESIAN_POINT('Ctrl Pts',(2.71813795325093,0.392467063959524,
7.50764697238949));
#387011=CARTESIAN_POINT('Ctrl Pts',(2.71797931494821,0.39204957291088,7.50862528291182));
#387012=CARTESIAN_POINT('Ctrl Pts',(2.71775696699509,0.391774233741938,
7.50965856837421));
#387013=CARTESIAN_POINT('Ctrl Pts',(2.71750939926049,0.391587065661377,
7.51067959873202));
#387014=CARTESIAN_POINT('Ctrl Pts',(2.71737316242388,0.391484066830562,
7.51124147302578));
#387015=CARTESIAN_POINT('Ctrl Pts',(2.7172289930161,0.391408090365477,7.51180065547253));
#387016=CARTESIAN_POINT('Ctrl Pts',(2.71708174754226,0.391352365308008,
7.51235175716501));
#387017=CARTESIAN_POINT('Ctrl Pts',(2.71657295577451,0.391159813036229,
7.51425603304535));
#387018=CARTESIAN_POINT('Ctrl Pts',(2.71596462603848,0.391191771758375,
7.51626900505179));
#387019=CARTESIAN_POINT('Ctrl Pts',(2.71530098268083,0.391407169895982,
7.51827788969241));
#387020=CARTESIAN_POINT('Ctrl Pts',(2.7152650650482,0.391418827650236,7.51838661432544));
#387021=CARTESIAN_POINT('Ctrl Pts',(2.71522898031722,0.391431031303721,
7.51849533314856));
#387022=CARTESIAN_POINT('Ctrl Pts',(2.71519273396521,0.391443777102021,
7.51860402984325));
#387023=CARTESIAN_POINT('Ctrl Pts',(2.63969113352968,0.42676479046314,7.57603338728985));
#387024=CARTESIAN_POINT('Ctrl Pts',(2.66553865185877,0.417715864043958,
7.55196141284922));
#387025=CARTESIAN_POINT('Ctrl Pts',(2.69134133978206,0.408681709879649,
7.52783573083105));
#387026=CARTESIAN_POINT('Ctrl Pts',(2.71710286904403,0.39966109973703,7.50366116530176));
#387027=CARTESIAN_POINT('Origin',(9.12135307609332E-16,1.4746696281933E-16,
7.49482233047033));
#387028=CARTESIAN_POINT('Origin',(2.69591402793581,0.475345983446739,7.49482233047033));
#387029=CARTESIAN_POINT('Origin',(0.,0.,7.50366116523517));
#387030=CARTESIAN_POINT('Origin',(2.70835812744774,0.398374827879226,7.49482233047033));
#387031=CARTESIAN_POINT('Ctrl Pts',(2.70021558301562,0.484076930308837,
7.51860402984325));
#387032=CARTESIAN_POINT('Ctrl Pts',(2.70623301486718,0.488733839148602,
7.51860402984325));
#387033=CARTESIAN_POINT('Ctrl Pts',(2.70486003209636,0.49621790250624,7.51860402984325));
#387034=CARTESIAN_POINT('Ctrl Pts',(2.70244989574947,0.485806073346375,
7.51041458714366));
#387035=CARTESIAN_POINT('Ctrl Pts',(2.70590772978589,0.490506897692874,
7.51004642900444));
#387036=CARTESIAN_POINT('Ctrl Pts',(2.70485965344402,0.496219966522045,
7.50729136483011));
#387037=CARTESIAN_POINT('Ctrl Pts',(2.70483489309648,0.484310906180456,
7.50215815450137));
#387038=CARTESIAN_POINT('Ctrl Pts',(2.70657018076301,0.48689679890752,7.49877163671527));
#387039=CARTESIAN_POINT('Ctrl Pts',(2.70597109473123,0.49029459518171,7.49481588533168));
#387040=CARTESIAN_POINT('Ctrl Pts',(2.70461804783867,0.476880684055324,
7.50366171572174));
#387041=CARTESIAN_POINT('Ctrl Pts',(2.70822413765248,0.477516513051137,
7.50000045605858));
#387042=CARTESIAN_POINT('Ctrl Pts',(2.70822413765245,0.47751651305126,7.49482233047317));
#387043=CARTESIAN_POINT('Origin',(2.69256521376865,0.493962366585757,7.51860402984325));
#387044=CARTESIAN_POINT('Origin',(2.69256521376865,0.493962366585757,9.));
#387045=CARTESIAN_POINT('Origin',(2.69256521376865,0.493962366585757,8.75721825406948));
#387046=CARTESIAN_POINT('Ctrl Pts',(2.68701019562603,0.473855492158912,
8.78942910404912));
#387047=CARTESIAN_POINT('Ctrl Pts',(2.69142915185674,0.477250378686132,
8.7967269950169));
#387048=CARTESIAN_POINT('Ctrl Pts',(2.68738353924325,0.485206917164866,
8.79893251111267));
#387049=CARTESIAN_POINT('Ctrl Pts',(2.69570433342994,0.480585082531835,
8.78111911759583));
#387050=CARTESIAN_POINT('Ctrl Pts',(2.70093852227643,0.484615662793375,
8.78644465894813));
#387051=CARTESIAN_POINT('Ctrl Pts',(2.69889957586775,0.492461566776851,
8.78817647674131));
#387052=CARTESIAN_POINT('Ctrl Pts',(2.7011227274646,0.484779123793268,8.76780923932029));
#387053=CARTESIAN_POINT('Ctrl Pts',(2.7072983573577,0.489541091054149,8.76988516158374));
#387054=CARTESIAN_POINT('Ctrl Pts',(2.70608633938462,0.497002149479685,
8.77093053738834));
#387055=CARTESIAN_POINT('Ctrl Pts',(2.70006621478272,0.483961343148155,
8.75371302330491));
#387056=CARTESIAN_POINT('Ctrl Pts',(2.70609074084473,0.488605833119703,
8.75300828287559));
#387057=CARTESIAN_POINT('Ctrl Pts',(2.70468438422376,0.496116938257354,
8.75267964240738));
#387058=CARTESIAN_POINT('Origin',(2.68147639343957,0.485379194369355,8.78727029226991));
#387059=CARTESIAN_POINT('Ctrl Pts',(2.6325925749723,0.431734128529253,8.85049129520029));
#387060=CARTESIAN_POINT('Ctrl Pts',(2.637210444489,0.435308536641068,8.85711686593484));
#387061=CARTESIAN_POINT('Ctrl Pts',(2.63365770878388,0.44308535032814,8.85933012996512));
#387062=CARTESIAN_POINT('Ctrl Pts',(2.65146500140033,0.446342110385393,
8.82945683644723));
#387063=CARTESIAN_POINT('Ctrl Pts',(2.65612120202604,0.449946188245652,
8.8360746990239));
#387064=CARTESIAN_POINT('Ctrl Pts',(2.65252392414127,0.457730251086974,
8.8382956714852));
#387065=CARTESIAN_POINT('Ctrl Pts',(2.6703092969549,0.460928317866582,8.80838214965001));
#387066=CARTESIAN_POINT('Ctrl Pts',(2.67498387312226,0.464546619100827,
8.81501364461995));
#387067=CARTESIAN_POINT('Ctrl Pts',(2.6713619303665,0.472352408187726,8.81722098428721));
#387068=CARTESIAN_POINT('Ctrl Pts',(2.68912759914126,0.475494405483876,
8.78727029226991));
#387069=CARTESIAN_POINT('Ctrl Pts',(2.69380295177103,0.479113307729818,
8.79393457792714));
#387070=CARTESIAN_POINT('Ctrl Pts',(2.69017388854614,0.486953544670625,
8.79610912703474));
#387071=CARTESIAN_POINT('Origin',(2.62494136927061,0.441618917414731,8.85049129520029));
#387072=CARTESIAN_POINT('Ctrl Pts',(2.6345200847159,0.419811799220462,8.85049129520029));
#387073=CARTESIAN_POINT('Ctrl Pts',(2.64002902569027,0.417874615294257,
8.85711686593484));
#387074=CARTESIAN_POINT('Ctrl Pts',(2.63910781935455,0.409374489353958,
8.85933012996512));
#387075=CARTESIAN_POINT('Ctrl Pts',(2.62964640415828,0.421525597876429,
8.86332496987232));
#387076=CARTESIAN_POINT('Ctrl Pts',(2.63066116705591,0.417017588267043,
8.86648636486738));
#387077=CARTESIAN_POINT('Ctrl Pts',(2.62547918270721,0.41418507346522,8.87206031107457));
#387078=CARTESIAN_POINT('Ctrl Pts',(2.62847945114438,0.428550412938709,
8.86341338519876));
#387079=CARTESIAN_POINT('Ctrl Pts',(2.62799125464308,0.43315857252909,8.86654584966058));
#387080=CARTESIAN_POINT('Ctrl Pts',(2.62214976138055,0.434159127000924,
8.87215952290714));
#387081=CARTESIAN_POINT('Ctrl Pts',(2.6325925749723,0.431734128529253,8.85049129520029));
#387082=CARTESIAN_POINT('Ctrl Pts',(2.637210444489,0.435308536641068,8.85711686593484));
#387083=CARTESIAN_POINT('Ctrl Pts',(2.63365770878387,0.44308535032814,8.85933012996512));
#387084=CARTESIAN_POINT('Origin',(2.6303734421844,0.408019625726321,8.85049129520029));
#387085=CARTESIAN_POINT('Ctrl Pts',(2.70196419720223,0.396095507607702,
8.78727029226991));
#387086=CARTESIAN_POINT('Ctrl Pts',(2.70754171332274,0.394134209669121,
8.79393457792714));
#387087=CARTESIAN_POINT('Ctrl Pts',(2.70656805310419,0.385549840096635,
8.79610912703474));
#387088=CARTESIAN_POINT('Ctrl Pts',(2.67951468545062,0.403989735104181,
8.80838214965002));
#387089=CARTESIAN_POINT('Ctrl Pts',(2.68509127528127,0.402028762889524,
8.81501364461993));
#387090=CARTESIAN_POINT('Ctrl Pts',(2.68411351798303,0.393479329969083,
8.81722098428721));
#387091=CARTESIAN_POINT('Ctrl Pts',(2.65703416460906,0.411894866749188,
8.82945683644722));
#387092=CARTESIAN_POINT('Ctrl Pts',(2.66258883312431,0.409941603025147,
8.8360746990239));
#387093=CARTESIAN_POINT('Ctrl Pts',(2.66162763804507,0.401420561626523,
8.8382956714852));
#387094=CARTESIAN_POINT('Ctrl Pts',(2.6345200847159,0.419811799220462,8.85049129520029));
#387095=CARTESIAN_POINT('Ctrl Pts',(2.64002902569027,0.417874615294257,
8.85711686593484));
#387096=CARTESIAN_POINT('Ctrl Pts',(2.63910781935455,0.409374489353958,
8.85933012996512));
#387097=CARTESIAN_POINT('Origin',(2.69781755467072,0.384303334113561,8.78727029226991));
#387098=CARTESIAN_POINT('Ctrl Pts',(2.71501805167228,0.391505183460855,
8.75374538247848));
#387099=CARTESIAN_POINT('Ctrl Pts',(2.72219106603803,0.38899674902948,8.75304829418602));
#387100=CARTESIAN_POINT('Ctrl Pts',(2.72322767091958,0.381433939133116,
8.75272238421917));
#387101=CARTESIAN_POINT('Ctrl Pts',(2.71626328993838,0.391067303825981,
8.76769408445022));
#387102=CARTESIAN_POINT('Ctrl Pts',(2.72361658136666,0.388495094631037,
8.76974318093969));
#387103=CARTESIAN_POINT('Ctrl Pts',(2.72481935447853,0.381040452176713,
8.7707786988043));
#387104=CARTESIAN_POINT('Ctrl Pts',(2.70988090795657,0.393311625404765,
8.78108014887987));
#387105=CARTESIAN_POINT('Ctrl Pts',(2.71611381205456,0.391135357083546,
8.78639403366325));
#387106=CARTESIAN_POINT('Ctrl Pts',(2.71667000517195,0.383059917470437,
8.78812224174741));
#387107=CARTESIAN_POINT('Ctrl Pts',(2.69942159280191,0.396989573000186,
8.78944554828686));
#387108=CARTESIAN_POINT('Ctrl Pts',(2.70467629853092,0.395160779595101,
8.79673892988685));
#387109=CARTESIAN_POINT('Ctrl Pts',(2.70334794704577,0.386343805247372,
8.79894799272499));
#387110=CARTESIAN_POINT('Origin',(2.71104609143371,0.379651603607884,8.75721825406948));
#387111=CARTESIAN_POINT('Origin',(2.71104609143371,0.379651603607884,9.));
#387112=CARTESIAN_POINT('Origin',(2.71104609143371,0.379651603607884,7.51860402984325));
#387113=CARTESIAN_POINT('Ctrl Pts',(2.71710209070083,0.399660985282296,
7.50366195182966));
#387114=CARTESIAN_POINT('Ctrl Pts',(2.72072505953656,0.40019389102009,7.50000065167735));
#387115=CARTESIAN_POINT('Ctrl Pts',(2.72072505953658,0.400193891019974,
7.49482233047108));
#387116=CARTESIAN_POINT('Ctrl Pts',(2.71965064636477,0.392671088027359,
7.50215800491338));
#387117=CARTESIAN_POINT('Ctrl Pts',(2.72211237908243,0.390762012544002,
7.49877273257265));
#387118=CARTESIAN_POINT('Ctrl Pts',(2.72261477294344,0.387346641882077,
7.49481816995647));
#387119=CARTESIAN_POINT('Ctrl Pts',(2.71785182623253,0.390509083754953,
7.51043025814042));
#387120=CARTESIAN_POINT('Ctrl Pts',(2.72261960393337,0.387138467671458,
7.51006209594515));
#387121=CARTESIAN_POINT('Ctrl Pts',(2.72342564846378,0.381382665175079,
7.50731281821701));
#387122=CARTESIAN_POINT('Ctrl Pts',(2.7151913081126,0.39144427839713,7.51860402984326));
#387123=CARTESIAN_POINT('Ctrl Pts',(2.72237000153422,0.388920911965361,
7.51860402984326));
#387124=CARTESIAN_POINT('Ctrl Pts',(2.72342529733067,0.381385172574125,
7.51860402984327));
#387125=CARTESIAN_POINT('Origin',(0.,0.,7.5));
#387126=CARTESIAN_POINT('Origin',(2.65600461497701,0.250154969482936,7.5));
#387127=CARTESIAN_POINT('',(2.65600461497701,0.250154969482936,7.59394543036555));
#387128=CARTESIAN_POINT('',(2.65600461497701,0.250154969482936,8.85049129520029));
#387129=CARTESIAN_POINT('',(2.65600461497701,0.250154969482936,7.5));
#387130=CARTESIAN_POINT('',(2.72179064828012,0.222166246411456,8.78727029226991));
#387131=CARTESIAN_POINT('Ctrl Pts',(2.65600461497701,0.250154969482936,
8.85049129520029));
#387132=CARTESIAN_POINT('Ctrl Pts',(2.67796516820153,0.240811833685928,
8.82945686509571));
#387133=CARTESIAN_POINT('Ctrl Pts',(2.69989307440824,0.231482587590037,
8.80838212259896));
#387134=CARTESIAN_POINT('Ctrl Pts',(2.72179064828012,0.222166246411456,
8.78727029226991));
#387135=CARTESIAN_POINT('',(2.73469396819878,0.216676518124572,8.75721825406948));
#387136=CARTESIAN_POINT('Origin',(2.69586348137518,0.233197200634467,8.75937679713141));
#387137=CARTESIAN_POINT('',(2.73469396819878,0.216676518124572,7.51860402984325));
#387138=CARTESIAN_POINT('',(2.73469396819878,0.216676518124572,7.5));
#387139=CARTESIAN_POINT('Ctrl Pts',(2.73469396819878,0.216676518124572,
7.51860402984325));
#387140=CARTESIAN_POINT('Ctrl Pts',(2.72456041724852,0.220987845879672,
7.52834476460825));
#387141=CARTESIAN_POINT('Ctrl Pts',(2.71442028774321,0.225301972486544,
7.53807742314407));
#387142=CARTESIAN_POINT('Ctrl Pts',(2.70427335879911,0.229618991920351,
7.54780169004674));
#387143=CARTESIAN_POINT('Ctrl Pts',(2.68820117174637,0.236456917388509,
7.5632044032688));
#387144=CARTESIAN_POINT('Ctrl Pts',(2.67211190534232,0.243302109280994,
7.57858609112103));
#387145=CARTESIAN_POINT('Ctrl Pts',(2.65600461497701,0.250154969482936,
7.59394543036555));
#387146=CARTESIAN_POINT('Origin',(2.88264819886835,0.416223926434595,7.5));
#387147=CARTESIAN_POINT('',(2.72568349213022,0.310079528408739,8.75721825406948));
#387148=CARTESIAN_POINT('',(2.71406752923974,0.302224454398009,8.78727029226991));
#387149=CARTESIAN_POINT('Origin',(2.68458188288363,0.282285346760939,8.75658640620963));
#387150=CARTESIAN_POINT('',(2.6548449317704,0.262176299060784,8.85049129520029));
#387151=CARTESIAN_POINT('Ctrl Pts',(2.71406752923974,0.302224454398009,
8.78727029226991));
#387152=CARTESIAN_POINT('Ctrl Pts',(2.69435466409412,0.288894004211287,
8.80838212259896));
#387153=CARTESIAN_POINT('Ctrl Pts',(2.67461449285379,0.275545088797271,
8.82945686509571));
#387154=CARTESIAN_POINT('Ctrl Pts',(2.6548449317704,0.262176299060784,8.85049129520029));
#387155=CARTESIAN_POINT('',(2.6548449317704,0.262176299060784,7.59394543036555));
#387156=CARTESIAN_POINT('',(2.6548449317704,0.262176299060784,7.5));
#387157=CARTESIAN_POINT('',(2.72568349213022,0.310079528408739,7.51860402984325));
#387158=CARTESIAN_POINT('Ctrl Pts',(2.6548449317704,0.262176299060783,7.59394543036555));
#387159=CARTESIAN_POINT('Ctrl Pts',(2.66934520676389,0.271981834281903,
7.57858609112103));
#387160=CARTESIAN_POINT('Ctrl Pts',(2.68382925603652,0.281776397167827,
7.56320440326857));
#387161=CARTESIAN_POINT('Ctrl Pts',(2.69829792995535,0.291560562763152,
7.54780169004651));
#387162=CARTESIAN_POINT('Ctrl Pts',(2.70743250546073,0.2977376457418,7.53807742314383));
#387163=CARTESIAN_POINT('Ctrl Pts',(2.7165609599037,0.3039105894684,7.52834476460825));
#387164=CARTESIAN_POINT('Ctrl Pts',(2.72568349213022,0.310079528408737,
7.51860402984324));
#387165=CARTESIAN_POINT('',(2.72568349213022,0.310079528408739,7.5));
#387166=CARTESIAN_POINT('Origin',(2.65869612245474,0.256481217383335,7.5));
#387167=CARTESIAN_POINT('Ctrl Pts',(2.6548449317704,0.262176299060783,8.85049129520029));
#387168=CARTESIAN_POINT('Ctrl Pts',(2.65468450732037,0.262067815077147,
8.85097269580138));
#387169=CARTESIAN_POINT('Ctrl Pts',(2.65453081876943,0.261953732011581,
8.85143669361005));
#387170=CARTESIAN_POINT('Ctrl Pts',(2.65437731036211,0.261828094693195,
8.8519052845931));
#387171=CARTESIAN_POINT('Ctrl Pts',(2.65407705765252,0.261582356066062,
8.85282181883899));
#387172=CARTESIAN_POINT('Ctrl Pts',(2.65378534264253,0.26129858365081,8.85372622499636));
#387173=CARTESIAN_POINT('Ctrl Pts',(2.65350833902008,0.260961272455542,
8.85462257735071));
#387174=CARTESIAN_POINT('Ctrl Pts',(2.65327838045095,0.260681248681391,
8.85536669723986));
#387175=CARTESIAN_POINT('Ctrl Pts',(2.65305848371428,0.260364283628691,
8.85610498449051));
#387176=CARTESIAN_POINT('Ctrl Pts',(2.65285873749404,0.259996917879283,
8.85681338218371));
#387177=CARTESIAN_POINT('Ctrl Pts',(2.65267746748548,0.259663532884738,
8.85745625420284));
#387178=CARTESIAN_POINT('Ctrl Pts',(2.65250999297828,0.259284743853906,
8.85808743050665));
#387179=CARTESIAN_POINT('Ctrl Pts',(2.65237491462936,0.258838828408651,
8.85866804508409));
#387180=CARTESIAN_POINT('Ctrl Pts',(2.6523125924073,0.25863309268847,8.85893592806395));
#387181=CARTESIAN_POINT('Ctrl Pts',(2.6522573448343,0.258412903800744,8.85919241173848));
#387182=CARTESIAN_POINT('Ctrl Pts',(2.65221231342864,0.258175223186696,
8.85943017985534));
#387183=CARTESIAN_POINT('Ctrl Pts',(2.65215150770028,0.25785428399674,8.8597512372));
#387184=CARTESIAN_POINT('Ctrl Pts',(2.65210841079494,0.257493164175779,
8.86004599534705));
#387185=CARTESIAN_POINT('Ctrl Pts',(2.65209388221267,0.257094968238574,
8.86026130871721));
#387186=CARTESIAN_POINT('Ctrl Pts',(2.6520885628891,0.256949177479631,8.86034014101235));
#387187=CARTESIAN_POINT('Ctrl Pts',(2.65208698092624,0.256796227185932,
8.86040910639692));
#387188=CARTESIAN_POINT('Ctrl Pts',(2.65208951578449,0.256640280923396,
8.86046313645506));
#387189=CARTESIAN_POINT('Ctrl Pts',(2.65209347140956,0.256396928086748,
8.86054744990829));
#387190=CARTESIAN_POINT('Ctrl Pts',(2.65210770704384,0.256139639254116,
8.86059655985669));
#387191=CARTESIAN_POINT('Ctrl Pts',(2.65213101720273,0.255884898957225,
8.86059725258816));
#387192=CARTESIAN_POINT('Ctrl Pts',(2.6521543812174,0.255629570108478,8.86059794692011));
#387193=CARTESIAN_POINT('Ctrl Pts',(2.65218976656293,0.255374212058251,
8.86056369958365));
#387194=CARTESIAN_POINT('Ctrl Pts',(2.65223151582429,0.255132235635948,
8.86048590497774));
#387195=CARTESIAN_POINT('Ctrl Pts',(2.65224241113849,0.255069086994233,
8.86046560290182));
#387196=CARTESIAN_POINT('Ctrl Pts',(2.65225397087203,0.255006043587067,
8.86044257503091));
#387197=CARTESIAN_POINT('Ctrl Pts',(2.65226580553172,0.254945047587569,
8.86041778462583));
#387198=CARTESIAN_POINT('Ctrl Pts',(2.65234543810585,0.254534620200674,
8.86025097596201));
#387199=CARTESIAN_POINT('Ctrl Pts',(2.65244852973477,0.254161880950984,
8.85998489822951));
#387200=CARTESIAN_POINT('Ctrl Pts',(2.65256390552944,0.253835450602003,
8.85968173251462));
#387201=CARTESIAN_POINT('Ctrl Pts',(2.65262493271457,0.253662787649621,
8.85952137522077));
#387202=CARTESIAN_POINT('Ctrl Pts',(2.65269039306684,0.253499689179489,
8.85934740853961));
#387203=CARTESIAN_POINT('Ctrl Pts',(2.65275792075998,0.253347876209786,
8.8591675900182));
#387204=CARTESIAN_POINT('Ctrl Pts',(2.65302907954814,0.252738268225621,
8.85844552518696));
#387205=CARTESIAN_POINT('Ctrl Pts',(2.6533461335036,0.252274948742803,8.85759444184126));
#387206=CARTESIAN_POINT('Ctrl Pts',(2.65363857348188,0.251920402392356,
8.85683498915141));
#387207=CARTESIAN_POINT('Ctrl Pts',(2.65366917654678,0.251883300061011,
8.85675551445));
#387208=CARTESIAN_POINT('Ctrl Pts',(2.65369952268128,0.251847404387458,
8.85667699793652));
#387209=CARTESIAN_POINT('Ctrl Pts',(2.65372953884553,0.251812682973008,
8.85659965593547));
#387210=CARTESIAN_POINT('Ctrl Pts',(2.65413469856212,0.251344011549065,
8.85555568965886));
#387211=CARTESIAN_POINT('Ctrl Pts',(2.6545917675788,0.250952102354077,8.85434650606346));
#387212=CARTESIAN_POINT('Ctrl Pts',(2.65509896008146,0.25063030012207,8.85297329937118));
#387213=CARTESIAN_POINT('Ctrl Pts',(2.65538422496052,0.250449305974264,
8.85220095427748));
#387214=CARTESIAN_POINT('Ctrl Pts',(2.65568563114289,0.250290681422829,
8.85137579139184));
#387215=CARTESIAN_POINT('Ctrl Pts',(2.65600461497701,0.250154969482936,
8.85049129520029));
#387216=CARTESIAN_POINT('Origin',(2.65869612245474,0.256481217383335,7.59394543036555));
#387217=CARTESIAN_POINT('Ctrl Pts',(2.65437916547328,0.261861333459561,
7.59443877723642));
#387218=CARTESIAN_POINT('Ctrl Pts',(2.64958222076125,0.258617490818736,
7.58783886950016));
#387219=CARTESIAN_POINT('Ctrl Pts',(2.65258170159906,0.250675054401599,
7.58559994247159));
#387220=CARTESIAN_POINT('Ctrl Pts',(2.68056554591985,0.279569375265512,
7.56670252222133));
#387221=CARTESIAN_POINT('Ctrl Pts',(2.67577553415482,0.276330220898256,
7.56004874999026));
#387222=CARTESIAN_POINT('Ctrl Pts',(2.67877280023321,0.268333174361465,
7.55786368756705));
#387223=CARTESIAN_POINT('Ctrl Pts',(2.70670302591731,0.297244349072657,
7.53888913333558));
#387224=CARTESIAN_POINT('Ctrl Pts',(2.70188454687784,0.293985944252378,
7.53222002137278));
#387225=CARTESIAN_POINT('Ctrl Pts',(2.70491526550984,0.285959912275532,
7.53005029815327));
#387226=CARTESIAN_POINT('Ctrl Pts',(2.73279042272696,0.314885455076452,
7.51101258149734));
#387227=CARTESIAN_POINT('Ctrl Pts',(2.72791353496612,0.311587552469099,
7.5043616886572));
#387228=CARTESIAN_POINT('Ctrl Pts',(2.73100785199465,0.303554328728184,
7.50217374673251));
#387229=CARTESIAN_POINT('',(2.72961551748768,0.302615468917139,7.50366116523517));
#387230=CARTESIAN_POINT('Ctrl Pts',(2.72568349213022,0.310079528408739,
7.51860402984325));
#387231=CARTESIAN_POINT('Ctrl Pts',(2.72604931204916,0.310326907172344,
7.51734760759493));
#387232=CARTESIAN_POINT('Ctrl Pts',(2.7264132111716,0.310501163560087,7.51608817408572));
#387233=CARTESIAN_POINT('Ctrl Pts',(2.72678011988137,0.310589852801548,
7.51481005913119));
#387234=CARTESIAN_POINT('Ctrl Pts',(2.72711247455824,0.310670189635761,
7.51365231206383));
#387235=CARTESIAN_POINT('Ctrl Pts',(2.72744770835602,0.310680673584736,
7.51247773061042));
#387236=CARTESIAN_POINT('Ctrl Pts',(2.72778117474014,0.310584216244789,
7.51129758471022));
#387237=CARTESIAN_POINT('Ctrl Pts',(2.72819563537232,0.31046433078708,7.50983079813402));
#387238=CARTESIAN_POINT('Ctrl Pts',(2.72859051930512,0.310170560553426,
7.50839324291155));
#387239=CARTESIAN_POINT('Ctrl Pts',(2.72891950166131,0.309634617944518,
7.50715379678855));
#387240=CARTESIAN_POINT('Ctrl Pts',(2.72907148203047,0.309387027902018,
7.50658120839351));
#387241=CARTESIAN_POINT('Ctrl Pts',(2.72922290543959,0.309047586153636,
7.50598221009429));
#387242=CARTESIAN_POINT('Ctrl Pts',(2.72934939496709,0.308615104077967,
7.50545747549611));
#387243=CARTESIAN_POINT('Ctrl Pts',(2.72941689369418,0.308384318255817,
7.50517746087247));
#387244=CARTESIAN_POINT('Ctrl Pts',(2.72947821848437,0.308124592386469,
7.50491486231392));
#387245=CARTESIAN_POINT('Ctrl Pts',(2.72953012197526,0.307842421146914,
7.50468370960993));
#387246=CARTESIAN_POINT('Ctrl Pts',(2.72960773406618,0.307420486137913,
7.50433806340447));
#387247=CARTESIAN_POINT('Ctrl Pts',(2.72966606023027,0.306935611055772,
7.50405484070984));
#387248=CARTESIAN_POINT('Ctrl Pts',(2.7297004610413,0.306420365776551,7.50385766036131));
#387249=CARTESIAN_POINT('Ctrl Pts',(2.72970413967333,0.306365268302659,
7.50383657498791));
#387250=CARTESIAN_POINT('Ctrl Pts',(2.72970755748387,0.306309848873761,
7.50381643264937));
#387251=CARTESIAN_POINT('Ctrl Pts',(2.7297107183599,0.306254165571787,7.50379723213559));
#387252=CARTESIAN_POINT('Ctrl Pts',(2.72973181824138,0.305882461315862,
7.50366906242519));
#387253=CARTESIAN_POINT('Ctrl Pts',(2.7297412101996,0.305490872696448,7.50358235568538));
#387254=CARTESIAN_POINT('Ctrl Pts',(2.72974118993311,0.30511321185333,7.5035341175365));
#387255=CARTESIAN_POINT('Ctrl Pts',(2.72974115954581,0.304546952162028,
7.50346178989176));
#387256=CARTESIAN_POINT('Ctrl Pts',(2.72971705014849,0.303937786884254,
7.50346967198527));
#387257=CARTESIAN_POINT('Ctrl Pts',(2.72967498135674,0.303340503578766,
7.50354272648692));
#387258=CARTESIAN_POINT('Ctrl Pts',(2.72965767759192,0.303094828592186,
7.50357277531559));
#387259=CARTESIAN_POINT('Ctrl Pts',(2.72963749980964,0.302851480312651,
7.50361331098761));
#387260=CARTESIAN_POINT('Ctrl Pts',(2.72961551748909,0.302615468917296,
7.50366116523659));
#387261=CARTESIAN_POINT('',(2.6616105180258,0.256762365618806,7.57603338622103));
#387262=CARTESIAN_POINT('Origin',(2.67040689596839,0.257608075198453,7.58486873427629));
#387263=CARTESIAN_POINT('Ctrl Pts',(2.72961551753202,0.302615468953502,
7.50366116529969));
#387264=CARTESIAN_POINT('Ctrl Pts',(2.70698464170165,0.287355349099742,
7.52783573079709));
#387265=CARTESIAN_POINT('Ctrl Pts',(2.68431738885518,0.272071688128246,
7.55196141284069));
#387266=CARTESIAN_POINT('Ctrl Pts',(2.66161051882396,0.256762366583483,
7.57603338728831));
#387267=CARTESIAN_POINT('Ctrl Pts',(2.65579532783698,0.262606743989991,
7.5963967733137));
#387268=CARTESIAN_POINT('Ctrl Pts',(2.63922637620257,0.254890413417597,
7.59959882295473));
#387269=CARTESIAN_POINT('Ctrl Pts',(2.65684465102774,0.249960382504451,
7.59642833564546));
#387270=CARTESIAN_POINT('Ctrl Pts',(2.65204060628408,0.261549781292375,
7.5870762605742));
#387271=CARTESIAN_POINT('Ctrl Pts',(2.64876165092591,0.255620131825807,
7.588099439206));
#387272=CARTESIAN_POINT('Ctrl Pts',(2.65302079876161,0.2503690309405,7.58710240504254));
#387273=CARTESIAN_POINT('Ctrl Pts',(2.65730239716172,0.258510177860652,
7.58015376756929));
#387274=CARTESIAN_POINT('Ctrl Pts',(2.65560985891301,0.256215709366007,
7.58205880659762));
#387275=CARTESIAN_POINT('Ctrl Pts',(2.65765471203255,0.254280340988258,
7.58020924244125));
#387276=CARTESIAN_POINT('Ctrl Pts',(2.66161051720204,0.256762365539542,
7.57603338509286));
#387277=CARTESIAN_POINT('Ctrl Pts',(2.66161051720204,0.256762365539542,
7.57603338509286));
#387278=CARTESIAN_POINT('Ctrl Pts',(2.66161051720204,0.256762365539542,
7.57603338509286));
#387279=CARTESIAN_POINT('Origin',(2.67040634802725,0.257613755182223,7.5848687342762));
#387280=CARTESIAN_POINT('Ctrl Pts',(2.74261348672104,0.213307152323814,
7.51098857897448));
#387281=CARTESIAN_POINT('Ctrl Pts',(2.73719608563612,0.215611990161267,
7.50433767179956));
#387282=CARTESIAN_POINT('Ctrl Pts',(2.73869774222272,0.224088609686666,
7.50214974420965));
#387283=CARTESIAN_POINT('Ctrl Pts',(2.71362657888527,0.225639656586166,
7.53887321589169));
#387284=CARTESIAN_POINT('Ctrl Pts',(2.70827408787951,0.227916878375974,
7.53220407452065));
#387285=CARTESIAN_POINT('Ctrl Pts',(2.70971466634537,0.236374280672535,
7.53003438070911));
#387286=CARTESIAN_POINT('Ctrl Pts',(2.68458400549363,0.237995843805974,
7.56669465659234));
#387287=CARTESIAN_POINT('Ctrl Pts',(2.67926314671456,0.240259607638394,
7.56004085833298));
#387288=CARTESIAN_POINT('Ctrl Pts',(2.68067642139728,0.24868215504385,7.55785582193789));
#387289=CARTESIAN_POINT('Ctrl Pts',(2.65548708002545,0.250375155162354,
7.59443891967696));
#387290=CARTESIAN_POINT('Ctrl Pts',(2.65015850666364,0.252642201170471,
7.58783901202978));
#387291=CARTESIAN_POINT('Ctrl Pts',(2.65158440916058,0.261011548818738,
7.58560008491213));
#387292=CARTESIAN_POINT('',(2.73712666431695,0.224754574642228,7.50366116523517));
#387293=CARTESIAN_POINT('Ctrl Pts',(2.73712666431733,0.224754574642259,
7.50366116523554));
#387294=CARTESIAN_POINT('Ctrl Pts',(2.73733969481484,0.22402741886535,7.50350835821027));
#387295=CARTESIAN_POINT('Ctrl Pts',(2.73751186429179,0.223352055494748,
7.50345484956));
#387296=CARTESIAN_POINT('Ctrl Pts',(2.73764887337768,0.222708553769215,
7.50349758195598));
#387297=CARTESIAN_POINT('Ctrl Pts',(2.7377191691996,0.222378389660684,7.50351950684424));
#387298=CARTESIAN_POINT('Ctrl Pts',(2.73778726446689,0.222024097627302,
7.50357029184312));
#387299=CARTESIAN_POINT('Ctrl Pts',(2.73784353695387,0.221680652932927,
7.50365515313923));
#387300=CARTESIAN_POINT('Ctrl Pts',(2.73793010682584,0.221152295918489,
7.50378570417639));
#387301=CARTESIAN_POINT('Ctrl Pts',(2.73799157957439,0.220634157925334,
7.50400001621911));
#387302=CARTESIAN_POINT('Ctrl Pts',(2.7380210216278,0.220165409289273,7.50428903009634));
#387303=CARTESIAN_POINT('Ctrl Pts',(2.73802428946922,0.220113381797004,
7.50432110841318));
#387304=CARTESIAN_POINT('Ctrl Pts',(2.73802718145414,0.220061938916616,
7.50435406373354));
#387305=CARTESIAN_POINT('Ctrl Pts',(2.73802970169419,0.22001111643043,7.50438785222352));
#387306=CARTESIAN_POINT('Ctrl Pts',(2.73804508897109,0.219700820723885,
7.50459414719561));
#387307=CARTESIAN_POINT('Ctrl Pts',(2.73804634861812,0.219408685618617,
7.50483629897752));
#387308=CARTESIAN_POINT('Ctrl Pts',(2.73803474839784,0.219145908398964,
7.5050991045531));
#387309=CARTESIAN_POINT('Ctrl Pts',(2.73800915714678,0.218566195458937,
7.50567888004914));
#387310=CARTESIAN_POINT('Ctrl Pts',(2.73792048980846,0.218106496852257,
7.50637912803144));
#387311=CARTESIAN_POINT('Ctrl Pts',(2.73779651599276,0.217753238076229,
7.50710440483569));
#387312=CARTESIAN_POINT('Ctrl Pts',(2.73776611515193,0.217666612011177,
7.50728225710685));
#387313=CARTESIAN_POINT('Ctrl Pts',(2.73773312376091,0.217584613677214,
7.50746498566954));
#387314=CARTESIAN_POINT('Ctrl Pts',(2.73769869842967,0.217509001681951,
7.50764697238949));
#387315=CARTESIAN_POINT('Ctrl Pts',(2.73751363732303,0.217102532404395,
7.50862528291182));
#387316=CARTESIAN_POINT('Ctrl Pts',(2.7372741051665,0.216842004831574,7.50965856837422));
#387317=CARTESIAN_POINT('Ctrl Pts',(2.73701505418627,0.216671083027123,
7.51067959873202));
#387318=CARTESIAN_POINT('Ctrl Pts',(2.7368724981051,0.216577024542544,7.51124147302579));
#387319=CARTESIAN_POINT('Ctrl Pts',(2.73672375708,0.216510441144925,7.51180065547253));
#387320=CARTESIAN_POINT('Ctrl Pts',(2.73657324382109,0.216464264630464,
7.51235175716501));
#387321=CARTESIAN_POINT('Ctrl Pts',(2.73605316055418,0.21630470637846,7.51425603304536));
#387322=CARTESIAN_POINT('Ctrl Pts',(2.73544812829919,0.216375575257993,
7.51626900505181));
#387323=CARTESIAN_POINT('Ctrl Pts',(2.73479964907405,0.21663305061294,7.51827788969244));
#387324=CARTESIAN_POINT('Ctrl Pts',(2.73476455215293,0.216646985665711,
7.51838661432546));
#387325=CARTESIAN_POINT('Ctrl Pts',(2.73472932345267,0.216661476202132,
7.51849533314857));
#387326=CARTESIAN_POINT('Ctrl Pts',(2.73469396819878,0.216676518124568,
7.51860402984325));
#387327=CARTESIAN_POINT('Ctrl Pts',(2.66161051899485,0.256762364824367,
7.57603338728985));
#387328=CARTESIAN_POINT('Ctrl Pts',(2.68682516411914,0.246075974209705,
7.55196141284922));
#387329=CARTESIAN_POINT('Ctrl Pts',(2.7119960174081,0.235407197792705,7.52783573083104));
#387330=CARTESIAN_POINT('Ctrl Pts',(2.73712666436909,0.224754574614226,
7.50366116530176));
#387331=CARTESIAN_POINT('Origin',(9.19709468541365E-16,8.87232663177303E-17,
7.49482233047033));
#387332=CARTESIAN_POINT('Origin',(2.72083050515592,0.301641529324114,7.49482233047033));
#387333=CARTESIAN_POINT('Origin',(0.,0.,7.50366116523517));
#387334=CARTESIAN_POINT('Origin',(2.7283174780614,0.224031223057655,7.49482233047033));
#387335=CARTESIAN_POINT('Ctrl Pts',(2.72568261591557,0.310078935939271,
7.51860402984325));
#387336=CARTESIAN_POINT('Ctrl Pts',(2.73198605348183,0.314340738477925,
7.51860402984325));
#387337=CARTESIAN_POINT('Ctrl Pts',(2.73109539723703,0.321897392332887,
7.51860402984325));
#387338=CARTESIAN_POINT('Ctrl Pts',(2.72802312458908,0.311661373358629,
7.51041458714367));
#387339=CARTESIAN_POINT('Ctrl Pts',(2.7317750369846,0.316130995169986,7.51004642900442));
#387340=CARTESIAN_POINT('Ctrl Pts',(2.73109515160461,0.321899476368297,
7.5072913648301));
#387341=CARTESIAN_POINT('Ctrl Pts',(2.73030742601402,0.310016470869326,
7.50215815450137));
#387342=CARTESIAN_POINT('Ctrl Pts',(2.7322048270618,0.312485870339915,7.49877163671531));
#387343=CARTESIAN_POINT('Ctrl Pts',(2.73182466947127,0.315915069051093,
7.4948158853317));
#387344=CARTESIAN_POINT('Ctrl Pts',(2.72961497032199,0.30261540825581,7.50366171572174));
#387345=CARTESIAN_POINT('Ctrl Pts',(2.73325438874115,0.303018887905119,
7.50000045605858));
#387346=CARTESIAN_POINT('Ctrl Pts',(2.73325438874114,0.303018887905242,
7.49482233047317));
#387347=CARTESIAN_POINT('Origin',(2.71868132724959,0.320434222367736,7.51860402984325));
#387348=CARTESIAN_POINT('Origin',(2.71868132724959,0.320434222367736,9.));
#387349=CARTESIAN_POINT('Origin',(2.71868132724959,0.320434222367736,8.75721825406948));
#387350=CARTESIAN_POINT('Ctrl Pts',(2.71184947061986,0.300724570905254,
8.78942910404913));
#387351=CARTESIAN_POINT('Ctrl Pts',(2.71647685875768,0.30382935877622,8.79672699501691));
#387352=CARTESIAN_POINT('Ctrl Pts',(2.71294933545981,0.312028752983415,
8.79893251111267));
#387353=CARTESIAN_POINT('Ctrl Pts',(2.72095691172079,0.306883299291368,
8.78111911759584));
#387354=CARTESIAN_POINT('Ctrl Pts',(2.72643858652893,0.310570242662666,
8.78644465894814));
#387355=CARTESIAN_POINT('Ctrl Pts',(2.72490651814849,0.31853066213987,8.78817647674132));
#387356=CARTESIAN_POINT('Ctrl Pts',(2.72663288623002,0.310721565747487,
8.7678092393203));
#387357=CARTESIAN_POINT('Ctrl Pts',(2.73310092791912,0.315078075070137,
8.76988516158373));
#387358=CARTESIAN_POINT('Ctrl Pts',(2.73236943182155,0.322601458209093,
8.77093053738833));
#387359=CARTESIAN_POINT('Ctrl Pts',(2.72552614888092,0.309973156320347,
8.75371302330492));
#387360=CARTESIAN_POINT('Ctrl Pts',(2.73183587040218,0.314222110979058,
8.75300828287559));
#387361=CARTESIAN_POINT('Ctrl Pts',(2.73091364145018,0.321807889323718,
8.75267964240738));
#387362=CARTESIAN_POINT('Origin',(2.70706536435911,0.312579148357006,8.78727029226991));
#387363=CARTESIAN_POINT('Ctrl Pts',(2.6548449317704,0.262176299060784,8.85049129520029));
#387364=CARTESIAN_POINT('Ctrl Pts',(2.65968232649294,0.265447495252001,
8.85711686593484));
#387365=CARTESIAN_POINT('Ctrl Pts',(2.65663515242803,0.273435955199454,
8.85933012996512));
#387366=CARTESIAN_POINT('Ctrl Pts',(2.67461451938527,0.27554510673868,8.82945683644721));
#387367=CARTESIAN_POINT('Ctrl Pts',(2.67949206740875,0.27884345583608,8.83607469902389));
#387368=CARTESIAN_POINT('Ctrl Pts',(2.67640090713581,0.28684200387085,8.83829567148518));
#387369=CARTESIAN_POINT('Ctrl Pts',(2.69435463883558,0.288893987130678,
8.80838214965003));
#387370=CARTESIAN_POINT('Ctrl Pts',(2.69925143594087,0.292205353053615,
8.81501364461992));
#387371=CARTESIAN_POINT('Ctrl Pts',(2.69613705347889,0.300227162978777,
8.81722098428722));
#387372=CARTESIAN_POINT('Ctrl Pts',(2.71406752923974,0.302224454398009,
8.78727029226991));
#387373=CARTESIAN_POINT('Ctrl Pts',(2.71896513971909,0.305536370349683,
8.79393457792714));
#387374=CARTESIAN_POINT('Ctrl Pts',(2.71584585849932,0.313593013561975,
8.79610912703474));
#387375=CARTESIAN_POINT('Origin',(2.64784276688977,0.272530993019781,8.85049129520029));
#387376=CARTESIAN_POINT('Ctrl Pts',(2.65600461497701,0.250154969482936,
8.85049129520029));
#387377=CARTESIAN_POINT('Ctrl Pts',(2.66137812144103,0.24786880664878,8.85711686593484));
#387378=CARTESIAN_POINT('Ctrl Pts',(2.65991420288366,0.239445167021439,
8.85933012996512));
#387379=CARTESIAN_POINT('Ctrl Pts',(2.65125075137568,0.252177504741206,
8.86332496987232));
#387380=CARTESIAN_POINT('Ctrl Pts',(2.65197460016676,0.247613741238966,
8.86648636486736));
#387381=CARTESIAN_POINT('Ctrl Pts',(2.64662178291422,0.245119057019738,
8.87206031107457));
#387382=CARTESIAN_POINT('Ctrl Pts',(2.65053627743827,0.259262653503836,
8.86341338519876));
#387383=CARTESIAN_POINT('Ctrl Pts',(2.6503443297877,0.263892623993351,8.86654584966058));
#387384=CARTESIAN_POINT('Ctrl Pts',(2.64457894424469,0.265265388477058,
8.87215952290714));
#387385=CARTESIAN_POINT('Ctrl Pts',(2.6548449317704,0.262176299060783,8.85049129520029));
#387386=CARTESIAN_POINT('Ctrl Pts',(2.65968232649294,0.265447495252001,
8.85711686593484));
#387387=CARTESIAN_POINT('Ctrl Pts',(2.65663515242803,0.273435955199453,
8.85933012996512));
#387388=CARTESIAN_POINT('Origin',(2.65111096501749,0.23865270057312,8.85049129520029));
#387389=CARTESIAN_POINT('Ctrl Pts',(2.72179064828012,0.222166246411456,
8.78727029226991));
#387390=CARTESIAN_POINT('Ctrl Pts',(2.7272310440052,0.219851625485051,8.79393457792714));
#387391=CARTESIAN_POINT('Ctrl Pts',(2.7257093818291,0.21134727604491,8.79610912703474));
#387392=CARTESIAN_POINT('Ctrl Pts',(2.69989304635039,0.231482599527275,
8.80838214965002));
#387393=CARTESIAN_POINT('Ctrl Pts',(2.70533253855793,0.229168363003168,
8.81501364461988));
#387394=CARTESIAN_POINT('Ctrl Pts',(2.70380902611905,0.220699140934762,
8.81722098428721));
#387395=CARTESIAN_POINT('Ctrl Pts',(2.67796519767341,0.240811821147091,
8.82945683644723));
#387396=CARTESIAN_POINT('Ctrl Pts',(2.68338330748996,0.238506681779163,
8.83607469902389));
#387397=CARTESIAN_POINT('Ctrl Pts',(2.68187814229223,0.230064731754138,
8.8382956714852));
#387398=CARTESIAN_POINT('Ctrl Pts',(2.65600461497701,0.250154969482936,
8.85049129520029));
#387399=CARTESIAN_POINT('Ctrl Pts',(2.66137812144103,0.24786880664878,8.85711686593484));
#387400=CARTESIAN_POINT('Ctrl Pts',(2.65991420288366,0.239445167021439,
8.85933012996512));
#387401=CARTESIAN_POINT('Origin',(2.71689699832061,0.21066397750164,8.78727029226991));
#387402=CARTESIAN_POINT('Ctrl Pts',(2.73452357912826,0.216748990250391,
8.75374538247847));
#387403=CARTESIAN_POINT('Ctrl Pts',(2.74152113982086,0.213786133058247,
8.75304829418601));
#387404=CARTESIAN_POINT('Ctrl Pts',(2.74207106399279,0.206172446263127,
8.75272238421917));
#387405=CARTESIAN_POINT('Ctrl Pts',(2.7357382038743,0.216232227596534,8.76769408445021));
#387406=CARTESIAN_POINT('Ctrl Pts',(2.74291158516778,0.213194176281851,
8.76974318093971));
#387407=CARTESIAN_POINT('Ctrl Pts',(2.7436342664713,0.205677788252101,8.7707786988043));
#387408=CARTESIAN_POINT('Ctrl Pts',(2.72951272935799,0.218880858593531,
8.78108014887987));
#387409=CARTESIAN_POINT('Ctrl Pts',(2.73559339329593,0.216309718112314,
8.78639403366322));
#387410=CARTESIAN_POINT('Ctrl Pts',(2.73563104846251,0.208215234940591,
8.78812224174741));
#387411=CARTESIAN_POINT('Ctrl Pts',(2.71931055089962,0.223221380073952,
8.78944554828685));
#387412=CARTESIAN_POINT('Ctrl Pts',(2.72443728907638,0.221059673969063,
8.79673892988686));
#387413=CARTESIAN_POINT('Ctrl Pts',(2.72254676134579,0.212345922812613,
8.79894799272499));
#387414=CARTESIAN_POINT('Origin',(2.72980031823926,0.205174249214755,8.75721825406948));
#387415=CARTESIAN_POINT('Origin',(2.72980031823926,0.205174249214755,9.));
#387416=CARTESIAN_POINT('Origin',(2.72980031823926,0.205174249214756,7.51860402984325));
#387417=CARTESIAN_POINT('Ctrl Pts',(2.73712588029194,0.22475451026327,7.50366195182966));
#387418=CARTESIAN_POINT('Ctrl Pts',(2.74077554873749,0.225054196678783,
7.50000065167735));
#387419=CARTESIAN_POINT('Ctrl Pts',(2.7407755487375,0.225054196678667,7.49482233047108));
#387420=CARTESIAN_POINT('Ctrl Pts',(2.73922135542018,0.217615687979893,
7.50215800491337));
#387421=CARTESIAN_POINT('Ctrl Pts',(2.74155571535778,0.215552811140105,
7.49877273257265));
#387422=CARTESIAN_POINT('Ctrl Pts',(2.74183825344708,0.212112269238307,
7.49481816995647));
#387423=CARTESIAN_POINT('Ctrl Pts',(2.73728771106749,0.215573376578712,
7.51043025814043));
#387424=CARTESIAN_POINT('Ctrl Pts',(2.74182973674376,0.211904213221347,
7.51006209594516));
#387425=CARTESIAN_POINT('Ctrl Pts',(2.74226534963713,0.206108593188127,
7.50731281821701));
#387426=CARTESIAN_POINT('Ctrl Pts',(2.73469257739382,0.216677109744404,
7.51860402984326));
#387427=CARTESIAN_POINT('Ctrl Pts',(2.74169484877752,0.213698987372904,
7.51860402984326));
#387428=CARTESIAN_POINT('Ctrl Pts',(2.74226515987506,0.206111117932626,
7.51860402984327));
#387429=CARTESIAN_POINT('Origin',(0.,0.,7.5));
#387430=CARTESIAN_POINT('Origin',(2.66657505256398,0.0794701993177319,7.5));
#387431=CARTESIAN_POINT('',(2.66657505256398,0.0794701993177319,7.59394543036555));
#387432=CARTESIAN_POINT('',(2.66657505256398,0.0794701993177319,8.85049129520029));
#387433=CARTESIAN_POINT('',(2.66657505256398,0.0794701993177319,7.5));
#387434=CARTESIAN_POINT('',(2.73043267776197,0.0473240564541946,8.78727029226991));
#387435=CARTESIAN_POINT('Ctrl Pts',(2.66657505256398,0.0794701993177318,
8.85049129520029));
#387436=CARTESIAN_POINT('Ctrl Pts',(2.68789186871081,0.0687392425192737,
8.82945686509571));
#387437=CARTESIAN_POINT('Ctrl Pts',(2.70917699483285,0.0580242385856641,
8.80838212259896));
#387438=CARTESIAN_POINT('Ctrl Pts',(2.73043267776197,0.0473240564541948,
8.78727029226991));
#387439=CARTESIAN_POINT('',(2.742957758327,0.0410188888571772,8.75721825406948));
#387440=CARTESIAN_POINT('Origin',(2.70526553666578,0.0599935056857609,8.75937679713137));
#387441=CARTESIAN_POINT('',(2.742957758327,0.0410188888571772,7.51860402984325));
#387442=CARTESIAN_POINT('',(2.742957758327,0.0410188888571772,7.5));
#387443=CARTESIAN_POINT('Ctrl Pts',(2.742957758327,0.041018888857177,7.51860402984325));
#387444=CARTESIAN_POINT('Ctrl Pts',(2.73312125556167,0.0459706173655847,
7.52834476460825));
#387445=CARTESIAN_POINT('Ctrl Pts',(2.72327836708068,0.0509255604646928,
7.53807742314407));
#387446=CARTESIAN_POINT('Ctrl Pts',(2.71342887847514,0.0558838260886514,
7.54780169004674));
#387447=CARTESIAN_POINT('Ctrl Pts',(2.69782782084339,0.0637374508656102,
7.5632044032688));
#387448=CARTESIAN_POINT('Ctrl Pts',(2.68221018451309,0.0715994214150438,
7.57858609112103));
#387449=CARTESIAN_POINT('Ctrl Pts',(2.66657505256398,0.0794701993177321,
7.59394543036555));
#387450=CARTESIAN_POINT('Origin',(2.90339304750862,0.230676845509359,7.5));
#387451=CARTESIAN_POINT('',(2.73995014666366,0.134807295823118,8.75721825406948));
#387452=CARTESIAN_POINT('',(2.72785477369492,0.127712598202077,8.78727029226991));
#387453=CARTESIAN_POINT('Origin',(2.6971522057523,0.109703609450326,8.75658640621094));
#387454=CARTESIAN_POINT('',(2.66618796128141,0.0915411309428337,8.85049129520029));
#387455=CARTESIAN_POINT('Ctrl Pts',(2.72785477369492,0.127712598202077,
8.78727029226991));
#387456=CARTESIAN_POINT('Ctrl Pts',(2.70732832586903,0.115672544461277,
8.80838212259895));
#387457=CARTESIAN_POINT('Ctrl Pts',(2.68677344498056,0.103615812939474,
8.82945686509571));
#387458=CARTESIAN_POINT('Ctrl Pts',(2.66618796128141,0.0915411309428339,
8.85049129520029));
#387459=CARTESIAN_POINT('',(2.66618796128141,0.0915411309428337,7.59394543036555));
#387460=CARTESIAN_POINT('',(2.66618796128141,0.0915411309428337,7.5));
#387461=CARTESIAN_POINT('',(2.73995014666366,0.134807295823118,7.51860402984325));
#387462=CARTESIAN_POINT('Ctrl Pts',(2.6661879612814,0.0915411309428325,
7.59394543036555));
#387463=CARTESIAN_POINT('Ctrl Pts',(2.68128668670342,0.100397483831588,
7.57858609112103));
#387464=CARTESIAN_POINT('Ctrl Pts',(2.69636851674212,0.10924392651449,7.56320440326857));
#387465=CARTESIAN_POINT('Ctrl Pts',(2.71143433686065,0.118080978371442,
7.54780169004651));
#387466=CARTESIAN_POINT('Ctrl Pts',(2.72094591146625,0.12366011560856,7.53807742314383));
#387467=CARTESIAN_POINT('Ctrl Pts',(2.73045111238304,0.129235514275984,
7.52834476460825));
#387468=CARTESIAN_POINT('Ctrl Pts',(2.73995014666366,0.134807295823118,
7.51860402984325));
#387469=CARTESIAN_POINT('',(2.73995014666366,0.134807295823118,7.5));
#387470=CARTESIAN_POINT('Origin',(2.66966635414557,0.0856110037871532,7.5));
#387471=CARTESIAN_POINT('Ctrl Pts',(2.66618796128141,0.0915411309428336,
8.85049129520029));
#387472=CARTESIAN_POINT('Ctrl Pts',(2.66602091584792,0.0914431482809804,
8.85097269580138));
#387473=CARTESIAN_POINT('Ctrl Pts',(2.66586023373948,0.0913391464705742,
8.85143669361005));
#387474=CARTESIAN_POINT('Ctrl Pts',(2.66569899112102,0.0912236026049601,
8.8519052845931));
#387475=CARTESIAN_POINT('Ctrl Pts',(2.66538361078493,0.0909976061313448,
8.85282181883899));
#387476=CARTESIAN_POINT('Ctrl Pts',(2.66507431377364,0.0907331070018158,
8.85372622499635));
#387477=CARTESIAN_POINT('Ctrl Pts',(2.66477626768235,0.0904142365316012,
8.85462257735071));
#387478=CARTESIAN_POINT('Ctrl Pts',(2.66452884040296,0.0901495215924372,
8.85536669723986));
#387479=CARTESIAN_POINT('Ctrl Pts',(2.66428908744706,0.0898472966107245,
8.85610498449051));
#387480=CARTESIAN_POINT('Ctrl Pts',(2.66406621442249,0.0894934834379194,
8.85681338218371));
#387481=CARTESIAN_POINT('Ctrl Pts',(2.66386395680265,0.0891723974279239,
8.85745625420285));
#387482=CARTESIAN_POINT('Ctrl Pts',(2.66367255729327,0.0888051167882957,
8.85808743050666));
#387483=CARTESIAN_POINT('Ctrl Pts',(2.66350918657662,0.0883687720236747,
8.85866804508411));
#387484=CARTESIAN_POINT('Ctrl Pts',(2.66343381086941,0.0881674520080747,
8.85893592806396));
#387485=CARTESIAN_POINT('Ctrl Pts',(2.663364569258,0.0879512552461915,8.85919241173848));
#387486=CARTESIAN_POINT('Ctrl Pts',(2.66330440212497,0.087716948144525,
8.85943017985534));
#387487=CARTESIAN_POINT('Ctrl Pts',(2.66322315868399,0.0874005641949481,
8.8597512372));
#387488=CARTESIAN_POINT('Ctrl Pts',(2.6631570132995,0.0870429475615944,
8.86004599534706));
#387489=CARTESIAN_POINT('Ctrl Pts',(2.66311700206647,0.086646500610111,
8.86026130871721));
#387490=CARTESIAN_POINT('Ctrl Pts',(2.66310235282602,0.0865013502041498,
8.86034014101235));
#387491=CARTESIAN_POINT('Ctrl Pts',(2.66309097455451,0.0863488155199414,
8.86040910639693));
#387492=CARTESIAN_POINT('Ctrl Pts',(2.66308351269328,0.0861930272568014,
8.86046313645507));
#387493=CARTESIAN_POINT('Ctrl Pts',(2.66307186852131,0.0859499209768873,
8.8605474499083));
#387494=CARTESIAN_POINT('Ctrl Pts',(2.66306959035485,0.0856922486915364,
8.86059655985668));
#387495=CARTESIAN_POINT('Ctrl Pts',(2.66307653135366,0.0854365382988978,
8.86059725258816));
#387496=CARTESIAN_POINT('Ctrl Pts',(2.66308348838895,0.0851802371130951,
8.86059794692011));
#387497=CARTESIAN_POINT('Ctrl Pts',(2.66310244018504,0.0849231365764974,
8.86056369958366));
#387498=CARTESIAN_POINT('Ctrl Pts',(2.66312860018546,0.0846789824363461,
8.86048590497774));
#387499=CARTESIAN_POINT('Ctrl Pts',(2.6631354271667,0.0846152654751113,
8.86046560290182));
#387500=CARTESIAN_POINT('Ctrl Pts',(2.66314292394457,0.0845516109627158,
8.86044257503091));
#387501=CARTESIAN_POINT('Ctrl Pts',(2.66315082626157,0.0844899820367909,
8.86041778462583));
#387502=CARTESIAN_POINT('Ctrl Pts',(2.66320399904907,0.0840752958404387,
8.86025097596201));
#387503=CARTESIAN_POINT('Ctrl Pts',(2.66328299737946,0.0836967173201699,
8.8599848982295));
#387504=CARTESIAN_POINT('Ctrl Pts',(2.66337722165791,0.0833635655048054,
8.85968173251461));
#387505=CARTESIAN_POINT('Ctrl Pts',(2.66342706090281,0.0831873472818008,
8.85952137522076));
#387506=CARTESIAN_POINT('Ctrl Pts',(2.6634819370049,0.0830203898557986,
8.85934740853961));
#387507=CARTESIAN_POINT('Ctrl Pts',(2.66353959926479,0.0828645622879688,
8.8591675900182));
#387508=CARTESIAN_POINT('Ctrl Pts',(2.66377114321049,0.0822388336055786,
8.85844552518696));
#387509=CARTESIAN_POINT('Ctrl Pts',(2.66405786076342,0.081756152345655,
8.85759444184125));
#387510=CARTESIAN_POINT('Ctrl Pts',(2.66432698402973,0.0813835977549701,
8.8568349891514));
#387511=CARTESIAN_POINT('Ctrl Pts',(2.66435514706282,0.0813446109092454,
8.85675551444999));
#387512=CARTESIAN_POINT('Ctrl Pts',(2.66438313100423,0.0813068447036919,
8.85667699793652));
#387513=CARTESIAN_POINT('Ctrl Pts',(2.66441086088838,0.0812702714858658,
8.85659965593547));
#387514=CARTESIAN_POINT('Ctrl Pts',(2.66478516027966,0.0807766043254579,
8.85555568965886));
#387515=CARTESIAN_POINT('Ctrl Pts',(2.66521618049069,0.0803562158374976,
8.85434650606346));
#387516=CARTESIAN_POINT('Ctrl Pts',(2.66570171297216,0.0800025788474723,
8.85297329937117));
#387517=CARTESIAN_POINT('Ctrl Pts',(2.66597479540906,0.0798036795880011,
8.85220095427747));
#387518=CARTESIAN_POINT('Ctrl Pts',(2.6662654192102,0.079626069787311,8.85137579139184));
#387519=CARTESIAN_POINT('Ctrl Pts',(2.66657505256398,0.0794701993177319,
8.85049129520029));
#387520=CARTESIAN_POINT('Origin',(2.66966635414557,0.0856110037871532,7.59394543036555));
#387521=CARTESIAN_POINT('Ctrl Pts',(2.66570297203574,0.0912566542213349,
7.59443877723642));
#387522=CARTESIAN_POINT('Ctrl Pts',(2.66070804944951,0.088326817706052,
7.58783886950016));
#387523=CARTESIAN_POINT('Ctrl Pts',(2.66319249388382,0.0802085224792507,
7.58559994247159));
#387524=CARTESIAN_POINT('Ctrl Pts',(2.69297010788919,0.107250545800535,
7.5667025222214));
#387525=CARTESIAN_POINT('Ctrl Pts',(2.68798240438419,0.104324943730763,
7.5600487499903));
#387526=CARTESIAN_POINT('Ctrl Pts',(2.69046113972711,0.0961522924868117,
7.55786368756705));
#387527=CARTESIAN_POINT('Ctrl Pts',(2.72018632509071,0.123214570385162,
7.5388891333356));
#387528=CARTESIAN_POINT('Ctrl Pts',(2.71516897941957,0.120271581319099,
7.5322200213728));
#387529=CARTESIAN_POINT('Ctrl Pts',(2.71767924148075,0.112067860876272,
7.53005029815327));
#387530=CARTESIAN_POINT('Ctrl Pts',(2.74735039208809,0.139148005592338,
7.51101258149734));
#387531=CARTESIAN_POINT('Ctrl Pts',(2.74227222707067,0.136169342151249,
7.5043616886572));
#387532=CARTESIAN_POINT('Ctrl Pts',(2.74484549608077,0.127954369957362,
7.50217374673251));
#387533=CARTESIAN_POINT('',(2.74339586931974,0.127106646312639,7.50366116523517));
#387534=CARTESIAN_POINT('Ctrl Pts',(2.73995014666366,0.134807295823118,
7.51860402984325));
#387535=CARTESIAN_POINT('Ctrl Pts',(2.74033106457816,0.135030728157842,
7.51734760759494));
#387536=CARTESIAN_POINT('Ctrl Pts',(2.74070538067591,0.135181311420322,
7.51608817408573));
#387537=CARTESIAN_POINT('Ctrl Pts',(2.74107721787159,0.135246310518477,
7.5148100591312));
#387538=CARTESIAN_POINT('Ctrl Pts',(2.74141403688878,0.13530518825479,7.51365231206384));
#387539=CARTESIAN_POINT('Ctrl Pts',(2.74174925362168,0.135294172160199,
7.51247773061043));
#387540=CARTESIAN_POINT('Ctrl Pts',(2.74207585482037,0.135176547737615,
7.51129758471022));
#387541=CARTESIAN_POINT('Ctrl Pts',(2.74248178281107,0.135030354013559,
7.50983079813402));
#387542=CARTESIAN_POINT('Ctrl Pts',(2.74285703348899,0.134711887061916,
7.50839324291155));
#387543=CARTESIAN_POINT('Ctrl Pts',(2.7431510019548,0.134155967632647,7.50715379678855));
#387544=CARTESIAN_POINT('Ctrl Pts',(2.7432868069155,0.133899148874757,7.50658120839351));
#387545=CARTESIAN_POINT('Ctrl Pts',(2.7434161711015,0.13355070281472,7.50598221009429));
#387546=CARTESIAN_POINT('Ctrl Pts',(2.74351469152097,0.133111005108007,
7.50545747549611));
#387547=CARTESIAN_POINT('Ctrl Pts',(2.74356726506629,0.132876368801788,
7.50517746087247));
#387548=CARTESIAN_POINT('Ctrl Pts',(2.74361182316454,0.132613247474295,
7.50491486231392));
#387549=CARTESIAN_POINT('Ctrl Pts',(2.74364554124075,0.132328330517735,
7.50468370960993));
#387550=CARTESIAN_POINT('Ctrl Pts',(2.74369596040046,0.131902289795719,
7.50433806340447));
#387551=CARTESIAN_POINT('Ctrl Pts',(2.74372310067401,0.131414673971269,
7.50405484070984));
#387552=CARTESIAN_POINT('Ctrl Pts',(2.74372441892651,0.130898283251197,
7.50385766036131));
#387553=CARTESIAN_POINT('Ctrl Pts',(2.74372455989312,0.130843063290216,
7.50383657498791));
#387554=CARTESIAN_POINT('Ctrl Pts',(2.74372441994641,0.13078753874661,7.50381643264937));
#387555=CARTESIAN_POINT('Ctrl Pts',(2.74372400668667,0.130731767333936,
7.50379723213559));
#387556=CARTESIAN_POINT('Ctrl Pts',(2.74372124804273,0.130359474910222,
7.50366906242519));
#387557=CARTESIAN_POINT('Ctrl Pts',(2.74370553153518,0.129968089106795,
7.50358235568538));
#387558=CARTESIAN_POINT('Ctrl Pts',(2.74368131449704,0.129591205506861,
7.5035341175365));
#387559=CARTESIAN_POINT('Ctrl Pts',(2.74364500378917,0.129026111203748,
7.50346178989176));
#387560=CARTESIAN_POINT('Ctrl Pts',(2.74358191457385,0.128419742215759,
7.50346967198527));
#387561=CARTESIAN_POINT('Ctrl Pts',(2.74350166414417,0.127826381449622,
7.50354272648692));
#387562=CARTESIAN_POINT('Ctrl Pts',(2.74346865548136,0.127582319884669,
7.50357277531559));
#387563=CARTESIAN_POINT('Ctrl Pts',(2.74343292777869,0.127340764385223,
7.50361331098761));
#387564=CARTESIAN_POINT('Ctrl Pts',(2.74339586932116,0.127106646312705,
7.50366116523659));
#387565=CARTESIAN_POINT('',(2.67259277500765,0.0857048484080739,7.57603338622103));
#387566=CARTESIAN_POINT('Origin',(2.68142526464665,0.0859852345169799,7.58486873427628));
#387567=CARTESIAN_POINT('Ctrl Pts',(2.74339586936632,0.127106646346087,
7.50366116529969));
#387568=CARTESIAN_POINT('Ctrl Pts',(2.71983377186153,0.113327845238031,
7.52783573079709));
#387569=CARTESIAN_POINT('Ctrl Pts',(2.69623386379653,0.099527882063393,
7.55196141284069));
#387570=CARTESIAN_POINT('Ctrl Pts',(2.67259277586597,0.0857048493196314,
7.57603338728831));
#387571=CARTESIAN_POINT('Ctrl Pts',(2.66716398335868,0.0919097993917303,
7.59639677331369));
#387572=CARTESIAN_POINT('Ctrl Pts',(2.65013468741495,0.0852708992241862,
7.59959882295478));
#387573=CARTESIAN_POINT('Ctrl Pts',(2.66740089544003,0.0792221908444998,
7.59642833564546));
#387574=CARTESIAN_POINT('Ctrl Pts',(2.66334925645134,0.0910955741732249,
7.58707626057418));
#387575=CARTESIAN_POINT('Ctrl Pts',(2.65969712411285,0.0853881911985396,
7.588099439206));
#387576=CARTESIAN_POINT('Ctrl Pts',(2.66361108188368,0.0798749947243845,
7.58710240504253));
#387577=CARTESIAN_POINT('Ctrl Pts',(2.66840548835475,0.0877250918336626,
7.58015376756928));
#387578=CARTESIAN_POINT('Ctrl Pts',(2.66656942050619,0.0855437788684957,
7.58205880659763));
#387579=CARTESIAN_POINT('Ctrl Pts',(2.66848607277801,0.0834813727234763,
7.58020924244124));
#387580=CARTESIAN_POINT('Ctrl Pts',(2.6725927741805,0.0857048483817501,
7.57603338509286));
#387581=CARTESIAN_POINT('Ctrl Pts',(2.6725927741805,0.0857048483817501,
7.57603338509286));
#387582=CARTESIAN_POINT('Ctrl Pts',(2.6725927741805,0.0857048483817501,
7.57603338509286));
#387583=CARTESIAN_POINT('Origin',(2.68142508174979,0.0859909379372544,7.58486873427624));
#387584=CARTESIAN_POINT('Ctrl Pts',(2.75064512934104,0.0371490404859579,
7.51098857897448));
#387585=CARTESIAN_POINT('Ctrl Pts',(2.74538653035493,0.0397962368661161,
7.50433767179956));
#387586=CARTESIAN_POINT('Ctrl Pts',(2.74742820050471,0.048159228799746,
7.50214974420965));
#387587=CARTESIAN_POINT('Ctrl Pts',(2.72250792447727,0.0513134038572373,
7.5388732158917));
#387588=CARTESIAN_POINT('Ctrl Pts',(2.71731233283935,0.0539288821268522,
7.53220407452064));
#387589=CARTESIAN_POINT('Ctrl Pts',(2.71929181910785,0.0622766096041079,
7.53003438070911));
#387590=CARTESIAN_POINT('Ctrl Pts',(2.69431668580073,0.065504968031232,
7.56669465659231));
#387591=CARTESIAN_POINT('Ctrl Pts',(2.68915179914344,0.0681049893104947,
7.560040858333));
#387592=CARTESIAN_POINT('Ctrl Pts',(2.69110180456681,0.0764196828692079,
7.55785582193789));
#387593=CARTESIAN_POINT('Ctrl Pts',(2.6660726882884,0.0797230911802505,
7.59443891967696));
#387594=CARTESIAN_POINT('Ctrl Pts',(2.6609003131885,0.0823268821666794,
7.58783901202978));
#387595=CARTESIAN_POINT('Ctrl Pts',(2.66285951196075,0.0905876762059419,
7.58560008491213));
#387596=CARTESIAN_POINT('',(2.7459030190682,0.0489244847659116,7.50366116523517));
#387597=CARTESIAN_POINT('Ctrl Pts',(2.74590301906857,0.0489244847659182,
7.50366116523554));
#387598=CARTESIAN_POINT('Ctrl Pts',(2.7460690228415,0.0481851740977019,
7.50350835821027));
#387599=CARTESIAN_POINT('Ctrl Pts',(2.74619756789807,0.047500167397315,
7.50345484956));
#387600=CARTESIAN_POINT('Ctrl Pts',(2.74629306618699,0.04684920961282,7.50349758195598));
#387601=CARTESIAN_POINT('Ctrl Pts',(2.74634206389154,0.0465152199930862,
7.50351950684424));
#387602=CARTESIAN_POINT('Ctrl Pts',(2.74638731968128,0.0461572930119301,
7.50357029184312));
#387603=CARTESIAN_POINT('Ctrl Pts',(2.74642147197328,0.0458109485708934,
7.50365515313923));
#387604=CARTESIAN_POINT('Ctrl Pts',(2.74647401202802,0.045278130571864,
7.50378570417639));
#387605=CARTESIAN_POINT('Ctrl Pts',(2.74650216125901,0.044757118576261,
7.50400001621911));
#387606=CARTESIAN_POINT('Ctrl Pts',(2.74650150999234,0.0442874466757047,
7.50428903009635));
#387607=CARTESIAN_POINT('Ctrl Pts',(2.74650143770675,0.0442353167081828,
7.50432110841318));
#387608=CARTESIAN_POINT('Ctrl Pts',(2.74650102779312,0.0441837942326017,
7.50435406373354));
#387609=CARTESIAN_POINT('Ctrl Pts',(2.7465002866472,0.0441329146943328,
7.50438785222352));
#387610=CARTESIAN_POINT('Ctrl Pts',(2.7464957615951,0.0438222706573802,
7.50459414719561));
#387611=CARTESIAN_POINT('Ctrl Pts',(2.7464783014936,0.043530655069155,7.50483629897752));
#387612=CARTESIAN_POINT('Ctrl Pts',(2.74644988891295,0.0432691609821475,
7.5050991045531));
#387613=CARTESIAN_POINT('Ctrl Pts',(2.74638720790626,0.0426922787616146,
7.50567888004914));
#387614=CARTESIAN_POINT('Ctrl Pts',(2.74626926975364,0.0422392055908945,
7.50637912803144));
#387615=CARTESIAN_POINT('Ctrl Pts',(2.74612291728795,0.041894615652552,
7.50710440483569));
#387616=CARTESIAN_POINT('Ctrl Pts',(2.74608702875786,0.0418101153586019,
7.50728225710685));
#387617=CARTESIAN_POINT('Ctrl Pts',(2.7460488514999,0.0417303992646909,
7.50746498566954));
#387618=CARTESIAN_POINT('Ctrl Pts',(2.74600965242202,0.0416571482609263,
7.50764697238949));
#387619=CARTESIAN_POINT('Ctrl Pts',(2.74579892896725,0.0412633710239055,
7.50862528291182));
#387620=CARTESIAN_POINT('Ctrl Pts',(2.74554319689632,0.041018725610885,
7.50965856837422));
#387621=CARTESIAN_POINT('Ctrl Pts',(2.7452737271665,0.0408647524369028,
7.51067959873204));
#387622=CARTESIAN_POINT('Ctrl Pts',(2.74512543763429,0.0407800208050494,
7.51124147302579));
#387623=CARTESIAN_POINT('Ctrl Pts',(2.74497273620065,0.0407231040803606,
7.51180065547253));
#387624=CARTESIAN_POINT('Ctrl Pts',(2.74481957364794,0.0406866658581097,
7.51235175716501));
#387625=CARTESIAN_POINT('Ctrl Pts',(2.74429033601557,0.0405607572849682,
7.51425603304535));
#387626=CARTESIAN_POINT('Ctrl Pts',(2.74369108744894,0.0406702451064588,
7.51626900505179));
#387627=CARTESIAN_POINT('Ctrl Pts',(2.74306043709656,0.0409687396572797,
7.51827788969242));
#387628=CARTESIAN_POINT('Ctrl Pts',(2.74302630510772,0.0409848947464477,
7.51838661432544));
#387629=CARTESIAN_POINT('Ctrl Pts',(2.74299207720045,0.0410016126210851,
7.51849533314856));
#387630=CARTESIAN_POINT('Ctrl Pts',(2.742957758327,0.0410188888571731,7.51860402984325));
#387631=CARTESIAN_POINT('Ctrl Pts',(2.67259277592381,0.0857048475531805,
7.57603338728985));
#387632=CARTESIAN_POINT('Ctrl Pts',(2.69707093545794,0.0734249054142994,
7.55196141284922));
#387633=CARTESIAN_POINT('Ctrl Pts',(2.7215065216773,0.0611653470353345,
7.52783573083105));
#387634=CARTESIAN_POINT('Ctrl Pts',(2.74590301911844,0.048924484734626,
7.50366116530176));
#387635=CARTESIAN_POINT('Origin',(9.235043459901E-16,2.96149868837505E-17,
7.49482233047033));
#387636=CARTESIAN_POINT('Origin',(2.73456650621404,0.126697565455592,7.49482233047033));
#387637=CARTESIAN_POINT('Origin',(0.,0.,7.50366116523517));
#387638=CARTESIAN_POINT('Origin',(2.73706558693544,0.0487670258859925,7.49482233047033));
#387639=CARTESIAN_POINT('Ctrl Pts',(2.73994923428965,0.134806760710208,
7.51860402984325));
#387640=CARTESIAN_POINT('Ctrl Pts',(2.74651277539354,0.138655944286965,
7.51860402984325));
#387641=CARTESIAN_POINT('Ctrl Pts',(2.74610810557233,0.146254136727663,
7.51860402984325));
#387642=CARTESIAN_POINT('Ctrl Pts',(2.74238632125063,0.136235989936594,
7.51041458714366));
#387643=CARTESIAN_POINT('Ctrl Pts',(2.74641689459242,0.140456042578031,
7.51004642900443));
#387644=CARTESIAN_POINT('Ctrl Pts',(2.7461079939692,0.146256232218917,7.5072913648301));
#387645=CARTESIAN_POINT('Ctrl Pts',(2.74456054006896,0.134448111381071,
7.50215815450137));
#387646=CARTESIAN_POINT('Ctrl Pts',(2.74661225767011,0.136790870303093,
7.4987716367153));
#387647=CARTESIAN_POINT('Ctrl Pts',(2.74645259066989,0.140237380138185,
7.49481588533171));
#387648=CARTESIAN_POINT('Ctrl Pts',(2.74339531939167,0.127106620832972,
7.50366171572174));
#387649=CARTESIAN_POINT('Ctrl Pts',(2.74705311126526,0.12727609315135,7.50000045605858));
#387650=CARTESIAN_POINT('Ctrl Pts',(2.74705311126525,0.127276093151474,
7.49482233047317));
#387651=CARTESIAN_POINT('Origin',(2.73362579600155,0.145589345197082,7.51860402984325));
#387652=CARTESIAN_POINT('Origin',(2.73362579600155,0.145589345197082,9.));
#387653=CARTESIAN_POINT('Origin',(2.73362579600155,0.145589345197082,8.75721825406948));
#387654=CARTESIAN_POINT('Ctrl Pts',(2.72554517444904,0.126357907884526,
8.78942910404912));
#387655=CARTESIAN_POINT('Ctrl Pts',(2.73036197956352,0.129159838859895,
8.79672699501691));
#387656=CARTESIAN_POINT('Ctrl Pts',(2.72736704093116,0.137568395725993,
8.79893251111267));
#387657=CARTESIAN_POINT('Ctrl Pts',(2.73502849441794,0.131920466747849,
8.78111911759583));
#387658=CARTESIAN_POINT('Ctrl Pts',(2.74073512981015,0.135248622787749,
8.78644465894813));
#387659=CARTESIAN_POINT('Ctrl Pts',(2.73971623505555,0.143290846687543,
8.78817647674132));
#387660=CARTESIAN_POINT('Ctrl Pts',(2.74093872560499,0.13538718613847,8.76780923932031));
#387661=CARTESIAN_POINT('Ctrl Pts',(2.7476726005194,0.139320335691617,8.76988516158374));
#387662=CARTESIAN_POINT('Ctrl Pts',(2.74742463217173,0.146875128348925,
8.77093053738832));
#387663=CARTESIAN_POINT('Ctrl Pts',(2.73978631140984,0.134711223304185,
8.75371302330492));
#387664=CARTESIAN_POINT('Ctrl Pts',(2.7463553003912,0.138547182783965,8.75300828287559));
#387665=CARTESIAN_POINT('Ctrl Pts',(2.74592098874475,0.146176462745271,
8.75267964240738));
#387666=CARTESIAN_POINT('Origin',(2.7215304230328,0.138494647576042,8.78727029226991));
#387667=CARTESIAN_POINT('Ctrl Pts',(2.66618796128141,0.0915411309428337,
8.85049129520029));
#387668=CARTESIAN_POINT('Ctrl Pts',(2.67122500331725,0.0944956731666353,
8.85711686593484));
#387669=CARTESIAN_POINT('Ctrl Pts',(2.66869591238441,0.102662953079024,
8.85933012996512));
#387670=CARTESIAN_POINT('Ctrl Pts',(2.68677347260705,0.103615829144148,
8.82945683644723));
#387671=CARTESIAN_POINT('Ctrl Pts',(2.69185232513725,0.106594895854754,
8.83607469902389));
#387672=CARTESIAN_POINT('Ctrl Pts',(2.68927998471671,0.114775061333436,
8.83829567148519));
#387673=CARTESIAN_POINT('Ctrl Pts',(2.70732829956803,0.115672529034086,
8.80838214965002));
#387674=CARTESIAN_POINT('Ctrl Pts',(2.71242719562162,0.118663352532845,
8.81501364461993));
#387675=CARTESIAN_POINT('Ctrl Pts',(2.70983317111897,0.126868219958632,
8.81722098428721));
#387676=CARTESIAN_POINT('Ctrl Pts',(2.72785477369492,0.127712598202077,
8.78727029226991));
#387677=CARTESIAN_POINT('Ctrl Pts',(2.73295451669185,0.130703918486436,
8.79393457792714));
#387678=CARTESIAN_POINT('Ctrl Pts',(2.7303578352728,0.138943861495108,8.79610912703474));
#387679=CARTESIAN_POINT('Origin',(2.65986361061929,0.102323180316798,8.85049129520029));
#387680=CARTESIAN_POINT('Ctrl Pts',(2.66657505256398,0.0794701993177319,
8.85049129520029));
#387681=CARTESIAN_POINT('Ctrl Pts',(2.67179104362696,0.0768444519090915,
8.85711686593484));
#387682=CARTESIAN_POINT('Ctrl Pts',(2.66979042840331,0.0685319131368021,
8.85933012996512));
#387683=CARTESIAN_POINT('Ctrl Pts',(2.66196054056419,0.0817931601470906,
8.86332496987232));
#387684=CARTESIAN_POINT('Ctrl Pts',(2.66239050079878,0.07719239623515,8.86648636486738));
#387685=CARTESIAN_POINT('Ctrl Pts',(2.65688884651666,0.0750457937910984,
8.87206031107456));
#387686=CARTESIAN_POINT('Ctrl Pts',(2.66170148162992,0.0889095282140474,
8.86341338519875));
#387687=CARTESIAN_POINT('Ctrl Pts',(2.66180657158416,0.0935422840608315,
8.86654584966058));
#387688=CARTESIAN_POINT('Ctrl Pts',(2.65614098496653,0.0952816175726944,
8.87215952290715));
#387689=CARTESIAN_POINT('Ctrl Pts',(2.66618796128141,0.0915411309428336,
8.85049129520029));
#387690=CARTESIAN_POINT('Ctrl Pts',(2.67122500331725,0.0944956731666351,
8.85711686593484));
#387691=CARTESIAN_POINT('Ctrl Pts',(2.66869591238441,0.102662953079024,
8.85933012996512));
#387692=CARTESIAN_POINT('Origin',(2.66095450423382,0.0683051002824203,8.85049129520029));
#387693=CARTESIAN_POINT('Ctrl Pts',(2.73043267776197,0.0473240564541944,
8.78727029226991));
#387694=CARTESIAN_POINT('Ctrl Pts',(2.73571359733862,0.0446656238138374,
8.79393457792714));
#387695=CARTESIAN_POINT('Ctrl Pts',(2.73365018604124,0.0362762407020694,
8.79610912703474));
#387696=CARTESIAN_POINT('Ctrl Pts',(2.70917696759746,0.05802425229605,8.80838214965003));
#387697=CARTESIAN_POINT('Ctrl Pts',(2.7144570101417,0.0553662611567555,
8.81501364461989));
#387698=CARTESIAN_POINT('Ctrl Pts',(2.71239400300152,0.0470120517905135,
8.81722098428721));
#387699=CARTESIAN_POINT('Ctrl Pts',(2.68789189731877,0.0687392281179318,
8.82945683644722));
#387700=CARTESIAN_POINT('Ctrl Pts',(2.69315118426123,0.0660916854182478,
8.83607469902389));
#387701=CARTESIAN_POINT('Ctrl Pts',(2.69110823399166,0.0577635165502676,
8.83829567148519));
#387702=CARTESIAN_POINT('Ctrl Pts',(2.66657505256398,0.0794701993177318,
8.85049129520029));
#387703=CARTESIAN_POINT('Ctrl Pts',(2.67179104362696,0.0768444519090914,
8.85711686593484));
#387704=CARTESIAN_POINT('Ctrl Pts',(2.66979042840331,0.0685319131368021,
8.85933012996512));
#387705=CARTESIAN_POINT('Origin',(2.72481212943181,0.0361589574188829,8.78727029226991));
#387706=CARTESIAN_POINT('Ctrl Pts',(2.74279236264415,0.0411021289464723,
8.75374538247848));
#387707=CARTESIAN_POINT('Ctrl Pts',(2.74958571518574,0.0376970240092931,
8.75304829418602));
#387708=CARTESIAN_POINT('Ctrl Pts',(2.74964669889166,0.0300637465875896,
8.75272238421917));
#387709=CARTESIAN_POINT('Ctrl Pts',(2.74397138271649,0.0405086067622311,
8.7676940844502));
#387710=CARTESIAN_POINT('Ctrl Pts',(2.75093537691271,0.0370171973323222,
8.76974318093968));
#387711=CARTESIAN_POINT('Ctrl Pts',(2.75117499675544,0.0294699501778223,
8.7707786988043));
#387712=CARTESIAN_POINT('Ctrl Pts',(2.73792839747585,0.043550663384532,
8.78108014887989));
#387713=CARTESIAN_POINT('Ctrl Pts',(2.74383183450135,0.0405952161110573,
8.78639403366326));
#387714=CARTESIAN_POINT('Ctrl Pts',(2.74335079698391,0.0325149513483312,
8.78812224174741));
#387715=CARTESIAN_POINT('Ctrl Pts',(2.72802527865339,0.0485359226161603,
8.78944554828685));
#387716=CARTESIAN_POINT('Ctrl Pts',(2.73300298241106,0.0460501867255351,
8.79673892988686));
#387717=CARTESIAN_POINT('Ctrl Pts',(2.73055804701899,0.0374754654329649,
8.79894799272499));
#387718=CARTESIAN_POINT('Origin',(2.73733720999684,0.0298537898218656,8.75721825406948));
#387719=CARTESIAN_POINT('Origin',(2.73733720999684,0.0298537898218656,9.));
#387720=CARTESIAN_POINT('Origin',(2.73733720999684,0.0298537898218657,7.51860402984325));
#387721=CARTESIAN_POINT('Ctrl Pts',(2.74590223252928,0.0489244707518819,
7.50366195182966));
#387722=CARTESIAN_POINT('Ctrl Pts',(2.74956360331414,0.0489897063693508,
7.50000065167735));
#387723=CARTESIAN_POINT('Ctrl Pts',(2.74956360331415,0.0489897063692339,
7.49482233047108));
#387724=CARTESIAN_POINT('Ctrl Pts',(2.74753601636502,0.0416660583920878,
7.50215800491338));
#387725=CARTESIAN_POINT('Ctrl Pts',(2.74973341113686,0.0394578569992938,
7.49877273257265));
#387726=CARTESIAN_POINT('Ctrl Pts',(2.74979493244485,0.0360062817823014,
7.49481816995647));
#387727=CARTESIAN_POINT('Ctrl Pts',(2.7454754935513,0.0397518321577599,
7.51043025814042));
#387728=CARTESIAN_POINT('Ctrl Pts',(2.74977310304522,0.0357991989057975,
7.51006209594515));
#387729=CARTESIAN_POINT('Ctrl Pts',(2.74983649427474,0.0299875767816046,
7.507312818217));
#387730=CARTESIAN_POINT('Ctrl Pts',(2.74295640828482,0.0410195683706412,
7.51860402984326));
#387731=CARTESIAN_POINT('Ctrl Pts',(2.7497534837955,0.0375989278030361,
7.51860402984326));
#387732=CARTESIAN_POINT('Ctrl Pts',(2.74983646666349,0.0299901084968461,
7.51860402984327));
#387733=CARTESIAN_POINT('Origin',(0.,0.,7.5));
#387734=CARTESIAN_POINT('Origin',(2.66618796128141,-0.0915411309427755,
7.5));
#387735=CARTESIAN_POINT('',(2.66618796128141,-0.0915411309427755,7.59394543036555));
#387736=CARTESIAN_POINT('',(2.66618796128141,-0.0915411309427755,8.85049129520029));
#387737=CARTESIAN_POINT('',(2.66618796128141,-0.0915411309427755,7.5));
#387738=CARTESIAN_POINT('',(2.72785477369492,-0.127712598202018,8.78727029226991));
#387739=CARTESIAN_POINT('Ctrl Pts',(2.66618796128141,-0.0915411309427756,
8.85049129520029));
#387740=CARTESIAN_POINT('Ctrl Pts',(2.68677344498056,-0.103615812939416,
8.82945686509571));
#387741=CARTESIAN_POINT('Ctrl Pts',(2.70732832586904,-0.115672544461219,
8.80838212259896));
#387742=CARTESIAN_POINT('Ctrl Pts',(2.72785477369492,-0.127712598202018,
8.78727029226991));
#387743=CARTESIAN_POINT('',(2.73995014666367,-0.134807295823058,8.75721825406948));
#387744=CARTESIAN_POINT('Origin',(2.70355107558665,-0.113456715445245,8.75937679713058));
#387745=CARTESIAN_POINT('',(2.73995014666367,-0.134807295823058,7.51860402984325));
#387746=CARTESIAN_POINT('',(2.73995014666367,-0.134807295823058,7.5));
#387747=CARTESIAN_POINT('Ctrl Pts',(2.73995014666367,-0.134807295823058,
7.51860402984325));
#387748=CARTESIAN_POINT('Ctrl Pts',(2.73045111238304,-0.129235514275926,
7.52834476460825));
#387749=CARTESIAN_POINT('Ctrl Pts',(2.72094591146644,-0.123660115608609,
7.53807742314407));
#387750=CARTESIAN_POINT('Ctrl Pts',(2.71143433686084,-0.118080978371492,
7.54780169004674));
#387751=CARTESIAN_POINT('Ctrl Pts',(2.69636851674231,-0.109243926514539,
7.5632044032688));
#387752=CARTESIAN_POINT('Ctrl Pts',(2.68128668670343,-0.100397483831532,
7.57858609112103));
#387753=CARTESIAN_POINT('Ctrl Pts',(2.66618796128141,-0.0915411309427754,
7.59394543036555));
#387754=CARTESIAN_POINT('Origin',(2.91220723134083,0.0441818639458939,7.5));
#387755=CARTESIAN_POINT('',(2.742957758327,-0.0410188888571173,8.75721825406948));
#387756=CARTESIAN_POINT('',(2.73043267776197,-0.047324056454135,8.78727029226991));
#387757=CARTESIAN_POINT('Origin',(2.69863935166543,-0.0633289235258057,
8.75658640621032));
#387758=CARTESIAN_POINT('',(2.66657505256398,-0.0794701993176737,8.85049129520029));
#387759=CARTESIAN_POINT('Ctrl Pts',(2.73043267776197,-0.0473240564541348,
8.78727029226991));
#387760=CARTESIAN_POINT('Ctrl Pts',(2.70917699483285,-0.0580242385856055,
8.80838212259896));
#387761=CARTESIAN_POINT('Ctrl Pts',(2.68789186871081,-0.0687392425192154,
8.82945686509571));
#387762=CARTESIAN_POINT('Ctrl Pts',(2.66657505256398,-0.0794701993176736,
8.85049129520029));
#387763=CARTESIAN_POINT('',(2.66657505256398,-0.0794701993176737,7.59394543036555));
#387764=CARTESIAN_POINT('',(2.66657505256398,-0.0794701993176737,7.5));
#387765=CARTESIAN_POINT('',(2.742957758327,-0.0410188888571173,7.51860402984325));
#387766=CARTESIAN_POINT('Ctrl Pts',(2.66657505256398,-0.0794701993176739,
7.59394543036555));
#387767=CARTESIAN_POINT('Ctrl Pts',(2.68221018451309,-0.0715994214149867,
7.57858609112103));
#387768=CARTESIAN_POINT('Ctrl Pts',(2.6978278208432,-0.0637374508656468,
7.56320440326857));
#387769=CARTESIAN_POINT('Ctrl Pts',(2.71342887847495,-0.0558838260886891,
7.54780169004651));
#387770=CARTESIAN_POINT('Ctrl Pts',(2.72327836708049,-0.0509255604647293,
7.53807742314383));
#387771=CARTESIAN_POINT('Ctrl Pts',(2.73312125556166,-0.0459706173655272,
7.52834476460825));
#387772=CARTESIAN_POINT('Ctrl Pts',(2.742957758327,-0.0410188888571183,
7.51860402984325));
#387773=CARTESIAN_POINT('',(2.742957758327,-0.0410188888571173,7.5));
#387774=CARTESIAN_POINT('Origin',(2.66966635414557,-0.0856110037870949,
7.5));
#387775=CARTESIAN_POINT('Ctrl Pts',(2.66657505256398,-0.0794701993176738,
8.85049129520029));
#387776=CARTESIAN_POINT('Ctrl Pts',(2.66640207257255,-0.079557278025969,
8.85097269580138));
#387777=CARTESIAN_POINT('Ctrl Pts',(2.66623505718387,-0.0796507712154674,
8.85143669361005));
#387778=CARTESIAN_POINT('Ctrl Pts',(2.66606674293477,-0.079755746833782,
8.8519052845931));
#387779=CARTESIAN_POINT('Ctrl Pts',(2.66573753093763,-0.0799610724858936,
8.85282181883899));
#387780=CARTESIAN_POINT('Ctrl Pts',(2.66541192289281,-0.0802052114460414,
8.85372622499636));
#387781=CARTESIAN_POINT('Ctrl Pts',(2.66509405906801,-0.0805043308840431,
8.85462257735071));
#387782=CARTESIAN_POINT('Ctrl Pts',(2.66483017981012,-0.0807526492177544,
8.85536669723986));
#387783=CARTESIAN_POINT('Ctrl Pts',(2.66457155583132,-0.0810388922212037,
8.85610498449051));
#387784=CARTESIAN_POINT('Ctrl Pts',(2.66432647183546,-0.0813776989231866,
8.85681338218371));
#387785=CARTESIAN_POINT('Ctrl Pts',(2.66410405772431,-0.0816851665373423,
8.85745625420284));
#387786=CARTESIAN_POINT('Ctrl Pts',(2.66388951971436,-0.0820394295508348,
8.85808743050666));
#387787=CARTESIAN_POINT('Ctrl Pts',(2.66369852795532,-0.0824644106005847,
8.85866804508411));
#387788=CARTESIAN_POINT('Ctrl Pts',(2.6636104084979,-0.0826604876444791,
8.85893592806396));
#387789=CARTESIAN_POINT('Ctrl Pts',(2.66352745737671,-0.0828718038816539,
8.85919241173848));
#387790=CARTESIAN_POINT('Ctrl Pts',(2.66345240175596,-0.083101774652802,
8.85943017985534));
#387791=CARTESIAN_POINT('Ctrl Pts',(2.6633510544491,-0.0834123032724869,
8.8597512372));
#387792=CARTESIAN_POINT('Ctrl Pts',(2.66326213239103,-0.0837649471947781,
8.86004599534705));
#387793=CARTESIAN_POINT('Ctrl Pts',(2.66319680292198,-0.0841580160749788,
8.86026130871721));
#387794=CARTESIAN_POINT('Ctrl Pts',(2.66317288396152,-0.0843019296738054,
8.86034014101235));
#387795=CARTESIAN_POINT('Ctrl Pts',(2.66315175613712,-0.0844534219507867,
8.86040910639693));
#387796=CARTESIAN_POINT('Ctrl Pts',(2.66313432821879,-0.084608412047141,
8.86046313645507));
#387797=CARTESIAN_POINT('Ctrl Pts',(2.66310713209819,-0.0848502727944706,
8.8605474499083));
#387798=CARTESIAN_POINT('Ctrl Pts',(2.66308834949246,-0.0851072697018491,
8.86059655985668));
#387799=CARTESIAN_POINT('Ctrl Pts',(2.66307889280913,-0.0853628994213819,
8.86059725258815));
#387800=CARTESIAN_POINT('Ctrl Pts',(2.66306941427709,-0.0856191197476916,
8.86059794692011));
#387801=CARTESIAN_POINT('Ctrl Pts',(2.66307185464675,-0.0858769062894076,
8.86056369958366));
#387802=CARTESIAN_POINT('Ctrl Pts',(2.66308231788918,-0.0861222348656741,
8.86048590497774));
#387803=CARTESIAN_POINT('Ctrl Pts',(2.66308504848392,-0.0861862583197678,
8.86046560290182));
#387804=CARTESIAN_POINT('Ctrl Pts',(2.66308845150025,-0.0862502623673478,
8.86044257503091));
#387805=CARTESIAN_POINT('Ctrl Pts',(2.66309238900225,-0.0863122709732237,
8.86041778462583));
#387806=CARTESIAN_POINT('Ctrl Pts',(2.66311888350473,-0.0867295119445019,
8.860250975962));
#387807=CARTESIAN_POINT('Ctrl Pts',(2.66317346391551,-0.0871123740750049,
8.8599848982295));
#387808=CARTESIAN_POINT('Ctrl Pts',(2.66324614948998,-0.0874508783644821,
8.85968173251461));
#387809=CARTESIAN_POINT('Ctrl Pts',(2.66328459599449,-0.087629927739632,
8.85952137522076));
#387810=CARTESIAN_POINT('Ctrl Pts',(2.66332866234873,-0.0878000580576296,
8.85934740853961));
#387811=CARTESIAN_POINT('Ctrl Pts',(2.66337622222878,-0.0879592598946845,
8.8591675900182));
#387812=CARTESIAN_POINT('Ctrl Pts',(2.66356719986828,-0.0885985380219406,
8.85844552518694));
#387813=CARTESIAN_POINT('Ctrl Pts',(2.66382240283475,-0.0890985976181462,
8.85759444184121));
#387814=CARTESIAN_POINT('Ctrl Pts',(2.66406710350387,-0.0894876295423471,
8.85683498915134));
#387815=CARTESIAN_POINT('Ctrl Pts',(2.6640927107772,-0.0895283406971303,
8.85675551444995));
#387816=CARTESIAN_POINT('Ctrl Pts',(2.6641182175335,-0.0895678222452359,
8.8566769979365));
#387817=CARTESIAN_POINT('Ctrl Pts',(2.66414354718951,-0.0896060969792316,
8.85659965593547));
#387818=CARTESIAN_POINT('Ctrl Pts',(2.66448544817898,-0.0901227312918511,
8.85555568965886));
#387819=CARTESIAN_POINT('Ctrl Pts',(2.66488864842986,-0.0905698716063139,
8.85434650606346));
#387820=CARTESIAN_POINT('Ctrl Pts',(2.66535052573303,-0.0909538901841117,
8.85297329937117));
#387821=CARTESIAN_POINT('Ctrl Pts',(2.66561030357347,-0.0911698772355271,
8.85220095427747));
#387822=CARTESIAN_POINT('Ctrl Pts',(2.66588895075784,-0.0913657424487038,
8.85137579139183));
#387823=CARTESIAN_POINT('Ctrl Pts',(2.66618796128141,-0.0915411309427756,
8.85049129520029));
#387824=CARTESIAN_POINT('Origin',(2.66966635414557,-0.085611003787095,7.59394543036555));
#387825=CARTESIAN_POINT('Ctrl Pts',(2.66607283329461,-0.0797230181835804,
7.59443877723642));
#387826=CARTESIAN_POINT('Ctrl Pts',(2.6609004580425,-0.0823268092466323,
7.58783886950016));
#387827=CARTESIAN_POINT('Ctrl Pts',(2.6628596569582,-0.0905876034666415,
7.58559994247159));
#387828=CARTESIAN_POINT('Ctrl Pts',(2.69430867804487,-0.0655089991623543,
7.56670252222138));
#387829=CARTESIAN_POINT('Ctrl Pts',(2.68914377834347,-0.0681090270081297,
7.56004874999028));
#387830=CARTESIAN_POINT('Ctrl Pts',(2.69109379729576,-0.0764236997822774,
7.55786368756705));
#387831=CARTESIAN_POINT('Ctrl Pts',(2.72249179517612,-0.0513215234015166,
7.53888913333557));
#387832=CARTESIAN_POINT('Ctrl Pts',(2.71729620022289,-0.0539370033400398,
7.53222002137276));
#387833=CARTESIAN_POINT('Ctrl Pts',(2.71927569050806,-0.0622847014018507,
7.53005029815326));
#387834=CARTESIAN_POINT('Ctrl Pts',(2.75062090938332,-0.0371612328939121,
7.51101258149734));
#387835=CARTESIAN_POINT('Ctrl Pts',(2.74536233437864,-0.0398084172017366,
7.5043616886572));
#387836=CARTESIAN_POINT('Ctrl Pts',(2.74740398125597,-0.0481713807657444,
7.50217374673251));
#387837=CARTESIAN_POINT('',(2.7459030190682,-0.0489244847658516,7.50366116523517));
#387838=CARTESIAN_POINT('Ctrl Pts',(2.742957758327,-0.0410188888571166,
7.51860402984325));
#387839=CARTESIAN_POINT('Ctrl Pts',(2.74335220896362,-0.0408203210826641,
7.51734760759494));
#387840=CARTESIAN_POINT('Ctrl Pts',(2.74373540389156,-0.0406940297243718,
7.51608817408573));
#387841=CARTESIAN_POINT('Ctrl Pts',(2.74411064161436,-0.0406529878647593,
7.51481005913119));
#387842=CARTESIAN_POINT('Ctrl Pts',(2.74445054091028,-0.0406158111675953,
7.51365231206383));
#387843=CARTESIAN_POINT('Ctrl Pts',(2.74478436310084,-0.0406482820382562,
7.51247773061042));
#387844=CARTESIAN_POINT('Ctrl Pts',(2.74510275703971,-0.0407865901994944,
7.51129758471022));
#387845=CARTESIAN_POINT('Ctrl Pts',(2.74549848434376,-0.0409584914485253,
7.50983079813402));
#387846=CARTESIAN_POINT('Ctrl Pts',(2.74585255978126,-0.0413003464691425,
7.50839324291155));
#387847=CARTESIAN_POINT('Ctrl Pts',(2.7461103063772,-0.041873958326594,
7.50715379678855));
#387848=CARTESIAN_POINT('Ctrl Pts',(2.74622937787774,-0.042138950476508,
7.50658120839351));
#387849=CARTESIAN_POINT('Ctrl Pts',(2.74633615125543,-0.0424949690085999,
7.50598221009429));
#387850=CARTESIAN_POINT('Ctrl Pts',(2.74640629772533,-0.0429400755341653,
7.50545747549611));
#387851=CARTESIAN_POINT('Ctrl Pts',(2.74644373005291,-0.0431775981535425,
7.50517746087247));
#387852=CARTESIAN_POINT('Ctrl Pts',(2.74647133836043,-0.0434430337172053,
7.50491486231392));
#387853=CARTESIAN_POINT('Ctrl Pts',(2.74648673246716,-0.0437295256058809,
7.50468370960992));
#387854=CARTESIAN_POINT('Ctrl Pts',(2.74650975151252,-0.0441579213481969,
7.50433806340446));
#387855=CARTESIAN_POINT('Ctrl Pts',(2.74650559437033,-0.0446462741969396,
7.50405484070983));
#387856=CARTESIAN_POINT('Ctrl Pts',(2.7464738246473,-0.0451616883976252,
7.5038576603613));
#387857=CARTESIAN_POINT('Ctrl Pts',(2.74647042736924,-0.0452168039350331,
7.50383657498791));
#387858=CARTESIAN_POINT('Ctrl Pts',(2.74646673024033,-0.0452722054310887,
7.50381643264937));
#387859=CARTESIAN_POINT('Ctrl Pts',(2.746462744543,-0.0453278357777696,
7.50379723213559));
#387860=CARTESIAN_POINT('Ctrl Pts',(2.74643613870952,-0.0456991865398469,
7.50366906242519));
#387861=CARTESIAN_POINT('Ctrl Pts',(2.74639537831869,-0.0460887612390686,
7.50358235568538));
#387862=CARTESIAN_POINT('Ctrl Pts',(2.74634706402189,-0.0464633189002641,
7.5035341175365));
#387863=CARTESIAN_POINT('Ctrl Pts',(2.74627462220197,-0.0470249257214849,
7.50346178989177));
#387864=CARTESIAN_POINT('Ctrl Pts',(2.74617281241575,-0.0476260067194501,
7.50346967198527));
#387865=CARTESIAN_POINT('Ctrl Pts',(2.74605471011437,-0.0482130066995723,
7.50354272648693));
#387866=CARTESIAN_POINT('Ctrl Pts',(2.74600613219324,-0.0484544519415771,
7.50357277531559));
#387867=CARTESIAN_POINT('Ctrl Pts',(2.74595500138299,-0.048693222057574,
7.50361331098762));
#387868=CARTESIAN_POINT('Ctrl Pts',(2.74590301906962,-0.0489244847658769,
7.50366116523659));
#387869=CARTESIAN_POINT('',(2.67259277500764,-0.0857048484084028,7.57603338622103));
#387870=CARTESIAN_POINT('Origin',(2.68142508174926,-0.0859909379370269,
7.5848687342763));
#387871=CARTESIAN_POINT('Ctrl Pts',(2.74590301911683,-0.048924484735458,
7.50366116529969));
#387872=CARTESIAN_POINT('Ctrl Pts',(2.72150652165033,-0.0611653470485443,
7.52783573079709));
#387873=CARTESIAN_POINT('Ctrl Pts',(2.69707093545121,-0.0734249054175328,
7.55196141284069));
#387874=CARTESIAN_POINT('Ctrl Pts',(2.6725927759226,-0.0857048475537104,
7.57603338728831));
#387875=CARTESIAN_POINT('Ctrl Pts',(2.66757268996768,-0.0791648222868913,
7.59639677331372));
#387876=CARTESIAN_POINT('Ctrl Pts',(2.64933465654094,-0.0849590058181688,
7.59974925422226));
#387877=CARTESIAN_POINT('Ctrl Pts',(2.66716398335852,-0.0919097993916128,
7.59639677331371));
#387878=CARTESIAN_POINT('Ctrl Pts',(2.66371363323709,-0.0797329642003548,
7.58707626057423));
#387879=CARTESIAN_POINT('Ctrl Pts',(2.65963383141741,-0.0852892803103274,
7.58811717123965));
#387880=CARTESIAN_POINT('Ctrl Pts',(2.66334925645125,-0.0910955741730033,
7.58707626057423));
#387881=CARTESIAN_POINT('Ctrl Pts',(2.66854352902493,-0.083420475412555,
7.5801537675693));
#387882=CARTESIAN_POINT('Ctrl Pts',(2.66654166217443,-0.0855108009974158,
7.58208760766041));
#387883=CARTESIAN_POINT('Ctrl Pts',(2.66840548835473,-0.0877250918336702,
7.58015376756929));
#387884=CARTESIAN_POINT('Ctrl Pts',(2.6725927741805,-0.0857048483816766,
7.57603338509286));
#387885=CARTESIAN_POINT('Ctrl Pts',(2.6725927741805,-0.0857048483816766,
7.57603338509286));
#387886=CARTESIAN_POINT('Ctrl Pts',(2.6725927741805,-0.0857048483816766,
7.57603338509286));
#387887=CARTESIAN_POINT('Origin',(2.68142526464748,-0.0859852345167185,
7.5848687342762));
#387888=CARTESIAN_POINT('Ctrl Pts',(2.74737378111305,-0.139161724727701,
7.51098857897448));
#387889=CARTESIAN_POINT('Ctrl Pts',(2.74229559293695,-0.136183047702587,
7.50433767179956));
#387890=CARTESIAN_POINT('Ctrl Pts',(2.74486888698932,-0.127968048688437,
7.50214974420965));
#387891=CARTESIAN_POINT('Ctrl Pts',(2.72020190103146,-0.123223706654822,
7.53887321589169));
#387892=CARTESIAN_POINT('Ctrl Pts',(2.71518455856187,-0.120280719466635,
7.53220407452062));
#387893=CARTESIAN_POINT('Ctrl Pts',(2.71769481849935,-0.112076969411449,
7.53003438070911));
#387894=CARTESIAN_POINT('Ctrl Pts',(2.69297784091681,-0.107255081707945,
7.56669465659233));
#387895=CARTESIAN_POINT('Ctrl Pts',(2.68799015000838,-0.104329487026956,
7.560040858333));
#387896=CARTESIAN_POINT('Ctrl Pts',(2.69046887318185,-0.0961568141743312,
7.55785582193789));
#387897=CARTESIAN_POINT('Ctrl Pts',(2.66570283200437,-0.091256572084064,
7.59443891967696));
#387898=CARTESIAN_POINT('Ctrl Pts',(2.66070790956513,-0.088326735654999,
7.58783901202978));
#387899=CARTESIAN_POINT('Ctrl Pts',(2.6631923538447,-0.0802084405993816,
7.58560008491213));
#387900=CARTESIAN_POINT('',(2.74339586931974,-0.12710664631258,7.50366116523517));
#387901=CARTESIAN_POINT('Ctrl Pts',(2.74339586932012,-0.127106646312597,
7.50366116523554));
#387902=CARTESIAN_POINT('Ctrl Pts',(2.74351416422334,-0.127855073886004,
7.50350835821027));
#387903=CARTESIAN_POINT('Ctrl Pts',(2.74359855664032,-0.12854690907671,
7.50345484955999));
#387904=CARTESIAN_POINT('Ctrl Pts',(2.74365215170931,-0.129202647995,7.50349758195598));
#387905=CARTESIAN_POINT('Ctrl Pts',(2.74367964995442,-0.129539090690949,
7.50351950684424));
#387906=CARTESIAN_POINT('Ctrl Pts',(2.74370188030086,-0.129899181821139,
7.50357029184312));
#387907=CARTESIAN_POINT('Ctrl Pts',(2.7437137720588,-0.130247002805238,
7.50365515313923));
#387908=CARTESIAN_POINT('Ctrl Pts',(2.74373206639795,-0.130782092325406,
7.50378570417639));
#387909=CARTESIAN_POINT('Ctrl Pts',(2.74372677644015,-0.131303837373406,
7.50400001621911));
#387910=CARTESIAN_POINT('Ctrl Pts',(2.7436960345296,-0.13177250255587,7.50428903009634));
#387911=CARTESIAN_POINT('Ctrl Pts',(2.74369262241404,-0.131824520785431,
7.50432110841318));
#387912=CARTESIAN_POINT('Ctrl Pts',(2.74368891228627,-0.131875911139305,
7.50435406373354));
#387913=CARTESIAN_POINT('Ctrl Pts',(2.7436849127999,-0.131926638654725,
7.50438785222352));
#387914=CARTESIAN_POINT('Ctrl Pts',(2.74366049401323,-0.132236354519104,
7.50459414719561));
#387915=CARTESIAN_POINT('Ctrl Pts',(2.74362438591049,-0.132526252279283,
7.50483629897752));
#387916=CARTESIAN_POINT('Ctrl Pts',(2.74357927772286,-0.132785388698351,
7.5050991045531));
#387917=CARTESIAN_POINT('Ctrl Pts',(2.74347976453025,-0.133357069666604,
7.50567888004914));
#387918=CARTESIAN_POINT('Ctrl Pts',(2.7433330401965,-0.13380165562652,7.50637912803144));
#387919=CARTESIAN_POINT('Ctrl Pts',(2.74316491047449,-0.134136160733206,
7.50710440483569));
#387920=CARTESIAN_POINT('Ctrl Pts',(2.74312368172882,-0.134218188026222,
7.50728225710685));
#387921=CARTESIAN_POINT('Ctrl Pts',(2.74308047548245,-0.134295294309552,
7.50746498566954));
#387922=CARTESIAN_POINT('Ctrl Pts',(2.74303666373536,-0.134365883317731,
7.50764697238949));
#387923=CARTESIAN_POINT('Ctrl Pts',(2.74280114384032,-0.134745350399082,
7.50862528291182));
#387924=CARTESIAN_POINT('Ctrl Pts',(2.74253026271293,-0.134973108351822,
7.50965856837422));
#387925=CARTESIAN_POINT('Ctrl Pts',(2.74225148154245,-0.135109500186538,
7.51067959873203));
#387926=CARTESIAN_POINT('Ctrl Pts',(2.74209806791269,-0.135184556785218,
7.51124147302579));
#387927=CARTESIAN_POINT('Ctrl Pts',(2.74194203355346,-0.135231572953947,
7.51180065547253));
#387928=CARTESIAN_POINT('Ctrl Pts',(2.74178685108471,-0.135258123151517,
7.51235175716501));
#387929=CARTESIAN_POINT('Ctrl Pts',(2.74125063383784,-0.135349864660465,
7.51425603304536));
#387930=CARTESIAN_POINT('Ctrl Pts',(2.74065963140047,-0.135202207805959,
7.5162690050518));
#387931=CARTESIAN_POINT('Ctrl Pts',(2.74004940139841,-0.134863920637395,
7.51827788969243));
#387932=CARTESIAN_POINT('Ctrl Pts',(2.74001637459752,-0.134845611896558,
7.51838661432545));
#387933=CARTESIAN_POINT('Ctrl Pts',(2.73998328813306,-0.13482673538104,
7.51849533314857));
#387934=CARTESIAN_POINT('Ctrl Pts',(2.73995014666366,-0.134807295823061,
7.51860402984325));
#387935=CARTESIAN_POINT('Ctrl Pts',(2.67259277586714,-0.0857048493202394,
7.57603338728985));
#387936=CARTESIAN_POINT('Ctrl Pts',(2.69623386380305,-0.0995278820670532,
7.55196141284922));
#387937=CARTESIAN_POINT('Ctrl Pts',(2.71983377188761,-0.113327845252912,
7.52783573083104));
#387938=CARTESIAN_POINT('Ctrl Pts',(2.74339586936787,-0.127106646347019,
7.50366116530176));
#387939=CARTESIAN_POINT('Origin',(9.23504345990101E-16,-2.96149868837303E-17,
7.49482233047033));
#387940=CARTESIAN_POINT('Origin',(2.73706558693544,-0.0487670258859327,
7.49482233047033));
#387941=CARTESIAN_POINT('Origin',(0.,0.,7.50366116523517));
#387942=CARTESIAN_POINT('Origin',(2.73456650621404,-0.126697565455532,7.49482233047033));
#387943=CARTESIAN_POINT('Ctrl Pts',(2.74295681354276,-0.0410193644145763,
7.51860402984325));
#387944=CARTESIAN_POINT('Ctrl Pts',(2.74975348718602,-0.0375986169206801,
7.51860402984325));
#387945=CARTESIAN_POINT('Ctrl Pts',(2.74983646666349,-0.0299901084967906,
7.51860402984325));
#387946=CARTESIAN_POINT('Ctrl Pts',(2.74548046427813,-0.0397492163906277,
7.51041458714366));
#387947=CARTESIAN_POINT('Ctrl Pts',(2.74977313607578,-0.0357960740205906,
7.51004642900442));
#387948=CARTESIAN_POINT('Ctrl Pts',(2.74983648954825,-0.0299880101605093,
7.5072913648301));
#387949=CARTESIAN_POINT('Ctrl Pts',(2.74753566615837,-0.0416727242358742,
7.50215815450137));
#387950=CARTESIAN_POINT('Ctrl Pts',(2.74973326936515,-0.0394662327613699,
7.49877163671529));
#387951=CARTESIAN_POINT('Ctrl Pts',(2.74979474906121,-0.0360165742505425,
7.49481588533171));
#387952=CARTESIAN_POINT('Ctrl Pts',(2.74590246863753,-0.0489244749591564,
7.50366171572174));
#387953=CARTESIAN_POINT('Ctrl Pts',(2.74956360331413,-0.0489897063698166,
7.50000045605858));
#387954=CARTESIAN_POINT('Ctrl Pts',(2.74956360331414,-0.048989706369692,
7.49482233047317));
#387955=CARTESIAN_POINT('Origin',(2.73733720999684,-0.0298537898218058,
7.51860402984325));
#387956=CARTESIAN_POINT('Origin',(2.73733720999684,-0.0298537898218058,
9.));
#387957=CARTESIAN_POINT('Origin',(2.73733720999684,-0.0298537898218059,
8.75721825406948));
#387958=CARTESIAN_POINT('Ctrl Pts',(2.72804102852879,-0.0485279868833891,
8.78942910404912));
#387959=CARTESIAN_POINT('Ctrl Pts',(2.73302745733453,-0.0460404265390077,
8.79672699501691));
#387960=CARTESIAN_POINT('Ctrl Pts',(2.73057741021293,-0.0374572595777989,
8.79893251111267));
#387961=CARTESIAN_POINT('Ctrl Pts',(2.73786125836976,-0.0435844552903896,
8.78111911759582));
#387962=CARTESIAN_POINT('Ctrl Pts',(2.74376940455713,-0.0406287626889416,
8.78644465894813));
#387963=CARTESIAN_POINT('Ctrl Pts',(2.74326787028548,-0.0325377815896124,
8.78817647674133));
#387964=CARTESIAN_POINT('Ctrl Pts',(2.74398145982693,-0.0405035284588546,
8.7678092393203));
#387965=CARTESIAN_POINT('Ctrl Pts',(2.7509534970302,-0.037009900830377,
8.76988516158373));
#387966=CARTESIAN_POINT('Ctrl Pts',(2.75119007538758,-0.0294547429182473,
8.77093053738833));
#387967=CARTESIAN_POINT('Ctrl Pts',(2.74278810430285,-0.0411042670240045,
8.75371302330492));
#387968=CARTESIAN_POINT('Ctrl Pts',(2.74958936735954,-0.0376970655034697,
8.75300828287559));
#387969=CARTESIAN_POINT('Ctrl Pts',(2.74964475769837,-0.0300556342733529,
8.75267964240738));
#387970=CARTESIAN_POINT('Origin',(2.72481212943181,-0.0361589574188236,
8.78727029226991));
#387971=CARTESIAN_POINT('Ctrl Pts',(2.66657505256398,-0.0794701993176737,
8.85049129520029));
#387972=CARTESIAN_POINT('Ctrl Pts',(2.67179104362696,-0.0768444519090332,
8.85711686593484));
#387973=CARTESIAN_POINT('Ctrl Pts',(2.66979042840332,-0.0685319131367439,
8.85933012996512));
#387974=CARTESIAN_POINT('Ctrl Pts',(2.68789189731878,-0.0687392281178691,
8.82945683644722));
#387975=CARTESIAN_POINT('Ctrl Pts',(2.69315118426121,-0.06609168541817,
8.83607469902389));
#387976=CARTESIAN_POINT('Ctrl Pts',(2.69110823399166,-0.0577635165501877,
8.83829567148519));
#387977=CARTESIAN_POINT('Ctrl Pts',(2.70917696759746,-0.0580242522959924,
8.80838214965003));
#387978=CARTESIAN_POINT('Ctrl Pts',(2.71445701014171,-0.0553662611567007,
8.81501364461988));
#387979=CARTESIAN_POINT('Ctrl Pts',(2.71239400300152,-0.0470120517904646,
8.81722098428721));
#387980=CARTESIAN_POINT('Ctrl Pts',(2.73043267776197,-0.0473240564541349,
8.78727029226991));
#387981=CARTESIAN_POINT('Ctrl Pts',(2.73571359733862,-0.0446656238137779,
8.79393457792714));
#387982=CARTESIAN_POINT('Ctrl Pts',(2.73365018604124,-0.0362762407020098,
8.79610912703474));
#387983=CARTESIAN_POINT('Origin',(2.66095450423382,-0.0683051002823623,
8.85049129520029));
#387984=CARTESIAN_POINT('Ctrl Pts',(2.66618796128141,-0.0915411309427756,
8.85049129520029));
#387985=CARTESIAN_POINT('Ctrl Pts',(2.67122500331725,-0.0944956731665771,
8.85711686593484));
#387986=CARTESIAN_POINT('Ctrl Pts',(2.66869591238441,-0.102662953078966,
8.85933012996512));
#387987=CARTESIAN_POINT('Ctrl Pts',(2.66173176290277,-0.0889272900866481,
8.8633249698723));
#387988=CARTESIAN_POINT('Ctrl Pts',(2.66186606778201,-0.0935461488825097,
8.86648636486736));
#387989=CARTESIAN_POINT('Ctrl Pts',(2.65623818394787,-0.0953358487015099,
8.87206031107457));
#387990=CARTESIAN_POINT('Ctrl Pts',(2.66192918350039,-0.0818089453981995,
8.86341338519877));
#387991=CARTESIAN_POINT('Ctrl Pts',(2.66233087922226,-0.0771924411816615,
8.86654584966058));
#387992=CARTESIAN_POINT('Ctrl Pts',(2.6567883726407,-0.0750936859361302,
8.87215952290714));
#387993=CARTESIAN_POINT('Ctrl Pts',(2.66657505256398,-0.0794701993176738,
8.85049129520029));
#387994=CARTESIAN_POINT('Ctrl Pts',(2.67179104362696,-0.0768444519090336,
8.85711686593485));
#387995=CARTESIAN_POINT('Ctrl Pts',(2.66979042840332,-0.068531913136744,
8.85933012996512));
#387996=CARTESIAN_POINT('Origin',(2.65986361061929,-0.10232318031674,8.85049129520029));
#387997=CARTESIAN_POINT('Ctrl Pts',(2.72785477369492,-0.127712598202018,
8.78727029226991));
#387998=CARTESIAN_POINT('Ctrl Pts',(2.73295451669186,-0.130703918486376,
8.79393457792714));
#387999=CARTESIAN_POINT('Ctrl Pts',(2.73035783527281,-0.138943861495048,
8.79610912703474));
#388000=CARTESIAN_POINT('Ctrl Pts',(2.70732829956804,-0.115672529034026,
8.80838214965002));
#388001=CARTESIAN_POINT('Ctrl Pts',(2.71242719562159,-0.118663352532773,
8.81501364461988));
#388002=CARTESIAN_POINT('Ctrl Pts',(2.70983317111897,-0.126868219958582,
8.81722098428721));
#388003=CARTESIAN_POINT('Ctrl Pts',(2.68677347260705,-0.103615829144088,
8.82945683644722));
#388004=CARTESIAN_POINT('Ctrl Pts',(2.69185232513724,-0.106594895854689,
8.83607469902389));
#388005=CARTESIAN_POINT('Ctrl Pts',(2.6892799847167,-0.114775061333372,
8.8382956714852));
#388006=CARTESIAN_POINT('Ctrl Pts',(2.66618796128141,-0.0915411309427756,
8.85049129520029));
#388007=CARTESIAN_POINT('Ctrl Pts',(2.67122500331725,-0.0944956731665771,
8.85711686593484));
#388008=CARTESIAN_POINT('Ctrl Pts',(2.66869591238441,-0.102662953078966,
8.85933012996512));
#388009=CARTESIAN_POINT('Origin',(2.72153042303281,-0.138494647575983,8.78727029226991));
#388010=CARTESIAN_POINT('Ctrl Pts',(2.73979042401482,-0.134713629821672,
8.75374538247847));
#388011=CARTESIAN_POINT('Ctrl Pts',(2.74635165306265,-0.13854699019731,
8.75304829418601));
#388012=CARTESIAN_POINT('Ctrl Pts',(2.74592344570742,-0.146168491471333,
8.75272238421917));
#388013=CARTESIAN_POINT('Ctrl Pts',(2.74092899456703,-0.13538147262631,
8.76769408445022));
#388014=CARTESIAN_POINT('Ctrl Pts',(2.74765498512006,-0.139311893221183,
8.76974318093972));
#388015=CARTESIAN_POINT('Ctrl Pts',(2.74741055885273,-0.146858986243019,
8.7707786988043));
#388016=CARTESIAN_POINT('Ctrl Pts',(2.73509333052471,-0.131958490841916,
8.78108014887986));
#388017=CARTESIAN_POINT('Ctrl Pts',(2.74079528214875,-0.135286100340862,
8.78639403366322));
#388018=CARTESIAN_POINT('Ctrl Pts',(2.7397975286336,-0.143318943153455,
8.78812224174741));
#388019=CARTESIAN_POINT('Ctrl Pts',(2.72552996537758,-0.126348979358583,
8.78944554828686));
#388020=CARTESIAN_POINT('Ctrl Pts',(2.73033818026369,-0.129148530612979,
8.79673892988686));
#388021=CARTESIAN_POINT('Ctrl Pts',(2.72734888397413,-0.137548986672613,
8.79894799272499));
#388022=CARTESIAN_POINT('Origin',(2.73362579600155,-0.145589345197023,8.75721825406948));
#388023=CARTESIAN_POINT('Origin',(2.73362579600155,-0.145589345197023,9.));
#388024=CARTESIAN_POINT('Origin',(2.73362579600155,-0.145589345197022,7.51860402984325));
#388025=CARTESIAN_POINT('Ctrl Pts',(2.74339508349897,-0.127106609904094,
7.50366195182966));
#388026=CARTESIAN_POINT('Ctrl Pts',(2.74705311126524,-0.127276093151815,
7.50000065167735));
#388027=CARTESIAN_POINT('Ctrl Pts',(2.74705311126523,-0.127276093151932,
7.49482233047108));
#388028=CARTESIAN_POINT('Ctrl Pts',(2.744560462474,-0.134454785966985,7.50215800491337));
#388029=CARTESIAN_POINT('Ctrl Pts',(2.74661186251358,-0.136799237939605,
7.49877273257267));
#388030=CARTESIAN_POINT('Ctrl Pts',(2.74645211423604,-0.140247663208879,
7.49481816995647));
#388031=CARTESIAN_POINT('Ctrl Pts',(2.74238152832946,-0.136233061068268,
7.51043025814042));
#388032=CARTESIAN_POINT('Ctrl Pts',(2.74641706184182,-0.140452921996967,
7.51006209594514));
#388033=CARTESIAN_POINT('Ctrl Pts',(2.7461079709193,-0.146256665010223,
7.50731281821701));
#388034=CARTESIAN_POINT('Ctrl Pts',(2.73994884293186,-0.134806531208225,
7.51860402984326));
#388035=CARTESIAN_POINT('Ctrl Pts',(2.74651279192828,-0.138655633826115,
7.51860402984327));
#388036=CARTESIAN_POINT('Ctrl Pts',(2.74610810557234,-0.146254136727608,
7.51860402984327));
#388037=CARTESIAN_POINT('Origin',(0.,0.,7.5));
#388038=CARTESIAN_POINT('Origin',(2.65484493177041,-0.262176299060726,7.5));
#388039=CARTESIAN_POINT('',(2.65484493177041,-0.262176299060726,7.59394543036555));
#388040=CARTESIAN_POINT('',(2.65484493177041,-0.262176299060726,8.85049129520029));
#388041=CARTESIAN_POINT('',(2.65484493177041,-0.262176299060726,7.5));
#388042=CARTESIAN_POINT('',(2.71406752923975,-0.302224454397949,8.78727029226991));
#388043=CARTESIAN_POINT('Ctrl Pts',(2.65484493177041,-0.262176299060726,
8.85049129520029));
#388044=CARTESIAN_POINT('Ctrl Pts',(2.67461449285379,-0.275545088797212,
8.82945686509571));
#388045=CARTESIAN_POINT('Ctrl Pts',(2.69435466409413,-0.288894004211227,
8.80838212259896));
#388046=CARTESIAN_POINT('Ctrl Pts',(2.71406752923975,-0.302224454397949,
8.78727029226991));
#388047=CARTESIAN_POINT('',(2.72568349213023,-0.310079528408679,8.75721825406948));
#388048=CARTESIAN_POINT('Origin',(2.69072714323144,-0.286440718598037,8.75937679713118));
#388049=CARTESIAN_POINT('',(2.72568349213023,-0.310079528408679,7.51860402984325));
#388050=CARTESIAN_POINT('',(2.72568349213023,-0.310079528408679,7.5));
#388051=CARTESIAN_POINT('Ctrl Pts',(2.72568349213022,-0.310079528408679,
7.51860402984325));
#388052=CARTESIAN_POINT('Ctrl Pts',(2.71656095990371,-0.303910589468343,
7.52834476460825));
#388053=CARTESIAN_POINT('Ctrl Pts',(2.70743250546091,-0.29773764574186,
7.53807742314406));
#388054=CARTESIAN_POINT('Ctrl Pts',(2.69829792995554,-0.291560562763214,
7.54780169004674));
#388055=CARTESIAN_POINT('Ctrl Pts',(2.6838292560367,-0.281776397167888,
7.5632044032688));
#388056=CARTESIAN_POINT('Ctrl Pts',(2.6693452067639,-0.271981834281848,
7.57858609112103));
#388057=CARTESIAN_POINT('Ctrl Pts',(2.65484493177041,-0.262176299060725,
7.59394543036555));
#388058=CARTESIAN_POINT('Origin',(2.90905453099297,-0.142494670373502,7.5));
#388059=CARTESIAN_POINT('',(2.73469396819878,-0.216676518124512,8.75721825406948));
#388060=CARTESIAN_POINT('',(2.72179064828013,-0.222166246411397,8.78727029226991));
#388061=CARTESIAN_POINT('Origin',(2.6890372096248,-0.236101224371513,8.75658640620901));
#388062=CARTESIAN_POINT('',(2.65600461497702,-0.250154969482878,8.85049129520029));
#388063=CARTESIAN_POINT('Ctrl Pts',(2.72179064828013,-0.222166246411397,
8.78727029226991));
#388064=CARTESIAN_POINT('Ctrl Pts',(2.69989307440824,-0.231482587589983,
8.80838212259894));
#388065=CARTESIAN_POINT('Ctrl Pts',(2.67796516820153,-0.240811833685869,
8.82945686509571));
#388066=CARTESIAN_POINT('Ctrl Pts',(2.65600461497702,-0.250154969482878,
8.85049129520029));
#388067=CARTESIAN_POINT('',(2.65600461497702,-0.250154969482878,7.59394543036555));
#388068=CARTESIAN_POINT('',(2.65600461497702,-0.250154969482878,7.5));
#388069=CARTESIAN_POINT('',(2.73469396819878,-0.216676518124512,7.51860402984325));
#388070=CARTESIAN_POINT('Ctrl Pts',(2.65600461497702,-0.250154969482878,
7.59394543036555));
#388071=CARTESIAN_POINT('Ctrl Pts',(2.67211190534232,-0.243302109280937,
7.57858609112103));
#388072=CARTESIAN_POINT('Ctrl Pts',(2.68820117174618,-0.236456917388534,
7.56320440326857));
#388073=CARTESIAN_POINT('Ctrl Pts',(2.70427335879892,-0.229618991920377,
7.54780169004651));
#388074=CARTESIAN_POINT('Ctrl Pts',(2.71442028774302,-0.225301972486568,
7.53807742314383));
#388075=CARTESIAN_POINT('Ctrl Pts',(2.72456041724852,-0.220987845879614,
7.52834476460825));
#388076=CARTESIAN_POINT('Ctrl Pts',(2.73469396819878,-0.216676518124513,
7.51860402984325));
#388077=CARTESIAN_POINT('',(2.73469396819878,-0.216676518124512,7.5));
#388078=CARTESIAN_POINT('Origin',(2.65869612245475,-0.256481217383277,7.5));
#388079=CARTESIAN_POINT('Ctrl Pts',(2.65600461497702,-0.250154969482878,
8.85049129520029));
#388080=CARTESIAN_POINT('Ctrl Pts',(2.65582641123954,-0.250230786412525,
8.85097269580139));
#388081=CARTESIAN_POINT('Ctrl Pts',(2.65565374887267,-0.250313386797546,
8.85143669361005));
#388082=CARTESIAN_POINT('Ctrl Pts',(2.65547905463229,-0.250407362801228,
8.8519052845931));
#388083=CARTESIAN_POINT('Ctrl Pts',(2.6551373637768,-0.250591173904689,
8.85282181883899));
#388084=CARTESIAN_POINT('Ctrl Pts',(2.65479678269175,-0.2508139494761,8.85372622499635));
#388085=CARTESIAN_POINT('Ctrl Pts',(2.65446040730407,-0.251092088735957,
8.8546225773507));
#388086=CARTESIAN_POINT('Ctrl Pts',(2.65418116040415,-0.251322990070918,
8.85536669723986));
#388087=CARTESIAN_POINT('Ctrl Pts',(2.65390472814385,-0.251592074862203,
8.85610498449051));
#388088=CARTESIAN_POINT('Ctrl Pts',(2.65363844027942,-0.251914482863951,
8.85681338218371));
#388089=CARTESIAN_POINT('Ctrl Pts',(2.65339678362424,-0.252207068631889,
8.85745625420284));
#388090=CARTESIAN_POINT('Ctrl Pts',(2.65315998869644,-0.252546858276533,
8.85808743050665));
#388091=CARTESIAN_POINT('Ctrl Pts',(2.65294216072111,-0.252958729273119,
8.8586680450841));
#388092=CARTESIAN_POINT('Ctrl Pts',(2.65284165961522,-0.253148757622676,
8.85893592806395));
#388093=CARTESIAN_POINT('Ctrl Pts',(2.65274533984821,-0.253354324991397,
8.85919241173848));
#388094=CARTESIAN_POINT('Ctrl Pts',(2.65265570415938,-0.253579014432801,
8.85943017985534));
#388095=CARTESIAN_POINT('Ctrl Pts',(2.65253466944446,-0.253882411693887,
8.8597512372));
#388096=CARTESIAN_POINT('Ctrl Pts',(2.65242333611262,-0.254228633815598,
8.86004599534706));
#388097=CARTESIAN_POINT('Ctrl Pts',(2.65233295686034,-0.254616709420175,
8.86026130871721));
#388098=CARTESIAN_POINT('Ctrl Pts',(2.65229986646803,-0.25475879484002,
8.86034014101236));
#388099=CARTESIAN_POINT('Ctrl Pts',(2.65226907590949,-0.254908622195513,
8.86040910639693));
#388100=CARTESIAN_POINT('Ctrl Pts',(2.65224175354912,-0.255062177237531,
8.86046313645507));
#388101=CARTESIAN_POINT('Ctrl Pts',(2.65219911723458,-0.255301798594587,
8.8605474499083));
#388102=CARTESIAN_POINT('Ctrl Pts',(2.65216390737134,-0.255557064068575,
8.86059655985668));
#388103=CARTESIAN_POINT('Ctrl Pts',(2.65213809186542,-0.255811562677652,
8.86059725258816));
#388104=CARTESIAN_POINT('Ctrl Pts',(2.65211221671537,-0.256066649280189,
8.86059794692011));
#388105=CARTESIAN_POINT('Ctrl Pts',(2.65209813563059,-0.256324062526829,
8.86056369958366));
#388106=CARTESIAN_POINT('Ctrl Pts',(2.65209285911932,-0.256569557431468,
8.86048590497774));
#388107=CARTESIAN_POINT('Ctrl Pts',(2.65209148210697,-0.256633624292315,
8.86046560290182));
#388108=CARTESIAN_POINT('Ctrl Pts',(2.65209077737803,-0.256697714868719,
8.86044257503091));
#388109=CARTESIAN_POINT('Ctrl Pts',(2.65209073388499,-0.256759848347883,
8.86041778462583));
#388110=CARTESIAN_POINT('Ctrl Pts',(2.65209044123086,-0.257177929561439,
8.860250975962));
#388111=CARTESIAN_POINT('Ctrl Pts',(2.65212037943941,-0.257563502039559,
8.8599848982295));
#388112=CARTESIAN_POINT('Ctrl Pts',(2.65217122762928,-0.257905967816415,
8.85968173251462));
#388113=CARTESIAN_POINT('Ctrl Pts',(2.65219812340846,-0.258087112591422,
8.85952137522077));
#388114=CARTESIAN_POINT('Ctrl Pts',(2.65223119893676,-0.258259716699445,
8.85934740853961));
#388115=CARTESIAN_POINT('Ctrl Pts',(2.65226846100321,-0.258421638611228,
8.8591675900182));
#388116=CARTESIAN_POINT('Ctrl Pts',(2.65241808756843,-0.259071839252373,
8.85844552518695));
#388117=CARTESIAN_POINT('Ctrl Pts',(2.65264072726469,-0.259587222332702,
8.85759444184124));
#388118=CARTESIAN_POINT('Ctrl Pts',(2.65285999980908,-0.259991132974789,
8.85683498915138));
#388119=CARTESIAN_POINT('Ctrl Pts',(2.65288294609688,-0.26003340114778,
8.85675551444998));
#388120=CARTESIAN_POINT('Ctrl Pts',(2.65290587085534,-0.260074435800304,
8.85667699793651));
#388121=CARTESIAN_POINT('Ctrl Pts',(2.65292869619824,-0.260114254771393,
8.85659965593547));
#388122=CARTESIAN_POINT('Ctrl Pts',(2.65323679384139,-0.260651733275015,
8.85555568965886));
#388123=CARTESIAN_POINT('Ctrl Pts',(2.65361051729581,-0.261123788020516,
8.85434650606346));
#388124=CARTESIAN_POINT('Ctrl Pts',(2.65404684146777,-0.261536610171378,
8.85297329937117));
#388125=CARTESIAN_POINT('Ctrl Pts',(2.65429224722887,-0.261768797477614,
8.85220095427747));
#388126=CARTESIAN_POINT('Ctrl Pts',(2.65455777277543,-0.261982113251104,
8.85137579139183));
#388127=CARTESIAN_POINT('Ctrl Pts',(2.65484493177041,-0.262176299060726,
8.85049129520029));
#388128=CARTESIAN_POINT('Origin',(2.65869612245475,-0.256481217383277,7.59394543036555));
#388129=CARTESIAN_POINT('Ctrl Pts',(2.65548722941064,-0.250375091606243,
7.59443877723642));
#388130=CARTESIAN_POINT('Ctrl Pts',(2.65015865589203,-0.252642137681074,
7.58783886950016));
#388131=CARTESIAN_POINT('Ctrl Pts',(2.65158455852055,-0.261011485518907,
7.58559994247159));
#388132=CARTESIAN_POINT('Ctrl Pts',(2.68457575591506,-0.237999353596044,
7.56670252222135));
#388133=CARTESIAN_POINT('Ctrl Pts',(2.67925488369801,-0.240263123145666,
7.56004874999029));
#388134=CARTESIAN_POINT('Ctrl Pts',(2.68066817321353,-0.248685650676148,
7.55786368756704));
#388135=CARTESIAN_POINT('Ctrl Pts',(2.71360996250254,-0.225646726040084,
7.5388891333356));
#388136=CARTESIAN_POINT('Ctrl Pts',(2.70825746808137,-0.227923949282997,
7.5322200213728));
#388137=CARTESIAN_POINT('Ctrl Pts',(2.70969805244026,-0.236381322481853,
7.53005029815327));
#388138=CARTESIAN_POINT('Ctrl Pts',(2.74258853535555,-0.213317767903139,
7.51101258149734));
#388139=CARTESIAN_POINT('Ctrl Pts',(2.73717115897627,-0.215622595229558,
7.5043616886572));
#388140=CARTESIAN_POINT('Ctrl Pts',(2.7386727941559,-0.224099184952553,
7.50217374673251));
#388141=CARTESIAN_POINT('',(2.73712666431696,-0.224754574642168,7.50366116523517));
#388142=CARTESIAN_POINT('Ctrl Pts',(2.73469396819878,-0.216676518124511,
7.51860402984325));
#388143=CARTESIAN_POINT('Ctrl Pts',(2.73510033067526,-0.216503630867908,
7.51734760759493));
#388144=CARTESIAN_POINT('Ctrl Pts',(2.73549082980322,-0.216402150372084,
7.51608817408572));
#388145=CARTESIAN_POINT('Ctrl Pts',(2.73586792612086,-0.216385234400819,
7.51481005913119));
#388146=CARTESIAN_POINT('Ctrl Pts',(2.73620950897638,-0.216369911509826,
7.51365231206383));
#388147=CARTESIAN_POINT('Ctrl Pts',(2.73654056487762,-0.216423703726785,
7.51247773061042));
#388148=CARTESIAN_POINT('Ctrl Pts',(2.73684944320768,-0.216582127288776,
7.51129758471022));
#388149=CARTESIAN_POINT('Ctrl Pts',(2.7372333436967,-0.216779029683677,
7.50983079813402));
#388150=CARTESIAN_POINT('Ctrl Pts',(2.73756478892187,-0.217142868017661,
7.50839324291155));
#388151=CARTESIAN_POINT('Ctrl Pts',(2.7377852545119,-0.217731815209133,
7.50715379678855));
#388152=CARTESIAN_POINT('Ctrl Pts',(2.73788710326193,-0.218003891841488,
7.50658120839351));
#388153=CARTESIAN_POINT('Ctrl Pts',(2.73797084707659,-0.218366019889119,
7.50598221009429));
#388154=CARTESIAN_POINT('Ctrl Pts',(2.73801233135004,-0.218814706195348,
7.50545747549611));
#388155=CARTESIAN_POINT('Ctrl Pts',(2.73803446864242,-0.219054139096492,
7.50517746087247));
#388156=CARTESIAN_POINT('Ctrl Pts',(2.73804501371075,-0.219320798164657,
7.50491486231392));
#388157=CARTESIAN_POINT('Ctrl Pts',(2.73804202059031,-0.219607687728826,
7.50468370960992));
#388158=CARTESIAN_POINT('Ctrl Pts',(2.73803754493112,-0.220036678121437,
7.50433806340447));
#388159=CARTESIAN_POINT('Ctrl Pts',(2.73800210745578,-0.220523761247855,
7.50405484070984));
#388160=CARTESIAN_POINT('Ctrl Pts',(2.73793738030584,-0.221036080981636,
7.50385766036131));
#388161=CARTESIAN_POINT('Ctrl Pts',(2.73793045874324,-0.221090865613916,
7.50383657498791));
#388162=CARTESIAN_POINT('Ctrl Pts',(2.73792321962444,-0.221145916405801,
7.50381643264937));
#388163=CARTESIAN_POINT('Ctrl Pts',(2.7379156778676,-0.221201177089471,
7.50379723213559));
#388164=CARTESIAN_POINT('Ctrl Pts',(2.73786533417364,-0.221570060229976,
7.50366906242519));
#388165=CARTESIAN_POINT('Ctrl Pts',(2.73779969739273,-0.22195622297899,
7.50358235568538));
#388166=CARTESIAN_POINT('Ctrl Pts',(2.73772748437109,-0.222326915563675,
7.5035341175365));
#388167=CARTESIAN_POINT('Ctrl Pts',(2.73761920911807,-0.22288272714011,
7.50346178989176));
#388168=CARTESIAN_POINT('Ctrl Pts',(2.73747909711921,-0.2234760501773,7.50346967198527));
#388169=CARTESIAN_POINT('Ctrl Pts',(2.73732362825383,-0.224054277262578,
7.50354272648692));
#388170=CARTESIAN_POINT('Ctrl Pts',(2.73725968069148,-0.224292114031345,
7.50357277531559));
#388171=CARTESIAN_POINT('Ctrl Pts',(2.73719335688109,-0.224527117606271,
7.50361331098761));
#388172=CARTESIAN_POINT('Ctrl Pts',(2.73712666431837,-0.224754574642284,
7.50366116523659));
#388173=CARTESIAN_POINT('',(2.66161051802577,-0.256762365619137,7.57603338622103));
#388174=CARTESIAN_POINT('Origin',(2.67040634802705,-0.25761375518207,7.58486873427628));
#388175=CARTESIAN_POINT('Ctrl Pts',(2.73712666436744,-0.224754574614952,
7.50366116529968));
#388176=CARTESIAN_POINT('Ctrl Pts',(2.71199601738035,-0.235407197804142,
7.52783573079709));
#388177=CARTESIAN_POINT('Ctrl Pts',(2.68682516411221,-0.246075974212514,
7.55196141284068));
#388178=CARTESIAN_POINT('Ctrl Pts',(2.66161051899361,-0.256762364824825,
7.57603338728831));
#388179=CARTESIAN_POINT('Ctrl Pts',(2.65701976820131,-0.24991413872985,
7.5963967733137));
#388180=CARTESIAN_POINT('Ctrl Pts',(2.63928131883209,-0.254320875588142,
7.59959882295472));
#388181=CARTESIAN_POINT('Ctrl Pts',(2.65563227986823,-0.262527877830806,
7.59642833564546));
#388182=CARTESIAN_POINT('Ctrl Pts',(2.65313223933926,-0.250233862721098,
7.5870762605742));
#388183=CARTESIAN_POINT('Ctrl Pts',(2.64878024702139,-0.255427363842895,
7.588099439206));
#388184=CARTESIAN_POINT('Ctrl Pts',(2.65195705933609,-0.261395802860866,
7.58710240504253));
#388185=CARTESIAN_POINT('Ctrl Pts',(2.65771595193358,-0.254223250031781,
7.58015376756929));
#388186=CARTESIAN_POINT('Ctrl Pts',(2.65561601806597,-0.256151863302553,
7.58205880659761));
#388187=CARTESIAN_POINT('Ctrl Pts',(2.65725320000503,-0.258442433174035,
7.58020924244126));
#388188=CARTESIAN_POINT('Ctrl Pts',(2.66161051720204,-0.256762365539468,
7.57603338509286));
#388189=CARTESIAN_POINT('Ctrl Pts',(2.66161051720205,-0.256762365539468,
7.57603338509286));
#388190=CARTESIAN_POINT('Ctrl Pts',(2.66161051720205,-0.256762365539468,
7.57603338509286));
#388191=CARTESIAN_POINT('Origin',(2.67040689596867,-0.257608075198336,7.58486873427622));
#388192=CARTESIAN_POINT('Ctrl Pts',(2.73281288470864,-0.314900644564356,
7.51098857897448));
#388193=CARTESIAN_POINT('Ctrl Pts',(2.72793597470703,-0.311602726917105,
7.50433767179956));
#388194=CARTESIAN_POINT('Ctrl Pts',(2.73103031844477,-0.303569478015496,
7.50214974420965));
#388195=CARTESIAN_POINT('Ctrl Pts',(2.70671798449283,-0.297254464524829,
7.53887321589167));
#388196=CARTESIAN_POINT('Ctrl Pts',(2.70189950852799,-0.293996061783733,
7.53220407452061));
#388197=CARTESIAN_POINT('Ctrl Pts',(2.70493022693792,-0.28597000011928,
7.53003438070911));
#388198=CARTESIAN_POINT('Ctrl Pts',(2.68057297244262,-0.279574397310241,
7.56669465659236));
#388199=CARTESIAN_POINT('Ctrl Pts',(2.67578297277488,-0.276335251123579,
7.56004085833303));
#388200=CARTESIAN_POINT('Ctrl Pts',(2.67878022809322,-0.268338182242846,
7.55785582193789));
#388201=CARTESIAN_POINT('Ctrl Pts',(2.65437903099218,-0.26186124251921,
7.59443891967696));
#388202=CARTESIAN_POINT('Ctrl Pts',(2.64958208642131,-0.258617399973843,
7.58783901202978));
#388203=CARTESIAN_POINT('Ctrl Pts',(2.65258156709373,-0.250674963717624,
7.58560008491213));
#388204=CARTESIAN_POINT('',(2.72961551748769,-0.30261546891708,7.50366116523517));
#388205=CARTESIAN_POINT('Ctrl Pts',(2.72961551748806,-0.302615468917121,
7.50366116523554));
#388206=CARTESIAN_POINT('Ctrl Pts',(2.72968561742245,-0.303369937946282,
7.50350835821027));
#388207=CARTESIAN_POINT('Ctrl Pts',(2.7297255104133,-0.30406575872811,7.50345484956));
#388208=CARTESIAN_POINT('Ctrl Pts',(2.72973698202872,-0.304723584208325,
7.50349758195598));
#388209=CARTESIAN_POINT('Ctrl Pts',(2.7297428678182,-0.305061097465285,
7.50351950684424));
#388210=CARTESIAN_POINT('Ctrl Pts',(2.72974198137209,-0.305421873052815,
7.50357029184312));
#388211=CARTESIAN_POINT('Ctrl Pts',(2.72973156373016,-0.305769741308945,
7.50365515313923));
#388212=CARTESIAN_POINT('Ctrl Pts',(2.72971553717836,-0.306304903552644,
7.50378570417639));
#388213=CARTESIAN_POINT('Ctrl Pts',(2.72967682976936,-0.306825237690729,
7.50400001621911));
#388214=CARTESIAN_POINT('Ctrl Pts',(2.72961612354001,-0.307290970309341,
7.50428903009635));
#388215=CARTESIAN_POINT('Ctrl Pts',(2.7296093856156,-0.307342663046873,
7.50432110841318));
#388216=CARTESIAN_POINT('Ctrl Pts',(2.72960239051942,-0.307393710105049,
7.50435406373354));
#388217=CARTESIAN_POINT('Ctrl Pts',(2.72959514912735,-0.307444077147374,
7.50438785222352));
#388218=CARTESIAN_POINT('Ctrl Pts',(2.72955093694813,-0.307751592150259,
7.50459414719561));
#388219=CARTESIAN_POINT('Ctrl Pts',(2.72949632922009,-0.308038580830313,
7.50483629897752));
#388220=CARTESIAN_POINT('Ctrl Pts',(2.72943471078469,-0.308294294734311,
7.5050991045531));
#388221=CARTESIAN_POINT('Ctrl Pts',(2.72929877432722,-0.308858425290561,
7.50567888004914));
#388222=CARTESIAN_POINT('Ctrl Pts',(2.72912386673409,-0.309292697140601,
7.50637912803144));
#388223=CARTESIAN_POINT('Ctrl Pts',(2.72893465063687,-0.309615742862395,
7.50710440483569));
#388224=CARTESIAN_POINT('Ctrl Pts',(2.72888825109336,-0.309694960086735,
7.50728225710685));
#388225=CARTESIAN_POINT('Ctrl Pts',(2.72884019340232,-0.309769139713227,
7.50746498566954));
#388226=CARTESIAN_POINT('Ctrl Pts',(2.72879194901789,-0.309836776660444,
7.50764697238949));
#388227=CARTESIAN_POINT('Ctrl Pts',(2.72853260048436,-0.310200374274494,
7.50862528291182));
#388228=CARTESIAN_POINT('Ctrl Pts',(2.72824768340916,-0.310410308860673,
7.50965856837422));
#388229=CARTESIAN_POINT('Ctrl Pts',(2.72796073636963,-0.310528558892816,
7.51067959873202));
#388230=CARTESIAN_POINT('Ctrl Pts',(2.72780282905185,-0.310593632034658,
7.51124147302579));
#388231=CARTESIAN_POINT('Ctrl Pts',(2.72764410294566,-0.310630554447905,
7.51180065547253));
#388232=CARTESIAN_POINT('Ctrl Pts',(2.72748753823894,-0.310647107520337,
7.51235175716501));
#388233=CARTESIAN_POINT('Ctrl Pts',(2.72694654480926,-0.310704304979551,
7.51425603304536));
#388234=CARTESIAN_POINT('Ctrl Pts',(2.72636621705692,-0.310519085845715,
7.51626900505181));
#388235=CARTESIAN_POINT('Ctrl Pts',(2.72577891497115,-0.310142396153948,
7.51827788969245));
#388236=CARTESIAN_POINT('Ctrl Pts',(2.72574712907242,-0.310122008995986,
7.51838661432546));
#388237=CARTESIAN_POINT('Ctrl Pts',(2.72571532001016,-0.310101051407239,
7.51849533314857));
#388238=CARTESIAN_POINT('Ctrl Pts',(2.72568349213022,-0.310079528408683,
7.51860402984325));
#388239=CARTESIAN_POINT('Ctrl Pts',(2.66161051882509,-0.256762366584167,
7.57603338728985));
#388240=CARTESIAN_POINT('Ctrl Pts',(2.68431738886144,-0.272071688132325,
7.55196141284922));
#388241=CARTESIAN_POINT('Ctrl Pts',(2.70698464172671,-0.287355349116283,
7.52783573083105));
#388242=CARTESIAN_POINT('Ctrl Pts',(2.72961551753351,-0.302615468954532,
7.50366116530176));
#388243=CARTESIAN_POINT('Origin',(9.19709468541367E-16,-8.87232663177103E-17,
7.49482233047033));
#388244=CARTESIAN_POINT('Origin',(2.7283174780614,-0.224031223057595,7.49482233047033));
#388245=CARTESIAN_POINT('Origin',(0.,0.,7.50366116523517));
#388246=CARTESIAN_POINT('Origin',(2.72083050515593,-0.301641529324055,7.49482233047033));
#388247=CARTESIAN_POINT('Ctrl Pts',(2.73469299488662,-0.216676932172354,
7.51860402984325));
#388248=CARTESIAN_POINT('Ctrl Pts',(2.74169487207939,-0.21369867734652,
7.51860402984325));
#388249=CARTESIAN_POINT('Ctrl Pts',(2.74226515987506,-0.206111117932571,
7.51860402984325));
#388250=CARTESIAN_POINT('Ctrl Pts',(2.73729283917419,-0.215571084661517,
7.51041458714366));
#388251=CARTESIAN_POINT('Ctrl Pts',(2.74182996991852,-0.211901096872824,
7.51004642900443));
#388252=CARTESIAN_POINT('Ctrl Pts',(2.74226531715367,-0.206109025373781,
7.5072913648301));
#388253=CARTESIAN_POINT('Ctrl Pts',(2.73922057885099,-0.217622317690166,
7.50215815450137));
#388254=CARTESIAN_POINT('Ctrl Pts',(2.74155503724043,-0.215561160609934,
7.49877163671529));
#388255=CARTESIAN_POINT('Ctrl Pts',(2.74183741099952,-0.212122528810137,
7.4948158853317));
#388256=CARTESIAN_POINT('Ctrl Pts',(2.73712611564553,-0.224754529589408,
7.50366171572174));
#388257=CARTESIAN_POINT('Ctrl Pts',(2.74077554873745,-0.225054196679248,
7.50000045605858));
#388258=CARTESIAN_POINT('Ctrl Pts',(2.74077554873746,-0.225054196679124,
7.49482233047317));
#388259=CARTESIAN_POINT('Origin',(2.72980031823927,-0.205174249214696,7.51860402984325));
#388260=CARTESIAN_POINT('Origin',(2.72980031823927,-0.205174249214696,9.));
#388261=CARTESIAN_POINT('Origin',(2.72980031823927,-0.205174249214696,8.75721825406948));
#388262=CARTESIAN_POINT('Ctrl Pts',(2.71932677685935,-0.223214469743979,
8.78942910404913));
#388263=CARTESIAN_POINT('Ctrl Pts',(2.7244623390508,-0.221051501949621,
8.7967269950169));
#388264=CARTESIAN_POINT('Ctrl Pts',(2.72256725120911,-0.212328994967426,
8.79893251111267));
#388265=CARTESIAN_POINT('Ctrl Pts',(2.72944356314156,-0.218910279452994,
8.78111911759579));
#388266=CARTESIAN_POINT('Ctrl Pts',(2.73552894228411,-0.216339195864893,
8.78644465894814));
#388267=CARTESIAN_POINT('Ctrl Pts',(2.73554682940729,-0.208232705142873,
8.78817647674132));
#388268=CARTESIAN_POINT('Ctrl Pts',(2.73574858564825,-0.216227805369768,
8.76780923932032));
#388269=CARTESIAN_POINT('Ctrl Pts',(2.74293013554404,-0.21318805573127,
8.76988516158373));
#388270=CARTESIAN_POINT('Ctrl Pts',(2.74365028845524,-0.205663578328759,
8.77093053738833));
#388271=CARTESIAN_POINT('Ctrl Pts',(2.73451919254909,-0.216750851102149,
8.75371302330491));
#388272=CARTESIAN_POINT('Ctrl Pts',(2.74152478183233,-0.21378640846275,
8.75300828287559));
#388273=CARTESIAN_POINT('Ctrl Pts',(2.74206964654565,-0.206164226243825,
8.75267964240737));
#388274=CARTESIAN_POINT('Origin',(2.71689699832061,-0.210663977501581,8.78727029226991));
#388275=CARTESIAN_POINT('Ctrl Pts',(2.65600461497702,-0.250154969482878,
8.85049129520029));
#388276=CARTESIAN_POINT('Ctrl Pts',(2.66137812144103,-0.247868806648722,
8.85711686593484));
#388277=CARTESIAN_POINT('Ctrl Pts',(2.65991420288367,-0.239445167021381,
8.85933012996512));
#388278=CARTESIAN_POINT('Ctrl Pts',(2.67796519767341,-0.240811821147034,
8.82945683644722));
#388279=CARTESIAN_POINT('Ctrl Pts',(2.68338330748995,-0.238506681779115,
8.83607469902389));
#388280=CARTESIAN_POINT('Ctrl Pts',(2.68187814229224,-0.230064731754072,
8.8382956714852));
#388281=CARTESIAN_POINT('Ctrl Pts',(2.69989304635038,-0.231482599527222,
8.80838214965001));
#388282=CARTESIAN_POINT('Ctrl Pts',(2.70533253855797,-0.229168363003102,
8.8150136446199));
#388283=CARTESIAN_POINT('Ctrl Pts',(2.70380902611905,-0.220699140934707,
8.81722098428721));
#388284=CARTESIAN_POINT('Ctrl Pts',(2.72179064828013,-0.222166246411397,
8.78727029226991));
#388285=CARTESIAN_POINT('Ctrl Pts',(2.72723104400521,-0.219851625484992,
8.79393457792714));
#388286=CARTESIAN_POINT('Ctrl Pts',(2.7257093818291,-0.211347276044851,
8.79610912703474));
#388287=CARTESIAN_POINT('Origin',(2.6511109650175,-0.238652700573062,8.85049129520029));
#388288=CARTESIAN_POINT('Ctrl Pts',(2.65484493177041,-0.262176299060726,
8.85049129520029));
#388289=CARTESIAN_POINT('Ctrl Pts',(2.65968232649295,-0.265447495251943,
8.85711686593484));
#388290=CARTESIAN_POINT('Ctrl Pts',(2.65663515242804,-0.273435955199396,
8.85933012996512));
#388291=CARTESIAN_POINT('Ctrl Pts',(2.6505653584879,-0.259282319010569,
8.86332496987231));
#388292=CARTESIAN_POINT('Ctrl Pts',(2.65040345612427,-0.263900292808822,
8.86648636486736));
#388293=CARTESIAN_POINT('Ctrl Pts',(2.64467246891995,-0.265325735742317,
8.87206031107457));
#388294=CARTESIAN_POINT('Ctrl Pts',(2.65121844737383,-0.252191248505847,
8.86341338519876));
#388295=CARTESIAN_POINT('Ctrl Pts',(2.65191509820944,-0.247609966125603,
8.86654584966059));
#388296=CARTESIAN_POINT('Ctrl Pts',(2.64651844701235,-0.245160413381895,
8.87215952290715));
#388297=CARTESIAN_POINT('Ctrl Pts',(2.65600461497702,-0.250154969482878,
8.85049129520029));
#388298=CARTESIAN_POINT('Ctrl Pts',(2.66137812144103,-0.247868806648722,
8.85711686593484));
#388299=CARTESIAN_POINT('Ctrl Pts',(2.65991420288367,-0.239445167021382,
8.85933012996512));
#388300=CARTESIAN_POINT('Origin',(2.64784276688978,-0.272530993019724,8.85049129520029));
#388301=CARTESIAN_POINT('Ctrl Pts',(2.71406752923975,-0.30222445439795,
8.78727029226991));
#388302=CARTESIAN_POINT('Ctrl Pts',(2.7189651397191,-0.305536370349624,
8.79393457792714));
#388303=CARTESIAN_POINT('Ctrl Pts',(2.71584585849932,-0.313593013561916,
8.79610912703474));
#388304=CARTESIAN_POINT('Ctrl Pts',(2.6943546388356,-0.288893987130622,
8.80838214965002));
#388305=CARTESIAN_POINT('Ctrl Pts',(2.69925143594085,-0.292205353053535,
8.81501364461988));
#388306=CARTESIAN_POINT('Ctrl Pts',(2.6961370534789,-0.300227162978743,
8.81722098428721));
#388307=CARTESIAN_POINT('Ctrl Pts',(2.67461451938527,-0.27554510673862,
8.82945683644722));
#388308=CARTESIAN_POINT('Ctrl Pts',(2.67949206740876,-0.278843455836032,
8.83607469902389));
#388309=CARTESIAN_POINT('Ctrl Pts',(2.6764009071358,-0.286842003870797,
8.8382956714852));
#388310=CARTESIAN_POINT('Ctrl Pts',(2.65484493177041,-0.262176299060726,
8.85049129520029));
#388311=CARTESIAN_POINT('Ctrl Pts',(2.65968232649295,-0.265447495251944,
8.85711686593484));
#388312=CARTESIAN_POINT('Ctrl Pts',(2.65663515242804,-0.273435955199396,
8.85933012996512));
#388313=CARTESIAN_POINT('Origin',(2.70706536435912,-0.312579148356947,8.78727029226991));
#388314=CARTESIAN_POINT('Ctrl Pts',(2.72553009885,-0.309975821388891,8.75374538247847));
#388315=CARTESIAN_POINT('Ctrl Pts',(2.73183224290654,-0.314221685102948,
8.75304829418602));
#388316=CARTESIAN_POINT('Ctrl Pts',(2.73091660408603,-0.321800091845756,
8.75272238421917));
#388317=CARTESIAN_POINT('Ctrl Pts',(2.72662354125151,-0.310715240504611,
8.76769408445022));
#388318=CARTESIAN_POINT('Ctrl Pts',(2.73308388962346,-0.315068521323158,
8.76974318093968));
#388319=CARTESIAN_POINT('Ctrl Pts',(2.73235642164598,-0.322584447588229,
8.77077869880429));
#388320=CARTESIAN_POINT('Ctrl Pts',(2.72101917840274,-0.306925399324471,
8.78108014887987));
#388321=CARTESIAN_POINT('Ctrl Pts',(2.72649621408303,-0.310611497187703,
8.78639403366327));
#388322=CARTESIAN_POINT('Ctrl Pts',(2.72498584455341,-0.318563909376018,
8.78812224174742));
#388323=CARTESIAN_POINT('Ctrl Pts',(2.7118348648497,-0.300714686275373,
8.78944554828686));
#388324=CARTESIAN_POINT('Ctrl Pts',(2.71645383287793,-0.303816548936929,
8.79673892988685));
#388325=CARTESIAN_POINT('Ctrl Pts',(2.71293245935052,-0.312008220487782,
8.79894799272499));
#388326=CARTESIAN_POINT('Origin',(2.7186813272496,-0.320434222367677,8.75721825406948));
#388327=CARTESIAN_POINT('Origin',(2.7186813272496,-0.320434222367677,9.));
#388328=CARTESIAN_POINT('Origin',(2.7186813272496,-0.320434222367677,7.51860402984325));
#388329=CARTESIAN_POINT('Ctrl Pts',(2.72961473561416,-0.30261538223569,
7.50366195182966));
#388330=CARTESIAN_POINT('Ctrl Pts',(2.7332543887411,-0.303018887905582,
7.50000065167735));
#388331=CARTESIAN_POINT('Ctrl Pts',(2.73325438874109,-0.303018887905698,
7.49482233047108));
#388332=CARTESIAN_POINT('Ctrl Pts',(2.73030692093631,-0.310023126770065,
7.50215800491337));
#388333=CARTESIAN_POINT('Ctrl Pts',(2.73220389660085,-0.312494195466464,
7.49877273257265));
#388334=CARTESIAN_POINT('Ctrl Pts',(2.73182353517771,-0.315925300468896,
7.49481816995647));
#388335=CARTESIAN_POINT('Ctrl Pts',(2.72801852916871,-0.311658143424456,
7.51043025814043));
#388336=CARTESIAN_POINT('Ctrl Pts',(2.73177540382666,-0.316127891716176,
7.51006209594516));
#388337=CARTESIAN_POINT('Ctrl Pts',(2.73109510087304,-0.321899906793571,
7.50731281821701));
#388338=CARTESIAN_POINT('Ctrl Pts',(2.72568224006611,-0.310078681834444,
7.51860402984326));
#388339=CARTESIAN_POINT('Ctrl Pts',(2.73198608987389,-0.314340429714334,
7.51860402984326));
#388340=CARTESIAN_POINT('Ctrl Pts',(2.73109539723704,-0.321897392332832,
7.51860402984327));
#388341=CARTESIAN_POINT('Origin',(0.,0.,7.5));
#388342=CARTESIAN_POINT('Origin',(2.63259257497231,-0.431734128529198,7.5));
#388343=CARTESIAN_POINT('',(2.63259257497231,-0.431734128529198,7.59394543036555));
#388344=CARTESIAN_POINT('',(2.63259257497231,-0.431734128529198,8.85049129520029));
#388345=CARTESIAN_POINT('',(2.63259257497231,-0.431734128529198,7.5));
#388346=CARTESIAN_POINT('',(2.68912759914127,-0.47549440548382,8.78727029226991));
#388347=CARTESIAN_POINT('Ctrl Pts',(2.63259257497231,-0.431734128529198,
8.85049129520029));
#388348=CARTESIAN_POINT('Ctrl Pts',(2.65146497607288,-0.446342090780907,
8.82945686509571));
#388349=CARTESIAN_POINT('Ctrl Pts',(2.6703093210672,-0.460928336530369,
8.80838212259897));
#388350=CARTESIAN_POINT('Ctrl Pts',(2.68912759914127,-0.47549440548382,
8.78727029226991));
#388351=CARTESIAN_POINT('',(2.70021641947035,-0.484077577700222,8.75721825406948));
#388352=CARTESIAN_POINT('Origin',(2.66684643588504,-0.45824767539666,8.75937679713162));
#388353=CARTESIAN_POINT('',(2.70021641947035,-0.484077577700222,7.51860402984325));
#388354=CARTESIAN_POINT('',(2.70021641947035,-0.484077577700222,7.5));
#388355=CARTESIAN_POINT('Ctrl Pts',(2.70021641947035,-0.484077577700221,
7.51860402984325));
#388356=CARTESIAN_POINT('Ctrl Pts',(2.69150787573963,-0.477336830860021,
7.52834476460825));
#388357=CARTESIAN_POINT('Ctrl Pts',(2.682793678548,-0.470591708024237,7.53807742314407));
#388358=CARTESIAN_POINT('Ctrl Pts',(2.67407363807296,-0.463842062263,7.54780169004674));
#388359=CARTESIAN_POINT('Ctrl Pts',(2.66026156523847,-0.453150988164429,
7.5632044032688));
#388360=CARTESIAN_POINT('Ctrl Pts',(2.64643481479703,-0.442448553035182,
7.57858609112103));
#388361=CARTESIAN_POINT('Ctrl Pts',(2.63259257497231,-0.431734128529198,
7.59394543036555));
#388362=CARTESIAN_POINT('Origin',(2.89394790158701,-0.328585663527325,7.5));
#388363=CARTESIAN_POINT('',(2.71519273396522,-0.391443777101968,8.75721825406948));
#388364=CARTESIAN_POINT('',(2.70196419720224,-0.396095507607646,8.78727029226991));
#388365=CARTESIAN_POINT('Origin',(2.66838523689802,-0.407903334640574,8.75658640620977));
#388366=CARTESIAN_POINT('',(2.63452008471591,-0.419811799220407,8.85049129520029));
#388367=CARTESIAN_POINT('Ctrl Pts',(2.70196419720224,-0.396095507607646,
8.78727029226991));
#388368=CARTESIAN_POINT('Ctrl Pts',(2.67951471421566,-0.403989724989084,
8.80838212259896));
#388369=CARTESIAN_POINT('Ctrl Pts',(2.65703413439439,-0.411894877373934,
8.82945686509571));
#388370=CARTESIAN_POINT('Ctrl Pts',(2.63452008471591,-0.419811799220407,
8.85049129520029));
#388371=CARTESIAN_POINT('',(2.63452008471591,-0.419811799220407,7.59394543036555));
#388372=CARTESIAN_POINT('',(2.63452008471591,-0.419811799220407,7.5));
#388373=CARTESIAN_POINT('',(2.71519273396522,-0.391443777101968,7.51860402984325));
#388374=CARTESIAN_POINT('Ctrl Pts',(2.63452008471591,-0.419811799220408,
7.59394543036555));
#388375=CARTESIAN_POINT('Ctrl Pts',(2.65103334518629,-0.414005016591717,
7.57858609112103));
#388376=CARTESIAN_POINT('Ctrl Pts',(2.66752812741711,-0.408204731718024,
7.56320440326857));
#388377=CARTESIAN_POINT('Ctrl Pts',(2.68400539982677,-0.402410604061146,
7.54780169004651));
#388378=CARTESIAN_POINT('Ctrl Pts',(2.69440807320189,-0.398752570376341,
7.53807742314383));
#388379=CARTESIAN_POINT('Ctrl Pts',(2.70480377576452,-0.395096987933239,
7.52834476460825));
#388380=CARTESIAN_POINT('Ctrl Pts',(2.71519273396522,-0.391443777101968,
7.51860402984325));
#388381=CARTESIAN_POINT('',(2.71519273396522,-0.391443777101968,7.5));
#388382=CARTESIAN_POINT('Origin',(2.63680073810824,-0.426297494642185,7.5));
#388383=CARTESIAN_POINT('Ctrl Pts',(2.63452008471591,-0.419811799220407,
8.85049129520029));
#388384=CARTESIAN_POINT('Ctrl Pts',(2.63433738950976,-0.419876042823379,
8.85097269580138));
#388385=CARTESIAN_POINT('Ctrl Pts',(2.6341597896714,-0.419947410981222,
8.85143669361005));
#388386=CARTESIAN_POINT('Ctrl Pts',(2.63397943329584,-0.420030001202715,
8.8519052845931));
#388387=CARTESIAN_POINT('Ctrl Pts',(2.63362666766303,-0.420191542438274,
8.85282181883899));
#388388=CARTESIAN_POINT('Ctrl Pts',(2.63327251305848,-0.420392039188342,
8.85372622499636));
#388389=CARTESIAN_POINT('Ctrl Pts',(2.63291900834655,-0.420648055336175,
8.85462257735071));
#388390=CARTESIAN_POINT('Ctrl Pts',(2.63262554129001,-0.420860590849272,
8.85536669723986));
#388391=CARTESIAN_POINT('Ctrl Pts',(2.63233243666767,-0.421111411701267,
8.85610498449051));
#388392=CARTESIAN_POINT('Ctrl Pts',(2.63204603916862,-0.421416096159145,
8.85681338218371));
#388393=CARTESIAN_POINT('Ctrl Pts',(2.63178613298843,-0.421692597783186,
8.85745625420285));
#388394=CARTESIAN_POINT('Ctrl Pts',(2.63152805418393,-0.42201651779045,
8.85808743050666));
#388395=CARTESIAN_POINT('Ctrl Pts',(2.63128428509418,-0.422413586267606,
8.8586680450841));
#388396=CARTESIAN_POINT('Ctrl Pts',(2.63117181532044,-0.422596785055575,
8.85893592806395));
#388397=CARTESIAN_POINT('Ctrl Pts',(2.63106252270619,-0.422795758835428,
8.85919241173848));
#388398=CARTESIAN_POINT('Ctrl Pts',(2.63095867528155,-0.423014243649973,
8.85943017985534));
#388399=CARTESIAN_POINT('Ctrl Pts',(2.63081845051617,-0.423309262828037,
8.8597512372));
#388400=CARTESIAN_POINT('Ctrl Pts',(2.6306851634031,-0.423647640448203,
8.86004599534705));
#388401=CARTESIAN_POINT('Ctrl Pts',(2.63057010575534,-0.424029128091254,
8.86026130871721));
#388402=CARTESIAN_POINT('Ctrl Pts',(2.63052797990668,-0.42416880147265,
8.86034014101235));
#388403=CARTESIAN_POINT('Ctrl Pts',(2.63048765313902,-0.424316348233914,
8.86040910639693));
#388404=CARTESIAN_POINT('Ctrl Pts',(2.63045054861005,-0.42446783723099,
8.86046313645507));
#388405=CARTESIAN_POINT('Ctrl Pts',(2.63039264730334,-0.424704234542217,
8.8605474499083));
#388406=CARTESIAN_POINT('Ctrl Pts',(2.63034115486746,-0.424956719642228,
8.86059655985668));
#388407=CARTESIAN_POINT('Ctrl Pts',(2.6302990866204,-0.425209041351474,
8.86059725258815));
#388408=CARTESIAN_POINT('Ctrl Pts',(2.63025692117888,-0.425461946024673,
8.86059794692011));
#388409=CARTESIAN_POINT('Ctrl Pts',(2.63022637650186,-0.42571792820999,
8.86056369958366));
#388410=CARTESIAN_POINT('Ctrl Pts',(2.6302053819192,-0.42596258065178,8.86048590497774));
#388411=CARTESIAN_POINT('Ctrl Pts',(2.63019990295821,-0.426026427654907,
8.86046560290182));
#388412=CARTESIAN_POINT('Ctrl Pts',(2.63019509337987,-0.426090341398209,
8.86044257503091));
#388413=CARTESIAN_POINT('Ctrl Pts',(2.63019106907053,-0.426152344430869,
8.86041778462583));
#388414=CARTESIAN_POINT('Ctrl Pts',(2.63016399046236,-0.426569547901318,
8.860250975962));
#388415=CARTESIAN_POINT('Ctrl Pts',(2.63016916344615,-0.426956246327036,
8.8599848982295));
#388416=CARTESIAN_POINT('Ctrl Pts',(2.6301979653053,-0.427301266325934,
8.85968173251461));
#388417=CARTESIAN_POINT('Ctrl Pts',(2.63021319983864,-0.427483762138062,
8.85952137522076));
#388418=CARTESIAN_POINT('Ctrl Pts',(2.63023514862655,-0.427658130768808,
8.85934740853961));
#388419=CARTESIAN_POINT('Ctrl Pts',(2.63026195976158,-0.427822107383451,
8.8591675900182));
#388420=CARTESIAN_POINT('Ctrl Pts',(2.63036962040486,-0.428480558724585,
8.85844552518696));
#388421=CARTESIAN_POINT('Ctrl Pts',(2.63055878195666,-0.429009147469412,
8.85759444184126));
#388422=CARTESIAN_POINT('Ctrl Pts',(2.63075172533839,-0.429426277073917,
8.85683498915141));
#388423=CARTESIAN_POINT('Ctrl Pts',(2.63077191634944,-0.429469928576126,
8.85675551445));
#388424=CARTESIAN_POINT('Ctrl Pts',(2.63079216490732,-0.429512347712879,
8.85667699793652));
#388425=CARTESIAN_POINT('Ctrl Pts',(2.63081239214287,-0.429553547296367,
8.85659965593547));
#388426=CARTESIAN_POINT('Ctrl Pts',(2.63108542040041,-0.430109661376531,
8.85555568965886));
#388427=CARTESIAN_POINT('Ctrl Pts',(2.63142813134851,-0.430604690778865,
8.85434650606346));
#388428=CARTESIAN_POINT('Ctrl Pts',(2.63183710943965,-0.431044620128023,
8.85297329937117));
#388429=CARTESIAN_POINT('Ctrl Pts',(2.63206713469651,-0.431292053581636,
8.85220095427747));
#388430=CARTESIAN_POINT('Ctrl Pts',(2.63231844750382,-0.43152194335517,
8.85137579139183));
#388431=CARTESIAN_POINT('Ctrl Pts',(2.63259257497231,-0.431734128529198,
8.85049129520029));
#388432=CARTESIAN_POINT('Origin',(2.63680073810824,-0.426297494642185,7.59394543036555));
#388433=CARTESIAN_POINT('Ctrl Pts',(2.6339896589008,-0.419998320072209,
7.59443877723642));
#388434=CARTESIAN_POINT('Ctrl Pts',(2.62852678336725,-0.421919305380218,
7.58783886950016));
#388435=CARTESIAN_POINT('Ctrl Pts',(2.62941353036883,-0.430362815390389,
7.58559994247159));
#388436=CARTESIAN_POINT('Ctrl Pts',(2.66381133616453,-0.409511717635095,
7.56670252222135));
#388437=CARTESIAN_POINT('Ctrl Pts',(2.65835635603704,-0.411429926574036,
7.56004874999023));
#388438=CARTESIAN_POINT('Ctrl Pts',(2.65922710860603,-0.419925698888471,
7.55786368756704));
#388439=CARTESIAN_POINT('Ctrl Pts',(2.69357732442548,-0.399044697880303,
7.53888913333558));
#388440=CARTESIAN_POINT('Ctrl Pts',(2.688089925084,-0.400974306828814,7.53222002137274));
#388441=CARTESIAN_POINT('Ctrl Pts',(2.68898568384657,-0.409506602004158,
7.53005029815327));
#388442=CARTESIAN_POINT('Ctrl Pts',(2.72328627675262,-0.388597734447536,
7.51101258149734));
#388443=CARTESIAN_POINT('Ctrl Pts',(2.7177323601603,-0.390550733762682,
7.5043616886572));
#388444=CARTESIAN_POINT('Ctrl Pts',(2.71868781310116,-0.399106117519269,
7.50217374673251));
#388445=CARTESIAN_POINT('',(2.71710286899021,-0.399661099761578,7.50366116523517));
#388446=CARTESIAN_POINT('Ctrl Pts',(2.71519273396522,-0.391443777101968,
7.51860402984325));
#388447=CARTESIAN_POINT('Ctrl Pts',(2.71560933845096,-0.391297280794034,
7.51734760759493));
#388448=CARTESIAN_POINT('Ctrl Pts',(2.71600553713428,-0.391221028165804,
7.51608817408572));
#388449=CARTESIAN_POINT('Ctrl Pts',(2.71638294247709,-0.391228307594241,
7.51481005913119));
#388450=CARTESIAN_POINT('Ctrl Pts',(2.71672480525499,-0.391234901474467,
7.51365231206383));
#388451=CARTESIAN_POINT('Ctrl Pts',(2.71705173448721,-0.391309793993965,
7.51247773061042));
#388452=CARTESIAN_POINT('Ctrl Pts',(2.71734982796114,-0.391487681960311,
7.51129758471022));
#388453=CARTESIAN_POINT('Ctrl Pts',(2.71772032410568,-0.391708776386907,
7.50983079813401));
#388454=CARTESIAN_POINT('Ctrl Pts',(2.71802777713899,-0.392093102944501,
7.50839324291155));
#388455=CARTESIAN_POINT('Ctrl Pts',(2.71821005578271,-0.392694965359655,
7.50715379678855));
#388456=CARTESIAN_POINT('Ctrl Pts',(2.71829426326387,-0.392973008453208,
7.50658120839351));
#388457=CARTESIAN_POINT('Ctrl Pts',(2.71835463339421,-0.393339757954554,
7.50598221009429));
#388458=CARTESIAN_POINT('Ctrl Pts',(2.71836728500343,-0.393790180293171,
7.50545747549611));
#388459=CARTESIAN_POINT('Ctrl Pts',(2.71837403629372,-0.394030539594932,
7.50517746087247));
#388460=CARTESIAN_POINT('Ctrl Pts',(2.71836747479092,-0.394297326408292,
7.50491486231392));
#388461=CARTESIAN_POINT('Ctrl Pts',(2.71834610674268,-0.394583434757196,
7.50468370960992));
#388462=CARTESIAN_POINT('Ctrl Pts',(2.71831415477039,-0.395011256986576,
7.50433806340446));
#388463=CARTESIAN_POINT('Ctrl Pts',(2.71824758258208,-0.39549506886164,
7.50405484070983));
#388464=CARTESIAN_POINT('Ctrl Pts',(2.71815016398296,-0.396002188896856,
7.5038576603613));
#388465=CARTESIAN_POINT('Ctrl Pts',(2.71813974657802,-0.396056417502185,
7.50383657498791));
#388466=CARTESIAN_POINT('Ctrl Pts',(2.71812899521642,-0.396110891374371,
7.50381643264937));
#388467=CARTESIAN_POINT('Ctrl Pts',(2.71811792839077,-0.396165555317011,
7.50379723213559));
#388468=CARTESIAN_POINT('Ctrl Pts',(2.71804405370937,-0.396530455015994,
7.50366906242519));
#388469=CARTESIAN_POINT('Ctrl Pts',(2.71795381025399,-0.396911618989233,
7.50358235568538));
#388470=CARTESIAN_POINT('Ctrl Pts',(2.7178579952463,-0.397276923242064,
7.5035341175365));
#388471=CARTESIAN_POINT('Ctrl Pts',(2.71771433148643,-0.397824655624726,
7.50346178989176));
#388472=CARTESIAN_POINT('Ctrl Pts',(2.71753649302519,-0.398407782609515,
7.50346967198527));
#388473=CARTESIAN_POINT('Ctrl Pts',(2.71734429645071,-0.398974860740826,
7.50354272648693));
#388474=CARTESIAN_POINT('Ctrl Pts',(2.71726524202139,-0.399208111714057,
7.50357277531559));
#388475=CARTESIAN_POINT('Ctrl Pts',(2.71718399774965,-0.399438383067811,
7.50361331098762));
#388476=CARTESIAN_POINT('Ctrl Pts',(2.71710286899161,-0.399661099761784,
7.50366116523659));
#388477=CARTESIAN_POINT('',(2.63969113251167,-0.426764791194187,7.57603338622103));
#388478=CARTESIAN_POINT('Origin',(2.64841434182012,-0.428177982248983,7.58486873427629));
#388479=CARTESIAN_POINT('Ctrl Pts',(2.71710286904233,-0.399661099737652,
7.50366116529968));
#388480=CARTESIAN_POINT('Ctrl Pts',(2.69134133975362,-0.408681709889291,
7.52783573079709));
#388481=CARTESIAN_POINT('Ctrl Pts',(2.66553865185168,-0.417715864046317,
7.55196141284068));
#388482=CARTESIAN_POINT('Ctrl Pts',(2.63969113352841,-0.426764790463517,
7.57603338728831));
#388483=CARTESIAN_POINT('Ctrl Pts',(2.63452008471591,-0.419811799220407,
7.59394543036555));
#388484=CARTESIAN_POINT('Ctrl Pts',(2.62260349002129,-0.42400219367279,
7.59394543036555));
#388485=CARTESIAN_POINT('Ctrl Pts',(2.63259257497231,-0.431734128529198,
7.59394543036555));
#388486=CARTESIAN_POINT('Ctrl Pts',(2.63231908349194,-0.42058576725028,
7.58587155981959));
#388487=CARTESIAN_POINT('Ctrl Pts',(2.62837738985167,-0.424935673020103,
7.58685956158229));
#388488=CARTESIAN_POINT('Ctrl Pts',(2.63074758579823,-0.430306036148894,
7.5858715598196));
#388489=CARTESIAN_POINT('Ctrl Pts',(2.63624690107239,-0.424282632632025,
7.57982961904599));
#388490=CARTESIAN_POINT('Ctrl Pts',(2.63431416214112,-0.425895484323621,
7.58148017275035));
#388491=CARTESIAN_POINT('Ctrl Pts',(2.63564021630889,-0.428035192411078,
7.57982961904594));
#388492=CARTESIAN_POINT('Ctrl Pts',(2.63969113169474,-0.426764791061906,
7.57603338509286));
#388493=CARTESIAN_POINT('Ctrl Pts',(2.63969113169474,-0.426764791061906,
7.57603338509286));
#388494=CARTESIAN_POINT('Ctrl Pts',(2.63969113169474,-0.426764791061906,
7.57603338509286));
#388495=CARTESIAN_POINT('Origin',(2.6484152525544,-0.428172349042147,7.58486873427623));
#388496=CARTESIAN_POINT('Ctrl Pts',(2.70702227397444,-0.489345570106521,
7.51098857897448));
#388497=CARTESIAN_POINT('Ctrl Pts',(2.70236668241661,-0.485741963688148,
7.50433767179956));
#388498=CARTESIAN_POINT('Ctrl Pts',(2.70596936051755,-0.477923475241943,
7.50214974420965));
#388499=CARTESIAN_POINT('Ctrl Pts',(2.68211158316674,-0.470063740039231,
7.53887321589167));
#388500=CARTESIAN_POINT('Ctrl Pts',(2.67751177385794,-0.466503311221007,
7.53220407452061));
#388501=CARTESIAN_POINT('Ctrl Pts',(2.68105049686829,-0.458687918756247,
7.53003438070911));
#388502=CARTESIAN_POINT('Ctrl Pts',(2.65715305464352,-0.450744881745442,
7.56669465659232));
#388503=CARTESIAN_POINT('Ctrl Pts',(2.65258042935253,-0.447205494399605,
7.56004085833298));
#388504=CARTESIAN_POINT('Ctrl Pts',(2.6560839004508,-0.439416891162163,
7.55785582193789));
#388505=CARTESIAN_POINT('Ctrl Pts',(2.63214781717912,-0.431389868939786,
7.59443891967696));
#388506=CARTESIAN_POINT('Ctrl Pts',(2.6275685621508,-0.427845349922939,
7.58783901202978));
#388507=CARTESIAN_POINT('Ctrl Pts',(2.6310707537066,-0.420111409640341,
7.58560008491213));
#388508=CARTESIAN_POINT('',(2.70461858999358,-0.476880779648988,7.50366116523517));
#388509=CARTESIAN_POINT('Ctrl Pts',(2.70461858999394,-0.476880779649052,
7.50366116523554));
#388510=CARTESIAN_POINT('Ctrl Pts',(2.70464020690383,-0.477638189858893,
7.50350835821027));
#388511=CARTESIAN_POINT('Ctrl Pts',(2.7046354365397,-0.478335136954998,
7.50345484955999));
#388512=CARTESIAN_POINT('Ctrl Pts',(2.70460473756223,-0.478992345851136,
7.50349758195598));
#388513=CARTESIAN_POINT('Ctrl Pts',(2.7045889867101,-0.479329542754738,
7.50351950684424));
#388514=CARTESIAN_POINT('Ctrl Pts',(2.70456498711403,-0.479689520295334,
7.50357029184312));
#388515=CARTESIAN_POINT('Ctrl Pts',(2.70453230288058,-0.480036006358213,
7.50365515313923));
#388516=CARTESIAN_POINT('Ctrl Pts',(2.70448202129437,-0.480569042228984,
7.50378570417639));
#388517=CARTESIAN_POINT('Ctrl Pts',(2.7044100554912,-0.481085827292566,
7.50400001621911));
#388518=CARTESIAN_POINT('Ctrl Pts',(2.70431963439798,-0.481546713552094,
7.50428903009634));
#388519=CARTESIAN_POINT('Ctrl Pts',(2.70430959835229,-0.481597868381055,
7.50432110841318));
#388520=CARTESIAN_POINT('Ctrl Pts',(2.70429934703204,-0.481648362380225,
7.50435406373354));
#388521=CARTESIAN_POINT('Ctrl Pts',(2.7042888934907,-0.481698161980479,
7.50438785222351));
#388522=CARTESIAN_POINT('Ctrl Pts',(2.70422506959627,-0.482002212476761,
7.50459414719561));
#388523=CARTESIAN_POINT('Ctrl Pts',(2.7041521866378,-0.482285112778645,
7.50483629897752));
#388524=CARTESIAN_POINT('Ctrl Pts',(2.704074311158,-0.482536353384292,7.5050991045531));
#388525=CARTESIAN_POINT('Ctrl Pts',(2.70390251002772,-0.483090615395077,
7.50567888004914));
#388526=CARTESIAN_POINT('Ctrl Pts',(2.70370013790804,-0.483512788619057,
7.50637912803144));
#388527=CARTESIAN_POINT('Ctrl Pts',(2.70349061296512,-0.483823047491796,
7.50710440483569));
#388528=CARTESIAN_POINT('Ctrl Pts',(2.70343923328946,-0.483899129126894,
7.50728225710685));
#388529=CARTESIAN_POINT('Ctrl Pts',(2.70338652163312,-0.483970077276551,
7.50746498566954));
#388530=CARTESIAN_POINT('Ctrl Pts',(2.70333404285786,-0.484034484228082,
7.50764697238949));
#388531=CARTESIAN_POINT('Ctrl Pts',(2.70305193140459,-0.484380718274245,
7.50862528291182));
#388532=CARTESIAN_POINT('Ctrl Pts',(2.70275414916696,-0.484571966827617,
7.50965856837422));
#388533=CARTESIAN_POINT('Ctrl Pts',(2.70246021538533,-0.484671589142442,
7.51067959873203));
#388534=CARTESIAN_POINT('Ctrl Pts',(2.70229846325455,-0.484726411427947,
7.51124147302579));
#388535=CARTESIAN_POINT('Ctrl Pts',(2.70213769764104,-0.484753088363596,
7.51180065547253));
#388536=CARTESIAN_POINT('Ctrl Pts',(2.70198039405431,-0.484759576290765,
7.51235175716501));
#388537=CARTESIAN_POINT('Ctrl Pts',(2.70143684749986,-0.484781994663616,
7.51425603304535));
#388538=CARTESIAN_POINT('Ctrl Pts',(2.70086957912379,-0.484559974355606,
7.51626900505178));
#388539=CARTESIAN_POINT('Ctrl Pts',(2.70030761830456,-0.484146430039385,
7.5182778896924));
#388540=CARTESIAN_POINT('Ctrl Pts',(2.70027720392306,-0.484124048239498,
7.51838661432543));
#388541=CARTESIAN_POINT('Ctrl Pts',(2.70024680297324,-0.484101095696744,
7.51849533314855));
#388542=CARTESIAN_POINT('Ctrl Pts',(2.70021641947034,-0.484077577700225,
7.51860402984325));
#388543=CARTESIAN_POINT('Ctrl Pts',(2.63969113324751,-0.426764792208446,
7.57603338728985));
#388544=CARTESIAN_POINT('Ctrl Pts',(2.66137047798472,-0.443497493271866,
7.55196141284922));
#388545=CARTESIAN_POINT('Ctrl Pts',(2.68301193102657,-0.460202048212605,
7.52783573083105));
#388546=CARTESIAN_POINT('Ctrl Pts',(2.7046185900369,-0.476880779689299,
7.50366116530176));
#388547=CARTESIAN_POINT('Origin',(9.12135307609335E-16,-1.47466962819311E-16,
7.49482233047033));
#388548=CARTESIAN_POINT('Origin',(2.70835812744774,-0.39837482787917,7.49482233047033));
#388549=CARTESIAN_POINT('Origin',(0.,0.,7.50366116523517));
#388550=CARTESIAN_POINT('Origin',(2.69591402793582,-0.475345983446682,7.49482233047033));
#388551=CARTESIAN_POINT('Ctrl Pts',(2.7151917361247,-0.391444127938779,
7.51860402984325));
#388552=CARTESIAN_POINT('Ctrl Pts',(2.72237004465167,-0.388920604068918,
7.51860402984325));
#388553=CARTESIAN_POINT('Ctrl Pts',(2.72342529733067,-0.381385172574072,
7.51860402984325));
#388554=CARTESIAN_POINT('Ctrl Pts',(2.71785709064665,-0.390507125105668,
7.51041458714366));
#388555=CARTESIAN_POINT('Ctrl Pts',(2.72262003629419,-0.387135372665372,
7.51004642900442));
#388556=CARTESIAN_POINT('Ctrl Pts',(2.72342558835683,-0.38138309439154,
7.5072913648301));
#388557=CARTESIAN_POINT('Ctrl Pts',(2.71964944662412,-0.392677654361235,
7.50215815450138));
#388558=CARTESIAN_POINT('Ctrl Pts',(2.72211116740598,-0.390770301411823,
7.4987716367153));
#388559=CARTESIAN_POINT('Ctrl Pts',(2.72261327489375,-0.387356826398718,
7.49481588533171));
#388560=CARTESIAN_POINT('Ctrl Pts',(2.71710232433262,-0.399661019647884,
7.50366171572174));
#388561=CARTESIAN_POINT('Ctrl Pts',(2.72072505953649,-0.400193891020553,
7.50000045605858));
#388562=CARTESIAN_POINT('Ctrl Pts',(2.72072505953651,-0.400193891020429,
7.49482233047317));
#388563=CARTESIAN_POINT('Origin',(2.71104609143371,-0.379651603607827,7.51860402984325));
#388564=CARTESIAN_POINT('Origin',(2.71104609143371,-0.379651603607827,9.));
#388565=CARTESIAN_POINT('Origin',(2.71104609143371,-0.379651603607827,8.75721825406948));
#388566=CARTESIAN_POINT('Ctrl Pts',(2.69943822817004,-0.396983716469034,
8.78942910404912));
#388567=CARTESIAN_POINT('Ctrl Pts',(2.70470182062058,-0.395154229323313,
8.79672699501691));
#388568=CARTESIAN_POINT('Ctrl Pts',(2.70336947938123,-0.386328224972305,
8.79893251111267));
#388569=CARTESIAN_POINT('Ctrl Pts',(2.70980999884858,-0.393336554321229,
8.78111911759582));
#388570=CARTESIAN_POINT('Ctrl Pts',(2.71604760481809,-0.391160644880441,
8.78644465894812));
#388571=CARTESIAN_POINT('Ctrl Pts',(2.71658483983411,-0.383071955844943,
8.78817647674132));
#388572=CARTESIAN_POINT('Ctrl Pts',(2.71627393371496,-0.391063555847674,
8.7678092393203));
#388573=CARTESIAN_POINT('Ctrl Pts',(2.7236354857743,-0.388490175182447,
8.76988516158376));
#388574=CARTESIAN_POINT('Ctrl Pts',(2.72483625397649,-0.381027297981203,
8.77093053738833));
#388575=CARTESIAN_POINT('Ctrl Pts',(2.71501355488061,-0.391506759440208,
8.75371302330492));
#388576=CARTESIAN_POINT('Ctrl Pts',(2.72219468292135,-0.388997257212617,
8.75300828287558));
#388577=CARTESIAN_POINT('Ctrl Pts',(2.72322678304318,-0.381425645186582,
8.75267964240737));
#388578=CARTESIAN_POINT('Origin',(2.69781755467073,-0.384303334113505,8.78727029226991));
#388579=CARTESIAN_POINT('Ctrl Pts',(2.63452008471591,-0.419811799220407,
8.85049129520029));
#388580=CARTESIAN_POINT('Ctrl Pts',(2.64002902569028,-0.417874615294201,
8.85711686593484));
#388581=CARTESIAN_POINT('Ctrl Pts',(2.63910781935456,-0.409374489353903,
8.85933012996512));
#388582=CARTESIAN_POINT('Ctrl Pts',(2.65703416460907,-0.411894866749133,
8.82945683644723));
#388583=CARTESIAN_POINT('Ctrl Pts',(2.66258883312431,-0.40994160302509,
8.8360746990239));
#388584=CARTESIAN_POINT('Ctrl Pts',(2.66162763804509,-0.401420561626453,
8.83829567148519));
#388585=CARTESIAN_POINT('Ctrl Pts',(2.67951468545064,-0.403989735104122,
8.80838214965002));
#388586=CARTESIAN_POINT('Ctrl Pts',(2.68509127528129,-0.402028762889457,
8.81501364461993));
#388587=CARTESIAN_POINT('Ctrl Pts',(2.68411351798303,-0.393479329969036,
8.81722098428722));
#388588=CARTESIAN_POINT('Ctrl Pts',(2.70196419720224,-0.396095507607646,
8.78727029226991));
#388589=CARTESIAN_POINT('Ctrl Pts',(2.70754171332274,-0.394134209669065,
8.79393457792714));
#388590=CARTESIAN_POINT('Ctrl Pts',(2.7065680531042,-0.385549840096578,
8.79610912703474));
#388591=CARTESIAN_POINT('Origin',(2.6303734421844,-0.408019625726266,8.85049129520029));
#388592=CARTESIAN_POINT('Ctrl Pts',(2.63259257497231,-0.431734128529198,
8.85049129520029));
#388593=CARTESIAN_POINT('Ctrl Pts',(2.63721044448901,-0.435308536641013,
8.85711686593484));
#388594=CARTESIAN_POINT('Ctrl Pts',(2.63365770878388,-0.443085350328085,
8.85933012996512));
#388595=CARTESIAN_POINT('Ctrl Pts',(2.62850721247053,-0.428571901269797,
8.86332496987233));
#388596=CARTESIAN_POINT('Ctrl Pts',(2.62804976815553,-0.433170013825567,
8.86648636486737));
#388597=CARTESIAN_POINT('Ctrl Pts',(2.62223922743675,-0.434225342422791,
8.87206031107457));
#388598=CARTESIAN_POINT('Ctrl Pts',(2.62961328596244,-0.421537243678529,
8.86341338519875));
#388599=CARTESIAN_POINT('Ctrl Pts',(2.63060202922409,-0.417010008606569,
8.86654584966057));
#388600=CARTESIAN_POINT('Ctrl Pts',(2.62537340940882,-0.414219724102321,
8.87215952290714));
#388601=CARTESIAN_POINT('Ctrl Pts',(2.63452008471591,-0.419811799220407,
8.85049129520029));
#388602=CARTESIAN_POINT('Ctrl Pts',(2.64002902569028,-0.417874615294201,
8.85711686593484));
#388603=CARTESIAN_POINT('Ctrl Pts',(2.63910781935456,-0.409374489353903,
8.85933012996512));
#388604=CARTESIAN_POINT('Origin',(2.62494136927062,-0.441618917414677,8.85049129520029));
#388605=CARTESIAN_POINT('Ctrl Pts',(2.68912759914127,-0.47549440548382,
8.78727029226991));
#388606=CARTESIAN_POINT('Ctrl Pts',(2.69380295177104,-0.479113307729762,
8.79393457792714));
#388607=CARTESIAN_POINT('Ctrl Pts',(2.69017388854615,-0.486953544670569,
8.79610912703474));
#388608=CARTESIAN_POINT('Ctrl Pts',(2.67030929695492,-0.460928317866537,
8.80838214965004));
#388609=CARTESIAN_POINT('Ctrl Pts',(2.67498387312222,-0.464546619100754,
8.81501364461989));
#388610=CARTESIAN_POINT('Ctrl Pts',(2.6713619303665,-0.472352408187678,
8.81722098428721));
#388611=CARTESIAN_POINT('Ctrl Pts',(2.65146500140035,-0.446342110385339,
8.82945683644723));
#388612=CARTESIAN_POINT('Ctrl Pts',(2.65612120202605,-0.449946188245605,
8.8360746990239));
#388613=CARTESIAN_POINT('Ctrl Pts',(2.65252392414128,-0.457730251086919,
8.8382956714852));
#388614=CARTESIAN_POINT('Ctrl Pts',(2.63259257497231,-0.431734128529198,
8.85049129520029));
#388615=CARTESIAN_POINT('Ctrl Pts',(2.63721044448901,-0.435308536641013,
8.85711686593484));
#388616=CARTESIAN_POINT('Ctrl Pts',(2.63365770878388,-0.443085350328085,
8.85933012996512));
#388617=CARTESIAN_POINT('Origin',(2.68147639343958,-0.485379194369299,8.78727029226991));
#388618=CARTESIAN_POINT('Ctrl Pts',(2.70006998588465,-0.483964255816424,
8.75374538247849));
#388619=CARTESIAN_POINT('Ctrl Pts',(2.70608714808813,-0.488605175704168,
8.75304829418602));
#388620=CARTESIAN_POINT('Ctrl Pts',(2.70468784035867,-0.496109346616881,
8.75272238421917));
#388621=CARTESIAN_POINT('Ctrl Pts',(2.70111380694607,-0.484772212811475,
8.76769408445016));
#388622=CARTESIAN_POINT('Ctrl Pts',(2.70728196617974,-0.489530465289032,
8.76974318093965));
#388623=CARTESIAN_POINT('Ctrl Pts',(2.70607444581406,-0.496984340244159,
8.77077869880429));
#388624=CARTESIAN_POINT('Ctrl Pts',(2.69576377481994,-0.480631085505929,
8.78108014887994));
#388625=CARTESIAN_POINT('Ctrl Pts',(2.70099338824204,-0.484660524766635,
8.7863940336633));
#388626=CARTESIAN_POINT('Ctrl Pts',(2.69897660913033,-0.492499828163205,
8.78812224174742));
#388627=CARTESIAN_POINT('Ctrl Pts',(2.6869962531754,-0.473844692043162,
8.78944554828685));
#388628=CARTESIAN_POINT('Ctrl Pts',(2.69140699401535,-0.477236119892865,
8.79673892988685));
#388629=CARTESIAN_POINT('Ctrl Pts',(2.68736801332924,-0.485185345599418,
8.79894799272499));
#388630=CARTESIAN_POINT('Origin',(2.69256521376866,-0.4939623665857,8.75721825406948));
#388631=CARTESIAN_POINT('Origin',(2.69256521376866,-0.4939623665857,9.));
#388632=CARTESIAN_POINT('Origin',(2.69256521376866,-0.4939623665857,7.51860402984325));
#388633=CARTESIAN_POINT('Ctrl Pts',(2.7046178152802,-0.476880643050886,
7.50366195182966));
#388634=CARTESIAN_POINT('Ctrl Pts',(2.70822413765239,-0.477516513051599,
7.50000065167734));
#388635=CARTESIAN_POINT('Ctrl Pts',(2.70822413765237,-0.477516513051714,
7.49482233047108));
#388636=CARTESIAN_POINT('Ctrl Pts',(2.70483396261146,-0.484317516045493,
7.50215800491338));
#388637=CARTESIAN_POINT('Ctrl Pts',(2.70656871882112,-0.486905047314359,
7.49877273257269));
#388638=CARTESIAN_POINT('Ctrl Pts',(2.70596930723901,-0.490304732903523,
7.49481816995649));
#388639=CARTESIAN_POINT('Ctrl Pts',(2.7024455167135,-0.485802555618879,
7.51043025814041));
#388640=CARTESIAN_POINT('Ctrl Pts',(2.70590829471323,-0.490503824119134,
7.51006209594513));
#388641=CARTESIAN_POINT('Ctrl Pts',(2.70485957523923,-0.496220392812597,
7.50731281821699));
#388642=CARTESIAN_POINT('Ctrl Pts',(2.70021522421894,-0.484076652645348,
7.51860402984326));
#388643=CARTESIAN_POINT('Ctrl Pts',(2.70623307096702,-0.488733533351057,
7.51860402984326));
#388644=CARTESIAN_POINT('Ctrl Pts',(2.70486003209637,-0.496217902506188,
7.51860402984327));
#388645=CARTESIAN_POINT('Origin',(0.,0.,7.5));
#388646=CARTESIAN_POINT('Origin',(2.59952233059431,-0.599517869856861,7.5));
#388647=CARTESIAN_POINT('',(2.59952233059431,-0.599517869856861,7.59394543036555));
#388648=CARTESIAN_POINT('',(2.59952233059431,-0.599517869856861,8.85049129520029));
#388649=CARTESIAN_POINT('',(2.59952233059431,-0.599517869856861,7.5));
#388650=CARTESIAN_POINT('',(2.65313746692185,-0.646810448064325,8.78727029226991));
#388651=CARTESIAN_POINT('Ctrl Pts',(2.59952233059431,-0.599517869856862,
8.85049129520029));
#388652=CARTESIAN_POINT('Ctrl Pts',(2.61742002096782,-0.615304977373503,
8.82945686509571));
#388653=CARTESIAN_POINT('Ctrl Pts',(2.63529110426045,-0.631068615445882,
8.80838212259897));
#388654=CARTESIAN_POINT('Ctrl Pts',(2.65313746692185,-0.646810448064325,
8.78727029226991));
#388655=CARTESIAN_POINT('',(2.66365357834826,-0.656086448390676,8.75721825406948));
#388656=CARTESIAN_POINT('Origin',(2.63200708449507,-0.628171594201918,8.75937679713125));
#388657=CARTESIAN_POINT('',(2.66365357834826,-0.656086448390676,7.51860402984325));
#388658=CARTESIAN_POINT('',(2.66365357834826,-0.656086448390676,7.5));
#388659=CARTESIAN_POINT('Ctrl Pts',(2.66365357834826,-0.656086448390676,
7.51860402984325));
#388660=CARTESIAN_POINT('Ctrl Pts',(2.65539480838751,-0.648801592825264,
7.52834476460825));
#388661=CARTESIAN_POINT('Ctrl Pts',(2.64713067695249,-0.641512008036736,
7.53807742314407));
#388662=CARTESIAN_POINT('Ctrl Pts',(2.63886100402454,-0.634217535235136,
7.54780169004674));
#388663=CARTESIAN_POINT('Ctrl Pts',(2.62576228904436,-0.62266348455002,
7.5632044032688));
#388664=CARTESIAN_POINT('Ctrl Pts',(2.61264965451768,-0.611097155779176,
7.57858609112103));
#388665=CARTESIAN_POINT('Ctrl Pts',(2.59952233059431,-0.599517869856862,
7.59394543036555));
#388666=CARTESIAN_POINT('Origin',(2.86694941950356,-0.513326427708308,7.5));
#388667=CARTESIAN_POINT('',(2.68453419038077,-0.564602509634883,8.75721825406948));
#388668=CARTESIAN_POINT('',(2.67103479566854,-0.568397127400913,8.78727029226991));
#388669=CARTESIAN_POINT('Origin',(2.63676829686558,-0.57802928261299,8.75658640621034));
#388670=CARTESIAN_POINT('',(2.60220974632392,-0.587743532225588,8.85049129520029));
#388671=CARTESIAN_POINT('Ctrl Pts',(2.67103479566854,-0.568397127400913,
8.78727029226991));
#388672=CARTESIAN_POINT('Ctrl Pts',(2.64812565330825,-0.574836781952687,
8.80838212259896));
#388673=CARTESIAN_POINT('Ctrl Pts',(2.62518477739698,-0.581285356659693,
8.82945686509571));
#388674=CARTESIAN_POINT('Ctrl Pts',(2.60220974632392,-0.587743532225588,
8.85049129520029));
#388675=CARTESIAN_POINT('',(2.60220974632392,-0.587743532225588,7.59394543036555));
#388676=CARTESIAN_POINT('',(2.60220974632392,-0.587743532225588,7.5));
#388677=CARTESIAN_POINT('',(2.68453419038077,-0.564602509634883,7.51860402984325));
#388678=CARTESIAN_POINT('Ctrl Pts',(2.60220974632392,-0.587743532225589,
7.59394543036555));
#388679=CARTESIAN_POINT('Ctrl Pts',(2.61906112037002,-0.58300668848552,
7.57858609112103));
#388680=CARTESIAN_POINT('Ctrl Pts',(2.6358936378295,-0.578275145245242,
7.56320440326857));
#388681=CARTESIAN_POINT('Ctrl Pts',(2.65270828694938,-0.573548624713022,
7.54780169004651));
#388682=CARTESIAN_POINT('Ctrl Pts',(2.66332395793925,-0.570564608422276,
7.53807742314383));
#388683=CARTESIAN_POINT('Ctrl Pts',(2.67393251538732,-0.567582591715406,
7.52834476460825));
#388684=CARTESIAN_POINT('Ctrl Pts',(2.68453419038077,-0.564602509634883,
7.51860402984325));
#388685=CARTESIAN_POINT('',(2.68453419038077,-0.564602509634883,7.5));
#388686=CARTESIAN_POINT('Origin',(2.60407017393685,-0.594362024055079,7.5));
#388687=CARTESIAN_POINT('Ctrl Pts',(2.60220974632392,-0.587743532225589,
8.85049129520029));
#388688=CARTESIAN_POINT('Ctrl Pts',(2.60202331038289,-0.58779593851114,
8.85097269580138));
#388689=CARTESIAN_POINT('Ctrl Pts',(2.60184150286887,-0.587855781174737,
8.85143669361005));
#388690=CARTESIAN_POINT('Ctrl Pts',(2.60165622548117,-0.587926646233105,
8.8519052845931));
#388691=CARTESIAN_POINT('Ctrl Pts',(2.60129383466069,-0.588065253793175,
8.85282181883899));
#388692=CARTESIAN_POINT('Ctrl Pts',(2.60092756183387,-0.588242647837744,
8.85372622499635));
#388693=CARTESIAN_POINT('Ctrl Pts',(2.60055838042438,-0.588475488848286,
8.85462257735071));
#388694=CARTESIAN_POINT('Ctrl Pts',(2.6002518991303,-0.588668785185507,
8.85536669723986));
#388695=CARTESIAN_POINT('Ctrl Pts',(2.59994332657568,-0.588900311421531,
8.85610498449051));
#388696=CARTESIAN_POINT('Ctrl Pts',(2.59963799631076,-0.589186020321747,
8.85681338218371));
#388697=CARTESIAN_POINT('Ctrl Pts',(2.59936090861582,-0.589445301597408,
8.85745625420284));
#388698=CARTESIAN_POINT('Ctrl Pts',(2.59908260643578,-0.5897520209105,8.85808743050666));
#388699=CARTESIAN_POINT('Ctrl Pts',(2.59881389793109,-0.590132655228678,
8.8586680450841));
#388700=CARTESIAN_POINT('Ctrl Pts',(2.59868992165192,-0.590308271651945,
8.85893592806396));
#388701=CARTESIAN_POINT('Ctrl Pts',(2.59856810529722,-0.59049983421699,
8.85919241173848));
#388702=CARTESIAN_POINT('Ctrl Pts',(2.59845047286813,-0.590711216603711,
8.85943017985534));
#388703=CARTESIAN_POINT('Ctrl Pts',(2.59829163426593,-0.590996645401669,
8.8597512372));
#388704=CARTESIAN_POINT('Ctrl Pts',(2.59813694107697,-0.591325788054068,
8.86004599534705));
#388705=CARTESIAN_POINT('Ctrl Pts',(2.59799767783027,-0.59169912012104,
8.86026130871721));
#388706=CARTESIAN_POINT('Ctrl Pts',(2.59794668962941,-0.591835807516104,
8.86034014101235));
#388707=CARTESIAN_POINT('Ctrl Pts',(2.59789699236397,-0.591980467381848,
8.86040910639692));
#388708=CARTESIAN_POINT('Ctrl Pts',(2.59785025813687,-0.592129267833198,
8.86046313645506));
#388709=CARTESIAN_POINT('Ctrl Pts',(2.59777732976686,-0.592361469691337,
8.86054744990829));
#388710=CARTESIAN_POINT('Ctrl Pts',(2.59770976635182,-0.592610136901937,
8.86059655985669));
#388711=CARTESIAN_POINT('Ctrl Pts',(2.59765161823107,-0.592859244867328,
8.86059725258816));
#388712=CARTESIAN_POINT('Ctrl Pts',(2.59759333576493,-0.593108928371637,
8.86059794692011));
#388713=CARTESIAN_POINT('Ctrl Pts',(2.5975464530103,-0.593362427609925,
8.86056369958366));
#388714=CARTESIAN_POINT('Ctrl Pts',(2.59750982662749,-0.593605232259505,
8.86048590497774));
#388715=CARTESIAN_POINT('Ctrl Pts',(2.59750026823208,-0.59366859704388,
8.86046560290182));
#388716=CARTESIAN_POINT('Ctrl Pts',(2.59749137356795,-0.593732071318801,
8.86044257503091));
#388717=CARTESIAN_POINT('Ctrl Pts',(2.59748338497903,-0.593793689121195,
8.86041778462583));
#388718=CARTESIAN_POINT('Ctrl Pts',(2.59742963168864,-0.594208300469986,
8.86025097596201));
#388719=CARTESIAN_POINT('Ctrl Pts',(2.59741001819078,-0.594594535816525,
8.8599848982295));
#388720=CARTESIAN_POINT('Ctrl Pts',(2.5974166553662,-0.594940692276284,
8.85968173251462));
#388721=CARTESIAN_POINT('Ctrl Pts',(2.59742016605173,-0.595123789211096,
8.85952137522077));
#388722=CARTESIAN_POINT('Ctrl Pts',(2.59743089790697,-0.595299205846458,
8.85934740853961));
#388723=CARTESIAN_POINT('Ctrl Pts',(2.59744714793787,-0.595464563348879,
8.8591675900182));
#388724=CARTESIAN_POINT('Ctrl Pts',(2.59751240025854,-0.596128559672226,
8.85844552518695));
#388725=CARTESIAN_POINT('Ctrl Pts',(2.59766730636048,-0.59666818199703,
8.85759444184123));
#388726=CARTESIAN_POINT('Ctrl Pts',(2.59783312773383,-0.597096816488941,
8.85683498915137));
#388727=CARTESIAN_POINT('Ctrl Pts',(2.59785048049893,-0.597141671946968,
8.85675551444997));
#388728=CARTESIAN_POINT('Ctrl Pts',(2.59786796965055,-0.597185301258604,
8.85667699793651));
#388729=CARTESIAN_POINT('Ctrl Pts',(2.59788551566069,-0.597227712156552,
8.85659965593547));
#388730=CARTESIAN_POINT('Ctrl Pts',(2.59812235260095,-0.597800176621216,
8.85555568965886));
#388731=CARTESIAN_POINT('Ctrl Pts',(2.59843264276995,-0.598316146498386,
8.85434650606346));
#388732=CARTESIAN_POINT('Ctrl Pts',(2.59881259420155,-0.59878137528178,
8.85297329937118));
#388733=CARTESIAN_POINT('Ctrl Pts',(2.59902629373105,-0.599043038125634,
8.85220095427748));
#388734=CARTESIAN_POINT('Ctrl Pts',(2.59926236110088,-0.599288557232821,
8.85137579139184));
#388735=CARTESIAN_POINT('Ctrl Pts',(2.59952233059431,-0.599517869856861,
8.85049129520029));
#388736=CARTESIAN_POINT('Origin',(2.60407017393685,-0.594362024055079,7.59394543036555));
#388737=CARTESIAN_POINT('Ctrl Pts',(2.60166845989353,-0.587895685351639,
7.59443877723642));
#388738=CARTESIAN_POINT('Ctrl Pts',(2.59609373047239,-0.589462716152146,
7.58783886950016));
#388739=CARTESIAN_POINT('Ctrl Pts',(2.59643767801339,-0.597945692140895,
7.58559994247159));
#388740=CARTESIAN_POINT('Ctrl Pts',(2.63210074424794,-0.579341310186399,
7.56670252222136));
#388741=CARTESIAN_POINT('Ctrl Pts',(2.62653407189352,-0.580906076182544,
7.56004874999027));
#388742=CARTESIAN_POINT('Ctrl Pts',(2.62685870940684,-0.589440182330275,
7.55786368756705));
#388743=CARTESIAN_POINT('Ctrl Pts',(2.66247619935189,-0.570802909462089,
7.5388891333356));
#388744=CARTESIAN_POINT('Ctrl Pts',(2.6568764439911,-0.572376974939164,
7.53222002137279));
#388745=CARTESIAN_POINT('Ctrl Pts',(2.65722369629234,-0.580949131059928,
7.53005029815326));
#388746=CARTESIAN_POINT('Ctrl Pts',(2.69279345069543,-0.562280869547134,
7.51101258149734));
#388747=CARTESIAN_POINT('Ctrl Pts',(2.68712581612466,-0.563874015557904,
7.5043616886572));
#388748=CARTESIAN_POINT('Ctrl Pts',(2.68753116066568,-0.572473037441103,
7.50217374673251));
#388749=CARTESIAN_POINT('',(2.68591391515804,-0.572925331695027,7.50366116523517));
#388750=CARTESIAN_POINT('Ctrl Pts',(2.68453419038077,-0.564602509634882,
7.51860402984325));
#388751=CARTESIAN_POINT('Ctrl Pts',(2.6849593249586,-0.564483006260371,
7.51734760759493));
#388752=CARTESIAN_POINT('Ctrl Pts',(2.68535959513189,-0.564432294838141,
7.51608817408573));
#388753=CARTESIAN_POINT('Ctrl Pts',(2.68573575866036,-0.564463739753546,
7.5148100591312));
#388754=CARTESIAN_POINT('Ctrl Pts',(2.68607649657317,-0.564492223309321,
7.51365231206384));
#388755=CARTESIAN_POINT('Ctrl Pts',(2.68639795571402,-0.564587908381932,
7.51247773061043));
#388756=CARTESIAN_POINT('Ctrl Pts',(2.68668403940181,-0.564784529772823,
7.51129758471022));
#388757=CARTESIAN_POINT('Ctrl Pts',(2.68703960875373,-0.565028907706691,
7.50983079813402));
#388758=CARTESIAN_POINT('Ctrl Pts',(2.68732180620472,-0.56543214320763,
7.50839324291155));
#388759=CARTESIAN_POINT('Ctrl Pts',(2.68746514888008,-0.566044447664703,
7.50715379678855));
#388760=CARTESIAN_POINT('Ctrl Pts',(2.68753136906577,-0.566327314680742,
7.50658120839351));
#388761=CARTESIAN_POINT('Ctrl Pts',(2.68756811743797,-0.566697178583436,
7.50598221009429));
#388762=CARTESIAN_POINT('Ctrl Pts',(2.68755188439479,-0.567147486072437,
7.50545747549611));
#388763=CARTESIAN_POINT('Ctrl Pts',(2.68754322194049,-0.567387784086888,
7.50517746087247));
#388764=CARTESIAN_POINT('Ctrl Pts',(2.68751958082918,-0.567653602361198,
7.50491486231392));
#388765=CARTESIAN_POINT('Ctrl Pts',(2.68747992565903,-0.567937753814264,
7.50468370960993));
#388766=CARTESIAN_POINT('Ctrl Pts',(2.68742062867114,-0.568362649867092,
7.50433806340447));
#388767=CARTESIAN_POINT('Ctrl Pts',(2.68732319532928,-0.568841202404014,
7.50405484070984));
#388768=CARTESIAN_POINT('Ctrl Pts',(2.68719348559491,-0.569341038875649,
7.50385766036131));
#388769=CARTESIAN_POINT('Ctrl Pts',(2.68717961515497,-0.569394488617071,
7.50383657498791));
#388770=CARTESIAN_POINT('Ctrl Pts',(2.68716539573022,-0.569448161724747,
7.50381643264937));
#388771=CARTESIAN_POINT('Ctrl Pts',(2.68715084931172,-0.569502004300505,
7.50379723213559));
#388772=CARTESIAN_POINT('Ctrl Pts',(2.68705374720979,-0.569861421106833,
7.50366906242519));
#388773=CARTESIAN_POINT('Ctrl Pts',(2.68693926790965,-0.570236020019771,
7.50358235568538));
#388774=CARTESIAN_POINT('Ctrl Pts',(2.68682024464033,-0.570594434827216,
7.5035341175365));
#388775=CARTESIAN_POINT('Ctrl Pts',(2.68664178271882,-0.571131837266257,
7.50346178989176));
#388776=CARTESIAN_POINT('Ctrl Pts',(2.68642694857157,-0.571702372004782,
7.50346967198527));
#388777=CARTESIAN_POINT('Ctrl Pts',(2.68619881406495,-0.572255970936448,
7.50354272648692));
#388778=CARTESIAN_POINT('Ctrl Pts',(2.68610497762027,-0.57248367763586,
7.50357277531559));
#388779=CARTESIAN_POINT('Ctrl Pts',(2.68600914673731,-0.572708270534058,
7.50361331098761));
#388780=CARTESIAN_POINT('Ctrl Pts',(2.68591391515943,-0.572925331695323,
7.50366116523658));
#388781=CARTESIAN_POINT('',(2.6069246899221,-0.595013548701457,7.57603338622103));
#388782=CARTESIAN_POINT('Origin',(2.61553943300004,-0.596982734143167,7.58486873427627));
#388783=CARTESIAN_POINT('Ctrl Pts',(2.68591391521158,-0.572925331674489,
7.50366116529968));
#388784=CARTESIAN_POINT('Ctrl Pts',(2.65962736327094,-0.580276861166546,
7.52783573079709));
#388785=CARTESIAN_POINT('Ctrl Pts',(2.63329886951445,-0.587639269794973,
7.55196141284068));
#388786=CARTESIAN_POINT('Ctrl Pts',(2.60692469098357,-0.595013548037431,
7.57603338728831));
#388787=CARTESIAN_POINT('Ctrl Pts',(2.6032473619073,-0.587634493602723,
7.59639677331372));
#388788=CARTESIAN_POINT('Ctrl Pts',(2.58509102396104,-0.589736708654588,
7.59959882295462));
#388789=CARTESIAN_POINT('Ctrl Pts',(2.60025825567991,-0.599967246010105,
7.59642833564546));
#388790=CARTESIAN_POINT('Ctrl Pts',(2.59935086420696,-0.587454466507662,
7.58707626057423));
#388791=CARTESIAN_POINT('Ctrl Pts',(2.59437047150332,-0.592048808631775,
7.58809943920598));
#388792=CARTESIAN_POINT('Ctrl Pts',(2.5967579751915,-0.598374488589822,
7.58710240504251));
#388793=CARTESIAN_POINT('Ctrl Pts',(2.6033867930582,-0.591997253160062,
7.58015376756929));
#388794=CARTESIAN_POINT('Ctrl Pts',(2.6010574740276,-0.593641498959718,
7.5820588065976));
#388795=CARTESIAN_POINT('Ctrl Pts',(2.60238830315171,-0.596122621463801,
7.58020924244129));
#388796=CARTESIAN_POINT('Ctrl Pts',(2.60692468911533,-0.595013548517107,
7.57603338509286));
#388797=CARTESIAN_POINT('Ctrl Pts',(2.60692468911533,-0.595013548517107,
7.57603338509286));
#388798=CARTESIAN_POINT('Ctrl Pts',(2.60692468911533,-0.595013548517107,
7.57603338509286));
#388799=CARTESIAN_POINT('Origin',(2.61554070278287,-0.596977170861152,7.58486873427624));
#388800=CARTESIAN_POINT('Ctrl Pts',(2.67010792806202,-0.661779669736821,
7.51098857897448));
#388801=CARTESIAN_POINT('Ctrl Pts',(2.66569278577231,-0.65788518253907,
7.50433767179956));
#388802=CARTESIAN_POINT('Ctrl Pts',(2.66978899405937,-0.650313582394355,
7.50214974420965));
#388803=CARTESIAN_POINT('Ctrl Pts',(2.64648381003428,-0.640941422817449,
7.53887321589167));
#388804=CARTESIAN_POINT('Ctrl Pts',(2.64212156898467,-0.637093598487795,
7.5322040745206));
#388805=CARTESIAN_POINT('Ctrl Pts',(2.64615375522351,-0.629520990346774,
7.53003438070911));
#388806=CARTESIAN_POINT('Ctrl Pts',(2.62281432498536,-0.620063158777086,
7.56669465659232));
#388807=CARTESIAN_POINT('Ctrl Pts',(2.61847786396932,-0.616238074373868,
7.560040858333));
#388808=CARTESIAN_POINT('Ctrl Pts',(2.62247315433322,-0.608689941821077,
7.55785582193789));
#388809=CARTESIAN_POINT('Ctrl Pts',(2.59910054339133,-0.599145821856049,
7.59443891967696));
#388810=CARTESIAN_POINT('Ctrl Pts',(2.59475779504673,-0.59531519155666,
7.58783901202978));
#388811=CARTESIAN_POINT('Ctrl Pts',(2.5987483062296,-0.587821527667229,
7.58560008491213));
#388812=CARTESIAN_POINT('',(2.66850780457432,-0.649186484966709,7.50366116523517));
#388813=CARTESIAN_POINT('Ctrl Pts',(2.66850780457468,-0.649186484966797,
7.50366116523554));
#388814=CARTESIAN_POINT('Ctrl Pts',(2.66848084963155,-0.649943723996302,
7.50350835821027));
#388815=CARTESIAN_POINT('Ctrl Pts',(2.66843143551488,-0.650638933501571,
7.50345484956));
#388816=CARTESIAN_POINT('Ctrl Pts',(2.66835869209321,-0.651292825201307,
7.50349758195598));
#388817=CARTESIAN_POINT('Ctrl Pts',(2.6683213693231,-0.651628320137145,
7.50351950684424));
#388818=CARTESIAN_POINT('Ctrl Pts',(2.66827435519656,-0.651986020405876,
7.50357029184312));
#388819=CARTESIAN_POINT('Ctrl Pts',(2.6682195386781,-0.652329700489952,
7.50365515313924));
#388820=CARTESIAN_POINT('Ctrl Pts',(2.6681352086753,-0.652858419629069,
7.50378570417639));
#388821=CARTESIAN_POINT('Ctrl Pts',(2.66803028020088,-0.653369532037473,
7.50400001621911));
#388822=CARTESIAN_POINT('Ctrl Pts',(2.66791051580347,-0.653823678057418,
7.50428903009635));
#388823=CARTESIAN_POINT('Ctrl Pts',(2.66789722287677,-0.653874084771641,
7.50432110841318));
#388824=CARTESIAN_POINT('Ctrl Pts',(2.66788375745731,-0.65392381822113,
7.50435406373355));
#388825=CARTESIAN_POINT('Ctrl Pts',(2.66787013472256,-0.653972845742071,
7.50438785222352));
#388826=CARTESIAN_POINT('Ctrl Pts',(2.66778696137898,-0.654272182323043,
7.50459414719561));
#388827=CARTESIAN_POINT('Ctrl Pts',(2.66769610268179,-0.654549831748733,
7.50483629897752));
#388828=CARTESIAN_POINT('Ctrl Pts',(2.66760229016465,-0.654795566654488,
7.5050991045531));
#388829=CARTESIAN_POINT('Ctrl Pts',(2.66739533032926,-0.655337682538318,
7.50567888004914));
#388830=CARTESIAN_POINT('Ctrl Pts',(2.66716632527347,-0.655746022335905,
7.50637912803144));
#388831=CARTESIAN_POINT('Ctrl Pts',(2.66693735246779,-0.656042219439331,
7.50710440483569));
#388832=CARTESIAN_POINT('Ctrl Pts',(2.66688120379009,-0.656114852849427,
7.50728225710685));
#388833=CARTESIAN_POINT('Ctrl Pts',(2.66682405477194,-0.656182277981084,
7.50746498566954));
#388834=CARTESIAN_POINT('Ctrl Pts',(2.6667675572524,-0.656243190274951,
7.50764697238949));
#388835=CARTESIAN_POINT('Ctrl Pts',(2.66646384213587,-0.65657063800326,
7.50862528291182));
#388836=CARTESIAN_POINT('Ctrl Pts',(2.6661544183869,-0.656742414642496,
7.50965856837422));
#388837=CARTESIAN_POINT('Ctrl Pts',(2.66585470570012,-0.656822999870543,
7.51067959873202));
#388838=CARTESIAN_POINT('Ctrl Pts',(2.66568977343055,-0.656867346023182,
7.51124147302578));
#388839=CARTESIAN_POINT('Ctrl Pts',(2.66552762893009,-0.656883667859983,
7.51180065547253));
#388840=CARTESIAN_POINT('Ctrl Pts',(2.66537023285753,-0.656880063981605,
7.512351757165));
#388841=CARTESIAN_POINT('Ctrl Pts',(2.66482636672769,-0.656867611146191,
7.51425603304535));
#388842=CARTESIAN_POINT('Ctrl Pts',(2.66427448875531,-0.656609701993072,
7.51626900505179));
#388843=CARTESIAN_POINT('Ctrl Pts',(2.66374017842016,-0.656161002394689,
7.51827788969243));
#388844=CARTESIAN_POINT('Ctrl Pts',(2.66371126053511,-0.656136717924499,
7.51838661432545));
#388845=CARTESIAN_POINT('Ctrl Pts',(2.66368239262177,-0.656111864744666,
7.51849533314856));
#388846=CARTESIAN_POINT('Ctrl Pts',(2.66365357834825,-0.65608644839068,
7.51860402984325));
#388847=CARTESIAN_POINT('Ctrl Pts',(2.60692469059145,-0.595013549760779,
7.57603338728985));
#388848=CARTESIAN_POINT('Ctrl Pts',(2.62748742495179,-0.613100872081639,
7.55196141284922));
#388849=CARTESIAN_POINT('Ctrl Pts',(2.6480141487976,-0.631157678379778,
7.52783573083104));
#388850=CARTESIAN_POINT('Ctrl Pts',(2.66850780461497,-0.649186485009713,
7.50366116530176));
#388851=CARTESIAN_POINT('Origin',(9.00812987045925E-16,-2.05604685939121E-16,
7.49482233047033));
#388852=CARTESIAN_POINT('Origin',(2.67726955234741,-0.571081425081853,7.49482233047033));
#388853=CARTESIAN_POINT('Origin',(0.,0.,7.50366116523517));
#388854=CARTESIAN_POINT('Origin',(2.65991946170317,-0.647097138961931,7.49482233047033));
#388855=CARTESIAN_POINT('Ctrl Pts',(2.68453317211224,-0.564602795819,7.51860402984325));
#388856=CARTESIAN_POINT('Ctrl Pts',(2.69185841476393,-0.562544372605989,
7.51860402984325));
#388857=CARTESIAN_POINT('Ctrl Pts',(2.69339429606666,-0.555092033734601,
7.51860402984325));
#388858=CARTESIAN_POINT('Ctrl Pts',(2.68725308435511,-0.563838488009249,
7.51041458714365));
#388859=CARTESIAN_POINT('Ctrl Pts',(2.69222227294058,-0.560778826171352,
7.51004642900443));
#388860=CARTESIAN_POINT('Ctrl Pts',(2.69339471964448,-0.555089978468018,
7.5072913648301));
#388861=CARTESIAN_POINT('Ctrl Pts',(2.68890269145811,-0.566119394321436,
7.50215815450138));
#388862=CARTESIAN_POINT('Ctrl Pts',(2.69148155889366,-0.564373683225253,
7.49877163671529));
#388863=CARTESIAN_POINT('Ctrl Pts',(2.69220133684272,-0.560999391699851,
7.49481588533171));
#388864=CARTESIAN_POINT('Ctrl Pts',(2.68591337675242,-0.572925216849604,
7.50366171572174));
#388865=CARTESIAN_POINT('Ctrl Pts',(2.6894945274722,-0.573689102822331,
7.50000045605858));
#388866=CARTESIAN_POINT('Ctrl Pts',(2.68949452747223,-0.57368910282221,
7.49482233047317));
#388867=CARTESIAN_POINT('Origin',(2.6811515947209,-0.552568888126717,7.51860402984325));
#388868=CARTESIAN_POINT('Origin',(2.6811515947209,-0.552568888126717,9.));
#388869=CARTESIAN_POINT('Origin',(2.6811515947209,-0.552568888126717,8.75721825406948));
#388870=CARTESIAN_POINT('Ctrl Pts',(2.66845710877349,-0.569121671950379,
8.78942910404912));
#388871=CARTESIAN_POINT('Ctrl Pts',(2.67382710225269,-0.567633183208407,
8.7967269950169));
#388872=CARTESIAN_POINT('Ctrl Pts',(2.67306298249164,-0.558739949433627,
8.79893251111267));
#388873=CARTESIAN_POINT('Ctrl Pts',(2.67904124401792,-0.566146524917328,
8.78111911759582));
#388874=CARTESIAN_POINT('Ctrl Pts',(2.68540544515353,-0.564374730902475,
8.78644465894816));
#388875=CARTESIAN_POINT('Ctrl Pts',(2.68645982044843,-0.556337081711761,
8.78817647674132));
#388876=CARTESIAN_POINT('Ctrl Pts',(2.68563752954907,-0.564292342291746,
8.76780923932029));
#388877=CARTESIAN_POINT('Ctrl Pts',(2.69314883357549,-0.562195905172935,
8.76988516158372));
#388878=CARTESIAN_POINT('Ctrl Pts',(2.69482528285461,-0.554825294736144,
8.77093053738833));
#388879=CARTESIAN_POINT('Ctrl Pts',(2.68435134414655,-0.564653882525788,
8.75371302330492));
#388880=CARTESIAN_POINT('Ctrl Pts',(2.69167850214931,-0.562609632792947,
8.75300828287559));
#388881=CARTESIAN_POINT('Ctrl Pts',(2.69319359655887,-0.555119704337719,
8.75267964240738));
#388882=CARTESIAN_POINT('Origin',(2.66765220000866,-0.556363505892747,8.78727029226991));
#388883=CARTESIAN_POINT('Ctrl Pts',(2.60220974632392,-0.587743532225588,
8.85049129520029));
#388884=CARTESIAN_POINT('Ctrl Pts',(2.60783148438852,-0.58616328751161,
8.85711686593484));
#388885=CARTESIAN_POINT('Ctrl Pts',(2.60745677570887,-0.577621604099115,
8.85933012996512));
#388886=CARTESIAN_POINT('Ctrl Pts',(2.62518480823033,-0.58128534799258,
8.82945683644723));
#388887=CARTESIAN_POINT('Ctrl Pts',(2.63085321011983,-0.57969198629205,
8.8360746990239));
#388888=CARTESIAN_POINT('Ctrl Pts',(2.63043993491586,-0.571126868306674,
8.8382956714852));
#388889=CARTESIAN_POINT('Ctrl Pts',(2.64812562395425,-0.574836790203962,
8.80838214965002));
#388890=CARTESIAN_POINT('Ctrl Pts',(2.65381639600414,-0.573237140354229,
8.81501364461987));
#388891=CARTESIAN_POINT('Ctrl Pts',(2.65338841166109,-0.564642628035467,
8.81722098428721));
#388892=CARTESIAN_POINT('Ctrl Pts',(2.67103479566854,-0.568397127400913,
8.78727029226991));
#388893=CARTESIAN_POINT('Ctrl Pts',(2.67672651297436,-0.566797211844082,
8.79393457792714));
#388894=CARTESIAN_POINT('Ctrl Pts',(2.67630485569207,-0.558168097155164,
8.79610912703474));
#388895=CARTESIAN_POINT('Origin',(2.59882715066404,-0.575709910717423,8.85049129520029));
#388896=CARTESIAN_POINT('Ctrl Pts',(2.59952233059431,-0.599517869856861,
8.85049129520029));
#388897=CARTESIAN_POINT('Ctrl Pts',(2.6039016990888,-0.603380801879633,
8.85711686593484));
#388898=CARTESIAN_POINT('Ctrl Pts',(2.59985800069653,-0.610914012710764,
8.85933012996512));
#388899=CARTESIAN_POINT('Ctrl Pts',(2.59564796650409,-0.596100389658331,
8.86332496987232));
#388900=CARTESIAN_POINT('Ctrl Pts',(2.59489685997457,-0.600659746340801,
8.86648636486738));
#388901=CARTESIAN_POINT('Ctrl Pts',(2.58903064249949,-0.601340624030181,
8.87206031107456));
#388902=CARTESIAN_POINT('Ctrl Pts',(2.59720247950873,-0.589151051897485,
8.86341338519876));
#388903=CARTESIAN_POINT('Ctrl Pts',(2.59847925223829,-0.584696467513797,
8.86654584966059));
#388904=CARTESIAN_POINT('Ctrl Pts',(2.59344014932518,-0.58157691712656,
8.87215952290715));
#388905=CARTESIAN_POINT('Ctrl Pts',(2.60220974632392,-0.587743532225589,
8.85049129520029));
#388906=CARTESIAN_POINT('Ctrl Pts',(2.60783148438852,-0.58616328751161,
8.85711686593484));
#388907=CARTESIAN_POINT('Ctrl Pts',(2.60745677570887,-0.577621604099115,
8.85933012996512));
#388908=CARTESIAN_POINT('Origin',(2.59125352451697,-0.608892134951009,8.85049129520029));
#388909=CARTESIAN_POINT('Ctrl Pts',(2.65313746692185,-0.646810448064325,
8.78727029226991));
#388910=CARTESIAN_POINT('Ctrl Pts',(2.65757134967523,-0.650721465758954,
8.79393457792714));
#388911=CARTESIAN_POINT('Ctrl Pts',(2.65344741704446,-0.658313079212961,
8.79610912703474));
#388912=CARTESIAN_POINT('Ctrl Pts',(2.63529108139351,-0.63106859527552,
8.80838214965003));
#388913=CARTESIAN_POINT('Ctrl Pts',(2.63972422778674,-0.634978963445167,
8.81501364461996));
#388914=CARTESIAN_POINT('Ctrl Pts',(2.63560960807689,-0.642536656032114,
8.81722098428721));
#388915=CARTESIAN_POINT('Ctrl Pts',(2.61742004498719,-0.615304998560392,
8.82945683644724));
#388916=CARTESIAN_POINT('Ctrl Pts',(2.62183576488801,-0.619199995254531,
8.83607469902391));
#388917=CARTESIAN_POINT('Ctrl Pts',(2.61774715137787,-0.626737586518466,
8.8382956714852));
#388918=CARTESIAN_POINT('Ctrl Pts',(2.59952233059431,-0.599517869856861,
8.85049129520029));
#388919=CARTESIAN_POINT('Ctrl Pts',(2.6039016990888,-0.603380801879633,
8.85711686593484));
#388920=CARTESIAN_POINT('Ctrl Pts',(2.59985800069653,-0.610914012710764,
8.85933012996512));
#388921=CARTESIAN_POINT('Origin',(2.64486866084451,-0.656184713158474,8.78727029226991));
#388922=CARTESIAN_POINT('Ctrl Pts',(2.66351470618409,-0.655963977306794,
8.75374538247849));
#388923=CARTESIAN_POINT('Ctrl Pts',(2.66922216072437,-0.660980882832925,
8.75304829418602));
#388924=CARTESIAN_POINT('Ctrl Pts',(2.66734493414156,-0.668379981667633,
8.75272238421917));
#388925=CARTESIAN_POINT('Ctrl Pts',(2.66450461662079,-0.656837152112578,
8.76769408445016));
#388926=CARTESIAN_POINT('Ctrl Pts',(2.6703552404268,-0.661980823569088,
8.76974318093967));
#388927=CARTESIAN_POINT('Ctrl Pts',(2.66867262963315,-0.669342017643224,
8.7707786988043));
#388928=CARTESIAN_POINT('Ctrl Pts',(2.65943089964688,-0.652361755461981,
8.78108014887994));
#388929=CARTESIAN_POINT('Ctrl Pts',(2.6643916012075,-0.656717978289939,
8.78639403366328));
#388930=CARTESIAN_POINT('Ctrl Pts',(2.66187669989166,-0.664411959515576,
8.78812224174741));
#388931=CARTESIAN_POINT('Ctrl Pts',(2.65111619753791,-0.645027568331975,
8.78944554828685));
#388932=CARTESIAN_POINT('Ctrl Pts',(2.65530058650937,-0.648694625265325,
8.79673892988685));
#388933=CARTESIAN_POINT('Ctrl Pts',(2.65076059570257,-0.656368740054055,
8.79894799272499));
#388934=CARTESIAN_POINT('Origin',(2.65538477227092,-0.665460713484825,8.75721825406948));
#388935=CARTESIAN_POINT('Origin',(2.65538477227092,-0.665460713484825,9.));
#388936=CARTESIAN_POINT('Origin',(2.65538477227092,-0.665460713484825,7.51860402984325));
#388937=CARTESIAN_POINT('Ctrl Pts',(2.66850704020454,-0.649186299013206,
7.50366195182966));
#388938=CARTESIAN_POINT('Ctrl Pts',(2.67206521266982,-0.650051920418514,
7.50000065167735));
#388939=CARTESIAN_POINT('Ctrl Pts',(2.67206521266979,-0.650051920418627,
7.49482233047108));
#388940=CARTESIAN_POINT('Ctrl Pts',(2.6682462613492,-0.656621740761695,
7.50215800491337));
#388941=CARTESIAN_POINT('Ctrl Pts',(2.66981166961859,-0.659315101882027,
7.49877273257266));
#388942=CARTESIAN_POINT('Ctrl Pts',(2.66899567098828,-0.662669398020607,
7.49481816995647));
#388943=CARTESIAN_POINT('Ctrl Pts',(2.66576757595735,-0.657950700907921,
7.51043025814041));
#388944=CARTESIAN_POINT('Ctrl Pts',(2.66892202800129,-0.662864171096018,
7.51006209594513));
#388945=CARTESIAN_POINT('Ctrl Pts',(2.6675092014202,-0.668501802798599,
7.50731281821699));
#388946=CARTESIAN_POINT('Ctrl Pts',(2.66365244482109,-0.656085448656407,
7.51860402984325));
#388947=CARTESIAN_POINT('Ctrl Pts',(2.66935955988638,-0.661118326066217,
7.51860402984324));
#388948=CARTESIAN_POINT('Ctrl Pts',(2.66750981689316,-0.668499346879738,
7.51860402984325));
#388949=CARTESIAN_POINT('Origin',(0.,0.,7.5));
#388950=CARTESIAN_POINT('Origin',(2.55577009136411,-0.764838063661105,7.5));
#388951=CARTESIAN_POINT('',(2.55577009136411,-0.764838063661105,7.59394543036555));
#388952=CARTESIAN_POINT('',(2.55577009136411,-0.764838063661105,8.85049129520029));
#388953=CARTESIAN_POINT('',(2.55577009136411,-0.764838063661105,7.5));
#388954=CARTESIAN_POINT('',(2.60624502375466,-0.81546860777333,8.78727029226991));
#388955=CARTESIAN_POINT('Ctrl Pts',(2.55577009136411,-0.764838063661105,
8.85049129520029));
#388956=CARTESIAN_POINT('Ctrl Pts',(2.57261952556178,-0.78173944383157,
8.82945686509571));
#388957=CARTESIAN_POINT('Ctrl Pts',(2.58944391103811,-0.798615698056724,
8.80838212259895));
#388958=CARTESIAN_POINT('Ctrl Pts',(2.60624502375466,-0.81546860777333,
8.78727029226991));
#388959=CARTESIAN_POINT('',(2.61614521332083,-0.825399319134594,8.75721825406948));
#388960=CARTESIAN_POINT('Origin',(2.58635225143055,-0.795514221183445,8.75937679713058));
#388961=CARTESIAN_POINT('',(2.61614521332083,-0.825399319134594,7.51860402984325));
#388962=CARTESIAN_POINT('',(2.61614521332083,-0.825399319134594,7.5));
#388963=CARTESIAN_POINT('Ctrl Pts',(2.61614521332084,-0.825399319134594,
7.51860402984325));
#388964=CARTESIAN_POINT('Ctrl Pts',(2.60837015418733,-0.817600289878085,
7.52834476460825));
#388965=CARTESIAN_POINT('Ctrl Pts',(2.60059004759763,-0.809796197604318,
7.53807742314407));
#388966=CARTESIAN_POINT('Ctrl Pts',(2.59280472407668,-0.801986872315757,
7.54780169004674));
#388967=CARTESIAN_POINT('Ctrl Pts',(2.58047319238032,-0.789617323116697,
7.5632044032688));
#388968=CARTESIAN_POINT('Ctrl Pts',(2.56812855639631,-0.777234629230145,
7.57858609112103));
#388969=CARTESIAN_POINT('Ctrl Pts',(2.55577009136411,-0.764838063661105,
7.59394543036555));
#388970=CARTESIAN_POINT('Origin',(2.82817002729664,-0.695957823489667,7.5));
#388971=CARTESIAN_POINT('',(2.64284431997728,-0.735441169348851,8.75721825406948));
#388972=CARTESIAN_POINT('',(2.62912953922427,-0.73836308147689,8.78727029226991));
#388973=CARTESIAN_POINT('Origin',(2.59431631031598,-0.745779984276522,8.75658640621069));
#388974=CARTESIAN_POINT('',(2.55920636991204,-0.753260100986265,8.85049129520029));
#388975=CARTESIAN_POINT('Ctrl Pts',(2.62912953922427,-0.73836308147689,
8.78727029226991));
#388976=CARTESIAN_POINT('Ctrl Pts',(2.60585487607023,-0.743321711277145,
8.80838212259895));
#388977=CARTESIAN_POINT('Ctrl Pts',(2.58254797304888,-0.748287209729622,
8.82945686509571));
#388978=CARTESIAN_POINT('Ctrl Pts',(2.55920636991204,-0.753260100986265,
8.85049129520029));
#388979=CARTESIAN_POINT('',(2.55920636991204,-0.753260100986265,7.59394543036555));
#388980=CARTESIAN_POINT('',(2.55920636991204,-0.753260100986265,7.5));
#388981=CARTESIAN_POINT('',(2.64284431997728,-0.735441169348851,7.51860402984325));
#388982=CARTESIAN_POINT('Ctrl Pts',(2.55920636991204,-0.753260100986265,
7.59394543036555));
#388983=CARTESIAN_POINT('Ctrl Pts',(2.5763266116233,-0.749612660841797,
7.57858609112103));
#388984=CARTESIAN_POINT('Ctrl Pts',(2.59342769588663,-0.74596930216102,
7.56320440326857));
#388985=CARTESIAN_POINT('Ctrl Pts',(2.61051062671677,-0.742329811040161,
7.54780169004651));
#388986=CARTESIAN_POINT('Ctrl Pts',(2.62129567325224,-0.740032074106483,
7.53807742314383));
#388987=CARTESIAN_POINT('Ctrl Pts',(2.63207349274766,-0.737735876882134,
7.52834476460825));
#388988=CARTESIAN_POINT('Ctrl Pts',(2.64284431997728,-0.735441169348852,
7.51860402984325));
#388989=CARTESIAN_POINT('',(2.64284431997728,-0.735441169348851,7.5));
#388990=CARTESIAN_POINT('Origin',(2.56063892684945,-0.75998419242088,7.5));
#388991=CARTESIAN_POINT('Ctrl Pts',(2.55920636991204,-0.753260100986265,
8.85049129520029));
#388992=CARTESIAN_POINT('Ctrl Pts',(2.5590169593414,-0.753300454605728,
8.85097269580138));
#388993=CARTESIAN_POINT('Ctrl Pts',(2.5588316912378,-0.753348525868738,
8.85143669361005));
#388994=CARTESIAN_POINT('Ctrl Pts',(2.55864225418249,-0.753407374564256,
8.8519052845931));
#388995=CARTESIAN_POINT('Ctrl Pts',(2.55827172731595,-0.753522478880641,
8.85282181883899));
#388996=CARTESIAN_POINT('Ctrl Pts',(2.55789484136048,-0.753676041269533,
8.85372622499636));
#388997=CARTESIAN_POINT('Ctrl Pts',(2.55751150029902,-0.753884750349128,
8.85462257735071));
#388998=CARTESIAN_POINT('Ctrl Pts',(2.55719326416478,-0.754058013214361,
8.85536669723986));
#388999=CARTESIAN_POINT('Ctrl Pts',(2.55687049166869,-0.754269293443448,
8.85610498449051));
#389000=CARTESIAN_POINT('Ctrl Pts',(2.55654748330547,-0.754534852746846,
8.85681338218371));
#389001=CARTESIAN_POINT('Ctrl Pts',(2.55625435270854,-0.754775848231751,
8.85745625420285));
#389002=CARTESIAN_POINT('Ctrl Pts',(2.55595697075632,-0.755064106475223,
8.85808743050666));
#389003=CARTESIAN_POINT('Ctrl Pts',(2.55566442701757,-0.755426742526368,
8.85866804508411));
#389004=CARTESIAN_POINT('Ctrl Pts',(2.55552945367809,-0.755594054939378,
8.85893592806396));
#389005=CARTESIAN_POINT('Ctrl Pts',(2.55539561415247,-0.755777419117943,
8.85919241173848));
#389006=CARTESIAN_POINT('Ctrl Pts',(2.5552646800958,-0.755980830461269,
8.85943017985534));
#389007=CARTESIAN_POINT('Ctrl Pts',(2.55508788035868,-0.756255495990965,
8.8597512372));
#389008=CARTESIAN_POINT('Ctrl Pts',(2.55491241676132,-0.756574051157839,
8.86004599534705));
#389009=CARTESIAN_POINT('Ctrl Pts',(2.55474952017824,-0.756937693547188,
8.86026130871721));
#389010=CARTESIAN_POINT('Ctrl Pts',(2.55468987914664,-0.757070833278094,
8.86034014101235));
#389011=CARTESIAN_POINT('Ctrl Pts',(2.55463101560014,-0.7572120118099,8.86040910639693));
#389012=CARTESIAN_POINT('Ctrl Pts',(2.55457484371587,-0.757357512262553,
8.86046313645507));
#389013=CARTESIAN_POINT('Ctrl Pts',(2.55448718796089,-0.757584564500361,
8.8605474499083));
#389014=CARTESIAN_POINT('Ctrl Pts',(2.55440383119924,-0.757828391994643,
8.86059655985668));
#389015=CARTESIAN_POINT('Ctrl Pts',(2.5543298421479,-0.758073262578114,
8.86059725258816));
#389016=CARTESIAN_POINT('Ctrl Pts',(2.55425568215229,-0.758318698910459,
8.86059794692011));
#389017=CARTESIAN_POINT('Ctrl Pts',(2.55419265397135,-0.758568673518972,
8.86056369958366));
#389018=CARTESIAN_POINT('Ctrl Pts',(2.55414054629406,-0.758808632639955,
8.86048590497774));
#389019=CARTESIAN_POINT('Ctrl Pts',(2.55412694774172,-0.758871254826088,
8.86046560290182));
#389020=CARTESIAN_POINT('Ctrl Pts',(2.55411400454188,-0.758934028803215,
8.86044257503091));
#389021=CARTESIAN_POINT('Ctrl Pts',(2.55410208450022,-0.758995008174577,
8.86041778462583));
#389022=CARTESIAN_POINT('Ctrl Pts',(2.5540218774114,-0.759405323674745,
8.86025097596201));
#389023=CARTESIAN_POINT('Ctrl Pts',(2.55397755802796,-0.759789508818218,
8.8599848982295));
#389024=CARTESIAN_POINT('Ctrl Pts',(2.55396200324607,-0.760135379307695,
8.85968173251461));
#389025=CARTESIAN_POINT('Ctrl Pts',(2.55395377565762,-0.760318324980611,
8.85952137522076));
#389026=CARTESIAN_POINT('Ctrl Pts',(2.5539532464807,-0.760494068796009,
8.85934740853961));
#389027=CARTESIAN_POINT('Ctrl Pts',(2.55395886863261,-0.760660127696761,
8.8591675900182));
#389028=CARTESIAN_POINT('Ctrl Pts',(2.55398144449489,-0.761326940498993,
8.85844552518694));
#389029=CARTESIAN_POINT('Ctrl Pts',(2.55410145860458,-0.761875378979886,
8.85759444184121));
#389030=CARTESIAN_POINT('Ctrl Pts',(2.55423947657395,-0.762313757008132,
8.85683498915135));
#389031=CARTESIAN_POINT('Ctrl Pts',(2.55425391978687,-0.762359632101284,
8.85675551444996));
#389032=CARTESIAN_POINT('Ctrl Pts',(2.55426857766555,-0.762404292305608,
8.8566769979365));
#389033=CARTESIAN_POINT('Ctrl Pts',(2.55428337034997,-0.762447740242545,
8.85659965593547));
#389034=CARTESIAN_POINT('Ctrl Pts',(2.55448304275915,-0.763034202712432,
8.85555568965886));
#389035=CARTESIAN_POINT('Ctrl Pts',(2.55475963710019,-0.763568992833538,
8.85434650606346));
#389036=CARTESIAN_POINT('Ctrl Pts',(2.55510900057033,-0.764057609326306,
8.85297329937117));
#389037=CARTESIAN_POINT('Ctrl Pts',(2.55530549623526,-0.764332426331648,
8.85220095427747));
#389038=CARTESIAN_POINT('Ctrl Pts',(2.55552534811616,-0.764592565881812,
8.85137579139183));
#389039=CARTESIAN_POINT('Ctrl Pts',(2.55577009136411,-0.764838063661105,
8.85049129520029));
#389040=CARTESIAN_POINT('Origin',(2.56063892684945,-0.75998419242088,7.59394543036555));
#389041=CARTESIAN_POINT('Ctrl Pts',(2.55865644712842,-0.753377261156732,
7.59443877723642));
#389042=CARTESIAN_POINT('Ctrl Pts',(2.55299277157866,-0.75458389818405,
7.58783886950016));
#389043=CARTESIAN_POINT('Ctrl Pts',(2.55279250630485,-0.763071481783448,
7.58559994247159));
#389044=CARTESIAN_POINT('Ctrl Pts',(2.5895742857894,-0.746790265025826,
7.56670252222135));
#389045=CARTESIAN_POINT('Ctrl Pts',(2.58391879585876,-0.747995158120077,
7.56004874999028));
#389046=CARTESIAN_POINT('Ctrl Pts',(2.58369598431129,-0.756532529628371,
7.55786368756704));
#389047=CARTESIAN_POINT('Ctrl Pts',(2.62043438847577,-0.740215569452069,
7.5388891333356));
#389048=CARTESIAN_POINT('Ctrl Pts',(2.61474528769158,-0.741427623284978,
7.5322200213728));
#389049=CARTESIAN_POINT('Ctrl Pts',(2.61454260659734,-0.750004415522975,
7.53005029815327));
#389050=CARTESIAN_POINT('Ctrl Pts',(2.65123535874696,-0.733653471944896,
7.51101258149734));
#389051=CARTESIAN_POINT('Ctrl Pts',(2.64547729572389,-0.734880218072603,
7.5043616886572));
#389052=CARTESIAN_POINT('Ctrl Pts',(2.6453308662174,-0.743487542857012,
7.50217374673251));
#389053=CARTESIAN_POINT('',(2.64368796492176,-0.743835290548446,7.50366116523517));
#389054=CARTESIAN_POINT('Ctrl Pts',(2.64284431997728,-0.735441169348851,
7.51860402984325));
#389055=CARTESIAN_POINT('Ctrl Pts',(2.64327623767801,-0.735349149972762,
7.51734760759494));
#389056=CARTESIAN_POINT('Ctrl Pts',(2.64367893454528,-0.735324188140642,
7.51608817408573));
#389057=CARTESIAN_POINT('Ctrl Pts',(2.64405231052279,-0.735379669329115,
7.5148100591312));
#389058=CARTESIAN_POINT('Ctrl Pts',(2.64439052340533,-0.735429925515399,
7.51365231206384));
#389059=CARTESIAN_POINT('Ctrl Pts',(2.64470519151025,-0.735546009950635,
7.51247773061043));
#389060=CARTESIAN_POINT('Ctrl Pts',(2.64497808983265,-0.7357605568066,7.51129758471022));
#389061=CARTESIAN_POINT('Ctrl Pts',(2.64531727128122,-0.736027214046389,
7.50983079813402));
#389062=CARTESIAN_POINT('Ctrl Pts',(2.64557305354003,-0.736447701509509,
7.50839324291155));
#389063=CARTESIAN_POINT('Ctrl Pts',(2.64567687122123,-0.737067931918148,
7.50715379678855));
#389064=CARTESIAN_POINT('Ctrl Pts',(2.6457248319985,-0.73735446049543,7.50658120839351));
#389065=CARTESIAN_POINT('Ctrl Pts',(2.64573780760563,-0.737725918949358,
7.50598221009429));
#389066=CARTESIAN_POINT('Ctrl Pts',(2.64569275661509,-0.73817426117868,
7.50545747549611));
#389067=CARTESIAN_POINT('Ctrl Pts',(2.64566871601209,-0.738413510469735,
7.50517746087247));
#389068=CARTESIAN_POINT('Ctrl Pts',(2.64562809243867,-0.73867726790069,
7.50491486231392));
#389069=CARTESIAN_POINT('Ctrl Pts',(2.64557031309822,-0.738958294818646,
7.50468370960992));
#389070=CARTESIAN_POINT('Ctrl Pts',(2.64548391475877,-0.739378518705906,
7.50433806340446));
#389071=CARTESIAN_POINT('Ctrl Pts',(2.64535602063784,-0.739849845429672,
7.50405484070983));
#389072=CARTESIAN_POINT('Ctrl Pts',(2.64519455277334,-0.740340344402456,
7.50385766036131));
#389073=CARTESIAN_POINT('Ctrl Pts',(2.64517728629502,-0.740392795643512,
7.50383657498791));
#389074=CARTESIAN_POINT('Ctrl Pts',(2.64515965723779,-0.740445447432358,
7.50381643264937));
#389075=CARTESIAN_POINT('Ctrl Pts',(2.64514169100079,-0.740498247390535,
7.50379723213559));
#389076=CARTESIAN_POINT('Ctrl Pts',(2.64502176049169,-0.740850704383455,
7.50366906242519));
#389077=CARTESIAN_POINT('Ctrl Pts',(2.6448835157668,-0.741217198928807,
7.50358235568538));
#389078=CARTESIAN_POINT('Ctrl Pts',(2.644741773328,-0.741567251487542,7.5035341175365));
#389079=CARTESIAN_POINT('Ctrl Pts',(2.64452924658315,-0.742092115681066,
7.50346178989176));
#389080=CARTESIAN_POINT('Ctrl Pts',(2.6442782995495,-0.742647713723708,
7.50346967198527));
#389081=CARTESIAN_POINT('Ctrl Pts',(2.64401516456436,-0.74318555859897,
7.50354272648692));
#389082=CARTESIAN_POINT('Ctrl Pts',(2.64390693169839,-0.743406785328894,
7.50357277531559));
#389083=CARTESIAN_POINT('Ctrl Pts',(2.64379690799386,-0.743624776871144,
7.50361331098761));
#389084=CARTESIAN_POINT('Ctrl Pts',(2.64368796492313,-0.74383529054883,
7.50366116523659));
#389085=CARTESIAN_POINT('',(2.56344583459805,-0.76081726790711,7.57603338622103));
#389086=CARTESIAN_POINT('Origin',(2.57191671161794,-0.763334355930191,7.58486873427627));
#389087=CARTESIAN_POINT('Ctrl Pts',(2.64368796497651,-0.743835290531381,
7.50366116529969));
#389088=CARTESIAN_POINT('Ctrl Pts',(2.6169844074643,-0.749487530352269,
7.52783573079709));
#389089=CARTESIAN_POINT('Ctrl Pts',(2.59023829728154,-0.755147939735823,
7.55196141284068));
#389090=CARTESIAN_POINT('Ctrl Pts',(2.56344583569989,-0.760817267312457,
7.57603338728831));
#389091=CARTESIAN_POINT('Ctrl Pts',(2.5602488397315,-0.753217766653626,
7.59639677331372));
#389092=CARTESIAN_POINT('Ctrl Pts',(2.54199511654789,-0.754152381912878,
7.59959882295465));
#389093=CARTESIAN_POINT('Ctrl Pts',(2.5564757127837,-0.76533366740497,7.59642833564546));
#389094=CARTESIAN_POINT('Ctrl Pts',(2.55637188217916,-0.752788459978709,
7.58707626057422));
#389095=CARTESIAN_POINT('Ctrl Pts',(2.55110736171589,-0.757054267678081,
7.58809943920599));
#389096=CARTESIAN_POINT('Ctrl Pts',(2.55308467231526,-0.763519918734743,
7.58710240504252));
#389097=CARTESIAN_POINT('Ctrl Pts',(2.56010846144155,-0.757580495838072,
7.58015376756929));
#389098=CARTESIAN_POINT('Ctrl Pts',(2.55767858105665,-0.75907212337566,
7.5820588065976));
#389099=CARTESIAN_POINT('Ctrl Pts',(2.55884770978496,-0.761633414662241,
7.58020924244128));
#389100=CARTESIAN_POINT('Ctrl Pts',(2.56344583380475,-0.760817267671448,
7.57603338509286));
#389101=CARTESIAN_POINT('Ctrl Pts',(2.56344583380475,-0.760817267671448,
7.57603338509286));
#389102=CARTESIAN_POINT('Ctrl Pts',(2.56344583380475,-0.760817267671448,
7.57603338509286));
#389103=CARTESIAN_POINT('Origin',(2.57191833523284,-0.763328885433835,7.58486873427623));
#389104=CARTESIAN_POINT('Ctrl Pts',(2.62222153593684,-0.831494374752881,
7.51098857897448));
#389105=CARTESIAN_POINT('Ctrl Pts',(2.61806498568195,-0.827325010059011,
7.50433767179956));
#389106=CARTESIAN_POINT('Ctrl Pts',(2.62263789195665,-0.820031411544884,
7.50214974420965));
#389107=CARTESIAN_POINT('Ctrl Pts',(2.59998106725742,-0.809185339807828,
7.53887321589168));
#389108=CARTESIAN_POINT('Ctrl Pts',(2.59587431985113,-0.805065931502269,
7.53220407452063));
#389109=CARTESIAN_POINT('Ctrl Pts',(2.6003834002003,-0.797767225156165,
7.53003438070911));
#389110=CARTESIAN_POINT('Ctrl Pts',(2.57769788867394,-0.786833463286194,
7.56669465659233));
#389111=CARTESIAN_POINT('Ctrl Pts',(2.57361541138128,-0.782738399917892,
7.56004085833298));
#389112=CARTESIAN_POINT('Ctrl Pts',(2.57808610350575,-0.775461754945457,
7.5578558219379));
#389113=CARTESIAN_POINT('Ctrl Pts',(2.55537300796543,-0.764439756073933,
7.59443891967696));
#389114=CARTESIAN_POINT('Ctrl Pts',(2.55128461158901,-0.760338755373568,
7.58783901202978));
#389115=CARTESIAN_POINT('Ctrl Pts',(2.55574704453253,-0.753116160949613,
7.58560008491213));
#389116=CARTESIAN_POINT('',(2.62143154819293,-0.81882454376764,7.50366116523517));
#389117=CARTESIAN_POINT('Ctrl Pts',(2.62143154819329,-0.818824543767751,
7.50366116523554));
#389118=CARTESIAN_POINT('Ctrl Pts',(2.62135613216078,-0.81957849995932,
7.50350835821026));
#389119=CARTESIAN_POINT('Ctrl Pts',(2.62126227734477,-0.820269115108774,
7.50345484955999));
#389120=CARTESIAN_POINT('Ctrl Pts',(2.62114778839722,-0.820917002630855,
7.50349758195598));
#389121=CARTESIAN_POINT('Ctrl Pts',(2.6210890470764,-0.821249416978274,
7.50351950684424));
#389122=CARTESIAN_POINT('Ctrl Pts',(2.62101921161052,-0.821603370108011,
7.50357029184312));
#389123=CARTESIAN_POINT('Ctrl Pts',(2.62094248805989,-0.821942831958098,
7.50365515313924));
#389124=CARTESIAN_POINT('Ctrl Pts',(2.62082445617058,-0.822465061745213,
7.50378570417639));
#389125=CARTESIAN_POINT('Ctrl Pts',(2.62068699619852,-0.822968401227922,
7.50400001621911));
#389126=CARTESIAN_POINT('Ctrl Pts',(2.62053838063451,-0.823413940824877,
7.50428903009635));
#389127=CARTESIAN_POINT('Ctrl Pts',(2.62052188545028,-0.823463392292358,
7.50432110841318));
#389128=CARTESIAN_POINT('Ctrl Pts',(2.62050526126392,-0.823512160826751,
7.50435406373354));
#389129=CARTESIAN_POINT('Ctrl Pts',(2.62048852531449,-0.823560214803777,
7.50438785222352));
#389130=CARTESIAN_POINT('Ctrl Pts',(2.62038634429887,-0.82385360743122,
7.50459414719561));
#389131=CARTESIAN_POINT('Ctrl Pts',(2.62027788322084,-0.824124865059671,
7.50483629897752));
#389132=CARTESIAN_POINT('Ctrl Pts',(2.6201685191621,-0.824364084488096,
7.5050991045531));
#389133=CARTESIAN_POINT('Ctrl Pts',(2.61992725106396,-0.82489182657452,
7.50567888004914));
#389134=CARTESIAN_POINT('Ctrl Pts',(2.61967255410297,-0.825284654989899,
7.50637912803144));
#389135=CARTESIAN_POINT('Ctrl Pts',(2.6194250743329,-0.825565573186579,
7.50710440483569));
#389136=CARTESIAN_POINT('Ctrl Pts',(2.61936438738011,-0.825634459905412,
7.50728225710685));
#389137=CARTESIAN_POINT('Ctrl Pts',(2.61930303583774,-0.825698084954741,
7.50746498566954));
#389138=CARTESIAN_POINT('Ctrl Pts',(2.61924275173434,-0.825755252289261,
7.50764697238949));
#389139=CARTESIAN_POINT('Ctrl Pts',(2.6189186809851,-0.826062568146767,
7.50862528291182));
#389140=CARTESIAN_POINT('Ctrl Pts',(2.61859888721334,-0.826214167004811,
7.50965856837422));
#389141=CARTESIAN_POINT('Ctrl Pts',(2.61829462720514,-0.826275384004091,
7.51067959873202));
#389142=CARTESIAN_POINT('Ctrl Pts',(2.61812719253885,-0.82630907179601,
7.51124147302579));
#389143=CARTESIAN_POINT('Ctrl Pts',(2.61796433543799,-0.826314971464034,
7.51180065547253));
#389144=CARTESIAN_POINT('Ctrl Pts',(2.61780749365382,-0.826301290589217,
7.51235175716501));
#389145=CARTESIAN_POINT('Ctrl Pts',(2.61726554281117,-0.82625401771691,
7.51425603304535));
#389146=CARTESIAN_POINT('Ctrl Pts',(2.61673132302745,-0.825961279522712,
7.51626900505179));
#389147=CARTESIAN_POINT('Ctrl Pts',(2.61622685877216,-0.825479268445067,
7.51827788969242));
#389148=CARTESIAN_POINT('Ctrl Pts',(2.61619955621336,-0.825453181094669,
7.51838661432544));
#389149=CARTESIAN_POINT('Ctrl Pts',(2.61617233996095,-0.825426529404801,
7.51849533314856));
#389150=CARTESIAN_POINT('Ctrl Pts',(2.61614521332083,-0.825399319134597,
7.51860402984325));
#389151=CARTESIAN_POINT('Ctrl Pts',(2.56344583519815,-0.760817269007141,
7.57603338728985));
#389152=CARTESIAN_POINT('Ctrl Pts',(2.58280746249545,-0.780184887898307,
7.55196141284922));
#389153=CARTESIAN_POINT('Ctrl Pts',(2.60213510843395,-0.799519746263608,
7.52783573083105));
#389154=CARTESIAN_POINT('Ctrl Pts',(2.62143154823075,-0.818824543813161,
7.50366116530176));
#389155=CARTESIAN_POINT('Origin',(8.85789032694965E-16,-2.62897535302342E-16,
7.49482233047033));
#389156=CARTESIAN_POINT('Origin',(2.63517950238396,-0.741441326212297,7.49482233047033));
#389157=CARTESIAN_POINT('Origin',(0.,0.,7.50366116523517));
#389158=CARTESIAN_POINT('Origin',(2.61299471585146,-0.816189233531286,7.49482233047033));
#389159=CARTESIAN_POINT('Ctrl Pts',(2.642843285465,-0.735441389704284,7.51860402984325));
#389160=CARTESIAN_POINT('Ctrl Pts',(2.65028536124811,-0.733856525650637,
7.51860402984325));
#389161=CARTESIAN_POINT('Ctrl Pts',(2.65229555990884,-0.726517902661649,
7.51860402984325));
#389162=CARTESIAN_POINT('Ctrl Pts',(2.64560657872595,-0.734852917622631,
7.51041458714366));
#389163=CARTESIAN_POINT('Ctrl Pts',(2.65076159078755,-0.732117919193931,
7.51004642900443));
#389164=CARTESIAN_POINT('Ctrl Pts',(2.65229611429776,-0.726515878756562,
7.5072913648301));
#389165=CARTESIAN_POINT('Ctrl Pts',(2.64710665836508,-0.737234828258142,
7.50215815450137));
#389166=CARTESIAN_POINT('Ctrl Pts',(2.64979207533486,-0.735657932516524,
7.49877163671529));
#389167=CARTESIAN_POINT('Ctrl Pts',(2.65072656602324,-0.732336690166488,
7.4948158853317));
#389168=CARTESIAN_POINT('Ctrl Pts',(2.64368743498052,-0.743835141443218,
7.50366171572174));
#389169=CARTESIAN_POINT('Ctrl Pts',(2.64721228549976,-0.744826903044689,
7.50000045605858));
#389170=CARTESIAN_POINT('Ctrl Pts',(2.6472122854998,-0.744826903044569,
7.49482233047317));
#389171=CARTESIAN_POINT('Origin',(2.64023967100016,-0.723215548558642,7.51860402984325));
#389172=CARTESIAN_POINT('Origin',(2.64023967100016,-0.723215548558642,9.));
#389173=CARTESIAN_POINT('Origin',(2.64023967100016,-0.723215548558642,8.75721825406948));
#389174=CARTESIAN_POINT('Ctrl Pts',(2.62651072673474,-0.738920984405465,
8.78942910404912));
#389175=CARTESIAN_POINT('Ctrl Pts',(2.63196505478754,-0.737779610586762,
8.79672699501691));
#389176=CARTESIAN_POINT('Ctrl Pts',(2.63177229643678,-0.728855691593386,
8.79893251111267));
#389177=CARTESIAN_POINT('Ctrl Pts',(2.63726373406304,-0.736630078004493,
8.78111911759583));
#389178=CARTESIAN_POINT('Ctrl Pts',(2.64372837849715,-0.735269680097221,
8.78644465894813));
#389179=CARTESIAN_POINT('Ctrl Pts',(2.64529556141671,-0.727316099175898,
8.78817647674132));
#389180=CARTESIAN_POINT('Ctrl Pts',(2.64396526470683,-0.735202330461012,
8.76780923932029));
#389181=CARTESIAN_POINT('Ctrl Pts',(2.6515954551409,-0.73359145159842,8.76988516158375));
#389182=CARTESIAN_POINT('Ctrl Pts',(2.65374069660727,-0.726343395345369,
8.77093053738833));
#389183=CARTESIAN_POINT('Ctrl Pts',(2.64265855794783,-0.735480721690193,
8.75371302330492));
#389184=CARTESIAN_POINT('Ctrl Pts',(2.65010163704873,-0.733910124712743,
8.75300828287559));
#389185=CARTESIAN_POINT('Ctrl Pts',(2.65209349989809,-0.72653265755093,
8.75267964240738));
#389186=CARTESIAN_POINT('Origin',(2.62652489024715,-0.726137460686681,8.78727029226991));
#389187=CARTESIAN_POINT('Ctrl Pts',(2.55920636991204,-0.753260100986265,
8.85049129520029));
#389188=CARTESIAN_POINT('Ctrl Pts',(2.56491780413931,-0.752043289049005,
8.85711686593484));
#389189=CARTESIAN_POINT('Ctrl Pts',(2.56509113287407,-0.74349514777364,
8.85933012996512));
#389190=CARTESIAN_POINT('Ctrl Pts',(2.58254800437418,-0.748287203055817,
8.82945683644722));
#389191=CARTESIAN_POINT('Ctrl Pts',(2.58830684695874,-0.747060290843777,
8.83607469902391));
#389192=CARTESIAN_POINT('Ctrl Pts',(2.58844318986648,-0.738486292178674,
8.83829567148519));
#389193=CARTESIAN_POINT('Ctrl Pts',(2.60585484624788,-0.743321717630749,
8.80838214965002));
#389194=CARTESIAN_POINT('Ctrl Pts',(2.61163641591406,-0.742089963450265,
8.81501364461993));
#389195=CARTESIAN_POINT('Ctrl Pts',(2.61175996320559,-0.73348568842784,
8.81722098428721));
#389196=CARTESIAN_POINT('Ctrl Pts',(2.62912953922427,-0.73836308147689,
8.78727029226991));
#389197=CARTESIAN_POINT('Ctrl Pts',(2.63491206922813,-0.737131122698014,
8.79393457792714));
#389198=CARTESIAN_POINT('Ctrl Pts',(2.63504414756231,-0.728492721775861,
8.79610912703474));
#389199=CARTESIAN_POINT('Origin',(2.55660172093492,-0.741034480196056,8.85049129520029));
#389200=CARTESIAN_POINT('Ctrl Pts',(2.55577009136411,-0.764838063661105,
8.85049129520029));
#389201=CARTESIAN_POINT('Ctrl Pts',(2.55989296307188,-0.768973645978557,
8.85711686593484));
#389202=CARTESIAN_POINT('Ctrl Pts',(2.55537491841653,-0.776232298374573,
8.85933012996512));
#389203=CARTESIAN_POINT('Ctrl Pts',(2.55212264627854,-0.761179373682616,
8.86332496987233));
#389204=CARTESIAN_POINT('Ctrl Pts',(2.55108096399232,-0.765681239117223,
8.86648636486738));
#389205=CARTESIAN_POINT('Ctrl Pts',(2.54518317530685,-0.76598486802628,
8.87206031107457));
#389206=CARTESIAN_POINT('Ctrl Pts',(2.55411921096855,-0.754343912071688,
8.86341338519876));
#389207=CARTESIAN_POINT('Ctrl Pts',(2.55567876663298,-0.749980283219023,
8.86654584966059));
#389208=CARTESIAN_POINT('Ctrl Pts',(2.55084988737681,-0.746544285850476,
8.87215952290714));
#389209=CARTESIAN_POINT('Ctrl Pts',(2.55920636991204,-0.753260100986265,
8.85049129520029));
#389210=CARTESIAN_POINT('Ctrl Pts',(2.56491780413931,-0.752043289049005,
8.85711686593484));
#389211=CARTESIAN_POINT('Ctrl Pts',(2.56509113287407,-0.74349514777364,
8.85933012996512));
#389212=CARTESIAN_POINT('Origin',(2.54691766320895,-0.773663284097878,8.85049129520029));
#389213=CARTESIAN_POINT('Ctrl Pts',(2.60624502375466,-0.81546860777333,
8.78727029226991));
#389214=CARTESIAN_POINT('Ctrl Pts',(2.61041921685634,-0.819655669706028,
8.79393457792714));
#389215=CARTESIAN_POINT('Ctrl Pts',(2.60581736094344,-0.826967464105156,
8.79610912703474));
#389216=CARTESIAN_POINT('Ctrl Pts',(2.58944388951046,-0.798615676462708,
8.80838214965002));
#389217=CARTESIAN_POINT('Ctrl Pts',(2.59361738938015,-0.802802043026193,
8.81501364461994));
#389218=CARTESIAN_POINT('Ctrl Pts',(2.58902700057123,-0.81008058293319,
8.8172209842872));
#389219=CARTESIAN_POINT('Ctrl Pts',(2.57261954817435,-0.781739466513853,
8.82945683644723));
#389220=CARTESIAN_POINT('Ctrl Pts',(2.57677664221001,-0.785909376664964,
8.83607469902389));
#389221=CARTESIAN_POINT('Ctrl Pts',(2.57221349406444,-0.793169522772234,
8.8382956714852));
#389222=CARTESIAN_POINT('Ctrl Pts',(2.55577009136411,-0.764838063661105,
8.85049129520029));
#389223=CARTESIAN_POINT('Ctrl Pts',(2.55989296307187,-0.768973645978557,
8.85711686593484));
#389224=CARTESIAN_POINT('Ctrl Pts',(2.55537491841653,-0.776232298374573,
8.85933012996512));
#389225=CARTESIAN_POINT('Origin',(2.59739259559949,-0.824293828210103,8.78727029226991));
#389226=CARTESIAN_POINT('Ctrl Pts',(2.61601447323371,-0.825268202110584,
8.75374538247849));
#389227=CARTESIAN_POINT('Ctrl Pts',(2.62138876695584,-0.830640477734179,
8.75304829418602));
#389228=CARTESIAN_POINT('Ctrl Pts',(2.61904133544637,-0.837904100006663,
8.75272238421917));
#389229=CARTESIAN_POINT('Ctrl Pts',(2.61694640529134,-0.826203006664499,
8.76769408445017));
#389230=CARTESIAN_POINT('Ctrl Pts',(2.62245545220154,-0.831710960650612,
8.76974318093966));
#389231=CARTESIAN_POINT('Ctrl Pts',(2.62030466518859,-0.838949225118367,
8.7707786988043));
#389232=CARTESIAN_POINT('Ctrl Pts',(2.61216985246104,-0.821411731033702,
8.78108014887994));
#389233=CARTESIAN_POINT('Ctrl Pts',(2.61684125757341,-0.826076836774897,
8.78639403366329));
#389234=CARTESIAN_POINT('Ctrl Pts',(2.61383856832237,-0.833593879610382,
8.78812224174741));
#389235=CARTESIAN_POINT('Ctrl Pts',(2.60434213678209,-0.813559887984529,
8.78944554828685));
#389236=CARTESIAN_POINT('Ctrl Pts',(2.60828297933323,-0.817487505278007,
8.79673892988685));
#389237=CARTESIAN_POINT('Ctrl Pts',(2.60326063420179,-0.82485497456516,
8.79894799272499));
#389238=CARTESIAN_POINT('Origin',(2.60729278516567,-0.834224539571367,8.75721825406948));
#389239=CARTESIAN_POINT('Origin',(2.60729278516567,-0.834224539571367,9.));
#389240=CARTESIAN_POINT('Origin',(2.60729278516567,-0.834224539571367,7.51860402984325));
#389241=CARTESIAN_POINT('Ctrl Pts',(2.62143079730771,-0.818824309222858,
7.50366195182966));
#389242=CARTESIAN_POINT('Ctrl Pts',(2.6249261985722,-0.819916125008732,
7.50000065167735));
#389243=CARTESIAN_POINT('Ctrl Pts',(2.62492619857216,-0.819916125008843,
7.49482233047108));
#389244=CARTESIAN_POINT('Ctrl Pts',(2.62069416386203,-0.826227765900201,
7.50215800491337));
#389245=CARTESIAN_POINT('Ctrl Pts',(2.62208379159276,-0.829015889273437,
7.49877273257264));
#389246=CARTESIAN_POINT('Ctrl Pts',(2.62105455902768,-0.832311012439098,
7.49481816995647));
#389247=CARTESIAN_POINT('Ctrl Pts',(2.61813542442623,-0.827395185636949,
7.51043025814041));
#389248=CARTESIAN_POINT('Ctrl Pts',(2.62096858819432,-0.832500667009942,
7.51006209594515));
#389249=CARTESIAN_POINT('Ctrl Pts',(2.61919746011361,-0.838036195483721,
7.50731281821699));
#389250=CARTESIAN_POINT('Ctrl Pts',(2.61614414617582,-0.825398248829051,
7.51860402984325));
#389251=CARTESIAN_POINT('Ctrl Pts',(2.62151707779834,-0.830786441770137,
7.51860402984325));
#389252=CARTESIAN_POINT('Ctrl Pts',(2.61919823167327,-0.838033784044301,
7.51860402984325));
#389253=CARTESIAN_POINT('Origin',(0.,0.,7.5));
#389254=CARTESIAN_POINT('Origin',(2.50151564461753,-0.927015373804513,7.5));
#389255=CARTESIAN_POINT('',(2.50151564461753,-0.927015373804513,7.59394543036555));
#389256=CARTESIAN_POINT('',(2.50151564461753,-0.927015373804513,8.85049129520029));
#389257=CARTESIAN_POINT('',(2.50151564461753,-0.927015373804513,7.5));
#389258=CARTESIAN_POINT('',(2.54864296074705,-0.980775832055524,8.78727029226991));
#389259=CARTESIAN_POINT('Ctrl Pts',(2.50151564461753,-0.927015373804513,
8.85049129520029));
#389260=CARTESIAN_POINT('Ctrl Pts',(2.51724758470005,-0.944961575232345,
8.82945686509571));
#389261=CARTESIAN_POINT('Ctrl Pts',(2.53295613735135,-0.962881097461731,
8.80838212259895));
#389262=CARTESIAN_POINT('Ctrl Pts',(2.54864296074705,-0.980775832055525,
8.78727029226991));
#389263=CARTESIAN_POINT('',(2.55788654645049,-0.991320447028587,8.75721825406948));
#389264=CARTESIAN_POINT('Origin',(2.53006954219644,-0.959587909595145,8.759376797131));
#389265=CARTESIAN_POINT('',(2.55788654645049,-0.991320447028587,7.51860402984325));
#389266=CARTESIAN_POINT('',(2.55788654645049,-0.991320447028587,7.5));
#389267=CARTESIAN_POINT('Ctrl Pts',(2.55788654645049,-0.991320447028587,
7.51860402984325));
#389268=CARTESIAN_POINT('Ctrl Pts',(2.55062714752995,-0.983039291965081,
7.52834476460825));
#389269=CARTESIAN_POINT('Ctrl Pts',(2.54336303591238,-0.974752760895201,
7.53807742314407));
#389270=CARTESIAN_POINT('Ctrl Pts',(2.53609405336271,-0.966460673312385,
7.54780169004674));
#389271=CARTESIAN_POINT('Ctrl Pts',(2.52458037785902,-0.953326454730298,
7.5632044032688));
#389272=CARTESIAN_POINT('Ctrl Pts',(2.51305446717487,-0.940178278873301,
7.57858609112103));
#389273=CARTESIAN_POINT('Ctrl Pts',(2.50151564461753,-0.927015373804512,
7.59394543036555));
#389274=CARTESIAN_POINT('Origin',(2.777769077807,-0.875729379291819,7.5));
#389275=CARTESIAN_POINT('',(2.59029443537467,-0.903257743546327,8.75721825406948));
#389276=CARTESIAN_POINT('',(2.57642062555681,-0.905294943272693,8.78727029226991));
#389277=CARTESIAN_POINT('Origin',(2.54120372156407,-0.910466116016109,8.75658640620982));
#389278=CARTESIAN_POINT('',(2.50568666557815,-0.915681362418202,8.85049129520029));
#389279=CARTESIAN_POINT('Ctrl Pts',(2.57642062555681,-0.905294943272693,
8.78727029226991));
#389280=CARTESIAN_POINT('Ctrl Pts',(2.55287608219231,-0.908752172247956,
8.80838212259895));
#389281=CARTESIAN_POINT('Ctrl Pts',(2.52929892512472,-0.912214190147666,
8.82945686509571));
#389282=CARTESIAN_POINT('Ctrl Pts',(2.50568666557815,-0.915681362418202,
8.85049129520029));
#389283=CARTESIAN_POINT('',(2.50568666557815,-0.915681362418202,7.59394543036555));
#389284=CARTESIAN_POINT('',(2.50568666557815,-0.915681362418202,7.5));
#389285=CARTESIAN_POINT('',(2.59029443537467,-0.903257743546327,7.51860402984325));
#389286=CARTESIAN_POINT('Ctrl Pts',(2.50568666557815,-0.915681362418202,
7.59394543036555));
#389287=CARTESIAN_POINT('Ctrl Pts',(2.5230054242091,-0.913138313983261,
7.57858609112103));
#389288=CARTESIAN_POINT('Ctrl Pts',(2.54030480325287,-0.910598111204303,
7.56320440326857));
#389289=CARTESIAN_POINT('Ctrl Pts',(2.55758581836621,-0.908060604944488,
7.54780169004651));
#389290=CARTESIAN_POINT('Ctrl Pts',(2.56849592237768,-0.906458589261801,
7.53807742314383));
#389291=CARTESIAN_POINT('Ctrl Pts',(2.57939871554832,-0.9048576470869,7.52834476460825));
#389292=CARTESIAN_POINT('Ctrl Pts',(2.59029443537467,-0.903257743546327,
7.51860402984325));
#389293=CARTESIAN_POINT('',(2.59029443537467,-0.903257743546327,7.5));
#389294=CARTESIAN_POINT('Origin',(2.50668546515631,-0.922483422723923,7.5));
#389295=CARTESIAN_POINT('Ctrl Pts',(2.50568666557815,-0.915681362418202,
8.85049129520029));
#389296=CARTESIAN_POINT('Ctrl Pts',(2.50549505870656,-0.915709497549898,
8.85097269580138));
#389297=CARTESIAN_POINT('Ctrl Pts',(2.50530709131976,-0.915745599877189,
8.85143669361005));
#389298=CARTESIAN_POINT('Ctrl Pts',(2.50511427303432,-0.915792190387944,
8.8519052845931));
#389299=CARTESIAN_POINT('Ctrl Pts',(2.5047371326961,-0.915883318472319,
8.85282181883899));
#389300=CARTESIAN_POINT('Ctrl Pts',(2.50435118231721,-0.916012418184739,
8.85372622499636));
#389301=CARTESIAN_POINT('Ctrl Pts',(2.50395525683443,-0.916196137703011,
8.85462257735071));
#389302=CARTESIAN_POINT('Ctrl Pts',(2.50362657356057,-0.916348655121979,
8.85536669723987));
#389303=CARTESIAN_POINT('Ctrl Pts',(2.50329092746444,-0.916538821148347,
8.85610498449051));
#389304=CARTESIAN_POINT('Ctrl Pts',(2.50295156831355,-0.916783139614788,
8.85681338218371));
#389305=CARTESIAN_POINT('Ctrl Pts',(2.50264359935115,-0.917004859006794,
8.85745625420285));
#389306=CARTESIAN_POINT('Ctrl Pts',(2.50232835963297,-0.917273471665691,
8.85808743050666));
#389307=CARTESIAN_POINT('Ctrl Pts',(2.50201318278514,-0.917616619300479,
8.85866804508411));
#389308=CARTESIAN_POINT('Ctrl Pts',(2.50186776701975,-0.917774940180641,
8.85893592806396));
#389309=CARTESIAN_POINT('Ctrl Pts',(2.50172245429853,-0.917949352489988,
8.85919241173848));
#389310=CARTESIAN_POINT('Ctrl Pts',(2.50157875665042,-0.918143956929082,
8.85943017985534));
#389311=CARTESIAN_POINT('Ctrl Pts',(2.5013847222864,-0.918406730530938,
8.8597512372));
#389312=CARTESIAN_POINT('Ctrl Pts',(2.5011892092982,-0.918713389200776,
8.86004599534705));
#389313=CARTESIAN_POINT('Ctrl Pts',(2.50100334875575,-0.919065847627924,
8.86026130871721));
#389314=CARTESIAN_POINT('Ctrl Pts',(2.50093529997119,-0.919194892594958,
8.86034014101235));
#389315=CARTESIAN_POINT('Ctrl Pts',(2.50086751202658,-0.919332009659955,
8.86040910639692));
#389316=CARTESIAN_POINT('Ctrl Pts',(2.50080213330745,-0.919473612221341,
8.86046313645506));
#389317=CARTESIAN_POINT('Ctrl Pts',(2.5007001103638,-0.919694581832473,
8.86054744990829));
#389318=CARTESIAN_POINT('Ctrl Pts',(2.50060130278637,-0.919932567670962,
8.86059655985668));
#389319=CARTESIAN_POINT('Ctrl Pts',(2.50051177684131,-0.92017219464676,
8.86059725258815));
#389320=CARTESIAN_POINT('Ctrl Pts',(2.50042204405556,-0.920412375256605,
8.86059794692011));
#389321=CARTESIAN_POINT('Ctrl Pts',(2.50034312944462,-0.920657798036057,
8.86056369958366));
#389322=CARTESIAN_POINT('Ctrl Pts',(2.50027575459448,-0.920893925584945,
8.86048590497774));
#389323=CARTESIAN_POINT('Ctrl Pts',(2.50025817176459,-0.92095554784484,
8.86046560290182));
#389324=CARTESIAN_POINT('Ctrl Pts',(2.50024123321541,-0.921017363572437,
8.86044257503091));
#389325=CARTESIAN_POINT('Ctrl Pts',(2.50022543070302,-0.921077453935449,
8.86041778462583));
#389326=CARTESIAN_POINT('Ctrl Pts',(2.50011909940391,-0.921481787512591,
8.86025097596201));
#389327=CARTESIAN_POINT('Ctrl Pts',(2.50005025625274,-0.921862343753837,
8.8599848982295));
#389328=CARTESIAN_POINT('Ctrl Pts',(2.50001257343147,-0.922206507017,8.85968173251461));
#389329=CARTESIAN_POINT('Ctrl Pts',(2.49999264137798,-0.92238854966501,
8.85952137522076));
#389330=CARTESIAN_POINT('Ctrl Pts',(2.49998085334339,-0.922563898491408,
8.85934740853961));
#389331=CARTESIAN_POINT('Ctrl Pts',(2.49997582451369,-0.922729976418849,
8.8591675900182));
#389332=CARTESIAN_POINT('Ctrl Pts',(2.49995563114852,-0.923396865623115,
8.85844552518695));
#389333=CARTESIAN_POINT('Ctrl Pts',(2.50004026010222,-0.923951866608731,
8.85759444184124));
#389334=CARTESIAN_POINT('Ctrl Pts',(2.50014990752216,-0.924398186783957,
8.85683498915138));
#389335=CARTESIAN_POINT('Ctrl Pts',(2.50016138183264,-0.924444893001646,
8.85675551444998));
#389336=CARTESIAN_POINT('Ctrl Pts',(2.50017314820603,-0.924490400580309,
8.85667699793651));
#389337=CARTESIAN_POINT('Ctrl Pts',(2.50018512677842,-0.924534707019351,
8.85659965593547));
#389338=CARTESIAN_POINT('Ctrl Pts',(2.50034681415976,-0.925132757594376,
8.85555568965886));
#389339=CARTESIAN_POINT('Ctrl Pts',(2.50058857608736,-0.925684170392098,
8.85434650606346));
#389340=CARTESIAN_POINT('Ctrl Pts',(2.5009059159866,-0.926194166764263,
8.85297329937118));
#389341=CARTESIAN_POINT('Ctrl Pts',(2.50108440034413,-0.926481008649071,
8.85220095427747));
#389342=CARTESIAN_POINT('Ctrl Pts',(2.50128713331755,-0.926754699673002,
8.85137579139184));
#389343=CARTESIAN_POINT('Ctrl Pts',(2.50151564461753,-0.927015373804513,
8.85049129520029));
#389344=CARTESIAN_POINT('Origin',(2.50668546515631,-0.922483422723923,7.59394543036555));
#389345=CARTESIAN_POINT('Ctrl Pts',(2.50513036619197,-0.915763048196814,
7.59443877723642));
#389346=CARTESIAN_POINT('Ctrl Pts',(2.49940101777127,-0.916604333120576,
7.58783886950016));
#389347=CARTESIAN_POINT('Ctrl Pts',(2.49865736261564,-0.925061647029031,
7.58559994247159));
#389348=CARTESIAN_POINT('Ctrl Pts',(2.5364067111286,-0.911170498480252,
7.56670252222135));
#389349=CARTESIAN_POINT('Ctrl Pts',(2.53068564324298,-0.912010567508453,
7.56004874999026));
#389350=CARTESIAN_POINT('Ctrl Pts',(2.52991629821514,-0.920516122486497,
7.55786368756704));
#389351=CARTESIAN_POINT('Ctrl Pts',(2.56762465061598,-0.906586524891429,
7.53888913333557));
#389352=CARTESIAN_POINT('Ctrl Pts',(2.56186958214379,-0.907431586490991,
7.53222002137278));
#389353=CARTESIAN_POINT('Ctrl Pts',(2.56111780051421,-0.915977770967209,
7.53005029815327));
#389354=CARTESIAN_POINT('Ctrl Pts',(2.59878277202119,-0.902011334858258,
7.51101258149734));
#389355=CARTESIAN_POINT('Ctrl Pts',(2.59295794166189,-0.902866640139928,
7.5043616886572));
#389356=CARTESIAN_POINT('Ctrl Pts',(2.59226033981814,-0.911446898481741,
7.50217374673251));
#389357=CARTESIAN_POINT('',(2.59059853376833,-0.91168867064083,7.50366116523517));
#389358=CARTESIAN_POINT('Ctrl Pts',(2.59029443537467,-0.903257743546327,
7.51860402984325));
#389359=CARTESIAN_POINT('Ctrl Pts',(2.59073136135583,-0.903193586296015,
7.51734760759494));
#389360=CARTESIAN_POINT('Ctrl Pts',(2.59113483014927,-0.903194476627528,
7.51608817408573));
#389361=CARTESIAN_POINT('Ctrl Pts',(2.59150388429384,-0.903273766104963,
7.5148100591312));
#389362=CARTESIAN_POINT('Ctrl Pts',(2.59183818235683,-0.903345588408308,
7.51365231206384));
#389363=CARTESIAN_POINT('Ctrl Pts',(2.59214476638707,-0.903481595190324,
7.51247773061043));
#389364=CARTESIAN_POINT('Ctrl Pts',(2.59240335794634,-0.903713185892312,
7.51129758471022));
#389365=CARTESIAN_POINT('Ctrl Pts',(2.59272475772225,-0.904001026686227,
7.50983079813402));
#389366=CARTESIAN_POINT('Ctrl Pts',(2.59295307372471,-0.904437038238346,
7.50839324291155));
#389367=CARTESIAN_POINT('Ctrl Pts',(2.59301693980263,-0.905062645938763,
7.50715379678855));
#389368=CARTESIAN_POINT('Ctrl Pts',(2.59304644409036,-0.905351658669903,
7.50658120839351));
#389369=CARTESIAN_POINT('Ctrl Pts',(2.59303559361286,-0.905723185272602,
7.50598221009429));
#389370=CARTESIAN_POINT('Ctrl Pts',(2.59296190979915,-0.906167719907855,
7.50545747549611));
#389371=CARTESIAN_POINT('Ctrl Pts',(2.59292258983543,-0.90640493734886,
7.50517746087247));
#389372=CARTESIAN_POINT('Ctrl Pts',(2.59286515073088,-0.906665550100599,
7.50491486231392));
#389373=CARTESIAN_POINT('Ctrl Pts',(2.59278948464783,-0.906942297683558,
7.50468370960992));
#389374=CARTESIAN_POINT('Ctrl Pts',(2.59267633998614,-0.907356122615158,
7.50433806340447));
#389375=CARTESIAN_POINT('Ctrl Pts',(2.59251851063053,-0.907818286743156,
7.50405484070984));
#389376=CARTESIAN_POINT('Ctrl Pts',(2.59232594814199,-0.908297432651594,
7.50385766036131));
#389377=CARTESIAN_POINT('Ctrl Pts',(2.59230535657694,-0.908348669858887,
7.50383657498791));
#389378=CARTESIAN_POINT('Ctrl Pts',(2.5922843903288,-0.908400083971413,
7.50381643264937));
#389379=CARTESIAN_POINT('Ctrl Pts',(2.59226307810043,-0.908451624345659,
7.50379723213559));
#389380=CARTESIAN_POINT('Ctrl Pts',(2.59212081200436,-0.908795673203785,
7.50366906242519));
#389381=CARTESIAN_POINT('Ctrl Pts',(2.59195936993194,-0.909152557376852,
7.50358235568538));
#389382=CARTESIAN_POINT('Ctrl Pts',(2.59179549077373,-0.909492809245827,
7.5035341175365));
#389383=CARTESIAN_POINT('Ctrl Pts',(2.59154977252354,-0.91000297841428,
7.50346178989176));
#389384=CARTESIAN_POINT('Ctrl Pts',(2.59126374379867,-0.910541356689506,
7.50346967198527));
#389385=CARTESIAN_POINT('Ctrl Pts',(2.5909666896131,-0.911061237388405,
7.50354272648692));
#389386=CARTESIAN_POINT('Ctrl Pts',(2.59084450507791,-0.911275075080755,
7.50357277531559));
#389387=CARTESIAN_POINT('Ctrl Pts',(2.59072074066282,-0.91148556949305,
7.50361331098761));
#389388=CARTESIAN_POINT('Ctrl Pts',(2.59059853376967,-0.9116886706413,7.50366116523659));
#389389=CARTESIAN_POINT('',(2.50943323048224,-0.923494625764139,7.57603338622103));
#389390=CARTESIAN_POINT('Origin',(2.51772543279387,-0.92654927311432,7.58486873427625));
#389391=CARTESIAN_POINT('Ctrl Pts',(2.59059853382406,-0.911688670627307,
7.50366116529968));
#389392=CARTESIAN_POINT('Ctrl Pts',(2.563587701386,-0.915618394511217,7.52783573079709));
#389393=CARTESIAN_POINT('Ctrl Pts',(2.53653388028073,-0.919553544813569,
7.55196141284068));
#389394=CARTESIAN_POINT('Ctrl Pts',(2.5094332316199,-0.923494625241301,
7.57603338728831));
#389395=CARTESIAN_POINT('Ctrl Pts',(2.50672970590158,-0.915705906336646,
7.59639677331371));
#389396=CARTESIAN_POINT('Ctrl Pts',(2.48845360594461,-0.915469081268716,
7.59959882295466));
#389397=CARTESIAN_POINT('Ctrl Pts',(2.50218806282135,-0.927555168596909,
7.59642833564546));
#389398=CARTESIAN_POINT('Ctrl Pts',(2.50288821974744,-0.915029084195087,
7.58707626057421));
#389399=CARTESIAN_POINT('Ctrl Pts',(2.49736120456837,-0.918948828350837,
7.58809943920599));
#389400=CARTESIAN_POINT('Ctrl Pts',(2.49892019688552,-0.925527881759068,
7.58710240504253));
#389401=CARTESIAN_POINT('Ctrl Pts',(2.5063100950153,-0.920050677758169,
7.5801537675693));
#389402=CARTESIAN_POINT('Ctrl Pts',(2.50378963817576,-0.921383557616306,
7.58205880659761));
#389403=CARTESIAN_POINT('Ctrl Pts',(2.50479226230758,-0.92401449278997,
7.58020924244128));
#389404=CARTESIAN_POINT('Ctrl Pts',(2.50943322970566,-0.923494625478133,
7.57603338509286));
#389405=CARTESIAN_POINT('Ctrl Pts',(2.50943322970566,-0.923494625478133,
7.57603338509286));
#389406=CARTESIAN_POINT('Ctrl Pts',(2.50943322970566,-0.923494625478133,
7.57603338509286));
#389407=CARTESIAN_POINT('Origin',(2.51772740356796,-0.926543917882699,7.58486873427622));
#389408=CARTESIAN_POINT('Ctrl Pts',(2.56355987305573,-0.997792291028094,
7.51098857897448));
#389409=CARTESIAN_POINT('Ctrl Pts',(2.55967899499225,-0.99336518165196,
7.50433767179956));
#389410=CARTESIAN_POINT('Ctrl Pts',(2.56470980820182,-0.986379555729187,
7.50214974420965));
#389411=CARTESIAN_POINT('Ctrl Pts',(2.54279444458098,-0.974104140667198,
7.53887321589167));
#389412=CARTESIAN_POINT('Ctrl Pts',(2.53896006632404,-0.969730075918102,
7.53220407452064));
#389413=CARTESIAN_POINT('Ctrl Pts',(2.54392751200519,-0.962735263316842,
7.53003438070911));
#389414=CARTESIAN_POINT('Ctrl Pts',(2.52198913882352,-0.950370500319426,
7.56669465659235));
#389415=CARTESIAN_POINT('Ctrl Pts',(2.51817742102915,-0.946022285479792,
7.56004085833302));
#389416=CARTESIAN_POINT('Ctrl Pts',(2.52310514388123,-0.939047029382757,
7.5578558219379));
#389417=CARTESIAN_POINT('Ctrl Pts',(2.50114489672401,-0.926592443362293,
7.59443891967696));
#389418=CARTESIAN_POINT('Ctrl Pts',(2.49732765241344,-0.922237924152493,
7.58783901202978));
#389419=CARTESIAN_POINT('Ctrl Pts',(2.50224367002345,-0.915316078383742,
7.58560008491213));
#389420=CARTESIAN_POINT('',(2.56358326728472,-0.985097876880914,7.50366116523517));
#389421=CARTESIAN_POINT('Ctrl Pts',(2.56358326728507,-0.985097876881048,
7.50366116523554));
#389422=CARTESIAN_POINT('Ctrl Pts',(2.56345970006384,-0.985845452066967,
7.50350835821027));
#389423=CARTESIAN_POINT('Ctrl Pts',(2.56332179021807,-0.98652863497482,
7.50345484956));
#389424=CARTESIAN_POINT('Ctrl Pts',(2.56316602620427,-0.987167856010446,
7.50349758195598));
#389425=CARTESIAN_POINT('Ctrl Pts',(2.56308610771344,-0.98749582380759,
7.50351950684424));
#389426=CARTESIAN_POINT('Ctrl Pts',(2.56299373787713,-0.987844575329,7.50357029184312));
#389427=CARTESIAN_POINT('Ctrl Pts',(2.56289542256784,-0.988178424023541,
7.50365515313924));
#389428=CARTESIAN_POINT('Ctrl Pts',(2.56274417381037,-0.988692018504435,
7.50378570417639));
#389429=CARTESIAN_POINT('Ctrl Pts',(2.56257474719319,-0.989185516731543,
7.50400001621911));
#389430=CARTESIAN_POINT('Ctrl Pts',(2.5623978911558,-0.989620619087731,
7.50428903009635));
#389431=CARTESIAN_POINT('Ctrl Pts',(2.5623782614963,-0.989668912101789,
7.50432110841318));
#389432=CARTESIAN_POINT('Ctrl Pts',(2.56235854685539,-0.989716515320723,
7.50435406373354));
#389433=CARTESIAN_POINT('Ctrl Pts',(2.56233876646288,-0.98976339828974,
7.50438785222352));
#389434=CARTESIAN_POINT('Ctrl Pts',(2.56221799765893,-0.990049641350414,
7.50459414719561));
#389435=CARTESIAN_POINT('Ctrl Pts',(2.56209237988989,-0.990313392525846,
7.50483629897752));
#389436=CARTESIAN_POINT('Ctrl Pts',(2.56196791368994,-0.990545113472999,
7.5050991045531));
#389437=CARTESIAN_POINT('Ctrl Pts',(2.56169332875141,-0.991056313156583,
7.50567888004914));
#389438=CARTESIAN_POINT('Ctrl Pts',(2.56141398648965,-0.991432015973533,
7.50637912803144));
#389439=CARTESIAN_POINT('Ctrl Pts',(2.56114901670265,-0.99169650091034,
7.50710440483569));
#389440=CARTESIAN_POINT('Ctrl Pts',(2.5610840408505,-0.991761357867607,
7.50728225710685));
#389441=CARTESIAN_POINT('Ctrl Pts',(2.56101873889053,-0.991820921385632,
7.50746498566954));
#389442=CARTESIAN_POINT('Ctrl Pts',(2.56095491592359,-0.991874108847966,
7.50764697238949));
#389443=CARTESIAN_POINT('Ctrl Pts',(2.56061182121787,-0.992160030007889,
7.50862528291181));
#389444=CARTESIAN_POINT('Ctrl Pts',(2.56028297152454,-0.992290828132516,
7.50965856837421));
#389445=CARTESIAN_POINT('Ctrl Pts',(2.55997541446454,-0.992332425349248,
7.51067959873201));
#389446=CARTESIAN_POINT('Ctrl Pts',(2.55980616542649,-0.992355316350085,
7.51124147302578));
#389447=CARTESIAN_POINT('Ctrl Pts',(2.55964326493998,-0.992350769606331,
7.51180065547252));
#389448=CARTESIAN_POINT('Ctrl Pts',(2.55948762194074,-0.992327067952724,
7.51235175716501));
#389449=CARTESIAN_POINT('Ctrl Pts',(2.55894981337755,-0.992245169297896,
7.51425603304536));
#389450=CARTESIAN_POINT('Ctrl Pts',(2.55843544700616,-0.991918804986652,
7.5162690050518));
#389451=CARTESIAN_POINT('Ctrl Pts',(2.55796290178257,-0.991405463116651,
7.51827788969244));
#389452=CARTESIAN_POINT('Ctrl Pts',(2.55793732674208,-0.991377680084565,
7.51838661432545));
#389453=CARTESIAN_POINT('Ctrl Pts',(2.55791187398801,-0.991349339402174,
7.51849533314857));
#389454=CARTESIAN_POINT('Ctrl Pts',(2.55788654645049,-0.99132044702859,
7.51860402984325));
#389455=CARTESIAN_POINT('Ctrl Pts',(2.50943323101062,-0.923494626900362,
7.57603338728985));
#389456=CARTESIAN_POINT('Ctrl Pts',(2.52751419016524,-0.944062956661477,
7.55196141284923));
#389457=CARTESIAN_POINT('Ctrl Pts',(2.54556333675353,-0.964596416013586,
7.52783573083105));
#389458=CARTESIAN_POINT('Ctrl Pts',(2.56358326731954,-0.985097876928764,
7.50366116530176));
#389459=CARTESIAN_POINT('Origin',(8.67125181207509E-16,-3.1911008230166E-16,
7.49482233047033));
#389460=CARTESIAN_POINT('Origin',(2.58226093460098,-0.908754485894666,7.49482233047033));
#389461=CARTESIAN_POINT('Origin',(0.,0.,7.50366116523517));
#389462=CARTESIAN_POINT('Origin',(2.55533261422669,-0.981927431468018,7.49482233047033));
#389463=CARTESIAN_POINT('Ctrl Pts',(2.59029338886968,-0.903257897167587,
7.51860402984325));
#389464=CARTESIAN_POINT('Ctrl Pts',(2.59782171669849,-0.902153104819651,
7.51860402984325));
#389465=CARTESIAN_POINT('Ctrl Pts',(2.60029797237974,-0.894958353689057,
7.51860402984325));
#389466=CARTESIAN_POINT('Ctrl Pts',(2.593088708184,-0.902847678972038,7.51041458714366));
#389467=CARTESIAN_POINT('Ctrl Pts',(2.59840836067142,-0.900448582647727,
7.51004642900443));
#389468=CARTESIAN_POINT('Ctrl Pts',(2.60029865530166,-0.894956369462121,
7.5072913648301));
#389469=CARTESIAN_POINT('Ctrl Pts',(2.59443309621023,-0.90532080614916,
7.50215815450137));
#389470=CARTESIAN_POINT('Ctrl Pts',(2.59721402775987,-0.903919205564955,
7.49877163671529));
#389471=CARTESIAN_POINT('Ctrl Pts',(2.5983593911649,-0.900664660087504,
7.4948158853317));
#389472=CARTESIAN_POINT('Ctrl Pts',(2.59059801446911,-0.911688487888502,
7.50366171572174));
#389473=CARTESIAN_POINT('Ctrl Pts',(2.59405208042095,-0.912904049757564,
7.50000045605858));
#389474=CARTESIAN_POINT('Ctrl Pts',(2.59405208042099,-0.912904049757446,
7.49482233047317));
#389475=CARTESIAN_POINT('Origin',(2.58847843614165,-0.890890361172289,7.51860402984325));
#389476=CARTESIAN_POINT('Origin',(2.58847843614165,-0.890890361172289,9.));
#389477=CARTESIAN_POINT('Origin',(2.58847843614165,-0.890890361172289,8.75721825406948));
#389478=CARTESIAN_POINT('Ctrl Pts',(2.57377144873504,-0.905683912037573,
8.78942910404913));
#389479=CARTESIAN_POINT('Ctrl Pts',(2.57928769835755,-0.904894343291985,
8.79672699501692));
#389480=CARTESIAN_POINT('Ctrl Pts',(2.57966709350248,-0.895976409377319,
8.79893251111267));
#389481=CARTESIAN_POINT('Ctrl Pts',(2.58464914173358,-0.904086660094482,
8.78111911759576));
#389482=CARTESIAN_POINT('Ctrl Pts',(2.59118766485554,-0.903143248461614,
8.78644465894809));
#389483=CARTESIAN_POINT('Ctrl Pts',(2.593261215509,-0.895306418779725,8.78817647674132));
#389484=CARTESIAN_POINT('Ctrl Pts',(2.59142837946313,-0.903091214554007,
8.76780923932035));
#389485=CARTESIAN_POINT('Ctrl Pts',(2.59914610221575,-0.901972513394413,
8.76988516158378));
#389486=CARTESIAN_POINT('Ctrl Pts',(2.60175132061198,-0.894876795142932,
8.77093053738833));
#389487=CARTESIAN_POINT('Ctrl Pts',(2.59010652088601,-0.903285312809052,
8.75371302330491));
#389488=CARTESIAN_POINT('Ctrl Pts',(2.59763493587648,-0.902194822506869,
8.75300828287558));
#389489=CARTESIAN_POINT('Ctrl Pts',(2.60009538217395,-0.894960132233495,
8.75267964240738));
#389490=CARTESIAN_POINT('Origin',(2.5746046263238,-0.892927560898654,8.78727029226991));
#389491=CARTESIAN_POINT('Ctrl Pts',(2.50568666557815,-0.915681362418202,
8.85049129520029));
#389492=CARTESIAN_POINT('Ctrl Pts',(2.51146432645974,-0.914832983398916,
8.85711686593484));
#389493=CARTESIAN_POINT('Ctrl Pts',(2.51218498036397,-0.906313510406752,
8.85933012996512));
#389494=CARTESIAN_POINT('Ctrl Pts',(2.52929895681325,-0.912214185494592,
8.82945683644724));
#389495=CARTESIAN_POINT('Ctrl Pts',(2.53512457577341,-0.911358764416513,
8.8360746990239));
#389496=CARTESIAN_POINT('Ctrl Pts',(2.5358099765306,-0.902811117471319,
8.8382956714852));
#389497=CARTESIAN_POINT('Ctrl Pts',(2.55287605202416,-0.908752176677781,
8.80838214965001));
#389498=CARTESIAN_POINT('Ctrl Pts',(2.55872466159663,-0.907893379708745,
8.81501364461986));
#389499=CARTESIAN_POINT('Ctrl Pts',(2.55939923284054,-0.899314698794276,
8.8172209842872));
#389500=CARTESIAN_POINT('Ctrl Pts',(2.57642062555681,-0.905294943272693,
8.78727029226991));
#389501=CARTESIAN_POINT('Ctrl Pts',(2.58227020660258,-0.904436003654647,
8.79393457792714));
#389502=CARTESIAN_POINT('Ctrl Pts',(2.58295547781501,-0.89582381354158,
8.79610912703474));
#389503=CARTESIAN_POINT('Origin',(2.50387066634513,-0.903313980044163,8.85049129520029));
#389504=CARTESIAN_POINT('Ctrl Pts',(2.50151564461753,-0.927015373804513,
8.85049129520029));
#389505=CARTESIAN_POINT('Ctrl Pts',(2.50536507777437,-0.931406612421822,
8.85711686593484));
#389506=CARTESIAN_POINT('Ctrl Pts',(2.50039125247055,-0.938360879023052,
8.85933012996512));
#389507=CARTESIAN_POINT('Ctrl Pts',(2.49811010667084,-0.923130508387983,
8.86332496987232));
#389508=CARTESIAN_POINT('Ctrl Pts',(2.49678212912386,-0.927556383443994,
8.86648636486737));
#389509=CARTESIAN_POINT('Ctrl Pts',(2.4908770045068,-0.927481515896429,
8.87206031107457));
#389510=CARTESIAN_POINT('Ctrl Pts',(2.50054051873364,-0.916437011304924,
8.86341338519876));
#389511=CARTESIAN_POINT('Ctrl Pts',(2.50237644878422,-0.912182269070235,
8.86654584966059));
#389512=CARTESIAN_POINT('Ctrl Pts',(2.49777763608562,-0.908443943970582,
8.87215952290714));
#389513=CARTESIAN_POINT('Ctrl Pts',(2.50568666557815,-0.915681362418202,
8.85049129520029));
#389514=CARTESIAN_POINT('Ctrl Pts',(2.51146432645974,-0.914832983398916,
8.85711686593484));
#389515=CARTESIAN_POINT('Ctrl Pts',(2.51218498036397,-0.906313510406752,
8.85933012996512));
#389516=CARTESIAN_POINT('Origin',(2.49211597091067,-0.935255284860132,8.85049129520029));
#389517=CARTESIAN_POINT('Ctrl Pts',(2.54864296074705,-0.980775832055525,
8.78727029226991));
#389518=CARTESIAN_POINT('Ctrl Pts',(2.55254031154223,-0.985221732690688,
8.79393457792714));
#389519=CARTESIAN_POINT('Ctrl Pts',(2.54747944236024,-0.992223662303376,
8.79610912703474));
#389520=CARTESIAN_POINT('Ctrl Pts',(2.53295611725147,-0.962881074532807,
8.80838214965001));
#389521=CARTESIAN_POINT('Ctrl Pts',(2.53685282079144,-0.967326236811936,
8.81501364461995));
#389522=CARTESIAN_POINT('Ctrl Pts',(2.53180552577563,-0.974295714957295,
8.81722098428721));
#389523=CARTESIAN_POINT('Ctrl Pts',(2.5172476058129,-0.944961599316815,
8.82945683644724));
#389524=CARTESIAN_POINT('Ctrl Pts',(2.52112899159235,-0.949389287869639,
8.8360746990239));
#389525=CARTESIAN_POINT('Ctrl Pts',(2.51611005976585,-0.956342155322605,
8.83829567148519));
#389526=CARTESIAN_POINT('Ctrl Pts',(2.50151564461753,-0.927015373804513,
8.85049129520029));
#389527=CARTESIAN_POINT('Ctrl Pts',(2.50536507777437,-0.931406612421822,
8.85711686593484));
#389528=CARTESIAN_POINT('Ctrl Pts',(2.50039125247055,-0.938360879023052,
8.85933012996512));
#389529=CARTESIAN_POINT('Origin',(2.53924328704018,-0.989015743111143,8.78727029226991));
#389530=CARTESIAN_POINT('Ctrl Pts',(2.55776447567946,-0.991181222852413,
8.75374538247848));
#389531=CARTESIAN_POINT('Ctrl Pts',(2.56278352445775,-0.996886792740585,
8.75304829418601));
#389532=CARTESIAN_POINT('Ctrl Pts',(2.55997553412123,-1.00398509066889,
8.75272238421917));
#389533=CARTESIAN_POINT('Ctrl Pts',(2.55863459984933,-0.992173815842068,
8.76769408445022));
#389534=CARTESIAN_POINT('Ctrl Pts',(2.56377943200829,-0.998023418993408,
8.76974318093971));
#389535=CARTESIAN_POINT('Ctrl Pts',(2.56116930682118,-1.00510901027346,
8.7707786988043));
#389536=CARTESIAN_POINT('Ctrl Pts',(2.55417483904274,-0.987086349610299,
8.78108014887987));
#389537=CARTESIAN_POINT('Ctrl Pts',(2.55853775190122,-0.992041168344586,
8.78639403366322));
#389538=CARTESIAN_POINT('Ctrl Pts',(2.55505961340924,-0.999350383648536,
8.78812224174741));
#389539=CARTESIAN_POINT('Ctrl Pts',(2.5468662755566,-0.978749115549309,
8.78944554828685));
#389540=CARTESIAN_POINT('Ctrl Pts',(2.55054737792009,-0.982921153780983,
8.79673892988686));
#389541=CARTESIAN_POINT('Ctrl Pts',(2.54506331635742,-0.989951703054938,
8.79894799272499));
#389542=CARTESIAN_POINT('Origin',(2.54848687274363,-0.999560358084206,8.75721825406948));
#389543=CARTESIAN_POINT('Origin',(2.54848687274363,-0.999560358084206,9.));
#389544=CARTESIAN_POINT('Origin',(2.54848687274363,-0.999560358084206,7.51860402984325));
#389545=CARTESIAN_POINT('Ctrl Pts',(2.56358253296961,-0.985097594708649,
7.50366195182966));
#389546=CARTESIAN_POINT('Ctrl Pts',(2.56700079967973,-0.986411118369829,
7.50000065167735));
#389547=CARTESIAN_POINT('Ctrl Pts',(2.56700079967969,-0.986411118369938,
7.49482233047108));
#389548=CARTESIAN_POINT('Ctrl Pts',(2.56237307191841,-0.992438643923323,
7.50215800491337));
#389549=CARTESIAN_POINT('Ctrl Pts',(2.56358120883207,-0.99531007255245,
7.49877273257265));
#389550=CARTESIAN_POINT('Ctrl Pts',(2.5623429716696,-0.998532482377318,
7.49481816995647));
#389551=CARTESIAN_POINT('Ctrl Pts',(2.55974479284785,-0.993439726072484,
7.51043025814041));
#389552=CARTESIAN_POINT('Ctrl Pts',(2.56224502626245,-0.998716239112309,
7.51006209594514));
#389553=CARTESIAN_POINT('Ctrl Pts',(2.56012287462732,-1.0041269176834,7.50731281821699));
#389554=CARTESIAN_POINT('Ctrl Pts',(2.55788555007275,-0.991319310549886,
7.51860402984325));
#389555=CARTESIAN_POINT('Ctrl Pts',(2.56290221972397,-0.997040677781688,
7.51860402984325));
#389556=CARTESIAN_POINT('Ctrl Pts',(2.56012379910318,-1.00412456063254,
7.51860402984325));
#389557=CARTESIAN_POINT('Origin',(0.,0.,7.5));
#389558=CARTESIAN_POINT('Origin',(2.4369819335138,-1.08538337893279,7.5));
#389559=CARTESIAN_POINT('',(2.4369819335138,-1.08538337893279,7.59394543036555));
#389560=CARTESIAN_POINT('',(2.4369819335138,-1.08538337893279,8.85049129520029));
#389561=CARTESIAN_POINT('',(2.4369819335138,-1.08538337893279,7.5));
#389562=CARTESIAN_POINT('',(2.48056797713153,-1.14205283806805,8.78727029226991));
#389563=CARTESIAN_POINT('Ctrl Pts',(2.4369819335138,-1.08538337893279,8.85049129520029));
#389564=CARTESIAN_POINT('Ctrl Pts',(2.45153173356487,-1.10430065682687,
8.82945686509571));
#389565=CARTESIAN_POINT('Ctrl Pts',(2.46605990357883,-1.12318981189993,
8.80838212259896));
#389566=CARTESIAN_POINT('Ctrl Pts',(2.48056797713153,-1.14205283806805,
8.78727029226991));
#389567=CARTESIAN_POINT('',(2.48911697509583,-1.15316802656817,8.75721825406948));
#389568=CARTESIAN_POINT('Origin',(2.46339023451441,-1.11971844545458,8.75937679713111));
#389569=CARTESIAN_POINT('',(2.48911697509583,-1.15316802656817,7.51860402984325));
#389570=CARTESIAN_POINT('',(2.48911697509583,-1.15316802656817,7.5));
#389571=CARTESIAN_POINT('Ctrl Pts',(2.48911697509583,-1.15316802656817,
7.51860402984325));
#389572=CARTESIAN_POINT('Ctrl Pts',(2.48240306681555,-1.14443877474013,
7.52834476460825));
#389573=CARTESIAN_POINT('Ctrl Pts',(2.47568479996291,-1.13570385600776,
7.53807742314407));
#389574=CARTESIAN_POINT('Ctrl Pts',(2.46896202819301,-1.12696308009721,
7.54780169004674));
#389575=CARTESIAN_POINT('Ctrl Pts',(2.45831352104431,-1.11311816345353,
7.5632044032688));
#389576=CARTESIAN_POINT('Ctrl Pts',(2.44765369809931,-1.09925853430096,
7.57858609112103));
#389577=CARTESIAN_POINT('Ctrl Pts',(2.4369819335138,-1.08538337893279,7.59394543036555));
#389578=CARTESIAN_POINT('Origin',(2.71595367934704,-1.0519023752311,7.5));
#389579=CARTESIAN_POINT('',(2.52710047532069,-1.0673626379274,8.75721825406948));
#389580=CARTESIAN_POINT('',(2.51312464689845,-1.06850675396143,8.78727029226991));
#389581=CARTESIAN_POINT('Origin',(2.47764878164183,-1.07141094718957,8.75658640621155));
#389582=CARTESIAN_POINT('',(2.44187055726729,-1.07433989271893,8.85049129520029));
#389583=CARTESIAN_POINT('Ctrl Pts',(2.51312464689845,-1.06850675396143,
8.78727029226991));
#389584=CARTESIAN_POINT('Ctrl Pts',(2.48940697290248,-1.07044837561627,
8.80838212259896));
#389585=CARTESIAN_POINT('Ctrl Pts',(2.4656564453843,-1.07239268678907,8.82945686509571));
#389586=CARTESIAN_POINT('Ctrl Pts',(2.44187055726729,-1.07433989271893,
8.85049129520029));
#389587=CARTESIAN_POINT('',(2.44187055726729,-1.07433989271893,7.59394543036555));
#389588=CARTESIAN_POINT('',(2.44187055726729,-1.07433989271893,7.5));
#389589=CARTESIAN_POINT('',(2.52710047532069,-1.0673626379274,7.51860402984325));
#389590=CARTESIAN_POINT('Ctrl Pts',(2.44187055726729,-1.07433989271893,
7.59394543036555));
#389591=CARTESIAN_POINT('Ctrl Pts',(2.45931666632385,-1.07291168592502,
7.57858609112103));
#389592=CARTESIAN_POINT('Ctrl Pts',(2.47674325328887,-1.07148507728597,
7.56320440326857));
#389593=CARTESIAN_POINT('Ctrl Pts',(2.49415134128755,-1.07005998304471,
7.54780169004651));
#389594=CARTESIAN_POINT('Ctrl Pts',(2.50514167081742,-1.06916027163909,
7.53807742314383));
#389595=CARTESIAN_POINT('Ctrl Pts',(2.51612463574749,-1.06826116312843,
7.52834476460825));
#389596=CARTESIAN_POINT('Ctrl Pts',(2.52710047532068,-1.0673626379274,7.51860402984325));
#389597=CARTESIAN_POINT('',(2.52710047532069,-1.0673626379274,7.5));
#389598=CARTESIAN_POINT('Origin',(2.44243149520449,-1.08119197077092,7.5));
#389599=CARTESIAN_POINT('Ctrl Pts',(2.44187055726729,-1.07433989271893,
8.85049129520029));
#389600=CARTESIAN_POINT('Ctrl Pts',(2.4416775414485,-1.07435569374957,8.85097269580138));
#389601=CARTESIAN_POINT('Ctrl Pts',(2.4414876471768,-1.07437967878893,8.85143669361005));
#389602=CARTESIAN_POINT('Ctrl Pts',(2.44129223999294,-1.07441381966452,
8.8519052845931));
#389603=CARTESIAN_POINT('Ctrl Pts',(2.44091003593358,-1.07448059705204,
8.85282181883899));
#389604=CARTESIAN_POINT('Ctrl Pts',(2.44051660708416,-1.07458470358958,
8.85372622499635));
#389605=CARTESIAN_POINT('Ctrl Pts',(2.4401097241228,-1.07474267860362,8.8546225773507));
#389606=CARTESIAN_POINT('Ctrl Pts',(2.43977194433939,-1.07487382384953,
8.85536669723986));
#389607=CARTESIAN_POINT('Ctrl Pts',(2.43942480388502,-1.07504209424019,
8.85610498449051));
#389608=CARTESIAN_POINT('Ctrl Pts',(2.43907048844601,-1.07526416791268,
8.85681338218371));
#389609=CARTESIAN_POINT('Ctrl Pts',(2.43874894662865,-1.07546570011925,
8.85745625420285));
#389610=CARTESIAN_POINT('Ctrl Pts',(2.43841714453213,-1.07571356340654,
8.85808743050666));
#389611=CARTESIAN_POINT('Ctrl Pts',(2.43808062970449,-1.07603581255774,
8.85866804508411));
#389612=CARTESIAN_POINT('Ctrl Pts',(2.43792536905777,-1.0761844913306,8.85893592806396));
#389613=CARTESIAN_POINT('Ctrl Pts',(2.4377691802621,-1.07634923507313,8.85919241173849));
#389614=CARTESIAN_POINT('Ctrl Pts',(2.43761330950699,-1.07653423293661,
8.85943017985535));
#389615=CARTESIAN_POINT('Ctrl Pts',(2.43740283784491,-1.07678403481753,
8.85975123720001));
#389616=CARTESIAN_POINT('Ctrl Pts',(2.43718807887067,-1.07707753686408,
8.86004599534706));
#389617=CARTESIAN_POINT('Ctrl Pts',(2.43698001810968,-1.07741736300175,
8.86026130871721));
#389618=CARTESIAN_POINT('Ctrl Pts',(2.43690384119922,-1.07754178293146,
8.86034014101236));
#389619=CARTESIAN_POINT('Ctrl Pts',(2.43682740741169,-1.07767427508622,
8.86040910639693));
#389620=CARTESIAN_POINT('Ctrl Pts',(2.4367530905129,-1.07781139788104,8.86046313645507));
#389621=CARTESIAN_POINT('Ctrl Pts',(2.43663711961474,-1.07802537685396,
8.8605474499083));
#389622=CARTESIAN_POINT('Ctrl Pts',(2.43652326724304,-1.0782565431018,8.86059655985669));
#389623=CARTESIAN_POINT('Ctrl Pts',(2.43641857228559,-1.07848994179129,
8.86059725258816));
#389624=CARTESIAN_POINT('Ctrl Pts',(2.43631363544096,-1.07872387972499,
8.86059794692012));
#389625=CARTESIAN_POINT('Ctrl Pts',(2.43621915867709,-1.07896374218053,
8.86056369958366));
#389626=CARTESIAN_POINT('Ctrl Pts',(2.4361367935118,-1.07919506785858,8.86048590497774));
#389627=CARTESIAN_POINT('Ctrl Pts',(2.43611529865597,-1.07925543697315,
8.86046560290182));
#389628=CARTESIAN_POINT('Ctrl Pts',(2.43609443436159,-1.07931604043714,
8.86044257503091));
#389629=CARTESIAN_POINT('Ctrl Pts',(2.43607481431438,-1.07937499486761,
8.86041778462583));
#389630=CARTESIAN_POINT('Ctrl Pts',(2.4359427957431,-1.07977168502833,8.86025097596201));
#389631=CARTESIAN_POINT('Ctrl Pts',(2.43584971171548,-1.08014704858012,
8.8599848982295));
#389632=CARTESIAN_POINT('Ctrl Pts',(2.43579005570162,-1.0804880903763,8.85968173251462));
#389633=CARTESIAN_POINT('Ctrl Pts',(2.43575850108817,-1.08066848194711,
8.85952137522077));
#389634=CARTESIAN_POINT('Ctrl Pts',(2.43573550263548,-1.08084271523857,
8.85934740853961));
#389635=CARTESIAN_POINT('Ctrl Pts',(2.43571984348871,-1.08100812974288,
8.8591675900182));
#389636=CARTESIAN_POINT('Ctrl Pts',(2.43565696387494,-1.0816723549584,8.85844552518695));
#389637=CARTESIAN_POINT('Ctrl Pts',(2.43570585991415,-1.08223163783065,
8.85759444184123));
#389638=CARTESIAN_POINT('Ctrl Pts',(2.4357866862199,-1.08268406612753,8.85683498915138));
#389639=CARTESIAN_POINT('Ctrl Pts',(2.43579514447754,-1.08273141154388,
8.85675551444997));
#389640=CARTESIAN_POINT('Ctrl Pts',(2.43580397099507,-1.08277757949647,
8.85667699793651));
#389641=CARTESIAN_POINT('Ctrl Pts',(2.4358130862329,-1.08282256237295,8.85659965593547));
#389642=CARTESIAN_POINT('Ctrl Pts',(2.43593612417828,-1.08342974353502,
8.85555568965886));
#389643=CARTESIAN_POINT('Ctrl Pts',(2.43614206024082,-1.08399551313589,
8.85434650606346));
#389644=CARTESIAN_POINT('Ctrl Pts',(2.43642607255145,-1.08452479370297,
8.85297329937117));
#389645=CARTESIAN_POINT('Ctrl Pts',(2.43658581217106,-1.08482248177241,
8.85220095427747));
#389646=CARTESIAN_POINT('Ctrl Pts',(2.43677059316374,-1.08510859961498,
8.85137579139183));
#389647=CARTESIAN_POINT('Ctrl Pts',(2.4369819335138,-1.08538337893279,8.85049129520029));
#389648=CARTESIAN_POINT('Origin',(2.44243149520449,-1.08119197077092,7.59394543036555));
#389649=CARTESIAN_POINT('Ctrl Pts',(2.44131016723206,-1.0743857684413,7.59443877723642));
#389650=CARTESIAN_POINT('Ctrl Pts',(2.43553868906203,-1.0748582442413,7.58783886950016));
#389651=CARTESIAN_POINT('Ctrl Pts',(2.43425469986311,-1.08325053554187,
7.58559994247159));
#389652=CARTESIAN_POINT('Ctrl Pts',(2.47281649723425,-1.07180653691096,
7.56670252222134));
#389653=CARTESIAN_POINT('Ctrl Pts',(2.46705336048877,-1.07227832984929,
7.56004874999028));
#389654=CARTESIAN_POINT('Ctrl Pts',(2.46574064338428,-1.08071711714724,
7.55786368756704));
#389655=CARTESIAN_POINT('Ctrl Pts',(2.50426399231308,-1.06923212183781,
7.53888913333559));
#389656=CARTESIAN_POINT('Ctrl Pts',(2.49846660496369,-1.06970671866468,
7.53222002137277));
#389657=CARTESIAN_POINT('Ctrl Pts',(2.49716881203072,-1.0781871772739,7.53005029815326));
#389658=CARTESIAN_POINT('Ctrl Pts',(2.53565122944802,-1.06666263971587,
7.51101258149734));
#389659=CARTESIAN_POINT('Ctrl Pts',(2.52978356722987,-1.06714298951863,
7.5043616886572));
#389660=CARTESIAN_POINT('Ctrl Pts',(2.52853765964447,-1.07566092329587,
7.50217374673251));
#389661=CARTESIAN_POINT('',(2.526863777558,-1.07579572642895,7.50366116523517));
#389662=CARTESIAN_POINT('Ctrl Pts',(2.52710047532069,-1.06736263792739,
7.51860402984325));
#389663=CARTESIAN_POINT('Ctrl Pts',(2.5275406141597,-1.06732660643876,7.51734760759493));
#389664=CARTESIAN_POINT('Ctrl Pts',(2.52794319693951,-1.06735334527535,
7.51608817408573));
#389665=CARTESIAN_POINT('Ctrl Pts',(2.52830641272849,-1.06745611722427,
7.51481005913119));
#389666=CARTESIAN_POINT('Ctrl Pts',(2.52863542226948,-1.06754921051143,
7.51365231206383));
#389667=CARTESIAN_POINT('Ctrl Pts',(2.52893266240551,-1.06770458075918,
7.51247773061042));
#389668=CARTESIAN_POINT('Ctrl Pts',(2.52917588459346,-1.06795226365132,
7.51129758471022));
#389669=CARTESIAN_POINT('Ctrl Pts',(2.52947818199607,-1.0682601051998,7.50983079813402));
#389670=CARTESIAN_POINT('Ctrl Pts',(2.52967809354277,-1.06870984917593,
7.50839324291155));
#389671=CARTESIAN_POINT('Ctrl Pts',(2.52970174557798,-1.06933826341189,
7.50715379678855));
#389672=CARTESIAN_POINT('Ctrl Pts',(2.52971267213674,-1.06962857268158,
7.50658120839351));
#389673=CARTESIAN_POINT('Ctrl Pts',(2.52967804016154,-1.06999864075055,
7.50598221009429));
#389674=CARTESIAN_POINT('Ctrl Pts',(2.52957602630726,-1.07043754110356,
7.50545747549611));
#389675=CARTESIAN_POINT('Ctrl Pts',(2.52952158855699,-1.07067175191717,
7.50517746087247));
#389676=CARTESIAN_POINT('Ctrl Pts',(2.52944756995091,-1.070928149076,7.50491486231392));
#389677=CARTESIAN_POINT('Ctrl Pts',(2.52935432805342,-1.07119948010878,
7.50468370960992));
#389678=CARTESIAN_POINT('Ctrl Pts',(2.52921490200518,-1.07160520558931,
7.50433806340447));
#389679=CARTESIAN_POINT('Ctrl Pts',(2.52902778596955,-1.07205630799,7.50405484070984));
#389680=CARTESIAN_POINT('Ctrl Pts',(2.52880492013754,-1.07252213192078,
7.50385766036131));
#389681=CARTESIAN_POINT('Ctrl Pts',(2.52878108810092,-1.07257194454964,
7.50383657498791));
#389682=CARTESIAN_POINT('Ctrl Pts',(2.5287568708167,-1.07262190971423,7.50381643264937));
#389683=CARTESIAN_POINT('Ctrl Pts',(2.52873230017347,-1.07267197871409,
7.50379723213559));
#389684=CARTESIAN_POINT('Ctrl Pts',(2.52856828309232,-1.07300620566686,
7.50366906242519));
#389685=CARTESIAN_POINT('Ctrl Pts',(2.52838430707248,-1.07335201295403,
7.50358235568538));
#389686=CARTESIAN_POINT('Ctrl Pts',(2.52819896460948,-1.07368106596533,
7.5035341175365));
#389687=CARTESIAN_POINT('Ctrl Pts',(2.52792106456294,-1.07417444371417,
7.50346178989176));
#389688=CARTESIAN_POINT('Ctrl Pts',(2.52760112950024,-1.07469338991016,
7.50346967198527));
#389689=CARTESIAN_POINT('Ctrl Pts',(2.5272713767736,-1.07519317013139,7.50354272648692));
#389690=CARTESIAN_POINT('Ctrl Pts',(2.52713574265166,-1.07539874008122,
7.50357277531559));
#389691=CARTESIAN_POINT('Ctrl Pts',(2.52699874610053,-1.07560087239687,
7.50361331098761));
#389692=CARTESIAN_POINT('Ctrl Pts',(2.5268637775593,-1.0757957264295,7.50366116523659));
#389693=CARTESIAN_POINT('',(2.44510882695063,-1.08237714611493,7.57603338622103));
#389694=CARTESIAN_POINT('Origin',(2.45318828011514,-1.08595680059038,7.58486873427632));
#389695=CARTESIAN_POINT('Ctrl Pts',(2.52686377761448,-1.07579572641902,
7.50366116529969));
#389696=CARTESIAN_POINT('Ctrl Pts',(2.49965666355486,-1.07798678628757,
7.52783573079709));
#389697=CARTESIAN_POINT('Ctrl Pts',(2.47240630148104,-1.08018050713206,
7.55196141284068));
#389698=CARTESIAN_POINT('Ctrl Pts',(2.44510882811946,-1.08237714566606,
7.57603338728831));
#389699=CARTESIAN_POINT('Ctrl Pts',(2.44272911426497,-1.07441992109173,
7.59642833564546));
#389700=CARTESIAN_POINT('Ctrl Pts',(2.42445489603489,-1.07354713207804,
7.59959882295456));
#389701=CARTESIAN_POINT('Ctrl Pts',(2.43774827562796,-1.08609137277743,
7.59639677331373));
#389702=CARTESIAN_POINT('Ctrl Pts',(2.43897129681562,-1.07360282396487,
7.58710240504251));
#389703=CARTESIAN_POINT('Ctrl Pts',(2.43327446304227,-1.07724431895329,
7.58809943920598));
#389704=CARTESIAN_POINT('Ctrl Pts',(2.43451789319205,-1.08390511263708,
7.58707626057424));
#389705=CARTESIAN_POINT('Ctrl Pts',(2.44213665289714,-1.07877505939748,
7.5802092424413));
#389706=CARTESIAN_POINT('Ctrl Pts',(2.43958612281158,-1.07996748185641,
7.58205880659758));
#389707=CARTESIAN_POINT('Ctrl Pts',(2.44046943008487,-1.08267839307895,
7.58015376756931));
#389708=CARTESIAN_POINT('Ctrl Pts',(2.44510882619397,-1.08237714577975,
7.57603338509286));
#389709=CARTESIAN_POINT('Ctrl Pts',(2.44510882619397,-1.08237714577975,
7.57603338509286));
#389710=CARTESIAN_POINT('Ctrl Pts',(2.44510882619397,-1.08237714577975,
7.57603338509286));
#389711=CARTESIAN_POINT('Origin',(2.45319058995175,-1.08595158263002,7.58486873427622));
#389712=CARTESIAN_POINT('Ctrl Pts',(2.49436399277438,-1.1599900647537,7.51098857897448));
#389713=CARTESIAN_POINT('Ctrl Pts',(2.49077473426271,-1.15532340263734,
7.50433767179956));
#389714=CARTESIAN_POINT('Ctrl Pts',(2.49624278171656,-1.14867445474125,
7.50214974420965));
#389715=CARTESIAN_POINT('Ctrl Pts',(2.47515893410405,-1.13502013866787,
7.53887321589163));
#389716=CARTESIAN_POINT('Ctrl Pts',(2.47161268127914,-1.13040939144548,
7.53220407452058));
#389717=CARTESIAN_POINT('Ctrl Pts',(2.47701807999251,-1.12374721577447,
7.53003438070911));
#389718=CARTESIAN_POINT('Ctrl Pts',(2.45591699463666,-1.11000226111298,
7.56669465659233));
#389719=CARTESIAN_POINT('Ctrl Pts',(2.4523916995066,-1.10541876254948,7.56004085833298));
#389720=CARTESIAN_POINT('Ctrl Pts',(2.45775620401618,-1.09877355815133,
7.55785582193789));
#389721=CARTESIAN_POINT('Ctrl Pts',(2.43663904460805,-1.08493756354742,
7.59443891967696));
#389722=CARTESIAN_POINT('Ctrl Pts',(2.433108638239,-1.08034741948166,7.58783901202978));
#389723=CARTESIAN_POINT('Ctrl Pts',(2.43845803954467,-1.07375476571711,
7.58560008491213));
#389724=CARTESIAN_POINT('',(2.49520067284434,-1.14732323151525,7.50366116523517));
#389725=CARTESIAN_POINT('Ctrl Pts',(2.49520067284468,-1.14732323151541,
7.50366116523554));
#389726=CARTESIAN_POINT('Ctrl Pts',(2.49502946219895,-1.14806135374889,
7.50350835821027));
#389727=CARTESIAN_POINT('Ctrl Pts',(2.49484806402456,-1.14873429707003,
7.50345484956));
#389728=CARTESIAN_POINT('Ctrl Pts',(2.49465166501226,-1.14936222492285,
7.50349758195598));
#389729=CARTESIAN_POINT('Ctrl Pts',(2.49455089775363,-1.14968439847969,
7.50351950684424));
#389730=CARTESIAN_POINT('Ctrl Pts',(2.49443637311436,-1.15002651529797,
7.50357029184312));
#389731=CARTESIAN_POINT('Ctrl Pts',(2.49431687004512,-1.15035337898107,
7.50365515313923));
#389732=CARTESIAN_POINT('Ctrl Pts',(2.49413302593307,-1.15085622768585,
7.50378570417639));
#389733=CARTESIAN_POINT('Ctrl Pts',(2.49393232888108,-1.15133785676729,
7.50400001621911));
#389734=CARTESIAN_POINT('Ctrl Pts',(2.49372795910971,-1.1517607339538,7.50428903009634));
#389735=CARTESIAN_POINT('Ctrl Pts',(2.49370527563742,-1.15180767006808,
7.50432110841318));
#389736=CARTESIAN_POINT('Ctrl Pts',(2.49368255155364,-1.15185391235972,
7.50435406373354));
#389737=CARTESIAN_POINT('Ctrl Pts',(2.49365980799993,-1.15189943166855,
7.50438785222352));
#389738=CARTESIAN_POINT('Ctrl Pts',(2.49352094767258,-1.15217734892832,
7.50459414719561));
#389739=CARTESIAN_POINT('Ctrl Pts',(2.49337868940289,-1.15243250984058,
7.50483629897752));
#389740=CARTESIAN_POINT('Ctrl Pts',(2.49323963252004,-1.15265578011538,
7.5050991045531));
#389741=CARTESIAN_POINT('Ctrl Pts',(2.49293285906953,-1.15314833676698,
7.50567888004914));
#389742=CARTESIAN_POINT('Ctrl Pts',(2.49263001938427,-1.15350537014203,
7.50637912803144));
#389743=CARTESIAN_POINT('Ctrl Pts',(2.49234864839804,-1.15375233499363,
7.50710440483569));
#389744=CARTESIAN_POINT('Ctrl Pts',(2.49227965064622,-1.15381289567818,
7.50728225710685));
#389745=CARTESIAN_POINT('Ctrl Pts',(2.49221066660843,-1.15386815290563,
7.50746498566954));
#389746=CARTESIAN_POINT('Ctrl Pts',(2.49214356704021,-1.15391714193709,
7.50764697238949));
#389747=CARTESIAN_POINT('Ctrl Pts',(2.49178285822775,-1.15418049348805,
7.50862528291181));
#389748=CARTESIAN_POINT('Ctrl Pts',(2.49144630392676,-1.15428995340171,
7.50965856837421));
#389749=CARTESIAN_POINT('Ctrl Pts',(2.4911367136329,-1.15431175990401,7.51067959873201));
#389750=CARTESIAN_POINT('Ctrl Pts',(2.49096634570369,-1.15432376004973,
7.51124147302578));
#389751=CARTESIAN_POINT('Ctrl Pts',(2.49080407122457,-1.15430878557774,
7.51180065547253));
#389752=CARTESIAN_POINT('Ctrl Pts',(2.49065026658073,-1.15427516054053,
7.51235175716501));
#389753=CARTESIAN_POINT('Ctrl Pts',(2.49011881026774,-1.15415897264232,
7.51425603304536));
#389754=CARTESIAN_POINT('Ctrl Pts',(2.48962641095044,-1.15380032331499,
7.51626900505181));
#389755=CARTESIAN_POINT('Ctrl Pts',(2.48918772654823,-1.15325776008449,
7.51827788969245));
#389756=CARTESIAN_POINT('Ctrl Pts',(2.48916398411938,-1.15322839553715,
7.51838661432546));
#389757=CARTESIAN_POINT('Ctrl Pts',(2.48914039945448,-1.15319848232018,
7.51849533314857));
#389758=CARTESIAN_POINT('Ctrl Pts',(2.48911697509583,-1.15316802656818,
7.51860402984325));
#389759=CARTESIAN_POINT('Ctrl Pts',(2.44510882740513,-1.08237714728266,
7.57603338728985));
#389760=CARTESIAN_POINT('Ctrl Pts',(2.46183481987757,-1.10406166823482,
7.55196141284922));
#389761=CARTESIAN_POINT('Ctrl Pts',(2.47853129930077,-1.12570935218487,
7.52783573083104));
#389762=CARTESIAN_POINT('Ctrl Pts',(2.49520067287603,-1.14732323156524,
7.50366116530176));
#389763=CARTESIAN_POINT('Origin',(8.44898126352703E-16,-3.74011337523904E-16,
7.49482233047033));
#389764=CARTESIAN_POINT('Origin',(2.5187313027445,-1.07233337846727,7.49482233047033));
#389765=CARTESIAN_POINT('Origin',(0.,0.,7.50366116523517));
#389766=CARTESIAN_POINT('Origin',(2.48717010277295,-1.14363067896608,7.49482233047033));
#389767=CARTESIAN_POINT('Ctrl Pts',(2.52709942112331,-1.06736272418322,
7.51860402984325));
#389768=CARTESIAN_POINT('Ctrl Pts',(2.53468306548395,-1.06674254336973,
7.51860402984325));
#389769=CARTESIAN_POINT('Ctrl Pts',(2.53761520271997,-1.05972122887319,
7.51860402984325));
#389770=CARTESIAN_POINT('Ctrl Pts',(2.52991527992432,-1.06713244554834,
7.51041458714367));
#389771=CARTESIAN_POINT('Ctrl Pts',(2.53537771324442,-1.06507910972981,
7.51004642900443));
#389772=CARTESIAN_POINT('Ctrl Pts',(2.5376160113686,-1.05971929247802,7.5072913648301));
#389773=CARTESIAN_POINT('Ctrl Pts',(2.5310984519589,-1.06968662665701,7.50215815450137));
#389774=CARTESIAN_POINT('Ctrl Pts',(2.53396347064419,-1.06846608070767,
7.49877163671529));
#389775=CARTESIAN_POINT('Ctrl Pts',(2.53531500022192,-1.06529160572826,
7.4948158853317));
#389776=CARTESIAN_POINT('Ctrl Pts',(2.52686327103472,-1.07579551078049,
7.50366171572174));
#389777=CARTESIAN_POINT('Ctrl Pts',(2.53023235892126,-1.07722987791268,
7.50000045605858));
#389778=CARTESIAN_POINT('Ctrl Pts',(2.53023235892131,-1.07722987791257,
7.49482233047317));
#389779=CARTESIAN_POINT('Origin',(2.52608058816215,-1.0549043141965,7.51860402984325));
#389780=CARTESIAN_POINT('Origin',(2.52608058816215,-1.0549043141965,9.));
#389781=CARTESIAN_POINT('Origin',(2.52608058816215,-1.0549043141965,8.75721825406948));
#389782=CARTESIAN_POINT('Ctrl Pts',(2.51045599178025,-1.06872519020653,
8.78942910404913));
#389783=CARTESIAN_POINT('Ctrl Pts',(2.51601149551951,-1.06829067104139,
8.79672699501691));
#389784=CARTESIAN_POINT('Ctrl Pts',(2.51696148514411,-1.0594153679088,8.79893251111267));
#389785=CARTESIAN_POINT('Ctrl Pts',(2.52141367167525,-1.06782815617216,
8.78111911759577));
#389786=CARTESIAN_POINT('Ctrl Pts',(2.52799920529107,-1.06730560749445,
8.78644465894813));
#389787=CARTESIAN_POINT('Ctrl Pts',(2.53057060301399,-1.05961773226614,
8.78817647674131));
#389788=CARTESIAN_POINT('Ctrl Pts',(2.52824275914858,-1.06726910313394,
8.76780923932033));
#389789=CARTESIAN_POINT('Ctrl Pts',(2.53601630044145,-1.06664717666037,
8.76988516158374));
#389790=CARTESIAN_POINT('Ctrl Pts',(2.53907079036638,-1.0597329542388,8.77093053738834));
#389791=CARTESIAN_POINT('Ctrl Pts',(2.52691118055377,-1.06737811082349,
8.75371302330491));
#389792=CARTESIAN_POINT('Ctrl Pts',(2.53449399556177,-1.06677220825513,
8.75300828287559));
#389793=CARTESIAN_POINT('Ctrl Pts',(2.53741291480575,-1.05971002376437,
8.75267964240737));
#389794=CARTESIAN_POINT('Origin',(2.51210475973992,-1.05604843023054,8.78727029226991));
#389795=CARTESIAN_POINT('Ctrl Pts',(2.44187055726729,-1.07433989271893,
8.85049129520029));
#389796=CARTESIAN_POINT('Ctrl Pts',(2.44769070315535,-1.07386343278898,
8.85711686593484));
#389797=CARTESIAN_POINT('Ctrl Pts',(2.44895572090757,-1.06540763642197,
8.85933012996512));
#389798=CARTESIAN_POINT('Ctrl Pts',(2.46565647730585,-1.07239268417584,
8.82945683644723));
#389799=CARTESIAN_POINT('Ctrl Pts',(2.4715249339237,-1.07191226934043,8.8360746990239));
#389800=CARTESIAN_POINT('Ctrl Pts',(2.47275657607163,-1.06342609822989,
8.8382956714852));
#389801=CARTESIAN_POINT('Ctrl Pts',(2.48940694251249,-1.07044837810411,
8.80838214965003));
#389802=CARTESIAN_POINT('Ctrl Pts',(2.49529855880008,-1.06996606732744,
8.81501364461988));
#389803=CARTESIAN_POINT('Ctrl Pts',(2.49652138203833,-1.06144823216095,
8.81722098428721));
#389804=CARTESIAN_POINT('Ctrl Pts',(2.51312464689845,-1.06850675396143,
8.78727029226991));
#389805=CARTESIAN_POINT('Ctrl Pts',(2.51901724180287,-1.06802436307135,
8.79393457792714));
#389806=CARTESIAN_POINT('Ctrl Pts',(2.52025288996717,-1.05947377310385,
8.79610912703474));
#389807=CARTESIAN_POINT('Origin',(2.44085067010875,-1.06188156898803,8.85049129520029));
#389808=CARTESIAN_POINT('Ctrl Pts',(2.4369819335138,-1.08538337893279,8.85049129520029));
#389809=CARTESIAN_POINT('Ctrl Pts',(2.44054210997316,-1.09001222930856,
8.85711686593484));
#389810=CARTESIAN_POINT('Ctrl Pts',(2.43513294253592,-1.09663353354185,
8.85933012996512));
#389811=CARTESIAN_POINT('Ctrl Pts',(2.43383229679189,-1.08128830182351,
8.8633249698723));
#389812=CARTESIAN_POINT('Ctrl Pts',(2.43222348092875,-1.08561999963098,
8.86648636486735));
#389813=CARTESIAN_POINT('Ctrl Pts',(2.42633528580379,-1.08516694327358,
8.87206031107458));
#389814=CARTESIAN_POINT('Ctrl Pts',(2.43668656914299,-1.07476427428359,
8.86341338519877));
#389815=CARTESIAN_POINT('Ctrl Pts',(2.4387913293493,-1.07063590231533,8.86654584966058));
#389816=CARTESIAN_POINT('Ctrl Pts',(2.43444148071613,-1.06661061106431,
8.87215952290713));
#389817=CARTESIAN_POINT('Ctrl Pts',(2.44187055726729,-1.07433989271893,
8.85049129520029));
#389818=CARTESIAN_POINT('Ctrl Pts',(2.44769070315535,-1.07386343278898,
8.85711686593484));
#389819=CARTESIAN_POINT('Ctrl Pts',(2.44895572090757,-1.06540763642197,
8.85933012996512));
#389820=CARTESIAN_POINT('Origin',(2.42707363953072,-1.09300412104527,8.85049129520029));
#389821=CARTESIAN_POINT('Ctrl Pts',(2.48056797713153,-1.14205283806805,
8.78727029226991));
#389822=CARTESIAN_POINT('Ctrl Pts',(2.4841724705698,-1.14673930824632,8.79393457792714));
#389823=CARTESIAN_POINT('Ctrl Pts',(2.47867338431575,-1.15340260064189,
8.79610912703474));
#389824=CARTESIAN_POINT('Ctrl Pts',(2.4660598849893,-1.12318978773031,8.80838214965003));
#389825=CARTESIAN_POINT('Ctrl Pts',(2.46966377980884,-1.12787547959981,
8.81501364461995));
#389826=CARTESIAN_POINT('Ctrl Pts',(2.46418031900404,-1.13450725690287,
8.81722098428722));
#389827=CARTESIAN_POINT('Ctrl Pts',(2.45153175309124,-1.10430068221456,
8.82945683644722));
#389828=CARTESIAN_POINT('Ctrl Pts',(2.45512148116773,-1.10896795484711,
8.83607469902388));
#389829=CARTESIAN_POINT('Ctrl Pts',(2.44966738952776,-1.11558497282199,
8.83829567148519));
#389830=CARTESIAN_POINT('Ctrl Pts',(2.4369819335138,-1.08538337893279,8.85049129520029));
#389831=CARTESIAN_POINT('Ctrl Pts',(2.44054210997316,-1.09001222930856,
8.85711686593484));
#389832=CARTESIAN_POINT('Ctrl Pts',(2.43513294253592,-1.09663353354185,
8.85933012996512));
#389833=CARTESIAN_POINT('Origin',(2.47065968314845,-1.14967358018053,8.78727029226991));
#389834=CARTESIAN_POINT('Ctrl Pts',(2.48900407525589,-1.15302126734185,
8.75374538247847));
#389835=CARTESIAN_POINT('Ctrl Pts',(2.49364725474232,-1.15903668608408,
8.75304829418602));
#389836=CARTESIAN_POINT('Ctrl Pts',(2.49039024421335,-1.16594049123944,
8.75272238421917));
#389837=CARTESIAN_POINT('Ctrl Pts',(2.48980881601113,-1.15406756998971,
8.76769408445022));
#389838=CARTESIAN_POINT('Ctrl Pts',(2.49456829219993,-1.16023478503221,
8.7697431809397));
#389839=CARTESIAN_POINT('Ctrl Pts',(2.49150955440295,-1.16713858691014,
8.7707786988043));
#389840=CARTESIAN_POINT('Ctrl Pts',(2.48568417334205,-1.14870481864703,
8.78108014887987));
#389841=CARTESIAN_POINT('Ctrl Pts',(2.48972066580186,-1.15392898996142,
8.78639403366324));
#389842=CARTESIAN_POINT('Ctrl Pts',(2.48578137048604,-1.1610003426003,8.7881222417474));
#389843=CARTESIAN_POINT('Ctrl Pts',(2.47892479450374,-1.13991645305727,
8.78944554828686));
#389844=CARTESIAN_POINT('Ctrl Pts',(2.48233103024035,-1.14431576842715,
8.79673892988686));
#389845=CARTESIAN_POINT('Ctrl Pts',(2.47640778743176,-1.15098050765289,
8.79894799272499));
#389846=CARTESIAN_POINT('Origin',(2.47920868111276,-1.16078876868065,8.75721825406948));
#389847=CARTESIAN_POINT('Origin',(2.47920868111276,-1.16078876868065,9.));
#389848=CARTESIAN_POINT('Origin',(2.47920868111276,-1.16078876868065,7.51860402984325));
#389849=CARTESIAN_POINT('Ctrl Pts',(2.4951999581168,-1.14732290287501,7.50366195182966));
#389850=CARTESIAN_POINT('Ctrl Pts',(2.49852704388144,-1.14885273686103,
7.50000065167735));
#389851=CARTESIAN_POINT('Ctrl Pts',(2.4985270438814,-1.14885273686113,7.49482233047108));
#389852=CARTESIAN_POINT('Ctrl Pts',(2.49352263939498,-1.15457137868114,
7.50215800491337));
#389853=CARTESIAN_POINT('Ctrl Pts',(2.49454432099785,-1.15751431325002,
7.49877273257263));
#389854=CARTESIAN_POINT('Ctrl Pts',(2.49310216742008,-1.1606507681609,7.49481816995647));
#389855=CARTESIAN_POINT('Ctrl Pts',(2.49083562085213,-1.15540200958143,
7.51043025814042));
#389856=CARTESIAN_POINT('Ctrl Pts',(2.49299264991785,-1.16082787196419,
7.51006209594515));
#389857=CARTESIAN_POINT('Ctrl Pts',(2.49052819510455,-1.16609146699378,
7.50731281821699));
#389858=CARTESIAN_POINT('Ctrl Pts',(2.4891160535797,-1.15316682858634,7.51860402984325));
#389859=CARTESIAN_POINT('Ctrl Pts',(2.49375584668795,-1.15919785978368,
7.51860402984325));
#389860=CARTESIAN_POINT('Ctrl Pts',(2.49052926869775,-1.1660891740171,7.51860402984325));
#389861=CARTESIAN_POINT('Origin',(0.,0.,7.5));
#389862=CARTESIAN_POINT('Origin',(2.36243414091427,-1.23929131094302,7.5));
#389863=CARTESIAN_POINT('',(2.36243414091427,-1.23929131094302,7.59394543036555));
#389864=CARTESIAN_POINT('',(2.36243414091427,-1.23929131094302,8.85049129520029));
#389865=CARTESIAN_POINT('',(2.36243414091427,-1.23929131094302,7.5));
#389866=CARTESIAN_POINT('',(2.40229980761781,-1.29863690399938,8.78727029226991));
#389867=CARTESIAN_POINT('Ctrl Pts',(2.36243414091427,-1.23929131094302,
8.85049129520029));
#389868=CARTESIAN_POINT('Ctrl Pts',(2.37574201268456,-1.25910193015075,
8.82945686509571));
#389869=CARTESIAN_POINT('Ctrl Pts',(2.3890301006943,-1.27888309847755,8.80838212259895));
#389870=CARTESIAN_POINT('Ctrl Pts',(2.40229980761781,-1.29863690399938,
8.78727029226991));
#389871=CARTESIAN_POINT('',(2.41011908817659,-1.31027699133282,8.75721825406948));
#389872=CARTESIAN_POINT('Origin',(2.38658832796362,-1.27524781804343,8.75937679713138));
#389873=CARTESIAN_POINT('',(2.41011908817659,-1.31027699133282,7.51860402984325));
#389874=CARTESIAN_POINT('',(2.41011908817659,-1.31027699133282,7.5));
#389875=CARTESIAN_POINT('Ctrl Pts',(2.41011908817659,-1.31027699133282,
7.51860402984325));
#389876=CARTESIAN_POINT('Ctrl Pts',(2.40397825942583,-1.30113551310842,
7.52834476460825));
#389877=CARTESIAN_POINT('Ctrl Pts',(2.39783344413766,-1.29198810036826,
7.53807742314407));
#389878=CARTESIAN_POINT('Ctrl Pts',(2.39168450845877,-1.28283455385309,
7.54780169004674));
#389879=CARTESIAN_POINT('Ctrl Pts',(2.38194492666503,-1.26833583088004,
7.5632044032688));
#389880=CARTESIAN_POINT('Ctrl Pts',(2.37219499495819,-1.25382170062096,
7.57858609112103));
#389881=CARTESIAN_POINT('Ctrl Pts',(2.36243414091427,-1.23929131094302,
7.59394543036555));
#389882=CARTESIAN_POINT('Origin',(2.64297784464841,-1.2237528786782,7.5));
#389883=CARTESIAN_POINT('',(2.45352211735226,-1.22708151028065,8.75721825406948));
#389884=CARTESIAN_POINT('',(2.43950170000244,-1.22732784120416,8.78727029226991));
#389885=CARTESIAN_POINT('Origin',(2.40391265141233,-1.22795312096492,8.75658640621001));
#389886=CARTESIAN_POINT('',(2.36802027905703,-1.22858372995529,8.85049129520029));
#389887=CARTESIAN_POINT('Ctrl Pts',(2.43950170000244,-1.22732784120416,
8.78727029226991));
#389888=CARTESIAN_POINT('Ctrl Pts',(2.41570835638485,-1.22774587699872,
8.80838212259895));
#389889=CARTESIAN_POINT('Ctrl Pts',(2.39188205442815,-1.22816449185294,
8.82945686509571));
#389890=CARTESIAN_POINT('Ctrl Pts',(2.36802027905703,-1.22858372995529,
8.85049129520029));
#389891=CARTESIAN_POINT('',(2.36802027905703,-1.22858372995529,7.59394543036555));
#389892=CARTESIAN_POINT('',(2.36802027905703,-1.22858372995529,7.5));
#389893=CARTESIAN_POINT('',(2.45352211735226,-1.22708151028065,7.51860402984325));
#389894=CARTESIAN_POINT('Ctrl Pts',(2.36802027905703,-1.22858372995529,
7.59394543036555));
#389895=CARTESIAN_POINT('Ctrl Pts',(2.38552204873491,-1.22827623361047,
7.57858609112103));
#389896=CARTESIAN_POINT('Ctrl Pts',(2.40300423403734,-1.22796908135223,
7.56320440326857));
#389897=CARTESIAN_POINT('Ctrl Pts',(2.42046786135375,-1.22766225514746,
7.54780169004651));
#389898=CARTESIAN_POINT('Ctrl Pts',(2.43149325478056,-1.22746854512605,
7.53807742314383));
#389899=CARTESIAN_POINT('Ctrl Pts',(2.44251126011133,-1.22727496490937,
7.52834476460825));
#389900=CARTESIAN_POINT('Ctrl Pts',(2.45352211735226,-1.22708151028065,
7.51860402984325));
#389901=CARTESIAN_POINT('',(2.45352211735226,-1.22708151028065,7.5));
#389902=CARTESIAN_POINT('Origin',(2.36814105033896,-1.23545766909507,7.5));
#389903=CARTESIAN_POINT('Ctrl Pts',(2.36802027905703,-1.22858372995529,
8.85049129520029));
#389904=CARTESIAN_POINT('Ctrl Pts',(2.36782664743443,-1.22858713195504,
8.85097269580138));
#389905=CARTESIAN_POINT('Ctrl Pts',(2.36763560659413,-1.22859890114681,
8.85143669361005));
#389906=CARTESIAN_POINT('Ctrl Pts',(2.36743841348188,-1.22862045209506,
8.8519052845931));
#389907=CARTESIAN_POINT('Ctrl Pts',(2.36705271625984,-1.22866260438311,
8.85282181883899));
#389908=CARTESIAN_POINT('Ctrl Pts',(2.36665342562342,-1.22874128994967,
8.85372622499636));
#389909=CARTESIAN_POINT('Ctrl Pts',(2.36623725715284,-1.22887287130626,
8.85462257735071));
#389910=CARTESIAN_POINT('Ctrl Pts',(2.36589176886947,-1.22898210547517,
8.85536669723986));
#389911=CARTESIAN_POINT('Ctrl Pts',(2.36553456053145,-1.22912778877099,
8.85610498449051));
#389912=CARTESIAN_POINT('Ctrl Pts',(2.36516674476246,-1.22932670510119,
8.8568133821837));
#389913=CARTESIAN_POINT('Ctrl Pts',(2.36483295137445,-1.22950722198325,
8.85745625420284));
#389914=CARTESIAN_POINT('Ctrl Pts',(2.36448595034558,-1.22973331737552,
8.85808743050665));
#389915=CARTESIAN_POINT('Ctrl Pts',(2.36412948034975,-1.23003334385224,
8.85866804508409));
#389916=CARTESIAN_POINT('Ctrl Pts',(2.36396501282099,-1.23017176956482,
8.85893592806395));
#389917=CARTESIAN_POINT('Ctrl Pts',(2.36379858976412,-1.23032616777317,
8.85919241173848));
#389918=CARTESIAN_POINT('Ctrl Pts',(2.36363118640838,-1.23050079886513,
8.85943017985534));
#389919=CARTESIAN_POINT('Ctrl Pts',(2.36340514232144,-1.23073660253561,
8.8597512372));
#389920=CARTESIAN_POINT('Ctrl Pts',(2.36317201985187,-1.23101574189601,
8.86004599534706));
#389921=CARTESIAN_POINT('Ctrl Pts',(2.36294261383862,-1.2313415393257,8.86026130871721));
#389922=CARTESIAN_POINT('Ctrl Pts',(2.36285862182954,-1.23146082294991,
8.86034014101235));
#389923=CARTESIAN_POINT('Ctrl Pts',(2.36277385628191,-1.23158814575575,
8.86040910639693));
#389924=CARTESIAN_POINT('Ctrl Pts',(2.36269090658754,-1.23172022531703,
8.86046313645507));
#389925=CARTESIAN_POINT('Ctrl Pts',(2.36256146428415,-1.23192633436625,
8.8605474499083));
#389926=CARTESIAN_POINT('Ctrl Pts',(2.36243303496201,-1.23214973111174,
8.86059655985668));
#389927=CARTESIAN_POINT('Ctrl Pts',(2.3623136012062,-1.23237594242963,8.86059725258816));
#389928=CARTESIAN_POINT('Ctrl Pts',(2.36219389151071,-1.23260267638603,
8.86059794692011));
#389929=CARTESIAN_POINT('Ctrl Pts',(2.36208424081918,-1.23283599287139,
8.86056369958366));
#389930=CARTESIAN_POINT('Ctrl Pts',(2.36198722379488,-1.23306156611176,
8.86048590497774));
#389931=CARTESIAN_POINT('Ctrl Pts',(2.36196190524008,-1.23312043401138,
8.86046560290182));
#389932=CARTESIAN_POINT('Ctrl Pts',(2.36193720093637,-1.23317957617911,
8.86044257503091));
#389933=CARTESIAN_POINT('Ctrl Pts',(2.36191384397732,-1.23323715242064,
8.86041778462583));
#389934=CARTESIAN_POINT('Ctrl Pts',(2.36175668062649,-1.23362456907998,
8.860250975962));
#389935=CARTESIAN_POINT('Ctrl Pts',(2.36163973822465,-1.23399319749297,
8.8599848982295));
#389936=CARTESIAN_POINT('Ctrl Pts',(2.36155835415756,-1.23432971640827,
8.85968173251461));
#389937=CARTESIAN_POINT('Ctrl Pts',(2.36151530664883,-1.23450771563423,
8.85952137522076));
#389938=CARTESIAN_POINT('Ctrl Pts',(2.36148119228362,-1.23468011742878,
8.85934740853961));
#389939=CARTESIAN_POINT('Ctrl Pts',(2.36145496716656,-1.23484418878627,
8.8591675900182));
#389940=CARTESIAN_POINT('Ctrl Pts',(2.36134965969003,-1.23550302056916,
8.85844552518695));
#389941=CARTESIAN_POINT('Ctrl Pts',(2.36136262189043,-1.23606428711475,
8.85759444184125));
#389942=CARTESIAN_POINT('Ctrl Pts',(2.36141429494935,-1.23652096440835,
8.8568349891514));
#389943=CARTESIAN_POINT('Ctrl Pts',(2.36141970239735,-1.2365687544709,8.85675551444999));
#389944=CARTESIAN_POINT('Ctrl Pts',(2.36142555278898,-1.2366153930834,8.85667699793652));
#389945=CARTESIAN_POINT('Ctrl Pts',(2.36143176723579,-1.23666086755304,
8.85659965593547));
#389946=CARTESIAN_POINT('Ctrl Pts',(2.36151565015589,-1.23727468426451,
8.85555568965886));
#389947=CARTESIAN_POINT('Ctrl Pts',(2.36168491411791,-1.23785248579989,
8.85434650606346));
#389948=CARTESIAN_POINT('Ctrl Pts',(2.36193443177243,-1.2383988756345,8.85297329937117));
#389949=CARTESIAN_POINT('Ctrl Pts',(2.36207477024977,-1.23870618662444,
8.85220095427747));
#389950=CARTESIAN_POINT('Ctrl Pts',(2.36224083995696,-1.23900355556607,
8.85137579139183));
#389951=CARTESIAN_POINT('Ctrl Pts',(2.36243414091427,-1.23929131094302,
8.85049129520029));
#389952=CARTESIAN_POINT('Origin',(2.36814105033896,-1.23545766909507,7.59394543036555));
#389953=CARTESIAN_POINT('Ctrl Pts',(2.36745810113561,-1.22859360710823,
7.59443877723642));
#389954=CARTESIAN_POINT('Ctrl Pts',(2.36166820945803,-1.22869533228006,
7.58783886950016));
#389955=CARTESIAN_POINT('Ctrl Pts',(2.35984916240285,-1.23698811524766,
7.58559994247159));
#389956=CARTESIAN_POINT('Ctrl Pts',(2.39906494993534,-1.22803829237972,
7.56670252222139));
#389957=CARTESIAN_POINT('Ctrl Pts',(2.39328342629499,-1.22813987052987,
7.56004874999027));
#389958=CARTESIAN_POINT('Ctrl Pts',(2.39143273135005,-1.23647721336053,
7.55786368756704));
#389959=CARTESIAN_POINT('Ctrl Pts',(2.43061277610281,-1.22748401464598,
7.5388891333356));
#389960=CARTESIAN_POINT('Ctrl Pts',(2.4247968925844,-1.22758619647998,7.53222002137277));
#389961=CARTESIAN_POINT('Ctrl Pts',(2.42295842125756,-1.23596608119878,
7.53005029815326));
#389962=CARTESIAN_POINT('Ctrl Pts',(2.46210015207758,-1.22693079898846,
7.51101258149734));
#389963=CARTESIAN_POINT('Ctrl Pts',(2.45621376948322,-1.22703421945195,
7.5043616886572));
#389964=CARTESIAN_POINT('Ctrl Pts',(2.4544246758577,-1.23545482664762,7.50217374673251));
#389965=CARTESIAN_POINT('',(2.4527455960751,-1.2354821068197,7.50366116523517));
#389966=CARTESIAN_POINT('Ctrl Pts',(2.45352211735226,-1.22708151028065,
7.51860402984325));
#389967=CARTESIAN_POINT('Ctrl Pts',(2.45396366042423,-1.22707375261481,
7.51734760759493));
#389968=CARTESIAN_POINT('Ctrl Pts',(2.45436370289139,-1.22712623008085,
7.51608817408572));
#389969=CARTESIAN_POINT('Ctrl Pts',(2.45471958779321,-1.22725206218929,
7.51481005913119));
#389970=CARTESIAN_POINT('Ctrl Pts',(2.45504195684142,-1.22736604391997,
7.51365231206383));
#389971=CARTESIAN_POINT('Ctrl Pts',(2.45532863165976,-1.22754013918379,
7.51247773061042));
#389972=CARTESIAN_POINT('Ctrl Pts',(2.45555548502426,-1.22780289648395,
7.51129758471022));
#389973=CARTESIAN_POINT('Ctrl Pts',(2.4558374378487,-1.22812947380003,7.50983079813402));
#389974=CARTESIAN_POINT('Ctrl Pts',(2.4560081234602,-1.2285911021057,7.50839324291155));
#389975=CARTESIAN_POINT('Ctrl Pts',(2.45599146426144,-1.22921974058831,
7.50715379678855));
#389976=CARTESIAN_POINT('Ctrl Pts',(2.45598376819163,-1.2295101534535,7.50658120839351));
#389977=CARTESIAN_POINT('Ctrl Pts',(2.45592549702895,-1.22987724229966,
7.50598221009429));
#389978=CARTESIAN_POINT('Ctrl Pts',(2.45579557233092,-1.23030870483474,
7.50545747549611));
#389979=CARTESIAN_POINT('Ctrl Pts',(2.4557262404905,-1.23053894659848,7.50517746087247));
#389980=CARTESIAN_POINT('Ctrl Pts',(2.45563594654121,-1.23079007457347,
7.50491486231392));
#389981=CARTESIAN_POINT('Ctrl Pts',(2.45552551198024,-1.23105487409866,
7.50468370960992));
#389982=CARTESIAN_POINT('Ctrl Pts',(2.45536037747697,-1.2314508329151,7.50433806340446));
#389983=CARTESIAN_POINT('Ctrl Pts',(2.45514474366126,-1.23188901991197,
7.50405484070983));
#389984=CARTESIAN_POINT('Ctrl Pts',(2.45489249028928,-1.23233960769465,
7.5038576603613));
#389985=CARTESIAN_POINT('Ctrl Pts',(2.45486551571206,-1.23238779105428,
7.50383657498791));
#389986=CARTESIAN_POINT('Ctrl Pts',(2.45483814690575,-1.23243610195335,
7.50381643264937));
#389987=CARTESIAN_POINT('Ctrl Pts',(2.45481041881372,-1.23248449383456,
7.50379723213559));
#389988=CARTESIAN_POINT('Ctrl Pts',(2.45462532472886,-1.23280752547174,
7.50366906242519));
#389989=CARTESIAN_POINT('Ctrl Pts',(2.45441957075853,-1.23314083487669,
7.50358235568538));
#389990=CARTESIAN_POINT('Ctrl Pts',(2.45421352660268,-1.23345733688091,
7.5035341175365));
#389991=CARTESIAN_POINT('Ctrl Pts',(2.45390458671068,-1.23393189581513,
7.50346178989176));
#389992=CARTESIAN_POINT('Ctrl Pts',(2.45355205999195,-1.23442927747066,
7.50346967198527));
#389993=CARTESIAN_POINT('Ctrl Pts',(2.45319096374894,-1.23490690351009,
7.50354272648692));
#389994=CARTESIAN_POINT('Ctrl Pts',(2.45304243738994,-1.23510336098639,
7.50357277531559));
#389995=CARTESIAN_POINT('Ctrl Pts',(2.45289277165099,-1.23529630060034,
7.50361331098761));
#389996=CARTESIAN_POINT('Ctrl Pts',(2.45274559607637,-1.23548210682034,
7.50366116523658));
#389997=CARTESIAN_POINT('',(2.37073694677488,-1.23681194660316,7.57603338622103));
#389998=CARTESIAN_POINT('Origin',(2.37857045058689,-1.24090189863638,7.58486873427626));
#389999=CARTESIAN_POINT('Ctrl Pts',(2.4527455961321,-1.23548210681342,7.50366116529969));
#390000=CARTESIAN_POINT('Ctrl Pts',(2.4254540003185,-1.23592549913165,7.52783573079709));
#390001=CARTESIAN_POINT('Ctrl Pts',(2.39811907485908,-1.23636877604875,
7.55196141284068));
#390002=CARTESIAN_POINT('Ctrl Pts',(2.37073694797006,-1.2368119462301,7.57603338728831));
#390003=CARTESIAN_POINT('Ctrl Pts',(2.36905161742718,-1.22874145340458,
7.59639677331371));
#390004=CARTESIAN_POINT('Ctrl Pts',(2.35095584851581,-1.22616947687808,
7.59959882295464));
#390005=CARTESIAN_POINT('Ctrl Pts',(2.36303201114798,-1.239912660959,7.59642833564546));
#390006=CARTESIAN_POINT('Ctrl Pts',(2.3653282199157,-1.22757894961742,7.58707626057423));
#390007=CARTESIAN_POINT('Ctrl Pts',(2.35934533569769,-1.23075973371418,
7.58809943920598));
#390008=CARTESIAN_POINT('Ctrl Pts',(2.36005021803306,-1.23748413269744,
7.58710240504251));
#390009=CARTESIAN_POINT('Ctrl Pts',(2.36807985450295,-1.23299689566364,
7.58015376756929));
#390010=CARTESIAN_POINT('Ctrl Pts',(2.36540964568615,-1.23399652372966,
7.58205880659761));
#390011=CARTESIAN_POINT('Ctrl Pts',(2.36606760176506,-1.23673407169023,
7.58020924244128));
#390012=CARTESIAN_POINT('Ctrl Pts',(2.37073694604125,-1.23681194622019,
7.57603338509286));
#390013=CARTESIAN_POINT('Ctrl Pts',(2.37073694604125,-1.23681194622019,
7.57603338509286));
#390014=CARTESIAN_POINT('Ctrl Pts',(2.37073694604125,-1.23681194622019,
7.57603338509286));
#390015=CARTESIAN_POINT('Origin',(2.37857308999301,-1.24089683938831,7.58486873427622));
#390016=CARTESIAN_POINT('Ctrl Pts',(2.41491823580731,-1.31742119048614,
7.51098857897448));
#390017=CARTESIAN_POINT('Ctrl Pts',(2.41163534588057,-1.31253415194519,
7.50433767179957));
#390018=CARTESIAN_POINT('Ctrl Pts',(2.41751815819882,-1.30624920402888,
7.50214974420965));
#390019=CARTESIAN_POINT('Ctrl Pts',(2.39735246464699,-1.29127209545774,
7.53887321589167));
#390020=CARTESIAN_POINT('Ctrl Pts',(2.39410890956768,-1.28644361231143,
7.53220407452063));
#390021=CARTESIAN_POINT('Ctrl Pts',(2.39993004937041,-1.2801414498795,7.53003438070911));
#390022=CARTESIAN_POINT('Ctrl Pts',(2.37975296072629,-1.26507278452087,
7.56669465659228));
#390023=CARTESIAN_POINT('Ctrl Pts',(2.37652857445443,-1.26027283681224,
7.56004085833293));
#390024=CARTESIAN_POINT('Ctrl Pts',(2.38230781672176,-1.25398499068329,
7.55785582193789));
#390025=CARTESIAN_POINT('Ctrl Pts',(2.36212052000037,-1.23882444256556,
7.59443891967696));
#390026=CARTESIAN_POINT('Ctrl Pts',(2.35889145876987,-1.23401753553038,
7.58783901202978));
#390027=CARTESIAN_POINT('Ctrl Pts',(2.36465226193379,-1.22778116439847,
7.58560008491213));
#390028=CARTESIAN_POINT('',(2.41656476362039,-1.30483398889123,7.50366116523517));
#390029=CARTESIAN_POINT('Ctrl Pts',(2.41656476362071,-1.30483398889141,
7.50366116523554));
#390030=CARTESIAN_POINT('Ctrl Pts',(2.41634661309174,-1.30555962506986,
7.50350835821027));
#390031=CARTESIAN_POINT('Ctrl Pts',(2.41612247199273,-1.30621956353584,
7.50345484956));
#390032=CARTESIAN_POINT('Ctrl Pts',(2.41588624502761,-1.30683361791562,
7.50349758195598));
#390033=CARTESIAN_POINT('Ctrl Pts',(2.41576504307546,-1.30714867335191,
7.50351950684424));
#390034=CARTESIAN_POINT('Ctrl Pts',(2.41562883423954,-1.30748274963566,
7.50357029184312));
#390035=CARTESIAN_POINT('Ctrl Pts',(2.4154886344741,-1.30780128515433,7.50365515313923));
#390036=CARTESIAN_POINT('Ctrl Pts',(2.41527295046236,-1.30829132176982,
7.50378570417639));
#390037=CARTESIAN_POINT('Ctrl Pts',(2.41504180768278,-1.30875910258838,
7.50400001621911));
#390038=CARTESIAN_POINT('Ctrl Pts',(2.41481076397667,-1.30916801691215,
7.50428903009634));
#390039=CARTESIAN_POINT('Ctrl Pts',(2.41478511990283,-1.30921340325609,
7.50432110841318));
#390040=CARTESIAN_POINT('Ctrl Pts',(2.41475947975433,-1.30925809460094,
7.50435406373354));
#390041=CARTESIAN_POINT('Ctrl Pts',(2.41473386649755,-1.30930206320098,
7.50438785222352));
#390042=CARTESIAN_POINT('Ctrl Pts',(2.41457748525367,-1.30957051263821,
7.50459414719561));
#390043=CARTESIAN_POINT('Ctrl Pts',(2.41441917105307,-1.30981603477638,
7.50483629897752));
#390044=CARTESIAN_POINT('Ctrl Pts',(2.41426609490188,-1.31002993691338,
7.5050991045531));
#390045=CARTESIAN_POINT('Ctrl Pts',(2.4139283935373,-1.31050182651205,7.50567888004914));
#390046=CARTESIAN_POINT('Ctrl Pts',(2.41360330086178,-1.31083872331849,
7.50637912803144));
#390047=CARTESIAN_POINT('Ctrl Pts',(2.41330668489005,-1.31106715325333,
7.50710440483569));
#390048=CARTESIAN_POINT('Ctrl Pts',(2.41323394876513,-1.31112316880832,
7.50728225710685));
#390049=CARTESIAN_POINT('Ctrl Pts',(2.41316156611973,-1.3111738926814,7.50746498566954));
#390050=CARTESIAN_POINT('Ctrl Pts',(2.41309146567674,-1.31121848197554,
7.50764697238949));
#390051=CARTESIAN_POINT('Ctrl Pts',(2.41271462498742,-1.31145818174953,
7.50862528291182));
#390052=CARTESIAN_POINT('Ctrl Pts',(2.41237174905259,-1.31154585365796,
7.50965856837422));
#390053=CARTESIAN_POINT('Ctrl Pts',(2.41206139769779,-1.31154777983823,
7.51067959873202));
#390054=CARTESIAN_POINT('Ctrl Pts',(2.41189061095579,-1.31154883981766,
7.51124147302578));
#390055=CARTESIAN_POINT('Ctrl Pts',(2.41172962930471,-1.31152349915076,
7.51180065547253));
#390056=CARTESIAN_POINT('Ctrl Pts',(2.41157829503253,-1.31148008890242,
7.51235175716501));
#390057=CARTESIAN_POINT('Ctrl Pts',(2.41105537483773,-1.31133008920183,
7.51425603304535));
#390058=CARTESIAN_POINT('Ctrl Pts',(2.41058696594895,-1.31094062862543,
7.51626900505179));
#390059=CARTESIAN_POINT('Ctrl Pts',(2.41018394501642,-1.31037107354313,
7.51827788969242));
#390060=CARTESIAN_POINT('Ctrl Pts',(2.41016213276194,-1.31034024814576,
7.51838661432544));
#390061=CARTESIAN_POINT('Ctrl Pts',(2.41014051310065,-1.31030888531403,
7.51849533314856));
#390062=CARTESIAN_POINT('Ctrl Pts',(2.41011908817659,-1.31027699133282,
7.51860402984325));
#390063=CARTESIAN_POINT('Ctrl Pts',(2.37073694715363,-1.23681194779762,
7.57603338728985));
#390064=CARTESIAN_POINT('Ctrl Pts',(2.3860392422531,-1.25952355359293,7.55196141284922));
#390065=CARTESIAN_POINT('Ctrl Pts',(2.40131444509586,-1.28219650716416,
7.52783573083105));
#390066=CARTESIAN_POINT('Ctrl Pts',(2.4165647636488,-1.30483398894315,7.50366116530176));
#390067=CARTESIAN_POINT('Origin',(8.19199203866634E-16,-4.2737569993508E-16,
7.49482233047033));
#390068=CARTESIAN_POINT('Origin',(2.44485166369886,-1.23150582317296,7.49482233047033));
#390069=CARTESIAN_POINT('Origin',(0.,0.,7.50366116523517));
#390070=CARTESIAN_POINT('Origin',(2.4087872758706,-1.30063450269625,7.49482233047033));
#390071=CARTESIAN_POINT('Ctrl Pts',(2.45352105979442,-1.22708152881659,
7.51860402984325));
#390072=CARTESIAN_POINT('Ctrl Pts',(2.46112885786553,-1.22694850799354,
7.51860402984325));
#390073=CARTESIAN_POINT('Ctrl Pts',(2.46450482787547,-1.2201294822184,7.51860402984325));
#390074=CARTESIAN_POINT('Ctrl Pts',(2.45634588711433,-1.22703213600668,
7.51041458714366));
#390075=CARTESIAN_POINT('Ctrl Pts',(2.46192865495691,-1.22533299829126,
7.51004642900444));
#390076=CARTESIAN_POINT('Ctrl Pts',(2.46450575892791,-1.22012760161205,
7.50729136483012));
#390077=CARTESIAN_POINT('Ctrl Pts',(2.45736298124955,-1.22965687536886,
7.50215815450137));
#390078=CARTESIAN_POINT('Ctrl Pts',(2.46030031409413,-1.22862239953949,
7.49877163671528));
#390079=CARTESIAN_POINT('Ctrl Pts',(2.46185245611966,-1.22554103965674,
7.49481588533168));
#390080=CARTESIAN_POINT('Ctrl Pts',(2.45274510440917,-1.23548185916126,
7.50366171572174));
#390081=CARTESIAN_POINT('Ctrl Pts',(2.45601536992562,-1.23712913743437,
7.50000045605858));
#390082=CARTESIAN_POINT('Ctrl Pts',(2.45601536992568,-1.23712913743426,
7.49482233047317));
#390083=CARTESIAN_POINT('Origin',(2.4533025332033,-1.2145834391174,7.51860402984325));
#390084=CARTESIAN_POINT('Origin',(2.4533025332033,-1.2145834391174,9.));
#390085=CARTESIAN_POINT('Origin',(2.4533025332033,-1.2145834391174,8.75721825406948));
#390086=CARTESIAN_POINT('Ctrl Pts',(2.43682453266412,-1.22737484732809,
8.78942910404913));
#390087=CARTESIAN_POINT('Ctrl Pts',(2.44239646176361,-1.22729716327585,
8.7967269950169));
#390088=CARTESIAN_POINT('Ctrl Pts',(2.44391314215674,-1.21850096144966,
8.79893251111267));
#390089=CARTESIAN_POINT('Ctrl Pts',(2.4478171719985,-1.2271817173077,8.78111911759583));
#390090=CARTESIAN_POINT('Ctrl Pts',(2.45442265473793,-1.22708217884974,
8.78644465894815));
#390091=CARTESIAN_POINT('Ctrl Pts',(2.4574813331055,-1.21957484920337,8.78817647674131));
#390092=CARTESIAN_POINT('Ctrl Pts',(2.45466804703033,-1.22706135404059,
8.7678092393203));
#390093=CARTESIAN_POINT('Ctrl Pts',(2.46246546371487,-1.22693875788232,
8.76988516158373));
#390094=CARTESIAN_POINT('Ctrl Pts',(2.46595667361419,-1.2202344433137,8.77093053738834));
#390095=CARTESIAN_POINT('Ctrl Pts',(2.4533322201599,-1.22708482322866,8.75371302330492));
#390096=CARTESIAN_POINT('Ctrl Pts',(2.46093827577204,-1.22696599817774,
8.75300828287559));
#390097=CARTESIAN_POINT('Ctrl Pts',(2.46430367349725,-1.22010533950051,
8.75267964240738));
#390098=CARTESIAN_POINT('Origin',(2.43928211585348,-1.21482977004092,8.78727029226991));
#390099=CARTESIAN_POINT('Ctrl Pts',(2.36802027905703,-1.22858372995529,
8.85049129520029));
#390100=CARTESIAN_POINT('Ctrl Pts',(2.37385899372368,-1.22848114699074,
8.85711686593484));
#390101=CARTESIAN_POINT('Ctrl Pts',(2.3756631770946,-1.2201237739299,8.85933012996512));
#390102=CARTESIAN_POINT('Ctrl Pts',(2.39188208645158,-1.2281644912903,8.82945683644727));
#390103=CARTESIAN_POINT('Ctrl Pts',(2.39776926598011,-1.22806105682512,
8.83607469902394));
#390104=CARTESIAN_POINT('Ctrl Pts',(2.39954208843698,-1.21967123304662,
8.8382956714852));
#390105=CARTESIAN_POINT('Ctrl Pts',(2.41570832589791,-1.22774587753436,
8.80838214965001));
#390106=CARTESIAN_POINT('Ctrl Pts',(2.42161873898552,-1.22764203486849,
8.81501364461988));
#390107=CARTESIAN_POINT('Ctrl Pts',(2.42338478937515,-1.21922004706177,
8.81722098428721));
#390108=CARTESIAN_POINT('Ctrl Pts',(2.43950170000244,-1.22732784120416,
8.78727029226991));
#390109=CARTESIAN_POINT('Ctrl Pts',(2.44541309482909,-1.22722398128969,
8.79393457792714));
#390110=CARTESIAN_POINT('Ctrl Pts',(2.44719404240189,-1.21877012767603,
8.79610912703474));
#390111=CARTESIAN_POINT('Origin',(2.36780069490807,-1.21608565879204,8.85049129520029));
#390112=CARTESIAN_POINT('Ctrl Pts',(2.36243414091427,-1.23929131094302,
8.85049129520029));
#390113=CARTESIAN_POINT('Ctrl Pts',(2.36569043114743,-1.24413875213817,
8.85711686593484));
#390114=CARTESIAN_POINT('Ctrl Pts',(2.35986814900604,-1.25039988564417,
8.85933012996512));
#390115=CARTESIAN_POINT('Ctrl Pts',(2.35955334795003,-1.23500284969122,
8.86332496987232));
#390116=CARTESIAN_POINT('Ctrl Pts',(2.35767030474025,-1.23922257037471,
8.86648636486737));
#390117=CARTESIAN_POINT('Ctrl Pts',(2.35182323496413,-1.23839318691325,
8.87206031107457));
#390118=CARTESIAN_POINT('Ctrl Pts',(2.36281975177211,-1.22867510032301,
8.86341338519876));
#390119=CARTESIAN_POINT('Ctrl Pts',(2.365184693223,-1.22469006298715,8.86654584966058));
#390120=CARTESIAN_POINT('Ctrl Pts',(2.36110168311631,-1.2203943463699,8.87215952290714));
#390121=CARTESIAN_POINT('Ctrl Pts',(2.36802027905703,-1.22858372995529,
8.85049129520029));
#390122=CARTESIAN_POINT('Ctrl Pts',(2.37385899372368,-1.22848114699074,
8.85711686593484));
#390123=CARTESIAN_POINT('Ctrl Pts',(2.3756631770946,-1.2201237739299,8.85933012996512));
#390124=CARTESIAN_POINT('Origin',(2.35205794196028,-1.24626156884838,8.85049129520029));
#390125=CARTESIAN_POINT('Ctrl Pts',(2.40229980761781,-1.29863690399938,
8.78727029226991));
#390126=CARTESIAN_POINT('Ctrl Pts',(2.40559663206248,-1.30354468600957,
8.79393457792714));
#390127=CARTESIAN_POINT('Ctrl Pts',(2.39968192566134,-1.30984196029027,
8.79610912703474));
#390128=CARTESIAN_POINT('Ctrl Pts',(2.38903008369152,-1.27888307316656,
8.80838214965002));
#390129=CARTESIAN_POINT('Ctrl Pts',(2.39232636061378,-1.28379004011344,
8.81501364461994));
#390130=CARTESIAN_POINT('Ctrl Pts',(2.38642926673667,-1.29005686517877,
8.81722098428721));
#390131=CARTESIAN_POINT('Ctrl Pts',(2.37574203054421,-1.25910195673733,
8.82945683644721));
#390132=CARTESIAN_POINT('Ctrl Pts',(2.37902534995513,-1.26398963462521,
8.83607469902388));
#390133=CARTESIAN_POINT('Ctrl Pts',(2.37315851053407,-1.27024361237585,
8.8382956714852));
#390134=CARTESIAN_POINT('Ctrl Pts',(2.36243414091427,-1.23929131094302,
8.85049129520029));
#390135=CARTESIAN_POINT('Ctrl Pts',(2.36569043114743,-1.24413875213817,
8.85711686593484));
#390136=CARTESIAN_POINT('Ctrl Pts',(2.35986814900604,-1.25039988564417,
8.85933012996512));
#390137=CARTESIAN_POINT('Origin',(2.39192360866382,-1.30560716190474,8.78727029226991));
#390138=CARTESIAN_POINT('Ctrl Pts',(2.41001582319739,-1.31012330012149,
8.75374538247848));
#390139=CARTESIAN_POINT('Ctrl Pts',(2.4142640535715,-1.31642384907187,8.75304829418602));
#390140=CARTESIAN_POINT('Ctrl Pts',(2.41057140660496,-1.32310479223804,
8.75272238421917));
#390141=CARTESIAN_POINT('Ctrl Pts',(2.41075187368563,-1.31121901294557,
8.76769408445017));
#390142=CARTESIAN_POINT('Ctrl Pts',(2.41510643619571,-1.31767849746976,
8.76974318093966));
#390143=CARTESIAN_POINT('Ctrl Pts',(2.41161165479856,-1.32437214074275,
8.77077869880429));
#390144=CARTESIAN_POINT('Ctrl Pts',(2.40697929819551,-1.30560301318752,
8.78108014887992));
#390145=CARTESIAN_POINT('Ctrl Pts',(2.41067278344331,-1.3110750698415,8.78639403366328));
#390146=CARTESIAN_POINT('Ctrl Pts',(2.40628851871305,-1.31787950211055,
8.78812224174742));
#390147=CARTESIAN_POINT('Ctrl Pts',(2.40079687974257,-1.29639962934831,
8.78944554828685));
#390148=CARTESIAN_POINT('Ctrl Pts',(2.40391425189903,-1.30100814412588,
8.79673892988685));
#390149=CARTESIAN_POINT('Ctrl Pts',(2.39757616771976,-1.30727968646034,
8.79894799272499));
#390150=CARTESIAN_POINT('Origin',(2.3997428892226,-1.31724724923818,8.75721825406948));
#390151=CARTESIAN_POINT('Origin',(2.3997428892226,-1.31724724923818,9.));
#390152=CARTESIAN_POINT('Origin',(2.3997428892226,-1.31724724923818,7.51860402984325));
#390153=CARTESIAN_POINT('Ctrl Pts',(2.41656407141738,-1.30483361513347,
7.50366195182966));
#390154=CARTESIAN_POINT('Ctrl Pts',(2.41978630452747,-1.30657347302832,
7.50000065167735));
#390155=CARTESIAN_POINT('Ctrl Pts',(2.41978630452742,-1.30657347302842,
7.49482233047108));
#390156=CARTESIAN_POINT('Ctrl Pts',(2.41442578748733,-1.31195973198917,
7.50215800491338));
#390157=CARTESIAN_POINT('Ctrl Pts',(2.41525681547057,-1.3149620793484,7.49877273257266));
#390158=CARTESIAN_POINT('Ctrl Pts',(2.41361667159589,-1.31799969097932,
7.49481816995647));
#390159=CARTESIAN_POINT('Ctrl Pts',(2.41169107100778,-1.31261649840008,
7.51043025814041));
#390160=CARTESIAN_POINT('Ctrl Pts',(2.41349603202948,-1.31816941409338,
7.51006209594513));
#390161=CARTESIAN_POINT('Ctrl Pts',(2.41069940101147,-1.32326429634043,
7.50731281821699));
#390162=CARTESIAN_POINT('Ctrl Pts',(2.41011824530877,-1.31027573677064,
7.51860402984325));
#390163=CARTESIAN_POINT('Ctrl Pts',(2.41436209596894,-1.31659164913266,
7.51860402984324));
#390164=CARTESIAN_POINT('Ctrl Pts',(2.41070061931038,-1.32326207686028,
7.51860402984325));
#390165=CARTESIAN_POINT('Origin',(0.,0.,7.5));
#390166=CARTESIAN_POINT('Origin',(-0.33515558185988,2.64662214142562,7.5));
#390167=CARTESIAN_POINT('',(-0.33515558185988,2.64662214142562,7.59394543036555));
#390168=CARTESIAN_POINT('',(-0.33515558185988,2.64662214142562,8.85049129520029));
#390169=CARTESIAN_POINT('',(-0.33515558185988,2.64662214142562,7.5));
#390170=CARTESIAN_POINT('',(-0.309289785090423,2.71327145765926,8.78727029226991));
#390171=CARTESIAN_POINT('Ctrl Pts',(-0.33515558185988,2.64662214142562,
8.85049129520029));
#390172=CARTESIAN_POINT('Ctrl Pts',(-0.32652111678987,2.66887087391543,
8.82945686509571));
#390173=CARTESIAN_POINT('Ctrl Pts',(-0.317899487896255,2.6910865309741,
8.80838212259895));
#390174=CARTESIAN_POINT('Ctrl Pts',(-0.309289785090423,2.71327145765926,
8.78727029226991));
#390175=CARTESIAN_POINT('',(-0.304216449096299,2.72634410251322,8.75721825406948));
#390176=CARTESIAN_POINT('Origin',(-0.319484065187221,2.68700405222604,8.7593767971307));
#390177=CARTESIAN_POINT('',(-0.304216449096299,2.72634410251322,7.51860402984325));
#390178=CARTESIAN_POINT('',(-0.304216449096299,2.72634410251322,7.5));
#390179=CARTESIAN_POINT('Ctrl Pts',(-0.304216449096299,2.72634410251322,
7.51860402984325));
#390180=CARTESIAN_POINT('Ctrl Pts',(-0.308200765466687,2.71607757316129,
7.52834476460825));
#390181=CARTESIAN_POINT('Ctrl Pts',(-0.312187668397775,2.70580437892665,
7.53807742314407));
#390182=CARTESIAN_POINT('Ctrl Pts',(-0.316177244736769,2.69552429602699,
7.54780169004674));
#390183=CARTESIAN_POINT('Ctrl Pts',(-0.322496518039534,2.67924120030501,
7.5632044032688));
#390184=CARTESIAN_POINT('Ctrl Pts',(-0.328822506613102,2.66294080110644,
7.57858609112103));
#390185=CARTESIAN_POINT('Ctrl Pts',(-0.33515558185988,2.64662214142562,
7.59394543036555));
#390186=CARTESIAN_POINT('Origin',(-0.508403499682097,2.86782650745936,7.5));
#390187=CARTESIAN_POINT('',(-0.397282670454307,2.71434454205174,8.75721825406948));
#390188=CARTESIAN_POINT('',(-0.389059322317692,2.70298631476879,8.78727029226991));
#390189=CARTESIAN_POINT('Origin',(-0.368185397591817,2.67415489751821,8.756586406211));
#390190=CARTESIAN_POINT('',(-0.347133565397089,2.64507775146798,8.85049129520029));
#390191=CARTESIAN_POINT('Ctrl Pts',(-0.389059322317692,2.70298631476879,
8.78727029226991));
#390192=CARTESIAN_POINT('Ctrl Pts',(-0.375103892673939,2.68371083973215,
8.80838212259896));
#390193=CARTESIAN_POINT('Ctrl Pts',(-0.361129132086614,2.66440866446988,
8.82945686509571));
#390194=CARTESIAN_POINT('Ctrl Pts',(-0.347133565397089,2.64507775146798,
8.85049129520029));
#390195=CARTESIAN_POINT('',(-0.347133565397089,2.64507775146798,7.59394543036555));
#390196=CARTESIAN_POINT('',(-0.347133565397089,2.64507775146798,7.5));
#390197=CARTESIAN_POINT('',(-0.397282670454307,2.71434454205174,7.51860402984325));
#390198=CARTESIAN_POINT('Ctrl Pts',(-0.347133565397089,2.64507775146798,
7.59394543036555));
#390199=CARTESIAN_POINT('Ctrl Pts',(-0.357398819381834,2.65925629358232,
7.57858609112103));
#390200=CARTESIAN_POINT('Ctrl Pts',(-0.367652586608838,2.67341896999297,
7.56320440326857));
#390201=CARTESIAN_POINT('Ctrl Pts',(-0.377895469082858,2.68756661219899,
7.54780169004651));
#390202=CARTESIAN_POINT('Ctrl Pts',(-0.384362155931739,2.6964985092532,
7.53807742314383));
#390203=CARTESIAN_POINT('Ctrl Pts',(-0.390824509465548,2.70542442105947,
7.52834476460825));
#390204=CARTESIAN_POINT('Ctrl Pts',(-0.397282670454307,2.71434454205174,
7.51860402984325));
#390205=CARTESIAN_POINT('',(-0.397282670454307,2.71434454205174,7.5));
#390206=CARTESIAN_POINT('Origin',(-0.341564846497304,2.6491094998251,7.5));
#390207=CARTESIAN_POINT('Ctrl Pts',(-0.347133565397089,2.64507775146798,
8.85049129520029));
#390208=CARTESIAN_POINT('Ctrl Pts',(-0.347019995294062,2.64492088652425,
8.85097269580139));
#390209=CARTESIAN_POINT('Ctrl Pts',(-0.346901044882014,2.64477093347823,
8.85143669361005));
#390210=CARTESIAN_POINT('Ctrl Pts',(-0.346770551927422,2.64462153081529,
8.8519052845931));
#390211=CARTESIAN_POINT('Ctrl Pts',(-0.346515315983802,2.64432930868135,
8.85282181883899));
#390212=CARTESIAN_POINT('Ctrl Pts',(-0.346222339439948,2.64404683890339,
8.85372622499636));
#390213=CARTESIAN_POINT('Ctrl Pts',(-0.345876323146614,2.64378078895684,
8.85462257735071));
#390214=CARTESIAN_POINT('Ctrl Pts',(-0.345589072709225,2.64355992374042,
8.85536669723986));
#390215=CARTESIAN_POINT('Ctrl Pts',(-0.345265222470721,2.64335029921311,
8.85610498449051));
#390216=CARTESIAN_POINT('Ctrl Pts',(-0.34489164328641,2.64316243027106,
8.85681338218371));
#390217=CARTESIAN_POINT('Ctrl Pts',(-0.344552619589932,2.6429919389111,
8.85745625420284));
#390218=CARTESIAN_POINT('Ctrl Pts',(-0.344168657352609,2.6428366912356,
8.85808743050666));
#390219=CARTESIAN_POINT('Ctrl Pts',(-0.343718641537305,2.64271597458123,
8.8586680450841));
#390220=CARTESIAN_POINT('Ctrl Pts',(-0.343511013995271,2.64266027853372,
8.85893592806395));
#390221=CARTESIAN_POINT('Ctrl Pts',(-0.343289167465158,2.64261211674724,
8.85919241173848));
#390222=CARTESIAN_POINT('Ctrl Pts',(-0.343050165639967,2.64257472651662,
8.85943017985534));
#390223=CARTESIAN_POINT('Ctrl Pts',(-0.342727442423848,2.6425242386366,
8.8597512372));
#390224=CARTESIAN_POINT('Ctrl Pts',(-0.342365126816596,2.64249273833371,
8.86004599534705));
#390225=CARTESIAN_POINT('Ctrl Pts',(-0.341966669802032,2.64249098002396,
8.86026130871721));
#390226=CARTESIAN_POINT('Ctrl Pts',(-0.341820783455307,2.64249033625719,
8.86034014101235));
#390227=CARTESIAN_POINT('Ctrl Pts',(-0.341667861040585,2.64249365740532,
8.86040910639693));
#390228=CARTESIAN_POINT('Ctrl Pts',(-0.341512076146919,2.64250118928493,
8.86046313645507));
#390229=CARTESIAN_POINT('Ctrl Pts',(-0.341268975125039,2.64251294271999,
8.8605474499083));
#390230=CARTESIAN_POINT('Ctrl Pts',(-0.341012274757778,2.6425354175532,
8.86059655985669));
#390231=CARTESIAN_POINT('Ctrl Pts',(-0.34075841246969,2.6425668805641,8.86059725258816));
#390232=CARTESIAN_POINT('Ctrl Pts',(-0.340503963658298,2.64259841626712,
8.86059794692011));
#390233=CARTESIAN_POINT('Ctrl Pts',(-0.340249870963048,2.64264196806059,
8.86056369958366));
#390234=CARTESIAN_POINT('Ctrl Pts',(-0.340009356993999,2.64269145159793,
8.86048590497774));
#390235=CARTESIAN_POINT('Ctrl Pts',(-0.339946590009041,2.64270436532787,
8.86046560290182));
#390236=CARTESIAN_POINT('Ctrl Pts',(-0.339883949500254,2.64271793976287,
8.86044257503091));
#390237=CARTESIAN_POINT('Ctrl Pts',(-0.339823364159025,2.64273172336011,
8.86041778462583));
#390238=CARTESIAN_POINT('Ctrl Pts',(-0.339415699992699,2.64282446986554,
8.860250975962));
#390239=CARTESIAN_POINT('Ctrl Pts',(-0.339046456499739,2.64293945540863,
8.8599848982295));
#390240=CARTESIAN_POINT('Ctrl Pts',(-0.338723891841615,2.64306523453273,
8.85968173251461));
#390241=CARTESIAN_POINT('Ctrl Pts',(-0.338553273618219,2.6431317644831,
8.85952137522076));
#390242=CARTESIAN_POINT('Ctrl Pts',(-0.338392357052997,2.64320241876617,
8.85934740853961));
#390243=CARTESIAN_POINT('Ctrl Pts',(-0.338242786451433,2.64327477760985,
8.8591675900182));
#390244=CARTESIAN_POINT('Ctrl Pts',(-0.33764218274091,2.64356533597861,
8.85844552518696));
#390245=CARTESIAN_POINT('Ctrl Pts',(-0.337189263383585,2.64389707715723,
8.85759444184127));
#390246=CARTESIAN_POINT('Ctrl Pts',(-0.336844272355958,2.64420073065444,
8.85683498915143));
#390247=CARTESIAN_POINT('Ctrl Pts',(-0.336808169963697,2.64423250718423,
8.85675551445001));
#390248=CARTESIAN_POINT('Ctrl Pts',(-0.336773265374242,2.64426398824035,
8.85667699793653));
#390249=CARTESIAN_POINT('Ctrl Pts',(-0.336739523864507,2.64429510185888,
8.85659965593548));
#390250=CARTESIAN_POINT('Ctrl Pts',(-0.336284079244434,2.64471507506948,
8.85555568965887));
#390251=CARTESIAN_POINT('Ctrl Pts',(-0.335907021189084,2.64518447055947,
8.85434650606346));
#390252=CARTESIAN_POINT('Ctrl Pts',(-0.335601640613694,2.64570171674404,
8.85297329937118));
#390253=CARTESIAN_POINT('Ctrl Pts',(-0.335429882647148,2.64599263620658,
8.85220095427747));
#390254=CARTESIAN_POINT('Ctrl Pts',(-0.335281000138073,2.64629897169846,
8.85137579139184));
#390255=CARTESIAN_POINT('Ctrl Pts',(-0.33515558185988,2.64662214142562,
8.85049129520029));
#390256=CARTESIAN_POINT('Origin',(-0.341564846497304,2.6491094998251,7.59394543036555));
#390257=CARTESIAN_POINT('Ctrl Pts',(-0.346803833075487,2.64462231961844,
7.59443877723642));
#390258=CARTESIAN_POINT('Ctrl Pts',(-0.343407907422914,2.63993180977292,
7.58783886950016));
#390259=CARTESIAN_POINT('Ctrl Pts',(-0.335565689793683,2.643184317143,7.58559994247159));
#390260=CARTESIAN_POINT('Ctrl Pts',(-0.365342091580668,2.67022767525142,
7.56670252222137));
#390261=CARTESIAN_POINT('Ctrl Pts',(-0.36195107400472,2.66554394452432,
7.56004874999028));
#390262=CARTESIAN_POINT('Ctrl Pts',(-0.35405420332713,2.66879598861332,
7.55786368756704));
#390263=CARTESIAN_POINT('Ctrl Pts',(-0.383845731740252,2.695785215441,7.53888913333557));
#390264=CARTESIAN_POINT('Ctrl Pts',(-0.380434561180877,2.69107364907285,
7.53222002137277));
#390265=CARTESIAN_POINT('Ctrl Pts',(-0.372509792162566,2.69436005755723,
7.53005029815326));
#390266=CARTESIAN_POINT('Ctrl Pts',(-0.402313916252076,2.72129378369128,
7.51101258149734));
#390267=CARTESIAN_POINT('Ctrl Pts',(-0.398861396107279,2.71652510457761,
7.5043616886572));
#390268=CARTESIAN_POINT('Ctrl Pts',(-0.39093147744885,2.71987530929006,
7.50217374673251));
#390269=CARTESIAN_POINT('',(-0.389948473491309,2.71851378208007,7.50366116523517));
#390270=CARTESIAN_POINT('Ctrl Pts',(-0.397282670454307,2.71434454205174,
7.51860402984325));
#390271=CARTESIAN_POINT('Ctrl Pts',(-0.397541647224221,2.71470224513871,
7.51734760759493));
#390272=CARTESIAN_POINT('Ctrl Pts',(-0.397727477622806,2.71506037210354,
7.51608817408572));
#390273=CARTESIAN_POINT('Ctrl Pts',(-0.397827881300144,2.71542424967146,
7.51481005913118));
#390274=CARTESIAN_POINT('Ctrl Pts',(-0.3979188293503,2.71575385866761,7.51365231206383));
#390275=CARTESIAN_POINT('Ctrl Pts',(-0.397940052684864,2.71608858420058,
7.51247773061042));
#390276=CARTESIAN_POINT('Ctrl Pts',(-0.397854333026815,2.716424970865,7.51129758471022));
#390277=CARTESIAN_POINT('Ctrl Pts',(-0.397747793281414,2.71684306107206,
7.50983079813402));
#390278=CARTESIAN_POINT('Ctrl Pts',(-0.397466830635151,2.71724715791932,
7.50839324291155));
#390279=CARTESIAN_POINT('Ctrl Pts',(-0.396941707788383,2.71759314905582,
7.50715379678855));
#390280=CARTESIAN_POINT('Ctrl Pts',(-0.396699116164227,2.71775298699138,
7.50658120839351));
#390281=CARTESIAN_POINT('Ctrl Pts',(-0.396364702174659,2.71791521224514,
7.50598221009429));
#390282=CARTESIAN_POINT('Ctrl Pts',(-0.395936496490176,2.71805549851716,
7.50545747549611));
#390283=CARTESIAN_POINT('Ctrl Pts',(-0.395707992682731,2.71813035961418,
7.50517746087247));
#390284=CARTESIAN_POINT('Ctrl Pts',(-0.395450365812596,2.71819997752053,
7.50491486231392));
#390285=CARTESIAN_POINT('Ctrl Pts',(-0.395170003136817,2.71826089837762,
7.50468370960993));
#390286=CARTESIAN_POINT('Ctrl Pts',(-0.394750772501136,2.71835199427538,
7.50433806340447));
#390287=CARTESIAN_POINT('Ctrl Pts',(-0.394268015985526,2.71842583148374,
7.50405484070984));
#390288=CARTESIAN_POINT('Ctrl Pts',(-0.39375413803124,2.71847672904423,
7.50385766036131));
#390289=CARTESIAN_POINT('Ctrl Pts',(-0.393699186771502,2.71848217174719,
7.50383657498791));
#390290=CARTESIAN_POINT('Ctrl Pts',(-0.393643905362433,2.71848736408184,
7.50381643264937));
#390291=CARTESIAN_POINT('Ctrl Pts',(-0.393588351980706,2.71849230807154,
7.50379723213559));
#390292=CARTESIAN_POINT('Ctrl Pts',(-0.393217514984894,2.71852531082003,
7.50366906242519));
#390293=CARTESIAN_POINT('Ctrl Pts',(-0.392826428584446,2.71854724898583,
7.50358235568538));
#390294=CARTESIAN_POINT('Ctrl Pts',(-0.392448961127778,2.71855933335556,
7.5035341175365));
#390295=CARTESIAN_POINT('Ctrl Pts',(-0.391882991397572,2.71857745250029,
7.50346178989176));
#390296=CARTESIAN_POINT('Ctrl Pts',(-0.391273366354832,2.71857288019814,
7.50346967198527));
#390297=CARTESIAN_POINT('Ctrl Pts',(-0.390675041552688,2.71854997689286,
7.50354272648692));
#390298=CARTESIAN_POINT('Ctrl Pts',(-0.390428938176975,2.71854055628932,
7.50357277531559));
#390299=CARTESIAN_POINT('Ctrl Pts',(-0.390185068196088,2.71852818857031,
7.50361331098761));
#390300=CARTESIAN_POINT('Ctrl Pts',(-0.389948473491511,2.71851378208147,
7.50366116523658));
#390301=CARTESIAN_POINT('',(-0.341939261259086,2.65201338678246,7.57603338622103));
#390302=CARTESIAN_POINT('Origin',(-0.343066474116784,2.6607781389627,7.58486873427628));
#390303=CARTESIAN_POINT('Ctrl Pts',(-0.389948473529075,2.71851378212322,
7.50366116529969));
#390304=CARTESIAN_POINT('Ctrl Pts',(-0.373970838805478,2.69638364458546,
7.52783573079709));
#390305=CARTESIAN_POINT('Ctrl Pts',(-0.357968509118427,2.67421790325149,
7.55196141284068));
#390306=CARTESIAN_POINT('Ctrl Pts',(-0.341939262248846,2.65201338754928,
7.57603338728831));
#390307=CARTESIAN_POINT('Ctrl Pts',(-0.347594250863845,2.64601386279727,
7.59639677331372));
#390308=CARTESIAN_POINT('Ctrl Pts',(-0.339350823778407,2.62970074459056,
7.5995988229546));
#390309=CARTESIAN_POINT('Ctrl Pts',(-0.334988019337677,2.64746798269907,
7.59642833564546));
#390310=CARTESIAN_POINT('Ctrl Pts',(-0.346417486467329,2.64229494768144,
7.58707626057423));
#390311=CARTESIAN_POINT('Ctrl Pts',(-0.34038578786662,2.63920773161741,
7.58809943920598));
#390312=CARTESIAN_POINT('Ctrl Pts',(-0.335273897319224,2.64363299723925,
7.58710240504252));
#390313=CARTESIAN_POINT('Ctrl Pts',(-0.343548093433324,2.6476514592214,
7.5801537675693));
#390314=CARTESIAN_POINT('Ctrl Pts',(-0.341200555278549,2.64603333190639,
7.5820588065976));
#390315=CARTESIAN_POINT('Ctrl Pts',(-0.339331722030058,2.64813916602316,
7.58020924244129));
#390316=CARTESIAN_POINT('Ctrl Pts',(-0.34193926115346,2.65201338596165,
7.57603338509286));
#390317=CARTESIAN_POINT('Ctrl Pts',(-0.34193926115346,2.65201338596165,
7.57603338509286));
#390318=CARTESIAN_POINT('Ctrl Pts',(-0.34193926115346,2.65201338596165,
7.57603338509286));
#390319=CARTESIAN_POINT('Origin',(-0.343072133619813,2.66077740925,7.58486873427622));
#390320=CARTESIAN_POINT('Ctrl Pts',(-0.30110264748335,2.73436754560449,
7.51098857897448));
#390321=CARTESIAN_POINT('Ctrl Pts',(-0.303232664881353,2.72887905420375,
7.50433767179956));
#390322=CARTESIAN_POINT('Ctrl Pts',(-0.311753059719538,2.73010825023526,
7.50214974420965));
#390323=CARTESIAN_POINT('Ctrl Pts',(-0.312499739379753,2.70500025455533,
7.53887321589167));
#390324=CARTESIAN_POINT('Ctrl Pts',(-0.314604235389233,2.69957752502185,
7.53220407452058));
#390325=CARTESIAN_POINT('Ctrl Pts',(-0.323103465221934,2.70074629025613,
7.53003438070911));
#390326=CARTESIAN_POINT('Ctrl Pts',(-0.3239187178968,2.67557656747423,7.56669465659233));
#390327=CARTESIAN_POINT('Ctrl Pts',(-0.326010776726107,2.67018588526414,
7.56004085833299));
#390328=CARTESIAN_POINT('Ctrl Pts',(-0.334474294446307,2.67132847789769,
7.55785582193789));
#390329=CARTESIAN_POINT('Ctrl Pts',(-0.335359066599817,2.64609781507675,
7.59443891967696));
#390330=CARTESIAN_POINT('Ctrl Pts',(-0.337454158653971,2.64069931704862,
7.58783901202978));
#390331=CARTESIAN_POINT('Ctrl Pts',(-0.345864908691495,2.64185623614459,
7.58560008491213));
#390332=CARTESIAN_POINT('',(-0.312368326987727,2.72851663429644,7.50366116523517));
#390333=CARTESIAN_POINT('Ctrl Pts',(-0.31236832698777,2.72851663429681,
7.50366116523554));
#390334=CARTESIAN_POINT('Ctrl Pts',(-0.311648372775235,2.7287528618325,
7.50350835821027));
#390335=CARTESIAN_POINT('Ctrl Pts',(-0.310978874698737,2.72894658931302,
7.50345484956));
#390336=CARTESIAN_POINT('Ctrl Pts',(-0.31034009495131,2.72910415325133,
7.50349758195598));
#390337=CARTESIAN_POINT('Ctrl Pts',(-0.310012353567739,2.72918499523694,
7.50351950684424));
#390338=CARTESIAN_POINT('Ctrl Pts',(-0.309660426124605,2.72926441113657,
7.50357029184312));
#390339=CARTESIAN_POINT('Ctrl Pts',(-0.309318961508532,2.72933166265592,
7.50365515313923));
#390340=CARTESIAN_POINT('Ctrl Pts',(-0.308793650656337,2.72943512272552,
7.50378570417639));
#390341=CARTESIAN_POINT('Ctrl Pts',(-0.308277749172659,2.72951317103045,
7.5040000162191));
#390342=CARTESIAN_POINT('Ctrl Pts',(-0.307810185036314,2.72955762209029,
7.50428903009634));
#390343=CARTESIAN_POINT('Ctrl Pts',(-0.307758289014399,2.72956255581594,
7.50432110841317));
#390344=CARTESIAN_POINT('Ctrl Pts',(-0.307706965257206,2.72956709514048,
7.50435406373354));
#390345=CARTESIAN_POINT('Ctrl Pts',(-0.307656249660458,2.72957124302654,
7.50438785222352));
#390346=CARTESIAN_POINT('Ctrl Pts',(-0.307346606565319,2.7295965678646,
7.50459414719561));
#390347=CARTESIAN_POINT('Ctrl Pts',(-0.30705466192801,2.72960719025544,
7.50483629897752));
#390348=CARTESIAN_POINT('Ctrl Pts',(-0.306791647913675,2.72960401841961,
7.5050991045531));
#390349=CARTESIAN_POINT('Ctrl Pts',(-0.306211412580796,2.72959702103118,
7.50567888004914));
#390350=CARTESIAN_POINT('Ctrl Pts',(-0.305749108231741,2.72952313331425,
7.50637912803144));
#390351=CARTESIAN_POINT('Ctrl Pts',(-0.305392057397979,2.72941054569536,
7.50710440483569));
#390352=CARTESIAN_POINT('Ctrl Pts',(-0.305304501445088,2.72938293697603,
7.50728225710685));
#390353=CARTESIAN_POINT('Ctrl Pts',(-0.305221487814413,2.72935259071141,
7.50746498566955));
#390354=CARTESIAN_POINT('Ctrl Pts',(-0.305144811281192,2.72932060655108,
7.50764697238949));
#390355=CARTESIAN_POINT('Ctrl Pts',(-0.304732619340553,2.72914866850742,
7.50862528291182));
#390356=CARTESIAN_POINT('Ctrl Pts',(-0.304464548239082,2.72891760973834,
7.50965856837421));
#390357=CARTESIAN_POINT('Ctrl Pts',(-0.304285411258898,2.72866417016778,
7.51067959873201));
#390358=CARTESIAN_POINT('Ctrl Pts',(-0.304186831952749,2.72852470205243,
7.51124147302578));
#390359=CARTESIAN_POINT('Ctrl Pts',(-0.304115515380097,2.728378171551,7.51180065547253));
#390360=CARTESIAN_POINT('Ctrl Pts',(-0.304064538402986,2.72822921565349,
7.51235175716501));
#390361=CARTESIAN_POINT('Ctrl Pts',(-0.303888392640254,2.72771451369063,
7.51425603304536));
#390362=CARTESIAN_POINT('Ctrl Pts',(-0.303939832870249,2.72710752083202,
7.51626900505181));
#390363=CARTESIAN_POINT('Ctrl Pts',(-0.304176391156343,2.72645112229369,
7.51827788969244));
#390364=CARTESIAN_POINT('Ctrl Pts',(-0.304189194137819,2.72641559676438,
7.51838661432546));
#390365=CARTESIAN_POINT('Ctrl Pts',(-0.304202548093819,2.7263799217195,
7.51849533314857));
#390366=CARTESIAN_POINT('Ctrl Pts',(-0.304216449096295,2.72634410251322,
7.51860402984325));
#390367=CARTESIAN_POINT('Ctrl Pts',(-0.341939260496117,2.65201338777647,
7.57603338728985));
#390368=CARTESIAN_POINT('Ctrl Pts',(-0.332066529529967,2.67755759370233,
7.55196141284922));
#390369=CARTESIAN_POINT('Ctrl Pts',(-0.322210000114179,2.70305746572958,
7.52783573083105));
#390370=CARTESIAN_POINT('Ctrl Pts',(-0.31236832696141,2.72851663434944,
7.50366116530176));
#390371=CARTESIAN_POINT('Origin',(-1.18155821115204E-16,9.16393216063563E-16,
7.49482233047033));
#390372=CARTESIAN_POINT('Origin',(-0.388693460788449,2.70976449964574,7.49482233047033));
#390373=CARTESIAN_POINT('Origin',(0.,0.,7.50366116523517));
#390374=CARTESIAN_POINT('Origin',(-0.311362998732866,2.71973515861749,7.49482233047033));
#390375=CARTESIAN_POINT('Ctrl Pts',(-0.397282050205177,2.71434368527686,
7.51860402984325));
#390376=CARTESIAN_POINT('Ctrl Pts',(-0.401743698216853,2.72050728674435,
7.51860402984325));
#390377=CARTESIAN_POINT('Ctrl Pts',(-0.409267922647769,2.71937488542709,
7.51860402984325));
#390378=CARTESIAN_POINT('Ctrl Pts',(-0.398938691589132,2.71663227181923,
7.51041458714367));
#390379=CARTESIAN_POINT('Ctrl Pts',(-0.403526271692389,2.72023899811274,
7.51004642900444));
#390380=CARTESIAN_POINT('Ctrl Pts',(-0.409269997739523,2.71937457312425,
7.50729136483011));
#390381=CARTESIAN_POINT('Ctrl Pts',(-0.397367849688397,2.71896812132684,
7.50215815450137));
#390382=CARTESIAN_POINT('Ctrl Pts',(-0.399896795118419,2.72078539937201,
7.49877163671528));
#390383=CARTESIAN_POINT('Ctrl Pts',(-0.403312047312352,2.72029552587179,
7.49481588533169));
#390384=CARTESIAN_POINT('Ctrl Pts',(-0.389948395323623,2.71851323713979,
7.50366171572174));
#390385=CARTESIAN_POINT('Ctrl Pts',(-0.390468316773402,2.72213785352545,
7.50000045605858));
#390386=CARTESIAN_POINT('Ctrl Pts',(-0.390468316773525,2.72213785352544,
7.49482233047317));
#390387=CARTESIAN_POINT('Origin',(-0.407407613908461,2.70701409049333,7.51860402984325));
#390388=CARTESIAN_POINT('Origin',(-0.407407613908461,2.70701409049333,9.));
#390389=CARTESIAN_POINT('Origin',(-0.40740761390846,2.70701409049333,8.75721825406948));
#390390=CARTESIAN_POINT('Ctrl Pts',(-0.387489117162865,2.70081746938362,
8.78942910404913));
#390391=CARTESIAN_POINT('Ctrl Pts',(-0.390740624933972,2.70534296669508,
8.7967269950169));
#390392=CARTESIAN_POINT('Ctrl Pts',(-0.39882274373864,2.70155445226207,
8.79893251111267));
#390393=CARTESIAN_POINT('Ctrl Pts',(-0.393936589149031,2.70972283426824,
8.78111911759585));
#390394=CARTESIAN_POINT('Ctrl Pts',(-0.397797334553896,2.7150835203292,
8.78644465894814));
#390395=CARTESIAN_POINT('Ctrl Pts',(-0.405704558887993,2.7132970950983,
8.78817647674132));
#390396=CARTESIAN_POINT('Ctrl Pts',(-0.39795480750331,2.71527287005867,
8.76780923932029));
#390397=CARTESIAN_POINT('Ctrl Pts',(-0.402516389461986,2.72159795557625,
8.76988516158373));
#390398=CARTESIAN_POINT('Ctrl Pts',(-0.410012461604652,2.72062569901123,
8.77093053738832));
#390399=CARTESIAN_POINT('Ctrl Pts',(-0.39717130991881,2.71419068903609,
8.75371302330492));
#390400=CARTESIAN_POINT('Ctrl Pts',(-0.401620318062246,2.72036098302482,
8.75300828287559));
#390401=CARTESIAN_POINT('Ctrl Pts',(-0.409172640064091,2.71919609173606,
8.75267964240738));
#390402=CARTESIAN_POINT('Origin',(-0.399184265771846,2.69565586321038,8.78727029226991));
#390403=CARTESIAN_POINT('Ctrl Pts',(-0.347133565397089,2.64507775146798,
8.85049129520029));
#390404=CARTESIAN_POINT('Ctrl Pts',(-0.350558127032893,2.649807813817,8.85711686593485));
#390405=CARTESIAN_POINT('Ctrl Pts',(-0.358444815903127,2.64650616259708,
8.85933012996512));
#390406=CARTESIAN_POINT('Ctrl Pts',(-0.361129150869188,2.66440869041269,
8.82945683644724));
#390407=CARTESIAN_POINT('Ctrl Pts',(-0.364582138437099,2.66917801513907,
8.83607469902392));
#390408=CARTESIAN_POINT('Ctrl Pts',(-0.372477500384183,2.66583207697137,
8.8382956714852));
#390409=CARTESIAN_POINT('Ctrl Pts',(-0.375103874792535,2.68371081503405,
8.80838214965002));
#390410=CARTESIAN_POINT('Ctrl Pts',(-0.378570489461573,2.68849896174259,
8.81501364461993));
#390411=CARTESIAN_POINT('Ctrl Pts',(-0.386488357039706,2.68512906773677,
8.81722098428721));
#390412=CARTESIAN_POINT('Ctrl Pts',(-0.389059322317692,2.70298631476879,
8.78727029226991));
#390413=CARTESIAN_POINT('Ctrl Pts',(-0.392526512802801,2.70777525680419,
8.79393457792714));
#390414=CARTESIAN_POINT('Ctrl Pts',(-0.400479038758349,2.70439935009568,
8.79610912703474));
#390415=CARTESIAN_POINT('Origin',(-0.357258508851243,2.63774729990957,8.85049129520029));
#390416=CARTESIAN_POINT('Ctrl Pts',(-0.33515558185988,2.64662214142562,
8.85049129520029));
#390417=CARTESIAN_POINT('Ctrl Pts',(-0.333042822978414,2.65206616219449,
8.85711686593484));
#390418=CARTESIAN_POINT('Ctrl Pts',(-0.324576590381445,2.65087298671372,
8.85933012996512));
#390419=CARTESIAN_POINT('Ctrl Pts',(-0.337024709144314,2.64180589483668,
8.86332496987231));
#390420=CARTESIAN_POINT('Ctrl Pts',(-0.332486490925511,2.64267564754589,
8.86648636486737));
#390421=CARTESIAN_POINT('Ctrl Pts',(-0.32982152219722,2.6374055390489,8.87206031107457));
#390422=CARTESIAN_POINT('Ctrl Pts',(-0.344083317655468,2.64086469778923,
8.86341338519876));
#390423=CARTESIAN_POINT('Ctrl Pts',(-0.348704757116131,2.64052445089996,
8.86654584966059));
#390424=CARTESIAN_POINT('Ctrl Pts',(-0.349892026593743,2.63471802825129,
8.87215952290714));
#390425=CARTESIAN_POINT('Ctrl Pts',(-0.347133565397089,2.64507775146798,
8.85049129520029));
#390426=CARTESIAN_POINT('Ctrl Pts',(-0.350558127032894,2.649807813817,8.85711686593484));
#390427=CARTESIAN_POINT('Ctrl Pts',(-0.358444815903127,2.64650616259708,
8.85933012996512));
#390428=CARTESIAN_POINT('Origin',(-0.323502373428199,2.64209967160839,8.85049129520029));
#390429=CARTESIAN_POINT('Ctrl Pts',(-0.309289785090423,2.71327145765926,
8.78727029226991));
#390430=CARTESIAN_POINT('Ctrl Pts',(-0.307150726644354,2.71878324544933,
8.79393457792714));
#390431=CARTESIAN_POINT('Ctrl Pts',(-0.298601974927904,2.71753494289437,
8.79610912703474));
#390432=CARTESIAN_POINT('Ctrl Pts',(-0.317899498928061,2.69108650254806,
8.80838214965001));
#390433=CARTESIAN_POINT('Ctrl Pts',(-0.315760795727614,2.69659737496409,
8.81501364461985));
#390434=CARTESIAN_POINT('Ctrl Pts',(-0.307247094031194,2.69534609720933,
8.81722098428721));
#390435=CARTESIAN_POINT('Ctrl Pts',(-0.326521105202102,2.66887090377404,
8.82945683644721));
#390436=CARTESIAN_POINT('Ctrl Pts',(-0.324390809144525,2.67436011320682,
8.83607469902389));
#390437=CARTESIAN_POINT('Ctrl Pts',(-0.315904953537554,2.67312629915468,
8.8382956714852));
#390438=CARTESIAN_POINT('Ctrl Pts',(-0.33515558185988,2.64662214142562,
8.85049129520029));
#390439=CARTESIAN_POINT('Ctrl Pts',(-0.333042822978414,2.65206616219449,
8.85711686593484));
#390440=CARTESIAN_POINT('Ctrl Pts',(-0.324576590381445,2.65087298671372,
8.85933012996512));
#390441=CARTESIAN_POINT('Origin',(-0.297636576658742,2.70874898784202,8.78727029226991));
#390442=CARTESIAN_POINT('Ctrl Pts',(-0.304283422748602,2.72617147813989,
8.75374538247847));
#390443=CARTESIAN_POINT('Ctrl Pts',(-0.301546370683836,2.73326040784629,
8.75304829418601));
#390444=CARTESIAN_POINT('Ctrl Pts',(-0.293954221614899,2.73405408014902,
8.75272238421917));
#390445=CARTESIAN_POINT('Ctrl Pts',(-0.303805856238297,2.72740204188969,
8.76769408445023));
#390446=CARTESIAN_POINT('Ctrl Pts',(-0.300999284012138,2.73466911195344,
8.76974318093973));
#390447=CARTESIAN_POINT('Ctrl Pts',(-0.293509920856647,2.73563233404903,
8.7707786988043));
#390448=CARTESIAN_POINT('Ctrl Pts',(-0.306253590132211,2.72109487311948,
8.78108014887986));
#390449=CARTESIAN_POINT('Ctrl Pts',(-0.30387866553322,2.72725482201938,
8.78639403366321));
#390450=CARTESIAN_POINT('Ctrl Pts',(-0.295789548083303,2.72755189879462,
8.78812224174741));
#390451=CARTESIAN_POINT('Ctrl Pts',(-0.310264885608762,2.71075881581417,
8.78944554828686));
#390452=CARTESIAN_POINT('Ctrl Pts',(-0.308268610199807,2.71595220604683,
8.79673892988687));
#390453=CARTESIAN_POINT('Ctrl Pts',(-0.299498741631327,2.71434193910989,
8.79894799272499));
#390454=CARTESIAN_POINT('Origin',(-0.292563240664618,2.72182163269598,8.75721825406948));
#390455=CARTESIAN_POINT('Origin',(-0.292563240664618,2.72182163269598,9.));
#390456=CARTESIAN_POINT('Origin',(-0.292563240664619,2.72182163269598,7.51860402984325));
#390457=CARTESIAN_POINT('Ctrl Pts',(-0.312368237512607,2.72851585273769,
7.50366195182966));
#390458=CARTESIAN_POINT('Ctrl Pts',(-0.312784747585389,2.73215404062032,
7.50000065167735));
#390459=CARTESIAN_POINT('Ctrl Pts',(-0.312784747585273,2.73215404062034,
7.49482233047108));
#390460=CARTESIAN_POINT('Ctrl Pts',(-0.305300246324094,2.73083906176095,
7.50215800491336));
#390461=CARTESIAN_POINT('Ctrl Pts',(-0.303313249275625,2.73323834079927,
7.49877273257266));
#390462=CARTESIAN_POINT('Ctrl Pts',(-0.299883530860003,2.73363100852074,
7.49481816995649));
#390463=CARTESIAN_POINT('Ctrl Pts',(-0.303197007877448,2.72897187018571,
7.51043025814043));
#390464=CARTESIAN_POINT('Ctrl Pts',(-0.299675308765067,2.73362916471674,
7.51006209594515));
#390465=CARTESIAN_POINT('Ctrl Pts',(-0.293896628507968,2.73425031256432,
7.507312818217));
#390466=CARTESIAN_POINT('Ctrl Pts',(-0.304216995834675,2.72634269346048,
7.51860402984326));
#390467=CARTESIAN_POINT('Ctrl Pts',(-0.301464837418634,2.7334368207108,
7.51860402984327));
#390468=CARTESIAN_POINT('Ctrl Pts',(-0.293899145873127,2.7342500419777,
7.51860402984327));
#390469=CARTESIAN_POINT('Origin',(0.,0.,7.5));
#390470=CARTESIAN_POINT('Origin',(-0.504036631578591,2.6197108805292,7.5));
#390471=CARTESIAN_POINT('',(-0.504036631578591,2.6197108805292,7.59394543036555));
#390472=CARTESIAN_POINT('',(-0.504036631578591,2.6197108805292,8.85049129520029));
#390473=CARTESIAN_POINT('',(-0.504036631578591,2.6197108805292,7.5));
#390474=CARTESIAN_POINT('',(-0.482494215215348,2.68788048588352,8.78727029226991));
#390475=CARTESIAN_POINT('Ctrl Pts',(-0.504036631578591,2.6197108805292,
8.85049129520029));
#390476=CARTESIAN_POINT('Ctrl Pts',(-0.496845388128025,2.64246711268839,
8.82945686509571));
#390477=CARTESIAN_POINT('Ctrl Pts',(-0.489664835330401,2.66518951495683,
8.80838212259896));
#390478=CARTESIAN_POINT('Ctrl Pts',(-0.482494215215348,2.68788048588352,
8.78727029226991));
#390479=CARTESIAN_POINT('',(-0.478268870165661,2.70125132133977,8.75721825406948));
#390480=CARTESIAN_POINT('Origin',(-0.490984591625891,2.6610138998837,8.75937679713081));
#390481=CARTESIAN_POINT('',(-0.478268870165661,2.70125132133977,7.51860402984325));
#390482=CARTESIAN_POINT('',(-0.478268870165661,2.70125132133977,7.5));
#390483=CARTESIAN_POINT('Ctrl Pts',(-0.478268870165661,2.70125132133977,
7.51860402984325));
#390484=CARTESIAN_POINT('Ctrl Pts',(-0.481587221536733,2.69075060964715,
7.52834476460825));
#390485=CARTESIAN_POINT('Ctrl Pts',(-0.484907727133636,2.68024308104402,
7.53807742314407));
#390486=CARTESIAN_POINT('Ctrl Pts',(-0.488230459287361,2.66972850664355,
7.54780169004674));
#390487=CARTESIAN_POINT('Ctrl Pts',(-0.493493487440511,2.65307398905746,
7.5632044032688));
#390488=CARTESIAN_POINT('Ctrl Pts',(-0.498762108429668,2.63640177329775,
7.57858609112103));
#390489=CARTESIAN_POINT('Ctrl Pts',(-0.504036631578591,2.6197108805292,
7.59394543036555));
#390490=CARTESIAN_POINT('Origin',(-0.691101205365338,2.82936072626276,7.5));
#390491=CARTESIAN_POINT('',(-0.570375062512128,2.68331364198702,8.75721825406948));
#390492=CARTESIAN_POINT('',(-0.561440886005602,2.67250562312429,8.78727029226991));
#390493=CARTESIAN_POINT('Origin',(-0.538762613750377,2.64507084006066,8.75658640621043));
#390494=CARTESIAN_POINT('',(-0.515891055659666,2.61740223164621,8.85049129520029));
#390495=CARTESIAN_POINT('Ctrl Pts',(-0.561440886005602,2.67250562312429,
8.78727029226991));
#390496=CARTESIAN_POINT('Ctrl Pts',(-0.546279145362939,2.6541638790656,
8.80838212259896));
#390497=CARTESIAN_POINT('Ctrl Pts',(-0.531096402804868,2.63579672817756,
8.82945686509571));
#390498=CARTESIAN_POINT('Ctrl Pts',(-0.515891055659666,2.61740223164621,
8.85049129520029));
#390499=CARTESIAN_POINT('',(-0.515891055659666,2.61740223164621,7.59394543036555));
#390500=CARTESIAN_POINT('',(-0.515891055659666,2.61740223164621,7.5));
#390501=CARTESIAN_POINT('',(-0.570375062512128,2.68331364198702,7.51860402984325));
#390502=CARTESIAN_POINT('Ctrl Pts',(-0.515891055659666,2.61740223164621,
7.59394543036555));
#390503=CARTESIAN_POINT('Ctrl Pts',(-0.527043640891426,2.63089394534417,
7.57858609112103));
#390504=CARTESIAN_POINT('Ctrl Pts',(-0.538183746447094,2.64437056189533,
7.56320440326857));
#390505=CARTESIAN_POINT('Ctrl Pts',(-0.549312026368875,2.65783287251976,
7.54780169004651));
#390506=CARTESIAN_POINT('Ctrl Pts',(-0.556337695325183,2.66633209598458,
7.53807742314383));
#390507=CARTESIAN_POINT('Ctrl Pts',(-0.563358656393526,2.67482562413523,
7.52834476460825));
#390508=CARTESIAN_POINT('Ctrl Pts',(-0.570375062512127,2.68331364198702,
7.51860402984325));
#390509=CARTESIAN_POINT('',(-0.570375062512128,2.68331364198702,7.5));
#390510=CARTESIAN_POINT('Origin',(-0.510592093294252,2.62178248538885,7.5));
#390511=CARTESIAN_POINT('Ctrl Pts',(-0.515891055659666,2.61740223164621,
8.85049129520029));
#390512=CARTESIAN_POINT('Ctrl Pts',(-0.515767668527143,2.61725296545981,
8.85097269580138));
#390513=CARTESIAN_POINT('Ctrl Pts',(-0.515639354986829,2.61711094168747,
8.85143669361005));
#390514=CARTESIAN_POINT('Ctrl Pts',(-0.515499557882527,2.61697020670063,
8.8519052845931));
#390515=CARTESIAN_POINT('Ctrl Pts',(-0.515226123612123,2.61669493799147,
8.85282181883899));
#390516=CARTESIAN_POINT('Ctrl Pts',(-0.514915651119187,2.61643181964957,
8.85372622499635));
#390517=CARTESIAN_POINT('Ctrl Pts',(-0.514553299874838,2.61618848567121,
8.8546225773507));
#390518=CARTESIAN_POINT('Ctrl Pts',(-0.514252488741278,2.61598647844478,
8.85536669723986));
#390519=CARTESIAN_POINT('Ctrl Pts',(-0.513915873198243,2.61579803376955,
8.85610498449051));
#390520=CARTESIAN_POINT('Ctrl Pts',(-0.513531024767989,2.61563448612492,
8.85681338218371));
#390521=CARTESIAN_POINT('Ctrl Pts',(-0.513181774213118,2.61548606638055,
8.85745625420284));
#390522=CARTESIAN_POINT('Ctrl Pts',(-0.512788654114669,2.61535573822306,
8.85808743050666));
#390523=CARTESIAN_POINT('Ctrl Pts',(-0.512331828562521,2.61526410220628,
8.8586680450841));
#390524=CARTESIAN_POINT('Ctrl Pts',(-0.512121059155524,2.61522182333457,
8.85893592806395));
#390525=CARTESIAN_POINT('Ctrl Pts',(-0.511896582696646,2.61518797425763,
8.85919241173848));
#390526=CARTESIAN_POINT('Ctrl Pts',(-0.511655676326038,2.61516597374877,
8.85943017985534));
#390527=CARTESIAN_POINT('Ctrl Pts',(-0.511330381409799,2.61513626654896,
8.8597512372));
#390528=CARTESIAN_POINT('Ctrl Pts',(-0.510966791987485,2.61512804460748,
8.86004599534705));
#390529=CARTESIAN_POINT('Ctrl Pts',(-0.510569040990299,2.61515181913895,
8.86026130871721));
#390530=CARTESIAN_POINT('Ctrl Pts',(-0.510423413136441,2.61516052366519,
8.86034014101235));
#390531=CARTESIAN_POINT('Ctrl Pts',(-0.510271017703912,2.61517363576241,
8.86040910639692));
#390532=CARTESIAN_POINT('Ctrl Pts',(-0.510116035456201,2.61519113333938,
8.86046313645506));
#390533=CARTESIAN_POINT('Ctrl Pts',(-0.509874186956613,2.61521843816169,
8.86054744990829));
#390534=CARTESIAN_POINT('Ctrl Pts',(-0.509619453975295,2.61525731366695,
8.86059655985668));
#390535=CARTESIAN_POINT('Ctrl Pts',(-0.509368129116534,2.61530497704636,
8.86059725258816));
#390536=CARTESIAN_POINT('Ctrl Pts',(-0.509116223596944,2.61535275054721,
8.86059794692011));
#390537=CARTESIAN_POINT('Ctrl Pts',(-0.508865443335376,2.61541249263374,
8.86056369958366));
#390538=CARTESIAN_POINT('Ctrl Pts',(-0.508628593949195,2.61547728428475,
8.86048590497774));
#390539=CARTESIAN_POINT('Ctrl Pts',(-0.508566783311257,2.61549419297658,
8.86046560290182));
#390540=CARTESIAN_POINT('Ctrl Pts',(-0.508505141221149,2.61551175291262,
8.86044257503091));
#390541=CARTESIAN_POINT('Ctrl Pts',(-0.50844556347711,2.61552938990613,
8.86041778462584));
#390542=CARTESIAN_POINT('Ctrl Pts',(-0.50804467918954,2.61564806498672,
8.86025097596201));
#390543=CARTESIAN_POINT('Ctrl Pts',(-0.507683561495978,2.61578647179151,
8.8599848982295));
#390544=CARTESIAN_POINT('Ctrl Pts',(-0.507369718277689,2.61593265927751,
8.85968173251461));
#390545=CARTESIAN_POINT('Ctrl Pts',(-0.507203713196287,2.61600998408207,
8.85952137522076));
#390546=CARTESIAN_POINT('Ctrl Pts',(-0.507047654086865,2.61609080315807,
8.85934740853961));
#390547=CARTESIAN_POINT('Ctrl Pts',(-0.506903026841176,2.61617259635409,
8.8591675900182));
#390548=CARTESIAN_POINT('Ctrl Pts',(-0.506322273273992,2.61650103855137,
8.85844552518696));
#390549=CARTESIAN_POINT('Ctrl Pts',(-0.505891539218353,2.61686111677502,
8.85759444184127));
#390550=CARTESIAN_POINT('Ctrl Pts',(-0.505566712158157,2.61718625003458,
8.85683498915142));
#390551=CARTESIAN_POINT('Ctrl Pts',(-0.505532719871388,2.6172202743643,
8.85675551445));
#390552=CARTESIAN_POINT('Ctrl Pts',(-0.505499903995347,2.61725392708393,
8.85667699793652));
#390553=CARTESIAN_POINT('Ctrl Pts',(-0.505468225267547,2.61728713860215,
8.85659965593547));
#390554=CARTESIAN_POINT('Ctrl Pts',(-0.50504062418328,2.61773542936974,
8.85555568965886));
#390555=CARTESIAN_POINT('Ctrl Pts',(-0.504694415106446,2.61822801862891,
8.85434650606346));
#390556=CARTESIAN_POINT('Ctrl Pts',(-0.50442280204503,2.61876376787636,
8.85297329937117));
#390557=CARTESIAN_POINT('Ctrl Pts',(-0.50427003624761,2.61906509418437,
8.85220095427747));
#390558=CARTESIAN_POINT('Ctrl Pts',(-0.50414108661597,2.61938033921224,
8.85137579139183));
#390559=CARTESIAN_POINT('Ctrl Pts',(-0.504036631578591,2.6197108805292,
8.85049129520029));
#390560=CARTESIAN_POINT('Origin',(-0.510592093294252,2.62178248538885,7.59394543036555));
#390561=CARTESIAN_POINT('Ctrl Pts',(-0.515532821189696,2.61696886155263,
7.59443877723642));
#390562=CARTESIAN_POINT('Ctrl Pts',(-0.511843350832965,2.61250556656624,
7.58783886950016));
#390563=CARTESIAN_POINT('Ctrl Pts',(-0.504225634743617,2.61625384391974,
7.58559994247159));
#390564=CARTESIAN_POINT('Ctrl Pts',(-0.535673531622635,2.6413338579358,
7.56670252222136));
#390565=CARTESIAN_POINT('Ctrl Pts',(-0.531989393598023,2.63687701367783,
7.56004874999029));
#390566=CARTESIAN_POINT('Ctrl Pts',(-0.524317107068314,2.64062833033498,
7.55786368756704));
#390567=CARTESIAN_POINT('Ctrl Pts',(-0.555776631291146,2.66565335512259,
7.53888913333559));
#390568=CARTESIAN_POINT('Ctrl Pts',(-0.552070598253881,2.66117002362097,
7.53222002137278));
#390569=CARTESIAN_POINT('Ctrl Pts',(-0.544372672437959,2.66495742152094,
7.53005029815327));
#390570=CARTESIAN_POINT('Ctrl Pts',(-0.575841210516351,2.68992625263927,
7.51101258149734));
#390571=CARTESIAN_POINT('Ctrl Pts',(-0.572090253624643,2.68538857501344,
7.5043616886572));
#390572=CARTESIAN_POINT('Ctrl Pts',(-0.564391276187486,2.68923996800388,
7.50217374673251));
#390573=CARTESIAN_POINT('',(-0.563323058569149,2.68794421947736,7.50366116523517));
#390574=CARTESIAN_POINT('Ctrl Pts',(-0.570375062512129,2.68331364198702,
7.51860402984325));
#390575=CARTESIAN_POINT('Ctrl Pts',(-0.570656425301962,2.68365401743601,
7.51734760759493));
#390576=CARTESIAN_POINT('Ctrl Pts',(-0.570864819165481,2.68399950239607,
7.51608817408573));
#390577=CARTESIAN_POINT('Ctrl Pts',(-0.570988330268519,2.6843561994528,
7.5148100591312));
#390578=CARTESIAN_POINT('Ctrl Pts',(-0.571100209577045,2.68467930417034,
7.51365231206383));
#390579=CARTESIAN_POINT('Ctrl Pts',(-0.571142835244524,2.6850119821901,
7.51247773061042));
#390580=CARTESIAN_POINT('Ctrl Pts',(-0.571078844074294,2.68535316978938,
7.51129758471022));
#390581=CARTESIAN_POINT('Ctrl Pts',(-0.570999310357765,2.6857772270102,
7.50983079813401));
#390582=CARTESIAN_POINT('Ctrl Pts',(-0.570744815553289,2.6861984949357,
7.50839324291155));
#390583=CARTESIAN_POINT('Ctrl Pts',(-0.570242939355954,2.6865774199326,
7.50715379678855));
#390584=CARTESIAN_POINT('Ctrl Pts',(-0.570011087014001,2.68675247236271,
7.50658120839351));
#390585=CARTESIAN_POINT('Ctrl Pts',(-0.569687753921535,2.68693579028516,
7.50598221009429));
#390586=CARTESIAN_POINT('Ctrl Pts',(-0.569269416203865,2.6871032235564,
7.50545747549611));
#390587=CARTESIAN_POINT('Ctrl Pts',(-0.569046178248952,2.68719257113247,
7.50517746087247));
#390588=CARTESIAN_POINT('Ctrl Pts',(-0.568793541135426,2.68727855221161,
7.50491486231392));
#390589=CARTESIAN_POINT('Ctrl Pts',(-0.568517657707549,2.68735731079858,
7.50468370960992));
#390590=CARTESIAN_POINT('Ctrl Pts',(-0.568105124960383,2.68747507972909,
7.50433806340447));
#390591=CARTESIAN_POINT('Ctrl Pts',(-0.567628091085996,2.68757969554714,
7.50405484070984));
#390592=CARTESIAN_POINT('Ctrl Pts',(-0.567118529966982,2.68766341280671,
7.50385766036131));
#390593=CARTESIAN_POINT('Ctrl Pts',(-0.567064040325673,2.68767236506636,
7.50383657498791));
#390594=CARTESIAN_POINT('Ctrl Pts',(-0.567009205172207,2.68768108862484,
7.50381643264937));
#390595=CARTESIAN_POINT('Ctrl Pts',(-0.566954082693363,2.68768958177397,
7.50379723213559));
#390596=CARTESIAN_POINT('Ctrl Pts',(-0.566586122115288,2.68774627632267,
7.50366906242519));
#390597=CARTESIAN_POINT('Ctrl Pts',(-0.566197244826902,2.68779322640586,
7.50358235568538));
#390598=CARTESIAN_POINT('Ctrl Pts',(-0.565821327165834,2.68782947036995,
7.5035341175365));
#390599=CARTESIAN_POINT('Ctrl Pts',(-0.565257681178725,2.68788381409206,
7.50346178989176));
#390600=CARTESIAN_POINT('Ctrl Pts',(-0.564649015727611,2.6879183099948,
7.50346967198527));
#390601=CARTESIAN_POINT('Ctrl Pts',(-0.564050452828134,2.6879337885485,
7.50354272648692));
#390602=CARTESIAN_POINT('Ctrl Pts',(-0.563804251518062,2.68794015519803,
7.50357277531559));
#390603=CARTESIAN_POINT('Ctrl Pts',(-0.56356009019173,2.68794343769315,
7.50361331098761));
#390604=CARTESIAN_POINT('Ctrl Pts',(-0.56332305856944,2.68794421947875,
7.50366116523658));
#390605=CARTESIAN_POINT('',(-0.511151791456907,2.62465641716285,7.57603338622103));
#390606=CARTESIAN_POINT('Origin',(-0.512838247935151,2.63333094044407,7.58486873427626));
#390607=CARTESIAN_POINT('Ctrl Pts',(-0.563323058609602,2.68794421951801,
7.50366116529968));
#390608=CARTESIAN_POINT('Ctrl Pts',(-0.545960368869896,2.66688324129278,
7.52783573079709));
#390609=CARTESIAN_POINT('Ctrl Pts',(-0.528570753762134,2.6457883146349,
7.55196141284068));
#390610=CARTESIAN_POINT('Ctrl Pts',(-0.511151792493766,2.62465641786469,
7.57603338728831));
#390611=CARTESIAN_POINT('Ctrl Pts',(-0.516410771457565,2.61830690341526,
7.59639677331371));
#390612=CARTESIAN_POINT('Ctrl Pts',(-0.507139096305122,2.60255546044572,
7.59959882295469));
#390613=CARTESIAN_POINT('Ctrl Pts',(-0.503923606568019,2.6205657196987,
7.59642833564546));
#390614=CARTESIAN_POINT('Ctrl Pts',(-0.514998153140207,2.6146710247631,
7.58707626057421));
#390615=CARTESIAN_POINT('Ctrl Pts',(-0.508781048698786,2.61197660397168,
7.58809943920599));
#390616=CARTESIAN_POINT('Ctrl Pts',(-0.503963188820572,2.61672029736263,
7.58710240504253));
#390617=CARTESIAN_POINT('Ctrl Pts',(-0.51247784845448,2.62020037341849,
7.5801537675693));
#390618=CARTESIAN_POINT('Ctrl Pts',(-0.510031459795522,2.61873597800557,
7.58205880659761));
#390619=CARTESIAN_POINT('Ctrl Pts',(-0.508301387520508,2.62095722201767,
7.58020924244127));
#390620=CARTESIAN_POINT('Ctrl Pts',(-0.511151791298909,2.62465641635051,
7.57603338509286));
#390621=CARTESIAN_POINT('Ctrl Pts',(-0.511151791298909,2.62465641635051,
7.57603338509286));
#390622=CARTESIAN_POINT('Ctrl Pts',(-0.511151791298909,2.62465641635051,
7.57603338509286));
#390623=CARTESIAN_POINT('Origin',(-0.512843849057692,2.63332984962579,7.58486873427619));
#390624=CARTESIAN_POINT('Ctrl Pts',(-0.475675529955941,2.70945778136102,
7.51098857897448));
#390625=CARTESIAN_POINT('Ctrl Pts',(-0.477449522153347,2.70384409597124,
7.50433767179956));
#390626=CARTESIAN_POINT('Ctrl Pts',(-0.486031165786666,2.70452486291607,
7.50214974420965));
#390627=CARTESIAN_POINT('Ctrl Pts',(-0.485167636506951,2.679420614376,7.53887321589167));
#390628=CARTESIAN_POINT('Ctrl Pts',(-0.486920373129571,2.67387419089971,
7.53220407452062));
#390629=CARTESIAN_POINT('Ctrl Pts',(-0.495477023428703,2.67449600725536,
7.53003438070911));
#390630=CARTESIAN_POINT('Ctrl Pts',(-0.494677971404018,2.64932576495017,
7.56669465659235));
#390631=CARTESIAN_POINT('Ctrl Pts',(-0.496420349679053,2.64381211980541,
7.560040858333));
#390632=CARTESIAN_POINT('Ctrl Pts',(-0.504939684355754,2.6444101054177,
7.55785582193789));
#390633=CARTESIAN_POINT('Ctrl Pts',(-0.504206104532792,2.619174594153,7.59443891967696));
#390634=CARTESIAN_POINT('Ctrl Pts',(-0.505951009039396,2.61365295490927,
7.58783901202978));
#390635=CARTESIAN_POINT('Ctrl Pts',(-0.514418602349896,2.61426861838577,
7.58560008491213));
#390636=CARTESIAN_POINT('',(-0.486543193738941,2.70289709681367,7.50366116523517));
#390637=CARTESIAN_POINT('Ctrl Pts',(-0.486543193739007,2.70289709681404,
7.50366116523554));
#390638=CARTESIAN_POINT('Ctrl Pts',(-0.485839853899794,2.7031789666197,
7.50350835821027));
#390639=CARTESIAN_POINT('Ctrl Pts',(-0.48518414354119,2.70341519095537,
7.50345484955999));
#390640=CARTESIAN_POINT('Ctrl Pts',(-0.484556771391452,2.70361335792061,
7.50349758195598));
#390641=CARTESIAN_POINT('Ctrl Pts',(-0.484234882951505,2.70371503227022,
7.50351950684424));
#390642=CARTESIAN_POINT('Ctrl Pts',(-0.483888766775207,2.70381683307007,
7.50357029184312));
#390643=CARTESIAN_POINT('Ctrl Pts',(-0.483552312554448,2.70390582412704,
7.50365515313923));
#390644=CARTESIAN_POINT('Ctrl Pts',(-0.48303470971915,2.70404272840869,
7.50378570417639));
#390645=CARTESIAN_POINT('Ctrl Pts',(-0.482524868782461,2.70415367027655,
7.50400001621911));
#390646=CARTESIAN_POINT('Ctrl Pts',(-0.482061113295957,2.70422798694399,
7.50428903009635));
#390647=CARTESIAN_POINT('Ctrl Pts',(-0.482009640004878,2.70423623552231,
7.50432110841318));
#390648=CARTESIAN_POINT('Ctrl Pts',(-0.481958712533376,2.70424405384474,
7.50435406373354));
#390649=CARTESIAN_POINT('Ctrl Pts',(-0.481908366893239,2.70425144256795,
7.50438785222351));
#390650=CARTESIAN_POINT('Ctrl Pts',(-0.481600982560994,2.70429655427464,
7.50459414719561));
#390651=CARTESIAN_POINT('Ctrl Pts',(-0.48131031833417,2.70432585979777,
7.50483629897752));
#390652=CARTESIAN_POINT('Ctrl Pts',(-0.481047641490116,2.70433954584457,
7.5050991045531));
#390653=CARTESIAN_POINT('Ctrl Pts',(-0.480468149988743,2.70436973863845,
7.50567888004914));
#390654=CARTESIAN_POINT('Ctrl Pts',(-0.480002061491276,2.7043256226731,
7.50637912803144));
#390655=CARTESIAN_POINT('Ctrl Pts',(-0.479638530743235,2.70423614270301,
7.50710440483569));
#390656=CARTESIAN_POINT('Ctrl Pts',(-0.479549385786719,2.70421420043792,
7.50728225710685));
#390657=CARTESIAN_POINT('Ctrl Pts',(-0.479464598424601,2.70418923522453,
7.50746498566954));
#390658=CARTESIAN_POINT('Ctrl Pts',(-0.479386030199354,2.70416222946144,
7.50764697238949));
#390659=CARTESIAN_POINT('Ctrl Pts',(-0.47896366904298,2.70401705391124,
7.50862528291182));
#390660=CARTESIAN_POINT('Ctrl Pts',(-0.478681344736173,2.70380364525162,
7.50965856837423));
#390661=CARTESIAN_POINT('Ctrl Pts',(-0.478486337883089,2.70356220374557,
7.51067959873204));
#390662=CARTESIAN_POINT('Ctrl Pts',(-0.47837902536587,2.70342933818025,
7.5112414730258));
#390663=CARTESIAN_POINT('Ctrl Pts',(-0.478298467079306,2.70328767800995,
7.51180065547253));
#390664=CARTESIAN_POINT('Ctrl Pts',(-0.478238051202743,2.70314229426445,
7.51235175716501));
#390665=CARTESIAN_POINT('Ctrl Pts',(-0.478029290282389,2.70263993550974,
7.51425603304535));
#390666=CARTESIAN_POINT('Ctrl Pts',(-0.478041734656937,2.70203089399621,
7.51626900505179));
#390667=CARTESIAN_POINT('Ctrl Pts',(-0.478235751309913,2.70136068775766,
7.51827788969242));
#390668=CARTESIAN_POINT('Ctrl Pts',(-0.478246251857814,2.70132441492951,
7.51838661432544));
#390669=CARTESIAN_POINT('Ctrl Pts',(-0.478257292668706,2.70128795759193,
7.51849533314856));
#390670=CARTESIAN_POINT('Ctrl Pts',(-0.478268870165657,2.70125132133976,
7.51860402984325));
#390671=CARTESIAN_POINT('Ctrl Pts',(-0.51115179075919,2.62465641820371,
7.57603338728985));
#390672=CARTESIAN_POINT('Ctrl Pts',(-0.502935967270557,2.6507806888637,
7.55196141284922));
#390673=CARTESIAN_POINT('Ctrl Pts',(-0.494733471561833,2.67685967867694,
7.52783573083105));
#390674=CARTESIAN_POINT('Ctrl Pts',(-0.486543193716074,2.70289709686826,
7.50366116530176));
#390675=CARTESIAN_POINT('Origin',(-1.76626572250576E-16,9.06940118467443E-16,
7.49482233047033));
#390676=CARTESIAN_POINT('Origin',(-0.561510055974246,2.6792933223221,7.49482233047033));
#390677=CARTESIAN_POINT('Origin',(0.,0.,7.50366116523517));
#390678=CARTESIAN_POINT('Origin',(-0.484977299960294,2.69419807522076,7.49482233047033));
#390679=CARTESIAN_POINT('Ctrl Pts',(-0.570374388643616,2.68331282671198,
7.51860402984325));
#390680=CARTESIAN_POINT('Ctrl Pts',(-0.575221773022837,2.68917790562962,
7.51860402984325));
#390681=CARTESIAN_POINT('Ctrl Pts',(-0.582657984926183,2.68756575223785,
7.51860402984325));
#390682=CARTESIAN_POINT('Ctrl Pts',(-0.572174256523385,2.68549056972994,
7.51041458714365));
#390683=CARTESIAN_POINT('Ctrl Pts',(-0.576983494698349,2.68879595835108,
7.5100464290044));
#390684=CARTESIAN_POINT('Ctrl Pts',(-0.582660035745125,2.68756530762508,
7.50729136483009));
#390685=CARTESIAN_POINT('Ctrl Pts',(-0.570756300477604,2.68792226417035,
7.50215815450138));
#390686=CARTESIAN_POINT('Ctrl Pts',(-0.573396483322125,2.68957377833286,
7.49877163671533));
#390687=CARTESIAN_POINT('Ctrl Pts',(-0.576773332211222,2.68886609537093,
7.49481588533172));
#390688=CARTESIAN_POINT('Ctrl Pts',(-0.563322945647624,2.68794368066495,
7.50366171572174));
#390689=CARTESIAN_POINT('Ctrl Pts',(-0.564074028832197,2.69152753840584,
7.50000045605858));
#390690=CARTESIAN_POINT('Ctrl Pts',(-0.564074028832319,2.69152753840582,
7.49482233047317));
#390691=CARTESIAN_POINT('Origin',(-0.580009539540154,2.67534954427313,7.51860402984325));
#390692=CARTESIAN_POINT('Origin',(-0.580009539540154,2.67534954427313,9.));
#390693=CARTESIAN_POINT('Origin',(-0.580009539540154,2.67534954427313,8.75721825406948));
#390694=CARTESIAN_POINT('Ctrl Pts',(-0.559734948604734,2.67044183725424,
8.78942910404913));
#390695=CARTESIAN_POINT('Ctrl Pts',(-0.563269725412667,2.67474971162797,
8.7967269950169));
#390696=CARTESIAN_POINT('Ctrl Pts',(-0.571092507684332,2.67045115797444,
8.79893251111267));
#390697=CARTESIAN_POINT('Ctrl Pts',(-0.566739742255377,2.67891581416313,
8.78111911759577));
#390698=CARTESIAN_POINT('Ctrl Pts',(-0.570936015679921,2.68401812731229,
8.78644465894813));
#390699=CARTESIAN_POINT('Ctrl Pts',(-0.578712537116064,2.68172875488109,
8.78817647674132));
#390700=CARTESIAN_POINT('Ctrl Pts',(-0.57110529676308,2.68419699867589,
8.76780923932035));
#390701=CARTESIAN_POINT('Ctrl Pts',(-0.576062756082901,2.69021682706735,
8.76988516158374));
#390702=CARTESIAN_POINT('Ctrl Pts',(-0.583481134049413,2.68876629311658,
8.77093053738834));
#390703=CARTESIAN_POINT('Ctrl Pts',(-0.570254073382235,2.6831672399729,
8.75371302330491));
#390704=CARTESIAN_POINT('Ctrl Pts',(-0.57508927265449,2.68903980750043,
8.75300828287559));
#390705=CARTESIAN_POINT('Ctrl Pts',(-0.582551442759682,2.68739343067373,
8.75267964240737));
#390706=CARTESIAN_POINT('Origin',(-0.571075363033628,2.66454152541039,8.78727029226991));
#390707=CARTESIAN_POINT('Ctrl Pts',(-0.515891055659666,2.61740223164621,
8.85049129520029));
#390708=CARTESIAN_POINT('Ctrl Pts',(-0.519611637301531,2.6219031631575,
8.85711686593484));
#390709=CARTESIAN_POINT('Ctrl Pts',(-0.527270584603676,2.61810299364327,
8.85933012996512));
#390710=CARTESIAN_POINT('Ctrl Pts',(-0.53109642321101,2.63579675286366,
8.82945683644724));
#390711=CARTESIAN_POINT('Ctrl Pts',(-0.53484788793001,2.64033504482781,
8.8360746990239));
#390712=CARTESIAN_POINT('Ctrl Pts',(-0.542512653014755,2.63649012367216,
8.8382956714852));
#390713=CARTESIAN_POINT('Ctrl Pts',(-0.54627912593586,2.65416385556391,
8.80838214965003));
#390714=CARTESIAN_POINT('Ctrl Pts',(-0.55004539568616,2.65872005774703,
8.81501364461989));
#390715=CARTESIAN_POINT('Ctrl Pts',(-0.557731085305916,2.6548497880324,
8.81722098428721));
#390716=CARTESIAN_POINT('Ctrl Pts',(-0.561440886005602,2.67250562312429,
8.78727029226991));
#390717=CARTESIAN_POINT('Ctrl Pts',(-0.565207781345687,2.67706258210756,
8.79393457792714));
#390718=CARTESIAN_POINT('Ctrl Pts',(-0.572927672898306,2.67318409147408,
8.79610912703474));
#390719=CARTESIAN_POINT('Origin',(-0.525525532687691,2.60943813393231,8.85049129520029));
#390720=CARTESIAN_POINT('Ctrl Pts',(-0.504036631578591,2.6197108805292,
8.85049129520029));
#390721=CARTESIAN_POINT('Ctrl Pts',(-0.502277013195081,2.62527908089984,
8.85711686593484));
#390722=CARTESIAN_POINT('Ctrl Pts',(-0.493751728365454,2.62463079031095,
8.85933012996512));
#390723=CARTESIAN_POINT('Ctrl Pts',(-0.505593340562126,2.61478477403912,
8.86332496987232));
#390724=CARTESIAN_POINT('Ctrl Pts',(-0.501120171846769,2.61594350438772,
8.86648636486738));
#390725=CARTESIAN_POINT('Ctrl Pts',(-0.498123021571836,2.61085496902652,
8.87206031107457));
#390726=CARTESIAN_POINT('Ctrl Pts',(-0.512577143703185,2.61339326418189,
8.86341338519875));
#390727=CARTESIAN_POINT('Ctrl Pts',(-0.517167288227793,2.61275761972348,
8.86654584966058));
#390728=CARTESIAN_POINT('Ctrl Pts',(-0.517980099556504,2.60688705837628,
8.87215952290714));
#390729=CARTESIAN_POINT('Ctrl Pts',(-0.515891055659666,2.61740223164621,
8.85049129520029));
#390730=CARTESIAN_POINT('Ctrl Pts',(-0.519611637301531,2.6219031631575,
8.85711686593484));
#390731=CARTESIAN_POINT('Ctrl Pts',(-0.527270584603676,2.61810299364327,
8.85933012996512));
#390732=CARTESIAN_POINT('Origin',(-0.492117610277389,2.61594432623894,8.85049129520029));
#390733=CARTESIAN_POINT('Ctrl Pts',(-0.482494215215348,2.68788048588352,
8.78727029226991));
#390734=CARTESIAN_POINT('Ctrl Pts',(-0.480712693150467,2.69351799905962,
8.79393457792714));
#390735=CARTESIAN_POINT('Ctrl Pts',(-0.472101526741971,2.69281998167918,
8.79610912703474));
#390736=CARTESIAN_POINT('Ctrl Pts',(-0.489664844518278,2.66518948588238,
8.80838214965002));
#390737=CARTESIAN_POINT('Ctrl Pts',(-0.487883618320903,2.67082606280458,
8.81501364461995));
#390738=CARTESIAN_POINT('Ctrl Pts',(-0.479307239296716,2.67012283067463,
8.81722098428721));
#390739=CARTESIAN_POINT('Ctrl Pts',(-0.496845378477109,2.6424671432281,
8.82945683644723));
#390740=CARTESIAN_POINT('Ctrl Pts',(-0.495071154197115,2.64808156302841,
8.8360746990239));
#390741=CARTESIAN_POINT('Ctrl Pts',(-0.486523682952882,2.64739397461503,
8.83829567148519));
#390742=CARTESIAN_POINT('Ctrl Pts',(-0.504036631578591,2.6197108805292,
8.85049129520029));
#390743=CARTESIAN_POINT('Ctrl Pts',(-0.50227701319508,2.62527908089984,
8.85711686593484));
#390744=CARTESIAN_POINT('Ctrl Pts',(-0.493751728365454,2.62463079031095,
8.85933012996512));
#390745=CARTESIAN_POINT('Origin',(-0.470575193914146,2.68411393159325,8.78727029226991));
#390746=CARTESIAN_POINT('Ctrl Pts',(-0.478324646131838,2.70107476062509,
8.75374538247847));
#390747=CARTESIAN_POINT('Ctrl Pts',(-0.476047406919802,2.70832448889302,
8.75304829418601));
#390748=CARTESIAN_POINT('Ctrl Pts',(-0.468521707494412,2.70960296117184,
8.75272238421917));
#390749=CARTESIAN_POINT('Ctrl Pts',(-0.477926903323299,2.70233339384106,
8.76769408445023));
#390750=CARTESIAN_POINT('Ctrl Pts',(-0.475591700278383,2.70976535062987,
8.76974318093971));
#390751=CARTESIAN_POINT('Ctrl Pts',(-0.468179438674284,2.71120643882727,
8.7707786988043));
#390752=CARTESIAN_POINT('Ctrl Pts',(-0.479965506394844,2.6958823569765,
8.78108014887987));
#390753=CARTESIAN_POINT('Ctrl Pts',(-0.47799013061423,2.70218181154224,
8.78639403366322));
#390754=CARTESIAN_POINT('Ctrl Pts',(-0.469936666898015,2.70299654947583,
8.78812224174741));
#390755=CARTESIAN_POINT('Ctrl Pts',(-0.483306326769345,2.68531053162587,
8.78944554828686));
#390756=CARTESIAN_POINT('Ctrl Pts',(-0.481646894576971,2.69062115328589,
8.79673892988687));
#390757=CARTESIAN_POINT('Ctrl Pts',(-0.472791874487153,2.68957608222346,
8.79894799272499));
#390758=CARTESIAN_POINT('Origin',(-0.466349848864459,2.6974847670495,8.75721825406948));
#390759=CARTESIAN_POINT('Origin',(-0.466349848864459,2.6974847670495,9.));
#390760=CARTESIAN_POINT('Origin',(-0.466349848864459,2.6974847670495,7.51860402984325));
#390761=CARTESIAN_POINT('Ctrl Pts',(-0.486543054373017,2.70289632259342,
7.50366195182966));
#390762=CARTESIAN_POINT('Ctrl Pts',(-0.487191808179154,2.70650034953686,
7.50000065167735));
#390763=CARTESIAN_POINT('Ctrl Pts',(-0.487191808179039,2.70650034953688,
7.49482233047108));
#390764=CARTESIAN_POINT('Ctrl Pts',(-0.479638433643609,2.70566760608483,
7.50215800491338));
#390765=CARTESIAN_POINT('Ctrl Pts',(-0.477809241429461,2.70818926288503,
7.49877273257264));
#390766=CARTESIAN_POINT('Ctrl Pts',(-0.47441172804546,2.70880086664194,
7.49481816995649));
#390767=CARTESIAN_POINT('Ctrl Pts',(-0.477419885150963,2.70393900580489,
7.51043025814042));
#390768=CARTESIAN_POINT('Ctrl Pts',(-0.474203815632229,2.70881236746164,
7.51006209594516));
#390769=CARTESIAN_POINT('Ctrl Pts',(-0.468476805372723,2.70980248040963,
7.507312818217));
#390770=CARTESIAN_POINT('Ctrl Pts',(-0.478269325502383,2.70124988015244,
7.51860402984326));
#390771=CARTESIAN_POINT('Ctrl Pts',(-0.475977343984474,2.70850576315261,
7.51860402984326));
#390772=CARTESIAN_POINT('Ctrl Pts',(-0.468479300229132,2.70980204909083,
7.51860402984327));
#390773=CARTESIAN_POINT('Origin',(0.,0.,7.5));
#390774=CARTESIAN_POINT('Origin',(-0.670846486662627,2.58203466569847,7.5));
#390775=CARTESIAN_POINT('',(-0.670846486662627,2.58203466569847,7.59394543036555));
#390776=CARTESIAN_POINT('',(-0.670846486662627,2.58203466569847,8.85049129520029));
#390777=CARTESIAN_POINT('',(-0.670846486662627,2.58203466569847,7.5));
#390778=CARTESIAN_POINT('',(-0.653715973115269,2.65144443664272,8.78727029226991));
#390779=CARTESIAN_POINT('Ctrl Pts',(-0.670846486662627,2.58203466569847,
8.85049129520029));
#390780=CARTESIAN_POINT('Ctrl Pts',(-0.66512801519336,2.6052048872879,8.82945686509571));
#390781=CARTESIAN_POINT('Ctrl Pts',(-0.659418044923399,2.62834066354124,
8.80838212259897));
#390782=CARTESIAN_POINT('Ctrl Pts',(-0.653715973115269,2.65144443664272,
8.78727029226991));
#390783=CARTESIAN_POINT('',(-0.650355981859161,2.66505851907034,8.75721825406948));
#390784=CARTESIAN_POINT('Origin',(-0.660467557061359,2.62408907064251,8.7593767971312));
#390785=CARTESIAN_POINT('',(-0.650355981859161,2.66505851907034,7.51860402984325));
#390786=CARTESIAN_POINT('',(-0.650355981859161,2.66505851907034,7.5));
#390787=CARTESIAN_POINT('Ctrl Pts',(-0.650355981859161,2.66505851907034,
7.51860402984325));
#390788=CARTESIAN_POINT('Ctrl Pts',(-0.652994732413348,2.65436677471377,
7.52834476460825));
#390789=CARTESIAN_POINT('Ctrl Pts',(-0.655635196006324,2.64366808943105,
7.53807742314407));
#390790=CARTESIAN_POINT('Ctrl Pts',(-0.658277430155635,2.63296223017134,
7.54780169004674));
#390791=CARTESIAN_POINT('Ctrl Pts',(-0.662462586247572,2.61600472770629,
7.5632044032688));
#390792=CARTESIAN_POINT('Ctrl Pts',(-0.66665218975856,2.59902920509617,
7.57858609112103));
#390793=CARTESIAN_POINT('Ctrl Pts',(-0.670846486662627,2.58203466569847,
7.59394543036555));
#390794=CARTESIAN_POINT('Origin',(-0.870959027954988,2.77926849494598,7.5));
#390795=CARTESIAN_POINT('',(-0.74112366109302,2.64125643059841,8.75721825406948));
#390796=CARTESIAN_POINT('',(-0.731515368664223,2.6310430326237,8.78727029226991));
#390797=CARTESIAN_POINT('Origin',(-0.707125938766606,2.60511761915751,8.75658640621092));
#390798=CARTESIAN_POINT('',(-0.682528638916253,2.57897124462358,8.85049129520029));
#390799=CARTESIAN_POINT('Ctrl Pts',(-0.731515368664224,2.6310430326237,
8.78727029226991));
#390800=CARTESIAN_POINT('Ctrl Pts',(-0.715209619867131,2.6137103897036,
8.80838212259896));
#390801=CARTESIAN_POINT('Ctrl Pts',(-0.698881284484175,2.59635373775254,
8.82945686509571));
#390802=CARTESIAN_POINT('Ctrl Pts',(-0.682528638916253,2.57897124462358,
8.85049129520029));
#390803=CARTESIAN_POINT('',(-0.682528638916253,2.57897124462358,7.59394543036555));
#390804=CARTESIAN_POINT('',(-0.682528638916253,2.57897124462358,7.5));
#390805=CARTESIAN_POINT('',(-0.74112366109302,2.64125643059841,7.51860402984325));
#390806=CARTESIAN_POINT('Ctrl Pts',(-0.682528638916253,2.57897124462358,
7.59394543036555));
#390807=CARTESIAN_POINT('Ctrl Pts',(-0.694522727030089,2.59172068955962,
7.57858609112103));
#390808=CARTESIAN_POINT('Ctrl Pts',(-0.706503393831148,2.60445586794315,
7.56320440326857));
#390809=CARTESIAN_POINT('Ctrl Pts',(-0.718471342711481,2.61717752746398,
7.54780169004651));
#390810=CARTESIAN_POINT('Ctrl Pts',(-0.726027123794475,2.62520915220711,
7.53807742314383));
#390811=CARTESIAN_POINT('Ctrl Pts',(-0.733577841762333,2.63323539497312,
7.52834476460825));
#390812=CARTESIAN_POINT('Ctrl Pts',(-0.741123661093021,2.64125643059841,
7.51860402984325));
#390813=CARTESIAN_POINT('',(-0.74112366109302,2.64125643059841,7.5));
#390814=CARTESIAN_POINT('Origin',(-0.677521207658193,2.58368200434955,7.5));
#390815=CARTESIAN_POINT('Ctrl Pts',(-0.682528638916253,2.57897124462358,
8.85049129520029));
#390816=CARTESIAN_POINT('Ctrl Pts',(-0.682395941778429,2.5788301905613,
8.85097269580138));
#390817=CARTESIAN_POINT('Ctrl Pts',(-0.682258792377709,2.57869667966879,
8.85143669361005));
#390818=CARTESIAN_POINT('Ctrl Pts',(-0.682110265579986,2.5785651906683,
8.8519052845931));
#390819=CARTESIAN_POINT('Ctrl Pts',(-0.681819756582866,2.57830800652208,
8.85282181883899));
#390820=CARTESIAN_POINT('Ctrl Pts',(-0.681493063938917,2.57806532082595,
8.85372622499636));
#390821=CARTESIAN_POINT('Ctrl Pts',(-0.681115866722538,2.57784570272728,
8.85462257735071));
#390822=CARTESIAN_POINT('Ctrl Pts',(-0.680802730990279,2.57766338358186,
8.85536669723986));
#390823=CARTESIAN_POINT('Ctrl Pts',(-0.680454733368184,2.57749689311832,
8.85610498449051));
#390824=CARTESIAN_POINT('Ctrl Pts',(-0.680060197116736,2.57735833882345,
8.85681338218371));
#390825=CARTESIAN_POINT('Ctrl Pts',(-0.679702154848916,2.57723260058325,
8.85745625420284));
#390826=CARTESIAN_POINT('Ctrl Pts',(-0.679301492304152,2.57712772749012,
8.85808743050666));
#390827=CARTESIAN_POINT('Ctrl Pts',(-0.678839734209342,2.57706554866298,
8.8586680450841));
#390828=CARTESIAN_POINT('Ctrl Pts',(-0.678626689034085,2.57703686070002,
8.85893592806395));
#390829=CARTESIAN_POINT('Ctrl Pts',(-0.678400505068362,2.57701746342574,
8.85919241173848));
#390830=CARTESIAN_POINT('Ctrl Pts',(-0.678158684088287,2.57701094304344,
8.85943017985534));
#390831=CARTESIAN_POINT('Ctrl Pts',(-0.677832154178514,2.5770021385971,
8.8597512372));
#390832=CARTESIAN_POINT('Ctrl Pts',(-0.677468785008064,2.57701722880275,
8.86004599534705));
#390833=CARTESIAN_POINT('Ctrl Pts',(-0.677073374472421,2.57706643848078,
8.86026130871721));
#390834=CARTESIAN_POINT('Ctrl Pts',(-0.676928603527518,2.57708445553128,
8.86034014101235));
#390835=CARTESIAN_POINT('Ctrl Pts',(-0.676777361302704,2.57710730469718,
8.86040910639692));
#390836=CARTESIAN_POINT('Ctrl Pts',(-0.676623818556248,2.5771346960702,
8.86046313645506));
#390837=CARTESIAN_POINT('Ctrl Pts',(-0.676384216386312,2.57717744007839,
8.86054744990829));
#390838=CARTESIAN_POINT('Ctrl Pts',(-0.676132497543398,2.57723255650791,
8.86059655985669));
#390839=CARTESIAN_POINT('Ctrl Pts',(-0.675884742861718,2.57729622439678,
8.86059725258816));
#390840=CARTESIAN_POINT('Ctrl Pts',(-0.675636415767744,2.57736003938391,
8.86059794692011));
#390841=CARTESIAN_POINT('Ctrl Pts',(-0.675389978449745,2.57743572627043,
8.86056369958366));
#390842=CARTESIAN_POINT('Ctrl Pts',(-0.675157766911362,2.57751555979232,
8.86048590497774));
#390843=CARTESIAN_POINT('Ctrl Pts',(-0.675097166613615,2.5775363939646,
8.86046560290182));
#390844=CARTESIAN_POINT('Ctrl Pts',(-0.675036776242757,2.57755786724415,
8.86044257503091));
#390845=CARTESIAN_POINT('Ctrl Pts',(-0.674978450913636,2.57757928515972,
8.86041778462583));
#390846=CARTESIAN_POINT('Ctrl Pts',(-0.67458599382435,2.57772340115413,
8.86025097596201));
#390847=CARTESIAN_POINT('Ctrl Pts',(-0.674234485840249,2.57788466047735,
8.8599848982295));
#390848=CARTESIAN_POINT('Ctrl Pts',(-0.673930653710898,2.57805065560953,
8.85968173251462));
#390849=CARTESIAN_POINT('Ctrl Pts',(-0.673769943921977,2.57813845752406,
8.85952137522077));
#390850=CARTESIAN_POINT('Ctrl Pts',(-0.673619383548711,2.57822910929007,
8.85934740853961));
#390851=CARTESIAN_POINT('Ctrl Pts',(-0.673480293963271,2.57832000073264,
8.8591675900182));
#390852=CARTESIAN_POINT('Ctrl Pts',(-0.672921776980401,2.57868497711901,
8.85844552518695));
#390853=CARTESIAN_POINT('Ctrl Pts',(-0.672514998205071,2.57907191274904,
8.85759444184124));
#390854=CARTESIAN_POINT('Ctrl Pts',(-0.672211669896369,2.57941718972865,
8.85683498915139));
#390855=CARTESIAN_POINT('Ctrl Pts',(-0.672179927396693,2.57945332204502,
8.85675551444998));
#390856=CARTESIAN_POINT('Ctrl Pts',(-0.672149335081543,2.57948900814193,
8.85667699793651));
#390857=CARTESIAN_POINT('Ctrl Pts',(-0.672119849310369,2.57952418108658,
8.85659965593547));
#390858=CARTESIAN_POINT('Ctrl Pts',(-0.671721848866485,2.57999894728824,
8.85555568965886));
#390859=CARTESIAN_POINT('Ctrl Pts',(-0.671407911415525,2.58051270616165,
8.85434650606346));
#390860=CARTESIAN_POINT('Ctrl Pts',(-0.671171181984412,2.58106475696341,
8.85297329937117));
#390861=CARTESIAN_POINT('Ctrl Pts',(-0.671038036103547,2.58137525190245,
8.85220095427747));
#390862=CARTESIAN_POINT('Ctrl Pts',(-0.670929549231038,2.58169811105686,
8.85137579139183));
#390863=CARTESIAN_POINT('Ctrl Pts',(-0.670846486662627,2.58203466569847,
8.85049129520029));
#390864=CARTESIAN_POINT('Origin',(-0.677521207658193,2.58368200434955,7.59394543036555));
#390865=CARTESIAN_POINT('Ctrl Pts',(-0.682143374360193,2.57856171709663,
7.59443877723642));
#390866=CARTESIAN_POINT('Ctrl Pts',(-0.678175520124387,2.57434397760585,
7.58783886950016));
#390867=CARTESIAN_POINT('Ctrl Pts',(-0.67081360840433,2.57857262246712,
7.58559994247159));
#390868=CARTESIAN_POINT('Ctrl Pts',(-0.703803774221552,2.60158623323358,
7.56670252222134));
#390869=CARTESIAN_POINT('Ctrl Pts',(-0.699841654661634,2.5973745895738,
7.56004874999027));
#390870=CARTESIAN_POINT('Ctrl Pts',(-0.692425479350873,2.60160976383429,
7.55786368756704));
#390871=CARTESIAN_POINT('Ctrl Pts',(-0.725423725450335,2.6245677533871,
7.53888913333559));
#390872=CARTESIAN_POINT('Ctrl Pts',(-0.721438058819866,2.62033107972285,
7.5322200213728));
#390873=CARTESIAN_POINT('Ctrl Pts',(-0.713998608634745,2.62460390380804,
7.53005029815327));
#390874=CARTESIAN_POINT('Ctrl Pts',(-0.747002249729062,2.6475052376278,
7.51101258149734));
#390875=CARTESIAN_POINT('Ctrl Pts',(-0.742968269576889,2.6432172077805,
7.5043616886572));
#390876=CARTESIAN_POINT('Ctrl Pts',(-0.735531870110719,2.64755396284901,
7.50217374673251));
#390877=CARTESIAN_POINT('',(-0.734382828366911,2.6463293175146,7.50366116523517));
#390878=CARTESIAN_POINT('Ctrl Pts',(-0.741123661093021,2.64125643059841,
7.51860402984325));
#390879=CARTESIAN_POINT('Ctrl Pts',(-0.74142625372272,2.6415780797337,7.51734760759494));
#390880=CARTESIAN_POINT('Ctrl Pts',(-0.741656354716085,2.64190950301717,
7.51608817408573));
#390881=CARTESIAN_POINT('Ctrl Pts',(-0.741802465711207,2.642257553818,7.5148100591312));
#390882=CARTESIAN_POINT('Ctrl Pts',(-0.741934816542025,2.64257282655034,
7.51365231206384));
#390883=CARTESIAN_POINT('Ctrl Pts',(-0.741998669384408,2.64290209001153,
7.51247773061043));
#390884=CARTESIAN_POINT('Ctrl Pts',(-0.74195666965544,2.64324667653265,
7.51129758471022));
#390885=CARTESIAN_POINT('Ctrl Pts',(-0.741904468788883,2.64367495822514,
7.50983079813402));
#390886=CARTESIAN_POINT('Ctrl Pts',(-0.741677487599936,2.64411166614862,
7.50839324291155));
#390887=CARTESIAN_POINT('Ctrl Pts',(-0.741200920368982,2.64452196792184,
7.50715379678855));
#390888=CARTESIAN_POINT('Ctrl Pts',(-0.740980760040236,2.64471151551851,
7.50658120839351));
#390889=CARTESIAN_POINT('Ctrl Pts',(-0.740669836489905,2.64491517281699,
7.50598221009429));
#390890=CARTESIAN_POINT('Ctrl Pts',(-0.740263085778462,2.64510906506821,
7.50545747549611));
#390891=CARTESIAN_POINT('Ctrl Pts',(-0.740046031008724,2.64521253197498,
7.50517746087247));
#390892=CARTESIAN_POINT('Ctrl Pts',(-0.739799421791897,2.64531452291222,
7.50491486231392));
#390893=CARTESIAN_POINT('Ctrl Pts',(-0.739529151276104,2.64541079559314,
7.50468370960992));
#390894=CARTESIAN_POINT('Ctrl Pts',(-0.739125011602992,2.64555475361861,
7.50433806340446));
#390895=CARTESIAN_POINT('Ctrl Pts',(-0.738655660604332,2.64568971815751,
7.50405484070983));
#390896=CARTESIAN_POINT('Ctrl Pts',(-0.738152510216519,2.64580591110398,
7.5038576603613));
#390897=CARTESIAN_POINT('Ctrl Pts',(-0.738098706103272,2.64581833613356,
7.50383657498791));
#390898=CARTESIAN_POINT('Ctrl Pts',(-0.738044542534825,2.6458305550689,
7.50381643264937));
#390899=CARTESIAN_POINT('Ctrl Pts',(-0.737990077468964,2.64584256247728,
7.50379723213559));
#390900=CARTESIAN_POINT('Ctrl Pts',(-0.737626505337567,2.64592271585614,
7.50366906242519));
#390901=CARTESIAN_POINT('Ctrl Pts',(-0.737241435141435,2.64599448492876,
7.50358235568538));
#390902=CARTESIAN_POINT('Ctrl Pts',(-0.73686861200227,2.64605473955297,
7.5035341175365));
#390903=CARTESIAN_POINT('Ctrl Pts',(-0.736309605900523,2.64614508454247,
7.50346178989176));
#390904=CARTESIAN_POINT('Ctrl Pts',(-0.735704401177935,2.64621850689902,
7.50346967198527));
#390905=CARTESIAN_POINT('Ctrl Pts',(-0.735108059804471,2.64627230370702,
7.50354272648692));
#390906=CARTESIAN_POINT('Ctrl Pts',(-0.734862772254031,2.64629443144767,
7.50357277531559));
#390907=CARTESIAN_POINT('Ctrl Pts',(-0.734619322893515,2.64631335066844,
7.50361331098761));
#390908=CARTESIAN_POINT('Ctrl Pts',(-0.73438282836729,2.64632931751596,
7.50366116523659));
#390909=CARTESIAN_POINT('',(-0.678263889301916,2.5865141713381,7.57603338622103));
#390910=CARTESIAN_POINT('Origin',(-0.680502659389315,2.59506282024345,7.58486873427627));
#390911=CARTESIAN_POINT('Ctrl Pts',(-0.734382828409885,2.64632931755257,
7.50366116529968));
#390912=CARTESIAN_POINT('Ctrl Pts',(-0.715706430670505,2.62642404271696,
7.52783573079709));
#390913=CARTESIAN_POINT('Ctrl Pts',(-0.697000987800555,2.60648661431366,
7.55196141284069));
#390914=CARTESIAN_POINT('Ctrl Pts',(-0.678263890381611,2.58651417197206,
7.57603338728831));
#390915=CARTESIAN_POINT('Ctrl Pts',(-0.683105249421492,2.57984075934186,
7.59639677331372));
#390916=CARTESIAN_POINT('Ctrl Pts',(-0.672361328299493,2.56400514804978,
7.59974925422227));
#390917=CARTESIAN_POINT('Ctrl Pts',(-0.670770761278395,2.58307524303173,
7.5963967733137));
#390918=CARTESIAN_POINT('Ctrl Pts',(-0.681462581934839,2.57630285775874,
7.58707626057425));
#390919=CARTESIAN_POINT('Ctrl Pts',(-0.674975104133204,2.57397260812082,
7.58811717123965));
#390920=CARTESIAN_POINT('Ctrl Pts',(-0.670465937779981,2.57918651744118,
7.58707626057421));
#390921=CARTESIAN_POINT('Ctrl Pts',(-0.679301722070269,2.58198232224995,
7.5801537675693));
#390922=CARTESIAN_POINT('Ctrl Pts',(-0.676728207785925,2.58065795214825,
7.58208760766041));
#390923=CARTESIAN_POINT('Ctrl Pts',(-0.675135748308942,2.58307476921869,
7.5801537675693));
#390924=CARTESIAN_POINT('Ctrl Pts',(-0.678263889092194,2.58651417053754,
7.57603338509286));
#390925=CARTESIAN_POINT('Ctrl Pts',(-0.678263889092194,2.58651417053754,
7.57603338509286));
#390926=CARTESIAN_POINT('Ctrl Pts',(-0.678263889092194,2.58651417053754,
7.57603338509286));
#390927=CARTESIAN_POINT('Origin',(-0.680508179114778,2.59506137280114,7.58486873427621));
#390928=CARTESIAN_POINT('Ctrl Pts',(-0.648293759643861,2.67341427391706,
7.51098857897448));
#390929=CARTESIAN_POINT('Ctrl Pts',(-0.649704436926212,2.66769846237564,
7.50433767179956));
#390930=CARTESIAN_POINT('Ctrl Pts',(-0.658312065540219,2.66782800281639,
7.50214974420965));
#390931=CARTESIAN_POINT('Ctrl Pts',(-0.655841875747604,2.64283066015831,
7.5388732158917));
#390932=CARTESIAN_POINT('Ctrl Pts',(-0.657235650612588,2.6371833341829,
7.53220407452063));
#390933=CARTESIAN_POINT('Ctrl Pts',(-0.665814560266708,2.6372556464832,
7.53003438070911));
#390934=CARTESIAN_POINT('Ctrl Pts',(-0.663404487018657,2.61218831457929,
7.56669465659232));
#390935=CARTESIAN_POINT('Ctrl Pts',(-0.664790024933311,2.60657436325045,
7.560040858333));
#390936=CARTESIAN_POINT('Ctrl Pts',(-0.673330168792972,2.60662528459036,
7.55785582193789));
#390937=CARTESIAN_POINT('Ctrl Pts',(-0.670981251430372,2.58148862301069,
7.59443891967696));
#390938=CARTESIAN_POINT('Ctrl Pts',(-0.672368798202527,2.57586653215139,
7.58783901202978));
#390939=CARTESIAN_POINT('Ctrl Pts',(-0.680858439628796,2.57593841011513,
7.58560008491213));
#390940=CARTESIAN_POINT('',(-0.658718750143892,2.66617077539049,7.50366116523517));
#390941=CARTESIAN_POINT('Ctrl Pts',(-0.658718750143982,2.66617077539085,
7.50366116523554));
#390942=CARTESIAN_POINT('Ctrl Pts',(-0.658034914852356,2.66649712920298,
7.50350835821027));
#390943=CARTESIAN_POINT('Ctrl Pts',(-0.657395686666161,2.66677487969734,
7.50345484956));
#390944=CARTESIAN_POINT('Ctrl Pts',(-0.656782300120846,2.66701283537894,
7.50349758195598));
#390945=CARTESIAN_POINT('Ctrl Pts',(-0.656467587333167,2.66713492429086,
7.50351950684424));
#390946=CARTESIAN_POINT('Ctrl Pts',(-0.656128704689314,2.6672586916696,
7.50357029184312));
#390947=CARTESIAN_POINT('Ctrl Pts',(-0.655798643426432,2.66736905658083,
7.50365515313924));
#390948=CARTESIAN_POINT('Ctrl Pts',(-0.655290875549116,2.66753884250547,
7.50378570417639));
#390949=CARTESIAN_POINT('Ctrl Pts',(-0.654789190205193,2.66768222205234,
7.50400001621911));
#390950=CARTESIAN_POINT('Ctrl Pts',(-0.654331149039306,2.66778609894425,
7.50428903009635));
#390951=CARTESIAN_POINT('Ctrl Pts',(-0.654280309993851,2.66779762848007,
7.50432110841318));
#390952=CARTESIAN_POINT('Ctrl Pts',(-0.654229988079937,2.66780869367321,
7.50435406373354));
#390953=CARTESIAN_POINT('Ctrl Pts',(-0.654180219277436,2.66781929287174,
7.50438785222352));
#390954=CARTESIAN_POINT('Ctrl Pts',(-0.65387635681624,2.66788400607338,
7.50459414719561));
#390955=CARTESIAN_POINT('Ctrl Pts',(-0.653588167401559,2.66793187430612,
7.50483629897752));
#390956=CARTESIAN_POINT('Ctrl Pts',(-0.653326907123282,2.66796236199666,
7.5050991045531));
#390957=CARTESIAN_POINT('Ctrl Pts',(-0.652750540708295,2.66802962090417,
7.50567888004914));
#390958=CARTESIAN_POINT('Ctrl Pts',(-0.652282583320029,2.66801545797237,
7.50637912803144));
#390959=CARTESIAN_POINT('Ctrl Pts',(-0.651914066483531,2.66794945334347,
7.50710440483569));
#390960=CARTESIAN_POINT('Ctrl Pts',(-0.651823698839137,2.66793326769808,
7.50728225710685));
#390961=CARTESIAN_POINT('Ctrl Pts',(-0.651737486155035,2.66791378612335,
7.50746498566954));
#390962=CARTESIAN_POINT('Ctrl Pts',(-0.651657349091451,2.66789186972997,
7.50764697238949));
#390963=CARTESIAN_POINT('Ctrl Pts',(-0.651226554291936,2.66777405323071,
7.50862528291182));
#390964=CARTESIAN_POINT('Ctrl Pts',(-0.65093113691093,2.66757917162252,
7.50965856837422));
#390965=CARTESIAN_POINT('Ctrl Pts',(-0.650721061509935,2.66735072031591,
7.51067959873202));
#390966=CARTESIAN_POINT('Ctrl Pts',(-0.650605456751792,2.66722500327373,
7.51124147302579));
#390967=CARTESIAN_POINT('Ctrl Pts',(-0.650515987782593,2.66708879554658,
7.51180065547253));
#390968=CARTESIAN_POINT('Ctrl Pts',(-0.650446381268371,2.66694758136608,
7.512351757165));
#390969=CARTESIAN_POINT('Ctrl Pts',(-0.650205863033793,2.6664596301194,
7.51425603304535));
#390970=CARTESIAN_POINT('Ctrl Pts',(-0.650179260416289,2.66585104263316,
7.5162690050518));
#390971=CARTESIAN_POINT('Ctrl Pts',(-0.650329938180108,2.66516978271556,
7.51827788969243));
#390972=CARTESIAN_POINT('Ctrl Pts',(-0.650338093145428,2.66513291164142,
7.51838661432545));
#390973=CARTESIAN_POINT('Ctrl Pts',(-0.650346775442151,2.66509582182217,
7.51849533314856));
#390974=CARTESIAN_POINT('Ctrl Pts',(-0.650355981859157,2.66505851907034,
7.51860402984325));
#390975=CARTESIAN_POINT('Ctrl Pts',(-0.678263888672321,2.58651417242152,
7.57603338728985));
#390976=CARTESIAN_POINT('Ctrl Pts',(-0.671738733242212,2.61311115758385,
7.55196141284922));
#390977=CARTESIAN_POINT('Ctrl Pts',(-0.665223977054838,2.63966210102001,
7.52783573083105));
#390978=CARTESIAN_POINT('Ctrl Pts',(-0.65871875012457,2.66617077544643,
7.50366116530176));
#390979=CARTESIAN_POINT('Origin',(-2.3437152691429E-16,8.93760209386495E-16,
7.49482233047033));
#390980=CARTESIAN_POINT('Origin',(-0.732019285896515,2.63781235403043,7.49482233047033));
#390981=CARTESIAN_POINT('Origin',(0.,0.,7.50366116523517));
#390982=CARTESIAN_POINT('Origin',(-0.656598725434881,2.65758995402927,7.49482233047033));
#390983=CARTESIAN_POINT('Ctrl Pts',(-0.741122936374192,2.64125566017334,
7.51860402984325));
#390984=CARTESIAN_POINT('Ctrl Pts',(-0.746336138178783,2.64679811567381,
7.51860402984325));
#390985=CARTESIAN_POINT('Ctrl Pts',(-0.753653780564788,2.64471283489161,
7.51860402984325));
#390986=CARTESIAN_POINT('Ctrl Pts',(-0.743058634706594,2.64331361085372,
7.51041458714365));
#390987=CARTESIAN_POINT('Ctrl Pts',(-0.748069768762018,2.64630407925161,
7.5100464290044));
#390988=CARTESIAN_POINT('Ctrl Pts',(-0.753655798683677,2.64471225979593,
7.50729136483009));
#390989=CARTESIAN_POINT('Ctrl Pts',(-0.7417993912013,2.64583115787287,7.50215815450138));
#390990=CARTESIAN_POINT('Ctrl Pts',(-0.744539962382695,2.64731012172676,
7.49877163671532));
#390991=CARTESIAN_POINT('Ctrl Pts',(-0.747864531770537,2.64638753732423,
7.49481588533172));
#390992=CARTESIAN_POINT('Ctrl Pts',(-0.734382681155565,2.64632878704414,
7.50366171572174));
#390993=CARTESIAN_POINT('Ctrl Pts',(-0.735361839713022,2.64985715930008,
7.50000045605858));
#390994=CARTESIAN_POINT('Ctrl Pts',(-0.735361839713142,2.64985715930005,
7.49482233047317));
#390995=CARTESIAN_POINT('Origin',(-0.75022808156222,2.63269141291483,7.51860402984325));
#390996=CARTESIAN_POINT('Origin',(-0.75022808156222,2.63269141291483,9.));
#390997=CARTESIAN_POINT('Origin',(-0.75022808156222,2.63269141291483,8.75721825406948));
#390998=CARTESIAN_POINT('Ctrl Pts',(-0.729680709080017,2.62909278680762,
8.78942910404913));
#390999=CARTESIAN_POINT('Ctrl Pts',(-0.733484229768665,2.63316533626376,
8.79672699501691));
#391000=CARTESIAN_POINT('Ctrl Pts',(-0.741015530016991,2.62837440706872,
8.79893251111267));
#391001=CARTESIAN_POINT('Ctrl Pts',(-0.737214040195502,2.63710055435199,
8.78111911759576));
#391002=CARTESIAN_POINT('Ctrl Pts',(-0.741728598252128,2.64192352809016,
8.78644465894812));
#391003=CARTESIAN_POINT('Ctrl Pts',(-0.749342461395661,2.63914061598106,
8.78817647674132));
#391004=CARTESIAN_POINT('Ctrl Pts',(-0.741908991856752,2.64209118606712,
8.76780923932033));
#391005=CARTESIAN_POINT('Ctrl Pts',(-0.747241957274005,2.64778102056638,
8.76988516158375));
#391006=CARTESIAN_POINT('Ctrl Pts',(-0.75455215735806,2.64585816978495,
8.77093053738833));
#391007=CARTESIAN_POINT('Ctrl Pts',(-0.740993540539016,2.64111808118309,
8.75371302330491));
#391008=CARTESIAN_POINT('Ctrl Pts',(-0.746195062069134,2.64666879060978,
8.75300828287558));
#391009=CARTESIAN_POINT('Ctrl Pts',(-0.753536416620075,2.64454769356067,
8.75267964240737));
#391010=CARTESIAN_POINT('Origin',(-0.740619789133423,2.62247801494012,8.78727029226991));
#391011=CARTESIAN_POINT('Ctrl Pts',(-0.682528638916253,2.57897124462358,
8.85049129520029));
#391012=CARTESIAN_POINT('Ctrl Pts',(-0.68652995189615,2.58322455000411,
8.85711686593484));
#391013=CARTESIAN_POINT('Ctrl Pts',(-0.693929685372903,2.57894147790724,
8.85933012996512));
#391014=CARTESIAN_POINT('Ctrl Pts',(-0.698881306430035,2.59635376108049,
8.82945683644723));
#391015=CARTESIAN_POINT('Ctrl Pts',(-0.7029158327269,2.60064237146728,8.8360746990239));
#391016=CARTESIAN_POINT('Ctrl Pts',(-0.710318504785493,2.59631426692943,
8.83829567148519));
#391017=CARTESIAN_POINT('Ctrl Pts',(-0.715209598974206,2.61371036749489,
8.80838214965003));
#391018=CARTESIAN_POINT('Ctrl Pts',(-0.719260047395539,2.61801590274055,
8.81501364461988));
#391019=CARTESIAN_POINT('Ctrl Pts',(-0.726681976909672,2.6136611610855,
8.81722098428721));
#391020=CARTESIAN_POINT('Ctrl Pts',(-0.731515368664224,2.6310430326237,
8.78727029226991));
#391021=CARTESIAN_POINT('Ctrl Pts',(-0.735566489878335,2.63534928303293,
8.79393457792714));
#391022=CARTESIAN_POINT('Ctrl Pts',(-0.743022024337723,2.63098414602442,
8.79610912703474));
#391023=CARTESIAN_POINT('Origin',(-0.691633059385452,2.57040622694001,8.85049129520029));
#391024=CARTESIAN_POINT('Ctrl Pts',(-0.670846486662627,2.58203466569847,
8.85049129520029));
#391025=CARTESIAN_POINT('Ctrl Pts',(-0.669447239426447,2.58770416474116,
8.85711686593485));
#391026=CARTESIAN_POINT('Ctrl Pts',(-0.660897934588195,2.58760342300925,
8.85933012996512));
#391027=CARTESIAN_POINT('Ctrl Pts',(-0.67208438049413,2.57701894173547,
8.86332496987231));
#391028=CARTESIAN_POINT('Ctrl Pts',(-0.667694642491979,2.5784618882519,
8.86648636486737));
#391029=CARTESIAN_POINT('Ctrl Pts',(-0.664377626603758,2.57357583590977,
8.87206031107457));
#391030=CARTESIAN_POINT('Ctrl Pts',(-0.678964680319968,2.57518283708094,
8.86341338519876));
#391031=CARTESIAN_POINT('Ctrl Pts',(-0.683504668020055,2.57425440705277,
8.86654584966056));
#391032=CARTESIAN_POINT('Ctrl Pts',(-0.683939681183819,2.56834383040287,
8.87215952290714));
#391033=CARTESIAN_POINT('Ctrl Pts',(-0.682528638916253,2.57897124462358,
8.85049129520029));
#391034=CARTESIAN_POINT('Ctrl Pts',(-0.68652995189615,2.58322455000411,
8.85711686593484));
#391035=CARTESIAN_POINT('Ctrl Pts',(-0.693929685372902,2.57894147790724,
8.85933012996512));
#391036=CARTESIAN_POINT('Origin',(-0.658710630307053,2.57903950451468,8.85049129520029));
#391037=CARTESIAN_POINT('Ctrl Pts',(-0.653715973115268,2.65144443664272,
8.78727029226991));
#391038=CARTESIAN_POINT('Ctrl Pts',(-0.652299308087875,2.65718450945398,
8.79393457792714));
#391039=CARTESIAN_POINT('Ctrl Pts',(-0.643661112117194,2.6570396455512,
8.79610912703474));
#391040=CARTESIAN_POINT('Ctrl Pts',(-0.659418052229592,2.62834063393786,
8.80838214965003));
#391041=CARTESIAN_POINT('Ctrl Pts',(-0.658001622475827,2.63407975346251,
8.8150136446199));
#391042=CARTESIAN_POINT('Ctrl Pts',(-0.649397808304885,2.63392745668914,
8.81722098428722));
#391043=CARTESIAN_POINT('Ctrl Pts',(-0.665128007518958,2.6052049183832,
8.82945683644723));
#391044=CARTESIAN_POINT('Ctrl Pts',(-0.663717145684714,2.6109214776958,
8.8360746990239));
#391045=CARTESIAN_POINT('Ctrl Pts',(-0.655143182195944,2.61078294036945,
8.83829567148519));
#391046=CARTESIAN_POINT('Ctrl Pts',(-0.670846486662627,2.58203466569847,
8.85049129520029));
#391047=CARTESIAN_POINT('Ctrl Pts',(-0.669447239426447,2.58770416474116,
8.85711686593485));
#391048=CARTESIAN_POINT('Ctrl Pts',(-0.660897934588195,2.58760342300925,
8.85933012996512));
#391049=CARTESIAN_POINT('Origin',(-0.641580116759695,2.64844927545893,8.78727029226991));
#391050=CARTESIAN_POINT('Ctrl Pts',(-0.650400330943802,2.66487874754017,
8.75374538247849));
#391051=CARTESIAN_POINT('Ctrl Pts',(-0.648592262248888,2.6722594836811,
8.75304829418602));
#391052=CARTESIAN_POINT('Ctrl Pts',(-0.64116393718024,2.6740175024192,8.75272238421917));
#391053=CARTESIAN_POINT('Ctrl Pts',(-0.650084046247546,2.66616027822844,
8.76769408445017));
#391054=CARTESIAN_POINT('Ctrl Pts',(-0.648229808234074,2.67372658223775,
8.76974318093967));
#391055=CARTESIAN_POINT('Ctrl Pts',(-0.640925106754231,2.67563961479641,
8.77077869880429));
#391056=CARTESIAN_POINT('Ctrl Pts',(-0.651705141439419,2.65959188196377,
8.78108014887993));
#391057=CARTESIAN_POINT('Ctrl Pts',(-0.650137431719988,2.66600495638529,
8.78639403366328));
#391058=CARTESIAN_POINT('Ctrl Pts',(-0.642152715147332,2.66733400754429,
8.78812224174742));
#391059=CARTESIAN_POINT('Ctrl Pts',(-0.654361758564352,2.64882773046581,
8.78944554828685));
#391060=CARTESIAN_POINT('Ctrl Pts',(-0.65304598855138,2.65423376106967,
8.79673892988685));
#391061=CARTESIAN_POINT('Ctrl Pts',(-0.644142204117176,2.65375818030292,
8.79894799272499));
#391062=CARTESIAN_POINT('Origin',(-0.638220125503587,2.66206335788655,8.75721825406948));
#391063=CARTESIAN_POINT('Origin',(-0.638220125503587,2.66206335788655,9.));
#391064=CARTESIAN_POINT('Origin',(-0.638220125503587,2.66206335788655,7.51860402984325));
#391065=CARTESIAN_POINT('Ctrl Pts',(-0.658718561459849,2.66617001169016,
7.50366195182966));
#391066=CARTESIAN_POINT('Ctrl Pts',(-0.659596893130796,2.66972506797464,
7.50000065167735));
#391067=CARTESIAN_POINT('Ctrl Pts',(-0.659596893130682,2.66972506797467,
7.49482233047108));
#391068=CARTESIAN_POINT('Ctrl Pts',(-0.652005683757179,2.66937798185144,
7.50215800491337));
#391069=CARTESIAN_POINT('Ctrl Pts',(-0.650341812920523,2.67201165438486,
7.49877273257265));
#391070=CARTESIAN_POINT('Ctrl Pts',(-0.646990465679397,2.67283968096613,
7.49481816995649));
#391071=CARTESIAN_POINT('Ctrl Pts',(-0.649680941710149,2.66779507605612,
7.51043025814042));
#391072=CARTESIAN_POINT('Ctrl Pts',(-0.646783717304557,2.67286447915024,
7.51006209594515));
#391073=CARTESIAN_POINT('Ctrl Pts',(-0.641131910556218,2.67421948861214,
7.507312818217));
#391074=CARTESIAN_POINT('Ctrl Pts',(-0.650356343923157,2.66505705167055,
7.51860402984326));
#391075=CARTESIAN_POINT('Ctrl Pts',(-0.648533957547067,2.67244487444096,
7.51860402984326));
#391076=CARTESIAN_POINT('Ctrl Pts',(-0.641134372652,2.67421889833352,7.51860402984327));
#391077=CARTESIAN_POINT('Origin',(0.,0.,7.5));
#391078=CARTESIAN_POINT('Origin',(-0.834899689636847,2.53374831658168,7.5));
#391079=CARTESIAN_POINT('',(-0.834899689636847,2.53374831658168,7.59394543036555));
#391080=CARTESIAN_POINT('',(-0.834899689636847,2.53374831658168,8.85049129520029));
#391081=CARTESIAN_POINT('',(-0.834899689636847,2.53374831658168,7.5));
#391082=CARTESIAN_POINT('',(-0.822251471860022,2.60411303347871,8.78727029226991));
#391083=CARTESIAN_POINT('Ctrl Pts',(-0.834899689636846,2.53374831658168,
8.85049129520029));
#391084=CARTESIAN_POINT('Ctrl Pts',(-0.830677488574754,2.55723731619084,
8.82945686509571));
#391085=CARTESIAN_POINT('Ctrl Pts',(-0.826461564325083,2.58069139656184,
8.80838212259895));
#391086=CARTESIAN_POINT('Ctrl Pts',(-0.822251471860022,2.60411303347871,
8.78727029226991));
#391087=CARTESIAN_POINT('',(-0.819770641322281,2.61791441969279,8.75721825406948));
#391088=CARTESIAN_POINT('Origin',(-0.827236519635746,2.57638129654181,8.75937679713087));
#391089=CARTESIAN_POINT('',(-0.819770641322281,2.61791441969279,7.51860402984325));
#391090=CARTESIAN_POINT('',(-0.819770641322281,2.61791441969279,7.5));
#391091=CARTESIAN_POINT('Ctrl Pts',(-0.819770641322281,2.61791441969279,
7.51860402984325));
#391092=CARTESIAN_POINT('Ctrl Pts',(-0.821718947867546,2.6070755773432,
7.52834476460825));
#391093=CARTESIAN_POINT('Ctrl Pts',(-0.823668519225313,2.59622969857358,
7.53807742314407));
#391094=CARTESIAN_POINT('Ctrl Pts',(-0.825619397863334,2.58537654712673,
7.54780169004674));
#391095=CARTESIAN_POINT('Ctrl Pts',(-0.828709484189964,2.56818574179771,
7.5632044032688));
#391096=CARTESIAN_POINT('Ctrl Pts',(-0.831802854243287,2.55097666840084,
7.57858609112103));
#391097=CARTESIAN_POINT('Ctrl Pts',(-0.834899689636846,2.53374831658168,
7.59394543036555));
#391098=CARTESIAN_POINT('Origin',(-1.04723789307865,2.71775565323223,7.5));
#391099=CARTESIAN_POINT('',(-0.908826823579954,2.58834572998874,8.75721825406948));
#391100=CARTESIAN_POINT('',(-0.898583897763448,2.57876892194511,8.78727029226991));
#391101=CARTESIAN_POINT('Origin',(-0.872583531620933,2.55445941115965,8.75658640621075));
#391102=CARTESIAN_POINT('',(-0.846361565593599,2.52994271156921,8.85049129520029));
#391103=CARTESIAN_POINT('Ctrl Pts',(-0.898583897763448,2.57876892194511,
8.78727029226991));
#391104=CARTESIAN_POINT('Ctrl Pts',(-0.881201144631306,2.56251660371118,
8.80838212259896));
#391105=CARTESIAN_POINT('Ctrl Pts',(-0.863794313055971,2.54624177290295,
8.82945686509571));
#391106=CARTESIAN_POINT('Ctrl Pts',(-0.846361565593599,2.52994271156921,
8.85049129520029));
#391107=CARTESIAN_POINT('',(-0.846361565593599,2.52994271156921,7.59394543036555));
#391108=CARTESIAN_POINT('',(-0.846361565593599,2.52994271156921,7.5));
#391109=CARTESIAN_POINT('',(-0.908826823579954,2.58834572998874,7.51860402984325));
#391110=CARTESIAN_POINT('Ctrl Pts',(-0.846361565593599,2.52994271156921,
7.59394543036555));
#391111=CARTESIAN_POINT('Ctrl Pts',(-0.859147870308727,2.54189749753933,
7.57858609112103));
#391112=CARTESIAN_POINT('Ctrl Pts',(-0.871919867225447,2.55383890617556,
7.56320440326857));
#391113=CARTESIAN_POINT('Ctrl Pts',(-0.884678306195266,2.56576763856503,
7.54780169004651));
#391114=CARTESIAN_POINT('Ctrl Pts',(-0.892733151079764,2.57329866091762,
7.53807742314383));
#391115=CARTESIAN_POINT('Ctrl Pts',(-0.900782598427383,2.58082463674585,
7.52834476460825));
#391116=CARTESIAN_POINT('Ctrl Pts',(-0.908826823579954,2.58834572998874,
7.51860402984325));
#391117=CARTESIAN_POINT('',(-0.908826823579954,2.58834572998874,7.5));
#391118=CARTESIAN_POINT('Origin',(-0.841666242052023,2.53496461975633,7.5));
#391119=CARTESIAN_POINT('Ctrl Pts',(-0.846361565593599,2.52994271156921,
8.85049129520029));
#391120=CARTESIAN_POINT('Ctrl Pts',(-0.846220103731476,2.52981044925243,
8.85097269580138));
#391121=CARTESIAN_POINT('Ctrl Pts',(-0.846074682046656,2.52968599986464,
8.85143669361005));
#391122=CARTESIAN_POINT('Ctrl Pts',(-0.845918035883981,2.52956429716701,
8.8519052845931));
#391123=CARTESIAN_POINT('Ctrl Pts',(-0.845611645923929,2.52932625440855,
8.85282181883899));
#391124=CARTESIAN_POINT('Ctrl Pts',(-0.845270075579119,2.52910499860578,
8.85372622499636));
#391125=CARTESIAN_POINT('Ctrl Pts',(-0.844879582374981,2.52890999884467,
8.85462257735071));
#391126=CARTESIAN_POINT('Ctrl Pts',(-0.844555408785914,2.52874811696874,
8.85536669723987));
#391127=CARTESIAN_POINT('Ctrl Pts',(-0.844197459081632,2.52860426486192,
8.85610498449051));
#391128=CARTESIAN_POINT('Ctrl Pts',(-0.843794856243075,2.52849127326612,
8.85681338218371));
#391129=CARTESIAN_POINT('Ctrl Pts',(-0.843429493534787,2.52838873321548,
8.85745625420284));
#391130=CARTESIAN_POINT('Ctrl Pts',(-0.843022934952048,2.52830974613276,
8.85808743050665));
#391131=CARTESIAN_POINT('Ctrl Pts',(-0.842558141777638,2.5282772800014,
8.85866804508409));
#391132=CARTESIAN_POINT('Ctrl Pts',(-0.842343696282442,2.52826230083217,
8.85893592806394));
#391133=CARTESIAN_POINT('Ctrl Pts',(-0.842116734248302,2.52825743506812,
8.85919241173848));
#391134=CARTESIAN_POINT('Ctrl Pts',(-0.841874992353034,2.52826642160604,
8.85943017985534));
#391135=CARTESIAN_POINT('Ctrl Pts',(-0.841548569231167,2.52827855609253,
8.8597512372));
#391136=CARTESIAN_POINT('Ctrl Pts',(-0.841186913474445,2.52831689643642,
8.86004599534705));
#391137=CARTESIAN_POINT('Ctrl Pts',(-0.840795468227052,2.52839133904788,
8.86026130871721));
#391138=CARTESIAN_POINT('Ctrl Pts',(-0.840652149085971,2.5284185945867,
8.86034014101235));
#391139=CARTESIAN_POINT('Ctrl Pts',(-0.840502681555613,2.52845108692915,
8.86040910639693));
#391140=CARTESIAN_POINT('Ctrl Pts',(-0.840351209250492,2.5284882595412,
8.86046313645507));
#391141=CARTESIAN_POINT('Ctrl Pts',(-0.84011483798692,2.52854626709098,
8.8605474499083));
#391142=CARTESIAN_POINT('Ctrl Pts',(-0.839867167649129,2.52861739795952,
8.86059655985668));
#391143=CARTESIAN_POINT('Ctrl Pts',(-0.83962400122166,2.52869680873284,
8.86059725258816));
#391144=CARTESIAN_POINT('Ctrl Pts',(-0.839380272982597,2.52877640297678,
8.86059794692011));
#391145=CARTESIAN_POINT('Ctrl Pts',(-0.839139191271967,2.52886772364965,
8.86056369958366));
#391146=CARTESIAN_POINT('Ctrl Pts',(-0.838912571788404,2.52896227098935,
8.86048590497774));
#391147=CARTESIAN_POINT('Ctrl Pts',(-0.83885343085047,2.52898694503,8.86046560290182));
#391148=CARTESIAN_POINT('Ctrl Pts',(-0.83879454035585,2.52901224341473,
8.86044257503091));
#391149=CARTESIAN_POINT('Ctrl Pts',(-0.838737707112935,2.52903735424157,
8.86041778462583));
#391150=CARTESIAN_POINT('Ctrl Pts',(-0.838355289912295,2.52920631894626,
8.86025097596201));
#391151=CARTESIAN_POINT('Ctrl Pts',(-0.838014836059358,2.52938976813877,
8.8599848982295));
#391152=CARTESIAN_POINT('Ctrl Pts',(-0.837722263530337,2.52957488880751,
8.85968173251461));
#391153=CARTESIAN_POINT('Ctrl Pts',(-0.837567509424893,2.52967280703512,
8.85952137522076));
#391154=CARTESIAN_POINT('Ctrl Pts',(-0.837423066472652,2.52977291898359,
8.85934740853961));
#391155=CARTESIAN_POINT('Ctrl Pts',(-0.837290086096403,2.52987253518028,
8.8591675900182));
#391156=CARTESIAN_POINT('Ctrl Pts',(-0.83675610076393,2.53027254598949,
8.85844552518694));
#391157=CARTESIAN_POINT('Ctrl Pts',(-0.836374948810151,2.53068474902438,
8.85759444184122));
#391158=CARTESIAN_POINT('Ctrl Pts',(-0.836094365694028,2.53104875090688,
8.85683498915136));
#391159=CARTESIAN_POINT('Ctrl Pts',(-0.836065003418184,2.53108684273446,
8.85675551444996));
#391160=CARTESIAN_POINT('Ctrl Pts',(-0.836036760374309,2.53112441556681,
8.8566769979365));
#391161=CARTESIAN_POINT('Ctrl Pts',(-0.836009588723119,2.53116140540471,
8.85659965593547));
#391162=CARTESIAN_POINT('Ctrl Pts',(-0.835642824388812,2.53166069612429,
8.85555568965886));
#391163=CARTESIAN_POINT('Ctrl Pts',(-0.835362448600052,2.53219351346654,
8.85434650606346));
#391164=CARTESIAN_POINT('Ctrl Pts',(-0.835161575571254,2.53275959732745,
8.85297329937117));
#391165=CARTESIAN_POINT('Ctrl Pts',(-0.835048596731928,2.53307798500721,
8.85220095427747));
#391166=CARTESIAN_POINT('Ctrl Pts',(-0.834961018414379,2.53340713159065,
8.85137579139183));
#391167=CARTESIAN_POINT('Ctrl Pts',(-0.834899689636846,2.53374831658168,
8.85049129520029));
#391168=CARTESIAN_POINT('Origin',(-0.841666242052023,2.53496461975633,7.59394543036555));
#391169=CARTESIAN_POINT('Ctrl Pts',(-0.845950854086149,2.52955870944534,
7.59443877723642));
#391170=CARTESIAN_POINT('Ctrl Pts',(-0.841720920735426,2.52560385704643,
7.58783886950016));
#391171=CARTESIAN_POINT('Ctrl Pts',(-0.834645065059042,2.53029549300669,
7.58559994247159));
#391172=CARTESIAN_POINT('Ctrl Pts',(-0.869041936146755,2.55114813266051,
7.56670252222133));
#391173=CARTESIAN_POINT('Ctrl Pts',(-0.864818116250629,2.54719899614617,
7.56004874999029));
#391174=CARTESIAN_POINT('Ctrl Pts',(-0.857688526813971,2.55190062477046,
7.55786368756704));
#391175=CARTESIAN_POINT('Ctrl Pts',(-0.892089897918728,2.57269723978491,
7.53888913333557));
#391176=CARTESIAN_POINT('Ctrl Pts',(-0.887840975654134,2.56872463335888,
7.53222002137276));
#391177=CARTESIAN_POINT('Ctrl Pts',(-0.880690571396409,2.57346532567864,
7.53005029815327));
#391178=CARTESIAN_POINT('Ctrl Pts',(-0.915093696466157,2.59420505570682,
7.51101258149734));
#391179=CARTESIAN_POINT('Ctrl Pts',(-0.910793269543249,2.59018429407248,
7.5043616886572));
#391180=CARTESIAN_POINT('Ctrl Pts',(-0.903650005808575,2.59498859056224,
7.50217374673251));
#391181=CARTESIAN_POINT('',(-0.90242486159829,2.59384008075031,7.50366116523517));
#391182=CARTESIAN_POINT('Ctrl Pts',(-0.908826823579954,2.58834572998874,
7.51860402984325));
#391183=CARTESIAN_POINT('Ctrl Pts',(-0.909149402631498,2.58864733108503,
7.51734760759494));
#391184=CARTESIAN_POINT('Ctrl Pts',(-0.909400265220373,2.58896333080256,
7.51608817408573));
#391185=CARTESIAN_POINT('Ctrl Pts',(-0.909568375706159,2.5893013051321,
7.5148100591312));
#391186=CARTESIAN_POINT('Ctrl Pts',(-0.909720654201314,2.58960745035595,
7.51365231206384));
#391187=CARTESIAN_POINT('Ctrl Pts',(-0.909805471833573,2.58993194624439,
7.51247773061042));
#391188=CARTESIAN_POINT('Ctrl Pts',(-0.909785636131764,2.59027851570742,
7.51129758471022));
#391189=CARTESIAN_POINT('Ctrl Pts',(-0.909760982619738,2.59070926197024,
7.50983079813401));
#391190=CARTESIAN_POINT('Ctrl Pts',(-0.909562447760712,2.59115961536516,
7.50839324291155));
#391191=CARTESIAN_POINT('Ctrl Pts',(-0.909113147813114,2.59159960789671,
7.50715379678855));
#391192=CARTESIAN_POINT('Ctrl Pts',(-0.908905584183591,2.5918028717682,
7.50658120839351));
#391193=CARTESIAN_POINT('Ctrl Pts',(-0.908608347826955,2.59202603157119,
7.50598221009429));
#391194=CARTESIAN_POINT('Ctrl Pts',(-0.908214855547661,2.59224558605754,
7.50545747549611));
#391195=CARTESIAN_POINT('Ctrl Pts',(-0.908004875887704,2.5923627471273,
7.50517746087247));
#391196=CARTESIAN_POINT('Ctrl Pts',(-0.907765307937747,2.59248032881999,
7.50491486231392));
#391197=CARTESIAN_POINT('Ctrl Pts',(-0.90750176093356,2.59259371998976,
7.50468370960992));
#391198=CARTESIAN_POINT('Ctrl Pts',(-0.907107675031109,2.59276327555579,
7.50433806340446));
#391199=CARTESIAN_POINT('Ctrl Pts',(-0.906647935572111,2.59292803421731,
7.50405484070983));
#391200=CARTESIAN_POINT('Ctrl Pts',(-0.906153263468371,2.59307622538894,
7.50385766036131));
#391201=CARTESIAN_POINT('Ctrl Pts',(-0.906100365975824,2.59309207213133,
7.50383657498791));
#391202=CARTESIAN_POINT('Ctrl Pts',(-0.906047096562114,2.5931077362333,
7.50381643264937));
#391203=CARTESIAN_POINT('Ctrl Pts',(-0.905993512717869,2.59312320855993,
7.50379723213559));
#391204=CARTESIAN_POINT('Ctrl Pts',(-0.905635823029025,2.59322649140151,
7.50366906242519));
#391205=CARTESIAN_POINT('Ctrl Pts',(-0.905256142261181,2.59332278454905,
7.50358235568538));
#391206=CARTESIAN_POINT('Ctrl Pts',(-0.904887945654168,2.59340680223421,
7.5035341175365));
#391207=CARTESIAN_POINT('Ctrl Pts',(-0.904335876513762,2.59353277724415,
7.50346178989176));
#391208=CARTESIAN_POINT('Ctrl Pts',(-0.90373661943572,2.5936448243463,7.50346967198527));
#391209=CARTESIAN_POINT('Ctrl Pts',(-0.903144950082889,2.59373671834597,
7.50354272648692));
#391210=CARTESIAN_POINT('Ctrl Pts',(-0.902901584231239,2.59377451625012,
7.50357277531559));
#391211=CARTESIAN_POINT('Ctrl Pts',(-0.90265984722218,2.59380899445341,
7.50361331098761));
#391212=CARTESIAN_POINT('Ctrl Pts',(-0.902424861598756,2.59384008075165,
7.50366116523658));
#391213=CARTESIAN_POINT('',(-0.842588855338633,2.53774338397776,7.57603338622103));
#391214=CARTESIAN_POINT('Origin',(-0.845370739448621,2.54613103027419,7.58486873427628));
#391215=CARTESIAN_POINT('Ctrl Pts',(-0.902424861643609,2.59384008078545,
7.50366116529969));
#391216=CARTESIAN_POINT('Ctrl Pts',(-0.882511501228924,2.57517230438344,
7.52783573079709));
#391217=CARTESIAN_POINT('Ctrl Pts',(-0.86256709527385,2.55647430140459,
7.55196141284068));
#391218=CARTESIAN_POINT('Ctrl Pts',(-0.842588856456727,2.53774338454124,
7.57603338728831));
#391219=CARTESIAN_POINT('Ctrl Pts',(-0.846992701390066,2.53077349621443,
7.5963967733137));
#391220=CARTESIAN_POINT('Ctrl Pts',(-0.835256263707593,2.51565878627362,
7.59974925422226));
#391221=CARTESIAN_POINT('Ctrl Pts',(-0.834890789857186,2.53479160767911,
7.59639677331372));
#391222=CARTESIAN_POINT('Ctrl Pts',(-0.845126734807296,2.5273481096967,
7.58707626057421));
#391223=CARTESIAN_POINT('Ctrl Pts',(-0.83850328661769,2.52543830193637,
7.58811717123966));
#391224=CARTESIAN_POINT('Ctrl Pts',(-0.834337441147403,2.53093040200096,
7.58707626057424));
#391225=CARTESIAN_POINT('Ctrl Pts',(-0.843334199200213,2.53315435188585,
7.58015376756929));
#391226=CARTESIAN_POINT('Ctrl Pts',(-0.840681119793224,2.53199758847089,
7.58208760766041));
#391227=CARTESIAN_POINT('Ctrl Pts',(-0.839246778196377,2.53451146916044,
7.58015376756931));
#391228=CARTESIAN_POINT('Ctrl Pts',(-0.842588855078052,2.53774338319229,
7.57603338509286));
#391229=CARTESIAN_POINT('Ctrl Pts',(-0.842588855078052,2.53774338319228,
7.57603338509286));
#391230=CARTESIAN_POINT('Ctrl Pts',(-0.842588855078052,2.53774338319228,
7.57603338509286));
#391231=CARTESIAN_POINT('Origin',(-0.845376155095137,2.54612923215639,7.58486873427622));
#391232=CARTESIAN_POINT('Ctrl Pts',(-0.818248011214828,2.62638513377601,
7.51098857897448));
#391233=CARTESIAN_POINT('Ctrl Pts',(-0.819289576806582,2.62059068357862,
7.50433767179956));
#391234=CARTESIAN_POINT('Ctrl Pts',(-0.827887819808971,2.62016846520583,
7.50214974420965));
#391235=CARTESIAN_POINT('Ctrl Pts',(-0.823821120043175,2.5953807478726,
7.53887321589169));
#391236=CARTESIAN_POINT('Ctrl Pts',(-0.824850205830686,2.58965572547187,
7.53220407452063));
#391237=CARTESIAN_POINT('Ctrl Pts',(-0.833416122259817,2.58917823657006,
7.53003438070911));
#391238=CARTESIAN_POINT('Ctrl Pts',(-0.829404931296306,2.56431682211122,
7.56669465659236));
#391239=CARTESIAN_POINT('Ctrl Pts',(-0.830427935378131,2.55862563352851,
7.56004085833303));
#391240=CARTESIAN_POINT('Ctrl Pts',(-0.838953795137743,2.55812928134927,
7.55785582193789));
#391241=CARTESIAN_POINT('Ctrl Pts',(-0.834999192440797,2.53319476138884,
7.59443891967696));
#391242=CARTESIAN_POINT('Ctrl Pts',(-0.836023679751188,2.52749532129126,
7.58783901202978));
#391243=CARTESIAN_POINT('Ctrl Pts',(-0.844500483535585,2.52702311838028,
7.58560008491213));
#391244=CARTESIAN_POINT('',(-0.828187489909775,2.61848858635939,7.50366116523517));
#391245=CARTESIAN_POINT('Ctrl Pts',(-0.828187489909887,2.61848858635975,
7.50366116523554));
#391246=CARTESIAN_POINT('Ctrl Pts',(-0.827525969191743,2.61885808312053,
7.50350835821027));
#391247=CARTESIAN_POINT('Ctrl Pts',(-0.826905849903686,2.61917621843722,
7.50345484956));
#391248=CARTESIAN_POINT('Ctrl Pts',(-0.82630896949968,2.61945298502425,
7.50349758195598));
#391249=CARTESIAN_POINT('Ctrl Pts',(-0.82600272558662,2.61959498680894,
7.50351950684424));
#391250=CARTESIAN_POINT('Ctrl Pts',(-0.825672469016687,2.61974021217986,
7.50357029184312));
#391251=CARTESIAN_POINT('Ctrl Pts',(-0.825350157004209,2.61987149743227,
7.50365515313923));
#391252=CARTESIAN_POINT('Ctrl Pts',(-0.824854310611997,2.62007346731311,
7.50378570417639));
#391253=CARTESIAN_POINT('Ctrl Pts',(-0.824362842393527,2.62024869536167,
7.50400001621911));
#391254=CARTESIAN_POINT('Ctrl Pts',(-0.823912397737656,2.62038170562562,
7.50428903009634));
#391255=CARTESIAN_POINT('Ctrl Pts',(-0.823862401846368,2.6203964687416,
7.50432110841318));
#391256=CARTESIAN_POINT('Ctrl Pts',(-0.823812892273582,2.62041073533622,
7.50435406373354));
#391257=CARTESIAN_POINT('Ctrl Pts',(-0.823763904819404,2.62042450145568,
7.50438785222352));
#391258=CARTESIAN_POINT('Ctrl Pts',(-0.823464812865288,2.62050855023184,
7.50459414719561));
#391259=CARTESIAN_POINT('Ctrl Pts',(-0.823180282494868,2.62057478447335,
7.50483629897752));
#391260=CARTESIAN_POINT('Ctrl Pts',(-0.822921512356893,2.62062194852716,
7.5050991045531));
#391261=CARTESIAN_POINT('Ctrl Pts',(-0.822350639441519,2.62072599716703,
7.50567888004914));
#391262=CARTESIAN_POINT('Ctrl Pts',(-0.821882736099741,2.6207418454673,
7.50637912803144));
#391263=CARTESIAN_POINT('Ctrl Pts',(-0.821510747489513,2.62069958740677,
7.50710440483569));
#391264=CARTESIAN_POINT('Ctrl Pts',(-0.821419528497277,2.62068922489138,
7.50728225710685));
#391265=CARTESIAN_POINT('Ctrl Pts',(-0.821332244757601,2.62067530700927,
7.50746498566954));
#391266=CARTESIAN_POINT('Ctrl Pts',(-0.821250868156063,2.62065857004476,
7.50764697238949));
#391267=CARTESIAN_POINT('Ctrl Pts',(-0.820813409941643,2.62056859672971,
7.50862528291181));
#391268=CARTESIAN_POINT('Ctrl Pts',(-0.820506113419823,2.62039304298327,
7.50965856837421));
#391269=CARTESIAN_POINT('Ctrl Pts',(-0.820281832715801,2.62017852063153,
7.51067959873201));
#391270=CARTESIAN_POINT('Ctrl Pts',(-0.820158410761484,2.62006046871078,
7.51124147302578));
#391271=CARTESIAN_POINT('Ctrl Pts',(-0.820060398756836,2.61993027313355,
7.51180065547253));
#391272=CARTESIAN_POINT('Ctrl Pts',(-0.819981887633053,2.61979380879741,
7.51235175716501));
#391273=CARTESIAN_POINT('Ctrl Pts',(-0.819710600425269,2.61932227015509,
7.51425603304536));
#391274=CARTESIAN_POINT('Ctrl Pts',(-0.819645060131577,2.61871663751267,
7.5162690050518));
#391275=CARTESIAN_POINT('Ctrl Pts',(-0.819751779838985,2.61802712335916,
7.51827788969244));
#391276=CARTESIAN_POINT('Ctrl Pts',(-0.819757555711223,2.61798980555018,
7.51838661432545));
#391277=CARTESIAN_POINT('Ctrl Pts',(-0.819763843816357,2.61795223565928,
7.51849533314857));
#391278=CARTESIAN_POINT('Ctrl Pts',(-0.819770641322276,2.61791441969279,
7.51860402984325));
#391279=CARTESIAN_POINT('Ctrl Pts',(-0.842588854779748,2.53774338509929,
7.57603338728985));
#391280=CARTESIAN_POINT('Ctrl Pts',(-0.837781180671465,2.56470379204691,
7.55196141284922));
#391281=CARTESIAN_POINT('Ctrl Pts',(-0.83298093453604,2.59161758558424,
7.52783573083105));
#391282=CARTESIAN_POINT('Ctrl Pts',(-0.828187489894076,2.61848858641645,
7.50366116530176));
#391283=CARTESIAN_POINT('Origin',(-2.91153398701378E-16,8.76907647894215E-16,
7.49482233047033));
#391284=CARTESIAN_POINT('Origin',(-0.89952049155539,2.58549204896707,7.49482233047033));
#391285=CARTESIAN_POINT('Origin',(0.,0.,7.50366116523517));
#391286=CARTESIAN_POINT('Origin',(-0.825522045906671,2.61006122566542,7.49482233047033));
#391287=CARTESIAN_POINT('Ctrl Pts',(-0.908826050988833,2.58834500757949,
7.51860402984325));
#391288=CARTESIAN_POINT('Ctrl Pts',(-0.914383648054351,2.59354206452428,
7.51860402984325));
#391289=CARTESIAN_POINT('Ctrl Pts',(-0.921552651160824,2.59099222521768,
7.51860402984325));
#391290=CARTESIAN_POINT('Ctrl Pts',(-0.910889625574214,2.59027470936151,
7.51041458714365));
#391291=CARTESIAN_POINT('Ctrl Pts',(-0.916082063685368,2.59293796906007,
7.5100464290044));
#391292=CARTESIAN_POINT('Ctrl Pts',(-0.921554628286757,2.59099152200228,
7.50729136483008));
#391293=CARTESIAN_POINT('Ctrl Pts',(-0.909794269111079,2.59286776381869,
7.50215815450138));
#391294=CARTESIAN_POINT('Ctrl Pts',(-0.912623967034531,2.59416809998427,
7.49877163671533));
#391295=CARTESIAN_POINT('Ctrl Pts',(-0.915882595552381,2.59303440523831,
7.49481588533172));
#391296=CARTESIAN_POINT('Ctrl Pts',(-0.902424680702047,2.59383956080162,
7.50366171572174));
#391297=CARTESIAN_POINT('Ctrl Pts',(-0.903627891059845,2.59729794873417,
7.50000045605858));
#391298=CARTESIAN_POINT('Ctrl Pts',(-0.903627891059962,2.59729794873413,
7.49482233047317));
#391299=CARTESIAN_POINT('Origin',(-0.917363775473728,2.57921498783033,7.51860402984325));
#391300=CARTESIAN_POINT('Origin',(-0.917363775473728,2.57921498783033,9.));
#391301=CARTESIAN_POINT('Origin',(-0.917363775473728,2.57921498783033,8.75721825406948));
#391302=CARTESIAN_POINT('Ctrl Pts',(-0.896628055005675,2.57694023016137,
8.78942910404912));
#391303=CARTESIAN_POINT('Ctrl Pts',(-0.900684690092687,2.58076071972064,
8.7967269950169));
#391304=CARTESIAN_POINT('Ctrl Pts',(-0.907893560589471,2.57549710193981,
8.79893251111266));
#391305=CARTESIAN_POINT('Ctrl Pts',(-0.904658967512578,2.58444888270675,
8.78111911759583));
#391306=CARTESIAN_POINT('Ctrl Pts',(-0.909473258913838,2.58897269840029,
8.78644465894814));
#391307=CARTESIAN_POINT('Ctrl Pts',(-0.916893176767939,2.58570768219607,
8.78817647674132));
#391308=CARTESIAN_POINT('Ctrl Pts',(-0.909664023763931,2.58912845404803,
8.76780923932029));
#391309=CARTESIAN_POINT('Ctrl Pts',(-0.915350580979807,2.59446491390463,
8.76988516158373));
#391310=CARTESIAN_POINT('Ctrl Pts',(-0.922522564001194,2.59207764769887,
8.77093053738833));
#391311=CARTESIAN_POINT('Ctrl Pts',(-0.908688106295119,2.58821600167966,
8.75371302330492));
#391312=CARTESIAN_POINT('Ctrl Pts',(-0.914234575915404,2.59342204394984,
8.7530082828756));
#391313=CARTESIAN_POINT('Ctrl Pts',(-0.921424947711518,2.59083494272108,
8.75267964240738));
#391314=CARTESIAN_POINT('Origin',(-0.907120849657222,2.5696381797867,8.78727029226991));
#391315=CARTESIAN_POINT('Ctrl Pts',(-0.846361565593599,2.52994271156921,
8.85049129520029));
#391316=CARTESIAN_POINT('Ctrl Pts',(-0.850627167658214,2.53393091307483,
8.85711686593484));
#391317=CARTESIAN_POINT('Ctrl Pts',(-0.857737280217481,2.52918253845729,
8.85933012996512));
#391318=CARTESIAN_POINT('Ctrl Pts',(-0.86379433645136,2.54624179477689,
8.82945683644721));
#391319=CARTESIAN_POINT('Ctrl Pts',(-0.868095345592135,2.55026310076633,
8.83607469902388));
#391320=CARTESIAN_POINT('Ctrl Pts',(-0.875205505457216,2.5454695979562,
8.8382956714852));
#391321=CARTESIAN_POINT('Ctrl Pts',(-0.88120112235839,2.56251658288671,
8.80838214965003));
#391322=CARTESIAN_POINT('Ctrl Pts',(-0.88551910528938,2.5665537588271,8.81501364461992));
#391323=CARTESIAN_POINT('Ctrl Pts',(-0.892646776397508,2.56173243979915,
8.81722098428721));
#391324=CARTESIAN_POINT('Ctrl Pts',(-0.898583897763448,2.57876892194511,
8.78727029226991));
#391325=CARTESIAN_POINT('Ctrl Pts',(-0.902902597925556,2.58280676847367,
8.79393457792714));
#391326=CARTESIAN_POINT('Ctrl Pts',(-0.910063138901412,2.57797292237441,
8.79610912703474));
#391327=CARTESIAN_POINT('Origin',(-0.854898517487372,2.52081196941079,8.85049129520029));
#391328=CARTESIAN_POINT('Ctrl Pts',(-0.834899689636846,2.53374831658168,
8.85049129520029));
#391329=CARTESIAN_POINT('Ctrl Pts',(-0.833866563355028,2.53949581710877,
8.85711686593484));
#391330=CARTESIAN_POINT('Ctrl Pts',(-0.825328369435551,2.53994303820322,
8.85933012996512));
#391331=CARTESIAN_POINT('Ctrl Pts',(-0.835813681545036,2.52866358583141,
8.86332496987232));
#391332=CARTESIAN_POINT('Ctrl Pts',(-0.831525412631142,2.5303848191389,
8.86648636486736));
#391333=CARTESIAN_POINT('Ctrl Pts',(-0.827902161459403,2.52572132765298,
8.87206031107457));
#391334=CARTESIAN_POINT('Ctrl Pts',(-0.842562205427849,2.52639043132742,
8.86341338519876));
#391335=CARTESIAN_POINT('Ctrl Pts',(-0.847033380520176,2.52517303084768,
8.86654584966058));
#391336=CARTESIAN_POINT('Ctrl Pts',(-0.847088807956552,2.5192467267223,
8.87215952290714));
#391337=CARTESIAN_POINT('Ctrl Pts',(-0.846361565593598,2.52994271156921,
8.85049129520029));
#391338=CARTESIAN_POINT('Ctrl Pts',(-0.850627167658214,2.53393091307483,
8.85711686593484));
#391339=CARTESIAN_POINT('Ctrl Pts',(-0.857737280217481,2.52918253845729,
8.85933012996512));
#391340=CARTESIAN_POINT('Origin',(-0.822596867063799,2.53153685626413,8.85049129520029));
#391341=CARTESIAN_POINT('Ctrl Pts',(-0.822251471860022,2.60411303347871,
8.78727029226991));
#391342=CARTESIAN_POINT('Ctrl Pts',(-0.821205485250586,2.60993207873471,
8.79393457792714));
#391343=CARTESIAN_POINT('Ctrl Pts',(-0.812575755917853,2.61034096358642,
8.79610912703474));
#391344=CARTESIAN_POINT('Ctrl Pts',(-0.826461569719569,2.58069136655117,
8.80838214965001));
#391345=CARTESIAN_POINT('Ctrl Pts',(-0.825415756823086,2.58650944540515,
8.81501364461989));
#391346=CARTESIAN_POINT('Ctrl Pts',(-0.816819862423338,2.58690870980846,
8.81722098428721));
#391347=CARTESIAN_POINT('Ctrl Pts',(-0.830677482908405,2.55723734771395,
8.82945683644722));
#391348=CARTESIAN_POINT('Ctrl Pts',(-0.829635781053811,2.5630325559704,
8.83607469902387));
#391349=CARTESIAN_POINT('Ctrl Pts',(-0.821070557575604,2.5634436390107,
8.8382956714852));
#391350=CARTESIAN_POINT('Ctrl Pts',(-0.834899689636846,2.53374831658168,
8.85049129520029));
#391351=CARTESIAN_POINT('Ctrl Pts',(-0.833866563355028,2.53949581710877,
8.85711686593484));
#391352=CARTESIAN_POINT('Ctrl Pts',(-0.825328369435551,2.53994303820322,
8.85933012996512));
#391353=CARTESIAN_POINT('Origin',(-0.809948649286974,2.60190157316116,8.78727029226991));
#391354=CARTESIAN_POINT('Ctrl Pts',(-0.819803381285488,2.6177321760669,
8.75374538247848));
#391355=CARTESIAN_POINT('Ctrl Pts',(-0.818471912849787,2.62521359105287,
8.75304829418602));
#391356=CARTESIAN_POINT('Ctrl Pts',(-0.811171486718964,2.62744393217416,
8.75272238421917));
#391357=CARTESIAN_POINT('Ctrl Pts',(-0.819569854383168,2.619031338143,8.76769408445017));
#391358=CARTESIAN_POINT('Ctrl Pts',(-0.818204200862884,2.62670089780666,
8.76974318093968));
#391359=CARTESIAN_POINT('Ctrl Pts',(-0.811037076092511,2.62907801366546,
8.7707786988043));
#391360=CARTESIAN_POINT('Ctrl Pts',(-0.820766780267511,2.61237257342735,
8.78108014887993));
#391361=CARTESIAN_POINT('Ctrl Pts',(-0.819613178664776,2.61887291500626,
8.78639403366327));
#391362=CARTESIAN_POINT('Ctrl Pts',(-0.811730020148806,2.62071081803442,
8.78812224174741));
#391363=CARTESIAN_POINT('Ctrl Pts',(-0.82272827753326,2.6014603279895,8.78944554828685));
#391364=CARTESIAN_POINT('Ctrl Pts',(-0.821761576480904,2.60693955299787,
8.79673892988685));
#391365=CARTESIAN_POINT('Ctrl Pts',(-0.812845615262405,2.60703541679017,
8.79894799272499));
#391366=CARTESIAN_POINT('Origin',(-0.807467818749233,2.61570295937524,8.75721825406948));
#391367=CARTESIAN_POINT('Origin',(-0.807467818749233,2.61570295937524,9.));
#391368=CARTESIAN_POINT('Origin',(-0.807467818749233,2.61570295937524,7.51860402984325));
#391369=CARTESIAN_POINT('Ctrl Pts',(-0.828187252682954,2.61848783631719,
7.50366195182966));
#391370=CARTESIAN_POINT('Ctrl Pts',(-0.829291552965473,2.62197931345389,
7.50000065167735));
#391371=CARTESIAN_POINT('Ctrl Pts',(-0.829291552965362,2.62197931345392,
7.49482233047108));
#391372=CARTESIAN_POINT('Ctrl Pts',(-0.821693702661397,2.62211931091084,
7.50215800491337));
#391373=CARTESIAN_POINT('Ctrl Pts',(-0.820201990404399,2.6248541768521,
7.49877273257267));
#391374=CARTESIAN_POINT('Ctrl Pts',(-0.816910580710811,2.62589522371893,
7.49481816995647));
#391375=CARTESIAN_POINT('Ctrl Pts',(-0.819272319923723,2.62068860409958,
7.51043025814042));
#391376=CARTESIAN_POINT('Ctrl Pts',(-0.816705845947807,2.62593321736633,
7.51006209594514));
#391377=CARTESIAN_POINT('Ctrl Pts',(-0.811152467196909,2.62764755531765,
7.50731281821701));
#391378=CARTESIAN_POINT('Ctrl Pts',(-0.81977090862575,2.61791293211042,
7.51860402984326));
#391379=CARTESIAN_POINT('Ctrl Pts',(-0.818425605967999,2.6254023365026,
7.51860402984327));
#391380=CARTESIAN_POINT('Ctrl Pts',(-0.811154886414749,2.62764680850481,
7.51860402984327));
#391381=CARTESIAN_POINT('Origin',(0.,0.,7.5));
#391382=CARTESIAN_POINT('Origin',(-0.995522110700926,2.47505025214474,7.5));
#391383=CARTESIAN_POINT('',(-0.995522110700926,2.47505025214474,7.59394543036555));
#391384=CARTESIAN_POINT('',(-0.995522110700926,2.47505025214474,8.85049129520029));
#391385=CARTESIAN_POINT('',(-0.995522110700926,2.47505025214474,7.5));
#391386=CARTESIAN_POINT('',(-0.987408162934515,2.54608077127965,8.78727029226991));
#391387=CARTESIAN_POINT('Ctrl Pts',(-0.995522110700926,2.47505025214474,
8.85049129520029));
#391388=CARTESIAN_POINT('Ctrl Pts',(-0.992813529975832,2.49876150843588,
8.82945686509571));
#391389=CARTESIAN_POINT('Ctrl Pts',(-0.990108975883502,2.52243751507741,
8.80838212259896));
#391390=CARTESIAN_POINT('Ctrl Pts',(-0.987408162934515,2.54608077127965,
8.78727029226991));
#391391=CARTESIAN_POINT('',(-0.985816687379956,2.56001274842384,8.75721825406948));
#391392=CARTESIAN_POINT('Origin',(-0.990606189908908,2.51808661906322,8.75937679713101));
#391393=CARTESIAN_POINT('',(-0.985816687379956,2.56001274842384,7.51860402984325));
#391394=CARTESIAN_POINT('',(-0.985816687379956,2.56001274842384,7.5));
#391395=CARTESIAN_POINT('Ctrl Pts',(-0.985816687379956,2.56001274842384,
7.51860402984325));
#391396=CARTESIAN_POINT('Ctrl Pts',(-0.987066543906795,2.54907134720938,
7.52834476460825));
#391397=CARTESIAN_POINT('Ctrl Pts',(-0.988317211822463,2.53812284299514,
7.53807742314407));
#391398=CARTESIAN_POINT('Ctrl Pts',(-0.989568718370407,2.52716699728844,
7.54780169004674));
#391399=CARTESIAN_POINT('Ctrl Pts',(-0.991551037104193,2.50981352980197,
7.5632044032688));
#391400=CARTESIAN_POINT('Ctrl Pts',(-0.993535462378776,2.49244162139227,
7.57858609112103));
#391401=CARTESIAN_POINT('Ctrl Pts',(-0.995522110700926,2.47505025214474,
7.59394543036555));
#391402=CARTESIAN_POINT('Origin',(-1.21921343306782,2.6450749705826,7.5));
#391403=CARTESIAN_POINT('',(-1.07279542170606,2.52479896157613,8.75721825406948));
#391404=CARTESIAN_POINT('',(-1.06195995288112,2.51589809662204,8.78727029226991));
#391405=CARTESIAN_POINT('Origin',(-1.03445549157308,2.49330438150983,8.7565864062095));
#391406=CARTESIAN_POINT('',(-1.00671661105393,2.47051810124198,8.85049129520029));
#391407=CARTESIAN_POINT('Ctrl Pts',(-1.06195995288112,2.51589809662204,
8.78727029226991));
#391408=CARTESIAN_POINT('Ctrl Pts',(-1.04357162487513,2.50079288733602,
8.80838212259895));
#391409=CARTESIAN_POINT('Ctrl Pts',(-1.02515782551212,2.48566675444137,
8.82945686509571));
#391410=CARTESIAN_POINT('Ctrl Pts',(-1.00671661105393,2.47051810124198,
8.85049129520029));
#391411=CARTESIAN_POINT('',(-1.00671661105393,2.47051810124198,7.59394543036555));
#391412=CARTESIAN_POINT('',(-1.00671661105393,2.47051810124198,7.5));
#391413=CARTESIAN_POINT('',(-1.07279542170606,2.52479896157613,7.51860402984325));
#391414=CARTESIAN_POINT('Ctrl Pts',(-1.00671661105393,2.47051810124198,
7.59394543036555));
#391415=CARTESIAN_POINT('Ctrl Pts',(-1.02024259070162,2.48162910346634,
7.57858609112103));
#391416=CARTESIAN_POINT('Ctrl Pts',(-1.03375343485909,2.49272767254577,
7.56320440326857));
#391417=CARTESIAN_POINT('Ctrl Pts',(-1.04724993675599,2.50381446008379,
7.54780169004651));
#391418=CARTESIAN_POINT('Ctrl Pts',(-1.05577074635661,2.5108139334596,7.53807742314383));
#391419=CARTESIAN_POINT('Ctrl Pts',(-1.06428584617823,2.51780871650104,
7.52834476460825));
#391420=CARTESIAN_POINT('Ctrl Pts',(-1.07279542170605,2.52479896157613,
7.51860402984324));
#391421=CARTESIAN_POINT('',(-1.07279542170606,2.52479896157613,7.5));
#391422=CARTESIAN_POINT('Origin',(-1.00235268932042,2.47583052179233,7.5));
#391423=CARTESIAN_POINT('Ctrl Pts',(-1.00671661105393,2.47051810124198,
8.85049129520029));
#391424=CARTESIAN_POINT('Ctrl Pts',(-1.00656696576465,2.47039517416494,
8.85097269580138));
#391425=CARTESIAN_POINT('Ctrl Pts',(-1.00641386936462,2.47028029767111,
8.85143669361005));
#391426=CARTESIAN_POINT('Ctrl Pts',(-1.00624974752968,2.47016888137882,
8.8519052845931));
#391427=CARTESIAN_POINT('Ctrl Pts',(-1.00592873562876,2.46995095817688,
8.85282181883899));
#391428=CARTESIAN_POINT('Ctrl Pts',(-1.0055736911689,2.46975204145501,8.85372622499636));
#391429=CARTESIAN_POINT('Ctrl Pts',(-1.00517150659735,2.46958246132732,
8.85462257735071));
#391430=CARTESIAN_POINT('Ctrl Pts',(-1.00483762725028,2.46944168192823,
8.85536669723986));
#391431=CARTESIAN_POINT('Ctrl Pts',(-1.00447119635593,2.46932105929728,
8.85610498449051));
#391432=CARTESIAN_POINT('Ctrl Pts',(-1.00406218131168,2.46923409470727,
8.85681338218371));
#391433=CARTESIAN_POINT('Ctrl Pts',(-1.00369099951666,2.46915517420526,
8.85745625420284));
#391434=CARTESIAN_POINT('Ctrl Pts',(-1.00328021553237,2.46910239770779,
8.85808743050665));
#391435=CARTESIAN_POINT('Ctrl Pts',(-1.0028142972132,2.46909977768252,8.85866804508409));
#391436=CARTESIAN_POINT('Ctrl Pts',(-1.00259933260061,2.46909856885965,
8.85893592806395));
#391437=CARTESIAN_POINT('Ctrl Pts',(-1.00237252513374,2.46910825460029,
8.85919241173848));
#391438=CARTESIAN_POINT('Ctrl Pts',(-1.00213185569258,2.46913271113081,
8.85943017985534));
#391439=CARTESIAN_POINT('Ctrl Pts',(-1.00180688070125,2.46916573468691,
8.8597512372));
#391440=CARTESIAN_POINT('Ctrl Pts',(-1.00144842447933,2.46922716762035,
8.86004599534706));
#391441=CARTESIAN_POINT('Ctrl Pts',(-1.00106255305268,2.4693265372646,8.86026130871721));
#391442=CARTESIAN_POINT('Ctrl Pts',(-1.00092127464451,2.46936291929288,
8.86034014101235));
#391443=CARTESIAN_POINT('Ctrl Pts',(-1.00077419600275,2.46940492129388,
8.86040910639693));
#391444=CARTESIAN_POINT('Ctrl Pts',(-1.00062541657116,2.46945172239472,
8.86046313645507));
#391445=CARTESIAN_POINT('Ctrl Pts',(-1.00039324751417,2.46952475512063,
8.8605474499083));
#391446=CARTESIAN_POINT('Ctrl Pts',(-1.00015064341205,2.46961160813619,
8.86059655985668));
#391447=CARTESIAN_POINT('Ctrl Pts',(-0.999913064461799,2.46970643547806,
8.86059725258816));
#391448=CARTESIAN_POINT('Ctrl Pts',(-0.999674936609261,2.46980148190898,
8.86059794692011));
#391449=CARTESIAN_POINT('Ctrl Pts',(-0.999440201162461,2.46990806111197,
8.86056369958366));
#391450=CARTESIAN_POINT('Ctrl Pts',(-0.999220104961786,2.47001693375418,
8.86048590497774));
#391451=CARTESIAN_POINT('Ctrl Pts',(-0.999162666406463,2.47004534627227,
8.86046560290182));
#391452=CARTESIAN_POINT('Ctrl Pts',(-0.999105517781755,2.47007436580571,
8.86044257503091));
#391453=CARTESIAN_POINT('Ctrl Pts',(-0.999050410165033,2.47010306635803,
8.86041778462583));
#391454=CARTESIAN_POINT('Ctrl Pts',(-0.998679604287343,2.47029618546078,
8.86025097596201));
#391455=CARTESIAN_POINT('Ctrl Pts',(-0.998351603563481,2.47050107069051,
8.8599848982295));
#391456=CARTESIAN_POINT('Ctrl Pts',(-0.998071492878068,2.47070455619527,
8.85968173251461));
#391457=CARTESIAN_POINT('Ctrl Pts',(-0.997923330373914,2.47081218836896,
8.85952137522076));
#391458=CARTESIAN_POINT('Ctrl Pts',(-0.99778559838977,2.47092134911842,
8.85934740853961));
#391459=CARTESIAN_POINT('Ctrl Pts',(-0.997659273667602,2.47102928072491,
8.8591675900182));
#391460=CARTESIAN_POINT('Ctrl Pts',(-0.997152014245809,2.47146268222672,
8.85844552518695));
#391461=CARTESIAN_POINT('Ctrl Pts',(-0.996798055348722,2.47189845883579,
8.85759444184124));
#391462=CARTESIAN_POINT('Ctrl Pts',(-0.99654137040139,2.47227968985935,
8.85683498915138));
#391463=CARTESIAN_POINT('Ctrl Pts',(-0.996514509005261,2.47231958467067,
8.85675551444998));
#391464=CARTESIAN_POINT('Ctrl Pts',(-0.99648873128938,2.47235888984364,
8.85667699793651));
#391465=CARTESIAN_POINT('Ctrl Pts',(-0.996463985412311,2.47239754457562,
8.85659965593547));
#391466=CARTESIAN_POINT('Ctrl Pts',(-0.996129964300902,2.47291930812045,
8.85555568965886));
#391467=CARTESIAN_POINT('Ctrl Pts',(-0.995884302298597,2.47346899447079,
8.85434650606346));
#391468=CARTESIAN_POINT('Ctrl Pts',(-0.995720111102476,2.47404678523083,
8.85297329937118));
#391469=CARTESIAN_POINT('Ctrl Pts',(-0.995627763558975,2.47437175732805,
8.85220095427747));
#391470=CARTESIAN_POINT('Ctrl Pts',(-0.995561453674479,2.4747058388066,
8.85137579139184));
#391471=CARTESIAN_POINT('Ctrl Pts',(-0.995522110700926,2.47505025214474,
8.85049129520029));
#391472=CARTESIAN_POINT('Origin',(-1.00235268932042,2.47583052179233,7.59394543036555));
#391473=CARTESIAN_POINT('Ctrl Pts',(-1.00628214029678,2.47016120246829,
7.59443877723642));
#391474=CARTESIAN_POINT('Ctrl Pts',(-1.00180750953459,2.46648548849808,
7.58783886950016));
#391475=CARTESIAN_POINT('Ctrl Pts',(-0.995046786110622,2.47162083661882,
7.58559994247159));
#391476=CARTESIAN_POINT('Ctrl Pts',(-1.03070901834743,2.49022681719079,
7.56670252222133));
#391477=CARTESIAN_POINT('Ctrl Pts',(-1.02624085469707,2.48655641567087,
7.56004874999028));
#391478=CARTESIAN_POINT('Ctrl Pts',(-1.01942714814677,2.49170517865849,
7.55786368756704));
#391479=CARTESIAN_POINT('Ctrl Pts',(-1.05509028164391,2.51025496138264,
7.53888913333558));
#391480=CARTESIAN_POINT('Ctrl Pts',(-1.05059556347818,2.50656274648674,
7.53222002137275));
#391481=CARTESIAN_POINT('Ctrl Pts',(-1.04376358769266,2.51175182651944,
7.53005029815326));
#391482=CARTESIAN_POINT('Ctrl Pts',(-1.07942482691749,2.5302447287567,7.51101258149734));
#391483=CARTESIAN_POINT('Ctrl Pts',(-1.07487562460051,2.52650775750732,
7.5043616886572));
#391484=CARTESIAN_POINT('Ctrl Pts',(-1.06805484980025,2.53175985353355,
7.50217374673251));
#391485=CARTESIAN_POINT('',(-1.06675863750384,2.53069219871726,7.50366116523517));
#391486=CARTESIAN_POINT('Ctrl Pts',(-1.07279542170606,2.52479896157613,
7.51860402984325));
#391487=CARTESIAN_POINT('Ctrl Pts',(-1.07313666163293,2.52507927528983,
7.51734760759493));
#391488=CARTESIAN_POINT('Ctrl Pts',(-1.07340725496913,2.52537855293079,
7.51608817408573));
#391489=CARTESIAN_POINT('Ctrl Pts',(-1.07359667414353,2.52570506198002,
7.5148100591312));
#391490=CARTESIAN_POINT('Ctrl Pts',(-1.07376825455802,2.52600082167899,
7.51365231206384));
#391491=CARTESIAN_POINT('Ctrl Pts',(-1.07387368844631,2.52631921657147,
7.51247773061043));
#391492=CARTESIAN_POINT('Ctrl Pts',(-1.07387609828082,2.52666634484815,
7.51129758471022));
#391493=CARTESIAN_POINT('Ctrl Pts',(-1.07387909342989,2.52709778565251,
7.50983079813402));
#391494=CARTESIAN_POINT('Ctrl Pts',(-1.07370982072311,2.52755993392017,
7.50839324291155));
#391495=CARTESIAN_POINT('Ctrl Pts',(-1.07328963432873,2.52802780918636,
7.50715379678855));
#391496=CARTESIAN_POINT('Ctrl Pts',(-1.0730955203219,2.52824395407783,7.50658120839351));
#391497=CARTESIAN_POINT('Ctrl Pts',(-1.0728131925669,2.52848569937382,7.50598221009429));
#391498=CARTESIAN_POINT('Ctrl Pts',(-1.07243457566394,2.52873001389883,
7.50545747549611));
#391499=CARTESIAN_POINT('Ctrl Pts',(-1.07223253396523,2.52886038769162,
7.50517746087247));
#391500=CARTESIAN_POINT('Ctrl Pts',(-1.07200099171823,2.52899307697136,
7.50491486231392));
#391501=CARTESIAN_POINT('Ctrl Pts',(-1.07174525119682,2.52912312068134,
7.50468370960993));
#391502=CARTESIAN_POINT('Ctrl Pts',(-1.07136283844854,2.52931757704774,
7.50433806340447));
#391503=CARTESIAN_POINT('Ctrl Pts',(-1.07091459969726,2.52951145280318,
7.50405484070984));
#391504=CARTESIAN_POINT('Ctrl Pts',(-1.07043043859138,2.52969103325066,
7.50385766036131));
#391505=CARTESIAN_POINT('Ctrl Pts',(-1.07037866508667,2.52971023658821,
7.50383657498791));
#391506=CARTESIAN_POINT('Ctrl Pts',(-1.07032650872314,2.52972928148965,
7.50381643264937));
#391507=CARTESIAN_POINT('Ctrl Pts',(-1.07027402628802,2.52974815515542,
7.50379723213559));
#391508=CARTESIAN_POINT('Ctrl Pts',(-1.06992368886538,2.52987414304837,
7.50366906242519));
#391509=CARTESIAN_POINT('Ctrl Pts',(-1.06955095771554,2.52999456458163,
7.50358235568538));
#391510=CARTESIAN_POINT('Ctrl Pts',(-1.06918890063952,2.53010200008106,
7.5035341175365));
#391511=CARTESIAN_POINT('Ctrl Pts',(-1.06864603703097,2.53026308745309,
7.50346178989176));
#391512=CARTESIAN_POINT('Ctrl Pts',(-1.06805519007335,2.53041329887528,
7.50346967198527));
#391513=CARTESIAN_POINT('Ctrl Pts',(-1.06747062403743,2.53054291245446,
7.50354272648692));
#391514=CARTESIAN_POINT('Ctrl Pts',(-1.06723017992706,2.53059622520241,
7.50357277531559));
#391515=CARTESIAN_POINT('Ctrl Pts',(-1.06699114861868,2.53064612070988,
7.50361331098761));
#391516=CARTESIAN_POINT('Ctrl Pts',(-1.06675863750439,2.53069219871857,
7.50366116523659));
#391517=CARTESIAN_POINT('',(-1.00345144303402,2.47854446470841,7.57603338622103));
#391518=CARTESIAN_POINT('Origin',(-1.00676500980815,2.48673664175956,7.58486873427627));
#391519=CARTESIAN_POINT('Ctrl Pts',(-1.06675863755131,2.53069219874943,
7.50366116529969));
#391520=CARTESIAN_POINT('Ctrl Pts',(-1.04569014273066,2.51333863067848,
7.52783573079709));
#391521=CARTESIAN_POINT('Ctrl Pts',(-1.0245887295326,2.49595688722903,7.55196141284068));
#391522=CARTESIAN_POINT('Ctrl Pts',(-1.00345144418592,2.4785444651991,7.57603338728831));
#391523=CARTESIAN_POINT('Ctrl Pts',(-1.00727768057273,2.47117287269355,
7.59642833564546));
#391524=CARTESIAN_POINT('Ctrl Pts',(-0.994757591870493,2.4578328505239,
7.59959882295464));
#391525=CARTESIAN_POINT('Ctrl Pts',(-0.995580073096938,2.47609196989962,
7.59639677331371));
#391526=CARTESIAN_POINT('Ctrl Pts',(-1.00514669506349,2.46797166347564,
7.58710240504252));
#391527=CARTESIAN_POINT('Ctrl Pts',(-0.998521053703182,2.46662434118415,
7.58809943920598));
#391528=CARTESIAN_POINT('Ctrl Pts',(-0.994780473004191,2.47227415065621,
7.58707626057423));
#391529=CARTESIAN_POINT('Ctrl Pts',(-1.00382229260949,2.47388921842956,
7.58020924244128));
#391530=CARTESIAN_POINT('Ctrl Pts',(-1.00116057348243,2.47297143505264,
7.5820588065976));
#391531=CARTESIAN_POINT('Ctrl Pts',(-0.999909163054414,2.4755333178244,
7.5801537675693));
#391532=CARTESIAN_POINT('Ctrl Pts',(-1.00345144272365,2.47854446394124,
7.57603338509286));
#391533=CARTESIAN_POINT('Ctrl Pts',(-1.00345144272365,2.47854446394124,
7.57603338509286));
#391534=CARTESIAN_POINT('Ctrl Pts',(-1.00345144272365,2.47854446394124,
7.57603338509286));
#391535=CARTESIAN_POINT('Origin',(-1.00677029912173,2.48673450035397,7.58486873427621));
#391536=CARTESIAN_POINT('Ctrl Pts',(-0.984839906194067,2.56856361376243,
7.51098857897448));
#391537=CARTESIAN_POINT('Ctrl Pts',(-0.985508080078791,2.56271433554784,
7.50433767179957));
#391538=CARTESIAN_POINT('Ctrl Pts',(-0.994061605444748,2.56174209334736,
7.50214974420965));
#391539=CARTESIAN_POINT('Ctrl Pts',(-0.988415106647414,2.53726585938646,
7.53887321589169));
#391540=CARTESIAN_POINT('Ctrl Pts',(-0.989075274623209,2.53148666590547,
7.53220407452062));
#391541=CARTESIAN_POINT('Ctrl Pts',(-0.997592998639362,2.53046133790587,
7.53003438070911));
#391542=CARTESIAN_POINT('Ctrl Pts',(-0.991997172804467,2.50590800177684,
7.56669465659237));
#391543=CARTESIAN_POINT('Ctrl Pts',(-0.992653439310206,2.50016296225487,
7.56004085833302));
#391544=CARTESIAN_POINT('Ctrl Pts',(-1.00112998038326,2.49912137617411,
7.55785582193789));
#391545=CARTESIAN_POINT('Ctrl Pts',(-0.995585942662718,2.47449145912389,
7.59443891967696));
#391546=CARTESIAN_POINT('Ctrl Pts',(-0.996243160673235,2.4687380900099,
7.58783901202978));
#391547=CARTESIAN_POINT('Ctrl Pts',(-1.00467229381074,2.46772374660725,
7.58560008491213));
#391548=CARTESIAN_POINT('',(-0.994253029633958,2.5600464660629,7.50366116523517));
#391549=CARTESIAN_POINT('Ctrl Pts',(-0.994253029634093,2.56004646606325,
7.50366116523554));
#391550=CARTESIAN_POINT('Ctrl Pts',(-0.993616541819959,2.56045758743125,
7.50350835821027));
#391551=CARTESIAN_POINT('Ctrl Pts',(-0.99301807963321,2.56081480028401,
7.50345484956));
#391552=CARTESIAN_POINT('Ctrl Pts',(-0.992440158080123,2.56112924048318,
7.50349758195598));
#391553=CARTESIAN_POINT('Ctrl Pts',(-0.99214364146361,2.56129057162485,
7.50351950684424));
#391554=CARTESIAN_POINT('Ctrl Pts',(-0.991823368062682,2.56145665822576,
7.50357029184312));
#391555=CARTESIAN_POINT('Ctrl Pts',(-0.991510129749804,2.56160832434008,
7.50365515313924));
#391556=CARTESIAN_POINT('Ctrl Pts',(-0.991028242381882,2.56184164823957,
7.50378570417639));
#391557=CARTESIAN_POINT('Ctrl Pts',(-0.990549010837197,2.56204800474018,
7.50400001621911));
#391558=CARTESIAN_POINT('Ctrl Pts',(-0.990108013665056,2.56220960180847,
7.50428903009634));
#391559=CARTESIAN_POINT('Ctrl Pts',(-0.990059066371773,2.5622275378398,
7.50432110841318));
#391560=CARTESIAN_POINT('Ctrl Pts',(-0.990010572585567,2.56224494721138,
7.50435406373354));
#391561=CARTESIAN_POINT('Ctrl Pts',(-0.989962567779668,2.56226182368384,
7.50438785222352));
#391562=CARTESIAN_POINT('Ctrl Pts',(-0.989669475365627,2.56236486266007,
7.50459414719561));
#391563=CARTESIAN_POINT('Ctrl Pts',(-0.989389773235793,2.56244919073966,
7.50483629897752));
#391564=CARTESIAN_POINT('Ctrl Pts',(-0.989134556580122,2.56251283734952,
7.5050991045531));
#391565=CARTESIAN_POINT('Ctrl Pts',(-0.988571523003624,2.56265324816357,
7.50567888004914));
#391566=CARTESIAN_POINT('Ctrl Pts',(-0.988105596423529,2.56269904257185,
7.50637912803144));
#391567=CARTESIAN_POINT('Ctrl Pts',(-0.987731664620562,2.56268070472712,
7.50710440483569));
#391568=CARTESIAN_POINT('Ctrl Pts',(-0.987639969118888,2.56267620792353,
7.50728225710685));
#391569=CARTESIAN_POINT('Ctrl Pts',(-0.987551972991248,2.5626679109256,
7.50746498566954));
#391570=CARTESIAN_POINT('Ctrl Pts',(-0.987469691245669,2.56265642216575,
7.50764697238949));
#391571=CARTESIAN_POINT('Ctrl Pts',(-0.987027367225978,2.56259466175455,
7.50862528291182));
#391572=CARTESIAN_POINT('Ctrl Pts',(-0.986709454310666,2.56243915725786,
7.50965856837422));
#391573=CARTESIAN_POINT('Ctrl Pts',(-0.986471889921137,2.56223944537934,
7.51067959873202));
#391574=CARTESIAN_POINT('Ctrl Pts',(-0.986341157937931,2.56212954368069,
7.51124147302579));
#391575=CARTESIAN_POINT('Ctrl Pts',(-0.986235005650185,2.56200589525494,
7.51180065547253));
#391576=CARTESIAN_POINT('Ctrl Pts',(-0.986147912535891,2.56187474152438,
7.51235175716501));
#391577=CARTESIAN_POINT('Ctrl Pts',(-0.985846971132227,2.56142155313986,
7.51425603304536));
#391578=CARTESIAN_POINT('Ctrl Pts',(-0.985742762481469,2.56082136401569,
7.51626900505181));
#391579=CARTESIAN_POINT('Ctrl Pts',(-0.985805085598299,2.56012642898783,
7.51827788969245));
#391580=CARTESIAN_POINT('Ctrl Pts',(-0.985808458643156,2.56008881779087,
7.51838661432546));
#391581=CARTESIAN_POINT('Ctrl Pts',(-0.98581232671753,2.56005092221107,
7.51849533314857));
#391582=CARTESIAN_POINT('Ctrl Pts',(-0.985816687379952,2.56001274842384,
7.51860402984325));
#391583=CARTESIAN_POINT('Ctrl Pts',(-1.00345144254814,2.47854446586344,
7.57603338728985));
#391584=CARTESIAN_POINT('Ctrl Pts',(-1.00038100552583,2.50575750850121,
7.55196141284922));
#391585=CARTESIAN_POINT('Ctrl Pts',(-0.997314994683384,2.53292355758908,
7.52783573083105));
#391586=CARTESIAN_POINT('Ctrl Pts',(-0.994253029621948,2.56004646612085,
7.50366116530176));
#391587=CARTESIAN_POINT('Origin',(-3.46738858720994E-16,8.56451684780636E-16,
7.49482233047033));
#391588=CARTESIAN_POINT('Origin',(-1.06332537456792,2.5225474024882,7.49482233047033));
#391589=CARTESIAN_POINT('Origin',(0.,0.,7.50366116523517));
#391590=CARTESIAN_POINT('Origin',(-0.991053119217907,2.55180719586893,7.49482233047033));
#391591=CARTESIAN_POINT('Ctrl Pts',(-1.07279460441739,2.52479829015122,
7.51860402984325));
#391592=CARTESIAN_POINT('Ctrl Pts',(-1.07867375938539,2.52962859271859,
7.51860402984325));
#391593=CARTESIAN_POINT('Ctrl Pts',(-1.08566466424082,2.52662467272424,
7.51860402984325));
#391594=CARTESIAN_POINT('Ctrl Pts',(-1.07497757558513,2.52659181347635,
7.51041458714366));
#391595=CARTESIAN_POINT('Ctrl Pts',(-1.08032998091005,2.52891692057021,
7.51004642900441));
#391596=CARTESIAN_POINT('Ctrl Pts',(-1.08566659224937,2.52662384427877,
7.5072913648301));
#391597=CARTESIAN_POINT('Ctrl Pts',(-1.07405060721883,2.5292497199546,7.50215815450137));
#391598=CARTESIAN_POINT('Ctrl Pts',(-1.07695780404858,2.53036608507162,
7.49877163671531));
#391599=CARTESIAN_POINT('Ctrl Pts',(-1.08013710129289,2.52902593857713,
7.49481588533171));
#391600=CARTESIAN_POINT('Ctrl Pts',(-1.06675842366604,2.53069169142693,
7.50366171572174));
#391601=CARTESIAN_POINT('Ctrl Pts',(-1.06818074157473,2.53406588377826,
7.50000045605858));
#391602=CARTESIAN_POINT('Ctrl Pts',(-1.06818074157484,2.53406588377821,
7.49482233047317));
#391603=CARTESIAN_POINT('Origin',(-1.0807298248579,2.51514001512095,7.51860402984325));
#391604=CARTESIAN_POINT('Origin',(-1.0807298248579,2.51514001512095,9.));
#391605=CARTESIAN_POINT('Origin',(-1.0807298248579,2.51514001512095,8.75721825406948));
#391606=CARTESIAN_POINT('Ctrl Pts',(-1.0598909639272,2.51419847335744,8.78942910404912));
#391607=CARTESIAN_POINT('Ctrl Pts',(-1.06418404382885,2.51775120380876,
8.79672699501691));
#391608=CARTESIAN_POINT('Ctrl Pts',(-1.07104086177894,2.51203652677664,
8.79893251111267));
#391609=CARTESIAN_POINT('Ctrl Pts',(-1.06838645708335,2.52117715623988,
8.78111911759581));
#391610=CARTESIAN_POINT('Ctrl Pts',(-1.07348069887324,2.52538322455977,
8.78644465894812));
#391611=CARTESIAN_POINT('Ctrl Pts',(-1.08067618140391,2.52164952091239,
8.78817647674132));
#391612=CARTESIAN_POINT('Ctrl Pts',(-1.07368105107515,2.52552643784496,
8.76780923932031));
#391613=CARTESIAN_POINT('Ctrl Pts',(-1.07969783280626,2.5304875944007,8.76988516158376));
#391614=CARTESIAN_POINT('Ctrl Pts',(-1.08670212754838,2.52764572255949,
8.77093053738833));
#391615=CARTESIAN_POINT('Ctrl Pts',(-1.07264867770945,2.52467838745472,
8.75371302330492));
#391616=CARTESIAN_POINT('Ctrl Pts',(-1.07851730378653,2.52951836982403,
8.75300828287558));
#391617=CARTESIAN_POINT('Ctrl Pts',(-1.08552714604779,2.52647589536948,
8.75267964240737));
#391618=CARTESIAN_POINT('Origin',(-1.06989435603297,2.50623915016686,8.78727029226991));
#391619=CARTESIAN_POINT('Ctrl Pts',(-1.00671661105393,2.47051810124198,
8.85049129520029));
#391620=CARTESIAN_POINT('Ctrl Pts',(-1.01122897392942,2.47422481049724,
8.85711686593484));
#391621=CARTESIAN_POINT('Ctrl Pts',(-1.01802024859358,2.46903064544886,
8.85933012996512));
#391622=CARTESIAN_POINT('Ctrl Pts',(-1.02515785026092,2.48566677477142,
8.82945683644722));
#391623=CARTESIAN_POINT('Ctrl Pts',(-1.02970766847649,2.48940425195463,
8.8360746990239));
#391624=CARTESIAN_POINT('Ctrl Pts',(-1.03649609897603,2.48416504840347,
8.8382956714852));
#391625=CARTESIAN_POINT('Ctrl Pts',(-1.04357160131376,2.50079286798138,
8.80838214965002));
#391626=CARTESIAN_POINT('Ctrl Pts',(-1.0481393752363,2.50454509499457,8.81501364461992));
#391627=CARTESIAN_POINT('Ctrl Pts',(-1.05494349880899,2.49927701042778,
8.81722098428721));
#391628=CARTESIAN_POINT('Ctrl Pts',(-1.06195995288112,2.51589809662204,
8.78727029226991));
#391629=CARTESIAN_POINT('Ctrl Pts',(-1.0665284855259,2.51965094689244,8.79393457792714));
#391630=CARTESIAN_POINT('Ctrl Pts',(-1.07336460881942,2.51436825501291,
8.79610912703474));
#391631=CARTESIAN_POINT('Origin',(-1.01465101420578,2.4608591547868,8.85049129520029));
#391632=CARTESIAN_POINT('Ctrl Pts',(-0.995522110700926,2.47505025214474,
8.85049129520029));
#391633=CARTESIAN_POINT('Ctrl Pts',(-0.994859350710966,2.48085213644373,
8.85711686593484));
#391634=CARTESIAN_POINT('Ctrl Pts',(-0.986367352980517,2.48184548263713,
8.85933012996512));
#391635=CARTESIAN_POINT('Ctrl Pts',(-0.996108444897003,2.46991740885651,
8.86332496987233));
#391636=CARTESIAN_POINT('Ctrl Pts',(-0.991939266488152,2.47190985603823,
8.86648636486737));
#391637=CARTESIAN_POINT('Ctrl Pts',(-0.988024668749171,2.46748808869535,
8.87206031107457));
#391638=CARTESIAN_POINT('Ctrl Pts',(-1.00269746170461,2.46721654538255,
8.86341338519876));
#391639=CARTESIAN_POINT('Ctrl Pts',(-1.00708145117164,2.46571517701092,
8.86654584966059));
#391640=CARTESIAN_POINT('Ctrl Pts',(-1.00675706511739,2.45979749786491,
8.87215952290714));
#391641=CARTESIAN_POINT('Ctrl Pts',(-1.00671661105393,2.47051810124198,
8.85049129520029));
#391642=CARTESIAN_POINT('Ctrl Pts',(-1.01122897392942,2.47422481049724,
8.85711686593484));
#391643=CARTESIAN_POINT('Ctrl Pts',(-1.01802024859358,2.46903064544886,
8.85933012996512));
#391644=CARTESIAN_POINT('Origin',(-0.983102876847304,2.47363158005823,8.85049129520029));
#391645=CARTESIAN_POINT('Ctrl Pts',(-0.987408162934515,2.54608077127965,
8.78727029226991));
#391646=CARTESIAN_POINT('Ctrl Pts',(-0.98673715292638,2.55195487727524,
8.79393457792714));
#391647=CARTESIAN_POINT('Ctrl Pts',(-0.978151351640492,2.55291583068589,
8.79610912703474));
#391648=CARTESIAN_POINT('Ctrl Pts',(-0.990108979344114,2.52243748478278,
8.80838214965002));
#391649=CARTESIAN_POINT('Ctrl Pts',(-0.98943808077443,2.52831061523215,
8.81501364461994));
#391650=CARTESIAN_POINT('Ctrl Pts',(-0.980885428519784,2.529259800149,8.81722098428721));
#391651=CARTESIAN_POINT('Ctrl Pts',(-0.992813526340817,2.49876154025726,
8.82945683644723));
#391652=CARTESIAN_POINT('Ctrl Pts',(-0.992145265042226,2.50461158370381,
8.83607469902389));
#391653=CARTESIAN_POINT('Ctrl Pts',(-0.9836239779151,2.50557059788233,8.8382956714852));
#391654=CARTESIAN_POINT('Ctrl Pts',(-0.995522110700926,2.47505025214474,
8.85049129520029));
#391655=CARTESIAN_POINT('Ctrl Pts',(-0.994859350710966,2.48085213644373,
8.85711686593484));
#391656=CARTESIAN_POINT('Ctrl Pts',(-0.986367352980517,2.48184548263713,
8.85933012996512));
#391657=CARTESIAN_POINT('Origin',(-0.974988929080893,2.54466209919314,8.78727029226991));
#391658=CARTESIAN_POINT('Ctrl Pts',(-0.985837683686198,2.55982878158037,
8.75374538247849));
#391659=CARTESIAN_POINT('Ctrl Pts',(-0.984988286799116,2.56738013267245,
8.75304829418602));
#391660=CARTESIAN_POINT('Ctrl Pts',(-0.977845758623018,2.57007363122687,
8.75272238421917));
#391661=CARTESIAN_POINT('Ctrl Pts',(-0.985687874189948,2.56114023650868,
8.76769408445016));
#391662=CARTESIAN_POINT('Ctrl Pts',(-0.984816416926097,2.56888153596093,
8.76974318093967));
#391663=CARTESIAN_POINT('Ctrl Pts',(-0.977816320118229,2.57171296704089,
8.77077869880429));
#391664=CARTESIAN_POINT('Ctrl Pts',(-0.986455712341564,2.55441846563454,
8.78108014887993));
#391665=CARTESIAN_POINT('Ctrl Pts',(-0.985720959251959,2.56097936307297,
8.78639403366327));
#391666=CARTESIAN_POINT('Ctrl Pts',(-0.977971752381943,2.56331856563253,
8.78812224174741));
#391667=CARTESIAN_POINT('Ctrl Pts',(-0.987714029535122,2.543402967014,8.78944554828685));
#391668=CARTESIAN_POINT('Ctrl Pts',(-0.987100369825368,2.54893287111602,
8.79673892988685));
#391669=CARTESIAN_POINT('Ctrl Pts',(-0.978208869419684,2.54959978554248,
8.79894799272499));
#391670=CARTESIAN_POINT('Origin',(-0.973397453526334,2.55859407633733,8.75721825406948));
#391671=CARTESIAN_POINT('Origin',(-0.973397453526334,2.55859407633733,9.));
#391672=CARTESIAN_POINT('Origin',(-0.973397453526334,2.55859407633733,7.51860402984325));
#391673=CARTESIAN_POINT('Ctrl Pts',(-0.994252744839177,2.56004573276092,
7.50366195182966));
#391674=CARTESIAN_POINT('Ctrl Pts',(-0.995578475926535,2.56345928352135,
7.50000065167735));
#391675=CARTESIAN_POINT('Ctrl Pts',(-0.995578475926426,2.5634592835214,
7.49482233047108));
#391676=CARTESIAN_POINT('Ctrl Pts',(-0.988005205888649,2.56408578927888,
7.50215800491337));
#391677=CARTESIAN_POINT('Ctrl Pts',(-0.986691781976944,2.5669106104772,
7.49877273257267));
#391678=CARTESIAN_POINT('Ctrl Pts',(-0.983473834939355,2.5681603997447,
7.49481816995649));
#391679=CARTESIAN_POINT('Ctrl Pts',(-0.985497132441371,2.56281316053287,
7.51043025814042));
#391680=CARTESIAN_POINT('Ctrl Pts',(-0.98327195508721,2.56821143273141,
7.51006209594513));
#391681=CARTESIAN_POINT('Ctrl Pts',(-0.977839824358198,2.57027805458973,
7.50731281821697));
#391682=CARTESIAN_POINT('Ctrl Pts',(-0.985816858824492,2.56001124677168,
7.51860402984325));
#391683=CARTESIAN_POINT('Ctrl Pts',(-0.984954168022263,2.56757145721652,
7.51860402984324));
#391684=CARTESIAN_POINT('Ctrl Pts',(-0.977842190757043,2.57027715431147,
7.51860402984325));
#391685=CARTESIAN_POINT('Origin',(0.,0.,7.5));
#391686=CARTESIAN_POINT('Origin',(-1.15205371787331,2.40618167532513,7.5));
#391687=CARTESIAN_POINT('',(-1.15205371787331,2.40618167532513,7.59394543036555));
#391688=CARTESIAN_POINT('',(-1.15205371787331,2.40618167532513,8.85049129520029));
#391689=CARTESIAN_POINT('',(-1.15205371787331,2.40618167532513,7.5));
#391690=CARTESIAN_POINT('',(-1.14850738206912,2.47758611705878,8.78727029226991));
#391691=CARTESIAN_POINT('Ctrl Pts',(-1.15205371787331,2.40618167532513,
8.85049129520029));
#391692=CARTESIAN_POINT('Ctrl Pts',(-1.1508698876244,2.43001775366008,8.82945686509571));
#391693=CARTESIAN_POINT('Ctrl Pts',(-1.14968781728231,2.45381839678238,
8.80838212259896));
#391694=CARTESIAN_POINT('Ctrl Pts',(-1.14850738206912,2.47758611705878,
8.78727029226991));
#391695=CARTESIAN_POINT('',(-1.14781180121217,2.4915914356506,8.75721825406948));
#391696=CARTESIAN_POINT('Origin',(-1.14990524686335,2.44944458354024,8.75937679713147));
#391697=CARTESIAN_POINT('',(-1.14781180121217,2.4915914356506,7.51860402984325));
#391698=CARTESIAN_POINT('',(-1.14781180121217,2.4915914356506,7.5));
#391699=CARTESIAN_POINT('Ctrl Pts',(-1.14781180121217,2.4915914356506,7.51860402984325));
#391700=CARTESIAN_POINT('Ctrl Pts',(-1.14835807179202,2.48059243613578,
7.52834476460825));
#391701=CARTESIAN_POINT('Ctrl Pts',(-1.14890469700286,2.4695862962292,7.53807742314407));
#391702=CARTESIAN_POINT('Ctrl Pts',(-1.14945168875187,2.45857277618268,
7.54780169004674));
#391703=CARTESIAN_POINT('Ctrl Pts',(-1.15031809411993,2.44112795565897,
7.5632044032688));
#391704=CARTESIAN_POINT('Ctrl Pts',(-1.15118542018666,2.42366459713434,
7.57858609112103));
#391705=CARTESIAN_POINT('Ctrl Pts',(-1.15205371787331,2.40618167532513,
7.59394543036555));
#391706=CARTESIAN_POINT('Origin',(-1.38617896354006,2.56152510751204,7.5));
#391707=CARTESIAN_POINT('',(-1.23235567333047,2.45087725266272,8.75721825406948));
#391708=CARTESIAN_POINT('',(-1.22097218676271,2.4426889063615,8.78727029226991));
#391709=CARTESIAN_POINT('Origin',(-1.19207665202441,2.42190382934773,8.75658640621025));
#391710=CARTESIAN_POINT('',(-1.16293484201941,2.40094160211228,8.85049129520029));
#391711=CARTESIAN_POINT('Ctrl Pts',(-1.22097218676271,2.4426889063615,8.78727029226991));
#391712=CARTESIAN_POINT('Ctrl Pts',(-1.20165384546695,2.42879287656842,
8.80838212259896));
#391713=CARTESIAN_POINT('Ctrl Pts',(-1.18230874456758,2.41487759811193,
8.82945686509571));
#391714=CARTESIAN_POINT('Ctrl Pts',(-1.16293484201941,2.40094160211228,
8.85049129520029));
#391715=CARTESIAN_POINT('',(-1.16293484201941,2.40094160211228,7.59394543036555));
#391716=CARTESIAN_POINT('',(-1.16293484201941,2.40094160211228,7.5));
#391717=CARTESIAN_POINT('',(-1.23235567333047,2.45087725266272,7.51860402984325));
#391718=CARTESIAN_POINT('Ctrl Pts',(-1.16293484201941,2.40094160211228,
7.59394543036555));
#391719=CARTESIAN_POINT('Ctrl Pts',(-1.17714491544798,2.41116316309944,
7.57858609112103));
#391720=CARTESIAN_POINT('Ctrl Pts',(-1.19133908788948,2.42137328622108,
7.56320440326857));
#391721=CARTESIAN_POINT('Ctrl Pts',(-1.20551819269218,2.43157257091954,
7.54780169004651));
#391722=CARTESIAN_POINT('Ctrl Pts',(-1.21446995317456,2.43801173298109,
7.53807742314383));
#391723=CARTESIAN_POINT('Ctrl Pts',(-1.22341571509854,2.44444658017185,
7.52834476460825));
#391724=CARTESIAN_POINT('Ctrl Pts',(-1.23235567333047,2.45087725266272,
7.51860402984325));
#391725=CARTESIAN_POINT('',(-1.23235567333047,2.45087725266272,7.5));
#391726=CARTESIAN_POINT('Origin',(-1.15892025438442,2.40652270515029,7.5));
#391727=CARTESIAN_POINT('Ctrl Pts',(-1.16293484201941,2.40094160211228,
8.85049129520029));
#391728=CARTESIAN_POINT('Ctrl Pts',(-1.16277762822756,2.40082851540871,
8.85097269580138));
#391729=CARTESIAN_POINT('Ctrl Pts',(-1.16261748621827,2.40072368386098,
8.85143669361005));
#391730=CARTESIAN_POINT('Ctrl Pts',(-1.16244656312289,2.40062301180748,
8.8519052845931));
#391731=CARTESIAN_POINT('Ctrl Pts',(-1.16211224838786,2.40042610365524,
8.85282181883899));
#391732=CARTESIAN_POINT('Ctrl Pts',(-1.16174518876679,2.40025034340576,
8.85372622499635));
#391733=CARTESIAN_POINT('Ctrl Pts',(-1.16133296549049,2.4001068797526,8.8546225773507));
#391734=CARTESIAN_POINT('Ctrl Pts',(-1.16099075236728,2.39998778132309,
8.85536669723986));
#391735=CARTESIAN_POINT('Ctrl Pts',(-1.160617346026,2.39989088383229,8.85610498449051));
#391736=CARTESIAN_POINT('Ctrl Pts',(-1.16020359950662,2.39983030360422,
8.8568133821837));
#391737=CARTESIAN_POINT('Ctrl Pts',(-1.15982812389048,2.3997753269521,8.85745625420284));
#391738=CARTESIAN_POINT('Ctrl Pts',(-1.15941480250413,2.39974897790985,
8.85808743050666));
#391739=CARTESIAN_POINT('Ctrl Pts',(-1.15894967359852,2.3997762147569,8.85866804508411));
#391740=CARTESIAN_POINT('Ctrl Pts',(-1.15873507320424,2.3997887812477,8.85893592806396));
#391741=CARTESIAN_POINT('Ctrl Pts',(-1.15850935230517,2.39981297869224,
8.85919241173848));
#391742=CARTESIAN_POINT('Ctrl Pts',(-1.15827074428048,2.39985280471823,
8.85943017985534));
#391743=CARTESIAN_POINT('Ctrl Pts',(-1.15794855281163,2.39990658164309,
8.8597512372));
#391744=CARTESIAN_POINT('Ctrl Pts',(-1.15759476909802,2.39999085472496,
8.86004599534705));
#391745=CARTESIAN_POINT('Ctrl Pts',(-1.15721605712056,2.40011474307081,
8.86026130871721));
#391746=CARTESIAN_POINT('Ctrl Pts',(-1.15707739998859,2.40016010208701,
8.86034014101235));
#391747=CARTESIAN_POINT('Ctrl Pts',(-1.15693331461312,2.40021144115132,
8.86040910639692));
#391748=CARTESIAN_POINT('Ctrl Pts',(-1.15678783942165,2.40026767842519,
8.86046313645506));
#391749=CARTESIAN_POINT('Ctrl Pts',(-1.15656082660371,2.40035543622008,
8.86054744990829));
#391750=CARTESIAN_POINT('Ctrl Pts',(-1.15632428564955,2.400457654485,8.86059655985668));
#391751=CARTESIAN_POINT('Ctrl Pts',(-1.15609327043939,2.40056750872953,
8.86059725258816));
#391752=CARTESIAN_POINT('Ctrl Pts',(-1.1558617214918,2.40067761678126,8.86059794692011));
#391753=CARTESIAN_POINT('Ctrl Pts',(-1.15563429688713,2.40079901655756,
8.86056369958366));
#391754=CARTESIAN_POINT('Ctrl Pts',(-1.15542162839184,2.40092176712125,
8.86048590497774));
#391755=CARTESIAN_POINT('Ctrl Pts',(-1.15536612824647,2.40095380136365,
8.86046560290182));
#391756=CARTESIAN_POINT('Ctrl Pts',(-1.15531095632764,2.40098642279829,
8.86044257503091));
#391757=CARTESIAN_POINT('Ctrl Pts',(-1.15525780078612,2.40101859513938,
8.86041778462583));
#391758=CARTESIAN_POINT('Ctrl Pts',(-1.15490012995227,2.40123507507238,
8.86025097596201));
#391759=CARTESIAN_POINT('Ctrl Pts',(-1.15458593018282,2.40146055442196,
8.8599848982295));
#391760=CARTESIAN_POINT('Ctrl Pts',(-1.1543194323759,2.40168156859716,8.85968173251462));
#391761=CARTESIAN_POINT('Ctrl Pts',(-1.15417847030455,2.40179847243324,
8.85952137522077));
#391762=CARTESIAN_POINT('Ctrl Pts',(-1.15404801525877,2.40191623341875,
8.85934740853961));
#391763=CARTESIAN_POINT('Ctrl Pts',(-1.15392886528606,2.40203203692092,
8.8591675900182));
#391764=CARTESIAN_POINT('Ctrl Pts',(-1.15345041621272,2.4024970481756,8.85844552518695));
#391765=CARTESIAN_POINT('Ctrl Pts',(-1.15312510486535,2.40295460765929,
8.85759444184124));
#391766=CARTESIAN_POINT('Ctrl Pts',(-1.15289337286031,2.40335150126387,
8.85683498915139));
#391767=CARTESIAN_POINT('Ctrl Pts',(-1.15286912272314,2.40339303512258,
8.85675551444998));
#391768=CARTESIAN_POINT('Ctrl Pts',(-1.15284591626142,2.40343391112278,
8.85667699793651));
#391769=CARTESIAN_POINT('Ctrl Pts',(-1.15282369784459,2.40347407190827,
8.85659965593547));
#391770=CARTESIAN_POINT('Ctrl Pts',(-1.15252379252047,2.40401616424001,
8.85555568965886));
#391771=CARTESIAN_POINT('Ctrl Pts',(-1.15231385378249,2.40458046081932,
8.85434650606346));
#391772=CARTESIAN_POINT('Ctrl Pts',(-1.15218701911588,2.40516758421234,
8.85297329937118));
#391773=CARTESIAN_POINT('Ctrl Pts',(-1.15211568234407,2.40549780534695,
8.85220095427748));
#391774=CARTESIAN_POINT('Ctrl Pts',(-1.15207091337417,2.40583544890816,
8.85137579139184));
#391775=CARTESIAN_POINT('Ctrl Pts',(-1.15205371787331,2.40618167532513,
8.85049129520029));
#391776=CARTESIAN_POINT('Origin',(-1.15892025438442,2.40652270515029,7.59394543036555));
#391777=CARTESIAN_POINT('Ctrl Pts',(-1.16247839734608,2.40061327326238,
7.59443877723642));
#391778=CARTESIAN_POINT('Ctrl Pts',(-1.15777745639004,2.39723180201801,
7.58783886950016));
#391779=CARTESIAN_POINT('Ctrl Pts',(-1.15135964648121,2.40278976005228,
7.58559994247159));
#391780=CARTESIAN_POINT('Ctrl Pts',(-1.18814069610537,2.4190726255773,7.56670252222139));
#391781=CARTESIAN_POINT('Ctrl Pts',(-1.1834465493436,2.41569604151893,7.5600487499903));
#391782=CARTESIAN_POINT('Ctrl Pts',(-1.17697672466144,2.4212707814983,7.55786368756704));
#391783=CARTESIAN_POINT('Ctrl Pts',(-1.21375507308567,2.43749750689605,
7.5388891333356));
#391784=CARTESIAN_POINT('Ctrl Pts',(-1.20903302877989,2.43410085563325,
7.53222002137279));
#391785=CARTESIAN_POINT('Ctrl Pts',(-1.20254755552054,2.43971700033597,
7.53005029815327));
#391786=CARTESIAN_POINT('Ctrl Pts',(-1.23932036921912,2.45588708348032,
7.51101258149734));
#391787=CARTESIAN_POINT('Ctrl Pts',(-1.23454108515619,2.45244925863236,
7.5043616886572));
#391788=CARTESIAN_POINT('Ctrl Pts',(-1.22807082731704,2.45812757220591,
7.50217374673251));
#391789=CARTESIAN_POINT('',(-1.22670887334887,2.45714515960792,7.50366116523517));
#391790=CARTESIAN_POINT('Ctrl Pts',(-1.23235567333047,2.45087725266272,
7.51860402984325));
#391791=CARTESIAN_POINT('Ctrl Pts',(-1.23271417190462,2.45113512712465,
7.51734760759493));
#391792=CARTESIAN_POINT('Ctrl Pts',(-1.23300338406208,2.45141645289303,
7.51608817408573));
#391793=CARTESIAN_POINT('Ctrl Pts',(-1.23321333356108,2.45173015496622,
7.5148100591312));
#391794=CARTESIAN_POINT('Ctrl Pts',(-1.23340351083418,2.45201431380027,
7.51365231206384));
#391795=CARTESIAN_POINT('Ctrl Pts',(-1.23352912772805,2.45232529934387,
7.51247773061043));
#391796=CARTESIAN_POINT('Ctrl Pts',(-1.23355377319633,2.45267156000965,
7.51129758471022));
#391797=CARTESIAN_POINT('Ctrl Pts',(-1.2335844046988,2.45310192247276,7.50983079813402));
#391798=CARTESIAN_POINT('Ctrl Pts',(-1.23344508972212,2.4535739665468,7.50839324291155));
#391799=CARTESIAN_POINT('Ctrl Pts',(-1.23305574351697,2.45406780194779,
7.50715379678855));
#391800=CARTESIAN_POINT('Ctrl Pts',(-1.23287587678894,2.45429593967352,
7.50658120839351));
#391801=CARTESIAN_POINT('Ctrl Pts',(-1.23260961778089,2.45455527707925,
7.50598221009429));
#391802=CARTESIAN_POINT('Ctrl Pts',(-1.23224743207232,2.45482334770212,
7.50545747549611));
#391803=CARTESIAN_POINT('Ctrl Pts',(-1.23205415856753,2.45496639848405,
7.50517746087247));
#391804=CARTESIAN_POINT('Ctrl Pts',(-1.23183159348026,2.45511365010213,
7.50491486231392));
#391805=CARTESIAN_POINT('Ctrl Pts',(-1.23158471033428,2.45525981197483,
7.50468370960992));
#391806=CARTESIAN_POINT('Ctrl Pts',(-1.23121554215618,2.45547837007868,
7.50433806340447));
#391807=CARTESIAN_POINT('Ctrl Pts',(-1.23078064602178,2.45570056625099,
7.50405484070984));
#391808=CARTESIAN_POINT('Ctrl Pts',(-1.23030898543559,2.45591079803974,
7.50385766036131));
#391809=CARTESIAN_POINT('Ctrl Pts',(-1.23025854866716,2.4559332790618,7.50383657498791));
#391810=CARTESIAN_POINT('Ctrl Pts',(-1.2302077196755,2.45595562650314,7.50381643264937));
#391811=CARTESIAN_POINT('Ctrl Pts',(-1.23015655431109,2.45597782395209,
7.50379723213559));
#391812=CARTESIAN_POINT('Ctrl Pts',(-1.22981500876628,2.45612599918515,
7.50366906242519));
#391813=CARTESIAN_POINT('Ctrl Pts',(-1.22945075886669,2.45627005426621,
7.50358235568538));
#391814=CARTESIAN_POINT('Ctrl Pts',(-1.22909632909184,2.45640046610439,
7.5035341175365));
#391815=CARTESIAN_POINT('Ctrl Pts',(-1.22856490175816,2.45659600389596,
7.50346178989176));
#391816=CARTESIAN_POINT('Ctrl Pts',(-1.22798489283784,2.45678376238722,
7.50346967198527));
#391817=CARTESIAN_POINT('Ctrl Pts',(-1.22740983222607,2.45695056293592,
7.50354272648692));
#391818=CARTESIAN_POINT('Ctrl Pts',(-1.2271732978934,2.45701917145416,7.50357277531559));
#391819=CARTESIAN_POINT('Ctrl Pts',(-1.22693795451662,2.45708427923446,
7.50361331098761));
#391820=CARTESIAN_POINT('Ctrl Pts',(-1.2267088733495,2.45714515960919,7.50366116523658));
#391821=CARTESIAN_POINT('',(-1.16019063351033,2.40916067458745,7.57603338622103));
#391822=CARTESIAN_POINT('Origin',(-1.16402226679194,2.41712371898021,7.58486873427626));
#391823=CARTESIAN_POINT('Ctrl Pts',(-1.22670887339831,2.45714515963697,
7.50366116529968));
#391824=CARTESIAN_POINT('Ctrl Pts',(-1.20457181913612,2.44117710943059,
7.5278357307971));
#391825=CARTESIAN_POINT('Ctrl Pts',(-1.18240010892814,2.42518305082276,
7.55196141284068));
#391826=CARTESIAN_POINT('Ctrl Pts',(-1.1601906346913,2.40916067500333,7.57603338728831));
#391827=CARTESIAN_POINT('Ctrl Pts',(-1.16366703458209,2.40168485817273,
7.59639677331371));
#391828=CARTESIAN_POINT('Ctrl Pts',(-1.150703165123,2.38880037120595,7.59959882295466));
#391829=CARTESIAN_POINT('Ctrl Pts',(-1.15216122323504,2.40703722617454,
7.59642833564546));
#391830=CARTESIAN_POINT('Ctrl Pts',(-1.1613783588536,2.39852620854139,7.58707626057423));
#391831=CARTESIAN_POINT('Ctrl Pts',(-1.15468113347973,2.39749690619124,
7.58809943920598));
#391832=CARTESIAN_POINT('Ctrl Pts',(-1.15122410194199,2.40330752868285,
7.58710240504253));
#391833=CARTESIAN_POINT('Ctrl Pts',(-1.16034302571033,2.40451400592808,
7.58015376756929));
#391834=CARTESIAN_POINT('Ctrl Pts',(-1.15760519591842,2.40371804146506,
7.58205880659761));
#391835=CARTESIAN_POINT('Ctrl Pts',(-1.15649513461972,2.40630548015058,
7.58020924244128));
#391836=CARTESIAN_POINT('Ctrl Pts',(-1.16019063315144,2.40916067384175,
7.57603338509286));
#391837=CARTESIAN_POINT('Ctrl Pts',(-1.16019063315144,2.40916067384175,
7.57603338509286));
#391838=CARTESIAN_POINT('Ctrl Pts',(-1.16019063315144,2.40916067384175,
7.57603338509286));
#391839=CARTESIAN_POINT('Origin',(-1.16402740803779,2.41712124308687,7.58486873427621));
#391840=CARTESIAN_POINT('Ctrl Pts',(-1.14738488275126,2.50018731490473,
7.51098857897448));
#391841=CARTESIAN_POINT('Ctrl Pts',(-1.14767691925914,2.49430724461179,
7.50433767179956));
#391842=CARTESIAN_POINT('Ctrl Pts',(-1.15615057871821,2.49278897373538,
7.50214974420965));
#391843=CARTESIAN_POINT('Ctrl Pts',(-1.14894748356406,2.46872480124226,
7.53887321589168));
#391844=CARTESIAN_POINT('Ctrl Pts',(-1.14923602095631,2.46291518462666,
7.5322040745206));
#391845=CARTESIAN_POINT('Ctrl Pts',(-1.15767055140445,2.46134623082198,
7.53003438070911));
#391846=CARTESIAN_POINT('Ctrl Pts',(-1.15051308514685,2.43720186794752,
7.5666946565923));
#391847=CARTESIAN_POINT('Ctrl Pts',(-1.15079991733676,2.431426585086,7.56004085833295));
#391848=CARTESIAN_POINT('Ctrl Pts',(-1.15919230779772,2.42984404520438,
7.55785582193789));
#391849=CARTESIAN_POINT('Ctrl Pts',(-1.15208161669372,2.40561994067663,
7.59443891967696));
#391850=CARTESIAN_POINT('Ctrl Pts',(-1.15236886475459,2.39983628437403,
7.58783901202978));
#391851=CARTESIAN_POINT('Ctrl Pts',(-1.1607156901291,2.39828396863432,7.58560008491213));
#391852=CARTESIAN_POINT('',(-1.15623297039277,2.49108456570912,7.50366116523517));
#391853=CARTESIAN_POINT('Ctrl Pts',(-1.15623297039293,2.49108456570945,
7.50366116523554));
#391854=CARTESIAN_POINT('Ctrl Pts',(-1.15562413094776,2.49153562229877,
7.50350835821027));
#391855=CARTESIAN_POINT('Ctrl Pts',(-1.15504978507181,2.49193044482337,
7.50345484956));
#391856=CARTESIAN_POINT('Ctrl Pts',(-1.15449319717327,2.49228126653247,
7.50349758195598));
#391857=CARTESIAN_POINT('Ctrl Pts',(-1.15420762630368,2.49246126408686,
7.50351950684424));
#391858=CARTESIAN_POINT('Ctrl Pts',(-1.15389865214386,2.49264752943229,
7.50357029184312));
#391859=CARTESIAN_POINT('Ctrl Pts',(-1.153595774694,2.49281895317992,7.50365515313923));
#391860=CARTESIAN_POINT('Ctrl Pts',(-1.15312982652892,2.4930826723201,7.50378570417639));
#391861=CARTESIAN_POINT('Ctrl Pts',(-1.15266480092322,2.49331930930964,
7.50400001621911));
#391862=CARTESIAN_POINT('Ctrl Pts',(-1.15223506338678,2.49350882914526,
7.50428903009635));
#391863=CARTESIAN_POINT('Ctrl Pts',(-1.15218736582644,2.49352986438893,
7.50432110841318));
#391864=CARTESIAN_POINT('Ctrl Pts',(-1.15214008709819,2.49355034499864,
7.50435406373354));
#391865=CARTESIAN_POINT('Ctrl Pts',(-1.15209326220262,2.49357026247505,
7.50438785222352));
#391866=CARTESIAN_POINT('Ctrl Pts',(-1.15180737370825,2.49369186824209,
7.50459414719561));
#391867=CARTESIAN_POINT('Ctrl Pts',(-1.15153364917505,2.49379394363759,
7.50483629897752));
#391868=CARTESIAN_POINT('Ctrl Pts',(-1.15128303474166,2.49387381126593,
7.5050991045531));
#391869=CARTESIAN_POINT('Ctrl Pts',(-1.15073015412978,2.49405000727601,
7.50567888004914));
#391870=CARTESIAN_POINT('Ctrl Pts',(-1.15026811890362,2.49412555961324,
7.50637912803144));
#391871=CARTESIAN_POINT('Ctrl Pts',(-1.1498937804739,2.49413121733846,7.50710440483569));
#391872=CARTESIAN_POINT('Ctrl Pts',(-1.14980198525928,2.494132604725,7.50728225710685));
#391873=CARTESIAN_POINT('Ctrl Pts',(-1.14971363833864,2.4941299627054,7.50746498566954));
#391874=CARTESIAN_POINT('Ctrl Pts',(-1.14963078956236,2.49412376935997,
7.50764697238949));
#391875=CARTESIAN_POINT('Ctrl Pts',(-1.14918541734167,2.49409047563941,
7.50862528291181));
#391876=CARTESIAN_POINT('Ctrl Pts',(-1.14885819440523,2.4939556593938,7.50965856837421));
#391877=CARTESIAN_POINT('Ctrl Pts',(-1.14860832253323,2.49377157864745,
7.51067959873201));
#391878=CARTESIAN_POINT('Ctrl Pts',(-1.1484708177269,2.49367027878055,7.51124147302578));
#391879=CARTESIAN_POINT('Ctrl Pts',(-1.14835696135857,2.49355368560418,
7.51180065547252));
#391880=CARTESIAN_POINT('Ctrl Pts',(-1.14826164413805,2.49342838141802,
7.512351757165));
#391881=CARTESIAN_POINT('Ctrl Pts',(-1.14793228517129,2.49299540553957,
7.51425603304535));
#391882=CARTESIAN_POINT('Ctrl Pts',(-1.14778983637917,2.4924031262395,7.5162690050518));
#391883=CARTESIAN_POINT('Ctrl Pts',(-1.14780750680636,2.49170562597439,
7.51827788969243));
#391884=CARTESIAN_POINT('Ctrl Pts',(-1.14780846316327,2.49166787594195,
7.51838661432545));
#391885=CARTESIAN_POINT('Ctrl Pts',(-1.14780989531214,2.4916298103943,7.51849533314856));
#391886=CARTESIAN_POINT('Ctrl Pts',(-1.14781180121217,2.4915914356506,7.51860402984325));
#391887=CARTESIAN_POINT('Ctrl Pts',(-1.16019063309945,2.40916067577124,
7.57603338728985));
#391888=CARTESIAN_POINT('Ctrl Pts',(-1.15887005024747,2.43651452986977,
7.55196141284922));
#391889=CARTESIAN_POINT('Ctrl Pts',(-1.15755087359416,2.46382120338538,
7.52783573083105));
#391890=CARTESIAN_POINT('Ctrl Pts',(-1.1562329703845,2.49108456576772,7.50366116530176));
#391891=CARTESIAN_POINT('Origin',(-4.00899494394873E-16,8.32476377985984E-16,
7.49482233047033));
#391892=CARTESIAN_POINT('Origin',(-1.22276082553378,2.44923706764779,7.49482233047033));
#391893=CARTESIAN_POINT('Origin',(0.,0.,7.50366116523517));
#391894=CARTESIAN_POINT('Origin',(-1.15251174268205,2.48306724294369,7.49482233047033));
#391895=CARTESIAN_POINT('Ctrl Pts',(-1.23235481470267,2.4508766349812,7.51860402984325));
#391896=CARTESIAN_POINT('Ctrl Pts',(-1.23853136886432,2.45532033442179,
7.51860402984325));
#391897=CARTESIAN_POINT('Ctrl Pts',(-1.2453154483411,2.45187467749129,7.51860402984325));
#391898=CARTESIAN_POINT('Ctrl Pts',(-1.23464821215601,2.45252660987737,
7.51041458714365));
#391899=CARTESIAN_POINT('Ctrl Pts',(-1.24013859051313,2.45450401000274,
7.51004642900441));
#391900=CARTESIAN_POINT('Ctrl Pts',(-1.24531731930967,2.45187372722002,
7.50729136483008));
#391901=CARTESIAN_POINT('Ctrl Pts',(-1.23389344099837,2.45523844646884,
7.50215815450138));
#391902=CARTESIAN_POINT('Ctrl Pts',(-1.23686619043908,2.4561662531536,7.49877163671531));
#391903=CARTESIAN_POINT('Ctrl Pts',(-1.23995309199552,2.45462516185998,
7.49481588533172));
#391904=CARTESIAN_POINT('Ctrl Pts',(-1.22670862744822,2.4571446670605,7.50366171572174));
#391905=CARTESIAN_POINT('Ctrl Pts',(-1.22834420829843,2.46042079855047,
7.50000045605858));
#391906=CARTESIAN_POINT('Ctrl Pts',(-1.22834420829854,2.46042079855041,
7.49482233047317));
#391907=CARTESIAN_POINT('Origin',(-1.23965492357592,2.4407297925936,7.51860402984325));
#391908=CARTESIAN_POINT('Origin',(-1.23965492357592,2.4407297925936,9.));
#391909=CARTESIAN_POINT('Origin',(-1.23965492357592,2.4407297925936,8.75721825406948));
#391910=CARTESIAN_POINT('Ctrl Pts',(-1.21879855353204,2.4411253357326,8.78942910404912));
#391911=CARTESIAN_POINT('Ctrl Pts',(-1.22331043706215,2.44439570814448,
8.79672699501691));
#391912=CARTESIAN_POINT('Ctrl Pts',(-1.2297870263298,2.43825345469479,8.79893251111267));
#391913=CARTESIAN_POINT('Ctrl Pts',(-1.22772371753385,2.44754537204725,
8.78111911759583));
#391914=CARTESIAN_POINT('Ctrl Pts',(-1.23307697638014,2.45141640935657,
8.78644465894813));
#391915=CARTESIAN_POINT('Ctrl Pts',(-1.24001845580617,2.44722936085515,
8.78817647674132));
#391916=CARTESIAN_POINT('Ctrl Pts',(-1.2332860926436,2.45154649178503,8.76780923932029));
#391917=CARTESIAN_POINT('Ctrl Pts',(-1.23960837464324,2.45611195858344,
8.76988516158374));
#391918=CARTESIAN_POINT('Ctrl Pts',(-1.24641619895659,2.45282715896781,
8.77093053738833));
#391919=CARTESIAN_POINT('Ctrl Pts',(-1.23220150562467,2.45076632819392,
8.75371302330492));
#391920=CARTESIAN_POINT('Ctrl Pts',(-1.23836817271516,2.45522036213663,
8.75300828287559));
#391921=CARTESIAN_POINT('Ctrl Pts',(-1.2451686804961,2.45173501663644,8.75267964240738));
#391922=CARTESIAN_POINT('Origin',(-1.22827143700815,2.43254144629238,8.78727029226991));
#391923=CARTESIAN_POINT('Ctrl Pts',(-1.16293484201941,2.40094160211228,
8.85049129520029));
#391924=CARTESIAN_POINT('Ctrl Pts',(-1.16767542343881,2.40435158745377,
8.85711686593484));
#391925=CARTESIAN_POINT('Ctrl Pts',(-1.17411995340354,2.39873297591287,
8.85933012996512));
#391926=CARTESIAN_POINT('Ctrl Pts',(-1.18230877056806,2.41487761681455,
8.82945683644722));
#391927=CARTESIAN_POINT('Ctrl Pts',(-1.18708870167946,2.41831590709606,
8.83607469902388));
#391928=CARTESIAN_POINT('Ctrl Pts',(-1.19352750769645,2.41265253181511,
8.8382956714852));
#391929=CARTESIAN_POINT('Ctrl Pts',(-1.20165382071392,2.42879285876312,
8.80838214965002));
#391930=CARTESIAN_POINT('Ctrl Pts',(-1.20645261566516,2.43224471814342,
8.81501364461987));
#391931=CARTESIAN_POINT('Ctrl Pts',(-1.21290523209919,2.42655151572733,
8.81722098428721));
#391932=CARTESIAN_POINT('Ctrl Pts',(-1.22097218676271,2.4426889063615,8.78727029226991));
#391933=CARTESIAN_POINT('Ctrl Pts',(-1.22577177880958,2.44614133910699,
8.79393457792714));
#391934=CARTESIAN_POINT('Ctrl Pts',(-1.23225539332381,2.44043150916127,
8.79610912703474));
#391935=CARTESIAN_POINT('Origin',(-1.17023409226486,2.39079414204316,8.85049129520029));
#391936=CARTESIAN_POINT('Ctrl Pts',(-1.15205371787331,2.40618167532513,
8.85049129520029));
#391937=CARTESIAN_POINT('Ctrl Pts',(-1.15176404759817,2.41201410220893,
8.85711686593484));
#391938=CARTESIAN_POINT('Ctrl Pts',(-1.14335314149695,2.41354949162871,
8.85933012996512));
#391939=CARTESIAN_POINT('Ctrl Pts',(-1.1523099849843,2.40102181145301,8.86332496987233));
#391940=CARTESIAN_POINT('Ctrl Pts',(-1.14827702912887,2.4032772851161,8.86648636486737));
#391941=CARTESIAN_POINT('Ctrl Pts',(-1.14408717074441,2.39911541190672,
8.87206031107457));
#391942=CARTESIAN_POINT('Ctrl Pts',(-1.15871241903328,2.3979043374364,8.86341338519875));
#391943=CARTESIAN_POINT('Ctrl Pts',(-1.16299120812191,2.39612517061758,
8.86654584966059));
#391944=CARTESIAN_POINT('Ctrl Pts',(-1.16228834154897,2.39024043346389,
8.87215952290714));
#391945=CARTESIAN_POINT('Ctrl Pts',(-1.16293484201941,2.40094160211228,
8.85049129520029));
#391946=CARTESIAN_POINT('Ctrl Pts',(-1.16767542343881,2.40435158745377,
8.85711686593484));
#391947=CARTESIAN_POINT('Ctrl Pts',(-1.17411995340354,2.39873297591287,
8.85933012996512));
#391948=CARTESIAN_POINT('Origin',(-1.13956910603494,2.40556162109757,8.85049129520029));
#391949=CARTESIAN_POINT('Ctrl Pts',(-1.14850738206912,2.47758611705878,
8.78727029226991));
#391950=CARTESIAN_POINT('Ctrl Pts',(-1.14821410598634,2.48349114583244,
8.79393457792714));
#391951=CARTESIAN_POINT('Ctrl Pts',(-1.13970751364643,2.48500021903835,
8.79610912703474));
#391952=CARTESIAN_POINT('Ctrl Pts',(-1.14968781879483,2.45381836632826,
8.80838214965003));
#391953=CARTESIAN_POINT('Ctrl Pts',(-1.14939459141807,2.45972241442017,
8.81501364461993));
#391954=CARTESIAN_POINT('Ctrl Pts',(-1.14092032599118,2.46121761944618,
8.81722098428721));
#391955=CARTESIAN_POINT('Ctrl Pts',(-1.15086988603566,2.43001778564899,
8.82945683644723));
#391956=CARTESIAN_POINT('Ctrl Pts',(-1.15057781132211,2.43589862520227,
8.8360746990239));
#391957=CARTESIAN_POINT('Ctrl Pts',(-1.14213547634267,2.43740162972406,
8.83829567148519));
#391958=CARTESIAN_POINT('Ctrl Pts',(-1.15205371787331,2.40618167532513,
8.85049129520029));
#391959=CARTESIAN_POINT('Ctrl Pts',(-1.15176404759817,2.41201410220893,
8.85711686593484));
#391960=CARTESIAN_POINT('Ctrl Pts',(-1.14335314149695,2.41354949162871,
8.85933012996512));
#391961=CARTESIAN_POINT('Origin',(-1.13602277023075,2.47696606283122,8.78727029226991));
#391962=CARTESIAN_POINT('Ctrl Pts',(-1.14782096758312,2.49140650154879,
8.75374538247848));
#391963=CARTESIAN_POINT('Ctrl Pts',(-1.14745713259866,2.49899675862558,
8.75304829418602));
#391964=CARTESIAN_POINT('Ctrl Pts',(-1.14050185255763,2.5021423464498,8.75272238421917));
#391965=CARTESIAN_POINT('Ctrl Pts',(-1.1477554910923,2.49272486027965,8.76769408445018));
#391966=CARTESIAN_POINT('Ctrl Pts',(-1.1473818110897,2.50050608886052,8.76974318093968));
#391967=CARTESIAN_POINT('Ctrl Pts',(-1.14057750714365,2.50378020020404,
8.7707786988043));
#391968=CARTESIAN_POINT('Ctrl Pts',(-1.14809108629952,2.48596770444543,
8.78108014887992));
#391969=CARTESIAN_POINT('Ctrl Pts',(-1.14777820098109,2.49256219760851,
8.78639403366326));
#391970=CARTESIAN_POINT('Ctrl Pts',(-1.14019478891025,2.49539308741435,
8.78812224174741));
#391971=CARTESIAN_POINT('Ctrl Pts',(-1.14864105272563,2.4748942176888,8.78944554828685));
#391972=CARTESIAN_POINT('Ctrl Pts',(-1.14838295601785,2.48045207732236,
8.79673892988686));
#391973=CARTESIAN_POINT('Ctrl Pts',(-1.13955245350738,2.48168730188856,
8.79894799272499));
#391974=CARTESIAN_POINT('Origin',(-1.1353271893738,2.49097138142304,8.75721825406948));
#391975=CARTESIAN_POINT('Origin',(-1.1353271893738,2.49097138142304,9.));
#391976=CARTESIAN_POINT('Origin',(-1.1353271893738,2.49097138142304,7.51860402984325));
#391977=CARTESIAN_POINT('Ctrl Pts',(-1.15623263920031,2.49108385216065,
7.50366195182966));
#391978=CARTESIAN_POINT('Ctrl Pts',(-1.1577743533791,2.49440544953254,7.50000065167735));
#391979=CARTESIAN_POINT('Ctrl Pts',(-1.157774353379,2.49440544953259,7.49482233047108));
#391980=CARTESIAN_POINT('Ctrl Pts',(-1.15025678379844,2.49551588914409,
7.50215800491337));
#391981=CARTESIAN_POINT('Ctrl Pts',(-1.14912704537262,2.49841905780326,
7.49877273257265));
#391982=CARTESIAN_POINT('Ctrl Pts',(-1.14599578422563,2.49987245381925,
7.49481816995647));
#391983=CARTESIAN_POINT('Ctrl Pts',(-1.14767232585334,2.49440656796784,
7.51043025814041));
#391984=CARTESIAN_POINT('Ctrl Pts',(-1.14579758885198,2.49993631643975,
7.51006209594514));
#391985=CARTESIAN_POINT('Ctrl Pts',(-1.14050902793523,2.50234673001258,
7.50731281821699));
#391986=CARTESIAN_POINT('Ctrl Pts',(-1.14781187609327,2.49158992609926,
7.51860402984325));
#391987=CARTESIAN_POINT('Ctrl Pts',(-1.14743534212812,2.49918987607039,
7.51860402984325));
#391988=CARTESIAN_POINT('Ctrl Pts',(-1.14051133179102,2.50234567996835,
7.51860402984325));
#391989=CARTESIAN_POINT('Origin',(0.,0.,7.5));
#391990=CARTESIAN_POINT('Origin',(-1.30385128920421,2.32742558187726,7.5));
#391991=CARTESIAN_POINT('',(-1.30385128920421,2.32742558187726,7.59394543036555));
#391992=CARTESIAN_POINT('',(-1.30385128920421,2.32742558187726,8.85049129520029));
#391993=CARTESIAN_POINT('',(-1.30385128920421,2.32742558187726,7.5));
#391994=CARTESIAN_POINT('',(-1.30488713801675,2.39891053004237,8.78727029226991));
#391995=CARTESIAN_POINT('Ctrl Pts',(-1.30385128920421,2.32742558187726,
8.85049129520029));
#391996=CARTESIAN_POINT('Ctrl Pts',(-1.30419707404391,2.35128853469733,
8.82945686509571));
#391997=CARTESIAN_POINT('Ctrl Pts',(-1.30454234483264,2.37511601235256,
8.80838212259895));
#391998=CARTESIAN_POINT('Ctrl Pts',(-1.30488713801675,2.39891053004237,
8.78727029226991));
#391999=CARTESIAN_POINT('',(-1.30509031014835,2.41293163922359,8.75721825406948));
#392000=CARTESIAN_POINT('Origin',(-1.30447909650469,2.37073725481655,8.75937679713112));
#392001=CARTESIAN_POINT('',(-1.30509031014835,2.41293163922359,7.51860402984325));
#392002=CARTESIAN_POINT('',(-1.30509031014835,2.41293163922359,7.5));
#392003=CARTESIAN_POINT('Ctrl Pts',(-1.30509031014835,2.4129316392236,7.51860402984325));
#392004=CARTESIAN_POINT('Ctrl Pts',(-1.30493075003822,2.4019202386567,7.52834476460825));
#392005=CARTESIAN_POINT('Ctrl Pts',(-1.30477108634398,2.39090168964745,
7.53807742314407));
#392006=CARTESIAN_POINT('Ctrl Pts',(-1.30461131558764,2.37987575217738,
7.54780169004674));
#392007=CARTESIAN_POINT('Ctrl Pts',(-1.30435824734447,2.36241126312586,
7.5632044032688));
#392008=CARTESIAN_POINT('Ctrl Pts',(-1.3041049101745,2.34492821517237,7.57858609112103));
#392009=CARTESIAN_POINT('Ctrl Pts',(-1.30385128920421,2.32742558187726,
7.59394543036555));
#392010=CARTESIAN_POINT('Origin',(-1.54744838731665,2.4674493883293,7.5));
#392011=CARTESIAN_POINT('',(-1.38685191115371,2.3668843634066,8.75721825406948));
#392012=CARTESIAN_POINT('',(-1.37496718403118,2.3594421834296,8.78727029226991));
#392013=CARTESIAN_POINT('Origin',(-1.34479931381131,2.34055115485281,8.75658640621015));
#392014=CARTESIAN_POINT('',(-1.31437432427029,2.32149911893914,8.85049129520029));
#392015=CARTESIAN_POINT('Ctrl Pts',(-1.37496718403118,2.3594421834296,8.78727029226991));
#392016=CARTESIAN_POINT('Ctrl Pts',(-1.35479821265379,2.34681243489655,
8.80838212259896));
#392017=CARTESIAN_POINT('Ctrl Pts',(-1.33460130338718,2.33416519174224,
8.82945686509571));
#392018=CARTESIAN_POINT('Ctrl Pts',(-1.31437432427029,2.32149911893914,
8.85049129520029));
#392019=CARTESIAN_POINT('',(-1.31437432427029,2.32149911893914,7.59394543036555));
#392020=CARTESIAN_POINT('',(-1.31437432427029,2.32149911893914,7.5));
#392021=CARTESIAN_POINT('',(-1.38685191115371,2.3668843634066,7.51860402984325));
#392022=CARTESIAN_POINT('Ctrl Pts',(-1.31437432427029,2.32149911893914,
7.59394543036555));
#392023=CARTESIAN_POINT('Ctrl Pts',(-1.32921009923997,2.33078923610248,
7.57858609112103));
#392024=CARTESIAN_POINT('Ctrl Pts',(-1.34402927306631,2.34006895768037,
7.56320440326857));
#392025=CARTESIAN_POINT('Ctrl Pts',(-1.35883271579176,2.34933882849071,
7.54780169004651));
#392026=CARTESIAN_POINT('Ctrl Pts',(-1.36817864245192,2.35519121933988,
7.53807742314383));
#392027=CARTESIAN_POINT('Ctrl Pts',(-1.37751830642366,2.36103968851259,
7.52834476460825));
#392028=CARTESIAN_POINT('Ctrl Pts',(-1.38685191115371,2.3668843634066,7.51860402984324));
#392029=CARTESIAN_POINT('',(-1.38685191115371,2.3668843634066,7.5));
#392030=CARTESIAN_POINT('Origin',(-1.31072556753554,2.3273259705153,7.5));
#392031=CARTESIAN_POINT('Ctrl Pts',(-1.31437432427029,2.32149911893914,
8.85049129520029));
#392032=CARTESIAN_POINT('Ctrl Pts',(-1.31421018800106,2.32139633730656,
8.85097269580138));
#392033=CARTESIAN_POINT('Ctrl Pts',(-1.31404365844039,2.32130198148025,
8.85143669361005));
#392034=CARTESIAN_POINT('Ctrl Pts',(-1.31386663644422,2.32121246734861,
8.8519052845931));
#392035=CARTESIAN_POINT('Ctrl Pts',(-1.31352039264604,2.3210373833839,8.85282181883899));
#392036=CARTESIAN_POINT('Ctrl Pts',(-1.31314282619048,2.32088550184337,
8.85372622499635));
#392037=CARTESIAN_POINT('Ctrl Pts',(-1.31272225812329,2.32076874418766,
8.8546225773507));
#392038=CARTESIAN_POINT('Ctrl Pts',(-1.31237311745107,2.32067181612874,
8.85536669723986));
#392039=CARTESIAN_POINT('Ctrl Pts',(-1.31199427006962,2.32059904195065,
8.85610498449051));
#392040=CARTESIAN_POINT('Ctrl Pts',(-1.31157749224829,2.32056509502167,
8.85681338218371));
#392041=CARTESIAN_POINT('Ctrl Pts',(-1.31119926572088,2.3205342881303,8.85745625420284));
#392042=CARTESIAN_POINT('Ctrl Pts',(-1.31078510535871,2.32053447481713,
8.85808743050666));
#392043=CARTESIAN_POINT('Ctrl Pts',(-1.31032267718111,2.32059145661445,
8.8586680450841));
#392044=CARTESIAN_POINT('Ctrl Pts',(-1.31010932284418,2.32061774678053,
8.85893592806396));
#392045=CARTESIAN_POINT('Ctrl Pts',(-1.3098856160485,2.32065635649648,8.85919241173848));
#392046=CARTESIAN_POINT('Ctrl Pts',(-1.30965004993184,2.32071138836426,
8.85943017985534));
#392047=CARTESIAN_POINT('Ctrl Pts',(-1.30933196593932,2.32078569767694,
8.8597512372));
#392048=CARTESIAN_POINT('Ctrl Pts',(-1.30898430850719,2.32089246461108,
8.86004599534705));
#392049=CARTESIAN_POINT('Ctrl Pts',(-1.30861431218768,2.32104036257474,
8.86026130871721));
#392050=CARTESIAN_POINT('Ctrl Pts',(-1.3084788461038,2.32109451218892,8.86034014101235));
#392051=CARTESIAN_POINT('Ctrl Pts',(-1.30833834607233,2.32115497735333,
8.86040910639692));
#392052=CARTESIAN_POINT('Ctrl Pts',(-1.30819677290975,2.32122041970921,
8.86046313645506));
#392053=CARTESIAN_POINT('Ctrl Pts',(-1.30797584917522,2.32132254195748,
8.86054744990829));
#392054=CARTESIAN_POINT('Ctrl Pts',(-1.30774634336653,2.32143970543498,
8.86059655985668));
#392055=CARTESIAN_POINT('Ctrl Pts',(-1.30752284118751,2.32156413516752,
8.86059725258816));
#392056=CARTESIAN_POINT('Ctrl Pts',(-1.30729882262916,2.32168885238245,
8.86059794692011));
#392057=CARTESIAN_POINT('Ctrl Pts',(-1.30707964340311,2.32182457387434,
8.86056369958366));
#392058=CARTESIAN_POINT('Ctrl Pts',(-1.30687527651367,2.32196069795111,
8.86048590497774));
#392059=CARTESIAN_POINT('Ctrl Pts',(-1.30682194284026,2.32199622228224,
8.86046560290182));
#392060=CARTESIAN_POINT('Ctrl Pts',(-1.30676897434054,2.32203231156963,
8.86044257503091));
#392061=CARTESIAN_POINT('Ctrl Pts',(-1.30671798930176,2.32206782349643,
8.86041778462583));
#392062=CARTESIAN_POINT('Ctrl Pts',(-1.30637492325793,2.32230677469719,
8.86025097596201));
#392063=CARTESIAN_POINT('Ctrl Pts',(-1.30607581555712,2.32255192162361,
8.8599848982295));
#392064=CARTESIAN_POINT('Ctrl Pts',(-1.30582402572536,2.3227895562746,8.85968173251461));
#392065=CARTESIAN_POINT('Ctrl Pts',(-1.30569084333019,2.32291525139013,
8.85952137522076));
#392066=CARTESIAN_POINT('Ctrl Pts',(-1.30556820129054,2.32304112870655,
8.85934740853961));
#392067=CARTESIAN_POINT('Ctrl Pts',(-1.30545671568009,2.32316432824297,
8.8591675900182));
#392068=CARTESIAN_POINT('Ctrl Pts',(-1.30500904300506,2.32365903841954,
8.85844552518694));
#392069=CARTESIAN_POINT('Ctrl Pts',(-1.30471371598152,2.32413650056779,
8.85759444184122));
#392070=CARTESIAN_POINT('Ctrl Pts',(-1.30450788915529,2.32454742583243,
8.85683498915136));
#392071=CARTESIAN_POINT('Ctrl Pts',(-1.30448634992609,2.32459042806699,
8.85675551444997));
#392072=CARTESIAN_POINT('Ctrl Pts',(-1.30446581007887,2.32463270692617,
8.8566769979365));
#392073=CARTESIAN_POINT('Ctrl Pts',(-1.30444621042252,2.32467420873586,
8.85659965593547));
#392074=CARTESIAN_POINT('Ctrl Pts',(-1.304181653261,2.32523440228086,8.85555568965886));
#392075=CARTESIAN_POINT('Ctrl Pts',(-1.30400830047063,2.32581099027345,
8.85434650606346));
#392076=CARTESIAN_POINT('Ctrl Pts',(-1.30391934352441,2.32640503368348,
8.85297329937117));
#392077=CARTESIAN_POINT('Ctrl Pts',(-1.30386931066238,2.32673914690602,
8.85220095427747));
#392078=CARTESIAN_POINT('Ctrl Pts',(-1.30384626657237,2.32707896510008,
8.85137579139183));
#392079=CARTESIAN_POINT('Ctrl Pts',(-1.30385128920421,2.32742558187726,
8.85049129520029));
#392080=CARTESIAN_POINT('Origin',(-1.31072556753554,2.3273259705153,7.59394543036555));
#392081=CARTESIAN_POINT('Ctrl Pts',(-1.31389778130986,2.32120070918671,
7.59443877723642));
#392082=CARTESIAN_POINT('Ctrl Pts',(-1.3089898473347,2.31812737585884,7.58783886950016));
#392083=CARTESIAN_POINT('Ctrl Pts',(-1.30294132309853,2.32408510496489,
7.58559994247159));
#392084=CARTESIAN_POINT('Ctrl Pts',(-1.34069004888757,2.3379779456558,7.56670252222137));
#392085=CARTESIAN_POINT('Ctrl Pts',(-1.33578920827042,2.33490905416713,
7.5600487499903));
#392086=CARTESIAN_POINT('Ctrl Pts',(-1.32968985135374,2.34088686333599,
7.55786368756705));
#392087=CARTESIAN_POINT('Ctrl Pts',(-1.36743228458244,2.35472385231203,
7.53888913333557));
#392088=CARTESIAN_POINT('Ctrl Pts',(-1.36250231802953,2.35163672225097,
7.53222002137277));
#392089=CARTESIAN_POINT('Ctrl Pts',(-1.35638999749711,2.35765685368049,
7.53005029815326));
#392090=CARTESIAN_POINT('Ctrl Pts',(-1.39412327829024,2.3714376713918,7.51101258149734));
#392091=CARTESIAN_POINT('Ctrl Pts',(-1.38913355158474,2.36831311970495,
7.5043616886572));
#392092=CARTESIAN_POINT('Ctrl Pts',(-1.38304039838402,2.37439431741735,
7.50217374673251));
#392093=CARTESIAN_POINT('',(-1.38161829930508,2.37350118398176,7.50366116523517));
#392094=CARTESIAN_POINT('Ctrl Pts',(-1.38685191115371,2.3668843634066,7.51860402984325));
#392095=CARTESIAN_POINT('Ctrl Pts',(-1.38722619522759,2.36711873895529,
7.51734760759493));
#392096=CARTESIAN_POINT('Ctrl Pts',(-1.38753283777152,2.36738095682315,
7.51608817408572));
#392097=CARTESIAN_POINT('Ctrl Pts',(-1.3877624548676,2.3676805628512,7.51481005913119));
#392098=CARTESIAN_POINT('Ctrl Pts',(-1.3879704475201,2.36795195315073,7.51365231206383));
#392099=CARTESIAN_POINT('Ctrl Pts',(-1.38811573123277,2.36825425143916,
7.51247773061043));
#392100=CARTESIAN_POINT('Ctrl Pts',(-1.38816251106133,2.36859822163469,
7.51129758471022));
#392101=CARTESIAN_POINT('Ctrl Pts',(-1.38822065304577,2.36902573730485,
7.50983079813402));
#392102=CARTESIAN_POINT('Ctrl Pts',(-1.38811186827432,2.36950573745492,
7.50839324291155));
#392103=CARTESIAN_POINT('Ctrl Pts',(-1.38775496216549,2.37002350371512,
7.50715379678855));
#392104=CARTESIAN_POINT('Ctrl Pts',(-1.38759008182721,2.37026269680826,
7.50658120839351));
#392105=CARTESIAN_POINT('Ctrl Pts',(-1.38734098568148,2.37053856065069,
7.50598221009429));
#392106=CARTESIAN_POINT('Ctrl Pts',(-1.38699671946607,2.37082928581175,
7.50545747549611));
#392107=CARTESIAN_POINT('Ctrl Pts',(-1.38681300835749,2.37098442575647,
7.50517746087247));
#392108=CARTESIAN_POINT('Ctrl Pts',(-1.38660033499762,2.37114563462441,
7.50491486231392));
#392109=CARTESIAN_POINT('Ctrl Pts',(-1.38636332372289,2.37130731404934,
7.50468370960992));
#392110=CARTESIAN_POINT('Ctrl Pts',(-1.38600891710619,2.3715490757885,7.50433806340446));
#392111=CARTESIAN_POINT('Ctrl Pts',(-1.38558915067018,2.37179867932595,
7.50405484070983));
#392112=CARTESIAN_POINT('Ctrl Pts',(-1.3851319287582,2.37203869856845,7.50385766036131));
#392113=CARTESIAN_POINT('Ctrl Pts',(-1.38508303598155,2.37206436489569,
7.50383657498791));
#392114=CARTESIAN_POINT('Ctrl Pts',(-1.38503374322899,2.37208992304649,
7.50381643264937));
#392115=CARTESIAN_POINT('Ctrl Pts',(-1.38498410518475,2.37211535306456,
7.50379723213559));
#392116=CARTESIAN_POINT('Ctrl Pts',(-1.38465275500166,2.3722851067539,7.50366906242519));
#392117=CARTESIAN_POINT('Ctrl Pts',(-1.38429848313329,2.37245220342954,
7.50358235568538));
#392118=CARTESIAN_POINT('Ctrl Pts',(-1.38395313708759,2.37260505571625,
7.5035341175365));
#392119=CARTESIAN_POINT('Ctrl Pts',(-1.38343532977768,2.37283424042064,
7.50346178989176));
#392120=CARTESIAN_POINT('Ctrl Pts',(-1.38286854227573,2.37305877444105,
7.50346967198527));
#392121=CARTESIAN_POINT('Ctrl Pts',(-1.38230535013551,2.37326207654003,
7.50354272648693));
#392122=CARTESIAN_POINT('Ctrl Pts',(-1.38207369755085,2.37334569890144,
7.50357277531559));
#392123=CARTESIAN_POINT('Ctrl Pts',(-1.38184300918209,2.37342575141275,
7.50361331098761));
#392124=CARTESIAN_POINT('Ctrl Pts',(-1.3816182993058,2.37350118398298,7.50366116523659));
#392125=CARTESIAN_POINT('',(-1.31216235181343,2.32987712649127,7.57603338622103));
#392126=CARTESIAN_POINT('Origin',(-1.31649630659949,2.3375783163681,7.58486873427625));
#392127=CARTESIAN_POINT('Ctrl Pts',(-1.38161829935628,2.37350118400758,
7.50366116529968));
#392128=CARTESIAN_POINT('Ctrl Pts',(-1.35850365155688,2.35898426780923,
7.52783573079709));
#392129=CARTESIAN_POINT('Ctrl Pts',(-1.33535275265205,2.34444361706052,
7.55196141284069));
#392130=CARTESIAN_POINT('Ctrl Pts',(-1.31216235301862,2.32987712683062,
7.57603338728831));
#392131=CARTESIAN_POINT('Ctrl Pts',(-1.31515263304416,2.32219393616178,
7.5963967733137));
#392132=CARTESIAN_POINT('Ctrl Pts',(-1.30074331794104,2.30960147554731,
7.59974925422225));
#392133=CARTESIAN_POINT('Ctrl Pts',(-1.30404198763951,2.328451335077,7.59639677331373));
#392134=CARTESIAN_POINT('Ctrl Pts',(-1.31266628426872,2.31918841227222,
7.58707626057421));
#392135=CARTESIAN_POINT('Ctrl Pts',(-1.30579990181482,2.31857995225015,
7.58811717123965));
#392136=CARTESIAN_POINT('Ctrl Pts',(-1.30276074036386,2.32476711066714,
7.58707626057425));
#392137=CARTESIAN_POINT('Ctrl Pts',(-1.3120167178241,2.32523024110926,7.58015376756929));
#392138=CARTESIAN_POINT('Ctrl Pts',(-1.30919143812975,2.32460196840813,
7.58208760766041));
#392139=CARTESIAN_POINT('Ctrl Pts',(-1.30826409698651,2.32734367779125,
7.58015376756931));
#392140=CARTESIAN_POINT('Ctrl Pts',(-1.3121623514075,2.32987712577009,7.57603338509286));
#392141=CARTESIAN_POINT('Ctrl Pts',(-1.3121623514075,2.32987712577009,7.57603338509286));
#392142=CARTESIAN_POINT('Ctrl Pts',(-1.3121623514075,2.32987712577009,7.57603338509286));
#392143=CARTESIAN_POINT('Origin',(-1.31650127865107,2.33757551616096,7.5848687342762));
#392144=CARTESIAN_POINT('Ctrl Pts',(-1.30521500871194,2.42153721008159,
7.51098857897448));
#392145=CARTESIAN_POINT('Ctrl Pts',(-1.30512970780232,2.4156505101804,7.50433767179956));
#392146=CARTESIAN_POINT('Ctrl Pts',(-1.31348868127019,2.41359244952876,
7.50214974420965));
#392147=CARTESIAN_POINT('Ctrl Pts',(-1.30475858882228,2.39003922334998,
7.53887321589168));
#392148=CARTESIAN_POINT('Ctrl Pts',(-1.30467430996893,2.38422305656061,
7.53220407452061));
#392149=CARTESIAN_POINT('Ctrl Pts',(-1.31299098755427,2.38211692411853,
7.53003438070911));
#392150=CARTESIAN_POINT('Ctrl Pts',(-1.30430129243808,2.35848074886471,
7.56669465659231));
#392151=CARTESIAN_POINT('Ctrl Pts',(-1.30421751165707,2.35269895453971,
7.56004085833296));
#392152=CARTESIAN_POINT('Ctrl Pts',(-1.31249126537342,2.350581963853,7.55785582193789));
#392153=CARTESIAN_POINT('Ctrl Pts',(-1.303843140241,2.32686321388928,7.59443891967696));
#392154=CARTESIAN_POINT('Ctrl Pts',(-1.30375923798832,2.3210730366824,7.58783901202978));
#392155=CARTESIAN_POINT('Ctrl Pts',(-1.31198945670398,2.31898912740397,
7.58560008491213));
#392156=CARTESIAN_POINT('',(-1.31346170186504,2.41188626453887,7.50366116523517));
#392157=CARTESIAN_POINT('Ctrl Pts',(-1.31346170186522,2.4118862645392,7.50366116523554));
#392158=CARTESIAN_POINT('Ctrl Pts',(-1.31288301264089,2.41237540286156,
7.50350835821027));
#392159=CARTESIAN_POINT('Ctrl Pts',(-1.31233514318615,2.41280621264755,
7.50345484956));
#392160=CARTESIAN_POINT('Ctrl Pts',(-1.31180217608121,2.41319197426493,
7.50349758195598));
#392161=CARTESIAN_POINT('Ctrl Pts',(-1.31152872443051,2.41338989858347,
7.50351950684424));
#392162=CARTESIAN_POINT('Ctrl Pts',(-1.3112323191529,2.41359557726915,7.50357029184312));
#392163=CARTESIAN_POINT('Ctrl Pts',(-1.31094104715446,2.41378605423315,
7.50365515313924));
#392164=CARTESIAN_POINT('Ctrl Pts',(-1.31049295287318,2.41407908493551,
7.50378570417639));
#392165=CARTESIAN_POINT('Ctrl Pts',(-1.31004404409644,2.41434503002183,
7.50400001621911));
#392166=CARTESIAN_POINT('Ctrl Pts',(-1.30962733207942,2.41456169384711,
7.50428903009635));
#392167=CARTESIAN_POINT('Ctrl Pts',(-1.30958108025152,2.4145857418648,7.50432110841318));
#392168=CARTESIAN_POINT('Ctrl Pts',(-1.30953521085965,2.41460920955342,
7.50435406373354));
#392169=CARTESIAN_POINT('Ctrl Pts',(-1.30948975828795,2.4146320861886,7.50438785222352));
#392170=CARTESIAN_POINT('Ctrl Pts',(-1.3092122484904,2.41477175904228,7.50459414719561));
#392171=CARTESIAN_POINT('Ctrl Pts',(-1.30894562634665,2.41489116230398,
7.50483629897752));
#392172=CARTESIAN_POINT('Ctrl Pts',(-1.30870064396402,2.4149869227576,7.5050991045531));
#392173=CARTESIAN_POINT('Ctrl Pts',(-1.30816018822177,2.4151981799365,7.50567888004914));
#392174=CARTESIAN_POINT('Ctrl Pts',(-1.30770394295141,2.41530317974193,
7.50637912803144));
#392175=CARTESIAN_POINT('Ctrl Pts',(-1.30733073613184,2.41533280978828,
7.50710440483569));
#392176=CARTESIAN_POINT('Ctrl Pts',(-1.30723921841049,2.41534007566389,
7.50728225710685));
#392177=CARTESIAN_POINT('Ctrl Pts',(-1.30715088373329,2.41534309947924,
7.50746498566954));
#392178=CARTESIAN_POINT('Ctrl Pts',(-1.3070678083697,2.41534222699803,7.50764697238949));
#392179=CARTESIAN_POINT('Ctrl Pts',(-1.30662121807801,2.41533753677913,
7.50862528291182));
#392180=CARTESIAN_POINT('Ctrl Pts',(-1.30628602974968,2.41522396277348,
7.50965856837421));
#392181=CARTESIAN_POINT('Ctrl Pts',(-1.30602487717232,2.41505626958658,
7.51067959873201));
#392182=CARTESIAN_POINT('Ctrl Pts',(-1.3058811645796,2.4149639878143,7.51124147302578));
#392183=CARTESIAN_POINT('Ctrl Pts',(-1.30576007199094,2.41485492899368,
7.51180065547253));
#392184=CARTESIAN_POINT('Ctrl Pts',(-1.3056569223431,2.4147359892537,7.51235175716501));
#392185=CARTESIAN_POINT('Ctrl Pts',(-1.30530049921988,2.41432500507208,
7.51425603304536));
#392186=CARTESIAN_POINT('Ctrl Pts',(-1.30512039563903,2.41374306939881,
7.5162690050518));
#392187=CARTESIAN_POINT('Ctrl Pts',(-1.30509334076502,2.41304587007464,
7.51827788969243));
#392188=CARTESIAN_POINT('Ctrl Pts',(-1.30509187650411,2.41300813632969,
7.51838661432545));
#392189=CARTESIAN_POINT('Ctrl Pts',(-1.30509086684246,2.41297005723369,
7.51849533314856));
#392190=CARTESIAN_POINT('Ctrl Pts',(-1.30509031014834,2.4129316392236,7.51860402984325));
#392191=CARTESIAN_POINT('Ctrl Pts',(-1.31216235147924,2.32987712769896,
7.57603338728985));
#392192=CARTESIAN_POINT('Ctrl Pts',(-1.31259704935576,2.35725939040438,
7.55196141284922));
#392193=CARTESIAN_POINT('Ctrl Pts',(-1.31303012767146,2.38459447936899,
7.52783573083105));
#392194=CARTESIAN_POINT('Ctrl Pts',(-1.31346170186054,2.41188626459788,
7.50366116530176));
#392195=CARTESIAN_POINT('Origin',(-4.53412748053612E-16,8.05080247188564E-16,
7.49482233047033));
#392196=CARTESIAN_POINT('Origin',(-1.37717168998615,2.36586229233671,7.49482233047033));
#392197=CARTESIAN_POINT('Origin',(0.,0.,7.50366116523517));
#392198=CARTESIAN_POINT('Origin',(-1.30923444818252,2.40412383410095,7.49482233047033));
#392199=CARTESIAN_POINT('Ctrl Pts',(-1.38685101471506,2.36688380200664,
7.51860402984325));
#392200=CARTESIAN_POINT('Ctrl Pts',(-1.39329958728443,2.37092263820629,
7.51860402984325));
#392201=CARTESIAN_POINT('Ctrl Pts',(-1.39984896414483,2.36704940328305,
7.51860402984325));
#392202=CARTESIAN_POINT('Ctrl Pts',(-1.38924541439192,2.36838344837309,
7.51041458714366));
#392203=CARTESIAN_POINT('Ctrl Pts',(-1.39485120463889,2.37000501596871,
7.51004642900442));
#392204=CARTESIAN_POINT('Ctrl Pts',(-1.39985077038519,2.36704833509086,
7.50729136483009));
#392205=CARTESIAN_POINT('Ctrl Pts',(-1.38866594195955,2.37113807155955,
7.50215815450138));
#392206=CARTESIAN_POINT('Ctrl Pts',(-1.3916920283461,2.37187350725536,7.4987716367153));
#392207=CARTESIAN_POINT('Ctrl Pts',(-1.39467384947402,2.37013780383729,
7.49481588533171));
#392208=CARTESIAN_POINT('Ctrl Pts',(-1.38161802235204,2.37350070820124,
7.50366171572174));
#392209=CARTESIAN_POINT('Ctrl Pts',(-1.38346014519123,2.37666531650283,
7.50000045605858));
#392210=CARTESIAN_POINT('Ctrl Pts',(-1.38346014519134,2.37666531650276,
7.49482233047317));
#392211=CARTESIAN_POINT('Origin',(-1.39348601430781,2.35629008781359,7.51860402984325));
#392212=CARTESIAN_POINT('Origin',(-1.39348601430781,2.35629008781359,9.));
#392213=CARTESIAN_POINT('Origin',(-1.39348601430781,2.35629008781359,8.75721825406948));
#392214=CARTESIAN_POINT('Ctrl Pts',(-1.37269783844895,2.35802109048349,
8.78942910404912));
#392215=CARTESIAN_POINT('Ctrl Pts',(-1.3774099853103,2.36099566619421,8.7967269950169));
#392216=CARTESIAN_POINT('Ctrl Pts',(-1.38347973220099,2.35445107616389,
8.79893251111267));
#392217=CARTESIAN_POINT('Ctrl Pts',(-1.38201599788306,2.36385609892403,
8.78111911759582));
#392218=CARTESIAN_POINT('Ctrl Pts',(-1.38760627609688,2.36737619830013,
8.78644465894816));
#392219=CARTESIAN_POINT('Ctrl Pts',(-1.39426522839041,2.36275301042509,
8.78817647674132));
#392220=CARTESIAN_POINT('Ctrl Pts',(-1.38782329711835,2.36749261533528,
8.7678092393203));
#392221=CARTESIAN_POINT('Ctrl Pts',(-1.39442509977365,2.37164363189404,
8.76988516158372));
#392222=CARTESIAN_POINT('Ctrl Pts',(-1.40100847884784,2.36792940245016,
8.77093053738833));
#392223=CARTESIAN_POINT('Ctrl Pts',(-1.38669095324687,2.36678354440285,
8.75371302330492));
#392224=CARTESIAN_POINT('Ctrl Pts',(-1.39313032119297,2.37083332733808,
8.7530082828756));
#392225=CARTESIAN_POINT('Ctrl Pts',(-1.39969354974842,2.36691943282452,
8.75267964240738));
#392226=CARTESIAN_POINT('Origin',(-1.38160128718528,2.34884790783659,8.78727029226991));
#392227=CARTESIAN_POINT('Ctrl Pts',(-1.31437432427029,2.32149911893914,
8.85049129520029));
#392228=CARTESIAN_POINT('Ctrl Pts',(-1.3193236441677,2.32459836800565,8.85711686593484));
#392229=CARTESIAN_POINT('Ctrl Pts',(-1.32539494747703,2.31857839805224,
8.85933012996512));
#392230=CARTESIAN_POINT('Ctrl Pts',(-1.33460133053253,2.33416520874058,
8.82945683644722));
#392231=CARTESIAN_POINT('Ctrl Pts',(-1.3395917327775,2.33729018344818,8.83607469902389));
#392232=CARTESIAN_POINT('Ctrl Pts',(-1.34565445587688,2.33122590846117,
8.8382956714852));
#392233=CARTESIAN_POINT('Ctrl Pts',(-1.35479818681084,2.34681241871377,
8.80838214965003));
#392234=CARTESIAN_POINT('Ctrl Pts',(-1.35980828351306,2.34994972603063,
8.81501364461995));
#392235=CARTESIAN_POINT('Ctrl Pts',(-1.36588287762334,2.34385480035509,
8.8172209842872));
#392236=CARTESIAN_POINT('Ctrl Pts',(-1.37496718403118,2.3594421834296,8.78727029226991));
#392237=CARTESIAN_POINT('Ctrl Pts',(-1.3799781129269,2.36258001186348,8.79393457792714));
#392238=CARTESIAN_POINT('Ctrl Pts',(-1.38608257609908,2.35646650676756,
8.79610912703474));
#392239=CARTESIAN_POINT('Origin',(-1.32100842742439,2.31090484334612,8.85049129520029));
#392240=CARTESIAN_POINT('Ctrl Pts',(-1.30385128920421,2.32742558187726,
8.85049129520029));
#392241=CARTESIAN_POINT('Ctrl Pts',(-1.30393589896118,2.33326458465275,
8.85711686593484));
#392242=CARTESIAN_POINT('Ctrl Pts',(-1.2956406467065,2.33533570805444,8.85933012996512));
#392243=CARTESIAN_POINT('Ctrl Pts',(-1.30377643617357,2.32225990040869,
8.86332496987232));
#392244=CARTESIAN_POINT('Ctrl Pts',(-1.29989627515222,2.32476913232806,
8.86648636486737));
#392245=CARTESIAN_POINT('Ctrl Pts',(-1.29544837314913,2.32088425528194,
8.87206031107457));
#392246=CARTESIAN_POINT('Ctrl Pts',(-1.30996597848912,2.31873862621885,
8.86341338519876));
#392247=CARTESIAN_POINT('Ctrl Pts',(-1.31412198473722,2.3166889719309,8.86654584966058));
#392248=CARTESIAN_POINT('Ctrl Pts',(-1.31304352587505,2.31086135841679,
8.87215952290714));
#392249=CARTESIAN_POINT('Ctrl Pts',(-1.31437432427029,2.32149911893914,
8.85049129520029));
#392250=CARTESIAN_POINT('Ctrl Pts',(-1.3193236441677,2.32459836800565,8.85711686593484));
#392251=CARTESIAN_POINT('Ctrl Pts',(-1.32539494747703,2.31857839805224,
8.85933012996512));
#392252=CARTESIAN_POINT('Origin',(-1.29135260132907,2.32760669344447,8.85049129520029));
#392253=CARTESIAN_POINT('Ctrl Pts',(-1.30488713801675,2.39891053004237,
8.78727029226991));
#392254=CARTESIAN_POINT('Ctrl Pts',(-1.30497280099365,2.40482221656423,
8.79393457792714));
#392255=CARTESIAN_POINT('Ctrl Pts',(-1.29658037301231,2.4068732084599,8.79610912703474));
#392256=CARTESIAN_POINT('Ctrl Pts',(-1.30454234439085,2.37511598186411,
8.80838214965002));
#392257=CARTESIAN_POINT('Ctrl Pts',(-1.30462799314121,2.3810266865985,8.81501364461988));
#392258=CARTESIAN_POINT('Ctrl Pts',(-1.29626693711645,2.38306176761554,
8.81722098428721));
#392259=CARTESIAN_POINT('Ctrl Pts',(-1.30419707450797,2.35128856672231,
8.82945683644724));
#392260=CARTESIAN_POINT('Ctrl Pts',(-1.30428238657708,2.35717603675116,
8.83607469902391));
#392261=CARTESIAN_POINT('Ctrl Pts',(-1.29595369511063,2.35921685544824,
8.8382956714852));
#392262=CARTESIAN_POINT('Ctrl Pts',(-1.30385128920421,2.32742558187726,
8.85049129520029));
#392263=CARTESIAN_POINT('Ctrl Pts',(-1.30393589896118,2.33326458465275,
8.85711686593484));
#392264=CARTESIAN_POINT('Ctrl Pts',(-1.2956406467065,2.33533570805444,8.85933012996512));
#392265=CARTESIAN_POINT('Origin',(-1.29238845014161,2.39909164160957,8.78727029226991));
#392266=CARTESIAN_POINT('Ctrl Pts',(-1.30508760891742,2.41274649779732,
8.75374538247848));
#392267=CARTESIAN_POINT('Ctrl Pts',(-1.30521083091158,2.42034447086438,
8.75304829418602));
#392268=CARTESIAN_POINT('Ctrl Pts',(-1.29847137974321,2.42392922206331,
8.75272238421917));
#392269=CARTESIAN_POINT('Ctrl Pts',(-1.30510673448897,2.41406634291194,
8.76769408445022));
#392270=CARTESIAN_POINT('Ctrl Pts',(-1.30523236727891,2.42185552588414,
8.76974318093968));
#392271=CARTESIAN_POINT('Ctrl Pts',(-1.29865181653908,2.4255588634654,8.7707786988043));
#392272=CARTESIAN_POINT('Ctrl Pts',(-1.3050087077191,2.40730156872033,8.78108014887988));
#392273=CARTESIAN_POINT('Ctrl Pts',(-1.30511897588473,2.41390255942112,
8.78639403366326));
#392274=CARTESIAN_POINT('Ctrl Pts',(-1.29773252047993,2.41721350373984,
8.78812224174741));
#392275=CARTESIAN_POINT('Ctrl Pts',(-1.30484806344775,2.39621559715997,
8.78944554828686));
#392276=CARTESIAN_POINT('Ctrl Pts',(-1.3049465903167,2.40177857388769,8.79673892988685));
#392277=CARTESIAN_POINT('Ctrl Pts',(-1.29621337213037,2.40357703279092,
8.79894799272499));
#392278=CARTESIAN_POINT('Origin',(-1.2925916222732,2.4131127507908,8.75721825406948));
#392279=CARTESIAN_POINT('Origin',(-1.2925916222732,2.4131127507908,9.));
#392280=CARTESIAN_POINT('Origin',(-1.2925916222732,2.4131127507908,7.51860402984325));
#392281=CARTESIAN_POINT('Ctrl Pts',(-1.31346132563585,2.41188557367603,
7.50366195182966));
#392282=CARTESIAN_POINT('Ctrl Pts',(-1.31521268767181,2.4151015685033,7.50000065167735));
#392283=CARTESIAN_POINT('Ctrl Pts',(-1.31521268767171,2.41510156850336,
7.49482233047108));
#392284=CARTESIAN_POINT('Ctrl Pts',(-1.3077817098543,2.41669137893433,7.50215800491337));
#392285=CARTESIAN_POINT('Ctrl Pts',(-1.30684029925185,2.41966096531158,
7.49877273257266));
#392286=CARTESIAN_POINT('Ctrl Pts',(-1.30380859101919,2.4213119957601,7.49481816995647));
#392287=CARTESIAN_POINT('Ctrl Pts',(-1.30513148750344,2.41574992376647,
7.51043025814042));
#392288=CARTESIAN_POINT('Ctrl Pts',(-1.30361489455134,2.42138842558916,
7.51006209594515));
#392289=CARTESIAN_POINT('Ctrl Pts',(-1.29849163527805,2.42413272597013,
7.50731281821701));
#392290=CARTESIAN_POINT('Ctrl Pts',(-1.30509028815831,2.41293012797613,
7.51860402984326));
#392291=CARTESIAN_POINT('Ctrl Pts',(-1.30520145828907,2.42053858764893,
7.51860402984327));
#392292=CARTESIAN_POINT('Ctrl Pts',(-1.29849386712376,2.42413153047478,
7.51860402984327));
#392293=CARTESIAN_POINT('Origin',(0.,0.,7.5));
#392294=CARTESIAN_POINT('Origin',(-1.45029105591254,2.23910559748223,7.5));
#392295=CARTESIAN_POINT('',(-1.45029105591254,2.23910559748223,7.59394543036555));
#392296=CARTESIAN_POINT('',(-1.45029105591254,2.23910559748223,8.85049129520029));
#392297=CARTESIAN_POINT('',(-1.45029105591254,2.23910559748223,7.5));
#392298=CARTESIAN_POINT('',(-1.45590483281685,2.31037730509331,8.78727029226991));
#392299=CARTESIAN_POINT('Ctrl Pts',(-1.45029105591254,2.23910559748223,
8.85049129520029));
#392300=CARTESIAN_POINT('Ctrl Pts',(-1.45216503493678,2.26289736679569,
8.82945686509571));
#392301=CARTESIAN_POINT('Ctrl Pts',(-1.45403622806459,2.28665376676721,
8.80838212259896));
#392302=CARTESIAN_POINT('Ctrl Pts',(-1.45590483281685,2.31037730509331,
8.78727029226991));
#392303=CARTESIAN_POINT('',(-1.45700592305913,2.3243565891188,8.75721825406948));
#392304=CARTESIAN_POINT('Origin',(-1.45369256172855,2.28228805819249,8.75937679713117));
#392305=CARTESIAN_POINT('',(-1.45700592305913,2.3243565891188,7.51860402984325));
#392306=CARTESIAN_POINT('',(-1.45700592305913,2.3243565891188,7.5));
#392307=CARTESIAN_POINT('Ctrl Pts',(-1.45700592305913,2.3243565891188,7.51860402984325));
#392308=CARTESIAN_POINT('Ctrl Pts',(-1.45614118792574,2.31337803570669,
7.52834476460825));
#392309=CARTESIAN_POINT('Ctrl Pts',(-1.4552758914188,2.30239235517613,7.53807742314407));
#392310=CARTESIAN_POINT('Ctrl Pts',(-1.45441001468941,2.29139930822463,
7.54780169004674));
#392311=CARTESIAN_POINT('Ctrl Pts',(-1.45303851274671,2.27398691597694,
7.5632044032688));
#392312=CARTESIAN_POINT('Ctrl Pts',(-1.45166555335681,2.25655602018873,
7.57858609112103));
#392313=CARTESIAN_POINT('Ctrl Pts',(-1.45029105591254,2.23910559748223,
7.59394543036555));
#392314=CARTESIAN_POINT('Origin',(-1.70235901374313,2.36323439034369,7.5));
#392315=CARTESIAN_POINT('',(-1.53564927699521,2.27316543860614,8.75721825406948));
#392316=CARTESIAN_POINT('',(-1.52331214621093,2.26650000646723,8.78727029226991));
#392317=CARTESIAN_POINT('Origin',(-1.49199590676139,2.24958065361715,8.75658640621095));
#392318=CARTESIAN_POINT('',(-1.46041276049034,2.23251709792628,8.85049129520029));
#392319=CARTESIAN_POINT('Ctrl Pts',(-1.52331214621093,2.26650000646723,
8.78727029226991));
#392320=CARTESIAN_POINT('Ctrl Pts',(-1.50237542338154,2.25518843754,8.80838212259896));
#392321=CARTESIAN_POINT('Ctrl Pts',(-1.48140969918007,2.24386119992281,
8.82945686509571));
#392322=CARTESIAN_POINT('Ctrl Pts',(-1.46041276049034,2.23251709792628,
8.85049129520029));
#392323=CARTESIAN_POINT('',(-1.46041276049034,2.23251709792628,7.59394543036555));
#392324=CARTESIAN_POINT('',(-1.46041276049034,2.23251709792628,7.5));
#392325=CARTESIAN_POINT('',(-1.53564927699521,2.27316543860614,7.51860402984325));
#392326=CARTESIAN_POINT('Ctrl Pts',(-1.46041276049034,2.23251709792628,
7.59394543036555));
#392327=CARTESIAN_POINT('Ctrl Pts',(-1.47581327361951,2.24083759618166,
7.57858609112103));
#392328=CARTESIAN_POINT('Ctrl Pts',(-1.49119655366672,2.24914878384933,
7.56320440326857));
#392329=CARTESIAN_POINT('Ctrl Pts',(-1.50656350379345,2.25745114888401,
7.54780169004651));
#392330=CARTESIAN_POINT('Ctrl Pts',(-1.51626519221406,2.26269271979147,
7.53807742314383));
#392331=CARTESIAN_POINT('Ctrl Pts',(-1.52596037955093,2.26793077833181,
7.52834476460825));
#392332=CARTESIAN_POINT('Ctrl Pts',(-1.53564927699521,2.27316543860614,
7.51860402984325));
#392333=CARTESIAN_POINT('',(-1.53564927699521,2.27316543860614,7.5));
#392334=CARTESIAN_POINT('Origin',(-1.4571448281799,2.2385657542576,7.5));
#392335=CARTESIAN_POINT('Ctrl Pts',(-1.46041276049034,2.23251709792628,
8.85049129520029));
#392336=CARTESIAN_POINT('Ctrl Pts',(-1.46024237621486,2.23242504371647,
8.85097269580138));
#392337=CARTESIAN_POINT('Ctrl Pts',(-1.46007014340848,2.2323415513399,8.85143669361005));
#392338=CARTESIAN_POINT('Ctrl Pts',(-1.45988774993289,2.23226356296288,
8.8519052845931));
#392339=CARTESIAN_POINT('Ctrl Pts',(-1.45953099986159,2.23211102264327,
8.85282181883899));
#392340=CARTESIAN_POINT('Ctrl Pts',(-1.4591444780731,2.23198364392552,8.85372622499635));
#392341=CARTESIAN_POINT('Ctrl Pts',(-1.45871729341942,2.23189407204953,
8.8546225773507));
#392342=CARTESIAN_POINT('Ctrl Pts',(-1.4583626598921,2.23181971265937,8.85536669723986));
#392343=CARTESIAN_POINT('Ctrl Pts',(-1.45797992823562,2.2317713608387,8.85610498449051));
#392344=CARTESIAN_POINT('Ctrl Pts',(-1.45756183174182,2.23176418670402,
8.85681338218371));
#392345=CARTESIAN_POINT('Ctrl Pts',(-1.45718240851707,2.23175767616552,
8.85745625420285));
#392346=CARTESIAN_POINT('Ctrl Pts',(-1.45676911105285,2.2317843978143,8.85808743050666));
#392347=CARTESIAN_POINT('Ctrl Pts',(-1.45631128381982,2.23187089041148,
8.85866804508411));
#392348=CARTESIAN_POINT('Ctrl Pts',(-1.45610005225898,2.23191079622088,
8.85893592806396));
#392349=CARTESIAN_POINT('Ctrl Pts',(-1.4558792788259,2.23196365955264,8.85919241173849));
#392350=CARTESIAN_POINT('Ctrl Pts',(-1.45564772260897,2.23203367112446,
8.85943017985534));
#392351=CARTESIAN_POINT('Ctrl Pts',(-1.45533505316813,2.23212820747206,
8.8597512372));
#392352=CARTESIAN_POINT('Ctrl Pts',(-1.45499495061645,2.23225702953025,
8.86004599534705));
#392353=CARTESIAN_POINT('Ctrl Pts',(-1.45463519034912,2.23242832936726,
8.86026130871721));
#392354=CARTESIAN_POINT('Ctrl Pts',(-1.45450347197253,2.23249104706704,
8.86034014101235));
#392355=CARTESIAN_POINT('Ctrl Pts',(-1.45436713462983,2.23256038986721,
8.86040910639692));
#392356=CARTESIAN_POINT('Ctrl Pts',(-1.45423004525064,2.23263476838842,
8.86046313645506));
#392357=CARTESIAN_POINT('Ctrl Pts',(-1.45401611842252,2.23275083544785,
8.86054744990829));
#392358=CARTESIAN_POINT('Ctrl Pts',(-1.45379459084791,2.23288246268807,
8.86059655985668));
#392359=CARTESIAN_POINT('Ctrl Pts',(-1.45357952011842,2.23302095660015,
8.86059725258816));
#392360=CARTESIAN_POINT('Ctrl Pts',(-1.45336395248962,2.2331597704885,8.86059794692011));
#392361=CARTESIAN_POINT('Ctrl Pts',(-1.45315391929664,2.23330925598726,
8.86056369958366));
#392362=CARTESIAN_POINT('Ctrl Pts',(-1.45295869380043,2.23345819421407,
8.86048590497774));
#392363=CARTESIAN_POINT('Ctrl Pts',(-1.45290774575849,2.23349706265685,
8.86046560290182));
#392364=CARTESIAN_POINT('Ctrl Pts',(-1.45285719833681,2.23353647149836,
8.86044257503091));
#392365=CARTESIAN_POINT('Ctrl Pts',(-1.45280859330923,2.23357517708475,
8.86041778462584));
#392366=CARTESIAN_POINT('Ctrl Pts',(-1.45248154178737,2.23383561765153,
8.86025097596201));
#392367=CARTESIAN_POINT('Ctrl Pts',(-1.45219875525292,2.23409942479349,
8.8599848982295));
#392368=CARTESIAN_POINT('Ctrl Pts',(-1.45196270805473,2.23435270342851,
8.85968173251461));
#392369=CARTESIAN_POINT('Ctrl Pts',(-1.45183785261078,2.2344866733153,8.85952137522076));
#392370=CARTESIAN_POINT('Ctrl Pts',(-1.45172352753971,2.23462014970573,
8.85934740853961));
#392371=CARTESIAN_POINT('Ctrl Pts',(-1.4516201644098,2.23475023902308,8.8591675900182));
#392372=CARTESIAN_POINT('Ctrl Pts',(-1.45120510771614,2.23527261525129,
8.85844552518695));
#392373=CARTESIAN_POINT('Ctrl Pts',(-1.45094097857851,2.23576801806972,
8.85759444184124));
#392374=CARTESIAN_POINT('Ctrl Pts',(-1.45076190271768,2.23619128641436,
8.85683498915138));
#392375=CARTESIAN_POINT('Ctrl Pts',(-1.45074316290576,2.23623558031937,
8.85675551444998));
#392376=CARTESIAN_POINT('Ctrl Pts',(-1.45072537407566,2.23627908830464,
8.85667699793651));
#392377=CARTESIAN_POINT('Ctrl Pts',(-1.45070847371898,2.23632176059871,
8.85659965593547));
#392378=CARTESIAN_POINT('Ctrl Pts',(-1.45048035184219,2.23689775340153,
8.85555568965886));
#392379=CARTESIAN_POINT('Ctrl Pts',(-1.45034429734325,2.23748426348366,
8.85434650606346));
#392380=CARTESIAN_POINT('Ctrl Pts',(-1.45029358366056,2.2380827858589,8.85297329937117));
#392381=CARTESIAN_POINT('Ctrl Pts',(-1.45026506030408,2.23841941822647,
8.85220095427747));
#392382=CARTESIAN_POINT('Ctrl Pts',(-1.45026383578707,2.23876001466752,
8.85137579139183));
#392383=CARTESIAN_POINT('Ctrl Pts',(-1.45029105591254,2.23910559748223,
8.85049129520029));
#392384=CARTESIAN_POINT('Origin',(-1.4571448281799,2.2385657542576,7.59394543036555));
#392385=CARTESIAN_POINT('Ctrl Pts',(-1.45991807746004,2.232249833501,7.59443877723642));
#392386=CARTESIAN_POINT('Ctrl Pts',(-1.45482331821922,2.2294972670755,7.58783886950016));
#392387=CARTESIAN_POINT('Ctrl Pts',(-1.4491689343392,2.23583028566651,7.58559994247159));
#392388=CARTESIAN_POINT('Ctrl Pts',(-1.48773021868178,2.24727601286091,
7.56670252222133));
#392389=CARTESIAN_POINT('Ctrl Pts',(-1.4826428228145,2.24452742467542,7.56004874999029));
#392390=CARTESIAN_POINT('Ctrl Pts',(-1.47693899722921,2.25088373893362,
7.55786368756703));
#392391=CARTESIAN_POINT('Ctrl Pts',(-1.51549042350858,2.26227413233218,
7.53888913333558));
#392392=CARTESIAN_POINT('Ctrl Pts',(-1.51037279299855,2.25950920915248,
7.53222002137275));
#392393=CARTESIAN_POINT('Ctrl Pts',(-1.5046587420292,2.26590858929744,7.53005029815326));
#392394=CARTESIAN_POINT('Ctrl Pts',(-1.54319743577236,2.27724351323975,
7.51101258149734));
#392395=CARTESIAN_POINT('Ctrl Pts',(-1.5380177702816,2.27444507416711,7.5043616886572));
#392396=CARTESIAN_POINT('Ctrl Pts',(-1.53232675979281,2.28090416707255,
7.50217374673251));
#392397=CARTESIAN_POINT('',(-1.53085035931326,2.28010398287621,7.50366116523517));
#392398=CARTESIAN_POINT('Ctrl Pts',(-1.53564927699521,2.27316543860614,
7.51860402984325));
#392399=CARTESIAN_POINT('Ctrl Pts',(-1.53603780855528,2.27337535214218,
7.51734760759494));
#392400=CARTESIAN_POINT('Ctrl Pts',(-1.5363606214257,2.27361738460006,7.51608817408573));
#392401=CARTESIAN_POINT('Ctrl Pts',(-1.53660896257295,2.27390166343754,
7.5148100591312));
#392402=CARTESIAN_POINT('Ctrl Pts',(-1.53683391591844,2.27415917000159,
7.51365231206384));
#392403=CARTESIAN_POINT('Ctrl Pts',(-1.53699826944798,2.27445153882633,
7.51247773061042));
#392404=CARTESIAN_POINT('Ctrl Pts',(-1.53706699140845,2.2747918051043,7.51129758471022));
#392405=CARTESIAN_POINT('Ctrl Pts',(-1.53715240495698,2.27521471722793,
7.50983079813402));
#392406=CARTESIAN_POINT('Ctrl Pts',(-1.53707459741071,2.27570070103045,
7.50839324291155));
#392407=CARTESIAN_POINT('Ctrl Pts',(-1.53675159800195,2.27624027053725,
7.50715379678855));
#392408=CARTESIAN_POINT('Ctrl Pts',(-1.53660238158211,2.27648953610207,
7.50658120839351));
#392409=CARTESIAN_POINT('Ctrl Pts',(-1.5363714718882,2.2767807927975,7.50598221009429));
#392410=CARTESIAN_POINT('Ctrl Pts',(-1.53604653982967,2.27709297784468,
7.50545747549611));
#392411=CARTESIAN_POINT('Ctrl Pts',(-1.53587314602565,2.27725956944889,
7.50517746087247));
#392412=CARTESIAN_POINT('Ctrl Pts',(-1.53567123831364,2.27743407312487,
7.50491486231392));
#392413=CARTESIAN_POINT('Ctrl Pts',(-1.53544507284031,2.2776106057266,7.50468370960993));
#392414=CARTESIAN_POINT('Ctrl Pts',(-1.53510688411783,2.27787457765022,
7.50433806340447));
#392415=CARTESIAN_POINT('Ctrl Pts',(-1.53470397229055,2.27815056287832,
7.50405484070984));
#392416=CARTESIAN_POINT('Ctrl Pts',(-1.5342630678757,2.27841938328403,7.50385766036132));
#392417=CARTESIAN_POINT('Ctrl Pts',(-1.53421592000173,2.27844812944801,
7.50383657498791));
#392418=CARTESIAN_POINT('Ctrl Pts',(-1.53416836604275,2.27847679328435,
7.50381643264937));
#392419=CARTESIAN_POINT('Ctrl Pts',(-1.53412045929204,2.27850535137414,
7.50379723213559));
#392420=CARTESIAN_POINT('Ctrl Pts',(-1.53380066605966,2.27869598596543,
7.50366906242519));
#392421=CARTESIAN_POINT('Ctrl Pts',(-1.5334578280016,2.27888543759958,7.50358235568538));
#392422=CARTESIAN_POINT('Ctrl Pts',(-1.53312298478602,2.27906010223199,
7.5035341175365));
#392423=CARTESIAN_POINT('Ctrl Pts',(-1.5326209252812,2.27932199208007,7.50346178989176));
#392424=CARTESIAN_POINT('Ctrl Pts',(-1.53206968824904,2.27958237897119,
7.50346967198527));
#392425=CARTESIAN_POINT('Ctrl Pts',(-1.53152067885768,2.27982134720852,
7.50354272648692));
#392426=CARTESIAN_POINT('Ctrl Pts',(-1.53129485993119,2.27991963979088,
7.50357277531559));
#392427=CARTESIAN_POINT('Ctrl Pts',(-1.53106977451843,2.28001430808025,
7.50361331098761));
#392428=CARTESIAN_POINT('Ctrl Pts',(-1.53085035931405,2.28010398287738,
7.50366116523658));
#392429=CARTESIAN_POINT('',(-1.45874211355498,2.24101961352526,7.57603338622103));
#392430=CARTESIAN_POINT('Origin',(-1.46356058069551,2.2484273030446,7.58486873427627));
#392431=CARTESIAN_POINT('Ctrl Pts',(-1.53085035936601,2.2801039828987,7.50366116529969));
#392432=CARTESIAN_POINT('Ctrl Pts',(-1.50685310107526,2.26709785383092,
7.52783573079709));
#392433=CARTESIAN_POINT('Ctrl Pts',(-1.482818145483,2.25407036159425,7.55196141284068));
#392434=CARTESIAN_POINT('Ctrl Pts',(-1.45874211477943,2.24101961378671,
7.57603338728831));
#392435=CARTESIAN_POINT('Ctrl Pts',(-1.46123398723767,2.23316062115807,
7.5963967733137));
#392436=CARTESIAN_POINT('Ctrl Pts',(-1.44604747589618,2.22151724109288,
7.59974925422225));
#392437=CARTESIAN_POINT('Ctrl Pts',(-1.4505470827706,2.2401170250713,7.59639677331373));
#392438=CARTESIAN_POINT('Ctrl Pts',(-1.45856018235568,2.23032057335267,
7.5870762605742));
#392439=CARTESIAN_POINT('Ctrl Pts',(-1.45166892345349,2.23015329411126,
7.58811717123965));
#392440=CARTESIAN_POINT('Ctrl Pts',(-1.44903241888651,2.23652246009042,
7.58707626057426));
#392441=CARTESIAN_POINT('Ctrl Pts',(-1.45829905181766,2.23639160646937,
7.58015376756929));
#392442=CARTESIAN_POINT('Ctrl Pts',(-1.45543932339328,2.23594564091341,
7.58208760766041));
#392443=CARTESIAN_POINT('Ctrl Pts',(-1.45468954949516,2.23874113211161,
7.5801537675693));
#392444=CARTESIAN_POINT('Ctrl Pts',(-1.45874211310368,2.24101961283157,
7.57603338509286));
#392445=CARTESIAN_POINT('Ctrl Pts',(-1.45874211310368,2.24101961283157,
7.57603338509286));
#392446=CARTESIAN_POINT('Ctrl Pts',(-1.45874211310368,2.24101961283157,
7.57603338509286));
#392447=CARTESIAN_POINT('Origin',(-1.46356536312157,2.24842419003061,7.58486873427624));
#392448=CARTESIAN_POINT('Ctrl Pts',(-1.45768172623408,2.33293648944412,
7.51098857897448));
#392449=CARTESIAN_POINT('Ctrl Pts',(-1.4572194384267,2.32706734964727,7.50433767179956));
#392450=CARTESIAN_POINT('Ctrl Pts',(-1.4654293770884,2.32447795623306,7.50214974420965));
#392451=CARTESIAN_POINT('Ctrl Pts',(-1.4552081611692,2.30153246162716,7.53887321589171));
#392452=CARTESIAN_POINT('Ctrl Pts',(-1.45475141239016,2.29573364454093,
7.53220407452068));
#392453=CARTESIAN_POINT('Ctrl Pts',(-1.46291606210055,2.29309898801139,
7.53003438070911));
#392454=CARTESIAN_POINT('Ctrl Pts',(-1.45272984594693,2.27006812649225,
7.56669465659231));
#392455=CARTESIAN_POINT('Ctrl Pts',(-1.45227579646822,2.26430357933688,
7.56004085833297));
#392456=CARTESIAN_POINT('Ctrl Pts',(-1.46039691481123,2.2616608370139,7.55785582193789));
#392457=CARTESIAN_POINT('Ctrl Pts',(-1.45024689265155,2.23854490704546,
7.59443891967696));
#392458=CARTESIAN_POINT('Ctrl Pts',(-1.44979218485767,2.23277200201443,
7.58783901202978));
#392459=CARTESIAN_POINT('Ctrl Pts',(-1.45787197718041,2.23016506242752,
7.58560008491213));
#392460=CARTESIAN_POINT('',(-1.4652931374677,2.32277700535965,7.50366116523517));
#392461=CARTESIAN_POINT('Ctrl Pts',(-1.4652931374679,2.32277700535996,7.50366116523554));
#392462=CARTESIAN_POINT('Ctrl Pts',(-1.46474697642256,2.32330221544109,
7.50350835821027));
#392463=CARTESIAN_POINT('Ctrl Pts',(-1.46422783470213,2.32376724219866,
7.50345484956));
#392464=CARTESIAN_POINT('Ctrl Pts',(-1.46372067846696,2.32418635854707,
7.50349758195598));
#392465=CARTESIAN_POINT('Ctrl Pts',(-1.46346046970663,2.32440139631628,
7.50351950684424));
#392466=CARTESIAN_POINT('Ctrl Pts',(-1.46317785130408,2.32462564316439,
7.50357029184312));
#392467=CARTESIAN_POINT('Ctrl Pts',(-1.46289938165619,2.32483439063405,
7.50365515313924));
#392468=CARTESIAN_POINT('Ctrl Pts',(-1.46247098257424,2.32515552877258,
7.50378570417639));
#392469=CARTESIAN_POINT('Ctrl Pts',(-1.46204003528892,2.32544968913027,
7.50400001621911));
#392470=CARTESIAN_POINT('Ctrl Pts',(-1.46163806115037,2.32569260662708,
7.50428903009634));
#392471=CARTESIAN_POINT('Ctrl Pts',(-1.46159344511359,2.32571956860033,
7.50432110841318));
#392472=CARTESIAN_POINT('Ctrl Pts',(-1.46154917354528,2.3257459269341,7.50435406373354));
#392473=CARTESIAN_POINT('Ctrl Pts',(-1.46150528007181,2.32577166872305,
7.50438785222352));
#392474=CARTESIAN_POINT('Ctrl Pts',(-1.46123728931836,2.32592883471765,
7.50459414719562));
#392475=CARTESIAN_POINT('Ctrl Pts',(-1.46097886517165,2.32606507519194,
7.50483629897752));
#392476=CARTESIAN_POINT('Ctrl Pts',(-1.46074052152492,2.32617633497058,
7.5050991045531));
#392477=CARTESIAN_POINT('Ctrl Pts',(-1.46021471150088,2.32642178521725,
7.50567888004914));
#392478=CARTESIAN_POINT('Ctrl Pts',(-1.45976613099599,2.32655580102416,
7.50637912803145));
#392479=CARTESIAN_POINT('Ctrl Pts',(-1.45939558937345,2.32660928163543,
7.50710440483569));
#392480=CARTESIAN_POINT('Ctrl Pts',(-1.45930472521132,2.32662239614305,
7.50728225710685));
#392481=CARTESIAN_POINT('Ctrl Pts',(-1.45921676576371,2.32663107336785,
7.50746498566954));
#392482=CARTESIAN_POINT('Ctrl Pts',(-1.4591338051873,2.32663552533606,7.50764697238949));
#392483=CARTESIAN_POINT('Ctrl Pts',(-1.45868783195991,2.32665945789196,
7.50862528291181));
#392484=CARTESIAN_POINT('Ctrl Pts',(-1.45834605560041,2.32656759282621,
7.50965856837421));
#392485=CARTESIAN_POINT('Ctrl Pts',(-1.45807469544966,2.32641697628602,
7.51067959873202));
#392486=CARTESIAN_POINT('Ctrl Pts',(-1.45792536561643,2.32633409181398,
7.51124147302578));
#392487=CARTESIAN_POINT('Ctrl Pts',(-1.45779753440284,2.32623301549519,
7.51180065547253));
#392488=CARTESIAN_POINT('Ctrl Pts',(-1.45768697619171,2.32612092895029,
7.51235175716501));
#392489=CARTESIAN_POINT('Ctrl Pts',(-1.4573049535311,2.32573362528766,7.51425603304537));
#392490=CARTESIAN_POINT('Ctrl Pts',(-1.45708793524577,2.32516442453968,
7.51626900505183));
#392491=CARTESIAN_POINT('Ctrl Pts',(-1.45701626624483,2.32447039109802,
7.51827788969247));
#392492=CARTESIAN_POINT('Ctrl Pts',(-1.45701238738306,2.32443282869662,
7.51838661432547));
#392493=CARTESIAN_POINT('Ctrl Pts',(-1.45700894005981,2.32439489252746,
7.51849533314857));
#392494=CARTESIAN_POINT('Ctrl Pts',(-1.45700592305912,2.3243565891188,7.51860402984325));
#392495=CARTESIAN_POINT('Ctrl Pts',(-1.45874211329886,2.24101961475187,
7.57603338728985));
#392496=CARTESIAN_POINT('Ctrl Pts',(-1.46093030563708,2.26831776647326,
7.55196141284922));
#392497=CARTESIAN_POINT('Ctrl Pts',(-1.46311385931009,2.29556894514296,
7.52783573083105));
#392498=CARTESIAN_POINT('Ctrl Pts',(-1.46529313746699,2.32277700541882,
7.50366116530176));
#392499=CARTESIAN_POINT('Origin',(-5.0406283147387E-16,7.74375868966275E-16,
7.49482233047033));
#392500=CARTESIAN_POINT('Origin',(-1.52592346056196,2.27276568139055,7.49482233047033));
#392501=CARTESIAN_POINT('Origin',(0.,0.,7.50366116523517));
#392502=CARTESIAN_POINT('Origin',(-1.4605772285055,2.31530136474093,7.49482233047033));
#392503=CARTESIAN_POINT('Ctrl Pts',(-1.53564834642937,2.27316493579466,
7.51860402984325));
#392504=CARTESIAN_POINT('Ctrl Pts',(-1.54234243883857,2.27678231230909,
7.51860402984325));
#392505=CARTESIAN_POINT('Ctrl Pts',(-1.54863020028822,2.27249741534622,
7.51860402984325));
#392506=CARTESIAN_POINT('Ctrl Pts',(-1.53813390922789,2.27450809126278,
7.51041458714365));
#392507=CARTESIAN_POINT('Ctrl Pts',(-1.54383207597013,2.27576716295958,
7.51004642900441));
#392508=CARTESIAN_POINT('Ctrl Pts',(-1.54863193437817,2.27249623362252,
7.5072913648301));
#392509=CARTESIAN_POINT('Ctrl Pts',(-1.53773211669731,2.2772941817067,7.50215815450137));
#392510=CARTESIAN_POINT('Ctrl Pts',(-1.54079910519163,2.27783422435051,
7.49877163671531));
#392511=CARTESIAN_POINT('Ctrl Pts',(-1.54366359294843,2.27591104118568,
7.4948158853317));
#392512=CARTESIAN_POINT('Ctrl Pts',(-1.53085005244588,2.28010352581767,
7.50366171572174));
#392513=CARTESIAN_POINT('Ctrl Pts',(-1.53289114759616,2.28314360687656,
7.50000045605858));
#392514=CARTESIAN_POINT('Ctrl Pts',(-1.53289114759627,2.28314360687649,
7.49482233047317));
#392515=CARTESIAN_POINT('Origin',(-1.5415909721051,2.2621678816401,7.51860402984325));
#392516=CARTESIAN_POINT('Origin',(-1.5415909721051,2.2621678816401,9.));
#392517=CARTESIAN_POINT('Origin',(-1.5415909721051,2.2621678816401,8.75721825406948));
#392518=CARTESIAN_POINT('Ctrl Pts',(-1.52095641350492,2.26522723077965,
8.78942910404913));
#392519=CARTESIAN_POINT('Ctrl Pts',(-1.52584946047529,2.26789378661956,
8.79672699501691));
#392520=CARTESIAN_POINT('Ctrl Pts',(-1.5314874230971,2.26097375313284,8.79893251111267));
#392521=CARTESIAN_POINT('Ctrl Pts',(-1.53062927805545,2.27045323404477,
8.78111911759578));
#392522=CARTESIAN_POINT('Ctrl Pts',(-1.53643360398451,2.27360793064428,
8.78644465894812));
#392523=CARTESIAN_POINT('Ctrl Pts',(-1.54278266608223,2.26856760106628,
8.78817647674131));
#392524=CARTESIAN_POINT('Ctrl Pts',(-1.53665763797808,2.27371020390355,
8.76780923932034));
#392525=CARTESIAN_POINT('Ctrl Pts',(-1.54351183306585,2.27742971280518,
8.76988516158375));
#392526=CARTESIAN_POINT('Ctrl Pts',(-1.54984371438415,2.27330131609856,
8.77093053738833));
#392527=CARTESIAN_POINT('Ctrl Pts',(-1.53548219029791,2.27307513935434,
8.75371302330491));
#392528=CARTESIAN_POINT('Ctrl Pts',(-1.54216779835547,2.27670402985536,
8.75300828287558));
#392529=CARTESIAN_POINT('Ctrl Pts',(-1.54846677797149,2.27237766936051,
8.75267964240738));
#392530=CARTESIAN_POINT('Origin',(-1.52925384132081,2.25550244950119,8.78727029226991));
#392531=CARTESIAN_POINT('Ctrl Pts',(-1.46041276049034,2.23251709792628,
8.85049129520029));
#392532=CARTESIAN_POINT('Ctrl Pts',(-1.46555048104866,2.23529287523861,
8.85711686593484));
#392533=CARTESIAN_POINT('Ctrl Pts',(-1.47122360941501,2.22889628422051,
8.85933012996512));
#392534=CARTESIAN_POINT('Ctrl Pts',(-1.48140972735874,2.24386121514701,
8.82945683644724));
#392535=CARTESIAN_POINT('Ctrl Pts',(-1.48659009410405,2.24666003308931,
8.8360746990239));
#392536=CARTESIAN_POINT('Ctrl Pts',(-1.49225182125613,2.240219777803,8.8382956714852));
#392537=CARTESIAN_POINT('Ctrl Pts',(-1.50237539655485,2.25518842304624,
8.80838214965001));
#392538=CARTESIAN_POINT('Ctrl Pts',(-1.507576207446,2.25799828643086,8.81501364461992));
#392539=CARTESIAN_POINT('Ctrl Pts',(-1.51324781742241,2.25152668285288,
8.81722098428721));
#392540=CARTESIAN_POINT('Ctrl Pts',(-1.52331214621093,2.26650000646723,
8.78727029226991));
#392541=CARTESIAN_POINT('Ctrl Pts',(-1.52851382097383,2.2693103365794,8.79393457792714));
#392542=CARTESIAN_POINT('Ctrl Pts',(-1.53421404825537,2.26281827803707,
8.79610912703474));
#392543=CARTESIAN_POINT('Origin',(-1.46635445560022,2.22151954096025,8.85049129520029));
#392544=CARTESIAN_POINT('Ctrl Pts',(-1.45029105591254,2.23910559748223,
8.85049129520029));
#392545=CARTESIAN_POINT('Ctrl Pts',(-1.45074959802199,2.24492718243454,
8.85711686593484));
#392546=CARTESIAN_POINT('Ctrl Pts',(-1.44260408658468,2.24752552912783,
8.85933012996512));
#392547=CARTESIAN_POINT('Ctrl Pts',(-1.44988539032744,2.23395532531039,
8.86332496987232));
#392548=CARTESIAN_POINT('Ctrl Pts',(-1.44617396855412,2.23670800451389,
8.86648636486738));
#392549=CARTESIAN_POINT('Ctrl Pts',(-1.44148630031577,2.23311608742407,
8.87206031107458));
#392550=CARTESIAN_POINT('Ctrl Pts',(-1.45583660675252,2.2300447206183,8.86341338519875));
#392551=CARTESIAN_POINT('Ctrl Pts',(-1.45985275223894,2.22773300133036,
8.86654584966059));
#392552=CARTESIAN_POINT('Ctrl Pts',(-1.45840313270636,2.22198645836977,
8.87215952290713));
#392553=CARTESIAN_POINT('Ctrl Pts',(-1.46041276049034,2.23251709792628,
8.85049129520029));
#392554=CARTESIAN_POINT('Ctrl Pts',(-1.46555048104866,2.23529287523861,
8.85711686593484));
#392555=CARTESIAN_POINT('Ctrl Pts',(-1.47122360941501,2.22889628422051,
8.85933012996512));
#392556=CARTESIAN_POINT('Origin',(-1.43782965179007,2.24008713061793,8.85049129520029));
#392557=CARTESIAN_POINT('Ctrl Pts',(-1.45590483281685,2.31037730509331,
8.78727029226991));
#392558=CARTESIAN_POINT('Ctrl Pts',(-1.4563690828459,2.31627135697541,8.79393457792714));
#392559=CARTESIAN_POINT('Ctrl Pts',(-1.44812530550985,2.3188558395952,8.79610912703474));
#392560=CARTESIAN_POINT('Ctrl Pts',(-1.45403622567031,2.28665373636971,
8.80838214965003));
#392561=CARTESIAN_POINT('Ctrl Pts',(-1.4545003985987,2.29254680939306,8.81501364461993));
#392562=CARTESIAN_POINT('Ctrl Pts',(-1.44628690934869,2.29511340381664,
8.81722098428721));
#392563=CARTESIAN_POINT('Ctrl Pts',(-1.45216503745173,2.26289739872514,
8.82945683644723));
#392564=CARTESIAN_POINT('Ctrl Pts',(-1.45262738573793,2.26876730635234,
8.83607469902391));
#392565=CARTESIAN_POINT('Ctrl Pts',(-1.44444656216421,2.27133755306294,
8.8382956714852));
#392566=CARTESIAN_POINT('Ctrl Pts',(-1.45029105591254,2.23910559748223,
8.85049129520029));
#392567=CARTESIAN_POINT('Ctrl Pts',(-1.45074959802199,2.24492718243454,
8.85711686593484));
#392568=CARTESIAN_POINT('Ctrl Pts',(-1.44260408658468,2.24752552912783,
8.85933012996512));
#392569=CARTESIAN_POINT('Origin',(-1.44344342869438,2.31135883822901,8.78727029226991));
#392570=CARTESIAN_POINT('Ctrl Pts',(-1.45699136532626,2.32417200115391,
8.75374538247848));
#392571=CARTESIAN_POINT('Ctrl Pts',(-1.45760113795343,2.33174646851016,
8.75304829418601));
#392572=CARTESIAN_POINT('Ctrl Pts',(-1.45110520950818,2.33575565257218,
8.75272238421917));
#392573=CARTESIAN_POINT('Ctrl Pts',(-1.45709501436911,2.3254879091256,8.76769408445022));
#392574=CARTESIAN_POINT('Ctrl Pts',(-1.45771944369952,2.33325303906547,
8.76974318093972));
#392575=CARTESIAN_POINT('Ctrl Pts',(-1.45138968706044,2.33737038507602,
8.77077869880429));
#392576=CARTESIAN_POINT('Ctrl Pts',(-1.45656376843517,2.3187433144848,8.78108014887986));
#392577=CARTESIAN_POINT('Ctrl Pts',(-1.45709673696933,2.32532367783663,
8.78639403366321));
#392578=CARTESIAN_POINT('Ctrl Pts',(-1.44993759076019,2.3291010712878,8.78812224174741));
#392579=CARTESIAN_POINT('Ctrl Pts',(-1.45569317358814,2.30769041275578,
8.78944554828685));
#392580=CARTESIAN_POINT('Ctrl Pts',(-1.45614791916575,2.31323564711302,
8.79673892988687));
#392581=CARTESIAN_POINT('Ctrl Pts',(-1.44754787197038,2.31558995009989,
8.79894799272499));
#392582=CARTESIAN_POINT('Origin',(-1.44454451893666,2.3253381222545,8.75721825406948));
#392583=CARTESIAN_POINT('Origin',(-1.44454451893666,2.3253381222545,9.));
#392584=CARTESIAN_POINT('Origin',(-1.44454451893666,2.3253381222545,7.51860402984325));
#392585=CARTESIAN_POINT('Ctrl Pts',(-1.46529271774777,2.32277634002135,
7.50366195182967));
#392586=CARTESIAN_POINT('Ctrl Pts',(-1.46724653091864,2.32587351709142,
7.50000065167736));
#392587=CARTESIAN_POINT('Ctrl Pts',(-1.46724653091855,2.32587351709148,
7.49482233047108));
#392588=CARTESIAN_POINT('Ctrl Pts',(-1.45993268034609,2.32793616546986,
7.50215800491335));
#392589=CARTESIAN_POINT('Ctrl Pts',(-1.45918346602513,2.33095996689781,
7.49877273257261));
#392590=CARTESIAN_POINT('Ctrl Pts',(-1.4562637686462,2.33280184734057,7.49481816995645));
#392591=CARTESIAN_POINT('Ctrl Pts',(-1.45722758392156,2.32716644495162,
7.51043025814045));
#392592=CARTESIAN_POINT('Ctrl Pts',(-1.45607536702449,2.33289053031166,
7.5100620959452));
#392593=CARTESIAN_POINT('Ctrl Pts',(-1.45113846196593,2.33595744058183,
7.50731281821702));
#392594=CARTESIAN_POINT('Ctrl Pts',(-1.45700580428831,2.32435508238525,
7.51860402984326));
#392595=CARTESIAN_POINT('Ctrl Pts',(-1.45760422169307,2.33194078696693,
7.51860402984326));
#392596=CARTESIAN_POINT('Ctrl Pts',(-1.45114061263043,2.3359561045479,7.51860402984327));
#392597=CARTESIAN_POINT('Origin',(0.,0.,7.5));
#392598=CARTESIAN_POINT('Origin',(-1.59077126558568,2.14158464790051,7.5));
#392599=CARTESIAN_POINT('',(-1.59077126558568,2.14158464790051,7.59394543036555));
#392600=CARTESIAN_POINT('',(-1.59077126558568,2.14158464790051,8.85049129520029));
#392601=CARTESIAN_POINT('',(-1.59077126558568,2.14158464790051,7.5));
#392602=CARTESIAN_POINT('',(-1.6009399023683,2.21235024422325,8.78727029226991));
#392603=CARTESIAN_POINT('Ctrl Pts',(-1.59077126558568,2.14158464790051,
8.85049129520029));
#392604=CARTESIAN_POINT('Ctrl Pts',(-1.59416573821266,2.16520746822393,
8.82945686509571));
#392605=CARTESIAN_POINT('Ctrl Pts',(-1.59755516454564,2.1887951703685,8.80838212259894));
#392606=CARTESIAN_POINT('Ctrl Pts',(-1.6009399023683,2.21235024422325,8.78727029226991));
#392607=CARTESIAN_POINT('',(-1.60293438610527,2.22623025921639,8.75721825406948));
#392608=CARTESIAN_POINT('Origin',(-1.59693249240023,2.18446045038835,8.75937679713127));
#392609=CARTESIAN_POINT('',(-1.60293438610527,2.22623025921639,7.51860402984325));
#392610=CARTESIAN_POINT('',(-1.60293438610527,2.22623025921639,7.5));
#392611=CARTESIAN_POINT('Ctrl Pts',(-1.60293438610527,2.22623025921639,
7.51860402984325));
#392612=CARTESIAN_POINT('Ctrl Pts',(-1.60136802933078,2.21532966618994,
7.52834476460825));
#392613=CARTESIAN_POINT('Ctrl Pts',(-1.59980065570007,2.20442199665579,
7.53807742314407));
#392614=CARTESIAN_POINT('Ctrl Pts',(-1.59823223107085,2.19350701301077,
7.54780169004674));
#392615=CARTESIAN_POINT('Ctrl Pts',(-1.59574793122428,2.1762182688216,7.5632044032688));
#392616=CARTESIAN_POINT('Ctrl Pts',(-1.59326099139909,2.15891115248838,
7.57858609112103));
#392617=CARTESIAN_POINT('Ctrl Pts',(-1.59077126558568,2.14158464790051,
7.59394543036555));
#392618=CARTESIAN_POINT('Origin',(-1.85027428182726,2.24930835533596,7.5));
#392619=CARTESIAN_POINT('',(-1.67813633056181,2.17010558942599,8.75721825406948));
#392620=CARTESIAN_POINT('',(-1.66539749203247,2.16424429481555,8.78727029226991));
#392621=CARTESIAN_POINT('Origin',(-1.63306156849634,2.14936614294093,8.75658640621094));
#392622=CARTESIAN_POINT('',(-1.60045004741997,2.13436118528463,8.85049129520029));
#392623=CARTESIAN_POINT('Ctrl Pts',(-1.66539749203247,2.16424429481555,
8.78727029226991));
#392624=CARTESIAN_POINT('Ctrl Pts',(-1.64377905123609,2.15429738715721,
8.80838212259896));
#392625=CARTESIAN_POINT('Ctrl Pts',(-1.62213066475766,2.14433670112618,
8.82945686509571));
#392626=CARTESIAN_POINT('Ctrl Pts',(-1.60045004741997,2.13436118528463,
8.85049129520029));
#392627=CARTESIAN_POINT('',(-1.60045004741997,2.13436118528463,7.59394543036555));
#392628=CARTESIAN_POINT('',(-1.60045004741997,2.13436118528463,7.5));
#392629=CARTESIAN_POINT('',(-1.67813633056181,2.17010558942599,7.51860402984325));
#392630=CARTESIAN_POINT('Ctrl Pts',(-1.60045004741997,2.13436118528463,
7.59394543036555));
#392631=CARTESIAN_POINT('Ctrl Pts',(-1.61635201469679,2.14167787391996,
7.57858609112103));
#392632=CARTESIAN_POINT('Ctrl Pts',(-1.63223618776747,2.14898637522455,
7.56320440326857));
#392633=CARTESIAN_POINT('Ctrl Pts',(-1.64810349920118,2.15628711828479,
7.54780169004651));
#392634=CARTESIAN_POINT('Ctrl Pts',(-1.65812108306352,2.16089633051137,
7.53807742314383));
#392635=CARTESIAN_POINT('Ctrl Pts',(-1.66813195416115,2.16550245411323,
7.52834476460825));
#392636=CARTESIAN_POINT('Ctrl Pts',(-1.67813633056181,2.17010558942599,
7.51860402984325));
#392637=CARTESIAN_POINT('',(-1.67813633056181,2.17010558942599,7.5));
#392638=CARTESIAN_POINT('Origin',(-1.59757636816869,2.14060679114481,7.5));
#392639=CARTESIAN_POINT('Ctrl Pts',(-1.60045004741997,2.13436118528463,
8.85049129520029));
#392640=CARTESIAN_POINT('Ctrl Pts',(-1.60027411528379,2.13428023676807,
8.85097269580138));
#392641=CARTESIAN_POINT('Ctrl Pts',(-1.60009688697325,2.13420795092934,
8.85143669361005));
#392642=CARTESIAN_POINT('Ctrl Pts',(-1.59990987151214,2.13414180877791,
8.8519052845931));
#392643=CARTESIAN_POINT('Ctrl Pts',(-1.59954408113029,2.13401243892429,
8.85282181883899));
#392644=CARTESIAN_POINT('Ctrl Pts',(-1.59915019230981,2.13391008645579,
8.85372622499635));
#392645=CARTESIAN_POINT('Ctrl Pts',(-1.59871814646302,2.13384806842956,
8.8546225773507));
#392646=CARTESIAN_POINT('Ctrl Pts',(-1.59835947734583,2.13379658326685,
8.85536669723986));
#392647=CARTESIAN_POINT('Ctrl Pts',(-1.5979744341408,2.13377285249161,8.85610498449051));
#392648=CARTESIAN_POINT('Ctrl Pts',(-1.5975567370227,2.13379248063128,8.85681338218371));
#392649=CARTESIAN_POINT('Ctrl Pts',(-1.59717767623202,2.13381029319887,
8.85745625420284));
#392650=CARTESIAN_POINT('Ctrl Pts',(-1.59676693999368,2.13386344000459,
8.85808743050666));
#392651=CARTESIAN_POINT('Ctrl Pts',(-1.59631559501554,2.13397908798499,
8.85866804508411));
#392652=CARTESIAN_POINT('Ctrl Pts',(-1.59610735422658,2.1340324454562,8.85893592806396));
#392653=CARTESIAN_POINT('Ctrl Pts',(-1.59589042136149,2.134099345177,8.85919241173848));
#392654=CARTESIAN_POINT('Ctrl Pts',(-1.59566382655845,2.13418404876029,
8.85943017985534));
#392655=CARTESIAN_POINT('Ctrl Pts',(-1.5953578564951,2.13429842367268,8.8597512372));
#392656=CARTESIAN_POINT('Ctrl Pts',(-1.59502670637818,2.13444877149743,
8.86004599534705));
#392657=CARTESIAN_POINT('Ctrl Pts',(-1.59467866049515,2.13464276930003,
8.86026130871721));
#392658=CARTESIAN_POINT('Ctrl Pts',(-1.59455123108491,2.13471379736494,
8.86034014101235));
#392659=CARTESIAN_POINT('Ctrl Pts',(-1.59441961667037,2.13479173285642,
8.86040910639693));
#392660=CARTESIAN_POINT('Ctrl Pts',(-1.59428757440422,2.13487474190566,
8.86046313645507));
#392661=CARTESIAN_POINT('Ctrl Pts',(-1.59408152355374,2.13500427683181,
8.8605474499083));
#392662=CARTESIAN_POINT('Ctrl Pts',(-1.59386888451753,2.13514982695018,
8.86059655985668));
#392663=CARTESIAN_POINT('Ctrl Pts',(-1.59366312900933,2.13530181594062,
8.86059725258816));
#392664=CARTESIAN_POINT('Ctrl Pts',(-1.59345689812371,2.13545415608635,
8.86059794692011));
#392665=CARTESIAN_POINT('Ctrl Pts',(-1.59325687403524,2.13561679132399,
8.86056369958366));
#392666=CARTESIAN_POINT('Ctrl Pts',(-1.59307159215571,2.13577793168174,
8.86048590497774));
#392667=CARTESIAN_POINT('Ctrl Pts',(-1.59302323910166,2.13581998451738,
8.86046560290182));
#392668=CARTESIAN_POINT('Ctrl Pts',(-1.59297532046823,2.13586255097362,
8.86044257503091));
#392669=CARTESIAN_POINT('Ctrl Pts',(-1.59292929518032,2.13590429117004,
8.86041778462583));
#392670=CARTESIAN_POINT('Ctrl Pts',(-1.5926196021053,2.1361851508967,8.860250975962));
#392671=CARTESIAN_POINT('Ctrl Pts',(-1.59235429876773,2.13646653421406,
8.8599848982295));
#392672=CARTESIAN_POINT('Ctrl Pts',(-1.59213496417169,2.13673441605688,
8.85968173251461));
#392673=CARTESIAN_POINT('Ctrl Pts',(-1.59201894873675,2.13687611020393,
8.85952137522076));
#392674=CARTESIAN_POINT('Ctrl Pts',(-1.5919134104205,2.13701663718526,8.85934740853961));
#392675=CARTESIAN_POINT('Ctrl Pts',(-1.59181859451241,2.13715308171862,
8.8591675900182));
#392676=CARTESIAN_POINT('Ctrl Pts',(-1.59143785935708,2.13770097744252,
8.85844552518694));
#392677=CARTESIAN_POINT('Ctrl Pts',(-1.59120601346866,2.13821228521468,
8.85759444184122));
#392678=CARTESIAN_POINT('Ctrl Pts',(-1.59105442443434,2.13864615733892,
8.85683498915135));
#392679=CARTESIAN_POINT('Ctrl Pts',(-1.59103856104561,2.13869156090121,
8.85675551444996));
#392680=CARTESIAN_POINT('Ctrl Pts',(-1.59102359633076,2.13873611922891,
8.8566769979365));
#392681=CARTESIAN_POINT('Ctrl Pts',(-1.59100946472095,2.13877978665774,
8.85659965593547));
#392682=CARTESIAN_POINT('Ctrl Pts',(-1.59081871553059,2.1393692118404,8.85555568965886));
#392683=CARTESIAN_POINT('Ctrl Pts',(-1.5907205184002,2.13996323391635,8.85434650606346));
#392684=CARTESIAN_POINT('Ctrl Pts',(-1.59070825637446,2.14056377579998,
8.85297329937117));
#392685=CARTESIAN_POINT('Ctrl Pts',(-1.59070135973212,2.14090154401798,
8.85220095427747));
#392686=CARTESIAN_POINT('Ctrl Pts',(-1.59072195981991,2.14124151912217,
8.85137579139183));
#392687=CARTESIAN_POINT('Ctrl Pts',(-1.59077126558568,2.14158464790051,
8.85049129520029));
#392688=CARTESIAN_POINT('Origin',(-1.59757636816869,2.14060679114481,7.59394543036555));
#392689=CARTESIAN_POINT('Ctrl Pts',(-1.5999392570785,2.13412616443334,7.59443877723642));
#392690=CARTESIAN_POINT('Ctrl Pts',(-1.59467860803055,2.13170567579608,
7.58783886950016));
#392691=CARTESIAN_POINT('Ctrl Pts',(-1.58944159958292,2.13838796014023,
7.58559994247159));
#392692=CARTESIAN_POINT('Ctrl Pts',(-1.6286569858903,2.14733954088999,7.56670252222132));
#392693=CARTESIAN_POINT('Ctrl Pts',(-1.62340393997377,2.14492255054603,
7.56004874999026));
#392694=CARTESIAN_POINT('Ctrl Pts',(-1.61811908396269,2.15163125043487,
7.55786368756704));
#392695=CARTESIAN_POINT('Ctrl Pts',(-1.65732108721283,2.16052824268631,
7.53888913333556));
#392696=CARTESIAN_POINT('Ctrl Pts',(-1.65203682218721,2.15809688805035,
7.53222002137275));
#392697=CARTESIAN_POINT('Ctrl Pts',(-1.64674452104204,2.16484922048508,
7.53005029815326));
#392698=CARTESIAN_POINT('Ctrl Pts',(-1.68593026397609,2.17369167302459,
7.51101258149734));
#392699=CARTESIAN_POINT('Ctrl Pts',(-1.68058194405661,2.17123084595258,
7.5043616886572));
#392700=CARTESIAN_POINT('Ctrl Pts',(-1.67531646186255,2.17804129225284,
7.50217374673251));
#392701=CARTESIAN_POINT('',(-1.67379182682864,2.17733734542425,7.50366116523517));
#392702=CARTESIAN_POINT('Ctrl Pts',(-1.67813633056181,2.17010558942599,
7.51860402984325));
#392703=CARTESIAN_POINT('Ctrl Pts',(-1.67853751304855,2.17029017836963,
7.51734760759494));
#392704=CARTESIAN_POINT('Ctrl Pts',(-1.67887516973812,2.17051103085425,
7.51608817408573));
#392705=CARTESIAN_POINT('Ctrl Pts',(-1.6791412144495,2.17077881433843,7.5148100591312));
#392706=CARTESIAN_POINT('Ctrl Pts',(-1.67938220410642,2.1710213790173,7.51365231206384));
#392707=CARTESIAN_POINT('Ctrl Pts',(-1.67956495208892,2.17130261697214,
7.51247773061043));
#392708=CARTESIAN_POINT('Ctrl Pts',(-1.67965533378804,2.17163778110542,
7.51129758471022));
#392709=CARTESIAN_POINT('Ctrl Pts',(-1.67976766791807,2.1720543518459,7.50983079813401));
#392710=CARTESIAN_POINT('Ctrl Pts',(-1.67972115732488,2.17254432228918,
7.50839324291155));
#392711=CARTESIAN_POINT('Ctrl Pts',(-1.67943339189004,2.17310347783573,
7.50715379678855));
#392712=CARTESIAN_POINT('Ctrl Pts',(-1.67930045255091,2.17336179158656,
7.50658120839351));
#392713=CARTESIAN_POINT('Ctrl Pts',(-1.67908867816628,2.17366724429875,
7.50598221009429));
#392714=CARTESIAN_POINT('Ctrl Pts',(-1.67878441548016,2.17399960639674,
7.50545747549611));
#392715=CARTESIAN_POINT('Ctrl Pts',(-1.67862205149304,2.1741769650998,7.50517746087247));
#392716=CARTESIAN_POINT('Ctrl Pts',(-1.67843173911099,2.17436404651079,
7.50491486231392));
#392717=CARTESIAN_POINT('Ctrl Pts',(-1.6782173488015,2.17455470687898,7.50468370960992));
#392718=CARTESIAN_POINT('Ctrl Pts',(-1.67789676766324,2.17483980426982,
7.50433806340447));
#392719=CARTESIAN_POINT('Ctrl Pts',(-1.67751236609578,2.17514103710608,
7.50405484070984));
#392720=CARTESIAN_POINT('Ctrl Pts',(-1.67708959094887,2.17543755403429,
7.50385766036131));
#392721=CARTESIAN_POINT('Ctrl Pts',(-1.67704438171832,2.17546926191084,
7.50383657498791));
#392722=CARTESIAN_POINT('Ctrl Pts',(-1.67699876196235,2.17550091364687,
7.50381643264937));
#392723=CARTESIAN_POINT('Ctrl Pts',(-1.67695278336429,2.17553248245705,
7.50379723213559));
#392724=CARTESIAN_POINT('Ctrl Pts',(-1.67664586118161,2.17574321459188,
7.50366906242519));
#392725=CARTESIAN_POINT('Ctrl Pts',(-1.67631586572899,2.17595424268713,
7.50358235568538));
#392726=CARTESIAN_POINT('Ctrl Pts',(-1.67599290128613,2.1761500019308,7.5035341175365));
#392727=CARTESIAN_POINT('Ctrl Pts',(-1.67550865265657,2.17644352076102,
7.50346178989176));
#392728=CARTESIAN_POINT('Ctrl Pts',(-1.67497523124542,2.17673869053725,
7.50346967198527));
#392729=CARTESIAN_POINT('Ctrl Pts',(-1.67444266060026,2.17701234294118,
7.50354272648693));
#392730=CARTESIAN_POINT('Ctrl Pts',(-1.67422360327035,2.17712490183919,
7.50357277531559));
#392731=CARTESIAN_POINT('Ctrl Pts',(-1.67400504573784,2.17723379689431,
7.50361331098761));
#392732=CARTESIAN_POINT('Ctrl Pts',(-1.67379182682951,2.17733734542537,
7.50366116523659));
#392733=CARTESIAN_POINT('',(-1.59932759105274,2.14295327027008,7.57603338622103));
#392734=CARTESIAN_POINT('Origin',(-1.60461077043295,2.15003701964751,7.58486873427628));
#392735=CARTESIAN_POINT('Ctrl Pts',(-1.67379182688272,2.17733734544332,
7.50366116529969));
#392736=CARTESIAN_POINT('Ctrl Pts',(-1.64901056798236,2.16589544848023,
7.52783573079709));
#392737=CARTESIAN_POINT('Ctrl Pts',(-1.62419032049072,2.15443464751556,
7.55196141284068));
#392738=CARTESIAN_POINT('Ctrl Pts',(-1.59932759229143,2.14295327045253,
7.57603338728831));
#392739=CARTESIAN_POINT('Ctrl Pts',(-1.60131081754386,2.13495077015054,
7.59639677331371));
#392740=CARTESIAN_POINT('Ctrl Pts',(-1.58612303190611,2.12478203949354,
7.59959882295467));
#392741=CARTESIAN_POINT('Ctrl Pts',(-1.59104033438506,2.14240387109349,
7.59642833564546));
#392742=CARTESIAN_POINT('Ctrl Pts',(-1.5984605437931,2.13228786879496,7.58707626057421));
#392743=CARTESIAN_POINT('Ctrl Pts',(-1.59169006087516,2.13255778006641,
7.58809943920599));
#392744=CARTESIAN_POINT('Ctrl Pts',(-1.58940753054067,2.13892209118902,
7.58710240504253));
#392745=CARTESIAN_POINT('Ctrl Pts',(-1.59858892220314,2.13836315901399,
7.58015376756929));
#392746=CARTESIAN_POINT('Ctrl Pts',(-1.59574942482533,2.13810523259534,
7.58205880659761));
#392747=CARTESIAN_POINT('Ctrl Pts',(-1.59515444522379,2.14085715452587,
7.58020924244127));
#392748=CARTESIAN_POINT('Ctrl Pts',(-1.59932759055792,2.14295326960673,
7.57603338509286));
#392749=CARTESIAN_POINT('Ctrl Pts',(-1.59932759055792,2.14295326960673,
7.57603338509286));
#392750=CARTESIAN_POINT('Ctrl Pts',(-1.59932759055792,2.14295326960673,
7.57603338509286));
#392751=CARTESIAN_POINT('Origin',(-1.60461534358171,2.15003360661839,7.58486873427622));
#392752=CARTESIAN_POINT('Ctrl Pts',(-1.60415851687137,2.23474923235822,
7.51098857897448));
#392753=CARTESIAN_POINT('Ctrl Pts',(-1.60332114180599,2.22892177022006,
7.50433767179956));
#392754=CARTESIAN_POINT('Ctrl Pts',(-1.61134830926253,2.22581168441625,
7.50214974420965));
#392755=CARTESIAN_POINT('Ctrl Pts',(-1.59967797104069,2.20356820934231,
7.53887321589168));
#392756=CARTESIAN_POINT('Ctrl Pts',(-1.59885062921467,2.19781057054244,
7.53220407452063));
#392757=CARTESIAN_POINT('Ctrl Pts',(-1.60682970075316,2.19465821629432,
7.53003438070911));
#392758=CARTESIAN_POINT('Ctrl Pts',(-1.5951888209092,2.17232730725995,7.56669465659229));
#392759=CARTESIAN_POINT('Ctrl Pts',(-1.59436636851957,2.16660369503491,
7.56004085833293));
#392760=CARTESIAN_POINT('Ctrl Pts',(-1.60230148007192,2.16344606067078,
7.55785582193789));
#392761=CARTESIAN_POINT('Ctrl Pts',(-1.59069126950322,2.14102793901222,
7.59443891967696));
#392762=CARTESIAN_POINT('Ctrl Pts',(-1.58986762466,2.1352960282621,7.58783901202978));
#392763=CARTESIAN_POINT('Ctrl Pts',(-1.59776378899004,2.13217677084064,
7.58560008491213));
#392764=CARTESIAN_POINT('',(-1.61110336926411,2.2241229572313,7.50366116523517));
#392765=CARTESIAN_POINT('Ctrl Pts',(-1.61110336926433,2.2241229572316,7.50366116523554));
#392766=CARTESIAN_POINT('Ctrl Pts',(-1.61059198069087,2.22468208087061,
7.50350835821027));
#392767=CARTESIAN_POINT('Ctrl Pts',(-1.61010369996943,2.22517941370506,
7.50345484956));
#392768=CARTESIAN_POINT('Ctrl Pts',(-1.60962443861778,2.22563016254553,
7.50349758195598));
#392769=CARTESIAN_POINT('Ctrl Pts',(-1.60937854200143,2.2258614301291,7.50351950684424));
#392770=CARTESIAN_POINT('Ctrl Pts',(-1.60911087181359,2.22610332366123,
7.50357029184312));
#392771=CARTESIAN_POINT('Ctrl Pts',(-1.60884634880776,2.22632948384843,
7.50365515313924));
#392772=CARTESIAN_POINT('Ctrl Pts',(-1.60843940530885,2.22667740979763,
7.50378570417639));
#392773=CARTESIAN_POINT('Ctrl Pts',(-1.60802819036976,2.22699857665869,
7.50400001621911));
#392774=CARTESIAN_POINT('Ctrl Pts',(-1.60764260590765,2.22726674962693,
7.50428903009634));
#392775=CARTESIAN_POINT('Ctrl Pts',(-1.60759980899887,2.22729651476321,
7.50432110841318));
#392776=CARTESIAN_POINT('Ctrl Pts',(-1.60755731717549,2.22732565543007,
7.50435406373354));
#392777=CARTESIAN_POINT('Ctrl Pts',(-1.60751516316794,2.22735415659425,
7.50438785222352));
#392778=CARTESIAN_POINT('Ctrl Pts',(-1.60725779269008,2.22752816990098,
7.50459414719561));
#392779=CARTESIAN_POINT('Ctrl Pts',(-1.60700862846065,2.22768068774654,
7.50483629897752));
#392780=CARTESIAN_POINT('Ctrl Pts',(-1.606777902955,2.22780698965991,7.5050991045531));
#392781=CARTESIAN_POINT('Ctrl Pts',(-1.60626889931535,2.22808562436663,
7.50567888004914));
#392782=CARTESIAN_POINT('Ctrl Pts',(-1.60582982688945,2.22824810547532,
7.50637912803144));
#392783=CARTESIAN_POINT('Ctrl Pts',(-1.60546347309894,2.22832521688821,
7.50710440483569));
#392784=CARTESIAN_POINT('Ctrl Pts',(-1.60537363587636,2.22834412613752,
7.50728225710685));
#392785=CARTESIAN_POINT('Ctrl Pts',(-1.60528641310257,2.22835842111519,
7.50746498566954));
#392786=CARTESIAN_POINT('Ctrl Pts',(-1.60520390821615,2.22836817923874,
7.50764697238949));
#392787=CARTESIAN_POINT('Ctrl Pts',(-1.6047603846527,2.22842063622541,7.50862528291181));
#392788=CARTESIAN_POINT('Ctrl Pts',(-1.60441342469442,2.22835085759284,
7.50965856837421));
#392789=CARTESIAN_POINT('Ctrl Pts',(-1.60413297204735,2.22821793661504,
7.51067959873201));
#392790=CARTESIAN_POINT('Ctrl Pts',(-1.60397863860191,2.22814479003329,
7.51124147302578));
#392791=CARTESIAN_POINT('Ctrl Pts',(-1.60384459404929,2.22805211156062,
7.51180065547253));
#392792=CARTESIAN_POINT('Ctrl Pts',(-1.60372708158227,2.22794733879845,
7.51235175716501));
#392793=CARTESIAN_POINT('Ctrl Pts',(-1.60332102919732,2.22758530716864,
7.51425603304536));
#392794=CARTESIAN_POINT('Ctrl Pts',(-1.6030679879822,2.22703118031393,7.51626900505181));
#392795=CARTESIAN_POINT('Ctrl Pts',(-1.60295199935763,2.22634316468707,
7.51827788969244));
#392796=CARTESIAN_POINT('Ctrl Pts',(-1.60294572183408,2.22630592798117,
7.51838661432546));
#392797=CARTESIAN_POINT('Ctrl Pts',(-1.60293985101502,2.2262682906267,7.51849533314857));
#392798=CARTESIAN_POINT('Ctrl Pts',(-1.60293438610526,2.2262302592164,7.51860402984325));
#392799=CARTESIAN_POINT('Ctrl Pts',(-1.59932759087573,2.14295327151058,
7.57603338728985));
#392800=CARTESIAN_POINT('Ctrl Pts',(-1.60326028592398,2.17005513828706,
7.55196141284922));
#392801=CARTESIAN_POINT('Ctrl Pts',(-1.60718534226387,2.19711042572333,
7.52783573083105));
#392802=CARTESIAN_POINT('Ctrl Pts',(-1.61110336926719,2.2241229572904,7.50366116530176));
#392803=CARTESIAN_POINT('Origin',(-5.52641612598462E-16,7.404894141953E-16,
7.49482233047033));
#392804=CARTESIAN_POINT('Origin',(-1.66840488432876,2.17032978875284,7.49482233047033));
#392805=CARTESIAN_POINT('Origin',(0.,0.,7.50366116523517));
#392806=CARTESIAN_POINT('Origin',(-1.60591818370371,2.21696482544261,7.49482233047033));
#392807=CARTESIAN_POINT('Ctrl Pts',(-1.67813536969267,2.17010514726915,
7.51860402984325));
#392808=CARTESIAN_POINT('Ctrl Pts',(-1.68504747448011,2.17328619952234,
7.51860402984325));
#392809=CARTESIAN_POINT('Ctrl Pts',(-1.6910477827585,2.16860724808057,7.51860402984325));
#392810=CARTESIAN_POINT('Ctrl Pts',(-1.68070188190216,2.17128629252504,
7.51041458714365));
#392811=CARTESIAN_POINT('Ctrl Pts',(-1.68646901015029,2.17217769452733,
7.51004642900442));
#392812=CARTESIAN_POINT('Ctrl Pts',(-1.69104943757228,2.16860595768131,
7.50729136483009));
#392813=CARTESIAN_POINT('Ctrl Pts',(-1.68047942032504,2.17409240158313,
7.50215815450138));
#392814=CARTESIAN_POINT('Ctrl Pts',(-1.68357470801357,2.17443483202392,
7.49877163671531));
#392815=CARTESIAN_POINT('Ctrl Pts',(-1.68631009160461,2.17233207188445,
7.49481588533172));
#392816=CARTESIAN_POINT('Ctrl Pts',(-1.67379149130792,2.17733690896585,
7.50366171572174));
#392817=CARTESIAN_POINT('Ctrl Pts',(-1.67602317147151,2.18023997043688,
7.50000045605858));
#392818=CARTESIAN_POINT('Ctrl Pts',(-1.67602317147161,2.1802399704368,7.49482233047317));
#392819=CARTESIAN_POINT('Origin',(-1.68336120192778,2.15874994240748,7.51860402984325));
#392820=CARTESIAN_POINT('Origin',(-1.68336120192778,2.15874994240748,9.));
#392821=CARTESIAN_POINT('Origin',(-1.68336120192778,2.15874994240748,8.75721825406948));
#392822=CARTESIAN_POINT('Ctrl Pts',(-1.66296505241367,2.16312506649482,
8.78942910404913));
#392823=CARTESIAN_POINT('Ctrl Pts',(-1.66801889291352,2.165472645014,8.79672699501691));
#392824=CARTESIAN_POINT('Ctrl Pts',(-1.67320190366867,2.15820560397284,
8.79893251111267));
#392825=CARTESIAN_POINT('Ctrl Pts',(-1.67295287420539,2.16772058981616,
8.78111911759583));
#392826=CARTESIAN_POINT('Ctrl Pts',(-1.6789473966294,2.17049692031401,8.78644465894815));
#392827=CARTESIAN_POINT('Ctrl Pts',(-1.68496047887327,2.16506016082846,
8.78817647674132));
#392828=CARTESIAN_POINT('Ctrl Pts',(-1.67917752299136,2.17058462953469,
8.76780923932029));
#392829=CARTESIAN_POINT('Ctrl Pts',(-1.68625594515375,2.17385734651933,
8.76988516158372));
#392830=CARTESIAN_POINT('Ctrl Pts',(-1.69231030965761,2.16933174701751,
8.77093053738832));
#392831=CARTESIAN_POINT('Ctrl Pts',(-1.67796380166912,2.17002618098514,
8.75371302330492));
#392832=CARTESIAN_POINT('Ctrl Pts',(-1.68486817724058,2.17321926716246,
8.75300828287559));
#392833=CARTESIAN_POINT('Ctrl Pts',(-1.69087702405879,2.16849821862961,
8.75267964240737));
#392834=CARTESIAN_POINT('Origin',(-1.67062236339843,2.15288864779704,8.78727029226991));
#392835=CARTESIAN_POINT('Ctrl Pts',(-1.60045004741997,2.13436118528463,
8.85049129520029));
#392836=CARTESIAN_POINT('Ctrl Pts',(-1.60575505664341,2.13680208457839,
8.85711686593484));
#392837=CARTESIAN_POINT('Ctrl Pts',(-1.61100669796544,2.13005515746016,
8.85933012996512));
#392838=CARTESIAN_POINT('Ctrl Pts',(-1.62213069385385,2.14433671451369,
8.82945683644722));
#392839=CARTESIAN_POINT('Ctrl Pts',(-1.62747973786132,2.14679787474737,
8.83607469902389));
#392840=CARTESIAN_POINT('Ctrl Pts',(-1.63271720381484,2.14000810355219,
8.83829567148519));
#392841=CARTESIAN_POINT('Ctrl Pts',(-1.6437790235359,2.15429737441201,8.80838214965002));
#392842=CARTESIAN_POINT('Ctrl Pts',(-1.64914917736843,2.15676824753307,
8.81501364461988));
#392843=CARTESIAN_POINT('Ctrl Pts',(-1.65439449734901,2.14994655925989,
8.81722098428722));
#392844=CARTESIAN_POINT('Ctrl Pts',(-1.66539749203247,2.16424429481555,
8.78727029226991));
#392845=CARTESIAN_POINT('Ctrl Pts',(-1.6707685378652,2.16671557835677,8.79393457792714));
#392846=CARTESIAN_POINT('Ctrl Pts',(-1.6760411057995,2.15987164362912,8.79610912703474));
#392847=CARTESIAN_POINT('Origin',(-1.60567491878594,2.12300553826611,8.85049129520029));
#392848=CARTESIAN_POINT('Ctrl Pts',(-1.59077126558568,2.14158464790051,
8.85049129520029));
#392849=CARTESIAN_POINT('Ctrl Pts',(-1.59160185579971,2.14736489288835,
8.85711686593484));
#392850=CARTESIAN_POINT('Ctrl Pts',(-1.58363955683347,2.15047978570932,
8.85933012996512));
#392851=CARTESIAN_POINT('Ctrl Pts',(-1.59003645441302,2.13647094859848,
8.86332496987231));
#392852=CARTESIAN_POINT('Ctrl Pts',(-1.58650902291588,2.13945576373678,
8.86648636486736));
#392853=CARTESIAN_POINT('Ctrl Pts',(-1.5816008510766,2.13617156656111,8.87206031107456));
#392854=CARTESIAN_POINT('Ctrl Pts',(-1.59572489012279,2.13218708291763,
8.86341338519877));
#392855=CARTESIAN_POINT('Ctrl Pts',(-1.59958467164427,2.1296227979801,8.86654584966058));
#392856=CARTESIAN_POINT('Ctrl Pts',(-1.59776984823888,2.12398093935066,
8.87215952290716));
#392857=CARTESIAN_POINT('Ctrl Pts',(-1.60045004741997,2.13436118528463,
8.85049129520029));
#392858=CARTESIAN_POINT('Ctrl Pts',(-1.60575505664341,2.13680208457839,
8.85711686593484));
#392859=CARTESIAN_POINT('Ctrl Pts',(-1.61100669796544,2.13005515746016,
8.85933012996512));
#392860=CARTESIAN_POINT('Origin',(-1.57839835179838,2.1433625692745,8.85049129520029));
#392861=CARTESIAN_POINT('Ctrl Pts',(-1.6009399023683,2.21235024422325,8.78727029226991));
#392862=CARTESIAN_POINT('Ctrl Pts',(-1.60178083174653,2.21820244154214,
8.79393457792714));
#392863=CARTESIAN_POINT('Ctrl Pts',(-1.59371958050516,2.22130979469259,
8.79610912703474));
#392864=CARTESIAN_POINT('Ctrl Pts',(-1.5975551602087,2.18879514018686,8.80838214965001));
#392865=CARTESIAN_POINT('Ctrl Pts',(-1.59839594992902,2.19464636559803,
8.81501364461995));
#392866=CARTESIAN_POINT('Ctrl Pts',(-1.59036377844289,2.19773392674114,
8.81722098428721));
#392867=CARTESIAN_POINT('Ctrl Pts',(-1.59416574276817,2.16520749992664,
8.82945683644723));
#392868=CARTESIAN_POINT('Ctrl Pts',(-1.59500322738317,2.17103572444267,
8.83607469902388));
#392869=CARTESIAN_POINT('Ctrl Pts',(-1.58700388846103,2.17412483747175,
8.83829567148519));
#392870=CARTESIAN_POINT('Ctrl Pts',(-1.59077126558568,2.14158464790051,
8.85049129520029));
#392871=CARTESIAN_POINT('Ctrl Pts',(-1.59160185579971,2.14736489288835,
8.85711686593484));
#392872=CARTESIAN_POINT('Ctrl Pts',(-1.58363955683347,2.15047978570932,
8.85933012996512));
#392873=CARTESIAN_POINT('Origin',(-1.588566988581,2.21412816559724,8.78727029226991));
#392874=CARTESIAN_POINT('Ctrl Pts',(-1.60290803169131,2.22604698322442,
8.75374538247848));
#392875=CARTESIAN_POINT('Ctrl Pts',(-1.60400184926497,2.23356681975876,
8.75304829418601));
#392876=CARTESIAN_POINT('Ctrl Pts',(-1.5977761367062,2.23798396208662,8.75272238421917));
#392877=CARTESIAN_POINT('Ctrl Pts',(-1.6030957782893,2.22735354670509,8.76769408445021));
#392878=CARTESIAN_POINT('Ctrl Pts',(-1.6042164382461,2.23506271502815,8.76974318093968));
#392879=CARTESIAN_POINT('Ctrl Pts',(-1.59816348603553,2.23957715041,8.77077869880429));
#392880=CARTESIAN_POINT('Ctrl Pts',(-1.60213349619479,2.22065684660117,
8.78108014887988));
#392881=CARTESIAN_POINT('Ctrl Pts',(-1.60308697501544,2.22718954247952,
8.78639403366325));
#392882=CARTESIAN_POINT('Ctrl Pts',(-1.59618455646937,2.23141786294322,
8.78812224174742));
#392883=CARTESIAN_POINT('Ctrl Pts',(-1.60055652823305,2.20968243344755,
8.78944554828686));
#392884=CARTESIAN_POINT('Ctrl Pts',(-1.60136562387221,2.21518713887687,
8.79673892988686));
#392885=CARTESIAN_POINT('Ctrl Pts',(-1.59293408710642,2.21808761161141,
8.79894799272499));
#392886=CARTESIAN_POINT('Origin',(-1.59056147231797,2.22800818059039,8.75721825406948));
#392887=CARTESIAN_POINT('Origin',(-1.59056147231797,2.22800818059039,9.));
#392888=CARTESIAN_POINT('Origin',(-1.59056147231797,2.22800818059039,7.51860402984325));
#392889=CARTESIAN_POINT('Ctrl Pts',(-1.61110290777817,2.22412232015156,
7.50366195182966));
#392890=CARTESIAN_POINT('Ctrl Pts',(-1.61325114344654,2.22708795249951,
7.50000065167735));
#392891=CARTESIAN_POINT('Ctrl Pts',(-1.61325114344644,2.22708795249958,
7.49482233047108));
#392892=CARTESIAN_POINT('Ctrl Pts',(-1.60608447429972,2.22961496296073,
7.50215800491337));
#392893=CARTESIAN_POINT('Ctrl Pts',(-1.60553053494261,2.23268055399069,
7.49877273257265));
#392894=CARTESIAN_POINT('Ctrl Pts',(-1.60273484608023,2.23470571574589,
7.49481816995647));
#392895=CARTESIAN_POINT('Ctrl Pts',(-1.603335619623,2.22902014003883,7.51043025814043));
#392896=CARTESIAN_POINT('Ctrl Pts',(-1.60255251348732,2.23480628744166,
7.51006209594516));
#392897=CARTESIAN_POINT('Ctrl Pts',(-1.59782224944537,2.23818320500886,
7.50731281821701));
#392898=CARTESIAN_POINT('Ctrl Pts',(-1.60293417104173,2.22622876318827,
7.51860402984326));
#392899=CARTESIAN_POINT('Ctrl Pts',(-1.604017376695,2.23376054139155,7.51860402984326));
#392900=CARTESIAN_POINT('Ctrl Pts',(-1.59782431009111,2.23818173392642,
7.51860402984327));
#392901=CARTESIAN_POINT('Origin',(0.,0.,7.5));
#392902=CARTESIAN_POINT('Origin',(-1.72471465490915,2.03526346763209,7.5));
#392903=CARTESIAN_POINT('',(-1.72471465490915,2.03526346763209,7.59394543036555));
#392904=CARTESIAN_POINT('',(-1.72471465490915,2.03526346763209,8.85049129520029));
#392905=CARTESIAN_POINT('',(-1.72471465490915,2.03526346763209,7.5));
#392906=CARTESIAN_POINT('',(-1.73939636646039,2.10523216165203,8.78727029226991));
#392907=CARTESIAN_POINT('Ctrl Pts',(-1.72471465490915,2.03526346763209,
8.85049129520029));
#392908=CARTESIAN_POINT('Ctrl Pts',(-1.72961567252276,2.05862026772969,
8.82945686509571));
#392909=CARTESIAN_POINT('Ctrl Pts',(-1.73450940418106,2.0819423451197,8.80838212259897));
#392910=CARTESIAN_POINT('Ctrl Pts',(-1.73939636646039,2.10523216165203,
8.78727029226991));
#392911=CARTESIAN_POINT('',(-1.74227604793056,2.11895587165397,8.75721825406948));
#392912=CARTESIAN_POINT('Origin',(-1.7336102849198,2.07765642602853,8.7593767971315));
#392913=CARTESIAN_POINT('',(-1.74227604793056,2.11895587165397,7.51860402984325));
#392914=CARTESIAN_POINT('',(-1.74227604793056,2.11895587165397,7.5));
#392915=CARTESIAN_POINT('Ctrl Pts',(-1.74227604793056,2.11895587165397,
7.51860402984325));
#392916=CARTESIAN_POINT('Ctrl Pts',(-1.74001450601092,2.10817803188809,
7.52834476460825));
#392917=CARTESIAN_POINT('Ctrl Pts',(-1.73775149593092,2.09739319530415,
7.53807742314407));
#392918=CARTESIAN_POINT('Ctrl Pts',(-1.73548696839508,2.08660112697468,
7.54780169004674));
#392919=CARTESIAN_POINT('Ctrl Pts',(-1.7319000791656,2.06950707400232,7.5632044032688));
#392920=CARTESIAN_POINT('Ctrl Pts',(-1.7283093782743,2.05239485577747,7.57858609112103));
#392921=CARTESIAN_POINT('Ctrl Pts',(-1.72471465490915,2.03526346763209,
7.59394543036555));
#392922=CARTESIAN_POINT('Origin',(-1.99058637600479,2.12613942982103,7.5));
#392923=CARTESIAN_POINT('',(-1.81372756198701,2.0581283108927,8.75721825406948));
#392924=CARTESIAN_POINT('',(-1.8006393623326,2.05309523912753,8.78727029226991));
#392925=CARTESIAN_POINT('Origin',(-1.76741662995628,2.040319425746,8.75658640621099));
#392926=CARTESIAN_POINT('',(-1.7339107418093,2.0274347247136,8.85049129520029));
#392927=CARTESIAN_POINT('Ctrl Pts',(-1.8006393623326,2.05309523912753,8.78727029226991));
#392928=CARTESIAN_POINT('Ctrl Pts',(-1.77842803837962,2.04455386671524,
8.80838212259896));
#392929=CARTESIAN_POINT('Ctrl Pts',(-1.75618594748781,2.03600066286584,
8.82945686509571));
#392930=CARTESIAN_POINT('Ctrl Pts',(-1.7339107418093,2.0274347247136,8.85049129520029));
#392931=CARTESIAN_POINT('',(-1.7339107418093,2.0274347247136,7.59394543036555));
#392932=CARTESIAN_POINT('',(-1.7339107418093,2.0274347247136,7.5));
#392933=CARTESIAN_POINT('',(-1.81372756198701,2.0581283108927,7.51860402984325));
#392934=CARTESIAN_POINT('Ctrl Pts',(-1.7339107418093,2.0274347247136,7.59394543036555));
#392935=CARTESIAN_POINT('Ctrl Pts',(-1.75024881863927,2.03371753788587,
7.57858609112103));
#392936=CARTESIAN_POINT('Ctrl Pts',(-1.76656861325911,2.03999332062785,
7.56320440326857));
#392937=CARTESIAN_POINT('Ctrl Pts',(-1.78287108381361,2.0462624413944,7.54780169004651));
#392938=CARTESIAN_POINT('Ctrl Pts',(-1.79316339871681,2.05022035469839,
7.53807742314383));
#392939=CARTESIAN_POINT('Ctrl Pts',(-1.80344881675855,2.05417561581188,
7.52834476460825));
#392940=CARTESIAN_POINT('Ctrl Pts',(-1.81372756198701,2.0581283108927,7.51860402984325));
#392941=CARTESIAN_POINT('',(-1.81372756198701,2.0581283108927,7.5));
#392942=CARTESIAN_POINT('Origin',(-1.73144312418161,2.03385161556849,7.5));
#392943=CARTESIAN_POINT('Ctrl Pts',(-1.7339107418093,2.0274347247136,8.85049129520029));
#392944=CARTESIAN_POINT('Ctrl Pts',(-1.7337299847553,2.02736521452512,8.85097269580139));
#392945=CARTESIAN_POINT('Ctrl Pts',(-1.73354848920974,2.02730443226224,
8.85143669361005));
#392946=CARTESIAN_POINT('Ctrl Pts',(-1.73335762024976,2.02725040812869,
8.8519052845931));
#392947=CARTESIAN_POINT('Ctrl Pts',(-1.7329842926685,2.02714474034954,8.85282181883899));
#392948=CARTESIAN_POINT('Ctrl Pts',(-1.73258465538967,2.02706783471854,
8.85372622499636));
#392949=CARTESIAN_POINT('Ctrl Pts',(-1.73214952371882,2.02703362538744,
8.85462257735071));
#392950=CARTESIAN_POINT('Ctrl Pts',(-1.7317882928601,2.02700522601576,8.85536669723986));
#392951=CARTESIAN_POINT('Ctrl Pts',(-1.73140252033164,2.02700621380079,
8.85610498449051));
#392952=CARTESIAN_POINT('Ctrl Pts',(-1.7309869389963,2.02705256355859,8.85681338218371));
#392953=CARTESIAN_POINT('Ctrl Pts',(-1.73060979828179,2.02709462603658,
8.85745625420284));
#392954=CARTESIAN_POINT('Ctrl Pts',(-1.73020331107265,2.02717397960764,
8.85808743050665));
#392955=CARTESIAN_POINT('Ctrl Pts',(-1.72976030302272,2.02731830774889,
8.85866804508409));
#392956=CARTESIAN_POINT('Ctrl Pts',(-1.72955590871171,2.02738489762462,
8.85893592806395));
#392957=CARTESIAN_POINT('Ctrl Pts',(-1.72934370783828,2.02746555882915,
8.85919241173848));
#392958=CARTESIAN_POINT('Ctrl Pts',(-1.72912300557577,2.02756460635873,
8.85943017985534));
#392959=CARTESIAN_POINT('Ctrl Pts',(-1.72882499218653,2.02769834984486,
8.8597512372));
#392960=CARTESIAN_POINT('Ctrl Pts',(-1.72850415527125,2.02786960562472,
8.86004599534706));
#392961=CARTESIAN_POINT('Ctrl Pts',(-1.7281692539677,2.02808550421431,8.86026130871721));
#392962=CARTESIAN_POINT('Ctrl Pts',(-1.7280466371586,2.02816455077479,8.86034014101236));
#392963=CARTESIAN_POINT('Ctrl Pts',(-1.72792028650407,2.02825075870394,
8.86040910639693));
#392964=CARTESIAN_POINT('Ctrl Pts',(-1.72779383394097,2.02834205717922,
8.86046313645507));
#392965=CARTESIAN_POINT('Ctrl Pts',(-1.72759650577527,2.02848452768529,
8.8605474499083));
#392966=CARTESIAN_POINT('Ctrl Pts',(-1.72739362905687,2.02864340258516,
8.86059655985668));
#392967=CARTESIAN_POINT('Ctrl Pts',(-1.72719803426348,2.02880826209859,
8.86059725258816));
#392968=CARTESIAN_POINT('Ctrl Pts',(-1.72700198756798,2.02897350250336,
8.86059794692011));
#392969=CARTESIAN_POINT('Ctrl Pts',(-1.7268127945259,2.02914861917682,8.86056369958366));
#392970=CARTESIAN_POINT('Ctrl Pts',(-1.72663821762604,2.02932129950519,
8.86048590497774));
#392971=CARTESIAN_POINT('Ctrl Pts',(-1.72659265825295,2.02936636392959,
8.86046560290182));
#392972=CARTESIAN_POINT('Ctrl Pts',(-1.72654756531571,2.02941191308586,
8.86044257503091));
#392973=CARTESIAN_POINT('Ctrl Pts',(-1.72650430889525,2.0294565163729,8.86041778462583));
#392974=CARTESIAN_POINT('Ctrl Pts',(-1.72621324686234,2.02975664114657,
8.86025097596201));
#392975=CARTESIAN_POINT('Ctrl Pts',(-1.72596651690997,2.03005444437492,
8.8599848982295));
#392976=CARTESIAN_POINT('Ctrl Pts',(-1.72576479620898,2.03033582864158,
8.85968173251462));
#392977=CARTESIAN_POINT('Ctrl Pts',(-1.72565809751538,2.03048466479724,
8.85952137522077));
#392978=CARTESIAN_POINT('Ctrl Pts',(-1.72556177963352,2.03063166491396,
8.85934740853961));
#392979=CARTESIAN_POINT('Ctrl Pts',(-1.72547590056615,2.03077390398348,
8.8591675900182));
#392980=CARTESIAN_POINT('Ctrl Pts',(-1.72513105147159,2.031345067782,8.85844552518695));
#392981=CARTESIAN_POINT('Ctrl Pts',(-1.72493244153685,2.03187017943457,
8.85759444184125));
#392982=CARTESIAN_POINT('Ctrl Pts',(-1.7248089622409,2.03231287246477,8.85683498915139));
#392983=CARTESIAN_POINT('Ctrl Pts',(-1.72479604046143,2.03235919911139,
8.85675551444999));
#392984=CARTESIAN_POINT('Ctrl Pts',(-1.72478396135505,2.0324046246818,8.85667699793652));
#392985=CARTESIAN_POINT('Ctrl Pts',(-1.72477265656191,2.03244910780657,
8.85659965593547));
#392986=CARTESIAN_POINT('Ctrl Pts',(-1.72462006388734,2.03304954329457,
8.85555568965886));
#392987=CARTESIAN_POINT('Ctrl Pts',(-1.72456012763856,2.03364863640019,
8.85434650606346));
#392988=CARTESIAN_POINT('Ctrl Pts',(-1.72458636765706,2.03424873003681,
8.85297329937117));
#392989=CARTESIAN_POINT('Ctrl Pts',(-1.72460112606864,2.03458624614316,
8.85220095427747));
#392990=CARTESIAN_POINT('Ctrl Pts',(-1.72464346611106,2.03492420287989,
8.85137579139184));
#392991=CARTESIAN_POINT('Ctrl Pts',(-1.72471465490915,2.03526346763209,
8.85049129520029));
#392992=CARTESIAN_POINT('Origin',(-1.73144312418161,2.03385161556849,7.59394543036555));
#392993=CARTESIAN_POINT('Ctrl Pts',(-1.73338594310372,2.0272329131874,7.59443877723642));
#392994=CARTESIAN_POINT('Ctrl Pts',(-1.727981021384,2.02515444864539,7.58783886950016));
#392995=CARTESIAN_POINT('Ctrl Pts',(-1.72318290835979,2.03215853980296,
7.58559994247159));
#392996=CARTESIAN_POINT('Ctrl Pts',(-1.76289125219803,2.03857919014269,
7.56670252222138));
#392997=CARTESIAN_POINT('Ctrl Pts',(-1.75749414212464,2.03650372957206,
7.56004874999027));
#392998=CARTESIAN_POINT('Ctrl Pts',(-1.75264997229472,2.04353724760462,
7.55786368756705));
#392999=CARTESIAN_POINT('Ctrl Pts',(-1.79234146307548,2.04990427905938,
7.53888913333557));
#393000=CARTESIAN_POINT('Ctrl Pts',(-1.78691227771271,2.04781648392494,
7.53222002137276));
#393001=CARTESIAN_POINT('Ctrl Pts',(-1.78206347359232,2.05489402186703,
7.53005029815327));
#393002=CARTESIAN_POINT('Ctrl Pts',(-1.82173524309422,2.06120766746957,
7.51101258149734));
#393003=CARTESIAN_POINT('Ctrl Pts',(-1.81624024613979,2.05909456446447,
7.5043616886572));
#393004=CARTESIAN_POINT('Ctrl Pts',(-1.81142192923624,2.06622837857486,
7.50217374673251));
#393005=CARTESIAN_POINT('',(-1.80985532470036,2.06562356178254,7.50366116523517));
#393006=CARTESIAN_POINT('Ctrl Pts',(-1.81372756198701,2.0581283108927,7.51860402984325));
#393007=CARTESIAN_POINT('Ctrl Pts',(-1.81413974685553,2.05828681672838,
7.51734760759493));
#393008=CARTESIAN_POINT('Ctrl Pts',(-1.81449085986049,2.05848558170951,
7.51608817408572));
#393009=CARTESIAN_POINT('Ctrl Pts',(-1.81477351490122,2.05873576946062,
7.51481005913119));
#393010=CARTESIAN_POINT('Ctrl Pts',(-1.81502955059138,2.058962395504,7.51365231206383));
#393011=CARTESIAN_POINT('Ctrl Pts',(-1.81522994207618,2.05923134692187,
7.51247773061043));
#393012=CARTESIAN_POINT('Ctrl Pts',(-1.81534161211616,2.05956003164914,
7.51129758471022));
#393013=CARTESIAN_POINT('Ctrl Pts',(-1.81548040522265,2.05996854922794,
7.50983079813402));
#393014=CARTESIAN_POINT('Ctrl Pts',(-1.81546538270455,2.06046049291832,
7.50839324291155));
#393015=CARTESIAN_POINT('Ctrl Pts',(-1.81521403373353,2.06103693681455,
7.50715379678855));
#393016=CARTESIAN_POINT('Ctrl Pts',(-1.81509791775136,2.06130323728478,
7.50658120839351));
#393017=CARTESIAN_POINT('Ctrl Pts',(-1.81490614890238,2.06162163084303,
7.50598221009429));
#393018=CARTESIAN_POINT('Ctrl Pts',(-1.81462380586932,2.06197280424467,
7.50545747549611));
#393019=CARTESIAN_POINT('Ctrl Pts',(-1.81447313888754,2.06216020124162,
7.50517746087247));
#393020=CARTESIAN_POINT('Ctrl Pts',(-1.81429520386984,2.06235909162997,
7.50491486231392));
#393021=CARTESIAN_POINT('Ctrl Pts',(-1.81409346969998,2.06256309630028,
7.50468370960993));
#393022=CARTESIAN_POINT('Ctrl Pts',(-1.81379181348259,2.06286814763201,
7.50433806340447));
#393023=CARTESIAN_POINT('Ctrl Pts',(-1.81342750176346,2.06319339024608,
7.50405484070984));
#393024=CARTESIAN_POINT('Ctrl Pts',(-1.81302459315824,2.06351638524513,
7.50385766036131));
#393025=CARTESIAN_POINT('Ctrl Pts',(-1.81298150834553,2.06355092453979,
7.50383657498791));
#393026=CARTESIAN_POINT('Ctrl Pts',(-1.81293801025394,2.06358543411174,
7.50381643264937));
#393027=CARTESIAN_POINT('Ctrl Pts',(-1.81289414874446,2.0636198839193,7.50379723213559));
#393028=CARTESIAN_POINT('Ctrl Pts',(-1.81260135882055,2.06384984765412,
7.50366906242519));
#393029=CARTESIAN_POINT('Ctrl Pts',(-1.81228556199546,2.06408158505075,
7.50358235568538));
#393030=CARTESIAN_POINT('Ctrl Pts',(-1.8119758034555,2.06429763448896,7.5035341175365));
#393031=CARTESIAN_POINT('Ctrl Pts',(-1.81151135558271,2.06462157616948,
7.50346178989176));
#393032=CARTESIAN_POINT('Ctrl Pts',(-1.81099794173554,2.06495031591491,
7.50346967198527));
#393033=CARTESIAN_POINT('Ctrl Pts',(-1.81048399828362,2.06525752798902,
7.50354272648692));
#393034=CARTESIAN_POINT('Ctrl Pts',(-1.81027260270384,2.06538389067401,
7.50357277531559));
#393035=CARTESIAN_POINT('Ctrl Pts',(-1.81006147115135,2.06550656502176,
7.50361331098761));
#393036=CARTESIAN_POINT('Ctrl Pts',(-1.8098553247013,2.06562356178361,7.50366116523658));
#393037=CARTESIAN_POINT('',(-1.73334108842417,2.03608107236531,7.57603338622103));
#393038=CARTESIAN_POINT('Origin',(-1.73906727032659,2.04281177295478,7.58486873427627));
#393039=CARTESIAN_POINT('Ctrl Pts',(-1.80985532475556,2.06562356179811,
7.50366116529969));
#393040=CARTESIAN_POINT('Ctrl Pts',(-1.78439189675398,2.0557929141486,7.52783573079709));
#393041=CARTESIAN_POINT('Ctrl Pts',(-1.75888834908382,2.04594589934544,
7.55196141284069));
#393042=CARTESIAN_POINT('Ctrl Pts',(-1.73334108967201,2.03608107246803,
7.57603338728831));
#393043=CARTESIAN_POINT('Ctrl Pts',(-1.73480751822067,2.02796794848296,
7.59639677331372));
#393044=CARTESIAN_POINT('Ctrl Pts',(-1.71825676553209,2.01836216837365,
7.59974925422225));
#393045=CARTESIAN_POINT('Ctrl Pts',(-1.72509791827961,2.03623385142679,
7.59639677331371));
#393046=CARTESIAN_POINT('Ctrl Pts',(-1.73179248798738,2.02549313601005,
7.58707626057423));
#393047=CARTESIAN_POINT('Ctrl Pts',(-1.72493641503091,2.02620846475782,
7.58811717123965));
#393048=CARTESIAN_POINT('Ctrl Pts',(-1.72313602699776,2.03286248869314,
7.58707626057423));
#393049=CARTESIAN_POINT('Ctrl Pts',(-1.73230984781104,2.03154771866077,
7.58015376756929));
#393050=CARTESIAN_POINT('Ctrl Pts',(-1.72941656890807,2.03147110842991,
7.5820876076604));
#393051=CARTESIAN_POINT('Ctrl Pts',(-1.72903043012316,2.03433952764207,
7.5801537675693));
#393052=CARTESIAN_POINT('Ctrl Pts',(-1.73334108788787,2.03608107173503,
7.57603338509286));
#393053=CARTESIAN_POINT('Ctrl Pts',(-1.73334108788787,2.03608107173503,
7.57603338509286));
#393054=CARTESIAN_POINT('Ctrl Pts',(-1.73334108788787,2.03608107173503,
7.57603338509286));
#393055=CARTESIAN_POINT('Origin',(-1.73907161540578,2.04280807393547,7.58486873427622));
#393056=CARTESIAN_POINT('Ctrl Pts',(-1.74404347607192,2.12737891132436,
7.51098857897448));
#393057=CARTESIAN_POINT('Ctrl Pts',(-1.7428344547023,2.1216170731368,7.50433767179956));
#393058=CARTESIAN_POINT('Ctrl Pts',(-1.75064586560078,2.11799907495306,
7.50214974420965));
#393059=CARTESIAN_POINT('Ctrl Pts',(-1.73757436099932,2.09654902262136,
7.53887321589166));
#393060=CARTESIAN_POINT('Ctrl Pts',(-1.73637982585133,2.09085622148072,
7.53220407452062));
#393061=CARTESIAN_POINT('Ctrl Pts',(-1.74414053150148,2.08719912321378,
7.53003438070911));
#393062=CARTESIAN_POINT('Ctrl Pts',(-1.73109282283944,2.06565992915942,
7.56669465659232));
#393063=CARTESIAN_POINT('Ctrl Pts',(-1.72990534717204,2.06000077141513,
7.56004085833301));
#393064=CARTESIAN_POINT('Ctrl Pts',(-1.73762184485837,2.05634122040666,
7.55785582193789));
#393065=CARTESIAN_POINT('Ctrl Pts',(-1.72459915472629,2.03471302792852,
7.59443891967696));
#393066=CARTESIAN_POINT('Ctrl Pts',(-1.72340995736706,2.02904566511007,
7.58783901202978));
#393067=CARTESIAN_POINT('Ctrl Pts',(-1.73109004667146,2.0254269075519,7.58560008491213));
#393068=CARTESIAN_POINT('',(-1.75029323173563,2.11632951079881,7.50366116523517));
#393069=CARTESIAN_POINT('Ctrl Pts',(-1.75029323173586,2.1163295107991,7.50366116523554));
#393070=CARTESIAN_POINT('Ctrl Pts',(-1.74981871703962,2.11692025043702,
7.50350835821027));
#393071=CARTESIAN_POINT('Ctrl Pts',(-1.7493633037674,2.11744784570105,7.50345484956));
#393072=CARTESIAN_POINT('Ctrl Pts',(-1.74891390668696,2.11792837480992,
7.50349758195598));
#393073=CARTESIAN_POINT('Ctrl Pts',(-1.74868333265654,2.11817492187974,
7.50351950684424));
#393074=CARTESIAN_POINT('Ctrl Pts',(-1.74843171059763,2.11843346810349,
7.50357029184312));
#393075=CARTESIAN_POINT('Ctrl Pts',(-1.74818222121562,2.11867611166749,
7.50365515313923));
#393076=CARTESIAN_POINT('Ctrl Pts',(-1.74779840551787,2.11904939572501,
7.50378570417639));
#393077=CARTESIAN_POINT('Ctrl Pts',(-1.74740861269543,2.11939624934591,
7.50400001621911));
#393078=CARTESIAN_POINT('Ctrl Pts',(-1.74704100235902,2.11968857580534,
7.50428903009634));
#393079=CARTESIAN_POINT('Ctrl Pts',(-1.7470002004399,2.11972102179331,7.50432110841318));
#393080=CARTESIAN_POINT('Ctrl Pts',(-1.74695966296946,2.11975282504803,
7.50435406373354));
#393081=CARTESIAN_POINT('Ctrl Pts',(-1.7469194216477,2.11978396847005,7.50438785222352));
#393082=CARTESIAN_POINT('Ctrl Pts',(-1.74667372903594,2.11997411403091,
7.50459414719561));
#393083=CARTESIAN_POINT('Ctrl Pts',(-1.74643484859306,2.12014228251918,
7.50483629897752));
#393084=CARTESIAN_POINT('Ctrl Pts',(-1.74621268932908,2.12028310756563,
7.5050991045531));
#393085=CARTESIAN_POINT('Ctrl Pts',(-1.74572258367895,2.12059378176262,
7.50567888004914));
#393086=CARTESIAN_POINT('Ctrl Pts',(-1.74529482357481,2.12078406050336,
7.50637912803144));
#393087=CARTESIAN_POINT('Ctrl Pts',(-1.74493416304264,2.12088448585053,
7.50710440483569));
#393088=CARTESIAN_POINT('Ctrl Pts',(-1.74484572192004,2.12090911213938,
7.50728225710685));
#393089=CARTESIAN_POINT('Ctrl Pts',(-1.74475959423715,2.12092896612878,
7.50746498566954));
#393090=CARTESIAN_POINT('Ctrl Pts',(-1.74467788407099,2.12094399030944,
7.50764697238949));
#393091=CARTESIAN_POINT('Ctrl Pts',(-1.74423863270495,2.12102475616989,
7.50862528291181));
#393092=CARTESIAN_POINT('Ctrl Pts',(-1.74388791488077,2.12097735070585,
7.50965856837421));
#393093=CARTESIAN_POINT('Ctrl Pts',(-1.74359952217745,2.12086267149125,
7.51067959873202));
#393094=CARTESIAN_POINT('Ctrl Pts',(-1.74344081930905,2.1207995633748,7.51124147302578));
#393095=CARTESIAN_POINT('Ctrl Pts',(-1.7433011122352,2.12071566358396,7.51180065547253));
#393096=CARTESIAN_POINT('Ctrl Pts',(-1.74317712839623,2.12061863513828,
7.51235175716501));
#393097=CARTESIAN_POINT('Ctrl Pts',(-1.7427487148433,2.12028336320691,7.51425603304536));
#393098=CARTESIAN_POINT('Ctrl Pts',(-1.74246069049901,2.11974658727157,
7.51626900505181));
#393099=CARTESIAN_POINT('Ctrl Pts',(-1.74230085887294,2.11906741666329,
7.51827788969245));
#393100=CARTESIAN_POINT('Ctrl Pts',(-1.7422922084833,2.11903065866652,7.51838661432546));
#393101=CARTESIAN_POINT('Ctrl Pts',(-1.74228393829289,2.11899347478669,
7.51849533314857));
#393102=CARTESIAN_POINT('Ctrl Pts',(-1.74227604793055,2.11895587165397,
7.51860402984325));
#393103=CARTESIAN_POINT('Ctrl Pts',(-1.733341088327,2.03608107361461,7.57603338728985));
#393104=CARTESIAN_POINT('Ctrl Pts',(-1.73900212579773,2.06287528806228,
7.55196141284922));
#393105=CARTESIAN_POINT('Ctrl Pts',(-1.74465255590613,2.0896235082857,7.52783573083105));
#393106=CARTESIAN_POINT('Ctrl Pts',(-1.75029323174249,2.11632951085759,
7.50366116530176));
#393107=CARTESIAN_POINT('Origin',(-5.98949470795634E-16,7.03560129586916E-16,
7.49482233047033));
#393108=CARTESIAN_POINT('Origin',(-1.80403047455413,2.05897554547887,7.49482233047033));
#393109=CARTESIAN_POINT('Origin',(0.,0.,7.50366116523517));
#393110=CARTESIAN_POINT('Origin',(-1.74466007661672,2.10951830213908,7.49482233047033));
#393111=CARTESIAN_POINT('Ctrl Pts',(-1.81372657476299,2.05812793120741,
7.51860402984325));
#393112=CARTESIAN_POINT('Ctrl Pts',(-1.82082828860746,2.06085958757332,
7.51860402984325));
#393113=CARTESIAN_POINT('Ctrl Pts',(-1.82651648716081,2.05580580846776,
7.51860402984325));
#393114=CARTESIAN_POINT('Ctrl Pts',(-1.81636349003426,2.05914221267185,
7.51041458714367));
#393115=CARTESIAN_POINT('Ctrl Pts',(-1.82217588142127,2.0596622820176,7.51004642900443));
#393116=CARTESIAN_POINT('Ctrl Pts',(-1.82651805589842,2.05580441469549,
7.5072913648301));
#393117=CARTESIAN_POINT('Ctrl Pts',(-1.81632127355297,2.06195680944013,
7.50215815450137));
#393118=CARTESIAN_POINT('Ctrl Pts',(-1.81943214123462,2.06210022055774,
7.49877163671531));
#393119=CARTESIAN_POINT('Ctrl Pts',(-1.82202718038202,2.05982652413607,
7.4948158853317));
#393120=CARTESIAN_POINT('Ctrl Pts',(-1.80985496190502,2.06562314771778,
7.50366171572174));
#393121=CARTESIAN_POINT('Ctrl Pts',(-1.81226805662943,2.06837726029866,
7.50000045605858));
#393122=CARTESIAN_POINT('Ctrl Pts',(-1.81226805662953,2.06837726029858,
7.49482233047317));
#393123=CARTESIAN_POINT('Origin',(-1.81821413949189,2.04646123661108,7.51860402984325));
#393124=CARTESIAN_POINT('Origin',(-1.81821413949189,2.04646123661108,9.));
#393125=CARTESIAN_POINT('Origin',(-1.81821413949189,2.04646123661108,8.75721825406948));
#393126=CARTESIAN_POINT('Ctrl Pts',(-1.79814021121715,2.05213415732288,
8.78942910404912));
#393127=CARTESIAN_POINT('Ctrl Pts',(-1.80333407793182,2.05415311181765,
8.7967269950169));
#393128=CARTESIAN_POINT('Ctrl Pts',(-1.80804083871739,2.04656892505245,
8.79893251111267));
#393129=CARTESIAN_POINT('Ctrl Pts',(-1.80840194814796,2.05608031670937,
8.78111911759582));
#393130=CARTESIAN_POINT('Ctrl Pts',(-1.8145620342885,2.05846687256809,8.78644465894816));
#393131=CARTESIAN_POINT('Ctrl Pts',(-1.82021442763375,2.05265602398583,
8.78817647674131));
#393132=CARTESIAN_POINT('Ctrl Pts',(-1.81479730738017,2.05853965733411,
8.7678092393203));
#393133=CARTESIAN_POINT('Ctrl Pts',(-1.8220708698622,2.06135213410563,8.76988516158372));
#393134=CARTESIAN_POINT('Ctrl Pts',(-1.82782283886924,2.05644792846779,
8.77093053738833));
#393135=CARTESIAN_POINT('Ctrl Pts',(-1.81355029985716,2.05806011956911,
8.75371302330492));
#393136=CARTESIAN_POINT('Ctrl Pts',(-1.82064507138233,2.06080428034674,
8.75300828287559));
#393137=CARTESIAN_POINT('Ctrl Pts',(-1.82633909376226,2.05570794357694,
8.75267964240737));
#393138=CARTESIAN_POINT('Origin',(-1.80512593983748,2.04142816484592,8.78727029226991));
#393139=CARTESIAN_POINT('Ctrl Pts',(-1.7339107418093,2.0274347247136,8.85049129520029));
#393140=CARTESIAN_POINT('Ctrl Pts',(-1.73936124027703,2.02953071581004,
8.85711686593484));
#393141=CARTESIAN_POINT('Ctrl Pts',(-1.74416981443406,2.02246117716241,
8.85933012996512));
#393142=CARTESIAN_POINT('Ctrl Pts',(-1.75618597738197,2.03600067436165,
8.82945683644724));
#393143=CARTESIAN_POINT('Ctrl Pts',(-1.76168171828244,2.03811406345141,
8.83607469902391));
#393144=CARTESIAN_POINT('Ctrl Pts',(-1.76647340116633,2.03100267697357,
8.8382956714852));
#393145=CARTESIAN_POINT('Ctrl Pts',(-1.77842800991975,2.04455385577099,
8.80838214965002));
#393146=CARTESIAN_POINT('Ctrl Pts',(-1.78394543957973,2.04667558528088,
8.81501364461994));
#393147=CARTESIAN_POINT('Ctrl Pts',(-1.7887429154195,2.03953184409285,8.8172209842872));
#393148=CARTESIAN_POINT('Ctrl Pts',(-1.8006393623326,2.05309523912753,8.78727029226991));
#393149=CARTESIAN_POINT('Ctrl Pts',(-1.80615770845575,2.05521732106364,
8.79393457792714));
#393150=CARTESIAN_POINT('Ctrl Pts',(-1.81098095093021,2.04804963334648,
8.79610912703474));
#393151=CARTESIAN_POINT('Origin',(-1.73839731931418,2.01576765043199,8.85049129520029));
#393152=CARTESIAN_POINT('Ctrl Pts',(-1.72471465490915,2.03526346763209,
8.85049129520029));
#393153=CARTESIAN_POINT('Ctrl Pts',(-1.72591388015442,2.04097862038895,
8.85711686593484));
#393154=CARTESIAN_POINT('Ctrl Pts',(-1.71816751245362,2.04459725957487,
8.85933012996512));
#393155=CARTESIAN_POINT('Ctrl Pts',(-1.72365371764566,2.0302073544872,8.86332496987232));
#393156=CARTESIAN_POINT('Ctrl Pts',(-1.72032477139737,2.03341204031466,
8.86648636486737));
#393157=CARTESIAN_POINT('Ctrl Pts',(-1.71521626468801,2.03044905852376,
8.87206031107457));
#393158=CARTESIAN_POINT('Ctrl Pts',(-1.72905599763765,2.02556783114056,
8.86341338519876));
#393159=CARTESIAN_POINT('Ctrl Pts',(-1.73274355452398,2.02276151775032,
8.86654584966059));
#393160=CARTESIAN_POINT('Ctrl Pts',(-1.73057098474443,2.01724752705932,
8.87215952290714));
#393161=CARTESIAN_POINT('Ctrl Pts',(-1.7339107418093,2.0274347247136,8.85049129520029));
#393162=CARTESIAN_POINT('Ctrl Pts',(-1.73936124027703,2.02953071581004,
8.85711686593484));
#393163=CARTESIAN_POINT('Ctrl Pts',(-1.74416981443406,2.02246117716241,
8.85933012996512));
#393164=CARTESIAN_POINT('Origin',(-1.71248107441376,2.0378304713841,8.85049129520029));
#393165=CARTESIAN_POINT('Ctrl Pts',(-1.73939636646039,2.10523216165203,
8.78727029226991));
#393166=CARTESIAN_POINT('Ctrl Pts',(-1.74061051962861,2.11101845647363,
8.79393457792714));
#393167=CARTESIAN_POINT('Ctrl Pts',(-1.73276491989239,2.11463591137413,
8.79610912703474));
#393168=CARTESIAN_POINT('Ctrl Pts',(-1.73450939791929,2.08194231527793,
8.80838214965004));
#393169=CARTESIAN_POINT('Ctrl Pts',(-1.73572334944619,2.08772764913661,
8.81501364461994));
#393170=CARTESIAN_POINT('Ctrl Pts',(-1.72790550163946,2.09132348954825,
8.81722098428721));
#393171=CARTESIAN_POINT('Ctrl Pts',(-1.7296156791001,2.05862029907538,8.82945683644722));
#393172=CARTESIAN_POINT('Ctrl Pts',(-1.73082485863997,2.06438289105556,
8.83607469902388));
#393173=CARTESIAN_POINT('Ctrl Pts',(-1.72303987536891,2.06797817657505,
8.83829567148519));
#393174=CARTESIAN_POINT('Ctrl Pts',(-1.72471465490915,2.03526346763209,
8.85049129520029));
#393175=CARTESIAN_POINT('Ctrl Pts',(-1.72591388015442,2.04097862038895,
8.85711686593484));
#393176=CARTESIAN_POINT('Ctrl Pts',(-1.71816751245362,2.04459725957487,
8.85933012996512));
#393177=CARTESIAN_POINT('Origin',(-1.727162785965,2.10779916540404,8.78727029226991));
#393178=CARTESIAN_POINT('Ctrl Pts',(-1.74223800513144,2.11877466075529,
8.75374538247848));
#393179=CARTESIAN_POINT('Ctrl Pts',(-1.74381137292056,2.1262089658464,8.75304829418602));
#393180=CARTESIAN_POINT('Ctrl Pts',(-1.73788145903658,2.13101591545478,
8.75272238421917));
#393181=CARTESIAN_POINT('Ctrl Pts',(-1.74250907779354,2.12006651079531,
8.76769408445018));
#393182=CARTESIAN_POINT('Ctrl Pts',(-1.74412136334459,2.12768803887528,
8.76974318093967));
#393183=CARTESIAN_POINT('Ctrl Pts',(-1.73837008844153,2.13258101284514,
8.7707786988043));
#393184=CARTESIAN_POINT('Ctrl Pts',(-1.741119713762,2.11344522340548,8.78108014887992));
#393185=CARTESIAN_POINT('Ctrl Pts',(-1.74248978482014,2.11990340756173,
8.78639403366326));
#393186=CARTESIAN_POINT('Ctrl Pts',(-1.7358724574555,2.12456527996219,8.78812224174741));
#393187=CARTESIAN_POINT('Ctrl Pts',(-1.73884285278514,2.10259439504487,
8.78944554828685));
#393188=CARTESIAN_POINT('Ctrl Pts',(-1.74000297373832,2.10803595153093,
8.79673892988686));
#393189=CARTESIAN_POINT('Ctrl Pts',(-1.73177459439526,2.11147067534852,
8.79894799272499));
#393190=CARTESIAN_POINT('Origin',(-1.73004246743517,2.12152287540598,8.75721825406948));
#393191=CARTESIAN_POINT('Origin',(-1.73004246743517,2.12152287540598,9.));
#393192=CARTESIAN_POINT('Origin',(-1.73004246743517,2.12152287540598,7.51860402984325));
#393193=CARTESIAN_POINT('Ctrl Pts',(-1.75029273038002,2.11632890459552,
7.50366195182966));
#393194=CARTESIAN_POINT('Ctrl Pts',(-1.75262656098472,2.11915080580191,
7.50000065167735));
#393195=CARTESIAN_POINT('Ctrl Pts',(-1.75262656098463,2.11915080580198,
7.49482233047108));
#393196=CARTESIAN_POINT('Ctrl Pts',(-1.74563652264444,2.12213179431787,
7.50215800491336));
#393197=CARTESIAN_POINT('Ctrl Pts',(-1.74528013450682,2.12522657777876,
7.49877273257264));
#393198=CARTESIAN_POINT('Ctrl Pts',(-1.7426199422462,2.12742669902233,7.49481816995649));
#393199=CARTESIAN_POINT('Ctrl Pts',(-1.74285520534901,2.1217143132473,7.51043025814042));
#393200=CARTESIAN_POINT('Ctrl Pts',(-1.74244442792582,2.12753874617212,
7.51006209594515));
#393201=CARTESIAN_POINT('Ctrl Pts',(-1.73794024257004,2.13121179455774,
7.50731281821698));
#393202=CARTESIAN_POINT('Ctrl Pts',(-1.74227573745804,2.11895439247877,
7.51860402984325));
#393203=CARTESIAN_POINT('Ctrl Pts',(-1.74383928023545,2.12640129461146,
7.51860402984325));
#393204=CARTESIAN_POINT('Ctrl Pts',(-1.73794220472939,2.13121019447176,
7.51860402984325));
#393205=CARTESIAN_POINT('Origin',(0.,0.,7.5));
#393206=CARTESIAN_POINT('Origin',(-1.85157082176547,1.92057895321253,7.5));
#393207=CARTESIAN_POINT('',(-1.85157082176547,1.92057895321253,7.59394543036555));
#393208=CARTESIAN_POINT('',(-1.85157082176547,1.92057895321253,8.85049129520029));
#393209=CARTESIAN_POINT('',(-1.85157082176547,1.92057895321253,7.5));
#393210=CARTESIAN_POINT('',(-1.87070527778333,1.98946322855771,8.78727029226991));
#393211=CARTESIAN_POINT('Ctrl Pts',(-1.85157082176547,1.92057895321253,
8.85049129520029));
#393212=CARTESIAN_POINT('Ctrl Pts',(-1.85795824503306,1.94357375498269,
8.82945686509571));
#393213=CARTESIAN_POINT('Ctrl Pts',(-1.8643361726236,1.96653437219952,8.80838212259895));
#393214=CARTESIAN_POINT('Ctrl Pts',(-1.87070527778333,1.98946322855771,
8.78727029226991));
#393215=CARTESIAN_POINT('',(-1.87445832375786,2.00297423990032,8.75721825406948));
#393216=CARTESIAN_POINT('Origin',(-1.86316430092012,1.96231486575702,8.75937679713127));
#393217=CARTESIAN_POINT('',(-1.87445832375786,2.00297423990032,7.51860402984325));
#393218=CARTESIAN_POINT('',(-1.87445832375786,2.00297423990032,7.5));
#393219=CARTESIAN_POINT('Ctrl Pts',(-1.87445832375786,2.00297423990032,
7.51860402984325));
#393220=CARTESIAN_POINT('Ctrl Pts',(-1.87151088985393,1.99236344185043,
7.52834476460825));
#393221=CARTESIAN_POINT('Ctrl Pts',(-1.86856154251845,1.98174575542357,
7.53807742314407));
#393222=CARTESIAN_POINT('Ctrl Pts',(-1.86561021750539,1.9711209493333,7.54780169004674));
#393223=CARTESIAN_POINT('Ctrl Pts',(-1.86093547819022,1.95429183070809,
7.5632044032688));
#393224=CARTESIAN_POINT('Ctrl Pts',(-1.85625577119299,1.93744482836685,
7.57858609112103));
#393225=CARTESIAN_POINT('Ctrl Pts',(-1.85157082176547,1.92057895321253,
7.59394543036555));
#393226=CARTESIAN_POINT('Origin',(-2.12271872378387,1.99423374133349,7.5));
#393227=CARTESIAN_POINT('',(-1.94186579781666,1.93769374166281,8.75721825406948));
#393228=CARTESIAN_POINT('',(-1.92848201925698,1.93350957471439,8.78727029226991));
#393229=CARTESIAN_POINT('Origin',(-1.89450899737115,1.92288859838258,8.75658640621016));
#393230=CARTESIAN_POINT('',(-1.86024642503785,1.91217709997534,8.85049129520029));
#393231=CARTESIAN_POINT('Ctrl Pts',(-1.92848201925698,1.93350957471439,
8.78727029226991));
#393232=CARTESIAN_POINT('Ctrl Pts',(-1.90576908324182,1.92640883587951,
8.80838212259896));
#393233=CARTESIAN_POINT('Ctrl Pts',(-1.88302468545904,1.91929826116101,
8.82945686509571));
#393234=CARTESIAN_POINT('Ctrl Pts',(-1.86024642503785,1.91217709997534,
8.85049129520029));
#393235=CARTESIAN_POINT('',(-1.86024642503785,1.91217709997534,7.59394543036555));
#393236=CARTESIAN_POINT('',(-1.86024642503785,1.91217709997534,7.5));
#393237=CARTESIAN_POINT('',(-1.94186579781666,1.93769374166281,7.51860402984325));
#393238=CARTESIAN_POINT('Ctrl Pts',(-1.86024642503785,1.91217709997534,
7.59394543036555));
#393239=CARTESIAN_POINT('Ctrl Pts',(-1.87695347475876,1.91740022025756,
7.57858609112103));
#393240=CARTESIAN_POINT('Ctrl Pts',(-1.89364182939109,1.92261749589948,
7.56320440326857));
#393241=CARTESIAN_POINT('Ctrl Pts',(-1.910312468718,1.92782923321041,7.54780169004651));
#393242=CARTESIAN_POINT('Ctrl Pts',(-1.92083722133244,1.93111958367707,
7.53807742314383));
#393243=CARTESIAN_POINT('Ctrl Pts',(-1.93135492132932,1.93440772928588,
7.52834476460825));
#393244=CARTESIAN_POINT('Ctrl Pts',(-1.94186579781666,1.93769374166281,
7.51860402984325));
#393245=CARTESIAN_POINT('',(-1.94186579781666,1.93769374166281,7.5));
#393246=CARTESIAN_POINT('Origin',(-1.85819500900389,1.91873890744399,7.5));
#393247=CARTESIAN_POINT('Ctrl Pts',(-1.86024642503785,1.91217709997534,
8.85049129520029));
#393248=CARTESIAN_POINT('Ctrl Pts',(-1.86006158583553,1.91211931374721,
8.85097269580138));
#393249=CARTESIAN_POINT('Ctrl Pts',(-1.85987656885909,1.91207028482754,
8.85143669361005));
#393250=CARTESIAN_POINT('Ctrl Pts',(-1.85968263072173,1.91202860070861,
8.8519052845931));
#393251=CARTESIAN_POINT('Ctrl Pts',(-1.85930330002417,1.91194706921551,
8.85282181883899));
#393252=CARTESIAN_POINT('Ctrl Pts',(-1.85889955648229,1.91189592644375,
8.85372622499635));
#393253=CARTESIAN_POINT('Ctrl Pts',(-1.85846312703677,1.91188966638125,
8.85462257735071));
#393254=CARTESIAN_POINT('Ctrl Pts',(-1.85810081881159,1.91188446949971,
8.85536669723986));
#393255=CARTESIAN_POINT('Ctrl Pts',(-1.85771590218177,1.91191017178599,
8.85610498449051));
#393256=CARTESIAN_POINT('Ctrl Pts',(-1.85730414434203,1.91198305270082,
8.85681338218371));
#393257=CARTESIAN_POINT('Ctrl Pts',(-1.85693047345579,1.91204919224548,
8.85745625420284));
#393258=CARTESIAN_POINT('Ctrl Pts',(-1.85652990561897,1.91215442650103,
8.85808743050665));
#393259=CARTESIAN_POINT('Ctrl Pts',(-1.85609705491234,1.91232684172785,
8.8586680450841));
#393260=CARTESIAN_POINT('Ctrl Pts',(-1.85589734697935,1.912406390376,8.85893592806395));
#393261=CARTESIAN_POINT('Ctrl Pts',(-1.8556907500765,1.91250048161008,8.85919241173848));
#393262=CARTESIAN_POINT('Ctrl Pts',(-1.85547684726747,1.91261346607839,
8.85943017985534));
#393263=CARTESIAN_POINT('Ctrl Pts',(-1.85518801515327,1.9127660285576,8.8597512372));
#393264=CARTESIAN_POINT('Ctrl Pts',(-1.85487880982734,1.91295748856583,
8.86004599534706));
#393265=CARTESIAN_POINT('Ctrl Pts',(-1.85455842928456,1.9131944007688,8.86026130871721));
#393266=CARTESIAN_POINT('Ctrl Pts',(-1.85444112893537,1.91328114100557,
8.86034014101235));
#393267=CARTESIAN_POINT('Ctrl Pts',(-1.85432056124279,1.91337526712552,
8.86040910639693));
#393268=CARTESIAN_POINT('Ctrl Pts',(-1.85420021800343,1.91347447986183,
8.86046313645507));
#393269=CARTESIAN_POINT('Ctrl Pts',(-1.85401242338628,1.91362930050595,
8.8605474499083));
#393270=CARTESIAN_POINT('Ctrl Pts',(-1.85382014264964,1.91380084733627,
8.86059655985668));
#393271=CARTESIAN_POINT('Ctrl Pts',(-1.85363551231202,1.91397789992959,
8.86059725258816));
#393272=CARTESIAN_POINT('Ctrl Pts',(-1.85345045540457,1.91415536158513,
8.86059794692011));
#393273=CARTESIAN_POINT('Ctrl Pts',(-1.85327287084368,1.91434224010243,
8.86056369958366));
#393274=CARTESIAN_POINT('Ctrl Pts',(-1.8531097162974,1.91452575082093,8.86048590497774));
#393275=CARTESIAN_POINT('Ctrl Pts',(-1.85306713781852,1.91457364165468,
8.86046560290182));
#393276=CARTESIAN_POINT('Ctrl Pts',(-1.85302505587401,1.91462198633974,
8.86044257503091));
#393277=CARTESIAN_POINT('Ctrl Pts',(-1.85298474607093,1.91466926943291,
8.86041778462583));
#393278=CARTESIAN_POINT('Ctrl Pts',(-1.85271351111645,1.91498742597652,
8.86025097596201));
#393279=CARTESIAN_POINT('Ctrl Pts',(-1.85248636841558,1.91530042537853,
8.8599848982295));
#393280=CARTESIAN_POINT('Ctrl Pts',(-1.85230309052327,1.91559415580072,
8.85968173251461));
#393281=CARTESIAN_POINT('Ctrl Pts',(-1.85220614701881,1.91574952236531,
8.85952137522076));
#393282=CARTESIAN_POINT('Ctrl Pts',(-1.85211944536218,1.9159023915624,8.85934740853961));
#393283=CARTESIAN_POINT('Ctrl Pts',(-1.85204285603104,1.91604984067723,
8.8591675900182));
#393284=CARTESIAN_POINT('Ctrl Pts',(-1.85173531005615,1.91664192551583,
8.85844552518695));
#393285=CARTESIAN_POINT('Ctrl Pts',(-1.85157075220591,1.9171786832524,8.85759444184124));
#393286=CARTESIAN_POINT('Ctrl Pts',(-1.85147589005125,1.91762837806794,
8.85683498915138));
#393287=CARTESIAN_POINT('Ctrl Pts',(-1.8514659629794,1.91767543743275,8.85675551444998));
#393288=CARTESIAN_POINT('Ctrl Pts',(-1.85145681911712,1.91772154358246,
8.85667699793651));
#393289=CARTESIAN_POINT('Ctrl Pts',(-1.85144838759449,1.91776665961246,
8.85659965593547));
#393290=CARTESIAN_POINT('Ctrl Pts',(-1.85133457847174,1.91837563808757,
8.85555568965886));
#393291=CARTESIAN_POINT('Ctrl Pts',(-1.85131314939547,1.91897734042081,
8.85434650606346));
#393292=CARTESIAN_POINT('Ctrl Pts',(-1.85137778363235,1.91957451989693,
8.85297329937118));
#393293=CARTESIAN_POINT('Ctrl Pts',(-1.85141413645237,1.91991039696557,
8.85220095427747));
#393294=CARTESIAN_POINT('Ctrl Pts',(-1.85147804246509,1.9202449465981,8.85137579139184));
#393295=CARTESIAN_POINT('Ctrl Pts',(-1.85157082176547,1.92057895321253,
8.85049129520029));
#393296=CARTESIAN_POINT('Origin',(-1.85819500900389,1.91873890744399,7.59394543036555));
#393297=CARTESIAN_POINT('Ctrl Pts',(-1.85970977447861,1.91200932706108,
7.59443877723642));
#393298=CARTESIAN_POINT('Ctrl Pts',(-1.85418279006981,1.91028142747094,
7.58783886950016));
#393299=CARTESIAN_POINT('Ctrl Pts',(-1.84984328894464,1.917578544129,7.58559994247159));
#393300=CARTESIAN_POINT('Ctrl Pts',(-1.88988142021143,1.92144188022921,
7.56670252222137));
#393301=CARTESIAN_POINT('Ctrl Pts',(-1.88436242386422,1.91971647794457,
7.56004874999028));
#393302=CARTESIAN_POINT('Ctrl Pts',(-1.87997884594832,1.92704591188663,
7.55786368756704));
#393303=CARTESIAN_POINT('Ctrl Pts',(-1.91999672341034,1.93085681904672,
7.5388891333356));
#393304=CARTESIAN_POINT('Ctrl Pts',(-1.91444492739764,1.9291211626118,7.53222002137279));
#393305=CARTESIAN_POINT('Ctrl Pts',(-1.91005954507819,1.93649482293976,
7.53005029815327));
#393306=CARTESIAN_POINT('Ctrl Pts',(-1.9500543213375,1.94025371748126,7.51101258149734));
#393307=CARTESIAN_POINT('Ctrl Pts',(-1.94443522746927,1.93849702173658,
7.5043616886572));
#393308=CARTESIAN_POINT('Ctrl Pts',(-1.94008387535392,1.94592488928473,
7.50217374673251));
#393309=CARTESIAN_POINT('',(-1.93848173883014,1.94542168785061,7.50366116523517));
#393310=CARTESIAN_POINT('Ctrl Pts',(-1.94186579781667,1.93769374166281,
7.51860402984325));
#393311=CARTESIAN_POINT('Ctrl Pts',(-1.94228729131093,1.93782551305605,
7.51734760759494));
#393312=CARTESIAN_POINT('Ctrl Pts',(-1.94265041783263,1.93800137376575,
7.51608817408572));
#393313=CARTESIAN_POINT('Ctrl Pts',(-1.94294852171251,1.93823293770865,
7.51481005913119));
#393314=CARTESIAN_POINT('Ctrl Pts',(-1.94321855133033,1.93844269386153,
7.51365231206383));
#393315=CARTESIAN_POINT('Ctrl Pts',(-1.94343576286585,1.93869825356335,
7.51247773061042));
#393316=CARTESIAN_POINT('Ctrl Pts',(-1.94356826237053,1.93901910824857,
7.51129758471022));
#393317=CARTESIAN_POINT('Ctrl Pts',(-1.94373294412284,1.93941789397932,
7.50983079813402));
#393318=CARTESIAN_POINT('Ctrl Pts',(-1.94374947141057,1.93990978941468,
7.50839324291155));
#393319=CARTESIAN_POINT('Ctrl Pts',(-1.94353557175021,1.94050115292896,
7.50715379678855));
#393320=CARTESIAN_POINT('Ctrl Pts',(-1.94343675627049,1.94077434583283,
7.50658120839351));
#393321=CARTESIAN_POINT('Ctrl Pts',(-1.94326578097649,1.94110437188971,
7.50598221009429));
#393322=CARTESIAN_POINT('Ctrl Pts',(-1.94300651780457,1.94147291354817,
7.50545747549611));
#393323=CARTESIAN_POINT('Ctrl Pts',(-1.94286816695108,1.94166957878456,
7.50517746087247));
#393324=CARTESIAN_POINT('Ctrl Pts',(-1.9427033404709,1.941879460867,7.50491486231392));
#393325=CARTESIAN_POINT('Ctrl Pts',(-1.94251509140962,1.94209597154048,
7.50468370960992));
#393326=CARTESIAN_POINT('Ctrl Pts',(-1.94223359968321,1.94241972329174,
7.50433806340447));
#393327=CARTESIAN_POINT('Ctrl Pts',(-1.94189087484742,1.94276763919197,
7.50405484070984));
#393328=CARTESIAN_POINT('Ctrl Pts',(-1.94150948842178,1.94311578500611,
7.50385766036131));
#393329=CARTESIAN_POINT('Ctrl Pts',(-1.94146870507165,1.94315301378952,
7.50383657498791));
#393330=CARTESIAN_POINT('Ctrl Pts',(-1.94142750738742,1.94319023939014,
7.50381643264937));
#393331=CARTESIAN_POINT('Ctrl Pts',(-1.94138594320286,1.94322742863344,
7.50379723213559));
#393332=CARTESIAN_POINT('Ctrl Pts',(-1.94110848867433,1.94347567899794,
7.50366906242519));
#393333=CARTESIAN_POINT('Ctrl Pts',(-1.94080818815367,1.94372717343729,
7.50358235568538));
#393334=CARTESIAN_POINT('Ctrl Pts',(-1.94051290838087,1.94396262527655,
7.5035341175365));
#393335=CARTESIAN_POINT('Ctrl Pts',(-1.94007016978078,1.94431565866153,
7.50346178989176));
#393336=CARTESIAN_POINT('Ctrl Pts',(-1.93957887322524,1.94467661751402,
7.50346967198527));
#393337=CARTESIAN_POINT('Ctrl Pts',(-1.93908566887042,1.945016126858,7.50354272648692));
#393338=CARTESIAN_POINT('Ctrl Pts',(-1.93888280371056,1.9451557740786,7.50357277531559));
#393339=CARTESIAN_POINT('Ctrl Pts',(-1.93867996572294,1.94529172362375,
7.50361331098761));
#393340=CARTESIAN_POINT('Ctrl Pts',(-1.93848173883115,1.94542168785162,
7.50366116523658));
#393341=CARTESIAN_POINT('',(-1.86023191546276,1.92084218059618,7.57603338622103));
#393342=CARTESIAN_POINT('Origin',(-1.86637756977754,1.92719217450495,7.58486873427628));
#393343=CARTESIAN_POINT('Ctrl Pts',(-1.93848173888622,1.94542168786261,
7.50366116529968));
#393344=CARTESIAN_POINT('Ctrl Pts',(-1.91244077647095,1.93724268576656,
7.52783573079709));
#393345=CARTESIAN_POINT('Ctrl Pts',(-1.88635872817013,1.92904992062092,
7.55196141284068));
#393346=CARTESIAN_POINT('Ctrl Pts',(-1.86023191671462,1.92084218061874,
7.57603338728831));
#393347=CARTESIAN_POINT('Ctrl Pts',(-1.86117552269009,1.91265177151732,
7.59639677331371));
#393348=CARTESIAN_POINT('Ctrl Pts',(-1.84404333085321,1.90412613787907,
7.59974925422226));
#393349=CARTESIAN_POINT('Ctrl Pts',(-1.85201547038344,1.92152278748121,
7.59639677331371));
#393350=CARTESIAN_POINT('Ctrl Pts',(-1.85800812538022,1.91037521746236,
7.58707626057423));
#393351=CARTESIAN_POINT('Ctrl Pts',(-1.85121197023118,1.91152834659303,
7.58811717123965));
#393352=CARTESIAN_POINT('Ctrl Pts',(-1.84984160606564,1.91828405037989,
7.58707626057423));
#393353=CARTESIAN_POINT('Ctrl Pts',(-1.85891234067498,1.91638421296596,
7.58015376756929));
#393354=CARTESIAN_POINT('Ctrl Pts',(-1.85602009788945,1.91649313315483,
7.5820876076604));
#393355=CARTESIAN_POINT('Ctrl Pts',(-1.85581853271804,1.91938039888895,
7.58015376756929));
#393356=CARTESIAN_POINT('Ctrl Pts',(-1.86023191488718,1.92084218000156,
7.57603338509286));
#393357=CARTESIAN_POINT('Ctrl Pts',(-1.86023191488718,1.92084218000156,
7.57603338509286));
#393358=CARTESIAN_POINT('Ctrl Pts',(-1.86023191488718,1.92084218000156,
7.57603338509286));
#393359=CARTESIAN_POINT('Origin',(-1.86638166893224,1.92718820469566,7.58486873427622));
#393360=CARTESIAN_POINT('Ctrl Pts',(-1.87676178653313,2.01126673402251,
7.51098857897448));
#393361=CARTESIAN_POINT('Ctrl Pts',(-1.87518608698741,2.00559419641458,
7.50433767179956));
#393362=CARTESIAN_POINT('Ctrl Pts',(-1.88274964256491,2.00148315298151,
7.50214974420965));
#393363=CARTESIAN_POINT('Ctrl Pts',(-1.86833068520009,1.98091466625814,
7.53887321589167));
#393364=CARTESIAN_POINT('Ctrl Pts',(-1.86677386533128,1.97531009571769,
7.5322040745206));
#393365=CARTESIAN_POINT('Ctrl Pts',(-1.87428431468887,1.97116328123316,
7.53003438070911));
#393366=CARTESIAN_POINT('Ctrl Pts',(-1.85988339304239,1.95050431132728,
7.56669465659234));
#393367=CARTESIAN_POINT('Ctrl Pts',(-1.85833577368953,1.94493286275673,
7.560040858333));
#393368=CARTESIAN_POINT('Ctrl Pts',(-1.86580194876562,1.94078643298405,
7.55785582193789));
#393369=CARTESIAN_POINT('Ctrl Pts',(-1.85142029209722,1.92003704456849,
7.59443891967696));
#393370=CARTESIAN_POINT('Ctrl Pts',(-1.84987042888903,1.91445751809118,
7.58783901202978));
#393371=CARTESIAN_POINT('Ctrl Pts',(-1.85730288403345,1.91035413064732,
7.58560008491213));
#393372=CARTESIAN_POINT('',(-1.88229076388122,1.99983961245519,7.50366116523517));
#393373=CARTESIAN_POINT('Ctrl Pts',(-1.88229076388148,1.99983961245546,
7.50366116523554));
#393374=CARTESIAN_POINT('Ctrl Pts',(-1.88185507294512,2.00045954061641,
7.50350835821027));
#393375=CARTESIAN_POINT('Ctrl Pts',(-1.88143439851294,2.00101523030793,
7.50345484955999));
#393376=CARTESIAN_POINT('Ctrl Pts',(-1.88101671237271,2.00152356508801,
7.50349758195598));
#393377=CARTESIAN_POINT('Ctrl Pts',(-1.88080240840636,2.00178437852928,
7.50351950684424));
#393378=CARTESIAN_POINT('Ctrl Pts',(-1.88056786844539,2.00205851502274,
7.50357029184312));
#393379=CARTESIAN_POINT('Ctrl Pts',(-1.8803344378926,2.00231664488911,7.50365515313923));
#393380=CARTESIAN_POINT('Ctrl Pts',(-1.87997532717705,2.00271375315069,
7.50378570417639));
#393381=CARTESIAN_POINT('Ctrl Pts',(-1.87960855821355,2.00308486823551,
7.50400001621911));
#393382=CARTESIAN_POINT('Ctrl Pts',(-1.87926043259256,2.00340014695399,
7.50428903009634));
#393383=CARTESIAN_POINT('Ctrl Pts',(-1.87922179332695,2.00343514046614,
7.50432110841317));
#393384=CARTESIAN_POINT('Ctrl Pts',(-1.87918337678662,2.0034694756223,7.50435406373354));
#393385=CARTESIAN_POINT('Ctrl Pts',(-1.87914521351087,2.00350313332716,
7.50438785222352));
#393386=CARTESIAN_POINT('Ctrl Pts',(-1.87891220836884,2.00370862979325,
7.50459414719561));
#393387=CARTESIAN_POINT('Ctrl Pts',(-1.87868459332349,2.00389175788386,
7.50483629897752));
#393388=CARTESIAN_POINT('Ctrl Pts',(-1.87847191320124,2.00404652738306,
7.5050991045531));
#393389=CARTESIAN_POINT('Ctrl Pts',(-1.87800271948988,2.00438796444341,
7.50567888004914));
#393390=CARTESIAN_POINT('Ctrl Pts',(-1.87758802946553,2.00460525892004,
7.50637912803144));
#393391=CARTESIAN_POINT('Ctrl Pts',(-1.87723454422319,2.0047285855322,7.50710440483569));
#393392=CARTESIAN_POINT('Ctrl Pts',(-1.8771478626241,2.00475882766588,7.50728225710685));
#393393=CARTESIAN_POINT('Ctrl Pts',(-1.87706318394925,2.00478415908272,
7.50746498566954));
#393394=CARTESIAN_POINT('Ctrl Pts',(-1.87698260426795,2.00480438758291,
7.50764697238949));
#393395=CARTESIAN_POINT('Ctrl Pts',(-1.87654943007739,2.00491313043288,
7.50862528291182));
#393396=CARTESIAN_POINT('Ctrl Pts',(-1.87619639556209,2.0048882929366,7.50965856837422));
#393397=CARTESIAN_POINT('Ctrl Pts',(-1.87590124787,2.00479232672669,7.51067959873202));
#393398=CARTESIAN_POINT('Ctrl Pts',(-1.87573882772276,2.00473951640032,
7.51124147302578));
#393399=CARTESIAN_POINT('Ctrl Pts',(-1.87559403221403,2.00466474005356,
7.51180065547253));
#393400=CARTESIAN_POINT('Ctrl Pts',(-1.87546408647929,2.00457585463506,
7.51235175716501));
#393401=CARTESIAN_POINT('Ctrl Pts',(-1.87501507220155,2.00426872010641,
7.51425603304536));
#393402=CARTESIAN_POINT('Ctrl Pts',(-1.87469324828192,2.00375150081789,
7.5162690050518));
#393403=CARTESIAN_POINT('Ctrl Pts',(-1.87449023043679,2.00308396608592,
7.51827788969243));
#393404=CARTESIAN_POINT('Ctrl Pts',(-1.87447924272736,2.00304783784476,
7.51838661432545));
#393405=CARTESIAN_POINT('Ctrl Pts',(-1.87446860714958,2.00301126023612,
7.51849533314856));
#393406=CARTESIAN_POINT('Ctrl Pts',(-1.87445832375785,2.00297423990032,
7.51860402984325));
#393407=CARTESIAN_POINT('Ctrl Pts',(-1.86023191544584,1.92084218184914,
7.57603338728985));
#393408=CARTESIAN_POINT('Ctrl Pts',(-1.86759803292181,1.94721864079349,
7.55196141284922));
#393409=CARTESIAN_POINT('Ctrl Pts',(-1.87495061796934,1.9735498796297,7.52783573083105));
#393410=CARTESIAN_POINT('Ctrl Pts',(-1.88229076389183,1.99983961251341,
7.50366116530176));
#393411=CARTESIAN_POINT('Origin',(-6.42796117143048E-16,6.63739765492884E-16,
7.49482233047033));
#393412=CARTESIAN_POINT('Origin',(-1.93224291659624,1.93916053003965,7.49482233047033));
#393413=CARTESIAN_POINT('Origin',(0.,0.,7.50366116523517));
#393414=CARTESIAN_POINT('Origin',(-1.87623278704649,1.99340331564181,7.49482233047033));
#393415=CARTESIAN_POINT('Ctrl Pts',(-1.94186478829449,1.93769342600929,
7.51860402984325));
#393416=CARTESIAN_POINT('Ctrl Pts',(-1.94912692873048,1.93996446152597,
7.51860402984325));
#393417=CARTESIAN_POINT('Ctrl Pts',(-1.95447964353081,1.93455662181898,
7.51860402984325));
#393418=CARTESIAN_POINT('Ctrl Pts',(-1.94456127097707,1.93853667578217,
7.51041458714366));
#393419=CARTESIAN_POINT('Ctrl Pts',(-1.95039504113998,1.93868327539491,
7.51004642900443));
#393420=CARTESIAN_POINT('Ctrl Pts',(-1.954481119746,1.934555130401,7.5072913648301));
#393421=CARTESIAN_POINT('Ctrl Pts',(-1.94469947306816,1.94134819447877,
7.50215815450137));
#393422=CARTESIAN_POINT('Ctrl Pts',(-1.94781313752039,1.94129199696616,
7.49877163671529));
#393423=CARTESIAN_POINT('Ctrl Pts',(-1.95025716865163,1.93885670736862,
7.4948158853317));
#393424=CARTESIAN_POINT('Ctrl Pts',(-1.93848135025098,1.94542129788097,
7.50366171572174));
#393425=CARTESIAN_POINT('Ctrl Pts',(-1.94106594361239,1.94801514433234,
7.50000045605858));
#393426=CARTESIAN_POINT('Ctrl Pts',(-1.94106594361248,1.94801514433226,
7.49482233047317));
#393427=CARTESIAN_POINT('Origin',(-1.94559564515113,1.9257631826289,7.51860402984325));
#393428=CARTESIAN_POINT('Origin',(-1.94559564515113,1.9257631826289,9.));
#393429=CARTESIAN_POINT('Origin',(-1.94559564515113,1.9257631826289,8.75721825406948));
#393430=CARTESIAN_POINT('Ctrl Pts',(-1.92592642619289,1.93271058871712,
8.78942910404913));
#393431=CARTESIAN_POINT('Ctrl Pts',(-1.93123897640996,1.93439262287038,
8.79672699501691));
#393432=CARTESIAN_POINT('Ctrl Pts',(-1.93545014613627,1.92652245543136,
8.79893251111267));
#393433=CARTESIAN_POINT('Ctrl Pts',(-1.93641991058457,1.93599116855338,
8.78111911759582));
#393434=CARTESIAN_POINT('Ctrl Pts',(-1.94272024732632,1.937978142903,8.78644465894813));
#393435=CARTESIAN_POINT('Ctrl Pts',(-1.9479887248763,1.93181708324733,8.78817647674132));
#393436=CARTESIAN_POINT('Ctrl Pts',(-1.94295970036018,1.93803570412618,
8.7678092393203));
#393437=CARTESIAN_POINT('Ctrl Pts',(-1.95039851453345,1.94037638361425,
8.76988516158374));
#393438=CARTESIAN_POINT('Ctrl Pts',(-1.95582445196923,1.93511372427327,
8.77093053738833));
#393439=CARTESIAN_POINT('Ctrl Pts',(-1.94168453085777,1.93763704766926,
8.75371302330492));
#393440=CARTESIAN_POINT('Ctrl Pts',(-1.94894054439861,1.93992100670194,
8.75300828287559));
#393441=CARTESIAN_POINT('Ctrl Pts',(-1.95429634438094,1.93447032363616,
8.75267964240738));
#393442=CARTESIAN_POINT('Origin',(-1.93221186659144,1.92157901568048,8.78727029226991));
#393443=CARTESIAN_POINT('Ctrl Pts',(-1.86024642503785,1.91217709997534,
8.85049129520029));
#393444=CARTESIAN_POINT('Ctrl Pts',(-1.86582001548254,1.91391956999744,
8.85711686593484));
#393445=CARTESIAN_POINT('Ctrl Pts',(-1.87016576301193,1.90655647007114,
8.85933012996512));
#393446=CARTESIAN_POINT('Ctrl Pts',(-1.88302471602832,1.91929827071788,
8.82945683644722));
#393447=CARTESIAN_POINT('Ctrl Pts',(-1.88864457064355,1.92105520429467,
8.8360746990239));
#393448=CARTESIAN_POINT('Ctrl Pts',(-1.89297078040507,1.91365142474657,
8.83829567148519));
#393449=CARTESIAN_POINT('Ctrl Pts',(-1.90576905413921,1.92640882678117,
8.80838214965003));
#393450=CARTESIAN_POINT('Ctrl Pts',(-1.91141108732462,1.92817269403818,
8.81501364461988));
#393451=CARTESIAN_POINT('Ctrl Pts',(-1.91574100516639,1.92073625510017,
8.81722098428721));
#393452=CARTESIAN_POINT('Ctrl Pts',(-1.92848201925698,1.93350957471439,
8.78727029226991));
#393453=CARTESIAN_POINT('Ctrl Pts',(-1.93412498960264,1.93527373495553,
8.79393457792714));
#393454=CARTESIAN_POINT('Ctrl Pts',(-1.93847908687936,1.92781174781516,
8.79610912703474));
#393455=CARTESIAN_POINT('Origin',(-1.86397627237231,1.90024654094143,8.85049129520029));
#393456=CARTESIAN_POINT('Ctrl Pts',(-1.85157082176547,1.92057895321253,
8.85049129520029));
#393457=CARTESIAN_POINT('Ctrl Pts',(-1.85313375416821,1.92620552894983,
8.85711686593484));
#393458=CARTESIAN_POINT('Ctrl Pts',(-1.84563514921932,1.93031304473609,
8.85933012996512));
#393459=CARTESIAN_POINT('Ctrl Pts',(-1.85018811802993,1.91560120287823,
8.86332496987232));
#393460=CARTESIAN_POINT('Ctrl Pts',(-1.84707133638466,1.91901259065339,
8.86648636486738));
#393461=CARTESIAN_POINT('Ctrl Pts',(-1.84178348675509,1.91638299977499,
8.87206031107456));
#393462=CARTESIAN_POINT('Ctrl Pts',(-1.85528204317686,1.9106250866624,8.86341338519876));
#393463=CARTESIAN_POINT('Ctrl Pts',(-1.85878222246584,1.90758827656308,
8.86654584966058));
#393464=CARTESIAN_POINT('Ctrl Pts',(-1.85626083386736,1.90222481198104,
8.87215952290715));
#393465=CARTESIAN_POINT('Ctrl Pts',(-1.86024642503785,1.91217709997534,
8.85049129520029));
#393466=CARTESIAN_POINT('Ctrl Pts',(-1.86582001548254,1.91391956999744,
8.85711686593484));
#393467=CARTESIAN_POINT('Ctrl Pts',(-1.87016576301193,1.90655647007114,
8.85933012996512));
#393468=CARTESIAN_POINT('Origin',(-1.83952684496834,1.92392449097351,8.85049129520029));
#393469=CARTESIAN_POINT('Ctrl Pts',(-1.87070527778333,1.98946322855771,
8.78727029226991));
#393470=CARTESIAN_POINT('Ctrl Pts',(-1.87228766552576,1.99515984375544,
8.79393457792714));
#393471=CARTESIAN_POINT('Ctrl Pts',(-1.86468995654687,1.99927253550785,
8.79610912703474));
#393472=CARTESIAN_POINT('Ctrl Pts',(-1.86433616446272,1.96653434282026,
8.80838214965001));
#393473=CARTESIAN_POINT('Ctrl Pts',(-1.86591828940899,1.97223001194868,
8.81501364461992));
#393474=CARTESIAN_POINT('Ctrl Pts',(-1.85834689049526,1.97631935554929,
8.81722098428721));
#393475=CARTESIAN_POINT('Ctrl Pts',(-1.85795825360522,1.94357378584257,
8.82945683644724));
#393476=CARTESIAN_POINT('Ctrl Pts',(-1.85953415929187,1.94924706556038,
8.8360746990239));
#393477=CARTESIAN_POINT('Ctrl Pts',(-1.85199552183799,1.95333374977089,
8.83829567148519));
#393478=CARTESIAN_POINT('Ctrl Pts',(-1.85157082176547,1.92057895321253,
8.85049129520029));
#393479=CARTESIAN_POINT('Ctrl Pts',(-1.85313375416821,1.92620552894983,
8.85711686593484));
#393480=CARTESIAN_POINT('Ctrl Pts',(-1.84563514921932,1.93031304473609,
8.85933012996512));
#393481=CARTESIAN_POINT('Origin',(-1.8586613009862,1.99280876631869,8.78727029226991));
#393482=CARTESIAN_POINT('Ctrl Pts',(-1.87440874889961,2.00279583872935,
8.75374538247848));
#393483=CARTESIAN_POINT('Ctrl Pts',(-1.87645520159846,2.01011406322297,
8.75304829418601));
#393484=CARTESIAN_POINT('Ctrl Pts',(-1.87084545367738,2.01529106732486,
8.75272238421917));
#393485=CARTESIAN_POINT('Ctrl Pts',(-1.8747620337301,2.00406766683986,8.76769408445021));
#393486=CARTESIAN_POINT('Ctrl Pts',(-1.87685931964825,2.01157023618307,
8.7697431809397));
#393487=CARTESIAN_POINT('Ctrl Pts',(-1.87143335527489,2.01682164246132,
8.7707786988043));
#393488=CARTESIAN_POINT('Ctrl Pts',(-1.87295129695634,1.99754900045418,
8.78108014887987));
#393489=CARTESIAN_POINT('Ctrl Pts',(-1.87473233033612,2.00390613482436,
8.78639403366323));
#393490=CARTESIAN_POINT('Ctrl Pts',(-1.8684272861705,2.00898240252795,8.78812224174741));
#393491=CARTESIAN_POINT('Ctrl Pts',(-1.86998389907453,1.98686634526788,
8.78944554828685));
#393492=CARTESIAN_POINT('Ctrl Pts',(-1.87149027815589,1.99222239228786,
8.79673892988686));
#393493=CARTESIAN_POINT('Ctrl Pts',(-1.86349886841123,1.99617725317158,
8.79894799272499));
#393494=CARTESIAN_POINT('Origin',(-1.86241434696072,2.0063197776613,8.75721825406948));
#393495=CARTESIAN_POINT('Origin',(-1.86241434696072,2.0063197776613,9.));
#393496=CARTESIAN_POINT('Origin',(-1.86241434696072,2.0063197776613,7.51860402984325));
#393497=CARTESIAN_POINT('Ctrl Pts',(-1.88229022471613,1.99983903961938,
7.50366195182966));
#393498=CARTESIAN_POINT('Ctrl Pts',(-1.88480006004661,2.00250561388684,
7.50000065167735));
#393499=CARTESIAN_POINT('Ctrl Pts',(-1.88480006004652,2.00250561388692,
7.49482233047108));
#393500=CARTESIAN_POINT('Ctrl Pts',(-1.87801537607974,2.00592833093633,
7.50215800491337));
#393501=CARTESIAN_POINT('Ctrl Pts',(-1.87785800363691,2.00903958969905,
7.49877273257265));
#393502=CARTESIAN_POINT('Ctrl Pts',(-1.87534423927865,2.0114056296609,7.49481816995647));
#393503=CARTESIAN_POINT('Ctrl Pts',(-1.87521302519497,2.00568990723636,
7.51043025814042));
#393504=CARTESIAN_POINT('Ctrl Pts',(-1.87517626445679,2.01152869183891,
7.51006209594515));
#393505=CARTESIAN_POINT('Ctrl Pts',(-1.87091666645098,2.01548277769927,
7.50731281821699));
#393506=CARTESIAN_POINT('Ctrl Pts',(-1.87445791915216,2.00297278365629,
7.51860402984325));
#393507=CARTESIAN_POINT('Ctrl Pts',(-1.87649537412106,2.01030420880017,
7.51860402984325));
#393508=CARTESIAN_POINT('Ctrl Pts',(-1.870918522061,2.01548105518487,7.51860402984325));
#393509=CARTESIAN_POINT('Origin',(0.,0.,7.5));
#393510=CARTESIAN_POINT('Origin',(-1.97081848695446,1.79800236791132,7.5));
#393511=CARTESIAN_POINT('',(-1.97081848695446,1.79800236791132,7.59394543036555));
#393512=CARTESIAN_POINT('',(-1.97081848695446,1.79800236791132,8.85049129520029));
#393513=CARTESIAN_POINT('',(-1.97081848695446,1.79800236791132,7.5));
#393514=CARTESIAN_POINT('',(-1.99432705985485,1.86551916431871,8.78727029226991));
#393515=CARTESIAN_POINT('Ctrl Pts',(-1.97081848695446,1.79800236791132,
8.85049129520029));
#393516=CARTESIAN_POINT('Ctrl Pts',(-1.97866606858372,1.8205406807812,8.82945686509571));
#393517=CARTESIAN_POINT('Ctrl Pts',(-1.98650198383397,1.84304548772369,
8.80838212259895));
#393518=CARTESIAN_POINT('Ctrl Pts',(-1.99432705985485,1.86551916431871,
8.78727029226991));
#393519=CARTESIAN_POINT('',(-1.99893804826279,1.87876195735828,8.75721825406948));
#393520=CARTESIAN_POINT('Origin',(-1.98506217516061,1.83890973278755,8.7593767971313));
#393521=CARTESIAN_POINT('',(-1.99893804826279,1.87876195735828,7.51860402984325));
#393522=CARTESIAN_POINT('',(-1.99893804826279,1.87876195735828,7.5));
#393523=CARTESIAN_POINT('Ctrl Pts',(-1.99893804826279,1.87876195735828,
7.51860402984325));
#393524=CARTESIAN_POINT('Ctrl Pts',(-1.9953168340127,1.8683618030696,7.52834476460825));
#393525=CARTESIAN_POINT('Ctrl Pts',(-1.99169326892258,1.85795489715083,
7.53807742314407));
#393526=CARTESIAN_POINT('Ctrl Pts',(-1.98806727405984,1.847541012907,7.54780169004674));
#393527=CARTESIAN_POINT('Ctrl Pts',(-1.98232389416555,1.8310459830872,7.5632044032688));
#393528=CARTESIAN_POINT('Ctrl Pts',(-1.97657441098222,1.81453342457586,
7.57858609112103));
#393529=CARTESIAN_POINT('Ctrl Pts',(-1.97081848695446,1.79800236791132,
7.59394543036555));
#393530=CARTESIAN_POINT('Origin',(-2.24612836500518,1.85413331864101,7.5));
#393531=CARTESIAN_POINT('',(-2.06202449055418,1.80929677321442,8.75721825406948));
#393532=CARTESIAN_POINT('',(-2.04840012990613,1.80597870472224,8.78727029226991));
#393533=CARTESIAN_POINT('Origin',(-2.01381642094786,1.79755620931114,8.75658640621029));
#393534=CARTESIAN_POINT('',(-1.9789379566843,1.78906192937258,8.85049129520029));
#393535=CARTESIAN_POINT('Ctrl Pts',(-2.04840012990613,1.80597870472224,
8.78727029226991));
#393536=CARTESIAN_POINT('Ctrl Pts',(-2.0252789141548,1.80034777792375,8.80838212259897));
#393537=CARTESIAN_POINT('Ctrl Pts',(-2.00212567109019,1.79470905121289,
8.82945686509571));
#393538=CARTESIAN_POINT('Ctrl Pts',(-1.9789379566843,1.78906192937258,8.85049129520029));
#393539=CARTESIAN_POINT('',(-1.9789379566843,1.78906192937258,7.59394543036555));
#393540=CARTESIAN_POINT('',(-1.9789379566843,1.78906192937258,7.5));
#393541=CARTESIAN_POINT('',(-2.06202449055418,1.80929677321442,7.51860402984325));
#393542=CARTESIAN_POINT('Ctrl Pts',(-1.9789379566843,1.78906192937258,7.59394543036555));
#393543=CARTESIAN_POINT('Ctrl Pts',(-1.99594532644521,1.79320389384316,
7.57858609112103));
#393544=CARTESIAN_POINT('Ctrl Pts',(-2.0129336650612,1.79734122348031,7.56320440326857));
#393545=CARTESIAN_POINT('Ctrl Pts',(-2.02990396992769,1.80147416118908,
7.54780169004651));
#393546=CARTESIAN_POINT('Ctrl Pts',(-2.04061791178732,1.80408342806257,
7.53807742314383));
#393547=CARTESIAN_POINT('Ctrl Pts',(-2.05132467425402,1.80669094647108,
7.52834476460825));
#393548=CARTESIAN_POINT('Ctrl Pts',(-2.06202449055418,1.80929677321442,
7.51860402984324));
#393549=CARTESIAN_POINT('',(-2.06202449055418,1.80929677321442,7.5));
#393550=CARTESIAN_POINT('Origin',(-1.97731117195259,1.7957416895806,7.5));
#393551=CARTESIAN_POINT('Ctrl Pts',(-1.9789379566843,1.78906192937258,8.85049129520029));
#393552=CARTESIAN_POINT('Ctrl Pts',(-1.97874979487761,1.78901610456081,
8.85097269580138));
#393553=CARTESIAN_POINT('Ctrl Pts',(-1.97856201674471,1.78897903045469,
8.85143669361005));
#393554=CARTESIAN_POINT('Ctrl Pts',(-1.97836580636339,1.78894985763938,
8.8519052845931));
#393555=CARTESIAN_POINT('Ctrl Pts',(-1.97798203130074,1.78889279746271,
8.85282181883899));
#393556=CARTESIAN_POINT('Ctrl Pts',(-1.97757584056463,1.7888676277068,8.85372622499636));
#393557=CARTESIAN_POINT('Ctrl Pts',(-1.97713990672662,1.78888934263686,
8.85462257735071));
#393558=CARTESIAN_POINT('Ctrl Pts',(-1.97677800993721,1.78890736960055,
8.85536669723986));
#393559=CARTESIAN_POINT('Ctrl Pts',(-1.97639553091103,1.78895768077188,
8.85610498449051));
#393560=CARTESIAN_POINT('Ctrl Pts',(-1.97598928856817,1.78905679336042,
8.85681338218371));
#393561=CARTESIAN_POINT('Ctrl Pts',(-1.97562062300402,1.78914673819018,
8.85745625420284));
#393562=CARTESIAN_POINT('Ctrl Pts',(-1.97522762055868,1.78927742070009,
8.85808743050666));
#393563=CARTESIAN_POINT('Ctrl Pts',(-1.97480670587176,1.78947721452132,
8.85866804508411));
#393564=CARTESIAN_POINT('Ctrl Pts',(-1.97461250495953,1.78956939505944,
8.85893592806396));
#393565=CARTESIAN_POINT('Ctrl Pts',(-1.97441236097823,1.789676529682,8.85919241173848));
#393566=CARTESIAN_POINT('Ctrl Pts',(-1.97420613659521,1.78980298681164,
8.85943017985534));
#393567=CARTESIAN_POINT('Ctrl Pts',(-1.97392767262917,1.78997374137196,
8.8597512372));
#393568=CARTESIAN_POINT('Ctrl Pts',(-1.97363136948358,1.79018461885832,
8.86004599534705));
#393569=CARTESIAN_POINT('Ctrl Pts',(-1.97332682621395,1.79044157115162,
8.86026130871721));
#393570=CARTESIAN_POINT('Ctrl Pts',(-1.97321532433696,1.79053564863045,
8.86034014101235));
#393571=CARTESIAN_POINT('Ctrl Pts',(-1.97310103504485,1.79063730615677,
8.86040910639692));
#393572=CARTESIAN_POINT('Ctrl Pts',(-1.97298729564542,1.79074402546769,
8.86046313645506));
#393573=CARTESIAN_POINT('Ctrl Pts',(-1.97280980626518,1.79091056005862,
8.86054744990829));
#393574=CARTESIAN_POINT('Ctrl Pts',(-1.97262891163309,1.79109407389668,
8.86059655985668));
#393575=CARTESIAN_POINT('Ctrl Pts',(-1.97245600443691,1.79128259202281,
8.86059725258816));
#393576=CARTESIAN_POINT('Ctrl Pts',(-1.97228269775603,1.79147154570111,
8.86059794692011));
#393577=CARTESIAN_POINT('Ctrl Pts',(-1.97211745140937,1.79166941813833,
8.86056369958366));
#393578=CARTESIAN_POINT('Ctrl Pts',(-1.97196638965371,1.79186300516205,
8.86048590497774));
#393579=CARTESIAN_POINT('Ctrl Pts',(-1.97192696703313,1.79191352561146,
8.86046560290182));
#393580=CARTESIAN_POINT('Ctrl Pts',(-1.9718880690051,1.79196446716662,8.86044257503091));
#393581=CARTESIAN_POINT('Ctrl Pts',(-1.97185087146101,1.79201423576956,
8.86041778462583));
#393582=CARTESIAN_POINT('Ctrl Pts',(-1.97160057814757,1.79234911670963,
8.860250975962));
#393583=CARTESIAN_POINT('Ctrl Pts',(-1.97139395607629,1.79267602610361,
8.8599848982295));
#393584=CARTESIAN_POINT('Ctrl Pts',(-1.97122987412082,1.79298089568002,
8.85968173251461));
#393585=CARTESIAN_POINT('Ctrl Pts',(-1.97114308416716,1.793142154219,8.85952137522076));
#393586=CARTESIAN_POINT('Ctrl Pts',(-1.97106635501147,1.79330026432413,
8.85934740853961));
#393587=CARTESIAN_POINT('Ctrl Pts',(-1.97099937013855,1.79345231758424,
8.8591675900182));
#393588=CARTESIAN_POINT('Ctrl Pts',(-1.97073039105571,1.7940628904593,8.85844552518695));
#393589=CARTESIAN_POINT('Ctrl Pts',(-1.97060056149348,1.7946090886272,8.85759444184124));
#393590=CARTESIAN_POINT('Ctrl Pts',(-1.97053470628904,1.79506393733563,
8.85683498915138));
#393591=CARTESIAN_POINT('Ctrl Pts',(-1.97052781471729,1.79511153604161,
8.85675551444998));
#393592=CARTESIAN_POINT('Ctrl Pts',(-1.97052164367321,1.79515813331055,
8.85667699793651));
#393593=CARTESIAN_POINT('Ctrl Pts',(-1.97051612006801,1.79520369685434,
8.85659965593547));
#393594=CARTESIAN_POINT('Ctrl Pts',(-1.97044156216317,1.7958187158934,8.85555568965886));
#393595=CARTESIAN_POINT('Ctrl Pts',(-1.97045872831609,1.79642055493028,
8.85434650606346));
#393596=CARTESIAN_POINT('Ctrl Pts',(-1.9705614911754,1.79701236630735,8.85297329937117));
#393597=CARTESIAN_POINT('Ctrl Pts',(-1.97061928902233,1.79734522414735,
8.85220095427747));
#393598=CARTESIAN_POINT('Ctrl Pts',(-1.97070449840185,1.79767499193949,
8.85137579139183));
#393599=CARTESIAN_POINT('Ctrl Pts',(-1.97081848695446,1.79800236791132,
8.85049129520029));
#393600=CARTESIAN_POINT('Origin',(-1.97731117195259,1.7957416895806,7.59394543036555));
#393601=CARTESIAN_POINT('Ctrl Pts',(-1.97839165948368,1.78892888448515,
7.59443877723642));
#393602=CARTESIAN_POINT('Ctrl Pts',(-1.97276532395027,1.78755865015694,
7.58783886950016));
#393603=CARTESIAN_POINT('Ctrl Pts',(-1.96890226666507,1.7951188068979,7.58559994247159));
#393604=CARTESIAN_POINT('Ctrl Pts',(-2.00910566009089,1.79640895348187,
7.56670252222136));
#393605=CARTESIAN_POINT('Ctrl Pts',(-2.00348745620966,1.7950406995313,7.56004874999026));
#393606=CARTESIAN_POINT('Ctrl Pts',(-1.99958248326974,1.80263593116663,
7.55786368756705));
#393607=CARTESIAN_POINT('Ctrl Pts',(-2.03976230537066,1.80387505419709,
7.53888913333558));
#393608=CARTESIAN_POINT('Ctrl Pts',(-2.03411071222869,1.80249866864629,
7.53222002137278));
#393609=CARTESIAN_POINT('Ctrl Pts',(-2.03020677218684,1.81013815140819,
7.53005029815327));
#393610=CARTESIAN_POINT('Ctrl Pts',(-2.07036020808906,1.8113268487847,7.51101258149734));
#393611=CARTESIAN_POINT('Ctrl Pts',(-2.06464010736903,1.80993377894006,
7.5043616886572));
#393612=CARTESIAN_POINT('Ctrl Pts',(-2.06077360068108,1.81762517722494,
7.50217374673251));
#393613=CARTESIAN_POINT('',(-2.05914251569204,1.81722565891166,7.50366116523517));
#393614=CARTESIAN_POINT('Ctrl Pts',(-2.06202449055418,1.80929677321442,
7.51860402984325));
#393615=CARTESIAN_POINT('Ctrl Pts',(-2.06245356066701,1.80940126868831,
7.51734760759493));
#393616=CARTESIAN_POINT('Ctrl Pts',(-2.06282720854068,1.80955350247719,
7.51608817408573));
#393617=CARTESIAN_POINT('Ctrl Pts',(-2.06313953628693,1.80976549106597,
7.5148100591312));
#393618=CARTESIAN_POINT('Ctrl Pts',(-2.0634224502228,1.80995751539533,7.51365231206384));
#393619=CARTESIAN_POINT('Ctrl Pts',(-2.06365558924024,1.81019863323146,
7.51247773061042));
#393620=CARTESIAN_POINT('Ctrl Pts',(-2.06380837374074,1.81051033941392,
7.51129758471022));
#393621=CARTESIAN_POINT('Ctrl Pts',(-2.06399826742622,1.81089775460052,
7.50983079813401));
#393622=CARTESIAN_POINT('Ctrl Pts',(-2.06404627660562,1.81138758047698,
7.50839324291155));
#393623=CARTESIAN_POINT('Ctrl Pts',(-2.0638707052155,1.8119914335698,7.50715379678855));
#393624=CARTESIAN_POINT('Ctrl Pts',(-2.06378959629223,1.81227039629907,
7.50658120839351));
#393625=CARTESIAN_POINT('Ctrl Pts',(-2.06364011712737,1.81261069870671,
7.50598221009429));
#393626=CARTESIAN_POINT('Ctrl Pts',(-2.06340499918457,1.81299509420527,
7.50545747549611));
#393627=CARTESIAN_POINT('Ctrl Pts',(-2.06327953297271,1.81320021954146,
7.50517746087247));
#393628=CARTESIAN_POINT('Ctrl Pts',(-2.0631284923374,1.8134202308675,7.50491486231392));
#393629=CARTESIAN_POINT('Ctrl Pts',(-2.06295450194049,1.81364835785534,
7.50468370960992));
#393630=CARTESIAN_POINT('Ctrl Pts',(-2.06269433141494,1.81398947966074,
7.50433806340446));
#393631=CARTESIAN_POINT('Ctrl Pts',(-2.06237460179234,1.81435863918606,
7.50405484070983));
#393632=CARTESIAN_POINT('Ctrl Pts',(-2.06201630474491,1.81473050520948,
7.5038576603613));
#393633=CARTESIAN_POINT('Ctrl Pts',(-2.06197799044489,1.81477027050058,
7.50383657498791));
#393634=CARTESIAN_POINT('Ctrl Pts',(-2.06193926245814,1.8148100591619,7.50381643264937));
#393635=CARTESIAN_POINT('Ctrl Pts',(-2.06190016639466,1.81484983502236,
7.50379723213559));
#393636=CARTESIAN_POINT('Ctrl Pts',(-2.06163918738168,1.81511535190253,
7.50366906242519));
#393637=CARTESIAN_POINT('Ctrl Pts',(-2.0613556171647,1.81538556994,7.50358235568538));
#393638=CARTESIAN_POINT('Ctrl Pts',(-2.061076029527,1.81563945665821,7.5035341175365));
#393639=CARTESIAN_POINT('Ctrl Pts',(-2.06065681950748,1.81602013105773,
7.50346178989176));
#393640=CARTESIAN_POINT('Ctrl Pts',(-2.06018965908649,1.81641182575994,
7.50346967198527));
#393641=CARTESIAN_POINT('Ctrl Pts',(-2.05971922051127,1.81678223725707,
7.50354272648692));
#393642=CARTESIAN_POINT('Ctrl Pts',(-2.05952571938778,1.8169345951729,7.50357277531559));
#393643=CARTESIAN_POINT('Ctrl Pts',(-2.05933200846982,1.81708326126962,
7.50361331098761));
#393644=CARTESIAN_POINT('Ctrl Pts',(-2.05914251569311,1.8172256589126,7.50366116523659));
#393645=CARTESIAN_POINT('',(-1.97947865054223,1.79771013628763,7.57603338622103));
#393646=CARTESIAN_POINT('Origin',(-1.98601852345765,1.80365333002892,7.58486873427627));
#393647=CARTESIAN_POINT('Ctrl Pts',(-2.05914251574877,1.81722565892004,
7.50366116529969));
#393648=CARTESIAN_POINT('Ctrl Pts',(-2.03263102682016,1.81073191165144,
7.52783573079709));
#393649=CARTESIAN_POINT('Ctrl Pts',(-2.00607765461973,1.80422706199264,
7.55196141284069));
#393650=CARTESIAN_POINT('Ctrl Pts',(-1.97947865179296,1.79771013622993,
7.57603338728831));
#393651=CARTESIAN_POINT('Ctrl Pts',(-1.9798955577159,1.78947609816001,7.59639677331371));
#393652=CARTESIAN_POINT('Ctrl Pts',(-1.96304400704085,1.78239816374436,
7.59959882295464));
#393653=CARTESIAN_POINT('Ctrl Pts',(-1.97123919548053,1.7987550491153,7.59642833564546));
#393654=CARTESIAN_POINT('Ctrl Pts',(-1.97658880884441,1.78740715737193,
7.58707626057423));
#393655=CARTESIAN_POINT('Ctrl Pts',(-1.96999477520762,1.78896632748225,
7.58809943920598));
#393656=CARTESIAN_POINT('Ctrl Pts',(-1.96897092964352,1.79564960071127,
7.58710240504252));
#393657=CARTESIAN_POINT('Ctrl Pts',(-1.97787616399563,1.79334587347696,
7.58015376756929));
#393658=CARTESIAN_POINT('Ctrl Pts',(-1.97503972448267,1.79363549786387,
7.58205880659761));
#393659=CARTESIAN_POINT('Ctrl Pts',(-1.97498177042911,1.7964504075188,7.58020924244128));
#393660=CARTESIAN_POINT('Ctrl Pts',(-1.97947864992973,1.7977101357311,7.57603338509286));
#393661=CARTESIAN_POINT('Ctrl Pts',(-1.97947864992973,1.7977101357311,7.57603338509286));
#393662=CARTESIAN_POINT('Ctrl Pts',(-1.97947864992973,1.7977101357311,7.57603338509286));
#393663=CARTESIAN_POINT('Origin',(-1.9860223598435,1.80364910574226,7.58486873427621));
#393664=CARTESIAN_POINT('Ctrl Pts',(-2.00176808024934,1.88688983029521,
7.51098857897448));
#393665=CARTESIAN_POINT('Ctrl Pts',(-1.99983217741494,1.88132990294068,
7.50433767179956));
#393666=CARTESIAN_POINT('Ctrl Pts',(-2.00711679739921,1.87674270741757,
7.50214974420965));
#393667=CARTESIAN_POINT('Ctrl Pts',(-1.99140963785969,1.85714030662641,
7.53887321589169));
#393668=CARTESIAN_POINT('Ctrl Pts',(-1.98949693057684,1.85164699706871,
7.53220407452066));
#393669=CARTESIAN_POINT('Ctrl Pts',(-1.99672626159447,1.84702750651676,
7.53003438070912));
#393670=CARTESIAN_POINT('Ctrl Pts',(-1.98103130343958,1.82733365289803,
7.56669465659235));
#393671=CARTESIAN_POINT('Ctrl Pts',(-1.97912989990116,1.82187280777846,
7.56004085833298));
#393672=CARTESIAN_POINT('Ctrl Pts',(-1.98631507225213,1.81725653781094,
7.55785582193789));
#393673=CARTESIAN_POINT('Ctrl Pts',(-1.97063354635953,1.79747121714567,
7.59443891967696));
#393674=CARTESIAN_POINT('Ctrl Pts',(-1.96872938602273,1.7920024544806,7.58783901202978));
#393675=CARTESIAN_POINT('Ctrl Pts',(-1.97588366545473,1.78743129885023,
7.58560008491213));
#393676=CARTESIAN_POINT('',(-2.00655355952792,1.87513194417974,7.50366116523517));
#393677=CARTESIAN_POINT('Ctrl Pts',(-2.00655355952819,1.87513194417999,
7.50366116523554));
#393678=CARTESIAN_POINT('Ctrl Pts',(-2.00615848269924,1.87577851344619,
7.50350835821027));
#393679=CARTESIAN_POINT('Ctrl Pts',(-2.00577427574858,1.87636001411704,
7.50345484955999));
#393680=CARTESIAN_POINT('Ctrl Pts',(-2.0053900169105,1.87689406571169,7.50349758195598));
#393681=CARTESIAN_POINT('Ctrl Pts',(-2.00519286362919,1.87716807378604,
7.50351950684424));
#393682=CARTESIAN_POINT('Ctrl Pts',(-2.00497636954116,1.87745667406357,
7.50357029184312));
#393683=CARTESIAN_POINT('Ctrl Pts',(-2.0047599570338,1.87772922952131,7.50365515313923));
#393684=CARTESIAN_POINT('Ctrl Pts',(-2.0044270269634,1.87814853018392,7.50378570417639));
#393685=CARTESIAN_POINT('Ctrl Pts',(-2.0040847889912,1.87854238174117,7.50400001621911));
#393686=CARTESIAN_POINT('Ctrl Pts',(-2.00375757860848,1.87887931717084,
7.50428903009634));
#393687=CARTESIAN_POINT('Ctrl Pts',(-2.00372126077341,1.8789167144113,7.50432110841318));
#393688=CARTESIAN_POINT('Ctrl Pts',(-2.00368512302499,1.87895344037839,
7.50435406373354));
#393689=CARTESIAN_POINT('Ctrl Pts',(-2.00364919461634,1.87898947405935,
7.50438785222351));
#393690=CARTESIAN_POINT('Ctrl Pts',(-2.00342983441215,1.87920947700163,
7.50459414719561));
#393691=CARTESIAN_POINT('Ctrl Pts',(-2.00321442008337,1.87940681218196,
7.50483629897752));
#393692=CARTESIAN_POINT('Ctrl Pts',(-2.00301209305111,1.87957489015284,
7.5050991045531));
#393693=CARTESIAN_POINT('Ctrl Pts',(-2.00256573929611,1.87994568703844,
7.50567888004914));
#393694=CARTESIAN_POINT('Ctrl Pts',(-2.00216582340181,1.88018910434134,
7.50637912803145));
#393695=CARTESIAN_POINT('Ctrl Pts',(-2.00182096599598,1.88033482544298,
7.50710440483569));
#393696=CARTESIAN_POINT('Ctrl Pts',(-2.00173640011369,1.88037055915008,
7.50728225710685));
#393697=CARTESIAN_POINT('Ctrl Pts',(-2.00165351840971,1.88040126390213,
7.50746498566955));
#393698=CARTESIAN_POINT('Ctrl Pts',(-2.00157440033246,1.8804266135986,7.50764697238949));
#393699=CARTESIAN_POINT('Ctrl Pts',(-2.00114908332306,1.88056288659041,
7.50862528291181));
#393700=CARTESIAN_POINT('Ctrl Pts',(-2.00079518281119,1.88056071912448,
7.5096585683742));
#393701=CARTESIAN_POINT('Ctrl Pts',(-2.0004944929555,1.880483860265,7.510679598732));
#393702=CARTESIAN_POINT('Ctrl Pts',(-2.00032902294865,1.88044156473768,
7.51124147302577));
#393703=CARTESIAN_POINT('Ctrl Pts',(-2.00017973400083,1.88037621910703,
7.51180065547252));
#393704=CARTESIAN_POINT('Ctrl Pts',(-2.00004436034522,1.88029584196497,
7.512351757165));
#393705=CARTESIAN_POINT('Ctrl Pts',(-1.99957659043866,1.8800181069207,7.51425603304536));
#393706=CARTESIAN_POINT('Ctrl Pts',(-1.99922228938719,1.87952256964401,
7.51626900505181));
#393707=CARTESIAN_POINT('Ctrl Pts',(-1.99897691956687,1.87886941383173,
7.51827788969244));
#393708=CARTESIAN_POINT('Ctrl Pts',(-1.99896363968851,1.87883406380488,
7.51838661432546));
#393709=CARTESIAN_POINT('Ctrl Pts',(-1.99895068242723,1.87879824277267,
7.51849533314857));
#393710=CARTESIAN_POINT('Ctrl Pts',(-1.99893804826278,1.87876195735829,
7.51860402984325));
#393711=CARTESIAN_POINT('Ctrl Pts',(-1.97947865060561,1.7977101375391,7.57603338728985));
#393712=CARTESIAN_POINT('Ctrl Pts',(-1.9885195791301,1.82356045445259,7.55196141284922));
#393713=CARTESIAN_POINT('Ctrl Pts',(-1.99754410576767,1.84936651119318,
7.52783573083105));
#393714=CARTESIAN_POINT('Ctrl Pts',(-2.00655355954224,1.87513194423716,
7.50366116530176));
#393715=CARTESIAN_POINT('Origin',(-6.84001376365786E-16,6.21191952330709E-16,
7.49482233047033));
#393716=CARTESIAN_POINT('Origin',(-2.05251535802925,1.81137708803387,7.49482233047033));
#393717=CARTESIAN_POINT('Origin',(0.,0.,7.50366116523517));
#393718=CARTESIAN_POINT('Origin',(-2.00009565450363,1.86909700733689,7.49482233047033));
#393719=CARTESIAN_POINT('Ctrl Pts',(-2.06202346288219,1.80929652288975,
7.51860402984325));
#393720=CARTESIAN_POINT('Ctrl Pts',(-2.06941618821693,1.81109760538513,
7.51860402984325));
#393721=CARTESIAN_POINT('Ctrl Pts',(-2.07441142381098,1.80535792705007,
7.51860402984325));
#393722=CARTESIAN_POINT('Ctrl Pts',(-2.06476843255036,1.8099652758769,7.51041458714365));
#393723=CARTESIAN_POINT('Ctrl Pts',(-2.07059960927625,1.80973780334734,
7.51004642900442));
#393724=CARTESIAN_POINT('Ctrl Pts',(-2.07441280143765,1.80535634411492,
7.5072913648301));
#393725=CARTESIAN_POINT('Ctrl Pts',(-2.06508648531179,1.81276216336841,
7.50215815450138));
#393726=CARTESIAN_POINT('Ctrl Pts',(-2.06819015181946,1.81250658815323,
7.49877163671531));
#393727=CARTESIAN_POINT('Ctrl Pts',(-2.07047313188639,1.80991971250713,
7.49481588533171));
#393728=CARTESIAN_POINT('Ctrl Pts',(-2.05914210292581,1.8172252946396,7.50366171572174));
#393729=CARTESIAN_POINT('Ctrl Pts',(-2.0618875742757,1.81964821629003,7.50000045605858));
#393730=CARTESIAN_POINT('Ctrl Pts',(-2.06188757427578,1.81964821628993,
7.49482233047317));
#393731=CARTESIAN_POINT('Origin',(-2.06498228097548,1.79715175465438,7.51860402984325));
#393732=CARTESIAN_POINT('Origin',(-2.06498228097548,1.79715175465438,9.));
#393733=CARTESIAN_POINT('Origin',(-2.06498228097548,1.79715175465438,8.75721825406948));
#393734=CARTESIAN_POINT('Ctrl Pts',(-2.04579859637347,1.80534509773719,
8.78942910404913));
#393735=CARTESIAN_POINT('Ctrl Pts',(-2.05120799968457,1.80668329970982,
8.79672699501691));
#393736=CARTESIAN_POINT('Ctrl Pts',(-2.05490627375193,1.79855949180314,
8.79893251111267));
#393737=CARTESIAN_POINT('Ctrl Pts',(-2.05648070824783,1.807946617417,8.78111911759583));
#393738=CARTESIAN_POINT('Ctrl Pts',(-2.06289540615571,1.80952584535372,
8.78644465894813));
#393739=CARTESIAN_POINT('Ctrl Pts',(-2.06775831860606,1.80303989174029,
8.78817647674131));
#393740=CARTESIAN_POINT('Ctrl Pts',(-2.06313805516785,1.80956794650264,
8.7678092393203));
#393741=CARTESIAN_POINT('Ctrl Pts',(-2.0707115533493,1.8114272103532,8.76988516158374));
#393742=CARTESIAN_POINT('Ctrl Pts',(-2.07578916287302,1.80582772270513,
8.77093053738833));
#393743=CARTESIAN_POINT('Ctrl Pts',(-2.06183996363106,1.8092518095187,8.75371302330492));
#393744=CARTESIAN_POINT('Ctrl Pts',(-2.06922740267153,1.81106618152884,
8.75300828287559));
#393745=CARTESIAN_POINT('Ctrl Pts',(-2.07422297212531,1.80528355019297,
8.75267964240738));
#393746=CARTESIAN_POINT('Origin',(-2.05135792032742,1.7938336861622,8.78727029226991));
#393747=CARTESIAN_POINT('Ctrl Pts',(-1.9789379566843,1.78906192937258,8.85049129520029));
#393748=CARTESIAN_POINT('Ctrl Pts',(-1.98461173602729,1.79044371813727,
8.85711686593484));
#393749=CARTESIAN_POINT('Ctrl Pts',(-1.98847679932028,1.78281731348927,
8.85933012996512));
#393750=CARTESIAN_POINT('Ctrl Pts',(-2.00212570220895,1.79470905879154,
8.82945683644721));
#393751=CARTESIAN_POINT('Ctrl Pts',(-2.00784657735091,1.79610231723841,
8.83607469902387));
#393752=CARTESIAN_POINT('Ctrl Pts',(-2.01168953666616,1.78843656833835,
8.8382956714852));
#393753=CARTESIAN_POINT('Ctrl Pts',(-2.02527888452907,1.80034777070872,
8.80838214965003));
#393754=CARTESIAN_POINT('Ctrl Pts',(-2.03102233691534,1.80174652760391,
8.81501364461987));
#393755=CARTESIAN_POINT('Ctrl Pts',(-2.03486690419791,1.79404794883865,
8.81722098428721));
#393756=CARTESIAN_POINT('Ctrl Pts',(-2.04840012990613,1.80597870472224,
8.78727029226991));
#393757=CARTESIAN_POINT('Ctrl Pts',(-2.05414453629874,1.80737769395557,
8.79393457792714));
#393758=CARTESIAN_POINT('Ctrl Pts',(-2.05801159645805,1.79965207029774,
8.79610912703474));
#393759=CARTESIAN_POINT('Origin',(-1.9818957471056,1.77691691081254,8.85049129520029));
#393760=CARTESIAN_POINT('Ctrl Pts',(-1.97081848695446,1.79800236791132,
8.85049129520029));
#393761=CARTESIAN_POINT('Ctrl Pts',(-1.97273870409018,1.80351724582246,
8.85711686593484));
#393762=CARTESIAN_POINT('Ctrl Pts',(-1.96551867526938,1.80809675954563,
8.85933012996512));
#393763=CARTESIAN_POINT('Ctrl Pts',(-1.96911969857311,1.79312343503146,
8.86332496987231));
#393764=CARTESIAN_POINT('Ctrl Pts',(-1.9662278890552,1.79672750663019,8.86648636486737));
#393765=CARTESIAN_POINT('Ctrl Pts',(-1.96078242541378,1.79444211221727,
8.87206031107457));
#393766=CARTESIAN_POINT('Ctrl Pts',(-1.97388433684391,1.78783117387535,
8.86341338519877));
#393767=CARTESIAN_POINT('Ctrl Pts',(-1.97718275554803,1.78457634597106,
8.86654584966058));
#393768=CARTESIAN_POINT('Ctrl Pts',(-1.97432290905723,1.7793854471244,8.87215952290714));
#393769=CARTESIAN_POINT('Ctrl Pts',(-1.9789379566843,1.78906192937258,8.85049129520029));
#393770=CARTESIAN_POINT('Ctrl Pts',(-1.98461173602729,1.79044371813727,
8.85711686593484));
#393771=CARTESIAN_POINT('Ctrl Pts',(-1.98847679932028,1.78281731348927,
8.85933012996512));
#393772=CARTESIAN_POINT('Origin',(-1.95901360513967,1.802112692149,8.85049129520029));
#393773=CARTESIAN_POINT('Ctrl Pts',(-1.99432705985485,1.86551916431871,
8.78727029226991));
#393774=CARTESIAN_POINT('Ctrl Pts',(-1.99627117980081,1.87110269127881,
8.79393457792714));
#393775=CARTESIAN_POINT('Ctrl Pts',(-1.98895258219516,1.87569371995056,
8.79610912703474));
#393776=CARTESIAN_POINT('Ctrl Pts',(-1.98650197380753,1.84304545892766,
8.80838214965002));
#393777=CARTESIAN_POINT('Ctrl Pts',(-1.98844577088241,1.84862805859966,
8.81501364461993));
#393778=CARTESIAN_POINT('Ctrl Pts',(-1.98115193336383,1.85319410139924,
8.81722098428721));
#393779=CARTESIAN_POINT('Ctrl Pts',(-1.97866607911547,1.82054071102845,
8.82945683644723));
#393780=CARTESIAN_POINT('Ctrl Pts',(-1.98060223521441,1.8261013657606,8.83607469902389));
#393781=CARTESIAN_POINT('Ctrl Pts',(-1.97334092145604,1.83066265560014,
8.8382956714852));
#393782=CARTESIAN_POINT('Ctrl Pts',(-1.97081848695446,1.79800236791132,
8.85049129520029));
#393783=CARTESIAN_POINT('Ctrl Pts',(-1.97273870409018,1.80351724582246,
8.85711686593484));
#393784=CARTESIAN_POINT('Ctrl Pts',(-1.96551867526938,1.80809675954563,
8.85933012996512));
#393785=CARTESIAN_POINT('Origin',(-1.98252217804006,1.86962948855639,8.78727029226991));
#393786=CARTESIAN_POINT('Ctrl Pts',(-1.99887714505914,1.87858709900374,
8.75374538247848));
#393787=CARTESIAN_POINT('Ctrl Pts',(-2.0013882733546,1.88575917074566,8.75304829418602));
#393788=CARTESIAN_POINT('Ctrl Pts',(-1.99612174305392,1.89128495592073,
8.75272238421917));
#393789=CARTESIAN_POINT('Ctrl Pts',(-1.99931119033487,1.87983367897016,
8.76769408445018));
#393790=CARTESIAN_POINT('Ctrl Pts',(-2.00188485842239,1.88718645990988,
8.76974318093967));
#393791=CARTESIAN_POINT('Ctrl Pts',(-1.99680650103025,1.89277471934172,
8.7707786988043));
#393792=CARTESIAN_POINT('Ctrl Pts',(-1.99708652152471,1.87344442018717,
8.78108014887992));
#393793=CARTESIAN_POINT('Ctrl Pts',(-1.99927119857792,1.87967438194253,
8.78639403366326));
#393794=CARTESIAN_POINT('Ctrl Pts',(-1.9933043463902,1.88514418547637,8.78812224174741));
#393795=CARTESIAN_POINT('Ctrl Pts',(-1.99344078041232,1.86297383549668,
8.78944554828685));
#393796=CARTESIAN_POINT('Ctrl Pts',(-1.9952872275871,1.86822236390451,8.79673892988685));
#393797=CARTESIAN_POINT('Ctrl Pts',(-1.98756562585766,1.87268111048268,
8.79894799272499));
#393798=CARTESIAN_POINT('Origin',(-1.987133166448,1.88287228159596,8.75721825406948));
#393799=CARTESIAN_POINT('Origin',(-1.987133166448,1.88287228159596,9.));
#393800=CARTESIAN_POINT('Origin',(-1.987133166448,1.88287228159596,7.51860402984325));
#393801=CARTESIAN_POINT('Ctrl Pts',(-2.00655298476889,1.87513140706531,
7.50366195182966));
#393802=CARTESIAN_POINT('Ctrl Pts',(-2.00922851137341,1.87763169686821,
7.50000065167735));
#393803=CARTESIAN_POINT('Ctrl Pts',(-2.00922851137333,1.8776316968683,7.49482233047108));
#393804=CARTESIAN_POINT('Ctrl Pts',(-2.00267706150171,1.88148207777269,
7.50215800491337));
#393805=CARTESIAN_POINT('Ctrl Pts',(-2.00271935143079,1.88459702700764,
7.49877273257265));
#393806=CARTESIAN_POINT('Ctrl Pts',(-2.00036234457183,1.88711926312204,
7.49481816995647));
#393807=CARTESIAN_POINT('Ctrl Pts',(-1.99986519248848,1.88142369117744,
7.51043025814042));
#393808=CARTESIAN_POINT('Ctrl Pts',(-2.0002025994931,1.8872528346394,7.51006209594514));
#393809=CARTESIAN_POINT('Ctrl Pts',(-1.99620509243911,1.89147170978754,
7.50731281821699));
#393810=CARTESIAN_POINT('Ctrl Pts',(-1.99893755118652,1.87876053002944,
7.51860402984325));
#393811=CARTESIAN_POINT('Ctrl Pts',(-2.00144054600741,1.88594635178601,
7.51860402984325));
#393812=CARTESIAN_POINT('Ctrl Pts',(-1.9962068338747,1.89146987192289,7.51860402984325));
#393813=CARTESIAN_POINT('Origin',(0.,0.,7.5));
#393814=CARTESIAN_POINT('Origin',(-2.08196763624131,1.66803740521007,7.5));
#393815=CARTESIAN_POINT('',(-2.08196763624131,1.66803740521007,7.59394543036555));
#393816=CARTESIAN_POINT('',(-2.08196763624131,1.66803740521007,8.85049129520029));
#393817=CARTESIAN_POINT('',(-2.08196763624131,1.66803740521007,7.5));
#393818=CARTESIAN_POINT('',(-2.10975372425561,1.73390928168093,8.78727029226991));
#393819=CARTESIAN_POINT('Ctrl Pts',(-2.08196763624131,1.66803740521007,
8.85049129520029));
#393820=CARTESIAN_POINT('Ctrl Pts',(-2.09124312883603,1.69002661441762,
8.82945686509571));
#393821=CARTESIAN_POINT('Ctrl Pts',(-2.10050483228943,1.71198313400678,
8.80838212259895));
#393822=CARTESIAN_POINT('Ctrl Pts',(-2.10975372425561,1.73390928168093,
8.78727029226991));
#393823=CARTESIAN_POINT('',(-2.11520370755654,1.74682943894029,8.75721825406948));
#393824=CARTESIAN_POINT('Origin',(-2.09880300312866,1.70794812528068,8.75937679713103));
#393825=CARTESIAN_POINT('',(-2.11520370755654,1.74682943894029,7.51860402984325));
#393826=CARTESIAN_POINT('',(-2.11520370755654,1.74682943894029,7.5));
#393827=CARTESIAN_POINT('Ctrl Pts',(-2.11520370755654,1.74682943894029,
7.51860402984325));
#393828=CARTESIAN_POINT('Ctrl Pts',(-2.11092359330639,1.73668266487761,
7.52834476460825));
#393829=CARTESIAN_POINT('Ctrl Pts',(-2.10664070046784,1.72652930367562,
7.53807742314407));
#393830=CARTESIAN_POINT('Ctrl Pts',(-2.10235493574608,1.71636913416236,
7.54780169004674));
#393831=CARTESIAN_POINT('Ctrl Pts',(-2.09556651605262,1.70027597476367,
7.5632044032688));
#393832=CARTESIAN_POINT('Ctrl Pts',(-2.08877088254285,1.68416571372709,
7.57858609112102));
#393833=CARTESIAN_POINT('Ctrl Pts',(-2.08196763624131,1.66803740521007,
7.59394543036555));
#393834=CARTESIAN_POINT('Origin',(-2.36030818298167,1.70641386443188,7.5));
#393835=CARTESIAN_POINT('',(-2.17370988235715,1.67346501623196,8.75721825406948));
#393836=CARTESIAN_POINT('',(-2.15990092504105,1.67102668085117,8.78727029226991));
#393837=CARTESIAN_POINT('Origin',(-2.12484864088886,1.66483727620104,8.75658640621056));
#393838=CARTESIAN_POINT('',(-2.08949760778589,1.65859511954945,8.85049129520029));
#393839=CARTESIAN_POINT('Ctrl Pts',(-2.15990092504105,1.67102668085117,
8.78727029226991));
#393840=CARTESIAN_POINT('Ctrl Pts',(-2.13646643958854,1.66688870477511,
8.80838212259895));
#393841=CARTESIAN_POINT('Ctrl Pts',(-2.11299949288422,1.66274499680945,
8.82945686509571));
#393842=CARTESIAN_POINT('Ctrl Pts',(-2.08949760778589,1.65859511954945,
8.85049129520029));
#393843=CARTESIAN_POINT('',(-2.08949760778589,1.65859511954945,7.59394543036555));
#393844=CARTESIAN_POINT('',(-2.08949760778589,1.65859511954945,7.5));
#393845=CARTESIAN_POINT('',(-2.17370988235715,1.67346501623196,7.51860402984325));
#393846=CARTESIAN_POINT('Ctrl Pts',(-2.08949760778588,1.65859511954945,
7.59394543036555));
#393847=CARTESIAN_POINT('Ctrl Pts',(-2.10673541065636,1.66163890798792,
7.57858609112103));
#393848=CARTESIAN_POINT('Ctrl Pts',(-2.12395392452866,1.66467929044538,
7.56320440326857));
#393849=CARTESIAN_POINT('Ctrl Pts',(-2.14115416031192,1.66771644542443,
7.54780169004651));
#393850=CARTESIAN_POINT('Ctrl Pts',(-2.1520132655315,1.66963390666748,7.53807742314383));
#393851=CARTESIAN_POINT('Ctrl Pts',(-2.16286509408445,1.67155008302324,
7.52834476460825));
#393852=CARTESIAN_POINT('Ctrl Pts',(-2.17370988235715,1.67346501623196,
7.51860402984325));
#393853=CARTESIAN_POINT('',(-2.17370988235715,1.67346501623196,7.5));
#393854=CARTESIAN_POINT('Origin',(-2.08830213916383,1.66536538392934,7.5));
#393855=CARTESIAN_POINT('Ctrl Pts',(-2.08949760778589,1.65859511954945,
8.85049129520029));
#393856=CARTESIAN_POINT('Ctrl Pts',(-2.08930689657203,1.65856144445801,
8.85097269580138));
#393857=CARTESIAN_POINT('Ctrl Pts',(-2.08911712890332,1.65853647751091,
8.85143669361005));
#393858=CARTESIAN_POINT('Ctrl Pts',(-2.08891945254857,1.65851993587657,
8.8519052845931));
#393859=CARTESIAN_POINT('Ctrl Pts',(-2.08853281013487,1.65848758148884,
8.85282181883899));
#393860=CARTESIAN_POINT('Ctrl Pts',(-2.0881258413294,1.65848848817671,8.85372622499635));
#393861=CARTESIAN_POINT('Ctrl Pts',(-2.08769219444456,1.65853808886801,
8.8546225773507));
#393862=CARTESIAN_POINT('Ctrl Pts',(-2.08733219620245,1.65857926560028,
8.85536669723986));
#393863=CARTESIAN_POINT('Ctrl Pts',(-2.08695372646825,1.65865397891726,
8.85610498449051));
#393864=CARTESIAN_POINT('Ctrl Pts',(-2.08655466895921,1.65877891590463,
8.85681338218371));
#393865=CARTESIAN_POINT('Ctrl Pts',(-2.08619252364303,1.65889229641688,
8.85745625420284));
#393866=CARTESIAN_POINT('Ctrl Pts',(-2.08580870152052,1.65904789017868,
8.85808743050665));
#393867=CARTESIAN_POINT('Ctrl Pts',(-2.08540145248205,1.65927424159867,
8.8586680450841));
#393868=CARTESIAN_POINT('Ctrl Pts',(-2.08521355660377,1.65937867523715,
8.85893592806395));
#393869=CARTESIAN_POINT('Ctrl Pts',(-2.08502068797859,1.65949841300905,
8.85919241173848));
#393870=CARTESIAN_POINT('Ctrl Pts',(-2.08482298944179,1.65963782316054,
8.85943017985534));
#393871=CARTESIAN_POINT('Ctrl Pts',(-2.08455603789208,1.65982606813486,
8.8597512372));
#393872=CARTESIAN_POINT('Ctrl Pts',(-2.08427385450002,1.66005549655853,
8.86004599534706));
#393873=CARTESIAN_POINT('Ctrl Pts',(-2.08398639993716,1.66033143307006,
8.86026130871721));
#393874=CARTESIAN_POINT('Ctrl Pts',(-2.08388115471749,1.66043246120641,
8.86034014101235));
#393875=CARTESIAN_POINT('Ctrl Pts',(-2.08377361346506,1.66054123240653,
8.86040910639692));
#393876=CARTESIAN_POINT('Ctrl Pts',(-2.08366694528516,1.66065501975952,
8.86046313645506));
#393877=CARTESIAN_POINT('Ctrl Pts',(-2.08350049048376,1.66083258397091,
8.86054744990829));
#393878=CARTESIAN_POINT('Ctrl Pts',(-2.08333172529106,1.66102731071898,
8.86059655985669));
#393879=CARTESIAN_POINT('Ctrl Pts',(-2.08317125174907,1.66122651971649,
8.86059725258816));
#393880=CARTESIAN_POINT('Ctrl Pts',(-2.08301040744909,1.66142618896637,
8.86059794692011));
#393881=CARTESIAN_POINT('Ctrl Pts',(-2.08285817834936,1.66163424222322,
8.86056369958366));
#393882=CARTESIAN_POINT('Ctrl Pts',(-2.08271983012947,1.66183711006156,
8.86048590497774));
#393883=CARTESIAN_POINT('Ctrl Pts',(-2.0826837253632,1.66189005252726,8.86046560290182));
#393884=CARTESIAN_POINT('Ctrl Pts',(-2.08264817109199,1.66194338162274,
8.86044257503091));
#393885=CARTESIAN_POINT('Ctrl Pts',(-2.08261423865958,1.66199543122558,
8.86041778462583));
#393886=CARTESIAN_POINT('Ctrl Pts',(-2.08238591549609,1.66234566046449,
8.86025097596201));
#393887=CARTESIAN_POINT('Ctrl Pts',(-2.0822006631088,1.66268513650962,8.8599848982295));
#393888=CARTESIAN_POINT('Ctrl Pts',(-2.08205645133814,1.66299989246577,
8.85968173251461));
#393889=CARTESIAN_POINT('Ctrl Pts',(-2.08198017157381,1.66316638033321,
8.85952137522076));
#393890=CARTESIAN_POINT('Ctrl Pts',(-2.08191373021562,1.66332908163806,
8.85934740853961));
#393891=CARTESIAN_POINT('Ctrl Pts',(-2.08185662505612,1.66348511422399,
8.8591675900182));
#393892=CARTESIAN_POINT('Ctrl Pts',(-2.08162731815807,1.66411166616059,
8.85844552518696));
#393893=CARTESIAN_POINT('Ctrl Pts',(-2.08153275038138,1.66466506031438,
8.85759444184126));
#393894=CARTESIAN_POINT('Ctrl Pts',(-2.08149617274033,1.66512319384479,
8.85683498915141));
#393895=CARTESIAN_POINT('Ctrl Pts',(-2.08149234498761,1.66517113629864,
8.85675551445));
#393896=CARTESIAN_POINT('Ctrl Pts',(-2.08148917211987,1.66521803320866,
8.85667699793652));
#393897=CARTESIAN_POINT('Ctrl Pts',(-2.08148657912978,1.66526385703586,
8.85659965593547));
#393898=CARTESIAN_POINT('Ctrl Pts',(-2.08145157881728,1.6658823893937,8.85555568965886));
#393899=CARTESIAN_POINT('Ctrl Pts',(-2.08150726965999,1.66648189204855,
8.85434650606346));
#393900=CARTESIAN_POINT('Ctrl Pts',(-2.08164773886709,1.66706590344667,
8.85297329937118));
#393901=CARTESIAN_POINT('Ctrl Pts',(-2.08172674423718,1.66739437427377,
8.85220095427748));
#393902=CARTESIAN_POINT('Ctrl Pts',(-2.08183290683987,1.66771800513893,
8.85137579139184));
#393903=CARTESIAN_POINT('Ctrl Pts',(-2.08196763624131,1.66803740521007,
8.85049129520029));
#393904=CARTESIAN_POINT('Origin',(-2.08830213916383,1.66536538392934,7.59394543036555));
#393905=CARTESIAN_POINT('Ctrl Pts',(-2.08894390879624,1.65849734939882,
7.59443877723642));
#393906=CARTESIAN_POINT('Ctrl Pts',(-2.08324134195778,1.65749041091931,
7.58783886950016));
#393907=CARTESIAN_POINT('Ctrl Pts',(-2.07987060264357,1.66528254143749,
7.58559994247159));
#393908=CARTESIAN_POINT('Ctrl Pts',(-2.12007405386119,1.66399419701616,
7.56670252222133));
#393909=CARTESIAN_POINT('Ctrl Pts',(-2.11437972885083,1.66298871384862,
7.56004874999027));
#393910=CARTESIAN_POINT('Ctrl Pts',(-2.11096940725828,1.6708185327413,7.55786368756704));
#393911=CARTESIAN_POINT('Ctrl Pts',(-2.1511460664906,1.66948077981979,7.5388891333356));
#393912=CARTESIAN_POINT('Ctrl Pts',(-2.14541789982786,1.66846932101657,
7.53222002137279));
#393913=CARTESIAN_POINT('Ctrl Pts',(-2.1420114441906,1.67634323393907,7.53005029815327));
#393914=CARTESIAN_POINT('Ctrl Pts',(-2.18215854065472,1.67495684953809,
7.51101258149734));
#393915=CARTESIAN_POINT('Ctrl Pts',(-2.17636093820369,1.6739331300163,7.5043616886572));
#393916=CARTESIAN_POINT('Ctrl Pts',(-2.17299516524849,1.68185645343256,
7.50217374673251));
#393917=CARTESIAN_POINT('',(-2.17134183427228,1.68156225994656,7.50366116523517));
#393918=CARTESIAN_POINT('Ctrl Pts',(-2.17370988235715,1.67346501623196,
7.51860402984325));
#393919=CARTESIAN_POINT('Ctrl Pts',(-2.17414476594741,1.67354180639217,
7.51734760759493));
#393920=CARTESIAN_POINT('Ctrl Pts',(-2.17452739977379,1.67366978769894,
7.51608817408572));
#393921=CARTESIAN_POINT('Ctrl Pts',(-2.17485266796471,1.67386132982703,
7.51481005913119));
#393922=CARTESIAN_POINT('Ctrl Pts',(-2.17514730366458,1.6740348332637,7.51365231206383));
#393923=CARTESIAN_POINT('Ctrl Pts',(-2.1753954121457,1.67426051842925,7.51247773061042));
#393924=CARTESIAN_POINT('Ctrl Pts',(-2.17556785381774,1.67456179524136,
7.51129758471022));
#393925=CARTESIAN_POINT('Ctrl Pts',(-2.17578217912251,1.67493624791171,
7.50983079813402));
#393926=CARTESIAN_POINT('Ctrl Pts',(-2.17586147291356,1.67542199142969,
7.50839324291155));
#393927=CARTESIAN_POINT('Ctrl Pts',(-2.17572495125418,1.67603585273915,
7.50715379678855));
#393928=CARTESIAN_POINT('Ctrl Pts',(-2.17566188218132,1.67631943897613,
7.50658120839351));
#393929=CARTESIAN_POINT('Ctrl Pts',(-2.17553451338756,1.67666861935896,
7.50598221009429));
#393930=CARTESIAN_POINT('Ctrl Pts',(-2.17532450682394,1.67706728913406,
7.50545747549611));
#393931=CARTESIAN_POINT('Ctrl Pts',(-2.17521244082128,1.67728003166603,
7.50517746087247));
#393932=CARTESIAN_POINT('Ctrl Pts',(-2.17507580668921,1.67750926816194,
7.50491486231392));
#393933=CARTESIAN_POINT('Ctrl Pts',(-2.17491678992052,1.67774807404142,
7.50468370960992));
#393934=CARTESIAN_POINT('Ctrl Pts',(-2.17467900969234,1.67810516415829,
7.50433806340446));
#393935=CARTESIAN_POINT('Ctrl Pts',(-2.17438358912053,1.67849405035303,
7.50405484070983));
#393936=CARTESIAN_POINT('Ctrl Pts',(-2.17404985377074,1.67888810850847,
7.5038576603613));
#393937=CARTESIAN_POINT('Ctrl Pts',(-2.1740141659625,1.67893024690314,7.50383657498791));
#393938=CARTESIAN_POINT('Ctrl Pts',(-2.17397806681484,1.67897243512502,
7.50381643264937));
#393939=CARTESIAN_POINT('Ctrl Pts',(-2.17394159952654,1.67901463415509,
7.50379723213559));
#393940=CARTESIAN_POINT('Ctrl Pts',(-2.17369816844786,1.67929632648513,
7.50366906242519));
#393941=CARTESIAN_POINT('Ctrl Pts',(-2.1734324937854,1.67958415773685,7.50358235568538));
#393942=CARTESIAN_POINT('Ctrl Pts',(-2.17316974716838,1.67985543605901,
7.5035341175365));
#393943=CARTESIAN_POINT('Ctrl Pts',(-2.17277578835333,1.68026218720033,
7.50346178989176));
#393944=CARTESIAN_POINT('Ctrl Pts',(-2.17233468372925,1.6806830081947,7.50346967198527));
#393945=CARTESIAN_POINT('Ctrl Pts',(-2.17188894406665,1.68108279974468,
7.50354272648692));
#393946=CARTESIAN_POINT('Ctrl Pts',(-2.17170560211715,1.68124724228438,
7.50357277531559));
#393947=CARTESIAN_POINT('Ctrl Pts',(-2.17152181426857,1.68140801403178,
7.50361331098761));
#393948=CARTESIAN_POINT('Ctrl Pts',(-2.1713418342734,1.68156225994742,7.50366116523658));
#393949=CARTESIAN_POINT('',(-2.09059128324977,1.66719091542145,7.57603338622103));
#393950=CARTESIAN_POINT('Origin',(-2.09749850102583,1.67270288713818,7.58486873427626));
#393951=CARTESIAN_POINT('Ctrl Pts',(-2.17134183432943,1.68156225995128,
7.50366116529969));
#393952=CARTESIAN_POINT('Ctrl Pts',(-2.14446876028216,1.67678045171058,
7.52783573079709));
#393953=CARTESIAN_POINT('Ctrl Pts',(-2.11755317768418,1.67199024736118,
7.55196141284068));
#393954=CARTESIAN_POINT('Ctrl Pts',(-2.09059128449423,1.66719091528374,
7.57603338728831));
#393955=CARTESIAN_POINT('Ctrl Pts',(-2.09047977720881,1.65894708367395,
7.59639677331371));
#393956=CARTESIAN_POINT('Ctrl Pts',(-2.07239800659894,1.65268226143542,
7.59974925422225));
#393957=CARTESIAN_POINT('Ctrl Pts',(-2.08252932914762,1.6689166302092,7.59639677331372));
#393958=CARTESIAN_POINT('Ctrl Pts',(-2.08704726491611,1.6570942578742,7.58707626057421));
#393959=CARTESIAN_POINT('Ctrl Pts',(-2.08045436498717,1.65910699286144,
7.58811717123966));
#393960=CARTESIAN_POINT('Ctrl Pts',(-2.0799591517179,1.66598247069354,7.58707626057424));
#393961=CARTESIAN_POINT('Ctrl Pts',(-2.08871246990531,1.66293829112236,
7.5801537675693));
#393962=CARTESIAN_POINT('Ctrl Pts',(-2.08585790079769,1.66341616887628,
7.5820876076604));
#393963=CARTESIAN_POINT('Ctrl Pts',(-2.08602720582064,1.66630550578067,
7.5801537675693));
#393964=CARTESIAN_POINT('Ctrl Pts',(-2.09059128260288,1.66719091490531,
7.57603338509286));
#393965=CARTESIAN_POINT('Ctrl Pts',(-2.09059128260288,1.66719091490531,
7.57603338509286));
#393966=CARTESIAN_POINT('Ctrl Pts',(-2.09059128260288,1.66719091490531,
7.57603338509286));
#393967=CARTESIAN_POINT('Origin',(-2.09750205887831,1.67269842573215,7.5848687342762));
#393968=CARTESIAN_POINT('Ctrl Pts',(-2.1185486795459,1.75475929151862,7.51098857897448));
#393969=CARTESIAN_POINT('Ctrl Pts',(-2.11626052846282,1.74933482135161,
7.50433767179956));
#393970=CARTESIAN_POINT('Ctrl Pts',(-2.1232362787878,1.74429032350881,7.50214974420965));
#393971=CARTESIAN_POINT('Ctrl Pts',(-2.1063054611613,1.72573455911939,7.53887321589169));
#393972=CARTESIAN_POINT('Ctrl Pts',(-2.10404472618889,1.72037508373168,
7.53220407452062));
#393973=CARTESIAN_POINT('Ctrl Pts',(-2.11096323199479,1.71530189958991,
7.53003438070911));
#393974=CARTESIAN_POINT('Ctrl Pts',(-2.09403873128105,1.69665408852716,
7.56669465659233));
#393975=CARTESIAN_POINT('Ctrl Pts',(-2.09179135683204,1.69132628664258,
7.560040858333));
#393976=CARTESIAN_POINT('Ctrl Pts',(-2.09866600104349,1.68625914572365,
7.55785582193789));
#393977=CARTESIAN_POINT('Ctrl Pts',(-2.08174904468027,1.66751919493523,
7.59443891967696));
#393978=CARTESIAN_POINT('Ctrl Pts',(-2.07949841181813,1.66218366840124,
7.58783901202978));
#393979=CARTESIAN_POINT('Ctrl Pts',(-2.08634511706894,1.65716352844335,
7.58560008491213));
#393980=CARTESIAN_POINT('',(-2.12257099619414,1.74271895653111,7.50366116523517));
#393981=CARTESIAN_POINT('Ctrl Pts',(-2.12257099619443,1.74271895653135,
7.50366116523554));
#393982=CARTESIAN_POINT('Ctrl Pts',(-2.1222181569283,1.74338951001098,7.50350835821027));
#393983=CARTESIAN_POINT('Ctrl Pts',(-2.12187199624793,1.74399443215019,
7.50345484956));
#393984=CARTESIAN_POINT('Ctrl Pts',(-2.121522743714,1.74455200602684,7.50349758195598));
#393985=CARTESIAN_POINT('Ctrl Pts',(-2.12134355126285,1.74483808277632,
7.50351950684424));
#393986=CARTESIAN_POINT('Ctrl Pts',(-2.12114599266841,1.74513996091748,
7.50357029184312));
#393987=CARTESIAN_POINT('Ctrl Pts',(-2.12094748749189,1.74542582197775,
7.50365515313924));
#393988=CARTESIAN_POINT('Ctrl Pts',(-2.12064210614772,1.74586559204503,
7.50378570417639));
#393989=CARTESIAN_POINT('Ctrl Pts',(-2.12032580549605,1.74628056165417,
7.50400001621911));
#393990=CARTESIAN_POINT('Ctrl Pts',(-2.12002085492926,1.74663776925506,
7.50428903009634));
#393991=CARTESIAN_POINT('Ctrl Pts',(-2.11998700776249,1.74667741655057,
7.50432110841318));
#393992=CARTESIAN_POINT('Ctrl Pts',(-2.11995329730374,1.74671638241371,
7.50435406373354));
#393993=CARTESIAN_POINT('Ctrl Pts',(-2.11991975139973,1.74675464400066,
7.50438785222352));
#393994=CARTESIAN_POINT('Ctrl Pts',(-2.11971493753151,1.74698824937983,
7.50459414719561));
#393995=CARTESIAN_POINT('Ctrl Pts',(-2.11951260910298,1.7471989807573,7.50483629897752));
#393996=CARTESIAN_POINT('Ctrl Pts',(-2.11932146656588,1.74737967653143,
7.5050991045531));
#393997=CARTESIAN_POINT('Ctrl Pts',(-2.11889978693057,1.74777830955833,
7.50567888004914));
#393998=CARTESIAN_POINT('Ctrl Pts',(-2.11851628850651,1.7480468494336,7.50637912803144));
#393999=CARTESIAN_POINT('Ctrl Pts',(-2.11818147603024,1.74821436622547,
7.50710440483569));
#394000=CARTESIAN_POINT('Ctrl Pts',(-2.11809937336411,1.74825544466851,
7.50728225710685));
#394001=CARTESIAN_POINT('Ctrl Pts',(-2.11801862920969,1.74829139658336,
7.50746498566954));
#394002=CARTESIAN_POINT('Ctrl Pts',(-2.11794129784965,1.74832176330878,
7.50764697238949));
#394003=CARTESIAN_POINT('Ctrl Pts',(-2.11752558574022,1.74848500646746,
7.50862528291181));
#394004=CARTESIAN_POINT('Ctrl Pts',(-2.11717227348488,1.74850551793847,
7.50965856837421));
#394005=CARTESIAN_POINT('Ctrl Pts',(-2.11686727706472,1.74844808225896,
7.51067959873201));
#394006=CARTESIAN_POINT('Ctrl Pts',(-2.11669943715,1.74841647533207,7.51124147302577));
#394007=CARTESIAN_POINT('Ctrl Pts',(-2.11654626822341,1.74836082893676,
7.51180065547252));
#394008=CARTESIAN_POINT('Ctrl Pts',(-2.11640602292632,1.74828929035805,
7.512351757165));
#394009=CARTESIAN_POINT('Ctrl Pts',(-2.11592141955782,1.74804209607103,
7.51425603304536));
#394010=CARTESIAN_POINT('Ctrl Pts',(-2.11553609727353,1.74757027707513,
7.51626900505181));
#394011=CARTESIAN_POINT('Ctrl Pts',(-2.11524938375525,1.74693418413988,
7.51827788969245));
#394012=CARTESIAN_POINT('Ctrl Pts',(-2.11523386627782,1.74689975758818,
7.51838661432546));
#394013=CARTESIAN_POINT('Ctrl Pts',(-2.11521864057722,1.7468648403287,7.51849533314857));
#394014=CARTESIAN_POINT('Ctrl Pts',(-2.11520370755653,1.74682943894029,
7.51860402984325));
#394015=CARTESIAN_POINT('Ctrl Pts',(-2.09059128339321,1.66719091666629,
7.57603338728985));
#394016=CARTESIAN_POINT('Ctrl Pts',(-2.10126987185163,1.69240886705185,
7.55196141284922));
#394017=CARTESIAN_POINT('Ctrl Pts',(-2.11192925636356,1.71758369907427,
7.52783573083105));
#394018=CARTESIAN_POINT('Ctrl Pts',(-2.12257099621211,1.7427189565875,7.50366116530176));
#394019=CARTESIAN_POINT('Origin',(-7.22395927215202E-16,5.76091528191151E-16,
7.49482233047033));
#394020=CARTESIAN_POINT('Origin',(-2.16435357359295,1.6761503090342,7.49482233047033));
#394021=CARTESIAN_POINT('Origin',(0.,0.,7.50366116523517));
#394022=CARTESIAN_POINT('Origin',(-2.11573969989723,1.73711017850878,7.49482233047033));
#394023=CARTESIAN_POINT('Ctrl Pts',(-2.17370884075826,1.67346483226478,
7.51860402984325));
#394024=CARTESIAN_POINT('Ctrl Pts',(-2.18120177269762,1.67478856070455,
7.51860402984325));
#394025=CARTESIAN_POINT('Ctrl Pts',(-2.18581900259086,1.66874062931084,
7.51860402984325));
#394026=CARTESIAN_POINT('Ctrl Pts',(-2.17649101774283,1.67395634041671,
7.51041458714366));
#394027=CARTESIAN_POINT('Ctrl Pts',(-2.18229563947574,1.6733557304783,7.51004642900443));
#394028=CARTESIAN_POINT('Ctrl Pts',(-2.18582027596804,1.66873896136317,
7.5072913648301));
#394029=CARTESIAN_POINT('Ctrl Pts',(-2.17698761422762,1.67672710369252,
7.50215815450137));
#394030=CARTESIAN_POINT('Ctrl Pts',(-2.18006852915933,1.67627320098812,
7.49877163671529));
#394031=CARTESIAN_POINT('Ctrl Pts',(-2.18218107690715,1.67354536932039,
7.4948158853317));
#394032=CARTESIAN_POINT('Ctrl Pts',(-2.17134139901513,1.68156192286896,
7.50366171572174));
#394033=CARTESIAN_POINT('Ctrl Pts',(-2.17423646662282,1.68380396341366,
7.50000045605858));
#394034=CARTESIAN_POINT('Ctrl Pts',(-2.17423646662289,1.68380396341356,
7.49482233047317));
#394035=CARTESIAN_POINT('Origin',(-2.17588346166999,1.66115544463215,7.51860402984325));
#394036=CARTESIAN_POINT('Origin',(-2.17588346166999,1.66115544463215,9.));
#394037=CARTESIAN_POINT('Origin',(-2.17588346166999,1.66115544463215,8.75721825406948));
#394038=CARTESIAN_POINT('Ctrl Pts',(-2.15726414129913,1.67056105650535,
8.78942910404913));
#394039=CARTESIAN_POINT('Ctrl Pts',(-2.16274816930574,1.6715499273384,8.79672699501691));
#394040=CARTESIAN_POINT('Ctrl Pts',(-2.16591835071273,1.66320586143329,
8.79893251111267));
#394041=CARTESIAN_POINT('Ctrl Pts',(-2.16809098556717,1.67247282582632,
8.78111911759582));
#394042=CARTESIAN_POINT('Ctrl Pts',(-2.17459368527152,1.67363781796381,
8.78644465894813));
#394043=CARTESIAN_POINT('Ctrl Pts',(-2.1790310498719,1.66685362256725,8.78817647674131));
#394044=CARTESIAN_POINT('Ctrl Pts',(-2.17483853316512,1.67366428603581,
8.76780923932031));
#394045=CARTESIAN_POINT('Ctrl Pts',(-2.18251559422621,1.67503449413488,
8.76988516158375));
#394046=CARTESIAN_POINT('Ctrl Pts',(-2.1872240108512,1.66912118767556,8.77093053738833));
#394047=CARTESIAN_POINT('Ctrl Pts',(-2.17352285373051,1.67343196759953,
8.75371302330491));
#394048=CARTESIAN_POINT('Ctrl Pts',(-2.18101136169898,1.67476929694336,
8.75300828287559));
#394049=CARTESIAN_POINT('Ctrl Pts',(-2.18562617275779,1.66867847940992,
8.75267964240737));
#394050=CARTESIAN_POINT('Origin',(-2.16207450435389,1.65871710925137,8.78727029226991));
#394051=CARTESIAN_POINT('Ctrl Pts',(-2.08949760778589,1.65859511954945,
8.85049129520029));
#394052=CARTESIAN_POINT('Ctrl Pts',(-2.09524826125082,1.6596105489903,8.85711686593484));
#394053=CARTESIAN_POINT('Ctrl Pts',(-2.09861675793329,1.65175217815315,
8.85933012996512));
#394054=CARTESIAN_POINT('Ctrl Pts',(-2.11299952442463,1.66274500237874,
8.82945683644724));
#394055=CARTESIAN_POINT('Ctrl Pts',(-2.11879791179024,1.66376886049789,
8.8360746990239));
#394056=CARTESIAN_POINT('Ctrl Pts',(-2.12214182911504,1.65587264245237,
8.8382956714852));
#394057=CARTESIAN_POINT('Ctrl Pts',(-2.1364664095614,1.66688869947303,8.80838214965002));
#394058=CARTESIAN_POINT('Ctrl Pts',(-2.14228768007071,1.66791659821434,
8.81501364461985));
#394059=CARTESIAN_POINT('Ctrl Pts',(-2.14563109864249,1.6599875147333,8.81722098428721));
#394060=CARTESIAN_POINT('Ctrl Pts',(-2.15990092504105,1.67102668085117,
8.78727029226991));
#394061=CARTESIAN_POINT('Ctrl Pts',(-2.16572316248257,1.67205475032985,
8.79393457792714));
#394062=CARTESIAN_POINT('Ctrl Pts',(-2.1690872949448,1.66409723639931,8.79610912703474));
#394063=CARTESIAN_POINT('Origin',(-2.09167118709872,1.64628554794964,8.85049129520029));
#394064=CARTESIAN_POINT('Ctrl Pts',(-2.08196763624131,1.66803740521007,
8.85049129520029));
#394065=CARTESIAN_POINT('Ctrl Pts',(-2.08423724752592,1.67341792347878,
8.85711686593484));
#394066=CARTESIAN_POINT('Ctrl Pts',(-2.07732546348033,1.67845061693467,
8.85933012996512));
#394067=CARTESIAN_POINT('Ctrl Pts',(-2.0799597439,1.66327733836635,8.86332496987233));
#394068=CARTESIAN_POINT('Ctrl Pts',(-2.07730478957506,1.66705928388543,
8.86648636486738));
#394069=CARTESIAN_POINT('Ctrl Pts',(-2.07172408849992,1.66512747711384,
8.87206031107457));
#394070=CARTESIAN_POINT('Ctrl Pts',(-2.08437551637401,1.65769067930626,
8.86341338519875));
#394071=CARTESIAN_POINT('Ctrl Pts',(-2.08745862058333,1.654231208383,8.86654584966058));
#394072=CARTESIAN_POINT('Ctrl Pts',(-2.08427206792284,1.64923420578852,
8.87215952290715));
#394073=CARTESIAN_POINT('Ctrl Pts',(-2.08949760778589,1.65859511954945,
8.85049129520029));
#394074=CARTESIAN_POINT('Ctrl Pts',(-2.09524826125082,1.6596105489903,8.85711686593484));
#394075=CARTESIAN_POINT('Ctrl Pts',(-2.09861675793329,1.65175217815315,
8.85933012996512));
#394076=CARTESIAN_POINT('Origin',(-2.07045035820038,1.67289562572049,8.85049129520029));
#394077=CARTESIAN_POINT('Ctrl Pts',(-2.10975372425561,1.73390928168093,
8.78727029226991));
#394078=CARTESIAN_POINT('Ctrl Pts',(-2.11205158759923,1.73935677649345,
8.79393457792714));
#394079=CARTESIAN_POINT('Ctrl Pts',(-2.10504217505422,1.74440727656295,
8.79610912703474));
#394080=CARTESIAN_POINT('Ctrl Pts',(-2.10050482043861,1.71198310591231,
8.80838214965002));
#394081=CARTESIAN_POINT('Ctrl Pts',(-2.10280230216296,1.71742969602831,
8.81501364461987));
#394082=CARTESIAN_POINT('Ctrl Pts',(-2.09581599798247,1.72245367517763,
8.81722098428721));
#394083=CARTESIAN_POINT('Ctrl Pts',(-2.09124314128409,1.69002664392797,
8.82945683644723));
#394084=CARTESIAN_POINT('Ctrl Pts',(-2.0935315917146,1.69545182375143,8.8360746990239));
#394085=CARTESIAN_POINT('Ctrl Pts',(-2.08657743994753,1.70046897590163,
8.8382956714852));
#394086=CARTESIAN_POINT('Ctrl Pts',(-2.08196763624131,1.66803740521007,
8.85049129520029));
#394087=CARTESIAN_POINT('Ctrl Pts',(-2.08423724752592,1.67341792347878,
8.85711686593484));
#394088=CARTESIAN_POINT('Ctrl Pts',(-2.07732546348033,1.67845061693467,
8.85933012996512));
#394089=CARTESIAN_POINT('Origin',(-2.09823644621467,1.73876750219135,8.78727029226991));
#394090=CARTESIAN_POINT('Ctrl Pts',(-2.11513172627181,1.74665884193264,
8.75374538247847));
#394091=CARTESIAN_POINT('Ctrl Pts',(-2.1180972113991,1.75365528934167,8.75304829418601));
#394092=CARTESIAN_POINT('Ctrl Pts',(-2.11319554002148,1.75950714895337,
8.75272238421917));
#394093=CARTESIAN_POINT('Ctrl Pts',(-2.11564474840764,1.74787505129053,
8.76769408445022));
#394094=CARTESIAN_POINT('Ctrl Pts',(-2.11868422291034,1.75504782967271,
8.7697431809397));
#394095=CARTESIAN_POINT('Ctrl Pts',(-2.11397434055921,1.76094997890146,
8.7707786988043));
#394096=CARTESIAN_POINT('Ctrl Pts',(-2.1130152892024,1.74164145494498,8.78108014887987));
#394097=CARTESIAN_POINT('Ctrl Pts',(-2.11559463262246,1.74771864383638,
8.78639403366323));
#394098=CARTESIAN_POINT('Ctrl Pts',(-2.10999049148816,1.75355950660449,
8.78812224174741));
#394099=CARTESIAN_POINT('Ctrl Pts',(-2.10870618599169,1.73142596662879,
8.78944554828686));
#394100=CARTESIAN_POINT('Ctrl Pts',(-2.11088511381239,1.73654540909543,
8.79673892988686));
#394101=CARTESIAN_POINT('Ctrl Pts',(-2.10346504981594,1.74148971942198,
8.79894799272499));
#394102=CARTESIAN_POINT('Origin',(-2.1036864295156,1.75168765945071,8.75721825406948));
#394103=CARTESIAN_POINT('Origin',(-2.1036864295156,1.75168765945071,9.));
#394104=CARTESIAN_POINT('Origin',(-2.1036864295156,1.75168765945071,7.51860402984325));
#394105=CARTESIAN_POINT('Ctrl Pts',(-2.12257038820296,1.74271845734518,
7.50366195182966));
#394106=CARTESIAN_POINT('Ctrl Pts',(-2.12540061176882,1.74504218845641,
7.50000065167735));
#394107=CARTESIAN_POINT('Ctrl Pts',(-2.12540061176874,1.7450421884565,7.49482233047108));
#394108=CARTESIAN_POINT('Ctrl Pts',(-2.11910931730508,1.74930441117484,
7.50215800491336));
#394109=CARTESIAN_POINT('Ctrl Pts',(-2.11935109582765,1.75241025088745,
7.49877273257265));
#394110=CARTESIAN_POINT('Ctrl Pts',(-2.11716053191478,1.7550783187452,7.49481816995649));
#394111=CARTESIAN_POINT('Ctrl Pts',(-2.1162994847363,1.74942630160733,7.51043025814042));
#394112=CARTESIAN_POINT('Ctrl Pts',(-2.11700967300595,1.75522185072787,
7.51006209594514));
#394113=CARTESIAN_POINT('Ctrl Pts',(-2.11329068351776,1.75968817890087,
7.50731281821698));
#394114=CARTESIAN_POINT('Ctrl Pts',(-2.11520312005229,1.74682804639183,
7.51860402984325));
#394115=CARTESIAN_POINT('Ctrl Pts',(-2.11816136938257,1.75383873667814,
7.51860402984324));
#394116=CARTESIAN_POINT('Ctrl Pts',(-2.11329230362298,1.75968623323816,
7.51860402984325));
#394117=CARTESIAN_POINT('Origin',(0.,0.,7.5));
#394118=CARTESIAN_POINT('Origin',(-2.18456153393019,1.53121811901791,7.5));
#394119=CARTESIAN_POINT('',(-2.18456153393019,1.53121811901791,7.59394543036555));
#394120=CARTESIAN_POINT('',(-2.18456153393019,1.53121811901791,8.85049129520029));
#394121=CARTESIAN_POINT('',(-2.18456153393019,1.53121811901791,7.5));
#394122=CARTESIAN_POINT('',(-2.21651095806264,1.59517439388234,8.78727029226991));
#394123=CARTESIAN_POINT('Ctrl Pts',(-2.18456153393019,1.53121811901791,
8.85049129520029));
#394124=CARTESIAN_POINT('Ctrl Pts',(-2.19522682250171,1.55256786618584,
8.82945686509571));
#394125=CARTESIAN_POINT('Ctrl Pts',(-2.20587625583214,1.57388587437302,
8.80838212259895));
#394126=CARTESIAN_POINT('Ctrl Pts',(-2.21651095806264,1.59517439388234,
8.78727029226991));
#394127=CARTESIAN_POINT('',(-2.22277754110617,1.60771882366395,8.75721825406948));
#394128=CARTESIAN_POINT('Origin',(-2.20391939936566,1.56996819257471,8.75937679713137));
#394129=CARTESIAN_POINT('',(-2.22277754110617,1.60771882366395,7.51860402984325));
#394130=CARTESIAN_POINT('',(-2.22277754110617,1.60771882366395,7.5));
#394131=CARTESIAN_POINT('Ctrl Pts',(-2.22277754110617,1.60771882366395,
7.51860402984325));
#394132=CARTESIAN_POINT('Ctrl Pts',(-2.2178561147635,1.59786712509837,7.52834476460825));
#394133=CARTESIAN_POINT('Ctrl Pts',(-2.21293149350187,1.58800903095223,
7.53807742314407));
#394134=CARTESIAN_POINT('Ctrl Pts',(-2.20800357004761,1.57814432648542,
7.54780169004674));
#394135=CARTESIAN_POINT('Ctrl Pts',(-2.20019800562761,1.56251916775178,
7.5632044032688));
#394136=CARTESIAN_POINT('Ctrl Pts',(-2.19238414650716,1.54687740470821,
7.57858609112103));
#394137=CARTESIAN_POINT('Ctrl Pts',(-2.18456153393019,1.53121811901791,
7.59394543036555));
#394138=CARTESIAN_POINT('Origin',(-2.46478898834976,1.55168238962918,7.5));
#394139=CARTESIAN_POINT('',(-2.2764630339942,1.53075663254068,8.75721825406948));
#394140=CARTESIAN_POINT('',(-2.26252622397768,1.52920804991439,8.78727029226991));
#394141=CARTESIAN_POINT('Origin',(-2.22714940198531,1.5252771696164,8.75658640621067));
#394142=CARTESIAN_POINT('',(-2.19147106502124,1.52131278661255,8.85049129520029));
#394143=CARTESIAN_POINT('Ctrl Pts',(-2.26252622397768,1.52920804991439,
8.78727029226991));
#394144=CARTESIAN_POINT('Ctrl Pts',(-2.2388747661514,1.52658002839205,8.80838212259895));
#394145=CARTESIAN_POINT('Ctrl Pts',(-2.21519054652501,1.52394836655644,
8.82945686509571));
#394146=CARTESIAN_POINT('Ctrl Pts',(-2.19147106502124,1.52131278661255,
8.85049129520029));
#394147=CARTESIAN_POINT('',(-2.19147106502124,1.52131278661255,7.59394543036555));
#394148=CARTESIAN_POINT('',(-2.19147106502124,1.52131278661255,7.5));
#394149=CARTESIAN_POINT('',(-2.2764630339942,1.53075663254068,7.51860402984325));
#394150=CARTESIAN_POINT('Ctrl Pts',(-2.19147106502124,1.52131278661255,
7.59394543036555));
#394151=CARTESIAN_POINT('Ctrl Pts',(-2.2088684671718,1.52324589143933,7.57858609112103));
#394152=CARTESIAN_POINT('Ctrl Pts',(-2.22624640173355,1.52517683313341,
7.56320440326857));
#394153=CARTESIAN_POINT('Ctrl Pts',(-2.24360588897529,1.52710572506147,
7.54780169004651));
#394154=CARTESIAN_POINT('Ctrl Pts',(-2.25456553516221,1.52832350141454,
7.53807742314383));
#394155=CARTESIAN_POINT('Ctrl Pts',(-2.26551783731018,1.52954046173788,
7.52834476460825));
#394156=CARTESIAN_POINT('Ctrl Pts',(-2.2764630339942,1.53075663254068,7.51860402984325));
#394157=CARTESIAN_POINT('',(-2.2764630339942,1.53075663254068,7.5));
#394158=CARTESIAN_POINT('Origin',(-2.19071182494583,1.52814573469576,7.5));
#394159=CARTESIAN_POINT('Ctrl Pts',(-2.19147106502124,1.52131278661255,
8.85049129520029));
#394160=CARTESIAN_POINT('Ctrl Pts',(-2.19127858807352,1.52129139961963,
8.85097269580138));
#394161=CARTESIAN_POINT('Ctrl Pts',(-2.19108761066503,1.52127864242607,
8.85143669361005));
#394162=CARTESIAN_POINT('Ctrl Pts',(-2.19088928063141,1.52127479994583,
8.8519052845931));
#394163=CARTESIAN_POINT('Ctrl Pts',(-2.19050135966328,1.52126728429815,
8.85282181883899));
#394164=CARTESIAN_POINT('Ctrl Pts',(-2.19009528511055,1.52129426370403,
8.85372622499636));
#394165=CARTESIAN_POINT('Ctrl Pts',(-2.18966570712695,1.5213715463367,8.85462257735071));
#394166=CARTESIAN_POINT('Ctrl Pts',(-2.18930908674213,1.52143570363352,
8.85536669723986));
#394167=CARTESIAN_POINT('Ctrl Pts',(-2.18893618151325,1.5215345120831,8.85610498449051));
#394168=CARTESIAN_POINT('Ctrl Pts',(-2.18854594865093,1.52168476007642,
8.85681338218371));
#394169=CARTESIAN_POINT('Ctrl Pts',(-2.1881918117155,1.52182111036632,8.85745625420284));
#394170=CARTESIAN_POINT('Ctrl Pts',(-2.18781874712325,1.52200097601188,
8.85808743050666));
#394171=CARTESIAN_POINT('Ctrl Pts',(-2.18742683720687,1.52225295490408,
8.85866804508411));
#394172=CARTESIAN_POINT('Ctrl Pts',(-2.18724601846702,1.5223692125027,8.85893592806396));
#394173=CARTESIAN_POINT('Ctrl Pts',(-2.1870612177365,1.52250106139575,8.85919241173848));
#394174=CARTESIAN_POINT('Ctrl Pts',(-2.18687285743162,1.52265285170287,
8.85943017985534));
#394175=CARTESIAN_POINT('Ctrl Pts',(-2.18661851525942,1.52285781355222,
8.8597512372));
#394176=CARTESIAN_POINT('Ctrl Pts',(-2.18635161117297,1.52310485014259,
8.86004599534705));
#394177=CARTESIAN_POINT('Ctrl Pts',(-2.18608242652933,1.52339863699004,
8.86026130871721));
#394178=CARTESIAN_POINT('Ctrl Pts',(-2.18598387044218,1.52350620063762,
8.86034014101235));
#394179=CARTESIAN_POINT('Ctrl Pts',(-2.1858835191395,1.52362163854734,8.86040910639693));
#394180=CARTESIAN_POINT('Ctrl Pts',(-2.18578436050156,1.52374202636577,
8.86046313645507));
#394181=CARTESIAN_POINT('Ctrl Pts',(-2.18562962427748,1.52392989054819,
8.8605474499083));
#394182=CARTESIAN_POINT('Ctrl Pts',(-2.18547368201656,1.52413503003229,
8.86059655985668));
#394183=CARTESIAN_POINT('Ctrl Pts',(-2.18532630154896,1.52434411130868,
8.86059725258815));
#394184=CARTESIAN_POINT('Ctrl Pts',(-2.18517858057361,1.52455367564636,
8.86059794692011));
#394185=CARTESIAN_POINT('Ctrl Pts',(-2.18503999426282,1.52477105478739,
8.86056369958366));
#394186=CARTESIAN_POINT('Ctrl Pts',(-2.18491492808122,1.52498236981287,
8.86048590497774));
#394187=CARTESIAN_POINT('Ctrl Pts',(-2.18488228953149,1.52503751674292,
8.86046560290182));
#394188=CARTESIAN_POINT('Ctrl Pts',(-2.18485022511722,1.52509301423803,
8.86044257503091));
#394189=CARTESIAN_POINT('Ctrl Pts',(-2.18481969723213,1.52514713095779,
8.86041778462583));
#394190=CARTESIAN_POINT('Ctrl Pts',(-2.18461428244746,1.52551126932848,
8.86025097596201));
#394191=CARTESIAN_POINT('Ctrl Pts',(-2.18445116098595,1.52586191704487,
8.8599848982295));
#394192=CARTESIAN_POINT('Ctrl Pts',(-2.18432741199719,1.52618526598102,
8.85968173251461));
#394193=CARTESIAN_POINT('Ctrl Pts',(-2.18426195587211,1.52635629904256,
8.85952137522076));
#394194=CARTESIAN_POINT('Ctrl Pts',(-2.18420607533321,1.52652292297257,
8.85934740853961));
#394195=CARTESIAN_POINT('Ctrl Pts',(-2.18415908454449,1.52668229371294,
8.8591675900182));
#394196=CARTESIAN_POINT('Ctrl Pts',(-2.18397039210246,1.52732225007481,
8.85844552518694));
#394197=CARTESIAN_POINT('Ctrl Pts',(-2.18391147471058,1.52788056619923,
8.85759444184121));
#394198=CARTESIAN_POINT('Ctrl Pts',(-2.18390432493829,1.52834010198268,
8.85683498915135));
#394199=CARTESIAN_POINT('Ctrl Pts',(-2.18390357673366,1.52838819117857,
8.85675551444995));
#394200=CARTESIAN_POINT('Ctrl Pts',(-2.18390341508026,1.52843519502018,
8.8566769979365));
#394201=CARTESIAN_POINT('Ctrl Pts',(-2.18390376336044,1.52848109083085,
8.85659965593547));
#394202=CARTESIAN_POINT('Ctrl Pts',(-2.18390846446407,1.52910059482535,
8.85555568965886));
#394203=CARTESIAN_POINT('Ctrl Pts',(-2.18400245115094,1.52969529761315,
8.85434650606346));
#394204=CARTESIAN_POINT('Ctrl Pts',(-2.18418004948775,1.53026910920421,
8.85297329937117));
#394205=CARTESIAN_POINT('Ctrl Pts',(-2.18427993773097,1.53059184326133,
8.85220095427747));
#394206=CARTESIAN_POINT('Ctrl Pts',(-2.18440661731194,1.53090800733086,
8.85137579139183));
#394207=CARTESIAN_POINT('Ctrl Pts',(-2.18456153393019,1.53121811901791,
8.85049129520029));
#394208=CARTESIAN_POINT('Origin',(-2.19071182494583,1.52814573469576,7.59394543036555));
#394209=CARTESIAN_POINT('Ctrl Pts',(-2.1909122395105,1.52125069295726,7.59443877723642));
#394210=CARTESIAN_POINT('Ctrl Pts',(-2.18515687443731,1.52061118805264,
7.58783886950016));
#394211=CARTESIAN_POINT('Ctrl Pts',(-2.18229230418495,1.52860327281232,
7.58559994247159));
#394212=CARTESIAN_POINT('Ctrl Pts',(-2.22233060858978,1.52474173146929,
7.56670252222134));
#394213=CARTESIAN_POINT('Ctrl Pts',(-2.21658356165307,1.52410315083086,
7.56004874999022));
#394214=CARTESIAN_POINT('Ctrl Pts',(-2.2136819051509,1.53213538257546,7.55786368756704));
#394215=CARTESIAN_POINT('Ctrl Pts',(-2.25369030700392,1.52822625081569,
7.53888913333559));
#394216=CARTESIAN_POINT('Ctrl Pts',(-2.24790910508591,1.52758387506124,
7.53222002137278));
#394217=CARTESIAN_POINT('Ctrl Pts',(-2.24501413171015,1.53565986254721,
7.53005029815326));
#394218=CARTESIAN_POINT('Ctrl Pts',(-2.28498991570528,1.53170409331962,
7.51101258149734));
#394219=CARTESIAN_POINT('Ctrl Pts',(-2.27913863511532,1.53105393080378,
7.5043616886572));
#394220=CARTESIAN_POINT('Ctrl Pts',(-2.27628742657589,1.53917662071595,
7.50217374673251));
#394221=CARTESIAN_POINT('',(-2.27461864350412,1.53898896096136,7.50366116523517));
#394222=CARTESIAN_POINT('Ctrl Pts',(-2.2764630339942,1.53075663254068,7.51860402984325));
#394223=CARTESIAN_POINT('Ctrl Pts',(-2.27690194403194,1.53080540183998,
7.51734760759494));
#394224=CARTESIAN_POINT('Ctrl Pts',(-2.27729199148657,1.530908604762,7.51608817408573));
#394225=CARTESIAN_POINT('Ctrl Pts',(-2.27762886352539,1.53107891334169,
7.5148100591312));
#394226=CARTESIAN_POINT('Ctrl Pts',(-2.27793401026797,1.53123318292284,
7.51365231206384));
#394227=CARTESIAN_POINT('Ctrl Pts',(-2.27819606868181,1.53144250802905,
7.51247773061043));
#394228=CARTESIAN_POINT('Ctrl Pts',(-2.27838745892557,1.53173211745978,
7.51129758471022));
#394229=CARTESIAN_POINT('Ctrl Pts',(-2.27862533514097,1.53209206890753,
7.50983079813402));
#394230=CARTESIAN_POINT('Ctrl Pts',(-2.27873558770847,1.53257173404272,
7.50839324291155));
#394231=CARTESIAN_POINT('Ctrl Pts',(-2.27863867677662,1.53319308108103,
7.50715379678855));
#394232=CARTESIAN_POINT('Ctrl Pts',(-2.27859390671852,1.53348012550905,
7.50658120839351));
#394233=CARTESIAN_POINT('Ctrl Pts',(-2.27848917168155,1.53383674900996,
7.50598221009429));
#394234=CARTESIAN_POINT('Ctrl Pts',(-2.27830513945913,1.53424805484198,
7.50545747549611));
#394235=CARTESIAN_POINT('Ctrl Pts',(-2.27820693416891,1.53446754036505,
7.50517746087247));
#394236=CARTESIAN_POINT('Ctrl Pts',(-2.27808526799904,1.53470506004889,
7.50491486231392));
#394237=CARTESIAN_POINT('Ctrl Pts',(-2.27794187829259,1.53495356351543,
7.50468370960992));
#394238=CARTESIAN_POINT('Ctrl Pts',(-2.27772746545172,1.53532515458389,
7.50433806340446));
#394239=CARTESIAN_POINT('Ctrl Pts',(-2.27745756787721,1.53573216943126,
7.50405484070983));
#394240=CARTESIAN_POINT('Ctrl Pts',(-2.27714976561519,1.53614680044923,
7.5038576603613));
#394241=CARTESIAN_POINT('Ctrl Pts',(-2.2771168509476,1.53619113879177,7.5038365749879));
#394242=CARTESIAN_POINT('Ctrl Pts',(-2.27708352897817,1.53623555321376,
7.50381643264937));
#394243=CARTESIAN_POINT('Ctrl Pts',(-2.27704984031696,1.53628000200858,
7.50379723213559));
#394244=CARTESIAN_POINT('Ctrl Pts',(-2.27682495748309,1.53657671225428,
7.50366906242519));
#394245=CARTESIAN_POINT('Ctrl Pts',(-2.27657827008934,1.53688097395988,
7.50358235568538));
#394246=CARTESIAN_POINT('Ctrl Pts',(-2.2763334441752,1.53716852914519,7.5035341175365));
#394247=CARTESIAN_POINT('Ctrl Pts',(-2.27596635542588,1.5375996856006,7.50346178989176));
#394248=CARTESIAN_POINT('Ctrl Pts',(-2.27555311919225,1.53804790364341,
7.50346967198526));
#394249=CARTESIAN_POINT('Ctrl Pts',(-2.27513391008214,1.53847543241701,
7.50354272648692));
#394250=CARTESIAN_POINT('Ctrl Pts',(-2.27496148069803,1.53865128385091,
7.50357277531559));
#394251=CARTESIAN_POINT('Ctrl Pts',(-2.27478837114252,1.53882350060341,
7.50361331098761));
#394252=CARTESIAN_POINT('Ctrl Pts',(-2.2746186435053,1.53898896096215,7.50366116523658));
#394253=CARTESIAN_POINT('',(-2.19311322794402,1.52982084947248,7.57603338622103));
#394254=CARTESIAN_POINT('Origin',(-2.20035940734066,1.53487894928966,7.58486873427627));
#394255=CARTESIAN_POINT('Ctrl Pts',(-2.27461864356146,1.53898896096242,
7.50366116529969));
#394256=CARTESIAN_POINT('Ctrl Pts',(-2.24749441162106,1.53593874122536,
7.52783573079709));
#394257=CARTESIAN_POINT('Ctrl Pts',(-2.2203272205278,1.5328828661625,7.55196141284068));
#394258=CARTESIAN_POINT('Ctrl Pts',(-2.1931132291771,1.52982084925532,7.57603338728831));
#394259=CARTESIAN_POINT('Ctrl Pts',(-2.19147106502124,1.52131278661255,
7.59394543036555));
#394260=CARTESIAN_POINT('Ctrl Pts',(-2.1789164401766,1.51991778489473,7.59394543036555));
#394261=CARTESIAN_POINT('Ctrl Pts',(-2.18456153393019,1.53121811901791,
7.59394543036555));
#394262=CARTESIAN_POINT('Ctrl Pts',(-2.18915221929748,1.52105512907136,
7.58587155981958));
#394263=CARTESIAN_POINT('Ctrl Pts',(-2.18371352266056,1.52326402197318,
7.58685956158229));
#394264=CARTESIAN_POINT('Ctrl Pts',(-2.1835188821845,1.52913094144129,7.58587155981959));
#394265=CARTESIAN_POINT('Ctrl Pts',(-2.19108705088142,1.5260901058675,7.57982961904599));
#394266=CARTESIAN_POINT('Ctrl Pts',(-2.18864592315195,1.52670465103599,
7.58148017275034));
#394267=CARTESIAN_POINT('Ctrl Pts',(-2.18891227212867,1.52920781474972,
7.57982961904595));
#394268=CARTESIAN_POINT('Ctrl Pts',(-2.19311322726539,1.52982084899885,
7.57603338509286));
#394269=CARTESIAN_POINT('Ctrl Pts',(-2.19311322726539,1.52982084899885,
7.57603338509286));
#394270=CARTESIAN_POINT('Ctrl Pts',(-2.19311322726539,1.52982084899885,
7.57603338509286));
#394271=CARTESIAN_POINT('Origin',(-2.20036267203999,1.53487426909781,7.5848687342762));
#394272=CARTESIAN_POINT('Ctrl Pts',(-2.22662370789094,1.6154180704185,7.51098857897448));
#394273=CARTESIAN_POINT('Ctrl Pts',(-2.22399271106278,1.61015134775046,
7.50433767179957));
#394274=CARTESIAN_POINT('Ctrl Pts',(-2.23063092687409,1.60467027651165,
7.50214974420965));
#394275=CARTESIAN_POINT('Ctrl Pts',(-2.21254602352188,1.58723739814004,
7.53887321589168));
#394276=CARTESIAN_POINT('Ctrl Pts',(-2.2099465507049,1.5820337801563,7.53220407452062));
#394277=CARTESIAN_POINT('Ctrl Pts',(-2.21652580167462,1.57652774922654,
7.53003438070912));
#394278=CARTESIAN_POINT('Ctrl Pts',(-2.19844130480579,1.55900260857537,
7.5666946565923));
#394279=CARTESIAN_POINT('Ctrl Pts',(-2.19585719438986,1.55382974300644,
7.56004085833292));
#394280=CARTESIAN_POINT('Ctrl Pts',(-2.20239306107414,1.54833255310514,
7.55785582193789));
#394281=CARTESIAN_POINT('Ctrl Pts',(-2.18431018964265,1.53071497867106,
7.59443891967696));
#394282=CARTESIAN_POINT('Ctrl Pts',(-2.18172233258836,1.52553461309114,
7.58783901202978));
#394283=CARTESIAN_POINT('Ctrl Pts',(-2.18823332907749,1.52008611763764,
7.58560008491213));
#394284=CARTESIAN_POINT('',(-2.22986633334694,1.60314476287806,7.50366116523517));
#394285=CARTESIAN_POINT('Ctrl Pts',(-2.22986633334724,1.60314476287828,
7.50366116523554));
#394286=CARTESIAN_POINT('Ctrl Pts',(-2.22955718153618,1.60383654512327,
7.50350835821027));
#394287=CARTESIAN_POINT('Ctrl Pts',(-2.22925048957458,1.60446240297601,
7.50345484956));
#394288=CARTESIAN_POINT('Ctrl Pts',(-2.22893767849837,1.60504120794401,
7.50349758195598));
#394289=CARTESIAN_POINT('Ctrl Pts',(-2.2287771832176,1.60533817781789,7.50351950684424));
#394290=CARTESIAN_POINT('Ctrl Pts',(-2.22859937192739,1.60565209334063,
7.50357029184312));
#394291=CARTESIAN_POINT('Ctrl Pts',(-2.22841958978206,1.60595008533902,
7.50365515313923));
#394292=CARTESIAN_POINT('Ctrl Pts',(-2.22814301204157,1.60640851770143,
7.50378570417639));
#394293=CARTESIAN_POINT('Ctrl Pts',(-2.22785394845765,1.60684290016334,
7.50400001621911));
#394294=CARTESIAN_POINT('Ctrl Pts',(-2.22757251081407,1.6072189120928,7.50428903009635));
#394295=CARTESIAN_POINT('Ctrl Pts',(-2.22754127340089,1.60726064652411,
7.50432110841318));
#394296=CARTESIAN_POINT('Ctrl Pts',(-2.22751012875531,1.60730169216422,
7.50435406373354));
#394297=CARTESIAN_POINT('Ctrl Pts',(-2.22747910320325,1.60734202443208,
7.50438785222352));
#394298=CARTESIAN_POINT('Ctrl Pts',(-2.22728967729513,1.60758827231354,
7.50459414719561));
#394299=CARTESIAN_POINT('Ctrl Pts',(-2.22710126617777,1.60781153394771,
7.50483629897752));
#394300=CARTESIAN_POINT('Ctrl Pts',(-2.2269220935815,1.60800410500739,7.5050991045531));
#394301=CARTESIAN_POINT('Ctrl Pts',(-2.22652682083796,1.60842893610698,
7.50567888004914));
#394302=CARTESIAN_POINT('Ctrl Pts',(-2.22616131576142,1.60872149506667,
7.50637912803144));
#394303=CARTESIAN_POINT('Ctrl Pts',(-2.225837924031,1.60891011918632,7.50710440483569));
#394304=CARTESIAN_POINT('Ctrl Pts',(-2.22575862195848,1.60895637356518,
7.50728225710685));
#394305=CARTESIAN_POINT('Ctrl Pts',(-2.22568034714868,1.60899742490871,
7.50746498566954));
#394306=CARTESIAN_POINT('Ctrl Pts',(-2.22560512027699,1.60903268387968,
7.50764697238949));
#394307=CARTESIAN_POINT('Ctrl Pts',(-2.22520072131776,1.60922222640408,
7.50862528291182));
#394308=CARTESIAN_POINT('Ctrl Pts',(-2.2248494491548,1.609265332526,7.50965856837422));
#394309=CARTESIAN_POINT('Ctrl Pts',(-2.22454139946587,1.60922755604198,
7.51067959873202));
#394310=CARTESIAN_POINT('Ctrl Pts',(-2.2243718793335,1.60920676759517,7.51124147302578));
#394311=CARTESIAN_POINT('Ctrl Pts',(-2.22421545983211,1.60916104909817,
7.51180065547253));
#394312=CARTESIAN_POINT('Ctrl Pts',(-2.22407091919156,1.60909864305018,
7.51235175716501));
#394313=CARTESIAN_POINT('Ctrl Pts',(-2.22357147370029,1.60888300529476,
7.51425603304536));
#394314=CARTESIAN_POINT('Ctrl Pts',(-2.2231567135551,1.6084368433851,7.51626900505181));
#394315=CARTESIAN_POINT('Ctrl Pts',(-2.22282983450621,1.60782042716919,
7.51827788969245));
#394316=CARTESIAN_POINT('Ctrl Pts',(-2.22281214319437,1.60778706555872,
7.51838661432546));
#394317=CARTESIAN_POINT('Ctrl Pts',(-2.2227947116201,1.60775319555449,7.51849533314857));
#394318=CARTESIAN_POINT('Ctrl Pts',(-2.22277754110616,1.60771882366395,
7.51860402984325));
#394319=CARTESIAN_POINT('Ctrl Pts',(-2.19311322816692,1.52982085070557,
7.57603338728985));
#394320=CARTESIAN_POINT('Ctrl Pts',(-2.20538559594875,1.55430280859583,
7.55196141284922));
#394321=CARTESIAN_POINT('Ctrl Pts',(-2.21763603663764,1.57874296711533,
7.52783573083105));
#394322=CARTESIAN_POINT('Ctrl Pts',(-2.22986633336848,1.60314476293318,
7.50366116530176));
#394323=CARTESIAN_POINT('Origin',(-7.5782199824625E-16,5.28623820391011E-16,
7.49482233047033));
#394324=CARTESIAN_POINT('Origin',(-2.26729799607037,1.53403586888159,7.49482233047033));
#394325=CARTESIAN_POINT('Origin',(0.,0.,7.50366116523517));
#394326=CARTESIAN_POINT('Origin',(-2.22268971703921,1.59798519134821,7.49482233047033));
#394327=CARTESIAN_POINT('Ctrl Pts',(-2.27646198274857,1.53075651568695,
7.51860402984325));
#394328=CARTESIAN_POINT('Ctrl Pts',(-2.28402433122797,1.53159745058702,
7.51860402984325));
#394329=CARTESIAN_POINT('Ctrl Pts',(-2.28824458223238,1.52526611838203,
7.51860402984325));
#394330=CARTESIAN_POINT('Ctrl Pts',(-2.27926993448757,1.53106875929124,
7.51041458714366));
#394331=CARTESIAN_POINT('Ctrl Pts',(-2.28502414879171,1.53009747997903,
7.51004642900442));
#394332=CARTESIAN_POINT('Ctrl Pts',(-2.2882457461275,1.52526437227578,7.50729136483009));
#394333=CARTESIAN_POINT('Ctrl Pts',(-2.2799430340742,1.53380201269071,7.50215815450138));
#394334=CARTESIAN_POINT('Ctrl Pts',(-2.28298853728963,1.53315164768069,
7.4987716367153));
#394335=CARTESIAN_POINT('Ctrl Pts',(-2.28492197180652,1.53029406923675,
7.49481588533172));
#394336=CARTESIAN_POINT('Ctrl Pts',(-2.27461818754462,1.53898865246334,
7.50366171572174));
#394337=CARTESIAN_POINT('Ctrl Pts',(-2.27765095495632,1.5410405988768,7.50000045605858));
#394338=CARTESIAN_POINT('Ctrl Pts',(-2.27765095495639,1.5410405988767,7.49482233047317));
#394339=CARTESIAN_POINT('Origin',(-2.27784347049496,1.5183330905712,7.51860402984325));
#394340=CARTESIAN_POINT('Origin',(-2.27784347049496,1.5183330905712,9.));
#394341=CARTESIAN_POINT('Origin',(-2.27784347049496,1.5183330905712,8.75721825406948));
#394342=CARTESIAN_POINT('Ctrl Pts',(-2.25986502513649,1.52891232155811,
8.78942910404912));
#394343=CARTESIAN_POINT('Ctrl Pts',(-2.2654011427912,1.52954779776922,8.79672699501689));
#394344=CARTESIAN_POINT('Ctrl Pts',(-2.26803020458242,1.52101776142228,
8.79893251111266));
#394345=CARTESIAN_POINT('Ctrl Pts',(-2.27079211197273,1.53012648465002,
8.78111911759583));
#394346=CARTESIAN_POINT('Ctrl Pts',(-2.27735609248566,1.5308724537857,8.78644465894817));
#394347=CARTESIAN_POINT('Ctrl Pts',(-2.28134967515312,1.5238178943201,8.78817647674132));
#394348=CARTESIAN_POINT('Ctrl Pts',(-2.27760213312821,1.5308831800178,8.76780923932029));
#394349=CARTESIAN_POINT('Ctrl Pts',(-2.28535121037833,1.53175870188639,
8.7698851615837));
#394350=CARTESIAN_POINT('Ctrl Pts',(-2.28967108621071,1.52555587566046,
8.77093053738832));
#394351=CARTESIAN_POINT('Ctrl Pts',(-2.27627427220477,1.53073563477546,
8.75371302330492));
#394352=CARTESIAN_POINT('Ctrl Pts',(-2.28383307721573,1.53159042607986,
8.7530082828756));
#394353=CARTESIAN_POINT('Ctrl Pts',(-2.28804816663106,1.52521645082458,
8.75267964240738));
#394354=CARTESIAN_POINT('Origin',(-2.26390666047844,1.51678450794491,8.78727029226991));
#394355=CARTESIAN_POINT('Ctrl Pts',(-2.19147106502124,1.52131278661255,
8.85049129520029));
#394356=CARTESIAN_POINT('Ctrl Pts',(-2.19727496193953,1.52195768411218,
8.85711686593484));
#394357=CARTESIAN_POINT('Ctrl Pts',(-2.20013305013607,1.51389963881728,
8.85933012996512));
#394358=CARTESIAN_POINT('Ctrl Pts',(-2.21519057835742,1.52394837009348,
8.8294568364472));
#394359=CARTESIAN_POINT('Ctrl Pts',(-2.2210426511292,1.52459862063228,8.83607469902385));
#394360=CARTESIAN_POINT('Ctrl Pts',(-2.2238737855901,1.516504380695,8.83829567148519));
#394361=CARTESIAN_POINT('Ctrl Pts',(-2.23887473584625,1.52658002502471,
8.80838214965002));
#394362=CARTESIAN_POINT('Ctrl Pts',(-2.24474990362954,1.52723284175572,
8.81501364461992));
#394363=CARTESIAN_POINT('Ctrl Pts',(-2.24757843466631,1.51910583586367,
8.81722098428721));
#394364=CARTESIAN_POINT('Ctrl Pts',(-2.26252622397768,1.52920804991439,
8.78727029226991));
#394365=CARTESIAN_POINT('Ctrl Pts',(-2.2684023676456,1.5298609750804,8.79393457792714));
#394366=CARTESIAN_POINT('Ctrl Pts',(-2.27124974846885,1.52170427000877,
8.79610912703474));
#394367=CARTESIAN_POINT('Origin',(-2.192851501522,1.50888924464307,8.85049129520029));
#394368=CARTESIAN_POINT('Ctrl Pts',(-2.18456153393019,1.53121811901791,
8.85049129520029));
#394369=CARTESIAN_POINT('Ctrl Pts',(-2.18717121304409,1.5364421679405,8.85711686593484));
#394370=CARTESIAN_POINT('Ctrl Pts',(-2.18059607577692,1.54190736071219,
8.85933012996512));
#394371=CARTESIAN_POINT('Ctrl Pts',(-2.18225278848925,1.52659647834605,
8.86332496987231));
#394372=CARTESIAN_POINT('Ctrl Pts',(-2.17984559913406,1.53054075696006,
8.86648636486738));
#394373=CARTESIAN_POINT('Ctrl Pts',(-2.174152592923,1.52897047603821,8.87206031107457));
#394374=CARTESIAN_POINT('Ctrl Pts',(-2.18630154981016,1.52073837816236,
8.86341338519877));
#394375=CARTESIAN_POINT('Ctrl Pts',(-2.18915667038817,1.51708847992824,
8.86654584966059));
#394376=CARTESIAN_POINT('Ctrl Pts',(-2.1856565057864,1.51230590734145,8.87215952290715));
#394377=CARTESIAN_POINT('Ctrl Pts',(-2.19147106502124,1.52131278661255,
8.85049129520029));
#394378=CARTESIAN_POINT('Ctrl Pts',(-2.19727496193953,1.52195768411218,
8.85711686593484));
#394379=CARTESIAN_POINT('Ctrl Pts',(-2.20013305013607,1.51389963881728,
8.85933012996512));
#394380=CARTESIAN_POINT('Origin',(-2.17337918662904,1.53680427233091,8.85049129520029));
#394381=CARTESIAN_POINT('Ctrl Pts',(-2.21651095806264,1.59517439388234,
8.78727029226991));
#394382=CARTESIAN_POINT('Ctrl Pts',(-2.21915312239057,1.60046347162262,
8.79393457792714));
#394383=CARTESIAN_POINT('Ctrl Pts',(-2.21248169808585,1.60595268950176,
8.79610912703474));
#394384=CARTESIAN_POINT('Ctrl Pts',(-2.20587624220566,1.57388584709556,
8.80838214965002));
#394385=CARTESIAN_POINT('Ctrl Pts',(-2.2085179677343,1.57917404644853,8.81501364461987));
#394386=CARTESIAN_POINT('Ctrl Pts',(-2.20186790511427,1.58463531733957,
8.81722098428721));
#394387=CARTESIAN_POINT('Ctrl Pts',(-2.19522683681493,1.552567894838,8.82945683644722));
#394388=CARTESIAN_POINT('Ctrl Pts',(-2.19785817784333,1.55783530652516,
8.83607469902391));
#394389=CARTESIAN_POINT('Ctrl Pts',(-2.19123976416883,1.56328770443168,
8.8382956714852));
#394390=CARTESIAN_POINT('Ctrl Pts',(-2.18456153393019,1.53121811901791,
8.85049129520029));
#394391=CARTESIAN_POINT('Ctrl Pts',(-2.18717121304409,1.5364421679405,8.85711686593484));
#394392=CARTESIAN_POINT('Ctrl Pts',(-2.18059607577692,1.54190736071219,
8.85933012996512));
#394393=CARTESIAN_POINT('Origin',(-2.20532861076149,1.60076054719534,8.78727029226991));
#394394=CARTESIAN_POINT('Ctrl Pts',(-2.2226947775269,1.60755318902291,8.75374538247848));
#394395=CARTESIAN_POINT('Ctrl Pts',(-2.22610243367153,1.61434526219592,
8.75304829418602));
#394396=CARTESIAN_POINT('Ctrl Pts',(-2.22158576323608,1.62049914969785,
8.75272238421917));
#394397=CARTESIAN_POINT('Ctrl Pts',(-2.22328466840483,1.60873403010711,
8.7676940844502));
#394398=CARTESIAN_POINT('Ctrl Pts',(-2.22677745946999,1.6156973314468,8.76974318093968));
#394399=CARTESIAN_POINT('Ctrl Pts',(-2.22245540607675,1.6218891172753,8.7707786988043));
#394400=CARTESIAN_POINT('Ctrl Pts',(-2.22026122381643,1.60268171138357,
8.78108014887991));
#394401=CARTESIAN_POINT('Ctrl Pts',(-2.22322463452793,1.60858115493827,
8.78639403366325));
#394402=CARTESIAN_POINT('Ctrl Pts',(-2.21800623306505,1.61476907558264,
8.78812224174741));
#394403=CARTESIAN_POINT('Ctrl Pts',(-2.21530646553677,1.59276329707432,
8.78944554828686));
#394404=CARTESIAN_POINT('Ctrl Pts',(-2.21780892032157,1.59773261671256,
8.79673892988686));
#394405=CARTESIAN_POINT('Ctrl Pts',(-2.21072088469269,1.60314217355579,
8.79894799272499));
#394406=CARTESIAN_POINT('Origin',(-2.21159519380501,1.61330497697695,8.75721825406948));
#394407=CARTESIAN_POINT('Origin',(-2.21159519380501,1.61330497697695,9.));
#394408=CARTESIAN_POINT('Origin',(-2.21159519380501,1.61330497697695,7.51860402984325));
#394409=CARTESIAN_POINT('Ctrl Pts',(-2.22986569462199,1.60314430367188,
7.50366195182966));
#394410=CARTESIAN_POINT('Ctrl Pts',(-2.23283898515346,1.60528192738187,
7.50000065167735));
#394411=CARTESIAN_POINT('Ctrl Pts',(-2.2328389851534,1.60528192738197,7.49482233047108));
#394412=CARTESIAN_POINT('Ctrl Pts',(-2.22683369837612,1.60993847752686,
7.50215800491336));
#394413=CARTESIAN_POINT('Ctrl Pts',(-2.22727397197241,1.61302244515553,
7.49877273257266));
#394414=CARTESIAN_POINT('Ctrl Pts',(-2.22525885250261,1.6158253810935,7.49481816995649));
#394415=CARTESIAN_POINT('Ctrl Pts',(-2.22403744845653,1.61024014411319,
7.51043025814043));
#394416=CARTESIAN_POINT('Ctrl Pts',(-2.22511749967526,1.61597828373783,
7.51006209594513));
#394417=CARTESIAN_POINT('Ctrl Pts',(-2.22169230987838,1.62067371183521,
7.50731281821698));
#394418=CARTESIAN_POINT('Ctrl Pts',(-2.22277686558813,1.60771747161815,
7.51860402984325));
#394419=CARTESIAN_POINT('Ctrl Pts',(-2.22617821334674,1.61452422200403,
7.51860402984324));
#394420=CARTESIAN_POINT('Ctrl Pts',(-2.2216938019959,1.62067166636954,7.51860402984325));
#394421=CARTESIAN_POINT('Origin',(0.,0.,7.5));
#394422=CARTESIAN_POINT('Origin',(-2.27817859968918,1.38810672912945,7.5));
#394423=CARTESIAN_POINT('',(-2.27817859968918,1.38810672912945,7.59394543036555));
#394424=CARTESIAN_POINT('',(-2.27817859968918,1.38810672912945,8.85049129520029));
#394425=CARTESIAN_POINT('',(-2.27817859968918,1.38810672912945,7.5));
#394426=CARTESIAN_POINT('',(-2.31416007290289,1.44988459233546,8.78727029226991));
#394427=CARTESIAN_POINT('Ctrl Pts',(-2.27817859968918,1.38810672912945,
8.85049129520029));
#394428=CARTESIAN_POINT('Ctrl Pts',(-2.29018985827906,1.40872928356713,
8.82945686509571));
#394429=CARTESIAN_POINT('Ctrl Pts',(-2.30218326068067,1.429321180084,8.80838212259896));
#394430=CARTESIAN_POINT('Ctrl Pts',(-2.31416007290289,1.44988459233546,
8.78727029226991));
#394431=CARTESIAN_POINT('',(-2.3212175049551,1.46200174688657,8.75721825406948));
#394432=CARTESIAN_POINT('Origin',(-2.29997941805091,1.42553692380718,8.7593767971313));
#394433=CARTESIAN_POINT('',(-2.3212175049551,1.46200174688657,7.51860402984325));
#394434=CARTESIAN_POINT('',(-2.3212175049551,1.46200174688657,7.5));
#394435=CARTESIAN_POINT('Ctrl Pts',(-2.3212175049551,1.46200174688657,7.51860402984325));
#394436=CARTESIAN_POINT('Ctrl Pts',(-2.31567498971639,1.45248560656067,
7.52834476460825));
#394437=CARTESIAN_POINT('Ctrl Pts',(-2.31012887635678,1.44296328849379,
7.53807742314407));
#394438=CARTESIAN_POINT('Ctrl Pts',(-2.30457904406455,1.43343458526006,
7.54780169004674));
#394439=CARTESIAN_POINT('Ctrl Pts',(-2.29578840965649,1.41834163432029,
7.5632044032688));
#394440=CARTESIAN_POINT('Ctrl Pts',(-2.28698843374855,1.40323264462921,
7.57858609112103));
#394441=CARTESIAN_POINT('Ctrl Pts',(-2.27817859968918,1.38810672912945,
7.59394543036555));
#394442=CARTESIAN_POINT('Origin',(-2.55914144706915,1.39057471905267,7.5));
#394443=CARTESIAN_POINT('',(-2.36986171072478,1.38175804150002,8.75721825406948));
#394444=CARTESIAN_POINT('',(-2.35585431734964,1.38110557508641,8.78727029226991));
#394445=CARTESIAN_POINT('Origin',(-2.32029832846756,1.37944937197089,8.75658640621095));
#394446=CARTESIAN_POINT('',(-2.28443929758136,1.37777905311489,8.85049129520029));
#394447=CARTESIAN_POINT('Ctrl Pts',(-2.35585431734964,1.38110557508641,
8.78727029226991));
#394448=CARTESIAN_POINT('Ctrl Pts',(-2.33208307606302,1.37999830722194,
8.80838212259896));
#394449=CARTESIAN_POINT('Ctrl Pts',(-2.30827890705325,1.37888950557934,
8.82945686509571));
#394450=CARTESIAN_POINT('Ctrl Pts',(-2.28443929758136,1.37777905311489,
8.85049129520029));
#394451=CARTESIAN_POINT('',(-2.28443929758136,1.37777905311489,7.59394543036555));
#394452=CARTESIAN_POINT('',(-2.28443929758136,1.37777905311489,7.5));
#394453=CARTESIAN_POINT('',(-2.36986171072478,1.38175804150002,7.51860402984325));
#394454=CARTESIAN_POINT('Ctrl Pts',(-2.28443929758136,1.37777905311489,
7.59394543036555));
#394455=CARTESIAN_POINT('Ctrl Pts',(-2.30192480935483,1.37859353078761,
7.57858609112103));
#394456=CARTESIAN_POINT('Ctrl Pts',(-2.31939075494535,1.3794070970647,7.56320440326857));
#394457=CARTESIAN_POINT('Ctrl Pts',(-2.3368381597889,1.38021979971109,7.54780169004651));
#394458=CARTESIAN_POINT('Ctrl Pts',(-2.34785331140614,1.38073288706993,
7.53807742314383));
#394459=CARTESIAN_POINT('Ctrl Pts',(-2.35886108179035,1.38124563060985,
7.52834476460825));
#394460=CARTESIAN_POINT('Ctrl Pts',(-2.36986171072478,1.38175804150002,
7.51860402984325));
#394461=CARTESIAN_POINT('',(-2.36986171072478,1.38175804150002,7.5));
#394462=CARTESIAN_POINT('Origin',(-2.28411940593292,1.38464660685209,7.5));
#394463=CARTESIAN_POINT('Ctrl Pts',(-2.28443929758136,1.37777905311489,
8.85049129520029));
#394464=CARTESIAN_POINT('Ctrl Pts',(-2.28424584582882,1.37777004210422,
8.85097269580138));
#394465=CARTESIAN_POINT('Ctrl Pts',(-2.28405444344771,1.37776954708626,
8.85143669361005));
#394466=CARTESIAN_POINT('Ctrl Pts',(-2.28385627471586,1.37777841954969,
8.8519052845931));
#394467=CARTESIAN_POINT('Ctrl Pts',(-2.28346866924376,1.37779577352548,
8.85282181883899));
#394468=CARTESIAN_POINT('Ctrl Pts',(-2.28306515759123,1.3778487147852,8.85372622499636));
#394469=CARTESIAN_POINT('Ctrl Pts',(-2.28264141373694,1.37795336178832,
8.85462257735071));
#394470=CARTESIAN_POINT('Ctrl Pts',(-2.28228963663907,1.3780402360136,8.85536669723986));
#394471=CARTESIAN_POINT('Ctrl Pts',(-2.28192382826308,1.37816273357066,
8.85610498449051));
#394472=CARTESIAN_POINT('Ctrl Pts',(-2.281544023598,1.3783376751687,8.85681338218371));
#394473=CARTESIAN_POINT('Ctrl Pts',(-2.28119935026796,1.37849643494367,
8.85745625420284));
#394474=CARTESIAN_POINT('Ctrl Pts',(-2.2808385762084,1.37869983336645,8.85808743050665));
#394475=CARTESIAN_POINT('Ctrl Pts',(-2.28046361585604,1.37897640429555,
8.8586680450841));
#394476=CARTESIAN_POINT('Ctrl Pts',(-2.2802906172776,1.37910400812691,8.85893592806395));
#394477=CARTESIAN_POINT('Ctrl Pts',(-2.28011464382758,1.37924742634572,
8.85919241173848));
#394478=CARTESIAN_POINT('Ctrl Pts',(-2.27993639576751,1.37941097306954,
8.85943017985534));
#394479=CARTESIAN_POINT('Ctrl Pts',(-2.27969570811935,1.37963180956172,
8.8597512372));
#394480=CARTESIAN_POINT('Ctrl Pts',(-2.27944518010467,1.37989543919245,
8.86004599534705));
#394481=CARTESIAN_POINT('Ctrl Pts',(-2.2791953715177,1.38020586914265,8.86026130871721));
#394482=CARTESIAN_POINT('Ctrl Pts',(-2.27910390955115,1.38031952629937,
8.86034014101235));
#394483=CARTESIAN_POINT('Ctrl Pts',(-2.27901116056326,1.38044115655956,
8.86040910639693));
#394484=CARTESIAN_POINT('Ctrl Pts',(-2.27891991893138,1.38056765014405,
8.86046313645507));
#394485=CARTESIAN_POINT('Ctrl Pts',(-2.27877753712897,1.38076504232326,
8.8605474499083));
#394486=CARTESIAN_POINT('Ctrl Pts',(-2.27863505860002,1.38097975158126,
8.86059655985668));
#394487=CARTESIAN_POINT('Ctrl Pts',(-2.27850137682477,1.38119784597673,
8.86059725258816));
#394488=CARTESIAN_POINT('Ctrl Pts',(-2.27836738619122,1.38141644425738,
8.86059794692012));
#394489=CARTESIAN_POINT('Ctrl Pts',(-2.27824301215026,1.38164225602507,
8.86056369958366));
#394490=CARTESIAN_POINT('Ctrl Pts',(-2.27813174193071,1.38186114989894,
8.86048590497774));
#394491=CARTESIAN_POINT('Ctrl Pts',(-2.27810270371632,1.38191827468276,
8.86046560290182));
#394492=CARTESIAN_POINT('Ctrl Pts',(-2.27807426091854,1.3819757125264,8.86044257503091));
#394493=CARTESIAN_POINT('Ctrl Pts',(-2.27804726302641,1.38203167398586,
8.86041778462583));
#394494=CARTESIAN_POINT('Ctrl Pts',(-2.27786560071395,1.38240822516566,
8.86025097596201));
#394495=CARTESIAN_POINT('Ctrl Pts',(-2.27772528047931,1.38276860366663,
8.8599848982295));
#394496=CARTESIAN_POINT('Ctrl Pts',(-2.27762250278359,1.38309921687265,
8.85968173251462));
#394497=CARTESIAN_POINT('Ctrl Pts',(-2.27756813927101,1.38327409231675,
8.85952137522077));
#394498=CARTESIAN_POINT('Ctrl Pts',(-2.27752304917652,1.38344395417844,
8.85934740853961));
#394499=CARTESIAN_POINT('Ctrl Pts',(-2.27748636585381,1.38360600818471,
8.8591675900182));
#394500=CARTESIAN_POINT('Ctrl Pts',(-2.27733906324553,1.38425673925387,
8.85844552518694));
#394501=CARTESIAN_POINT('Ctrl Pts',(-2.27731603834265,1.38481768310818,
8.85759444184122));
#394502=CARTESIAN_POINT('Ctrl Pts',(-2.27733834581908,1.38527673281356,
8.85683498915136));
#394503=CARTESIAN_POINT('Ctrl Pts',(-2.27734068023707,1.38532477114268,
8.85675551444996));
#394504=CARTESIAN_POINT('Ctrl Pts',(-2.27734353046228,1.38537168876702,
8.85667699793651));
#394505=CARTESIAN_POINT('Ctrl Pts',(-2.27734681858157,1.38541746796544,
8.85659965593547));
#394506=CARTESIAN_POINT('Ctrl Pts',(-2.27739120178348,1.3860353979218,8.85555568965886));
#394507=CARTESIAN_POINT('Ctrl Pts',(-2.27752309810306,1.38662285708124,
8.85434650606346));
#394508=CARTESIAN_POINT('Ctrl Pts',(-2.2777370957799,1.38718411095034,8.85297329937117));
#394509=CARTESIAN_POINT('Ctrl Pts',(-2.27785745643406,1.38749978205401,
8.85220095427747));
#394510=CARTESIAN_POINT('Ctrl Pts',(-2.27800413243972,1.38780718014193,
8.85137579139183));
#394511=CARTESIAN_POINT('Ctrl Pts',(-2.27817859968918,1.38810672912945,
8.85049129520029));
#394512=CARTESIAN_POINT('Origin',(-2.28411940593292,1.38464660685209,7.59394543036555));
#394513=CARTESIAN_POINT('Ctrl Pts',(-2.28387764188341,1.37775289111108,
7.59443877723642));
#394514=CARTESIAN_POINT('Ctrl Pts',(-2.27809312860511,1.37748344764418,
7.58783886950016));
#394515=CARTESIAN_POINT('Ctrl Pts',(-2.27574649854821,1.38564264545479,
7.58559994247159));
#394516=CARTESIAN_POINT('Ctrl Pts',(-2.31545513015923,1.37922377509172,
7.56670252222134));
#394517=CARTESIAN_POINT('Ctrl Pts',(-2.30967897714489,1.37895472104714,
7.56004874999028));
#394518=CARTESIAN_POINT('Ctrl Pts',(-2.30729790926197,1.38715635948061,
7.55786368756704));
#394519=CARTESIAN_POINT('Ctrl Pts',(-2.34697365063074,1.3806919123435,7.5388891333356));
#394520=CARTESIAN_POINT('Ctrl Pts',(-2.34116316965618,1.38042125929756,
7.53222002137278));
#394521=CARTESIAN_POINT('Ctrl Pts',(-2.3387915746085,1.38866613538212,7.53005029815326));
#394522=CARTESIAN_POINT('Ctrl Pts',(-2.37843177706341,1.3821572364322,7.51101258149734));
#394523=CARTESIAN_POINT('Ctrl Pts',(-2.37255086250156,1.38188330257954,
7.5043616886572));
#394524=CARTESIAN_POINT('Ctrl Pts',(-2.37022593460537,1.39017198111247,
7.50217374673251));
#394525=CARTESIAN_POINT('',(-2.36854855682564,1.39009162622348,7.50366116523517));
#394526=CARTESIAN_POINT('Ctrl Pts',(-2.36986171072478,1.38175804150002,
7.51860402984325));
#394527=CARTESIAN_POINT('Ctrl Pts',(-2.37030284363451,1.38177858953489,
7.51734760759494));
#394528=CARTESIAN_POINT('Ctrl Pts',(-2.37069870192873,1.38185658998922,
7.51608817408573));
#394529=CARTESIAN_POINT('Ctrl Pts',(-2.37104579353598,1.38200496518604,
7.5148100591312));
#394530=CARTESIAN_POINT('Ctrl Pts',(-2.37136019740785,1.38213936698486,
7.51365231206384));
#394531=CARTESIAN_POINT('Ctrl Pts',(-2.37163512890018,1.38233147186997,
7.51247773061043));
#394532=CARTESIAN_POINT('Ctrl Pts',(-2.37184468125209,1.38260822385204,
7.51129758471022));
#394533=CARTESIAN_POINT('Ctrl Pts',(-2.37210513089373,1.38295219495949,
7.50983079813402));
#394534=CARTESIAN_POINT('Ctrl Pts',(-2.37224588918624,1.38342381066497,
7.50839324291155));
#394535=CARTESIAN_POINT('Ctrl Pts',(-2.37218898720972,1.38405009018387,
7.50715379678855));
#394536=CARTESIAN_POINT('Ctrl Pts',(-2.37216270013615,1.38433941327579,
7.50658120839351));
#394537=CARTESIAN_POINT('Ctrl Pts',(-2.3720810292347,1.38470201445234,7.50598221009429));
#394538=CARTESIAN_POINT('Ctrl Pts',(-2.37192372758135,1.38512426619738,
7.50545747549611));
#394539=CARTESIAN_POINT('Ctrl Pts',(-2.37183978655018,1.38534959279845,
7.50517746087247));
#394540=CARTESIAN_POINT('Ctrl Pts',(-2.3717335882949,1.3855944196509,7.50491486231392));
#394541=CARTESIAN_POINT('Ctrl Pts',(-2.37160641486975,1.38585159955045,
7.50468370960992));
#394542=CARTESIAN_POINT('Ctrl Pts',(-2.37141625048456,1.38623616462308,
7.50433806340446));
#394543=CARTESIAN_POINT('Ctrl Pts',(-2.37117298497437,1.38665963561176,
7.50405484070983));
#394544=CARTESIAN_POINT('Ctrl Pts',(-2.37089238062564,1.38709313568448,
7.5038576603613));
#394545=CARTESIAN_POINT('Ctrl Pts',(-2.37086237435212,1.38713949177914,
7.5038365749879));
#394546=CARTESIAN_POINT('Ctrl Pts',(-2.37083196648804,1.38718594989284,
7.50381643264937));
#394547=CARTESIAN_POINT('Ctrl Pts',(-2.37080119488786,1.38723246580278,
7.50379723213559));
#394548=CARTESIAN_POINT('Ctrl Pts',(-2.37059578439061,1.38754297471809,
7.50366906242519));
#394549=CARTESIAN_POINT('Ctrl Pts',(-2.37036909795697,1.38786241660097,
7.50358235568538));
#394550=CARTESIAN_POINT('Ctrl Pts',(-2.3701431987879,1.38816506702349,7.5035341175365));
#394551=CARTESIAN_POINT('Ctrl Pts',(-2.36980448855074,1.38861885707865,
7.50346178989176));
#394552=CARTESIAN_POINT('Ctrl Pts',(-2.36942081878387,1.38909263034581,
7.50346967198527));
#394553=CARTESIAN_POINT('Ctrl Pts',(-2.36902986284641,1.38954613953559,
7.50354272648692));
#394554=CARTESIAN_POINT('Ctrl Pts',(-2.36886905457702,1.38973267725243,
7.50357277531559));
#394555=CARTESIAN_POINT('Ctrl Pts',(-2.36870733465887,1.38991563133445,
7.50361331098761));
#394556=CARTESIAN_POINT('Ctrl Pts',(-2.36854855682687,1.39009162622419,
7.50366116523659));
#394557=CARTESIAN_POINT('',(-2.28662319996334,1.38616442150748,7.57603338622103));
#394558=CARTESIAN_POINT('Origin',(-2.29417856487493,1.39074786460783,7.58486873427627));
#394559=CARTESIAN_POINT('Ctrl Pts',(-2.36854855688293,1.39009162622086,
7.50366116529968));
#394560=CARTESIAN_POINT('Ctrl Pts',(-2.34128462633658,1.38878552899461,
7.52783573079709));
#394561=CARTESIAN_POINT('Ctrl Pts',(-2.31397746256357,1.38747654046441,
7.55196141284068));
#394562=CARTESIAN_POINT('Ctrl Pts',(-2.28662320117997,1.38616442121176,
7.57603338728831));
#394563=CARTESIAN_POINT('Ctrl Pts',(-2.2854584115801,1.37800253058068,7.59639677331372));
#394564=CARTESIAN_POINT('Ctrl Pts',(-2.26756460946867,1.37427643856106,
7.59959882295461));
#394565=CARTESIAN_POINT('Ctrl Pts',(-2.27873543150216,1.38876510819258,
7.59642833564546));
#394566=CARTESIAN_POINT('Ctrl Pts',(-2.2818171460615,1.37660385638462,7.58707626057424));
#394567=CARTESIAN_POINT('Ctrl Pts',(-2.27564276078402,1.37939478051135,
7.58809943920598));
#394568=CARTESIAN_POINT('Ctrl Pts',(-2.27591536114094,1.38615052546198,
7.58710240504252));
#394569=CARTESIAN_POINT('Ctrl Pts',(-2.2842159981254,1.3821869685129,7.5801537675693));
#394570=CARTESIAN_POINT('Ctrl Pts',(-2.28148722914889,1.3830134618696,7.5820588065976));
#394571=CARTESIAN_POINT('Ctrl Pts',(-2.28196843808644,1.38578754063495,
7.58020924244129));
#394572=CARTESIAN_POINT('Ctrl Pts',(-2.28662319925575,1.3861644210783,7.57603338509286));
#394573=CARTESIAN_POINT('Ctrl Pts',(-2.28662319925575,1.3861644210783,7.57603338509286));
#394574=CARTESIAN_POINT('Ctrl Pts',(-2.28662319925575,1.3861644210783,7.57603338509286));
#394575=CARTESIAN_POINT('Origin',(-2.29418152300553,1.39074298486212,7.58486873427623));
#394576=CARTESIAN_POINT('Ctrl Pts',(-2.32554906181097,1.46943874996094,
7.51098857897448));
#394577=CARTESIAN_POINT('Ctrl Pts',(-2.32258603056804,1.46435141688502,
7.50433767179956));
#394578=CARTESIAN_POINT('Ctrl Pts',(-2.32885943401302,1.4584562951476,7.50214974420965));
#394579=CARTESIAN_POINT('Ctrl Pts',(-2.30969475968219,1.44221793823038,
7.53887321589168));
#394580=CARTESIAN_POINT('Ctrl Pts',(-2.30676723081199,1.4371915604331,7.53220407452061));
#394581=CARTESIAN_POINT('Ctrl Pts',(-2.31298019139209,1.43127530817746,
7.53003438070911));
#394582=CARTESIAN_POINT('Ctrl Pts',(-2.29381001144491,1.41494485249997,
7.56669465659232));
#394583=CARTESIAN_POINT('Ctrl Pts',(-2.29089978372601,1.40994817966099,
7.56004085833298));
#394584=CARTESIAN_POINT('Ctrl Pts',(-2.29707001560499,1.40404352990962,
7.55785582193789));
#394585=CARTESIAN_POINT('Ctrl Pts',(-2.27789553550272,1.3876207262222,7.59443891967696));
#394586=CARTESIAN_POINT('Ctrl Pts',(-2.27498108831601,1.3826168088297,7.58783901202978));
#394587=CARTESIAN_POINT('Ctrl Pts',(-2.28112962096229,1.3767623469171,7.58560008491213));
#394588=CARTESIAN_POINT('',(-2.32799867143119,1.45698290352087,7.50366116523517));
#394589=CARTESIAN_POINT('Ctrl Pts',(-2.3279986714315,1.45698290352106,7.50366116523554));
#394590=CARTESIAN_POINT('Ctrl Pts',(-2.32773447744661,1.45769307184978,
7.50350835821027));
#394591=CARTESIAN_POINT('Ctrl Pts',(-2.32746851446684,1.45833729363188,
7.50345484956));
#394592=CARTESIAN_POINT('Ctrl Pts',(-2.32719343025616,1.45893495125746,
7.50349758195598));
#394593=CARTESIAN_POINT('Ctrl Pts',(-2.32705229165531,1.45924159394283,
7.50351950684424));
#394594=CARTESIAN_POINT('Ctrl Pts',(-2.32689495833406,1.45956625690094,
7.50357029184312));
#394595=CARTESIAN_POINT('Ctrl Pts',(-2.32673463798332,1.45987515532442,
7.50365515313923));
#394596=CARTESIAN_POINT('Ctrl Pts',(-2.32648800036376,1.46035036618505,
7.50378570417639));
#394597=CARTESIAN_POINT('Ctrl Pts',(-2.32622736167187,1.46080237652902,
7.50400001621911));
#394598=CARTESIAN_POINT('Ctrl Pts',(-2.32597059343915,1.46119564767338,
7.50428903009635));
#394599=CARTESIAN_POINT('Ctrl Pts',(-2.32594209414077,1.46123929774475,
7.50432110841318));
#394600=CARTESIAN_POINT('Ctrl Pts',(-2.3259136432884,1.46128225449648,7.50435406373354));
#394601=CARTESIAN_POINT('Ctrl Pts',(-2.32588526557894,1.46132449171132,
7.50438785222351));
#394602=CARTESIAN_POINT('Ctrl Pts',(-2.32571200602259,1.46158237020969,
7.50459414719561));
#394603=CARTESIAN_POINT('Ctrl Pts',(-2.3255382864381,1.46181724467064,7.50483629897752));
#394604=CARTESIAN_POINT('Ctrl Pts',(-2.3253718200413,1.46202089970008,7.5050991045531));
#394605=CARTESIAN_POINT('Ctrl Pts',(-2.32500457845001,1.46247018315024,
7.50567888004914));
#394606=CARTESIAN_POINT('Ctrl Pts',(-2.32465856865975,1.46278555900683,
7.50637912803144));
#394607=CARTESIAN_POINT('Ctrl Pts',(-2.32434792656117,1.46299451535731,
7.50710440483569));
#394608=CARTESIAN_POINT('Ctrl Pts',(-2.32427175095149,1.46304575560281,
7.50728225710685));
#394609=CARTESIAN_POINT('Ctrl Pts',(-2.32419626713429,1.46309173768623,
7.50746498566954));
#394610=CARTESIAN_POINT('Ctrl Pts',(-2.3241234538743,1.46313174401608,7.50764697238949));
#394611=CARTESIAN_POINT('Ctrl Pts',(-2.32373202982733,1.46334680703533,
7.50862528291182));
#394612=CARTESIAN_POINT('Ctrl Pts',(-2.32338424120943,1.46341233067584,
7.50965856837422));
#394613=CARTESIAN_POINT('Ctrl Pts',(-2.32307440409398,1.46339436861899,
7.51067959873203));
#394614=CARTESIAN_POINT('Ctrl Pts',(-2.32290390033854,1.46338448407646,
7.51124147302579));
#394615=CARTESIAN_POINT('Ctrl Pts',(-2.32274487302363,1.46334888134487,
7.51180065547253));
#394616=CARTESIAN_POINT('Ctrl Pts',(-2.32259663098811,1.46329586426744,
7.51235175716501));
#394617=CARTESIAN_POINT('Ctrl Pts',(-2.32208439570275,1.4631126691454,7.51425603304535));
#394618=CARTESIAN_POINT('Ctrl Pts',(-2.32164190203507,1.46269399769698,
7.51626900505179));
#394619=CARTESIAN_POINT('Ctrl Pts',(-2.32127620067168,1.46209979118688,
7.51827788969242));
#394620=CARTESIAN_POINT('Ctrl Pts',(-2.32125640822281,1.46206763160766,
7.51838661432544));
#394621=CARTESIAN_POINT('Ctrl Pts',(-2.32123684240496,1.46203494803777,
7.51849533314856));
#394622=CARTESIAN_POINT('Ctrl Pts',(-2.3212175049551,1.46200174688657,7.51860402984325));
#394623=CARTESIAN_POINT('Ctrl Pts',(-2.28662320026479,1.38616442272375,
7.57603338728984));
#394624=CARTESIAN_POINT('Ctrl Pts',(-2.30043891757839,1.40980978650237,
7.55196141284922));
#394625=CARTESIAN_POINT('Ctrl Pts',(-2.31423007475574,1.4334148416652,7.52783573083104));
#394626=CARTESIAN_POINT('Ctrl Pts',(-2.32799867145622,1.45698290357449,
7.50366116530176));
#394627=CARTESIAN_POINT('Origin',(-7.90134016134196E-16,4.7898388392343E-16,
7.49482233047033));
#394628=CARTESIAN_POINT('Origin',(-2.36092560474804,1.38561774629408,7.49482233047033));
#394629=CARTESIAN_POINT('Origin',(0.,0.,7.50366116523517));
#394630=CARTESIAN_POINT('Origin',(-2.32050622536843,1.45229374026964,7.49482233047033));
#394631=CARTESIAN_POINT('Ctrl Pts',(-2.36986065415221,1.38175799223992,
7.51860402984325));
#394632=CARTESIAN_POINT('Ctrl Pts',(-2.37746134385964,1.38211267801839,
7.51860402984325));
#394633=CARTESIAN_POINT('Ctrl Pts',(-2.38126727405859,1.37552396180423,
7.51860402984325));
#394634=CARTESIAN_POINT('Ctrl Pts',(-2.37268284216962,1.38188968822062,
7.51041458714365));
#394635=CARTESIAN_POINT('Ctrl Pts',(-2.37836300374412,1.38055173072964,
7.51004642900441));
#394636=CARTESIAN_POINT('Ctrl Pts',(-2.38126832368895,1.37552214471453,
7.50729136483009));
#394637=CARTESIAN_POINT('Ctrl Pts',(-2.37352967894752,1.38457420021926,
7.50215815450138));
#394638=CARTESIAN_POINT('Ctrl Pts',(-2.37652725582071,1.38373004539293,
7.49877163671531));
#394639=CARTESIAN_POINT('Ctrl Pts',(-2.37827363220951,1.38075446257557,
7.49481588533172));
#394640=CARTESIAN_POINT('Ctrl Pts',(-2.36854808203743,1.39009134757273,
7.50366171572174));
#394641=CARTESIAN_POINT('Ctrl Pts',(-2.37170608696131,1.39194476796699,
7.50000045605858));
#394642=CARTESIAN_POINT('Ctrl Pts',(-2.37170608696137,1.39194476796689,
7.49482233047317));
#394643=CARTESIAN_POINT('Origin',(-2.37044333190377,1.36927158015967,7.51860402984325));
#394644=CARTESIAN_POINT('Origin',(-2.37044333190377,1.36927158015967,9.));
#394645=CARTESIAN_POINT('Origin',(-2.37044333190377,1.36927158015967,8.75721825406948));
#394646=CARTESIAN_POINT('Ctrl Pts',(-2.35317963884603,1.38098095793092,
8.78942910404913));
#394647=CARTESIAN_POINT('Ctrl Pts',(-2.35874509705392,1.38126042821203,
8.7967269950169));
#394648=CARTESIAN_POINT('Ctrl Pts',(-2.36082223585053,1.37257947317229,
8.79893251111267));
#394649=CARTESIAN_POINT('Ctrl Pts',(-2.36416206650684,1.3814925255372,8.78111911759576));
#394650=CARTESIAN_POINT('Ctrl Pts',(-2.37076035502444,1.38181640632387,
8.78644465894814));
#394651=CARTESIAN_POINT('Ctrl Pts',(-2.37429374527117,1.37452047148728,
8.78817647674131));
#394652=CARTESIAN_POINT('Ctrl Pts',(-2.37100657738213,1.38181134663968,
8.76780923932034));
#394653=CARTESIAN_POINT('Ctrl Pts',(-2.37879582820066,1.38218858457062,
8.76988516158373));
#394654=CARTESIAN_POINT('Ctrl Pts',(-2.38270941194407,1.37572172732156,
8.77093053738834));
#394655=CARTESIAN_POINT('Ctrl Pts',(-2.36967199143526,1.38174918088633,
8.75371302330491));
#394656=CARTESIAN_POINT('Ctrl Pts',(-2.37727003273756,1.38211792163049,
8.75300828287559));
#394657=CARTESIAN_POINT('Ctrl Pts',(-2.38106807980286,1.37548698068488,
8.75267964240737));
#394658=CARTESIAN_POINT('Origin',(-2.35643593852862,1.36861911374606,8.78727029226991));
#394659=CARTESIAN_POINT('Ctrl Pts',(-2.28443929758136,1.37777905311489,
8.85049129520029));
#394660=CARTESIAN_POINT('Ctrl Pts',(-2.29027258849563,1.37805076865114,
8.85711686593484));
#394661=CARTESIAN_POINT('Ctrl Pts',(-2.29260852370878,1.36982616113504,
8.85933012996512));
#394662=CARTESIAN_POINT('Ctrl Pts',(-2.3082789390469,1.37888950706961,8.82945683644723));
#394663=CARTESIAN_POINT('Ctrl Pts',(-2.31416064980263,1.37916347800909,
8.83607469902389));
#394664=CARTESIAN_POINT('Ctrl Pts',(-2.31646736766073,1.37090447714819,
8.8382956714852));
#394665=CARTESIAN_POINT('Ctrl Pts',(-2.3320830456044,1.37999830580317,8.80838214965002));
#394666=CARTESIAN_POINT('Ctrl Pts',(-2.33798796833688,1.3802733579599,8.8150136446199));
#394667=CARTESIAN_POINT('Ctrl Pts',(-2.34028998879803,1.37198182526734,
8.81722098428721));
#394668=CARTESIAN_POINT('Ctrl Pts',(-2.35585431734964,1.38110557508641,
8.78727029226991));
#394669=CARTESIAN_POINT('Ctrl Pts',(-2.36176022090919,1.3813806729302,8.79393457792714));
#394670=CARTESIAN_POINT('Ctrl Pts',(-2.36407914959491,1.37305829436823,
8.79610912703474));
#394671=CARTESIAN_POINT('Origin',(-2.28502091876035,1.36529259177454,8.85049129520029));
#394672=CARTESIAN_POINT('Ctrl Pts',(-2.27817859968918,1.38810672912945,
8.85049129520029));
#394673=CARTESIAN_POINT('Ctrl Pts',(-2.28111762290111,1.39315284196834,
8.85711686593484));
#394674=CARTESIAN_POINT('Ctrl Pts',(-2.27490615106175,1.39902807640646,
8.85933012996512));
#394675=CARTESIAN_POINT('Ctrl Pts',(-2.27557848827882,1.38364250594229,
8.86332496987234));
#394676=CARTESIAN_POINT('Ctrl Pts',(-2.27342895555081,1.38773290976439,
8.86648636486737));
#394677=CARTESIAN_POINT('Ctrl Pts',(-2.26764703798749,1.38653060731341,
8.87206031107457));
#394678=CARTESIAN_POINT('Ctrl Pts',(-2.27924360121796,1.37753703682523,
8.86341338519875));
#394679=CARTESIAN_POINT('Ctrl Pts',(-2.28185900586174,1.37371170949497,
8.86654584966057));
#394680=CARTESIAN_POINT('Ctrl Pts',(-2.27805961224584,1.3691632195325,8.87215952290714));
#394681=CARTESIAN_POINT('Ctrl Pts',(-2.28443929758136,1.37777905311489,
8.85049129520029));
#394682=CARTESIAN_POINT('Ctrl Pts',(-2.29027258849563,1.37805076865114,
8.85711686593484));
#394683=CARTESIAN_POINT('Ctrl Pts',(-2.29260852370878,1.36982616113504,
8.85933012996512));
#394684=CARTESIAN_POINT('Origin',(-2.26737713379146,1.39439786054284,8.85049129520029));
#394685=CARTESIAN_POINT('Ctrl Pts',(-2.31416007290289,1.44988459233546,
8.78727029226991));
#394686=CARTESIAN_POINT('Ctrl Pts',(-2.31713568099515,1.45499351904855,
8.79393457792714));
#394687=CARTESIAN_POINT('Ctrl Pts',(-2.31082965924421,1.46089889836363,
8.79610912703474));
#394688=CARTESIAN_POINT('Ctrl Pts',(-2.30218324533451,1.42932115373564,
8.80838214965002));
#394689=CARTESIAN_POINT('Ctrl Pts',(-2.30515835925056,1.43442923198015,
8.81501364461988));
#394690=CARTESIAN_POINT('Ctrl Pts',(-2.29887186472477,1.44030535307934,
8.81722098428722));
#394691=CARTESIAN_POINT('Ctrl Pts',(-2.29018987439861,1.40872931124336,
8.82945683644723));
#394692=CARTESIAN_POINT('Ctrl Pts',(-2.29315329328018,1.41381730986974,
8.83607469902389));
#394693=CARTESIAN_POINT('Ctrl Pts',(-2.2868978141797,1.41968254846007,8.8382956714852));
#394694=CARTESIAN_POINT('Ctrl Pts',(-2.27817859968918,1.38810672912945,
8.85049129520029));
#394695=CARTESIAN_POINT('Ctrl Pts',(-2.28111762290111,1.39315284196834,
8.85711686593484));
#394696=CARTESIAN_POINT('Ctrl Pts',(-2.27490615106175,1.39902807640646,
8.85933012996512));
#394697=CARTESIAN_POINT('Origin',(-2.30335860700518,1.45617572374885,8.78727029226991));
#394698=CARTESIAN_POINT('Ctrl Pts',(-2.3211242991746,1.46184175524038,8.75374538247848));
#394699=CARTESIAN_POINT('Ctrl Pts',(-2.32496012354653,1.4684015440918,8.75304829418601));
#394700=CARTESIAN_POINT('Ctrl Pts',(-2.32084701402088,1.47483217184025,
8.75272238421917));
#394701=CARTESIAN_POINT('Ctrl Pts',(-2.32178863480649,1.46298237572165,
8.7676940844502));
#394702=CARTESIAN_POINT('Ctrl Pts',(-2.32572038980645,1.46970758632004,
8.76974318093969));
#394703=CARTESIAN_POINT('Ctrl Pts',(-2.32180392561551,1.47616356537214,
8.7707786988043));
#394704=CARTESIAN_POINT('Ctrl Pts',(-2.31838362881722,1.45713620489586,
8.78108014887988));
#394705=CARTESIAN_POINT('Ctrl Pts',(-2.32171892952989,1.4628336610349,8.78639403366325));
#394706=CARTESIAN_POINT('Ctrl Pts',(-2.31690771126942,1.46934321206235,
8.78812224174741));
#394707=CARTESIAN_POINT('Ctrl Pts',(-2.31280357563321,1.44755562148552,
8.78944554828685));
#394708=CARTESIAN_POINT('Ctrl Pts',(-2.31561927425866,1.45235439829505,
8.79673892988686));
#394709=CARTESIAN_POINT('Ctrl Pts',(-2.30889239325609,1.45820697262554,
8.79894799272499));
#394710=CARTESIAN_POINT('Origin',(-2.31041603905739,1.46829287829996,8.75721825406948));
#394711=CARTESIAN_POINT('Origin',(-2.31041603905739,1.46829287829996,9.));
#394712=CARTESIAN_POINT('Origin',(-2.31041603905739,1.46829287829996,7.51860402984325));
#394713=CARTESIAN_POINT('Ctrl Pts',(-2.32799800459713,1.45698248618143,
7.50366195182966));
#394714=CARTESIAN_POINT('Ctrl Pts',(-2.33110214420566,1.45892521853583,
7.50000065167735));
#394715=CARTESIAN_POINT('Ctrl Pts',(-2.33110214420559,1.45892521853592,
7.49482233047108));
#394716=CARTESIAN_POINT('Ctrl Pts',(-2.32540754212619,1.46395696134399,
7.50215800491338));
#394717=CARTESIAN_POINT('Ctrl Pts',(-2.32604450161754,1.46700638420426,
7.49877273257267));
#394718=CARTESIAN_POINT('Ctrl Pts',(-2.32421310714895,1.46993267035745,
7.49481816995647));
#394719=CARTESIAN_POINT('Ctrl Pts',(-2.32263636524651,1.46443716447144,
7.5104302581404));
#394720=CARTESIAN_POINT('Ctrl Pts',(-2.32408184125221,1.47009431535362,
7.51006209594513));
#394721=CARTESIAN_POINT('Ctrl Pts',(-2.32096452598623,1.47499954885415,
7.50731281821699));
#394722=CARTESIAN_POINT('Ctrl Pts',(-2.32121674419912,1.46200044089929,
7.51860402984325));
#394723=CARTESIAN_POINT('Ctrl Pts',(-2.32504721351854,1.46857528098735,
7.51860402984324));
#394724=CARTESIAN_POINT('Ctrl Pts',(-2.32096588398459,1.47499741199083,
7.51860402984325));
#394725=CARTESIAN_POINT('Origin',(0.,0.,7.5));
#394726=CARTESIAN_POINT('Origin',(-2.36243414091426,1.23929131094303,7.5));
#394727=CARTESIAN_POINT('',(-2.36243414091426,1.23929131094303,7.59394543036555));
#394728=CARTESIAN_POINT('',(-2.36243414091426,1.23929131094303,8.85049129520029));
#394729=CARTESIAN_POINT('',(-2.36243414091426,1.23929131094303,7.5));
#394730=CARTESIAN_POINT('',(-2.4022998076178,1.2986369039994,8.78727029226991));
#394731=CARTESIAN_POINT('Ctrl Pts',(-2.36243414091426,1.23929131094303,
8.85049129520029));
#394732=CARTESIAN_POINT('Ctrl Pts',(-2.37574201268455,1.25910193015076,
8.82945686509571));
#394733=CARTESIAN_POINT('Ctrl Pts',(-2.38903010069429,1.27888309847756,
8.80838212259894));
#394734=CARTESIAN_POINT('Ctrl Pts',(-2.4022998076178,1.2986369039994,8.78727029226991));
#394735=CARTESIAN_POINT('',(-2.41011908817658,1.31027699133284,8.75721825406948));
#394736=CARTESIAN_POINT('Origin',(-2.38658832796283,1.27524781804229,8.75937679713088));
#394737=CARTESIAN_POINT('',(-2.41011908817658,1.31027699133284,7.51860402984325));
#394738=CARTESIAN_POINT('',(-2.41011908817658,1.31027699133284,7.5));
#394739=CARTESIAN_POINT('Ctrl Pts',(-2.41011908817658,1.31027699133284,
7.51860402984325));
#394740=CARTESIAN_POINT('Ctrl Pts',(-2.40397825942582,1.30113551310844,
7.52834476460825));
#394741=CARTESIAN_POINT('Ctrl Pts',(-2.39783344413765,1.29198810036828,
7.53807742314407));
#394742=CARTESIAN_POINT('Ctrl Pts',(-2.39168450845876,1.28283455385311,
7.54780169004674));
#394743=CARTESIAN_POINT('Ctrl Pts',(-2.38194492666502,1.26833583088006,
7.5632044032688));
#394744=CARTESIAN_POINT('Ctrl Pts',(-2.37219499495818,1.25382170062098,
7.57858609112103));
#394745=CARTESIAN_POINT('Ctrl Pts',(-2.36243414091426,1.23929131094303,
7.59394543036555));
#394746=CARTESIAN_POINT('Origin',(-2.64297784464841,1.22375287867822,7.5));
#394747=CARTESIAN_POINT('',(-2.45352211735225,1.22708151028067,8.75721825406948));
#394748=CARTESIAN_POINT('',(-2.43950170000243,1.22732784120418,8.78727029226991));
#394749=CARTESIAN_POINT('Origin',(-2.4039126514152,1.22795312096489,8.75658640621105));
#394750=CARTESIAN_POINT('',(-2.36802027905702,1.2285837299553,8.85049129520029));
#394751=CARTESIAN_POINT('Ctrl Pts',(-2.43950170000243,1.22732784120418,
8.78727029226991));
#394752=CARTESIAN_POINT('Ctrl Pts',(-2.41570835638484,1.22774587699874,
8.80838212259895));
#394753=CARTESIAN_POINT('Ctrl Pts',(-2.39188205442814,1.22816449185295,
8.82945686509571));
#394754=CARTESIAN_POINT('Ctrl Pts',(-2.36802027905702,1.2285837299553,8.85049129520029));
#394755=CARTESIAN_POINT('',(-2.36802027905702,1.2285837299553,7.59394543036555));
#394756=CARTESIAN_POINT('',(-2.36802027905702,1.2285837299553,7.5));
#394757=CARTESIAN_POINT('',(-2.45352211735225,1.22708151028067,7.51860402984325));
#394758=CARTESIAN_POINT('Ctrl Pts',(-2.36802027905702,1.2285837299553,7.59394543036555));
#394759=CARTESIAN_POINT('Ctrl Pts',(-2.3855220487349,1.22827623361048,7.57858609112103));
#394760=CARTESIAN_POINT('Ctrl Pts',(-2.40300423403733,1.22796908135225,
7.56320440326857));
#394761=CARTESIAN_POINT('Ctrl Pts',(-2.42046786135374,1.22766225514747,
7.54780169004651));
#394762=CARTESIAN_POINT('Ctrl Pts',(-2.43149325478056,1.22746854512606,
7.53807742314383));
#394763=CARTESIAN_POINT('Ctrl Pts',(-2.44251126011132,1.22727496490938,
7.52834476460825));
#394764=CARTESIAN_POINT('Ctrl Pts',(-2.45352211735225,1.22708151028067,
7.51860402984325));
#394765=CARTESIAN_POINT('',(-2.45352211735225,1.22708151028067,7.5));
#394766=CARTESIAN_POINT('Origin',(-2.36814105033895,1.23545766909509,7.5));
#394767=CARTESIAN_POINT('Ctrl Pts',(-2.36802027905702,1.2285837299553,8.85049129520029));
#394768=CARTESIAN_POINT('Ctrl Pts',(-2.36782664743442,1.22858713195506,
8.85097269580138));
#394769=CARTESIAN_POINT('Ctrl Pts',(-2.36763560659412,1.22859890114683,
8.85143669361005));
#394770=CARTESIAN_POINT('Ctrl Pts',(-2.36743841348187,1.22862045209507,
8.8519052845931));
#394771=CARTESIAN_POINT('Ctrl Pts',(-2.36705271625983,1.22866260438312,
8.85282181883899));
#394772=CARTESIAN_POINT('Ctrl Pts',(-2.36665342562341,1.22874128994969,
8.85372622499635));
#394773=CARTESIAN_POINT('Ctrl Pts',(-2.36623725715283,1.22887287130628,
8.85462257735071));
#394774=CARTESIAN_POINT('Ctrl Pts',(-2.36589176886946,1.22898210547519,
8.85536669723986));
#394775=CARTESIAN_POINT('Ctrl Pts',(-2.36553456053144,1.22912778877101,
8.85610498449051));
#394776=CARTESIAN_POINT('Ctrl Pts',(-2.36516674476246,1.22932670510121,
8.85681338218371));
#394777=CARTESIAN_POINT('Ctrl Pts',(-2.36483295137444,1.22950722198327,
8.85745625420284));
#394778=CARTESIAN_POINT('Ctrl Pts',(-2.36448595034557,1.22973331737554,
8.85808743050666));
#394779=CARTESIAN_POINT('Ctrl Pts',(-2.36412948034973,1.23003334385226,
8.8586680450841));
#394780=CARTESIAN_POINT('Ctrl Pts',(-2.36396501282097,1.23017176956484,
8.85893592806395));
#394781=CARTESIAN_POINT('Ctrl Pts',(-2.36379858976411,1.23032616777319,
8.85919241173848));
#394782=CARTESIAN_POINT('Ctrl Pts',(-2.36363118640837,1.23050079886515,
8.85943017985534));
#394783=CARTESIAN_POINT('Ctrl Pts',(-2.36340514232143,1.23073660253563,
8.8597512372));
#394784=CARTESIAN_POINT('Ctrl Pts',(-2.36317201985186,1.23101574189602,
8.86004599534706));
#394785=CARTESIAN_POINT('Ctrl Pts',(-2.36294261383862,1.23134153932572,
8.86026130871721));
#394786=CARTESIAN_POINT('Ctrl Pts',(-2.36285862182953,1.23146082294993,
8.86034014101235));
#394787=CARTESIAN_POINT('Ctrl Pts',(-2.36277385628191,1.23158814575577,
8.86040910639693));
#394788=CARTESIAN_POINT('Ctrl Pts',(-2.36269090658753,1.23172022531705,
8.86046313645507));
#394789=CARTESIAN_POINT('Ctrl Pts',(-2.36256146428415,1.23192633436627,
8.8605474499083));
#394790=CARTESIAN_POINT('Ctrl Pts',(-2.36243303496201,1.23214973111175,
8.86059655985669));
#394791=CARTESIAN_POINT('Ctrl Pts',(-2.3623136012062,1.23237594242964,8.86059725258816));
#394792=CARTESIAN_POINT('Ctrl Pts',(-2.3621938915107,1.23260267638605,8.86059794692012));
#394793=CARTESIAN_POINT('Ctrl Pts',(-2.36208424081917,1.23283599287141,
8.86056369958366));
#394794=CARTESIAN_POINT('Ctrl Pts',(-2.36198722379487,1.23306156611178,
8.86048590497774));
#394795=CARTESIAN_POINT('Ctrl Pts',(-2.36196190524008,1.23312043401139,
8.86046560290182));
#394796=CARTESIAN_POINT('Ctrl Pts',(-2.36193720093636,1.23317957617913,
8.8604425750309));
#394797=CARTESIAN_POINT('Ctrl Pts',(-2.36191384397731,1.23323715242066,
8.86041778462583));
#394798=CARTESIAN_POINT('Ctrl Pts',(-2.36175668062648,1.23362456908,8.860250975962));
#394799=CARTESIAN_POINT('Ctrl Pts',(-2.36163973822464,1.23399319749299,
8.8599848982295));
#394800=CARTESIAN_POINT('Ctrl Pts',(-2.36155835415756,1.23432971640829,
8.85968173251461));
#394801=CARTESIAN_POINT('Ctrl Pts',(-2.36151530664882,1.23450771563425,
8.85952137522076));
#394802=CARTESIAN_POINT('Ctrl Pts',(-2.36148119228361,1.2346801174288,8.85934740853961));
#394803=CARTESIAN_POINT('Ctrl Pts',(-2.36145496716655,1.23484418878629,
8.8591675900182));
#394804=CARTESIAN_POINT('Ctrl Pts',(-2.36134965969002,1.23550302056918,
8.85844552518695));
#394805=CARTESIAN_POINT('Ctrl Pts',(-2.36136262189042,1.23606428711478,
8.85759444184123));
#394806=CARTESIAN_POINT('Ctrl Pts',(-2.36141429494935,1.23652096440839,
8.85683498915137));
#394807=CARTESIAN_POINT('Ctrl Pts',(-2.36141970239735,1.23656875447093,
8.85675551444997));
#394808=CARTESIAN_POINT('Ctrl Pts',(-2.36142555278897,1.23661539308343,
8.85667699793651));
#394809=CARTESIAN_POINT('Ctrl Pts',(-2.36143176723578,1.23666086755305,
8.85659965593547));
#394810=CARTESIAN_POINT('Ctrl Pts',(-2.36151565015588,1.23727468426453,
8.85555568965886));
#394811=CARTESIAN_POINT('Ctrl Pts',(-2.3616849141179,1.23785248579991,8.85434650606346));
#394812=CARTESIAN_POINT('Ctrl Pts',(-2.36193443177242,1.23839887563451,
8.85297329937117));
#394813=CARTESIAN_POINT('Ctrl Pts',(-2.36207477024976,1.23870618662446,
8.85220095427747));
#394814=CARTESIAN_POINT('Ctrl Pts',(-2.36224083995695,1.23900355556609,
8.85137579139183));
#394815=CARTESIAN_POINT('Ctrl Pts',(-2.36243414091426,1.23929131094303,
8.85049129520029));
#394816=CARTESIAN_POINT('Origin',(-2.36814105033895,1.23545766909509,7.59394543036555));
#394817=CARTESIAN_POINT('Ctrl Pts',(-2.3674581011356,1.22859360710825,7.59443877723642));
#394818=CARTESIAN_POINT('Ctrl Pts',(-2.36166820945802,1.22869533228008,
7.58783886950016));
#394819=CARTESIAN_POINT('Ctrl Pts',(-2.35984916240284,1.23698811524768,
7.58559994247159));
#394820=CARTESIAN_POINT('Ctrl Pts',(-2.39906494993531,1.22803829237974,
7.56670252222137));
#394821=CARTESIAN_POINT('Ctrl Pts',(-2.39328342629498,1.22813987052983,
7.56004874999026));
#394822=CARTESIAN_POINT('Ctrl Pts',(-2.39143273135004,1.23647721336054,
7.55786368756704));
#394823=CARTESIAN_POINT('Ctrl Pts',(-2.43061277610281,1.227484014646,7.5388891333356));
#394824=CARTESIAN_POINT('Ctrl Pts',(-2.4247968925844,1.22758619647999,7.53222002137278));
#394825=CARTESIAN_POINT('Ctrl Pts',(-2.42295842125755,1.23596608119879,
7.53005029815327));
#394826=CARTESIAN_POINT('Ctrl Pts',(-2.46210015207757,1.22693079898848,
7.51101258149734));
#394827=CARTESIAN_POINT('Ctrl Pts',(-2.45621376948321,1.22703421945197,
7.5043616886572));
#394828=CARTESIAN_POINT('Ctrl Pts',(-2.45442467585769,1.23545482664764,
7.50217374673251));
#394829=CARTESIAN_POINT('',(-2.45274559607509,1.23548210681972,7.50366116523517));
#394830=CARTESIAN_POINT('Ctrl Pts',(-2.45352211735225,1.22708151028067,
7.51860402984325));
#394831=CARTESIAN_POINT('Ctrl Pts',(-2.45396366042422,1.22707375261483,
7.51734760759494));
#394832=CARTESIAN_POINT('Ctrl Pts',(-2.45436370289138,1.22712623008087,
7.51608817408573));
#394833=CARTESIAN_POINT('Ctrl Pts',(-2.4547195877932,1.22725206218931,7.5148100591312));
#394834=CARTESIAN_POINT('Ctrl Pts',(-2.45504195684141,1.22736604391998,
7.51365231206384));
#394835=CARTESIAN_POINT('Ctrl Pts',(-2.45532863165975,1.2275401391838,7.51247773061043));
#394836=CARTESIAN_POINT('Ctrl Pts',(-2.45555548502425,1.22780289648397,
7.51129758471022));
#394837=CARTESIAN_POINT('Ctrl Pts',(-2.45583743784869,1.22812947380005,
7.50983079813402));
#394838=CARTESIAN_POINT('Ctrl Pts',(-2.45600812346019,1.22859110210571,
7.50839324291155));
#394839=CARTESIAN_POINT('Ctrl Pts',(-2.45599146426143,1.22921974058833,
7.50715379678855));
#394840=CARTESIAN_POINT('Ctrl Pts',(-2.45598376819163,1.22951015345352,
7.50658120839351));
#394841=CARTESIAN_POINT('Ctrl Pts',(-2.45592549702894,1.22987724229968,
7.50598221009429));
#394842=CARTESIAN_POINT('Ctrl Pts',(-2.45579557233091,1.23030870483476,
7.50545747549611));
#394843=CARTESIAN_POINT('Ctrl Pts',(-2.45572624049049,1.2305389465985,7.50517746087247));
#394844=CARTESIAN_POINT('Ctrl Pts',(-2.4556359465412,1.23079007457349,7.50491486231392));
#394845=CARTESIAN_POINT('Ctrl Pts',(-2.45552551198023,1.23105487409868,
7.50468370960993));
#394846=CARTESIAN_POINT('Ctrl Pts',(-2.45536037747697,1.23145083291511,
7.50433806340447));
#394847=CARTESIAN_POINT('Ctrl Pts',(-2.45514474366126,1.23188901991197,
7.50405484070984));
#394848=CARTESIAN_POINT('Ctrl Pts',(-2.45489249028929,1.23233960769464,
7.50385766036131));
#394849=CARTESIAN_POINT('Ctrl Pts',(-2.45486551571206,1.23238779105428,
7.50383657498791));
#394850=CARTESIAN_POINT('Ctrl Pts',(-2.45483814690575,1.23243610195336,
7.50381643264937));
#394851=CARTESIAN_POINT('Ctrl Pts',(-2.45481041881371,1.23248449383457,
7.50379723213559));
#394852=CARTESIAN_POINT('Ctrl Pts',(-2.45462532472886,1.23280752547176,
7.50366906242519));
#394853=CARTESIAN_POINT('Ctrl Pts',(-2.45441957075851,1.2331408348767,7.50358235568538));
#394854=CARTESIAN_POINT('Ctrl Pts',(-2.45421352660267,1.23345733688093,
7.5035341175365));
#394855=CARTESIAN_POINT('Ctrl Pts',(-2.45390458671067,1.23393189581515,
7.50346178989176));
#394856=CARTESIAN_POINT('Ctrl Pts',(-2.45355205999194,1.23442927747068,
7.50346967198527));
#394857=CARTESIAN_POINT('Ctrl Pts',(-2.45319096374893,1.23490690351011,
7.50354272648692));
#394858=CARTESIAN_POINT('Ctrl Pts',(-2.45304243738993,1.2351033609864,7.50357277531559));
#394859=CARTESIAN_POINT('Ctrl Pts',(-2.45289277165098,1.23529630060036,
7.50361331098761));
#394860=CARTESIAN_POINT('Ctrl Pts',(-2.45274559607636,1.23548210682036,
7.50366116523658));
#394861=CARTESIAN_POINT('',(-2.37073694677487,1.23681194660317,7.57603338622103));
#394862=CARTESIAN_POINT('Origin',(-2.37857045058673,1.24090189863625,7.58486873427629));
#394863=CARTESIAN_POINT('Ctrl Pts',(-2.45274559613209,1.23548210681344,
7.50366116529969));
#394864=CARTESIAN_POINT('Ctrl Pts',(-2.4254540003185,1.23592549913166,7.52783573079709));
#394865=CARTESIAN_POINT('Ctrl Pts',(-2.39811907485907,1.23636877604877,
7.55196141284068));
#394866=CARTESIAN_POINT('Ctrl Pts',(-2.37073694797006,1.23681194623011,
7.57603338728831));
#394867=CARTESIAN_POINT('Ctrl Pts',(-2.36887194462182,1.22871860183693,
7.59642833564546));
#394868=CARTESIAN_POINT('Ctrl Pts',(-2.35069119251645,1.22667677287982,
7.59959882295468));
#394869=CARTESIAN_POINT('Ctrl Pts',(-2.36315354717508,1.24004694984633,
7.59639677331371));
#394870=CARTESIAN_POINT('Ctrl Pts',(-2.3651741996041,1.22766241933315,7.58710240504253));
#394871=CARTESIAN_POINT('Ctrl Pts',(-2.35925575920166,1.23093143508659,
7.58809943920599));
#394872=CARTESIAN_POINT('Ctrl Pts',(-2.36006987607439,1.23765821029868,
7.58707626057422));
#394873=CARTESIAN_POINT('Ctrl Pts',(-2.3680016658602,1.2330268329137,7.58020924244127));
#394874=CARTESIAN_POINT('Ctrl Pts',(-2.36537997734295,1.23405339238908,
7.58205880659761));
#394875=CARTESIAN_POINT('Ctrl Pts',(-2.36608778108834,1.23681532744518,
7.58015376756929));
#394876=CARTESIAN_POINT('Ctrl Pts',(-2.37073694604124,1.23681194622021,
7.57603338509286));
#394877=CARTESIAN_POINT('Ctrl Pts',(-2.37073694604124,1.23681194622021,
7.57603338509286));
#394878=CARTESIAN_POINT('Ctrl Pts',(-2.37073694604124,1.23681194622021,
7.57603338509286));
#394879=CARTESIAN_POINT('Origin',(-2.37857308999325,1.24089683938839,7.58486873427622));
#394880=CARTESIAN_POINT('Ctrl Pts',(-2.4149182358073,1.31742119048616,7.51098857897448));
#394881=CARTESIAN_POINT('Ctrl Pts',(-2.41163534588056,1.31253415194521,
7.50433767179957));
#394882=CARTESIAN_POINT('Ctrl Pts',(-2.41751815819881,1.3062492040289,7.50214974420965));
#394883=CARTESIAN_POINT('Ctrl Pts',(-2.39735246464699,1.29127209545777,
7.53887321589167));
#394884=CARTESIAN_POINT('Ctrl Pts',(-2.39410890956764,1.28644361231146,
7.53220407452061));
#394885=CARTESIAN_POINT('Ctrl Pts',(-2.39993004937042,1.2801414498795,7.53003438070911));
#394886=CARTESIAN_POINT('Ctrl Pts',(-2.3797529607263,1.26507278452091,7.56669465659233));
#394887=CARTESIAN_POINT('Ctrl Pts',(-2.37652857445444,1.26027283681232,
7.56004085833301));
#394888=CARTESIAN_POINT('Ctrl Pts',(-2.38230781672175,1.25398499068331,
7.55785582193789));
#394889=CARTESIAN_POINT('Ctrl Pts',(-2.36212052000036,1.23882444256557,
7.59443891967696));
#394890=CARTESIAN_POINT('Ctrl Pts',(-2.35889145876986,1.2340175355304,7.58783901202978));
#394891=CARTESIAN_POINT('Ctrl Pts',(-2.36465226193378,1.22778116439849,
7.58560008491213));
#394892=CARTESIAN_POINT('',(-2.41656476362038,1.30483398889125,7.50366116523517));
#394893=CARTESIAN_POINT('Ctrl Pts',(-2.41656476362071,1.30483398889143,
7.50366116523554));
#394894=CARTESIAN_POINT('Ctrl Pts',(-2.41634661309173,1.30555962506988,
7.50350835821027));
#394895=CARTESIAN_POINT('Ctrl Pts',(-2.41612247199273,1.30621956353586,
7.50345484956));
#394896=CARTESIAN_POINT('Ctrl Pts',(-2.41588624502761,1.30683361791564,
7.50349758195598));
#394897=CARTESIAN_POINT('Ctrl Pts',(-2.41576504307545,1.30714867335193,
7.50351950684424));
#394898=CARTESIAN_POINT('Ctrl Pts',(-2.41562883423953,1.30748274963568,
7.50357029184312));
#394899=CARTESIAN_POINT('Ctrl Pts',(-2.41548863447409,1.30780128515435,
7.50365515313924));
#394900=CARTESIAN_POINT('Ctrl Pts',(-2.41527295046235,1.30829132176983,
7.50378570417639));
#394901=CARTESIAN_POINT('Ctrl Pts',(-2.41504180768278,1.30875910258839,
7.5040000162191));
#394902=CARTESIAN_POINT('Ctrl Pts',(-2.41481076397667,1.30916801691215,
7.50428903009634));
#394903=CARTESIAN_POINT('Ctrl Pts',(-2.41478511990283,1.3092134032561,7.50432110841317));
#394904=CARTESIAN_POINT('Ctrl Pts',(-2.41475947975432,1.30925809460095,
7.50435406373354));
#394905=CARTESIAN_POINT('Ctrl Pts',(-2.41473386649755,1.30930206320099,
7.50438785222352));
#394906=CARTESIAN_POINT('Ctrl Pts',(-2.41457748525366,1.30957051263823,
7.50459414719561));
#394907=CARTESIAN_POINT('Ctrl Pts',(-2.41441917105306,1.30981603477639,
7.50483629897752));
#394908=CARTESIAN_POINT('Ctrl Pts',(-2.41426609490187,1.3100299369134,7.5050991045531));
#394909=CARTESIAN_POINT('Ctrl Pts',(-2.4139283935373,1.31050182651207,7.50567888004914));
#394910=CARTESIAN_POINT('Ctrl Pts',(-2.41360330086178,1.31083872331851,
7.50637912803144));
#394911=CARTESIAN_POINT('Ctrl Pts',(-2.41330668489004,1.31106715325335,
7.50710440483569));
#394912=CARTESIAN_POINT('Ctrl Pts',(-2.41323394876512,1.31112316880834,
7.50728225710685));
#394913=CARTESIAN_POINT('Ctrl Pts',(-2.41316156611972,1.31117389268141,
7.50746498566954));
#394914=CARTESIAN_POINT('Ctrl Pts',(-2.41309146567674,1.31121848197555,
7.50764697238949));
#394915=CARTESIAN_POINT('Ctrl Pts',(-2.41271462498741,1.31145818174955,
7.50862528291181));
#394916=CARTESIAN_POINT('Ctrl Pts',(-2.41237174905258,1.31154585365798,
7.50965856837421));
#394917=CARTESIAN_POINT('Ctrl Pts',(-2.41206139769779,1.31154777983825,
7.51067959873202));
#394918=CARTESIAN_POINT('Ctrl Pts',(-2.41189061095578,1.31154883981768,
7.51124147302578));
#394919=CARTESIAN_POINT('Ctrl Pts',(-2.4117296293047,1.31152349915077,7.51180065547253));
#394920=CARTESIAN_POINT('Ctrl Pts',(-2.41157829503252,1.31148008890244,
7.51235175716501));
#394921=CARTESIAN_POINT('Ctrl Pts',(-2.41105537483772,1.31133008920184,
7.51425603304537));
#394922=CARTESIAN_POINT('Ctrl Pts',(-2.41058696594893,1.31094062862544,
7.51626900505183));
#394923=CARTESIAN_POINT('Ctrl Pts',(-2.4101839450164,1.31037107354313,7.51827788969247));
#394924=CARTESIAN_POINT('Ctrl Pts',(-2.41016213276193,1.31034024814577,
7.51838661432548));
#394925=CARTESIAN_POINT('Ctrl Pts',(-2.41014051310064,1.31030888531404,
7.51849533314857));
#394926=CARTESIAN_POINT('Ctrl Pts',(-2.41011908817658,1.31027699133284,
7.51860402984325));
#394927=CARTESIAN_POINT('Ctrl Pts',(-2.37073694715362,1.23681194779763,
7.57603338728985));
#394928=CARTESIAN_POINT('Ctrl Pts',(-2.38603924225309,1.25952355359294,
7.55196141284922));
#394929=CARTESIAN_POINT('Ctrl Pts',(-2.40131444509586,1.28219650716416,
7.52783573083104));
#394930=CARTESIAN_POINT('Ctrl Pts',(-2.4165647636488,1.30483398894316,7.50366116530176));
#394931=CARTESIAN_POINT('Origin',(-8.19199203866632E-16,4.27375699935086E-16,
7.49482233047033));
#394932=CARTESIAN_POINT('Origin',(-2.44485166369885,1.23150582317298,7.49482233047033));
#394933=CARTESIAN_POINT('Origin',(0.,0.,7.50366116523517));
#394934=CARTESIAN_POINT('Origin',(-2.40878727587059,1.30063450269627,7.49482233047033));
#394935=CARTESIAN_POINT('Ctrl Pts',(-2.45352105979441,1.22708152881661,
7.51860402984325));
#394936=CARTESIAN_POINT('Ctrl Pts',(-2.46112885786552,1.22694850799356,
7.51860402984325));
#394937=CARTESIAN_POINT('Ctrl Pts',(-2.46450482787546,1.22012948221841,
7.51860402984325));
#394938=CARTESIAN_POINT('Ctrl Pts',(-2.45634588711432,1.22703213600669,
7.51041458714366));
#394939=CARTESIAN_POINT('Ctrl Pts',(-2.4619286549569,1.22533299829127,7.51004642900443));
#394940=CARTESIAN_POINT('Ctrl Pts',(-2.46450575892791,1.22012760161206,
7.5072913648301));
#394941=CARTESIAN_POINT('Ctrl Pts',(-2.45736298124953,1.22965687536887,
7.50215815450137));
#394942=CARTESIAN_POINT('Ctrl Pts',(-2.46030031409413,1.2286223995395,7.49877163671529));
#394943=CARTESIAN_POINT('Ctrl Pts',(-2.46185245611965,1.22554103965677,
7.4948158853317));
#394944=CARTESIAN_POINT('Ctrl Pts',(-2.45274510440916,1.23548185916128,
7.50366171572174));
#394945=CARTESIAN_POINT('Ctrl Pts',(-2.45601536992562,1.23712913743439,
7.50000045605858));
#394946=CARTESIAN_POINT('Ctrl Pts',(-2.45601536992567,1.23712913743428,
7.49482233047317));
#394947=CARTESIAN_POINT('Origin',(-2.4533025332033,1.21458343911742,7.51860402984325));
#394948=CARTESIAN_POINT('Origin',(-2.4533025332033,1.21458343911742,9.));
#394949=CARTESIAN_POINT('Origin',(-2.4533025332033,1.21458343911742,8.75721825406948));
#394950=CARTESIAN_POINT('Ctrl Pts',(-2.43682453266412,1.22737484732811,
8.78942910404912));
#394951=CARTESIAN_POINT('Ctrl Pts',(-2.4423964617636,1.22729716327587,8.7967269950169));
#394952=CARTESIAN_POINT('Ctrl Pts',(-2.44391314215674,1.21850096144968,
8.79893251111267));
#394953=CARTESIAN_POINT('Ctrl Pts',(-2.44781717199849,1.22718171730772,
8.78111911759584));
#394954=CARTESIAN_POINT('Ctrl Pts',(-2.45442265473791,1.22708217884976,
8.78644465894815));
#394955=CARTESIAN_POINT('Ctrl Pts',(-2.45748133310548,1.2195748492034,8.78817647674132));
#394956=CARTESIAN_POINT('Ctrl Pts',(-2.45466804703032,1.22706135404061,
8.76780923932029));
#394957=CARTESIAN_POINT('Ctrl Pts',(-2.46246546371488,1.22693875788234,
8.76988516158373));
#394958=CARTESIAN_POINT('Ctrl Pts',(-2.46595667361419,1.22023444331371,
8.77093053738832));
#394959=CARTESIAN_POINT('Ctrl Pts',(-2.45333222015989,1.22708482322868,
8.75371302330492));
#394960=CARTESIAN_POINT('Ctrl Pts',(-2.46093827577203,1.22696599817776,
8.75300828287559));
#394961=CARTESIAN_POINT('Ctrl Pts',(-2.46430367349724,1.22010533950053,
8.75267964240738));
#394962=CARTESIAN_POINT('Origin',(-2.43928211585347,1.21482977004094,8.78727029226991));
#394963=CARTESIAN_POINT('Ctrl Pts',(-2.36802027905702,1.2285837299553,8.85049129520029));
#394964=CARTESIAN_POINT('Ctrl Pts',(-2.37385899372367,1.22848114699075,
8.85711686593484));
#394965=CARTESIAN_POINT('Ctrl Pts',(-2.37566317709459,1.22012377392992,
8.85933012996512));
#394966=CARTESIAN_POINT('Ctrl Pts',(-2.39188208645152,1.22816449129032,
8.82945683644721));
#394967=CARTESIAN_POINT('Ctrl Pts',(-2.39776926598005,1.22806105682515,
8.83607469902388));
#394968=CARTESIAN_POINT('Ctrl Pts',(-2.39954208843695,1.21967123304667,
8.8382956714852));
#394969=CARTESIAN_POINT('Ctrl Pts',(-2.41570832589789,1.22774587753438,
8.80838214965002));
#394970=CARTESIAN_POINT('Ctrl Pts',(-2.42161873898548,1.2276420348685,8.81501364461985));
#394971=CARTESIAN_POINT('Ctrl Pts',(-2.42338478937515,1.2192200470618,8.81722098428721));
#394972=CARTESIAN_POINT('Ctrl Pts',(-2.43950170000243,1.22732784120418,
8.78727029226991));
#394973=CARTESIAN_POINT('Ctrl Pts',(-2.44541309482909,1.2272239812897,8.79393457792714));
#394974=CARTESIAN_POINT('Ctrl Pts',(-2.44719404240189,1.21877012767605,
8.79610912703474));
#394975=CARTESIAN_POINT('Origin',(-2.36780069490807,1.21608565879206,8.85049129520029));
#394976=CARTESIAN_POINT('Ctrl Pts',(-2.36243414091426,1.23929131094304,
8.85049129520029));
#394977=CARTESIAN_POINT('Ctrl Pts',(-2.36569043114742,1.24413875213819,
8.85711686593484));
#394978=CARTESIAN_POINT('Ctrl Pts',(-2.35986814900603,1.25039988564418,
8.85933012996512));
#394979=CARTESIAN_POINT('Ctrl Pts',(-2.35955334795002,1.23500284969123,
8.86332496987233));
#394980=CARTESIAN_POINT('Ctrl Pts',(-2.35767030474023,1.23922257037475,
8.86648636486738));
#394981=CARTESIAN_POINT('Ctrl Pts',(-2.35182323496412,1.23839318691327,
8.87206031107457));
#394982=CARTESIAN_POINT('Ctrl Pts',(-2.36281975177212,1.22867510032302,
8.86341338519876));
#394983=CARTESIAN_POINT('Ctrl Pts',(-2.36518469322302,1.22469006298717,
8.86654584966059));
#394984=CARTESIAN_POINT('Ctrl Pts',(-2.3611016831163,1.22039434636991,8.87215952290714));
#394985=CARTESIAN_POINT('Ctrl Pts',(-2.36802027905702,1.2285837299553,8.85049129520029));
#394986=CARTESIAN_POINT('Ctrl Pts',(-2.37385899372367,1.22848114699075,
8.85711686593484));
#394987=CARTESIAN_POINT('Ctrl Pts',(-2.37566317709459,1.22012377392992,
8.85933012996512));
#394988=CARTESIAN_POINT('Origin',(-2.35205794196027,1.24626156884839,8.85049129520029));
#394989=CARTESIAN_POINT('Ctrl Pts',(-2.4022998076178,1.2986369039994,8.78727029226991));
#394990=CARTESIAN_POINT('Ctrl Pts',(-2.40559663206247,1.30354468600958,
8.79393457792714));
#394991=CARTESIAN_POINT('Ctrl Pts',(-2.39968192566133,1.30984196029029,
8.79610912703474));
#394992=CARTESIAN_POINT('Ctrl Pts',(-2.38903008369151,1.27888307316657,
8.80838214965001));
#394993=CARTESIAN_POINT('Ctrl Pts',(-2.39232636061377,1.28379004011346,
8.81501364461993));
#394994=CARTESIAN_POINT('Ctrl Pts',(-2.38642926673666,1.29005686517878,
8.81722098428721));
#394995=CARTESIAN_POINT('Ctrl Pts',(-2.3757420305442,1.25910195673734,8.82945683644722));
#394996=CARTESIAN_POINT('Ctrl Pts',(-2.37902534995512,1.26398963462523,
8.83607469902389));
#394997=CARTESIAN_POINT('Ctrl Pts',(-2.37315851053408,1.27024361237586,
8.83829567148519));
#394998=CARTESIAN_POINT('Ctrl Pts',(-2.36243414091426,1.23929131094303,
8.85049129520029));
#394999=CARTESIAN_POINT('Ctrl Pts',(-2.36569043114742,1.24413875213819,
8.85711686593484));
#395000=CARTESIAN_POINT('Ctrl Pts',(-2.35986814900603,1.25039988564418,
8.85933012996512));
#395001=CARTESIAN_POINT('Origin',(-2.39192360866381,1.30560716190476,8.78727029226991));
#395002=CARTESIAN_POINT('Ctrl Pts',(-2.41001582319738,1.31012330012151,
8.75374538247848));
#395003=CARTESIAN_POINT('Ctrl Pts',(-2.41426405357149,1.31642384907189,
8.75304829418601));
#395004=CARTESIAN_POINT('Ctrl Pts',(-2.41057140660495,1.32310479223806,
8.75272238421917));
#395005=CARTESIAN_POINT('Ctrl Pts',(-2.41075187368563,1.31121901294559,
8.76769408445018));
#395006=CARTESIAN_POINT('Ctrl Pts',(-2.4151064361957,1.31767849746975,8.76974318093969));
#395007=CARTESIAN_POINT('Ctrl Pts',(-2.41161165479856,1.32437214074276,
8.7707786988043));
#395008=CARTESIAN_POINT('Ctrl Pts',(-2.4069792981955,1.30560301318754,8.78108014887992));
#395009=CARTESIAN_POINT('Ctrl Pts',(-2.41067278344333,1.31107506984152,
8.78639403366326));
#395010=CARTESIAN_POINT('Ctrl Pts',(-2.40628851871305,1.31787950211056,
8.78812224174741));
#395011=CARTESIAN_POINT('Ctrl Pts',(-2.40079687974256,1.29639962934832,
8.78944554828684));
#395012=CARTESIAN_POINT('Ctrl Pts',(-2.40391425189901,1.3010081441259,8.79673892988686));
#395013=CARTESIAN_POINT('Ctrl Pts',(-2.39757616771974,1.30727968646036,
8.79894799272499));
#395014=CARTESIAN_POINT('Origin',(-2.39974288922259,1.3172472492382,8.75721825406948));
#395015=CARTESIAN_POINT('Origin',(-2.39974288922259,1.3172472492382,9.));
#395016=CARTESIAN_POINT('Origin',(-2.39974288922259,1.3172472492382,7.51860402984325));
#395017=CARTESIAN_POINT('Ctrl Pts',(-2.41656407141737,1.30483361513348,
7.50366195182967));
#395018=CARTESIAN_POINT('Ctrl Pts',(-2.41978630452746,1.30657347302834,
7.50000065167736));
#395019=CARTESIAN_POINT('Ctrl Pts',(-2.41978630452741,1.30657347302844,
7.49482233047108));
#395020=CARTESIAN_POINT('Ctrl Pts',(-2.41442578748734,1.31195973198919,
7.50215800491335));
#395021=CARTESIAN_POINT('Ctrl Pts',(-2.41525681547057,1.31496207934841,
7.49877273257265));
#395022=CARTESIAN_POINT('Ctrl Pts',(-2.41361667159588,1.31799969097933,
7.49481816995647));
#395023=CARTESIAN_POINT('Ctrl Pts',(-2.41169107100776,1.31261649840007,
7.51043025814043));
#395024=CARTESIAN_POINT('Ctrl Pts',(-2.41349603202947,1.3181694140934,7.51006209594515));
#395025=CARTESIAN_POINT('Ctrl Pts',(-2.41069940101147,1.32326429634045,
7.507312818217));
#395026=CARTESIAN_POINT('Ctrl Pts',(-2.41011824530876,1.31027573677064,
7.51860402984325));
#395027=CARTESIAN_POINT('Ctrl Pts',(-2.41436209596894,1.31659164913267,
7.51860402984325));
#395028=CARTESIAN_POINT('Ctrl Pts',(-2.41070061931037,1.3232620768603,7.51860402984325));
#395029=CARTESIAN_POINT('Origin',(0.,0.,7.5));
#395030=CARTESIAN_POINT('Origin',(-2.43698193351379,1.0853833789328,7.5));
#395031=CARTESIAN_POINT('',(-2.43698193351379,1.0853833789328,7.59394543036555));
#395032=CARTESIAN_POINT('',(-2.43698193351379,1.0853833789328,8.85049129520029));
#395033=CARTESIAN_POINT('',(-2.43698193351379,1.0853833789328,7.5));
#395034=CARTESIAN_POINT('',(-2.48056797713152,1.14205283806807,8.78727029226991));
#395035=CARTESIAN_POINT('Ctrl Pts',(-2.43698193351379,1.0853833789328,8.85049129520029));
#395036=CARTESIAN_POINT('Ctrl Pts',(-2.45153173356486,1.10430065682689,
8.82945686509571));
#395037=CARTESIAN_POINT('Ctrl Pts',(-2.46605990357881,1.12318981189994,
8.80838212259895));
#395038=CARTESIAN_POINT('Ctrl Pts',(-2.48056797713152,1.14205283806807,
8.78727029226991));
#395039=CARTESIAN_POINT('',(-2.48911697509583,1.15316802656819,8.75721825406948));
#395040=CARTESIAN_POINT('Origin',(-2.4633902345141,1.11971844545421,8.75937679713085));
#395041=CARTESIAN_POINT('',(-2.48911697509583,1.15316802656819,7.51860402984325));
#395042=CARTESIAN_POINT('',(-2.48911697509583,1.15316802656819,7.5));
#395043=CARTESIAN_POINT('Ctrl Pts',(-2.48911697509583,1.15316802656819,
7.51860402984325));
#395044=CARTESIAN_POINT('Ctrl Pts',(-2.48240306681555,1.14443877474015,
7.52834476460825));
#395045=CARTESIAN_POINT('Ctrl Pts',(-2.4756847999629,1.13570385600777,7.53807742314407));
#395046=CARTESIAN_POINT('Ctrl Pts',(-2.468962028193,1.12696308009723,7.54780169004674));
#395047=CARTESIAN_POINT('Ctrl Pts',(-2.4583135210443,1.11311816345355,7.5632044032688));
#395048=CARTESIAN_POINT('Ctrl Pts',(-2.4476536980993,1.09925853430098,7.57858609112103));
#395049=CARTESIAN_POINT('Ctrl Pts',(-2.43698193351379,1.0853833789328,7.59394543036555));
#395050=CARTESIAN_POINT('Origin',(-2.71595367934704,1.05190237523112,7.5));
#395051=CARTESIAN_POINT('',(-2.52710047532068,1.06736263792741,8.75721825406948));
#395052=CARTESIAN_POINT('',(-2.51312464689845,1.06850675396145,8.78727029226991));
#395053=CARTESIAN_POINT('Origin',(-2.47764878163776,1.07141094718992,8.75658640621009));
#395054=CARTESIAN_POINT('',(-2.44187055726728,1.07433989271894,8.85049129520029));
#395055=CARTESIAN_POINT('Ctrl Pts',(-2.51312464689845,1.06850675396145,
8.78727029226991));
#395056=CARTESIAN_POINT('Ctrl Pts',(-2.48940697290247,1.07044837561629,
8.80838212259896));
#395057=CARTESIAN_POINT('Ctrl Pts',(-2.46565644538429,1.07239268678908,
8.82945686509571));
#395058=CARTESIAN_POINT('Ctrl Pts',(-2.44187055726729,1.07433989271894,
8.85049129520029));
#395059=CARTESIAN_POINT('',(-2.44187055726728,1.07433989271894,7.59394543036555));
#395060=CARTESIAN_POINT('',(-2.44187055726728,1.07433989271894,7.5));
#395061=CARTESIAN_POINT('',(-2.52710047532068,1.06736263792741,7.51860402984325));
#395062=CARTESIAN_POINT('Ctrl Pts',(-2.44187055726728,1.07433989271894,
7.59394543036555));
#395063=CARTESIAN_POINT('Ctrl Pts',(-2.45931666632384,1.07291168592503,
7.57858609112103));
#395064=CARTESIAN_POINT('Ctrl Pts',(-2.47674325328886,1.07148507728598,
7.56320440326857));
#395065=CARTESIAN_POINT('Ctrl Pts',(-2.49415134128754,1.07005998304473,
7.54780169004651));
#395066=CARTESIAN_POINT('Ctrl Pts',(-2.50514167081741,1.0691602716391,7.53807742314383));
#395067=CARTESIAN_POINT('Ctrl Pts',(-2.51612463574748,1.06826116312845,
7.52834476460825));
#395068=CARTESIAN_POINT('Ctrl Pts',(-2.52710047532068,1.06736263792741,
7.51860402984325));
#395069=CARTESIAN_POINT('',(-2.52710047532068,1.06736263792741,7.5));
#395070=CARTESIAN_POINT('Origin',(-2.44243149520448,1.08119197077094,7.5));
#395071=CARTESIAN_POINT('Ctrl Pts',(-2.44187055726728,1.07433989271894,
8.85049129520029));
#395072=CARTESIAN_POINT('Ctrl Pts',(-2.44167754144849,1.07435569374958,
8.85097269580138));
#395073=CARTESIAN_POINT('Ctrl Pts',(-2.44148764717679,1.07437967878895,
8.85143669361005));
#395074=CARTESIAN_POINT('Ctrl Pts',(-2.44129223999293,1.07441381966454,
8.8519052845931));
#395075=CARTESIAN_POINT('Ctrl Pts',(-2.44091003593357,1.07448059705206,
8.85282181883899));
#395076=CARTESIAN_POINT('Ctrl Pts',(-2.44051660708415,1.07458470358959,
8.85372622499635));
#395077=CARTESIAN_POINT('Ctrl Pts',(-2.44010972412279,1.07474267860363,
8.8546225773507));
#395078=CARTESIAN_POINT('Ctrl Pts',(-2.43977194433938,1.07487382384955,
8.85536669723986));
#395079=CARTESIAN_POINT('Ctrl Pts',(-2.43942480388501,1.0750420942402,8.85610498449051));
#395080=CARTESIAN_POINT('Ctrl Pts',(-2.439070488446,1.0752641679127,8.85681338218371));
#395081=CARTESIAN_POINT('Ctrl Pts',(-2.43874894662864,1.07546570011927,
8.85745625420285));
#395082=CARTESIAN_POINT('Ctrl Pts',(-2.43841714453212,1.07571356340656,
8.85808743050666));
#395083=CARTESIAN_POINT('Ctrl Pts',(-2.43808062970449,1.07603581255776,
8.85866804508411));
#395084=CARTESIAN_POINT('Ctrl Pts',(-2.43792536905776,1.07618449133062,
8.85893592806396));
#395085=CARTESIAN_POINT('Ctrl Pts',(-2.43776918026209,1.07634923507315,
8.85919241173848));
#395086=CARTESIAN_POINT('Ctrl Pts',(-2.43761330950698,1.07653423293663,
8.85943017985534));
#395087=CARTESIAN_POINT('Ctrl Pts',(-2.4374028378449,1.07678403481755,8.8597512372));
#395088=CARTESIAN_POINT('Ctrl Pts',(-2.43718807887067,1.0770775368641,8.86004599534706));
#395089=CARTESIAN_POINT('Ctrl Pts',(-2.43698001810968,1.07741736300177,
8.86026130871721));
#395090=CARTESIAN_POINT('Ctrl Pts',(-2.43690384119922,1.07754178293148,
8.86034014101235));
#395091=CARTESIAN_POINT('Ctrl Pts',(-2.43682740741169,1.07767427508624,
8.86040910639692));
#395092=CARTESIAN_POINT('Ctrl Pts',(-2.4367530905129,1.07781139788106,8.86046313645506));
#395093=CARTESIAN_POINT('Ctrl Pts',(-2.43663711961473,1.07802537685398,
8.86054744990829));
#395094=CARTESIAN_POINT('Ctrl Pts',(-2.43652326724304,1.07825654310182,
8.86059655985668));
#395095=CARTESIAN_POINT('Ctrl Pts',(-2.43641857228559,1.07848994179131,
8.86059725258816));
#395096=CARTESIAN_POINT('Ctrl Pts',(-2.43631363544096,1.07872387972501,
8.86059794692011));
#395097=CARTESIAN_POINT('Ctrl Pts',(-2.43621915867709,1.07896374218055,
8.86056369958366));
#395098=CARTESIAN_POINT('Ctrl Pts',(-2.4361367935118,1.0791950678586,8.86048590497774));
#395099=CARTESIAN_POINT('Ctrl Pts',(-2.43611529865597,1.07925543697317,
8.86046560290182));
#395100=CARTESIAN_POINT('Ctrl Pts',(-2.43609443436159,1.07931604043715,
8.86044257503091));
#395101=CARTESIAN_POINT('Ctrl Pts',(-2.43607481431438,1.07937499486763,
8.86041778462584));
#395102=CARTESIAN_POINT('Ctrl Pts',(-2.43594279574309,1.07977168502834,
8.86025097596201));
#395103=CARTESIAN_POINT('Ctrl Pts',(-2.43584971171547,1.08014704858014,
8.8599848982295));
#395104=CARTESIAN_POINT('Ctrl Pts',(-2.43579005570161,1.08048809037632,
8.85968173251461));
#395105=CARTESIAN_POINT('Ctrl Pts',(-2.43575850108816,1.08066848194713,
8.85952137522076));
#395106=CARTESIAN_POINT('Ctrl Pts',(-2.43573550263548,1.08084271523859,
8.85934740853961));
#395107=CARTESIAN_POINT('Ctrl Pts',(-2.4357198434887,1.08100812974289,8.8591675900182));
#395108=CARTESIAN_POINT('Ctrl Pts',(-2.43565696387494,1.08167235495841,
8.85844552518696));
#395109=CARTESIAN_POINT('Ctrl Pts',(-2.43570585991415,1.08223163783065,
8.85759444184126));
#395110=CARTESIAN_POINT('Ctrl Pts',(-2.43578668621989,1.08268406612752,
8.85683498915141));
#395111=CARTESIAN_POINT('Ctrl Pts',(-2.43579514447753,1.08273141154388,
8.85675551445));
#395112=CARTESIAN_POINT('Ctrl Pts',(-2.43580397099506,1.08277757949648,
8.85667699793652));
#395113=CARTESIAN_POINT('Ctrl Pts',(-2.4358130862329,1.08282256237296,8.85659965593547));
#395114=CARTESIAN_POINT('Ctrl Pts',(-2.43593612417827,1.08342974353503,
8.85555568965886));
#395115=CARTESIAN_POINT('Ctrl Pts',(-2.43614206024081,1.08399551313591,
8.85434650606346));
#395116=CARTESIAN_POINT('Ctrl Pts',(-2.43642607255145,1.08452479370298,
8.85297329937117));
#395117=CARTESIAN_POINT('Ctrl Pts',(-2.43658581217106,1.08482248177242,
8.85220095427747));
#395118=CARTESIAN_POINT('Ctrl Pts',(-2.43677059316373,1.085108599615,8.85137579139183));
#395119=CARTESIAN_POINT('Ctrl Pts',(-2.43698193351379,1.0853833789328,8.85049129520029));
#395120=CARTESIAN_POINT('Origin',(-2.44243149520448,1.08119197077094,7.59394543036555));
#395121=CARTESIAN_POINT('Ctrl Pts',(-2.44131016723206,1.07438576844132,
7.59443877723642));
#395122=CARTESIAN_POINT('Ctrl Pts',(-2.43553868906203,1.07485824424131,
7.58783886950016));
#395123=CARTESIAN_POINT('Ctrl Pts',(-2.4342546998631,1.08325053554189,7.58559994247159));
#395124=CARTESIAN_POINT('Ctrl Pts',(-2.47281649723427,1.07180653691098,
7.56670252222137));
#395125=CARTESIAN_POINT('Ctrl Pts',(-2.46705336048875,1.07227832984935,
7.56004874999027));
#395126=CARTESIAN_POINT('Ctrl Pts',(-2.46574064338428,1.08071711714724,
7.55786368756704));
#395127=CARTESIAN_POINT('Ctrl Pts',(-2.50426399231304,1.06923212183783,
7.53888913333556));
#395128=CARTESIAN_POINT('Ctrl Pts',(-2.49846660496366,1.0697067186647,7.53222002137274));
#395129=CARTESIAN_POINT('Ctrl Pts',(-2.49716881203071,1.07818717727394,
7.53005029815327));
#395130=CARTESIAN_POINT('Ctrl Pts',(-2.53565122944802,1.06666263971588,
7.51101258149734));
#395131=CARTESIAN_POINT('Ctrl Pts',(-2.52978356722986,1.06714298951865,
7.5043616886572));
#395132=CARTESIAN_POINT('Ctrl Pts',(-2.52853765964446,1.07566092329588,
7.50217374673251));
#395133=CARTESIAN_POINT('',(-2.52686377755799,1.07579572642896,7.50366116523517));
#395134=CARTESIAN_POINT('Ctrl Pts',(-2.52710047532068,1.06736263792741,
7.51860402984325));
#395135=CARTESIAN_POINT('Ctrl Pts',(-2.52754061415969,1.06732660643878,
7.51734760759493));
#395136=CARTESIAN_POINT('Ctrl Pts',(-2.5279431969395,1.06735334527536,7.51608817408572));
#395137=CARTESIAN_POINT('Ctrl Pts',(-2.52830641272848,1.06745611722429,
7.51481005913119));
#395138=CARTESIAN_POINT('Ctrl Pts',(-2.52863542226947,1.06754921051145,
7.51365231206383));
#395139=CARTESIAN_POINT('Ctrl Pts',(-2.5289326624055,1.0677045807592,7.51247773061042));
#395140=CARTESIAN_POINT('Ctrl Pts',(-2.52917588459346,1.06795226365134,
7.51129758471022));
#395141=CARTESIAN_POINT('Ctrl Pts',(-2.52947818199606,1.06826010519982,
7.50983079813402));
#395142=CARTESIAN_POINT('Ctrl Pts',(-2.52967809354276,1.06870984917595,
7.50839324291155));
#395143=CARTESIAN_POINT('Ctrl Pts',(-2.52970174557798,1.06933826341191,
7.50715379678855));
#395144=CARTESIAN_POINT('Ctrl Pts',(-2.52971267213673,1.0696285726816,7.50658120839351));
#395145=CARTESIAN_POINT('Ctrl Pts',(-2.52967804016153,1.06999864075057,
7.50598221009429));
#395146=CARTESIAN_POINT('Ctrl Pts',(-2.52957602630725,1.07043754110358,
7.50545747549611));
#395147=CARTESIAN_POINT('Ctrl Pts',(-2.52952158855699,1.07067175191719,
7.50517746087247));
#395148=CARTESIAN_POINT('Ctrl Pts',(-2.5294475699509,1.07092814907601,7.50491486231392));
#395149=CARTESIAN_POINT('Ctrl Pts',(-2.52935432805341,1.0711994801088,7.50468370960993));
#395150=CARTESIAN_POINT('Ctrl Pts',(-2.52921490200517,1.07160520558933,
7.50433806340447));
#395151=CARTESIAN_POINT('Ctrl Pts',(-2.52902778596954,1.07205630799002,
7.50405484070984));
#395152=CARTESIAN_POINT('Ctrl Pts',(-2.52880492013753,1.0725221319208,7.50385766036131));
#395153=CARTESIAN_POINT('Ctrl Pts',(-2.52878108810092,1.07257194454966,
7.50383657498791));
#395154=CARTESIAN_POINT('Ctrl Pts',(-2.52875687081669,1.07262190971424,
7.50381643264937));
#395155=CARTESIAN_POINT('Ctrl Pts',(-2.52873230017346,1.0726719787141,7.50379723213559));
#395156=CARTESIAN_POINT('Ctrl Pts',(-2.52856828309231,1.07300620566688,
7.50366906242519));
#395157=CARTESIAN_POINT('Ctrl Pts',(-2.52838430707247,1.07335201295404,
7.50358235568538));
#395158=CARTESIAN_POINT('Ctrl Pts',(-2.52819896460947,1.07368106596535,
7.5035341175365));
#395159=CARTESIAN_POINT('Ctrl Pts',(-2.52792106456293,1.07417444371418,
7.50346178989176));
#395160=CARTESIAN_POINT('Ctrl Pts',(-2.52760112950023,1.07469338991018,
7.50346967198527));
#395161=CARTESIAN_POINT('Ctrl Pts',(-2.5272713767736,1.07519317013141,7.50354272648692));
#395162=CARTESIAN_POINT('Ctrl Pts',(-2.52713574265166,1.07539874008124,
7.50357277531559));
#395163=CARTESIAN_POINT('Ctrl Pts',(-2.52699874610053,1.07560087239689,
7.50361331098761));
#395164=CARTESIAN_POINT('Ctrl Pts',(-2.5268637775593,1.07579572642952,7.50366116523659));
#395165=CARTESIAN_POINT('',(-2.44510882695062,1.08237714611494,7.57603338622103));
#395166=CARTESIAN_POINT('Origin',(-2.45318828011502,1.08595680059032,7.58486873427628));
#395167=CARTESIAN_POINT('Ctrl Pts',(-2.52686377761447,1.07579572641904,
7.50366116529969));
#395168=CARTESIAN_POINT('Ctrl Pts',(-2.49965666355485,1.0779867862876,7.52783573079709));
#395169=CARTESIAN_POINT('Ctrl Pts',(-2.47240630148104,1.08018050713207,
7.55196141284069));
#395170=CARTESIAN_POINT('Ctrl Pts',(-2.44510882811945,1.08237714566607,
7.57603338728831));
#395171=CARTESIAN_POINT('Ctrl Pts',(-2.44290988201821,1.07443121403224,
7.59639677331372));
#395172=CARTESIAN_POINT('Ctrl Pts',(-2.42383037731441,1.07295780766364,
7.59974925422225));
#395173=CARTESIAN_POINT('Ctrl Pts',(-2.43774827562803,1.08609137277752,
7.59639677331371));
#395174=CARTESIAN_POINT('Ctrl Pts',(-2.43911965275287,1.07350965763145,
7.58707626057423));
#395175=CARTESIAN_POINT('Ctrl Pts',(-2.43325291397481,1.07712888513353,
7.58811717123965));
#395176=CARTESIAN_POINT('Ctrl Pts',(-2.43451789319206,1.08390511263723,
7.58707626057423));
#395177=CARTESIAN_POINT('Ctrl Pts',(-2.44221276280681,1.0787401740931,7.5801537675693));
#395178=CARTESIAN_POINT('Ctrl Pts',(-2.43957276865564,1.07992649732889,
7.5820876076604));
#395179=CARTESIAN_POINT('Ctrl Pts',(-2.4404694300849,1.08267839307892,7.5801537675693));
#395180=CARTESIAN_POINT('Ctrl Pts',(-2.44510882619396,1.08237714577977,
7.57603338509286));
#395181=CARTESIAN_POINT('Ctrl Pts',(-2.44510882619396,1.08237714577977,
7.57603338509286));
#395182=CARTESIAN_POINT('Ctrl Pts',(-2.44510882619396,1.08237714577977,
7.57603338509286));
#395183=CARTESIAN_POINT('Origin',(-2.4531905899516,1.08595158263,7.5848687342762));
#395184=CARTESIAN_POINT('Ctrl Pts',(-2.49436399277437,1.15999006475372,
7.51098857897448));
#395185=CARTESIAN_POINT('Ctrl Pts',(-2.4907747342627,1.15532340263736,7.50433767179956));
#395186=CARTESIAN_POINT('Ctrl Pts',(-2.49624278171655,1.14867445474127,
7.50214974420965));
#395187=CARTESIAN_POINT('Ctrl Pts',(-2.47515893410406,1.13502013866792,
7.53887321589168));
#395188=CARTESIAN_POINT('Ctrl Pts',(-2.47161268127916,1.13040939144553,
7.53220407452062));
#395189=CARTESIAN_POINT('Ctrl Pts',(-2.47701807999249,1.1237472157745,7.53003438070911));
#395190=CARTESIAN_POINT('Ctrl Pts',(-2.45591699463667,1.11000226111302,
7.56669465659236));
#395191=CARTESIAN_POINT('Ctrl Pts',(-2.45239169950658,1.10541876254954,
7.56004085833301));
#395192=CARTESIAN_POINT('Ctrl Pts',(-2.45775620401614,1.09877355815139,
7.5578558219379));
#395193=CARTESIAN_POINT('Ctrl Pts',(-2.43663904460805,1.08493756354744,
7.59443891967696));
#395194=CARTESIAN_POINT('Ctrl Pts',(-2.43310863823899,1.08034741948168,
7.58783901202978));
#395195=CARTESIAN_POINT('Ctrl Pts',(-2.43845803954466,1.07375476571713,
7.58560008491213));
#395196=CARTESIAN_POINT('',(-2.49520067284433,1.14732323151527,7.50366116523517));
#395197=CARTESIAN_POINT('Ctrl Pts',(-2.49520067284467,1.14732323151543,
7.50366116523554));
#395198=CARTESIAN_POINT('Ctrl Pts',(-2.49502946219894,1.1480613537489,7.50350835821027));
#395199=CARTESIAN_POINT('Ctrl Pts',(-2.49484806402455,1.14873429707004,
7.50345484956));
#395200=CARTESIAN_POINT('Ctrl Pts',(-2.49465166501225,1.14936222492287,
7.50349758195598));
#395201=CARTESIAN_POINT('Ctrl Pts',(-2.49455089775362,1.14968439847971,
7.50351950684424));
#395202=CARTESIAN_POINT('Ctrl Pts',(-2.49443637311435,1.15002651529798,
7.50357029184312));
#395203=CARTESIAN_POINT('Ctrl Pts',(-2.49431687004512,1.15035337898108,
7.50365515313923));
#395204=CARTESIAN_POINT('Ctrl Pts',(-2.49413302593306,1.15085622768587,
7.50378570417639));
#395205=CARTESIAN_POINT('Ctrl Pts',(-2.49393232888106,1.15133785676731,
7.50400001621911));
#395206=CARTESIAN_POINT('Ctrl Pts',(-2.4937279591097,1.15176073395383,7.50428903009635));
#395207=CARTESIAN_POINT('Ctrl Pts',(-2.4937052756374,1.1518076700681,7.50432110841318));
#395208=CARTESIAN_POINT('Ctrl Pts',(-2.49368255155363,1.15185391235974,
7.50435406373355));
#395209=CARTESIAN_POINT('Ctrl Pts',(-2.49365980799992,1.15189943166856,
7.50438785222352));
#395210=CARTESIAN_POINT('Ctrl Pts',(-2.49352094767257,1.15217734892834,
7.50459414719561));
#395211=CARTESIAN_POINT('Ctrl Pts',(-2.49337868940288,1.1524325098406,7.50483629897752));
#395212=CARTESIAN_POINT('Ctrl Pts',(-2.49323963252003,1.1526557801154,7.5050991045531));
#395213=CARTESIAN_POINT('Ctrl Pts',(-2.49293285906952,1.15314833676699,
7.50567888004914));
#395214=CARTESIAN_POINT('Ctrl Pts',(-2.49263001938426,1.15350537014205,
7.50637912803144));
#395215=CARTESIAN_POINT('Ctrl Pts',(-2.49234864839803,1.15375233499365,
7.50710440483569));
#395216=CARTESIAN_POINT('Ctrl Pts',(-2.49227965064621,1.1538128956782,7.50728225710685));
#395217=CARTESIAN_POINT('Ctrl Pts',(-2.49221066660843,1.15386815290565,
7.50746498566954));
#395218=CARTESIAN_POINT('Ctrl Pts',(-2.4921435670402,1.1539171419371,7.50764697238949));
#395219=CARTESIAN_POINT('Ctrl Pts',(-2.49178285822774,1.15418049348807,
7.50862528291181));
#395220=CARTESIAN_POINT('Ctrl Pts',(-2.49144630392675,1.15428995340173,
7.50965856837422));
#395221=CARTESIAN_POINT('Ctrl Pts',(-2.49113671363289,1.15431175990403,
7.51067959873202));
#395222=CARTESIAN_POINT('Ctrl Pts',(-2.49096634570368,1.15432376004975,
7.51124147302578));
#395223=CARTESIAN_POINT('Ctrl Pts',(-2.49080407122456,1.15430878557776,
7.51180065547253));
#395224=CARTESIAN_POINT('Ctrl Pts',(-2.49065026658072,1.15427516054054,
7.512351757165));
#395225=CARTESIAN_POINT('Ctrl Pts',(-2.49011881026773,1.15415897264233,
7.51425603304536));
#395226=CARTESIAN_POINT('Ctrl Pts',(-2.48962641095044,1.15380032331501,
7.5162690050518));
#395227=CARTESIAN_POINT('Ctrl Pts',(-2.48918772654822,1.15325776008451,
7.51827788969244));
#395228=CARTESIAN_POINT('Ctrl Pts',(-2.48916398411938,1.15322839553717,
7.51838661432545));
#395229=CARTESIAN_POINT('Ctrl Pts',(-2.48914039945447,1.1531984823202,7.51849533314857));
#395230=CARTESIAN_POINT('Ctrl Pts',(-2.48911697509582,1.15316802656819,
7.51860402984325));
#395231=CARTESIAN_POINT('Ctrl Pts',(-2.44510882740512,1.08237714728269,
7.57603338728985));
#395232=CARTESIAN_POINT('Ctrl Pts',(-2.46183481987753,1.10406166823487,
7.55196141284923));
#395233=CARTESIAN_POINT('Ctrl Pts',(-2.47853129930075,1.1257093521849,7.52783573083105));
#395234=CARTESIAN_POINT('Ctrl Pts',(-2.49520067287602,1.14732323156525,
7.50366116530176));
#395235=CARTESIAN_POINT('Origin',(-8.44898126352701E-16,3.74011337523909E-16,
7.49482233047033));
#395236=CARTESIAN_POINT('Origin',(-2.51873130274449,1.07233337846729,7.49482233047033));
#395237=CARTESIAN_POINT('Origin',(0.,0.,7.50366116523517));
#395238=CARTESIAN_POINT('Origin',(-2.48717010277294,1.14363067896609,7.49482233047033));
#395239=CARTESIAN_POINT('Ctrl Pts',(-2.5270994211233,1.06736272418324,7.51860402984325));
#395240=CARTESIAN_POINT('Ctrl Pts',(-2.53468306548394,1.06674254336975,
7.51860402984325));
#395241=CARTESIAN_POINT('Ctrl Pts',(-2.53761520271996,1.05972122887321,
7.51860402984325));
#395242=CARTESIAN_POINT('Ctrl Pts',(-2.52991527992432,1.06713244554835,
7.51041458714367));
#395243=CARTESIAN_POINT('Ctrl Pts',(-2.53537771324442,1.06507910972982,
7.51004642900442));
#395244=CARTESIAN_POINT('Ctrl Pts',(-2.5376160113686,1.05971929247804,7.5072913648301));
#395245=CARTESIAN_POINT('Ctrl Pts',(-2.53109845195889,1.06968662665703,
7.50215815450137));
#395246=CARTESIAN_POINT('Ctrl Pts',(-2.53396347064417,1.06846608070768,
7.4987716367153));
#395247=CARTESIAN_POINT('Ctrl Pts',(-2.53531500022191,1.06529160572828,
7.49481588533171));
#395248=CARTESIAN_POINT('Ctrl Pts',(-2.52686327103471,1.0757955107805,7.50366171572174));
#395249=CARTESIAN_POINT('Ctrl Pts',(-2.53023235892125,1.0772298779127,7.50000045605858));
#395250=CARTESIAN_POINT('Ctrl Pts',(-2.5302323589213,1.07722987791258,7.49482233047317));
#395251=CARTESIAN_POINT('Origin',(-2.52608058816214,1.05490431419651,7.51860402984325));
#395252=CARTESIAN_POINT('Origin',(-2.52608058816214,1.05490431419651,9.));
#395253=CARTESIAN_POINT('Origin',(-2.52608058816214,1.05490431419651,8.75721825406948));
#395254=CARTESIAN_POINT('Ctrl Pts',(-2.51045599178025,1.06872519020655,
8.78942910404912));
#395255=CARTESIAN_POINT('Ctrl Pts',(-2.5160114955195,1.0682906710414,8.7967269950169));
#395256=CARTESIAN_POINT('Ctrl Pts',(-2.51696148514411,1.05941536790882,
8.79893251111267));
#395257=CARTESIAN_POINT('Ctrl Pts',(-2.52141367167526,1.06782815617218,
8.78111911759584));
#395258=CARTESIAN_POINT('Ctrl Pts',(-2.52799920529106,1.06730560749445,
8.78644465894814));
#395259=CARTESIAN_POINT('Ctrl Pts',(-2.53057060301398,1.05961773226615,
8.78817647674132));
#395260=CARTESIAN_POINT('Ctrl Pts',(-2.5282427591486,1.06726910313396,8.76780923932029));
#395261=CARTESIAN_POINT('Ctrl Pts',(-2.53601630044146,1.06664717666037,
8.76988516158373));
#395262=CARTESIAN_POINT('Ctrl Pts',(-2.53907079036638,1.05973295423882,
8.77093053738833));
#395263=CARTESIAN_POINT('Ctrl Pts',(-2.52691118055377,1.0673781108235,8.75371302330492));
#395264=CARTESIAN_POINT('Ctrl Pts',(-2.53449399556176,1.06677220825514,
8.75300828287559));
#395265=CARTESIAN_POINT('Ctrl Pts',(-2.53741291480574,1.05971002376439,
8.75267964240738));
#395266=CARTESIAN_POINT('Origin',(-2.51210475973991,1.05604843023055,8.78727029226991));
#395267=CARTESIAN_POINT('Ctrl Pts',(-2.44187055726728,1.07433989271894,
8.85049129520029));
#395268=CARTESIAN_POINT('Ctrl Pts',(-2.44769070315534,1.073863432789,8.85711686593484));
#395269=CARTESIAN_POINT('Ctrl Pts',(-2.44895572090756,1.06540763642198,
8.85933012996512));
#395270=CARTESIAN_POINT('Ctrl Pts',(-2.46565647730584,1.07239268417586,
8.82945683644723));
#395271=CARTESIAN_POINT('Ctrl Pts',(-2.4715249339237,1.07191226934043,8.8360746990239));
#395272=CARTESIAN_POINT('Ctrl Pts',(-2.47275657607163,1.06342609822992,
8.83829567148519));
#395273=CARTESIAN_POINT('Ctrl Pts',(-2.48940694251248,1.07044837810413,
8.80838214965003));
#395274=CARTESIAN_POINT('Ctrl Pts',(-2.49529855880007,1.06996606732746,
8.81501364461988));
#395275=CARTESIAN_POINT('Ctrl Pts',(-2.49652138203832,1.06144823216098,
8.81722098428721));
#395276=CARTESIAN_POINT('Ctrl Pts',(-2.51312464689845,1.06850675396145,
8.78727029226991));
#395277=CARTESIAN_POINT('Ctrl Pts',(-2.51901724180287,1.06802436307137,
8.79393457792714));
#395278=CARTESIAN_POINT('Ctrl Pts',(-2.52025288996716,1.05947377310387,
8.79610912703474));
#395279=CARTESIAN_POINT('Origin',(-2.44085067010875,1.06188156898805,8.85049129520029));
#395280=CARTESIAN_POINT('Ctrl Pts',(-2.43698193351379,1.0853833789328,8.85049129520029));
#395281=CARTESIAN_POINT('Ctrl Pts',(-2.44054210997315,1.09001222930857,
8.85711686593484));
#395282=CARTESIAN_POINT('Ctrl Pts',(-2.43513294253591,1.09663353354187,
8.85933012996512));
#395283=CARTESIAN_POINT('Ctrl Pts',(-2.43383229679188,1.08128830182353,
8.86332496987231));
#395284=CARTESIAN_POINT('Ctrl Pts',(-2.43222348092876,1.08561999963099,
8.86648636486737));
#395285=CARTESIAN_POINT('Ctrl Pts',(-2.42633528580379,1.08516694327359,
8.87206031107457));
#395286=CARTESIAN_POINT('Ctrl Pts',(-2.436686569143,1.07476427428361,8.86341338519877));
#395287=CARTESIAN_POINT('Ctrl Pts',(-2.4387913293493,1.07063590231536,8.86654584966059));
#395288=CARTESIAN_POINT('Ctrl Pts',(-2.43444148071611,1.06661061106433,
8.87215952290714));
#395289=CARTESIAN_POINT('Ctrl Pts',(-2.44187055726728,1.07433989271894,
8.85049129520029));
#395290=CARTESIAN_POINT('Ctrl Pts',(-2.44769070315534,1.073863432789,8.85711686593484));
#395291=CARTESIAN_POINT('Ctrl Pts',(-2.44895572090756,1.06540763642198,
8.85933012996512));
#395292=CARTESIAN_POINT('Origin',(-2.42707363953071,1.09300412104528,8.85049129520029));
#395293=CARTESIAN_POINT('Ctrl Pts',(-2.48056797713152,1.14205283806807,
8.78727029226991));
#395294=CARTESIAN_POINT('Ctrl Pts',(-2.48417247056979,1.14673930824634,
8.79393457792714));
#395295=CARTESIAN_POINT('Ctrl Pts',(-2.47867338431574,1.1534026006419,8.79610912703474));
#395296=CARTESIAN_POINT('Ctrl Pts',(-2.46605988498929,1.12318978773032,
8.80838214965001));
#395297=CARTESIAN_POINT('Ctrl Pts',(-2.46966377980882,1.12787547959983,
8.81501364461993));
#395298=CARTESIAN_POINT('Ctrl Pts',(-2.46418031900403,1.1345072569029,8.81722098428721));
#395299=CARTESIAN_POINT('Ctrl Pts',(-2.45153175309122,1.10430068221457,
8.82945683644722));
#395300=CARTESIAN_POINT('Ctrl Pts',(-2.4551214811677,1.10896795484712,8.83607469902389));
#395301=CARTESIAN_POINT('Ctrl Pts',(-2.44966738952775,1.11558497282201,
8.83829567148519));
#395302=CARTESIAN_POINT('Ctrl Pts',(-2.43698193351379,1.0853833789328,8.85049129520029));
#395303=CARTESIAN_POINT('Ctrl Pts',(-2.44054210997315,1.09001222930857,
8.85711686593484));
#395304=CARTESIAN_POINT('Ctrl Pts',(-2.43513294253591,1.09663353354187,
8.85933012996512));
#395305=CARTESIAN_POINT('Origin',(-2.47065968314844,1.14967358018055,8.78727029226991));
#395306=CARTESIAN_POINT('Ctrl Pts',(-2.48900407525588,1.15302126734187,
8.75374538247849));
#395307=CARTESIAN_POINT('Ctrl Pts',(-2.49364725474231,1.1590366860841,8.75304829418602));
#395308=CARTESIAN_POINT('Ctrl Pts',(-2.49039024421334,1.16594049123946,
8.75272238421917));
#395309=CARTESIAN_POINT('Ctrl Pts',(-2.48980881601113,1.15406756998975,
8.76769408445016));
#395310=CARTESIAN_POINT('Ctrl Pts',(-2.49456829219992,1.16023478503224,
8.76974318093967));
#395311=CARTESIAN_POINT('Ctrl Pts',(-2.49150955440295,1.16713858691016,
8.7707786988043));
#395312=CARTESIAN_POINT('Ctrl Pts',(-2.48568417334204,1.14870481864704,
8.78108014887994));
#395313=CARTESIAN_POINT('Ctrl Pts',(-2.48972066580186,1.15392898996144,
8.78639403366327));
#395314=CARTESIAN_POINT('Ctrl Pts',(-2.48578137048602,1.16100034260033,
8.78812224174741));
#395315=CARTESIAN_POINT('Ctrl Pts',(-2.47892479450374,1.13991645305729,
8.78944554828685));
#395316=CARTESIAN_POINT('Ctrl Pts',(-2.48233103024034,1.14431576842716,
8.79673892988685));
#395317=CARTESIAN_POINT('Ctrl Pts',(-2.47640778743176,1.1509805076529,8.79894799272499));
#395318=CARTESIAN_POINT('Origin',(-2.47920868111275,1.16078876868067,8.75721825406948));
#395319=CARTESIAN_POINT('Origin',(-2.47920868111275,1.16078876868067,9.));
#395320=CARTESIAN_POINT('Origin',(-2.47920868111275,1.16078876868067,7.51860402984325));
#395321=CARTESIAN_POINT('Ctrl Pts',(-2.49519995811679,1.14732290287503,
7.50366195182966));
#395322=CARTESIAN_POINT('Ctrl Pts',(-2.49852704388144,1.14885273686104,
7.50000065167735));
#395323=CARTESIAN_POINT('Ctrl Pts',(-2.49852704388139,1.14885273686115,
7.49482233047108));
#395324=CARTESIAN_POINT('Ctrl Pts',(-2.49352263939497,1.15457137868116,
7.50215800491337));
#395325=CARTESIAN_POINT('Ctrl Pts',(-2.49454432099783,1.15751431325004,
7.49877273257264));
#395326=CARTESIAN_POINT('Ctrl Pts',(-2.49310216742007,1.16065076816093,
7.49481816995647));
#395327=CARTESIAN_POINT('Ctrl Pts',(-2.49083562085213,1.15540200958145,
7.51043025814042));
#395328=CARTESIAN_POINT('Ctrl Pts',(-2.49299264991784,1.1608278719642,7.51006209594515));
#395329=CARTESIAN_POINT('Ctrl Pts',(-2.49052819510454,1.16609146699379,
7.50731281821699));
#395330=CARTESIAN_POINT('Ctrl Pts',(-2.48911605357969,1.15316682858636,
7.51860402984325));
#395331=CARTESIAN_POINT('Ctrl Pts',(-2.49375584668794,1.1591978597837,7.51860402984325));
#395332=CARTESIAN_POINT('Ctrl Pts',(-2.49052926869774,1.16608917401712,
7.51860402984325));
#395333=CARTESIAN_POINT('Origin',(0.,0.,7.5));
#395334=CARTESIAN_POINT('Origin',(-2.50151564461753,0.927015373804532,7.5));
#395335=CARTESIAN_POINT('',(-2.50151564461753,0.927015373804532,7.59394543036555));
#395336=CARTESIAN_POINT('',(-2.50151564461753,0.927015373804532,8.85049129520029));
#395337=CARTESIAN_POINT('',(-2.50151564461753,0.927015373804532,7.5));
#395338=CARTESIAN_POINT('',(-2.54864296074704,0.980775832055543,8.78727029226991));
#395339=CARTESIAN_POINT('Ctrl Pts',(-2.50151564461753,0.927015373804532,
8.85049129520029));
#395340=CARTESIAN_POINT('Ctrl Pts',(-2.51724758470004,0.944961575232364,
8.82945686509571));
#395341=CARTESIAN_POINT('Ctrl Pts',(-2.53295613735134,0.96288109746175,
8.80838212259895));
#395342=CARTESIAN_POINT('Ctrl Pts',(-2.54864296074704,0.980775832055543,
8.78727029226991));
#395343=CARTESIAN_POINT('',(-2.55788654645048,0.991320447028606,8.75721825406948));
#395344=CARTESIAN_POINT('Origin',(-2.53006954219739,0.959587909596253,8.75937679713144));
#395345=CARTESIAN_POINT('',(-2.55788654645048,0.991320447028606,7.51860402984325));
#395346=CARTESIAN_POINT('',(-2.55788654645048,0.991320447028606,7.5));
#395347=CARTESIAN_POINT('Ctrl Pts',(-2.55788654645048,0.991320447028606,
7.51860402984325));
#395348=CARTESIAN_POINT('Ctrl Pts',(-2.55062714752994,0.9830392919651,7.52834476460825));
#395349=CARTESIAN_POINT('Ctrl Pts',(-2.54336303591238,0.974752760895221,
7.53807742314407));
#395350=CARTESIAN_POINT('Ctrl Pts',(-2.53609405336271,0.966460673312405,
7.54780169004674));
#395351=CARTESIAN_POINT('Ctrl Pts',(-2.52458037785902,0.953326454730319,
7.5632044032688));
#395352=CARTESIAN_POINT('Ctrl Pts',(-2.51305446717486,0.94017827887332,
7.57858609112103));
#395353=CARTESIAN_POINT('Ctrl Pts',(-2.50151564461753,0.927015373804532,
7.59394543036555));
#395354=CARTESIAN_POINT('Origin',(-2.77776907780699,0.87572937929184,7.5));
#395355=CARTESIAN_POINT('',(-2.59029443537466,0.903257743546346,8.75721825406948));
#395356=CARTESIAN_POINT('',(-2.57642062555681,0.905294943272712,8.78727029226991));
#395357=CARTESIAN_POINT('Origin',(-2.54120372156563,0.910466116015902,8.75658640621026));
#395358=CARTESIAN_POINT('',(-2.50568666557814,0.91568136241822,8.85049129520029));
#395359=CARTESIAN_POINT('Ctrl Pts',(-2.57642062555681,0.905294943272712,
8.78727029226991));
#395360=CARTESIAN_POINT('Ctrl Pts',(-2.5528760821923,0.908752172247975,
8.80838212259895));
#395361=CARTESIAN_POINT('Ctrl Pts',(-2.52929892512471,0.912214190147685,
8.82945686509571));
#395362=CARTESIAN_POINT('Ctrl Pts',(-2.50568666557814,0.91568136241822,
8.85049129520029));
#395363=CARTESIAN_POINT('',(-2.50568666557814,0.91568136241822,7.59394543036555));
#395364=CARTESIAN_POINT('',(-2.50568666557814,0.91568136241822,7.5));
#395365=CARTESIAN_POINT('',(-2.59029443537466,0.903257743546346,7.51860402984325));
#395366=CARTESIAN_POINT('Ctrl Pts',(-2.50568666557814,0.91568136241822,
7.59394543036555));
#395367=CARTESIAN_POINT('Ctrl Pts',(-2.52300542420909,0.913138313983279,
7.57858609112103));
#395368=CARTESIAN_POINT('Ctrl Pts',(-2.54030480325286,0.910598111204322,
7.56320440326857));
#395369=CARTESIAN_POINT('Ctrl Pts',(-2.5575858183662,0.908060604944507,
7.54780169004651));
#395370=CARTESIAN_POINT('Ctrl Pts',(-2.56849592237767,0.906458589261821,
7.53807742314383));
#395371=CARTESIAN_POINT('Ctrl Pts',(-2.57939871554831,0.904857647086919,
7.52834476460825));
#395372=CARTESIAN_POINT('Ctrl Pts',(-2.59029443537466,0.903257743546347,
7.51860402984324));
#395373=CARTESIAN_POINT('',(-2.59029443537466,0.903257743546346,7.5));
#395374=CARTESIAN_POINT('Origin',(-2.5066854651563,0.922483422723941,7.5));
#395375=CARTESIAN_POINT('Ctrl Pts',(-2.50568666557814,0.91568136241822,
8.85049129520029));
#395376=CARTESIAN_POINT('Ctrl Pts',(-2.50549505870656,0.915709497549917,
8.85097269580138));
#395377=CARTESIAN_POINT('Ctrl Pts',(-2.50530709131976,0.915745599877208,
8.85143669361005));
#395378=CARTESIAN_POINT('Ctrl Pts',(-2.50511427303432,0.915792190387963,
8.8519052845931));
#395379=CARTESIAN_POINT('Ctrl Pts',(-2.5047371326961,0.915883318472337,
8.85282181883899));
#395380=CARTESIAN_POINT('Ctrl Pts',(-2.50435118231721,0.916012418184756,
8.85372622499635));
#395381=CARTESIAN_POINT('Ctrl Pts',(-2.50395525683443,0.916196137703026,
8.8546225773507));
#395382=CARTESIAN_POINT('Ctrl Pts',(-2.50362657356056,0.916348655121995,
8.85536669723986));
#395383=CARTESIAN_POINT('Ctrl Pts',(-2.50329092746443,0.916538821148363,
8.8561049844905));
#395384=CARTESIAN_POINT('Ctrl Pts',(-2.50295156831354,0.916783139614805,
8.8568133821837));
#395385=CARTESIAN_POINT('Ctrl Pts',(-2.50264359935114,0.91700485900681,
8.85745625420284));
#395386=CARTESIAN_POINT('Ctrl Pts',(-2.50232835963296,0.917273471665707,
8.85808743050666));
#395387=CARTESIAN_POINT('Ctrl Pts',(-2.50201318278513,0.917616619300495,
8.8586680450841));
#395388=CARTESIAN_POINT('Ctrl Pts',(-2.50186776701974,0.917774940180657,
8.85893592806395));
#395389=CARTESIAN_POINT('Ctrl Pts',(-2.50172245429852,0.917949352490005,
8.85919241173848));
#395390=CARTESIAN_POINT('Ctrl Pts',(-2.50157875665041,0.918143956929098,
8.85943017985534));
#395391=CARTESIAN_POINT('Ctrl Pts',(-2.50138472228639,0.918406730530955,
8.8597512372));
#395392=CARTESIAN_POINT('Ctrl Pts',(-2.50118920929819,0.918713389200792,
8.86004599534705));
#395393=CARTESIAN_POINT('Ctrl Pts',(-2.50100334875574,0.91906584762794,
8.86026130871721));
#395394=CARTESIAN_POINT('Ctrl Pts',(-2.50093529997118,0.919194892594974,
8.86034014101235));
#395395=CARTESIAN_POINT('Ctrl Pts',(-2.50086751202657,0.919332009659972,
8.86040910639693));
#395396=CARTESIAN_POINT('Ctrl Pts',(-2.50080213330744,0.919473612221358,
8.86046313645507));
#395397=CARTESIAN_POINT('Ctrl Pts',(-2.50070011036379,0.91969458183249,
8.8605474499083));
#395398=CARTESIAN_POINT('Ctrl Pts',(-2.50060130278636,0.919932567670979,
8.86059655985669));
#395399=CARTESIAN_POINT('Ctrl Pts',(-2.5005117768413,0.920172194646778,
8.86059725258816));
#395400=CARTESIAN_POINT('Ctrl Pts',(-2.50042204405555,0.920412375256622,
8.86059794692011));
#395401=CARTESIAN_POINT('Ctrl Pts',(-2.50034312944461,0.920657798036075,
8.86056369958366));
#395402=CARTESIAN_POINT('Ctrl Pts',(-2.50027575459447,0.920893925584962,
8.86048590497774));
#395403=CARTESIAN_POINT('Ctrl Pts',(-2.50025817176458,0.920955547844857,
8.86046560290182));
#395404=CARTESIAN_POINT('Ctrl Pts',(-2.5002412332154,0.921017363572455,
8.86044257503091));
#395405=CARTESIAN_POINT('Ctrl Pts',(-2.50022543070301,0.921077453935466,
8.86041778462584));
#395406=CARTESIAN_POINT('Ctrl Pts',(-2.5001190994039,0.921481787512609,
8.86025097596201));
#395407=CARTESIAN_POINT('Ctrl Pts',(-2.50005025625273,0.921862343753855,
8.8599848982295));
#395408=CARTESIAN_POINT('Ctrl Pts',(-2.50001257343146,0.922206507017019,
8.85968173251461));
#395409=CARTESIAN_POINT('Ctrl Pts',(-2.49999264137797,0.922388549665028,
8.85952137522076));
#395410=CARTESIAN_POINT('Ctrl Pts',(-2.49998085334338,0.922563898491426,
8.85934740853961));
#395411=CARTESIAN_POINT('Ctrl Pts',(-2.49997582451368,0.922729976418867,
8.8591675900182));
#395412=CARTESIAN_POINT('Ctrl Pts',(-2.49995563114851,0.923396865623127,
8.85844552518696));
#395413=CARTESIAN_POINT('Ctrl Pts',(-2.50004026010221,0.923951866608739,
8.85759444184126));
#395414=CARTESIAN_POINT('Ctrl Pts',(-2.50014990752215,0.924398186783963,
8.85683498915141));
#395415=CARTESIAN_POINT('Ctrl Pts',(-2.50016138183263,0.924444893001657,
8.85675551445));
#395416=CARTESIAN_POINT('Ctrl Pts',(-2.50017314820602,0.924490400580325,
8.85667699793652));
#395417=CARTESIAN_POINT('Ctrl Pts',(-2.50018512677841,0.92453470701937,
8.85659965593547));
#395418=CARTESIAN_POINT('Ctrl Pts',(-2.50034681415975,0.925132757594396,
8.85555568965886));
#395419=CARTESIAN_POINT('Ctrl Pts',(-2.50058857608735,0.925684170392119,
8.85434650606345));
#395420=CARTESIAN_POINT('Ctrl Pts',(-2.5009059159866,0.926194166764285,
8.85297329937116));
#395421=CARTESIAN_POINT('Ctrl Pts',(-2.50108440034412,0.926481008649092,
8.85220095427747));
#395422=CARTESIAN_POINT('Ctrl Pts',(-2.50128713331755,0.926754699673022,
8.85137579139183));
#395423=CARTESIAN_POINT('Ctrl Pts',(-2.50151564461753,0.927015373804532,
8.85049129520029));
#395424=CARTESIAN_POINT('Origin',(-2.5066854651563,0.922483422723941,7.59394543036555));
#395425=CARTESIAN_POINT('Ctrl Pts',(-2.50513036619197,0.915763048196833,
7.59443877723642));
#395426=CARTESIAN_POINT('Ctrl Pts',(-2.49940101777127,0.916604333120594,
7.58783886950016));
#395427=CARTESIAN_POINT('Ctrl Pts',(-2.49865736261563,0.925061647029049,
7.58559994247159));
#395428=CARTESIAN_POINT('Ctrl Pts',(-2.5364067111286,0.911170498480271,
7.56670252222134));
#395429=CARTESIAN_POINT('Ctrl Pts',(-2.53068564324298,0.912010567508487,
7.56004874999028));
#395430=CARTESIAN_POINT('Ctrl Pts',(-2.52991629821513,0.920516122486533,
7.55786368756704));
#395431=CARTESIAN_POINT('Ctrl Pts',(-2.56762465061597,0.906586524891448,
7.53888913333557));
#395432=CARTESIAN_POINT('Ctrl Pts',(-2.5618695821438,0.907431586491008,
7.53222002137279));
#395433=CARTESIAN_POINT('Ctrl Pts',(-2.56111780051421,0.915977770967222,
7.53005029815326));
#395434=CARTESIAN_POINT('Ctrl Pts',(-2.59878277202118,0.902011334858278,
7.51101258149734));
#395435=CARTESIAN_POINT('Ctrl Pts',(-2.59295794166188,0.902866640139947,
7.5043616886572));
#395436=CARTESIAN_POINT('Ctrl Pts',(-2.59226033981814,0.911446898481761,
7.50217374673251));
#395437=CARTESIAN_POINT('',(-2.59059853376832,0.911688670640849,7.50366116523517));
#395438=CARTESIAN_POINT('Ctrl Pts',(-2.59029443537466,0.903257743546346,
7.51860402984325));
#395439=CARTESIAN_POINT('Ctrl Pts',(-2.59073136135582,0.903193586296034,
7.51734760759493));
#395440=CARTESIAN_POINT('Ctrl Pts',(-2.59113483014927,0.903194476627547,
7.51608817408572));
#395441=CARTESIAN_POINT('Ctrl Pts',(-2.59150388429384,0.903273766104983,
7.51481005913119));
#395442=CARTESIAN_POINT('Ctrl Pts',(-2.59183818235682,0.903345588408327,
7.51365231206383));
#395443=CARTESIAN_POINT('Ctrl Pts',(-2.59214476638707,0.903481595190344,
7.51247773061042));
#395444=CARTESIAN_POINT('Ctrl Pts',(-2.59240335794634,0.903713185892332,
7.51129758471022));
#395445=CARTESIAN_POINT('Ctrl Pts',(-2.59272475772224,0.904001026686246,
7.50983079813402));
#395446=CARTESIAN_POINT('Ctrl Pts',(-2.59295307372471,0.904437038238365,
7.50839324291155));
#395447=CARTESIAN_POINT('Ctrl Pts',(-2.59301693980262,0.905062645938782,
7.50715379678855));
#395448=CARTESIAN_POINT('Ctrl Pts',(-2.59304644409036,0.905351658669921,
7.50658120839351));
#395449=CARTESIAN_POINT('Ctrl Pts',(-2.59303559361285,0.905723185272621,
7.50598221009429));
#395450=CARTESIAN_POINT('Ctrl Pts',(-2.59296190979915,0.906167719907874,
7.50545747549611));
#395451=CARTESIAN_POINT('Ctrl Pts',(-2.59292258983543,0.906404937348878,
7.50517746087247));
#395452=CARTESIAN_POINT('Ctrl Pts',(-2.59286515073088,0.906665550100618,
7.50491486231392));
#395453=CARTESIAN_POINT('Ctrl Pts',(-2.59278948464782,0.906942297683577,
7.50468370960993));
#395454=CARTESIAN_POINT('Ctrl Pts',(-2.59267633998614,0.907356122615175,
7.50433806340447));
#395455=CARTESIAN_POINT('Ctrl Pts',(-2.59251851063052,0.907818286743171,
7.50405484070984));
#395456=CARTESIAN_POINT('Ctrl Pts',(-2.59232594814198,0.908297432651606,
7.50385766036131));
#395457=CARTESIAN_POINT('Ctrl Pts',(-2.59230535657693,0.908348669858901,
7.50383657498791));
#395458=CARTESIAN_POINT('Ctrl Pts',(-2.59228439032879,0.90840008397143,
7.50381643264937));
#395459=CARTESIAN_POINT('Ctrl Pts',(-2.59226307810043,0.908451624345678,
7.50379723213559));
#395460=CARTESIAN_POINT('Ctrl Pts',(-2.59212081200435,0.908795673203805,
7.50366906242519));
#395461=CARTESIAN_POINT('Ctrl Pts',(-2.59195936993193,0.909152557376872,
7.50358235568538));
#395462=CARTESIAN_POINT('Ctrl Pts',(-2.59179549077372,0.909492809245847,
7.5035341175365));
#395463=CARTESIAN_POINT('Ctrl Pts',(-2.59154977252353,0.910002978414299,
7.50346178989176));
#395464=CARTESIAN_POINT('Ctrl Pts',(-2.59126374379866,0.910541356689525,
7.50346967198527));
#395465=CARTESIAN_POINT('Ctrl Pts',(-2.59096668961309,0.911061237388423,
7.50354272648692));
#395466=CARTESIAN_POINT('Ctrl Pts',(-2.59084450507791,0.911275075080774,
7.50357277531559));
#395467=CARTESIAN_POINT('Ctrl Pts',(-2.59072074066281,0.911485569493069,
7.50361331098761));
#395468=CARTESIAN_POINT('Ctrl Pts',(-2.59059853376966,0.91168867064132,
7.50366116523659));
#395469=CARTESIAN_POINT('',(-2.50943323048223,0.923494625764158,7.57603338622103));
#395470=CARTESIAN_POINT('Origin',(-2.51772543279346,0.926549273114053,7.58486873427626));
#395471=CARTESIAN_POINT('Ctrl Pts',(-2.59059853382405,0.911688670627326,
7.50366116529969));
#395472=CARTESIAN_POINT('Ctrl Pts',(-2.56358770138599,0.915618394511231,
7.52783573079709));
#395473=CARTESIAN_POINT('Ctrl Pts',(-2.53653388028073,0.919553544813599,
7.55196141284068));
#395474=CARTESIAN_POINT('Ctrl Pts',(-2.5094332316199,0.923494625241324,
7.57603338728831));
#395475=CARTESIAN_POINT('Ctrl Pts',(-2.50672970590163,0.915705906336666,
7.5963967733137));
#395476=CARTESIAN_POINT('Ctrl Pts',(-2.48759500061638,0.915457955302635,
7.59974925422226));
#395477=CARTESIAN_POINT('Ctrl Pts',(-2.502325773521,0.927672813292059,7.59639677331373));
#395478=CARTESIAN_POINT('Ctrl Pts',(-2.50288821974749,0.915029084195064,
7.58707626057421));
#395479=CARTESIAN_POINT('Ctrl Pts',(-2.49726541951563,0.919016758850096,
7.58811717123965));
#395480=CARTESIAN_POINT('Ctrl Pts',(-2.49896195408413,0.925698016370938,
7.58707626057425));
#395481=CARTESIAN_POINT('Ctrl Pts',(-2.5063100950153,0.920050677758216,
7.58015376756929));
#395482=CARTESIAN_POINT('Ctrl Pts',(-2.50375153300591,0.921403708571725,
7.58208760766041));
#395483=CARTESIAN_POINT('Ctrl Pts',(-2.50482266671417,0.924092500961744,
7.58015376756931));
#395484=CARTESIAN_POINT('Ctrl Pts',(-2.50943322970565,0.923494625478152,
7.57603338509286));
#395485=CARTESIAN_POINT('Ctrl Pts',(-2.50943322970565,0.923494625478151,
7.57603338509286));
#395486=CARTESIAN_POINT('Ctrl Pts',(-2.50943322970565,0.923494625478151,
7.57603338509286));
#395487=CARTESIAN_POINT('Origin',(-2.51772740356828,0.926543917882751,7.58486873427622));
#395488=CARTESIAN_POINT('Ctrl Pts',(-2.56355987305573,0.997792291028113,
7.51098857897448));
#395489=CARTESIAN_POINT('Ctrl Pts',(-2.55967899499225,0.993365181651979,
7.50433767179956));
#395490=CARTESIAN_POINT('Ctrl Pts',(-2.56470980820181,0.986379555729206,
7.50214974420965));
#395491=CARTESIAN_POINT('Ctrl Pts',(-2.54279444458098,0.974104140667222,
7.53887321589168));
#395492=CARTESIAN_POINT('Ctrl Pts',(-2.53896006632403,0.969730075918122,
7.53220407452065));
#395493=CARTESIAN_POINT('Ctrl Pts',(-2.54392751200518,0.962735263316863,
7.53003438070911));
#395494=CARTESIAN_POINT('Ctrl Pts',(-2.52198913882351,0.950370500319441,
7.56669465659234));
#395495=CARTESIAN_POINT('Ctrl Pts',(-2.51817742102916,0.9460222854798,7.56004085833302));
#395496=CARTESIAN_POINT('Ctrl Pts',(-2.52310514388124,0.939047029382759,
7.55785582193789));
#395497=CARTESIAN_POINT('Ctrl Pts',(-2.501144896724,0.926592443362311,7.59443891967696));
#395498=CARTESIAN_POINT('Ctrl Pts',(-2.49732765241344,0.922237924152511,
7.58783901202978));
#395499=CARTESIAN_POINT('Ctrl Pts',(-2.50224367002345,0.915316078383761,
7.58560008491213));
#395500=CARTESIAN_POINT('',(-2.56358326728471,0.985097876880933,7.50366116523517));
#395501=CARTESIAN_POINT('Ctrl Pts',(-2.56358326728506,0.985097876881066,
7.50366116523554));
#395502=CARTESIAN_POINT('Ctrl Pts',(-2.56345970006383,0.985845452066986,
7.50350835821027));
#395503=CARTESIAN_POINT('Ctrl Pts',(-2.56332179021806,0.98652863497484,
7.50345484956));
#395504=CARTESIAN_POINT('Ctrl Pts',(-2.56316602620426,0.987167856010466,
7.50349758195598));
#395505=CARTESIAN_POINT('Ctrl Pts',(-2.56308610771343,0.987495823807609,
7.50351950684424));
#395506=CARTESIAN_POINT('Ctrl Pts',(-2.56299373787712,0.987844575329019,
7.50357029184312));
#395507=CARTESIAN_POINT('Ctrl Pts',(-2.56289542256784,0.98817842402356,
7.50365515313923));
#395508=CARTESIAN_POINT('Ctrl Pts',(-2.56274417381036,0.98869201850445,
7.50378570417639));
#395509=CARTESIAN_POINT('Ctrl Pts',(-2.56257474719318,0.989185516731555,
7.50400001621911));
#395510=CARTESIAN_POINT('Ctrl Pts',(-2.5623978911558,0.989620619087741,
7.50428903009634));
#395511=CARTESIAN_POINT('Ctrl Pts',(-2.56237826149629,0.989668912101802,
7.50432110841318));
#395512=CARTESIAN_POINT('Ctrl Pts',(-2.56235854685538,0.989716515320739,
7.50435406373354));
#395513=CARTESIAN_POINT('Ctrl Pts',(-2.56233876646287,0.989763398289759,
7.50438785222352));
#395514=CARTESIAN_POINT('Ctrl Pts',(-2.56221799765893,0.990049641350433,
7.50459414719561));
#395515=CARTESIAN_POINT('Ctrl Pts',(-2.56209237988989,0.990313392525865,
7.50483629897752));
#395516=CARTESIAN_POINT('Ctrl Pts',(-2.56196791368994,0.990545113473018,
7.5050991045531));
#395517=CARTESIAN_POINT('Ctrl Pts',(-2.56169332875141,0.991056313156602,
7.50567888004914));
#395518=CARTESIAN_POINT('Ctrl Pts',(-2.56141398648965,0.991432015973551,
7.50637912803144));
#395519=CARTESIAN_POINT('Ctrl Pts',(-2.56114901670265,0.991696500910359,
7.50710440483569));
#395520=CARTESIAN_POINT('Ctrl Pts',(-2.56108404085049,0.991761357867625,
7.50728225710685));
#395521=CARTESIAN_POINT('Ctrl Pts',(-2.56101873889053,0.99182092138565,
7.50746498566954));
#395522=CARTESIAN_POINT('Ctrl Pts',(-2.56095491592359,0.991874108847984,
7.50764697238949));
#395523=CARTESIAN_POINT('Ctrl Pts',(-2.56061182121787,0.992160030007908,
7.50862528291182));
#395524=CARTESIAN_POINT('Ctrl Pts',(-2.56028297152453,0.992290828132535,
7.50965856837421));
#395525=CARTESIAN_POINT('Ctrl Pts',(-2.55997541446453,0.992332425349267,
7.51067959873202));
#395526=CARTESIAN_POINT('Ctrl Pts',(-2.55980616542648,0.992355316350103,
7.51124147302578));
#395527=CARTESIAN_POINT('Ctrl Pts',(-2.55964326493997,0.992350769606349,
7.51180065547253));
#395528=CARTESIAN_POINT('Ctrl Pts',(-2.55948762194073,0.992327067952742,
7.51235175716501));
#395529=CARTESIAN_POINT('Ctrl Pts',(-2.55894981337754,0.992245169297914,
7.51425603304536));
#395530=CARTESIAN_POINT('Ctrl Pts',(-2.55843544700615,0.991918804986669,
7.51626900505181));
#395531=CARTESIAN_POINT('Ctrl Pts',(-2.55796290178256,0.991405463116667,
7.51827788969244));
#395532=CARTESIAN_POINT('Ctrl Pts',(-2.55793732674207,0.991377680084582,
7.51838661432546));
#395533=CARTESIAN_POINT('Ctrl Pts',(-2.557911873988,0.991349339402192,7.51849533314857));
#395534=CARTESIAN_POINT('Ctrl Pts',(-2.55788654645048,0.991320447028609,
7.51860402984325));
#395535=CARTESIAN_POINT('Ctrl Pts',(-2.50943323101062,0.923494626900376,
7.57603338728985));
#395536=CARTESIAN_POINT('Ctrl Pts',(-2.52751419016524,0.944062956661482,
7.55196141284922));
#395537=CARTESIAN_POINT('Ctrl Pts',(-2.54556333675352,0.964596416013609,
7.52783573083105));
#395538=CARTESIAN_POINT('Ctrl Pts',(-2.56358326731953,0.985097876928784,
7.50366116530176));
#395539=CARTESIAN_POINT('Origin',(-8.67125181207506E-16,3.19110082301667E-16,
7.49482233047033));
#395540=CARTESIAN_POINT('Origin',(-2.58226093460097,0.908754485894685,7.49482233047033));
#395541=CARTESIAN_POINT('Origin',(0.,0.,7.50366116523517));
#395542=CARTESIAN_POINT('Origin',(-2.55533261422669,0.981927431468037,7.49482233047033));
#395543=CARTESIAN_POINT('Ctrl Pts',(-2.59029338886968,0.903257897167606,
7.51860402984325));
#395544=CARTESIAN_POINT('Ctrl Pts',(-2.59782171669849,0.902153104819671,
7.51860402984325));
#395545=CARTESIAN_POINT('Ctrl Pts',(-2.60029797237973,0.894958353689076,
7.51860402984325));
#395546=CARTESIAN_POINT('Ctrl Pts',(-2.59308870818399,0.902847678972059,
7.51041458714366));
#395547=CARTESIAN_POINT('Ctrl Pts',(-2.59840836067141,0.90044858264775,
7.51004642900443));
#395548=CARTESIAN_POINT('Ctrl Pts',(-2.60029865530165,0.894956369462144,
7.5072913648301));
#395549=CARTESIAN_POINT('Ctrl Pts',(-2.59443309621022,0.905320806149179,
7.50215815450137));
#395550=CARTESIAN_POINT('Ctrl Pts',(-2.59721402775987,0.903919205564972,
7.49877163671529));
#395551=CARTESIAN_POINT('Ctrl Pts',(-2.59835939116489,0.900664660087521,
7.4948158853317));
#395552=CARTESIAN_POINT('Ctrl Pts',(-2.5905980144691,0.911688487888521,
7.50366171572174));
#395553=CARTESIAN_POINT('Ctrl Pts',(-2.59405208042094,0.912904049757583,
7.50000045605858));
#395554=CARTESIAN_POINT('Ctrl Pts',(-2.59405208042098,0.912904049757465,
7.49482233047317));
#395555=CARTESIAN_POINT('Origin',(-2.58847843614164,0.890890361172308,7.51860402984325));
#395556=CARTESIAN_POINT('Origin',(-2.58847843614164,0.890890361172308,9.));
#395557=CARTESIAN_POINT('Origin',(-2.58847843614164,0.890890361172308,8.75721825406948));
#395558=CARTESIAN_POINT('Ctrl Pts',(-2.57377144873504,0.905683912037591,
8.78942910404912));
#395559=CARTESIAN_POINT('Ctrl Pts',(-2.57928769835754,0.904894343291997,
8.79672699501691));
#395560=CARTESIAN_POINT('Ctrl Pts',(-2.57966709350247,0.895976409377347,
8.79893251111267));
#395561=CARTESIAN_POINT('Ctrl Pts',(-2.58464914173359,0.904086660094499,
8.78111911759583));
#395562=CARTESIAN_POINT('Ctrl Pts',(-2.59118766485554,0.903143248461625,
8.78644465894812));
#395563=CARTESIAN_POINT('Ctrl Pts',(-2.593261215509,0.895306418779735,8.78817647674132));
#395564=CARTESIAN_POINT('Ctrl Pts',(-2.59142837946314,0.903091214554023,
8.76780923932029));
#395565=CARTESIAN_POINT('Ctrl Pts',(-2.59914610221573,0.901972513394419,
8.76988516158374));
#395566=CARTESIAN_POINT('Ctrl Pts',(-2.60175132061197,0.894876795142954,
8.77093053738833));
#395567=CARTESIAN_POINT('Ctrl Pts',(-2.59010652088601,0.90328531280907,
8.75371302330492));
#395568=CARTESIAN_POINT('Ctrl Pts',(-2.59763493587647,0.902194822506885,
8.75300828287559));
#395569=CARTESIAN_POINT('Ctrl Pts',(-2.60009538217394,0.89496013223352,
8.75267964240738));
#395570=CARTESIAN_POINT('Origin',(-2.57460462632379,0.892927560898673,8.78727029226991));
#395571=CARTESIAN_POINT('Ctrl Pts',(-2.50568666557814,0.91568136241822,
8.85049129520029));
#395572=CARTESIAN_POINT('Ctrl Pts',(-2.51146432645974,0.914832983398935,
8.85711686593484));
#395573=CARTESIAN_POINT('Ctrl Pts',(-2.51218498036397,0.90631351040677,
8.85933012996512));
#395574=CARTESIAN_POINT('Ctrl Pts',(-2.52929895681326,0.912214185494608,
8.82945683644725));
#395575=CARTESIAN_POINT('Ctrl Pts',(-2.5351245757734,0.911358764416525,
8.8360746990239));
#395576=CARTESIAN_POINT('Ctrl Pts',(-2.5358099765306,0.90281111747134,8.83829567148519));
#395577=CARTESIAN_POINT('Ctrl Pts',(-2.55287605202415,0.9087521766778,8.80838214965001));
#395578=CARTESIAN_POINT('Ctrl Pts',(-2.5587246615967,0.907893379708743,
8.81501364461994));
#395579=CARTESIAN_POINT('Ctrl Pts',(-2.55939923284053,0.899314698794289,
8.81722098428721));
#395580=CARTESIAN_POINT('Ctrl Pts',(-2.57642062555681,0.905294943272712,
8.78727029226991));
#395581=CARTESIAN_POINT('Ctrl Pts',(-2.58227020660257,0.904436003654666,
8.79393457792714));
#395582=CARTESIAN_POINT('Ctrl Pts',(-2.58295547781501,0.895823813541599,
8.79610912703474));
#395583=CARTESIAN_POINT('Origin',(-2.50387066634512,0.903313980044182,8.85049129520029));
#395584=CARTESIAN_POINT('Ctrl Pts',(-2.50151564461753,0.927015373804532,
8.85049129520029));
#395585=CARTESIAN_POINT('Ctrl Pts',(-2.50536507777436,0.931406612421841,
8.85711686593484));
#395586=CARTESIAN_POINT('Ctrl Pts',(-2.50039125247054,0.93836087902307,
8.85933012996512));
#395587=CARTESIAN_POINT('Ctrl Pts',(-2.49811010667082,0.923130508387991,
8.86332496987231));
#395588=CARTESIAN_POINT('Ctrl Pts',(-2.49678212912387,0.927556383444011,
8.86648636486738));
#395589=CARTESIAN_POINT('Ctrl Pts',(-2.4908770045068,0.927481515896442,
8.87206031107457));
#395590=CARTESIAN_POINT('Ctrl Pts',(-2.50054051873363,0.916437011304943,
8.86341338519877));
#395591=CARTESIAN_POINT('Ctrl Pts',(-2.5023764487842,0.912182269070248,
8.86654584966059));
#395592=CARTESIAN_POINT('Ctrl Pts',(-2.49777763608561,0.908443943970601,
8.87215952290714));
#395593=CARTESIAN_POINT('Ctrl Pts',(-2.50568666557814,0.91568136241822,
8.85049129520029));
#395594=CARTESIAN_POINT('Ctrl Pts',(-2.51146432645974,0.914832983398934,
8.85711686593484));
#395595=CARTESIAN_POINT('Ctrl Pts',(-2.51218498036396,0.90631351040677,
8.85933012996512));
#395596=CARTESIAN_POINT('Origin',(-2.49211597091066,0.93525528486015,8.85049129520029));
#395597=CARTESIAN_POINT('Ctrl Pts',(-2.54864296074704,0.980775832055543,
8.78727029226991));
#395598=CARTESIAN_POINT('Ctrl Pts',(-2.55254031154222,0.985221732690706,
8.79393457792714));
#395599=CARTESIAN_POINT('Ctrl Pts',(-2.54747944236023,0.992223662303395,
8.79610912703474));
#395600=CARTESIAN_POINT('Ctrl Pts',(-2.53295611725146,0.962881074532825,
8.80838214965002));
#395601=CARTESIAN_POINT('Ctrl Pts',(-2.53685282079141,0.967326236811945,
8.81501364461993));
#395602=CARTESIAN_POINT('Ctrl Pts',(-2.53180552577562,0.974295714957313,
8.81722098428721));
#395603=CARTESIAN_POINT('Ctrl Pts',(-2.51724760581289,0.944961599316835,
8.82945683644723));
#395604=CARTESIAN_POINT('Ctrl Pts',(-2.52112899159234,0.94938928786966,
8.8360746990239));
#395605=CARTESIAN_POINT('Ctrl Pts',(-2.51611005976584,0.956342155322624,
8.83829567148519));
#395606=CARTESIAN_POINT('Ctrl Pts',(-2.50151564461753,0.927015373804532,
8.85049129520029));
#395607=CARTESIAN_POINT('Ctrl Pts',(-2.50536507777436,0.931406612421841,
8.85711686593484));
#395608=CARTESIAN_POINT('Ctrl Pts',(-2.50039125247054,0.93836087902307,
8.85933012996512));
#395609=CARTESIAN_POINT('Origin',(-2.53924328704018,0.989015743111162,8.78727029226991));
#395610=CARTESIAN_POINT('Ctrl Pts',(-2.55776447567946,0.991181222852442,
8.75374538247848));
#395611=CARTESIAN_POINT('Ctrl Pts',(-2.56278352445774,0.996886792740612,
8.75304829418602));
#395612=CARTESIAN_POINT('Ctrl Pts',(-2.55997553412122,1.00398509066891,
8.75272238421917));
#395613=CARTESIAN_POINT('Ctrl Pts',(-2.55863459984932,0.99217381584208,
8.76769408445019));
#395614=CARTESIAN_POINT('Ctrl Pts',(-2.56377943200827,0.998023418993422,
8.76974318093969));
#395615=CARTESIAN_POINT('Ctrl Pts',(-2.56116930682118,1.00510901027348,
8.7707786988043));
#395616=CARTESIAN_POINT('Ctrl Pts',(-2.55417483904275,0.987086349610347,
8.78108014887992));
#395617=CARTESIAN_POINT('Ctrl Pts',(-2.55853775190122,0.992041168344635,
8.78639403366325));
#395618=CARTESIAN_POINT('Ctrl Pts',(-2.55505961340922,0.999350383648577,
8.78812224174741));
#395619=CARTESIAN_POINT('Ctrl Pts',(-2.54686627555659,0.978749115549326,
8.78944554828685));
#395620=CARTESIAN_POINT('Ctrl Pts',(-2.55054737792007,0.982921153781,8.79673892988686));
#395621=CARTESIAN_POINT('Ctrl Pts',(-2.54506331635741,0.989951703054951,
8.79894799272499));
#395622=CARTESIAN_POINT('Origin',(-2.54848687274362,0.999560358084225,8.75721825406948));
#395623=CARTESIAN_POINT('Origin',(-2.54848687274362,0.999560358084225,9.));
#395624=CARTESIAN_POINT('Origin',(-2.54848687274362,0.999560358084225,7.51860402984325));
#395625=CARTESIAN_POINT('Ctrl Pts',(-2.5635825329696,0.985097594708666,
7.50366195182966));
#395626=CARTESIAN_POINT('Ctrl Pts',(-2.56700079967973,0.986411118369848,
7.50000065167735));
#395627=CARTESIAN_POINT('Ctrl Pts',(-2.56700079967969,0.986411118369957,
7.49482233047108));
#395628=CARTESIAN_POINT('Ctrl Pts',(-2.56237307191841,0.99243864392334,
7.50215800491336));
#395629=CARTESIAN_POINT('Ctrl Pts',(-2.56358120883208,0.995310072552473,
7.49877273257264));
#395630=CARTESIAN_POINT('Ctrl Pts',(-2.56234297166959,0.998532482377338,
7.49481816995647));
#395631=CARTESIAN_POINT('Ctrl Pts',(-2.55974479284784,0.993439726072497,
7.51043025814042));
#395632=CARTESIAN_POINT('Ctrl Pts',(-2.56224502626245,0.998716239112324,
7.51006209594515));
#395633=CARTESIAN_POINT('Ctrl Pts',(-2.56012287462731,1.00412691768342,
7.50731281821699));
#395634=CARTESIAN_POINT('Ctrl Pts',(-2.55788555007274,0.9913193105499,7.51860402984325));
#395635=CARTESIAN_POINT('Ctrl Pts',(-2.56290221972396,0.997040677781703,
7.51860402984324));
#395636=CARTESIAN_POINT('Ctrl Pts',(-2.56012379910318,1.00412456063256,
7.51860402984325));
#395637=CARTESIAN_POINT('Origin',(0.,0.,7.5));
#395638=CARTESIAN_POINT('Origin',(-2.55577009136411,0.764838063661123,7.5));
#395639=CARTESIAN_POINT('',(-2.55577009136411,0.764838063661123,7.59394543036555));
#395640=CARTESIAN_POINT('',(-2.55577009136411,0.764838063661123,8.85049129520029));
#395641=CARTESIAN_POINT('',(-2.55577009136411,0.764838063661123,7.5));
#395642=CARTESIAN_POINT('',(-2.60624502375465,0.815468607773348,8.78727029226991));
#395643=CARTESIAN_POINT('Ctrl Pts',(-2.55577009136411,0.764838063661123,
8.85049129520029));
#395644=CARTESIAN_POINT('Ctrl Pts',(-2.57261952556177,0.781739443831588,
8.82945686509571));
#395645=CARTESIAN_POINT('Ctrl Pts',(-2.5894439110381,0.798615698056739,
8.80838212259895));
#395646=CARTESIAN_POINT('Ctrl Pts',(-2.60624502375465,0.815468607773348,
8.78727029226991));
#395647=CARTESIAN_POINT('',(-2.61614521332083,0.825399319134613,8.75721825406948));
#395648=CARTESIAN_POINT('Origin',(-2.58635225143102,0.795514221183931,8.75937679713083));
#395649=CARTESIAN_POINT('',(-2.61614521332083,0.825399319134613,7.51860402984325));
#395650=CARTESIAN_POINT('',(-2.61614521332083,0.825399319134613,7.5));
#395651=CARTESIAN_POINT('Ctrl Pts',(-2.61614521332083,0.825399319134613,
7.51860402984325));
#395652=CARTESIAN_POINT('Ctrl Pts',(-2.60837015418732,0.817600289878103,
7.52834476460825));
#395653=CARTESIAN_POINT('Ctrl Pts',(-2.60059004759763,0.809796197604334,
7.53807742314407));
#395654=CARTESIAN_POINT('Ctrl Pts',(-2.59280472407667,0.801986872315774,
7.54780169004674));
#395655=CARTESIAN_POINT('Ctrl Pts',(-2.58047319238031,0.789617323116712,
7.5632044032688));
#395656=CARTESIAN_POINT('Ctrl Pts',(-2.56812855639631,0.777234629230163,
7.57858609112103));
#395657=CARTESIAN_POINT('Ctrl Pts',(-2.55577009136411,0.764838063661123,
7.59394543036555));
#395658=CARTESIAN_POINT('Origin',(-2.82817002729664,0.695957823489687,7.5));
#395659=CARTESIAN_POINT('',(-2.64284431997727,0.73544116934887,8.75721825406948));
#395660=CARTESIAN_POINT('',(-2.62912953922427,0.738363081476909,8.78727029226991));
#395661=CARTESIAN_POINT('Origin',(-2.59431631031274,0.745779984277226,8.75658640620964));
#395662=CARTESIAN_POINT('',(-2.55920636991203,0.753260100986283,8.85049129520029));
#395663=CARTESIAN_POINT('Ctrl Pts',(-2.62912953922427,0.738363081476909,
8.78727029226991));
#395664=CARTESIAN_POINT('Ctrl Pts',(-2.60585487607022,0.743321711277163,
8.80838212259895));
#395665=CARTESIAN_POINT('Ctrl Pts',(-2.58254797304887,0.74828720972964,
8.82945686509571));
#395666=CARTESIAN_POINT('Ctrl Pts',(-2.55920636991203,0.753260100986283,
8.85049129520029));
#395667=CARTESIAN_POINT('',(-2.55920636991203,0.753260100986283,7.59394543036555));
#395668=CARTESIAN_POINT('',(-2.55920636991203,0.753260100986283,7.5));
#395669=CARTESIAN_POINT('',(-2.64284431997727,0.73544116934887,7.51860402984325));
#395670=CARTESIAN_POINT('Ctrl Pts',(-2.55920636991203,0.753260100986283,
7.59394543036555));
#395671=CARTESIAN_POINT('Ctrl Pts',(-2.5763266116233,0.749612660841815,
7.57858609112103));
#395672=CARTESIAN_POINT('Ctrl Pts',(-2.59342769588662,0.745969302161038,
7.56320440326857));
#395673=CARTESIAN_POINT('Ctrl Pts',(-2.61051062671677,0.742329811040179,
7.54780169004651));
#395674=CARTESIAN_POINT('Ctrl Pts',(-2.62129567325223,0.740032074106501,
7.53807742314383));
#395675=CARTESIAN_POINT('Ctrl Pts',(-2.63207349274766,0.737735876882151,
7.52834476460825));
#395676=CARTESIAN_POINT('Ctrl Pts',(-2.64284431997727,0.73544116934887,
7.51860402984325));
#395677=CARTESIAN_POINT('',(-2.64284431997727,0.73544116934887,7.5));
#395678=CARTESIAN_POINT('Origin',(-2.56063892684945,0.759984192420898,7.5));
#395679=CARTESIAN_POINT('Ctrl Pts',(-2.55920636991203,0.753260100986283,
8.85049129520029));
#395680=CARTESIAN_POINT('Ctrl Pts',(-2.55901695934139,0.753300454605746,
8.85097269580138));
#395681=CARTESIAN_POINT('Ctrl Pts',(-2.5588316912378,0.753348525868755,
8.85143669361005));
#395682=CARTESIAN_POINT('Ctrl Pts',(-2.55864225418248,0.753407374564274,
8.8519052845931));
#395683=CARTESIAN_POINT('Ctrl Pts',(-2.55827172731594,0.753522478880658,
8.85282181883899));
#395684=CARTESIAN_POINT('Ctrl Pts',(-2.55789484136047,0.75367604126955,
8.85372622499635));
#395685=CARTESIAN_POINT('Ctrl Pts',(-2.55751150029901,0.753884750349144,
8.8546225773507));
#395686=CARTESIAN_POINT('Ctrl Pts',(-2.55719326416477,0.754058013214378,
8.85536669723986));
#395687=CARTESIAN_POINT('Ctrl Pts',(-2.55687049166869,0.754269293443464,
8.85610498449051));
#395688=CARTESIAN_POINT('Ctrl Pts',(-2.55654748330546,0.754534852746864,
8.85681338218371));
#395689=CARTESIAN_POINT('Ctrl Pts',(-2.55625435270854,0.754775848231767,
8.85745625420284));
#395690=CARTESIAN_POINT('Ctrl Pts',(-2.55595697075631,0.755064106475237,
8.85808743050666));
#395691=CARTESIAN_POINT('Ctrl Pts',(-2.55566442701757,0.75542674252638,
8.8586680450841));
#395692=CARTESIAN_POINT('Ctrl Pts',(-2.55552945367808,0.755594054939391,
8.85893592806395));
#395693=CARTESIAN_POINT('Ctrl Pts',(-2.55539561415247,0.755777419117959,
8.85919241173848));
#395694=CARTESIAN_POINT('Ctrl Pts',(-2.5552646800958,0.755980830461287,
8.85943017985535));
#395695=CARTESIAN_POINT('Ctrl Pts',(-2.55508788035867,0.756255495990983,
8.85975123720001));
#395696=CARTESIAN_POINT('Ctrl Pts',(-2.55491241676131,0.756574051157857,
8.86004599534706));
#395697=CARTESIAN_POINT('Ctrl Pts',(-2.55474952017824,0.756937693547207,
8.86026130871721));
#395698=CARTESIAN_POINT('Ctrl Pts',(-2.55468987914663,0.757070833278112,
8.86034014101236));
#395699=CARTESIAN_POINT('Ctrl Pts',(-2.55463101560014,0.757212011809917,
8.86040910639693));
#395700=CARTESIAN_POINT('Ctrl Pts',(-2.55457484371586,0.757357512262571,
8.86046313645507));
#395701=CARTESIAN_POINT('Ctrl Pts',(-2.55448718796089,0.75758456450038,
8.8605474499083));
#395702=CARTESIAN_POINT('Ctrl Pts',(-2.55440383119924,0.757828391994662,
8.86059655985668));
#395703=CARTESIAN_POINT('Ctrl Pts',(-2.55432984214789,0.758073262578132,
8.86059725258816));
#395704=CARTESIAN_POINT('Ctrl Pts',(-2.55425568215228,0.758318698910477,
8.86059794692011));
#395705=CARTESIAN_POINT('Ctrl Pts',(-2.55419265397134,0.75856867351899,
8.86056369958366));
#395706=CARTESIAN_POINT('Ctrl Pts',(-2.55414054629406,0.758808632639973,
8.86048590497774));
#395707=CARTESIAN_POINT('Ctrl Pts',(-2.55412694774172,0.758871254826106,
8.86046560290182));
#395708=CARTESIAN_POINT('Ctrl Pts',(-2.55411400454187,0.758934028803233,
8.8604425750309));
#395709=CARTESIAN_POINT('Ctrl Pts',(-2.55410208450021,0.758995008174594,
8.86041778462583));
#395710=CARTESIAN_POINT('Ctrl Pts',(-2.5540218774114,0.759405323674763,
8.860250975962));
#395711=CARTESIAN_POINT('Ctrl Pts',(-2.55397755802796,0.759789508818236,
8.8599848982295));
#395712=CARTESIAN_POINT('Ctrl Pts',(-2.55396200324606,0.760135379307712,
8.85968173251461));
#395713=CARTESIAN_POINT('Ctrl Pts',(-2.55395377565762,0.760318324980629,
8.85952137522076));
#395714=CARTESIAN_POINT('Ctrl Pts',(-2.55395324648069,0.760494068796026,
8.85934740853961));
#395715=CARTESIAN_POINT('Ctrl Pts',(-2.55395886863261,0.760660127696779,
8.8591675900182));
#395716=CARTESIAN_POINT('Ctrl Pts',(-2.55398144449489,0.761326940499001,
8.85844552518695));
#395717=CARTESIAN_POINT('Ctrl Pts',(-2.55410145860457,0.761875378979888,
8.85759444184124));
#395718=CARTESIAN_POINT('Ctrl Pts',(-2.55423947657393,0.762313757008131,
8.85683498915138));
#395719=CARTESIAN_POINT('Ctrl Pts',(-2.55425391978686,0.76235963210129,
8.85675551444998));
#395720=CARTESIAN_POINT('Ctrl Pts',(-2.55426857766554,0.76240429230562,
8.85667699793651));
#395721=CARTESIAN_POINT('Ctrl Pts',(-2.55428337034997,0.762447740242562,
8.85659965593547));
#395722=CARTESIAN_POINT('Ctrl Pts',(-2.55448304275914,0.76303420271245,
8.85555568965886));
#395723=CARTESIAN_POINT('Ctrl Pts',(-2.55475963710018,0.763568992833556,
8.85434650606346));
#395724=CARTESIAN_POINT('Ctrl Pts',(-2.55510900057033,0.764057609326325,
8.85297329937117));
#395725=CARTESIAN_POINT('Ctrl Pts',(-2.55530549623525,0.764332426331667,
8.85220095427747));
#395726=CARTESIAN_POINT('Ctrl Pts',(-2.55552534811615,0.764592565881831,
8.85137579139183));
#395727=CARTESIAN_POINT('Ctrl Pts',(-2.55577009136411,0.764838063661123,
8.85049129520029));
#395728=CARTESIAN_POINT('Origin',(-2.56063892684945,0.759984192420898,7.59394543036555));
#395729=CARTESIAN_POINT('Ctrl Pts',(-2.55865644712841,0.75337726115675,
7.59443877723642));
#395730=CARTESIAN_POINT('Ctrl Pts',(-2.55299277157865,0.754583898184068,
7.58783886950016));
#395731=CARTESIAN_POINT('Ctrl Pts',(-2.55279250630485,0.763071481783466,
7.58559994247159));
#395732=CARTESIAN_POINT('Ctrl Pts',(-2.58957428578941,0.746790265025842,
7.56670252222137));
#395733=CARTESIAN_POINT('Ctrl Pts',(-2.58391879585875,0.747995158120122,
7.56004874999027));
#395734=CARTESIAN_POINT('Ctrl Pts',(-2.58369598431129,0.756532529628374,
7.55786368756704));
#395735=CARTESIAN_POINT('Ctrl Pts',(-2.62043438847577,0.740215569452088,
7.5388891333356));
#395736=CARTESIAN_POINT('Ctrl Pts',(-2.61474528769158,0.741427623284989,
7.5322200213728));
#395737=CARTESIAN_POINT('Ctrl Pts',(-2.61454260659733,0.750004415522996,
7.53005029815327));
#395738=CARTESIAN_POINT('Ctrl Pts',(-2.65123535874695,0.733653471944914,
7.51101258149734));
#395739=CARTESIAN_POINT('Ctrl Pts',(-2.64547729572389,0.734880218072622,
7.5043616886572));
#395740=CARTESIAN_POINT('Ctrl Pts',(-2.6453308662174,0.74348754285703,7.50217374673251));
#395741=CARTESIAN_POINT('',(-2.64368796492176,0.743835290548465,7.50366116523517));
#395742=CARTESIAN_POINT('Ctrl Pts',(-2.64284431997727,0.735441169348869,
7.51860402984325));
#395743=CARTESIAN_POINT('Ctrl Pts',(-2.643276237678,0.735349149972781,7.51734760759494));
#395744=CARTESIAN_POINT('Ctrl Pts',(-2.64367893454528,0.735324188140661,
7.51608817408573));
#395745=CARTESIAN_POINT('Ctrl Pts',(-2.64405231052279,0.735379669329133,
7.5148100591312));
#395746=CARTESIAN_POINT('Ctrl Pts',(-2.64439052340533,0.735429925515418,
7.51365231206384));
#395747=CARTESIAN_POINT('Ctrl Pts',(-2.64470519151024,0.735546009950654,
7.51247773061043));
#395748=CARTESIAN_POINT('Ctrl Pts',(-2.64497808983264,0.735760556806619,
7.51129758471022));
#395749=CARTESIAN_POINT('Ctrl Pts',(-2.64531727128122,0.736027214046408,
7.50983079813402));
#395750=CARTESIAN_POINT('Ctrl Pts',(-2.64557305354003,0.736447701509528,
7.50839324291155));
#395751=CARTESIAN_POINT('Ctrl Pts',(-2.64567687122122,0.737067931918167,
7.50715379678855));
#395752=CARTESIAN_POINT('Ctrl Pts',(-2.6457248319985,0.737354460495448,
7.50658120839351));
#395753=CARTESIAN_POINT('Ctrl Pts',(-2.64573780760563,0.737725918949378,
7.50598221009429));
#395754=CARTESIAN_POINT('Ctrl Pts',(-2.64569275661509,0.738174261178699,
7.50545747549611));
#395755=CARTESIAN_POINT('Ctrl Pts',(-2.64566871601208,0.738413510469755,
7.50517746087247));
#395756=CARTESIAN_POINT('Ctrl Pts',(-2.64562809243867,0.738677267900709,
7.50491486231392));
#395757=CARTESIAN_POINT('Ctrl Pts',(-2.64557031309821,0.738958294818664,
7.50468370960993));
#395758=CARTESIAN_POINT('Ctrl Pts',(-2.64548391475877,0.739378518705923,
7.50433806340447));
#395759=CARTESIAN_POINT('Ctrl Pts',(-2.64535602063784,0.739849845429687,
7.50405484070984));
#395760=CARTESIAN_POINT('Ctrl Pts',(-2.64519455277334,0.740340344402469,
7.50385766036131));
#395761=CARTESIAN_POINT('Ctrl Pts',(-2.64517728629501,0.740392795643526,
7.50383657498791));
#395762=CARTESIAN_POINT('Ctrl Pts',(-2.64515965723778,0.740445447432375,
7.50381643264937));
#395763=CARTESIAN_POINT('Ctrl Pts',(-2.64514169100079,0.740498247390553,
7.50379723213559));
#395764=CARTESIAN_POINT('Ctrl Pts',(-2.64502176049169,0.740850704383473,
7.50366906242519));
#395765=CARTESIAN_POINT('Ctrl Pts',(-2.6448835157668,0.741217198928826,
7.50358235568538));
#395766=CARTESIAN_POINT('Ctrl Pts',(-2.64474177332799,0.741567251487561,
7.5035341175365));
#395767=CARTESIAN_POINT('Ctrl Pts',(-2.64452924658315,0.742092115681084,
7.50346178989176));
#395768=CARTESIAN_POINT('Ctrl Pts',(-2.6442782995495,0.742647713723726,
7.50346967198527));
#395769=CARTESIAN_POINT('Ctrl Pts',(-2.64401516456435,0.743185558598988,
7.50354272648693));
#395770=CARTESIAN_POINT('Ctrl Pts',(-2.64390693169839,0.743406785328913,
7.50357277531559));
#395771=CARTESIAN_POINT('Ctrl Pts',(-2.64379690799386,0.743624776871163,
7.50361331098761));
#395772=CARTESIAN_POINT('Ctrl Pts',(-2.64368796492312,0.743835290548849,
7.50366116523659));
#395773=CARTESIAN_POINT('',(-2.56344583459805,0.760817267907127,7.57603338622103));
#395774=CARTESIAN_POINT('Origin',(-2.57191671161806,0.763334355930278,7.58486873427629));
#395775=CARTESIAN_POINT('Ctrl Pts',(-2.64368796497651,0.743835290531399,
7.50366116529968));
#395776=CARTESIAN_POINT('Ctrl Pts',(-2.6169844074643,0.749487530352289,
7.52783573079709));
#395777=CARTESIAN_POINT('Ctrl Pts',(-2.59023829728154,0.755147939735831,
7.55196141284069));
#395778=CARTESIAN_POINT('Ctrl Pts',(-2.56344583569988,0.760817267312471,
7.57603338728831));
#395779=CARTESIAN_POINT('Ctrl Pts',(-2.5602488397315,0.753217766653644,
7.59639677331371));
#395780=CARTESIAN_POINT('Ctrl Pts',(-2.54113756247317,0.754196289838703,
7.59974925422225));
#395781=CARTESIAN_POINT('Ctrl Pts',(-2.5566206780635,0.765442247231691,
7.59639677331372));
#395782=CARTESIAN_POINT('Ctrl Pts',(-2.55637188217917,0.752788459978717,
7.58707626057422));
#395783=CARTESIAN_POINT('Ctrl Pts',(-2.55101612578582,0.757128195576277,
7.58811717123966));
#395784=CARTESIAN_POINT('Ctrl Pts',(-2.55313724428125,0.763687028393967,
7.58707626057424));
#395785=CARTESIAN_POINT('Ctrl Pts',(-2.56010846144155,0.757580495838095,
7.5801537675693));
#395786=CARTESIAN_POINT('Ctrl Pts',(-2.55764184525408,0.759094674335491,
7.5820876076604));
#395787=CARTESIAN_POINT('Ctrl Pts',(-2.55888304972318,0.761709314540829,
7.5801537675693));
#395788=CARTESIAN_POINT('Ctrl Pts',(-2.56344583380474,0.760817267671466,
7.57603338509286));
#395789=CARTESIAN_POINT('Ctrl Pts',(-2.56344583380474,0.760817267671466,
7.57603338509286));
#395790=CARTESIAN_POINT('Ctrl Pts',(-2.56344583380474,0.760817267671466,
7.57603338509286));
#395791=CARTESIAN_POINT('Origin',(-2.57191833523281,0.763328885433854,7.58486873427624));
#395792=CARTESIAN_POINT('Ctrl Pts',(-2.62222153593683,0.831494374752899,
7.51098857897448));
#395793=CARTESIAN_POINT('Ctrl Pts',(-2.61806498568195,0.82732501005903,
7.50433767179956));
#395794=CARTESIAN_POINT('Ctrl Pts',(-2.62263789195665,0.820031411544902,
7.50214974420965));
#395795=CARTESIAN_POINT('Ctrl Pts',(-2.59998106725738,0.809185339807811,
7.53887321589163));
#395796=CARTESIAN_POINT('Ctrl Pts',(-2.5958743198511,0.805065931502258,
7.53220407452058));
#395797=CARTESIAN_POINT('Ctrl Pts',(-2.6003834002003,0.797767225156164,
7.53003438070911));
#395798=CARTESIAN_POINT('Ctrl Pts',(-2.57769788867395,0.786833463286226,
7.56669465659234));
#395799=CARTESIAN_POINT('Ctrl Pts',(-2.57361541138129,0.782738399917917,
7.560040858333));
#395800=CARTESIAN_POINT('Ctrl Pts',(-2.57808610350574,0.77546175494548,
7.55785582193789));
#395801=CARTESIAN_POINT('Ctrl Pts',(-2.55537300796543,0.76443975607395,
7.59443891967696));
#395802=CARTESIAN_POINT('Ctrl Pts',(-2.55128461158901,0.760338755373586,
7.58783901202978));
#395803=CARTESIAN_POINT('Ctrl Pts',(-2.55574704453252,0.753116160949631,
7.58560008491213));
#395804=CARTESIAN_POINT('',(-2.62143154819292,0.818824543767658,7.50366116523517));
#395805=CARTESIAN_POINT('Ctrl Pts',(-2.62143154819328,0.81882454376777,
7.50366116523554));
#395806=CARTESIAN_POINT('Ctrl Pts',(-2.62135613216077,0.819578499959339,
7.50350835821027));
#395807=CARTESIAN_POINT('Ctrl Pts',(-2.62126227734477,0.820269115108793,
7.50345484956));
#395808=CARTESIAN_POINT('Ctrl Pts',(-2.62114778839721,0.820917002630874,
7.50349758195598));
#395809=CARTESIAN_POINT('Ctrl Pts',(-2.6210890470764,0.821249416978292,
7.50351950684424));
#395810=CARTESIAN_POINT('Ctrl Pts',(-2.62101921161052,0.821603370108029,
7.50357029184312));
#395811=CARTESIAN_POINT('Ctrl Pts',(-2.62094248805988,0.821942831958116,
7.50365515313923));
#395812=CARTESIAN_POINT('Ctrl Pts',(-2.62082445617057,0.822465061745227,
7.50378570417639));
#395813=CARTESIAN_POINT('Ctrl Pts',(-2.62068699619852,0.822968401227933,
7.50400001621911));
#395814=CARTESIAN_POINT('Ctrl Pts',(-2.6205383806345,0.823413940824885,
7.50428903009634));
#395815=CARTESIAN_POINT('Ctrl Pts',(-2.62052188545027,0.82346339229237,
7.50432110841318));
#395816=CARTESIAN_POINT('Ctrl Pts',(-2.62050526126392,0.823512160826767,
7.50435406373354));
#395817=CARTESIAN_POINT('Ctrl Pts',(-2.62048852531448,0.823560214803795,
7.50438785222351));
#395818=CARTESIAN_POINT('Ctrl Pts',(-2.62038634429886,0.823853607431238,
7.50459414719561));
#395819=CARTESIAN_POINT('Ctrl Pts',(-2.62027788322083,0.824124865059689,
7.50483629897752));
#395820=CARTESIAN_POINT('Ctrl Pts',(-2.6201685191621,0.824364084488115,
7.5050991045531));
#395821=CARTESIAN_POINT('Ctrl Pts',(-2.61992725106395,0.824891826574538,
7.50567888004914));
#395822=CARTESIAN_POINT('Ctrl Pts',(-2.61967255410296,0.825284654989918,
7.50637912803144));
#395823=CARTESIAN_POINT('Ctrl Pts',(-2.61942507433289,0.825565573186598,
7.50710440483569));
#395824=CARTESIAN_POINT('Ctrl Pts',(-2.6193643873801,0.825634459905432,
7.50728225710685));
#395825=CARTESIAN_POINT('Ctrl Pts',(-2.61930303583773,0.825698084954761,
7.50746498566954));
#395826=CARTESIAN_POINT('Ctrl Pts',(-2.61924275173433,0.825755252289281,
7.50764697238949));
#395827=CARTESIAN_POINT('Ctrl Pts',(-2.61891868098509,0.826062568146788,
7.50862528291182));
#395828=CARTESIAN_POINT('Ctrl Pts',(-2.61859888721333,0.826214167004833,
7.50965856837423));
#395829=CARTESIAN_POINT('Ctrl Pts',(-2.61829462720512,0.826275384004112,
7.51067959873204));
#395830=CARTESIAN_POINT('Ctrl Pts',(-2.61812719253884,0.82630907179603,
7.5112414730258));
#395831=CARTESIAN_POINT('Ctrl Pts',(-2.61796433543798,0.826314971464054,
7.51180065547253));
#395832=CARTESIAN_POINT('Ctrl Pts',(-2.61780749365381,0.826301290589236,
7.512351757165));
#395833=CARTESIAN_POINT('Ctrl Pts',(-2.61726554281117,0.826254017716928,
7.51425603304535));
#395834=CARTESIAN_POINT('Ctrl Pts',(-2.61673132302744,0.825961279522731,
7.51626900505178));
#395835=CARTESIAN_POINT('Ctrl Pts',(-2.61622685877216,0.825479268445089,
7.51827788969241));
#395836=CARTESIAN_POINT('Ctrl Pts',(-2.61619955621336,0.82545318109469,
7.51838661432543));
#395837=CARTESIAN_POINT('Ctrl Pts',(-2.61617233996094,0.825426529404821,
7.51849533314855));
#395838=CARTESIAN_POINT('Ctrl Pts',(-2.61614521332083,0.825399319134616,
7.51860402984325));
#395839=CARTESIAN_POINT('Ctrl Pts',(-2.56344583519815,0.760817269007159,
7.57603338728985));
#395840=CARTESIAN_POINT('Ctrl Pts',(-2.58280746249544,0.780184887898324,
7.55196141284922));
#395841=CARTESIAN_POINT('Ctrl Pts',(-2.60213510843396,0.799519746263615,
7.52783573083104));
#395842=CARTESIAN_POINT('Ctrl Pts',(-2.62143154823074,0.818824543813179,
7.50366116530176));
#395843=CARTESIAN_POINT('Origin',(-8.85789032694963E-16,2.62897535302348E-16,
7.49482233047033));
#395844=CARTESIAN_POINT('Origin',(-2.63517950238395,0.741441326212315,7.49482233047033));
#395845=CARTESIAN_POINT('Origin',(0.,0.,7.50366116523517));
#395846=CARTESIAN_POINT('Origin',(-2.61299471585145,0.816189233531305,7.49482233047033));
#395847=CARTESIAN_POINT('Ctrl Pts',(-2.64284328546499,0.735441389704302,
7.51860402984325));
#395848=CARTESIAN_POINT('Ctrl Pts',(-2.6502853612481,0.733856525650656,
7.51860402984325));
#395849=CARTESIAN_POINT('Ctrl Pts',(-2.65229555990883,0.726517902661667,
7.51860402984325));
#395850=CARTESIAN_POINT('Ctrl Pts',(-2.64560657872596,0.734852917622648,
7.51041458714366));
#395851=CARTESIAN_POINT('Ctrl Pts',(-2.65076159078754,0.732117919193946,
7.51004642900443));
#395852=CARTESIAN_POINT('Ctrl Pts',(-2.65229611429775,0.726515878756583,
7.5072913648301));
#395853=CARTESIAN_POINT('Ctrl Pts',(-2.64710665836507,0.737234828258163,
7.50215815450137));
#395854=CARTESIAN_POINT('Ctrl Pts',(-2.64979207533485,0.735657932516545,
7.49877163671529));
#395855=CARTESIAN_POINT('Ctrl Pts',(-2.65072656602323,0.732336690166504,
7.4948158853317));
#395856=CARTESIAN_POINT('Ctrl Pts',(-2.64368743498051,0.743835141443236,
7.50366171572174));
#395857=CARTESIAN_POINT('Ctrl Pts',(-2.64721228549976,0.744826903044707,
7.50000045605858));
#395858=CARTESIAN_POINT('Ctrl Pts',(-2.64721228549979,0.744826903044587,
7.49482233047317));
#395859=CARTESIAN_POINT('Origin',(-2.64023967100015,0.72321554855866,7.51860402984325));
#395860=CARTESIAN_POINT('Origin',(-2.64023967100015,0.72321554855866,9.));
#395861=CARTESIAN_POINT('Origin',(-2.64023967100015,0.72321554855866,8.75721825406948));
#395862=CARTESIAN_POINT('Ctrl Pts',(-2.62651072673473,0.738920984405482,
8.78942910404912));
#395863=CARTESIAN_POINT('Ctrl Pts',(-2.63196505478754,0.737779610586776,
8.79672699501691));
#395864=CARTESIAN_POINT('Ctrl Pts',(-2.63177229643678,0.728855691593404,
8.79893251111266));
#395865=CARTESIAN_POINT('Ctrl Pts',(-2.63726373406303,0.736630078004512,
8.78111911759583));
#395866=CARTESIAN_POINT('Ctrl Pts',(-2.64372837849713,0.735269680097243,
8.78644465894813));
#395867=CARTESIAN_POINT('Ctrl Pts',(-2.64529556141671,0.727316099175921,
8.78817647674132));
#395868=CARTESIAN_POINT('Ctrl Pts',(-2.64396526470684,0.735202330461026,
8.76780923932029));
#395869=CARTESIAN_POINT('Ctrl Pts',(-2.65159545514092,0.733591451598431,
8.76988516158374));
#395870=CARTESIAN_POINT('Ctrl Pts',(-2.65374069660727,0.726343395345381,
8.77093053738833));
#395871=CARTESIAN_POINT('Ctrl Pts',(-2.64265855794782,0.735480721690211,
8.75371302330492));
#395872=CARTESIAN_POINT('Ctrl Pts',(-2.65010163704872,0.733910124712761,
8.75300828287559));
#395873=CARTESIAN_POINT('Ctrl Pts',(-2.65209349989808,0.72653265755095,
8.75267964240738));
#395874=CARTESIAN_POINT('Origin',(-2.62652489024715,0.726137460686699,8.78727029226991));
#395875=CARTESIAN_POINT('Ctrl Pts',(-2.55920636991203,0.753260100986283,
8.85049129520029));
#395876=CARTESIAN_POINT('Ctrl Pts',(-2.5649178041393,0.752043289049023,
8.85711686593484));
#395877=CARTESIAN_POINT('Ctrl Pts',(-2.56509113287407,0.743495147773657,
8.85933012996512));
#395878=CARTESIAN_POINT('Ctrl Pts',(-2.58254800437417,0.748287203055835,
8.82945683644722));
#395879=CARTESIAN_POINT('Ctrl Pts',(-2.58830684695874,0.747060290843812,
8.8360746990239));
#395880=CARTESIAN_POINT('Ctrl Pts',(-2.58844318986647,0.738486292178717,
8.83829567148519));
#395881=CARTESIAN_POINT('Ctrl Pts',(-2.60585484624787,0.743321717630768,
8.80838214965002));
#395882=CARTESIAN_POINT('Ctrl Pts',(-2.61163641591407,0.742089963450301,
8.81501364461994));
#395883=CARTESIAN_POINT('Ctrl Pts',(-2.61175996320559,0.733485688427861,
8.81722098428721));
#395884=CARTESIAN_POINT('Ctrl Pts',(-2.62912953922427,0.738363081476909,
8.78727029226991));
#395885=CARTESIAN_POINT('Ctrl Pts',(-2.63491206922813,0.737131122698032,
8.79393457792714));
#395886=CARTESIAN_POINT('Ctrl Pts',(-2.6350441475623,0.728492721775879,
8.79610912703474));
#395887=CARTESIAN_POINT('Origin',(-2.55660172093491,0.741034480196073,8.85049129520029));
#395888=CARTESIAN_POINT('Ctrl Pts',(-2.55577009136411,0.764838063661123,
8.85049129520029));
#395889=CARTESIAN_POINT('Ctrl Pts',(-2.55989296307187,0.768973645978575,
8.85711686593484));
#395890=CARTESIAN_POINT('Ctrl Pts',(-2.55537491841652,0.776232298374591,
8.85933012996512));
#395891=CARTESIAN_POINT('Ctrl Pts',(-2.55212264627854,0.761179373682638,
8.86332496987231));
#395892=CARTESIAN_POINT('Ctrl Pts',(-2.55108096399231,0.765681239117246,
8.86648636486738));
#395893=CARTESIAN_POINT('Ctrl Pts',(-2.54518317530685,0.765984868026305,
8.87206031107457));
#395894=CARTESIAN_POINT('Ctrl Pts',(-2.55411921096854,0.754343912071706,
8.86341338519876));
#395895=CARTESIAN_POINT('Ctrl Pts',(-2.55567876663298,0.749980283219038,
8.8665458496606));
#395896=CARTESIAN_POINT('Ctrl Pts',(-2.5508498873768,0.746544285850494,
8.87215952290715));
#395897=CARTESIAN_POINT('Ctrl Pts',(-2.55920636991203,0.753260100986283,
8.85049129520029));
#395898=CARTESIAN_POINT('Ctrl Pts',(-2.5649178041393,0.752043289049023,
8.85711686593484));
#395899=CARTESIAN_POINT('Ctrl Pts',(-2.56509113287407,0.743495147773658,
8.85933012996512));
#395900=CARTESIAN_POINT('Origin',(-2.54691766320894,0.773663284097895,8.85049129520029));
#395901=CARTESIAN_POINT('Ctrl Pts',(-2.60624502375465,0.815468607773348,
8.78727029226991));
#395902=CARTESIAN_POINT('Ctrl Pts',(-2.61041921685634,0.819655669706046,
8.79393457792714));
#395903=CARTESIAN_POINT('Ctrl Pts',(-2.60581736094344,0.826967464105174,
8.79610912703474));
#395904=CARTESIAN_POINT('Ctrl Pts',(-2.58944388951045,0.798615676462725,
8.80838214965001));
#395905=CARTESIAN_POINT('Ctrl Pts',(-2.59361738938011,0.802802043026238,
8.81501364461992));
#395906=CARTESIAN_POINT('Ctrl Pts',(-2.5890270005712,0.810080582933235,
8.81722098428721));
#395907=CARTESIAN_POINT('Ctrl Pts',(-2.57261954817434,0.781739466513871,
8.82945683644723));
#395908=CARTESIAN_POINT('Ctrl Pts',(-2.57677664221002,0.785909376664977,
8.83607469902391));
#395909=CARTESIAN_POINT('Ctrl Pts',(-2.57221349406444,0.793169522772258,
8.8382956714852));
#395910=CARTESIAN_POINT('Ctrl Pts',(-2.55577009136411,0.764838063661123,
8.85049129520029));
#395911=CARTESIAN_POINT('Ctrl Pts',(-2.55989296307187,0.768973645978575,
8.85711686593484));
#395912=CARTESIAN_POINT('Ctrl Pts',(-2.55537491841652,0.776232298374591,
8.85933012996512));
#395913=CARTESIAN_POINT('Origin',(-2.59739259559948,0.824293828210121,8.78727029226991));
#395914=CARTESIAN_POINT('Ctrl Pts',(-2.61601447323369,0.825268202110593,
8.75374538247848));
#395915=CARTESIAN_POINT('Ctrl Pts',(-2.62138876695583,0.830640477734187,
8.75304829418601));
#395916=CARTESIAN_POINT('Ctrl Pts',(-2.61904133544637,0.83790410000668,
8.75272238421917));
#395917=CARTESIAN_POINT('Ctrl Pts',(-2.61694640529134,0.826203006664529,
8.7676940844502));
#395918=CARTESIAN_POINT('Ctrl Pts',(-2.62245545220154,0.831710960650642,
8.76974318093971));
#395919=CARTESIAN_POINT('Ctrl Pts',(-2.62030466518858,0.83894922511839,
8.7707786988043));
#395920=CARTESIAN_POINT('Ctrl Pts',(-2.61216985246101,0.82141173103369,
8.78108014887988));
#395921=CARTESIAN_POINT('Ctrl Pts',(-2.61684125757339,0.826076836774891,
8.78639403366323));
#395922=CARTESIAN_POINT('Ctrl Pts',(-2.61383856832237,0.833593879610395,
8.78812224174741));
#395923=CARTESIAN_POINT('Ctrl Pts',(-2.60434213678208,0.81355988798455,
8.78944554828686));
#395924=CARTESIAN_POINT('Ctrl Pts',(-2.60828297933323,0.817487505278025,
8.79673892988686));
#395925=CARTESIAN_POINT('Ctrl Pts',(-2.60326063420178,0.824854974565179,
8.79894799272499));
#395926=CARTESIAN_POINT('Origin',(-2.60729278516566,0.834224539571385,8.75721825406948));
#395927=CARTESIAN_POINT('Origin',(-2.60729278516566,0.834224539571385,9.));
#395928=CARTESIAN_POINT('Origin',(-2.60729278516566,0.834224539571385,7.51860402984325));
#395929=CARTESIAN_POINT('Ctrl Pts',(-2.62143079730771,0.818824309222877,
7.50366195182966));
#395930=CARTESIAN_POINT('Ctrl Pts',(-2.62492619857219,0.81991612500875,
7.50000065167735));
#395931=CARTESIAN_POINT('Ctrl Pts',(-2.62492619857216,0.819916125008861,
7.49482233047108));
#395932=CARTESIAN_POINT('Ctrl Pts',(-2.62069416386201,0.826227765900225,
7.50215800491338));
#395933=CARTESIAN_POINT('Ctrl Pts',(-2.62208379159276,0.829015889273454,
7.49877273257264));
#395934=CARTESIAN_POINT('Ctrl Pts',(-2.62105455902767,0.83231101243912,
7.49481816995647));
#395935=CARTESIAN_POINT('Ctrl Pts',(-2.61813542442621,0.827395185636962,
7.5104302581404));
#395936=CARTESIAN_POINT('Ctrl Pts',(-2.62096858819431,0.832500667009961,
7.51006209594514));
#395937=CARTESIAN_POINT('Ctrl Pts',(-2.61919746011361,0.838036195483735,
7.50731281821699));
#395938=CARTESIAN_POINT('Ctrl Pts',(-2.61614414617581,0.825398248829071,
7.51860402984325));
#395939=CARTESIAN_POINT('Ctrl Pts',(-2.62151707779833,0.830786441770156,
7.51860402984325));
#395940=CARTESIAN_POINT('Ctrl Pts',(-2.61919823167327,0.83803378404432,
7.51860402984325));
#395941=CARTESIAN_POINT('Origin',(0.,0.,7.5));
#395942=CARTESIAN_POINT('Origin',(-2.59952233059431,0.59951786985688,7.5));
#395943=CARTESIAN_POINT('',(-2.59952233059431,0.59951786985688,7.59394543036555));
#395944=CARTESIAN_POINT('',(-2.59952233059431,0.59951786985688,8.85049129520029));
#395945=CARTESIAN_POINT('',(-2.59952233059431,0.59951786985688,7.5));
#395946=CARTESIAN_POINT('',(-2.65313746692185,0.646810448064345,8.78727029226991));
#395947=CARTESIAN_POINT('Ctrl Pts',(-2.59952233059431,0.59951786985688,
8.85049129520029));
#395948=CARTESIAN_POINT('Ctrl Pts',(-2.61742002096782,0.615304977373523,
8.82945686509571));
#395949=CARTESIAN_POINT('Ctrl Pts',(-2.63529110426044,0.631068615445895,
8.80838212259896));
#395950=CARTESIAN_POINT('Ctrl Pts',(-2.65313746692185,0.646810448064345,
8.78727029226991));
#395951=CARTESIAN_POINT('',(-2.66365357834825,0.656086448390696,8.75721825406948));
#395952=CARTESIAN_POINT('Origin',(-2.63200708449499,0.628171594201884,8.75937679713114));
#395953=CARTESIAN_POINT('',(-2.66365357834825,0.656086448390696,7.51860402984325));
#395954=CARTESIAN_POINT('',(-2.66365357834825,0.656086448390696,7.5));
#395955=CARTESIAN_POINT('Ctrl Pts',(-2.66365357834825,0.656086448390696,
7.51860402984325));
#395956=CARTESIAN_POINT('Ctrl Pts',(-2.65539480838751,0.648801592825284,
7.52834476460825));
#395957=CARTESIAN_POINT('Ctrl Pts',(-2.64713067695249,0.641512008036755,
7.53807742314407));
#395958=CARTESIAN_POINT('Ctrl Pts',(-2.63886100402454,0.634217535235156,
7.54780169004674));
#395959=CARTESIAN_POINT('Ctrl Pts',(-2.62576228904436,0.622663484550039,
7.5632044032688));
#395960=CARTESIAN_POINT('Ctrl Pts',(-2.61264965451767,0.611097155779194,
7.57858609112102));
#395961=CARTESIAN_POINT('Ctrl Pts',(-2.59952233059431,0.59951786985688,
7.59394543036555));
#395962=CARTESIAN_POINT('Origin',(-2.86694941950356,0.51332642770833,7.5));
#395963=CARTESIAN_POINT('',(-2.68453419038077,0.564602509634903,8.75721825406948));
#395964=CARTESIAN_POINT('',(-2.67103479566853,0.568397127400933,8.78727029226991));
#395965=CARTESIAN_POINT('Origin',(-2.63676829686931,0.578029282611961,8.75658640621177));
#395966=CARTESIAN_POINT('',(-2.60220974632391,0.587743532225608,8.85049129520029));
#395967=CARTESIAN_POINT('Ctrl Pts',(-2.67103479566853,0.568397127400933,
8.78727029226991));
#395968=CARTESIAN_POINT('Ctrl Pts',(-2.64812565330825,0.574836781952707,
8.80838212259896));
#395969=CARTESIAN_POINT('Ctrl Pts',(-2.62518477739697,0.581285356659713,
8.82945686509571));
#395970=CARTESIAN_POINT('Ctrl Pts',(-2.60220974632391,0.587743532225608,
8.85049129520029));
#395971=CARTESIAN_POINT('',(-2.60220974632391,0.587743532225608,7.59394543036555));
#395972=CARTESIAN_POINT('',(-2.60220974632391,0.587743532225608,7.5));
#395973=CARTESIAN_POINT('',(-2.68453419038077,0.564602509634903,7.51860402984325));
#395974=CARTESIAN_POINT('Ctrl Pts',(-2.60220974632391,0.587743532225608,
7.59394543036555));
#395975=CARTESIAN_POINT('Ctrl Pts',(-2.61906112037001,0.58300668848554,
7.57858609112103));
#395976=CARTESIAN_POINT('Ctrl Pts',(-2.63589363782949,0.578275145245262,
7.56320440326857));
#395977=CARTESIAN_POINT('Ctrl Pts',(-2.65270828694937,0.573548624713042,
7.54780169004651));
#395978=CARTESIAN_POINT('Ctrl Pts',(-2.66332395793924,0.570564608422297,
7.53807742314383));
#395979=CARTESIAN_POINT('Ctrl Pts',(-2.67393251538731,0.567582591715426,
7.52834476460825));
#395980=CARTESIAN_POINT('Ctrl Pts',(-2.68453419038077,0.564602509634903,
7.51860402984325));
#395981=CARTESIAN_POINT('',(-2.68453419038077,0.564602509634903,7.5));
#395982=CARTESIAN_POINT('Origin',(-2.60407017393684,0.594362024055099,7.5));
#395983=CARTESIAN_POINT('Ctrl Pts',(-2.60220974632391,0.587743532225608,
8.85049129520029));
#395984=CARTESIAN_POINT('Ctrl Pts',(-2.60202331038288,0.587795938511159,
8.85097269580138));
#395985=CARTESIAN_POINT('Ctrl Pts',(-2.60184150286887,0.587855781174756,
8.85143669361005));
#395986=CARTESIAN_POINT('Ctrl Pts',(-2.60165622548117,0.587926646233124,
8.8519052845931));
#395987=CARTESIAN_POINT('Ctrl Pts',(-2.60129383466069,0.588065253793194,
8.85282181883899));
#395988=CARTESIAN_POINT('Ctrl Pts',(-2.60092756183387,0.588242647837763,
8.85372622499635));
#395989=CARTESIAN_POINT('Ctrl Pts',(-2.60055838042438,0.588475488848304,
8.8546225773507));
#395990=CARTESIAN_POINT('Ctrl Pts',(-2.60025189913029,0.588668785185525,
8.85536669723986));
#395991=CARTESIAN_POINT('Ctrl Pts',(-2.59994332657567,0.588900311421549,
8.85610498449051));
#395992=CARTESIAN_POINT('Ctrl Pts',(-2.59963799631076,0.589186020321766,
8.85681338218371));
#395993=CARTESIAN_POINT('Ctrl Pts',(-2.59936090861582,0.589445301597426,
8.85745625420284));
#395994=CARTESIAN_POINT('Ctrl Pts',(-2.59908260643578,0.589752020910516,
8.85808743050665));
#395995=CARTESIAN_POINT('Ctrl Pts',(-2.59881389793109,0.590132655228693,
8.8586680450841));
#395996=CARTESIAN_POINT('Ctrl Pts',(-2.59868992165191,0.59030827165196,
8.85893592806395));
#395997=CARTESIAN_POINT('Ctrl Pts',(-2.59856810529721,0.590499834217007,
8.85919241173848));
#395998=CARTESIAN_POINT('Ctrl Pts',(-2.59845047286812,0.590711216603729,
8.85943017985534));
#395999=CARTESIAN_POINT('Ctrl Pts',(-2.59829163426592,0.590996645401686,
8.8597512372));
#396000=CARTESIAN_POINT('Ctrl Pts',(-2.59813694107696,0.591325788054087,
8.86004599534705));
#396001=CARTESIAN_POINT('Ctrl Pts',(-2.59799767783027,0.591699120121058,
8.86026130871721));
#396002=CARTESIAN_POINT('Ctrl Pts',(-2.5979466896294,0.591835807516122,
8.86034014101235));
#396003=CARTESIAN_POINT('Ctrl Pts',(-2.59789699236396,0.591980467381866,
8.86040910639693));
#396004=CARTESIAN_POINT('Ctrl Pts',(-2.59785025813686,0.592129267833217,
8.86046313645507));
#396005=CARTESIAN_POINT('Ctrl Pts',(-2.59777732976686,0.592361469691356,
8.8605474499083));
#396006=CARTESIAN_POINT('Ctrl Pts',(-2.59770976635181,0.592610136901956,
8.86059655985668));
#396007=CARTESIAN_POINT('Ctrl Pts',(-2.59765161823106,0.592859244867346,
8.86059725258816));
#396008=CARTESIAN_POINT('Ctrl Pts',(-2.59759333576492,0.593108928371656,
8.86059794692011));
#396009=CARTESIAN_POINT('Ctrl Pts',(-2.59754645301029,0.593362427609944,
8.86056369958366));
#396010=CARTESIAN_POINT('Ctrl Pts',(-2.59750982662749,0.593605232259524,
8.86048590497774));
#396011=CARTESIAN_POINT('Ctrl Pts',(-2.59750026823207,0.593668597043899,
8.86046560290182));
#396012=CARTESIAN_POINT('Ctrl Pts',(-2.59749137356794,0.59373207131882,
8.86044257503091));
#396013=CARTESIAN_POINT('Ctrl Pts',(-2.59748338497902,0.593793689121214,
8.86041778462583));
#396014=CARTESIAN_POINT('Ctrl Pts',(-2.59742963168863,0.594208300470006,
8.86025097596201));
#396015=CARTESIAN_POINT('Ctrl Pts',(-2.59741001819078,0.594594535816544,
8.8599848982295));
#396016=CARTESIAN_POINT('Ctrl Pts',(-2.59741665536619,0.594940692276304,
8.85968173251462));
#396017=CARTESIAN_POINT('Ctrl Pts',(-2.59742016605172,0.595123789211116,
8.85952137522077));
#396018=CARTESIAN_POINT('Ctrl Pts',(-2.59743089790696,0.595299205846478,
8.85934740853961));
#396019=CARTESIAN_POINT('Ctrl Pts',(-2.59744714793786,0.595464563348899,
8.8591675900182));
#396020=CARTESIAN_POINT('Ctrl Pts',(-2.59751240025853,0.596128559672241,
8.85844552518695));
#396021=CARTESIAN_POINT('Ctrl Pts',(-2.59766730636048,0.59666818199704,
8.85759444184124));
#396022=CARTESIAN_POINT('Ctrl Pts',(-2.59783312773382,0.597096816488949,
8.85683498915139));
#396023=CARTESIAN_POINT('Ctrl Pts',(-2.59785048049892,0.59714167194698,
8.85675551444998));
#396024=CARTESIAN_POINT('Ctrl Pts',(-2.59786796965054,0.59718530125862,
8.85667699793651));
#396025=CARTESIAN_POINT('Ctrl Pts',(-2.59788551566069,0.597227712156571,
8.85659965593547));
#396026=CARTESIAN_POINT('Ctrl Pts',(-2.59812235260094,0.597800176621236,
8.85555568965886));
#396027=CARTESIAN_POINT('Ctrl Pts',(-2.59843264276994,0.598316146498407,
8.85434650606346));
#396028=CARTESIAN_POINT('Ctrl Pts',(-2.59881259420155,0.598781375281802,
8.85297329937117));
#396029=CARTESIAN_POINT('Ctrl Pts',(-2.59902629373105,0.599043038125655,
8.85220095427747));
#396030=CARTESIAN_POINT('Ctrl Pts',(-2.59926236110088,0.599288557232841,
8.85137579139183));
#396031=CARTESIAN_POINT('Ctrl Pts',(-2.59952233059431,0.59951786985688,
8.85049129520029));
#396032=CARTESIAN_POINT('Origin',(-2.60407017393684,0.594362024055099,7.59394543036555));
#396033=CARTESIAN_POINT('Ctrl Pts',(-2.60166845989353,0.587895685351658,
7.59443877723642));
#396034=CARTESIAN_POINT('Ctrl Pts',(-2.59609373047238,0.589462716152165,
7.58783886950016));
#396035=CARTESIAN_POINT('Ctrl Pts',(-2.59643767801338,0.597945692140914,
7.58559994247159));
#396036=CARTESIAN_POINT('Ctrl Pts',(-2.63210074424794,0.579341310186416,
7.56670252222136));
#396037=CARTESIAN_POINT('Ctrl Pts',(-2.6265340718935,0.580906076182574,
7.56004874999025));
#396038=CARTESIAN_POINT('Ctrl Pts',(-2.62685870940684,0.589440182330292,
7.55786368756705));
#396039=CARTESIAN_POINT('Ctrl Pts',(-2.66247619935184,0.57080290946212,
7.53888913333556));
#396040=CARTESIAN_POINT('Ctrl Pts',(-2.65687644399105,0.572376974939169,
7.53222002137275));
#396041=CARTESIAN_POINT('Ctrl Pts',(-2.65722369629234,0.580949131059962,
7.53005029815326));
#396042=CARTESIAN_POINT('Ctrl Pts',(-2.69279345069543,0.562280869547154,
7.51101258149734));
#396043=CARTESIAN_POINT('Ctrl Pts',(-2.68712581612466,0.563874015557924,
7.5043616886572));
#396044=CARTESIAN_POINT('Ctrl Pts',(-2.68753116066568,0.572473037441123,
7.50217374673251));
#396045=CARTESIAN_POINT('',(-2.68591391515804,0.572925331695047,7.50366116523517));
#396046=CARTESIAN_POINT('Ctrl Pts',(-2.68453419038077,0.564602509634902,
7.51860402984325));
#396047=CARTESIAN_POINT('Ctrl Pts',(-2.68495932495859,0.564483006260392,
7.51734760759494));
#396048=CARTESIAN_POINT('Ctrl Pts',(-2.68535959513189,0.564432294838161,
7.51608817408573));
#396049=CARTESIAN_POINT('Ctrl Pts',(-2.68573575866036,0.564463739753566,
7.5148100591312));
#396050=CARTESIAN_POINT('Ctrl Pts',(-2.68607649657317,0.564492223309341,
7.51365231206384));
#396051=CARTESIAN_POINT('Ctrl Pts',(-2.68639795571401,0.564587908381951,
7.51247773061043));
#396052=CARTESIAN_POINT('Ctrl Pts',(-2.6866840394018,0.564784529772842,
7.51129758471022));
#396053=CARTESIAN_POINT('Ctrl Pts',(-2.68703960875373,0.565028907706709,
7.50983079813402));
#396054=CARTESIAN_POINT('Ctrl Pts',(-2.68732180620472,0.565432143207649,
7.50839324291155));
#396055=CARTESIAN_POINT('Ctrl Pts',(-2.68746514888007,0.566044447664722,
7.50715379678855));
#396056=CARTESIAN_POINT('Ctrl Pts',(-2.68753136906576,0.566327314680761,
7.50658120839351));
#396057=CARTESIAN_POINT('Ctrl Pts',(-2.68756811743797,0.566697178583455,
7.50598221009429));
#396058=CARTESIAN_POINT('Ctrl Pts',(-2.68755188439478,0.567147486072456,
7.50545747549611));
#396059=CARTESIAN_POINT('Ctrl Pts',(-2.68754322194048,0.567387784086907,
7.50517746087247));
#396060=CARTESIAN_POINT('Ctrl Pts',(-2.68751958082918,0.567653602361217,
7.50491486231392));
#396061=CARTESIAN_POINT('Ctrl Pts',(-2.68747992565903,0.567937753814282,
7.50468370960992));
#396062=CARTESIAN_POINT('Ctrl Pts',(-2.68742062867114,0.568362649867107,
7.50433806340447));
#396063=CARTESIAN_POINT('Ctrl Pts',(-2.68732319532927,0.568841202404026,
7.50405484070984));
#396064=CARTESIAN_POINT('Ctrl Pts',(-2.68719348559491,0.569341038875656,
7.50385766036131));
#396065=CARTESIAN_POINT('Ctrl Pts',(-2.68717961515496,0.569394488617083,
7.50383657498791));
#396066=CARTESIAN_POINT('Ctrl Pts',(-2.68716539573021,0.569448161724763,
7.50381643264937));
#396067=CARTESIAN_POINT('Ctrl Pts',(-2.68715084931171,0.569502004300525,
7.50379723213559));
#396068=CARTESIAN_POINT('Ctrl Pts',(-2.68705374720978,0.569861421106853,
7.50366906242519));
#396069=CARTESIAN_POINT('Ctrl Pts',(-2.68693926790964,0.570236020019791,
7.50358235568538));
#396070=CARTESIAN_POINT('Ctrl Pts',(-2.68682024464032,0.570594434827236,
7.5035341175365));
#396071=CARTESIAN_POINT('Ctrl Pts',(-2.68664178271881,0.571131837266276,
7.50346178989176));
#396072=CARTESIAN_POINT('Ctrl Pts',(-2.68642694857157,0.571702372004801,
7.50346967198527));
#396073=CARTESIAN_POINT('Ctrl Pts',(-2.68619881406494,0.572255970936466,
7.50354272648692));
#396074=CARTESIAN_POINT('Ctrl Pts',(-2.68610497762026,0.572483677635879,
7.50357277531559));
#396075=CARTESIAN_POINT('Ctrl Pts',(-2.6860091467373,0.572708270534078,
7.50361331098761));
#396076=CARTESIAN_POINT('Ctrl Pts',(-2.68591391515943,0.572925331695343,
7.50366116523659));
#396077=CARTESIAN_POINT('',(-2.6069246899221,0.595013548701475,7.57603338622103));
#396078=CARTESIAN_POINT('Origin',(-2.61553943299995,0.596982734143139,7.58486873427628));
#396079=CARTESIAN_POINT('Ctrl Pts',(-2.68591391521158,0.57292533167451,
7.50366116529969));
#396080=CARTESIAN_POINT('Ctrl Pts',(-2.65962736327094,0.580276861166578,
7.52783573079709));
#396081=CARTESIAN_POINT('Ctrl Pts',(-2.63329886951444,0.587639269794993,
7.55196141284068));
#396082=CARTESIAN_POINT('Ctrl Pts',(-2.60692469098357,0.59501354803745,
7.57603338728831));
#396083=CARTESIAN_POINT('Ctrl Pts',(-2.60324736190728,0.587634493602744,
7.59639677331372));
#396084=CARTESIAN_POINT('Ctrl Pts',(-2.58509102396111,0.589736708654646,
7.59959882295461));
#396085=CARTESIAN_POINT('Ctrl Pts',(-2.60025825567991,0.599967246010122,
7.59642833564546));
#396086=CARTESIAN_POINT('Ctrl Pts',(-2.59935086420695,0.587454466507696,
7.58707626057424));
#396087=CARTESIAN_POINT('Ctrl Pts',(-2.59437047150332,0.592048808631819,
7.58809943920598));
#396088=CARTESIAN_POINT('Ctrl Pts',(-2.5967579751915,0.598374488589847,
7.58710240504252));
#396089=CARTESIAN_POINT('Ctrl Pts',(-2.60338679305819,0.591997253160073,
7.5801537675693));
#396090=CARTESIAN_POINT('Ctrl Pts',(-2.60105747402761,0.593641498959686,
7.5820588065976));
#396091=CARTESIAN_POINT('Ctrl Pts',(-2.60238830315171,0.596122621463806,
7.58020924244129));
#396092=CARTESIAN_POINT('Ctrl Pts',(-2.60692468911532,0.595013548517127,
7.57603338509286));
#396093=CARTESIAN_POINT('Ctrl Pts',(-2.60692468911532,0.595013548517126,
7.57603338509286));
#396094=CARTESIAN_POINT('Ctrl Pts',(-2.60692468911532,0.595013548517126,
7.57603338509286));
#396095=CARTESIAN_POINT('Origin',(-2.61554070278294,0.596977170861169,7.58486873427623));
#396096=CARTESIAN_POINT('Ctrl Pts',(-2.67010792806202,0.661779669736841,
7.51098857897448));
#396097=CARTESIAN_POINT('Ctrl Pts',(-2.6656927857723,0.657885182539089,
7.50433767179956));
#396098=CARTESIAN_POINT('Ctrl Pts',(-2.66978899405937,0.650313582394374,
7.50214974420965));
#396099=CARTESIAN_POINT('Ctrl Pts',(-2.64648381003428,0.64094142281747,
7.53887321589167));
#396100=CARTESIAN_POINT('Ctrl Pts',(-2.64212156898465,0.637093598487822,
7.53220407452062));
#396101=CARTESIAN_POINT('Ctrl Pts',(-2.6461537552235,0.629520990346805,
7.53003438070911));
#396102=CARTESIAN_POINT('Ctrl Pts',(-2.62281432498534,0.620063158777091,
7.56669465659229));
#396103=CARTESIAN_POINT('Ctrl Pts',(-2.61847786396929,0.616238074373824,
7.56004085833292));
#396104=CARTESIAN_POINT('Ctrl Pts',(-2.62247315433322,0.60868994182108,
7.55785582193789));
#396105=CARTESIAN_POINT('Ctrl Pts',(-2.59910054339133,0.599145821856068,
7.59443891967696));
#396106=CARTESIAN_POINT('Ctrl Pts',(-2.59475779504673,0.595315191556679,
7.58783901202978));
#396107=CARTESIAN_POINT('Ctrl Pts',(-2.59874830622959,0.587821527667248,
7.58560008491213));
#396108=CARTESIAN_POINT('',(-2.66850780457431,0.649186484966729,7.50366116523517));
#396109=CARTESIAN_POINT('Ctrl Pts',(-2.66850780457467,0.649186484966817,
7.50366116523554));
#396110=CARTESIAN_POINT('Ctrl Pts',(-2.66848084963154,0.649943723996322,
7.50350835821027));
#396111=CARTESIAN_POINT('Ctrl Pts',(-2.66843143551487,0.650638933501591,
7.50345484956));
#396112=CARTESIAN_POINT('Ctrl Pts',(-2.6683586920932,0.651292825201327,
7.50349758195598));
#396113=CARTESIAN_POINT('Ctrl Pts',(-2.66832136932309,0.651628320137165,
7.50351950684424));
#396114=CARTESIAN_POINT('Ctrl Pts',(-2.66827435519655,0.651986020405896,
7.50357029184312));
#396115=CARTESIAN_POINT('Ctrl Pts',(-2.66821953867809,0.652329700489972,
7.50365515313923));
#396116=CARTESIAN_POINT('Ctrl Pts',(-2.6681352086753,0.652858419629088,
7.50378570417639));
#396117=CARTESIAN_POINT('Ctrl Pts',(-2.66803028020088,0.65336953203749,
7.50400001621911));
#396118=CARTESIAN_POINT('Ctrl Pts',(-2.66791051580347,0.653823678057434,
7.50428903009635));
#396119=CARTESIAN_POINT('Ctrl Pts',(-2.66789722287677,0.653874084771659,
7.50432110841318));
#396120=CARTESIAN_POINT('Ctrl Pts',(-2.66788375745731,0.653923818221149,
7.50435406373354));
#396121=CARTESIAN_POINT('Ctrl Pts',(-2.66787013472256,0.653972845742091,
7.50438785222352));
#396122=CARTESIAN_POINT('Ctrl Pts',(-2.66778696137897,0.654272182323062,
7.50459414719561));
#396123=CARTESIAN_POINT('Ctrl Pts',(-2.66769610268179,0.654549831748752,
7.50483629897752));
#396124=CARTESIAN_POINT('Ctrl Pts',(-2.66760229016464,0.654795566654507,
7.5050991045531));
#396125=CARTESIAN_POINT('Ctrl Pts',(-2.66739533032925,0.655337682538336,
7.50567888004914));
#396126=CARTESIAN_POINT('Ctrl Pts',(-2.66716632527347,0.655746022335924,
7.50637912803144));
#396127=CARTESIAN_POINT('Ctrl Pts',(-2.66693735246779,0.65604221943935,
7.50710440483569));
#396128=CARTESIAN_POINT('Ctrl Pts',(-2.66688120379009,0.656114852849446,
7.50728225710685));
#396129=CARTESIAN_POINT('Ctrl Pts',(-2.66682405477194,0.656182277981104,
7.50746498566954));
#396130=CARTESIAN_POINT('Ctrl Pts',(-2.66676755725239,0.65624319027497,
7.50764697238949));
#396131=CARTESIAN_POINT('Ctrl Pts',(-2.66646384213586,0.65657063800328,
7.50862528291182));
#396132=CARTESIAN_POINT('Ctrl Pts',(-2.66615441838689,0.656742414642516,
7.50965856837422));
#396133=CARTESIAN_POINT('Ctrl Pts',(-2.66585470570012,0.656822999870563,
7.51067959873202));
#396134=CARTESIAN_POINT('Ctrl Pts',(-2.66568977343054,0.656867346023202,
7.51124147302579));
#396135=CARTESIAN_POINT('Ctrl Pts',(-2.66552762893009,0.656883667860003,
7.51180065547253));
#396136=CARTESIAN_POINT('Ctrl Pts',(-2.66537023285753,0.656880063981624,
7.512351757165));
#396137=CARTESIAN_POINT('Ctrl Pts',(-2.66482636672768,0.656867611146211,
7.51425603304536));
#396138=CARTESIAN_POINT('Ctrl Pts',(-2.6642744887553,0.65660970199309,7.5162690050518));
#396139=CARTESIAN_POINT('Ctrl Pts',(-2.66374017842015,0.656161002394707,
7.51827788969243));
#396140=CARTESIAN_POINT('Ctrl Pts',(-2.66371126053511,0.656136717924517,
7.51838661432545));
#396141=CARTESIAN_POINT('Ctrl Pts',(-2.66368239262177,0.656111864744685,
7.51849533314856));
#396142=CARTESIAN_POINT('Ctrl Pts',(-2.66365357834825,0.6560864483907,7.51860402984325));
#396143=CARTESIAN_POINT('Ctrl Pts',(-2.60692469059145,0.595013549760795,
7.57603338728985));
#396144=CARTESIAN_POINT('Ctrl Pts',(-2.62748742495179,0.613100872081649,
7.55196141284922));
#396145=CARTESIAN_POINT('Ctrl Pts',(-2.64801414879759,0.631157678379805,
7.52783573083105));
#396146=CARTESIAN_POINT('Ctrl Pts',(-2.66850780461497,0.649186485009733,
7.50366116530176));
#396147=CARTESIAN_POINT('Origin',(-9.00812987045924E-16,2.05604685939128E-16,
7.49482233047033));
#396148=CARTESIAN_POINT('Origin',(-2.6772695523474,0.571081425081873,7.49482233047033));
#396149=CARTESIAN_POINT('Origin',(0.,0.,7.50366116523517));
#396150=CARTESIAN_POINT('Origin',(-2.65991946170317,0.647097138961951,7.49482233047033));
#396151=CARTESIAN_POINT('Ctrl Pts',(-2.68453317211223,0.56460279581902,
7.51860402984325));
#396152=CARTESIAN_POINT('Ctrl Pts',(-2.69185841476393,0.56254437260601,
7.51860402984325));
#396153=CARTESIAN_POINT('Ctrl Pts',(-2.69339429606665,0.555092033734621,
7.51860402984325));
#396154=CARTESIAN_POINT('Ctrl Pts',(-2.68725308435509,0.563838488009272,
7.51041458714365));
#396155=CARTESIAN_POINT('Ctrl Pts',(-2.69222227294056,0.560778826171376,
7.51004642900443));
#396156=CARTESIAN_POINT('Ctrl Pts',(-2.69339471964448,0.555089978468046,
7.5072913648301));
#396157=CARTESIAN_POINT('Ctrl Pts',(-2.68890269145811,0.566119394321452,
7.50215815450137));
#396158=CARTESIAN_POINT('Ctrl Pts',(-2.69148155889365,0.564373683225266,
7.4987716367153));
#396159=CARTESIAN_POINT('Ctrl Pts',(-2.69220133684272,0.560999391699865,
7.49481588533171));
#396160=CARTESIAN_POINT('Ctrl Pts',(-2.68591337675241,0.572925216849624,
7.50366171572174));
#396161=CARTESIAN_POINT('Ctrl Pts',(-2.6894945274722,0.573689102822351,
7.50000045605858));
#396162=CARTESIAN_POINT('Ctrl Pts',(-2.68949452747222,0.57368910282223,
7.49482233047317));
#396163=CARTESIAN_POINT('Origin',(-2.68115159472089,0.552568888126737,7.51860402984325));
#396164=CARTESIAN_POINT('Origin',(-2.68115159472089,0.552568888126737,9.));
#396165=CARTESIAN_POINT('Origin',(-2.68115159472089,0.552568888126737,8.75721825406948));
#396166=CARTESIAN_POINT('Ctrl Pts',(-2.66845710877349,0.569121671950397,
8.78942910404912));
#396167=CARTESIAN_POINT('Ctrl Pts',(-2.67382710225269,0.567633183208423,
8.79672699501691));
#396168=CARTESIAN_POINT('Ctrl Pts',(-2.67306298249164,0.558739949433648,
8.79893251111267));
#396169=CARTESIAN_POINT('Ctrl Pts',(-2.67904124401791,0.566146524917349,
8.78111911759583));
#396170=CARTESIAN_POINT('Ctrl Pts',(-2.68540544515351,0.564374730902493,
8.78644465894813));
#396171=CARTESIAN_POINT('Ctrl Pts',(-2.68645982044843,0.556337081711785,
8.78817647674132));
#396172=CARTESIAN_POINT('Ctrl Pts',(-2.68563752954908,0.564292342291762,
8.76780923932029));
#396173=CARTESIAN_POINT('Ctrl Pts',(-2.69314883357549,0.562195905172953,
8.76988516158374));
#396174=CARTESIAN_POINT('Ctrl Pts',(-2.69482528285461,0.554825294736158,
8.77093053738833));
#396175=CARTESIAN_POINT('Ctrl Pts',(-2.68435134414654,0.564653882525808,
8.75371302330492));
#396176=CARTESIAN_POINT('Ctrl Pts',(-2.69167850214931,0.562609632792963,
8.75300828287559));
#396177=CARTESIAN_POINT('Ctrl Pts',(-2.69319359655887,0.555119704337743,
8.75267964240738));
#396178=CARTESIAN_POINT('Origin',(-2.66765220000866,0.556363505892767,8.78727029226991));
#396179=CARTESIAN_POINT('Ctrl Pts',(-2.60220974632391,0.587743532225608,
8.85049129520029));
#396180=CARTESIAN_POINT('Ctrl Pts',(-2.60783148438852,0.586163287511629,
8.85711686593484));
#396181=CARTESIAN_POINT('Ctrl Pts',(-2.60745677570887,0.577621604099134,
8.85933012996512));
#396182=CARTESIAN_POINT('Ctrl Pts',(-2.62518480823032,0.581285347992601,
8.82945683644724));
#396183=CARTESIAN_POINT('Ctrl Pts',(-2.63085321011983,0.579691986292063,
8.8360746990239));
#396184=CARTESIAN_POINT('Ctrl Pts',(-2.63043993491586,0.571126868306685,
8.8382956714852));
#396185=CARTESIAN_POINT('Ctrl Pts',(-2.64812562395425,0.57483679020398,
8.80838214965002));
#396186=CARTESIAN_POINT('Ctrl Pts',(-2.6538163960042,0.573237140354248,
8.81501364461995));
#396187=CARTESIAN_POINT('Ctrl Pts',(-2.65338841166109,0.564642628035487,
8.81722098428721));
#396188=CARTESIAN_POINT('Ctrl Pts',(-2.67103479566853,0.568397127400933,
8.78727029226991));
#396189=CARTESIAN_POINT('Ctrl Pts',(-2.67672651297436,0.566797211844102,
8.79393457792714));
#396190=CARTESIAN_POINT('Ctrl Pts',(-2.67630485569206,0.558168097155184,
8.79610912703474));
#396191=CARTESIAN_POINT('Origin',(-2.59882715066404,0.575709910717442,8.85049129520029));
#396192=CARTESIAN_POINT('Ctrl Pts',(-2.59952233059431,0.59951786985688,
8.85049129520029));
#396193=CARTESIAN_POINT('Ctrl Pts',(-2.6039016990888,0.603380801879653,
8.85711686593484));
#396194=CARTESIAN_POINT('Ctrl Pts',(-2.59985800069653,0.610914012710784,
8.85933012996512));
#396195=CARTESIAN_POINT('Ctrl Pts',(-2.59564796650408,0.596100389658347,
8.86332496987231));
#396196=CARTESIAN_POINT('Ctrl Pts',(-2.59489685997454,0.600659746340822,
8.86648636486737));
#396197=CARTESIAN_POINT('Ctrl Pts',(-2.58903064249948,0.601340624030199,
8.87206031107457));
#396198=CARTESIAN_POINT('Ctrl Pts',(-2.59720247950872,0.589151051897506,
8.86341338519877));
#396199=CARTESIAN_POINT('Ctrl Pts',(-2.59847925223829,0.584696467513824,
8.86654584966059));
#396200=CARTESIAN_POINT('Ctrl Pts',(-2.59344014932518,0.581576917126584,
8.87215952290714));
#396201=CARTESIAN_POINT('Ctrl Pts',(-2.60220974632391,0.587743532225608,
8.85049129520029));
#396202=CARTESIAN_POINT('Ctrl Pts',(-2.60783148438852,0.586163287511629,
8.85711686593484));
#396203=CARTESIAN_POINT('Ctrl Pts',(-2.60745677570887,0.577621604099134,
8.85933012996512));
#396204=CARTESIAN_POINT('Origin',(-2.59125352451697,0.608892134951029,8.85049129520029));
#396205=CARTESIAN_POINT('Ctrl Pts',(-2.65313746692185,0.646810448064345,
8.78727029226991));
#396206=CARTESIAN_POINT('Ctrl Pts',(-2.65757134967523,0.650721465758973,
8.79393457792714));
#396207=CARTESIAN_POINT('Ctrl Pts',(-2.65344741704445,0.65831307921298,
8.79610912703474));
#396208=CARTESIAN_POINT('Ctrl Pts',(-2.63529108139349,0.631068595275529,
8.80838214965003));
#396209=CARTESIAN_POINT('Ctrl Pts',(-2.63972422778674,0.634978963445187,
8.81501364461995));
#396210=CARTESIAN_POINT('Ctrl Pts',(-2.63560960807689,0.642536656032112,
8.81722098428721));
#396211=CARTESIAN_POINT('Ctrl Pts',(-2.61742004498719,0.615304998560408,
8.82945683644722));
#396212=CARTESIAN_POINT('Ctrl Pts',(-2.62183576488799,0.619199995254543,
8.83607469902389));
#396213=CARTESIAN_POINT('Ctrl Pts',(-2.61774715137787,0.626737586518493,
8.8382956714852));
#396214=CARTESIAN_POINT('Ctrl Pts',(-2.59952233059431,0.59951786985688,
8.85049129520029));
#396215=CARTESIAN_POINT('Ctrl Pts',(-2.6039016990888,0.603380801879653,
8.85711686593484));
#396216=CARTESIAN_POINT('Ctrl Pts',(-2.59985800069653,0.610914012710784,
8.85933012996512));
#396217=CARTESIAN_POINT('Origin',(-2.64486866084451,0.656184713158493,8.78727029226991));
#396218=CARTESIAN_POINT('Ctrl Pts',(-2.66351470618408,0.655963977306816,
8.75374538247848));
#396219=CARTESIAN_POINT('Ctrl Pts',(-2.66922216072437,0.660980882832946,
8.75304829418602));
#396220=CARTESIAN_POINT('Ctrl Pts',(-2.66734493414156,0.668379981667657,
8.75272238421917));
#396221=CARTESIAN_POINT('Ctrl Pts',(-2.66450461662075,0.65683715211257,
8.76769408445019));
#396222=CARTESIAN_POINT('Ctrl Pts',(-2.67035524042678,0.661980823569082,
8.76974318093969));
#396223=CARTESIAN_POINT('Ctrl Pts',(-2.66867262963315,0.669342017643231,
8.7707786988043));
#396224=CARTESIAN_POINT('Ctrl Pts',(-2.65943089964689,0.652361755462014,
8.78108014887991));
#396225=CARTESIAN_POINT('Ctrl Pts',(-2.66439160120751,0.656717978289954,
8.78639403366325));
#396226=CARTESIAN_POINT('Ctrl Pts',(-2.66187669989166,0.664411959515594,
8.78812224174741));
#396227=CARTESIAN_POINT('Ctrl Pts',(-2.6511161975379,0.645027568331988,
8.78944554828685));
#396228=CARTESIAN_POINT('Ctrl Pts',(-2.65530058650936,0.648694625265341,
8.79673892988685));
#396229=CARTESIAN_POINT('Ctrl Pts',(-2.65076059570256,0.656368740054075,
8.79894799272499));
#396230=CARTESIAN_POINT('Origin',(-2.65538477227091,0.665460713484845,8.75721825406948));
#396231=CARTESIAN_POINT('Origin',(-2.65538477227091,0.665460713484845,9.));
#396232=CARTESIAN_POINT('Origin',(-2.65538477227091,0.665460713484844,7.51860402984325));
#396233=CARTESIAN_POINT('Ctrl Pts',(-2.66850704020453,0.649186299013225,
7.50366195182966));
#396234=CARTESIAN_POINT('Ctrl Pts',(-2.67206521266982,0.650051920418533,
7.50000065167735));
#396235=CARTESIAN_POINT('Ctrl Pts',(-2.67206521266979,0.650051920418647,
7.49482233047108));
#396236=CARTESIAN_POINT('Ctrl Pts',(-2.6682462613492,0.656621740761716,
7.50215800491337));
#396237=CARTESIAN_POINT('Ctrl Pts',(-2.6698116696186,0.65931510188205,7.49877273257264));
#396238=CARTESIAN_POINT('Ctrl Pts',(-2.66899567098828,0.662669398020626,
7.49481816995647));
#396239=CARTESIAN_POINT('Ctrl Pts',(-2.66576757595734,0.657950700907936,
7.51043025814041));
#396240=CARTESIAN_POINT('Ctrl Pts',(-2.66892202800129,0.662864171096034,
7.51006209594515));
#396241=CARTESIAN_POINT('Ctrl Pts',(-2.6675092014202,0.66850180279862,7.50731281821699));
#396242=CARTESIAN_POINT('Ctrl Pts',(-2.66365244482109,0.656085448656425,
7.51860402984325));
#396243=CARTESIAN_POINT('Ctrl Pts',(-2.66935955988637,0.661118326066235,
7.51860402984324));
#396244=CARTESIAN_POINT('Ctrl Pts',(-2.66750981689315,0.668499346879757,
7.51860402984325));
#396245=CARTESIAN_POINT('Origin',(0.,0.,7.5));
#396246=CARTESIAN_POINT('Origin',(-2.6325925749723,0.431734128529216,7.5));
#396247=CARTESIAN_POINT('',(-2.6325925749723,0.431734128529216,7.59394543036555));
#396248=CARTESIAN_POINT('',(-2.6325925749723,0.431734128529216,8.85049129520029));
#396249=CARTESIAN_POINT('',(-2.6325925749723,0.431734128529216,7.5));
#396250=CARTESIAN_POINT('',(-2.68912759914126,0.475494405483839,8.78727029226991));
#396251=CARTESIAN_POINT('Ctrl Pts',(-2.63259257497231,0.431734128529216,
8.85049129520029));
#396252=CARTESIAN_POINT('Ctrl Pts',(-2.65146497607287,0.446342090780926,
8.82945686509571));
#396253=CARTESIAN_POINT('Ctrl Pts',(-2.6703093210672,0.460928336530387,
8.80838212259897));
#396254=CARTESIAN_POINT('Ctrl Pts',(-2.68912759914126,0.475494405483838,
8.78727029226991));
#396255=CARTESIAN_POINT('',(-2.70021641947034,0.48407757770024,8.75721825406948));
#396256=CARTESIAN_POINT('Origin',(-2.66684643588357,0.45824767539555,8.75937679713099));
#396257=CARTESIAN_POINT('',(-2.70021641947034,0.48407757770024,7.51860402984325));
#396258=CARTESIAN_POINT('',(-2.70021641947034,0.48407757770024,7.5));
#396259=CARTESIAN_POINT('Ctrl Pts',(-2.70021641947034,0.48407757770024,
7.51860402984325));
#396260=CARTESIAN_POINT('Ctrl Pts',(-2.69150787573963,0.47733683086004,
7.52834476460825));
#396261=CARTESIAN_POINT('Ctrl Pts',(-2.68279367854799,0.470591708024255,
7.53807742314407));
#396262=CARTESIAN_POINT('Ctrl Pts',(-2.67407363807296,0.463842062263019,
7.54780169004674));
#396263=CARTESIAN_POINT('Ctrl Pts',(-2.66026156523847,0.453150988164448,
7.5632044032688));
#396264=CARTESIAN_POINT('Ctrl Pts',(-2.64643481479703,0.4424485530352,7.57858609112103));
#396265=CARTESIAN_POINT('Ctrl Pts',(-2.6325925749723,0.431734128529216,
7.59394543036555));
#396266=CARTESIAN_POINT('Origin',(-2.89394790158701,0.328585663527346,7.5));
#396267=CARTESIAN_POINT('',(-2.71519273396521,0.391443777101987,8.75721825406948));
#396268=CARTESIAN_POINT('',(-2.70196419720223,0.396095507607665,8.78727029226991));
#396269=CARTESIAN_POINT('Origin',(-2.66838523689962,0.40790333464003,8.75658640621052));
#396270=CARTESIAN_POINT('',(-2.6345200847159,0.419811799220425,8.85049129520029));
#396271=CARTESIAN_POINT('Ctrl Pts',(-2.70196419720223,0.396095507607665,
8.78727029226991));
#396272=CARTESIAN_POINT('Ctrl Pts',(-2.67951471421566,0.403989724989103,
8.80838212259896));
#396273=CARTESIAN_POINT('Ctrl Pts',(-2.65703413439438,0.411894877373953,
8.82945686509571));
#396274=CARTESIAN_POINT('Ctrl Pts',(-2.63452008471591,0.419811799220425,
8.85049129520029));
#396275=CARTESIAN_POINT('',(-2.6345200847159,0.419811799220425,7.59394543036555));
#396276=CARTESIAN_POINT('',(-2.6345200847159,0.419811799220425,7.5));
#396277=CARTESIAN_POINT('',(-2.71519273396521,0.391443777101987,7.51860402984325));
#396278=CARTESIAN_POINT('Ctrl Pts',(-2.63452008471591,0.419811799220425,
7.59394543036555));
#396279=CARTESIAN_POINT('Ctrl Pts',(-2.65103334518629,0.414005016591735,
7.57858609112103));
#396280=CARTESIAN_POINT('Ctrl Pts',(-2.66752812741711,0.408204731718043,
7.56320440326857));
#396281=CARTESIAN_POINT('Ctrl Pts',(-2.68400539982677,0.402410604061165,
7.54780169004651));
#396282=CARTESIAN_POINT('Ctrl Pts',(-2.69440807320188,0.39875257037636,
7.53807742314383));
#396283=CARTESIAN_POINT('Ctrl Pts',(-2.70480377576452,0.395096987933257,
7.52834476460825));
#396284=CARTESIAN_POINT('Ctrl Pts',(-2.71519273396521,0.391443777101987,
7.51860402984325));
#396285=CARTESIAN_POINT('',(-2.71519273396521,0.391443777101987,7.5));
#396286=CARTESIAN_POINT('Origin',(-2.63680073810823,0.426297494642203,7.5));
#396287=CARTESIAN_POINT('Ctrl Pts',(-2.6345200847159,0.419811799220425,
8.85049129520029));
#396288=CARTESIAN_POINT('Ctrl Pts',(-2.63433738950975,0.419876042823397,
8.85097269580139));
#396289=CARTESIAN_POINT('Ctrl Pts',(-2.6341597896714,0.41994741098124,8.85143669361005));
#396290=CARTESIAN_POINT('Ctrl Pts',(-2.63397943329584,0.420030001202733,
8.8519052845931));
#396291=CARTESIAN_POINT('Ctrl Pts',(-2.63362666766303,0.420191542438292,
8.85282181883899));
#396292=CARTESIAN_POINT('Ctrl Pts',(-2.63327251305848,0.420392039188358,
8.85372622499635));
#396293=CARTESIAN_POINT('Ctrl Pts',(-2.63291900834655,0.420648055336189,
8.8546225773507));
#396294=CARTESIAN_POINT('Ctrl Pts',(-2.63262554129001,0.420860590849287,
8.85536669723986));
#396295=CARTESIAN_POINT('Ctrl Pts',(-2.63233243666767,0.421111411701283,
8.85610498449051));
#396296=CARTESIAN_POINT('Ctrl Pts',(-2.63204603916861,0.421416096159162,
8.85681338218371));
#396297=CARTESIAN_POINT('Ctrl Pts',(-2.63178613298843,0.421692597783202,
8.85745625420284));
#396298=CARTESIAN_POINT('Ctrl Pts',(-2.63152805418393,0.422016517790465,
8.85808743050665));
#396299=CARTESIAN_POINT('Ctrl Pts',(-2.63128428509418,0.422413586267619,
8.8586680450841));
#396300=CARTESIAN_POINT('Ctrl Pts',(-2.63117181532044,0.422596785055589,
8.85893592806395));
#396301=CARTESIAN_POINT('Ctrl Pts',(-2.63106252270618,0.422795758835443,
8.85919241173848));
#396302=CARTESIAN_POINT('Ctrl Pts',(-2.63095867528155,0.42301424364999,
8.85943017985534));
#396303=CARTESIAN_POINT('Ctrl Pts',(-2.63081845051617,0.423309262828054,
8.8597512372));
#396304=CARTESIAN_POINT('Ctrl Pts',(-2.6306851634031,0.42364764044822,8.86004599534706));
#396305=CARTESIAN_POINT('Ctrl Pts',(-2.63057010575534,0.424029128091272,
8.86026130871721));
#396306=CARTESIAN_POINT('Ctrl Pts',(-2.63052797990667,0.424168801472668,
8.86034014101235));
#396307=CARTESIAN_POINT('Ctrl Pts',(-2.63048765313902,0.424316348233932,
8.86040910639692));
#396308=CARTESIAN_POINT('Ctrl Pts',(-2.63045054861005,0.424467837231008,
8.86046313645506));
#396309=CARTESIAN_POINT('Ctrl Pts',(-2.63039264730333,0.424704234542235,
8.86054744990829));
#396310=CARTESIAN_POINT('Ctrl Pts',(-2.63034115486745,0.424956719642246,
8.86059655985668));
#396311=CARTESIAN_POINT('Ctrl Pts',(-2.63029908662039,0.425209041351492,
8.86059725258816));
#396312=CARTESIAN_POINT('Ctrl Pts',(-2.63025692117888,0.425461946024691,
8.86059794692011));
#396313=CARTESIAN_POINT('Ctrl Pts',(-2.63022637650186,0.425717928210008,
8.86056369958366));
#396314=CARTESIAN_POINT('Ctrl Pts',(-2.6302053819192,0.425962580651799,
8.86048590497774));
#396315=CARTESIAN_POINT('Ctrl Pts',(-2.63019990295821,0.426026427654925,
8.86046560290182));
#396316=CARTESIAN_POINT('Ctrl Pts',(-2.63019509337987,0.426090341398228,
8.86044257503091));
#396317=CARTESIAN_POINT('Ctrl Pts',(-2.63019106907052,0.426152344430887,
8.86041778462584));
#396318=CARTESIAN_POINT('Ctrl Pts',(-2.63016399046235,0.426569547901336,
8.86025097596201));
#396319=CARTESIAN_POINT('Ctrl Pts',(-2.63016916344615,0.426956246327054,
8.8599848982295));
#396320=CARTESIAN_POINT('Ctrl Pts',(-2.6301979653053,0.427301266325953,
8.85968173251462));
#396321=CARTESIAN_POINT('Ctrl Pts',(-2.63021319983864,0.427483762138081,
8.85952137522077));
#396322=CARTESIAN_POINT('Ctrl Pts',(-2.63023514862655,0.427658130768826,
8.85934740853961));
#396323=CARTESIAN_POINT('Ctrl Pts',(-2.63026195976158,0.42782210738347,
8.8591675900182));
#396324=CARTESIAN_POINT('Ctrl Pts',(-2.63036962040486,0.428480558724614,
8.85844552518695));
#396325=CARTESIAN_POINT('Ctrl Pts',(-2.63055878195666,0.429009147469447,
8.85759444184123));
#396326=CARTESIAN_POINT('Ctrl Pts',(-2.6307517253384,0.429426277073954,
8.85683498915138));
#396327=CARTESIAN_POINT('Ctrl Pts',(-2.63077191634944,0.429469928576157,
8.85675551444997));
#396328=CARTESIAN_POINT('Ctrl Pts',(-2.63079216490732,0.429512347712904,
8.85667699793651));
#396329=CARTESIAN_POINT('Ctrl Pts',(-2.63081239214286,0.429553547296386,
8.85659965593547));
#396330=CARTESIAN_POINT('Ctrl Pts',(-2.63108542040041,0.43010966137655,
8.85555568965886));
#396331=CARTESIAN_POINT('Ctrl Pts',(-2.63142813134851,0.430604690778885,
8.85434650606346));
#396332=CARTESIAN_POINT('Ctrl Pts',(-2.63183710943965,0.431044620128043,
8.85297329937117));
#396333=CARTESIAN_POINT('Ctrl Pts',(-2.63206713469651,0.431292053581656,
8.85220095427747));
#396334=CARTESIAN_POINT('Ctrl Pts',(-2.63231844750382,0.431521943355189,
8.85137579139183));
#396335=CARTESIAN_POINT('Ctrl Pts',(-2.6325925749723,0.431734128529216,
8.85049129520029));
#396336=CARTESIAN_POINT('Origin',(-2.63680073810823,0.426297494642203,7.59394543036555));
#396337=CARTESIAN_POINT('Ctrl Pts',(-2.6339896589008,0.419998320072227,
7.59443877723642));
#396338=CARTESIAN_POINT('Ctrl Pts',(-2.62852678336725,0.421919305380237,
7.58783886950016));
#396339=CARTESIAN_POINT('Ctrl Pts',(-2.62941353036882,0.430362815390407,
7.58559994247159));
#396340=CARTESIAN_POINT('Ctrl Pts',(-2.66381133616454,0.409511717635108,
7.56670252222138));
#396341=CARTESIAN_POINT('Ctrl Pts',(-2.65835635603707,0.411429926574002,
7.56004874999029));
#396342=CARTESIAN_POINT('Ctrl Pts',(-2.65922710860603,0.419925698888489,
7.55786368756704));
#396343=CARTESIAN_POINT('Ctrl Pts',(-2.69357732442549,0.399044697880317,
7.53888913333559));
#396344=CARTESIAN_POINT('Ctrl Pts',(-2.68808992508402,0.400974306828835,
7.53222002137275));
#396345=CARTESIAN_POINT('Ctrl Pts',(-2.68898568384657,0.409506602004173,
7.53005029815327));
#396346=CARTESIAN_POINT('Ctrl Pts',(-2.72328627675262,0.388597734447555,
7.51101258149734));
#396347=CARTESIAN_POINT('Ctrl Pts',(-2.7177323601603,0.390550733762701,
7.5043616886572));
#396348=CARTESIAN_POINT('Ctrl Pts',(-2.71868781310115,0.399106117519288,
7.50217374673251));
#396349=CARTESIAN_POINT('',(-2.71710286899021,0.399661099761597,7.50366116523517));
#396350=CARTESIAN_POINT('Ctrl Pts',(-2.71519273396521,0.391443777101986,
7.51860402984325));
#396351=CARTESIAN_POINT('Ctrl Pts',(-2.71560933845096,0.391297280794053,
7.51734760759494));
#396352=CARTESIAN_POINT('Ctrl Pts',(-2.71600553713428,0.391221028165823,
7.51608817408573));
#396353=CARTESIAN_POINT('Ctrl Pts',(-2.71638294247708,0.39122830759426,
7.5148100591312));
#396354=CARTESIAN_POINT('Ctrl Pts',(-2.71672480525499,0.391234901474485,
7.51365231206384));
#396355=CARTESIAN_POINT('Ctrl Pts',(-2.7170517344872,0.391309793993984,
7.51247773061042));
#396356=CARTESIAN_POINT('Ctrl Pts',(-2.71734982796114,0.39148768196033,
7.51129758471022));
#396357=CARTESIAN_POINT('Ctrl Pts',(-2.71772032410568,0.391708776386926,
7.50983079813401));
#396358=CARTESIAN_POINT('Ctrl Pts',(-2.71802777713899,0.39209310294452,
7.50839324291155));
#396359=CARTESIAN_POINT('Ctrl Pts',(-2.7182100557827,0.392694965359674,
7.50715379678855));
#396360=CARTESIAN_POINT('Ctrl Pts',(-2.71829426326387,0.392973008453226,
7.50658120839351));
#396361=CARTESIAN_POINT('Ctrl Pts',(-2.71835463339421,0.393339757954573,
7.50598221009429));
#396362=CARTESIAN_POINT('Ctrl Pts',(-2.71836728500343,0.39379018029319,
7.50545747549611));
#396363=CARTESIAN_POINT('Ctrl Pts',(-2.71837403629372,0.394030539594952,
7.50517746087247));
#396364=CARTESIAN_POINT('Ctrl Pts',(-2.71836747479092,0.39429732640831,
7.50491486231392));
#396365=CARTESIAN_POINT('Ctrl Pts',(-2.71834610674268,0.394583434757215,
7.50468370960992));
#396366=CARTESIAN_POINT('Ctrl Pts',(-2.71831415477038,0.395011256986588,
7.50433806340447));
#396367=CARTESIAN_POINT('Ctrl Pts',(-2.71824758258208,0.395495068861645,
7.50405484070984));
#396368=CARTESIAN_POINT('Ctrl Pts',(-2.71815016398297,0.396002188896854,
7.50385766036131));
#396369=CARTESIAN_POINT('Ctrl Pts',(-2.71813974657802,0.39605641750219,
7.50383657498791));
#396370=CARTESIAN_POINT('Ctrl Pts',(-2.71812899521642,0.396110891374383,
7.50381643264937));
#396371=CARTESIAN_POINT('Ctrl Pts',(-2.71811792839077,0.39616555531703,
7.50379723213559));
#396372=CARTESIAN_POINT('Ctrl Pts',(-2.71804405370936,0.396530455016013,
7.50366906242519));
#396373=CARTESIAN_POINT('Ctrl Pts',(-2.71795381025398,0.396911618989251,
7.50358235568538));
#396374=CARTESIAN_POINT('Ctrl Pts',(-2.71785799524629,0.397276923242083,
7.5035341175365));
#396375=CARTESIAN_POINT('Ctrl Pts',(-2.71771433148642,0.397824655624746,
7.50346178989176));
#396376=CARTESIAN_POINT('Ctrl Pts',(-2.71753649302518,0.398407782609535,
7.50346967198527));
#396377=CARTESIAN_POINT('Ctrl Pts',(-2.7173442964507,0.398974860740847,
7.50354272648692));
#396378=CARTESIAN_POINT('Ctrl Pts',(-2.71726524202138,0.399208111714077,
7.50357277531559));
#396379=CARTESIAN_POINT('Ctrl Pts',(-2.71718399774964,0.39943838306783,
7.50361331098761));
#396380=CARTESIAN_POINT('Ctrl Pts',(-2.71710286899161,0.399661099761803,
7.50366116523659));
#396381=CARTESIAN_POINT('',(-2.63969113251167,0.426764791194204,7.57603338622103));
#396382=CARTESIAN_POINT('Origin',(-2.64841434182066,0.428177982249233,7.58486873427627));
#396383=CARTESIAN_POINT('Ctrl Pts',(-2.71710286904232,0.399661099737671,
7.50366116529969));
#396384=CARTESIAN_POINT('Ctrl Pts',(-2.69134133975362,0.408681709889307,
7.52783573079709));
#396385=CARTESIAN_POINT('Ctrl Pts',(-2.66553865185168,0.417715864046332,
7.55196141284068));
#396386=CARTESIAN_POINT('Ctrl Pts',(-2.63969113352841,0.426764790463535,
7.57603338728831));
#396387=CARTESIAN_POINT('Ctrl Pts',(-2.6355485822783,0.419636504370411,
7.59639677331371));
#396388=CARTESIAN_POINT('Ctrl Pts',(-2.61671933910964,0.42305088978551,
7.59974925422225));
#396389=CARTESIAN_POINT('Ctrl Pts',(-2.63351343964677,0.43222458114812,
7.59639677331372));
#396390=CARTESIAN_POINT('Ctrl Pts',(-2.63164855597479,0.419706496625095,
7.58707626057422));
#396391=CARTESIAN_POINT('Ctrl Pts',(-2.62689172333806,0.424695481979636,
7.58811717123965));
#396392=CARTESIAN_POINT('Ctrl Pts',(-2.62983415240462,0.430929224257757,
7.58707626057423));
#396393=CARTESIAN_POINT('Ctrl Pts',(-2.63596724991744,0.423981366785865,
7.58015376756929));
#396394=CARTESIAN_POINT('Ctrl Pts',(-2.63371451346331,0.425798537775723,
7.5820876076604));
#396395=CARTESIAN_POINT('Ctrl Pts',(-2.63527988042915,0.428232990116566,
7.5801537675693));
#396396=CARTESIAN_POINT('Ctrl Pts',(-2.63969113169474,0.426764791061924,
7.57603338509286));
#396397=CARTESIAN_POINT('Ctrl Pts',(-2.63969113169474,0.426764791061924,
7.57603338509286));
#396398=CARTESIAN_POINT('Ctrl Pts',(-2.63969113169474,0.426764791061924,
7.57603338509286));
#396399=CARTESIAN_POINT('Origin',(-2.64841525255382,0.428172349042207,7.5848687342762));
#396400=CARTESIAN_POINT('Ctrl Pts',(-2.70702227397444,0.489345570106541,
7.51098857897448));
#396401=CARTESIAN_POINT('Ctrl Pts',(-2.70236668241661,0.485741963688167,
7.50433767179956));
#396402=CARTESIAN_POINT('Ctrl Pts',(-2.70596936051755,0.477923475241962,
7.50214974420965));
#396403=CARTESIAN_POINT('Ctrl Pts',(-2.68211158316672,0.470063740039235,
7.53887321589164));
#396404=CARTESIAN_POINT('Ctrl Pts',(-2.67751177385793,0.466503311220993,
7.53220407452058));
#396405=CARTESIAN_POINT('Ctrl Pts',(-2.6810504968683,0.458687918756245,
7.53003438070911));
#396406=CARTESIAN_POINT('Ctrl Pts',(-2.65715305464352,0.450744881745466,
7.56669465659234));
#396407=CARTESIAN_POINT('Ctrl Pts',(-2.65258042935257,0.447205494399617,
7.56004085833301));
#396408=CARTESIAN_POINT('Ctrl Pts',(-2.6560839004508,0.439416891162178,
7.55785582193789));
#396409=CARTESIAN_POINT('Ctrl Pts',(-2.63214781717911,0.431389868939804,
7.59443891967696));
#396410=CARTESIAN_POINT('Ctrl Pts',(-2.6275685621508,0.427845349922958,
7.58783901202978));
#396411=CARTESIAN_POINT('Ctrl Pts',(-2.6310707537066,0.420111409640359,
7.58560008491213));
#396412=CARTESIAN_POINT('',(-2.70461858999357,0.476880779649006,7.50366116523517));
#396413=CARTESIAN_POINT('Ctrl Pts',(-2.70461858999394,0.476880779649071,
7.50366116523554));
#396414=CARTESIAN_POINT('Ctrl Pts',(-2.70464020690383,0.477638189858912,
7.50350835821027));
#396415=CARTESIAN_POINT('Ctrl Pts',(-2.70463543653969,0.478335136955017,
7.50345484956));
#396416=CARTESIAN_POINT('Ctrl Pts',(-2.70460473756223,0.478992345851155,
7.50349758195598));
#396417=CARTESIAN_POINT('Ctrl Pts',(-2.7045889867101,0.479329542754757,
7.50351950684424));
#396418=CARTESIAN_POINT('Ctrl Pts',(-2.70456498711403,0.479689520295352,
7.50357029184312));
#396419=CARTESIAN_POINT('Ctrl Pts',(-2.70453230288058,0.480036006358231,
7.50365515313923));
#396420=CARTESIAN_POINT('Ctrl Pts',(-2.70448202129437,0.480569042228999,
7.50378570417639));
#396421=CARTESIAN_POINT('Ctrl Pts',(-2.7044100554912,0.481085827292577,
7.50400001621911));
#396422=CARTESIAN_POINT('Ctrl Pts',(-2.70431963439798,0.481546713552103,
7.50428903009634));
#396423=CARTESIAN_POINT('Ctrl Pts',(-2.70430959835229,0.481597868381067,
7.50432110841318));
#396424=CARTESIAN_POINT('Ctrl Pts',(-2.70429934703203,0.48164836238024,
7.50435406373354));
#396425=CARTESIAN_POINT('Ctrl Pts',(-2.7042888934907,0.481698161980497,
7.50438785222352));
#396426=CARTESIAN_POINT('Ctrl Pts',(-2.70422506959627,0.482002212476779,
7.50459414719561));
#396427=CARTESIAN_POINT('Ctrl Pts',(-2.7041521866378,0.482285112778662,
7.50483629897752));
#396428=CARTESIAN_POINT('Ctrl Pts',(-2.704074311158,0.482536353384309,7.5050991045531));
#396429=CARTESIAN_POINT('Ctrl Pts',(-2.70390251002772,0.483090615395093,
7.50567888004914));
#396430=CARTESIAN_POINT('Ctrl Pts',(-2.70370013790804,0.483512788619073,
7.50637912803145));
#396431=CARTESIAN_POINT('Ctrl Pts',(-2.70349061296512,0.483823047491813,
7.50710440483569));
#396432=CARTESIAN_POINT('Ctrl Pts',(-2.70343923328946,0.48389912912691,
7.50728225710685));
#396433=CARTESIAN_POINT('Ctrl Pts',(-2.70338652163312,0.483970077276568,
7.50746498566954));
#396434=CARTESIAN_POINT('Ctrl Pts',(-2.70333404285786,0.484034484228099,
7.50764697238949));
#396435=CARTESIAN_POINT('Ctrl Pts',(-2.70305193140459,0.48438071827426,
7.50862528291182));
#396436=CARTESIAN_POINT('Ctrl Pts',(-2.70275414916696,0.484571966827631,
7.50965856837422));
#396437=CARTESIAN_POINT('Ctrl Pts',(-2.70246021538533,0.484671589142456,
7.51067959873202));
#396438=CARTESIAN_POINT('Ctrl Pts',(-2.70229846325455,0.484726411427962,
7.51124147302579));
#396439=CARTESIAN_POINT('Ctrl Pts',(-2.70213769764104,0.484753088363612,
7.51180065547253));
#396440=CARTESIAN_POINT('Ctrl Pts',(-2.70198039405431,0.484759576290781,
7.51235175716501));
#396441=CARTESIAN_POINT('Ctrl Pts',(-2.70143684749985,0.484781994663633,
7.51425603304536));
#396442=CARTESIAN_POINT('Ctrl Pts',(-2.70086957912378,0.484559974355621,
7.5162690050518));
#396443=CARTESIAN_POINT('Ctrl Pts',(-2.70030761830454,0.484146430039397,
7.51827788969244));
#396444=CARTESIAN_POINT('Ctrl Pts',(-2.70027720392305,0.484124048239512,
7.51838661432545));
#396445=CARTESIAN_POINT('Ctrl Pts',(-2.70024680297323,0.484101095696761,
7.51849533314856));
#396446=CARTESIAN_POINT('Ctrl Pts',(-2.70021641947034,0.484077577700244,
7.51860402984325));
#396447=CARTESIAN_POINT('Ctrl Pts',(-2.63969113324751,0.426764792208463,
7.57603338728985));
#396448=CARTESIAN_POINT('Ctrl Pts',(-2.66137047798473,0.443497493271876,
7.55196141284922));
#396449=CARTESIAN_POINT('Ctrl Pts',(-2.68301193102658,0.460202048212608,
7.52783573083104));
#396450=CARTESIAN_POINT('Ctrl Pts',(-2.7046185900369,0.476880779689317,
7.50366116530176));
#396451=CARTESIAN_POINT('Origin',(-9.12135307609333E-16,1.47466962819317E-16,
7.49482233047033));
#396452=CARTESIAN_POINT('Origin',(-2.70835812744774,0.398374827879188,7.49482233047033));
#396453=CARTESIAN_POINT('Origin',(0.,0.,7.50366116523517));
#396454=CARTESIAN_POINT('Origin',(-2.69591402793581,0.475345983446701,7.49482233047033));
#396455=CARTESIAN_POINT('Ctrl Pts',(-2.7151917361247,0.391444127938797,
7.51860402984325));
#396456=CARTESIAN_POINT('Ctrl Pts',(-2.72237004465166,0.388920604068936,
7.51860402984325));
#396457=CARTESIAN_POINT('Ctrl Pts',(-2.72342529733067,0.381385172574091,
7.51860402984325));
#396458=CARTESIAN_POINT('Ctrl Pts',(-2.71785709064666,0.390507125105682,
7.51041458714365));
#396459=CARTESIAN_POINT('Ctrl Pts',(-2.7226200362942,0.387135372665384,
7.51004642900441));
#396460=CARTESIAN_POINT('Ctrl Pts',(-2.72342558835683,0.381383094391554,
7.50729136483009));
#396461=CARTESIAN_POINT('Ctrl Pts',(-2.71964944662411,0.392677654361255,
7.50215815450138));
#396462=CARTESIAN_POINT('Ctrl Pts',(-2.72211116740598,0.390770301411846,
7.49877163671532));
#396463=CARTESIAN_POINT('Ctrl Pts',(-2.72261327489375,0.387356826398741,
7.49481588533172));
#396464=CARTESIAN_POINT('Ctrl Pts',(-2.71710232433262,0.399661019647903,
7.50366171572174));
#396465=CARTESIAN_POINT('Ctrl Pts',(-2.72072505953649,0.400193891020572,
7.50000045605858));
#396466=CARTESIAN_POINT('Ctrl Pts',(-2.72072505953651,0.400193891020448,
7.49482233047317));
#396467=CARTESIAN_POINT('Origin',(-2.71104609143371,0.379651603607846,7.51860402984325));
#396468=CARTESIAN_POINT('Origin',(-2.71104609143371,0.379651603607846,9.));
#396469=CARTESIAN_POINT('Origin',(-2.71104609143371,0.379651603607846,8.75721825406948));
#396470=CARTESIAN_POINT('Ctrl Pts',(-2.69943822817004,0.396983716469052,
8.78942910404912));
#396471=CARTESIAN_POINT('Ctrl Pts',(-2.70470182062058,0.395154229323329,
8.7967269950169));
#396472=CARTESIAN_POINT('Ctrl Pts',(-2.70336947938123,0.386328224972321,
8.79893251111267));
#396473=CARTESIAN_POINT('Ctrl Pts',(-2.70980999884857,0.393336554321251,
8.78111911759583));
#396474=CARTESIAN_POINT('Ctrl Pts',(-2.71604760481807,0.391160644880466,
8.78644465894814));
#396475=CARTESIAN_POINT('Ctrl Pts',(-2.71658483983411,0.383071955844967,
8.78817647674132));
#396476=CARTESIAN_POINT('Ctrl Pts',(-2.71627393371497,0.391063555847688,
8.76780923932029));
#396477=CARTESIAN_POINT('Ctrl Pts',(-2.72363548577431,0.388490175182464,
8.76988516158374));
#396478=CARTESIAN_POINT('Ctrl Pts',(-2.72483625397649,0.381027297981215,
8.77093053738832));
#396479=CARTESIAN_POINT('Ctrl Pts',(-2.7150135548806,0.391506759440228,
8.75371302330492));
#396480=CARTESIAN_POINT('Ctrl Pts',(-2.72219468292134,0.388997257212635,
8.75300828287559));
#396481=CARTESIAN_POINT('Ctrl Pts',(-2.72322678304317,0.381425645186602,
8.75267964240738));
#396482=CARTESIAN_POINT('Origin',(-2.69781755467073,0.384303334113524,8.78727029226991));
#396483=CARTESIAN_POINT('Ctrl Pts',(-2.63452008471591,0.419811799220425,
8.85049129520029));
#396484=CARTESIAN_POINT('Ctrl Pts',(-2.64002902569028,0.417874615294219,
8.85711686593484));
#396485=CARTESIAN_POINT('Ctrl Pts',(-2.63910781935456,0.409374489353921,
8.85933012996512));
#396486=CARTESIAN_POINT('Ctrl Pts',(-2.65703416460908,0.411894866749149,
8.82945683644722));
#396487=CARTESIAN_POINT('Ctrl Pts',(-2.66258883312432,0.409941603025127,
8.83607469902391));
#396488=CARTESIAN_POINT('Ctrl Pts',(-2.66162763804508,0.401420561626479,
8.8382956714852));
#396489=CARTESIAN_POINT('Ctrl Pts',(-2.67951468545063,0.403989735104143,
8.80838214965003));
#396490=CARTESIAN_POINT('Ctrl Pts',(-2.68509127528126,0.402028762889477,
8.8150136446199));
#396491=CARTESIAN_POINT('Ctrl Pts',(-2.68411351798304,0.393479329969056,
8.81722098428721));
#396492=CARTESIAN_POINT('Ctrl Pts',(-2.70196419720223,0.396095507607664,
8.78727029226991));
#396493=CARTESIAN_POINT('Ctrl Pts',(-2.70754171332274,0.394134209669084,
8.79393457792714));
#396494=CARTESIAN_POINT('Ctrl Pts',(-2.7065680531042,0.385549840096597,
8.79610912703474));
#396495=CARTESIAN_POINT('Origin',(-2.6303734421844,0.408019625726284,8.85049129520029));
#396496=CARTESIAN_POINT('Ctrl Pts',(-2.6325925749723,0.431734128529216,
8.85049129520029));
#396497=CARTESIAN_POINT('Ctrl Pts',(-2.63721044448901,0.435308536641031,
8.85711686593484));
#396498=CARTESIAN_POINT('Ctrl Pts',(-2.63365770878388,0.443085350328103,
8.85933012996512));
#396499=CARTESIAN_POINT('Ctrl Pts',(-2.62850721247053,0.428571901269819,
8.86332496987231));
#396500=CARTESIAN_POINT('Ctrl Pts',(-2.62804976815553,0.433170013825585,
8.86648636486736));
#396501=CARTESIAN_POINT('Ctrl Pts',(-2.62223922743675,0.434225342422805,
8.87206031107457));
#396502=CARTESIAN_POINT('Ctrl Pts',(-2.62961328596242,0.42153724367855,
8.86341338519877));
#396503=CARTESIAN_POINT('Ctrl Pts',(-2.63060202922408,0.417010008606594,
8.86654584966058));
#396504=CARTESIAN_POINT('Ctrl Pts',(-2.62537340940882,0.414219724102341,
8.87215952290714));
#396505=CARTESIAN_POINT('Ctrl Pts',(-2.6345200847159,0.419811799220425,
8.85049129520029));
#396506=CARTESIAN_POINT('Ctrl Pts',(-2.64002902569028,0.417874615294219,
8.85711686593485));
#396507=CARTESIAN_POINT('Ctrl Pts',(-2.63910781935455,0.409374489353921,
8.85933012996512));
#396508=CARTESIAN_POINT('Origin',(-2.62494136927062,0.441618917414695,8.85049129520029));
#396509=CARTESIAN_POINT('Ctrl Pts',(-2.68912759914126,0.475494405483839,
8.78727029226991));
#396510=CARTESIAN_POINT('Ctrl Pts',(-2.69380295177104,0.479113307729781,
8.79393457792714));
#396511=CARTESIAN_POINT('Ctrl Pts',(-2.69017388854615,0.486953544670587,
8.79610912703474));
#396512=CARTESIAN_POINT('Ctrl Pts',(-2.67030929695491,0.460928317866552,
8.80838214965004));
#396513=CARTESIAN_POINT('Ctrl Pts',(-2.67498387312222,0.464546619100771,
8.81501364461989));
#396514=CARTESIAN_POINT('Ctrl Pts',(-2.6713619303665,0.472352408187695,
8.81722098428721));
#396515=CARTESIAN_POINT('Ctrl Pts',(-2.65146500140035,0.44634211038536,
8.82945683644723));
#396516=CARTESIAN_POINT('Ctrl Pts',(-2.65612120202605,0.449946188245617,
8.83607469902389));
#396517=CARTESIAN_POINT('Ctrl Pts',(-2.65252392414128,0.457730251086941,
8.8382956714852));
#396518=CARTESIAN_POINT('Ctrl Pts',(-2.63259257497231,0.431734128529216,
8.85049129520029));
#396519=CARTESIAN_POINT('Ctrl Pts',(-2.63721044448901,0.435308536641031,
8.85711686593484));
#396520=CARTESIAN_POINT('Ctrl Pts',(-2.63365770878388,0.443085350328103,
8.85933012996512));
#396521=CARTESIAN_POINT('Origin',(-2.68147639343958,0.485379194369317,8.78727029226991));
#396522=CARTESIAN_POINT('Ctrl Pts',(-2.70006998588464,0.483964255816441,
8.75374538247848));
#396523=CARTESIAN_POINT('Ctrl Pts',(-2.70608714808814,0.488605175704185,
8.75304829418602));
#396524=CARTESIAN_POINT('Ctrl Pts',(-2.70468784035867,0.496109346616901,
8.75272238421917));
#396525=CARTESIAN_POINT('Ctrl Pts',(-2.70111380694607,0.484772212811493,
8.76769408445017));
#396526=CARTESIAN_POINT('Ctrl Pts',(-2.70728196617972,0.489530465289048,
8.76974318093969));
#396527=CARTESIAN_POINT('Ctrl Pts',(-2.70607444581406,0.496984340244175,
8.77077869880429));
#396528=CARTESIAN_POINT('Ctrl Pts',(-2.69576377481994,0.480631085505944,
8.78108014887993));
#396529=CARTESIAN_POINT('Ctrl Pts',(-2.70099338824204,0.484660524766653,
8.78639403366326));
#396530=CARTESIAN_POINT('Ctrl Pts',(-2.69897660913032,0.492499828163215,
8.78812224174742));
#396531=CARTESIAN_POINT('Ctrl Pts',(-2.68699625317539,0.47384469204318,
8.78944554828685));
#396532=CARTESIAN_POINT('Ctrl Pts',(-2.69140699401534,0.477236119892881,
8.79673892988686));
#396533=CARTESIAN_POINT('Ctrl Pts',(-2.68736801332924,0.485185345599439,
8.79894799272499));
#396534=CARTESIAN_POINT('Origin',(-2.69256521376866,0.493962366585719,8.75721825406948));
#396535=CARTESIAN_POINT('Origin',(-2.69256521376866,0.493962366585719,9.));
#396536=CARTESIAN_POINT('Origin',(-2.69256521376866,0.493962366585719,7.51860402984325));
#396537=CARTESIAN_POINT('Ctrl Pts',(-2.70461781528019,0.476880643050904,
7.50366195182966));
#396538=CARTESIAN_POINT('Ctrl Pts',(-2.70822413765239,0.477516513051618,
7.50000065167735));
#396539=CARTESIAN_POINT('Ctrl Pts',(-2.70822413765237,0.477516513051733,
7.49482233047108));
#396540=CARTESIAN_POINT('Ctrl Pts',(-2.70483396261147,0.484317516045507,
7.50215800491337));
#396541=CARTESIAN_POINT('Ctrl Pts',(-2.70656871882114,0.486905047314383,
7.49877273257267));
#396542=CARTESIAN_POINT('Ctrl Pts',(-2.70596930723901,0.490304732903542,
7.49481816995649));
#396543=CARTESIAN_POINT('Ctrl Pts',(-2.70244551671349,0.48580255561889,
7.51043025814043));
#396544=CARTESIAN_POINT('Ctrl Pts',(-2.70590829471324,0.490503824119143,
7.51006209594515));
#396545=CARTESIAN_POINT('Ctrl Pts',(-2.70485957523922,0.496220392812616,
7.50731281821699));
#396546=CARTESIAN_POINT('Ctrl Pts',(-2.70021522421893,0.48407665264536,
7.51860402984326));
#396547=CARTESIAN_POINT('Ctrl Pts',(-2.70623307096702,0.488733533351069,
7.51860402984327));
#396548=CARTESIAN_POINT('Ctrl Pts',(-2.70486003209637,0.496217902506207,
7.51860402984327));
#396549=CARTESIAN_POINT('Origin',(0.,0.,7.5));
#396550=CARTESIAN_POINT('Origin',(-2.6548449317704,0.262176299060745,7.5));
#396551=CARTESIAN_POINT('',(-2.6548449317704,0.262176299060745,7.59394543036555));
#396552=CARTESIAN_POINT('',(-2.6548449317704,0.262176299060745,8.85049129520029));
#396553=CARTESIAN_POINT('',(-2.6548449317704,0.262176299060745,7.5));
#396554=CARTESIAN_POINT('',(-2.71406752923974,0.30222445439797,8.78727029226991));
#396555=CARTESIAN_POINT('Ctrl Pts',(-2.6548449317704,0.262176299060745,
8.85049129520029));
#396556=CARTESIAN_POINT('Ctrl Pts',(-2.67461449285379,0.275545088797232,
8.82945686509571));
#396557=CARTESIAN_POINT('Ctrl Pts',(-2.69435466409413,0.288894004211245,
8.80838212259896));
#396558=CARTESIAN_POINT('Ctrl Pts',(-2.71406752923974,0.30222445439797,
8.78727029226991));
#396559=CARTESIAN_POINT('',(-2.72568349213022,0.310079528408699,8.75721825406948));
#396560=CARTESIAN_POINT('Origin',(-2.69072714323187,0.286440718598347,8.75937679713131));
#396561=CARTESIAN_POINT('',(-2.72568349213022,0.310079528408699,7.51860402984325));
#396562=CARTESIAN_POINT('',(-2.72568349213022,0.310079528408699,7.5));
#396563=CARTESIAN_POINT('Ctrl Pts',(-2.72568349213022,0.3100795284087,7.51860402984325));
#396564=CARTESIAN_POINT('Ctrl Pts',(-2.71656095990371,0.303910589468364,
7.52834476460825));
#396565=CARTESIAN_POINT('Ctrl Pts',(-2.70743250546091,0.297737645741883,
7.53807742314407));
#396566=CARTESIAN_POINT('Ctrl Pts',(-2.69829792995554,0.291560562763236,
7.54780169004674));
#396567=CARTESIAN_POINT('Ctrl Pts',(-2.6838292560367,0.28177639716791,7.5632044032688));
#396568=CARTESIAN_POINT('Ctrl Pts',(-2.6693452067639,0.271981834281868,
7.57858609112103));
#396569=CARTESIAN_POINT('Ctrl Pts',(-2.6548449317704,0.262176299060745,
7.59394543036555));
#396570=CARTESIAN_POINT('Origin',(-2.90905453099297,0.142494670373524,7.5));
#396571=CARTESIAN_POINT('',(-2.73469396819878,0.216676518124532,8.75721825406948));
#396572=CARTESIAN_POINT('',(-2.72179064828012,0.222166246411417,8.78727029226991));
#396573=CARTESIAN_POINT('Origin',(-2.68903720962739,0.236101224370437,8.7565864062101));
#396574=CARTESIAN_POINT('',(-2.65600461497701,0.250154969482898,8.85049129520029));
#396575=CARTESIAN_POINT('Ctrl Pts',(-2.72179064828012,0.222166246411417,
8.78727029226991));
#396576=CARTESIAN_POINT('Ctrl Pts',(-2.69989307440825,0.231482587589998,
8.80838212259895));
#396577=CARTESIAN_POINT('Ctrl Pts',(-2.67796516820153,0.240811833685889,
8.82945686509571));
#396578=CARTESIAN_POINT('Ctrl Pts',(-2.65600461497701,0.250154969482898,
8.85049129520029));
#396579=CARTESIAN_POINT('',(-2.65600461497701,0.250154969482898,7.59394543036555));
#396580=CARTESIAN_POINT('',(-2.65600461497701,0.250154969482898,7.5));
#396581=CARTESIAN_POINT('',(-2.73469396819878,0.216676518124532,7.51860402984325));
#396582=CARTESIAN_POINT('Ctrl Pts',(-2.65600461497701,0.250154969482899,
7.59394543036555));
#396583=CARTESIAN_POINT('Ctrl Pts',(-2.67211190534232,0.243302109280958,
7.57858609112103));
#396584=CARTESIAN_POINT('Ctrl Pts',(-2.68820117174618,0.236456917388554,
7.56320440326857));
#396585=CARTESIAN_POINT('Ctrl Pts',(-2.70427335879892,0.229618991920397,
7.54780169004651));
#396586=CARTESIAN_POINT('Ctrl Pts',(-2.71442028774302,0.225301972486589,
7.53807742314383));
#396587=CARTESIAN_POINT('Ctrl Pts',(-2.72456041724852,0.220987845879634,
7.52834476460825));
#396588=CARTESIAN_POINT('Ctrl Pts',(-2.73469396819878,0.216676518124533,
7.51860402984325));
#396589=CARTESIAN_POINT('',(-2.73469396819878,0.216676518124532,7.5));
#396590=CARTESIAN_POINT('Origin',(-2.65869612245475,0.256481217383297,7.5));
#396591=CARTESIAN_POINT('Ctrl Pts',(-2.65600461497701,0.250154969482898,
8.85049129520029));
#396592=CARTESIAN_POINT('Ctrl Pts',(-2.65582641123953,0.250230786412545,
8.85097269580138));
#396593=CARTESIAN_POINT('Ctrl Pts',(-2.65565374887267,0.250313386797565,
8.85143669361005));
#396594=CARTESIAN_POINT('Ctrl Pts',(-2.65547905463228,0.250407362801248,
8.8519052845931));
#396595=CARTESIAN_POINT('Ctrl Pts',(-2.6551373637768,0.250591173904709,
8.85282181883899));
#396596=CARTESIAN_POINT('Ctrl Pts',(-2.65479678269175,0.25081394947612,
8.85372622499635));
#396597=CARTESIAN_POINT('Ctrl Pts',(-2.65446040730407,0.251092088735977,
8.85462257735071));
#396598=CARTESIAN_POINT('Ctrl Pts',(-2.65418116040415,0.251322990070938,
8.85536669723986));
#396599=CARTESIAN_POINT('Ctrl Pts',(-2.65390472814385,0.251592074862224,
8.85610498449051));
#396600=CARTESIAN_POINT('Ctrl Pts',(-2.65363844027942,0.251914482863972,
8.8568133821837));
#396601=CARTESIAN_POINT('Ctrl Pts',(-2.65339678362424,0.252207068631909,
8.85745625420284));
#396602=CARTESIAN_POINT('Ctrl Pts',(-2.65315998869644,0.252546858276553,
8.85808743050665));
#396603=CARTESIAN_POINT('Ctrl Pts',(-2.65294216072111,0.252958729273139,
8.85866804508409));
#396604=CARTESIAN_POINT('Ctrl Pts',(-2.65284165961522,0.253148757622697,
8.85893592806395));
#396605=CARTESIAN_POINT('Ctrl Pts',(-2.65274533984821,0.253354324991418,
8.85919241173848));
#396606=CARTESIAN_POINT('Ctrl Pts',(-2.65265570415938,0.253579014432822,
8.85943017985534));
#396607=CARTESIAN_POINT('Ctrl Pts',(-2.65253466944446,0.253882411693908,
8.8597512372));
#396608=CARTESIAN_POINT('Ctrl Pts',(-2.65242333611262,0.254228633815619,
8.86004599534705));
#396609=CARTESIAN_POINT('Ctrl Pts',(-2.65233295686034,0.254616709420195,
8.86026130871721));
#396610=CARTESIAN_POINT('Ctrl Pts',(-2.65229986646803,0.254758794840041,
8.86034014101235));
#396611=CARTESIAN_POINT('Ctrl Pts',(-2.65226907590949,0.254908622195534,
8.86040910639692));
#396612=CARTESIAN_POINT('Ctrl Pts',(-2.65224175354912,0.255062177237551,
8.86046313645506));
#396613=CARTESIAN_POINT('Ctrl Pts',(-2.65219911723458,0.255301798594607,
8.86054744990829));
#396614=CARTESIAN_POINT('Ctrl Pts',(-2.65216390737134,0.255557064068595,
8.86059655985668));
#396615=CARTESIAN_POINT('Ctrl Pts',(-2.65213809186542,0.255811562677672,
8.86059725258816));
#396616=CARTESIAN_POINT('Ctrl Pts',(-2.65211221671537,0.256066649280209,
8.86059794692011));
#396617=CARTESIAN_POINT('Ctrl Pts',(-2.65209813563059,0.256324062526848,
8.86056369958366));
#396618=CARTESIAN_POINT('Ctrl Pts',(-2.65209285911932,0.256569557431487,
8.86048590497774));
#396619=CARTESIAN_POINT('Ctrl Pts',(-2.65209148210697,0.256633624292334,
8.86046560290182));
#396620=CARTESIAN_POINT('Ctrl Pts',(-2.65209077737803,0.256697714868739,
8.86044257503091));
#396621=CARTESIAN_POINT('Ctrl Pts',(-2.65209073388499,0.256759848347903,
8.86041778462583));
#396622=CARTESIAN_POINT('Ctrl Pts',(-2.65209044123086,0.257177929561459,
8.86025097596201));
#396623=CARTESIAN_POINT('Ctrl Pts',(-2.65212037943941,0.257563502039578,
8.8599848982295));
#396624=CARTESIAN_POINT('Ctrl Pts',(-2.65217122762928,0.257905967816434,
8.85968173251461));
#396625=CARTESIAN_POINT('Ctrl Pts',(-2.65219812340846,0.258087112591441,
8.85952137522076));
#396626=CARTESIAN_POINT('Ctrl Pts',(-2.65223119893676,0.258259716699464,
8.85934740853961));
#396627=CARTESIAN_POINT('Ctrl Pts',(-2.65226846100321,0.258421638611247,
8.8591675900182));
#396628=CARTESIAN_POINT('Ctrl Pts',(-2.65241808756843,0.2590718392524,8.85844552518694));
#396629=CARTESIAN_POINT('Ctrl Pts',(-2.65264072726469,0.259587222332733,
8.85759444184122));
#396630=CARTESIAN_POINT('Ctrl Pts',(-2.65285999980908,0.259991132974821,
8.85683498915136));
#396631=CARTESIAN_POINT('Ctrl Pts',(-2.65288294609688,0.260033401147807,
8.85675551444996));
#396632=CARTESIAN_POINT('Ctrl Pts',(-2.65290587085534,0.260074435800327,
8.8566769979365));
#396633=CARTESIAN_POINT('Ctrl Pts',(-2.65292869619824,0.260114254771412,
8.85659965593547));
#396634=CARTESIAN_POINT('Ctrl Pts',(-2.65323679384139,0.260651733275033,
8.85555568965886));
#396635=CARTESIAN_POINT('Ctrl Pts',(-2.6536105172958,0.261123788020533,
8.85434650606346));
#396636=CARTESIAN_POINT('Ctrl Pts',(-2.65404684146776,0.261536610171395,
8.85297329937117));
#396637=CARTESIAN_POINT('Ctrl Pts',(-2.65429224722887,0.261768797477633,
8.85220095427747));
#396638=CARTESIAN_POINT('Ctrl Pts',(-2.65455777277542,0.261982113251123,
8.85137579139184));
#396639=CARTESIAN_POINT('Ctrl Pts',(-2.6548449317704,0.262176299060745,
8.85049129520029));
#396640=CARTESIAN_POINT('Origin',(-2.65869612245475,0.256481217383297,7.59394543036555));
#396641=CARTESIAN_POINT('Ctrl Pts',(-2.65548722941064,0.250375091606262,
7.59443877723642));
#396642=CARTESIAN_POINT('Ctrl Pts',(-2.65015865589203,0.252642137681094,
7.58783886950016));
#396643=CARTESIAN_POINT('Ctrl Pts',(-2.65158455852055,0.261011485518926,
7.58559994247159));
#396644=CARTESIAN_POINT('Ctrl Pts',(-2.68457575591505,0.237999353596066,
7.56670252222135));
#396645=CARTESIAN_POINT('Ctrl Pts',(-2.67925488369801,0.24026312314568,
7.5600487499903));
#396646=CARTESIAN_POINT('Ctrl Pts',(-2.68066817321352,0.248685650676173,
7.55786368756704));
#396647=CARTESIAN_POINT('Ctrl Pts',(-2.71360996250253,0.225646726040107,
7.53888913333558));
#396648=CARTESIAN_POINT('Ctrl Pts',(-2.70825746808134,0.227923949283006,
7.53222002137277));
#396649=CARTESIAN_POINT('Ctrl Pts',(-2.70969805244026,0.236381322481881,
7.53005029815326));
#396650=CARTESIAN_POINT('Ctrl Pts',(-2.74258853535555,0.213317767903159,
7.51101258149734));
#396651=CARTESIAN_POINT('Ctrl Pts',(-2.73717115897627,0.215622595229579,
7.5043616886572));
#396652=CARTESIAN_POINT('Ctrl Pts',(-2.73867279415589,0.224099184952573,
7.50217374673251));
#396653=CARTESIAN_POINT('',(-2.73712666431696,0.224754574642189,7.50366116523517));
#396654=CARTESIAN_POINT('Ctrl Pts',(-2.73469396819878,0.216676518124532,
7.51860402984325));
#396655=CARTESIAN_POINT('Ctrl Pts',(-2.73510033067525,0.216503630867928,
7.51734760759493));
#396656=CARTESIAN_POINT('Ctrl Pts',(-2.73549082980322,0.216402150372104,
7.51608817408572));
#396657=CARTESIAN_POINT('Ctrl Pts',(-2.73586792612086,0.21638523440084,
7.51481005913118));
#396658=CARTESIAN_POINT('Ctrl Pts',(-2.73620950897638,0.216369911509849,
7.51365231206383));
#396659=CARTESIAN_POINT('Ctrl Pts',(-2.73654056487762,0.216423703726808,
7.51247773061042));
#396660=CARTESIAN_POINT('Ctrl Pts',(-2.73684944320768,0.216582127288799,
7.51129758471022));
#396661=CARTESIAN_POINT('Ctrl Pts',(-2.7372333436967,0.216779029683701,
7.50983079813402));
#396662=CARTESIAN_POINT('Ctrl Pts',(-2.73756478892187,0.217142868017685,
7.50839324291155));
#396663=CARTESIAN_POINT('Ctrl Pts',(-2.7377852545119,0.217731815209157,
7.50715379678855));
#396664=CARTESIAN_POINT('Ctrl Pts',(-2.73788710326193,0.218003891841511,
7.50658120839351));
#396665=CARTESIAN_POINT('Ctrl Pts',(-2.73797084707659,0.218366019889142,
7.50598221009429));
#396666=CARTESIAN_POINT('Ctrl Pts',(-2.73801233135005,0.218814706195371,
7.50545747549611));
#396667=CARTESIAN_POINT('Ctrl Pts',(-2.73803446864242,0.219054139096515,
7.50517746087247));
#396668=CARTESIAN_POINT('Ctrl Pts',(-2.73804501371076,0.21932079816468,
7.50491486231392));
#396669=CARTESIAN_POINT('Ctrl Pts',(-2.73804202059031,0.219607687728848,
7.50468370960993));
#396670=CARTESIAN_POINT('Ctrl Pts',(-2.73803754493112,0.220036678121463,
7.50433806340447));
#396671=CARTESIAN_POINT('Ctrl Pts',(-2.73800210745578,0.220523761247884,
7.50405484070984));
#396672=CARTESIAN_POINT('Ctrl Pts',(-2.73793738030584,0.221036080981669,
7.50385766036131));
#396673=CARTESIAN_POINT('Ctrl Pts',(-2.73793045874324,0.221090865613945,
7.50383657498791));
#396674=CARTESIAN_POINT('Ctrl Pts',(-2.73792321962444,0.221145916405826,
7.50381643264937));
#396675=CARTESIAN_POINT('Ctrl Pts',(-2.7379156778676,0.221201177089492,
7.50379723213559));
#396676=CARTESIAN_POINT('Ctrl Pts',(-2.73786533417364,0.221570060229997,
7.50366906242519));
#396677=CARTESIAN_POINT('Ctrl Pts',(-2.73779969739273,0.22195622297901,
7.50358235568538));
#396678=CARTESIAN_POINT('Ctrl Pts',(-2.73772748437109,0.222326915563695,
7.5035341175365));
#396679=CARTESIAN_POINT('Ctrl Pts',(-2.73761920911807,0.22288272714013,
7.50346178989176));
#396680=CARTESIAN_POINT('Ctrl Pts',(-2.73747909711921,0.223476050177319,
7.50346967198527));
#396681=CARTESIAN_POINT('Ctrl Pts',(-2.73732362825383,0.224054277262595,
7.50354272648692));
#396682=CARTESIAN_POINT('Ctrl Pts',(-2.73725968069148,0.224292114031364,
7.50357277531559));
#396683=CARTESIAN_POINT('Ctrl Pts',(-2.73719335688109,0.22452711760629,
7.50361331098761));
#396684=CARTESIAN_POINT('Ctrl Pts',(-2.73712666431837,0.224754574642305,
7.50366116523659));
#396685=CARTESIAN_POINT('',(-2.66161051802577,0.256762365619155,7.57603338622103));
#396686=CARTESIAN_POINT('Origin',(-2.67040634802763,0.257613755182305,7.58486873427626));
#396687=CARTESIAN_POINT('Ctrl Pts',(-2.73712666436743,0.224754574614973,
7.50366116529969));
#396688=CARTESIAN_POINT('Ctrl Pts',(-2.71199601738034,0.235407197804172,
7.52783573079709));
#396689=CARTESIAN_POINT('Ctrl Pts',(-2.68682516411221,0.246075974212539,
7.55196141284068));
#396690=CARTESIAN_POINT('Ctrl Pts',(-2.66161051899361,0.256762364824846,
7.57603338728831));
#396691=CARTESIAN_POINT('Ctrl Pts',(-2.65701976820119,0.249914138729897,
7.59639677331372));
#396692=CARTESIAN_POINT('Ctrl Pts',(-2.63844797215671,0.254527902676073,
7.59974925422226));
#396693=CARTESIAN_POINT('Ctrl Pts',(-2.65579532783688,0.262606743989909,
7.59639677331371));
#396694=CARTESIAN_POINT('Ctrl Pts',(-2.65313223933917,0.250233862721232,
7.58707626057423));
#396695=CARTESIAN_POINT('Ctrl Pts',(-2.64870482551445,0.25551736898378,
7.58811717123965));
#396696=CARTESIAN_POINT('Ctrl Pts',(-2.65204060628403,0.26154978129223,
7.58707626057423));
#396697=CARTESIAN_POINT('Ctrl Pts',(-2.65771595193357,0.254223250031748,
7.5801537675693));
#396698=CARTESIAN_POINT('Ctrl Pts',(-2.65558427051316,0.256181020769049,
7.58208760766041));
#396699=CARTESIAN_POINT('Ctrl Pts',(-2.6573023971617,0.258510177860652,
7.5801537675693));
#396700=CARTESIAN_POINT('Ctrl Pts',(-2.66161051720204,0.256762365539488,
7.57603338509286));
#396701=CARTESIAN_POINT('Ctrl Pts',(-2.66161051720204,0.256762365539488,
7.57603338509286));
#396702=CARTESIAN_POINT('Ctrl Pts',(-2.66161051720204,0.256762365539488,
7.57603338509286));
#396703=CARTESIAN_POINT('Origin',(-2.67040689596895,0.257608075198315,7.58486873427623));
#396704=CARTESIAN_POINT('Ctrl Pts',(-2.73281288470864,0.314900644564376,
7.51098857897448));
#396705=CARTESIAN_POINT('Ctrl Pts',(-2.72793597470703,0.311602726917125,
7.50433767179956));
#396706=CARTESIAN_POINT('Ctrl Pts',(-2.73103031844476,0.303569478015516,
7.50214974420965));
#396707=CARTESIAN_POINT('Ctrl Pts',(-2.70671798449284,0.297254464524858,
7.53887321589169));
#396708=CARTESIAN_POINT('Ctrl Pts',(-2.701899508528,0.293996061783762,7.53220407452062));
#396709=CARTESIAN_POINT('Ctrl Pts',(-2.70493022693791,0.285970000119303,
7.53003438070912));
#396710=CARTESIAN_POINT('Ctrl Pts',(-2.68057297244259,0.279574397310247,
7.56669465659233));
#396711=CARTESIAN_POINT('Ctrl Pts',(-2.67578297277486,0.276335251123581,
7.56004085833301));
#396712=CARTESIAN_POINT('Ctrl Pts',(-2.67878022809323,0.26833818224285,
7.55785582193788));
#396713=CARTESIAN_POINT('Ctrl Pts',(-2.65437903099217,0.261861242519229,
7.59443891967696));
#396714=CARTESIAN_POINT('Ctrl Pts',(-2.64958208642131,0.258617399973863,
7.58783901202978));
#396715=CARTESIAN_POINT('Ctrl Pts',(-2.65258156709372,0.250674963717643,
7.58560008491213));
#396716=CARTESIAN_POINT('',(-2.72961551748768,0.3026154689171,7.50366116523517));
#396717=CARTESIAN_POINT('Ctrl Pts',(-2.72961551748805,0.302615468917141,
7.50366116523554));
#396718=CARTESIAN_POINT('Ctrl Pts',(-2.72968561742244,0.303369937946302,
7.50350835821027));
#396719=CARTESIAN_POINT('Ctrl Pts',(-2.72972551041329,0.30406575872813,
7.50345484955999));
#396720=CARTESIAN_POINT('Ctrl Pts',(-2.72973698202872,0.304723584208345,
7.50349758195598));
#396721=CARTESIAN_POINT('Ctrl Pts',(-2.72974286781819,0.305061097465305,
7.50351950684424));
#396722=CARTESIAN_POINT('Ctrl Pts',(-2.72974198137209,0.305421873052835,
7.50357029184312));
#396723=CARTESIAN_POINT('Ctrl Pts',(-2.72973156373016,0.305769741308966,
7.50365515313923));
#396724=CARTESIAN_POINT('Ctrl Pts',(-2.72971553717836,0.306304903552658,
7.50378570417639));
#396725=CARTESIAN_POINT('Ctrl Pts',(-2.72967682976936,0.306825237690739,
7.50400001621911));
#396726=CARTESIAN_POINT('Ctrl Pts',(-2.72961612354001,0.307290970309348,
7.50428903009634));
#396727=CARTESIAN_POINT('Ctrl Pts',(-2.7296093856156,0.307342663046885,
7.50432110841318));
#396728=CARTESIAN_POINT('Ctrl Pts',(-2.72960239051941,0.307393710105065,
7.50435406373354));
#396729=CARTESIAN_POINT('Ctrl Pts',(-2.72959514912735,0.307444077147395,
7.50438785222352));
#396730=CARTESIAN_POINT('Ctrl Pts',(-2.72955093694813,0.30775159215028,
7.50459414719561));
#396731=CARTESIAN_POINT('Ctrl Pts',(-2.72949632922009,0.308038580830333,
7.50483629897752));
#396732=CARTESIAN_POINT('Ctrl Pts',(-2.72943471078469,0.308294294734331,
7.5050991045531));
#396733=CARTESIAN_POINT('Ctrl Pts',(-2.72929877432721,0.308858425290581,
7.50567888004914));
#396734=CARTESIAN_POINT('Ctrl Pts',(-2.72912386673409,0.309292697140621,
7.50637912803144));
#396735=CARTESIAN_POINT('Ctrl Pts',(-2.72893465063686,0.309615742862416,
7.50710440483569));
#396736=CARTESIAN_POINT('Ctrl Pts',(-2.72888825109336,0.309694960086756,
7.50728225710685));
#396737=CARTESIAN_POINT('Ctrl Pts',(-2.72884019340232,0.309769139713248,
7.50746498566954));
#396738=CARTESIAN_POINT('Ctrl Pts',(-2.72879194901788,0.309836776660465,
7.50764697238949));
#396739=CARTESIAN_POINT('Ctrl Pts',(-2.72853260048435,0.310200374274514,
7.50862528291181));
#396740=CARTESIAN_POINT('Ctrl Pts',(-2.72824768340916,0.310410308860692,
7.50965856837421));
#396741=CARTESIAN_POINT('Ctrl Pts',(-2.72796073636963,0.310528558892836,
7.51067959873201));
#396742=CARTESIAN_POINT('Ctrl Pts',(-2.72780282905185,0.310593632034678,
7.51124147302578));
#396743=CARTESIAN_POINT('Ctrl Pts',(-2.72764410294566,0.310630554447926,
7.51180065547252));
#396744=CARTESIAN_POINT('Ctrl Pts',(-2.72748753823894,0.310647107520359,
7.512351757165));
#396745=CARTESIAN_POINT('Ctrl Pts',(-2.72694654480926,0.310704304979572,
7.51425603304535));
#396746=CARTESIAN_POINT('Ctrl Pts',(-2.72636621705693,0.310519085845738,
7.51626900505179));
#396747=CARTESIAN_POINT('Ctrl Pts',(-2.72577891497116,0.310142396153974,
7.51827788969242));
#396748=CARTESIAN_POINT('Ctrl Pts',(-2.72574712907243,0.31012200899601,
7.51838661432544));
#396749=CARTESIAN_POINT('Ctrl Pts',(-2.72571532001016,0.310101051407261,
7.51849533314856));
#396750=CARTESIAN_POINT('Ctrl Pts',(-2.72568349213022,0.310079528408703,
7.51860402984325));
#396751=CARTESIAN_POINT('Ctrl Pts',(-2.66161051882509,0.256762366584182,
7.57603338728985));
#396752=CARTESIAN_POINT('Ctrl Pts',(-2.68431738886144,0.272071688132332,
7.55196141284922));
#396753=CARTESIAN_POINT('Ctrl Pts',(-2.7069846417267,0.287355349116307,
7.52783573083105));
#396754=CARTESIAN_POINT('Ctrl Pts',(-2.7296155175335,0.302615468954552,
7.50366116530176));
#396755=CARTESIAN_POINT('Origin',(-9.19709468541367E-16,8.87232663177171E-17,
7.49482233047033));
#396756=CARTESIAN_POINT('Origin',(-2.7283174780614,0.224031223057615,7.49482233047033));
#396757=CARTESIAN_POINT('Origin',(0.,0.,7.50366116523517));
#396758=CARTESIAN_POINT('Origin',(-2.72083050515592,0.301641529324075,7.49482233047033));
#396759=CARTESIAN_POINT('Ctrl Pts',(-2.73469299488662,0.216676932172375,
7.51860402984325));
#396760=CARTESIAN_POINT('Ctrl Pts',(-2.74169487207938,0.213698677346542,
7.51860402984325));
#396761=CARTESIAN_POINT('Ctrl Pts',(-2.74226515987506,0.206111117932591,
7.51860402984325));
#396762=CARTESIAN_POINT('Ctrl Pts',(-2.7372928391742,0.215571084661534,
7.51041458714367));
#396763=CARTESIAN_POINT('Ctrl Pts',(-2.74182996991853,0.211901096872849,
7.51004642900444));
#396764=CARTESIAN_POINT('Ctrl Pts',(-2.74226531715366,0.206109025373795,
7.50729136483012));
#396765=CARTESIAN_POINT('Ctrl Pts',(-2.73922057885099,0.217622317690195,
7.50215815450136));
#396766=CARTESIAN_POINT('Ctrl Pts',(-2.74155503724043,0.215561160609954,
7.49877163671529));
#396767=CARTESIAN_POINT('Ctrl Pts',(-2.74183741099952,0.212122528810162,
7.49481588533168));
#396768=CARTESIAN_POINT('Ctrl Pts',(-2.73712611564552,0.224754529589428,
7.50366171572174));
#396769=CARTESIAN_POINT('Ctrl Pts',(-2.74077554873745,0.225054196679268,
7.50000045605858));
#396770=CARTESIAN_POINT('Ctrl Pts',(-2.74077554873746,0.225054196679144,
7.49482233047317));
#396771=CARTESIAN_POINT('Origin',(-2.72980031823926,0.205174249214716,7.51860402984325));
#396772=CARTESIAN_POINT('Origin',(-2.72980031823926,0.205174249214716,9.));
#396773=CARTESIAN_POINT('Origin',(-2.72980031823926,0.205174249214716,8.75721825406948));
#396774=CARTESIAN_POINT('Ctrl Pts',(-2.71932677685935,0.223214469743997,
8.78942910404912));
#396775=CARTESIAN_POINT('Ctrl Pts',(-2.7244623390508,0.221051501949632,
8.79672699501691));
#396776=CARTESIAN_POINT('Ctrl Pts',(-2.72256725120911,0.212328994967445,
8.79893251111267));
#396777=CARTESIAN_POINT('Ctrl Pts',(-2.72944356314156,0.218910279453015,
8.78111911759583));
#396778=CARTESIAN_POINT('Ctrl Pts',(-2.73552894228411,0.216339195864926,
8.78644465894814));
#396779=CARTESIAN_POINT('Ctrl Pts',(-2.73554682940729,0.2082327051429,8.78817647674132));
#396780=CARTESIAN_POINT('Ctrl Pts',(-2.73574858564827,0.216227805369778,
8.76780923932029));
#396781=CARTESIAN_POINT('Ctrl Pts',(-2.74293013554405,0.21318805573127,
8.76988516158375));
#396782=CARTESIAN_POINT('Ctrl Pts',(-2.74365028845523,0.205663578328771,
8.77093053738833));
#396783=CARTESIAN_POINT('Ctrl Pts',(-2.73451919254909,0.216750851102169,
8.75371302330492));
#396784=CARTESIAN_POINT('Ctrl Pts',(-2.74152478183233,0.213786408462771,
8.75300828287558));
#396785=CARTESIAN_POINT('Ctrl Pts',(-2.74206964654565,0.206164226243848,
8.75267964240738));
#396786=CARTESIAN_POINT('Origin',(-2.71689699832061,0.210663977501601,8.78727029226991));
#396787=CARTESIAN_POINT('Ctrl Pts',(-2.65600461497701,0.250154969482898,
8.85049129520029));
#396788=CARTESIAN_POINT('Ctrl Pts',(-2.66137812144103,0.247868806648742,
8.85711686593484));
#396789=CARTESIAN_POINT('Ctrl Pts',(-2.65991420288366,0.239445167021401,
8.85933012996512));
#396790=CARTESIAN_POINT('Ctrl Pts',(-2.67796519767341,0.240811821147055,
8.82945683644724));
#396791=CARTESIAN_POINT('Ctrl Pts',(-2.68338330748995,0.238506681779115,
8.83607469902389));
#396792=CARTESIAN_POINT('Ctrl Pts',(-2.68187814229224,0.230064731754094,
8.8382956714852));
#396793=CARTESIAN_POINT('Ctrl Pts',(-2.6998930463504,0.231482599527234,
8.80838214965001));
#396794=CARTESIAN_POINT('Ctrl Pts',(-2.70533253855799,0.22916836300311,
8.81501364461993));
#396795=CARTESIAN_POINT('Ctrl Pts',(-2.70380902611905,0.220699140934728,
8.81722098428721));
#396796=CARTESIAN_POINT('Ctrl Pts',(-2.72179064828012,0.222166246411417,
8.78727029226991));
#396797=CARTESIAN_POINT('Ctrl Pts',(-2.7272310440052,0.219851625485012,
8.79393457792714));
#396798=CARTESIAN_POINT('Ctrl Pts',(-2.7257093818291,0.211347276044871,
8.79610912703474));
#396799=CARTESIAN_POINT('Origin',(-2.6511109650175,0.238652700573082,8.85049129520029));
#396800=CARTESIAN_POINT('Ctrl Pts',(-2.6548449317704,0.262176299060745,
8.85049129520029));
#396801=CARTESIAN_POINT('Ctrl Pts',(-2.65968232649294,0.265447495251963,
8.85711686593484));
#396802=CARTESIAN_POINT('Ctrl Pts',(-2.65663515242803,0.273435955199415,
8.85933012996512));
#396803=CARTESIAN_POINT('Ctrl Pts',(-2.65056535848791,0.259282319010592,
8.86332496987233));
#396804=CARTESIAN_POINT('Ctrl Pts',(-2.65040345612426,0.263900292808847,
8.86648636486737));
#396805=CARTESIAN_POINT('Ctrl Pts',(-2.64467246891994,0.265325735742342,
8.87206031107457));
#396806=CARTESIAN_POINT('Ctrl Pts',(-2.65121844737383,0.252191248505865,
8.86341338519875));
#396807=CARTESIAN_POINT('Ctrl Pts',(-2.65191509820944,0.247609966125634,
8.86654584966058));
#396808=CARTESIAN_POINT('Ctrl Pts',(-2.64651844701235,0.24516041338191,
8.87215952290714));
#396809=CARTESIAN_POINT('Ctrl Pts',(-2.65600461497701,0.250154969482898,
8.85049129520029));
#396810=CARTESIAN_POINT('Ctrl Pts',(-2.66137812144103,0.247868806648741,
8.85711686593484));
#396811=CARTESIAN_POINT('Ctrl Pts',(-2.65991420288366,0.239445167021401,
8.85933012996512));
#396812=CARTESIAN_POINT('Origin',(-2.64784276688978,0.272530993019743,8.85049129520029));
#396813=CARTESIAN_POINT('Ctrl Pts',(-2.71406752923974,0.30222445439797,
8.78727029226991));
#396814=CARTESIAN_POINT('Ctrl Pts',(-2.7189651397191,0.305536370349644,
8.79393457792714));
#396815=CARTESIAN_POINT('Ctrl Pts',(-2.71584585849932,0.313593013561936,
8.79610912703474));
#396816=CARTESIAN_POINT('Ctrl Pts',(-2.69435463883559,0.288893987130641,
8.80838214965001));
#396817=CARTESIAN_POINT('Ctrl Pts',(-2.69925143594083,0.292205353053551,
8.81501364461986));
#396818=CARTESIAN_POINT('Ctrl Pts',(-2.6961370534789,0.300227162978756,
8.81722098428721));
#396819=CARTESIAN_POINT('Ctrl Pts',(-2.67461451938528,0.275545106738646,
8.82945683644724));
#396820=CARTESIAN_POINT('Ctrl Pts',(-2.67949206740876,0.278843455836047,
8.83607469902389));
#396821=CARTESIAN_POINT('Ctrl Pts',(-2.6764009071358,0.286842003870814,
8.83829567148519));
#396822=CARTESIAN_POINT('Ctrl Pts',(-2.6548449317704,0.262176299060745,
8.85049129520029));
#396823=CARTESIAN_POINT('Ctrl Pts',(-2.65968232649294,0.265447495251963,
8.85711686593484));
#396824=CARTESIAN_POINT('Ctrl Pts',(-2.65663515242803,0.273435955199415,
8.85933012996512));
#396825=CARTESIAN_POINT('Origin',(-2.70706536435912,0.312579148356967,8.78727029226991));
#396826=CARTESIAN_POINT('Ctrl Pts',(-2.72553009885001,0.309975821388915,
8.75374538247848));
#396827=CARTESIAN_POINT('Ctrl Pts',(-2.73183224290654,0.314221685102973,
8.75304829418602));
#396828=CARTESIAN_POINT('Ctrl Pts',(-2.73091660408602,0.321800091845777,
8.75272238421917));
#396829=CARTESIAN_POINT('Ctrl Pts',(-2.7266235412515,0.310715240504627,
8.76769408445017));
#396830=CARTESIAN_POINT('Ctrl Pts',(-2.73308388962344,0.315068521323175,
8.76974318093968));
#396831=CARTESIAN_POINT('Ctrl Pts',(-2.73235642164598,0.322584447588244,
8.77077869880429));
#396832=CARTESIAN_POINT('Ctrl Pts',(-2.72101917840275,0.306925399324504,
8.78108014887992));
#396833=CARTESIAN_POINT('Ctrl Pts',(-2.72649621408304,0.310611497187727,
8.78639403366327));
#396834=CARTESIAN_POINT('Ctrl Pts',(-2.72498584455341,0.318563909376041,
8.78812224174742));
#396835=CARTESIAN_POINT('Ctrl Pts',(-2.7118348648497,0.300714686275392,
8.78944554828685));
#396836=CARTESIAN_POINT('Ctrl Pts',(-2.71645383287792,0.303816548936953,
8.79673892988685));
#396837=CARTESIAN_POINT('Ctrl Pts',(-2.71293245935051,0.312008220487802,
8.79894799272499));
#396838=CARTESIAN_POINT('Origin',(-2.7186813272496,0.320434222367697,8.75721825406948));
#396839=CARTESIAN_POINT('Origin',(-2.7186813272496,0.320434222367697,9.));
#396840=CARTESIAN_POINT('Origin',(-2.7186813272496,0.320434222367697,7.51860402984325));
#396841=CARTESIAN_POINT('Ctrl Pts',(-2.72961473561416,0.30261538223571,
7.50366195182966));
#396842=CARTESIAN_POINT('Ctrl Pts',(-2.7332543887411,0.303018887905602,
7.50000065167735));
#396843=CARTESIAN_POINT('Ctrl Pts',(-2.73325438874108,0.303018887905718,
7.49482233047108));
#396844=CARTESIAN_POINT('Ctrl Pts',(-2.73030692093629,0.310023126770085,
7.50215800491338));
#396845=CARTESIAN_POINT('Ctrl Pts',(-2.73220389660087,0.312494195466482,
7.49877273257266));
#396846=CARTESIAN_POINT('Ctrl Pts',(-2.7318235351777,0.315925300468913,
7.49481816995647));
#396847=CARTESIAN_POINT('Ctrl Pts',(-2.72801852916872,0.311658143424489,
7.51043025814042));
#396848=CARTESIAN_POINT('Ctrl Pts',(-2.73177540382666,0.316127891716211,
7.51006209594515));
#396849=CARTESIAN_POINT('Ctrl Pts',(-2.73109510087304,0.321899906793596,
7.507312818217));
#396850=CARTESIAN_POINT('Ctrl Pts',(-2.72568224006612,0.310078681834469,
7.51860402984326));
#396851=CARTESIAN_POINT('Ctrl Pts',(-2.73198608987389,0.31434042971436,
7.51860402984327));
#396852=CARTESIAN_POINT('Ctrl Pts',(-2.73109539723704,0.321897392332852,
7.51860402984327));
#396853=CARTESIAN_POINT('Origin',(0.,0.,7.5));
#396854=CARTESIAN_POINT('Origin',(-2.66618796128141,0.0915411309427941,
7.5));
#396855=CARTESIAN_POINT('',(-2.66618796128141,0.0915411309427941,7.59394543036555));
#396856=CARTESIAN_POINT('',(-2.66618796128141,0.0915411309427941,8.85049129520029));
#396857=CARTESIAN_POINT('',(-2.66618796128141,0.0915411309427941,7.5));
#396858=CARTESIAN_POINT('',(-2.72785477369492,0.127712598202037,8.78727029226991));
#396859=CARTESIAN_POINT('Ctrl Pts',(-2.66618796128141,0.0915411309427944,
8.85049129520029));
#396860=CARTESIAN_POINT('Ctrl Pts',(-2.68677344498056,0.103615812939434,
8.82945686509571));
#396861=CARTESIAN_POINT('Ctrl Pts',(-2.70732832586904,0.115672544461242,
8.80838212259897));
#396862=CARTESIAN_POINT('Ctrl Pts',(-2.72785477369492,0.127712598202037,
8.78727029226991));
#396863=CARTESIAN_POINT('',(-2.73995014666367,0.134807295823077,8.75721825406948));
#396864=CARTESIAN_POINT('Origin',(-2.70355107558758,0.113456715445809,8.75937679713089));
#396865=CARTESIAN_POINT('',(-2.73995014666367,0.134807295823077,7.51860402984325));
#396866=CARTESIAN_POINT('',(-2.73995014666367,0.134807295823077,7.5));
#396867=CARTESIAN_POINT('Ctrl Pts',(-2.73995014666367,0.134807295823077,
7.51860402984325));
#396868=CARTESIAN_POINT('Ctrl Pts',(-2.73045111238304,0.129235514275945,
7.52834476460825));
#396869=CARTESIAN_POINT('Ctrl Pts',(-2.72094591146644,0.123660115608629,
7.53807742314407));
#396870=CARTESIAN_POINT('Ctrl Pts',(-2.71143433686084,0.118080978371512,
7.54780169004674));
#396871=CARTESIAN_POINT('Ctrl Pts',(-2.69636851674231,0.109243926514559,
7.5632044032688));
#396872=CARTESIAN_POINT('Ctrl Pts',(-2.68128668670342,0.100397483831551,
7.57858609112103));
#396873=CARTESIAN_POINT('Ctrl Pts',(-2.66618796128141,0.0915411309427943,
7.59394543036555));
#396874=CARTESIAN_POINT('Origin',(-2.91220723134083,-0.0441818639458735,
7.5));
#396875=CARTESIAN_POINT('',(-2.742957758327,0.0410188888571364,8.75721825406948));
#396876=CARTESIAN_POINT('',(-2.73043267776197,0.0473240564541541,8.78727029226991));
#396877=CARTESIAN_POINT('Origin',(-2.69863935166689,0.0633289235250963,
8.75658640621089));
#396878=CARTESIAN_POINT('',(-2.66657505256398,0.0794701993176923,8.85049129520029));
#396879=CARTESIAN_POINT('Ctrl Pts',(-2.73043267776197,0.0473240564541541,
8.78727029226991));
#396880=CARTESIAN_POINT('Ctrl Pts',(-2.70917699483285,0.0580242385856248,
8.80838212259895));
#396881=CARTESIAN_POINT('Ctrl Pts',(-2.68789186871081,0.0687392425192337,
8.82945686509571));
#396882=CARTESIAN_POINT('Ctrl Pts',(-2.66657505256398,0.0794701993176922,
8.85049129520029));
#396883=CARTESIAN_POINT('',(-2.66657505256398,0.0794701993176923,7.59394543036555));
#396884=CARTESIAN_POINT('',(-2.66657505256398,0.0794701993176923,7.5));
#396885=CARTESIAN_POINT('',(-2.742957758327,0.0410188888571365,7.51860402984325));
#396886=CARTESIAN_POINT('Ctrl Pts',(-2.66657505256398,0.0794701993176932,
7.59394543036555));
#396887=CARTESIAN_POINT('Ctrl Pts',(-2.68221018451309,0.071599421415006,
7.57858609112103));
#396888=CARTESIAN_POINT('Ctrl Pts',(-2.6978278208432,0.0637374508656658,
7.56320440326857));
#396889=CARTESIAN_POINT('Ctrl Pts',(-2.71342887847494,0.0558838260887081,
7.54780169004651));
#396890=CARTESIAN_POINT('Ctrl Pts',(-2.72327836708049,0.0509255604647482,
7.53807742314383));
#396891=CARTESIAN_POINT('Ctrl Pts',(-2.73312125556166,0.0459706173655463,
7.52834476460825));
#396892=CARTESIAN_POINT('Ctrl Pts',(-2.742957758327,0.0410188888571374,
7.51860402984325));
#396893=CARTESIAN_POINT('',(-2.742957758327,0.0410188888571364,7.5));
#396894=CARTESIAN_POINT('Origin',(-2.66966635414557,0.0856110037871136,
7.5));
#396895=CARTESIAN_POINT('Ctrl Pts',(-2.66657505256398,0.0794701993176923,
8.85049129520029));
#396896=CARTESIAN_POINT('Ctrl Pts',(-2.66640207257255,0.0795572780259876,
8.85097269580138));
#396897=CARTESIAN_POINT('Ctrl Pts',(-2.66623505718387,0.0796507712154861,
8.85143669361005));
#396898=CARTESIAN_POINT('Ctrl Pts',(-2.66606674293477,0.0797557468338007,
8.8519052845931));
#396899=CARTESIAN_POINT('Ctrl Pts',(-2.66573753093763,0.0799610724859122,
8.85282181883899));
#396900=CARTESIAN_POINT('Ctrl Pts',(-2.66541192289281,0.0802052114460603,
8.85372622499636));
#396901=CARTESIAN_POINT('Ctrl Pts',(-2.66509405906801,0.0805043308840623,
8.85462257735071));
#396902=CARTESIAN_POINT('Ctrl Pts',(-2.66483017981012,0.0807526492177738,
8.85536669723986));
#396903=CARTESIAN_POINT('Ctrl Pts',(-2.66457155583132,0.0810388922212234,
8.85610498449051));
#396904=CARTESIAN_POINT('Ctrl Pts',(-2.66432647183546,0.0813776989232064,
8.85681338218371));
#396905=CARTESIAN_POINT('Ctrl Pts',(-2.66410405772431,0.0816851665373628,
8.85745625420284));
#396906=CARTESIAN_POINT('Ctrl Pts',(-2.66388951971436,0.0820394295508556,
8.85808743050666));
#396907=CARTESIAN_POINT('Ctrl Pts',(-2.66369852795532,0.0824644106006063,
8.8586680450841));
#396908=CARTESIAN_POINT('Ctrl Pts',(-2.6636104084979,0.0826604876445001,
8.85893592806395));
#396909=CARTESIAN_POINT('Ctrl Pts',(-2.66352745737671,0.0828718038816741,
8.85919241173848));
#396910=CARTESIAN_POINT('Ctrl Pts',(-2.66345240175596,0.0831017746528214,
8.85943017985534));
#396911=CARTESIAN_POINT('Ctrl Pts',(-2.6633510544491,0.0834123032725063,
8.8597512372));
#396912=CARTESIAN_POINT('Ctrl Pts',(-2.66326213239103,0.0837649471947974,
8.86004599534706));
#396913=CARTESIAN_POINT('Ctrl Pts',(-2.66319680292198,0.0841580160749979,
8.86026130871721));
#396914=CARTESIAN_POINT('Ctrl Pts',(-2.66317288396152,0.0843019296738245,
8.86034014101235));
#396915=CARTESIAN_POINT('Ctrl Pts',(-2.66315175613712,0.0844534219508058,
8.86040910639692));
#396916=CARTESIAN_POINT('Ctrl Pts',(-2.66313432821879,0.08460841204716,
8.86046313645506));
#396917=CARTESIAN_POINT('Ctrl Pts',(-2.66310713209819,0.0848502727944896,
8.86054744990829));
#396918=CARTESIAN_POINT('Ctrl Pts',(-2.66308834949246,0.085107269701868,
8.86059655985668));
#396919=CARTESIAN_POINT('Ctrl Pts',(-2.66307889280913,0.0853628994214006,
8.86059725258815));
#396920=CARTESIAN_POINT('Ctrl Pts',(-2.66306941427709,0.0856191197477102,
8.86059794692011));
#396921=CARTESIAN_POINT('Ctrl Pts',(-2.66307185464676,0.0858769062894261,
8.86056369958366));
#396922=CARTESIAN_POINT('Ctrl Pts',(-2.66308231788918,0.0861222348656925,
8.86048590497774));
#396923=CARTESIAN_POINT('Ctrl Pts',(-2.66308504848393,0.0861862583197862,
8.86046560290182));
#396924=CARTESIAN_POINT('Ctrl Pts',(-2.66308845150025,0.0862502623673663,
8.86044257503091));
#396925=CARTESIAN_POINT('Ctrl Pts',(-2.66309238900226,0.0863122709732421,
8.86041778462583));
#396926=CARTESIAN_POINT('Ctrl Pts',(-2.66311888350473,0.0867295119445202,
8.860250975962));
#396927=CARTESIAN_POINT('Ctrl Pts',(-2.66317346391551,0.0871123740750228,
8.8599848982295));
#396928=CARTESIAN_POINT('Ctrl Pts',(-2.66324614948998,0.0874508783645,8.85968173251461));
#396929=CARTESIAN_POINT('Ctrl Pts',(-2.66328459599449,0.08762992773965,
8.85952137522076));
#396930=CARTESIAN_POINT('Ctrl Pts',(-2.66332866234873,0.0878000580576475,
8.85934740853961));
#396931=CARTESIAN_POINT('Ctrl Pts',(-2.66337622222878,0.0879592598947022,
8.8591675900182));
#396932=CARTESIAN_POINT('Ctrl Pts',(-2.66356719986828,0.0885985380219589,
8.85844552518694));
#396933=CARTESIAN_POINT('Ctrl Pts',(-2.66382240283475,0.0890985976181652,
8.85759444184121));
#396934=CARTESIAN_POINT('Ctrl Pts',(-2.66406710350387,0.0894876295423664,
8.85683498915134));
#396935=CARTESIAN_POINT('Ctrl Pts',(-2.6640927107772,0.0895283406971491,
8.85675551444995));
#396936=CARTESIAN_POINT('Ctrl Pts',(-2.6641182175335,0.0895678222452543,
8.8566769979365));
#396937=CARTESIAN_POINT('Ctrl Pts',(-2.66414354718951,0.0896060969792497,
8.85659965593547));
#396938=CARTESIAN_POINT('Ctrl Pts',(-2.66448544817898,0.090122731291868,
8.85555568965886));
#396939=CARTESIAN_POINT('Ctrl Pts',(-2.66488864842986,0.0905698716063301,
8.85434650606346));
#396940=CARTESIAN_POINT('Ctrl Pts',(-2.66535052573303,0.0909538901841275,
8.85297329937118));
#396941=CARTESIAN_POINT('Ctrl Pts',(-2.66561030357346,0.0911698772355441,
8.85220095427748));
#396942=CARTESIAN_POINT('Ctrl Pts',(-2.66588895075784,0.0913657424487217,
8.85137579139184));
#396943=CARTESIAN_POINT('Ctrl Pts',(-2.66618796128141,0.0915411309427942,
8.85049129520029));
#396944=CARTESIAN_POINT('Origin',(-2.66966635414557,0.0856110037871136,
7.59394543036555));
#396945=CARTESIAN_POINT('Ctrl Pts',(-2.66607283329461,0.0797230181835987,
7.59443877723642));
#396946=CARTESIAN_POINT('Ctrl Pts',(-2.6609004580425,0.0823268092466506,
7.58783886950016));
#396947=CARTESIAN_POINT('Ctrl Pts',(-2.6628596569582,0.0905876034666598,
7.58559994247159));
#396948=CARTESIAN_POINT('Ctrl Pts',(-2.69430867804486,0.0655089991623795,
7.56670252222136));
#396949=CARTESIAN_POINT('Ctrl Pts',(-2.68914377834347,0.0681090270081165,
7.5600487499903));
#396950=CARTESIAN_POINT('Ctrl Pts',(-2.69109379729577,0.0764236997823088,
7.55786368756704));
#396951=CARTESIAN_POINT('Ctrl Pts',(-2.72249179517612,0.0513215234015378,
7.53888913333557));
#396952=CARTESIAN_POINT('Ctrl Pts',(-2.71729620022289,0.0539370033400496,
7.53222002137277));
#396953=CARTESIAN_POINT('Ctrl Pts',(-2.71927569050806,0.0622847014018697,
7.53005029815327));
#396954=CARTESIAN_POINT('Ctrl Pts',(-2.75062090938332,0.0371612328939311,
7.51101258149734));
#396955=CARTESIAN_POINT('Ctrl Pts',(-2.74536233437864,0.0398084172017556,
7.5043616886572));
#396956=CARTESIAN_POINT('Ctrl Pts',(-2.74740398125597,0.0481713807657634,
7.50217374673251));
#396957=CARTESIAN_POINT('',(-2.7459030190682,0.0489244847658708,7.50366116523517));
#396958=CARTESIAN_POINT('Ctrl Pts',(-2.742957758327,0.0410188888571359,
7.51860402984325));
#396959=CARTESIAN_POINT('Ctrl Pts',(-2.74335220896362,0.0408203210826832,
7.51734760759493));
#396960=CARTESIAN_POINT('Ctrl Pts',(-2.74373540389156,0.040694029724391,
7.51608817408572));
#396961=CARTESIAN_POINT('Ctrl Pts',(-2.74411064161436,0.0406529878647785,
7.51481005913119));
#396962=CARTESIAN_POINT('Ctrl Pts',(-2.74445054091028,0.0406158111676145,
7.51365231206383));
#396963=CARTESIAN_POINT('Ctrl Pts',(-2.74478436310084,0.0406482820382755,
7.51247773061043));
#396964=CARTESIAN_POINT('Ctrl Pts',(-2.74510275703971,0.0407865901995139,
7.51129758471022));
#396965=CARTESIAN_POINT('Ctrl Pts',(-2.74549848434376,0.040958491448545,
7.50983079813402));
#396966=CARTESIAN_POINT('Ctrl Pts',(-2.74585255978126,0.0413003464691624,
7.50839324291155));
#396967=CARTESIAN_POINT('Ctrl Pts',(-2.74611030637721,0.0418739583266141,
7.50715379678855));
#396968=CARTESIAN_POINT('Ctrl Pts',(-2.74622937787774,0.0421389504765283,
7.50658120839351));
#396969=CARTESIAN_POINT('Ctrl Pts',(-2.74633615125543,0.0424949690086202,
7.50598221009429));
#396970=CARTESIAN_POINT('Ctrl Pts',(-2.74640629772534,0.0429400755341853,
7.50545747549611));
#396971=CARTESIAN_POINT('Ctrl Pts',(-2.74644373005291,0.0431775981535625,
7.50517746087247));
#396972=CARTESIAN_POINT('Ctrl Pts',(-2.74647133836043,0.0434430337172244,
7.50491486231392));
#396973=CARTESIAN_POINT('Ctrl Pts',(-2.74648673246716,0.0437295256058998,
7.50468370960992));
#396974=CARTESIAN_POINT('Ctrl Pts',(-2.74650975151252,0.0441579213482125,
7.50433806340446));
#396975=CARTESIAN_POINT('Ctrl Pts',(-2.74650559437033,0.0446462741969512,
7.50405484070984));
#396976=CARTESIAN_POINT('Ctrl Pts',(-2.74647382464731,0.0451616883976327,
7.50385766036131));
#396977=CARTESIAN_POINT('Ctrl Pts',(-2.74647042736924,0.0452168039350443,
7.50383657498791));
#396978=CARTESIAN_POINT('Ctrl Pts',(-2.74646673024033,0.0452722054311037,
7.50381643264937));
#396979=CARTESIAN_POINT('Ctrl Pts',(-2.746462744543,0.0453278357777885,
7.50379723213559));
#396980=CARTESIAN_POINT('Ctrl Pts',(-2.74643613870952,0.0456991865398658,
7.50366906242519));
#396981=CARTESIAN_POINT('Ctrl Pts',(-2.74639537831869,0.0460887612390877,
7.50358235568538));
#396982=CARTESIAN_POINT('Ctrl Pts',(-2.74634706402189,0.0464633189002832,
7.5035341175365));
#396983=CARTESIAN_POINT('Ctrl Pts',(-2.74627462220196,0.0470249257215047,
7.50346178989176));
#396984=CARTESIAN_POINT('Ctrl Pts',(-2.74617281241575,0.0476260067194705,
7.50346967198527));
#396985=CARTESIAN_POINT('Ctrl Pts',(-2.74605471011437,0.0482130066995933,
7.50354272648692));
#396986=CARTESIAN_POINT('Ctrl Pts',(-2.74600613219324,0.0484544519415974,
7.50357277531559));
#396987=CARTESIAN_POINT('Ctrl Pts',(-2.74595500138298,0.0486932220575937,
7.50361331098761));
#396988=CARTESIAN_POINT('Ctrl Pts',(-2.74590301906962,0.048924484765896,
7.50366116523658));
#396989=CARTESIAN_POINT('',(-2.67259277500764,0.0857048484084221,7.57603338622103));
#396990=CARTESIAN_POINT('Origin',(-2.68142508174932,0.0859909379370601,
7.58486873427631));
#396991=CARTESIAN_POINT('Ctrl Pts',(-2.74590301911683,0.0489244847354774,
7.50366116529969));
#396992=CARTESIAN_POINT('Ctrl Pts',(-2.72150652165033,0.0611653470485632,
7.52783573079709));
#396993=CARTESIAN_POINT('Ctrl Pts',(-2.69707093545121,0.0734249054175621,
7.55196141284069));
#396994=CARTESIAN_POINT('Ctrl Pts',(-2.6725927759226,0.0857048475537328,
7.57603338728831));
#396995=CARTESIAN_POINT('Ctrl Pts',(-2.66757268996772,0.0791648222868977,
7.59639677331371));
#396996=CARTESIAN_POINT('Ctrl Pts',(-2.65015302674541,0.0846990113849867,
7.59959882295467));
#396997=CARTESIAN_POINT('Ctrl Pts',(-2.66699621741726,0.0918415417907545,
7.59642833564546));
#396998=CARTESIAN_POINT('Ctrl Pts',(-2.66371363323712,0.0797329642003343,
7.58707626057421));
#396999=CARTESIAN_POINT('Ctrl Pts',(-2.65970333131362,0.0851946278222303,
7.58809943920599));
#397000=CARTESIAN_POINT('Ctrl Pts',(-2.66325601572751,0.0909472649782365,
7.58710240504252));
#397001=CARTESIAN_POINT('Ctrl Pts',(-2.66854352902493,0.08342047541259,
7.58015376756929));
#397002=CARTESIAN_POINT('Ctrl Pts',(-2.6665714763732,0.0854796693653381,
7.58205880659761));
#397003=CARTESIAN_POINT('Ctrl Pts',(-2.66835205186191,0.0876606384084056,
7.58020924244127));
#397004=CARTESIAN_POINT('Ctrl Pts',(-2.6725927741805,0.0857048483816951,
7.57603338509286));
#397005=CARTESIAN_POINT('Ctrl Pts',(-2.6725927741805,0.0857048483816951,
7.57603338509286));
#397006=CARTESIAN_POINT('Ctrl Pts',(-2.6725927741805,0.0857048483816951,
7.57603338509286));
#397007=CARTESIAN_POINT('Origin',(-2.68142526464777,0.0859852345166785,
7.58486873427621));
#397008=CARTESIAN_POINT('Ctrl Pts',(-2.74737378111305,0.139161724727721,
7.51098857897448));
#397009=CARTESIAN_POINT('Ctrl Pts',(-2.74229559293695,0.136183047702606,
7.50433767179956));
#397010=CARTESIAN_POINT('Ctrl Pts',(-2.74486888698932,0.127968048688456,
7.50214974420965));
#397011=CARTESIAN_POINT('Ctrl Pts',(-2.72020190103144,0.123223706654827,
7.53887321589166));
#397012=CARTESIAN_POINT('Ctrl Pts',(-2.71518455856185,0.120280719466672,
7.5322040745206));
#397013=CARTESIAN_POINT('Ctrl Pts',(-2.71769481849935,0.112076969411473,
7.53003438070911));
#397014=CARTESIAN_POINT('Ctrl Pts',(-2.69297784091682,0.107255081707971,
7.56669465659235));
#397015=CARTESIAN_POINT('Ctrl Pts',(-2.68799015000839,0.104329487026961,
7.56004085833303));
#397016=CARTESIAN_POINT('Ctrl Pts',(-2.69046887318185,0.0961568141743418,
7.55785582193789));
#397017=CARTESIAN_POINT('Ctrl Pts',(-2.66570283200437,0.0912565720840829,
7.59443891967696));
#397018=CARTESIAN_POINT('Ctrl Pts',(-2.66070790956513,0.088326735655018,
7.58783901202978));
#397019=CARTESIAN_POINT('Ctrl Pts',(-2.6631923538447,0.0802084405994005,
7.58560008491213));
#397020=CARTESIAN_POINT('',(-2.74339586931974,0.127106646312599,7.50366116523517));
#397021=CARTESIAN_POINT('Ctrl Pts',(-2.74339586932012,0.127106646312616,
7.50366116523554));
#397022=CARTESIAN_POINT('Ctrl Pts',(-2.74351416422334,0.127855073886023,
7.50350835821027));
#397023=CARTESIAN_POINT('Ctrl Pts',(-2.74359855664032,0.128546909076729,
7.50345484955999));
#397024=CARTESIAN_POINT('Ctrl Pts',(-2.74365215170931,0.129202647995019,
7.50349758195598));
#397025=CARTESIAN_POINT('Ctrl Pts',(-2.74367964995442,0.129539090690968,
7.50351950684424));
#397026=CARTESIAN_POINT('Ctrl Pts',(-2.74370188030086,0.129899181821158,
7.50357029184312));
#397027=CARTESIAN_POINT('Ctrl Pts',(-2.7437137720588,0.130247002805257,
7.50365515313923));
#397028=CARTESIAN_POINT('Ctrl Pts',(-2.74373206639795,0.130782092325426,
7.50378570417639));
#397029=CARTESIAN_POINT('Ctrl Pts',(-2.74372677644016,0.131303837373427,
7.50400001621911));
#397030=CARTESIAN_POINT('Ctrl Pts',(-2.7436960345296,0.131772502555892,
7.50428903009634));
#397031=CARTESIAN_POINT('Ctrl Pts',(-2.74369262241404,0.131824520785452,
7.50432110841318));
#397032=CARTESIAN_POINT('Ctrl Pts',(-2.74368891228627,0.131875911139325,
7.50435406373354));
#397033=CARTESIAN_POINT('Ctrl Pts',(-2.7436849127999,0.131926638654744,
7.50438785222352));
#397034=CARTESIAN_POINT('Ctrl Pts',(-2.74366049401323,0.132236354519123,
7.50459414719561));
#397035=CARTESIAN_POINT('Ctrl Pts',(-2.74362438591049,0.132526252279303,
7.50483629897752));
#397036=CARTESIAN_POINT('Ctrl Pts',(-2.74357927772285,0.132785388698371,
7.5050991045531));
#397037=CARTESIAN_POINT('Ctrl Pts',(-2.74347976453025,0.133357069666624,
7.50567888004914));
#397038=CARTESIAN_POINT('Ctrl Pts',(-2.7433330401965,0.133801655626539,
7.50637912803145));
#397039=CARTESIAN_POINT('Ctrl Pts',(-2.74316491047449,0.134136160733225,
7.50710440483569));
#397040=CARTESIAN_POINT('Ctrl Pts',(-2.74312368172882,0.134218188026241,
7.50728225710685));
#397041=CARTESIAN_POINT('Ctrl Pts',(-2.74308047548245,0.134295294309571,
7.50746498566954));
#397042=CARTESIAN_POINT('Ctrl Pts',(-2.74303666373536,0.13436588331775,
7.50764697238949));
#397043=CARTESIAN_POINT('Ctrl Pts',(-2.74280114384032,0.134745350399101,
7.50862528291182));
#397044=CARTESIAN_POINT('Ctrl Pts',(-2.74253026271293,0.134973108351841,
7.50965856837422));
#397045=CARTESIAN_POINT('Ctrl Pts',(-2.74225148154245,0.135109500186557,
7.51067959873203));
#397046=CARTESIAN_POINT('Ctrl Pts',(-2.74209806791269,0.135184556785237,
7.51124147302579));
#397047=CARTESIAN_POINT('Ctrl Pts',(-2.74194203355346,0.135231572953966,
7.51180065547253));
#397048=CARTESIAN_POINT('Ctrl Pts',(-2.74178685108471,0.135258123151537,
7.51235175716501));
#397049=CARTESIAN_POINT('Ctrl Pts',(-2.74125063383784,0.135349864660484,
7.51425603304535));
#397050=CARTESIAN_POINT('Ctrl Pts',(-2.74065963140047,0.135202207805979,
7.51626900505179));
#397051=CARTESIAN_POINT('Ctrl Pts',(-2.74004940139841,0.134863920637417,
7.51827788969242));
#397052=CARTESIAN_POINT('Ctrl Pts',(-2.74001637459752,0.134845611896579,
7.51838661432544));
#397053=CARTESIAN_POINT('Ctrl Pts',(-2.73998328813306,0.13482673538106,
7.51849533314856));
#397054=CARTESIAN_POINT('Ctrl Pts',(-2.73995014666366,0.134807295823081,
7.51860402984325));
#397055=CARTESIAN_POINT('Ctrl Pts',(-2.67259277586714,0.0857048493202557,
7.57603338728985));
#397056=CARTESIAN_POINT('Ctrl Pts',(-2.69623386380305,0.0995278820670658,
7.55196141284922));
#397057=CARTESIAN_POINT('Ctrl Pts',(-2.7198337718876,0.113327845252936,
7.52783573083105));
#397058=CARTESIAN_POINT('Ctrl Pts',(-2.74339586936787,0.127106646347039,
7.50366116530176));
#397059=CARTESIAN_POINT('Origin',(-9.23504345990101E-16,2.96149868837368E-17,
7.49482233047033));
#397060=CARTESIAN_POINT('Origin',(-2.73706558693544,0.0487670258859518,
7.49482233047033));
#397061=CARTESIAN_POINT('Origin',(0.,0.,7.50366116523517));
#397062=CARTESIAN_POINT('Origin',(-2.73456650621404,0.126697565455551,7.49482233047033));
#397063=CARTESIAN_POINT('Ctrl Pts',(-2.74295681354276,0.0410193644145955,
7.51860402984325));
#397064=CARTESIAN_POINT('Ctrl Pts',(-2.74975348718602,0.0375986169206993,
7.51860402984324));
#397065=CARTESIAN_POINT('Ctrl Pts',(-2.74983646666349,0.0299901084968098,
7.51860402984325));
#397066=CARTESIAN_POINT('Ctrl Pts',(-2.74548046427814,0.0397492163906409,
7.51041458714366));
#397067=CARTESIAN_POINT('Ctrl Pts',(-2.74977313607579,0.0357960740206069,
7.51004642900442));
#397068=CARTESIAN_POINT('Ctrl Pts',(-2.74983648954825,0.0299880101605301,
7.50729136483009));
#397069=CARTESIAN_POINT('Ctrl Pts',(-2.74753566615836,0.0416727242358977,
7.50215815450138));
#397070=CARTESIAN_POINT('Ctrl Pts',(-2.74973326936515,0.0394662327613908,
7.49877163671531));
#397071=CARTESIAN_POINT('Ctrl Pts',(-2.74979474906121,0.0360165742505611,
7.49481588533172));
#397072=CARTESIAN_POINT('Ctrl Pts',(-2.74590246863753,0.0489244749591755,
7.50366171572174));
#397073=CARTESIAN_POINT('Ctrl Pts',(-2.74956360331414,0.0489897063698358,
7.50000045605858));
#397074=CARTESIAN_POINT('Ctrl Pts',(-2.74956360331414,0.0489897063697111,
7.49482233047317));
#397075=CARTESIAN_POINT('Origin',(-2.73733720999684,0.0298537898218249,
7.51860402984325));
#397076=CARTESIAN_POINT('Origin',(-2.73733720999684,0.0298537898218249,
9.));
#397077=CARTESIAN_POINT('Origin',(-2.73733720999684,0.029853789821825,8.75721825406948));
#397078=CARTESIAN_POINT('Ctrl Pts',(-2.72804102852879,0.0485279868834066,
8.78942910404913));
#397079=CARTESIAN_POINT('Ctrl Pts',(-2.73302745733453,0.0460404265390274,
8.7967269950169));
#397080=CARTESIAN_POINT('Ctrl Pts',(-2.73057741021293,0.0374572595778216,
8.79893251111267));
#397081=CARTESIAN_POINT('Ctrl Pts',(-2.73786125836976,0.0435844552904106,
8.78111911759583));
#397082=CARTESIAN_POINT('Ctrl Pts',(-2.74376940455713,0.0406287626889506,
8.78644465894815));
#397083=CARTESIAN_POINT('Ctrl Pts',(-2.74326787028547,0.0325377815896275,
8.78817647674132));
#397084=CARTESIAN_POINT('Ctrl Pts',(-2.74398145982695,0.0405035284588668,
8.76780923932029));
#397085=CARTESIAN_POINT('Ctrl Pts',(-2.75095349703021,0.0370099008303957,
8.76988516158372));
#397086=CARTESIAN_POINT('Ctrl Pts',(-2.75119007538758,0.0294547429182708,
8.77093053738833));
#397087=CARTESIAN_POINT('Ctrl Pts',(-2.74278810430285,0.0411042670240238,
8.75371302330492));
#397088=CARTESIAN_POINT('Ctrl Pts',(-2.74958936735954,0.0376970655034874,
8.75300828287559));
#397089=CARTESIAN_POINT('Ctrl Pts',(-2.74964475769837,0.0300556342733736,
8.75267964240738));
#397090=CARTESIAN_POINT('Origin',(-2.72481212943181,0.0361589574188426,
8.78727029226991));
#397091=CARTESIAN_POINT('Ctrl Pts',(-2.66657505256398,0.0794701993176923,
8.85049129520029));
#397092=CARTESIAN_POINT('Ctrl Pts',(-2.67179104362696,0.0768444519090519,
8.85711686593484));
#397093=CARTESIAN_POINT('Ctrl Pts',(-2.66979042840331,0.0685319131367625,
8.85933012996512));
#397094=CARTESIAN_POINT('Ctrl Pts',(-2.68789189731877,0.0687392281178933,
8.82945683644722));
#397095=CARTESIAN_POINT('Ctrl Pts',(-2.69315118426123,0.0660916854182248,
8.83607469902389));
#397096=CARTESIAN_POINT('Ctrl Pts',(-2.69110823399166,0.0577635165502321,
8.83829567148519));
#397097=CARTESIAN_POINT('Ctrl Pts',(-2.70917696759746,0.0580242522960096,
8.80838214965002));
#397098=CARTESIAN_POINT('Ctrl Pts',(-2.71445701014171,0.0553662611567229,
8.81501364461988));
#397099=CARTESIAN_POINT('Ctrl Pts',(-2.71239400300152,0.0470120517904829,
8.81722098428721));
#397100=CARTESIAN_POINT('Ctrl Pts',(-2.73043267776197,0.047324056454154,
8.78727029226991));
#397101=CARTESIAN_POINT('Ctrl Pts',(-2.73571359733862,0.0446656238137969,
8.79393457792714));
#397102=CARTESIAN_POINT('Ctrl Pts',(-2.73365018604124,0.0362762407020289,
8.79610912703474));
#397103=CARTESIAN_POINT('Origin',(-2.66095450423382,0.0683051002823809,
8.85049129520029));
#397104=CARTESIAN_POINT('Ctrl Pts',(-2.66618796128141,0.0915411309427942,
8.85049129520029));
#397105=CARTESIAN_POINT('Ctrl Pts',(-2.67122500331725,0.0944956731665959,
8.85711686593485));
#397106=CARTESIAN_POINT('Ctrl Pts',(-2.66869591238441,0.102662953078985,
8.85933012996512));
#397107=CARTESIAN_POINT('Ctrl Pts',(-2.66173176290277,0.0889272900866667,
8.86332496987232));
#397108=CARTESIAN_POINT('Ctrl Pts',(-2.66186606778202,0.0935461488825231,
8.86648636486737));
#397109=CARTESIAN_POINT('Ctrl Pts',(-2.65623818394787,0.095335848701524,
8.87206031107457));
#397110=CARTESIAN_POINT('Ctrl Pts',(-2.6619291835004,0.0818089453982159,
8.86341338519876));
#397111=CARTESIAN_POINT('Ctrl Pts',(-2.66233087922226,0.0771924411816848,
8.8665458496606));
#397112=CARTESIAN_POINT('Ctrl Pts',(-2.65678837264069,0.075093685936153,
8.87215952290714));
#397113=CARTESIAN_POINT('Ctrl Pts',(-2.66657505256398,0.0794701993176923,
8.85049129520029));
#397114=CARTESIAN_POINT('Ctrl Pts',(-2.67179104362696,0.0768444519090517,
8.85711686593484));
#397115=CARTESIAN_POINT('Ctrl Pts',(-2.66979042840331,0.0685319131367627,
8.85933012996512));
#397116=CARTESIAN_POINT('Origin',(-2.65986361061929,0.102323180316759,8.85049129520029));
#397117=CARTESIAN_POINT('Ctrl Pts',(-2.72785477369492,0.127712598202037,
8.78727029226991));
#397118=CARTESIAN_POINT('Ctrl Pts',(-2.73295451669186,0.130703918486395,
8.79393457792714));
#397119=CARTESIAN_POINT('Ctrl Pts',(-2.73035783527281,0.138943861495067,
8.79610912703474));
#397120=CARTESIAN_POINT('Ctrl Pts',(-2.70732829956804,0.115672529034048,
8.80838214965003));
#397121=CARTESIAN_POINT('Ctrl Pts',(-2.71242719562158,0.1186633525328,8.81501364461989));
#397122=CARTESIAN_POINT('Ctrl Pts',(-2.70983317111897,0.126868219958618,
8.81722098428721));
#397123=CARTESIAN_POINT('Ctrl Pts',(-2.68677347260706,0.103615829144114,
8.82945683644724));
#397124=CARTESIAN_POINT('Ctrl Pts',(-2.69185232513724,0.106594895854727,
8.8360746990239));
#397125=CARTESIAN_POINT('Ctrl Pts',(-2.6892799847167,0.114775061333389,
8.8382956714852));
#397126=CARTESIAN_POINT('Ctrl Pts',(-2.66618796128141,0.0915411309427942,
8.85049129520029));
#397127=CARTESIAN_POINT('Ctrl Pts',(-2.67122500331725,0.0944956731665958,
8.85711686593484));
#397128=CARTESIAN_POINT('Ctrl Pts',(-2.66869591238441,0.102662953078985,
8.85933012996512));
#397129=CARTESIAN_POINT('Origin',(-2.72153042303281,0.138494647576002,8.78727029226991));
#397130=CARTESIAN_POINT('Ctrl Pts',(-2.73979042401482,0.134713629821695,
8.75374538247848));
#397131=CARTESIAN_POINT('Ctrl Pts',(-2.74635165306265,0.138546990197332,
8.75304829418602));
#397132=CARTESIAN_POINT('Ctrl Pts',(-2.74592344570741,0.146168491471352,
8.75272238421917));
#397133=CARTESIAN_POINT('Ctrl Pts',(-2.74092899456704,0.135381472626339,
8.76769408445018));
#397134=CARTESIAN_POINT('Ctrl Pts',(-2.74765498512005,0.13931189322122,
8.76974318093969));
#397135=CARTESIAN_POINT('Ctrl Pts',(-2.74741055885273,0.146858986243038,
8.7707786988043));
#397136=CARTESIAN_POINT('Ctrl Pts',(-2.73509333052472,0.131958490841943,
8.78108014887993));
#397137=CARTESIAN_POINT('Ctrl Pts',(-2.74079528214875,0.135286100340894,
8.78639403366325));
#397138=CARTESIAN_POINT('Ctrl Pts',(-2.7397975286336,0.143318943153492,
8.78812224174742));
#397139=CARTESIAN_POINT('Ctrl Pts',(-2.72552996537758,0.126348979358604,
8.78944554828685));
#397140=CARTESIAN_POINT('Ctrl Pts',(-2.73033818026369,0.129148530613003,
8.79673892988686));
#397141=CARTESIAN_POINT('Ctrl Pts',(-2.72734888397413,0.137548986672627,
8.79894799272499));
#397142=CARTESIAN_POINT('Origin',(-2.73362579600155,0.145589345197042,8.75721825406948));
#397143=CARTESIAN_POINT('Origin',(-2.73362579600155,0.145589345197042,9.));
#397144=CARTESIAN_POINT('Origin',(-2.73362579600155,0.145589345197042,7.51860402984325));
#397145=CARTESIAN_POINT('Ctrl Pts',(-2.74339508349897,0.127106609904114,
7.50366195182966));
#397146=CARTESIAN_POINT('Ctrl Pts',(-2.74705311126524,0.127276093151834,
7.50000065167735));
#397147=CARTESIAN_POINT('Ctrl Pts',(-2.74705311126523,0.127276093151951,
7.49482233047108));
#397148=CARTESIAN_POINT('Ctrl Pts',(-2.744560462474,0.134454785967003,7.50215800491337));
#397149=CARTESIAN_POINT('Ctrl Pts',(-2.74661186251359,0.136799237939623,
7.49877273257265));
#397150=CARTESIAN_POINT('Ctrl Pts',(-2.74645211423604,0.140247663208896,
7.49481816995649));
#397151=CARTESIAN_POINT('Ctrl Pts',(-2.74238152832947,0.136233061068291,
7.51043025814043));
#397152=CARTESIAN_POINT('Ctrl Pts',(-2.74641706184182,0.140452921996988,
7.51006209594515));
#397153=CARTESIAN_POINT('Ctrl Pts',(-2.7461079709193,0.146256665010245,
7.50731281821699));
#397154=CARTESIAN_POINT('Ctrl Pts',(-2.73994884293186,0.134806531208245,
7.51860402984326));
#397155=CARTESIAN_POINT('Ctrl Pts',(-2.74651279192828,0.138655633826135,
7.51860402984327));
#397156=CARTESIAN_POINT('Ctrl Pts',(-2.74610810557233,0.146254136727627,
7.51860402984327));
#397157=CARTESIAN_POINT('Origin',(0.,0.,7.5));
#397158=CARTESIAN_POINT('Origin',(-2.66657505256398,-0.0794701993177115,
7.5));
#397159=CARTESIAN_POINT('',(-2.66657505256398,-0.0794701993177115,7.59394543036555));
#397160=CARTESIAN_POINT('',(-2.66657505256398,-0.0794701993177115,8.85049129520029));
#397161=CARTESIAN_POINT('',(-2.66657505256398,-0.0794701993177115,7.5));
#397162=CARTESIAN_POINT('',(-2.73043267776197,-0.0473240564541737,8.78727029226991));
#397163=CARTESIAN_POINT('Ctrl Pts',(-2.66657505256398,-0.0794701993177114,
8.85049129520029));
#397164=CARTESIAN_POINT('Ctrl Pts',(-2.68789186871081,-0.0687392425192531,
8.82945686509571));
#397165=CARTESIAN_POINT('Ctrl Pts',(-2.70917699483285,-0.0580242385856441,
8.80838212259895));
#397166=CARTESIAN_POINT('Ctrl Pts',(-2.73043267776197,-0.0473240564541735,
8.78727029226991));
#397167=CARTESIAN_POINT('',(-2.742957758327,-0.0410188888571562,8.75721825406948));
#397168=CARTESIAN_POINT('Origin',(-2.70526553666451,-0.0599935056863788,
8.75937679713089));
#397169=CARTESIAN_POINT('',(-2.742957758327,-0.0410188888571562,7.51860402984325));
#397170=CARTESIAN_POINT('',(-2.742957758327,-0.0410188888571562,7.5));
#397171=CARTESIAN_POINT('Ctrl Pts',(-2.742957758327,-0.0410188888571564,
7.51860402984325));
#397172=CARTESIAN_POINT('Ctrl Pts',(-2.73312125556167,-0.0459706173655643,
7.52834476460825));
#397173=CARTESIAN_POINT('Ctrl Pts',(-2.72327836708068,-0.0509255604646721,
7.53807742314407));
#397174=CARTESIAN_POINT('Ctrl Pts',(-2.71342887847514,-0.0558838260886309,
7.54780169004674));
#397175=CARTESIAN_POINT('Ctrl Pts',(-2.69782782084339,-0.0637374508655898,
7.5632044032688));
#397176=CARTESIAN_POINT('Ctrl Pts',(-2.68221018451309,-0.0715994214150238,
7.57858609112103));
#397177=CARTESIAN_POINT('Ctrl Pts',(-2.66657505256398,-0.0794701993177118,
7.59394543036555));
#397178=CARTESIAN_POINT('Origin',(-2.90339304750863,-0.230676845509337,
7.5));
#397179=CARTESIAN_POINT('',(-2.73995014666366,-0.134807295823097,8.75721825406948));
#397180=CARTESIAN_POINT('',(-2.72785477369492,-0.127712598202056,8.78727029226991));
#397181=CARTESIAN_POINT('Origin',(-2.6971522057511,-0.109703609449603,8.75658640621057));
#397182=CARTESIAN_POINT('',(-2.66618796128141,-0.0915411309428133,8.85049129520029));
#397183=CARTESIAN_POINT('Ctrl Pts',(-2.72785477369492,-0.127712598202057,
8.78727029226991));
#397184=CARTESIAN_POINT('Ctrl Pts',(-2.70732832586903,-0.115672544461257,
8.80838212259895));
#397185=CARTESIAN_POINT('Ctrl Pts',(-2.68677344498056,-0.103615812939454,
8.82945686509571));
#397186=CARTESIAN_POINT('Ctrl Pts',(-2.66618796128141,-0.0915411309428135,
8.85049129520029));
#397187=CARTESIAN_POINT('',(-2.66618796128141,-0.0915411309428133,7.59394543036555));
#397188=CARTESIAN_POINT('',(-2.66618796128141,-0.0915411309428133,7.5));
#397189=CARTESIAN_POINT('',(-2.73995014666366,-0.134807295823097,7.51860402984325));
#397190=CARTESIAN_POINT('Ctrl Pts',(-2.66618796128141,-0.0915411309428125,
7.59394543036555));
#397191=CARTESIAN_POINT('Ctrl Pts',(-2.68128668670342,-0.100397483831567,
7.57858609112103));
#397192=CARTESIAN_POINT('Ctrl Pts',(-2.69636851674213,-0.109243926514469,
7.56320440326857));
#397193=CARTESIAN_POINT('Ctrl Pts',(-2.71143433686065,-0.118080978371422,
7.54780169004651));
#397194=CARTESIAN_POINT('Ctrl Pts',(-2.72094591146625,-0.12366011560854,
7.53807742314383));
#397195=CARTESIAN_POINT('Ctrl Pts',(-2.73045111238304,-0.129235514275963,
7.52834476460825));
#397196=CARTESIAN_POINT('Ctrl Pts',(-2.73995014666366,-0.134807295823096,
7.51860402984325));
#397197=CARTESIAN_POINT('',(-2.73995014666366,-0.134807295823097,7.5));
#397198=CARTESIAN_POINT('Origin',(-2.66966635414557,-0.0856110037871328,
7.5));
#397199=CARTESIAN_POINT('Ctrl Pts',(-2.66618796128141,-0.0915411309428132,
8.85049129520029));
#397200=CARTESIAN_POINT('Ctrl Pts',(-2.66602091584792,-0.0914431482809603,
8.85097269580138));
#397201=CARTESIAN_POINT('Ctrl Pts',(-2.66586023373949,-0.0913391464705544,
8.85143669361005));
#397202=CARTESIAN_POINT('Ctrl Pts',(-2.66569899112102,-0.0912236026049402,
8.8519052845931));
#397203=CARTESIAN_POINT('Ctrl Pts',(-2.66538361078493,-0.0909976061313247,
8.85282181883899));
#397204=CARTESIAN_POINT('Ctrl Pts',(-2.66507431377364,-0.0907331070017954,
8.85372622499635));
#397205=CARTESIAN_POINT('Ctrl Pts',(-2.66477626768236,-0.0904142365315805,
8.85462257735071));
#397206=CARTESIAN_POINT('Ctrl Pts',(-2.66452884040296,-0.0901495215924163,
8.85536669723986));
#397207=CARTESIAN_POINT('Ctrl Pts',(-2.66428908744707,-0.0898472966107034,
8.85610498449051));
#397208=CARTESIAN_POINT('Ctrl Pts',(-2.66406621442249,-0.0894934834378981,
8.85681338218371));
#397209=CARTESIAN_POINT('Ctrl Pts',(-2.66386395680266,-0.0891723974279031,
8.85745625420285));
#397210=CARTESIAN_POINT('Ctrl Pts',(-2.66367255729327,-0.0888051167882754,
8.85808743050666));
#397211=CARTESIAN_POINT('Ctrl Pts',(-2.66350918657663,-0.0883687720236555,
8.8586680450841));
#397212=CARTESIAN_POINT('Ctrl Pts',(-2.66343381086941,-0.0881674520080548,
8.85893592806396));
#397213=CARTESIAN_POINT('Ctrl Pts',(-2.66336456925801,-0.0879512552461709,
8.85919241173848));
#397214=CARTESIAN_POINT('Ctrl Pts',(-2.66330440212497,-0.0877169481445036,
8.85943017985534));
#397215=CARTESIAN_POINT('Ctrl Pts',(-2.66322315868399,-0.0874005641949268,
8.8597512372));
#397216=CARTESIAN_POINT('Ctrl Pts',(-2.6631570132995,-0.0870429475615733,
8.86004599534705));
#397217=CARTESIAN_POINT('Ctrl Pts',(-2.66311700206647,-0.08664650061009,
8.86026130871721));
#397218=CARTESIAN_POINT('Ctrl Pts',(-2.66310235282603,-0.0865013502041289,
8.86034014101235));
#397219=CARTESIAN_POINT('Ctrl Pts',(-2.66309097455451,-0.0863488155199207,
8.86040910639693));
#397220=CARTESIAN_POINT('Ctrl Pts',(-2.66308351269328,-0.0861930272567808,
8.86046313645507));
#397221=CARTESIAN_POINT('Ctrl Pts',(-2.66307186852132,-0.0859499209768667,
8.8605474499083));
#397222=CARTESIAN_POINT('Ctrl Pts',(-2.66306959035485,-0.0856922486915159,
8.86059655985668));
#397223=CARTESIAN_POINT('Ctrl Pts',(-2.66307653135366,-0.0854365382988774,
8.86059725258816));
#397224=CARTESIAN_POINT('Ctrl Pts',(-2.66308348838895,-0.0851802371130747,
8.86059794692011));
#397225=CARTESIAN_POINT('Ctrl Pts',(-2.66310244018505,-0.0849231365764772,
8.86056369958366));
#397226=CARTESIAN_POINT('Ctrl Pts',(-2.66312860018547,-0.0846789824363259,
8.86048590497774));
#397227=CARTESIAN_POINT('Ctrl Pts',(-2.6631354271667,-0.0846152654750911,
8.86046560290182));
#397228=CARTESIAN_POINT('Ctrl Pts',(-2.66314292394457,-0.0845516109626956,
8.86044257503091));
#397229=CARTESIAN_POINT('Ctrl Pts',(-2.66315082626158,-0.0844899820367707,
8.86041778462583));
#397230=CARTESIAN_POINT('Ctrl Pts',(-2.66320399904907,-0.0840752958404186,
8.86025097596201));
#397231=CARTESIAN_POINT('Ctrl Pts',(-2.66328299737946,-0.0836967173201501,
8.8599848982295));
#397232=CARTESIAN_POINT('Ctrl Pts',(-2.66337722165792,-0.0833635655047856,
8.85968173251461));
#397233=CARTESIAN_POINT('Ctrl Pts',(-2.66342706090281,-0.083187347281781,
8.85952137522076));
#397234=CARTESIAN_POINT('Ctrl Pts',(-2.66348193700491,-0.0830203898557786,
8.85934740853961));
#397235=CARTESIAN_POINT('Ctrl Pts',(-2.66353959926479,-0.0828645622879489,
8.8591675900182));
#397236=CARTESIAN_POINT('Ctrl Pts',(-2.6637711432105,-0.0822388336055553,
8.85844552518695));
#397237=CARTESIAN_POINT('Ctrl Pts',(-2.66405786076342,-0.0817561523456297,
8.85759444184125));
#397238=CARTESIAN_POINT('Ctrl Pts',(-2.66432698402973,-0.0813835977549439,
8.85683498915139));
#397239=CARTESIAN_POINT('Ctrl Pts',(-2.66435514706282,-0.0813446109092215,
8.85675551444999));
#397240=CARTESIAN_POINT('Ctrl Pts',(-2.66438313100423,-0.0813068447036701,
8.85667699793651));
#397241=CARTESIAN_POINT('Ctrl Pts',(-2.66441086088839,-0.081270271485846,
8.85659965593547));
#397242=CARTESIAN_POINT('Ctrl Pts',(-2.66478516027966,-0.0807766043254381,
8.85555568965886));
#397243=CARTESIAN_POINT('Ctrl Pts',(-2.66521618049069,-0.0803562158374777,
8.85434650606346));
#397244=CARTESIAN_POINT('Ctrl Pts',(-2.66570171297216,-0.0800025788474523,
8.85297329937118));
#397245=CARTESIAN_POINT('Ctrl Pts',(-2.66597479540906,-0.079803679587981,
8.85220095427748));
#397246=CARTESIAN_POINT('Ctrl Pts',(-2.6662654192102,-0.0796260697872908,
8.85137579139184));
#397247=CARTESIAN_POINT('Ctrl Pts',(-2.66657505256398,-0.0794701993177116,
8.85049129520029));
#397248=CARTESIAN_POINT('Origin',(-2.66966635414557,-0.0856110037871328,
7.59394543036555));
#397249=CARTESIAN_POINT('Ctrl Pts',(-2.66570297203574,-0.0912566542213146,
7.59443877723642));
#397250=CARTESIAN_POINT('Ctrl Pts',(-2.66070804944951,-0.0883268177060317,
7.58783886950016));
#397251=CARTESIAN_POINT('Ctrl Pts',(-2.66319249388382,-0.0802085224792304,
7.58559994247159));
#397252=CARTESIAN_POINT('Ctrl Pts',(-2.69297010788915,-0.107250545800486,
7.56670252222133));
#397253=CARTESIAN_POINT('Ctrl Pts',(-2.68798240438414,-0.104324943730775,
7.56004874999027));
#397254=CARTESIAN_POINT('Ctrl Pts',(-2.69046113972712,-0.0961522924867714,
7.55786368756704));
#397255=CARTESIAN_POINT('Ctrl Pts',(-2.7201863250907,-0.123214570385138,
7.53888913333561));
#397256=CARTESIAN_POINT('Ctrl Pts',(-2.71516897941958,-0.120271581319056,
7.53222002137279));
#397257=CARTESIAN_POINT('Ctrl Pts',(-2.71767924148075,-0.112067860876243,
7.53005029815327));
#397258=CARTESIAN_POINT('Ctrl Pts',(-2.74735039208809,-0.139148005592317,
7.51101258149734));
#397259=CARTESIAN_POINT('Ctrl Pts',(-2.74227222707067,-0.136169342151228,
7.5043616886572));
#397260=CARTESIAN_POINT('Ctrl Pts',(-2.74484549608077,-0.127954369957341,
7.50217374673251));
#397261=CARTESIAN_POINT('',(-2.74339586931974,-0.127106646312618,7.50366116523517));
#397262=CARTESIAN_POINT('Ctrl Pts',(-2.73995014666366,-0.134807295823097,
7.51860402984325));
#397263=CARTESIAN_POINT('Ctrl Pts',(-2.74033106457815,-0.13503072815782,
7.51734760759494));
#397264=CARTESIAN_POINT('Ctrl Pts',(-2.74070538067591,-0.1351813114203,
7.51608817408573));
#397265=CARTESIAN_POINT('Ctrl Pts',(-2.74107721787159,-0.135246310518456,
7.51481005913121));
#397266=CARTESIAN_POINT('Ctrl Pts',(-2.74141403688878,-0.13530518825477,
7.51365231206384));
#397267=CARTESIAN_POINT('Ctrl Pts',(-2.74174925362168,-0.13529417216018,
7.51247773061043));
#397268=CARTESIAN_POINT('Ctrl Pts',(-2.74207585482037,-0.135176547737596,
7.51129758471022));
#397269=CARTESIAN_POINT('Ctrl Pts',(-2.74248178281107,-0.13503035401354,
7.50983079813402));
#397270=CARTESIAN_POINT('Ctrl Pts',(-2.74285703348899,-0.134711887061897,
7.50839324291155));
#397271=CARTESIAN_POINT('Ctrl Pts',(-2.74315100195479,-0.134155967632627,
7.50715379678855));
#397272=CARTESIAN_POINT('Ctrl Pts',(-2.7432868069155,-0.133899148874738,
7.50658120839351));
#397273=CARTESIAN_POINT('Ctrl Pts',(-2.7434161711015,-0.1335507028147,7.50598221009429));
#397274=CARTESIAN_POINT('Ctrl Pts',(-2.74351469152097,-0.133111005107987,
7.50545747549611));
#397275=CARTESIAN_POINT('Ctrl Pts',(-2.74356726506629,-0.132876368801768,
7.50517746087247));
#397276=CARTESIAN_POINT('Ctrl Pts',(-2.74361182316454,-0.132613247474275,
7.50491486231392));
#397277=CARTESIAN_POINT('Ctrl Pts',(-2.74364554124075,-0.132328330517715,
7.50468370960992));
#397278=CARTESIAN_POINT('Ctrl Pts',(-2.74369596040046,-0.131902289795704,
7.50433806340447));
#397279=CARTESIAN_POINT('Ctrl Pts',(-2.74372310067401,-0.131414673971259,
7.50405484070984));
#397280=CARTESIAN_POINT('Ctrl Pts',(-2.74372441892651,-0.130898283251192,
7.50385766036131));
#397281=CARTESIAN_POINT('Ctrl Pts',(-2.74372455989313,-0.130843063290206,
7.50383657498791));
#397282=CARTESIAN_POINT('Ctrl Pts',(-2.74372441994641,-0.130787538746595,
7.50381643264937));
#397283=CARTESIAN_POINT('Ctrl Pts',(-2.74372400668667,-0.130731767333915,
7.50379723213559));
#397284=CARTESIAN_POINT('Ctrl Pts',(-2.74372124804273,-0.130359474910201,
7.50366906242519));
#397285=CARTESIAN_POINT('Ctrl Pts',(-2.74370553153518,-0.129968089106774,
7.50358235568538));
#397286=CARTESIAN_POINT('Ctrl Pts',(-2.74368131449704,-0.129591205506841,
7.5035341175365));
#397287=CARTESIAN_POINT('Ctrl Pts',(-2.74364500378917,-0.129026111203727,
7.50346178989176));
#397288=CARTESIAN_POINT('Ctrl Pts',(-2.74358191457385,-0.128419742215738,
7.50346967198527));
#397289=CARTESIAN_POINT('Ctrl Pts',(-2.74350166414417,-0.127826381449601,
7.50354272648692));
#397290=CARTESIAN_POINT('Ctrl Pts',(-2.74346865548136,-0.127582319884648,
7.50357277531559));
#397291=CARTESIAN_POINT('Ctrl Pts',(-2.74343292777869,-0.127340764385202,
7.50361331098761));
#397292=CARTESIAN_POINT('Ctrl Pts',(-2.74339586932116,-0.127106646312684,
7.50366116523658));
#397293=CARTESIAN_POINT('',(-2.67259277500765,-0.0857048484080524,7.57603338622103));
#397294=CARTESIAN_POINT('Origin',(-2.68142526464731,-0.0859852345168127,
7.58486873427627));
#397295=CARTESIAN_POINT('Ctrl Pts',(-2.74339586936632,-0.127106646346066,
7.50366116529969));
#397296=CARTESIAN_POINT('Ctrl Pts',(-2.71983377186154,-0.113327845238004,
7.52783573079709));
#397297=CARTESIAN_POINT('Ctrl Pts',(-2.69623386379654,-0.0995278820633557,
7.55196141284068));
#397298=CARTESIAN_POINT('Ctrl Pts',(-2.67259277586597,-0.0857048493196056,
7.57603338728831));
#397299=CARTESIAN_POINT('Ctrl Pts',(-2.66716398335853,-0.0919097993916527,
7.59639677331372));
#397300=CARTESIAN_POINT('Ctrl Pts',(-2.64933465654095,-0.0849590058182218,
7.59974925422226));
#397301=CARTESIAN_POINT('Ctrl Pts',(-2.66757268996767,-0.0791648222869322,
7.59639677331371));
#397302=CARTESIAN_POINT('Ctrl Pts',(-2.66334925645125,-0.0910955741730429,
7.58707626057422));
#397303=CARTESIAN_POINT('Ctrl Pts',(-2.65963383141741,-0.0852892803103875,
7.58811717123965));
#397304=CARTESIAN_POINT('Ctrl Pts',(-2.66371363323709,-0.0797329642003973,
7.58707626057424));
#397305=CARTESIAN_POINT('Ctrl Pts',(-2.66840548835473,-0.0877250918337127,
7.5801537675693));
#397306=CARTESIAN_POINT('Ctrl Pts',(-2.66654166217443,-0.0855108009973929,
7.58208760766041));
#397307=CARTESIAN_POINT('Ctrl Pts',(-2.66854352902492,-0.0834204754125948,
7.5801537675693));
#397308=CARTESIAN_POINT('Ctrl Pts',(-2.6725927741805,-0.0857048483817295,
7.57603338509286));
#397309=CARTESIAN_POINT('Ctrl Pts',(-2.6725927741805,-0.0857048483817295,
7.57603338509286));
#397310=CARTESIAN_POINT('Ctrl Pts',(-2.6725927741805,-0.0857048483817295,
7.57603338509286));
#397311=CARTESIAN_POINT('Origin',(-2.6814250817504,-0.0859909379374167,
7.5848687342762));
#397312=CARTESIAN_POINT('Ctrl Pts',(-2.75064512934104,-0.0371490404859369,
7.51098857897448));
#397313=CARTESIAN_POINT('Ctrl Pts',(-2.74538653035493,-0.0397962368660951,
7.50433767179956));
#397314=CARTESIAN_POINT('Ctrl Pts',(-2.74742820050471,-0.0481592287997251,
7.50214974420965));
#397315=CARTESIAN_POINT('Ctrl Pts',(-2.72250792447726,-0.0513134038572253,
7.53887321589168));
#397316=CARTESIAN_POINT('Ctrl Pts',(-2.71731233283933,-0.0539288821268316,
7.53220407452062));
#397317=CARTESIAN_POINT('Ctrl Pts',(-2.71929181910785,-0.062276609604089,
7.53003438070911));
#397318=CARTESIAN_POINT('Ctrl Pts',(-2.69431668580073,-0.065504968031212,
7.5666946565923));
#397319=CARTESIAN_POINT('Ctrl Pts',(-2.6891517991434,-0.0681049893104966,
7.56004085833295));
#397320=CARTESIAN_POINT('Ctrl Pts',(-2.69110180456681,-0.0764196828691923,
7.55785582193789));
#397321=CARTESIAN_POINT('Ctrl Pts',(-2.6660726882884,-0.0797230911802304,
7.59443891967696));
#397322=CARTESIAN_POINT('Ctrl Pts',(-2.6609003131885,-0.0823268821666591,
7.58783901202978));
#397323=CARTESIAN_POINT('Ctrl Pts',(-2.66285951196075,-0.0905876762059219,
7.58560008491213));
#397324=CARTESIAN_POINT('',(-2.7459030190682,-0.0489244847658906,7.50366116523517));
#397325=CARTESIAN_POINT('Ctrl Pts',(-2.74590301906857,-0.0489244847658972,
7.50366116523554));
#397326=CARTESIAN_POINT('Ctrl Pts',(-2.7460690228415,-0.0481851740976808,
7.50350835821027));
#397327=CARTESIAN_POINT('Ctrl Pts',(-2.74619756789807,-0.0475001673972941,
7.50345484956));
#397328=CARTESIAN_POINT('Ctrl Pts',(-2.74629306618699,-0.0468492096127992,
7.50349758195598));
#397329=CARTESIAN_POINT('Ctrl Pts',(-2.74634206389154,-0.0465152199930655,
7.50351950684424));
#397330=CARTESIAN_POINT('Ctrl Pts',(-2.74638731968128,-0.046157293011909,
7.50357029184312));
#397331=CARTESIAN_POINT('Ctrl Pts',(-2.74642147197328,-0.0458109485708723,
7.50365515313923));
#397332=CARTESIAN_POINT('Ctrl Pts',(-2.74647401202802,-0.0452781305718466,
7.50378570417639));
#397333=CARTESIAN_POINT('Ctrl Pts',(-2.74650216125901,-0.0447571185762471,
7.50400001621911));
#397334=CARTESIAN_POINT('Ctrl Pts',(-2.74650150999234,-0.0442874466756935,
7.50428903009634));
#397335=CARTESIAN_POINT('Ctrl Pts',(-2.74650143770675,-0.0442353167081682,
7.50432110841318));
#397336=CARTESIAN_POINT('Ctrl Pts',(-2.74650102779312,-0.044183794232584,
7.50435406373354));
#397337=CARTESIAN_POINT('Ctrl Pts',(-2.7465002866472,-0.0441329146943119,
7.50438785222352));
#397338=CARTESIAN_POINT('Ctrl Pts',(-2.7464957615951,-0.0438222706573593,
7.50459414719561));
#397339=CARTESIAN_POINT('Ctrl Pts',(-2.7464783014936,-0.0435306550691341,
7.50483629897752));
#397340=CARTESIAN_POINT('Ctrl Pts',(-2.74644988891295,-0.0432691609821266,
7.5050991045531));
#397341=CARTESIAN_POINT('Ctrl Pts',(-2.74638720790626,-0.0426922787615938,
7.50567888004914));
#397342=CARTESIAN_POINT('Ctrl Pts',(-2.74626926975364,-0.0422392055908742,
7.50637912803144));
#397343=CARTESIAN_POINT('Ctrl Pts',(-2.74612291728795,-0.0418946156525315,
7.50710440483569));
#397344=CARTESIAN_POINT('Ctrl Pts',(-2.74608702875786,-0.0418101153585814,
7.50728225710685));
#397345=CARTESIAN_POINT('Ctrl Pts',(-2.7460488514999,-0.0417303992646702,
7.50746498566954));
#397346=CARTESIAN_POINT('Ctrl Pts',(-2.74600965242202,-0.0416571482609055,
7.50764697238949));
#397347=CARTESIAN_POINT('Ctrl Pts',(-2.74579892896725,-0.0412633710238883,
7.50862528291181));
#397348=CARTESIAN_POINT('Ctrl Pts',(-2.74554319689632,-0.041018725610869,
7.50965856837421));
#397349=CARTESIAN_POINT('Ctrl Pts',(-2.74527372716651,-0.0408647524368866,
7.51067959873201));
#397350=CARTESIAN_POINT('Ctrl Pts',(-2.7451254376343,-0.0407800208050308,
7.51124147302578));
#397351=CARTESIAN_POINT('Ctrl Pts',(-2.74497273620066,-0.0407231040803407,
7.51180065547252));
#397352=CARTESIAN_POINT('Ctrl Pts',(-2.74481957364794,-0.0406866658580891,
7.51235175716501));
#397353=CARTESIAN_POINT('Ctrl Pts',(-2.74429033601557,-0.0405607572849474,
7.51425603304535));
#397354=CARTESIAN_POINT('Ctrl Pts',(-2.74369108744894,-0.0406702451064386,
7.5162690050518));
#397355=CARTESIAN_POINT('Ctrl Pts',(-2.74306043709656,-0.0409687396572608,
7.51827788969243));
#397356=CARTESIAN_POINT('Ctrl Pts',(-2.74302630510772,-0.0409848947464281,
7.51838661432545));
#397357=CARTESIAN_POINT('Ctrl Pts',(-2.74299207720045,-0.0410016126210649,
7.51849533314856));
#397358=CARTESIAN_POINT('Ctrl Pts',(-2.742957758327,-0.0410188888571523,
7.51860402984325));
#397359=CARTESIAN_POINT('Ctrl Pts',(-2.67259277592381,-0.0857048475531615,
7.57603338728985));
#397360=CARTESIAN_POINT('Ctrl Pts',(-2.69707093545794,-0.0734249054142831,
7.55196141284922));
#397361=CARTESIAN_POINT('Ctrl Pts',(-2.7215065216773,-0.0611653470353149,
7.52783573083105));
#397362=CARTESIAN_POINT('Ctrl Pts',(-2.74590301911844,-0.0489244847346051,
7.50366116530176));
#397363=CARTESIAN_POINT('Origin',(-9.23504345990101E-16,-2.96149868837434E-17,
7.49482233047033));
#397364=CARTESIAN_POINT('Origin',(-2.73456650621404,-0.126697565455571,
7.49482233047033));
#397365=CARTESIAN_POINT('Origin',(0.,0.,7.50366116523517));
#397366=CARTESIAN_POINT('Origin',(-2.73706558693544,-0.0487670258859716,
7.49482233047033));
#397367=CARTESIAN_POINT('Ctrl Pts',(-2.73994923428965,-0.134806760710188,
7.51860402984325));
#397368=CARTESIAN_POINT('Ctrl Pts',(-2.74651277539354,-0.138655944286946,
7.51860402984325));
#397369=CARTESIAN_POINT('Ctrl Pts',(-2.74610810557233,-0.146254136727642,
7.51860402984325));
#397370=CARTESIAN_POINT('Ctrl Pts',(-2.74238632125063,-0.136235989936575,
7.51041458714365));
#397371=CARTESIAN_POINT('Ctrl Pts',(-2.74641689459241,-0.140456042578019,
7.51004642900442));
#397372=CARTESIAN_POINT('Ctrl Pts',(-2.7461079939692,-0.146256232218901,
7.50729136483009));
#397373=CARTESIAN_POINT('Ctrl Pts',(-2.74456054006895,-0.134448111381053,
7.50215815450138));
#397374=CARTESIAN_POINT('Ctrl Pts',(-2.7466122576701,-0.136790870303067,
7.4987716367153));
#397375=CARTESIAN_POINT('Ctrl Pts',(-2.74645259066989,-0.14023738013816,
7.49481588533172));
#397376=CARTESIAN_POINT('Ctrl Pts',(-2.74339531939168,-0.127106620832951,
7.50366171572174));
#397377=CARTESIAN_POINT('Ctrl Pts',(-2.74705311126526,-0.127276093151329,
7.50000045605858));
#397378=CARTESIAN_POINT('Ctrl Pts',(-2.74705311126525,-0.127276093151453,
7.49482233047317));
#397379=CARTESIAN_POINT('Origin',(-2.73362579600155,-0.145589345197061,
7.51860402984325));
#397380=CARTESIAN_POINT('Origin',(-2.73362579600155,-0.145589345197061,
9.));
#397381=CARTESIAN_POINT('Origin',(-2.73362579600155,-0.145589345197061,
8.75721825406948));
#397382=CARTESIAN_POINT('Ctrl Pts',(-2.72554517444904,-0.126357907884503,
8.78942910404912));
#397383=CARTESIAN_POINT('Ctrl Pts',(-2.73036197956352,-0.129159838859871,
8.79672699501691));
#397384=CARTESIAN_POINT('Ctrl Pts',(-2.72736704093116,-0.137568395725972,
8.79893251111267));
#397385=CARTESIAN_POINT('Ctrl Pts',(-2.73502849441794,-0.131920466747828,
8.78111911759583));
#397386=CARTESIAN_POINT('Ctrl Pts',(-2.74073512981015,-0.135248622787726,
8.78644465894813));
#397387=CARTESIAN_POINT('Ctrl Pts',(-2.73971623505555,-0.143290846687523,
8.78817647674132));
#397388=CARTESIAN_POINT('Ctrl Pts',(-2.74093872560498,-0.135387186138442,
8.76780923932029));
#397389=CARTESIAN_POINT('Ctrl Pts',(-2.74767260051939,-0.139320335691599,
8.76988516158374));
#397390=CARTESIAN_POINT('Ctrl Pts',(-2.74742463217173,-0.146875128348903,
8.77093053738833));
#397391=CARTESIAN_POINT('Ctrl Pts',(-2.73978631140984,-0.134711223304163,
8.75371302330492));
#397392=CARTESIAN_POINT('Ctrl Pts',(-2.7463553003912,-0.13854718278394,
8.75300828287559));
#397393=CARTESIAN_POINT('Ctrl Pts',(-2.74592098874476,-0.14617646274525,
8.75267964240738));
#397394=CARTESIAN_POINT('Origin',(-2.7215304230328,-0.138494647576021,8.78727029226991));
#397395=CARTESIAN_POINT('Ctrl Pts',(-2.66618796128141,-0.0915411309428134,
8.85049129520029));
#397396=CARTESIAN_POINT('Ctrl Pts',(-2.67122500331725,-0.0944956731666149,
8.85711686593484));
#397397=CARTESIAN_POINT('Ctrl Pts',(-2.66869591238441,-0.102662953079004,
8.85933012996512));
#397398=CARTESIAN_POINT('Ctrl Pts',(-2.68677347260704,-0.103615829144124,
8.82945683644723));
#397399=CARTESIAN_POINT('Ctrl Pts',(-2.69185232513724,-0.106594895854732,
8.83607469902389));
#397400=CARTESIAN_POINT('Ctrl Pts',(-2.6892799847167,-0.114775061333413,
8.8382956714852));
#397401=CARTESIAN_POINT('Ctrl Pts',(-2.70732829956804,-0.115672529034066,
8.80838214965002));
#397402=CARTESIAN_POINT('Ctrl Pts',(-2.71242719562158,-0.118663352532825,
8.81501364461988));
#397403=CARTESIAN_POINT('Ctrl Pts',(-2.70983317111897,-0.126868219958614,
8.81722098428721));
#397404=CARTESIAN_POINT('Ctrl Pts',(-2.72785477369492,-0.127712598202057,
8.78727029226991));
#397405=CARTESIAN_POINT('Ctrl Pts',(-2.73295451669185,-0.130703918486415,
8.79393457792714));
#397406=CARTESIAN_POINT('Ctrl Pts',(-2.7303578352728,-0.138943861495087,
8.79610912703474));
#397407=CARTESIAN_POINT('Origin',(-2.65986361061929,-0.102323180316778,
8.85049129520029));
#397408=CARTESIAN_POINT('Ctrl Pts',(-2.66657505256398,-0.0794701993177115,
8.85049129520029));
#397409=CARTESIAN_POINT('Ctrl Pts',(-2.67179104362696,-0.0768444519090711,
8.85711686593485));
#397410=CARTESIAN_POINT('Ctrl Pts',(-2.66979042840331,-0.0685319131367817,
8.85933012996512));
#397411=CARTESIAN_POINT('Ctrl Pts',(-2.66196054056419,-0.0817931601470715,
8.86332496987233));
#397412=CARTESIAN_POINT('Ctrl Pts',(-2.66239050079877,-0.0771923962351356,
8.86648636486738));
#397413=CARTESIAN_POINT('Ctrl Pts',(-2.65688884651665,-0.0750457937910786,
8.87206031107457));
#397414=CARTESIAN_POINT('Ctrl Pts',(-2.66170148162993,-0.0889095282140341,
8.86341338519875));
#397415=CARTESIAN_POINT('Ctrl Pts',(-2.66180657158416,-0.093542284060803,
8.86654584966058));
#397416=CARTESIAN_POINT('Ctrl Pts',(-2.65614098496653,-0.095281617572672,
8.87215952290715));
#397417=CARTESIAN_POINT('Ctrl Pts',(-2.66618796128141,-0.0915411309428132,
8.85049129520029));
#397418=CARTESIAN_POINT('Ctrl Pts',(-2.67122500331725,-0.0944956731666149,
8.85711686593484));
#397419=CARTESIAN_POINT('Ctrl Pts',(-2.66869591238441,-0.102662953079003,
8.85933012996512));
#397420=CARTESIAN_POINT('Origin',(-2.66095450423382,-0.0683051002824,8.85049129520029));
#397421=CARTESIAN_POINT('Ctrl Pts',(-2.73043267776197,-0.0473240564541735,
8.78727029226991));
#397422=CARTESIAN_POINT('Ctrl Pts',(-2.73571359733862,-0.0446656238138165,
8.79393457792714));
#397423=CARTESIAN_POINT('Ctrl Pts',(-2.73365018604124,-0.0362762407020484,
8.79610912703474));
#397424=CARTESIAN_POINT('Ctrl Pts',(-2.70917696759746,-0.0580242522960278,
8.80838214965002));
#397425=CARTESIAN_POINT('Ctrl Pts',(-2.71445701014171,-0.0553662611567412,
8.81501364461988));
#397426=CARTESIAN_POINT('Ctrl Pts',(-2.71239400300153,-0.0470120517905022,
8.81722098428721));
#397427=CARTESIAN_POINT('Ctrl Pts',(-2.68789189731876,-0.0687392281179148,
8.82945683644722));
#397428=CARTESIAN_POINT('Ctrl Pts',(-2.69315118426122,-0.066091685418231,
8.8360746990239));
#397429=CARTESIAN_POINT('Ctrl Pts',(-2.69110823399166,-0.0577635165502493,
8.8382956714852));
#397430=CARTESIAN_POINT('Ctrl Pts',(-2.66657505256398,-0.0794701993177114,
8.85049129520029));
#397431=CARTESIAN_POINT('Ctrl Pts',(-2.67179104362696,-0.076844451909071,
8.85711686593484));
#397432=CARTESIAN_POINT('Ctrl Pts',(-2.66979042840331,-0.0685319131367817,
8.85933012996512));
#397433=CARTESIAN_POINT('Origin',(-2.72481212943181,-0.0361589574188621,
8.78727029226991));
#397434=CARTESIAN_POINT('Ctrl Pts',(-2.74279236264415,-0.0411021289464491,
8.75374538247847));
#397435=CARTESIAN_POINT('Ctrl Pts',(-2.74958571518575,-0.0376970240092693,
8.75304829418601));
#397436=CARTESIAN_POINT('Ctrl Pts',(-2.74964669889166,-0.0300637465875672,
8.75272238421917));
#397437=CARTESIAN_POINT('Ctrl Pts',(-2.74397138271647,-0.0405086067622189,
8.76769408445022));
#397438=CARTESIAN_POINT('Ctrl Pts',(-2.75093537691269,-0.0370171973323106,
8.76974318093971));
#397439=CARTESIAN_POINT('Ctrl Pts',(-2.75117499675545,-0.0294699501778062,
8.7707786988043));
#397440=CARTESIAN_POINT('Ctrl Pts',(-2.73792839747587,-0.0435506633845036,
8.78108014887987));
#397441=CARTESIAN_POINT('Ctrl Pts',(-2.74383183450136,-0.04059521611103,
8.78639403366323));
#397442=CARTESIAN_POINT('Ctrl Pts',(-2.74335079698391,-0.0325149513483094,
8.78812224174741));
#397443=CARTESIAN_POINT('Ctrl Pts',(-2.72802527865339,-0.0485359226161412,
8.78944554828685));
#397444=CARTESIAN_POINT('Ctrl Pts',(-2.73300298241105,-0.0460501867255157,
8.79673892988686));
#397445=CARTESIAN_POINT('Ctrl Pts',(-2.73055804701899,-0.0374754654329442,
8.79894799272499));
#397446=CARTESIAN_POINT('Origin',(-2.73733720999684,-0.0298537898218447,
8.75721825406948));
#397447=CARTESIAN_POINT('Origin',(-2.73733720999684,-0.0298537898218447,
9.));
#397448=CARTESIAN_POINT('Origin',(-2.73733720999684,-0.0298537898218447,
7.51860402984325));
#397449=CARTESIAN_POINT('Ctrl Pts',(-2.74590223252928,-0.0489244707518609,
7.50366195182966));
#397450=CARTESIAN_POINT('Ctrl Pts',(-2.74956360331414,-0.0489897063693297,
7.50000065167735));
#397451=CARTESIAN_POINT('Ctrl Pts',(-2.74956360331415,-0.0489897063692129,
7.49482233047108));
#397452=CARTESIAN_POINT('Ctrl Pts',(-2.74753601636503,-0.0416660583920684,
7.50215800491337));
#397453=CARTESIAN_POINT('Ctrl Pts',(-2.74973341113685,-0.039457856999275,
7.49877273257264));
#397454=CARTESIAN_POINT('Ctrl Pts',(-2.74979493244485,-0.0360062817822748,
7.49481816995647));
#397455=CARTESIAN_POINT('Ctrl Pts',(-2.7454754935513,-0.0397518321577423,
7.51043025814042));
#397456=CARTESIAN_POINT('Ctrl Pts',(-2.74977310304523,-0.0357991989057771,
7.51006209594516));
#397457=CARTESIAN_POINT('Ctrl Pts',(-2.74983649427474,-0.0299875767815907,
7.50731281821701));
#397458=CARTESIAN_POINT('Ctrl Pts',(-2.74295640828481,-0.0410195683706217,
7.51860402984326));
#397459=CARTESIAN_POINT('Ctrl Pts',(-2.7497534837955,-0.0375989278030173,
7.51860402984327));
#397460=CARTESIAN_POINT('Ctrl Pts',(-2.74983646666349,-0.0299901084968249,
7.51860402984327));
#397461=CARTESIAN_POINT('Origin',(0.,0.,7.5));
#397462=CARTESIAN_POINT('Origin',(-2.65600461497701,-0.250154969482917,
7.5));
#397463=CARTESIAN_POINT('',(-2.65600461497701,-0.250154969482917,7.59394543036555));
#397464=CARTESIAN_POINT('',(-2.65600461497701,-0.250154969482917,8.85049129520029));
#397465=CARTESIAN_POINT('',(-2.65600461497701,-0.250154969482917,7.5));
#397466=CARTESIAN_POINT('',(-2.72179064828012,-0.222166246411436,8.78727029226991));
#397467=CARTESIAN_POINT('Ctrl Pts',(-2.65600461497701,-0.250154969482917,
8.85049129520029));
#397468=CARTESIAN_POINT('Ctrl Pts',(-2.67796516820153,-0.240811833685908,
8.82945686509571));
#397469=CARTESIAN_POINT('Ctrl Pts',(-2.69989307440825,-0.231482587590015,
8.80838212259896));
#397470=CARTESIAN_POINT('Ctrl Pts',(-2.72179064828012,-0.222166246411436,
8.78727029226991));
#397471=CARTESIAN_POINT('',(-2.73469396819878,-0.216676518124552,8.75721825406948));
#397472=CARTESIAN_POINT('Origin',(-2.69586348137444,-0.23319720063476,8.75937679713098));
#397473=CARTESIAN_POINT('',(-2.73469396819878,-0.216676518124552,7.51860402984325));
#397474=CARTESIAN_POINT('',(-2.73469396819878,-0.216676518124552,7.5));
#397475=CARTESIAN_POINT('Ctrl Pts',(-2.73469396819878,-0.216676518124552,
7.51860402984325));
#397476=CARTESIAN_POINT('Ctrl Pts',(-2.72456041724852,-0.220987845879652,
7.52834476460825));
#397477=CARTESIAN_POINT('Ctrl Pts',(-2.71442028774322,-0.225301972486524,
7.53807742314407));
#397478=CARTESIAN_POINT('Ctrl Pts',(-2.70427335879911,-0.229618991920331,
7.54780169004675));
#397479=CARTESIAN_POINT('Ctrl Pts',(-2.68820117174638,-0.236456917388489,
7.5632044032688));
#397480=CARTESIAN_POINT('Ctrl Pts',(-2.67211190534232,-0.243302109280976,
7.57858609112102));
#397481=CARTESIAN_POINT('Ctrl Pts',(-2.65600461497701,-0.250154969482917,
7.59394543036555));
#397482=CARTESIAN_POINT('Origin',(-2.88264819886835,-0.416223926434574,
7.5));
#397483=CARTESIAN_POINT('',(-2.72568349213022,-0.310079528408719,8.75721825406948));
#397484=CARTESIAN_POINT('',(-2.71406752923974,-0.302224454397989,8.78727029226991));
#397485=CARTESIAN_POINT('Origin',(-2.68458188288295,-0.282285346760464,
8.75658640620939));
#397486=CARTESIAN_POINT('',(-2.6548449317704,-0.262176299060764,8.85049129520029));
#397487=CARTESIAN_POINT('Ctrl Pts',(-2.71406752923974,-0.302224454397989,
8.78727029226991));
#397488=CARTESIAN_POINT('Ctrl Pts',(-2.69435466409413,-0.288894004211271,
8.80838212259897));
#397489=CARTESIAN_POINT('Ctrl Pts',(-2.67461449285379,-0.275545088797251,
8.82945686509571));
#397490=CARTESIAN_POINT('Ctrl Pts',(-2.6548449317704,-0.262176299060765,
8.85049129520029));
#397491=CARTESIAN_POINT('',(-2.6548449317704,-0.262176299060764,7.59394543036555));
#397492=CARTESIAN_POINT('',(-2.6548449317704,-0.262176299060764,7.5));
#397493=CARTESIAN_POINT('',(-2.72568349213022,-0.310079528408719,7.51860402984325));
#397494=CARTESIAN_POINT('Ctrl Pts',(-2.6548449317704,-0.262176299060764,
7.59394543036555));
#397495=CARTESIAN_POINT('Ctrl Pts',(-2.6693452067639,-0.271981834281885,
7.57858609112103));
#397496=CARTESIAN_POINT('Ctrl Pts',(-2.68382925603652,-0.281776397167808,
7.56320440326857));
#397497=CARTESIAN_POINT('Ctrl Pts',(-2.69829792995536,-0.291560562763133,
7.54780169004651));
#397498=CARTESIAN_POINT('Ctrl Pts',(-2.70743250546073,-0.297737645741781,
7.53807742314383));
#397499=CARTESIAN_POINT('Ctrl Pts',(-2.7165609599037,-0.303910589468382,
7.52834476460825));
#397500=CARTESIAN_POINT('Ctrl Pts',(-2.72568349213022,-0.310079528408719,
7.51860402984325));
#397501=CARTESIAN_POINT('',(-2.72568349213022,-0.310079528408719,7.5));
#397502=CARTESIAN_POINT('Origin',(-2.65869612245475,-0.256481217383316,
7.5));
#397503=CARTESIAN_POINT('Ctrl Pts',(-2.6548449317704,-0.262176299060764,
8.85049129520029));
#397504=CARTESIAN_POINT('Ctrl Pts',(-2.65468450732037,-0.262067815077129,
8.85097269580138));
#397505=CARTESIAN_POINT('Ctrl Pts',(-2.65453081876944,-0.261953732011562,
8.85143669361005));
#397506=CARTESIAN_POINT('Ctrl Pts',(-2.65437731036211,-0.261828094693177,
8.8519052845931));
#397507=CARTESIAN_POINT('Ctrl Pts',(-2.65407705765253,-0.261582356066044,
8.85282181883899));
#397508=CARTESIAN_POINT('Ctrl Pts',(-2.65378534264253,-0.261298583650791,
8.85372622499635));
#397509=CARTESIAN_POINT('Ctrl Pts',(-2.65350833902008,-0.260961272455523,
8.8546225773507));
#397510=CARTESIAN_POINT('Ctrl Pts',(-2.65327838045095,-0.260681248681371,
8.85536669723986));
#397511=CARTESIAN_POINT('Ctrl Pts',(-2.65305848371428,-0.260364283628671,
8.85610498449051));
#397512=CARTESIAN_POINT('Ctrl Pts',(-2.65285873749405,-0.259996917879263,
8.8568133821837));
#397513=CARTESIAN_POINT('Ctrl Pts',(-2.65267746748548,-0.259663532884715,
8.85745625420284));
#397514=CARTESIAN_POINT('Ctrl Pts',(-2.65250999297829,-0.25928474385388,
8.85808743050666));
#397515=CARTESIAN_POINT('Ctrl Pts',(-2.65237491462936,-0.258838828408621,
8.85866804508411));
#397516=CARTESIAN_POINT('Ctrl Pts',(-2.65231259240731,-0.258633092688443,
8.85893592806396));
#397517=CARTESIAN_POINT('Ctrl Pts',(-2.65225734483431,-0.258412903800721,
8.85919241173849));
#397518=CARTESIAN_POINT('Ctrl Pts',(-2.65221231342865,-0.258175223186676,
8.85943017985534));
#397519=CARTESIAN_POINT('Ctrl Pts',(-2.65215150770028,-0.25785428399672,
8.8597512372));
#397520=CARTESIAN_POINT('Ctrl Pts',(-2.65210841079495,-0.257493164175759,
8.86004599534705));
#397521=CARTESIAN_POINT('Ctrl Pts',(-2.65209388221268,-0.257094968238555,
8.86026130871721));
#397522=CARTESIAN_POINT('Ctrl Pts',(-2.65208856288911,-0.256949177479612,
8.86034014101235));
#397523=CARTESIAN_POINT('Ctrl Pts',(-2.65208698092624,-0.256796227185913,
8.86040910639693));
#397524=CARTESIAN_POINT('Ctrl Pts',(-2.65208951578449,-0.256640280923377,
8.86046313645507));
#397525=CARTESIAN_POINT('Ctrl Pts',(-2.65209347140956,-0.256396928086729,
8.8605474499083));
#397526=CARTESIAN_POINT('Ctrl Pts',(-2.65210770704384,-0.256139639254097,
8.86059655985668));
#397527=CARTESIAN_POINT('Ctrl Pts',(-2.65213101720273,-0.255884898957206,
8.86059725258816));
#397528=CARTESIAN_POINT('Ctrl Pts',(-2.6521543812174,-0.255629570108459,
8.86059794692011));
#397529=CARTESIAN_POINT('Ctrl Pts',(-2.65218976656294,-0.255374212058233,
8.86056369958366));
#397530=CARTESIAN_POINT('Ctrl Pts',(-2.6522315158243,-0.25513223563593,
8.86048590497774));
#397531=CARTESIAN_POINT('Ctrl Pts',(-2.65224241113849,-0.255069086994215,
8.86046560290182));
#397532=CARTESIAN_POINT('Ctrl Pts',(-2.65225397087204,-0.255006043587049,
8.86044257503091));
#397533=CARTESIAN_POINT('Ctrl Pts',(-2.65226580553173,-0.254945047587551,
8.86041778462583));
#397534=CARTESIAN_POINT('Ctrl Pts',(-2.65234543810585,-0.254534620200656,
8.860250975962));
#397535=CARTESIAN_POINT('Ctrl Pts',(-2.65244852973478,-0.254161880950966,
8.8599848982295));
#397536=CARTESIAN_POINT('Ctrl Pts',(-2.65256390552944,-0.253835450601984,
8.85968173251461));
#397537=CARTESIAN_POINT('Ctrl Pts',(-2.65262493271457,-0.253662787649602,
8.85952137522076));
#397538=CARTESIAN_POINT('Ctrl Pts',(-2.65269039306684,-0.253499689179471,
8.85934740853961));
#397539=CARTESIAN_POINT('Ctrl Pts',(-2.65275792075998,-0.253347876209768,
8.8591675900182));
#397540=CARTESIAN_POINT('Ctrl Pts',(-2.65302907954814,-0.252738268225599,
8.85844552518696));
#397541=CARTESIAN_POINT('Ctrl Pts',(-2.65334613350361,-0.252274948742778,
8.85759444184125));
#397542=CARTESIAN_POINT('Ctrl Pts',(-2.65363857348189,-0.25192040239233,
8.8568349891514));
#397543=CARTESIAN_POINT('Ctrl Pts',(-2.65366917654679,-0.251883300060988,
8.85675551444999));
#397544=CARTESIAN_POINT('Ctrl Pts',(-2.65369952268129,-0.251847404387438,
8.85667699793652));
#397545=CARTESIAN_POINT('Ctrl Pts',(-2.65372953884553,-0.251812682972989,
8.85659965593547));
#397546=CARTESIAN_POINT('Ctrl Pts',(-2.65413469856212,-0.251344011549046,
8.85555568965886));
#397547=CARTESIAN_POINT('Ctrl Pts',(-2.65459176757881,-0.250952102354057,
8.85434650606346));
#397548=CARTESIAN_POINT('Ctrl Pts',(-2.65509896008146,-0.250630300122051,
8.85297329937118));
#397549=CARTESIAN_POINT('Ctrl Pts',(-2.65538422496052,-0.250449305974245,
8.85220095427748));
#397550=CARTESIAN_POINT('Ctrl Pts',(-2.65568563114289,-0.25029068142281,
8.85137579139184));
#397551=CARTESIAN_POINT('Ctrl Pts',(-2.65600461497701,-0.250154969482917,
8.85049129520029));
#397552=CARTESIAN_POINT('Origin',(-2.65869612245475,-0.256481217383316,
7.59394543036555));
#397553=CARTESIAN_POINT('Ctrl Pts',(-2.65437916547328,-0.261861333459542,
7.59443877723642));
#397554=CARTESIAN_POINT('Ctrl Pts',(-2.64958222076125,-0.258617490818717,
7.58783886950015));
#397555=CARTESIAN_POINT('Ctrl Pts',(-2.65258170159906,-0.25067505440158,
7.58559994247159));
#397556=CARTESIAN_POINT('Ctrl Pts',(-2.68056554591988,-0.279569375265508,
7.56670252222136));
#397557=CARTESIAN_POINT('Ctrl Pts',(-2.67577553415485,-0.276330220898249,
7.56004874999029));
#397558=CARTESIAN_POINT('Ctrl Pts',(-2.6787728002332,-0.268333174361455,
7.55786368756705));
#397559=CARTESIAN_POINT('Ctrl Pts',(-2.70670302591733,-0.297244349072653,
7.53888913333561));
#397560=CARTESIAN_POINT('Ctrl Pts',(-2.70188454687783,-0.293985944252403,
7.5322200213728));
#397561=CARTESIAN_POINT('Ctrl Pts',(-2.70491526550984,-0.285959912275527,
7.53005029815327));
#397562=CARTESIAN_POINT('Ctrl Pts',(-2.73279042272696,-0.314885455076433,
7.51101258149734));
#397563=CARTESIAN_POINT('Ctrl Pts',(-2.72791353496612,-0.311587552469079,
7.5043616886572));
#397564=CARTESIAN_POINT('Ctrl Pts',(-2.73100785199465,-0.303554328728165,
7.50217374673251));
#397565=CARTESIAN_POINT('',(-2.72961551748768,-0.30261546891712,7.50366116523517));
#397566=CARTESIAN_POINT('Ctrl Pts',(-2.72568349213022,-0.310079528408719,
7.51860402984325));
#397567=CARTESIAN_POINT('Ctrl Pts',(-2.72604931204917,-0.310326907172325,
7.51734760759494));
#397568=CARTESIAN_POINT('Ctrl Pts',(-2.7264132111716,-0.310501163560067,
7.51608817408572));
#397569=CARTESIAN_POINT('Ctrl Pts',(-2.72678011988137,-0.310589852801529,
7.51481005913119));
#397570=CARTESIAN_POINT('Ctrl Pts',(-2.72711247455825,-0.310670189635742,
7.51365231206383));
#397571=CARTESIAN_POINT('Ctrl Pts',(-2.72744770835602,-0.310680673584717,
7.51247773061042));
#397572=CARTESIAN_POINT('Ctrl Pts',(-2.72778117474015,-0.31058421624477,
7.51129758471022));
#397573=CARTESIAN_POINT('Ctrl Pts',(-2.72819563537232,-0.310464330787061,
7.50983079813402));
#397574=CARTESIAN_POINT('Ctrl Pts',(-2.72859051930512,-0.310170560553407,
7.50839324291155));
#397575=CARTESIAN_POINT('Ctrl Pts',(-2.72891950166131,-0.309634617944499,
7.50715379678855));
#397576=CARTESIAN_POINT('Ctrl Pts',(-2.72907148203047,-0.309387027901999,
7.50658120839351));
#397577=CARTESIAN_POINT('Ctrl Pts',(-2.7292229054396,-0.309047586153617,
7.50598221009429));
#397578=CARTESIAN_POINT('Ctrl Pts',(-2.72934939496709,-0.308615104077948,
7.50545747549611));
#397579=CARTESIAN_POINT('Ctrl Pts',(-2.72941689369418,-0.308384318255798,
7.50517746087247));
#397580=CARTESIAN_POINT('Ctrl Pts',(-2.72947821848437,-0.308124592386449,
7.50491486231392));
#397581=CARTESIAN_POINT('Ctrl Pts',(-2.72953012197526,-0.307842421146894,
7.50468370960993));
#397582=CARTESIAN_POINT('Ctrl Pts',(-2.72960773406618,-0.307420486137888,
7.50433806340447));
#397583=CARTESIAN_POINT('Ctrl Pts',(-2.72966606023027,-0.306935611055743,
7.50405484070984));
#397584=CARTESIAN_POINT('Ctrl Pts',(-2.7297004610413,-0.306420365776516,
7.50385766036131));
#397585=CARTESIAN_POINT('Ctrl Pts',(-2.72970413967333,-0.306365268302629,
7.50383657498791));
#397586=CARTESIAN_POINT('Ctrl Pts',(-2.72970755748387,-0.306309848873736,
7.50381643264937));
#397587=CARTESIAN_POINT('Ctrl Pts',(-2.7297107183599,-0.306254165571768,
7.50379723213559));
#397588=CARTESIAN_POINT('Ctrl Pts',(-2.72973181824138,-0.305882461315843,
7.50366906242519));
#397589=CARTESIAN_POINT('Ctrl Pts',(-2.7297412101996,-0.305490872696429,
7.50358235568538));
#397590=CARTESIAN_POINT('Ctrl Pts',(-2.72974118993311,-0.30511321185331,
7.5035341175365));
#397591=CARTESIAN_POINT('Ctrl Pts',(-2.72974115954581,-0.304546952162009,
7.50346178989176));
#397592=CARTESIAN_POINT('Ctrl Pts',(-2.72971705014849,-0.303937786884236,
7.50346967198527));
#397593=CARTESIAN_POINT('Ctrl Pts',(-2.72967498135674,-0.303340503578748,
7.50354272648692));
#397594=CARTESIAN_POINT('Ctrl Pts',(-2.72965767759192,-0.303094828592168,
7.50357277531559));
#397595=CARTESIAN_POINT('Ctrl Pts',(-2.72963749980964,-0.302851480312632,
7.50361331098761));
#397596=CARTESIAN_POINT('Ctrl Pts',(-2.72961551748909,-0.302615468917276,
7.50366116523658));
#397597=CARTESIAN_POINT('',(-2.66161051802581,-0.256762365618787,7.57603338622103));
#397598=CARTESIAN_POINT('Origin',(-2.67040689596866,-0.257608075198384,
7.58486873427625));
#397599=CARTESIAN_POINT('Ctrl Pts',(-2.72961551753202,-0.302615468953483,
7.50366116529968));
#397600=CARTESIAN_POINT('Ctrl Pts',(-2.70698464170165,-0.287355349099734,
7.52783573079709));
#397601=CARTESIAN_POINT('Ctrl Pts',(-2.68431738885518,-0.272071688128237,
7.55196141284069));
#397602=CARTESIAN_POINT('Ctrl Pts',(-2.66161051882396,-0.256762366583466,
7.57603338728831));
#397603=CARTESIAN_POINT('Ctrl Pts',(-2.65579532783697,-0.262606743989967,
7.5963967733137));
#397604=CARTESIAN_POINT('Ctrl Pts',(-2.63922637620262,-0.254890413417566,
7.59959882295472));
#397605=CARTESIAN_POINT('Ctrl Pts',(-2.65684465102774,-0.249960382504432,
7.59642833564545));
#397606=CARTESIAN_POINT('Ctrl Pts',(-2.65204060628407,-0.261549781292344,
7.58707626057419));
#397607=CARTESIAN_POINT('Ctrl Pts',(-2.64876165092592,-0.255620131825776,
7.58809943920599));
#397608=CARTESIAN_POINT('Ctrl Pts',(-2.65302079876161,-0.250369030940479,
7.58710240504253));
#397609=CARTESIAN_POINT('Ctrl Pts',(-2.65730239716171,-0.258510177860639,
7.58015376756929));
#397610=CARTESIAN_POINT('Ctrl Pts',(-2.655609858913,-0.25621570936601,7.58205880659762));
#397611=CARTESIAN_POINT('Ctrl Pts',(-2.65765471203255,-0.254280340988251,
7.58020924244125));
#397612=CARTESIAN_POINT('Ctrl Pts',(-2.66161051720204,-0.256762365539522,
7.57603338509286));
#397613=CARTESIAN_POINT('Ctrl Pts',(-2.66161051720204,-0.256762365539522,
7.57603338509286));
#397614=CARTESIAN_POINT('Ctrl Pts',(-2.66161051720204,-0.256762365539522,
7.57603338509286));
#397615=CARTESIAN_POINT('Origin',(-2.67040634802769,-0.257613755182354,
7.58486873427622));
#397616=CARTESIAN_POINT('Ctrl Pts',(-2.74261348672104,-0.213307152323794,
7.51098857897448));
#397617=CARTESIAN_POINT('Ctrl Pts',(-2.73719608563612,-0.215611990161248,
7.50433767179957));
#397618=CARTESIAN_POINT('Ctrl Pts',(-2.73869774222272,-0.224088609686646,
7.50214974420965));
#397619=CARTESIAN_POINT('Ctrl Pts',(-2.71362657888527,-0.225639656586148,
7.53887321589168));
#397620=CARTESIAN_POINT('Ctrl Pts',(-2.7082740878795,-0.227916878375978,
7.53220407452062));
#397621=CARTESIAN_POINT('Ctrl Pts',(-2.70971466634537,-0.236374280672515,
7.53003438070911));
#397622=CARTESIAN_POINT('Ctrl Pts',(-2.68458400549364,-0.237995843805953,
7.56669465659234));
#397623=CARTESIAN_POINT('Ctrl Pts',(-2.67926314671457,-0.24025960763831,
7.56004085833301));
#397624=CARTESIAN_POINT('Ctrl Pts',(-2.68067642139727,-0.248682155043822,
7.5578558219379));
#397625=CARTESIAN_POINT('Ctrl Pts',(-2.65548708002545,-0.250375155162335,
7.59443891967696));
#397626=CARTESIAN_POINT('Ctrl Pts',(-2.65015850666364,-0.252642201170453,
7.58783901202978));
#397627=CARTESIAN_POINT('Ctrl Pts',(-2.65158440916059,-0.261011548818718,
7.58560008491213));
#397628=CARTESIAN_POINT('',(-2.73712666431696,-0.224754574642208,7.50366116523517));
#397629=CARTESIAN_POINT('Ctrl Pts',(-2.73712666431733,-0.224754574642239,
7.50366116523554));
#397630=CARTESIAN_POINT('Ctrl Pts',(-2.73733969481485,-0.22402741886533,
7.50350835821027));
#397631=CARTESIAN_POINT('Ctrl Pts',(-2.73751186429179,-0.223352055494728,
7.50345484956));
#397632=CARTESIAN_POINT('Ctrl Pts',(-2.73764887337768,-0.222708553769195,
7.50349758195598));
#397633=CARTESIAN_POINT('Ctrl Pts',(-2.7377191691996,-0.222378389660665,
7.50351950684424));
#397634=CARTESIAN_POINT('Ctrl Pts',(-2.73778726446689,-0.222024097627282,
7.50357029184312));
#397635=CARTESIAN_POINT('Ctrl Pts',(-2.73784353695387,-0.221680652932907,
7.50365515313924));
#397636=CARTESIAN_POINT('Ctrl Pts',(-2.73793010682584,-0.221152295918462,
7.50378570417639));
#397637=CARTESIAN_POINT('Ctrl Pts',(-2.73799157957439,-0.220634157925302,
7.50400001621911));
#397638=CARTESIAN_POINT('Ctrl Pts',(-2.73802102162781,-0.220165409289237,
7.50428903009635));
#397639=CARTESIAN_POINT('Ctrl Pts',(-2.73802428946922,-0.220113381796974,
7.50432110841319));
#397640=CARTESIAN_POINT('Ctrl Pts',(-2.73802718145414,-0.220061938916591,
7.50435406373355));
#397641=CARTESIAN_POINT('Ctrl Pts',(-2.7380297016942,-0.220011116430411,
7.50438785222352));
#397642=CARTESIAN_POINT('Ctrl Pts',(-2.73804508897109,-0.219700820723866,
7.50459414719561));
#397643=CARTESIAN_POINT('Ctrl Pts',(-2.73804634861812,-0.219408685618597,
7.50483629897752));
#397644=CARTESIAN_POINT('Ctrl Pts',(-2.73803474839784,-0.219145908398944,
7.5050991045531));
#397645=CARTESIAN_POINT('Ctrl Pts',(-2.73800915714678,-0.218566195458917,
7.50567888004914));
#397646=CARTESIAN_POINT('Ctrl Pts',(-2.73792048980846,-0.218106496852237,
7.50637912803144));
#397647=CARTESIAN_POINT('Ctrl Pts',(-2.73779651599276,-0.217753238076209,
7.50710440483569));
#397648=CARTESIAN_POINT('Ctrl Pts',(-2.73776611515193,-0.217666612011158,
7.50728225710685));
#397649=CARTESIAN_POINT('Ctrl Pts',(-2.73773312376091,-0.217584613677195,
7.50746498566954));
#397650=CARTESIAN_POINT('Ctrl Pts',(-2.73769869842967,-0.217509001681931,
7.50764697238949));
#397651=CARTESIAN_POINT('Ctrl Pts',(-2.73751363732303,-0.217102532404377,
7.50862528291181));
#397652=CARTESIAN_POINT('Ctrl Pts',(-2.7372741051665,-0.216842004831557,
7.50965856837421));
#397653=CARTESIAN_POINT('Ctrl Pts',(-2.73701505418627,-0.216671083027106,
7.51067959873201));
#397654=CARTESIAN_POINT('Ctrl Pts',(-2.7368724981051,-0.216577024542526,
7.51124147302578));
#397655=CARTESIAN_POINT('Ctrl Pts',(-2.73672375708001,-0.216510441144906,
7.51180065547252));
#397656=CARTESIAN_POINT('Ctrl Pts',(-2.73657324382109,-0.216464264630444,
7.51235175716501));
#397657=CARTESIAN_POINT('Ctrl Pts',(-2.73605316055418,-0.216304706378441,
7.51425603304536));
#397658=CARTESIAN_POINT('Ctrl Pts',(-2.73544812829919,-0.216375575257973,
7.51626900505181));
#397659=CARTESIAN_POINT('Ctrl Pts',(-2.73479964907405,-0.21663305061292,
7.51827788969244));
#397660=CARTESIAN_POINT('Ctrl Pts',(-2.73476455215294,-0.216646985665691,
7.51838661432546));
#397661=CARTESIAN_POINT('Ctrl Pts',(-2.73472932345267,-0.216661476202113,
7.51849533314857));
#397662=CARTESIAN_POINT('Ctrl Pts',(-2.73469396819878,-0.216676518124548,
7.51860402984325));
#397663=CARTESIAN_POINT('Ctrl Pts',(-2.66161051899485,-0.256762364824346,
7.57603338728985));
#397664=CARTESIAN_POINT('Ctrl Pts',(-2.68682516411913,-0.246075974209679,
7.55196141284922));
#397665=CARTESIAN_POINT('Ctrl Pts',(-2.7119960174081,-0.235407197792685,
7.52783573083105));
#397666=CARTESIAN_POINT('Ctrl Pts',(-2.73712666436909,-0.224754574614206,
7.50366116530176));
#397667=CARTESIAN_POINT('Origin',(-9.19709468541366E-16,-8.87232663177237E-17,
7.49482233047033));
#397668=CARTESIAN_POINT('Origin',(-2.72083050515592,-0.301641529324094,
7.49482233047033));
#397669=CARTESIAN_POINT('Origin',(0.,0.,7.50366116523517));
#397670=CARTESIAN_POINT('Origin',(-2.7283174780614,-0.224031223057635,7.49482233047033));
#397671=CARTESIAN_POINT('Ctrl Pts',(-2.72568261591557,-0.31007893593925,
7.51860402984325));
#397672=CARTESIAN_POINT('Ctrl Pts',(-2.73198605348183,-0.314340738477903,
7.51860402984325));
#397673=CARTESIAN_POINT('Ctrl Pts',(-2.73109539723703,-0.321897392332867,
7.51860402984325));
#397674=CARTESIAN_POINT('Ctrl Pts',(-2.72802312458908,-0.311661373358606,
7.51041458714366));
#397675=CARTESIAN_POINT('Ctrl Pts',(-2.7317750369846,-0.31613099516997,
7.51004642900443));
#397676=CARTESIAN_POINT('Ctrl Pts',(-2.73109515160462,-0.321899476368271,
7.5072913648301));
#397677=CARTESIAN_POINT('Ctrl Pts',(-2.73030742601402,-0.310016470869305,
7.50215815450137));
#397678=CARTESIAN_POINT('Ctrl Pts',(-2.7322048270618,-0.312485870339889,
7.49877163671529));
#397679=CARTESIAN_POINT('Ctrl Pts',(-2.73182466947127,-0.315915069051078,
7.4948158853317));
#397680=CARTESIAN_POINT('Ctrl Pts',(-2.72961497032199,-0.30261540825579,
7.50366171572174));
#397681=CARTESIAN_POINT('Ctrl Pts',(-2.73325438874115,-0.303018887905099,
7.50000045605858));
#397682=CARTESIAN_POINT('Ctrl Pts',(-2.73325438874114,-0.303018887905223,
7.49482233047317));
#397683=CARTESIAN_POINT('Origin',(-2.71868132724959,-0.320434222367717,
7.51860402984325));
#397684=CARTESIAN_POINT('Origin',(-2.71868132724959,-0.320434222367717,
9.));
#397685=CARTESIAN_POINT('Origin',(-2.71868132724959,-0.320434222367717,
8.75721825406948));
#397686=CARTESIAN_POINT('Ctrl Pts',(-2.71184947061986,-0.300724570905234,
8.78942910404912));
#397687=CARTESIAN_POINT('Ctrl Pts',(-2.71647685875768,-0.30382935877619,
8.79672699501689));
#397688=CARTESIAN_POINT('Ctrl Pts',(-2.71294933545981,-0.31202875298339,
8.79893251111266));
#397689=CARTESIAN_POINT('Ctrl Pts',(-2.72095691172078,-0.306883299291342,
8.78111911759583));
#397690=CARTESIAN_POINT('Ctrl Pts',(-2.72643858652894,-0.310570242662659,
8.78644465894818));
#397691=CARTESIAN_POINT('Ctrl Pts',(-2.72490651814849,-0.318530662139858,
8.78817647674132));
#397692=CARTESIAN_POINT('Ctrl Pts',(-2.72663288623001,-0.31072156574746,
8.76780923932029));
#397693=CARTESIAN_POINT('Ctrl Pts',(-2.73310092791911,-0.315078075070106,
8.7698851615837));
#397694=CARTESIAN_POINT('Ctrl Pts',(-2.73236943182156,-0.322601458209069,
8.77093053738833));
#397695=CARTESIAN_POINT('Ctrl Pts',(-2.72552614888092,-0.309973156320326,
8.75371302330492));
#397696=CARTESIAN_POINT('Ctrl Pts',(-2.73183587040219,-0.314222110979036,
8.7530082828756));
#397697=CARTESIAN_POINT('Ctrl Pts',(-2.73091364145019,-0.321807889323696,
8.75267964240738));
#397698=CARTESIAN_POINT('Origin',(-2.70706536435911,-0.312579148356987,
8.78727029226991));
#397699=CARTESIAN_POINT('Ctrl Pts',(-2.6548449317704,-0.262176299060765,
8.85049129520029));
#397700=CARTESIAN_POINT('Ctrl Pts',(-2.65968232649294,-0.265447495251982,
8.85711686593484));
#397701=CARTESIAN_POINT('Ctrl Pts',(-2.65663515242803,-0.273435955199434,
8.85933012996512));
#397702=CARTESIAN_POINT('Ctrl Pts',(-2.67461451938527,-0.275545106738663,
8.82945683644722));
#397703=CARTESIAN_POINT('Ctrl Pts',(-2.67949206740875,-0.278843455836075,
8.8360746990239));
#397704=CARTESIAN_POINT('Ctrl Pts',(-2.6764009071358,-0.286842003870841,
8.8382956714852));
#397705=CARTESIAN_POINT('Ctrl Pts',(-2.69435463883559,-0.288893987130663,
8.80838214965004));
#397706=CARTESIAN_POINT('Ctrl Pts',(-2.69925143594086,-0.292205353053579,
8.81501364461989));
#397707=CARTESIAN_POINT('Ctrl Pts',(-2.6961370534789,-0.300227162978778,
8.81722098428721));
#397708=CARTESIAN_POINT('Ctrl Pts',(-2.71406752923974,-0.302224454397989,
8.78727029226991));
#397709=CARTESIAN_POINT('Ctrl Pts',(-2.71896513971909,-0.305536370349664,
8.79393457792714));
#397710=CARTESIAN_POINT('Ctrl Pts',(-2.71584585849932,-0.313593013561955,
8.79610912703474));
#397711=CARTESIAN_POINT('Origin',(-2.64784276688977,-0.272530993019762,
8.85049129520029));
#397712=CARTESIAN_POINT('Ctrl Pts',(-2.65600461497701,-0.250154969482917,
8.85049129520029));
#397713=CARTESIAN_POINT('Ctrl Pts',(-2.66137812144103,-0.247868806648761,
8.85711686593484));
#397714=CARTESIAN_POINT('Ctrl Pts',(-2.65991420288366,-0.23944516702142,
8.85933012996512));
#397715=CARTESIAN_POINT('Ctrl Pts',(-2.65125075137568,-0.252177504741186,
8.86332496987232));
#397716=CARTESIAN_POINT('Ctrl Pts',(-2.65197460016677,-0.247613741238949,
8.86648636486738));
#397717=CARTESIAN_POINT('Ctrl Pts',(-2.64662178291423,-0.245119057019721,
8.87206031107457));
#397718=CARTESIAN_POINT('Ctrl Pts',(-2.65053627743828,-0.259262653503821,
8.86341338519876));
#397719=CARTESIAN_POINT('Ctrl Pts',(-2.65034432978771,-0.263892623993324,
8.86654584966058));
#397720=CARTESIAN_POINT('Ctrl Pts',(-2.6445789442447,-0.265265388477037,
8.87215952290714));
#397721=CARTESIAN_POINT('Ctrl Pts',(-2.6548449317704,-0.262176299060764,
8.85049129520029));
#397722=CARTESIAN_POINT('Ctrl Pts',(-2.65968232649294,-0.265447495251982,
8.85711686593484));
#397723=CARTESIAN_POINT('Ctrl Pts',(-2.65663515242803,-0.273435955199434,
8.85933012996512));
#397724=CARTESIAN_POINT('Origin',(-2.6511109650175,-0.238652700573101,8.85049129520029));
#397725=CARTESIAN_POINT('Ctrl Pts',(-2.72179064828012,-0.222166246411436,
8.78727029226991));
#397726=CARTESIAN_POINT('Ctrl Pts',(-2.7272310440052,-0.219851625485032,
8.79393457792714));
#397727=CARTESIAN_POINT('Ctrl Pts',(-2.7257093818291,-0.211347276044891,
8.79610912703474));
#397728=CARTESIAN_POINT('Ctrl Pts',(-2.69989304635039,-0.231482599527254,
8.80838214965003));
#397729=CARTESIAN_POINT('Ctrl Pts',(-2.70533253855794,-0.229168363003135,
8.81501364461988));
#397730=CARTESIAN_POINT('Ctrl Pts',(-2.70380902611904,-0.220699140934737,
8.81722098428722));
#397731=CARTESIAN_POINT('Ctrl Pts',(-2.67796519767341,-0.240811821147071,
8.82945683644723));
#397732=CARTESIAN_POINT('Ctrl Pts',(-2.68338330748996,-0.238506681779171,
8.83607469902389));
#397733=CARTESIAN_POINT('Ctrl Pts',(-2.68187814229224,-0.230064731754116,
8.83829567148519));
#397734=CARTESIAN_POINT('Ctrl Pts',(-2.65600461497701,-0.250154969482917,
8.85049129520029));
#397735=CARTESIAN_POINT('Ctrl Pts',(-2.66137812144103,-0.247868806648761,
8.85711686593484));
#397736=CARTESIAN_POINT('Ctrl Pts',(-2.65991420288366,-0.23944516702142,
8.85933012996512));
#397737=CARTESIAN_POINT('Origin',(-2.71689699832061,-0.21066397750162,8.78727029226991));
#397738=CARTESIAN_POINT('Ctrl Pts',(-2.73452357912827,-0.216748990250367,
8.75374538247848));
#397739=CARTESIAN_POINT('Ctrl Pts',(-2.74152113982087,-0.213786133058224,
8.75304829418603));
#397740=CARTESIAN_POINT('Ctrl Pts',(-2.74207106399279,-0.206172446263106,
8.75272238421917));
#397741=CARTESIAN_POINT('Ctrl Pts',(-2.7357382038743,-0.216232227596518,
8.76769408445017));
#397742=CARTESIAN_POINT('Ctrl Pts',(-2.74291158516777,-0.213194176281819,
8.76974318093965));
#397743=CARTESIAN_POINT('Ctrl Pts',(-2.74363426647131,-0.205677788252088,
8.77077869880429));
#397744=CARTESIAN_POINT('Ctrl Pts',(-2.72951272935803,-0.218880858593496,
8.78108014887993));
#397745=CARTESIAN_POINT('Ctrl Pts',(-2.73559339329596,-0.216309718112288,
8.78639403366329));
#397746=CARTESIAN_POINT('Ctrl Pts',(-2.73563104846251,-0.208215234940551,
8.78812224174742));
#397747=CARTESIAN_POINT('Ctrl Pts',(-2.71931055089962,-0.223221380073934,
8.78944554828685));
#397748=CARTESIAN_POINT('Ctrl Pts',(-2.72443728907637,-0.221059673969037,
8.79673892988685));
#397749=CARTESIAN_POINT('Ctrl Pts',(-2.72254676134579,-0.212345922812599,
8.79894799272499));
#397750=CARTESIAN_POINT('Origin',(-2.72980031823926,-0.205174249214736,
8.75721825406948));
#397751=CARTESIAN_POINT('Origin',(-2.72980031823926,-0.205174249214736,
9.));
#397752=CARTESIAN_POINT('Origin',(-2.72980031823926,-0.205174249214736,
7.51860402984325));
#397753=CARTESIAN_POINT('Ctrl Pts',(-2.73712588029195,-0.22475451026325,
7.50366195182966));
#397754=CARTESIAN_POINT('Ctrl Pts',(-2.74077554873749,-0.225054196678764,
7.50000065167735));
#397755=CARTESIAN_POINT('Ctrl Pts',(-2.7407755487375,-0.225054196678647,
7.49482233047108));
#397756=CARTESIAN_POINT('Ctrl Pts',(-2.73922135542018,-0.217615687979874,
7.50215800491337));
#397757=CARTESIAN_POINT('Ctrl Pts',(-2.74155571535778,-0.215552811140091,
7.49877273257265));
#397758=CARTESIAN_POINT('Ctrl Pts',(-2.74183825344709,-0.212112269238285,
7.49481816995647));
#397759=CARTESIAN_POINT('Ctrl Pts',(-2.7372877110675,-0.21557337657869,
7.51043025814043));
#397760=CARTESIAN_POINT('Ctrl Pts',(-2.74182973674376,-0.211904213221319,
7.51006209594515));
#397761=CARTESIAN_POINT('Ctrl Pts',(-2.74226534963713,-0.20610859318811,
7.50731281821701));
#397762=CARTESIAN_POINT('Ctrl Pts',(-2.73469257739382,-0.216677109744384,
7.51860402984326));
#397763=CARTESIAN_POINT('Ctrl Pts',(-2.74169484877752,-0.213698987372884,
7.51860402984326));
#397764=CARTESIAN_POINT('Ctrl Pts',(-2.74226515987506,-0.206111117932606,
7.51860402984327));
#397765=CARTESIAN_POINT('Origin',(0.,0.,7.5));
#397766=CARTESIAN_POINT('Origin',(-2.6345200847159,-0.419811799220444,7.5));
#397767=CARTESIAN_POINT('',(-2.6345200847159,-0.419811799220444,7.59394543036555));
#397768=CARTESIAN_POINT('',(-2.6345200847159,-0.419811799220444,8.85049129520029));
#397769=CARTESIAN_POINT('',(-2.6345200847159,-0.419811799220444,7.5));
#397770=CARTESIAN_POINT('',(-2.70196419720223,-0.396095507607684,8.78727029226991));
#397771=CARTESIAN_POINT('Ctrl Pts',(-2.6345200847159,-0.419811799220444,
8.85049129520029));
#397772=CARTESIAN_POINT('Ctrl Pts',(-2.65703413439438,-0.411894877373972,
8.82945686509571));
#397773=CARTESIAN_POINT('Ctrl Pts',(-2.67951471421565,-0.403989724989127,
8.80838212259895));
#397774=CARTESIAN_POINT('Ctrl Pts',(-2.70196419720223,-0.396095507607684,
8.78727029226991));
#397775=CARTESIAN_POINT('',(-2.71519273396521,-0.391443777102006,8.75721825406948));
#397776=CARTESIAN_POINT('Origin',(-2.6753835447784,-0.405442638265208,8.75937679713125));
#397777=CARTESIAN_POINT('',(-2.71519273396521,-0.391443777102006,7.51860402984325));
#397778=CARTESIAN_POINT('',(-2.71519273396521,-0.391443777102006,7.5));
#397779=CARTESIAN_POINT('Ctrl Pts',(-2.71519273396521,-0.391443777102006,
7.51860402984325));
#397780=CARTESIAN_POINT('Ctrl Pts',(-2.70480377576452,-0.395096987933276,
7.52834476460825));
#397781=CARTESIAN_POINT('Ctrl Pts',(-2.69440807320208,-0.398752570376309,
7.53807742314407));
#397782=CARTESIAN_POINT('Ctrl Pts',(-2.68400539982697,-0.402410604061113,
7.54780169004674));
#397783=CARTESIAN_POINT('Ctrl Pts',(-2.66752812741731,-0.408204731717991,
7.5632044032688));
#397784=CARTESIAN_POINT('Ctrl Pts',(-2.65103334518629,-0.414005016591753,
7.57858609112103));
#397785=CARTESIAN_POINT('Ctrl Pts',(-2.6345200847159,-0.419811799220444,
7.59394543036555));
#397786=CARTESIAN_POINT('Origin',(-2.85005793045283,-0.60006065396634,7.5));
#397787=CARTESIAN_POINT('',(-2.70021641947034,-0.48407757770026,8.75721825406948));
#397788=CARTESIAN_POINT('',(-2.68912759914126,-0.475494405483858,8.78727029226991));
#397789=CARTESIAN_POINT('Origin',(-2.66098003722165,-0.453707113034527,
8.75658640621012));
#397790=CARTESIAN_POINT('',(-2.6325925749723,-0.431734128529235,8.85049129520029));
#397791=CARTESIAN_POINT('Ctrl Pts',(-2.68912759914126,-0.475494405483858,
8.78727029226991));
#397792=CARTESIAN_POINT('Ctrl Pts',(-2.67030932106718,-0.460928336530396,
8.80838212259895));
#397793=CARTESIAN_POINT('Ctrl Pts',(-2.65146497607287,-0.446342090780945,
8.82945686509571));
#397794=CARTESIAN_POINT('Ctrl Pts',(-2.6325925749723,-0.431734128529236,
8.85049129520029));
#397795=CARTESIAN_POINT('',(-2.6325925749723,-0.431734128529235,7.59394543036555));
#397796=CARTESIAN_POINT('',(-2.6325925749723,-0.431734128529235,7.5));
#397797=CARTESIAN_POINT('',(-2.70021641947034,-0.48407757770026,7.51860402984325));
#397798=CARTESIAN_POINT('Ctrl Pts',(-2.6325925749723,-0.431734128529234,
7.59394543036555));
#397799=CARTESIAN_POINT('Ctrl Pts',(-2.64643481479702,-0.442448553035217,
7.57858609112103));
#397800=CARTESIAN_POINT('Ctrl Pts',(-2.6602615652383,-0.453150988164337,
7.56320440326857));
#397801=CARTESIAN_POINT('Ctrl Pts',(-2.67407363807278,-0.463842062262906,
7.54780169004651));
#397802=CARTESIAN_POINT('Ctrl Pts',(-2.68279367854782,-0.470591708024144,
7.53807742314383));
#397803=CARTESIAN_POINT('Ctrl Pts',(-2.69150787573962,-0.477336830860056,
7.52834476460825));
#397804=CARTESIAN_POINT('Ctrl Pts',(-2.70021641947034,-0.484077577700258,
7.51860402984324));
#397805=CARTESIAN_POINT('',(-2.70021641947034,-0.48407757770026,7.5));
#397806=CARTESIAN_POINT('Origin',(-2.63680073810823,-0.426297494642222,
7.5));
#397807=CARTESIAN_POINT('Ctrl Pts',(-2.6325925749723,-0.431734128529235,
8.85049129520029));
#397808=CARTESIAN_POINT('Ctrl Pts',(-2.6324394307242,-0.431615589007775,
8.85097269580138));
#397809=CARTESIAN_POINT('Ctrl Pts',(-2.63229336726999,-0.431491893478835,
8.85143669361005));
#397810=CARTESIAN_POINT('Ctrl Pts',(-2.63214822387277,-0.431356678978368,
8.8519052845931));
#397811=CARTESIAN_POINT('Ctrl Pts',(-2.63186433259248,-0.431092207990448,
8.85282181883899));
#397812=CARTESIAN_POINT('Ctrl Pts',(-2.63159139830333,-0.430790328371194,
8.85372622499635));
#397813=CARTESIAN_POINT('Ctrl Pts',(-2.63133657541701,-0.430435962534927,
8.8546225773507));
#397814=CARTESIAN_POINT('Ctrl Pts',(-2.63112503050724,-0.430141780603542,
8.85536669723986));
#397815=CARTESIAN_POINT('Ctrl Pts',(-2.63092589359265,-0.429811377957245,
8.85610498449051));
#397816=CARTESIAN_POINT('Ctrl Pts',(-2.63075009497682,-0.429431969215898,
8.85681338218371));
#397817=CARTESIAN_POINT('Ctrl Pts',(-2.63059055745687,-0.429087655187255,
8.85745625420284));
#397818=CARTESIAN_POINT('Ctrl Pts',(-2.63044769614055,-0.428698914290595,
8.85808743050665));
#397819=CARTESIAN_POINT('Ctrl Pts',(-2.63034146522525,-0.428245260526917,
8.85866804508409));
#397820=CARTESIAN_POINT('Ctrl Pts',(-2.63029245258373,-0.428035954514361,
8.85893592806395));
#397821=CARTESIAN_POINT('Ctrl Pts',(-2.63025142607327,-0.427812678304165,
8.85919241173848));
#397822=CARTESIAN_POINT('Ctrl Pts',(-2.63022171543869,-0.427572600858362,
8.85943017985534));
#397823=CARTESIAN_POINT('Ctrl Pts',(-2.63018159728671,-0.427248425236,8.8597512372));
#397824=CARTESIAN_POINT('Ctrl Pts',(-2.63016172595496,-0.426885286146236,
8.86004599534706));
#397825=CARTESIAN_POINT('Ctrl Pts',(-2.63017273972452,-0.426486977495829,
8.86026130871721));
#397826=CARTESIAN_POINT('Ctrl Pts',(-2.63017677217606,-0.426341145469406,
8.86034014101235));
#397827=CARTESIAN_POINT('Ctrl Pts',(-2.63018499302248,-0.42618840807178,
8.86040910639692));
#397828=CARTESIAN_POINT('Ctrl Pts',(-2.63019751418393,-0.426032944626492,
8.86046313645506));
#397829=CARTESIAN_POINT('Ctrl Pts',(-2.63021705335152,-0.425790345222114,
8.86054744990829));
#397830=CARTESIAN_POINT('Ctrl Pts',(-2.63024774428927,-0.425534497097203,
8.86059655985668));
#397831=CARTESIAN_POINT('Ctrl Pts',(-2.6302873278218,-0.42528177367858,
8.86059725258816));
#397832=CARTESIAN_POINT('Ctrl Pts',(-2.6303270028081,-0.425028466367897,
8.86059794692011));
#397833=CARTESIAN_POINT('Ctrl Pts',(-2.6303786762971,-0.424775900125044,
8.86056369958366));
#397834=CARTESIAN_POINT('Ctrl Pts',(-2.63043584326274,-0.424537095753612,
8.86048590497774));
#397835=CARTESIAN_POINT('Ctrl Pts',(-2.6304507621387,-0.424474774922731,
8.86046560290182));
#397836=CARTESIAN_POINT('Ctrl Pts',(-2.6304663373265,-0.424412601679678,
8.86044257503091));
#397837=CARTESIAN_POINT('Ctrl Pts',(-2.63048205569772,-0.424352489252253,
8.86041778462583));
#397838=CARTESIAN_POINT('Ctrl Pts',(-2.63058782083114,-0.423948007208984,
8.86025097596201));
#397839=CARTESIAN_POINT('Ctrl Pts',(-2.63071458213299,-0.423582638895403,
8.8599848982295));
#397840=CARTESIAN_POINT('Ctrl Pts',(-2.63085063533997,-0.423264271385127,
8.85968173251462));
#397841=CARTESIAN_POINT('Ctrl Pts',(-2.63092259969155,-0.423095873212475,
8.85952137522077));
#397842=CARTESIAN_POINT('Ctrl Pts',(-2.63099837530336,-0.422937303904813,
8.85934740853961));
#397843=CARTESIAN_POINT('Ctrl Pts',(-2.63107549094398,-0.422790129365292,
8.8591675900182));
#397844=CARTESIAN_POINT('Ctrl Pts',(-2.63138515032498,-0.422199147089306,
8.85844552518695));
#397845=CARTESIAN_POINT('Ctrl Pts',(-2.63173123784028,-0.421757093262724,
8.85759444184123));
#397846=CARTESIAN_POINT('Ctrl Pts',(-2.63204579283193,-0.421422012059516,
8.85683498915137));
#397847=CARTESIAN_POINT('Ctrl Pts',(-2.63207871017408,-0.421386946703997,
8.85675551444997));
#397848=CARTESIAN_POINT('Ctrl Pts',(-2.63211129380289,-0.421353069065475,
8.85667699793651));
#397849=CARTESIAN_POINT('Ctrl Pts',(-2.63214347290436,-0.421320342132146,
8.85659965593547));
#397850=CARTESIAN_POINT('Ctrl Pts',(-2.63257782805809,-0.420878592316076,
8.85555568965886));
#397851=CARTESIAN_POINT('Ctrl Pts',(-2.6330590676858,-0.420516772853006,
8.85434650606346));
#397852=CARTESIAN_POINT('Ctrl Pts',(-2.63358583604686,-0.420228127733416,
8.85297329937117));
#397853=CARTESIAN_POINT('Ctrl Pts',(-2.63388211115349,-0.420065782441052,
8.85220095427747));
#397854=CARTESIAN_POINT('Ctrl Pts',(-2.63419306117444,-0.419926794961179,
8.85137579139183));
#397855=CARTESIAN_POINT('Ctrl Pts',(-2.6345200847159,-0.419811799220444,
8.85049129520029));
#397856=CARTESIAN_POINT('Origin',(-2.63680073810823,-0.426297494642222,
7.59394543036555));
#397857=CARTESIAN_POINT('Ctrl Pts',(-2.63214794555735,-0.431389968309504,
7.59443877723642));
#397858=CARTESIAN_POINT('Ctrl Pts',(-2.62756869039428,-0.427845449188351,
7.58783886950016));
#397859=CARTESIAN_POINT('Ctrl Pts',(-2.63107088212544,-0.420111508755763,
7.58559994247159));
#397860=CARTESIAN_POINT('Ctrl Pts',(-2.65714596514287,-0.45073939420009,
7.56670252222133));
#397861=CARTESIAN_POINT('Ctrl Pts',(-2.65257332830362,-0.447199997915386,
7.56004874999028));
#397862=CARTESIAN_POINT('Ctrl Pts',(-2.6560768087082,-0.439411417665357,
7.55786368756704));
#397863=CARTESIAN_POINT('Ctrl Pts',(-2.68209730342447,-0.470052686971096,
7.53888913333557));
#397864=CARTESIAN_POINT('Ctrl Pts',(-2.67749749118057,-0.466492255880973,
7.53222002137277));
#397865=CARTESIAN_POINT('Ctrl Pts',(-2.68103621251044,-0.458676893057046,
7.53005029815327));
#397866=CARTESIAN_POINT('Ctrl Pts',(-2.70700083133714,-0.489328972682922,
7.51101258149734));
#397867=CARTESIAN_POINT('Ctrl Pts',(-2.70234526101078,-0.485725382698516,
7.5043616886572));
#397868=CARTESIAN_POINT('Ctrl Pts',(-2.70594791084535,-0.477906917650045,
7.50217374673251));
#397869=CARTESIAN_POINT('',(-2.70461858999357,-0.476880779649026,7.50366116523517));
#397870=CARTESIAN_POINT('Ctrl Pts',(-2.70021641947034,-0.48407757770026,
7.51860402984325));
#397871=CARTESIAN_POINT('Ctrl Pts',(-2.70056563816122,-0.484347886360344,
7.51734760759493));
#397872=CARTESIAN_POINT('Ctrl Pts',(-2.70091762496879,-0.484545099816474,
7.51608817408573));
#397873=CARTESIAN_POINT('Ctrl Pts',(-2.70127809748605,-0.484657114758125,
7.5148100591312));
#397874=CARTESIAN_POINT('Ctrl Pts',(-2.70160462210596,-0.484758580568956,
7.51365231206384));
#397875=CARTESIAN_POINT('Ctrl Pts',(-2.70193849542102,-0.484790521480701,
7.51247773061042));
#397876=CARTESIAN_POINT('Ctrl Pts',(-2.70227745670569,-0.484715627587292,
7.51129758471022));
#397877=CARTESIAN_POINT('Ctrl Pts',(-2.70269874687169,-0.48462254303099,
7.50983079813402));
#397878=CARTESIAN_POINT('Ctrl Pts',(-2.70311164139659,-0.484354676680229,
7.50839324291155));
#397879=CARTESIAN_POINT('Ctrl Pts',(-2.7034742857841,-0.483840913194821,
7.50715379678855));
#397880=CARTESIAN_POINT('Ctrl Pts',(-2.70364181704178,-0.483603569268302,
7.50658120839351));
#397881=CARTESIAN_POINT('Ctrl Pts',(-2.70381467744276,-0.48327452667053,
7.50598221009429));
#397882=CARTESIAN_POINT('Ctrl Pts',(-2.70396861630568,-0.48285103738752,
7.50545747549611));
#397883=CARTESIAN_POINT('Ctrl Pts',(-2.70405076284779,-0.482625050397887,
7.50517746087247));
#397884=CARTESIAN_POINT('Ctrl Pts',(-2.7041286023332,-0.48236978725599,
7.50491486231392));
#397885=CARTESIAN_POINT('Ctrl Pts',(-2.7041984779562,-0.48209152123559,
7.50468370960993));
#397886=CARTESIAN_POINT('Ctrl Pts',(-2.7043029640536,-0.481675425761052,
7.50433806340447));
#397887=CARTESIAN_POINT('Ctrl Pts',(-2.7043922364335,-0.481195283876931,
7.50405484070984));
#397888=CARTESIAN_POINT('Ctrl Pts',(-2.70445957844277,-0.480683301291921,
7.50385766036131));
#397889=CARTESIAN_POINT('Ctrl Pts',(-2.70446677962393,-0.480628552712466,
7.50383657498791));
#397890=CARTESIAN_POINT('Ctrl Pts',(-2.70447374114721,-0.480573466128605,
7.50381643264937));
#397891=CARTESIAN_POINT('Ctrl Pts',(-2.70448046317028,-0.480518099751973,
7.50379723213559));
#397892=CARTESIAN_POINT('Ctrl Pts',(-2.70452533487324,-0.480148511076355,
7.50366906242519));
#397893=CARTESIAN_POINT('Ctrl Pts',(-2.70455979670366,-0.479758328762587,
7.50358235568538));
#397894=CARTESIAN_POINT('Ctrl Pts',(-2.70458397329211,-0.479381442565697,
7.5035341175365));
#397895=CARTESIAN_POINT('Ctrl Pts',(-2.70462022335022,-0.47881634436874,
7.50346178989176));
#397896=CARTESIAN_POINT('Ctrl Pts',(-2.7046351928416,-0.478206885991972,
7.50346967198527));
#397897=CARTESIAN_POINT('Ctrl Pts',(-2.70463147855747,-0.477608134512351,
7.50354272648692));
#397898=CARTESIAN_POINT('Ctrl Pts',(-2.70462995079553,-0.477361855635362,
7.50357277531559));
#397899=CARTESIAN_POINT('Ctrl Pts',(-2.70462540584846,-0.477117714546017,
7.50361331098761));
#397900=CARTESIAN_POINT('Ctrl Pts',(-2.70461858999497,-0.476880779649272,
7.50366116523658));
#397901=CARTESIAN_POINT('',(-2.63969113251173,-0.426764791193839,7.57603338622103));
#397902=CARTESIAN_POINT('Origin',(-2.64841525255386,-0.428172349042246,
7.58486873427628));
#397903=CARTESIAN_POINT('Ctrl Pts',(-2.70461859003549,-0.476880779688155,
7.50366116529968));
#397904=CARTESIAN_POINT('Ctrl Pts',(-2.68301193100263,-0.460202048194472,
7.52783573079709));
#397905=CARTESIAN_POINT('Ctrl Pts',(-2.66137047797874,-0.443497493267363,
7.55196141284068));
#397906=CARTESIAN_POINT('Ctrl Pts',(-2.63969113324643,-0.426764792207667,
7.57603338728831));
#397907=CARTESIAN_POINT('Ctrl Pts',(-2.63351343964692,-0.432224581148218,
7.5963967733137));
#397908=CARTESIAN_POINT('Ctrl Pts',(-2.61671933910955,-0.423050889786067,
7.59974925422224));
#397909=CARTESIAN_POINT('Ctrl Pts',(-2.63554858227812,-0.419636504370458,
7.59639677331373));
#397910=CARTESIAN_POINT('Ctrl Pts',(-2.62983415240469,-0.430929224257954,
7.5870762605742));
#397911=CARTESIAN_POINT('Ctrl Pts',(-2.62689172333802,-0.424695481979904,
7.58811717123965));
#397912=CARTESIAN_POINT('Ctrl Pts',(-2.63164855597466,-0.41970649662526,
7.58707626057426));
#397913=CARTESIAN_POINT('Ctrl Pts',(-2.63527988042917,-0.428232990116521,
7.58015376756929));
#397914=CARTESIAN_POINT('Ctrl Pts',(-2.63371451346334,-0.425798537775517,
7.5820876076604));
#397915=CARTESIAN_POINT('Ctrl Pts',(-2.63596724991743,-0.423981366785814,
7.58015376756931));
#397916=CARTESIAN_POINT('Ctrl Pts',(-2.63969113169473,-0.426764791061958,
7.57603338509286));
#397917=CARTESIAN_POINT('Ctrl Pts',(-2.63969113169473,-0.426764791061958,
7.57603338509286));
#397918=CARTESIAN_POINT('Ctrl Pts',(-2.63969113169473,-0.426764791061958,
7.57603338509286));
#397919=CARTESIAN_POINT('Origin',(-2.64841434182015,-0.428177982249053,
7.58486873427621));
#397920=CARTESIAN_POINT('Ctrl Pts',(-2.72331185699535,-0.388588739318512,
7.51098857897448));
#397921=CARTESIAN_POINT('Ctrl Pts',(-2.71775791507471,-0.390541747540201,
7.50433767179956));
#397922=CARTESIAN_POINT('Ctrl Pts',(-2.71871338746912,-0.399097162409509,
7.50214974420965));
#397923=CARTESIAN_POINT('Ctrl Pts',(-2.69359435960954,-0.399038707566613,
7.53887321589164));
#397924=CARTESIAN_POINT('Ctrl Pts',(-2.68810696376955,-0.40096831528384,
7.53220407452058));
#397925=CARTESIAN_POINT('Ctrl Pts',(-2.68900271478691,-0.409500639119532,
7.53003438070911));
#397926=CARTESIAN_POINT('Ctrl Pts',(-2.66381979366646,-0.409508743608567,
7.56669465659232));
#397927=CARTESIAN_POINT('Ctrl Pts',(-2.65836482731572,-0.411426947702915,
7.56004085833301));
#397928=CARTESIAN_POINT('Ctrl Pts',(-2.65923556380894,-0.419922738901258,
7.55785582193789));
#397929=CARTESIAN_POINT('Ctrl Pts',(-2.63398950575049,-0.419998373926575,
7.59443891967696));
#397930=CARTESIAN_POINT('Ctrl Pts',(-2.62852663037769,-0.421919359178055,
7.58783901202978));
#397931=CARTESIAN_POINT('Ctrl Pts',(-2.62941337726011,-0.430362868990617,
7.58560008491213));
#397932=CARTESIAN_POINT('',(-2.7171028689902,-0.399661099761616,7.50366116523517));
#397933=CARTESIAN_POINT('Ctrl Pts',(-2.71710286899057,-0.399661099761671,
7.50366116523554));
#397934=CARTESIAN_POINT('Ctrl Pts',(-2.71736205082467,-0.398949086915132,
7.50350835821027));
#397935=CARTESIAN_POINT('Ctrl Pts',(-2.71757713724069,-0.398286142087269,
7.50345484956));
#397936=CARTESIAN_POINT('Ctrl Pts',(-2.71775509412383,-0.397652740707318,
7.50349758195598));
#397937=CARTESIAN_POINT('Ctrl Pts',(-2.71784639920251,-0.397327758825133,
7.50351950684424));
#397938=CARTESIAN_POINT('Ctrl Pts',(-2.71793705412928,-0.396978557601486,
7.50357029184312));
#397939=CARTESIAN_POINT('Ctrl Pts',(-2.71801521557553,-0.39663942394169,
7.50365515313924));
#397940=CARTESIAN_POINT('Ctrl Pts',(-2.71813545953055,-0.396117699044139,
7.50378570417639));
#397941=CARTESIAN_POINT('Ctrl Pts',(-2.71823000319195,-0.395604564193579,
7.50400001621911));
#397942=CARTESIAN_POINT('Ctrl Pts',(-2.71828941758173,-0.395138665010699,
7.50428903009635));
#397943=CARTESIAN_POINT('Ctrl Pts',(-2.71829601212189,-0.395086953785816,
7.50432110841318));
#397944=CARTESIAN_POINT('Ctrl Pts',(-2.71830219412158,-0.395035801890458,
7.50435406373354));
#397945=CARTESIAN_POINT('Ctrl Pts',(-2.7183079653914,-0.39498524529686,
7.50438785222352));
#397946=CARTESIAN_POINT('Ctrl Pts',(-2.71834320176766,-0.394676572992338,
7.50459414719561));
#397947=CARTESIAN_POINT('Ctrl Pts',(-2.71836317598707,-0.394385118815837,
7.50483629897752));
#397948=CARTESIAN_POINT('Ctrl Pts',(-2.71836843579496,-0.394122138271499,
7.5050991045531));
#397949=CARTESIAN_POINT('Ctrl Pts',(-2.71838003945946,-0.393541976776796,
7.50567888004914));
#397950=CARTESIAN_POINT('Ctrl Pts',(-2.71832100728855,-0.393077541734335,
7.50637912803144));
#397951=CARTESIAN_POINT('Ctrl Pts',(-2.71821992155784,-0.392717065736705,
7.50710440483569));
#397952=CARTESIAN_POINT('Ctrl Pts',(-2.71819513332984,-0.392628669865636,
7.50728225710685));
#397953=CARTESIAN_POINT('Ctrl Pts',(-2.71816746337447,-0.392544726240364,
7.50746498566954));
#397954=CARTESIAN_POINT('Ctrl Pts',(-2.71813795325093,-0.392467063959509,
7.50764697238949));
#397955=CARTESIAN_POINT('Ctrl Pts',(-2.71797931494821,-0.392049572910864,
7.50862528291182));
#397956=CARTESIAN_POINT('Ctrl Pts',(-2.71775696699509,-0.391774233741921,
7.50965856837422));
#397957=CARTESIAN_POINT('Ctrl Pts',(-2.71750939926049,-0.391587065661359,
7.51067959873203));
#397958=CARTESIAN_POINT('Ctrl Pts',(-2.71737316242388,-0.391484066830545,
7.51124147302579));
#397959=CARTESIAN_POINT('Ctrl Pts',(-2.71722899301611,-0.39140809036546,
7.51180065547253));
#397960=CARTESIAN_POINT('Ctrl Pts',(-2.71708174754227,-0.391352365307991,
7.512351757165));
#397961=CARTESIAN_POINT('Ctrl Pts',(-2.71657295577451,-0.391159813036211,
7.51425603304535));
#397962=CARTESIAN_POINT('Ctrl Pts',(-2.71596462603848,-0.391191771758356,
7.51626900505179));
#397963=CARTESIAN_POINT('Ctrl Pts',(-2.71530098268083,-0.391407169895963,
7.51827788969242));
#397964=CARTESIAN_POINT('Ctrl Pts',(-2.71526506504821,-0.391418827650217,
7.51838661432544));
#397965=CARTESIAN_POINT('Ctrl Pts',(-2.71522898031722,-0.391431031303703,
7.51849533314856));
#397966=CARTESIAN_POINT('Ctrl Pts',(-2.71519273396521,-0.391443777102002,
7.51860402984325));
#397967=CARTESIAN_POINT('Ctrl Pts',(-2.63969113352968,-0.426764790463122,
7.57603338728985));
#397968=CARTESIAN_POINT('Ctrl Pts',(-2.66553865185878,-0.417715864043942,
7.55196141284922));
#397969=CARTESIAN_POINT('Ctrl Pts',(-2.69134133978206,-0.40868170987964,
7.52783573083104));
#397970=CARTESIAN_POINT('Ctrl Pts',(-2.71710286904403,-0.399661099737013,
7.50366116530176));
#397971=CARTESIAN_POINT('Origin',(-9.12135307609332E-16,-1.47466962819323E-16,
7.49482233047033));
#397972=CARTESIAN_POINT('Origin',(-2.69591402793581,-0.47534598344672,7.49482233047033));
#397973=CARTESIAN_POINT('Origin',(0.,0.,7.50366116523517));
#397974=CARTESIAN_POINT('Origin',(-2.70835812744774,-0.398374827879208,
7.49482233047033));
#397975=CARTESIAN_POINT('Ctrl Pts',(-2.70021558301562,-0.484076930308821,
7.51860402984325));
#397976=CARTESIAN_POINT('Ctrl Pts',(-2.70623301486718,-0.488733839148586,
7.51860402984325));
#397977=CARTESIAN_POINT('Ctrl Pts',(-2.70486003209636,-0.496217902506222,
7.51860402984325));
#397978=CARTESIAN_POINT('Ctrl Pts',(-2.70244989574948,-0.485806073346367,
7.51041458714366));
#397979=CARTESIAN_POINT('Ctrl Pts',(-2.7059077297859,-0.490506897692872,
7.51004642900443));
#397980=CARTESIAN_POINT('Ctrl Pts',(-2.70485965344402,-0.496219966522037,
7.5072913648301));
#397981=CARTESIAN_POINT('Ctrl Pts',(-2.70483489309648,-0.484310906180435,
7.50215815450138));
#397982=CARTESIAN_POINT('Ctrl Pts',(-2.70657018076302,-0.486896798907495,
7.4987716367153));
#397983=CARTESIAN_POINT('Ctrl Pts',(-2.70597109473124,-0.490294595181685,
7.49481588533171));
#397984=CARTESIAN_POINT('Ctrl Pts',(-2.70461804783867,-0.476880684055306,
7.50366171572174));
#397985=CARTESIAN_POINT('Ctrl Pts',(-2.70822413765248,-0.477516513051119,
7.50000045605858));
#397986=CARTESIAN_POINT('Ctrl Pts',(-2.70822413765246,-0.477516513051242,
7.49482233047317));
#397987=CARTESIAN_POINT('Origin',(-2.69256521376865,-0.493962366585738,
7.51860402984325));
#397988=CARTESIAN_POINT('Origin',(-2.69256521376865,-0.493962366585738,
9.));
#397989=CARTESIAN_POINT('Origin',(-2.69256521376865,-0.493962366585738,
8.75721825406948));
#397990=CARTESIAN_POINT('Ctrl Pts',(-2.68701019562603,-0.473855492158896,
8.78942910404912));
#397991=CARTESIAN_POINT('Ctrl Pts',(-2.69142915185674,-0.47725037868611,
8.7967269950169));
#397992=CARTESIAN_POINT('Ctrl Pts',(-2.68738353924326,-0.485206917164847,
8.79893251111267));
#397993=CARTESIAN_POINT('Ctrl Pts',(-2.69570433342993,-0.480585082531806,
8.78111911759583));
#397994=CARTESIAN_POINT('Ctrl Pts',(-2.70093852227643,-0.484615662793361,
8.78644465894816));
#397995=CARTESIAN_POINT('Ctrl Pts',(-2.69889957586774,-0.492461566776834,
8.78817647674132));
#397996=CARTESIAN_POINT('Ctrl Pts',(-2.70112272746461,-0.484779123793258,
8.7678092393203));
#397997=CARTESIAN_POINT('Ctrl Pts',(-2.70729835735771,-0.489541091054135,
8.76988516158372));
#397998=CARTESIAN_POINT('Ctrl Pts',(-2.70608633938462,-0.497002149479666,
8.77093053738832));
#397999=CARTESIAN_POINT('Ctrl Pts',(-2.70006621478272,-0.483961343148133,
8.75371302330492));
#398000=CARTESIAN_POINT('Ctrl Pts',(-2.70609074084473,-0.488605833119682,
8.75300828287559));
#398001=CARTESIAN_POINT('Ctrl Pts',(-2.70468438422376,-0.496116938257335,
8.75267964240738));
#398002=CARTESIAN_POINT('Origin',(-2.68147639343957,-0.485379194369336,
8.78727029226991));
#398003=CARTESIAN_POINT('Ctrl Pts',(-2.6325925749723,-0.431734128529235,
8.85049129520029));
#398004=CARTESIAN_POINT('Ctrl Pts',(-2.637210444489,-0.43530853664105,8.85711686593484));
#398005=CARTESIAN_POINT('Ctrl Pts',(-2.63365770878388,-0.443085350328122,
8.85933012996512));
#398006=CARTESIAN_POINT('Ctrl Pts',(-2.65146500140032,-0.446342110385364,
8.82945683644722));
#398007=CARTESIAN_POINT('Ctrl Pts',(-2.65612120202604,-0.449946188245629,
8.83607469902387));
#398008=CARTESIAN_POINT('Ctrl Pts',(-2.65252392414128,-0.457730251086948,
8.83829567148519));
#398009=CARTESIAN_POINT('Ctrl Pts',(-2.6703092969549,-0.460928317866566,
8.80838214965001));
#398010=CARTESIAN_POINT('Ctrl Pts',(-2.6749838731222,-0.464546619100782,
8.81501364461988));
#398011=CARTESIAN_POINT('Ctrl Pts',(-2.6713619303665,-0.472352408187708,
8.81722098428721));
#398012=CARTESIAN_POINT('Ctrl Pts',(-2.68912759914126,-0.475494405483858,
8.78727029226991));
#398013=CARTESIAN_POINT('Ctrl Pts',(-2.69380295177103,-0.4791133077298,
8.79393457792714));
#398014=CARTESIAN_POINT('Ctrl Pts',(-2.69017388854615,-0.486953544670607,
8.79610912703474));
#398015=CARTESIAN_POINT('Origin',(-2.62494136927061,-0.441618917414714,
8.85049129520029));
#398016=CARTESIAN_POINT('Ctrl Pts',(-2.6345200847159,-0.419811799220444,
8.85049129520029));
#398017=CARTESIAN_POINT('Ctrl Pts',(-2.64002902569028,-0.417874615294239,
8.85711686593484));
#398018=CARTESIAN_POINT('Ctrl Pts',(-2.63910781935455,-0.40937448935394,
8.85933012996512));
#398019=CARTESIAN_POINT('Ctrl Pts',(-2.62964640415828,-0.421525597876414,
8.86332496987231));
#398020=CARTESIAN_POINT('Ctrl Pts',(-2.63066116705591,-0.417017588267029,
8.86648636486737));
#398021=CARTESIAN_POINT('Ctrl Pts',(-2.62547918270721,-0.414185073465195,
8.87206031107457));
#398022=CARTESIAN_POINT('Ctrl Pts',(-2.62847945114439,-0.428550412938697,
8.86341338519877));
#398023=CARTESIAN_POINT('Ctrl Pts',(-2.6279912546431,-0.43315857252908,
8.8665458496606));
#398024=CARTESIAN_POINT('Ctrl Pts',(-2.62214976138055,-0.434159127000912,
8.87215952290714));
#398025=CARTESIAN_POINT('Ctrl Pts',(-2.6325925749723,-0.431734128529235,
8.85049129520029));
#398026=CARTESIAN_POINT('Ctrl Pts',(-2.637210444489,-0.43530853664105,8.85711686593484));
#398027=CARTESIAN_POINT('Ctrl Pts',(-2.63365770878388,-0.443085350328122,
8.85933012996512));
#398028=CARTESIAN_POINT('Origin',(-2.6303734421844,-0.408019625726303,8.85049129520029));
#398029=CARTESIAN_POINT('Ctrl Pts',(-2.70196419720223,-0.396095507607684,
8.78727029226991));
#398030=CARTESIAN_POINT('Ctrl Pts',(-2.70754171332274,-0.394134209669103,
8.79393457792714));
#398031=CARTESIAN_POINT('Ctrl Pts',(-2.7065680531042,-0.385549840096616,
8.79610912703474));
#398032=CARTESIAN_POINT('Ctrl Pts',(-2.67951468545062,-0.403989735104165,
8.80838214965001));
#398033=CARTESIAN_POINT('Ctrl Pts',(-2.68509127528122,-0.402028762889512,
8.81501364461987));
#398034=CARTESIAN_POINT('Ctrl Pts',(-2.68411351798304,-0.393479329969075,
8.81722098428721));
#398035=CARTESIAN_POINT('Ctrl Pts',(-2.65703416460907,-0.411894866749169,
8.82945683644722));
#398036=CARTESIAN_POINT('Ctrl Pts',(-2.66258883312429,-0.409941603025111,
8.83607469902388));
#398037=CARTESIAN_POINT('Ctrl Pts',(-2.66162763804508,-0.401420561626501,
8.8382956714852));
#398038=CARTESIAN_POINT('Ctrl Pts',(-2.6345200847159,-0.419811799220444,
8.85049129520029));
#398039=CARTESIAN_POINT('Ctrl Pts',(-2.64002902569028,-0.417874615294238,
8.85711686593484));
#398040=CARTESIAN_POINT('Ctrl Pts',(-2.63910781935455,-0.40937448935394,
8.85933012996512));
#398041=CARTESIAN_POINT('Origin',(-2.69781755467073,-0.384303334113543,
8.78727029226991));
#398042=CARTESIAN_POINT('Ctrl Pts',(-2.71501805167228,-0.391505183460838,
8.75374538247847));
#398043=CARTESIAN_POINT('Ctrl Pts',(-2.72219106603802,-0.388996749029462,
8.75304829418601));
#398044=CARTESIAN_POINT('Ctrl Pts',(-2.72322767091958,-0.381433939133099,
8.75272238421917));
#398045=CARTESIAN_POINT('Ctrl Pts',(-2.7162632899384,-0.391067303825958,
8.76769408445021));
#398046=CARTESIAN_POINT('Ctrl Pts',(-2.7236165813667,-0.388495094631014,
8.76974318093971));
#398047=CARTESIAN_POINT('Ctrl Pts',(-2.72481935447853,-0.38104045217669,
8.7707786988043));
#398048=CARTESIAN_POINT('Ctrl Pts',(-2.70988090795657,-0.393311625404748,
8.78108014887987));
#398049=CARTESIAN_POINT('Ctrl Pts',(-2.71611381205453,-0.39113535708353,
8.78639403366322));
#398050=CARTESIAN_POINT('Ctrl Pts',(-2.71667000517196,-0.383059917470429,
8.78812224174741));
#398051=CARTESIAN_POINT('Ctrl Pts',(-2.69942159280191,-0.396989573000167,
8.78944554828685));
#398052=CARTESIAN_POINT('Ctrl Pts',(-2.70467629853093,-0.395160779595081,
8.79673892988686));
#398053=CARTESIAN_POINT('Ctrl Pts',(-2.70334794704577,-0.38634380524735,
8.79894799272499));
#398054=CARTESIAN_POINT('Origin',(-2.71104609143371,-0.379651603607865,
8.75721825406948));
#398055=CARTESIAN_POINT('Origin',(-2.71104609143371,-0.379651603607865,
9.));
#398056=CARTESIAN_POINT('Origin',(-2.71104609143371,-0.379651603607865,
7.51860402984325));
#398057=CARTESIAN_POINT('Ctrl Pts',(-2.71710209070084,-0.399660985282277,
7.50366195182966));
#398058=CARTESIAN_POINT('Ctrl Pts',(-2.72072505953656,-0.400193891020071,
7.50000065167735));
#398059=CARTESIAN_POINT('Ctrl Pts',(-2.72072505953658,-0.400193891019955,
7.49482233047108));
#398060=CARTESIAN_POINT('Ctrl Pts',(-2.71965064636477,-0.392671088027347,
7.50215800491338));
#398061=CARTESIAN_POINT('Ctrl Pts',(-2.72211237908244,-0.390762012543981,
7.49877273257264));
#398062=CARTESIAN_POINT('Ctrl Pts',(-2.72261477294344,-0.387346641882056,
7.49481816995647));
#398063=CARTESIAN_POINT('Ctrl Pts',(-2.71785182623255,-0.390509083754931,
7.51043025814042));
#398064=CARTESIAN_POINT('Ctrl Pts',(-2.72261960393336,-0.387138467671442,
7.51006209594516));
#398065=CARTESIAN_POINT('Ctrl Pts',(-2.72342564846379,-0.381382665175063,
7.50731281821701));
#398066=CARTESIAN_POINT('Ctrl Pts',(-2.7151913081126,-0.391444278397112,
7.51860402984326));
#398067=CARTESIAN_POINT('Ctrl Pts',(-2.72237000153422,-0.388920911965344,
7.51860402984326));
#398068=CARTESIAN_POINT('Ctrl Pts',(-2.72342529733067,-0.381385172574106,
7.51860402984327));
#398069=CARTESIAN_POINT('Origin',(0.,0.,7.5));
#398070=CARTESIAN_POINT('Origin',(-2.60220974632391,-0.587743532225626,
7.5));
#398071=CARTESIAN_POINT('',(-2.60220974632391,-0.587743532225626,7.59394543036555));
#398072=CARTESIAN_POINT('',(-2.60220974632391,-0.587743532225626,8.85049129520029));
#398073=CARTESIAN_POINT('',(-2.60220974632391,-0.587743532225626,7.5));
#398074=CARTESIAN_POINT('',(-2.67103479566853,-0.568397127400952,8.78727029226991));
#398075=CARTESIAN_POINT('Ctrl Pts',(-2.60220974632391,-0.587743532225626,
8.85049129520029));
#398076=CARTESIAN_POINT('Ctrl Pts',(-2.62518477739697,-0.581285356659731,
8.82945686509571));
#398077=CARTESIAN_POINT('Ctrl Pts',(-2.64812565330825,-0.574836781952725,
8.80838212259896));
#398078=CARTESIAN_POINT('Ctrl Pts',(-2.67103479566853,-0.568397127400952,
8.78727029226991));
#398079=CARTESIAN_POINT('',(-2.68453419038077,-0.564602509634922,8.75721825406948));
#398080=CARTESIAN_POINT('Origin',(-2.64390988332796,-0.576022025128176,
8.75937679713109));
#398081=CARTESIAN_POINT('',(-2.68453419038077,-0.564602509634922,7.51860402984325));
#398082=CARTESIAN_POINT('',(-2.68453419038077,-0.564602509634922,7.5));
#398083=CARTESIAN_POINT('Ctrl Pts',(-2.68453419038077,-0.564602509634922,
7.51860402984325));
#398084=CARTESIAN_POINT('Ctrl Pts',(-2.67393251538731,-0.567582591715445,
7.52834476460825));
#398085=CARTESIAN_POINT('Ctrl Pts',(-2.66332395793944,-0.570564608422258,
7.53807742314407));
#398086=CARTESIAN_POINT('Ctrl Pts',(-2.65270828694958,-0.573548624713003,
7.54780169004674));
#398087=CARTESIAN_POINT('Ctrl Pts',(-2.63589363782969,-0.578275145245223,
7.5632044032688));
#398088=CARTESIAN_POINT('Ctrl Pts',(-2.61906112037001,-0.583006688485557,
7.57858609112103));
#398089=CARTESIAN_POINT('Ctrl Pts',(-2.60220974632391,-0.587743532225626,
7.59394543036555));
#398090=CARTESIAN_POINT('Origin',(-2.80575616266556,-0.781431603558352,
7.5));
#398091=CARTESIAN_POINT('',(-2.66365357834825,-0.656086448390715,8.75721825406948));
#398092=CARTESIAN_POINT('',(-2.65313746692184,-0.646810448064364,8.78727029226991));
#398093=CARTESIAN_POINT('Origin',(-2.62644365380542,-0.623264499458519,
8.75658640620935));
#398094=CARTESIAN_POINT('',(-2.5995223305943,-0.599517869856899,8.85049129520029));
#398095=CARTESIAN_POINT('Ctrl Pts',(-2.65313746692184,-0.646810448064364,
8.78727029226991));
#398096=CARTESIAN_POINT('Ctrl Pts',(-2.63529110426043,-0.631068615445907,
8.80838212259895));
#398097=CARTESIAN_POINT('Ctrl Pts',(-2.61742002096782,-0.615304977373541,
8.82945686509571));
#398098=CARTESIAN_POINT('Ctrl Pts',(-2.5995223305943,-0.599517869856899,
8.85049129520029));
#398099=CARTESIAN_POINT('',(-2.5995223305943,-0.599517869856899,7.59394543036555));
#398100=CARTESIAN_POINT('',(-2.5995223305943,-0.599517869856899,7.5));
#398101=CARTESIAN_POINT('',(-2.66365357834825,-0.656086448390715,7.51860402984325));
#398102=CARTESIAN_POINT('Ctrl Pts',(-2.5995223305943,-0.599517869856899,
7.59394543036555));
#398103=CARTESIAN_POINT('Ctrl Pts',(-2.61264965451767,-0.611097155779211,
7.57858609112103));
#398104=CARTESIAN_POINT('Ctrl Pts',(-2.62576228904419,-0.622663484549916,
7.56320440326857));
#398105=CARTESIAN_POINT('Ctrl Pts',(-2.63886100402437,-0.634217535235031,
7.54780169004651));
#398106=CARTESIAN_POINT('Ctrl Pts',(-2.64713067695232,-0.641512008036632,
7.53807742314383));
#398107=CARTESIAN_POINT('Ctrl Pts',(-2.6553948083875,-0.648801592825299,
7.52834476460825));
#398108=CARTESIAN_POINT('Ctrl Pts',(-2.66365357834825,-0.656086448390714,
7.51860402984325));
#398109=CARTESIAN_POINT('',(-2.66365357834825,-0.656086448390715,7.5));
#398110=CARTESIAN_POINT('Origin',(-2.60407017393684,-0.594362024055118,
7.5));
#398111=CARTESIAN_POINT('Ctrl Pts',(-2.5995223305943,-0.599517869856899,
8.85049129520029));
#398112=CARTESIAN_POINT('Ctrl Pts',(-2.5993770958507,-0.599389761901934,
8.85097269580138));
#398113=CARTESIAN_POINT('Ctrl Pts',(-2.59923925769927,-0.599256962201082,
8.85143669361005));
#398114=CARTESIAN_POINT('Ctrl Pts',(-2.59910307573752,-0.59911272614392,
8.8519052845931));
#398115=CARTESIAN_POINT('Ctrl Pts',(-2.59883671245669,-0.59883060956323,
8.85282181883899));
#398116=CARTESIAN_POINT('Ctrl Pts',(-2.59858368043392,-0.598511863228085,
8.85372622499635));
#398117=CARTESIAN_POINT('Ctrl Pts',(-2.59835208540563,-0.598141898916052,
8.8546225773507));
#398118=CARTESIAN_POINT('Ctrl Pts',(-2.59815982343862,-0.59783476768409,
8.85536669723986));
#398119=CARTESIAN_POINT('Ctrl Pts',(-2.59798226464241,-0.597492285139542,
8.85610498449051));
#398120=CARTESIAN_POINT('Ctrl Pts',(-2.59783113602522,-0.597102392478157,
8.85681338218371));
#398121=CARTESIAN_POINT('Ctrl Pts',(-2.59769398656777,-0.596748564275613,
8.85745625420284));
#398122=CARTESIAN_POINT('Ctrl Pts',(-2.5975763254901,-0.596351468932853,
8.85808743050666));
#398123=CARTESIAN_POINT('Ctrl Pts',(-2.59749937853405,-0.595891941011372,
8.8586680450841));
#398124=CARTESIAN_POINT('Ctrl Pts',(-2.59746387687653,-0.595679924789745,
8.85893592806395));
#398125=CARTESIAN_POINT('Ctrl Pts',(-2.59743724001534,-0.59545447874692,
8.85919241173848));
#398126=CARTESIAN_POINT('Ctrl Pts',(-2.5974229722392,-0.595212990999087,
8.85943017985534));
#398127=CARTESIAN_POINT('Ctrl Pts',(-2.59740370651771,-0.594886911051487,
8.8597512372));
#398128=CARTESIAN_POINT('Ctrl Pts',(-2.59740714241511,-0.594523244909332,
8.86004599534706));
#398129=CARTESIAN_POINT('Ctrl Pts',(-2.59744365327854,-0.594126460281404,
8.86026130871721));
#398130=CARTESIAN_POINT('Ctrl Pts',(-2.597457020935,-0.593981186242577,
8.86034014101235));
#398131=CARTESIAN_POINT('Ctrl Pts',(-2.59747501080947,-0.593829289371754,
8.86040910639693));
#398132=CARTESIAN_POINT('Ctrl Pts',(-2.59749746682199,-0.593674947576356,
8.86046313645507));
#398133=CARTESIAN_POINT('Ctrl Pts',(-2.59753250924147,-0.593434098497239,
8.8605474499083));
#398134=CARTESIAN_POINT('Ctrl Pts',(-2.59757952936704,-0.593180742414873,
8.86059655985668));
#398135=CARTESIAN_POINT('Ctrl Pts',(-2.59763522361598,-0.592931074369255,
8.86059725258816));
#398136=CARTESIAN_POINT('Ctrl Pts',(-2.59769104654089,-0.592680829490709,
8.86059794692011));
#398137=CARTESIAN_POINT('Ctrl Pts',(-2.5977587958359,-0.592432092904097,
8.86056369958366));
#398138=CARTESIAN_POINT('Ctrl Pts',(-2.59783114559449,-0.592197441881922,
8.86048590497774));
#398139=CARTESIAN_POINT('Ctrl Pts',(-2.59785002672736,-0.592136204951537,
8.86046560290182));
#398140=CARTESIAN_POINT('Ctrl Pts',(-2.59786955336763,-0.592075157355788,
8.86044257503091));
#398141=CARTESIAN_POINT('Ctrl Pts',(-2.59788909086022,-0.592016175515294,
8.86041778462583));
#398142=CARTESIAN_POINT('Ctrl Pts',(-2.59802055394132,-0.591619300919128,
8.860250975962));
#398143=CARTESIAN_POINT('Ctrl Pts',(-2.5981704640267,-0.591262804918427,
8.8599848982295));
#398144=CARTESIAN_POINT('Ctrl Pts',(-2.5983266355742,-0.590953808487247,
8.85968173251462));
#398145=CARTESIAN_POINT('Ctrl Pts',(-2.59840924137526,-0.590790367078537,
8.85952137522077));
#398146=CARTESIAN_POINT('Ctrl Pts',(-2.59849502086838,-0.590636978528642,
8.85934740853961));
#398147=CARTESIAN_POINT('Ctrl Pts',(-2.59858140757177,-0.590495047191055,
8.8591675900182));
#398148=CARTESIAN_POINT('Ctrl Pts',(-2.59892829508878,-0.589925119096205,
8.85844552518695));
#398149=CARTESIAN_POINT('Ctrl Pts',(-2.59930199401607,-0.589506147419861,
8.85759444184125));
#398150=CARTESIAN_POINT('Ctrl Pts',(-2.59963737144715,-0.589191908284434,
8.8568349891514));
#398151=CARTESIAN_POINT('Ctrl Pts',(-2.59967246780213,-0.589159023995797,
8.85675551444999));
#398152=CARTESIAN_POINT('Ctrl Pts',(-2.59970715503214,-0.589127303602779,
8.85667699793652));
#398153=CARTESIAN_POINT('Ctrl Pts',(-2.59974136484002,-0.589096705632551,
8.85659965593547));
#398154=CARTESIAN_POINT('Ctrl Pts',(-2.6002031305724,-0.588683692669106,
8.85555568965886));
#398155=CARTESIAN_POINT('Ctrl Pts',(-2.60070656329426,-0.588353449731737,
8.85434650606346));
#398156=CARTESIAN_POINT('Ctrl Pts',(-2.60125074290954,-0.588099147829275,
8.85297329937117));
#398157=CARTESIAN_POINT('Ctrl Pts',(-2.60155681078578,-0.587956118503982,
8.85220095427747));
#398158=CARTESIAN_POINT('Ctrl Pts',(-2.60187602688498,-0.587837339225038,
8.85137579139183));
#398159=CARTESIAN_POINT('Ctrl Pts',(-2.60220974632391,-0.587743532225626,
8.85049129520029));
#398160=CARTESIAN_POINT('Origin',(-2.60407017393684,-0.594362024055118,
7.59394543036555));
#398161=CARTESIAN_POINT('Ctrl Pts',(-2.59910066513916,-0.599145929246824,
7.59443877723642));
#398162=CARTESIAN_POINT('Ctrl Pts',(-2.59475791666676,-0.595315298834709,
7.58783886950016));
#398163=CARTESIAN_POINT('Ctrl Pts',(-2.59874842803424,-0.587821634806831,
7.58559994247159));
#398164=CARTESIAN_POINT('Ctrl Pts',(-2.62280760163912,-0.620057228280637,
7.56670252222134));
#398165=CARTESIAN_POINT('Ctrl Pts',(-2.61847112967122,-0.616232134217014,
7.56004874999029));
#398166=CARTESIAN_POINT('Ctrl Pts',(-2.62246642784951,-0.608684025200632,
7.55786368756704));
#398167=CARTESIAN_POINT('Ctrl Pts',(-2.6464702678038,-0.640929477552819,
7.5388891333356));
#398168=CARTESIAN_POINT('Ctrl Pts',(-2.64210802397066,-0.637081650767868,
7.53222002137279));
#398169=CARTESIAN_POINT('Ctrl Pts',(-2.64614020663337,-0.629509072099121,
7.53005029815327));
#398170=CARTESIAN_POINT('Ctrl Pts',(-2.6700875928815,-0.661761732579921,
7.51101258149734));
#398171=CARTESIAN_POINT('Ctrl Pts',(-2.6656724707267,-0.657867263142676,
7.5043616886572));
#398172=CARTESIAN_POINT('Ctrl Pts',(-2.66976864930637,-0.650295684536589,
7.50217374673251));
#398173=CARTESIAN_POINT('',(-2.66850780457431,-0.649186484966748,7.50366116523517));
#398174=CARTESIAN_POINT('Ctrl Pts',(-2.66365357834825,-0.656086448390716,
7.51860402984325));
#398175=CARTESIAN_POINT('Ctrl Pts',(-2.66398476079657,-0.656378576191014,
7.51734760759493));
#398176=CARTESIAN_POINT('Ctrl Pts',(-2.66432338889996,-0.656597936323138,
7.51608817408572));
#398177=CARTESIAN_POINT('Ctrl Pts',(-2.66467594396583,-0.656732816671555,
7.51481005913119));
#398178=CARTESIAN_POINT('Ctrl Pts',(-2.66499529676907,-0.656854994514222,
7.51365231206383));
#398179=CARTESIAN_POINT('Ctrl Pts',(-2.66532643764435,-0.65690826113668,
7.51247773061042));
#398180=CARTESIAN_POINT('Ctrl Pts',(-2.66566950096493,-0.656855238444881,
7.51129758471022));
#398181=CARTESIAN_POINT('Ctrl Pts',(-2.6660958894931,-0.656789337294395,
7.50983079813402));
#398182=CARTESIAN_POINT('Ctrl Pts',(-2.66652509793794,-0.65654847554682,
7.50839324291155));
#398183=CARTESIAN_POINT('Ctrl Pts',(-2.66691991417319,-0.656059002349277,
7.50715379678855));
#398184=CARTESIAN_POINT('Ctrl Pts',(-2.66710230789752,-0.655832879835843,
7.50658120839351));
#398185=CARTESIAN_POINT('Ctrl Pts',(-2.66729589496989,-0.655515588495294,
7.50598221009429));
#398186=CARTESIAN_POINT('Ctrl Pts',(-2.66747665060042,-0.655102832213246,
7.50545747549611));
#398187=CARTESIAN_POINT('Ctrl Pts',(-2.66757310739979,-0.654882572685144,
7.50517746087247));
#398188=CARTESIAN_POINT('Ctrl Pts',(-2.66766714172129,-0.654632821201703,
7.50491486231392));
#398189=CARTESIAN_POINT('Ctrl Pts',(-2.66775470234246,-0.654359603855222,
7.50468370960993));
#398190=CARTESIAN_POINT('Ctrl Pts',(-2.66788563309055,-0.653951057740708,
7.50433806340447));
#398191=CARTESIAN_POINT('Ctrl Pts',(-2.66800548484692,-0.653477622060605,
7.50405484070984));
#398192=CARTESIAN_POINT('Ctrl Pts',(-2.66810549133165,-0.652971006016076,
7.50385766036131));
#398193=CARTESIAN_POINT('Ctrl Pts',(-2.66811618547074,-0.652916831304707,
7.50383657498791));
#398194=CARTESIAN_POINT('Ctrl Pts',(-2.66812666210037,-0.652862303928467,
7.50381643264937));
#398195=CARTESIAN_POINT('Ctrl Pts',(-2.66813691764826,-0.652807481989489,
7.50379723213559));
#398196=CARTESIAN_POINT('Ctrl Pts',(-2.66820537678524,-0.652441527613323,
7.50366906242519));
#398197=CARTESIAN_POINT('Ctrl Pts',(-2.66826476687681,-0.652054354948022,
7.50358235568538));
#398198=CARTESIAN_POINT('Ctrl Pts',(-2.6683130409734,-0.651679792103584,
7.5035341175365));
#398199=CARTESIAN_POINT('Ctrl Pts',(-2.66838542251768,-0.651118177510677,
7.50346178989176));
#398200=CARTESIAN_POINT('Ctrl Pts',(-2.6684394093849,-0.650510930430115,
7.50346967198527));
#398201=CARTESIAN_POINT('Ctrl Pts',(-2.66847406487117,-0.649913171174624,
7.50354272648692));
#398202=CARTESIAN_POINT('Ctrl Pts',(-2.66848831939001,-0.649667300419956,
7.50357277531559));
#398203=CARTESIAN_POINT('Ctrl Pts',(-2.66849942595432,-0.649423369748904,
7.50361331098761));
#398204=CARTESIAN_POINT('Ctrl Pts',(-2.66850780457568,-0.649186484967083,
7.50366116523659));
#398205=CARTESIAN_POINT('',(-2.60692468992218,-0.595013548701113,7.57603338622103));
#398206=CARTESIAN_POINT('Origin',(-2.61554070278267,-0.596977170861205,
7.58486873427627));
#398207=CARTESIAN_POINT('Ctrl Pts',(-2.66850780461363,-0.649186485008482,
7.50366116529969));
#398208=CARTESIAN_POINT('Ctrl Pts',(-2.64801414877486,-0.631157678360157,
7.52783573079709));
#398209=CARTESIAN_POINT('Ctrl Pts',(-2.62748742494612,-0.613100872076757,
7.55196141284068));
#398210=CARTESIAN_POINT('Ctrl Pts',(-2.60692469059042,-0.595013549759931,
7.57603338728831));
#398211=CARTESIAN_POINT('Ctrl Pts',(-2.60040987984642,-0.600066314790606,
7.59639677331371));
#398212=CARTESIAN_POINT('Ctrl Pts',(-2.58423804501347,-0.589835470045179,
7.59974925422226));
#398213=CARTESIAN_POINT('Ctrl Pts',(-2.60324736190728,-0.587634493602762,
7.59639677331372));
#398214=CARTESIAN_POINT('Ctrl Pts',(-2.59682114589539,-0.598537886606972,
7.58707626057422));
#398215=CARTESIAN_POINT('Ctrl Pts',(-2.59428415960393,-0.592128430143379,
7.58811717123965));
#398216=CARTESIAN_POINT('Ctrl Pts',(-2.59935086420695,-0.587454466507708,
7.58707626057423));
#398217=CARTESIAN_POINT('Ctrl Pts',(-2.60242843340217,-0.596196101160362,
7.5801537675693));
#398218=CARTESIAN_POINT('Ctrl Pts',(-2.60102225854766,-0.593666357257013,
7.58208760766041));
#398219=CARTESIAN_POINT('Ctrl Pts',(-2.60338679305818,-0.591997253160099,
7.5801537675693));
#398220=CARTESIAN_POINT('Ctrl Pts',(-2.60692468911532,-0.59501354851716,
7.57603338509286));
#398221=CARTESIAN_POINT('Ctrl Pts',(-2.60692468911532,-0.59501354851716,
7.57603338509286));
#398222=CARTESIAN_POINT('Ctrl Pts',(-2.60692468911532,-0.59501354851716,
7.57603338509286));
#398223=CARTESIAN_POINT('Origin',(-2.61553943300043,-0.596982734143423,
7.58486873427623));
#398224=CARTESIAN_POINT('Ctrl Pts',(-2.69281955470071,-0.562273531831347,
7.51098857897448));
#398225=CARTESIAN_POINT('Ctrl Pts',(-2.68715189428301,-0.563866685107569,
7.50433767179956));
#398226=CARTESIAN_POINT('Ctrl Pts',(-2.68755725624421,-0.572465739285958,
7.50214974420965));
#398227=CARTESIAN_POINT('Ctrl Pts',(-2.66249358333605,-0.570798022904131,
7.53887321589169));
#398228=CARTESIAN_POINT('Ctrl Pts',(-2.65689383154844,-0.572372087376776,
7.53220407452063));
#398229=CARTESIAN_POINT('Ctrl Pts',(-2.65724107428411,-0.580944271602769,
7.53003438070911));
#398230=CARTESIAN_POINT('Ctrl Pts',(-2.63210937491957,-0.579338884144335,
7.56669465659233));
#398231=CARTESIAN_POINT('Ctrl Pts',(-2.62654271662394,-0.580903646188561,
7.56004085833301));
#398232=CARTESIAN_POINT('Ctrl Pts',(-2.62686733688466,-0.589437770151378,
7.55785582193789));
#398233=CARTESIAN_POINT('Ctrl Pts',(-2.60166830360742,-0.587895729282982,
7.59443891967696));
#398234=CARTESIAN_POINT('Ctrl Pts',(-2.59609357435033,-0.589462760037375,
7.58783901202978));
#398235=CARTESIAN_POINT('Ctrl Pts',(-2.59643752178507,-0.597945735821288,
7.58560008491213));
#398236=CARTESIAN_POINT('',(-2.68591391515804,-0.572925331695067,7.50366116523517));
#398237=CARTESIAN_POINT('Ctrl Pts',(-2.6859139151584,-0.572925331695144,
7.50366116523554));
#398238=CARTESIAN_POINT('Ctrl Pts',(-2.68621818329533,-0.572231387592487,
7.50350835821027));
#398239=CARTESIAN_POINT('Ctrl Pts',(-2.68647530281419,-0.571583585489863,
7.50345484956));
#398240=CARTESIAN_POINT('Ctrl Pts',(-2.68669347623158,-0.57096288723763,
7.50349758195598));
#398241=CARTESIAN_POINT('Ctrl Pts',(-2.68680541537486,-0.570644423002052,
7.50351950684424));
#398242=CARTESIAN_POINT('Ctrl Pts',(-2.68691825744058,-0.570301747530871,
7.50357029184312));
#398243=CARTESIAN_POINT('Ctrl Pts',(-2.68701798666394,-0.569968318478606,
7.50365515313924));
#398244=CARTESIAN_POINT('Ctrl Pts',(-2.68717141059382,-0.569455369577467,
7.50378570417639));
#398245=CARTESIAN_POINT('Ctrl Pts',(-2.68729863666788,-0.568949346450679,
7.50400001621911));
#398246=CARTESIAN_POINT('Ctrl Pts',(-2.68738777924756,-0.568488211200666,
7.50428903009634));
#398247=CARTESIAN_POINT('Ctrl Pts',(-2.68739767338809,-0.568437028735674,
7.50432110841318));
#398248=CARTESIAN_POINT('Ctrl Pts',(-2.68740711999939,-0.568386378019446,
7.50435406373354));
#398249=CARTESIAN_POINT('Ctrl Pts',(-2.68741611858358,-0.568336295066315,
7.50438785222352));
#398250=CARTESIAN_POINT('Ctrl Pts',(-2.68747105926538,-0.568030514564526,
7.50459414719561));
#398251=CARTESIAN_POINT('Ctrl Pts',(-2.68750966597882,-0.567740938964522,
7.50483629897752));
#398252=CARTESIAN_POINT('Ctrl Pts',(-2.6875317642012,-0.567478835738966,
7.5050991045531));
#398253=CARTESIAN_POINT('Ctrl Pts',(-2.68758051509931,-0.566900609697613,
7.50567888004914));
#398254=CARTESIAN_POINT('Ctrl Pts',(-2.68755136067167,-0.566433346682581,
7.50637912803144));
#398255=CARTESIAN_POINT('Ctrl Pts',(-2.6874735784089,-0.566067134736547,
7.50710440483569));
#398256=CARTESIAN_POINT('Ctrl Pts',(-2.68745450465388,-0.565977332297053,
7.50728225710685));
#398257=CARTESIAN_POINT('Ctrl Pts',(-2.68743226983593,-0.565891788322835,
7.50746498566954));
#398258=CARTESIAN_POINT('Ctrl Pts',(-2.68740779618353,-0.565812394887358,
7.50764697238949));
#398259=CARTESIAN_POINT('Ctrl Pts',(-2.68727623256355,-0.565385597627898,
7.50862528291182));
#398260=CARTESIAN_POINT('Ctrl Pts',(-2.68707198248926,-0.565096578290538,
7.50965856837422));
#398261=CARTESIAN_POINT('Ctrl Pts',(-2.68683691530922,-0.564893933047656,
7.51067959873202));
#398262=CARTESIAN_POINT('Ctrl Pts',(-2.68670755754355,-0.564782417114894,
7.51124147302579));
#398263=CARTESIAN_POINT('Ctrl Pts',(-2.68656855217612,-0.564697359785934,
7.51180065547253));
#398264=CARTESIAN_POINT('Ctrl Pts',(-2.68642517955058,-0.564632315171672,
7.51235175716501));
#398265=CARTESIAN_POINT('Ctrl Pts',(-2.68592977001649,-0.564407560118699,
7.51425603304536));
#398266=CARTESIAN_POINT('Ctrl Pts',(-2.68532064255679,-0.564400477358213,
7.5162690050518));
#398267=CARTESIAN_POINT('Ctrl Pts',(-2.68464456211953,-0.564572913161334,
7.51827788969244));
#398268=CARTESIAN_POINT('Ctrl Pts',(-2.68460797136865,-0.564582245712857,
7.51838661432545));
#398269=CARTESIAN_POINT('Ctrl Pts',(-2.68457117888686,-0.564592112335976,
7.51849533314857));
#398270=CARTESIAN_POINT('Ctrl Pts',(-2.68453419038077,-0.564602509634918,
7.51860402984325));
#398271=CARTESIAN_POINT('Ctrl Pts',(-2.60692469098487,-0.595013548037117,
7.57603338728985));
#398272=CARTESIAN_POINT('Ctrl Pts',(-2.63329886952168,-0.587639269793053,
7.55196141284922));
#398273=CARTESIAN_POINT('Ctrl Pts',(-2.65962736329994,-0.580276861158725,
7.52783573083105));
#398274=CARTESIAN_POINT('Ctrl Pts',(-2.68591391521332,-0.572925331673961,
7.50366116530176));
#398275=CARTESIAN_POINT('Origin',(-9.00812987045923E-16,-2.05604685939134E-16,
7.49482233047033));
#398276=CARTESIAN_POINT('Origin',(-2.65991946170316,-0.64709713896197,7.49482233047033));
#398277=CARTESIAN_POINT('Origin',(0.,0.,7.50366116523517));
#398278=CARTESIAN_POINT('Origin',(-2.6772695523474,-0.571081425081893,7.49482233047033));
#398279=CARTESIAN_POINT('Ctrl Pts',(-2.66365278509063,-0.656085748737571,
7.51860402984325));
#398280=CARTESIAN_POINT('Ctrl Pts',(-2.66935948430929,-0.661118627641122,
7.51860402984325));
#398281=CARTESIAN_POINT('Ctrl Pts',(-2.66750981689315,-0.668499346879772,
7.51860402984325));
#398282=CARTESIAN_POINT('Ctrl Pts',(-2.66577172061455,-0.657954491973657,
7.51041458714366));
#398283=CARTESIAN_POINT('Ctrl Pts',(-2.66892126731013,-0.662867202159749,
7.51004642900442));
#398284=CARTESIAN_POINT('Ctrl Pts',(-2.66750930677684,-0.668501382394503,
7.5072913648301));
#398285=CARTESIAN_POINT('Ctrl Pts',(-2.66824761341794,-0.656615204093706,
7.50215815450137));
#398286=CARTESIAN_POINT('Ctrl Pts',(-2.66981365703397,-0.659306964089347,
7.49877163671531));
#398287=CARTESIAN_POINT('Ctrl Pts',(-2.66899810433398,-0.662659395652838,
7.4948158853317));
#398288=CARTESIAN_POINT('Ctrl Pts',(-2.66850726965803,-0.649186354833451,
7.50366171572174));
#398289=CARTESIAN_POINT('Ctrl Pts',(-2.67206521266994,-0.650051920418041,
7.50000045605858));
#398290=CARTESIAN_POINT('Ctrl Pts',(-2.67206521266991,-0.650051920418163,
7.49482233047317));
#398291=CARTESIAN_POINT('Origin',(-2.65538477227091,-0.665460713484864,
7.51860402984325));
#398292=CARTESIAN_POINT('Origin',(-2.65538477227091,-0.665460713484864,
9.));
#398293=CARTESIAN_POINT('Origin',(-2.65538477227091,-0.665460713484863,
8.75721825406948));
#398294=CARTESIAN_POINT('Ctrl Pts',(-2.65112941937648,-0.645039239553588,
8.78942910404912));
#398295=CARTESIAN_POINT('Ctrl Pts',(-2.65532178526109,-0.648710274420128,
8.79672699501691));
#398296=CARTESIAN_POINT('Ctrl Pts',(-2.65077470762198,-0.656391262047123,
8.79893251111267));
#398297=CARTESIAN_POINT('Ctrl Pts',(-2.65937452780626,-0.652312038582979,
8.78111911759582));
#398298=CARTESIAN_POINT('Ctrl Pts',(-2.6643397222864,-0.656669693215895,
8.78644465894812));
#398299=CARTESIAN_POINT('Ctrl Pts',(-2.66180227631762,-0.664368841203243,
8.78817647674132));
#398300=CARTESIAN_POINT('Ctrl Pts',(-2.66451307602302,-0.656844620434572,
8.7678092393203));
#398301=CARTESIAN_POINT('Ctrl Pts',(-2.67037091713225,-0.661992477688777,
8.76988516158375));
#398302=CARTESIAN_POINT('Ctrl Pts',(-2.66868335772546,-0.669360552311429,
8.77093053738833));
#398303=CARTESIAN_POINT('Ctrl Pts',(-2.66351112944559,-0.655960829007565,
8.75371302330492));
#398304=CARTESIAN_POINT('Ctrl Pts',(-2.66922570397851,-0.660981769086419,
8.75300828287558));
#398305=CARTESIAN_POINT('Ctrl Pts',(-2.66734099870958,-0.66838733627493,
8.75267964240738));
#398306=CARTESIAN_POINT('Origin',(-2.6448686608445,-0.656184713158512,8.78727029226991));
#398307=CARTESIAN_POINT('Ctrl Pts',(-2.5995223305943,-0.599517869856899,
8.85049129520029));
#398308=CARTESIAN_POINT('Ctrl Pts',(-2.60390169908879,-0.603380801879671,
8.85711686593484));
#398309=CARTESIAN_POINT('Ctrl Pts',(-2.59985800069652,-0.610914012710802,
8.85933012996512));
#398310=CARTESIAN_POINT('Ctrl Pts',(-2.61742004498719,-0.615304998560432,
8.82945683644723));
#398311=CARTESIAN_POINT('Ctrl Pts',(-2.62183576488801,-0.619199995254551,
8.83607469902389));
#398312=CARTESIAN_POINT('Ctrl Pts',(-2.61774715137788,-0.626737586518493,
8.83829567148519));
#398313=CARTESIAN_POINT('Ctrl Pts',(-2.63529108139348,-0.631068595275541,
8.80838214965001));
#398314=CARTESIAN_POINT('Ctrl Pts',(-2.63972422778671,-0.634978963445188,
8.81501364461993));
#398315=CARTESIAN_POINT('Ctrl Pts',(-2.6356096080769,-0.642536656032115,
8.81722098428721));
#398316=CARTESIAN_POINT('Ctrl Pts',(-2.65313746692184,-0.646810448064364,
8.78727029226991));
#398317=CARTESIAN_POINT('Ctrl Pts',(-2.65757134967522,-0.650721465758992,
8.79393457792714));
#398318=CARTESIAN_POINT('Ctrl Pts',(-2.65344741704445,-0.658313079212999,
8.79610912703474));
#398319=CARTESIAN_POINT('Origin',(-2.59125352451696,-0.608892134951047,
8.85049129520029));
#398320=CARTESIAN_POINT('Ctrl Pts',(-2.60220974632391,-0.587743532225626,
8.85049129520029));
#398321=CARTESIAN_POINT('Ctrl Pts',(-2.60783148438851,-0.586163287511648,
8.85711686593484));
#398322=CARTESIAN_POINT('Ctrl Pts',(-2.60745677570886,-0.577621604099153,
8.85933012996512));
#398323=CARTESIAN_POINT('Ctrl Pts',(-2.5972362758088,-0.589141551913008,
8.86332496987232));
#398324=CARTESIAN_POINT('Ctrl Pts',(-2.59853778293458,-0.584707820574939,
8.86648636486737));
#398325=CARTESIAN_POINT('Ctrl Pts',(-2.59354792537494,-0.581549114601394,
8.87206031107457));
#398326=CARTESIAN_POINT('Ctrl Pts',(-2.59562163897866,-0.596077166803026,
8.86341338519876));
#398327=CARTESIAN_POINT('Ctrl Pts',(-2.59483919973077,-0.600644579578075,
8.86654584966058));
#398328=CARTESIAN_POINT('Ctrl Pts',(-2.58894560269753,-0.60126881254509,
8.87215952290715));
#398329=CARTESIAN_POINT('Ctrl Pts',(-2.5995223305943,-0.599517869856899,
8.85049129520029));
#398330=CARTESIAN_POINT('Ctrl Pts',(-2.60390169908879,-0.603380801879671,
8.85711686593484));
#398331=CARTESIAN_POINT('Ctrl Pts',(-2.59985800069652,-0.610914012710802,
8.85933012996512));
#398332=CARTESIAN_POINT('Origin',(-2.59882715066403,-0.575709910717461,
8.85049129520029));
#398333=CARTESIAN_POINT('Ctrl Pts',(-2.67103479566853,-0.568397127400952,
8.78727029226991));
#398334=CARTESIAN_POINT('Ctrl Pts',(-2.67672651297436,-0.566797211844121,
8.79393457792714));
#398335=CARTESIAN_POINT('Ctrl Pts',(-2.67630485569206,-0.558168097155203,
8.79610912703474));
#398336=CARTESIAN_POINT('Ctrl Pts',(-2.64812562395424,-0.574836790204001,
8.80838214965003));
#398337=CARTESIAN_POINT('Ctrl Pts',(-2.65381639600413,-0.573237140354252,
8.81501364461989));
#398338=CARTESIAN_POINT('Ctrl Pts',(-2.65338841166108,-0.564642628035495,
8.81722098428721));
#398339=CARTESIAN_POINT('Ctrl Pts',(-2.62518480823033,-0.581285347992617,
8.82945683644723));
#398340=CARTESIAN_POINT('Ctrl Pts',(-2.63085321011983,-0.57969198629208,
8.8360746990239));
#398341=CARTESIAN_POINT('Ctrl Pts',(-2.63043993491585,-0.571126868306709,
8.8382956714852));
#398342=CARTESIAN_POINT('Ctrl Pts',(-2.60220974632391,-0.587743532225626,
8.85049129520029));
#398343=CARTESIAN_POINT('Ctrl Pts',(-2.60783148438851,-0.586163287511648,
8.85711686593484));
#398344=CARTESIAN_POINT('Ctrl Pts',(-2.60745677570886,-0.577621604099153,
8.85933012996512));
#398345=CARTESIAN_POINT('Origin',(-2.66765220000865,-0.556363505892786,
8.78727029226991));
#398346=CARTESIAN_POINT('Ctrl Pts',(-2.68435593267242,-0.564652597894868,
8.75374538247847));
#398347=CARTESIAN_POINT('Ctrl Pts',(-2.69167492525667,-0.5626088939194,
8.75304829418601));
#398348=CARTESIAN_POINT('Ctrl Pts',(-2.69319395121606,-0.55512803812987,
8.75272238421917));
#398349=CARTESIAN_POINT('Ctrl Pts',(-2.68562666750749,-0.564295400620303,
8.76769408445023));
#398350=CARTESIAN_POINT('Ctrl Pts',(-2.69312965281887,-0.56219960330441,
8.76974318093973));
#398351=CARTESIAN_POINT('Ctrl Pts',(-2.69480757528628,-0.554837339150378,
8.7707786988043));
#398352=CARTESIAN_POINT('Ctrl Pts',(-2.6791136046367,-0.566126190382126,
8.78108014887986));
#398353=CARTESIAN_POINT('Ctrl Pts',(-2.6854731365548,-0.56435373697426,
8.78639403366319));
#398354=CARTESIAN_POINT('Ctrl Pts',(-2.68654558210626,-0.556330524633315,
8.78812224174741));
#398355=CARTESIAN_POINT('Ctrl Pts',(-2.66844013235527,-0.569126450616946,
8.78944554828686));
#398356=CARTESIAN_POINT('Ctrl Pts',(-2.67380121292356,-0.56763808481604,
8.79673892988687));
#398357=CARTESIAN_POINT('Ctrl Pts',(-2.67304049616502,-0.558754118115857,
8.79894799272499));
#398358=CARTESIAN_POINT('Origin',(-2.68115159472089,-0.552568888126756,
8.75721825406948));
#398359=CARTESIAN_POINT('Origin',(-2.68115159472089,-0.552568888126756,
9.));
#398360=CARTESIAN_POINT('Origin',(-2.68115159472089,-0.552568888126756,
7.51860402984325));
#398361=CARTESIAN_POINT('Ctrl Pts',(-2.68591314580246,-0.572925167585766,
7.50366195182966));
#398362=CARTESIAN_POINT('Ctrl Pts',(-2.6894945274723,-0.573689102821856,
7.50000065167735));
#398363=CARTESIAN_POINT('Ctrl Pts',(-2.68949452747233,-0.573689102821742,
7.49482233047108));
#398364=CARTESIAN_POINT('Ctrl Pts',(-2.68890430944023,-0.566112918346439,
7.50215800491337));
#398365=CARTESIAN_POINT('Ctrl Pts',(-2.69148329915019,-0.564365489020161,
7.49877273257265));
#398366=CARTESIAN_POINT('Ctrl Pts',(-2.69220348433874,-0.560989324088742,
7.49481816995647));
#398367=CARTESIAN_POINT('Ctrl Pts',(-2.68724770526621,-0.563840105342091,
7.51043025814043));
#398368=CARTESIAN_POINT('Ctrl Pts',(-2.69222164317036,-0.560781887116949,
7.51006209594516));
#398369=CARTESIAN_POINT('Ctrl Pts',(-2.69339480712794,-0.555089553984483,
7.50731281821701));
#398370=CARTESIAN_POINT('Ctrl Pts',(-2.68453273533963,-0.564602918545373,
7.51860402984326));
#398371=CARTESIAN_POINT('Ctrl Pts',(-2.69185835200809,-0.562544677107268,
7.51860402984327));
#398372=CARTESIAN_POINT('Ctrl Pts',(-2.69339429606665,-0.555092033734636,
7.51860402984327));
#398373=CARTESIAN_POINT('Origin',(0.,0.,7.5));
#398374=CARTESIAN_POINT('Origin',(-2.55920636991203,-0.753260100986301,
7.5));
#398375=CARTESIAN_POINT('',(-2.55920636991203,-0.753260100986301,7.59394543036555));
#398376=CARTESIAN_POINT('',(-2.55920636991203,-0.753260100986301,8.85049129520029));
#398377=CARTESIAN_POINT('',(-2.55920636991203,-0.753260100986301,7.5));
#398378=CARTESIAN_POINT('',(-2.62912953922426,-0.738363081476928,8.78727029226991));
#398379=CARTESIAN_POINT('Ctrl Pts',(-2.55920636991203,-0.753260100986301,
8.85049129520029));
#398380=CARTESIAN_POINT('Ctrl Pts',(-2.58254797304887,-0.748287209729658,
8.82945686509571));
#398381=CARTESIAN_POINT('Ctrl Pts',(-2.60585487607022,-0.743321711277182,
8.80838212259895));
#398382=CARTESIAN_POINT('Ctrl Pts',(-2.62912953922426,-0.738363081476928,
8.78727029226991));
#398383=CARTESIAN_POINT('',(-2.64284431997727,-0.735441169348889,8.75721825406948));
#398384=CARTESIAN_POINT('Origin',(-2.60157182905119,-0.744234413933245,
8.75937679713137));
#398385=CARTESIAN_POINT('',(-2.64284431997727,-0.735441169348889,7.51860402984325));
#398386=CARTESIAN_POINT('',(-2.64284431997727,-0.735441169348889,7.5));
#398387=CARTESIAN_POINT('Ctrl Pts',(-2.64284431997727,-0.735441169348889,
7.51860402984325));
#398388=CARTESIAN_POINT('Ctrl Pts',(-2.63207349274766,-0.73773587688217,
7.52834476460825));
#398389=CARTESIAN_POINT('Ctrl Pts',(-2.62129567325243,-0.740032074106476,
7.53807742314407));
#398390=CARTESIAN_POINT('Ctrl Pts',(-2.61051062671697,-0.742329811040153,
7.54780169004674));
#398391=CARTESIAN_POINT('Ctrl Pts',(-2.59342769588683,-0.745969302161013,
7.5632044032688));
#398392=CARTESIAN_POINT('Ctrl Pts',(-2.57632661162329,-0.749612660841833,
7.57858609112103));
#398393=CARTESIAN_POINT('Ctrl Pts',(-2.55920636991203,-0.753260100986301,
7.59394543036555));
#398394=CARTESIAN_POINT('Origin',(-2.7499249409731,-0.959591483074788,7.5));
#398395=CARTESIAN_POINT('',(-2.61614521332082,-0.825399319134631,8.75721825406948));
#398396=CARTESIAN_POINT('',(-2.60624502375464,-0.815468607773367,8.78727029226991));
#398397=CARTESIAN_POINT('Origin',(-2.58111465004912,-0.790260758367852,
8.75658640621046));
#398398=CARTESIAN_POINT('',(-2.5557700913641,-0.764838063661141,8.85049129520029));
#398399=CARTESIAN_POINT('Ctrl Pts',(-2.60624502375464,-0.815468607773367,
8.78727029226991));
#398400=CARTESIAN_POINT('Ctrl Pts',(-2.5894439110381,-0.798615698056765,
8.80838212259896));
#398401=CARTESIAN_POINT('Ctrl Pts',(-2.57261952556177,-0.781739443831607,
8.82945686509571));
#398402=CARTESIAN_POINT('Ctrl Pts',(-2.5557700913641,-0.764838063661142,
8.85049129520029));
#398403=CARTESIAN_POINT('',(-2.5557700913641,-0.764838063661141,7.59394543036555));
#398404=CARTESIAN_POINT('',(-2.5557700913641,-0.764838063661141,7.5));
#398405=CARTESIAN_POINT('',(-2.61614521332082,-0.825399319134631,7.51860402984325));
#398406=CARTESIAN_POINT('Ctrl Pts',(-2.5557700913641,-0.764838063661141,
7.59394543036555));
#398407=CARTESIAN_POINT('Ctrl Pts',(-2.5681285563963,-0.777234629230179,
7.57858609112103));
#398408=CARTESIAN_POINT('Ctrl Pts',(-2.58047319238016,-0.789617323116581,
7.56320440326857));
#398409=CARTESIAN_POINT('Ctrl Pts',(-2.59280472407651,-0.801986872315641,
7.54780169004651));
#398410=CARTESIAN_POINT('Ctrl Pts',(-2.60059004759747,-0.809796197604203,
7.53807742314383));
#398411=CARTESIAN_POINT('Ctrl Pts',(-2.60837015418731,-0.81760028987812,
7.52834476460825));
#398412=CARTESIAN_POINT('Ctrl Pts',(-2.61614521332082,-0.825399319134632,
7.51860402984325));
#398413=CARTESIAN_POINT('',(-2.61614521332082,-0.825399319134631,7.5));
#398414=CARTESIAN_POINT('Origin',(-2.56063892684944,-0.759984192420916,
7.5));
#398415=CARTESIAN_POINT('Ctrl Pts',(-2.5557700913641,-0.764838063661142,
8.85049129520029));
#398416=CARTESIAN_POINT('Ctrl Pts',(-2.55563336292572,-0.764700913695738,
8.85097269580138));
#398417=CARTESIAN_POINT('Ctrl Pts',(-2.55550431648359,-0.76455955552543,
8.85143669361005));
#398418=CARTESIAN_POINT('Ctrl Pts',(-2.5553776555582,-0.76440689060847,
8.8519052845931));
#398419=CARTESIAN_POINT('Ctrl Pts',(-2.55512991482068,-0.764108287712554,
8.85282181883899));
#398420=CARTESIAN_POINT('Ctrl Pts',(-2.55489782482715,-0.76377398445858,
8.85372622499635));
#398421=CARTESIAN_POINT('Ctrl Pts',(-2.55469040933054,-0.763389941933495,
8.8546225773507));
#398422=CARTESIAN_POINT('Ctrl Pts',(-2.55451822035196,-0.763071123469069,
8.85536669723986));
#398423=CARTESIAN_POINT('Ctrl Pts',(-2.55436296930131,-0.762717968360507,
8.85610498449051));
#398424=CARTESIAN_POINT('Ctrl Pts',(-2.55423713170265,-0.762319193931662,
8.85681338218371));
#398425=CARTESIAN_POINT('Ctrl Pts',(-2.55412293388424,-0.761957305511198,
8.85745625420284));
#398426=CARTESIAN_POINT('Ctrl Pts',(-2.55403095653985,-0.761553487472278,
8.85808743050666));
#398427=CARTESIAN_POINT('Ctrl Pts',(-2.55398360973458,-0.761089973691792,
8.85866804508411));
#398428=CARTESIAN_POINT('Ctrl Pts',(-2.55396176494498,-0.760876118481226,
8.85893592806396));
#398429=CARTESIAN_POINT('Ctrl Pts',(-2.55394962718964,-0.76064942901192,
8.85919241173848));
#398430=CARTESIAN_POINT('Ctrl Pts',(-2.55395086090131,-0.76040752328701,
8.85943017985534));
#398431=CARTESIAN_POINT('Ctrl Pts',(-2.55395252677728,-0.76008087894662,
8.8597512372));
#398432=CARTESIAN_POINT('Ctrl Pts',(-2.55397925578498,-0.759718180134259,
8.86004599534706));
#398433=CARTESIAN_POINT('Ctrl Pts',(-2.55404111371133,-0.759324550001956,
8.86026130871721));
#398434=CARTESIAN_POINT('Ctrl Pts',(-2.55406376164213,-0.759180430912912,
8.86034014101235));
#398435=CARTESIAN_POINT('Ctrl Pts',(-2.5540914466204,-0.759029998745715,
8.86040910639692));
#398436=CARTESIAN_POINT('Ctrl Pts',(-2.55412374520742,-0.758877412823752,
8.86046313645506));
#398437=CARTESIAN_POINT('Ctrl Pts',(-2.55417414688197,-0.758639303770424,
8.86054744990829));
#398438=CARTESIAN_POINT('Ctrl Pts',(-2.55423730297958,-0.758389480825089,
8.86059655985669));
#398439=CARTESIAN_POINT('Ctrl Pts',(-2.55430887908532,-0.758143894092029,
8.86059725258816));
#398440=CARTESIAN_POINT('Ctrl Pts',(-2.55438062056046,-0.757897739955503,
8.86059794692011));
#398441=CARTESIAN_POINT('Ctrl Pts',(-2.5544641672651,-0.757653855137121,
8.86056369958366));
#398442=CARTESIAN_POINT('Ctrl Pts',(-2.55455140251595,-0.757424321695584,
8.86048590497774));
#398443=CARTESIAN_POINT('Ctrl Pts',(-2.55457416831912,-0.757364420301377,
8.86046560290182));
#398444=CARTESIAN_POINT('Ctrl Pts',(-2.5545975661727,-0.757304749210599,
8.86044257503091));
#398445=CARTESIAN_POINT('Ctrl Pts',(-2.55462084250291,-0.757247140326069,
8.86041778462583));
#398446=CARTESIAN_POINT('Ctrl Pts',(-2.55477746332169,-0.756859504019852,
8.86025097596201));
#398447=CARTESIAN_POINT('Ctrl Pts',(-2.55494990617791,-0.756513345250565,
8.8599848982295));
#398448=CARTESIAN_POINT('Ctrl Pts',(-2.55512555432353,-0.756214989631096,
8.85968173251461));
#398449=CARTESIAN_POINT('Ctrl Pts',(-2.55521846212913,-0.756057176602136,
8.85952137522076));
#398450=CARTESIAN_POINT('Ctrl Pts',(-2.55531389301721,-0.755909599116461,
8.85934740853961));
#398451=CARTESIAN_POINT('Ctrl Pts',(-2.55540919580188,-0.755773494207119,
8.8591675900182));
#398452=CARTESIAN_POINT('Ctrl Pts',(-2.55579188601969,-0.755226962250188,
8.85844552518695));
#398453=CARTESIAN_POINT('Ctrl Pts',(-2.55619166074993,-0.754832794368564,
8.85759444184125));
#398454=CARTESIAN_POINT('Ctrl Pts',(-2.55654648248264,-0.754540688576929,
8.8568349891514));
#398455=CARTESIAN_POINT('Ctrl Pts',(-2.556583613632,-0.754510120483775,
8.85675551444999));
#398456=CARTESIAN_POINT('Ctrl Pts',(-2.55662026192593,-0.754480687682163,
8.85667699793652));
#398457=CARTESIAN_POINT('Ctrl Pts',(-2.55665636186478,-0.754452344408663,
8.85659965593547));
#398458=CARTESIAN_POINT('Ctrl Pts',(-2.55714364068136,-0.7540697654567,
8.85555568965886));
#398459=CARTESIAN_POINT('Ctrl Pts',(-2.55766719778435,-0.753772456084101,
8.85434650606346));
#398460=CARTESIAN_POINT('Ctrl Pts',(-2.55822655250307,-0.753553542379831,
8.85297329937117));
#398461=CARTESIAN_POINT('Ctrl Pts',(-2.55854115545037,-0.753430416759787,
8.85220095427747));
#398462=CARTESIAN_POINT('Ctrl Pts',(-2.55886732590039,-0.753332333771308,
8.85137579139183));
#398463=CARTESIAN_POINT('Ctrl Pts',(-2.55920636991203,-0.753260100986301,
8.85049129520029));
#398464=CARTESIAN_POINT('Origin',(-2.56063892684944,-0.759984192420916,
7.59394543036555));
#398465=CARTESIAN_POINT('Ctrl Pts',(-2.55537312258256,-0.764439871044471,
7.59443877723642));
#398466=CARTESIAN_POINT('Ctrl Pts',(-2.55128472608583,-0.760338870223424,
7.58783886950016));
#398467=CARTESIAN_POINT('Ctrl Pts',(-2.55574715922245,-0.753116275673134,
7.58559994247159));
#398468=CARTESIAN_POINT('Ctrl Pts',(-2.57769155910977,-0.786827114208337,
7.56670252222139));
#398469=CARTESIAN_POINT('Ctrl Pts',(-2.57360907150671,-0.78273204049773,
7.56004874999028));
#398470=CARTESIAN_POINT('Ctrl Pts',(-2.57807976992149,-0.775455419514081,
7.55786368756704));
#398471=CARTESIAN_POINT('Ctrl Pts',(-2.59996831818662,-0.809172551432327,
7.53888913333561));
#398472=CARTESIAN_POINT('Ctrl Pts',(-2.59586156815991,-0.80505314049819,
7.53222002137285));
#398473=CARTESIAN_POINT('Ctrl Pts',(-2.60037064305195,-0.797754463334659,
7.53005029815327));
#398474=CARTESIAN_POINT('Ctrl Pts',(-2.62220239177471,-0.831475171570302,
7.51101258149734));
#398475=CARTESIAN_POINT('Ctrl Pts',(-2.61804586047546,-0.827305825890497,
7.5043616886572));
#398476=CARTESIAN_POINT('Ctrl Pts',(-2.62261873572381,-0.820012246967386,
7.50217374673251));
#398477=CARTESIAN_POINT('',(-2.62143154819292,-0.818824543767677,7.50366116523517));
#398478=CARTESIAN_POINT('Ctrl Pts',(-2.61614521332082,-0.825399319134632,
7.51860402984325));
#398479=CARTESIAN_POINT('Ctrl Pts',(-2.61645699862685,-0.825712065659352,
7.51734760759493));
#398480=CARTESIAN_POINT('Ctrl Pts',(-2.61678087653058,-0.825952671069635,
7.51608817408572));
#398481=CARTESIAN_POINT('Ctrl Pts',(-2.61712406542065,-0.826109862572535,
7.51481005913119));
#398482=CARTESIAN_POINT('Ctrl Pts',(-2.61743493411805,-0.826252250392075,
7.51365231206383));
#398483=CARTESIAN_POINT('Ctrl Pts',(-2.61776198182467,-0.826326623841268,
7.51247773061042));
#398484=CARTESIAN_POINT('Ctrl Pts',(-2.6181077374604,-0.826295690232693,
7.51129758471022));
#398485=CARTESIAN_POINT('Ctrl Pts',(-2.61853747222882,-0.826257243289985,
7.50983079813402));
#398486=CARTESIAN_POINT('Ctrl Pts',(-2.61898123088402,-0.82604437589818,
7.50839324291155));
#398487=CARTESIAN_POINT('Ctrl Pts',(-2.61940659658241,-0.825581204338862,
7.50715379678855));
#398488=CARTESIAN_POINT('Ctrl Pts',(-2.61960310327845,-0.825367232424425,
7.50658120839351));
#398489=CARTESIAN_POINT('Ctrl Pts',(-2.6198166215314,-0.825062996159276,
7.50598221009429));
#398490=CARTESIAN_POINT('Ctrl Pts',(-2.6200234511659,-0.82466266898229,
7.50545747549612));
#398491=CARTESIAN_POINT('Ctrl Pts',(-2.62013382186085,-0.824449042009365,
7.50517746087247));
#398492=CARTESIAN_POINT('Ctrl Pts',(-2.62024366461123,-0.824205828466795,
7.50491486231392));
#398493=CARTESIAN_POINT('Ctrl Pts',(-2.62034855042521,-0.823938782502916,
7.50468370960993));
#398494=CARTESIAN_POINT('Ctrl Pts',(-2.62050538780146,-0.823539464552042,
7.50433806340447));
#398495=CARTESIAN_POINT('Ctrl Pts',(-2.62065532643771,-0.823074680524712,
7.50405484070984));
#398496=CARTESIAN_POINT('Ctrl Pts',(-2.62078758644981,-0.822575512814655,
7.50385766036131));
#398497=CARTESIAN_POINT('Ctrl Pts',(-2.62080172960232,-0.822522134586887,
7.50383657498791));
#398498=CARTESIAN_POINT('Ctrl Pts',(-2.62081567828759,-0.822468390482957,
7.50381643264937));
#398499=CARTESIAN_POINT('Ctrl Pts',(-2.62082942521804,-0.822414338256744,
7.50379723213559));
#398500=CARTESIAN_POINT('Ctrl Pts',(-2.62092119047576,-0.822053521965059,
7.50366906242519));
#398501=CARTESIAN_POINT('Ctrl Pts',(-2.62100526478186,-0.821670949923754,
7.50358235568538));
#398502=CARTESIAN_POINT('Ctrl Pts',(-2.62107743801799,-0.82130024959084,
7.5035341175365));
#398503=CARTESIAN_POINT('Ctrl Pts',(-2.62118565361712,-0.820744426396813,
7.50346178989177));
#398504=CARTESIAN_POINT('Ctrl Pts',(-2.62127843601657,-0.820141885920964,
7.50346967198527));
#398505=CARTESIAN_POINT('Ctrl Pts',(-2.62135131886643,-0.819547575210604,
7.50354272648693));
#398506=CARTESIAN_POINT('Ctrl Pts',(-2.62138129709116,-0.819303122913928,
7.50357277531559));
#398507=CARTESIAN_POINT('Ctrl Pts',(-2.62140800952761,-0.819060405024619,
7.50361331098761));
#398508=CARTESIAN_POINT('Ctrl Pts',(-2.62143154819427,-0.8188245437681,
7.50366116523659));
#398509=CARTESIAN_POINT('',(-2.56344583459816,-0.760817267906771,7.57603338622103));
#398510=CARTESIAN_POINT('Origin',(-2.57191833523299,-0.763328885433893,
7.58486873427629));
#398511=CARTESIAN_POINT('Ctrl Pts',(-2.62143154822949,-0.818824543811846,
7.50366116529968));
#398512=CARTESIAN_POINT('Ctrl Pts',(-2.60213510841253,-0.799519746242561,
7.52783573079709));
#398513=CARTESIAN_POINT('Ctrl Pts',(-2.58280746249009,-0.780184887893086,
7.55196141284069));
#398514=CARTESIAN_POINT('Ctrl Pts',(-2.56344583519718,-0.760817269006234,
7.57603338728831));
#398515=CARTESIAN_POINT('Ctrl Pts',(-2.55662067806349,-0.765442247231706,
7.59639677331371));
#398516=CARTESIAN_POINT('Ctrl Pts',(-2.54113756247318,-0.754196289838708,
7.59974925422224));
#398517=CARTESIAN_POINT('Ctrl Pts',(-2.5602488397315,-0.753217766653662,
7.59639677331371));
#398518=CARTESIAN_POINT('Ctrl Pts',(-2.55313724428124,-0.76368702839398,
7.58707626057424));
#398519=CARTESIAN_POINT('Ctrl Pts',(-2.55101612578582,-0.757128195576305,
7.58811717123965));
#398520=CARTESIAN_POINT('Ctrl Pts',(-2.55637188217917,-0.752788459978733,
7.58707626057423));
#398521=CARTESIAN_POINT('Ctrl Pts',(-2.55888304972318,-0.761709314540856,
7.58015376756929));
#398522=CARTESIAN_POINT('Ctrl Pts',(-2.55764184525409,-0.759094674335462,
7.5820876076604));
#398523=CARTESIAN_POINT('Ctrl Pts',(-2.56010846144153,-0.757580495838117,
7.58015376756929));
#398524=CARTESIAN_POINT('Ctrl Pts',(-2.56344583380473,-0.760817267671499,
7.57603338509286));
#398525=CARTESIAN_POINT('Ctrl Pts',(-2.56344583380473,-0.760817267671499,
7.57603338509286));
#398526=CARTESIAN_POINT('Ctrl Pts',(-2.56344583380473,-0.760817267671499,
7.57603338509286));
#398527=CARTESIAN_POINT('Origin',(-2.57191671161821,-0.763334355930412,
7.58486873427621));
#398528=CARTESIAN_POINT('Ctrl Pts',(-2.65126187924782,-0.733647821794593,
7.51098857897448));
#398529=CARTESIAN_POINT('Ctrl Pts',(-2.64550378996544,-0.734874573516806,
7.50433767179956));
#398530=CARTESIAN_POINT('Ctrl Pts',(-2.64535737577417,-0.743481931646165,
7.50214974420965));
#398531=CARTESIAN_POINT('Ctrl Pts',(-2.62045204982553,-0.740211806729756,
7.53887321589168));
#398532=CARTESIAN_POINT('Ctrl Pts',(-2.61476295267151,-0.741423859789234,
7.53220407452063));
#398533=CARTESIAN_POINT('Ctrl Pts',(-2.61456026023066,-0.750000679461849,
7.53003438070911));
#398534=CARTESIAN_POINT('Ctrl Pts',(-2.58958305416547,-0.746788396937349,
7.56669465659237));
#398535=CARTESIAN_POINT('Ctrl Pts',(-2.58392757851793,-0.747993286988579,
7.56004085833303));
#398536=CARTESIAN_POINT('Ctrl Pts',(-2.58370474861186,-0.75653067516994,
7.5578558219379));
#398537=CARTESIAN_POINT('Ctrl Pts',(-2.55865628834872,-0.753377294984527,
7.59443891967696));
#398538=CARTESIAN_POINT('Ctrl Pts',(-2.55299261296563,-0.754583931976337,
7.58783901202978));
#398539=CARTESIAN_POINT('Ctrl Pts',(-2.55279234759891,-0.763071515364511,
7.58560008491213));
#398540=CARTESIAN_POINT('',(-2.64368796492175,-0.743835290548484,7.50366116523517));
#398541=CARTESIAN_POINT('Ctrl Pts',(-2.64368796492211,-0.743835290548585,
7.50366116523554));
#398542=CARTESIAN_POINT('Ctrl Pts',(-2.64403606905884,-0.743162266754978,
7.50350835821027));
#398543=CARTESIAN_POINT('Ctrl Pts',(-2.64433416512129,-0.742532269335384,
7.50345484956));
#398544=CARTESIAN_POINT('Ctrl Pts',(-2.64459165855155,-0.741926824793127,
7.50349758195598));
#398545=CARTESIAN_POINT('Ctrl Pts',(-2.64472377177749,-0.74161618684201,
7.50351950684424));
#398546=CARTESIAN_POINT('Ctrl Pts',(-2.6448583372899,-0.74128144525031,
7.50357029184312));
#398547=CARTESIAN_POINT('Ctrl Pts',(-2.6449792244816,-0.740955090937072,
7.50365515313924));
#398548=CARTESIAN_POINT('Ctrl Pts',(-2.64516519793449,-0.7404530258494,
7.50378570417639));
#398549=CARTESIAN_POINT('Ctrl Pts',(-2.64532458362199,-0.739956193803948,
7.50400001621911));
#398550=CARTESIAN_POINT('Ctrl Pts',(-2.64544308808559,-0.739501717390452,
7.50428903009635));
#398551=CARTESIAN_POINT('Ctrl Pts',(-2.64545624116934,-0.739451274005085,
7.50432110841318));
#398552=CARTESIAN_POINT('Ctrl Pts',(-2.64546891357409,-0.739401332602651,
7.50435406373354));
#398553=CARTESIAN_POINT('Ctrl Pts',(-2.64548110249556,-0.739351929091587,
7.50438785222352));
#398554=CARTESIAN_POINT('Ctrl Pts',(-2.64555552171985,-0.739050296910203,
7.50459414719561));
#398555=CARTESIAN_POINT('Ctrl Pts',(-2.64561260228404,-0.738763789814949,
7.50483629897752));
#398556=CARTESIAN_POINT('Ctrl Pts',(-2.64565144811457,-0.738503640946549,
7.5050991045531));
#398557=CARTESIAN_POINT('Ctrl Pts',(-2.64573714591841,-0.737929726413378,
7.50567888004914));
#398558=CARTESIAN_POINT('Ctrl Pts',(-2.64573798903582,-0.737461555509731,
7.50637912803144));
#398559=CARTESIAN_POINT('Ctrl Pts',(-2.645683829865,-0.737091112458729,
7.50710440483569));
#398560=CARTESIAN_POINT('Ctrl Pts',(-2.6456705489611,-0.737000272468299,
7.50728225710685));
#398561=CARTESIAN_POINT('Ctrl Pts',(-2.64565384064822,-0.736913479663673,
7.50746498566954));
#398562=CARTESIAN_POINT('Ctrl Pts',(-2.64563450403444,-0.736832681318231,
7.50764697238949));
#398563=CARTESIAN_POINT('Ctrl Pts',(-2.64553055572032,-0.736398331649443,
7.50862528291181));
#398564=CARTESIAN_POINT('Ctrl Pts',(-2.64534524283225,-0.736096819786121,
7.5096585683742));
#398565=CARTESIAN_POINT('Ctrl Pts',(-2.64512364214823,-0.73587953009369,
7.510679598732));
#398566=CARTESIAN_POINT('Ctrl Pts',(-2.6450016950123,-0.735759955301867,
7.51124147302577));
#398567=CARTESIAN_POINT('Ctrl Pts',(-2.64486842488808,-0.73566616662784,
7.51180065547252));
#398568=CARTESIAN_POINT('Ctrl Pts',(-2.64472951425973,-0.735592069739056,
7.512351757165));
#398569=CARTESIAN_POINT('Ctrl Pts',(-2.64424952270334,-0.735336035471616,
7.51425603304536));
#398570=CARTESIAN_POINT('Ctrl Pts',(-2.64364210055535,-0.735289940333083,
7.51626900505181));
#398571=CARTESIAN_POINT('Ctrl Pts',(-2.64295636119803,-0.735418705226013,
7.51827788969245));
#398572=CARTESIAN_POINT('Ctrl Pts',(-2.64291924768814,-0.73542567422535,
7.51838661432546));
#398573=CARTESIAN_POINT('Ctrl Pts',(-2.64288189864374,-0.735433163274031,
7.51849533314857));
#398574=CARTESIAN_POINT('Ctrl Pts',(-2.64284431997727,-0.735441169348884,
7.51860402984325));
#398575=CARTESIAN_POINT('Ctrl Pts',(-2.5634458357012,-0.760817267312222,
7.57603338728985));
#398576=CARTESIAN_POINT('Ctrl Pts',(-2.59023829728888,-0.755147939734358,
7.55196141284922));
#398577=CARTESIAN_POINT('Ctrl Pts',(-2.61698440749374,-0.749487530346323,
7.52783573083105));
#398578=CARTESIAN_POINT('Ctrl Pts',(-2.64368796497828,-0.743835290530964,
7.50366116530176));
#398579=CARTESIAN_POINT('Origin',(-8.85789032694961E-16,-2.62897535302355E-16,
7.49482233047033));
#398580=CARTESIAN_POINT('Origin',(-2.61299471585144,-0.816189233531323,
7.49482233047033));
#398581=CARTESIAN_POINT('Origin',(0.,0.,7.50366116523517));
#398582=CARTESIAN_POINT('Origin',(-2.63517950238395,-0.741441326212334,
7.49482233047033));
#398583=CARTESIAN_POINT('Ctrl Pts',(-2.61614446651996,-0.825398570094808,
7.51860402984325));
#398584=CARTESIAN_POINT('Ctrl Pts',(-2.62151698305456,-0.83078673788318,
7.51860402984325));
#398585=CARTESIAN_POINT('Ctrl Pts',(-2.61919823167326,-0.838033784044334,
7.51860402984325));
#398586=CARTESIAN_POINT('Ctrl Pts',(-2.61813931767337,-0.827399234462638,
7.51041458714367));
#398587=CARTESIAN_POINT('Ctrl Pts',(-2.62096763486516,-0.832503643108394,
7.51004642900444));
#398588=CARTESIAN_POINT('Ctrl Pts',(-2.61919759218916,-0.838035782693619,
7.50729136483012));
#398589=CARTESIAN_POINT('Ctrl Pts',(-2.62069593195856,-0.826221329289833,
7.50215815450137));
#398590=CARTESIAN_POINT('Ctrl Pts',(-2.62208629631497,-0.829007895534854,
7.49877163671527));
#398591=CARTESIAN_POINT('Ctrl Pts',(-2.62105762822771,-0.832301186527254,
7.49481588533168));
#398592=CARTESIAN_POINT('Ctrl Pts',(-2.62143102271336,-0.81882437962955,
7.50366171572174));
#398593=CARTESIAN_POINT('Ctrl Pts',(-2.62492619857234,-0.819916125008266,
7.50000045605858));
#398594=CARTESIAN_POINT('Ctrl Pts',(-2.6249261985723,-0.819916125008385,
7.49482233047317));
#398595=CARTESIAN_POINT('Origin',(-2.60729278516566,-0.834224539571404,
7.51860402984325));
#398596=CARTESIAN_POINT('Origin',(-2.60729278516566,-0.834224539571404,
9.));
#398597=CARTESIAN_POINT('Origin',(-2.60729278516566,-0.834224539571404,
8.75721825406948));
#398598=CARTESIAN_POINT('Ctrl Pts',(-2.60435458367725,-0.81357238235248,
8.78942910404912));
#398599=CARTESIAN_POINT('Ctrl Pts',(-2.60830313188505,-0.81750448048863,
8.79672699501691));
#398600=CARTESIAN_POINT('Ctrl Pts',(-2.6032732741377,-0.824878354438151,
8.79893251111267));
#398601=CARTESIAN_POINT('Ctrl Pts',(-2.61211678181377,-0.821358504547104,
8.78111911759584));
#398602=CARTESIAN_POINT('Ctrl Pts',(-2.61679257887839,-0.826025327013831,
8.78644465894814));
#398603=CARTESIAN_POINT('Ctrl Pts',(-2.6137670602593,-0.833546081554491,
8.78817647674132));
#398604=CARTESIAN_POINT('Ctrl Pts',(-2.61695436881583,-0.826211001637831,
8.76780923932029));
#398605=CARTESIAN_POINT('Ctrl Pts',(-2.62247035001554,-0.831723595235668,
8.76988516158373));
#398606=CARTESIAN_POINT('Ctrl Pts',(-2.62031418371861,-0.838968409056351,
8.77093053738832));
#398607=CARTESIAN_POINT('Ctrl Pts',(-2.61601110555622,-0.825264831117445,
8.75371302330492));
#398608=CARTESIAN_POINT('Ctrl Pts',(-2.62139224614751,-0.830641589183835,
8.75300828287559));
#398609=CARTESIAN_POINT('Ctrl Pts',(-2.61903693688884,-0.837911187359129,
8.75267964240737));
#398610=CARTESIAN_POINT('Origin',(-2.59739259559948,-0.82429382821014,8.78727029226991));
#398611=CARTESIAN_POINT('Ctrl Pts',(-2.5557700913641,-0.764838063661141,
8.85049129520029));
#398612=CARTESIAN_POINT('Ctrl Pts',(-2.55989296307186,-0.768973645978593,
8.85711686593484));
#398613=CARTESIAN_POINT('Ctrl Pts',(-2.55537491841651,-0.776232298374609,
8.85933012996512));
#398614=CARTESIAN_POINT('Ctrl Pts',(-2.57261954817435,-0.781739466513898,
8.82945683644724));
#398615=CARTESIAN_POINT('Ctrl Pts',(-2.57677664221004,-0.785909376664987,
8.83607469902391));
#398616=CARTESIAN_POINT('Ctrl Pts',(-2.57221349406445,-0.793169522772272,
8.83829567148518));
#398617=CARTESIAN_POINT('Ctrl Pts',(-2.58944388951045,-0.798615676462751,
8.80838214965003));
#398618=CARTESIAN_POINT('Ctrl Pts',(-2.59361738938013,-0.80280204302623,
8.81501364461993));
#398619=CARTESIAN_POINT('Ctrl Pts',(-2.58902700057119,-0.810080582933243,
8.81722098428722));
#398620=CARTESIAN_POINT('Ctrl Pts',(-2.60624502375464,-0.815468607773367,
8.78727029226991));
#398621=CARTESIAN_POINT('Ctrl Pts',(-2.61041921685633,-0.819655669706065,
8.79393457792714));
#398622=CARTESIAN_POINT('Ctrl Pts',(-2.60581736094343,-0.826967464105193,
8.79610912703474));
#398623=CARTESIAN_POINT('Origin',(-2.54691766320894,-0.773663284097914,
8.85049129520029));
#398624=CARTESIAN_POINT('Ctrl Pts',(-2.55920636991203,-0.753260100986301,
8.85049129520029));
#398625=CARTESIAN_POINT('Ctrl Pts',(-2.5649178041393,-0.752043289049042,
8.85711686593484));
#398626=CARTESIAN_POINT('Ctrl Pts',(-2.56509113287406,-0.743495147773676,
8.85933012996512));
#398627=CARTESIAN_POINT('Ctrl Pts',(-2.55415354649658,-0.75433659694233,
8.86332496987231));
#398628=CARTESIAN_POINT('Ctrl Pts',(-2.55573644967855,-0.749995363028656,
8.86648636486736));
#398629=CARTESIAN_POINT('Ctrl Pts',(-2.55095922330301,-0.74652344568379,
8.87206031107457));
#398630=CARTESIAN_POINT('Ctrl Pts',(-2.55209786073928,-0.76115451173082,
8.86341338519877));
#398631=CARTESIAN_POINT('Ctrl Pts',(-2.55102439395551,-0.765662409211723,
8.8665458496606));
#398632=CARTESIAN_POINT('Ctrl Pts',(-2.54510291120594,-0.765907755566773,
8.87215952290714));
#398633=CARTESIAN_POINT('Ctrl Pts',(-2.5557700913641,-0.764838063661141,
8.85049129520029));
#398634=CARTESIAN_POINT('Ctrl Pts',(-2.55989296307186,-0.768973645978593,
8.85711686593484));
#398635=CARTESIAN_POINT('Ctrl Pts',(-2.55537491841651,-0.776232298374608,
8.85933012996512));
#398636=CARTESIAN_POINT('Origin',(-2.55660172093491,-0.741034480196092,
8.85049129520029));
#398637=CARTESIAN_POINT('Ctrl Pts',(-2.62912953922426,-0.738363081476928,
8.78727029226991));
#398638=CARTESIAN_POINT('Ctrl Pts',(-2.63491206922812,-0.737131122698051,
8.79393457792714));
#398639=CARTESIAN_POINT('Ctrl Pts',(-2.6350441475623,-0.728492721775898,
8.79610912703474));
#398640=CARTESIAN_POINT('Ctrl Pts',(-2.60585484624786,-0.743321717630787,
8.80838214965002));
#398641=CARTESIAN_POINT('Ctrl Pts',(-2.61163641591405,-0.742089963450328,
8.81501364461993));
#398642=CARTESIAN_POINT('Ctrl Pts',(-2.61175996320559,-0.733485688427872,
8.81722098428721));
#398643=CARTESIAN_POINT('Ctrl Pts',(-2.58254800437418,-0.748287203055851,
8.82945683644723));
#398644=CARTESIAN_POINT('Ctrl Pts',(-2.58830684695873,-0.74706029084382,
8.83607469902391));
#398645=CARTESIAN_POINT('Ctrl Pts',(-2.58844318986647,-0.738486292178717,
8.8382956714852));
#398646=CARTESIAN_POINT('Ctrl Pts',(-2.55920636991203,-0.753260100986301,
8.85049129520029));
#398647=CARTESIAN_POINT('Ctrl Pts',(-2.5649178041393,-0.752043289049042,
8.85711686593484));
#398648=CARTESIAN_POINT('Ctrl Pts',(-2.56509113287406,-0.743495147773676,
8.85933012996512));
#398649=CARTESIAN_POINT('Origin',(-2.62652489024714,-0.726137460686718,
8.78727029226991));
#398650=CARTESIAN_POINT('Ctrl Pts',(-2.64266321935266,-0.735479733686548,
8.75374538247848));
#398651=CARTESIAN_POINT('Ctrl Pts',(-2.65009811484497,-0.733909158184994,
8.75304829418601));
#398652=CARTESIAN_POINT('Ctrl Pts',(-2.6520933198787,-0.726540996943379,
8.75272238421917));
#398653=CARTESIAN_POINT('Ctrl Pts',(-2.64395422903473,-0.735204686572502,
8.76769408445021));
#398654=CARTESIAN_POINT('Ctrl Pts',(-2.65157607685315,-0.733593913216367,
8.76974318093971));
#398655=CARTESIAN_POINT('Ctrl Pts',(-2.65372225373277,-0.726354280485249,
8.7707786988043));
#398656=CARTESIAN_POINT('Ctrl Pts',(-2.6373372488473,-0.736614421409541,
8.78108014887987));
#398657=CARTESIAN_POINT('Ctrl Pts',(-2.64379727590477,-0.73525306630627,
8.78639403366323));
#398658=CARTESIAN_POINT('Ctrl Pts',(-2.64538156698147,-0.727315050337957,
8.78812224174741));
#398659=CARTESIAN_POINT('Ctrl Pts',(-2.62649347902618,-0.738924665570897,
8.78944554828686));
#398660=CARTESIAN_POINT('Ctrl Pts',(-2.63193890460374,-0.737782843388496,
8.79673892988686));
#398661=CARTESIAN_POINT('Ctrl Pts',(-2.63174894852015,-0.728868390460644,
8.79894799272499));
#398662=CARTESIAN_POINT('Origin',(-2.64023967100015,-0.72321554855868,8.75721825406948));
#398663=CARTESIAN_POINT('Origin',(-2.64023967100015,-0.72321554855868,9.));
#398664=CARTESIAN_POINT('Origin',(-2.64023967100015,-0.72321554855868,7.51860402984325));
#398665=CARTESIAN_POINT('Ctrl Pts',(-2.64368720766142,-0.743835077483582,
7.50366195182966));
#398666=CARTESIAN_POINT('Ctrl Pts',(-2.64721228549989,-0.74482690304422,
7.50000065167735));
#398667=CARTESIAN_POINT('Ctrl Pts',(-2.64721228549992,-0.744826903044107,
7.49482233047108));
#398668=CARTESIAN_POINT('Ctrl Pts',(-2.64710868794002,-0.737228469253189,
7.50215800491337));
#398669=CARTESIAN_POINT('Ctrl Pts',(-2.64979433702036,-0.735649866645916,
7.49877273257265));
#398670=CARTESIAN_POINT('Ctrl Pts',(-2.65072935414105,-0.732326780830906,
7.49481816995647));
#398671=CARTESIAN_POINT('Ctrl Pts',(-2.6456011070661,-0.734854186993081,
7.51043025814043));
#398672=CARTESIAN_POINT('Ctrl Pts',(-2.6507607661958,-0.732120933500968,
7.51006209594516));
#398673=CARTESIAN_POINT('Ctrl Pts',(-2.65229622879822,-0.726515460750259,
7.50731281821701));
#398674=CARTESIAN_POINT('Ctrl Pts',(-2.64284284172669,-0.735441484194384,
7.51860402984326));
#398675=CARTESIAN_POINT('Ctrl Pts',(-2.65028527911174,-0.733856825505501,
7.51860402984326));
#398676=CARTESIAN_POINT('Ctrl Pts',(-2.65229555990883,-0.726517902661682,
7.51860402984327));
#398677=CARTESIAN_POINT('Origin',(0.,0.,7.5));
#398678=CARTESIAN_POINT('Origin',(-2.50568666557813,-0.915681362418238,
7.5));
#398679=CARTESIAN_POINT('',(-2.50568666557813,-0.915681362418238,7.59394543036555));
#398680=CARTESIAN_POINT('',(-2.50568666557813,-0.915681362418238,8.85049129520029));
#398681=CARTESIAN_POINT('',(-2.50568666557813,-0.915681362418238,7.5));
#398682=CARTESIAN_POINT('',(-2.5764206255568,-0.90529494327273,8.78727029226991));
#398683=CARTESIAN_POINT('Ctrl Pts',(-2.50568666557814,-0.915681362418238,
8.85049129520029));
#398684=CARTESIAN_POINT('Ctrl Pts',(-2.5292989251247,-0.912214190147702,
8.82945686509571));
#398685=CARTESIAN_POINT('Ctrl Pts',(-2.55287608219231,-0.90875217224799,
8.80838212259897));
#398686=CARTESIAN_POINT('Ctrl Pts',(-2.5764206255568,-0.90529494327273,
8.78727029226991));
#398687=CARTESIAN_POINT('',(-2.59029443537465,-0.903257743546365,8.75721825406948));
#398688=CARTESIAN_POINT('Origin',(-2.54854335809393,-0.909388583893695,
8.75937679713171));
#398689=CARTESIAN_POINT('',(-2.59029443537465,-0.903257743546365,7.51860402984325));
#398690=CARTESIAN_POINT('',(-2.59029443537465,-0.903257743546365,7.5));
#398691=CARTESIAN_POINT('Ctrl Pts',(-2.59029443537465,-0.903257743546365,
7.51860402984325));
#398692=CARTESIAN_POINT('Ctrl Pts',(-2.57939871554831,-0.904857647086937,
7.52834476460825));
#398693=CARTESIAN_POINT('Ctrl Pts',(-2.56849592237787,-0.906458589261808,
7.53807742314407));
#398694=CARTESIAN_POINT('Ctrl Pts',(-2.55758581836641,-0.908060604944494,
7.54780169004674));
#398695=CARTESIAN_POINT('Ctrl Pts',(-2.54030480325306,-0.910598111204309,
7.5632044032688));
#398696=CARTESIAN_POINT('Ctrl Pts',(-2.52300542420909,-0.913138313983296,
7.57858609112103));
#398697=CARTESIAN_POINT('Ctrl Pts',(-2.50568666557813,-0.915681362418238,
7.59394543036555));
#398698=CARTESIAN_POINT('Origin',(-2.68279368784112,-1.13380819535554,7.5));
#398699=CARTESIAN_POINT('',(-2.55788654645048,-0.991320447028624,8.75721825406948));
#398700=CARTESIAN_POINT('',(-2.54864296074703,-0.980775832055561,8.78727029226991));
#398701=CARTESIAN_POINT('Origin',(-2.52517929254661,-0.954009666309173,
8.75658640621072));
#398702=CARTESIAN_POINT('',(-2.50151564461752,-0.927015373804549,8.85049129520029));
#398703=CARTESIAN_POINT('Ctrl Pts',(-2.54864296074703,-0.980775832055561,
8.78727029226991));
#398704=CARTESIAN_POINT('Ctrl Pts',(-2.53295613735134,-0.962881097461776,
8.80838212259897));
#398705=CARTESIAN_POINT('Ctrl Pts',(-2.51724758470003,-0.944961575232382,
8.82945686509571));
#398706=CARTESIAN_POINT('Ctrl Pts',(-2.50151564461752,-0.927015373804549,
8.85049129520029));
#398707=CARTESIAN_POINT('',(-2.50151564461752,-0.927015373804549,7.59394543036555));
#398708=CARTESIAN_POINT('',(-2.50151564461752,-0.927015373804549,7.5));
#398709=CARTESIAN_POINT('',(-2.55788654645048,-0.991320447028624,7.51860402984325));
#398710=CARTESIAN_POINT('Ctrl Pts',(-2.50151564461752,-0.927015373804549,
7.59394543036555));
#398711=CARTESIAN_POINT('Ctrl Pts',(-2.51305446717486,-0.940178278873335,
7.57858609112103));
#398712=CARTESIAN_POINT('Ctrl Pts',(-2.52458037785887,-0.953326454730175,
7.56320440326857));
#398713=CARTESIAN_POINT('Ctrl Pts',(-2.53609405336256,-0.96646067331226,
7.54780169004651));
#398714=CARTESIAN_POINT('Ctrl Pts',(-2.54336303591223,-0.974752760895078,
7.53807742314384));
#398715=CARTESIAN_POINT('Ctrl Pts',(-2.55062714752993,-0.983039291965115,
7.52834476460825));
#398716=CARTESIAN_POINT('Ctrl Pts',(-2.55788654645047,-0.991320447028623,
7.51860402984325));
#398717=CARTESIAN_POINT('',(-2.55788654645048,-0.991320447028624,7.5));
#398718=CARTESIAN_POINT('Origin',(-2.50668546515629,-0.922483422723959,
7.5));
#398719=CARTESIAN_POINT('Ctrl Pts',(-2.50151564461752,-0.927015373804549,
8.85049129520029));
#398720=CARTESIAN_POINT('Ctrl Pts',(-2.50138798433083,-0.926869745407334,
8.85097269580138));
#398721=CARTESIAN_POINT('Ctrl Pts',(-2.50126825987753,-0.926720409638613,
8.85143669361005));
#398722=CARTESIAN_POINT('Ctrl Pts',(-2.50115164046541,-0.926559943194745,
8.8519052845931));
#398723=CARTESIAN_POINT('Ctrl Pts',(-2.50092354029103,-0.926246081006952,
8.85282181883899));
#398724=CARTESIAN_POINT('Ctrl Pts',(-2.50071334603431,-0.925897594557926,
8.85372622499636));
#398725=CARTESIAN_POINT('Ctrl Pts',(-2.50053096238415,-0.925501051932902,
8.85462257735071));
#398726=CARTESIAN_POINT('Ctrl Pts',(-2.50037955395544,-0.925171856329469,
8.85536669723986));
#398727=CARTESIAN_POINT('Ctrl Pts',(-2.50024724861021,-0.924809479846986,
8.85610498449051));
#398728=CARTESIAN_POINT('Ctrl Pts',(-2.50014721912378,-0.924403462300347,
8.85681338218371));
#398729=CARTESIAN_POINT('Ctrl Pts',(-2.50005644220774,-0.924035000739112,
8.85745625420284));
#398730=CARTESIAN_POINT('Ctrl Pts',(-2.49999052655125,-0.923626119378977,
8.85808743050665));
#398731=CARTESIAN_POINT('Ctrl Pts',(-2.49997297445495,-0.923160524417042,
8.85866804508409));
#398732=CARTESIAN_POINT('Ctrl Pts',(-2.4999648762982,-0.922945708994462,
8.85893592806395));
#398733=CARTESIAN_POINT('Ctrl Pts',(-2.49996728752534,-0.922718707614324,
8.85919241173848));
#398734=CARTESIAN_POINT('Ctrl Pts',(-2.49998401765523,-0.922477377954843,
8.85943017985534));
#398735=CARTESIAN_POINT('Ctrl Pts',(-2.50000660828322,-0.922151511473323,
8.8597512372));
#398736=CARTESIAN_POINT('Ctrl Pts',(-2.50005652056601,-0.921791270397976,
8.86004599534705));
#398737=CARTESIAN_POINT('Ctrl Pts',(-2.50014347136778,-0.921402412271945,
8.86026130871721));
#398738=CARTESIAN_POINT('Ctrl Pts',(-2.50017530650771,-0.921260040348933,
8.86034014101235));
#398739=CARTESIAN_POINT('Ctrl Pts',(-2.50021257282627,-0.921111691043407,
8.86040910639693));
#398740=CARTESIAN_POINT('Ctrl Pts',(-2.50025458126597,-0.92096148800316,
8.86046313645507));
#398741=CARTESIAN_POINT('Ctrl Pts',(-2.5003201350843,-0.920727097416795,
8.8605474499083));
#398742=CARTESIAN_POINT('Ctrl Pts',(-2.50039916763199,-0.920481834184562,
8.86059655985669));
#398743=CARTESIAN_POINT('Ctrl Pts',(-2.50048633147296,-0.920241337932624,
8.86059725258816));
#398744=CARTESIAN_POINT('Ctrl Pts',(-2.50057369669722,-0.920000286038266,
8.86059794692012));
#398745=CARTESIAN_POINT('Ctrl Pts',(-2.50067269750016,-0.919762255163144,
8.86056369958366));
#398746=CARTESIAN_POINT('Ctrl Pts',(-2.50077445977493,-0.919538782504393,
8.86048590497774));
#398747=CARTESIAN_POINT('Ctrl Pts',(-2.50080101669881,-0.919480462794041,
8.86046560290182));
#398748=CARTESIAN_POINT('Ctrl Pts',(-2.5008281896189,-0.919422413409545,
8.86044257503091));
#398749=CARTESIAN_POINT('Ctrl Pts',(-2.5008551091393,-0.919366414208244,
8.86041778462583));
#398750=CARTESIAN_POINT('Ctrl Pts',(-2.50103624410723,-0.918989609072704,
8.86025097596201));
#398751=CARTESIAN_POINT('Ctrl Pts',(-2.5012305111296,-0.918655209975466,
8.8599848982295));
#398752=CARTESIAN_POINT('Ctrl Pts',(-2.50142491409744,-0.918368721174945,
8.85968173251462));
#398753=CARTESIAN_POINT('Ctrl Pts',(-2.50152774212947,-0.91821718501332,
8.85952137522077));
#398754=CARTESIAN_POINT('Ctrl Pts',(-2.50163243226653,-0.91807602501941,
8.85934740853961));
#398755=CARTESIAN_POINT('Ctrl Pts',(-2.50173625951288,-0.91794630582258,
8.8591675900182));
#398756=CARTESIAN_POINT('Ctrl Pts',(-2.50215317987531,-0.917425415820611,
8.85844552518696));
#398757=CARTESIAN_POINT('Ctrl Pts',(-2.50257738764837,-0.917057671454084,
8.85759444184126));
#398758=CARTESIAN_POINT('Ctrl Pts',(-2.5029501956441,-0.916788899331596,
8.8568349891514));
#398759=CARTESIAN_POINT('Ctrl Pts',(-2.50298920900799,-0.916760773044774,
8.85675551444999));
#398760=CARTESIAN_POINT('Ctrl Pts',(-2.50302766777015,-0.916733748780263,
8.85667699793652));
#398761=CARTESIAN_POINT('Ctrl Pts',(-2.50306550949756,-0.916707776672081,
8.85659965593547));
#398762=CARTESIAN_POINT('Ctrl Pts',(-2.50357629906517,-0.916357203830577,
8.85555568965886));
#398763=CARTESIAN_POINT('Ctrl Pts',(-2.50411782914084,-0.916094049730731,
8.85434650606346));
#398764=CARTESIAN_POINT('Ctrl Pts',(-2.5046900604545,-0.915911423788021,
8.85297329937117));
#398765=CARTESIAN_POINT('Ctrl Pts',(-2.50501190570186,-0.915808707822809,
8.85220095427747));
#398766=CARTESIAN_POINT('Ctrl Pts',(-2.50534369019836,-0.915731724168832,
8.85137579139183));
#398767=CARTESIAN_POINT('Ctrl Pts',(-2.50568666557814,-0.915681362418238,
8.85049129520029));
#398768=CARTESIAN_POINT('Origin',(-2.50668546515629,-0.922483422723959,
7.59394543036555));
#398769=CARTESIAN_POINT('Ctrl Pts',(-2.50114500373946,-0.926592565440157,
7.59443877723642));
#398770=CARTESIAN_POINT('Ctrl Pts',(-2.49732775931656,-0.922238046102214,
7.58783886950016));
#398771=CARTESIAN_POINT('Ctrl Pts',(-2.50224377712737,-0.915316200219761,
7.58559994247159));
#398772=CARTESIAN_POINT('Ctrl Pts',(-2.52198322905089,-0.950363758749818,
7.56670252222135));
#398773=CARTESIAN_POINT('Ctrl Pts',(-2.51817150162991,-0.946015532928607,
7.56004874999028));
#398774=CARTESIAN_POINT('Ctrl Pts',(-2.5230992292225,-0.939040301174026,
7.55786368756704));
#398775=CARTESIAN_POINT('Ctrl Pts',(-2.54278254105856,-0.974090561731022,
7.5388891333356));
#398776=CARTESIAN_POINT('Ctrl Pts',(-2.53894816035487,-0.96971649419084,
7.53222002137278));
#398777=CARTESIAN_POINT('Ctrl Pts',(-2.54391559872046,-0.962721710362594,
7.53005029815327));
#398778=CARTESIAN_POINT('Ctrl Pts',(-2.56354199857948,-0.997771900729836,
7.51101258149734));
#398779=CARTESIAN_POINT('Ctrl Pts',(-2.55966113821444,-0.993344811543191,
7.5043616886572));
#398780=CARTESIAN_POINT('Ctrl Pts',(-2.56469191920621,-0.986359203183317,
7.50217374673251));
#398781=CARTESIAN_POINT('',(-2.5635832672847,-0.985097876880951,7.50366116523517));
#398782=CARTESIAN_POINT('Ctrl Pts',(-2.55788654645047,-0.991320447028625,
7.51860402984325));
#398783=CARTESIAN_POINT('Ctrl Pts',(-2.55817765342152,-0.99165252713521,
7.51734760759494));
#398784=CARTESIAN_POINT('Ctrl Pts',(-2.55848545024178,-0.991913389124411,
7.51608817408573));
#398785=CARTESIAN_POINT('Ctrl Pts',(-2.55881786271931,-0.992092245848193,
7.5148100591312));
#398786=CARTESIAN_POINT('Ctrl Pts',(-2.5591189698847,-0.992254258542515,
7.51365231206384));
#398787=CARTESIAN_POINT('Ctrl Pts',(-2.55944058051349,-0.992349433201989,
7.51247773061043));
#398788=CARTESIAN_POINT('Ctrl Pts',(-2.55978760768028,-0.992340715789471,
7.51129758471022));
#398789=CARTESIAN_POINT('Ctrl Pts',(-2.56021892281661,-0.992329881041276,
7.50983079813402));
#398790=CARTESIAN_POINT('Ctrl Pts',(-2.56067540818268,-0.992145882723016,
7.50839324291155));
#398791=CARTESIAN_POINT('Ctrl Pts',(-2.56112957542532,-0.991710916073209,
7.50715379678855));
#398792=CARTESIAN_POINT('Ctrl Pts',(-2.5613393876049,-0.991509974014261,
7.50658120839351));
#398793=CARTESIAN_POINT('Ctrl Pts',(-2.56157195964614,-0.991220042996585,
7.50598221009429));
#398794=CARTESIAN_POINT('Ctrl Pts',(-2.56180401337727,-0.9908337899549,
7.50545747549611));
#398795=CARTESIAN_POINT('Ctrl Pts',(-2.56192784443093,-0.990627673376206,
7.50517746087247));
#398796=CARTESIAN_POINT('Ctrl Pts',(-2.56205304424278,-0.990391997191125,
7.50491486231392));
#398797=CARTESIAN_POINT('Ctrl Pts',(-2.56217482425125,-0.990132219958992,
7.50468370960992));
#398798=CARTESIAN_POINT('Ctrl Pts',(-2.56235692377725,-0.989743771054873,
7.50433806340447));
#398799=CARTESIAN_POINT('Ctrl Pts',(-2.56253633316337,-0.989289548577583,
7.50405484070984));
#398800=CARTESIAN_POINT('Ctrl Pts',(-2.56270030321808,-0.988799880389192,
7.50385766036131));
#398801=CARTESIAN_POINT('Ctrl Pts',(-2.56271783726676,-0.98874751798761,
7.50383657498791));
#398802=CARTESIAN_POINT('Ctrl Pts',(-2.56273520068951,-0.988694778002039,
7.50381643264937));
#398803=CARTESIAN_POINT('Ctrl Pts',(-2.56275238251345,-0.98864171760078,
7.50379723213559));
#398804=CARTESIAN_POINT('Ctrl Pts',(-2.56286707680879,-0.988287522065112,
7.50366906242519));
#398805=CARTESIAN_POINT('Ctrl Pts',(-2.56297548985005,-0.987911122718383,
7.50358235568538));
#398806=CARTESIAN_POINT('Ctrl Pts',(-2.5630712656504,-0.987545808184175,
7.5035341175365));
#398807=CARTESIAN_POINT('Ctrl Pts',(-2.5632148706233,-0.986998060385753,
7.50346178989176));
#398808=CARTESIAN_POINT('Ctrl Pts',(-2.56334606729219,-0.986402702482677,
7.50346967198527));
#398809=CARTESIAN_POINT('Ctrl Pts',(-2.56345687801437,-0.985814282467633,
7.50354272648692));
#398810=CARTESIAN_POINT('Ctrl Pts',(-2.56350245675805,-0.985572253135872,
7.50357277531559));
#398811=CARTESIAN_POINT('Ctrl Pts',(-2.56354466529949,-0.985331745408178,
7.50361331098761));
#398812=CARTESIAN_POINT('Ctrl Pts',(-2.56358326728603,-0.985097876881459,
7.50366116523659));
#398813=CARTESIAN_POINT('',(-2.50943323048236,-0.923494625763807,7.57603338622103));
#398814=CARTESIAN_POINT('Origin',(-2.51772740356821,-0.926543917882773,
7.58486873427628));
#398815=CARTESIAN_POINT('Ctrl Pts',(-2.56358326731837,-0.985097876927373,
7.50366116529968));
#398816=CARTESIAN_POINT('Ctrl Pts',(-2.54556333673348,-0.96459641599123,
7.5278357307971));
#398817=CARTESIAN_POINT('Ctrl Pts',(-2.52751419016024,-0.944062956655898,
7.55196141284068));
#398818=CARTESIAN_POINT('Ctrl Pts',(-2.50943323100972,-0.923494626899385,
7.57603338728831));
#398819=CARTESIAN_POINT('Ctrl Pts',(-2.50232577352112,-0.92767281329218,
7.5963967733137));
#398820=CARTESIAN_POINT('Ctrl Pts',(-2.48759500061618,-0.915457955303132,
7.59974925422226));
#398821=CARTESIAN_POINT('Ctrl Pts',(-2.50672970590147,-0.91570590633668,
7.59639677331373));
#398822=CARTESIAN_POINT('Ctrl Pts',(-2.49896195408416,-0.925698016371134,
7.58707626057421));
#398823=CARTESIAN_POINT('Ctrl Pts',(-2.49726541951554,-0.919016758850335,
7.58811717123965));
#398824=CARTESIAN_POINT('Ctrl Pts',(-2.50288821974734,-0.915029084195192,
7.58707626057425));
#398825=CARTESIAN_POINT('Ctrl Pts',(-2.50482266671421,-0.924092500961708,
7.58015376756929));
#398826=CARTESIAN_POINT('Ctrl Pts',(-2.50375153300597,-0.921403708571554,
7.58208760766041));
#398827=CARTESIAN_POINT('Ctrl Pts',(-2.50631009501529,-0.920050677758166,
7.5801537675693));
#398828=CARTESIAN_POINT('Ctrl Pts',(-2.50943322970564,-0.923494625478183,
7.57603338509286));
#398829=CARTESIAN_POINT('Ctrl Pts',(-2.50943322970564,-0.923494625478183,
7.57603338509286));
#398830=CARTESIAN_POINT('Ctrl Pts',(-2.50943322970564,-0.923494625478183,
7.57603338509286));
#398831=CARTESIAN_POINT('Origin',(-2.51772543279396,-0.926549273114443,
7.5848687342762));
#398832=CARTESIAN_POINT('Ctrl Pts',(-2.59880960003921,-0.90200739549112,
7.51098857897448));
#398833=CARTESIAN_POINT('Ctrl Pts',(-2.5929847431161,-0.90286270467336,
7.50433767179956));
#398834=CARTESIAN_POINT('Ctrl Pts',(-2.5922871544197,-0.911442997272864,
7.50214974420965));
#398835=CARTESIAN_POINT('Ctrl Pts',(-2.56764251675709,-0.90658390146659,
7.53887321589172));
#398836=CARTESIAN_POINT('Ctrl Pts',(-2.56188745195717,-0.907428962526923,
7.53220407452065));
#398837=CARTESIAN_POINT('Ctrl Pts',(-2.5611356572465,-0.915975173654377,
7.53003438070911));
#398838=CARTESIAN_POINT('Ctrl Pts',(-2.53641558117792,-0.911169196021749,
7.56669465659233));
#398839=CARTESIAN_POINT('Ctrl Pts',(-2.53069452774099,-0.912009262928298,
7.56004085833298));
#398840=CARTESIAN_POINT('Ctrl Pts',(-2.52992516332407,-0.920514833368937,
7.55785582193789));
#398841=CARTESIAN_POINT('Ctrl Pts',(-2.50513020557115,-0.915763071782057,
7.59443891967696));
#398842=CARTESIAN_POINT('Ctrl Pts',(-2.49940085731906,-0.916604356681062,
7.58783901202978));
#398843=CARTESIAN_POINT('Ctrl Pts',(-2.49865720208423,-0.925061670372774,
7.58560008491213));
#398844=CARTESIAN_POINT('',(-2.59059853376832,-0.911688670640867,7.50366116523517));
#398845=CARTESIAN_POINT('Ctrl Pts',(-2.59059853376867,-0.911688670640991,
7.50366116523554));
#398846=CARTESIAN_POINT('Ctrl Pts',(-2.59098904347062,-0.911039332755566,
7.50350835821027));
#398847=CARTESIAN_POINT('Ctrl Pts',(-2.591326891136,-0.910429728813534,
7.50345484955999));
#398848=CARTESIAN_POINT('Ctrl Pts',(-2.5916226464834,-0.909842025882743,
7.50349758195598));
#398849=CARTESIAN_POINT('Ctrl Pts',(-2.59177439091041,-0.909540490694061,
7.50351950684424));
#398850=CARTESIAN_POINT('Ctrl Pts',(-2.59193012691097,-0.909215058506846,
7.50357029184312));
#398851=CARTESIAN_POINT('Ctrl Pts',(-2.5920716753196,-0.90889711999251,
7.50365515313923));
#398852=CARTESIAN_POINT('Ctrl Pts',(-2.5922894340907,-0.908408001811447,
7.50378570417639));
#398853=CARTESIAN_POINT('Ctrl Pts',(-2.59248032444165,-0.90792240243678,
7.50400001621911));
#398854=CARTESIAN_POINT('Ctrl Pts',(-2.59262770382892,-0.907476452400872,
7.50428903009634));
#398855=CARTESIAN_POINT('Ctrl Pts',(-2.59264406180704,-0.907426955377816,
7.50432110841318));
#398856=CARTESIAN_POINT('Ctrl Pts',(-2.59265990793162,-0.907377928509107,
7.50435406373354));
#398857=CARTESIAN_POINT('Ctrl Pts',(-2.59267523710346,-0.907329407449733,
7.50438785222352));
#398858=CARTESIAN_POINT('Ctrl Pts',(-2.59276882906569,-0.907033163060087,
7.50459414719561));
#398859=CARTESIAN_POINT('Ctrl Pts',(-2.59284414892436,-0.906750901788691,
7.50483629897752));
#398860=CARTESIAN_POINT('Ctrl Pts',(-2.59289958273719,-0.90649377628495,
7.5050991045531));
#398861=CARTESIAN_POINT('Ctrl Pts',(-2.59302187529609,-0.905926531597884,
7.50567888004914));
#398862=CARTESIAN_POINT('Ctrl Pts',(-2.59305271249401,-0.905459376620288,
7.50637912803145));
#398863=CARTESIAN_POINT('Ctrl Pts',(-2.59302239896678,-0.905086224694276,
7.50710440483569));
#398864=CARTESIAN_POINT('Ctrl Pts',(-2.5930149654881,-0.904994720433914,
7.50728225710685));
#398865=CARTESIAN_POINT('Ctrl Pts',(-2.59300385233832,-0.904907035449132,
7.50746498566954));
#398866=CARTESIAN_POINT('Ctrl Pts',(-2.59298973222145,-0.904825164211458,
7.50764697238949));
#398867=CARTESIAN_POINT('Ctrl Pts',(-2.59291382635912,-0.904385046969295,
7.50862528291181));
#398868=CARTESIAN_POINT('Ctrl Pts',(-2.59274821214766,-0.904072281556928,
7.50965856837421));
#398869=CARTESIAN_POINT('Ctrl Pts',(-2.59254098856441,-0.903841240304901,
7.51067959873201));
#398870=CARTESIAN_POINT('Ctrl Pts',(-2.59242695316517,-0.903714098012488,
7.51124147302577));
#398871=CARTESIAN_POINT('Ctrl Pts',(-2.59229996591969,-0.903611963391176,
7.51180065547252));
#398872=CARTESIAN_POINT('Ctrl Pts',(-2.59216608810208,-0.903529118707881,
7.512351757165));
#398873=CARTESIAN_POINT('Ctrl Pts',(-2.59170348691167,-0.903242857325696,
7.51425603304536));
#398874=CARTESIAN_POINT('Ctrl Pts',(-2.59110026610329,-0.903157939223925,
7.5162690050518));
#398875=CARTESIAN_POINT('Ctrl Pts',(-2.59040768567601,-0.903242504084099,
7.51827788969244));
#398876=CARTESIAN_POINT('Ctrl Pts',(-2.59037020191449,-0.903247080894137,
7.51838661432545));
#398877=CARTESIAN_POINT('Ctrl Pts',(-2.5903324497827,-0.903252161594273,
7.51849533314857));
#398878=CARTESIAN_POINT('Ctrl Pts',(-2.59029443537466,-0.90325774354636,
7.51860402984325));
#398879=CARTESIAN_POINT('Ctrl Pts',(-2.50943323162123,-0.923494625241156,
7.57603338728985));
#398880=CARTESIAN_POINT('Ctrl Pts',(-2.53653388028815,-0.919553544812591,
7.55196141284922));
#398881=CARTESIAN_POINT('Ctrl Pts',(-2.56358770141576,-0.915618394507157,
7.52783573083105));
#398882=CARTESIAN_POINT('Ctrl Pts',(-2.59059853382585,-0.911688670627004,
7.50366116530176));
#398883=CARTESIAN_POINT('Origin',(-8.67125181207504E-16,-3.19110082301673E-16,
7.49482233047033));
#398884=CARTESIAN_POINT('Origin',(-2.55533261422668,-0.981927431468055,
7.49482233047033));
#398885=CARTESIAN_POINT('Origin',(0.,0.,7.50366116523517));
#398886=CARTESIAN_POINT('Origin',(-2.58226093460097,-0.908754485894703,
7.49482233047033));
#398887=CARTESIAN_POINT('Ctrl Pts',(-2.55788584917515,-0.991319651680091,
7.51860402984325));
#398888=CARTESIAN_POINT('Ctrl Pts',(-2.56290210620282,-0.997040967216085,
7.51860402984325));
#398889=CARTESIAN_POINT('Ctrl Pts',(-2.56012379910317,-1.00412456063257,
7.51860402984325));
#398890=CARTESIAN_POINT('Ctrl Pts',(-2.55974841868675,-0.993444016020627,
7.51041458714365));
#398891=CARTESIAN_POINT('Ctrl Pts',(-2.56224388421272,-0.998719148016021,
7.51004642900443));
#398892=CARTESIAN_POINT('Ctrl Pts',(-2.56012303287906,-1.00412651420352,
7.5072913648301));
#398893=CARTESIAN_POINT('Ctrl Pts',(-2.56237524877722,-0.992432333819996,
7.50215815450137));
#398894=CARTESIAN_POINT('Ctrl Pts',(-2.56358422056865,-0.995302255715978,
7.49877163671529));
#398895=CARTESIAN_POINT('Ctrl Pts',(-2.56234666411196,-0.998522873298193,
7.4948158853317));
#398896=CARTESIAN_POINT('Ctrl Pts',(-2.56358275340116,-0.985097679412473,
7.50366171572174));
#398897=CARTESIAN_POINT('Ctrl Pts',(-2.56700079967991,-0.986411118369375,
7.50000045605858));
#398898=CARTESIAN_POINT('Ctrl Pts',(-2.56700079967986,-0.986411118369491,
7.49482233047317));
#398899=CARTESIAN_POINT('Origin',(-2.54848687274361,-0.999560358084243,
7.51860402984325));
#398900=CARTESIAN_POINT('Origin',(-2.54848687274361,-0.999560358084243,
9.));
#398901=CARTESIAN_POINT('Origin',(-2.54848687274361,-0.999560358084243,
8.75721825406948));
#398902=CARTESIAN_POINT('Ctrl Pts',(-2.54687789636137,-0.978762381721547,
8.78942910404913));
#398903=CARTESIAN_POINT('Ctrl Pts',(-2.55056640146084,-0.982939385292637,
8.7967269950169));
#398904=CARTESIAN_POINT('Ctrl Pts',(-2.54507443236962,-0.989975844734951,
8.79893251111267));
#398905=CARTESIAN_POINT('Ctrl Pts',(-2.55412528766752,-0.987029832235209,
8.78111911759576));
#398906=CARTESIAN_POINT('Ctrl Pts',(-2.55849247346357,-0.991986645561183,
8.78644465894812));
#398907=CARTESIAN_POINT('Ctrl Pts',(-2.5549913146991,-0.999298102261562,
8.78817647674132));
#398908=CARTESIAN_POINT('Ctrl Pts',(-2.55864203477218,-0.9921823046136,
8.76780923932033));
#398909=CARTESIAN_POINT('Ctrl Pts',(-2.56379348971245,-0.99803698212555,
8.76988516158375));
#398910=CARTESIAN_POINT('Ctrl Pts',(-2.56117757667524,-1.00512876465029,
8.77093053738833));
#398911=CARTESIAN_POINT('Ctrl Pts',(-2.55776133090151,-0.991177643017514,
8.75371302330491));
#398912=CARTESIAN_POINT('Ctrl Pts',(-2.56278692529024,-0.996888124819234,
8.75300828287559));
#398913=CARTESIAN_POINT('Ctrl Pts',(-2.55997069051277,-1.0039918816431,
8.75267964240738));
#398914=CARTESIAN_POINT('Origin',(-2.53924328704017,-0.989015743111179,
8.78727029226991));
#398915=CARTESIAN_POINT('Ctrl Pts',(-2.50151564461752,-0.927015373804549,
8.85049129520029));
#398916=CARTESIAN_POINT('Ctrl Pts',(-2.50536507777435,-0.931406612421859,
8.85711686593484));
#398917=CARTESIAN_POINT('Ctrl Pts',(-2.50039125247053,-0.938360879023088,
8.85933012996512));
#398918=CARTESIAN_POINT('Ctrl Pts',(-2.51724760581288,-0.944961599316854,
8.82945683644723));
#398919=CARTESIAN_POINT('Ctrl Pts',(-2.52112899159233,-0.949389287869671,
8.83607469902389));
#398920=CARTESIAN_POINT('Ctrl Pts',(-2.51611005976584,-0.956342155322635,
8.83829567148519));
#398921=CARTESIAN_POINT('Ctrl Pts',(-2.53295611725146,-0.962881074532847,
8.80838214965003));
#398922=CARTESIAN_POINT('Ctrl Pts',(-2.53685282079138,-0.967326236811942,
8.81501364461988));
#398923=CARTESIAN_POINT('Ctrl Pts',(-2.53180552577561,-0.974295714957338,
8.81722098428721));
#398924=CARTESIAN_POINT('Ctrl Pts',(-2.54864296074703,-0.980775832055561,
8.78727029226991));
#398925=CARTESIAN_POINT('Ctrl Pts',(-2.55254031154221,-0.985221732690724,
8.79393457792714));
#398926=CARTESIAN_POINT('Ctrl Pts',(-2.54747944236023,-0.992223662303413,
8.79610912703474));
#398927=CARTESIAN_POINT('Origin',(-2.49211597091066,-0.935255284860168,
8.85049129520029));
#398928=CARTESIAN_POINT('Ctrl Pts',(-2.50568666557814,-0.915681362418238,
8.85049129520029));
#398929=CARTESIAN_POINT('Ctrl Pts',(-2.51146432645973,-0.914832983398953,
8.85711686593484));
#398930=CARTESIAN_POINT('Ctrl Pts',(-2.51218498036396,-0.906313510406788,
8.85933012996512));
#398931=CARTESIAN_POINT('Ctrl Pts',(-2.5005752523976,-0.916431911090119,
8.86332496987231));
#398932=CARTESIAN_POINT('Ctrl Pts',(-2.50243304714704,-0.912201013662185,
8.86648636486737));
#398933=CARTESIAN_POINT('Ctrl Pts',(-2.4978880826035,-0.908430151799093,
8.87206031107457));
#398934=CARTESIAN_POINT('Ctrl Pts',(-2.49808696496685,-0.923104109502771,
8.86341338519876));
#398935=CARTESIAN_POINT('Ctrl Pts',(-2.49672688175245,-0.927533967771866,
8.86654584966057));
#398936=CARTESIAN_POINT('Ctrl Pts',(-2.49080184592933,-0.927399419334132,
8.87215952290714));
#398937=CARTESIAN_POINT('Ctrl Pts',(-2.50151564461752,-0.927015373804549,
8.85049129520029));
#398938=CARTESIAN_POINT('Ctrl Pts',(-2.50536507777435,-0.931406612421859,
8.85711686593484));
#398939=CARTESIAN_POINT('Ctrl Pts',(-2.50039125247053,-0.938360879023087,
8.85933012996512));
#398940=CARTESIAN_POINT('Origin',(-2.50387066634512,-0.903313980044199,
8.85049129520029));
#398941=CARTESIAN_POINT('Ctrl Pts',(-2.5764206255568,-0.90529494327273,
8.78727029226991));
#398942=CARTESIAN_POINT('Ctrl Pts',(-2.58227020660257,-0.904436003654684,
8.79393457792714));
#398943=CARTESIAN_POINT('Ctrl Pts',(-2.582955477815,-0.895823813541617,
8.79610912703474));
#398944=CARTESIAN_POINT('Ctrl Pts',(-2.55287605202416,-0.908752176677816,
8.80838214965003));
#398945=CARTESIAN_POINT('Ctrl Pts',(-2.55872466159673,-0.90789337970876,
8.81501364461996));
#398946=CARTESIAN_POINT('Ctrl Pts',(-2.55939923284052,-0.899314698794302,
8.81722098428721));
#398947=CARTESIAN_POINT('Ctrl Pts',(-2.52929895681325,-0.912214185494627,
8.82945683644723));
#398948=CARTESIAN_POINT('Ctrl Pts',(-2.53512457577338,-0.911358764416542,
8.83607469902389));
#398949=CARTESIAN_POINT('Ctrl Pts',(-2.5358099765306,-0.902811117471346,
8.8382956714852));
#398950=CARTESIAN_POINT('Ctrl Pts',(-2.50568666557814,-0.915681362418238,
8.85049129520029));
#398951=CARTESIAN_POINT('Ctrl Pts',(-2.51146432645973,-0.914832983398953,
8.85711686593484));
#398952=CARTESIAN_POINT('Ctrl Pts',(-2.51218498036396,-0.906313510406788,
8.85933012996512));
#398953=CARTESIAN_POINT('Origin',(-2.57460462632379,-0.892927560898691,
8.78727029226991));
#398954=CARTESIAN_POINT('Ctrl Pts',(-2.59011123601512,-0.903284625492598,
8.75374538247847));
#398955=CARTESIAN_POINT('Ctrl Pts',(-2.59763148283513,-0.902193632296583,
8.75304829418601));
#398956=CARTESIAN_POINT('Ctrl Pts',(-2.60009466821772,-0.894968442957884,
8.75272238421917));
#398957=CARTESIAN_POINT('Ctrl Pts',(-2.59141721550838,-0.903092858766682,
8.76769408445022));
#398958=CARTESIAN_POINT('Ctrl Pts',(-2.59912660602629,-0.901973728383557,
8.76974318093972));
#398959=CARTESIAN_POINT('Ctrl Pts',(-2.60173221821703,-0.894886476279129,
8.77077869880429));
#398960=CARTESIAN_POINT('Ctrl Pts',(-2.58472350859536,-0.904075745776078,
8.78108014887986));
#398961=CARTESIAN_POINT('Ctrl Pts',(-2.59125748515534,-0.903131083077525,
8.7863940336632));
#398962=CARTESIAN_POINT('Ctrl Pts',(-2.59334711156538,-0.895310882492168,
8.78812224174741));
#398963=CARTESIAN_POINT('Ctrl Pts',(-2.57375400061067,-0.905686480575177,
8.78944554828686));
#398964=CARTESIAN_POINT('Ctrl Pts',(-2.57926139477577,-0.904895894003556,
8.79673892988687));
#398965=CARTESIAN_POINT('Ctrl Pts',(-2.57964297993742,-0.895987586247249,
8.79894799272499));
#398966=CARTESIAN_POINT('Origin',(-2.58847843614164,-0.890890361172326,
8.75721825406948));
#398967=CARTESIAN_POINT('Origin',(-2.58847843614164,-0.890890361172326,
9.));
#398968=CARTESIAN_POINT('Origin',(-2.58847843614164,-0.890890361172326,
7.51860402984325));
#398969=CARTESIAN_POINT('Ctrl Pts',(-2.59059779171497,-0.911688409495895,
7.50366195182966));
#398970=CARTESIAN_POINT('Ctrl Pts',(-2.59405208042111,-0.912904049757105,
7.50000065167735));
#398971=CARTESIAN_POINT('Ctrl Pts',(-2.59405208042115,-0.912904049756995,
7.49482233047108));
#398972=CARTESIAN_POINT('Ctrl Pts',(-2.59443552903803,-0.90531459024478,
7.50215800491337));
#398973=CARTESIAN_POINT('Ctrl Pts',(-2.5972168015806,-0.903911301173237,
7.49877273257267));
#398974=CARTESIAN_POINT('Ctrl Pts',(-2.59836280844753,-0.90065494974704,
7.49481816995647));
#398975=CARTESIAN_POINT('Ctrl Pts',(-2.59308316643742,-0.902848595163979,
7.51043025814043));
#398976=CARTESIAN_POINT('Ctrl Pts',(-2.59840734464658,-0.900451537929768,
7.51006209594514));
#398977=CARTESIAN_POINT('Ctrl Pts',(-2.60029879634862,-0.894955959650723,
7.50731281821701));
#398978=CARTESIAN_POINT('Ctrl Pts',(-2.59029293998908,-0.903257963033136,
7.51860402984326));
#398979=CARTESIAN_POINT('Ctrl Pts',(-2.59782161551912,-0.902153398795935,
7.51860402984327));
#398980=CARTESIAN_POINT('Ctrl Pts',(-2.60029797237973,-0.89495835368909,
7.51860402984327));
#398981=CARTESIAN_POINT('Origin',(0.,0.,7.5));
#398982=CARTESIAN_POINT('Origin',(-2.44187055726728,-1.07433989271896,7.5));
#398983=CARTESIAN_POINT('',(-2.44187055726728,-1.07433989271896,7.59394543036555));
#398984=CARTESIAN_POINT('',(-2.44187055726728,-1.07433989271896,8.85049129520029));
#398985=CARTESIAN_POINT('',(-2.44187055726728,-1.07433989271896,7.5));
#398986=CARTESIAN_POINT('',(-2.51312464689844,-1.06850675396147,8.78727029226991));
#398987=CARTESIAN_POINT('Ctrl Pts',(-2.44187055726728,-1.07433989271896,
8.85049129520029));
#398988=CARTESIAN_POINT('Ctrl Pts',(-2.46565644538429,-1.0723926867891,
8.82945686509571));
#398989=CARTESIAN_POINT('Ctrl Pts',(-2.48940697290247,-1.0704483756163,
8.80838212259897));
#398990=CARTESIAN_POINT('Ctrl Pts',(-2.51312464689844,-1.06850675396147,
8.78727029226991));
#398991=CARTESIAN_POINT('',(-2.52710047532067,-1.06736263792743,8.75721825406948));
#398992=CARTESIAN_POINT('Origin',(-2.48504237581409,-1.07080588110011,8.75937679713092));
#398993=CARTESIAN_POINT('',(-2.52710047532067,-1.06736263792743,7.51860402984325));
#398994=CARTESIAN_POINT('',(-2.52710047532067,-1.06736263792743,7.5));
#398995=CARTESIAN_POINT('Ctrl Pts',(-2.52710047532067,-1.06736263792743,
7.51860402984325));
#398996=CARTESIAN_POINT('Ctrl Pts',(-2.51612463574747,-1.06826116312847,
7.52834476460825));
#398997=CARTESIAN_POINT('Ctrl Pts',(-2.50514167081761,-1.06916027163911,
7.53807742314407));
#398998=CARTESIAN_POINT('Ctrl Pts',(-2.49415134128775,-1.07005998304473,
7.54780169004674));
#398999=CARTESIAN_POINT('Ctrl Pts',(-2.47674325328907,-1.07148507728598,
7.5632044032688));
#399000=CARTESIAN_POINT('Ctrl Pts',(-2.45931666632384,-1.07291168592505,
7.57858609112103));
#399001=CARTESIAN_POINT('Ctrl Pts',(-2.44187055726728,-1.07433989271896,
7.59394543036555));
#399002=CARTESIAN_POINT('Origin',(-2.60463825998837,-1.30336584656049,7.5));
#399003=CARTESIAN_POINT('',(-2.48911697509582,-1.15316802656821,8.75721825406948));
#399004=CARTESIAN_POINT('',(-2.48056797713151,-1.14205283806808,8.78727029226991));
#399005=CARTESIAN_POINT('Origin',(-2.45886743168094,-1.11383834389628,8.75658640621053));
#399006=CARTESIAN_POINT('',(-2.43698193351378,-1.08538337893282,8.85049129520029));
#399007=CARTESIAN_POINT('Ctrl Pts',(-2.48056797713151,-1.14205283806808,
8.78727029226991));
#399008=CARTESIAN_POINT('Ctrl Pts',(-2.4660599035788,-1.12318981189995,
8.80838212259894));
#399009=CARTESIAN_POINT('Ctrl Pts',(-2.45153173356485,-1.10430065682691,
8.82945686509571));
#399010=CARTESIAN_POINT('Ctrl Pts',(-2.43698193351378,-1.08538337893282,
8.85049129520029));
#399011=CARTESIAN_POINT('',(-2.43698193351378,-1.08538337893282,7.59394543036555));
#399012=CARTESIAN_POINT('',(-2.43698193351378,-1.08538337893282,7.5));
#399013=CARTESIAN_POINT('',(-2.48911697509582,-1.15316802656821,7.51860402984325));
#399014=CARTESIAN_POINT('Ctrl Pts',(-2.43698193351378,-1.08538337893282,
7.59394543036555));
#399015=CARTESIAN_POINT('Ctrl Pts',(-2.4476536980993,-1.09925853430099,
7.57858609112103));
#399016=CARTESIAN_POINT('Ctrl Pts',(-2.45831352104417,-1.1131181634534,
7.56320440326857));
#399017=CARTESIAN_POINT('Ctrl Pts',(-2.46896202819287,-1.12696308009707,
7.54780169004651));
#399018=CARTESIAN_POINT('Ctrl Pts',(-2.47568479996276,-1.13570385600762,
7.53807742314383));
#399019=CARTESIAN_POINT('Ctrl Pts',(-2.48240306681554,-1.14443877474016,
7.52834476460825));
#399020=CARTESIAN_POINT('Ctrl Pts',(-2.48911697509582,-1.15316802656821,
7.51860402984325));
#399021=CARTESIAN_POINT('',(-2.48911697509582,-1.15316802656821,7.5));
#399022=CARTESIAN_POINT('Origin',(-2.44243149520447,-1.08119197077096,7.5));
#399023=CARTESIAN_POINT('Ctrl Pts',(-2.43698193351378,-1.08538337893282,
8.85049129520029));
#399024=CARTESIAN_POINT('Ctrl Pts',(-2.43686386596228,-1.08522987052212,
8.85097269580138));
#399025=CARTESIAN_POINT('Ctrl Pts',(-2.43675395547127,-1.08507317080769,
8.85143669361005));
#399026=CARTESIAN_POINT('Ctrl Pts',(-2.43664785678659,-1.08490556222795,
8.8519052845931));
#399027=CARTESIAN_POINT('Ctrl Pts',(-2.43644033448791,-1.08457773047533,
8.85282181883899));
#399028=CARTESIAN_POINT('Ctrl Pts',(-2.43625289970128,-1.08421649283683,
8.85372622499635));
#399029=CARTESIAN_POINT('Ctrl Pts',(-2.4360962973511,-1.08380907959057,
8.8546225773507));
#399030=CARTESIAN_POINT('Ctrl Pts',(-2.43596629164197,-1.08347085958347,
8.85536669723986));
#399031=CARTESIAN_POINT('Ctrl Pts',(-2.43585747567322,-1.08310075080976,
8.85610498449051));
#399032=CARTESIAN_POINT('Ctrl Pts',(-2.43578366534162,-1.08268915855852,
8.85681338218371));
#399033=CARTESIAN_POINT('Ctrl Pts',(-2.43571668234978,-1.0823156379441,
8.85745625420284));
#399034=CARTESIAN_POINT('Ctrl Pts',(-2.43567709924276,-1.08190337344395,
8.85808743050666));
#399035=CARTESIAN_POINT('Ctrl Pts',(-2.43568941398076,-1.08143761053013,
8.8586680450841));
#399036=CARTESIAN_POINT('Ctrl Pts',(-2.43569509573392,-1.08122271761819,
8.85893592806395));
#399037=CARTESIAN_POINT('Ctrl Pts',(-2.4357120460353,-1.08099633712459,
8.85919241173848));
#399038=CARTESIAN_POINT('Ctrl Pts',(-2.43574420383571,-1.08075657520588,
8.85943017985534));
#399039=CARTESIAN_POINT('Ctrl Pts',(-2.435787626386,-1.0804328256385,8.8597512372));
#399040=CARTESIAN_POINT('Ctrl Pts',(-2.43586051684359,-1.08007652260802,
8.86004599534705));
#399041=CARTESIAN_POINT('Ctrl Pts',(-2.43597220322129,-1.07969403438971,
8.86026130871721));
#399042=CARTESIAN_POINT('Ctrl Pts',(-2.43601309475293,-1.0795539946695,
8.86034014101235));
#399043=CARTESIAN_POINT('Ctrl Pts',(-2.43605978927648,-1.07940833782476,
8.86040910639693));
#399044=CARTESIAN_POINT('Ctrl Pts',(-2.43611133494717,-1.07926113488274,
8.86046313645507));
#399045=CARTESIAN_POINT('Ctrl Pts',(-2.43619177153458,-1.07903142592454,
8.8605474499083));
#399046=CARTESIAN_POINT('Ctrl Pts',(-2.43628635577067,-1.07879173024464,
8.86059655985669));
#399047=CARTESIAN_POINT('Ctrl Pts',(-2.43638874917194,-1.07855731272451,
8.86059725258816));
#399048=CARTESIAN_POINT('Ctrl Pts',(-2.43649137914288,-1.07832235360626,
8.86059794692012));
#399049=CARTESIAN_POINT('Ctrl Pts',(-2.43660542722858,-1.07809115479432,
8.86056369958366));
#399050=CARTESIAN_POINT('Ctrl Pts',(-2.43672129836425,-1.07787466121544,
8.86048590497774));
#399051=CARTESIAN_POINT('Ctrl Pts',(-2.43675153728076,-1.07781816283715,
8.86046560290182));
#399052=CARTESIAN_POINT('Ctrl Pts',(-2.436782373608,-1.0777619736963,8.86044257503091));
#399053=CARTESIAN_POINT('Ctrl Pts',(-2.43681282570051,-1.07770781429096,
8.86041778462583));
#399054=CARTESIAN_POINT('Ctrl Pts',(-2.43701773049514,-1.07734338869923,
8.86025097596201));
#399055=CARTESIAN_POINT('Ctrl Pts',(-2.4372330233988,-1.07702212339166,
8.85998489822951));
#399056=CARTESIAN_POINT('Ctrl Pts',(-2.43744538234537,-1.07674867865402,
8.85968173251462));
#399057=CARTESIAN_POINT('Ctrl Pts',(-2.43755770806138,-1.07660404205432,
8.85952137522077));
#399058=CARTESIAN_POINT('Ctrl Pts',(-2.43767122725319,-1.07646987960887,
8.85934740853961));
#399059=CARTESIAN_POINT('Ctrl Pts',(-2.43778315231281,-1.07634707916855,
8.8591675900182));
#399060=CARTESIAN_POINT('Ctrl Pts',(-2.43823258960465,-1.07585397157029,
8.85844552518695));
#399061=CARTESIAN_POINT('Ctrl Pts',(-2.43867948725982,-1.07551416185933,
8.85759444184122));
#399062=CARTESIAN_POINT('Ctrl Pts',(-2.43906874957056,-1.07526982784829,
8.85683498915136));
#399063=CARTESIAN_POINT('Ctrl Pts',(-2.43910948483468,-1.07524425894475,
8.85675551444997));
#399064=CARTESIAN_POINT('Ctrl Pts',(-2.43914959602975,-1.07521975426585,
8.8566769979365));
#399065=CARTESIAN_POINT('Ctrl Pts',(-2.43918902404596,-1.07519626004795,
8.85659965593547));
#399066=CARTESIAN_POINT('Ctrl Pts',(-2.43972122542069,-1.07487913389591,
8.85555568965886));
#399067=CARTESIAN_POINT('Ctrl Pts',(-2.44027850320581,-1.07465121642546,
8.85434650606345));
#399068=CARTESIAN_POINT('Ctrl Pts',(-2.44086125969318,-1.07450562869348,
8.85297329937116));
#399069=CARTESIAN_POINT('Ctrl Pts',(-2.44118902470945,-1.07442374446503,
8.85220095427747));
#399070=CARTESIAN_POINT('Ctrl Pts',(-2.44152505987876,-1.07436817648791,
8.85137579139183));
#399071=CARTESIAN_POINT('Ctrl Pts',(-2.44187055726728,-1.07433989271896,
8.85049129520029));
#399072=CARTESIAN_POINT('Origin',(-2.44243149520447,-1.08119197077096,7.59394543036555));
#399073=CARTESIAN_POINT('Ctrl Pts',(-2.43663914358208,-1.08493769223097,
7.59443877723642));
#399074=CARTESIAN_POINT('Ctrl Pts',(-2.43310873710913,-1.08034754803013,
7.58783886950016));
#399075=CARTESIAN_POINT('Ctrl Pts',(-2.43845813862247,-1.07375489416498,
7.58559994247159));
#399076=CARTESIAN_POINT('Ctrl Pts',(-2.45591152894015,-1.10999515475423,
7.56670252222134));
#399077=CARTESIAN_POINT('Ctrl Pts',(-2.45238622490689,-1.10541164461494,
7.56004874999029));
#399078=CARTESIAN_POINT('Ctrl Pts',(-2.45775073258754,-1.09876646481297,
7.55786368756704));
#399079=CARTESIAN_POINT('Ctrl Pts',(-2.4751479250441,-1.13500582496976,
7.53888913333554));
#399080=CARTESIAN_POINT('Ctrl Pts',(-2.47160166995632,-1.13039507480528,
7.53222002137272));
#399081=CARTESIAN_POINT('Ctrl Pts',(-2.47700705952568,-1.12373292737944,
7.53005029815326));
#399082=CARTESIAN_POINT('Ctrl Pts',(-2.49434746143405,-1.15996857112787,
7.51101258149734));
#399083=CARTESIAN_POINT('Ctrl Pts',(-2.49075821929091,-1.15530193029346,
7.5043616886572));
#399084=CARTESIAN_POINT('Ctrl Pts',(-2.4962262334679,-1.14865299785998,
7.50217374673251));
#399085=CARTESIAN_POINT('',(-2.49520067284433,-1.14732323151529,7.50366116523517));
#399086=CARTESIAN_POINT('Ctrl Pts',(-2.48911697509582,-1.15316802656821,
7.51860402984325));
#399087=CARTESIAN_POINT('Ctrl Pts',(-2.48938620751089,-1.15351807566827,
7.51734760759494));
#399088=CARTESIAN_POINT('Ctrl Pts',(-2.48967665844454,-1.15379812229852,
7.51608817408573));
#399089=CARTESIAN_POINT('Ctrl Pts',(-2.48999692855534,-1.15399790928254,
7.5148100591312));
#399090=CARTESIAN_POINT('Ctrl Pts',(-2.49028703687481,-1.15417888110673,
7.51365231206384));
#399091=CARTESIAN_POINT('Ctrl Pts',(-2.4906018888587,-1.1542944658834,7.51247773061043));
#399092=CARTESIAN_POINT('Ctrl Pts',(-2.49094876154749,-1.15430800048865,
7.51129758471022));
#399093=CARTESIAN_POINT('Ctrl Pts',(-2.49137988468531,-1.15432482245728,
7.50983079813402));
#399094=CARTESIAN_POINT('Ctrl Pts',(-2.49184722096597,-1.15417044930112,
7.50839324291155));
#399095=CARTESIAN_POINT('Ctrl Pts',(-2.49232832348224,-1.15376547493209,
7.50715379678855));
#399096=CARTESIAN_POINT('Ctrl Pts',(-2.49255057898211,-1.15357838844265,
7.50658120839351));
#399097=CARTESIAN_POINT('Ctrl Pts',(-2.49280124912323,-1.15330395406119,
7.50598221009429));
#399098=CARTESIAN_POINT('Ctrl Pts',(-2.49305757339243,-1.1529333623514,
7.50545747549611));
#399099=CARTESIAN_POINT('Ctrl Pts',(-2.49319435595645,-1.15273560314417,
7.50517746087247));
#399100=CARTESIAN_POINT('Ctrl Pts',(-2.49333439835688,-1.15250843276058,
7.50491486231392));
#399101=CARTESIAN_POINT('Ctrl Pts',(-2.49347257213968,-1.15225699174056,
7.50468370960992));
#399102=CARTESIAN_POINT('Ctrl Pts',(-2.49367918552941,-1.15188100810307,
7.50433806340447));
#399103=CARTESIAN_POINT('Ctrl Pts',(-2.49388732843374,-1.15143921367341,
7.50405484070984));
#399104=CARTESIAN_POINT('Ctrl Pts',(-2.49408233474293,-1.1509610571583,
7.50385766036131));
#399105=CARTESIAN_POINT('Ctrl Pts',(-2.49410318763662,-1.15090992575125,
7.50383657498791));
#399106=CARTESIAN_POINT('Ctrl Pts',(-2.49412389444684,-1.15085840660395,
7.50381643264937));
#399107=CARTESIAN_POINT('Ctrl Pts',(-2.49414444056045,-1.15080655606421,
7.50379723213559));
#399108=CARTESIAN_POINT('Ctrl Pts',(-2.49428159258995,-1.15046043674999,
7.50366906242519));
#399109=CARTESIAN_POINT('Ctrl Pts',(-2.49441389887394,-1.15009175680349,
7.50358235568538));
#399110=CARTESIAN_POINT('Ctrl Pts',(-2.4945328836752,-1.14973332922377,
7.5035341175365));
#399111=CARTESIAN_POINT('Ctrl Pts',(-2.49471128791822,-1.14919590763415,
7.50346178989176));
#399112=CARTESIAN_POINT('Ctrl Pts',(-2.4948803597413,-1.14861017875717,
7.50346967198527));
#399113=CARTESIAN_POINT('Ctrl Pts',(-2.49502864299077,-1.1480300673815,
7.50354272648692));
#399114=CARTESIAN_POINT('Ctrl Pts',(-2.49508963496056,-1.1477914555651,
7.50357277531559));
#399115=CARTESIAN_POINT('Ctrl Pts',(-2.49514716616304,-1.14755414629686,
7.50361331098761));
#399116=CARTESIAN_POINT('Ctrl Pts',(-2.49520067284562,-1.14732323151588,
7.50366116523659));
#399117=CARTESIAN_POINT('',(-2.44510882695077,-1.0823771461146,7.57603338622103));
#399118=CARTESIAN_POINT('Origin',(-2.45319058995134,-1.08595158263,7.58486873427628));
#399119=CARTESIAN_POINT('Ctrl Pts',(-2.49520067287495,-1.14732323156377,
7.50366116529968));
#399120=CARTESIAN_POINT('Ctrl Pts',(-2.47853129928221,-1.12570935216126,
7.52783573079709));
#399121=CARTESIAN_POINT('Ctrl Pts',(-2.46183481987292,-1.10406166822896,
7.55196141284068));
#399122=CARTESIAN_POINT('Ctrl Pts',(-2.44510882740428,-1.08237714728164,
7.57603338728831));
#399123=CARTESIAN_POINT('Ctrl Pts',(-2.43774827562808,-1.08609137277759,
7.5963967733137));
#399124=CARTESIAN_POINT('Ctrl Pts',(-2.42383037731431,-1.07295780766384,
7.59974925422225));
#399125=CARTESIAN_POINT('Ctrl Pts',(-2.44290988201814,-1.07443121403225,
7.59639677331373));
#399126=CARTESIAN_POINT('Ctrl Pts',(-2.43451789319206,-1.08390511263732,
7.5870762605742));
#399127=CARTESIAN_POINT('Ctrl Pts',(-2.43325291397476,-1.07712888513364,
7.58811717123966));
#399128=CARTESIAN_POINT('Ctrl Pts',(-2.4391196527528,-1.07350965763151,
7.58707626057425));
#399129=CARTESIAN_POINT('Ctrl Pts',(-2.44046943008491,-1.08267839307892,
7.58015376756929));
#399130=CARTESIAN_POINT('Ctrl Pts',(-2.43957276865569,-1.07992649732878,
7.5820876076604));
#399131=CARTESIAN_POINT('Ctrl Pts',(-2.4422127628068,-1.07874017409309,
7.58015376756931));
#399132=CARTESIAN_POINT('Ctrl Pts',(-2.44510882619395,-1.0823771457798,
7.57603338509286));
#399133=CARTESIAN_POINT('Ctrl Pts',(-2.44510882619395,-1.0823771457798,
7.57603338509286));
#399134=CARTESIAN_POINT('Ctrl Pts',(-2.44510882619395,-1.0823771457798,
7.57603338509286));
#399135=CARTESIAN_POINT('Origin',(-2.45318828011509,-1.08595680059041,7.58486873427625));
#399136=CARTESIAN_POINT('Ctrl Pts',(-2.53567825474113,-1.0666604273196,
7.51098857897448));
#399137=CARTESIAN_POINT('Ctrl Pts',(-2.52981056576383,-1.06714077931297,
7.50433767179956));
#399138=CARTESIAN_POINT('Ctrl Pts',(-2.52856466910387,-1.07565874811986,
7.50214974420965));
#399139=CARTESIAN_POINT('Ctrl Pts',(-2.50428198982964,-1.06923064849067,
7.53887321589167));
#399140=CARTESIAN_POINT('Ctrl Pts',(-2.49848460617954,-1.06970524501471,
7.53220407452059));
#399141=CARTESIAN_POINT('Ctrl Pts',(-2.49718679848484,-1.07818572938232,
7.53003438070911));
#399142=CARTESIAN_POINT('Ctrl Pts',(-2.47282543250793,-1.07180580543451,
7.56669465659234));
#399143=CARTESIAN_POINT('Ctrl Pts',(-2.46706231031738,-1.07227759718128,
7.56004085833301));
#399144=CARTESIAN_POINT('Ctrl Pts',(-2.46574957287294,-1.08071639866779,
7.55785582193789));
#399145=CARTESIAN_POINT('Ctrl Pts',(-2.44131000543014,-1.07438578168707,
7.59443891967696));
#399146=CARTESIAN_POINT('Ctrl Pts',(-2.43553852742996,-1.07485825747317,
7.58783901202978));
#399147=CARTESIAN_POINT('Ctrl Pts',(-2.43425453816589,-1.08325054855237,
7.58560008491213));
#399148=CARTESIAN_POINT('',(-2.52686377755798,-1.07579572642898,7.50366116523517));
#399149=CARTESIAN_POINT('Ctrl Pts',(-2.52686377755833,-1.07579572642913,
7.50366116523554));
#399150=CARTESIAN_POINT('Ctrl Pts',(-2.52729508813737,-1.07517274272054,
7.50350835821027));
#399151=CARTESIAN_POINT('Ctrl Pts',(-2.52767129911716,-1.07458603724943,
7.50345484956));
#399152=CARTESIAN_POINT('Ctrl Pts',(-2.52800410105954,-1.07401849092751,
7.50349758195598));
#399153=CARTESIAN_POINT('Ctrl Pts',(-2.52817485313722,-1.07372729757403,
7.50351950684424));
#399154=CARTESIAN_POINT('Ctrl Pts',(-2.52835111967328,-1.07341251206196,
7.50357029184312));
#399155=CARTESIAN_POINT('Ctrl Pts',(-2.52851274764609,-1.07310429582408,
7.50365515313923));
#399156=CARTESIAN_POINT('Ctrl Pts',(-2.52876139691789,-1.07263013444114,
7.50378570417639));
#399157=CARTESIAN_POINT('Ctrl Pts',(-2.5289830075229,-1.07215776316925,
7.50400001621911));
#399158=CARTESIAN_POINT('Ctrl Pts',(-2.52915865622031,-1.07172217201528,
7.50428903009634));
#399159=CARTESIAN_POINT('Ctrl Pts',(-2.52917815187436,-1.07167382474842,
7.50432110841318));
#399160=CARTESIAN_POINT('Ctrl Pts',(-2.52919710660364,-1.07162591387536,
7.50435406373354));
#399161=CARTESIAN_POINT('Ctrl Pts',(-2.52921551303501,-1.07157847465112,
7.50438785222352));
#399162=CARTESIAN_POINT('Ctrl Pts',(-2.52932789314572,-1.07128883538495,
7.50459414719561));
#399163=CARTESIAN_POINT('Ctrl Pts',(-2.52942114279342,-1.07101197980953,
7.50483629897752));
#399164=CARTESIAN_POINT('Ctrl Pts',(-2.52949293679912,-1.07075893425429,
7.5050991045531));
#399165=CARTESIAN_POINT('Ctrl Pts',(-2.52965132158672,-1.07020069034342,
7.50567888004914));
#399166=CARTESIAN_POINT('Ctrl Pts',(-2.5297120261485,-1.06973647093188,
7.50637912803144));
#399167=CARTESIAN_POINT('Ctrl Pts',(-2.52970568282965,-1.06936214349217,
7.50710440483569));
#399168=CARTESIAN_POINT('Ctrl Pts',(-2.52970412732194,-1.06927035097251,
7.50728225710685));
#399169=CARTESIAN_POINT('Ctrl Pts',(-2.52969865500158,-1.06918213412398,
7.50746498566954));
#399170=CARTESIAN_POINT('Ctrl Pts',(-2.52968980940421,-1.06909952642055,
7.50764697238949));
#399171=CARTESIAN_POINT('Ctrl Pts',(-2.52964225790714,-1.06865545014116,
7.50862528291182));
#399172=CARTESIAN_POINT('Ctrl Pts',(-2.52949702291661,-1.06833271639992,
7.50965856837422));
#399173=CARTESIAN_POINT('Ctrl Pts',(-2.52930502796028,-1.06808887298636,
7.51067959873203));
#399174=CARTESIAN_POINT('Ctrl Pts',(-2.52919937289364,-1.06795468564831,
7.51124147302579));
#399175=CARTESIAN_POINT('Ctrl Pts',(-2.52907919034473,-1.06784462477278,
7.51180065547253));
#399176=CARTESIAN_POINT('Ctrl Pts',(-2.52895089547054,-1.06775337272155,
7.512351757165));
#399177=CARTESIAN_POINT('Ctrl Pts',(-2.52850758557362,-1.06743806053404,
7.51425603304535));
#399178=CARTESIAN_POINT('Ctrl Pts',(-2.52791104486855,-1.06731466841573,
7.51626900505179));
#399179=CARTESIAN_POINT('Ctrl Pts',(-2.52721446933284,-1.067354685748,7.51827788969242));
#399180=CARTESIAN_POINT('Ctrl Pts',(-2.5271767693485,-1.06735685156164,
7.51838661432544));
#399181=CARTESIAN_POINT('Ctrl Pts',(-2.52713876926094,-1.06735950303554,
7.51849533314856));
#399182=CARTESIAN_POINT('Ctrl Pts',(-2.52710047532067,-1.06736263792743,
7.51860402984325));
#399183=CARTESIAN_POINT('Ctrl Pts',(-2.44510882812078,-1.08237714566599,
7.57603338728985));
#399184=CARTESIAN_POINT('Ctrl Pts',(-2.47240630148851,-1.08018050713156,
7.55196141284922));
#399185=CARTESIAN_POINT('Ctrl Pts',(-2.49965666358482,-1.07798678628545,
7.52783573083105));
#399186=CARTESIAN_POINT('Ctrl Pts',(-2.52686377761629,-1.07579572641883,
7.50366116530176));
#399187=CARTESIAN_POINT('Origin',(-8.44898126352698E-16,-3.74011337523916E-16,
7.49482233047033));
#399188=CARTESIAN_POINT('Origin',(-2.48717010277293,-1.14363067896611,7.49482233047033));
#399189=CARTESIAN_POINT('Origin',(0.,0.,7.50366116523517));
#399190=CARTESIAN_POINT('Origin',(-2.51873130274448,-1.07233337846731,7.49482233047033));
#399191=CARTESIAN_POINT('Ctrl Pts',(-2.48911633021128,-1.15316718817922,
7.51860402984325));
#399192=CARTESIAN_POINT('Ctrl Pts',(-2.49375571485592,-1.15919814135008,
7.51860402984325));
#399193=CARTESIAN_POINT('Ctrl Pts',(-2.49052926869773,-1.16608917401713,
7.51860402984325));
#399194=CARTESIAN_POINT('Ctrl Pts',(-2.49083896438345,-1.15540652302373,
7.51041458714365));
#399195=CARTESIAN_POINT('Ctrl Pts',(-2.49299132384048,-1.16083070171987,
7.51004642900442));
#399196=CARTESIAN_POINT('Ctrl Pts',(-2.4905283788822,-1.16609107448211,
7.50729136483008));
#399197=CARTESIAN_POINT('Ctrl Pts',(-2.4935252160709,-1.15456522101442,
7.50215815450138));
#399198=CARTESIAN_POINT('Ctrl Pts',(-2.49454782737291,-1.1575067054367,
7.49877163671531));
#399199=CARTESIAN_POINT('Ctrl Pts',(-2.49310646793173,-1.16064141540026,
7.49481588533172));
#399200=CARTESIAN_POINT('Ctrl Pts',(-2.49520017266847,-1.1473230015279,
7.50366171572174));
#399201=CARTESIAN_POINT('Ctrl Pts',(-2.49852704388165,-1.14885273686058,
7.50000045605858));
#399202=CARTESIAN_POINT('Ctrl Pts',(-2.49852704388159,-1.1488527368607,
7.49482233047317));
#399203=CARTESIAN_POINT('Origin',(-2.47920868111274,-1.16078876868069,7.51860402984325));
#399204=CARTESIAN_POINT('Origin',(-2.47920868111274,-1.16078876868069,9.));
#399205=CARTESIAN_POINT('Origin',(-2.47920868111274,-1.16078876868069,8.75721825406948));
#399206=CARTESIAN_POINT('Ctrl Pts',(-2.47893554146576,-1.13993043652026,
8.78942910404913));
#399207=CARTESIAN_POINT('Ctrl Pts',(-2.48234884659824,-1.14433518132265,
8.7967269950169));
#399208=CARTESIAN_POINT('Ctrl Pts',(-2.47641733384219,-1.15100531193657,
8.79893251111267));
#399209=CARTESIAN_POINT('Ctrl Pts',(-2.48563834485611,-1.14864524262544,
8.78111911759582));
#399210=CARTESIAN_POINT('Ctrl Pts',(-2.48967897368034,-1.15387167820146,
8.78644465894816));
#399211=CARTESIAN_POINT('Ctrl Pts',(-2.48571656178288,-1.16094379271766,
8.78817647674132));
#399212=CARTESIAN_POINT('Ctrl Pts',(-2.48981569178069,-1.15407651767732,
8.76780923932031));
#399213=CARTESIAN_POINT('Ctrl Pts',(-2.49458145202817,-1.16024922097765,
8.76988516158372));
#399214=CARTESIAN_POINT('Ctrl Pts',(-2.49151654159844,-1.16715883055085,
8.77093053738833));
#399215=CARTESIAN_POINT('Ctrl Pts',(-2.48900116630003,-1.15301749337549,
8.75371302330492));
#399216=CARTESIAN_POINT('Ctrl Pts',(-2.49365056324086,-1.15903823331792,
8.75300828287559));
#399217=CARTESIAN_POINT('Ctrl Pts',(-2.4903849754574,-1.16594695792979,
8.75267964240738));
#399218=CARTESIAN_POINT('Origin',(-2.47065968314844,-1.14967358018056,8.78727029226991));
#399219=CARTESIAN_POINT('Ctrl Pts',(-2.43698193351378,-1.08538337893282,
8.85049129520029));
#399220=CARTESIAN_POINT('Ctrl Pts',(-2.44054210997315,-1.09001222930859,
8.85711686593484));
#399221=CARTESIAN_POINT('Ctrl Pts',(-2.43513294253591,-1.09663353354188,
8.85933012996512));
#399222=CARTESIAN_POINT('Ctrl Pts',(-2.45153175309123,-1.1043006822146,
8.82945683644722));
#399223=CARTESIAN_POINT('Ctrl Pts',(-2.45512148116771,-1.10896795484714,
8.83607469902389));
#399224=CARTESIAN_POINT('Ctrl Pts',(-2.44966738952774,-1.11558497282202,
8.83829567148519));
#399225=CARTESIAN_POINT('Ctrl Pts',(-2.46605988498928,-1.12318978773033,
8.80838214965001));
#399226=CARTESIAN_POINT('Ctrl Pts',(-2.4696637798088,-1.12787547959982,
8.81501364461991));
#399227=CARTESIAN_POINT('Ctrl Pts',(-2.46418031900404,-1.1345072569029,
8.81722098428721));
#399228=CARTESIAN_POINT('Ctrl Pts',(-2.48056797713151,-1.14205283806808,
8.78727029226991));
#399229=CARTESIAN_POINT('Ctrl Pts',(-2.48417247056978,-1.14673930824636,
8.79393457792714));
#399230=CARTESIAN_POINT('Ctrl Pts',(-2.47867338431574,-1.15340260064192,
8.79610912703474));
#399231=CARTESIAN_POINT('Origin',(-2.4270736395307,-1.0930041210453,8.85049129520029));
#399232=CARTESIAN_POINT('Ctrl Pts',(-2.44187055726728,-1.07433989271896,
8.85049129520029));
#399233=CARTESIAN_POINT('Ctrl Pts',(-2.44769070315533,-1.07386343278902,
8.85711686593484));
#399234=CARTESIAN_POINT('Ctrl Pts',(-2.44895572090755,-1.065407636422,8.85933012996512));
#399235=CARTESIAN_POINT('Ctrl Pts',(-2.43672155821481,-1.07476140994121,
8.8633249698723));
#399236=CARTESIAN_POINT('Ctrl Pts',(-2.43884661045463,-1.07065823466408,
8.86648636486738));
#399237=CARTESIAN_POINT('Ctrl Pts',(-2.43455258397725,-1.06660392356299,
8.87206031107458));
#399238=CARTESIAN_POINT('Ctrl Pts',(-2.4338108940174,-1.08126047448357,
8.86341338519877));
#399239=CARTESIAN_POINT('Ctrl Pts',(-2.43216978324604,-1.08559409030301,
8.86654584966058));
#399240=CARTESIAN_POINT('Ctrl Pts',(-2.4262655415925,-1.08508019996089,
8.87215952290714));
#399241=CARTESIAN_POINT('Ctrl Pts',(-2.43698193351378,-1.08538337893282,
8.85049129520029));
#399242=CARTESIAN_POINT('Ctrl Pts',(-2.44054210997315,-1.09001222930859,
8.85711686593484));
#399243=CARTESIAN_POINT('Ctrl Pts',(-2.43513294253591,-1.09663353354188,
8.85933012996512));
#399244=CARTESIAN_POINT('Origin',(-2.44085067010874,-1.06188156898806,8.85049129520029));
#399245=CARTESIAN_POINT('Ctrl Pts',(-2.51312464689844,-1.06850675396147,
8.78727029226991));
#399246=CARTESIAN_POINT('Ctrl Pts',(-2.51901724180286,-1.06802436307139,
8.79393457792714));
#399247=CARTESIAN_POINT('Ctrl Pts',(-2.52025288996715,-1.05947377310389,
8.79610912703474));
#399248=CARTESIAN_POINT('Ctrl Pts',(-2.48940694251248,-1.07044837810415,
8.80838214965003));
#399249=CARTESIAN_POINT('Ctrl Pts',(-2.4952985588001,-1.06996606732748,
8.81501364461992));
#399250=CARTESIAN_POINT('Ctrl Pts',(-2.49652138203831,-1.061448232161,8.81722098428721));
#399251=CARTESIAN_POINT('Ctrl Pts',(-2.46565647730583,-1.07239268417588,
8.82945683644723));
#399252=CARTESIAN_POINT('Ctrl Pts',(-2.47152493392369,-1.07191226934045,
8.8360746990239));
#399253=CARTESIAN_POINT('Ctrl Pts',(-2.47275657607162,-1.06342609822993,
8.83829567148519));
#399254=CARTESIAN_POINT('Ctrl Pts',(-2.44187055726728,-1.07433989271896,
8.85049129520029));
#399255=CARTESIAN_POINT('Ctrl Pts',(-2.44769070315533,-1.07386343278902,
8.85711686593484));
#399256=CARTESIAN_POINT('Ctrl Pts',(-2.44895572090755,-1.065407636422,8.85933012996512));
#399257=CARTESIAN_POINT('Origin',(-2.5121047597399,-1.05604843023057,8.78727029226991));
#399258=CARTESIAN_POINT('Ctrl Pts',(-2.52691593003166,-1.06737772701856,
8.75374538247847));
#399259=CARTESIAN_POINT('Ctrl Pts',(-2.53449062587209,-1.06677079925314,
8.75304829418602));
#399260=CARTESIAN_POINT('Ctrl Pts',(-2.53741166984649,-1.05971827167015,
8.75272238421917));
#399261=CARTESIAN_POINT('Ctrl Pts',(-2.52823151278631,-1.06727002869137,
8.76769408445023));
#399262=CARTESIAN_POINT('Ctrl Pts',(-2.53599676646443,-1.06664714002804,
8.76974318093966));
#399263=CARTESIAN_POINT('Ctrl Pts',(-2.53905110694683,-1.05974139158942,
8.7707786988043));
#399264=CARTESIAN_POINT('Ctrl Pts',(-2.52148858502513,-1.06782202897959,
8.78108014887987));
#399265=CARTESIAN_POINT('Ctrl Pts',(-2.5280696615764,-1.06729794050741,
8.78639403366329));
#399266=CARTESIAN_POINT('Ctrl Pts',(-2.53065603659667,-1.05962769018663,
8.78812224174741));
#399267=CARTESIAN_POINT('Ctrl Pts',(-2.51043841493816,-1.06872663556163,
8.78944554828686));
#399268=CARTESIAN_POINT('Ctrl Pts',(-2.51598514662683,-1.06829053329059,
8.79673892988684));
#399269=CARTESIAN_POINT('Ctrl Pts',(-2.51693670501845,-1.05942497685323,
8.79894799272499));
#399270=CARTESIAN_POINT('Origin',(-2.52608058816213,-1.05490431419653,8.75721825406948));
#399271=CARTESIAN_POINT('Origin',(-2.52608058816213,-1.05490431419653,9.));
#399272=CARTESIAN_POINT('Origin',(-2.52608058816213,-1.05490431419653,7.51860402984325));
#399273=CARTESIAN_POINT('Ctrl Pts',(-2.52686305376089,-1.07579541827704,
7.50366195182966));
#399274=CARTESIAN_POINT('Ctrl Pts',(-2.53023235892145,-1.07722987791223,
7.50000065167735));
#399275=CARTESIAN_POINT('Ctrl Pts',(-2.5302323589215,-1.07722987791213,
7.49482233047108));
#399276=CARTESIAN_POINT('Ctrl Pts',(-2.53110127804255,-1.06968057939568,
7.50215800491338));
#399277=CARTESIAN_POINT('Ctrl Pts',(-2.5339667452019,-1.06845837027566,
7.49877273257264));
#399278=CARTESIAN_POINT('Ctrl Pts',(-2.53531903262703,-1.06528213428478,
7.49481816995647));
#399279=CARTESIAN_POINT('Ctrl Pts',(-2.52990969086325,-1.06713300479694,
7.51043025814042));
#399280=CARTESIAN_POINT('Ctrl Pts',(-2.53537650996154,-1.06508199384297,
7.51006209594516));
#399281=CARTESIAN_POINT('Ctrl Pts',(-2.53761617838248,-1.05971889254554,
7.50731281821701));
#399282=CARTESIAN_POINT('Ctrl Pts',(-2.52709896894496,-1.06736276115356,
7.51860402984326));
#399283=CARTESIAN_POINT('Ctrl Pts',(-2.53468294567733,-1.06674283025942,
7.51860402984327));
#399284=CARTESIAN_POINT('Ctrl Pts',(-2.53761520271996,-1.05972122887323,
7.51860402984327));
#399285=CARTESIAN_POINT('Origin',(0.,0.,7.5));
#399286=CARTESIAN_POINT('Origin',(-2.36802027905702,-1.22858372995532,7.5));
#399287=CARTESIAN_POINT('',(-2.36802027905702,-1.22858372995532,7.59394543036555));
#399288=CARTESIAN_POINT('',(-2.36802027905702,-1.22858372995532,8.85049129520029));
#399289=CARTESIAN_POINT('',(-2.36802027905702,-1.22858372995532,7.5));
#399290=CARTESIAN_POINT('',(-2.43950170000242,-1.2273278412042,8.78727029226991));
#399291=CARTESIAN_POINT('Ctrl Pts',(-2.36802027905702,-1.22858372995532,
8.85049129520029));
#399292=CARTESIAN_POINT('Ctrl Pts',(-2.39188205442813,-1.22816449185297,
8.82945686509571));
#399293=CARTESIAN_POINT('Ctrl Pts',(-2.41570835638483,-1.22774587699876,
8.80838212259895));
#399294=CARTESIAN_POINT('Ctrl Pts',(-2.43950170000242,-1.2273278412042,
8.78727029226991));
#399295=CARTESIAN_POINT('',(-2.45352211735224,-1.22708151028068,8.75721825406948));
#399296=CARTESIAN_POINT('Origin',(-2.41132982137612,-1.22782300725359,8.75937679713158));
#399297=CARTESIAN_POINT('',(-2.45352211735224,-1.22708151028068,7.51860402984325));
#399298=CARTESIAN_POINT('',(-2.45352211735224,-1.22708151028068,7.5));
#399299=CARTESIAN_POINT('Ctrl Pts',(-2.45352211735224,-1.22708151028068,
7.51860402984325));
#399300=CARTESIAN_POINT('Ctrl Pts',(-2.44251126011132,-1.2272749649094,
7.52834476460825));
#399301=CARTESIAN_POINT('Ctrl Pts',(-2.43149325478076,-1.22746854512608,
7.53807742314407));
#399302=CARTESIAN_POINT('Ctrl Pts',(-2.42046786135394,-1.22766225514749,
7.54780169004674));
#399303=CARTESIAN_POINT('Ctrl Pts',(-2.40300423403754,-1.22796908135226,
7.5632044032688));
#399304=CARTESIAN_POINT('Ctrl Pts',(-2.3855220487349,-1.2282762336105,7.57858609112103));
#399305=CARTESIAN_POINT('Ctrl Pts',(-2.36802027905702,-1.22858372995532,
7.59394543036555));
#399306=CARTESIAN_POINT('Origin',(-2.51577981483217,-1.46756768793082,7.5));
#399307=CARTESIAN_POINT('',(-2.41011908817657,-1.31027699133286,8.75721825406948));
#399308=CARTESIAN_POINT('',(-2.40229980761779,-1.29863690399942,8.78727029226991));
#399309=CARTESIAN_POINT('Origin',(-2.38245155711314,-1.2690900208107,8.75658640621029));
#399310=CARTESIAN_POINT('',(-2.36243414091425,-1.23929131094305,8.85049129520029));
#399311=CARTESIAN_POINT('Ctrl Pts',(-2.40229980761779,-1.29863690399942,
8.78727029226991));
#399312=CARTESIAN_POINT('Ctrl Pts',(-2.38903010069429,-1.27888309847759,
8.80838212259896));
#399313=CARTESIAN_POINT('Ctrl Pts',(-2.37574201268454,-1.25910193015078,
8.82945686509571));
#399314=CARTESIAN_POINT('Ctrl Pts',(-2.36243414091425,-1.23929131094305,
8.85049129520029));
#399315=CARTESIAN_POINT('',(-2.36243414091425,-1.23929131094305,7.59394543036555));
#399316=CARTESIAN_POINT('',(-2.36243414091425,-1.23929131094305,7.5));
#399317=CARTESIAN_POINT('',(-2.41011908817657,-1.31027699133286,7.51860402984325));
#399318=CARTESIAN_POINT('Ctrl Pts',(-2.36243414091425,-1.23929131094305,
7.59394543036555));
#399319=CARTESIAN_POINT('Ctrl Pts',(-2.37219499495817,-1.25382170062099,
7.57858609112103));
#399320=CARTESIAN_POINT('Ctrl Pts',(-2.3819449266649,-1.2683358308799,7.56320440326857));
#399321=CARTESIAN_POINT('Ctrl Pts',(-2.39168450845863,-1.28283455385295,
7.54780169004651));
#399322=CARTESIAN_POINT('Ctrl Pts',(-2.39783344413752,-1.29198810036812,
7.53807742314383));
#399323=CARTESIAN_POINT('Ctrl Pts',(-2.40397825942581,-1.30113551310845,
7.52834476460825));
#399324=CARTESIAN_POINT('Ctrl Pts',(-2.41011908817657,-1.31027699133286,
7.51860402984325));
#399325=CARTESIAN_POINT('',(-2.41011908817657,-1.31027699133286,7.5));
#399326=CARTESIAN_POINT('Origin',(-2.36814105033894,-1.2354576690951,7.5));
#399327=CARTESIAN_POINT('Ctrl Pts',(-2.36243414091425,-1.23929131094305,
8.85049129520029));
#399328=CARTESIAN_POINT('Ctrl Pts',(-2.36232615126284,-1.23913055331784,
8.85097269580138));
#399329=CARTESIAN_POINT('Ctrl Pts',(-2.36222650637989,-1.23896713357045,
8.85143669361005));
#399330=CARTESIAN_POINT('Ctrl Pts',(-2.36213136440492,-1.23879307159445,
8.8519052845931));
#399331=CARTESIAN_POINT('Ctrl Pts',(-2.36194527273555,-1.238452617408,8.85282181883899));
#399332=CARTESIAN_POINT('Ctrl Pts',(-2.36178136762876,-1.23808011298295,
8.85372622499636));
#399333=CARTESIAN_POINT('Ctrl Pts',(-2.36165119009122,-1.23766350326387,
8.85462257735071));
#399334=CARTESIAN_POINT('Ctrl Pts',(-2.36154312132302,-1.23731764867168,
8.85536669723986));
#399335=CARTESIAN_POINT('Ctrl Pts',(-2.36145824187889,-1.23694132846308,
8.85610498449051));
#399336=CARTESIAN_POINT('Ctrl Pts',(-2.36141095400462,-1.23652585282808,
8.85681338218371));
#399337=CARTESIAN_POINT('Ctrl Pts',(-2.36136804018445,-1.2361488080368,
8.85745625420284));
#399338=CARTESIAN_POINT('Ctrl Pts',(-2.36135495228239,-1.23573485447991,
8.85808743050665));
#399339=CARTESIAN_POINT('Ctrl Pts',(-2.36139708325078,-1.23527083753392,
8.8586680450841));
#399340=CARTESIAN_POINT('Ctrl Pts',(-2.36141652156631,-1.23505675017369,
8.85893592806395));
#399341=CARTESIAN_POINT('Ctrl Pts',(-2.3614479412895,-1.23483192081263,
8.85919241173848));
#399342=CARTESIAN_POINT('Ctrl Pts',(-2.36149539461714,-1.23459471186785,
8.85943017985534));
#399343=CARTESIAN_POINT('Ctrl Pts',(-2.36155947065714,-1.23427440957102,
8.8597512372));
#399344=CARTESIAN_POINT('Ctrl Pts',(-2.36165503976701,-1.23392350871098,
8.86004599534705));
#399345=CARTESIAN_POINT('Ctrl Pts',(-2.36179100277735,-1.23354896212652,
8.86026130871721));
#399346=CARTESIAN_POINT('Ctrl Pts',(-2.36184078266865,-1.23341183006237,
8.86034014101235));
#399347=CARTESIAN_POINT('Ctrl Pts',(-2.36189671351937,-1.23326946421363,
8.86040910639693));
#399348=CARTESIAN_POINT('Ctrl Pts',(-2.36195758460882,-1.23312586625831,
8.86046313645507));
#399349=CARTESIAN_POINT('Ctrl Pts',(-2.36205257343412,-1.23290178285164,
8.8605474499083));
#399350=CARTESIAN_POINT('Ctrl Pts',(-2.3621623206917,-1.23266863968503,
8.86059655985668));
#399351=CARTESIAN_POINT('Ctrl Pts',(-2.36227952289683,-1.23244126416859,
8.86059725258816));
#399352=CARTESIAN_POINT('Ctrl Pts',(-2.36239699588587,-1.23221336332386,
8.86059794692011));
#399353=CARTESIAN_POINT('Ctrl Pts',(-2.36252562260629,-1.23198994662061,
8.86056369958366));
#399354=CARTESIAN_POINT('Ctrl Pts',(-2.36265512646351,-1.23178132174017,
8.86048590497774));
#399355=CARTESIAN_POINT('Ctrl Pts',(-2.36268892311445,-1.23172687685788,
8.86046560290182));
#399356=CARTESIAN_POINT('Ctrl Pts',(-2.36272329613576,-1.23167277885392,
8.86044257503091));
#399357=CARTESIAN_POINT('Ctrl Pts',(-2.36275715566619,-1.23162068179715,
8.86041778462583));
#399358=CARTESIAN_POINT('Ctrl Pts',(-2.36298498828978,-1.23127013325215,
8.86025097596201));
#399359=CARTESIAN_POINT('Ctrl Pts',(-2.36322042239,-1.23096332188231,8.8599848982295));
#399360=CARTESIAN_POINT('Ctrl Pts',(-2.36344986468683,-1.23070404485063,
8.85968173251462));
#399361=CARTESIAN_POINT('Ctrl Pts',(-2.36357122651638,-1.23056690215567,
8.85952137522077));
#399362=CARTESIAN_POINT('Ctrl Pts',(-2.36369310828823,-1.23044028856094,
8.85934740853961));
#399363=CARTESIAN_POINT('Ctrl Pts',(-2.36381267123703,-1.2303249114905,
8.8591675900182));
#399364=CARTESIAN_POINT('Ctrl Pts',(-2.36429277862405,-1.22986161258083,
8.85844552518694));
#399365=CARTESIAN_POINT('Ctrl Pts',(-2.36476052976299,-1.22955113387645,
8.85759444184121));
#399366=CARTESIAN_POINT('Ctrl Pts',(-2.3651646468264,-1.22933224199772,
8.85683498915135));
#399367=CARTESIAN_POINT('Ctrl Pts',(-2.36520693660083,-1.22930933554557,
8.85675551444996));
#399368=CARTESIAN_POINT('Ctrl Pts',(-2.36524853540331,-1.22928745114724,
8.8566769979365));
#399369=CARTESIAN_POINT('Ctrl Pts',(-2.36528938769014,-1.22926653136241,
8.85659965593547));
#399370=CARTESIAN_POINT('Ctrl Pts',(-2.36584081394239,-1.22898415503921,
8.85555568965886));
#399371=CARTESIAN_POINT('Ctrl Pts',(-2.366411549463,-1.22879241075993,8.85434650606346));
#399372=CARTESIAN_POINT('Ctrl Pts',(-2.36700243645268,-1.22868445948991,
8.85297329937117));
#399373=CARTESIAN_POINT('Ctrl Pts',(-2.36733477438111,-1.22862374347808,
8.85220095427747));
#399374=CARTESIAN_POINT('Ctrl Pts',(-2.36767367938264,-1.22858981951854,
8.85137579139183));
#399375=CARTESIAN_POINT('Ctrl Pts',(-2.36802027905702,-1.22858372995532,
8.85049129520029));
#399376=CARTESIAN_POINT('Origin',(-2.36814105033894,-1.2354576690951,7.59394543036555));
#399377=CARTESIAN_POINT('Ctrl Pts',(-2.36212061052625,-1.238824577326,7.59443877723642));
#399378=CARTESIAN_POINT('Ctrl Pts',(-2.35889154920073,-1.23401767014937,
7.58783886950016));
#399379=CARTESIAN_POINT('Ctrl Pts',(-2.36465235257834,-1.22778129893036,
7.58559994247159));
#399380=CARTESIAN_POINT('Ctrl Pts',(-2.37974796156563,-1.26506534257455,
7.56670252222136));
#399381=CARTESIAN_POINT('Ctrl Pts',(-2.3765235671505,-1.26026538274347,
7.56004874999025));
#399382=CARTESIAN_POINT('Ctrl Pts',(-2.3823028110065,-1.25397756136332,
7.55786368756704));
#399383=CARTESIAN_POINT('Ctrl Pts',(-2.39734239528812,-1.29125710581576,
7.53888913333556));
#399384=CARTESIAN_POINT('Ctrl Pts',(-2.39409883813908,-1.28642861958838,
7.53222002137273));
#399385=CARTESIAN_POINT('Ctrl Pts',(-2.39991996700693,-1.28012648475776,
7.53005029815327));
#399386=CARTESIAN_POINT('Ctrl Pts',(-2.41490311553373,-1.31739868185466,
7.51101258149734));
#399387=CARTESIAN_POINT('Ctrl Pts',(-2.41162024057835,-1.31251166560067,
7.5043616886572));
#399388=CARTESIAN_POINT('Ctrl Pts',(-2.41750301869742,-1.30622673098315,
7.50217374673251));
#399389=CARTESIAN_POINT('',(-2.41656476362037,-1.30483398889127,7.50366116523517));
#399390=CARTESIAN_POINT('Ctrl Pts',(-2.41011908817657,-1.31027699133286,
7.51860402984325));
#399391=CARTESIAN_POINT('Ctrl Pts',(-2.41036533970193,-1.31064357099956,
7.51734760759493));
#399392=CARTESIAN_POINT('Ctrl Pts',(-2.41063725122379,-1.31094165149919,
7.51608817408572));
#399393=CARTESIAN_POINT('Ctrl Pts',(-2.41094406290928,-1.31116154777588,
7.51481005913119));
#399394=CARTESIAN_POINT('Ctrl Pts',(-2.4112219802655,-1.31136073507789,
7.51365231206383));
#399395=CARTESIAN_POINT('Ctrl Pts',(-2.41152877981015,-1.3114962550091,
7.51247773061042));
#399396=CARTESIAN_POINT('Ctrl Pts',(-2.41187407264667,-1.31153198601554,
7.51129758471022));
#399397=CARTESIAN_POINT('Ctrl Pts',(-2.41230323220854,-1.3115763955759,
7.50983079813402));
#399398=CARTESIAN_POINT('Ctrl Pts',(-2.41277949901876,-1.31145228193425,
7.50839324291155));
#399399=CARTESIAN_POINT('Ctrl Pts',(-2.41328555985522,-1.31107896397255,
7.50715379678855));
#399400=CARTESIAN_POINT('Ctrl Pts',(-2.41351934537987,-1.31090650183114,
7.50658120839351));
#399401=CARTESIAN_POINT('Ctrl Pts',(-2.41378708356349,-1.31064869179563,
7.50598221009429));
#399402=CARTESIAN_POINT('Ctrl Pts',(-2.41406662507935,-1.31029528425857,
7.50545747549611));
#399403=CARTESIAN_POINT('Ctrl Pts',(-2.41421579708484,-1.31010669505781,
7.50517746087247));
#399404=CARTESIAN_POINT('Ctrl Pts',(-2.41437010660959,-1.30988896396753,
7.50491486231392));
#399405=CARTESIAN_POINT('Ctrl Pts',(-2.41452410638099,-1.30964689238472,
7.50468370960993));
#399406=CARTESIAN_POINT('Ctrl Pts',(-2.41475438461572,-1.30928491901126,
7.50433806340447));
#399407=CARTESIAN_POINT('Ctrl Pts',(-2.41499040573442,-1.3088573680573,
7.50405484070983));
#399408=CARTESIAN_POINT('Ctrl Pts',(-2.41521564697535,-1.30839268806317,
7.50385766036131));
#399409=CARTESIAN_POINT('Ctrl Pts',(-2.41523973302503,-1.30834299776056,
7.50383657498791));
#399410=CARTESIAN_POINT('Ctrl Pts',(-2.41526369813398,-1.30829291115476,
7.50381643264937));
#399411=CARTESIAN_POINT('Ctrl Pts',(-2.41528752410889,-1.30824248354154,
7.50379723213559));
#399412=CARTESIAN_POINT('Ctrl Pts',(-2.41544657028544,-1.30790586272728,
7.50366906242519));
#399413=CARTESIAN_POINT('Ctrl Pts',(-2.41560222613725,-1.30754641716599,
7.50358235568538));
#399414=CARTESIAN_POINT('Ctrl Pts',(-2.41574393100536,-1.30719634939656,
7.5035341175365));
#399415=CARTESIAN_POINT('Ctrl Pts',(-2.41595640141719,-1.30667146239633,
7.50346178989176));
#399416=CARTESIAN_POINT('Ctrl Pts',(-2.41616265364207,-1.30609776943105,
7.50346967198527));
#399417=CARTESIAN_POINT('Ctrl Pts',(-2.41634780009116,-1.30552835049683,
7.50354272648692));
#399418=CARTESIAN_POINT('Ctrl Pts',(-2.41642395465797,-1.30529413670291,
7.50357277531559));
#399419=CARTESIAN_POINT('Ctrl Pts',(-2.41649657211345,-1.30506100104882,
7.50361331098761));
#399420=CARTESIAN_POINT('Ctrl Pts',(-2.41656476362162,-1.30483398889194,
7.50366116523659));
#399421=CARTESIAN_POINT('',(-2.37073694677504,-1.23681194660284,7.57603338622103));
#399422=CARTESIAN_POINT('Origin',(-2.37857308999325,-1.24089683938842,7.58486873427628));
#399423=CARTESIAN_POINT('Ctrl Pts',(-2.41656476364782,-1.30483398894162,
7.50366116529969));
#399424=CARTESIAN_POINT('Ctrl Pts',(-2.40131444507885,-1.2821965071394,
7.52783573079709));
#399425=CARTESIAN_POINT('Ctrl Pts',(-2.38603924224883,-1.25952355358678,
7.55196141284069));
#399426=CARTESIAN_POINT('Ctrl Pts',(-2.37073694715285,-1.23681194779654,
7.57603338728831));
#399427=CARTESIAN_POINT('Ctrl Pts',(-2.36243414091425,-1.23929131094305,
7.59394543036555));
#399428=CARTESIAN_POINT('Ctrl Pts',(-2.35539033864858,-1.22880563097346,
7.59394543036555));
#399429=CARTESIAN_POINT('Ctrl Pts',(-2.36802027905701,-1.22858372995532,
7.59394543036555));
#399430=CARTESIAN_POINT('Ctrl Pts',(-2.36113314698054,-1.23735460041134,
7.58587155981958));
#399431=CARTESIAN_POINT('Ctrl Pts',(-2.36057594445157,-1.23151095819934,
7.58685956158229));
#399432=CARTESIAN_POINT('Ctrl Pts',(-2.36568752250954,-1.22862471518852,
7.5858715598196));
#399433=CARTESIAN_POINT('Ctrl Pts',(-2.36649208760835,-1.23674115119295,
7.57982961904598));
#399434=CARTESIAN_POINT('Ctrl Pts',(-2.36590782788217,-1.23429259836977,
7.58148017275035));
#399435=CARTESIAN_POINT('Ctrl Pts',(-2.36825032769483,-1.2333709341234,
7.57982961904596));
#399436=CARTESIAN_POINT('Ctrl Pts',(-2.37073694604122,-1.23681194622024,
7.57603338509286));
#399437=CARTESIAN_POINT('Ctrl Pts',(-2.37073694604122,-1.23681194622024,
7.57603338509286));
#399438=CARTESIAN_POINT('Ctrl Pts',(-2.37073694604122,-1.23681194622024,
7.57603338509286));
#399439=CARTESIAN_POINT('Origin',(-2.37857045058693,-1.24090189863649,7.5848687342762));
#399440=CARTESIAN_POINT('Ctrl Pts',(-2.46212726359303,-1.22693032265427,
7.51098857897448));
#399441=CARTESIAN_POINT('Ctrl Pts',(-2.45624085415416,-1.2270337435894,
7.50433767179956));
#399442=CARTESIAN_POINT('Ctrl Pts',(-2.45445176918726,-1.23545438644275,
7.50214974420965));
#399443=CARTESIAN_POINT('Ctrl Pts',(-2.43063083103924,-1.22748369743084,
7.5388732158917));
#399444=CARTESIAN_POINT('Ctrl Pts',(-2.42481495123192,-1.22758587919962,
7.53220407452063));
#399445=CARTESIAN_POINT('Ctrl Pts',(-2.42297646352332,-1.23596578867809,
7.53003438070912));
#399446=CARTESIAN_POINT('Ctrl Pts',(-2.39907391371632,-1.22803813489112,
7.5666946565923));
#399447=CARTESIAN_POINT('Ctrl Pts',(-2.39329240467737,-1.22813971278464,
7.56004085833294));
#399448=CARTESIAN_POINT('Ctrl Pts',(-2.39144168852526,-1.23647706847156,
7.55785582193789));
#399449=CARTESIAN_POINT('Ctrl Pts',(-2.36745793881747,-1.22859360996011,
7.59443891967696));
#399450=CARTESIAN_POINT('Ctrl Pts',(-2.36166804731027,-1.22869533512894,
7.58783901202978));
#399451=CARTESIAN_POINT('Ctrl Pts',(-2.35984900020427,-1.23698811787145,
7.58560008491213));
#399452=CARTESIAN_POINT('',(-2.45274559607508,-1.23548210681974,7.50366116523517));
#399453=CARTESIAN_POINT('Ctrl Pts',(-2.45274559607542,-1.23548210681991,
7.50366116523554));
#399454=CARTESIAN_POINT('Ctrl Pts',(-2.45321593518388,-1.23488803726184,
7.50350835821027));
#399455=CARTESIAN_POINT('Ctrl Pts',(-2.45362896354645,-1.23432664116028,
7.50345484956));
#399456=CARTESIAN_POINT('Ctrl Pts',(-2.45399744452925,-1.2337815836168,
7.50349758195598));
#399457=CARTESIAN_POINT('Ctrl Pts',(-2.45418650260068,-1.23350192867448,
7.50351950684424));
#399458=CARTESIAN_POINT('Ctrl Pts',(-2.45438257535525,-1.23319908335874,
7.50357029184312));
#399459=CARTESIAN_POINT('Ctrl Pts',(-2.45456361872821,-1.23290185592395,
7.50365515313924));
#399460=CARTESIAN_POINT('Ctrl Pts',(-2.45484213674753,-1.23244459976998,
7.50378570417639));
#399461=CARTESIAN_POINT('Ctrl Pts',(-2.45509355696109,-1.23198739767573,
7.50400001621911));
#399462=CARTESIAN_POINT('Ctrl Pts',(-2.45529675319047,-1.23156395534119,
7.50428903009634));
#399463=CARTESIAN_POINT('Ctrl Pts',(-2.45531930640863,-1.23151695649982,
7.50432110841318));
#399464=CARTESIAN_POINT('Ctrl Pts',(-2.45534129185356,-1.23147035849846,
7.50435406373354));
#399465=CARTESIAN_POINT('Ctrl Pts',(-2.45536269990847,-1.2314241960473,
7.50438785222352));
#399466=CARTESIAN_POINT('Ctrl Pts',(-2.4554934063737,-1.23114235209449,
7.50459414719561));
#399467=CARTESIAN_POINT('Ctrl Pts',(-2.45560420262761,-1.23087203987398,
7.50483629897752));
#399468=CARTESIAN_POINT('Ctrl Pts',(-2.45569206180922,-1.23062411408571,
7.5050991045531));
#399469=CARTESIAN_POINT('Ctrl Pts',(-2.45588588798846,-1.23007716489501,
7.50567888004914));
#399470=CARTESIAN_POINT('Ctrl Pts',(-2.45597621046602,-1.22961778862667,
7.50637912803144));
#399471=CARTESIAN_POINT('Ctrl Pts',(-2.4559938634216,-1.22924382386499,
7.50710440483569));
#399472=CARTESIAN_POINT('Ctrl Pts',(-2.45599819227677,-1.22915212028119,
7.50728225710685));
#399473=CARTESIAN_POINT('Ctrl Pts',(-2.45599838327278,-1.22906373407087,
7.50746498566954));
#399474=CARTESIAN_POINT('Ctrl Pts',(-2.45599484854337,-1.22898072935445,
7.50764697238949));
#399475=CARTESIAN_POINT('Ctrl Pts',(-2.45597584681086,-1.22853451884254,
7.50862528291181));
#399476=CARTESIAN_POINT('Ctrl Pts',(-2.45585158784299,-1.22820314295458,
7.50965856837421));
#399477=CARTESIAN_POINT('Ctrl Pts',(-2.45567561046203,-1.22794749938438,
7.51067959873201));
#399478=CARTESIAN_POINT('Ctrl Pts',(-2.45557876988733,-1.22780681840524,
7.51124147302578));
#399479=CARTESIAN_POINT('Ctrl Pts',(-2.45546588589086,-1.22768928353924,
7.51180065547252));
#399480=CARTESIAN_POINT('Ctrl Pts',(-2.45534370115125,-1.22758999909432,
7.51235175716501));
#399481=CARTESIAN_POINT('Ctrl Pts',(-2.45492150420326,-1.2272469317869,
7.51425603304537));
#399482=CARTESIAN_POINT('Ctrl Pts',(-2.45433409491521,-1.22708557269673,
7.51626900505184));
#399483=CARTESIAN_POINT('Ctrl Pts',(-2.45363638664935,-1.22708087806129,
7.51827788969249));
#399484=CARTESIAN_POINT('Ctrl Pts',(-2.45359862535952,-1.22708062397875,
7.51838661432549));
#399485=CARTESIAN_POINT('Ctrl Pts',(-2.45356053346671,-1.22708083533095,
7.51849533314858));
#399486=CARTESIAN_POINT('Ctrl Pts',(-2.45352211735224,-1.22708151028068,
7.51860402984325));
#399487=CARTESIAN_POINT('Ctrl Pts',(-2.37073694797139,-1.23681194623012,
7.57603338728985));
#399488=CARTESIAN_POINT('Ctrl Pts',(-2.39811907486656,-1.23636877604872,
7.55196141284922));
#399489=CARTESIAN_POINT('Ctrl Pts',(-2.42545400034854,-1.23592549913143,
7.52783573083105));
#399490=CARTESIAN_POINT('Ctrl Pts',(-2.45274559613392,-1.23548210681335,
7.50366116530176));
#399491=CARTESIAN_POINT('Origin',(-8.19199203866628E-16,-4.27375699935092E-16,
7.49482233047033));
#399492=CARTESIAN_POINT('Origin',(-2.40878727587058,-1.30063450269628,7.49482233047033));
#399493=CARTESIAN_POINT('Origin',(0.,0.,7.50366116523517));
#399494=CARTESIAN_POINT('Origin',(-2.44485166369885,-1.231505823173,7.49482233047033));
#399495=CARTESIAN_POINT('Ctrl Pts',(-2.41011849833278,-1.31027611334853,
7.51860402984325));
#399496=CARTESIAN_POINT('Ctrl Pts',(-2.41436194636776,-1.31659192167404,
7.51860402984325));
#399497=CARTESIAN_POINT('Ctrl Pts',(-2.41070061931036,-1.32326207686031,
7.51860402984325));
#399498=CARTESIAN_POINT('Ctrl Pts',(-2.4116941184922,-1.31262121678979,
7.51041458714366));
#399499=CARTESIAN_POINT('Ctrl Pts',(-2.41349452737362,-1.31817215307297,
7.51004642900442));
#399500=CARTESIAN_POINT('Ctrl Pts',(-2.41069960955983,-1.32326391640991,
7.5072913648301));
#399501=CARTESIAN_POINT('Ctrl Pts',(-2.41442875339229,-1.31195375206223,
7.50215815450137));
#399502=CARTESIAN_POINT('Ctrl Pts',(-2.41526080207569,-1.31495471182036,
7.49877163671531));
#399503=CARTESIAN_POINT('Ctrl Pts',(-2.41362156250511,-1.31799063296964,
7.4948158853317));
#399504=CARTESIAN_POINT('Ctrl Pts',(-2.41656427920751,-1.30483372733004,
7.50366171572174));
#399505=CARTESIAN_POINT('Ctrl Pts',(-2.41978630452771,-1.30657347302789,
7.50000045605858));
#399506=CARTESIAN_POINT('Ctrl Pts',(-2.41978630452765,-1.306573473028,7.49482233047317));
#399507=CARTESIAN_POINT('Origin',(-2.39974288922259,-1.31724724923822,7.51860402984325));
#399508=CARTESIAN_POINT('Origin',(-2.39974288922259,-1.31724724923822,9.));
#399509=CARTESIAN_POINT('Origin',(-2.39974288922259,-1.31724724923822,8.75721825406948));
#399510=CARTESIAN_POINT('Ctrl Pts',(-2.40080670870025,-1.29641427264099,
8.78942910404913));
#399511=CARTESIAN_POINT('Ctrl Pts',(-2.40393078786281,-1.30102865863348,
8.7967269950169));
#399512=CARTESIAN_POINT('Ctrl Pts',(-2.39758410530013,-1.30730505142159,
8.79893251111266));
#399513=CARTESIAN_POINT('Ctrl Pts',(-2.40693738091791,-1.30554062333008,
8.78111911759582));
#399514=CARTESIAN_POINT('Ctrl Pts',(-2.41063484895981,-1.31101520461129,
8.78644465894813));
#399515=CARTESIAN_POINT('Ctrl Pts',(-2.40622746632977,-1.31781891610782,
8.78817647674133));
#399516=CARTESIAN_POINT('Ctrl Pts',(-2.41075816204787,-1.31122838278126,
8.76780923932031));
#399517=CARTESIAN_POINT('Ctrl Pts',(-2.41511864407147,-1.31769374690807,
8.76988516158374));
#399518=CARTESIAN_POINT('Ctrl Pts',(-2.41161733062359,-1.32439279046189,
8.77093053738832));
#399519=CARTESIAN_POINT('Ctrl Pts',(-2.41001316201716,-1.31011934753171,
8.75371302330492));
#399520=CARTESIAN_POINT('Ctrl Pts',(-2.41426725614076,-1.31642560510298,
8.75300828287559));
#399521=CARTESIAN_POINT('Ctrl Pts',(-2.41056573435197,-1.32311090807153,
8.75267964240738));
#399522=CARTESIAN_POINT('Origin',(-2.3919236086638,-1.30560716190478,8.78727029226991));
#399523=CARTESIAN_POINT('Ctrl Pts',(-2.36243414091425,-1.23929131094305,
8.85049129520029));
#399524=CARTESIAN_POINT('Ctrl Pts',(-2.36569043114742,-1.2441387521382,
8.85711686593484));
#399525=CARTESIAN_POINT('Ctrl Pts',(-2.35986814900602,-1.2503998856442,
8.85933012996512));
#399526=CARTESIAN_POINT('Ctrl Pts',(-2.37574203054419,-1.25910195673735,
8.82945683644722));
#399527=CARTESIAN_POINT('Ctrl Pts',(-2.3790253499551,-1.26398963462525,
8.83607469902389));
#399528=CARTESIAN_POINT('Ctrl Pts',(-2.37315851053407,-1.27024361237588,
8.83829567148519));
#399529=CARTESIAN_POINT('Ctrl Pts',(-2.38903008369151,-1.2788830731666,
8.80838214965002));
#399530=CARTESIAN_POINT('Ctrl Pts',(-2.39232636061376,-1.28379004011343,
8.81501364461988));
#399531=CARTESIAN_POINT('Ctrl Pts',(-2.38642926673664,-1.2900568651788,
8.81722098428721));
#399532=CARTESIAN_POINT('Ctrl Pts',(-2.40229980761779,-1.29863690399942,
8.78727029226991));
#399533=CARTESIAN_POINT('Ctrl Pts',(-2.40559663206246,-1.3035446860096,
8.79393457792714));
#399534=CARTESIAN_POINT('Ctrl Pts',(-2.39968192566132,-1.30984196029031,
8.79610912703474));
#399535=CARTESIAN_POINT('Origin',(-2.35205794196026,-1.24626156884841,8.85049129520029));
#399536=CARTESIAN_POINT('Ctrl Pts',(-2.36802027905702,-1.22858372995532,
8.85049129520029));
#399537=CARTESIAN_POINT('Ctrl Pts',(-2.37385899372366,-1.22848114699077,
8.85711686593484));
#399538=CARTESIAN_POINT('Ctrl Pts',(-2.37566317709458,-1.22012377392993,
8.85933012996512));
#399539=CARTESIAN_POINT('Ctrl Pts',(-2.36285485247417,-1.22867448362326,
8.86332496987232));
#399540=CARTESIAN_POINT('Ctrl Pts',(-2.36523842990886,-1.22471589132427,
8.86648636486737));
#399541=CARTESIAN_POINT('Ctrl Pts',(-2.36121298657355,-1.22039479101916,
8.87206031107457));
#399542=CARTESIAN_POINT('Ctrl Pts',(-2.35953377205362,-1.23497370824507,
8.86341338519875));
#399543=CARTESIAN_POINT('Ctrl Pts',(-2.3576183774015,-1.23919327385791,
8.86654584966058));
#399544=CARTESIAN_POINT('Ctrl Pts',(-2.35175919171291,-1.23830215329704,
8.87215952290714));
#399545=CARTESIAN_POINT('Ctrl Pts',(-2.36243414091425,-1.23929131094305,
8.85049129520029));
#399546=CARTESIAN_POINT('Ctrl Pts',(-2.36569043114742,-1.2441387521382,
8.85711686593484));
#399547=CARTESIAN_POINT('Ctrl Pts',(-2.35986814900602,-1.2503998856442,
8.85933012996512));
#399548=CARTESIAN_POINT('Origin',(-2.36780069490806,-1.21608565879207,8.85049129520029));
#399549=CARTESIAN_POINT('Ctrl Pts',(-2.43950170000242,-1.2273278412042,
8.78727029226991));
#399550=CARTESIAN_POINT('Ctrl Pts',(-2.44541309482908,-1.22722398128972,
8.79393457792714));
#399551=CARTESIAN_POINT('Ctrl Pts',(-2.44719404240188,-1.21877012767606,
8.79610912703474));
#399552=CARTESIAN_POINT('Ctrl Pts',(-2.41570832589788,-1.22774587753439,
8.80838214965002));
#399553=CARTESIAN_POINT('Ctrl Pts',(-2.42161873898549,-1.22764203486851,
8.81501364461987));
#399554=CARTESIAN_POINT('Ctrl Pts',(-2.42338478937514,-1.21922004706179,
8.81722098428721));
#399555=CARTESIAN_POINT('Ctrl Pts',(-2.39188208645153,-1.22816449129034,
8.82945683644722));
#399556=CARTESIAN_POINT('Ctrl Pts',(-2.39776926598008,-1.22806105682515,
8.83607469902391));
#399557=CARTESIAN_POINT('Ctrl Pts',(-2.39954208843695,-1.21967123304667,
8.8382956714852));
#399558=CARTESIAN_POINT('Ctrl Pts',(-2.36802027905702,-1.22858372995532,
8.85049129520029));
#399559=CARTESIAN_POINT('Ctrl Pts',(-2.37385899372366,-1.22848114699077,
8.85711686593484));
#399560=CARTESIAN_POINT('Ctrl Pts',(-2.37566317709458,-1.22012377392993,
8.85933012996512));
#399561=CARTESIAN_POINT('Origin',(-2.43928211585347,-1.21482977004095,8.78727029226991));
#399562=CARTESIAN_POINT('Ctrl Pts',(-2.45333698446993,-1.22708474451239,
8.75374538247849));
#399563=CARTESIAN_POINT('Ctrl Pts',(-2.46093500328082,-1.22696437617394,
8.75304829418602));
#399564=CARTESIAN_POINT('Ctrl Pts',(-2.46430190265075,-1.22011349069528,
8.75272238421917));
#399565=CARTESIAN_POINT('Ctrl Pts',(-2.45465676447428,-1.22706155713946,
8.76769408445017));
#399566=CARTESIAN_POINT('Ctrl Pts',(-2.46244597221954,-1.22693746977904,
8.76974318093968));
#399567=CARTESIAN_POINT('Ctrl Pts',(-2.46593649005344,-1.22024160220782,
8.77077869880429));
#399568=CARTESIAN_POINT('Ctrl Pts',(-2.44789232400141,-1.22718040241891,
8.78108014887994));
#399569=CARTESIAN_POINT('Ctrl Pts',(-2.45449345748878,-1.22707904176505,
8.78639403366326));
#399570=CARTESIAN_POINT('Ctrl Pts',(-2.45756595314955,-1.2195902604127,
8.78812224174742));
#399571=CARTESIAN_POINT('Ctrl Pts',(-2.43680689933132,-1.22737516356142,
8.78944554828685));
#399572=CARTESIAN_POINT('Ctrl Pts',(-2.44237017583329,-1.22729533762872,
8.79673892988686));
#399573=CARTESIAN_POINT('Ctrl Pts',(-2.44388779729733,-1.21850896298338,
8.79894799272499));
#399574=CARTESIAN_POINT('Origin',(-2.45330253320329,-1.21458343911744,8.75721825406948));
#399575=CARTESIAN_POINT('Origin',(-2.45330253320329,-1.21458343911744,9.));
#399576=CARTESIAN_POINT('Origin',(-2.45330253320329,-1.21458343911744,7.51860402984325));
#399577=CARTESIAN_POINT('Ctrl Pts',(-2.45274489350846,-1.23548175292708,
7.50366195182967));
#399578=CARTESIAN_POINT('Ctrl Pts',(-2.45601536992584,-1.23712913743394,
7.50000065167736));
#399579=CARTESIAN_POINT('Ctrl Pts',(-2.4560153699259,-1.23712913743383,
7.49482233047108));
#399580=CARTESIAN_POINT('Ctrl Pts',(-2.45736618897609,-1.22965102160009,
7.50215800491335));
#399581=CARTESIAN_POINT('Ctrl Pts',(-2.46030407593303,-1.22861491475103,
7.49877273257261));
#399582=CARTESIAN_POINT('Ctrl Pts',(-2.46185708707724,-1.22553184603044,
7.49481816995644));
#399583=CARTESIAN_POINT('Ctrl Pts',(-2.45634027370535,-1.22703233601387,
7.51043025814045));
#399584=CARTESIAN_POINT('Ctrl Pts',(-2.46192726936052,-1.22533579938412,
7.51006209594519));
#399585=CARTESIAN_POINT('Ctrl Pts',(-2.46450595122239,-1.2201272132019,
7.50731281821703));
#399586=CARTESIAN_POINT('Ctrl Pts',(-2.45352060617641,-1.22708153673981,
7.51860402984326));
#399587=CARTESIAN_POINT('Ctrl Pts',(-2.46112871992397,-1.22694878661776,
7.51860402984326));
#399588=CARTESIAN_POINT('Ctrl Pts',(-2.46450482787545,-1.22012948221843,
7.51860402984327));
#399589=CARTESIAN_POINT('Origin',(0.,0.,7.5));
#399590=CARTESIAN_POINT('Origin',(-2.28443929758135,-1.37777905311491,7.5));
#399591=CARTESIAN_POINT('',(-2.28443929758135,-1.37777905311491,7.59394543036555));
#399592=CARTESIAN_POINT('',(-2.28443929758135,-1.37777905311491,8.85049129520029));
#399593=CARTESIAN_POINT('',(-2.28443929758135,-1.37777905311491,7.5));
#399594=CARTESIAN_POINT('',(-2.35585431734963,-1.38110557508643,8.78727029226991));
#399595=CARTESIAN_POINT('Ctrl Pts',(-2.28443929758135,-1.37777905311491,
8.85049129520029));
#399596=CARTESIAN_POINT('Ctrl Pts',(-2.30827890705324,-1.37888950557936,
8.82945686509571));
#399597=CARTESIAN_POINT('Ctrl Pts',(-2.33208307606301,-1.37999830722195,
8.80838212259896));
#399598=CARTESIAN_POINT('Ctrl Pts',(-2.35585431734963,-1.38110557508643,
8.78727029226991));
#399599=CARTESIAN_POINT('',(-2.36986171072477,-1.38175804150004,8.75721825406948));
#399600=CARTESIAN_POINT('Origin',(-2.32770859547033,-1.37979474530314,8.75937679713115));
#399601=CARTESIAN_POINT('',(-2.36986171072477,-1.38175804150004,7.51860402984325));
#399602=CARTESIAN_POINT('',(-2.36986171072477,-1.38175804150004,7.5));
#399603=CARTESIAN_POINT('Ctrl Pts',(-2.36986171072477,-1.38175804150004,
7.51860402984325));
#399604=CARTESIAN_POINT('Ctrl Pts',(-2.35886108179034,-1.38124563060987,
7.52834476460825));
#399605=CARTESIAN_POINT('Ctrl Pts',(-2.34785331140635,-1.38073288706995,
7.53807742314407));
#399606=CARTESIAN_POINT('Ctrl Pts',(-2.33683815978911,-1.38021979971112,
7.54780169004674));
#399607=CARTESIAN_POINT('Ctrl Pts',(-2.31939075494556,-1.37940709706472,
7.5632044032688));
#399608=CARTESIAN_POINT('Ctrl Pts',(-2.30192480935483,-1.37859353078762,
7.57858609112103));
#399609=CARTESIAN_POINT('Ctrl Pts',(-2.28443929758135,-1.37777905311491,
7.59394543036555));
#399610=CARTESIAN_POINT('Origin',(-2.41658349078374,-1.62573897887916,7.5));
#399611=CARTESIAN_POINT('',(-2.32121750495509,-1.46200174688659,8.75721825406948));
#399612=CARTESIAN_POINT('',(-2.31416007290288,-1.44988459233548,8.78727029226991));
#399613=CARTESIAN_POINT('Origin',(-2.29624567806399,-1.41912673461236,8.75658640621088));
#399614=CARTESIAN_POINT('',(-2.27817859968916,-1.38810672912947,8.85049129520029));
#399615=CARTESIAN_POINT('Ctrl Pts',(-2.31416007290288,-1.44988459233548,
8.78727029226991));
#399616=CARTESIAN_POINT('Ctrl Pts',(-2.30218326068066,-1.42932118008402,
8.80838212259897));
#399617=CARTESIAN_POINT('Ctrl Pts',(-2.29018985827905,-1.40872928356715,
8.82945686509571));
#399618=CARTESIAN_POINT('Ctrl Pts',(-2.27817859968917,-1.38810672912947,
8.85049129520029));
#399619=CARTESIAN_POINT('',(-2.27817859968916,-1.38810672912947,7.59394543036555));
#399620=CARTESIAN_POINT('',(-2.27817859968916,-1.38810672912947,7.5));
#399621=CARTESIAN_POINT('',(-2.32121750495509,-1.46200174688659,7.51860402984325));
#399622=CARTESIAN_POINT('Ctrl Pts',(-2.27817859968916,-1.38810672912946,
7.59394543036555));
#399623=CARTESIAN_POINT('Ctrl Pts',(-2.28698843374854,-1.40323264462922,
7.57858609112103));
#399624=CARTESIAN_POINT('Ctrl Pts',(-2.29578840965637,-1.41834163432013,
7.56320440326857));
#399625=CARTESIAN_POINT('Ctrl Pts',(-2.30457904406443,-1.43343458525989,
7.54780169004651));
#399626=CARTESIAN_POINT('Ctrl Pts',(-2.31012887635666,-1.44296328849363,
7.53807742314383));
#399627=CARTESIAN_POINT('Ctrl Pts',(-2.31567498971638,-1.45248560656069,
7.52834476460825));
#399628=CARTESIAN_POINT('Ctrl Pts',(-2.32121750495509,-1.46200174688659,
7.51860402984325));
#399629=CARTESIAN_POINT('',(-2.32121750495509,-1.46200174688659,7.5));
#399630=CARTESIAN_POINT('Origin',(-2.28411940593291,-1.3846466068521,7.5));
#399631=CARTESIAN_POINT('Ctrl Pts',(-2.27817859968916,-1.38810672912947,
8.85049129520029));
#399632=CARTESIAN_POINT('Ctrl Pts',(-2.27808113169049,-1.38793938287732,
8.85097269580138));
#399633=CARTESIAN_POINT('Ctrl Pts',(-2.2779921618778,-1.38776991462375,
8.85143669361005));
#399634=CARTESIAN_POINT('Ctrl Pts',(-2.27790836757131,-1.38759011450948,
8.8519052845931));
#399635=CARTESIAN_POINT('Ctrl Pts',(-2.27774447122186,-1.38723843688848,
8.85282181883899));
#399636=CARTESIAN_POINT('Ctrl Pts',(-2.27760476931615,-1.38685619637747,
8.85372622499635));
#399637=CARTESIAN_POINT('Ctrl Pts',(-2.27750155151867,-1.38643210212428,
8.8546225773507));
#399638=CARTESIAN_POINT('Ctrl Pts',(-2.27741586376915,-1.38608003413768,
8.85536669723986));
#399639=CARTESIAN_POINT('Ctrl Pts',(-2.27735526963749,-1.38569904887466,
8.85610498449051));
#399640=CARTESIAN_POINT('Ctrl Pts',(-2.27733469853656,-1.3852813971344,
8.85681338218371));
#399641=CARTESIAN_POINT('Ctrl Pts',(-2.27731603023015,-1.38490237752418,
8.85745625420284));
#399642=CARTESIAN_POINT('Ctrl Pts',(-2.27732949131404,-1.38448843593451,
8.85808743050666));
#399643=CARTESIAN_POINT('Ctrl Pts',(-2.27740126538765,-1.38402807170151,
8.8586680450841));
#399644=CARTESIAN_POINT('Ctrl Pts',(-2.27743438038934,-1.38381566962388,
8.85893592806395));
#399645=CARTESIAN_POINT('Ctrl Pts',(-2.27748014042396,-1.38359331526743,
8.85919241173848));
#399646=CARTESIAN_POINT('Ctrl Pts',(-2.27754269428292,-1.38335963403901,
8.85943017985534));
#399647=CARTESIAN_POINT('Ctrl Pts',(-2.27762716051044,-1.38304409520358,
8.8597512372));
#399648=CARTESIAN_POINT('Ctrl Pts',(-2.27774501555862,-1.38270003844088,
8.86004599534705));
#399649=CARTESIAN_POINT('Ctrl Pts',(-2.27790469650044,-1.38233497258254,
8.86026130871721));
#399650=CARTESIAN_POINT('Ctrl Pts',(-2.27796316019512,-1.3822013116795,
8.86034014101235));
#399651=CARTESIAN_POINT('Ctrl Pts',(-2.27802809754116,-1.38206282183858,
8.86040910639692));
#399652=CARTESIAN_POINT('Ctrl Pts',(-2.27809804391702,-1.38192341894475,
8.86046313645506));
#399653=CARTESIAN_POINT('Ctrl Pts',(-2.27820719465075,-1.38170588189641,
8.86054744990829));
#399654=CARTESIAN_POINT('Ctrl Pts',(-2.27833165395478,-1.38148024927838,
8.86059655985668));
#399655=CARTESIAN_POINT('Ctrl Pts',(-2.27846318335477,-1.38126085010038,
8.86059725258816));
#399656=CARTESIAN_POINT('Ctrl Pts',(-2.27859501664021,-1.38104094402262,
8.86059794692011));
#399657=CARTESIAN_POINT('Ctrl Pts',(-2.27873769344056,-1.38082622749523,
8.86056369958366));
#399658=CARTESIAN_POINT('Ctrl Pts',(-2.2788802978602,-1.3806263285976,8.86048590497774));
#399659=CARTESIAN_POINT('Ctrl Pts',(-2.27891751336788,-1.38057416093702,
8.86046560290182));
#399660=CARTESIAN_POINT('Ctrl Pts',(-2.27895528183715,-1.38052237637025,
8.86044257503091));
#399661=CARTESIAN_POINT('Ctrl Pts',(-2.27899240966943,-1.38047255574004,
8.86041778462583));
#399662=CARTESIAN_POINT('Ctrl Pts',(-2.27924223390885,-1.38013732472093,
8.86025097596201));
#399663=CARTESIAN_POINT('Ctrl Pts',(-2.27949684175642,-1.37984622804254,
8.8599848982295));
#399664=CARTESIAN_POINT('Ctrl Pts',(-2.2797424245759,-1.37960218414176,
8.85968173251462));
#399665=CARTESIAN_POINT('Ctrl Pts',(-2.27987232381719,-1.3794730989003,
8.85952137522077));
#399666=CARTESIAN_POINT('Ctrl Pts',(-2.28000206733073,-1.37935455443871,
8.85934740853961));
#399667=CARTESIAN_POINT('Ctrl Pts',(-2.28012877685891,-1.37924707484726,
8.8591675900182));
#399668=CARTESIAN_POINT('Ctrl Pts',(-2.28063758147687,-1.3788154884208,
8.85844552518695));
#399669=CARTESIAN_POINT('Ctrl Pts',(-2.28112426400981,-1.37853561654659,
8.85759444184125));
#399670=CARTESIAN_POINT('Ctrl Pts',(-2.28154157522219,-1.37834306627385,
8.85683498915139));
#399671=CARTESIAN_POINT('Ctrl Pts',(-2.28158524572917,-1.37832291640061,
8.85675551444998));
#399672=CARTESIAN_POINT('Ctrl Pts',(-2.28162816120068,-1.37830374221055,
8.85667699793651));
#399673=CARTESIAN_POINT('Ctrl Pts',(-2.28167026988732,-1.37828548282266,
8.85659965593547));
#399674=CARTESIAN_POINT('Ctrl Pts',(-2.28223865508834,-1.37803901667319,
8.85555568965886));
#399675=CARTESIAN_POINT('Ctrl Pts',(-2.28282050306977,-1.37788423350345,
8.85434650606346));
#399676=CARTESIAN_POINT('Ctrl Pts',(-2.28341709248037,-1.3778143622903,
8.85297329937118));
#399677=CARTESIAN_POINT('Ctrl Pts',(-2.28375263767312,-1.37777506399021,
8.85220095427748));
#399678=CARTESIAN_POINT('Ctrl Pts',(-2.28409301987352,-1.37776292344909,
8.85137579139184));
#399679=CARTESIAN_POINT('Ctrl Pts',(-2.28443929758135,-1.37777905311491,
8.85049129520029));
#399680=CARTESIAN_POINT('Origin',(-2.28411940593291,-1.3846466068521,7.59394543036555));
#399681=CARTESIAN_POINT('Ctrl Pts',(-2.27789561720849,-1.38762086650575,
7.59443877723642));
#399682=CARTESIAN_POINT('Ctrl Pts',(-2.27498116993602,-1.382616948966,7.58783886950016));
#399683=CARTESIAN_POINT('Ctrl Pts',(-2.28112970280112,-1.37676248698019,
7.58559994247159));
#399684=CARTESIAN_POINT('Ctrl Pts',(-2.29380549936271,-1.41493710554657,
7.56670252222137));
#399685=CARTESIAN_POINT('Ctrl Pts',(-2.29089526429399,-1.40994042008827,
7.56004874999026));
#399686=CARTESIAN_POINT('Ctrl Pts',(-2.29706549617267,-1.40403579513669,
7.55786368756705));
#399687=CARTESIAN_POINT('Ctrl Pts',(-2.30968567140157,-1.44220233424018,
7.53888913333557));
#399688=CARTESIAN_POINT('Ctrl Pts',(-2.30675814066331,-1.43717595323558,
7.53222002137276));
#399689=CARTESIAN_POINT('Ctrl Pts',(-2.31297108856254,-1.43125972782393,
7.53005029815326));
#399690=CARTESIAN_POINT('Ctrl Pts',(-2.32553541473659,-1.46941531881658,
7.51101258149734));
#399691=CARTESIAN_POINT('Ctrl Pts',(-2.32257239700634,-1.46432800894105,
7.5043616886572));
#399692=CARTESIAN_POINT('Ctrl Pts',(-2.32884576547034,-1.45843289828395,
7.50217374673251));
#399693=CARTESIAN_POINT('',(-2.32799867143118,-1.45698290352088,7.50366116523517));
#399694=CARTESIAN_POINT('Ctrl Pts',(-2.32121750495509,-1.46200174688659,
7.51860402984325));
#399695=CARTESIAN_POINT('Ctrl Pts',(-2.32143976369039,-1.46238335076545,
7.51734760759494));
#399696=CARTESIAN_POINT('Ctrl Pts',(-2.32169201845768,-1.46269824025774,
7.51608817408573));
#399697=CARTESIAN_POINT('Ctrl Pts',(-2.32198411096284,-1.46293734222612,
7.51481005913121));
#399698=CARTESIAN_POINT('Ctrl Pts',(-2.32224869533379,-1.46315392650261,
7.51365231206384));
#399699=CARTESIAN_POINT('Ctrl Pts',(-2.32254618173406,-1.46330882470791,
7.51247773061043));
#399700=CARTESIAN_POINT('Ctrl Pts',(-2.32288847583598,-1.46336660528915,
7.51129758471022));
#399701=CARTESIAN_POINT('Ctrl Pts',(-2.32331390831319,-1.46343841995285,
7.50983079813401));
#399702=CARTESIAN_POINT('Ctrl Pts',(-2.3237971485705,-1.46334507583529,
7.50839324291155));
#399703=CARTESIAN_POINT('Ctrl Pts',(-2.32432608821462,-1.46300494832449,
7.50715379678855));
#399704=CARTESIAN_POINT('Ctrl Pts',(-2.32457044308918,-1.46284781921504,
7.50658120839351));
#399705=CARTESIAN_POINT('Ctrl Pts',(-2.32485414912167,-1.46260769292222,
7.50598221009429));
#399706=CARTESIAN_POINT('Ctrl Pts',(-2.32515575918815,-1.46227292178526,
7.50545747549611));
#399707=CARTESIAN_POINT('Ctrl Pts',(-2.32531670765533,-1.46209427754445,
7.50517746087247));
#399708=CARTESIAN_POINT('Ctrl Pts',(-2.32548465021346,-1.46188688045124,
7.50491486231392));
#399709=CARTESIAN_POINT('Ctrl Pts',(-2.32565384315538,-1.46165517302969,
7.50468370960992));
#399710=CARTESIAN_POINT('Ctrl Pts',(-2.32590683997245,-1.4613086973465,
7.50433806340446));
#399711=CARTESIAN_POINT('Ctrl Pts',(-2.32616976944412,-1.46089714676683,
7.50405484070983));
#399712=CARTESIAN_POINT('Ctrl Pts',(-2.32642432005221,-1.46044785276343,
7.5038576603613));
#399713=CARTESIAN_POINT('Ctrl Pts',(-2.32645154028313,-1.46039980775338,
7.5038365749879));
#399714=CARTESIAN_POINT('Ctrl Pts',(-2.32647866521305,-1.46035135950569,
7.50381643264937));
#399715=CARTESIAN_POINT('Ctrl Pts',(-2.32650567314321,-1.46030256203687,
7.50379723213559));
#399716=CARTESIAN_POINT('Ctrl Pts',(-2.32668595991195,-1.45997682296968,
7.50366906242519));
#399717=CARTESIAN_POINT('Ctrl Pts',(-2.3268643257083,-1.45962808883252,
7.50358235568538));
#399718=CARTESIAN_POINT('Ctrl Pts',(-2.32702816834756,-1.45928781937694,
7.5035341175365));
#399719=CARTESIAN_POINT('Ctrl Pts',(-2.32727383184171,-1.45877762383937,
7.50346178989176));
#399720=CARTESIAN_POINT('Ctrl Pts',(-2.32751641693377,-1.45821832421323,
7.50346967198527));
#399721=CARTESIAN_POINT('Ctrl Pts',(-2.32773766577599,-1.45766193758501,
7.50354272648692));
#399722=CARTESIAN_POINT('Ctrl Pts',(-2.32782867000438,-1.4574330842483,
7.50357277531559));
#399723=CARTESIAN_POINT('Ctrl Pts',(-2.32791607531215,-1.45720508021275,
7.50361331098761));
#399724=CARTESIAN_POINT('Ctrl Pts',(-2.32799867143238,-1.45698290352164,
7.50366116523659));
#399725=CARTESIAN_POINT('',(-2.28662319996353,-1.38616442150716,7.57603338622103));
#399726=CARTESIAN_POINT('Origin',(-2.29418152300564,-1.39074298486218,7.58486873427625));
#399727=CARTESIAN_POINT('Ctrl Pts',(-2.32799867145535,-1.45698290357288,
7.50366116529969));
#399728=CARTESIAN_POINT('Ctrl Pts',(-2.31423007474035,-1.4334148416394,
7.52783573079709));
#399729=CARTESIAN_POINT('Ctrl Pts',(-2.30043891757452,-1.40980978649596,
7.55196141284069));
#399730=CARTESIAN_POINT('Ctrl Pts',(-2.28662320026408,-1.38616442272262,
7.57603338728831));
#399731=CARTESIAN_POINT('Ctrl Pts',(-2.27884811390188,-1.38890690800894,
7.59639677331371));
#399732=CARTESIAN_POINT('Ctrl Pts',(-2.26672396437063,-1.3741013879501,
7.59974925422224));
#399733=CARTESIAN_POINT('Ctrl Pts',(-2.28545841158011,-1.37800253058071,
7.59639677331371));
#399734=CARTESIAN_POINT('Ctrl Pts',(-2.27592382560251,-1.38632550489709,
7.58707626057423));
#399735=CARTESIAN_POINT('Ctrl Pts',(-2.27553575658726,-1.37944314817564,
7.58811717123965));
#399736=CARTESIAN_POINT('Ctrl Pts',(-2.28181714606151,-1.37660385638463,
7.58707626057423));
#399737=CARTESIAN_POINT('Ctrl Pts',(-2.28198336987502,-1.38586992233497,
7.5801537675693));
#399738=CARTESIAN_POINT('Ctrl Pts',(-2.28144597464146,-1.38302595709244,
7.5820876076604));
#399739=CARTESIAN_POINT('Ctrl Pts',(-2.28421599812537,-1.38218696851292,
7.5801537675693));
#399740=CARTESIAN_POINT('Ctrl Pts',(-2.28662319925574,-1.38616442107833,
7.57603338509286));
#399741=CARTESIAN_POINT('Ctrl Pts',(-2.28662319925574,-1.38616442107833,
7.57603338509286));
#399742=CARTESIAN_POINT('Ctrl Pts',(-2.28662319925574,-1.38616442107833,
7.57603338509286));
#399743=CARTESIAN_POINT('Origin',(-2.29417856487524,-1.39074786460819,7.58486873427621));
#399744=CARTESIAN_POINT('Ctrl Pts',(-2.37845886339419,-1.38215849811743,
7.51098857897448));
#399745=CARTESIAN_POINT('Ctrl Pts',(-2.37257792201277,-1.38188456301551,
7.50433767179956));
#399746=CARTESIAN_POINT('Ctrl Pts',(-2.37025300047282,-1.39017327768762,
7.50214974420965));
#399747=CARTESIAN_POINT('Ctrl Pts',(-2.34699168879538,-1.38069275256384,
7.53887321589168));
#399748=CARTESIAN_POINT('Ctrl Pts',(-2.34118121152851,-1.38042209969059,
7.53220407452065));
#399749=CARTESIAN_POINT('Ctrl Pts',(-2.33880959854636,-1.38866699943436,
7.53003438070912));
#399750=CARTESIAN_POINT('Ctrl Pts',(-2.31546408561356,-1.3792241922381,
7.56669465659232));
#399751=CARTESIAN_POINT('Ctrl Pts',(-2.30968794718705,-1.37895513887298,
7.560040858333));
#399752=CARTESIAN_POINT('Ctrl Pts',(-2.30730685731679,-1.38715678877749,
7.55785582193789));
#399753=CARTESIAN_POINT('Ctrl Pts',(-2.28387747971606,-1.37775288355731,
7.59443891967696));
#399754=CARTESIAN_POINT('Ctrl Pts',(-2.27809296660798,-1.37748344009835,
7.58783901202978));
#399755=CARTESIAN_POINT('Ctrl Pts',(-2.27574633651479,-1.38564263768108,
7.58560008491213));
#399756=CARTESIAN_POINT('',(-2.36854855682563,-1.39009162622349,7.50366116523517));
#399757=CARTESIAN_POINT('Ctrl Pts',(-2.36854855682595,-1.39009162622368,
7.50366116523554));
#399758=CARTESIAN_POINT('Ctrl Pts',(-2.36905599173954,-1.38952891197538,
7.50350835821027));
#399759=CARTESIAN_POINT('Ctrl Pts',(-2.36950414026277,-1.38899513214037,
7.50345484956));
#399760=CARTESIAN_POINT('Ctrl Pts',(-2.36990678611858,-1.3884748031337,
7.50349758195598));
#399761=CARTESIAN_POINT('Ctrl Pts',(-2.37011337330361,-1.38820783576467,
7.50351950684424));
#399762=CARTESIAN_POINT('Ctrl Pts',(-2.37032844657167,-1.38791817510164,
7.50357029184312));
#399763=CARTESIAN_POINT('Ctrl Pts',(-2.37052816139873,-1.38763315784122,
7.50365515313924));
#399764=CARTESIAN_POINT('Ctrl Pts',(-2.37083540367529,-1.38719468587981,
7.50378570417639));
#399765=CARTESIAN_POINT('Ctrl Pts',(-2.37111560035781,-1.3867545317047,
7.50400001621911));
#399766=CARTESIAN_POINT('Ctrl Pts',(-2.37134550914226,-1.38634497820496,
7.50428903009635));
#399767=CARTESIAN_POINT('Ctrl Pts',(-2.37137102724852,-1.3862995209174,
7.50432110841318));
#399768=CARTESIAN_POINT('Ctrl Pts',(-2.3713959530662,-1.38625442726893,
7.50435406373354));
#399769=CARTESIAN_POINT('Ctrl Pts',(-2.37142027477436,-1.38620973128227,
7.50438785222352));
#399770=CARTESIAN_POINT('Ctrl Pts',(-2.37156877049319,-1.38593684080006,
7.50459414719561));
#399771=CARTESIAN_POINT('Ctrl Pts',(-2.37169665806775,-1.38567418270535,
7.50483629897752));
#399772=CARTESIAN_POINT('Ctrl Pts',(-2.37180022139304,-1.3854323954643,
7.5050991045531));
#399773=CARTESIAN_POINT('Ctrl Pts',(-2.37202869249058,-1.38489898852532,
7.50567888004914));
#399774=CARTESIAN_POINT('Ctrl Pts',(-2.37214826172948,-1.38444634307579,
7.50637912803145));
#399775=CARTESIAN_POINT('Ctrl Pts',(-2.37218983841972,-1.38407427769357,
7.50710440483569));
#399776=CARTESIAN_POINT('Ctrl Pts',(-2.37220003384959,-1.38398303987532,
7.50728225710685));
#399777=CARTESIAN_POINT('Ctrl Pts',(-2.37220588737711,-1.3838948475011,
7.50746498566954));
#399778=CARTESIAN_POINT('Ctrl Pts',(-2.37220767804062,-1.38381178685589,
7.50764697238949));
#399779=CARTESIAN_POINT('Ctrl Pts',(-2.37221730415486,-1.38336527568614,
7.50862528291182));
#399780=CARTESIAN_POINT('Ctrl Pts',(-2.3721145318164,-1.38302661934609,
7.50965856837422));
#399781=CARTESIAN_POINT('Ctrl Pts',(-2.37195529513963,-1.38276022611351,
7.51067959873202));
#399782=CARTESIAN_POINT('Ctrl Pts',(-2.37186766699555,-1.38261362958161,
7.51124147302579));
#399783=CARTESIAN_POINT('Ctrl Pts',(-2.37176254541608,-1.38248910370111,
7.51180065547253));
#399784=CARTESIAN_POINT('Ctrl Pts',(-2.37164697289435,-1.38238219484358,
7.51235175716501));
#399785=CARTESIAN_POINT('Ctrl Pts',(-2.37124762379313,-1.38201278215341,
7.51425603304536));
#399786=CARTESIAN_POINT('Ctrl Pts',(-2.37067175971287,-1.38181411915049,
7.51626900505179));
#399787=CARTESIAN_POINT('Ctrl Pts',(-2.36997578574981,-1.38176473183861,
7.51827788969242));
#399788=CARTESIAN_POINT('Ctrl Pts',(-2.36993811832372,-1.38176205890396,
7.51838661432544));
#399789=CARTESIAN_POINT('Ctrl Pts',(-2.3699000911534,-1.38175982926596,
7.51849533314856));
#399790=CARTESIAN_POINT('Ctrl Pts',(-2.36986171072477,-1.38175804150003,
7.51860402984325));
#399791=CARTESIAN_POINT('Ctrl Pts',(-2.28662320118131,-1.38616442121185,
7.57603338728985));
#399792=CARTESIAN_POINT('Ctrl Pts',(-2.31397746257106,-1.38747654046483,
7.55196141284922));
#399793=CARTESIAN_POINT('Ctrl Pts',(-2.34128462636657,-1.3887855289963,
7.52783573083105));
#399794=CARTESIAN_POINT('Ctrl Pts',(-2.36854855688476,-1.39009162622088,
7.50366116530176));
#399795=CARTESIAN_POINT('Origin',(-7.90134016134193E-16,-4.78983883923435E-16,
7.49482233047033));
#399796=CARTESIAN_POINT('Origin',(-2.32050622536842,-1.45229374026965,7.49482233047033));
#399797=CARTESIAN_POINT('Origin',(0.,0.,7.50366116523517));
#399798=CARTESIAN_POINT('Origin',(-2.36092560474803,-1.3856177462941,7.49482233047033));
#399799=CARTESIAN_POINT('Ctrl Pts',(-2.32121697257585,-1.46200083291476,
7.51860402984325));
#399800=CARTESIAN_POINT('Ctrl Pts',(-2.32504704676295,-1.46857554338377,
7.51860402984325));
#399801=CARTESIAN_POINT('Ctrl Pts',(-2.32096588398458,-1.47499741199084,
7.51860402984325));
#399802=CARTESIAN_POINT('Ctrl Pts',(-2.3226391041613,-1.46444206841971,
7.51041458714364));
#399803=CARTESIAN_POINT('Ctrl Pts',(-2.32408016420081,-1.47009695230204,
7.51004642900441));
#399804=CARTESIAN_POINT('Ctrl Pts',(-2.32096475844835,-1.47499918306595,
7.50729136483009));
#399805=CARTESIAN_POINT('Ctrl Pts',(-2.32541088507259,-1.46395118372962,
7.50215815450139));
#399806=CARTESIAN_POINT('Ctrl Pts',(-2.32604895207089,-1.46699928723625,
7.49877163671531));
#399807=CARTESIAN_POINT('Ctrl Pts',(-2.32421856835796,-1.46992394432005,
7.49481588533172));
#399808=CARTESIAN_POINT('Ctrl Pts',(-2.32799820477189,-1.45698261146062,
7.50366171572174));
#399809=CARTESIAN_POINT('Ctrl Pts',(-2.33110214420592,-1.4589252185354,
7.50000045605858));
#399810=CARTESIAN_POINT('Ctrl Pts',(-2.33110214420586,-1.4589252185355,
7.49482233047317));
#399811=CARTESIAN_POINT('Origin',(-2.31041603905738,-1.46829287829998,7.51860402984325));
#399812=CARTESIAN_POINT('Origin',(-2.31041603905738,-1.46829287829998,9.));
#399813=CARTESIAN_POINT('Origin',(-2.31041603905738,-1.46829287829998,8.75721825406948));
#399814=CARTESIAN_POINT('Ctrl Pts',(-2.31281244619727,-1.44757086443545,
8.78942910404912));
#399815=CARTESIAN_POINT('Ctrl Pts',(-2.31563446187852,-1.45237593011621,
8.7967269950169));
#399816=CARTESIAN_POINT('Ctrl Pts',(-2.30889868938922,-1.45823279403425,
8.79893251111267));
#399817=CARTESIAN_POINT('Ctrl Pts',(-2.31834579499507,-1.45707125757586,
8.78111911759583));
#399818=CARTESIAN_POINT('Ctrl Pts',(-2.32168490856532,-1.46277148833351,
8.78644465894814));
#399819=CARTESIAN_POINT('Ctrl Pts',(-2.31685066608334,-1.46927883890042,
8.78817647674132));
#399820=CARTESIAN_POINT('Ctrl Pts',(-2.32179430992119,-1.46299212920274,
8.76780923932029));
#399821=CARTESIAN_POINT('Ctrl Pts',(-2.32573159556496,-1.46972358658801,
8.76988516158374));
#399822=CARTESIAN_POINT('Ctrl Pts',(-2.32180826674691,-1.47618453631556,
8.77093053738833));
#399823=CARTESIAN_POINT('Ctrl Pts',(-2.32112189670534,-1.4618376402692,
8.75371302330492));
#399824=CARTESIAN_POINT('Ctrl Pts',(-2.32496320702648,-1.46840350170426,
8.75300828287559));
#399825=CARTESIAN_POINT('Ctrl Pts',(-2.32084096157935,-1.47483791168559,
8.75267964240737));
#399826=CARTESIAN_POINT('Origin',(-2.30335860700517,-1.45617572374887,8.78727029226991));
#399827=CARTESIAN_POINT('Ctrl Pts',(-2.27817859968917,-1.38810672912947,
8.85049129520029));
#399828=CARTESIAN_POINT('Ctrl Pts',(-2.2811176229011,-1.39315284196836,
8.85711686593484));
#399829=CARTESIAN_POINT('Ctrl Pts',(-2.27490615106174,-1.39902807640647,
8.85933012996512));
#399830=CARTESIAN_POINT('Ctrl Pts',(-2.2901898743986,-1.40872931124338,
8.82945683644721));
#399831=CARTESIAN_POINT('Ctrl Pts',(-2.29315329328014,-1.41381730986978,
8.83607469902388));
#399832=CARTESIAN_POINT('Ctrl Pts',(-2.28689781417968,-1.41968254846008,
8.8382956714852));
#399833=CARTESIAN_POINT('Ctrl Pts',(-2.3021832453345,-1.42932115373565,
8.80838214965004));
#399834=CARTESIAN_POINT('Ctrl Pts',(-2.30515835925056,-1.43442923198015,
8.81501364461989));
#399835=CARTESIAN_POINT('Ctrl Pts',(-2.29887186472477,-1.44030535307936,
8.81722098428721));
#399836=CARTESIAN_POINT('Ctrl Pts',(-2.31416007290288,-1.44988459233548,
8.78727029226991));
#399837=CARTESIAN_POINT('Ctrl Pts',(-2.31713568099513,-1.45499351904857,
8.79393457792714));
#399838=CARTESIAN_POINT('Ctrl Pts',(-2.3108296592442,-1.46089889836364,
8.79610912703474));
#399839=CARTESIAN_POINT('Origin',(-2.26737713379145,-1.39439786054286,8.85049129520029));
#399840=CARTESIAN_POINT('Ctrl Pts',(-2.28443929758135,-1.37777905311491,
8.85049129520029));
#399841=CARTESIAN_POINT('Ctrl Pts',(-2.29027258849562,-1.37805076865116,
8.85711686593484));
#399842=CARTESIAN_POINT('Ctrl Pts',(-2.29260852370877,-1.36982616113506,
8.85933012996512));
#399843=CARTESIAN_POINT('Ctrl Pts',(-2.27927866931395,-1.37753867030224,
8.86332496987232));
#399844=CARTESIAN_POINT('Ctrl Pts',(-2.28191097731258,-1.37374092768628,
8.86648636486738));
#399845=CARTESIAN_POINT('Ctrl Pts',(-2.27817065852942,-1.36917079450517,
8.87206031107457));
#399846=CARTESIAN_POINT('Ctrl Pts',(-2.27556081970208,-1.38361217013837,
8.86341338519877));
#399847=CARTESIAN_POINT('Ctrl Pts',(-2.27337901193668,-1.38770034644438,
8.86654584966059));
#399848=CARTESIAN_POINT('Ctrl Pts',(-2.26758895886383,-1.3864356574703,
8.87215952290714));
#399849=CARTESIAN_POINT('Ctrl Pts',(-2.27817859968916,-1.38810672912947,
8.85049129520029));
#399850=CARTESIAN_POINT('Ctrl Pts',(-2.2811176229011,-1.39315284196836,
8.85711686593484));
#399851=CARTESIAN_POINT('Ctrl Pts',(-2.27490615106174,-1.39902807640647,
8.85933012996512));
#399852=CARTESIAN_POINT('Origin',(-2.28502091876034,-1.36529259177455,8.85049129520029));
#399853=CARTESIAN_POINT('Ctrl Pts',(-2.35585431734963,-1.38110557508643,
8.78727029226991));
#399854=CARTESIAN_POINT('Ctrl Pts',(-2.36176022090918,-1.38138067293022,
8.79393457792714));
#399855=CARTESIAN_POINT('Ctrl Pts',(-2.3640791495949,-1.37305829436825,
8.79610912703474));
#399856=CARTESIAN_POINT('Ctrl Pts',(-2.33208304560438,-1.37999830580319,
8.80838214965003));
#399857=CARTESIAN_POINT('Ctrl Pts',(-2.33798796833693,-1.38027335795992,
8.81501364461995));
#399858=CARTESIAN_POINT('Ctrl Pts',(-2.34028998879802,-1.37198182526734,
8.81722098428721));
#399859=CARTESIAN_POINT('Ctrl Pts',(-2.30827893904688,-1.37888950706963,
8.82945683644722));
#399860=CARTESIAN_POINT('Ctrl Pts',(-2.31416064980261,-1.37916347800912,
8.83607469902389));
#399861=CARTESIAN_POINT('Ctrl Pts',(-2.31646736766072,-1.3709044771482,
8.83829567148519));
#399862=CARTESIAN_POINT('Ctrl Pts',(-2.28443929758135,-1.37777905311491,
8.85049129520029));
#399863=CARTESIAN_POINT('Ctrl Pts',(-2.29027258849562,-1.37805076865116,
8.85711686593484));
#399864=CARTESIAN_POINT('Ctrl Pts',(-2.29260852370877,-1.36982616113506,
8.85933012996512));
#399865=CARTESIAN_POINT('Origin',(-2.35643593852862,-1.36861911374607,8.78727029226991));
#399866=CARTESIAN_POINT('Ctrl Pts',(-2.36967675099988,-1.38174940758217,
8.75374538247847));
#399867=CARTESIAN_POINT('Ctrl Pts',(-2.37726687089216,-1.38211609329002,
8.75304829418601));
#399868=CARTESIAN_POINT('Ctrl Pts',(-2.38106579034592,-1.3754950016736,
8.75272238421917));
#399869=CARTESIAN_POINT('Ctrl Pts',(-2.37099530499473,-1.38181082644539,
8.76769408445023));
#399870=CARTESIAN_POINT('Ctrl Pts',(-2.37877645928179,-1.38218605028949,
8.76974318093971));
#399871=CARTESIAN_POINT('Ctrl Pts',(-2.38268881118069,-1.37572757834178,
8.7707786988043));
#399872=CARTESIAN_POINT('Ctrl Pts',(-2.3642371483471,-1.38149602835533,
8.78108014887987));
#399873=CARTESIAN_POINT('Ctrl Pts',(-2.37083121329715,-1.38181781203245,
8.78639403366322));
#399874=CARTESIAN_POINT('Ctrl Pts',(-2.37437720405471,-1.37454127265745,
8.78812224174741));
#399875=CARTESIAN_POINT('Ctrl Pts',(-2.35316202148167,-1.38098014374298,
8.78944554828686));
#399876=CARTESIAN_POINT('Ctrl Pts',(-2.35871898210048,-1.38125692217053,
8.79673892988686));
#399877=CARTESIAN_POINT('Ctrl Pts',(-2.36079643040482,-1.37258583441527,
8.79894799272499));
#399878=CARTESIAN_POINT('Origin',(-2.37044333190376,-1.36927158015968,8.75721825406948));
#399879=CARTESIAN_POINT('Origin',(-2.37044333190376,-1.36927158015968,9.));
#399880=CARTESIAN_POINT('Origin',(-2.37044333190376,-1.36927158015968,7.51860402984325));
#399881=CARTESIAN_POINT('Ctrl Pts',(-2.36854787837649,-1.39009122804435,
7.50366195182966));
#399882=CARTESIAN_POINT('Ctrl Pts',(-2.37170608696157,-1.39194476796656,
7.50000065167735));
#399883=CARTESIAN_POINT('Ctrl Pts',(-2.37170608696163,-1.39194476796646,
7.49482233047108));
#399884=CARTESIAN_POINT('Ctrl Pts',(-2.3735332551357,-1.38456856399741,
7.50215800491337));
#399885=CARTESIAN_POINT('Ctrl Pts',(-2.37653148948253,-1.38372281700463,
7.49877273257266));
#399886=CARTESIAN_POINT('Ctrl Pts',(-2.37827884268994,-1.38074558454502,
7.49481816995647));
#399887=CARTESIAN_POINT('Ctrl Pts',(-2.37267722747953,-1.38188952816452,
7.51043025814041));
#399888=CARTESIAN_POINT('Ctrl Pts',(-2.37836144152799,-1.38055443729186,
7.51006209594514));
#399889=CARTESIAN_POINT('Ctrl Pts',(-2.38126854047388,-1.37552176942273,
7.50731281821699));
#399890=CARTESIAN_POINT('Ctrl Pts',(-2.36986020095858,-1.38175797108343,
7.51860402984325));
#399891=CARTESIAN_POINT('Ctrl Pts',(-2.37746118835,-1.38211294723218,7.51860402984324));
#399892=CARTESIAN_POINT('Ctrl Pts',(-2.38126727405858,-1.37552396180424,
7.51860402984325));
#399893=CARTESIAN_POINT('Origin',(0.,0.,7.5));
#399894=CARTESIAN_POINT('Origin',(-2.19147106502123,-1.52131278661257,7.5));
#399895=CARTESIAN_POINT('',(-2.19147106502123,-1.52131278661257,7.59394543036555));
#399896=CARTESIAN_POINT('',(-2.19147106502123,-1.52131278661257,8.85049129520029));
#399897=CARTESIAN_POINT('',(-2.19147106502123,-1.52131278661257,7.5));
#399898=CARTESIAN_POINT('',(-2.26252622397767,-1.52920804991441,8.78727029226991));
#399899=CARTESIAN_POINT('Ctrl Pts',(-2.19147106502123,-1.52131278661257,
8.85049129520029));
#399900=CARTESIAN_POINT('Ctrl Pts',(-2.215190546525,-1.52394836655645,8.82945686509571));
#399901=CARTESIAN_POINT('Ctrl Pts',(-2.23887476615139,-1.52658002839207,
8.80838212259895));
#399902=CARTESIAN_POINT('Ctrl Pts',(-2.26252622397767,-1.52920804991441,
8.78727029226991));
#399903=CARTESIAN_POINT('',(-2.27646303399419,-1.5307566325407,8.75721825406948));
#399904=CARTESIAN_POINT('Origin',(-2.23452231565444,-1.52609661077909,8.7593767971309));
#399905=CARTESIAN_POINT('',(-2.27646303399419,-1.5307566325407,7.51860402984325));
#399906=CARTESIAN_POINT('',(-2.27646303399419,-1.5307566325407,7.5));
#399907=CARTESIAN_POINT('Ctrl Pts',(-2.27646303399419,-1.5307566325407,
7.51860402984325));
#399908=CARTESIAN_POINT('Ctrl Pts',(-2.26551783731017,-1.5295404617379,
7.52834476460825));
#399909=CARTESIAN_POINT('Ctrl Pts',(-2.25456553516241,-1.52832350141458,
7.53807742314407));
#399910=CARTESIAN_POINT('Ctrl Pts',(-2.24360588897549,-1.52710572506151,
7.54780169004674));
#399911=CARTESIAN_POINT('Ctrl Pts',(-2.22624640173375,-1.52517683313345,
7.5632044032688));
#399912=CARTESIAN_POINT('Ctrl Pts',(-2.20886846717179,-1.52324589143935,
7.57858609112102));
#399913=CARTESIAN_POINT('Ctrl Pts',(-2.19147106502123,-1.52131278661257,
7.59394543036555));
#399914=CARTESIAN_POINT('Origin',(-2.30745690681615,-1.77722975964336,7.5));
#399915=CARTESIAN_POINT('',(-2.22277754110615,-1.60771882366397,8.75721825406948));
#399916=CARTESIAN_POINT('',(-2.21651095806263,-1.59517439388236,8.78727029226991));
#399917=CARTESIAN_POINT('Origin',(-2.20060403297877,-1.5633319522567,8.75658640621004));
#399918=CARTESIAN_POINT('',(-2.18456153393018,-1.53121811901793,8.85049129520029));
#399919=CARTESIAN_POINT('Ctrl Pts',(-2.21651095806263,-1.59517439388236,
8.78727029226991));
#399920=CARTESIAN_POINT('Ctrl Pts',(-2.20587625583213,-1.57388587437304,
8.80838212259896));
#399921=CARTESIAN_POINT('Ctrl Pts',(-2.1952268225017,-1.55256786618585,
8.82945686509571));
#399922=CARTESIAN_POINT('Ctrl Pts',(-2.18456153393018,-1.53121811901793,
8.85049129520029));
#399923=CARTESIAN_POINT('',(-2.18456153393018,-1.53121811901793,7.59394543036555));
#399924=CARTESIAN_POINT('',(-2.18456153393018,-1.53121811901793,7.5));
#399925=CARTESIAN_POINT('',(-2.22277754110615,-1.60771882366397,7.51860402984325));
#399926=CARTESIAN_POINT('Ctrl Pts',(-2.18456153393018,-1.53121811901793,
7.59394543036555));
#399927=CARTESIAN_POINT('Ctrl Pts',(-2.19238414650715,-1.54687740470822,
7.57858609112103));
#399928=CARTESIAN_POINT('Ctrl Pts',(-2.20019800562751,-1.56251916775161,
7.56320440326857));
#399929=CARTESIAN_POINT('Ctrl Pts',(-2.20800357004751,-1.57814432648525,
7.54780169004651));
#399930=CARTESIAN_POINT('Ctrl Pts',(-2.21293149350176,-1.58800903095206,
7.53807742314383));
#399931=CARTESIAN_POINT('Ctrl Pts',(-2.21785611476348,-1.59786712509838,
7.52834476460825));
#399932=CARTESIAN_POINT('Ctrl Pts',(-2.22277754110615,-1.60771882366397,
7.51860402984325));
#399933=CARTESIAN_POINT('',(-2.22277754110615,-1.60771882366397,7.5));
#399934=CARTESIAN_POINT('Origin',(-2.19071182494582,-1.52814573469578,7.5));
#399935=CARTESIAN_POINT('Ctrl Pts',(-2.18456153393018,-1.53121811901793,
8.85049129520029));
#399936=CARTESIAN_POINT('Ctrl Pts',(-2.18447498810115,-1.53104487180049,
8.85097269580138));
#399937=CARTESIAN_POINT('Ctrl Pts',(-2.18439705895477,-1.53087005142215,
8.85143669361005));
#399938=CARTESIAN_POINT('Ctrl Pts',(-2.18432495664555,-1.53068525200685,
8.8519052845931));
#399939=CARTESIAN_POINT('Ctrl Pts',(-2.18418392910126,-1.53032379607007,
8.85282181883899));
#399940=CARTESIAN_POINT('Ctrl Pts',(-2.18406900446172,-1.52993339018136,
8.85372622499636));
#399941=CARTESIAN_POINT('Ctrl Pts',(-2.18399317054837,-1.52950355408831,
8.85462257735071));
#399942=CARTESIAN_POINT('Ctrl Pts',(-2.18393021592687,-1.52914671943019,
8.85536669723986));
#399943=CARTESIAN_POINT('Ctrl Pts',(-2.18389415610197,-1.5287626346629,
8.85610498449051));
#399944=CARTESIAN_POINT('Ctrl Pts',(-2.18390038630544,-1.52834452303797,
8.85681338218371));
#399945=CARTESIAN_POINT('Ctrl Pts',(-2.18390604022488,-1.5279650860817,
8.85745625420284));
#399946=CARTESIAN_POINT('Ctrl Pts',(-2.18394599498023,-1.52755285743402,
8.85808743050665));
#399947=CARTESIAN_POINT('Ctrl Pts',(-2.18404711722399,-1.5270980376494,
8.85866804508409));
#399948=CARTESIAN_POINT('Ctrl Pts',(-2.18409377283519,-1.52688819366006,
8.85893592806395));
#399949=CARTESIAN_POINT('Ctrl Pts',(-2.18415368514345,-1.52666922800997,
8.85919241173848));
#399950=CARTESIAN_POINT('Ctrl Pts',(-2.18423108248651,-1.52644003474419,
8.85943017985534));
#399951=CARTESIAN_POINT('Ctrl Pts',(-2.1843355918117,-1.52613055598692,
8.8597512372));
#399952=CARTESIAN_POINT('Ctrl Pts',(-2.18447524850651,-1.52579475712461,
8.86004599534706));
#399953=CARTESIAN_POINT('Ctrl Pts',(-2.18465799121656,-1.52544067212629,
8.86026130871721));
#399954=CARTESIAN_POINT('Ctrl Pts',(-2.18472489847477,-1.52531103162569,
8.86034014101235));
#399955=CARTESIAN_POINT('Ctrl Pts',(-2.18479857547465,-1.52517698687705,
8.86040910639693));
#399956=CARTESIAN_POINT('Ctrl Pts',(-2.18487730971225,-1.5250423518811,
8.86046313645507));
#399957=CARTESIAN_POINT('Ctrl Pts',(-2.18500017383063,-1.52483225509748,
8.8605474499083));
#399958=CARTESIAN_POINT('Ctrl Pts',(-2.18513883375115,-1.52461506020084,
8.86059655985669));
#399959=CARTESIAN_POINT('Ctrl Pts',(-2.18528414986347,-1.52440453891958,
8.86059725258816));
#399960=CARTESIAN_POINT('Ctrl Pts',(-2.18542980171407,-1.52419353125005,
8.86059794692011));
#399961=CARTESIAN_POINT('Ctrl Pts',(-2.18558594230478,-1.52398839721477,
8.86056369958366));
#399962=CARTESIAN_POINT('Ctrl Pts',(-2.18574106129468,-1.5237980457274,
8.86048590497774));
#399963=CARTESIAN_POINT('Ctrl Pts',(-2.1857815427326,-1.52374836965664,
8.86046560290182));
#399964=CARTESIAN_POINT('Ctrl Pts',(-2.18582255145109,-1.52369911132095,
8.86044257503091));
#399965=CARTESIAN_POINT('Ctrl Pts',(-2.18586279501899,-1.52365177184095,
8.86041778462584));
#399966=CARTESIAN_POINT('Ctrl Pts',(-2.18613358429285,-1.52333323588389,
8.86025097596201));
#399967=CARTESIAN_POINT('Ctrl Pts',(-2.18640631964952,-1.52305905007566,
8.8599848982295));
#399968=CARTESIAN_POINT('Ctrl Pts',(-2.18666703383916,-1.52283124213451,
8.85968173251462));
#399969=CARTESIAN_POINT('Ctrl Pts',(-2.18680493670834,-1.52271074478549,
8.85952137522077));
#399970=CARTESIAN_POINT('Ctrl Pts',(-2.18694200881965,-1.52260075658167,
8.85934740853961));
#399971=CARTESIAN_POINT('Ctrl Pts',(-2.18707534425059,-1.52250161612591,
8.8591675900182));
#399972=CARTESIAN_POINT('Ctrl Pts',(-2.18761075531217,-1.52210351566385,
8.85844552518696));
#399973=CARTESIAN_POINT('Ctrl Pts',(-2.18811436935619,-1.52185540067336,
8.85759444184127));
#399974=CARTESIAN_POINT('Ctrl Pts',(-2.18854315989625,-1.52168998323699,
8.85683498915142));
#399975=CARTESIAN_POINT('Ctrl Pts',(-2.18858803168432,-1.52167267274281,
8.85675551445));
#399976=CARTESIAN_POINT('Ctrl Pts',(-2.18863208747596,-1.52165628755188,
8.85667699793652));
#399977=CARTESIAN_POINT('Ctrl Pts',(-2.1886752795288,-1.52164076359268,
8.85659965593547));
#399978=CARTESIAN_POINT('Ctrl Pts',(-2.18925828806187,-1.52143122039921,
8.85555568965886));
#399979=CARTESIAN_POINT('Ctrl Pts',(-2.18984885756596,-1.52131403437626,
8.85434650606346));
#399980=CARTESIAN_POINT('Ctrl Pts',(-2.19044869788364,-1.52128253033578,
8.85297329937117));
#399981=CARTESIAN_POINT('Ctrl Pts',(-2.19078607151352,-1.52126481123258,
8.85220095427747));
#399982=CARTESIAN_POINT('Ctrl Pts',(-2.19112653220933,-1.52127450399796,
8.85137579139183));
#399983=CARTESIAN_POINT('Ctrl Pts',(-2.19147106502123,-1.52131278661257,
8.85049129520029));
#399984=CARTESIAN_POINT('Origin',(-2.19071182494582,-1.52814573469578,7.59394543036555));
#399985=CARTESIAN_POINT('Ctrl Pts',(-2.18431026219255,-1.5307151239013,
7.59443877723642));
#399986=CARTESIAN_POINT('Ctrl Pts',(-2.1817224050621,-1.52553475816893,
7.58783886950016));
#399987=CARTESIAN_POINT('Ctrl Pts',(-2.18823340177431,-1.52008626265638,
7.58559994247159));
#399988=CARTESIAN_POINT('Ctrl Pts',(-2.19843729834314,-1.55899458844882,
7.56670252222135));
#399989=CARTESIAN_POINT('Ctrl Pts',(-2.19585318140097,-1.55382170981567,
7.56004874999027));
#399990=CARTESIAN_POINT('Ctrl Pts',(-2.20238904649611,-1.54832454466309,
7.55786368756704));
#399991=CARTESIAN_POINT('Ctrl Pts',(-2.2125379536652,-1.58722124392178,
7.53888913333558));
#399992=CARTESIAN_POINT('Ctrl Pts',(-2.20993847918949,-1.58201762261763,
7.53222002137276));
#399993=CARTESIAN_POINT('Ctrl Pts',(-2.21651771578449,-1.57651161766423,
7.53005029815327));
#399994=CARTESIAN_POINT('Ctrl Pts',(-2.22661159009451,-1.61539381304489,
7.51101258149734));
#399995=CARTESIAN_POINT('Ctrl Pts',(-2.22398060526481,-1.61012711439532,
7.5043616886572));
#399996=CARTESIAN_POINT('Ctrl Pts',(-2.2306187854571,-1.60464605197282,
7.50217374673251));
#399997=CARTESIAN_POINT('',(-2.22986633334693,-1.60314476287808,7.50366116523517));
#399998=CARTESIAN_POINT('Ctrl Pts',(-2.22277754110615,-1.60771882366397,
7.51860402984325));
#399999=CARTESIAN_POINT('Ctrl Pts',(-2.22297489374258,-1.6081138836628,
7.51734760759494));
#400000=CARTESIAN_POINT('Ctrl Pts',(-2.22320645518636,-1.60844428819929,
7.51608817408573));
#400001=CARTESIAN_POINT('Ctrl Pts',(-2.22348262824042,-1.6087016133381,
7.5148100591312));
#400002=CARTESIAN_POINT('Ctrl Pts',(-2.22373279239217,-1.60893470459781,
7.51365231206384));
#400003=CARTESIAN_POINT('Ctrl Pts',(-2.22401974321264,-1.60910834456724,
7.51247773061042));
#400004=CARTESIAN_POINT('Ctrl Pts',(-2.22435763202006,-1.60918793729049,
7.51129758471022));
#400005=CARTESIAN_POINT('Ctrl Pts',(-2.22477758921932,-1.60928686195565,
7.50983079813402));
#400006=CARTESIAN_POINT('Ctrl Pts',(-2.22526581718584,-1.60922467093318,
7.50839324291155));
#400007=CARTESIAN_POINT('Ctrl Pts',(-2.22581546211117,-1.60891913153019,
7.50715379678855));
#400008=CARTESIAN_POINT('Ctrl Pts',(-2.22606938222904,-1.60877798112991,
7.50658120839351));
#400009=CARTESIAN_POINT('Ctrl Pts',(-2.22636789030147,-1.60855652531023,
7.50598221009429));
#400010=CARTESIAN_POINT('Ctrl Pts',(-2.22669032953811,-1.60824176621978,
7.50545747549611));
#400011=CARTESIAN_POINT('Ctrl Pts',(-2.22686239309521,-1.60807380102642,
7.50517746087247));
#400012=CARTESIAN_POINT('Ctrl Pts',(-2.22704327857473,-1.60787759016943,
7.50491486231392));
#400013=CARTESIAN_POINT('Ctrl Pts',(-2.22722696943707,-1.60765719904463,
7.50468370960992));
#400014=CARTESIAN_POINT('Ctrl Pts',(-2.22750164521828,-1.60732764479462,
7.50433806340447));
#400015=CARTESIAN_POINT('Ctrl Pts',(-2.22779040260933,-1.60693378573885,
7.50405484070984));
#400016=CARTESIAN_POINT('Ctrl Pts',(-2.22807321658152,-1.60650172397162,
7.50385766036131));
#400017=CARTESIAN_POINT('Ctrl Pts',(-2.22810345913992,-1.60645552168138,
7.50383657498791));
#400018=CARTESIAN_POINT('Ctrl Pts',(-2.22813363242865,-1.60640891087603,
7.50381643264937));
#400019=CARTESIAN_POINT('Ctrl Pts',(-2.22816371133269,-1.60636194407087,
7.50379723213559));
#400020=CARTESIAN_POINT('Ctrl Pts',(-2.22836449785661,-1.60604842528247,
7.50366906242519));
#400021=CARTESIAN_POINT('Ctrl Pts',(-2.22856484065419,-1.60571183559279,
7.50358235568538));
#400022=CARTESIAN_POINT('Ctrl Pts',(-2.22875014780004,-1.60538276269125,
7.5035341175365));
#400023=CARTESIAN_POINT('Ctrl Pts',(-2.22902799489253,-1.60488935511924,
7.50346178989176));
#400024=CARTESIAN_POINT('Ctrl Pts',(-2.22930591601758,-1.60434674711438,
7.50346967198527));
#400025=CARTESIAN_POINT('Ctrl Pts',(-2.22956235809399,-1.60380567910415,
7.50354272648692));
#400026=CARTESIAN_POINT('Ctrl Pts',(-2.22966783802805,-1.6035831266321,
7.50357277531559));
#400027=CARTESIAN_POINT('Ctrl Pts',(-2.22976967202096,-1.60336119113259,
7.50361331098761));
#400028=CARTESIAN_POINT('Ctrl Pts',(-2.22986633334808,-1.6031447628789,
7.50366116523658));
#400029=CARTESIAN_POINT('',(-2.19311322794424,-1.52982084947218,7.57603338622103));
#400030=CARTESIAN_POINT('Origin',(-2.20036267203955,-1.53487426909768,7.58486873427629));
#400031=CARTESIAN_POINT('Ctrl Pts',(-2.22986633336772,-1.60314476293152,
7.50366116529969));
#400032=CARTESIAN_POINT('Ctrl Pts',(-2.21763603662393,-1.5787429670886,
7.5278357307971));
#400033=CARTESIAN_POINT('Ctrl Pts',(-2.20538559594532,-1.55430280858916,
7.55196141284068));
#400034=CARTESIAN_POINT('Ctrl Pts',(-2.1931132281663,-1.52982085070438,
7.57603338728831));
#400035=CARTESIAN_POINT('Ctrl Pts',(-2.18517840491731,-1.53205954976697,
7.59639677331371));
#400036=CARTESIAN_POINT('Ctrl Pts',(-2.17402775867868,-1.51650765230946,
7.59974925422225));
#400037=CARTESIAN_POINT('Ctrl Pts',(-2.19247376689057,-1.52160109977802,
7.59639677331372));
#400038=CARTESIAN_POINT('Ctrl Pts',(-2.18242551594711,-1.52929609063005,
7.58707626057422));
#400039=CARTESIAN_POINT('Ctrl Pts',(-2.1824791983704,-1.52240301078146,
7.58811717123964));
#400040=CARTESIAN_POINT('Ctrl Pts',(-2.18892959610593,-1.51997200262531,
7.58707626057424));
#400041=CARTESIAN_POINT('Ctrl Pts',(-2.18850179951101,-1.52922968044567,
7.58015376756929));
#400042=CARTESIAN_POINT('Ctrl Pts',(-2.18814772189234,-1.52635712740384,
7.58208760766041));
#400043=CARTESIAN_POINT('Ctrl Pts',(-2.19096580824873,-1.52569733863038,
7.5801537675693));
#400044=CARTESIAN_POINT('Ctrl Pts',(-2.19311322726537,-1.52982084899888,
7.57603338509286));
#400045=CARTESIAN_POINT('Ctrl Pts',(-2.19311322726537,-1.52982084899888,
7.57603338509286));
#400046=CARTESIAN_POINT('Ctrl Pts',(-2.19311322726537,-1.52982084899888,
7.57603338509286));
#400047=CARTESIAN_POINT('Origin',(-2.20035940734054,-1.53487894928956,7.58486873427621));
#400048=CARTESIAN_POINT('Ctrl Pts',(-2.28501686554784,-1.53170708783975,
7.51098857897448));
#400049=CARTESIAN_POINT('Ctrl Pts',(-2.27916555827345,-1.53105692235888,
7.50433767179957));
#400050=CARTESIAN_POINT('Ctrl Pts',(-2.27631435376175,-1.53917964874323,
7.50214974420965));
#400051=CARTESIAN_POINT('Ctrl Pts',(-2.25370825427415,-1.52822824501889,
7.5388732158917));
#400052=CARTESIAN_POINT('Ctrl Pts',(-2.24792705604509,-1.52758586967431,
7.53220407452063));
#400053=CARTESIAN_POINT('Ctrl Pts',(-2.24503206325589,-1.53566187962183,
7.53003438070911));
#400054=CARTESIAN_POINT('Ctrl Pts',(-2.22233951891752,-1.52474272153652,
7.56669465659234));
#400055=CARTESIAN_POINT('Ctrl Pts',(-2.21659248649516,-1.52410414251082,
7.56004085833299));
#400056=CARTESIAN_POINT('Ctrl Pts',(-2.21369080731583,-1.53213638429416,
7.55785582193789));
#400057=CARTESIAN_POINT('Ctrl Pts',(-2.19091207816031,-1.52125067502892,
7.59443891967696));
#400058=CARTESIAN_POINT('Ctrl Pts',(-2.18515671325649,-1.52061117014312,
7.58783901202978));
#400059=CARTESIAN_POINT('Ctrl Pts',(-2.1822921429825,-1.52860325467306,
7.58560008491213));
#400060=CARTESIAN_POINT('',(-2.27461864350411,-1.53898896096138,7.50366116523517));
#400061=CARTESIAN_POINT('Ctrl Pts',(-2.27461864350442,-1.53898896096159,
7.50366116523554));
#400062=CARTESIAN_POINT('Ctrl Pts',(-2.27516108906423,-1.5384599143366,
7.50350835821027));
#400063=CARTESIAN_POINT('Ctrl Pts',(-2.27564251620971,-1.53795594418397,
7.50345484956));
#400064=CARTESIAN_POINT('Ctrl Pts',(-2.27607767238034,-1.53746248185761,
7.50349758195598));
#400065=CARTESIAN_POINT('Ctrl Pts',(-2.2763009397679,-1.53720929908806,
7.50351950684424));
#400066=CARTESIAN_POINT('Ctrl Pts',(-2.27653412976726,-1.53693401335552,
7.50357029184312));
#400067=CARTESIAN_POINT('Ctrl Pts',(-2.27675169537738,-1.53666237746654,
7.50365515313923));
#400068=CARTESIAN_POINT('Ctrl Pts',(-2.27708639938674,-1.53624449147305,
7.50378570417639));
#400069=CARTESIAN_POINT('Ctrl Pts',(-2.27739422114995,-1.53582319390498,
7.50400001621911));
#400070=CARTESIAN_POINT('Ctrl Pts',(-2.27764989774498,-1.53542921218322,
7.50428903009635));
#400071=CARTESIAN_POINT('Ctrl Pts',(-2.27767827587996,-1.53538548324322,
7.50432110841318));
#400072=CARTESIAN_POINT('Ctrl Pts',(-2.27770603964485,-1.53534207924711,
7.50435406373354));
#400073=CARTESIAN_POINT('Ctrl Pts',(-2.27773317506315,-1.53529903339034,
7.50438785222352));
#400074=CARTESIAN_POINT('Ctrl Pts',(-2.27789884983483,-1.53503621774426,
7.50459414719561));
#400075=CARTESIAN_POINT('Ctrl Pts',(-2.27804330321256,-1.53478229309382,
7.50483629897752));
#400076=CARTESIAN_POINT('Ctrl Pts',(-2.27816214511761,-1.53454763795562,
7.5050991045531));
#400077=CARTESIAN_POINT('Ctrl Pts',(-2.27842432229669,-1.53402996515188,
7.50567888004914));
#400078=CARTESIAN_POINT('Ctrl Pts',(-2.2785726469613,-1.53358591053842,
7.50637912803144));
#400079=CARTESIAN_POINT('Ctrl Pts',(-2.27863797653866,-1.53321727343212,
7.50710440483569));
#400080=CARTESIAN_POINT('Ctrl Pts',(-2.278653996648,-1.53312687629518,7.50728225710685));
#400081=CARTESIAN_POINT('Ctrl Pts',(-2.27866548865364,-1.53303924015845,
7.50746498566954));
#400082=CARTESIAN_POINT('Ctrl Pts',(-2.27867259735185,-1.53295646489845,
7.50764697238949));
#400083=CARTESIAN_POINT('Ctrl Pts',(-2.27871081175708,-1.53251148788104,
7.50862528291182));
#400084=CARTESIAN_POINT('Ctrl Pts',(-2.27862994836162,-1.53216694270042,
7.50965856837423));
#400085=CARTESIAN_POINT('Ctrl Pts',(-2.27848810672668,-1.5318908944724,
7.51067959873204));
#400086=CARTESIAN_POINT('Ctrl Pts',(-2.27841005109607,-1.53173898478433,
7.5112414730258));
#400087=CARTESIAN_POINT('Ctrl Pts',(-2.27831312390072,-1.53160797959289,
7.51180065547253));
#400088=CARTESIAN_POINT('Ctrl Pts',(-2.27820463850915,-1.53149388563419,
7.51235175716501));
#400089=CARTESIAN_POINT('Ctrl Pts',(-2.27782977826581,-1.53109964555724,
7.51425603304536));
#400090=CARTESIAN_POINT('Ctrl Pts',(-2.27726782574237,-1.53086449499047,
7.5162690050518));
#400091=CARTESIAN_POINT('Ctrl Pts',(-2.27657644598839,-1.5307706179452,
7.51827788969243));
#400092=CARTESIAN_POINT('Ctrl Pts',(-2.27653902720958,-1.53076553714211,
7.51838661432545));
#400093=CARTESIAN_POINT('Ctrl Pts',(-2.27650122102355,-1.53076087567597,
7.51849533314856));
#400094=CARTESIAN_POINT('Ctrl Pts',(-2.27646303399419,-1.53075663254069,
7.51860402984325));
#400095=CARTESIAN_POINT('Ctrl Pts',(-2.19311322917843,-1.5298208492555,
7.57603338728985));
#400096=CARTESIAN_POINT('Ctrl Pts',(-2.22032722053524,-1.53288286616341,
7.55196141284922));
#400097=CARTESIAN_POINT('Ctrl Pts',(-2.24749441165089,-1.53593874122896,
7.52783573083105));
#400098=CARTESIAN_POINT('Ctrl Pts',(-2.27461864356328,-1.53898896096256,
7.50366116530176));
#400099=CARTESIAN_POINT('Origin',(-7.57821998246247E-16,-5.28623820391016E-16,
7.49482233047033));
#400100=CARTESIAN_POINT('Origin',(-2.2226897170392,-1.59798519134822,7.49482233047033));
#400101=CARTESIAN_POINT('Origin',(0.,0.,7.50366116523517));
#400102=CARTESIAN_POINT('Origin',(-2.26729799607036,-1.53403586888161,7.49482233047033));
#400103=CARTESIAN_POINT('Ctrl Pts',(-2.22277706837911,-1.60771787746033,
7.51860402984325));
#400104=CARTESIAN_POINT('Ctrl Pts',(-2.22617803012197,-1.61452447317726,
7.51860402984325));
#400105=CARTESIAN_POINT('Ctrl Pts',(-2.22169380199589,-1.62067166636955,
7.51860402984325));
#400106=CARTESIAN_POINT('Ctrl Pts',(-2.22403986754687,-1.61024521346863,
7.51041458714366));
#400107=CARTESIAN_POINT('Ctrl Pts',(-2.22511565711965,-1.61598080781928,
7.51004642900442));
#400108=CARTESIAN_POINT('Ctrl Pts',(-2.22169256529901,-1.62067336169245,
7.5072913648301));
#400109=CARTESIAN_POINT('Ctrl Pts',(-2.22683740462711,-1.60993292596653,
7.50215815450137));
#400110=CARTESIAN_POINT('Ctrl Pts',(-2.22727886798614,-1.61301564791053,
7.4987716367153));
#400111=CARTESIAN_POINT('Ctrl Pts',(-2.22526486157011,-1.61581702288554,
7.4948158853317));
#400112=CARTESIAN_POINT('Ctrl Pts',(-2.2298658863588,-1.60314444151892,
7.50366171572174));
#400113=CARTESIAN_POINT('Ctrl Pts',(-2.23283898515376,-1.60528192738146,
7.50000045605858));
#400114=CARTESIAN_POINT('Ctrl Pts',(-2.23283898515369,-1.60528192738156,
7.49482233047317));
#400115=CARTESIAN_POINT('Origin',(-2.211595193805,-1.61330497697696,7.51860402984325));
#400116=CARTESIAN_POINT('Origin',(-2.211595193805,-1.61330497697696,9.));
#400117=CARTESIAN_POINT('Origin',(-2.211595193805,-1.61330497697696,8.75721825406948));
#400118=CARTESIAN_POINT('Ctrl Pts',(-2.21531434125615,-1.59277907704497,
8.78942910404912));
#400119=CARTESIAN_POINT('Ctrl Pts',(-2.21782269718833,-1.59775507736844,
8.79672699501691));
#400120=CARTESIAN_POINT('Ctrl Pts',(-2.21072551350639,-1.60316834530628,
8.79893251111267));
#400121=CARTESIAN_POINT('Ctrl Pts',(-2.22022762891699,-1.60261447348346,
8.78111911759583));
#400122=CARTESIAN_POINT('Ctrl Pts',(-2.22319466688172,-1.60851693024666,
8.78644465894813));
#400123=CARTESIAN_POINT('Ctrl Pts',(-2.21795342948707,-1.61470117978466,
8.78817647674132));
#400124=CARTESIAN_POINT('Ctrl Pts',(-2.22328970695173,-1.6087441271545,
8.76780923932029));
#400125=CARTESIAN_POINT('Ctrl Pts',(-2.22678761706441,-1.61571401679595,
8.76988516158374));
#400126=CARTESIAN_POINT('Ctrl Pts',(-2.22245839467586,-1.62191032326892,
8.77093053738833));
#400127=CARTESIAN_POINT('Ctrl Pts',(-2.22269264364088,-1.60754892857963,
8.75371302330492));
#400128=CARTESIAN_POINT('Ctrl Pts',(-2.22610538539148,-1.61434741334548,
8.75300828287559));
#400129=CARTESIAN_POINT('Ctrl Pts',(-2.22157935547678,-1.62050448996881,
8.75267964240738));
#400130=CARTESIAN_POINT('Origin',(-2.20532861076148,-1.60076054719536,8.78727029226991));
#400131=CARTESIAN_POINT('Ctrl Pts',(-2.18456153393018,-1.53121811901793,
8.85049129520029));
#400132=CARTESIAN_POINT('Ctrl Pts',(-2.18717121304408,-1.53644216794051,
8.85711686593484));
#400133=CARTESIAN_POINT('Ctrl Pts',(-2.18059607577691,-1.54190736071221,
8.85933012996512));
#400134=CARTESIAN_POINT('Ctrl Pts',(-2.19522683681492,-1.55256789483801,
8.82945683644723));
#400135=CARTESIAN_POINT('Ctrl Pts',(-2.19785817784331,-1.55783530652517,
8.8360746990239));
#400136=CARTESIAN_POINT('Ctrl Pts',(-2.19123976416883,-1.56328770443169,
8.83829567148519));
#400137=CARTESIAN_POINT('Ctrl Pts',(-2.20587624220565,-1.57388584709558,
8.80838214965003));
#400138=CARTESIAN_POINT('Ctrl Pts',(-2.20851796773429,-1.57917404644855,
8.81501364461988));
#400139=CARTESIAN_POINT('Ctrl Pts',(-2.20186790511426,-1.58463531733958,
8.81722098428721));
#400140=CARTESIAN_POINT('Ctrl Pts',(-2.21651095806263,-1.59517439388236,
8.78727029226991));
#400141=CARTESIAN_POINT('Ctrl Pts',(-2.21915312239055,-1.60046347162264,
8.79393457792714));
#400142=CARTESIAN_POINT('Ctrl Pts',(-2.21248169808584,-1.60595268950177,
8.79610912703474));
#400143=CARTESIAN_POINT('Origin',(-2.17337918662903,-1.53680427233093,8.85049129520029));
#400144=CARTESIAN_POINT('Ctrl Pts',(-2.19147106502123,-1.52131278661257,
8.85049129520029));
#400145=CARTESIAN_POINT('Ctrl Pts',(-2.19727496193952,-1.52195768411219,
8.85711686593484));
#400146=CARTESIAN_POINT('Ctrl Pts',(-2.20013305013606,-1.51389963881729,
8.85933012996512));
#400147=CARTESIAN_POINT('Ctrl Pts',(-2.18633644119776,-1.52074225510384,
8.86332496987231));
#400148=CARTESIAN_POINT('Ctrl Pts',(-2.18920666304214,-1.51712096790993,
8.86648636486737));
#400149=CARTESIAN_POINT('Ctrl Pts',(-2.18576683858332,-1.51232058151034,
8.87206031107457));
#400150=CARTESIAN_POINT('Ctrl Pts',(-2.18223709983611,-1.52656507284068,
8.86341338519877));
#400151=CARTESIAN_POINT('Ctrl Pts',(-2.17979784447351,-1.53050506064653,
8.86654584966059));
#400152=CARTESIAN_POINT('Ctrl Pts',(-2.17410071658646,-1.52887200013751,
8.87215952290715));
#400153=CARTESIAN_POINT('Ctrl Pts',(-2.18456153393018,-1.53121811901793,
8.85049129520029));
#400154=CARTESIAN_POINT('Ctrl Pts',(-2.18717121304408,-1.53644216794051,
8.85711686593484));
#400155=CARTESIAN_POINT('Ctrl Pts',(-2.18059607577691,-1.54190736071221,
8.85933012996512));
#400156=CARTESIAN_POINT('Origin',(-2.19285150152199,-1.50888924464309,8.85049129520029));
#400157=CARTESIAN_POINT('Ctrl Pts',(-2.26252622397767,-1.52920804991441,
8.78727029226991));
#400158=CARTESIAN_POINT('Ctrl Pts',(-2.26840236764559,-1.52986097508042,
8.79393457792714));
#400159=CARTESIAN_POINT('Ctrl Pts',(-2.27124974846884,-1.52170427000879,
8.79610912703474));
#400160=CARTESIAN_POINT('Ctrl Pts',(-2.23887473584625,-1.52658002502472,
8.80838214965001));
#400161=CARTESIAN_POINT('Ctrl Pts',(-2.24474990362948,-1.52723284175572,
8.81501364461986));
#400162=CARTESIAN_POINT('Ctrl Pts',(-2.24757843466631,-1.5191058358637,
8.81722098428721));
#400163=CARTESIAN_POINT('Ctrl Pts',(-2.21519057835742,-1.5239483700935,
8.82945683644723));
#400164=CARTESIAN_POINT('Ctrl Pts',(-2.22104265112923,-1.52459862063229,
8.83607469902389));
#400165=CARTESIAN_POINT('Ctrl Pts',(-2.22387378559008,-1.51650438069502,
8.8382956714852));
#400166=CARTESIAN_POINT('Ctrl Pts',(-2.19147106502123,-1.52131278661257,
8.85049129520029));
#400167=CARTESIAN_POINT('Ctrl Pts',(-2.19727496193952,-1.52195768411219,
8.85711686593484));
#400168=CARTESIAN_POINT('Ctrl Pts',(-2.20013305013606,-1.51389963881729,
8.85933012996512));
#400169=CARTESIAN_POINT('Origin',(-2.26390666047843,-1.51678450794493,8.78727029226991));
#400170=CARTESIAN_POINT('Ctrl Pts',(-2.2762790074659,-1.53073616595188,
8.75374538247848));
#400171=CARTESIAN_POINT('Ctrl Pts',(-2.28383003900887,-1.53158839891579,
8.75304829418601));
#400172=CARTESIAN_POINT('Ctrl Pts',(-2.28804536797155,-1.5252243086473,
8.75272238421917));
#400173=CARTESIAN_POINT('Ctrl Pts',(-2.27759091723009,-1.53088193866796,
8.76769408445021));
#400174=CARTESIAN_POINT('Ctrl Pts',(-2.28533204362691,-1.53175493184132,
8.7697431809397));
#400175=CARTESIAN_POINT('Ctrl Pts',(-2.28965015289765,-1.52556039476369,
8.77077869880429));
#400176=CARTESIAN_POINT('Ctrl Pts',(-2.27086681512297,-1.53013479078126,
8.78108014887988));
#400177=CARTESIAN_POINT('Ctrl Pts',(-2.27742671510839,-1.53087839651124,
8.78639403366323));
#400178=CARTESIAN_POINT('Ctrl Pts',(-2.2814316297261,-1.52384399997465,
8.78812224174741));
#400179=CARTESIAN_POINT('Ctrl Pts',(-2.25984749613409,-1.5289103802946,
8.78944554828685));
#400180=CARTESIAN_POINT('Ctrl Pts',(-2.2653753061266,-1.52954262574045,
8.79673892988686));
#400181=CARTESIAN_POINT('Ctrl Pts',(-2.26800404459053,-1.52102245623481,
8.79894799272499));
#400182=CARTESIAN_POINT('Origin',(-2.27784347049495,-1.51833309057122,8.75721825406948));
#400183=CARTESIAN_POINT('Origin',(-2.27784347049495,-1.51833309057122,9.));
#400184=CARTESIAN_POINT('Origin',(-2.27784347049495,-1.51833309057122,7.51860402984325));
#400185=CARTESIAN_POINT('Ctrl Pts',(-2.27461799196034,-1.53898852013195,
7.50366195182966));
#400186=CARTESIAN_POINT('Ctrl Pts',(-2.2776509549566,-1.54104059887638,
7.50000065167735));
#400187=CARTESIAN_POINT('Ctrl Pts',(-2.27765095495667,-1.54104059887629,
7.49482233047108));
#400188=CARTESIAN_POINT('Ctrl Pts',(-2.27994696402869,-1.53379661717625,
7.50215800491337));
#400189=CARTESIAN_POINT('Ctrl Pts',(-2.28299322537738,-1.53314470539552,
7.49877273257265));
#400190=CARTESIAN_POINT('Ctrl Pts',(-2.28492774039884,-1.53028554328369,
7.49481816995647));
#400191=CARTESIAN_POINT('Ctrl Pts',(-2.2792643415883,-1.53106823982956,
7.51043025814043));
#400192=CARTESIAN_POINT('Ctrl Pts',(-2.28502241637527,-1.53010008088879,
7.51006209594515));
#400193=CARTESIAN_POINT('Ctrl Pts',(-2.28824598651205,-1.52526401164451,
7.50731281821701));
#400194=CARTESIAN_POINT('Ctrl Pts',(-2.27646153184158,-1.53075646553772,
7.51860402984326));
#400195=CARTESIAN_POINT('Ctrl Pts',(-2.28402415878926,-1.53159770928414,
7.51860402984326));
#400196=CARTESIAN_POINT('Ctrl Pts',(-2.28824458223237,-1.52526611838204,
7.51860402984327));
#400197=CARTESIAN_POINT('Origin',(0.,0.,7.5));
#400198=CARTESIAN_POINT('Origin',(-2.08949760778587,-1.65859511954946,7.5));
#400199=CARTESIAN_POINT('',(-2.08949760778587,-1.65859511954946,7.59394543036555));
#400200=CARTESIAN_POINT('',(-2.08949760778587,-1.65859511954946,8.85049129520029));
#400201=CARTESIAN_POINT('',(-2.08949760778587,-1.65859511954946,7.5));
#400202=CARTESIAN_POINT('',(-2.15990092504104,-1.67102668085119,8.78727029226991));
#400203=CARTESIAN_POINT('Ctrl Pts',(-2.08949760778587,-1.65859511954946,
8.85049129520029));
#400204=CARTESIAN_POINT('Ctrl Pts',(-2.1129994928842,-1.66274499680947,
8.82945686509571));
#400205=CARTESIAN_POINT('Ctrl Pts',(-2.13646643958853,-1.66688870477513,
8.80838212259895));
#400206=CARTESIAN_POINT('Ctrl Pts',(-2.15990092504104,-1.67102668085119,
8.78727029226991));
#400207=CARTESIAN_POINT('',(-2.17370988235714,-1.67346501623198,8.75721825406948));
#400208=CARTESIAN_POINT('Origin',(-2.13215390434231,-1.66612741793497,8.75937679713138));
#400209=CARTESIAN_POINT('',(-2.17370988235714,-1.67346501623198,7.51860402984325));
#400210=CARTESIAN_POINT('',(-2.17370988235714,-1.67346501623198,7.5));
#400211=CARTESIAN_POINT('Ctrl Pts',(-2.17370988235714,-1.67346501623198,
7.51860402984325));
#400212=CARTESIAN_POINT('Ctrl Pts',(-2.16286509408444,-1.67155008302325,
7.52834476460825));
#400213=CARTESIAN_POINT('Ctrl Pts',(-2.15201326553169,-1.66963390666753,
7.53807742314407));
#400214=CARTESIAN_POINT('Ctrl Pts',(-2.14115416031211,-1.66771644542448,
7.54780169004674));
#400215=CARTESIAN_POINT('Ctrl Pts',(-2.12395392452886,-1.66467929044543,
7.5632044032688));
#400216=CARTESIAN_POINT('Ctrl Pts',(-2.10673541065635,-1.66163890798794,
7.57858609112103));
#400217=CARTESIAN_POINT('Ctrl Pts',(-2.08949760778587,-1.65859511954946,
7.59394543036555));
#400218=CARTESIAN_POINT('Origin',(-2.1888484874705,-1.92141752211061,7.5));
#400219=CARTESIAN_POINT('',(-2.11520370755652,-1.74682943894031,8.75721825406948));
#400220=CARTESIAN_POINT('',(-2.10975372425559,-1.73390928168094,8.78727029226991));
#400221=CARTESIAN_POINT('Origin',(-2.09591963389519,-1.70111310357778,8.75658640621024));
#400222=CARTESIAN_POINT('',(-2.0819676362413,-1.66803740521009,8.85049129520029));
#400223=CARTESIAN_POINT('Ctrl Pts',(-2.10975372425559,-1.73390928168094,
8.78727029226991));
#400224=CARTESIAN_POINT('Ctrl Pts',(-2.10050483228942,-1.71198313400681,
8.80838212259896));
#400225=CARTESIAN_POINT('Ctrl Pts',(-2.09124312883602,-1.69002661441764,
8.82945686509571));
#400226=CARTESIAN_POINT('Ctrl Pts',(-2.0819676362413,-1.66803740521009,
8.85049129520029));
#400227=CARTESIAN_POINT('',(-2.0819676362413,-1.66803740521009,7.59394543036555));
#400228=CARTESIAN_POINT('',(-2.0819676362413,-1.66803740521009,7.5));
#400229=CARTESIAN_POINT('',(-2.11520370755652,-1.7468294389403,7.51860402984325));
#400230=CARTESIAN_POINT('Ctrl Pts',(-2.0819676362413,-1.66803740521009,
7.59394543036555));
#400231=CARTESIAN_POINT('Ctrl Pts',(-2.08877088254284,-1.68416571372711,
7.57858609112103));
#400232=CARTESIAN_POINT('Ctrl Pts',(-2.09556651605252,-1.70027597476349,
7.56320440326857));
#400233=CARTESIAN_POINT('Ctrl Pts',(-2.10235493574598,-1.71636913416218,
7.54780169004651));
#400234=CARTESIAN_POINT('Ctrl Pts',(-2.10664070046775,-1.72652930367544,
7.53807742314383));
#400235=CARTESIAN_POINT('Ctrl Pts',(-2.11092359330638,-1.73668266487762,
7.52834476460825));
#400236=CARTESIAN_POINT('Ctrl Pts',(-2.11520370755652,-1.7468294389403,
7.51860402984325));
#400237=CARTESIAN_POINT('',(-2.11520370755652,-1.74682943894031,7.5));
#400238=CARTESIAN_POINT('Origin',(-2.08830213916381,-1.66536538392936,7.5));
#400239=CARTESIAN_POINT('Ctrl Pts',(-2.0819676362413,-1.66803740521009,
8.85049129520029));
#400240=CARTESIAN_POINT('Ctrl Pts',(-2.08189236821729,-1.66785896893733,
8.85097269580138));
#400241=CARTESIAN_POINT('Ctrl Pts',(-2.0818257999648,-1.66767951480866,
8.85143669361005));
#400242=CARTESIAN_POINT('Ctrl Pts',(-2.08176568593669,-1.66749047547276,
8.8519052845931));
#400243=CARTESIAN_POINT('Ctrl Pts',(-2.08164810671,-1.66712072652019,8.85282181883899));
#400244=CARTESIAN_POINT('Ctrl Pts',(-2.08155843158663,-1.66672375951531,
8.85372622499635));
#400245=CARTESIAN_POINT('Ctrl Pts',(-2.08151029317523,-1.6662899478711,
8.85462257735071));
#400246=CARTESIAN_POINT('Ctrl Pts',(-2.08147033037579,-1.66592981285161,
8.85536669723986));
#400247=CARTESIAN_POINT('Ctrl Pts',(-2.08145895303519,-1.66554420686675,
8.85610498449051));
#400248=CARTESIAN_POINT('Ctrl Pts',(-2.08149195894183,-1.66512735346751,
8.85681338218371));
#400249=CARTESIAN_POINT('Ctrl Pts',(-2.08152191185394,-1.66474905835301,
8.85745625420285));
#400250=CARTESIAN_POINT('Ctrl Pts',(-2.08158819609811,-1.66434023658327,
8.85808743050666));
#400251=CARTESIAN_POINT('Ctrl Pts',(-2.08171825097903,-1.66389283019907,
8.85866804508411));
#400252=CARTESIAN_POINT('Ctrl Pts',(-2.08177825548183,-1.66368640659199,
8.85893592806396));
#400253=CARTESIAN_POINT('Ctrl Pts',(-2.08185207387119,-1.66347172942508,
8.85919241173848));
#400254=CARTESIAN_POINT('Ctrl Pts',(-2.08194399665606,-1.66324796592625,
8.85943017985534));
#400255=CARTESIAN_POINT('Ctrl Pts',(-2.0820681196277,-1.66294581896174,
8.8597512372));
#400256=CARTESIAN_POINT('Ctrl Pts',(-2.08222900408983,-1.66261965786936,
8.86004599534706));
#400257=CARTESIAN_POINT('Ctrl Pts',(-2.08243405763912,-1.66227800874228,
8.86026130871721));
#400258=CARTESIAN_POINT('Ctrl Pts',(-2.08250913352459,-1.66215292136474,
8.86034014101235));
#400259=CARTESIAN_POINT('Ctrl Pts',(-2.08259124742369,-1.662023872527,8.86040910639692));
#400260=CARTESIAN_POINT('Ctrl Pts',(-2.08267844598716,-1.66189455867301,
8.86046313645506));
#400261=CARTESIAN_POINT('Ctrl Pts',(-2.08281451861518,-1.66169276548686,
8.86054744990829));
#400262=CARTESIAN_POINT('Ctrl Pts',(-2.08296680936883,-1.66148490081205,
8.86059655985668));
#400263=CARTESIAN_POINT('Ctrl Pts',(-2.08312531505842,-1.66128412250461,
8.86059725258816));
#400264=CARTESIAN_POINT('Ctrl Pts',(-2.08328418695947,-1.66108288031908,
8.86059794692011));
#400265=CARTESIAN_POINT('Ctrl Pts',(-2.08345314972536,-1.66088817171568,
8.86056369958366));
#400266=CARTESIAN_POINT('Ctrl Pts',(-2.08362014586833,-1.66070814983365,
8.86048590497774));
#400267=CARTESIAN_POINT('Ctrl Pts',(-2.08366372688957,-1.66066116948234,
8.86046560290182));
#400268=CARTESIAN_POINT('Ctrl Pts',(-2.08370780734365,-1.6606146397908,
8.86044257503091));
#400269=CARTESIAN_POINT('Ctrl Pts',(-2.08375100127772,-1.66056997598908,
8.86041778462583));
#400270=CARTESIAN_POINT('Ctrl Pts',(-2.08404164285482,-1.66026944402666,
8.86025097596201));
#400271=CARTESIAN_POINT('Ctrl Pts',(-2.08433138499249,-1.66001329577687,
8.8599848982295));
#400272=CARTESIAN_POINT('Ctrl Pts',(-2.08460615922178,-1.65980265990706,
8.85968173251461));
#400273=CARTESIAN_POINT('Ctrl Pts',(-2.08475149904638,-1.65969124559992,
8.85952137522076));
#400274=CARTESIAN_POINT('Ctrl Pts',(-2.08489533649675,-1.65959026561899,
8.85934740853961));
#400275=CARTESIAN_POINT('Ctrl Pts',(-2.08503474992656,-1.65949987168832,
8.8591675900182));
#400276=CARTESIAN_POINT('Ctrl Pts',(-2.08559456731288,-1.65913689307085,
8.85844552518694));
#400277=CARTESIAN_POINT('Ctrl Pts',(-2.08611304340986,-1.6589215545218,
8.85759444184122));
#400278=CARTESIAN_POINT('Ctrl Pts',(-2.08655155128532,-1.65878394965752,
8.85683498915135));
#400279=CARTESIAN_POINT('Ctrl Pts',(-2.08659743996664,-1.65876954967494,
8.85675551444996));
#400280=CARTESIAN_POINT('Ctrl Pts',(-2.08664245504371,-1.65875602081341,
8.8566769979365));
#400281=CARTESIAN_POINT('Ctrl Pts',(-2.08668655297731,-1.65874329607418,
8.85659965593547));
#400282=CARTESIAN_POINT('Ctrl Pts',(-2.08728178913533,-1.65857153689463,
8.85555568965886));
#400283=CARTESIAN_POINT('Ctrl Pts',(-2.0878786533853,-1.65849242956098,
8.85434650606346));
#400284=CARTESIAN_POINT('Ctrl Pts',(-2.08847927973752,-1.65849942215004,
8.85297329937117));
#400285=CARTESIAN_POINT('Ctrl Pts',(-2.08881709546394,-1.65850335505532,
8.85220095427747));
#400286=CARTESIAN_POINT('Ctrl Pts',(-2.08915623562913,-1.65853484129755,
8.85137579139183));
#400287=CARTESIAN_POINT('Ctrl Pts',(-2.08949760778587,-1.65859511954946,
8.85049129520029));
#400288=CARTESIAN_POINT('Origin',(-2.08830213916381,-1.66536538392936,7.59394543036555));
#400289=CARTESIAN_POINT('Ctrl Pts',(-2.08174910777617,-1.66751934451537,
7.59443877723642));
#400290=CARTESIAN_POINT('Ctrl Pts',(-2.0794984748478,-1.66218381782436,
7.58783886950016));
#400291=CARTESIAN_POINT('Ctrl Pts',(-2.08634518032501,-1.65716367782183,
7.58559994247159));
#400292=CARTESIAN_POINT('Ctrl Pts',(-2.0940352469014,-1.69664582818389,
7.56670252222139));
#400293=CARTESIAN_POINT('Ctrl Pts',(-2.09178786677668,-1.69131801284369,
7.5600487499903));
#400294=CARTESIAN_POINT('Ctrl Pts',(-2.09866250781647,-1.68625089652093,
7.55786368756705));
#400295=CARTESIAN_POINT('Ctrl Pts',(-2.10629844288932,-1.72571792105421,
7.53888913333559));
#400296=CARTESIAN_POINT('Ctrl Pts',(-2.10403770647443,-1.72035844224663,
7.53222002137282));
#400297=CARTESIAN_POINT('Ctrl Pts',(-2.11095619627074,-1.71528528310685,
7.53005029815326));
#400298=CARTESIAN_POINT('Ctrl Pts',(-2.11853814082205,-1.7547343075945,
7.51101258149734));
#400299=CARTESIAN_POINT('Ctrl Pts',(-2.1162500001739,-1.74930986216536,
7.5043616886572));
#400300=CARTESIAN_POINT('Ctrl Pts',(-2.12322571438818,-1.74426537083864,
7.50217374673251));
#400301=CARTESIAN_POINT('',(-2.12257099619412,-1.74271895653113,7.50366116523517));
#400302=CARTESIAN_POINT('Ctrl Pts',(-2.11520370755652,-1.74682943894031,
7.51860402984325));
#400303=CARTESIAN_POINT('Ctrl Pts',(-2.11537534312976,-1.74723633167283,
7.51734760759493));
#400304=CARTESIAN_POINT('Ctrl Pts',(-2.11558525971438,-1.74758089355041,
7.51608817408572));
#400305=CARTESIAN_POINT('Ctrl Pts',(-2.11584437846304,-1.74785538445544,
7.51481005913119));
#400306=CARTESIAN_POINT('Ctrl Pts',(-2.11607909441742,-1.7481040248764,
7.51365231206383));
#400307=CARTESIAN_POINT('Ctrl Pts',(-2.11635433051562,-1.74829569308608,
7.51247773061042));
#400308=CARTESIAN_POINT('Ctrl Pts',(-2.11668642557096,-1.74839677088776,
7.51129758471022));
#400309=CARTESIAN_POINT('Ctrl Pts',(-2.11709918179806,-1.74852239905173,
7.50983079813402));
#400310=CARTESIAN_POINT('Ctrl Pts',(-2.11759039124035,-1.74849161668061,
7.50839324291155));
#400311=CARTESIAN_POINT('Ctrl Pts',(-2.118158482838,-1.74822192091236,7.50715379678855));
#400312=CARTESIAN_POINT('Ctrl Pts',(-2.11842092478694,-1.74809732923853,
7.50658120839351));
#400313=CARTESIAN_POINT('Ctrl Pts',(-2.1187330082656,-1.74789545390144,
7.50598221009429));
#400314=CARTESIAN_POINT('Ctrl Pts',(-2.11907495170042,-1.74760200027013,
7.50545747549612));
#400315=CARTESIAN_POINT('Ctrl Pts',(-2.11925742330137,-1.74744540432923,
7.50517746087247));
#400316=CARTESIAN_POINT('Ctrl Pts',(-2.11945050840504,-1.74726118598095,
7.50491486231392));
#400317=CARTESIAN_POINT('Ctrl Pts',(-2.11964794236266,-1.74705301678731,
7.50468370960993));
#400318=CARTESIAN_POINT('Ctrl Pts',(-2.11994316840631,-1.74674173817957,
7.50433806340446));
#400319=CARTESIAN_POINT('Ctrl Pts',(-2.12025656715067,-1.74636718909903,
7.50405484070983));
#400320=CARTESIAN_POINT('Ctrl Pts',(-2.12056648234371,-1.74595413500245,
7.5038576603613));
#400321=CARTESIAN_POINT('Ctrl Pts',(-2.12059962295642,-1.74590996528715,
7.50383657498791));
#400322=CARTESIAN_POINT('Ctrl Pts',(-2.12063272061545,-1.74586538345795,
7.50381643264937));
#400323=CARTESIAN_POINT('Ctrl Pts',(-2.12066574689268,-1.74582044031312,
7.50379723213559));
#400324=CARTESIAN_POINT('Ctrl Pts',(-2.1208862080969,-1.74552043011945,
7.50366906242519));
#400325=CARTESIAN_POINT('Ctrl Pts',(-2.12110770464417,-1.74519736799651,
7.50358235568538));
#400326=CARTESIAN_POINT('Ctrl Pts',(-2.12131371482981,-1.74488084388013,
7.5035341175365));
#400327=CARTESIAN_POINT('Ctrl Pts',(-2.12162260378732,-1.74440625179124,
7.50346178989176));
#400328=CARTESIAN_POINT('Ctrl Pts',(-2.12193471890785,-1.74388256510034,
7.50346967198527));
#400329=CARTESIAN_POINT('Ctrl Pts',(-2.12222530044295,-1.74335903907261,
7.50354272648692));
#400330=CARTESIAN_POINT('Ctrl Pts',(-2.12234482264302,-1.74314370198106,
7.50357277531559));
#400331=CARTESIAN_POINT('Ctrl Pts',(-2.12246066686334,-1.74292874699817,
7.50361331098761));
#400332=CARTESIAN_POINT('Ctrl Pts',(-2.12257099619522,-1.74271895653203,
7.50366116523658));
#400333=CARTESIAN_POINT('',(-2.09059128325,-1.66719091542116,7.57603338622103));
#400334=CARTESIAN_POINT('Origin',(-2.09750205887796,-1.67269842573203,7.58486873427627));
#400335=CARTESIAN_POINT('Ctrl Pts',(-2.12257099621145,-1.7427189565858,
7.50366116529969));
#400336=CARTESIAN_POINT('Ctrl Pts',(-2.11192925635161,-1.71758369904671,
7.52783573079709));
#400337=CARTESIAN_POINT('Ctrl Pts',(-2.10126987184862,-1.69240886704498,
7.55196141284069));
#400338=CARTESIAN_POINT('Ctrl Pts',(-2.09059128339266,-1.66719091666507,
7.57603338728831));
#400339=CARTESIAN_POINT('Ctrl Pts',(-2.0824357048269,-1.66876158506199,
7.59642833564546));
#400340=CARTESIAN_POINT('Ctrl Pts',(-2.07320936503718,-1.65296337419292,
7.59959882295454));
#400341=CARTESIAN_POINT('Ctrl Pts',(-2.09047977720865,-1.65894708367391,
7.59639677331373));
#400342=CARTESIAN_POINT('Ctrl Pts',(-2.07997313262292,-1.66580784542594,
7.58710240504251));
#400343=CARTESIAN_POINT('Ctrl Pts',(-2.08056667580051,-1.65907270568811,
7.58809943920597));
#400344=CARTESIAN_POINT('Ctrl Pts',(-2.08704726491593,-1.65709425787427,
7.58707626057426));
#400345=CARTESIAN_POINT('Ctrl Pts',(-2.08602293135984,-1.66622189099849,
7.58020924244131));
#400346=CARTESIAN_POINT('Ctrl Pts',(-2.08590041445982,-1.66340905174837,
7.58205880659759));
#400347=CARTESIAN_POINT('Ctrl Pts',(-2.08871246990533,-1.66293829112231,
7.58015376756931));
#400348=CARTESIAN_POINT('Ctrl Pts',(-2.09059128260286,-1.66719091490534,
7.57603338509286));
#400349=CARTESIAN_POINT('Ctrl Pts',(-2.09059128260286,-1.66719091490534,
7.57603338509286));
#400350=CARTESIAN_POINT('Ctrl Pts',(-2.09059128260286,-1.66719091490534,
7.57603338509286));
#400351=CARTESIAN_POINT('Origin',(-2.09749850102522,-1.67270288713742,7.58486873427623));
#400352=CARTESIAN_POINT('Ctrl Pts',(-2.18218524326637,-1.67496156458801,
7.51098857897448));
#400353=CARTESIAN_POINT('Ctrl Pts',(-2.17638761437571,-1.6739378403976,
7.50433767179956));
#400354=CARTESIAN_POINT('Ctrl Pts',(-2.17302184310319,-1.68186120046916,
7.50214974420965));
#400355=CARTESIAN_POINT('Ctrl Pts',(-2.15116384911717,-1.66948391981123,
7.53887321589168));
#400356=CARTESIAN_POINT('Ctrl Pts',(-2.14543568610955,-1.6684724616534,
7.53220407452062));
#400357=CARTESIAN_POINT('Ctrl Pts',(-2.14202920965963,-1.67634639574748,
7.53003438070912));
#400358=CARTESIAN_POINT('Ctrl Pts',(-2.1200828824479,-1.66399575593586,
7.56669465659233));
#400359=CARTESIAN_POINT('Ctrl Pts',(-2.11438857181869,-1.66299027530768,
7.560040858333));
#400360=CARTESIAN_POINT('Ctrl Pts',(-2.11097822695242,-1.67082010276551,
7.55785582193789));
#400361=CARTESIAN_POINT('Ctrl Pts',(-2.08894374892624,-1.65849732116958,
7.59443891967696));
#400362=CARTESIAN_POINT('Ctrl Pts',(-2.08324118225558,-1.6574903827197,
7.58783901202978));
#400363=CARTESIAN_POINT('Ctrl Pts',(-2.07987044293451,-1.66528251300722,
7.58560008491213));
#400364=CARTESIAN_POINT('',(-2.17134183427226,-1.68156225994657,7.50366116523517));
#400365=CARTESIAN_POINT('Ctrl Pts',(-2.17134183427256,-1.6815622599468,
7.50366116523554));
#400366=CARTESIAN_POINT('Ctrl Pts',(-2.17191706145343,-1.68106905491119,
7.50350835821027));
#400367=CARTESIAN_POINT('Ctrl Pts',(-2.17242978893375,-1.6805969653624,
7.50345484956));
#400368=CARTESIAN_POINT('Ctrl Pts',(-2.17289566726916,-1.68013239745889,
7.50349758195598));
#400369=CARTESIAN_POINT('Ctrl Pts',(-2.17313469740567,-1.67989403967114,
7.50351950684424));
#400370=CARTESIAN_POINT('Ctrl Pts',(-2.17338504590861,-1.67963426007722,
7.50357029184312));
#400371=CARTESIAN_POINT('Ctrl Pts',(-2.173619568278,-1.6793771217698,7.50365515313924));
#400372=CARTESIAN_POINT('Ctrl Pts',(-2.17398035864961,-1.67898153892741,
7.50378570417639));
#400373=CARTESIAN_POINT('Ctrl Pts',(-2.17431454058786,-1.67858082916846,
7.50400001621911));
#400374=CARTESIAN_POINT('Ctrl Pts',(-2.17459493436348,-1.6782040381801,
7.50428903009635));
#400375=CARTESIAN_POINT('Ctrl Pts',(-2.17462605591535,-1.67816221727924,
7.50432110841318));
#400376=CARTESIAN_POINT('Ctrl Pts',(-2.17465654354018,-1.67812068129182,
7.50435406373354));
#400377=CARTESIAN_POINT('Ctrl Pts',(-2.17468638116337,-1.67807946244959,
7.50438785222352));
#400378=CARTESIAN_POINT('Ctrl Pts',(-2.17486855419472,-1.67782780160552,
7.50459414719561));
#400379=CARTESIAN_POINT('Ctrl Pts',(-2.1750289797857,-1.67758365383019,
7.50483629897752));
#400380=CARTESIAN_POINT('Ctrl Pts',(-2.17516261192364,-1.67735709504314,
7.5050991045531));
#400381=CARTESIAN_POINT('Ctrl Pts',(-2.175457417842,-1.67685728360323,7.50567888004914));
#400382=CARTESIAN_POINT('Ctrl Pts',(-2.17563388843445,-1.67642364454149,
7.50637912803145));
#400383=CARTESIAN_POINT('Ctrl Pts',(-2.17572270244567,-1.67605995052005,
7.50710440483569));
#400384=CARTESIAN_POINT('Ctrl Pts',(-2.17574448140443,-1.67597076552566,
7.50728225710685));
#400385=CARTESIAN_POINT('Ctrl Pts',(-2.17576156466507,-1.6758840457421,
7.50746498566954));
#400386=CARTESIAN_POINT('Ctrl Pts',(-2.17577396218682,-1.6758018960086,
7.50764697238949));
#400387=CARTESIAN_POINT('Ctrl Pts',(-2.17584060785185,-1.67536028164955,
7.50862528291182));
#400388=CARTESIAN_POINT('Ctrl Pts',(-2.17578198568442,-1.67501126343843,
7.50965856837422));
#400389=CARTESIAN_POINT('Ctrl Pts',(-2.17565812194903,-1.67472669455634,
7.51067959873202));
#400390=CARTESIAN_POINT('Ctrl Pts',(-2.17558995957922,-1.67457009594159,
7.51124147302579));
#400391=CARTESIAN_POINT('Ctrl Pts',(-2.17550162506262,-1.67443314976764,
7.51180065547253));
#400392=CARTESIAN_POINT('Ctrl Pts',(-2.17540067259095,-1.67431233954431,
7.512351757165));
#400393=CARTESIAN_POINT('Ctrl Pts',(-2.17505184158664,-1.67389489209763,
7.51425603304536));
#400394=CARTESIAN_POINT('Ctrl Pts',(-2.17450610980346,-1.67362422025112,
7.5162690050518));
#400395=CARTESIAN_POINT('Ctrl Pts',(-2.17382216528628,-1.67348623923338,
7.51827788969244));
#400396=CARTESIAN_POINT('Ctrl Pts',(-2.17378514891654,-1.67347877143995,
7.51838661432545));
#400397=CARTESIAN_POINT('Ctrl Pts',(-2.17374771906854,-1.67347169730064,
7.51849533314856));
#400398=CARTESIAN_POINT('Ctrl Pts',(-2.17370988235714,-1.67346501623197,
7.51860402984325));
#400399=CARTESIAN_POINT('Ctrl Pts',(-2.09059128449555,-1.667190915284,7.57603338728985));
#400400=CARTESIAN_POINT('Ctrl Pts',(-2.11755317769155,-1.67199024736255,
7.55196141284922));
#400401=CARTESIAN_POINT('Ctrl Pts',(-2.1444687603117,-1.67678045171609,
7.52783573083105));
#400402=CARTESIAN_POINT('Ctrl Pts',(-2.17134183433124,-1.68156225995155,
7.50366116530176));
#400403=CARTESIAN_POINT('Origin',(-7.22395927215198E-16,-5.76091528191156E-16,
7.49482233047033));
#400404=CARTESIAN_POINT('Origin',(-2.11573969989722,-1.73711017850879,7.49482233047033));
#400405=CARTESIAN_POINT('Origin',(0.,0.,7.50366116523517));
#400406=CARTESIAN_POINT('Origin',(-2.16435357359294,-1.67615030903422,7.49482233047033));
#400407=CARTESIAN_POINT('Ctrl Pts',(-2.11520329642423,-1.74682846439302,
7.51860402984325));
#400408=CARTESIAN_POINT('Ctrl Pts',(-2.11816117044153,-1.75383897559606,
7.51860402984325));
#400409=CARTESIAN_POINT('Ctrl Pts',(-2.11329230362297,-1.75968623323817,
7.51860402984325));
#400410=CARTESIAN_POINT('Ctrl Pts',(-2.11630157406165,-1.74943151553891,
7.51041458714367));
#400411=CARTESIAN_POINT('Ctrl Pts',(-2.11700767251761,-1.7552242515704,
7.51004642900444));
#400412=CARTESIAN_POINT('Ctrl Pts',(-2.11329096084731,-1.7596878458424,
7.50729136483011));
#400413=CARTESIAN_POINT('Ctrl Pts',(-2.11911337163088,-1.7492991084811,
7.50215815450137));
#400414=CARTESIAN_POINT('Ctrl Pts',(-2.11935641728299,-1.75240378129678,
7.49877163671527));
#400415=CARTESIAN_POINT('Ctrl Pts',(-2.11716706414825,-1.75507036271234,
7.49481588533168));
#400416=CARTESIAN_POINT('Ctrl Pts',(-2.12257057071394,-1.74271860719361,
7.50366171572174));
#400417=CARTESIAN_POINT('Ctrl Pts',(-2.12540061176914,-1.74504218845602,
7.50000045605858));
#400418=CARTESIAN_POINT('Ctrl Pts',(-2.12540061176906,-1.74504218845612,
7.49482233047317));
#400419=CARTESIAN_POINT('Origin',(-2.10368642951559,-1.75168765945072,7.51860402984325));
#400420=CARTESIAN_POINT('Origin',(-2.10368642951559,-1.75168765945072,9.));
#400421=CARTESIAN_POINT('Origin',(-2.10368642951559,-1.75168765945072,8.75721825406948));
#400422=CARTESIAN_POINT('Ctrl Pts',(-2.10871303450337,-1.73144221877687,
8.78942910404913));
#400423=CARTESIAN_POINT('Ctrl Pts',(-2.11089742331394,-1.73656870629036,
8.79672699501692));
#400424=CARTESIAN_POINT('Ctrl Pts',(-2.10346799228943,-1.74151613396892,
8.79893251111267));
#400425=CARTESIAN_POINT('Ctrl Pts',(-2.11298607127434,-1.74157220275977,
8.78111911759577));
#400426=CARTESIAN_POINT('Ctrl Pts',(-2.11556884143811,-1.74765263106761,
8.78644465894808));
#400427=CARTESIAN_POINT('Ctrl Pts',(-2.10994214649951,-1.75348836716885,
8.78817647674131));
#400428=CARTESIAN_POINT('Ctrl Pts',(-2.11564912968225,-1.74788545041324,
8.76780923932033));
#400429=CARTESIAN_POINT('Ctrl Pts',(-2.1186932906009,-1.7550651315393,8.76988516158378));
#400430=CARTESIAN_POINT('Ctrl Pts',(-2.11397596434525,-1.76097133280529,
8.77093053738833));
#400431=CARTESIAN_POINT('Ctrl Pts',(-2.11512986973763,-1.74665445352436,
8.75371302330491));
#400432=CARTESIAN_POINT('Ctrl Pts',(-2.1181000192298,-1.75365762518883,
8.75300828287558));
#400433=CARTESIAN_POINT('Ctrl Pts',(-2.11318880327528,-1.75951206770562,
8.75267964240738));
#400434=CARTESIAN_POINT('Origin',(-2.09823644621466,-1.73876750219136,8.78727029226991));
#400435=CARTESIAN_POINT('Ctrl Pts',(-2.0819676362413,-1.66803740521009,
8.85049129520029));
#400436=CARTESIAN_POINT('Ctrl Pts',(-2.08423724752591,-1.67341792347879,
8.85711686593484));
#400437=CARTESIAN_POINT('Ctrl Pts',(-2.07732546348032,-1.67845061693468,
8.85933012996512));
#400438=CARTESIAN_POINT('Ctrl Pts',(-2.09124314128408,-1.69002664392798,
8.82945683644723));
#400439=CARTESIAN_POINT('Ctrl Pts',(-2.09353159171458,-1.69545182375142,
8.83607469902389));
#400440=CARTESIAN_POINT('Ctrl Pts',(-2.08657743994754,-1.70046897590164,
8.83829567148519));
#400441=CARTESIAN_POINT('Ctrl Pts',(-2.10050482043861,-1.71198310591234,
8.80838214965002));
#400442=CARTESIAN_POINT('Ctrl Pts',(-2.10280230216299,-1.71742969602838,
8.81501364461993));
#400443=CARTESIAN_POINT('Ctrl Pts',(-2.09581599798245,-1.72245367517764,
8.81722098428721));
#400444=CARTESIAN_POINT('Ctrl Pts',(-2.10975372425559,-1.73390928168094,
8.78727029226991));
#400445=CARTESIAN_POINT('Ctrl Pts',(-2.11205158759922,-1.73935677649347,
8.79393457792714));
#400446=CARTESIAN_POINT('Ctrl Pts',(-2.1050421750542,-1.74440727656297,
8.79610912703474));
#400447=CARTESIAN_POINT('Origin',(-2.07045035820037,-1.67289562572051,8.85049129520029));
#400448=CARTESIAN_POINT('Ctrl Pts',(-2.08949760778587,-1.65859511954946,
8.85049129520029));
#400449=CARTESIAN_POINT('Ctrl Pts',(-2.09524826125081,-1.65961054899031,
8.85711686593484));
#400450=CARTESIAN_POINT('Ctrl Pts',(-2.09861675793328,-1.65175217815317,
8.85933012996512));
#400451=CARTESIAN_POINT('Ctrl Pts',(-2.08441008767702,-1.65769678378102,
8.86332496987232));
#400452=CARTESIAN_POINT('Ctrl Pts',(-2.08750642900991,-1.65426683265499,
8.86648636486738));
#400453=CARTESIAN_POINT('Ctrl Pts',(-2.08438123385197,-1.64925591885433,
8.87206031107457));
#400454=CARTESIAN_POINT('Ctrl Pts',(-2.07994609963853,-1.66324499221152,
8.86341338519876));
#400455=CARTESIAN_POINT('Ctrl Pts',(-2.07725942010221,-1.66702060126219,
8.86654584966059));
#400456=CARTESIAN_POINT('Ctrl Pts',(-2.0716786281215,-1.66502587981416,
8.87215952290713));
#400457=CARTESIAN_POINT('Ctrl Pts',(-2.0819676362413,-1.66803740521009,
8.85049129520029));
#400458=CARTESIAN_POINT('Ctrl Pts',(-2.08423724752591,-1.67341792347879,
8.85711686593484));
#400459=CARTESIAN_POINT('Ctrl Pts',(-2.07732546348032,-1.67845061693468,
8.85933012996512));
#400460=CARTESIAN_POINT('Origin',(-2.09167118709871,-1.64628554794966,8.85049129520029));
#400461=CARTESIAN_POINT('Ctrl Pts',(-2.15990092504104,-1.67102668085119,
8.78727029226991));
#400462=CARTESIAN_POINT('Ctrl Pts',(-2.16572316248256,-1.67205475032986,
8.79393457792714));
#400463=CARTESIAN_POINT('Ctrl Pts',(-2.16908729494479,-1.66409723639932,
8.79610912703474));
#400464=CARTESIAN_POINT('Ctrl Pts',(-2.13646640956138,-1.66688869947304,
8.80838214965003));
#400465=CARTESIAN_POINT('Ctrl Pts',(-2.14228768007073,-1.66791659821436,
8.81501364461985));
#400466=CARTESIAN_POINT('Ctrl Pts',(-2.14563109864247,-1.65998751473331,
8.81722098428721));
#400467=CARTESIAN_POINT('Ctrl Pts',(-2.11299952442461,-1.66274500237876,
8.82945683644721));
#400468=CARTESIAN_POINT('Ctrl Pts',(-2.1187979117902,-1.6637688604979,8.83607469902389));
#400469=CARTESIAN_POINT('Ctrl Pts',(-2.12214182911503,-1.65587264245239,
8.8382956714852));
#400470=CARTESIAN_POINT('Ctrl Pts',(-2.08949760778587,-1.65859511954946,
8.85049129520029));
#400471=CARTESIAN_POINT('Ctrl Pts',(-2.09524826125081,-1.65961054899031,
8.85711686593484));
#400472=CARTESIAN_POINT('Ctrl Pts',(-2.09861675793328,-1.65175217815317,
8.85933012996512));
#400473=CARTESIAN_POINT('Origin',(-2.16207450435388,-1.65871710925138,8.78727029226991));
#400474=CARTESIAN_POINT('Ctrl Pts',(-2.17352754522994,-1.67343280107381,
8.75374538247848));
#400475=CARTESIAN_POINT('Ctrl Pts',(-2.18100845961528,-1.67476707928573,
8.75304829418602));
#400476=CARTESIAN_POINT('Ctrl Pts',(-2.18562287639599,-1.66868614177718,
8.75272238421917));
#400477=CARTESIAN_POINT('Ctrl Pts',(-2.17482741984483,-1.6736623286314,
8.76769408445018));
#400478=CARTESIAN_POINT('Ctrl Pts',(-2.18249670840255,-1.67502950381778,
8.76974318093967));
#400479=CARTESIAN_POINT('Ctrl Pts',(-2.18720283100794,-1.66912435629184,
8.7707786988043));
#400480=CARTESIAN_POINT('Ctrl Pts',(-2.16816500305613,-1.67248590113899,
8.78108014887993));
#400481=CARTESIAN_POINT('Ctrl Pts',(-2.17466378204077,-1.67364827328635,
8.78639403366326));
#400482=CARTESIAN_POINT('Ctrl Pts',(-2.17911116346539,-1.66688492543245,
8.78812224174741));
#400483=CARTESIAN_POINT('Ctrl Pts',(-2.15724677268913,-1.67055799614333,
8.78944554828685));
#400484=CARTESIAN_POINT('Ctrl Pts',(-2.16272271709835,-1.67154311057534,
8.79673892988686));
#400485=CARTESIAN_POINT('Ctrl Pts',(-2.16589194367168,-1.6632088705234,
8.79894799272499));
#400486=CARTESIAN_POINT('Origin',(-2.17588346166998,-1.66115544463217,8.75721825406948));
#400487=CARTESIAN_POINT('Origin',(-2.17588346166998,-1.66115544463217,9.));
#400488=CARTESIAN_POINT('Origin',(-2.17588346166998,-1.66115544463217,7.51860402984325));
#400489=CARTESIAN_POINT('Ctrl Pts',(-2.1713412123112,-1.68156177827833,
7.50366195182966));
#400490=CARTESIAN_POINT('Ctrl Pts',(-2.17423646662313,-1.68380396341326,
7.50000065167735));
#400491=CARTESIAN_POINT('Ctrl Pts',(-2.1742364666232,-1.68380396341317,
7.49482233047108));
#400492=CARTESIAN_POINT('Ctrl Pts',(-2.1769918817994,-1.67672197105677,
7.50215800491337));
#400493=CARTESIAN_POINT('Ctrl Pts',(-2.18007365240864,-1.67626657333344,
7.49877273257265));
#400494=CARTESIAN_POINT('Ctrl Pts',(-2.18218737990697,-1.67353723047978,
7.49481816995649));
#400495=CARTESIAN_POINT('Ctrl Pts',(-2.17648546961679,-1.67395546368403,
7.51043025814043));
#400496=CARTESIAN_POINT('Ctrl Pts',(-2.18229374397787,-1.67335821504791,
7.51006209594516));
#400497=CARTESIAN_POINT('Ctrl Pts',(-2.18582053896442,-1.66873861687435,
7.50731281821699));
#400498=CARTESIAN_POINT('Ctrl Pts',(-2.17370839399078,-1.67346475332887,
7.51860402984326));
#400499=CARTESIAN_POINT('Ctrl Pts',(-2.18120158403841,-1.67478880782197,
7.51860402984326));
#400500=CARTESIAN_POINT('Ctrl Pts',(-2.18581900259085,-1.66874062931085,
7.51860402984327));
#400501=CARTESIAN_POINT('Origin',(0.,0.,7.5));
#400502=CARTESIAN_POINT('Origin',(-1.97893795668429,-1.78906192937259,7.5));
#400503=CARTESIAN_POINT('',(-1.97893795668429,-1.78906192937259,7.59394543036555));
#400504=CARTESIAN_POINT('',(-1.97893795668429,-1.78906192937259,8.85049129520029));
#400505=CARTESIAN_POINT('',(-1.97893795668429,-1.78906192937259,7.5));
#400506=CARTESIAN_POINT('',(-2.04840012990612,-1.80597870472226,8.78727029226991));
#400507=CARTESIAN_POINT('Ctrl Pts',(-1.97893795668429,-1.7890619293726,
8.85049129520029));
#400508=CARTESIAN_POINT('Ctrl Pts',(-2.00212567109017,-1.79470905121291,
8.82945686509571));
#400509=CARTESIAN_POINT('Ctrl Pts',(-2.02527891415478,-1.80034777792376,
8.80838212259896));
#400510=CARTESIAN_POINT('Ctrl Pts',(-2.04840012990612,-1.80597870472226,
8.78727029226991));
#400511=CARTESIAN_POINT('',(-2.06202449055417,-1.80929677321444,8.75721825406948));
#400512=CARTESIAN_POINT('Origin',(-2.02102401529018,-1.7993117501472,8.75937679713149));
#400513=CARTESIAN_POINT('',(-2.06202449055417,-1.80929677321444,7.51860402984325));
#400514=CARTESIAN_POINT('',(-2.06202449055417,-1.80929677321444,7.5));
#400515=CARTESIAN_POINT('Ctrl Pts',(-2.06202449055417,-1.80929677321444,
7.51860402984325));
#400516=CARTESIAN_POINT('Ctrl Pts',(-2.05132467425402,-1.80669094647109,
7.52834476460825));
#400517=CARTESIAN_POINT('Ctrl Pts',(-2.04061791178752,-1.80408342806264,
7.53807742314407));
#400518=CARTESIAN_POINT('Ctrl Pts',(-2.02990396992789,-1.80147416118915,
7.54780169004674));
#400519=CARTESIAN_POINT('Ctrl Pts',(-2.0129336650614,-1.79734122348038,
7.5632044032688));
#400520=CARTESIAN_POINT('Ctrl Pts',(-1.9959453264452,-1.79320389384317,
7.57858609112103));
#400521=CARTESIAN_POINT('Ctrl Pts',(-1.97893795668429,-1.7890619293726,
7.59394543036555));
#400522=CARTESIAN_POINT('Origin',(-2.0612456201833,-2.05770976783674,7.5));
#400523=CARTESIAN_POINT('',(-1.99893804826277,-1.8787619573583,8.75721825406948));
#400524=CARTESIAN_POINT('',(-1.99432705985483,-1.86551916431873,8.78727029226991));
#400525=CARTESIAN_POINT('Origin',(-1.98262265146148,-1.83190401626567,8.75658640620927));
#400526=CARTESIAN_POINT('',(-1.97081848695445,-1.79800236791134,8.85049129520029));
#400527=CARTESIAN_POINT('Ctrl Pts',(-1.99432705985483,-1.86551916431873,
8.78727029226991));
#400528=CARTESIAN_POINT('Ctrl Pts',(-1.98650198383396,-1.84304548772371,
8.80838212259896));
#400529=CARTESIAN_POINT('Ctrl Pts',(-1.97866606858371,-1.82054068078121,
8.82945686509571));
#400530=CARTESIAN_POINT('Ctrl Pts',(-1.97081848695445,-1.79800236791134,
8.85049129520029));
#400531=CARTESIAN_POINT('',(-1.97081848695445,-1.79800236791134,7.59394543036555));
#400532=CARTESIAN_POINT('',(-1.97081848695445,-1.79800236791134,7.5));
#400533=CARTESIAN_POINT('',(-1.99893804826277,-1.8787619573583,7.51860402984325));
#400534=CARTESIAN_POINT('Ctrl Pts',(-1.97081848695445,-1.79800236791134,
7.59394543036555));
#400535=CARTESIAN_POINT('Ctrl Pts',(-1.97657441098221,-1.81453342457588,
7.57858609112103));
#400536=CARTESIAN_POINT('Ctrl Pts',(-1.98232389416547,-1.83104598308701,
7.56320440326857));
#400537=CARTESIAN_POINT('Ctrl Pts',(-1.98806727405975,-1.84754101290681,
7.54780169004651));
#400538=CARTESIAN_POINT('Ctrl Pts',(-1.9916932689225,-1.85795489715064,
7.53807742314383));
#400539=CARTESIAN_POINT('Ctrl Pts',(-1.99531683401268,-1.86836180306961,
7.52834476460825));
#400540=CARTESIAN_POINT('Ctrl Pts',(-1.99893804826277,-1.8787619573583,
7.51860402984324));
#400541=CARTESIAN_POINT('',(-1.99893804826277,-1.8787619573583,7.5));
#400542=CARTESIAN_POINT('Origin',(-1.97731117195258,-1.79574168958062,7.5));
#400543=CARTESIAN_POINT('Ctrl Pts',(-1.97081848695445,-1.79800236791134,
8.85049129520029));
#400544=CARTESIAN_POINT('Ctrl Pts',(-1.97075480602791,-1.79781947581619,
8.85097269580138));
#400545=CARTESIAN_POINT('Ctrl Pts',(-1.97069987221253,-1.79763612535269,
8.85143669361005));
#400546=CARTESIAN_POINT('Ctrl Pts',(-1.97065199348698,-1.79744362289938,
8.8519052845931));
#400547=CARTESIAN_POINT('Ctrl Pts',(-1.97055834573615,-1.79706710030876,
8.85282181883899));
#400548=CARTESIAN_POINT('Ctrl Pts',(-1.97049428862327,-1.79666520341029,
8.85372622499636));
#400549=CARTESIAN_POINT('Ctrl Pts',(-1.97047404352487,-1.79622919884002,
8.85462257735071));
#400550=CARTESIAN_POINT('Ctrl Pts',(-1.97045723676321,-1.7958672433312,
8.85536669723986));
#400551=CARTESIAN_POINT('Ctrl Pts',(-1.97047058865886,-1.79548170066648,
8.85610498449051));
#400552=CARTESIAN_POINT('Ctrl Pts',(-1.97053023464031,-1.79506781843295,
8.8568133821837));
#400553=CARTESIAN_POINT('Ctrl Pts',(-1.97058436346215,-1.79469221965601,
8.85745625420284));
#400554=CARTESIAN_POINT('Ctrl Pts',(-1.97067670481895,-1.79428848470054,
8.85808743050666));
#400555=CARTESIAN_POINT('Ctrl Pts',(-1.97083515791362,-1.79385033020558,
8.8586680450841));
#400556=CARTESIAN_POINT('Ctrl Pts',(-1.97090826473665,-1.79364817521963,
8.85893592806395));
#400557=CARTESIAN_POINT('Ctrl Pts',(-1.97099568587152,-1.79343866869043,
8.85919241173848));
#400558=CARTESIAN_POINT('Ctrl Pts',(-1.97110175636777,-1.79322125445075,
8.85943017985534));
#400559=CARTESIAN_POINT('Ctrl Pts',(-1.97124498293793,-1.79292768086568,
8.8597512372));
#400560=CARTESIAN_POINT('Ctrl Pts',(-1.97142643405862,-1.79261249780912,
8.86004599534706));
#400561=CARTESIAN_POINT('Ctrl Pts',(-1.97165295583813,-1.79228468846282,
8.86026130871721));
#400562=CARTESIAN_POINT('Ctrl Pts',(-1.97173589184793,-1.79216466821922,
8.86034014101236));
#400563=CARTESIAN_POINT('Ctrl Pts',(-1.97182610522264,-1.79204114558174,
8.86040910639693));
#400564=CARTESIAN_POINT('Ctrl Pts',(-1.97192140979439,-1.79191768424807,
8.86046313645507));
#400565=CARTESIAN_POINT('Ctrl Pts',(-1.97207013178043,-1.79172502387087,
8.8605474499083));
#400566=CARTESIAN_POINT('Ctrl Pts',(-1.97223542757183,-1.79152734357841,
8.86059655985668));
#400567=CARTESIAN_POINT('Ctrl Pts',(-1.9724064715048,-1.79133713328595,
8.86059725258816));
#400568=CARTESIAN_POINT('Ctrl Pts',(-1.97257791061759,-1.79114648353172,
8.86059794692011));
#400569=CARTESIAN_POINT('Ctrl Pts',(-1.97275900125441,-1.7909630004596,
8.86056369958366));
#400570=CARTESIAN_POINT('Ctrl Pts',(-1.97293718832747,-1.79079404793146,
8.86048590497774));
#400571=CARTESIAN_POINT('Ctrl Pts',(-1.97298368984828,-1.79074995635193,
8.86046560290182));
#400572=CARTESIAN_POINT('Ctrl Pts',(-1.97303066090191,-1.79070634650503,
8.86044257503091));
#400573=CARTESIAN_POINT('Ctrl Pts',(-1.97307662770901,-1.79066454191473,
8.86041778462583));
#400574=CARTESIAN_POINT('Ctrl Pts',(-1.97338592728076,-1.79038324889724,
8.860250975962));
#400575=CARTESIAN_POINT('Ctrl Pts',(-1.97369148558685,-1.790146190774,8.8599848982295));
#400576=CARTESIAN_POINT('Ctrl Pts',(-1.97397919074953,-1.78995359252349,
8.85968173251461));
#400577=CARTESIAN_POINT('Ctrl Pts',(-1.97413137029704,-1.78985171908353,
8.85952137522076));
#400578=CARTESIAN_POINT('Ctrl Pts',(-1.97428138202754,-1.78976016227389,
8.85934740853961));
#400579=CARTESIAN_POINT('Ctrl Pts',(-1.97442630057652,-1.78967888631636,
8.8591675900182));
#400580=CARTESIAN_POINT('Ctrl Pts',(-1.97500822387785,-1.78935252110047,
8.85844552518694));
#400581=CARTESIAN_POINT('Ctrl Pts',(-1.97553943149829,-1.78917084386516,
8.85759444184123));
#400582=CARTESIAN_POINT('Ctrl Pts',(-1.97598585478622,-1.78906161702088,
8.85683498915137));
#400583=CARTESIAN_POINT('Ctrl Pts',(-1.97603257179437,-1.78905018672252,
8.85675551444997));
#400584=CARTESIAN_POINT('Ctrl Pts',(-1.97607836118027,-1.78903956978337,
8.85667699793651));
#400585=CARTESIAN_POINT('Ctrl Pts',(-1.97612318378679,-1.78902969655278,
8.85659965593547));
#400586=CARTESIAN_POINT('Ctrl Pts',(-1.9767282016167,-1.78889642718248,
8.85555568965886));
#400587=CARTESIAN_POINT('Ctrl Pts',(-1.97732890796932,-1.78885572360712,
8.85434650606346));
#400588=CARTESIAN_POINT('Ctrl Pts',(-1.97792785225356,-1.78890118409167,
8.85297329937117));
#400589=CARTESIAN_POINT('Ctrl Pts',(-1.97826472191923,-1.78892675284428,
8.85220095427747));
#400590=CARTESIAN_POINT('Ctrl Pts',(-1.97860114795411,-1.78897990317963,
8.85137579139183));
#400591=CARTESIAN_POINT('Ctrl Pts',(-1.97893795668429,-1.7890619293726,
8.85049129520029));
#400592=CARTESIAN_POINT('Origin',(-1.97731117195258,-1.79574168958062,7.59394543036555));
#400593=CARTESIAN_POINT('Ctrl Pts',(-1.97063359974216,-1.79747137046104,
7.59443877723642));
#400594=CARTESIAN_POINT('Ctrl Pts',(-1.96872943934933,-1.79200260763504,
7.58783886950016));
#400595=CARTESIAN_POINT('Ctrl Pts',(-1.97588371901012,-1.78743145197463,
7.58559994247159));
#400596=CARTESIAN_POINT('Ctrl Pts',(-1.98102835546094,-1.82732518628148,
7.56670252222134));
#400597=CARTESIAN_POINT('Ctrl Pts',(-1.97912694712048,-1.82186432737039,
7.56004874999026));
#400598=CARTESIAN_POINT('Ctrl Pts',(-1.98631211473056,-1.81724808174524,
7.55786368756704));
#400599=CARTESIAN_POINT('Ctrl Pts',(-1.99140370001201,-1.8571232530837,
7.5388891333356));
#400600=CARTESIAN_POINT('Ctrl Pts',(-1.98949099150868,-1.85162994002071,
7.53222002137281));
#400601=CARTESIAN_POINT('Ctrl Pts',(-1.99672030494783,-1.84701047339366,
7.53005029815326));
#400602=CARTESIAN_POINT('Ctrl Pts',(-2.00175916390394,-1.88686422248488,
7.51101258149734));
#400603=CARTESIAN_POINT('Ctrl Pts',(-1.99982326989808,-1.88130432048597,
7.5043616886572));
#400604=CARTESIAN_POINT('Ctrl Pts',(-2.00710785342835,-1.87671712915194,
7.50217374673251));
#400605=CARTESIAN_POINT('',(-2.00655355952791,-1.87513194417975,7.50366116523517));
#400606=CARTESIAN_POINT('Ctrl Pts',(-1.99893804826277,-1.8787619573583,
7.51860402984325));
#400607=CARTESIAN_POINT('Ctrl Pts',(-1.99908326148543,-1.879179010815,7.51734760759493));
#400608=CARTESIAN_POINT('Ctrl Pts',(-1.99927067061862,-1.879536314155,7.51608817408573));
#400609=CARTESIAN_POINT('Ctrl Pts',(-1.99951167028735,-1.87982684288426,
7.5148100591312));
#400610=CARTESIAN_POINT('Ctrl Pts',(-1.99972997354617,-1.88009001074963,
7.51365231206384));
#400611=CARTESIAN_POINT('Ctrl Pts',(-1.99999236391793,-1.88029891959378,
7.51247773061043));
#400612=CARTESIAN_POINT('Ctrl Pts',(-2.00031730057137,-1.88042106712353,
7.51129758471022));
#400613=CARTESIAN_POINT('Ctrl Pts',(-2.00072115972243,-1.88057288255323,
7.50983079813402));
#400614=CARTESIAN_POINT('Ctrl Pts',(-2.00121333215552,-1.88057363532481,
7.50839324291155));
#400615=CARTESIAN_POINT('Ctrl Pts',(-2.00179753601526,-1.88034089142908,
7.50715379678855));
#400616=CARTESIAN_POINT('Ctrl Pts',(-2.00206742136502,-1.8802333704556,
7.50658120839351));
#400617=CARTESIAN_POINT('Ctrl Pts',(-2.00239179783196,-1.88005190515018,
7.50598221009429));
#400618=CARTESIAN_POINT('Ctrl Pts',(-2.00275184034603,-1.87978096284191,
7.50545747549611));
#400619=CARTESIAN_POINT('Ctrl Pts',(-2.00294397017589,-1.87963637963978,
7.50517746087247));
#400620=CARTESIAN_POINT('Ctrl Pts',(-2.0031484614756,-1.87946491079292,
7.50491486231392));
#400621=CARTESIAN_POINT('Ctrl Pts',(-2.00335882723001,-1.87926981894231,
7.50468370960992));
#400622=CARTESIAN_POINT('Ctrl Pts',(-2.00367339038896,-1.87897809508742,
7.50433806340446));
#400623=CARTESIAN_POINT('Ctrl Pts',(-2.00401014266398,-1.87862439508463,
7.50405484070983));
#400624=CARTESIAN_POINT('Ctrl Pts',(-2.00434588556985,-1.87823204598658,
7.5038576603613));
#400625=CARTESIAN_POINT('Ctrl Pts',(-2.004381788055,-1.87819009034904,7.50383657498791));
#400626=CARTESIAN_POINT('Ctrl Pts',(-2.00441767407893,-1.87814772069229,
7.50381643264937));
#400627=CARTESIAN_POINT('Ctrl Pts',(-2.00445351201731,-1.87810498588882,
7.50379723213559));
#400628=CARTESIAN_POINT('Ctrl Pts',(-2.00469274197945,-1.87781971709612,
7.50366906242519));
#400629=CARTESIAN_POINT('Ctrl Pts',(-2.0049344820996,-1.87751151007147,
7.50358235568538));
#400630=CARTESIAN_POINT('Ctrl Pts',(-2.00516034878498,-1.87720883540575,
7.5035341175365));
#400631=CARTESIAN_POINT('Ctrl Pts',(-2.00549901031654,-1.87675500900065,
7.50346178989176));
#400632=CARTESIAN_POINT('Ctrl Pts',(-2.00584403688456,-1.87625239556466,
7.50346967198527));
#400633=CARTESIAN_POINT('Ctrl Pts',(-2.0061675638165,-1.87574856280017,
7.50354272648692));
#400634=CARTESIAN_POINT('Ctrl Pts',(-2.00630063714021,-1.87554132595542,
7.50357277531559));
#400635=CARTESIAN_POINT('Ctrl Pts',(-2.0064300155592,-1.87533423478528,
7.50361331098761));
#400636=CARTESIAN_POINT('Ctrl Pts',(-2.00655355952895,-1.87513194418072,
7.50366116523659));
#400637=CARTESIAN_POINT('',(-1.97947865054248,-1.79771013628735,7.57603338622103));
#400638=CARTESIAN_POINT('Origin',(-1.98602235984329,-1.80364910574218,7.58486873427627));
#400639=CARTESIAN_POINT('Ctrl Pts',(-2.0065535595417,-1.87513194423542,
7.50366116529968));
#400640=CARTESIAN_POINT('Ctrl Pts',(-1.99754410575752,-1.8493665111649,
7.52783573079709));
#400641=CARTESIAN_POINT('Ctrl Pts',(-1.98851957912756,-1.82356045444553,
7.55196141284068));
#400642=CARTESIAN_POINT('Ctrl Pts',(-1.97947865060515,-1.79771013753784,
7.57603338728831));
#400643=CARTESIAN_POINT('Ctrl Pts',(-1.97132269366337,-1.79891577423654,
7.59639677331371));
#400644=CARTESIAN_POINT('Ctrl Pts',(-1.96265932869603,-1.78282173735349,
7.59959882295466));
#400645=CARTESIAN_POINT('Ctrl Pts',(-1.97972755753913,-1.78940841912533,
7.59642833564546));
#400646=CARTESIAN_POINT('Ctrl Pts',(-1.9689457891844,-1.79582297143299,
7.58707626057422));
#400647=CARTESIAN_POINT('Ctrl Pts',(-1.96986457548299,-1.78910969184893,
7.58809943920599));
#400648=CARTESIAN_POINT('Ctrl Pts',(-1.97641865331219,-1.78744882924111,
7.58710240504253));
#400649=CARTESIAN_POINT('Ctrl Pts',(-1.97498067889014,-1.79653412437102,
7.58015376756929));
#400650=CARTESIAN_POINT('Ctrl Pts',(-1.97499660145064,-1.79368298111467,
7.5820588065976));
#400651=CARTESIAN_POINT('Ctrl Pts',(-1.97779293880242,-1.79335499871752,
7.58020924244127));
#400652=CARTESIAN_POINT('Ctrl Pts',(-1.97947864992971,-1.79771013573113,
7.57603338509286));
#400653=CARTESIAN_POINT('Ctrl Pts',(-1.97947864992971,-1.79771013573113,
7.57603338509286));
#400654=CARTESIAN_POINT('Ctrl Pts',(-1.97947864992971,-1.79771013573113,
7.57603338509286));
#400655=CARTESIAN_POINT('Origin',(-1.98601852345799,-1.80365333002949,7.58486873427621));
#400656=CARTESIAN_POINT('Ctrl Pts',(-2.07038655374306,-1.81133326498924,
7.51098857897448));
#400657=CARTESIAN_POINT('Ctrl Pts',(-2.06466642693682,-1.80994018879159,
7.50433767179956));
#400658=CARTESIAN_POINT('Ctrl Pts',(-2.06079991957958,-1.81763162376426,
7.50214974420965));
#400659=CARTESIAN_POINT('Ctrl Pts',(-2.03977985028097,-1.80387932707387,
7.53887321589165));
#400660=CARTESIAN_POINT('Ctrl Pts',(-2.03412826074525,-1.80250294240135,
7.53220407452058));
#400661=CARTESIAN_POINT('Ctrl Pts',(-2.03022429857704,-1.81014244495788,
7.5300343807091));
#400662=CARTESIAN_POINT('Ctrl Pts',(-2.00911437065794,-1.79641107484808,
7.56669465659233));
#400663=CARTESIAN_POINT('Ctrl Pts',(-2.00349618096568,-1.79504282435305,
7.560040858333));
#400664=CARTESIAN_POINT('Ctrl Pts',(-1.99959118425106,-1.80263806304482,
7.5578558219379));
#400665=CARTESIAN_POINT('Ctrl Pts',(-1.97839150175079,-1.78892884607099,
7.59443891967696));
#400666=CARTESIAN_POINT('Ctrl Pts',(-1.97276516638296,-1.78755861178311,
7.58783901202978));
#400667=CARTESIAN_POINT('Ctrl Pts',(-1.96890210910569,-1.79511876829345,
7.58560008491213));
#400668=CARTESIAN_POINT('',(-2.05914251569203,-1.81722565891167,7.50366116523517));
#400669=CARTESIAN_POINT('Ctrl Pts',(-2.05914251569231,-1.81722565891192,
7.50366116523554));
#400670=CARTESIAN_POINT('Ctrl Pts',(-2.05974816076237,-1.81677032215097,
7.50350835821027));
#400671=CARTESIAN_POINT('Ctrl Pts',(-2.06029008167033,-1.81633205312325,
7.50345484955999));
#400672=CARTESIAN_POINT('Ctrl Pts',(-2.06078476777651,-1.81589828865175,
7.50349758195598));
#400673=CARTESIAN_POINT('Ctrl Pts',(-2.06103857843586,-1.81567573530907,
7.50351950684424));
#400674=CARTESIAN_POINT('Ctrl Pts',(-2.06130505670668,-1.81543252934383,
7.50357029184312));
#400675=CARTESIAN_POINT('Ctrl Pts',(-2.06155557213264,-1.81519094525445,
7.50365515313923));
#400676=CARTESIAN_POINT('Ctrl Pts',(-2.06194096630147,-1.81481929109791,
7.50378570417639));
#400677=CARTESIAN_POINT('Ctrl Pts',(-2.06230013518949,-1.81444081575043,
7.50400001621911));
#400678=CARTESIAN_POINT('Ctrl Pts',(-2.06260409394753,-1.81408276381045,
7.50428903009634));
#400679=CARTESIAN_POINT('Ctrl Pts',(-2.06263783103116,-1.8140430227998,
7.50432110841318));
#400680=CARTESIAN_POINT('Ctrl Pts',(-2.06267091723574,-1.81400352550134,
7.50435406373354));
#400681=CARTESIAN_POINT('Ctrl Pts',(-2.06270333445462,-1.81396430305073,
7.50438785222351));
#400682=CARTESIAN_POINT('Ctrl Pts',(-2.06290125715758,-1.81372483113704,
7.50459414719561));
#400683=CARTESIAN_POINT('Ctrl Pts',(-2.06307699573866,-1.81349146349241,
7.50483629897752));
#400684=CARTESIAN_POINT('Ctrl Pts',(-2.06322486898636,-1.81327393203516,
7.5050991045531));
#400685=CARTESIAN_POINT('Ctrl Pts',(-2.06355109222325,-1.8127940357915,
7.50567888004914));
#400686=CARTESIAN_POINT('Ctrl Pts',(-2.06375498358801,-1.81237259419739,
7.50637912803144));
#400687=CARTESIAN_POINT('Ctrl Pts',(-2.06386691707729,-1.81201533775757,
7.50710440483569));
#400688=CARTESIAN_POINT('Ctrl Pts',(-2.06389436539105,-1.81192773138599,
7.50728225710685));
#400689=CARTESIAN_POINT('Ctrl Pts',(-2.06391696970791,-1.81184228430579,
7.50746498566954));
#400690=CARTESIAN_POINT('Ctrl Pts',(-2.06393460510911,-1.81176109766968,
7.50764697238949));
#400691=CARTESIAN_POINT('Ctrl Pts',(-2.0640294081726,-1.81132466065711,
7.50862528291182));
#400692=CARTESIAN_POINT('Ctrl Pts',(-2.06399326812427,-1.81097260360617,
7.50965856837421));
#400693=CARTESIAN_POINT('Ctrl Pts',(-2.06388789127109,-1.8106806834246,
7.51067959873202));
#400694=CARTESIAN_POINT('Ctrl Pts',(-2.06382990225587,-1.81052003938047,
7.51124147302578));
#400695=CARTESIAN_POINT('Ctrl Pts',(-2.0637505234035,-1.81037771496521,
7.51180065547253));
#400696=CARTESIAN_POINT('Ctrl Pts',(-2.0636575186871,-1.81025068491237,
7.51235175716501));
#400697=CARTESIAN_POINT('Ctrl Pts',(-2.06333615034324,-1.80981174547706,
7.51425603304536));
#400698=CARTESIAN_POINT('Ctrl Pts',(-2.06280888182929,-1.80950666459949,
7.5162690050518));
#400699=CARTESIAN_POINT('Ctrl Pts',(-2.06213518302363,-1.80932514660288,
7.51827788969243));
#400700=CARTESIAN_POINT('Ctrl Pts',(-2.06209872117116,-1.80931532250589,
7.51838661432545));
#400701=CARTESIAN_POINT('Ctrl Pts',(-2.06206182146845,-1.80930586476256,
7.51849533314856));
#400702=CARTESIAN_POINT('Ctrl Pts',(-2.06202449055417,-1.80929677321444,
7.51860402984325));
#400703=CARTESIAN_POINT('Ctrl Pts',(-1.97947865179425,-1.79771013623028,
7.57603338728985));
#400704=CARTESIAN_POINT('Ctrl Pts',(-2.00607765462698,-1.80422706199452,
7.55196141284922));
#400705=CARTESIAN_POINT('Ctrl Pts',(-2.03263102684926,-1.81073191165887,
7.52783573083104));
#400706=CARTESIAN_POINT('Ctrl Pts',(-2.05914251575056,-1.81722565892042,
7.50366116530176));
#400707=CARTESIAN_POINT('Origin',(-6.84001376365782E-16,-6.21191952330714E-16,
7.49482233047033));
#400708=CARTESIAN_POINT('Origin',(-2.00009565450361,-1.86909700733691,7.49482233047033));
#400709=CARTESIAN_POINT('Origin',(0.,0.,7.50366116523517));
#400710=CARTESIAN_POINT('Origin',(-2.05251535802923,-1.81137708803389,7.49482233047033));
#400711=CARTESIAN_POINT('Ctrl Pts',(-1.99893770041465,-1.87876095847199,
7.51860402984325));
#400712=CARTESIAN_POINT('Ctrl Pts',(-2.00144033216759,-1.88594657746685,
7.51860402984325));
#400713=CARTESIAN_POINT('Ctrl Pts',(-1.99620683387468,-1.8914698719229,
7.51860402984325));
#400714=CARTESIAN_POINT('Ctrl Pts',(-1.99986694346334,-1.88142902825996,
7.51041458714366));
#400715=CARTESIAN_POINT('Ctrl Pts',(-2.00020044929248,-1.88725510237742,
7.51004642900442));
#400716=CARTESIAN_POINT('Ctrl Pts',(-1.99620539053799,-1.89147139518193,
7.5072913648301));
#400717=CARTESIAN_POINT('Ctrl Pts',(-2.00268144724221,-1.88147704573545,
7.50215815450137));
#400718=CARTESIAN_POINT('Ctrl Pts',(-2.0027250764607,-1.88459091165625,
7.49877163671529));
#400719=CARTESIAN_POINT('Ctrl Pts',(-2.00036937312889,-1.88711174195734,
7.49481588533171));
#400720=CARTESIAN_POINT('Ctrl Pts',(-2.00655315730405,-1.87513156829938,
7.50366171572174));
#400721=CARTESIAN_POINT('Ctrl Pts',(-2.00922851137376,-1.87763169686784,
7.50000045605858));
#400722=CARTESIAN_POINT('Ctrl Pts',(-2.00922851137367,-1.87763169686793,
7.49482233047317));
#400723=CARTESIAN_POINT('Origin',(-1.98713316644798,-1.88287228159597,7.51860402984325));
#400724=CARTESIAN_POINT('Origin',(-1.98713316644798,-1.88287228159597,9.));
#400725=CARTESIAN_POINT('Origin',(-1.98713316644798,-1.88287228159597,8.75721825406948));
#400726=CARTESIAN_POINT('Ctrl Pts',(-1.99344657357429,-1.86299049303862,
8.78942910404913));
#400727=CARTESIAN_POINT('Ctrl Pts',(-1.99529801914105,-1.86824640190532,
8.79672699501692));
#400728=CARTESIAN_POINT('Ctrl Pts',(-1.98756686989969,-1.87270765928303,
8.79893251111267));
#400729=CARTESIAN_POINT('Ctrl Pts',(-1.99706180063075,-1.8733734382889,
8.78111911759577));
#400730=CARTESIAN_POINT('Ctrl Pts',(-1.99924968983697,-1.87960685235721,
8.78644465894809));
#400731=CARTESIAN_POINT('Ctrl Pts',(-1.99326065865081,-1.88507009473026,
8.78817647674131));
#400732=CARTESIAN_POINT('Ctrl Pts',(-1.9993148963336,-1.87984433743598,
8.76780923932034));
#400733=CARTESIAN_POINT('Ctrl Pts',(-2.001892798948,-1.88720430719687,8.76988516158377));
#400734=CARTESIAN_POINT('Ctrl Pts',(-1.99680675333073,-1.892796133408,8.77093053738833));
#400735=CARTESIAN_POINT('Ctrl Pts',(-1.99887557350569,-1.87858260066336,
8.75371302330491));
#400736=CARTESIAN_POINT('Ctrl Pts',(-2.00139092575808,-1.88576168169189,
8.75300828287558));
#400737=CARTESIAN_POINT('Ctrl Pts',(-1.99611470500354,-1.89128943294206,
8.75267964240738));
#400738=CARTESIAN_POINT('Origin',(-1.98252217804004,-1.8696294885564,8.78727029226991));
#400739=CARTESIAN_POINT('Ctrl Pts',(-1.97081848695445,-1.79800236791134,
8.85049129520029));
#400740=CARTESIAN_POINT('Ctrl Pts',(-1.97273870409017,-1.80351724582248,
8.85711686593484));
#400741=CARTESIAN_POINT('Ctrl Pts',(-1.96551867526937,-1.80809675954565,
8.85933012996512));
#400742=CARTESIAN_POINT('Ctrl Pts',(-1.97866607911545,-1.82054071102847,
8.82945683644723));
#400743=CARTESIAN_POINT('Ctrl Pts',(-1.98060223521441,-1.82610136576062,
8.83607469902389));
#400744=CARTESIAN_POINT('Ctrl Pts',(-1.97334092145605,-1.83066265560015,
8.83829567148519));
#400745=CARTESIAN_POINT('Ctrl Pts',(-1.98650197380751,-1.84304545892768,
8.80838214965003));
#400746=CARTESIAN_POINT('Ctrl Pts',(-1.98844577088239,-1.84862805859967,
8.81501364461995));
#400747=CARTESIAN_POINT('Ctrl Pts',(-1.98115193336382,-1.85319410139924,
8.81722098428721));
#400748=CARTESIAN_POINT('Ctrl Pts',(-1.99432705985483,-1.86551916431873,
8.78727029226991));
#400749=CARTESIAN_POINT('Ctrl Pts',(-1.99627117980079,-1.87110269127883,
8.79393457792714));
#400750=CARTESIAN_POINT('Ctrl Pts',(-1.98895258219515,-1.87569371995058,
8.79610912703474));
#400751=CARTESIAN_POINT('Origin',(-1.95901360513965,-1.80211269214901,8.85049129520029));
#400752=CARTESIAN_POINT('Ctrl Pts',(-1.97893795668429,-1.7890619293726,
8.85049129520029));
#400753=CARTESIAN_POINT('Ctrl Pts',(-1.98461173602728,-1.79044371813728,
8.85711686593484));
#400754=CARTESIAN_POINT('Ctrl Pts',(-1.98847679932027,-1.78281731348928,
8.85933012996512));
#400755=CARTESIAN_POINT('Ctrl Pts',(-1.97391844600142,-1.78783948079881,
8.86332496987231));
#400756=CARTESIAN_POINT('Ctrl Pts',(-1.97722818329212,-1.78461496014556,
8.86648636486737));
#400757=CARTESIAN_POINT('Ctrl Pts',(-1.97443045953234,-1.77941410986347,
8.87206031107458));
#400758=CARTESIAN_POINT('Ctrl Pts',(-1.96910815477049,-1.79309028114442,
8.86341338519877));
#400759=CARTESIAN_POINT('Ctrl Pts',(-1.96618509120301,-1.79668599665246,
8.86654584966059));
#400760=CARTESIAN_POINT('Ctrl Pts',(-1.96074356779992,-1.7943378110037,
8.87215952290714));
#400761=CARTESIAN_POINT('Ctrl Pts',(-1.97081848695445,-1.79800236791134,
8.85049129520029));
#400762=CARTESIAN_POINT('Ctrl Pts',(-1.97273870409017,-1.80351724582248,
8.85711686593484));
#400763=CARTESIAN_POINT('Ctrl Pts',(-1.96551867526937,-1.80809675954565,
8.85933012996512));
#400764=CARTESIAN_POINT('Origin',(-1.98189574710558,-1.77691691081256,8.85049129520029));
#400765=CARTESIAN_POINT('Ctrl Pts',(-2.04840012990612,-1.80597870472226,
8.78727029226991));
#400766=CARTESIAN_POINT('Ctrl Pts',(-2.05414453629873,-1.80737769395559,
8.79393457792714));
#400767=CARTESIAN_POINT('Ctrl Pts',(-2.05801159645804,-1.79965207029775,
8.79610912703474));
#400768=CARTESIAN_POINT('Ctrl Pts',(-2.02527888452904,-1.80034777070873,
8.80838214965003));
#400769=CARTESIAN_POINT('Ctrl Pts',(-2.03102233691532,-1.80174652760395,
8.81501364461987));
#400770=CARTESIAN_POINT('Ctrl Pts',(-2.0348669041979,-1.79404794883867,
8.81722098428721));
#400771=CARTESIAN_POINT('Ctrl Pts',(-2.00212570220896,-1.79470905879156,
8.82945683644722));
#400772=CARTESIAN_POINT('Ctrl Pts',(-2.00784657735091,-1.79610231723843,
8.83607469902389));
#400773=CARTESIAN_POINT('Ctrl Pts',(-2.01168953666615,-1.78843656833836,
8.8382956714852));
#400774=CARTESIAN_POINT('Ctrl Pts',(-1.97893795668429,-1.7890619293726,
8.85049129520029));
#400775=CARTESIAN_POINT('Ctrl Pts',(-1.98461173602728,-1.79044371813728,
8.85711686593484));
#400776=CARTESIAN_POINT('Ctrl Pts',(-1.98847679932027,-1.78281731348928,
8.85933012996512));
#400777=CARTESIAN_POINT('Origin',(-2.05135792032741,-1.79383368616222,8.78727029226991));
#400778=CARTESIAN_POINT('Ctrl Pts',(-2.06184459209043,-1.80925294186592,
8.75374538247848));
#400779=CARTESIAN_POINT('Ctrl Pts',(-2.06922464863629,-1.81106378249048,
8.75304829418601));
#400780=CARTESIAN_POINT('Ctrl Pts',(-2.07421919160669,-1.80529098561844,
8.75272238421917));
#400781=CARTESIAN_POINT('Ctrl Pts',(-2.06312709009239,-1.80956528108705,
8.76769408445021));
#400782=CARTESIAN_POINT('Ctrl Pts',(-2.07069302605931,-1.81142102027037,
8.76974318093969));
#400783=CARTESIAN_POINT('Ctrl Pts',(-2.07576782353208,-1.80582952781393,
8.7707786988043));
#400784=CARTESIAN_POINT('Ctrl Pts',(-2.05655373592175,-1.80796440818184,
8.78108014887988));
#400785=CARTESIAN_POINT('Ctrl Pts',(-2.06296468902881,-1.80954077031012,
8.78639403366325));
#400786=CARTESIAN_POINT('Ctrl Pts',(-2.06783626201611,-1.80307626318597,
8.78812224174741));
#400787=CARTESIAN_POINT('Ctrl Pts',(-2.0457814595272,-1.80534093085235,
8.78944554828685));
#400788=CARTESIAN_POINT('Ctrl Pts',(-2.05118303652298,-1.806674866224,8.79673892988686));
#400789=CARTESIAN_POINT('Ctrl Pts',(-2.05487972817392,-1.79856080280581,
8.79894799272499));
#400790=CARTESIAN_POINT('Origin',(-2.06498228097546,-1.7971517546544,8.75721825406948));
#400791=CARTESIAN_POINT('Origin',(-2.06498228097546,-1.7971517546544,9.));
#400792=CARTESIAN_POINT('Origin',(-2.06498228097546,-1.7971517546544,7.51860402984325));
#400793=CARTESIAN_POINT('Ctrl Pts',(-2.05914192586944,-1.81722513838389,
7.50366195182966));
#400794=CARTESIAN_POINT('Ctrl Pts',(-2.06188757427604,-1.81964821628965,
7.50000065167735));
#400795=CARTESIAN_POINT('Ctrl Pts',(-2.06188757427611,-1.81964821628956,
7.49482233047108));
#400796=CARTESIAN_POINT('Ctrl Pts',(-2.06509107296448,-1.81275731470247,
7.50215800491337));
#400797=CARTESIAN_POINT('Ctrl Pts',(-2.06819568917779,-1.81250030236346,
7.49877273257265));
#400798=CARTESIAN_POINT('Ctrl Pts',(-2.07047994339333,-1.80991199422324,
7.49481816995649));
#400799=CARTESIAN_POINT('Ctrl Pts',(-2.06476295199598,-1.8099640454759,
7.51043025814041));
#400800=CARTESIAN_POINT('Ctrl Pts',(-2.07059755848594,-1.80974016136719,
7.51006209594514));
#400801=CARTESIAN_POINT('Ctrl Pts',(-2.07441308596515,-1.80535601718414,
7.50731281821698));
#400802=CARTESIAN_POINT('Ctrl Pts',(-2.06202302209009,-1.80929641549154,
7.51860402984325));
#400803=CARTESIAN_POINT('Ctrl Pts',(-2.06941598411249,-1.81109783990738,
7.51860402984325));
#400804=CARTESIAN_POINT('Ctrl Pts',(-2.07441142381097,-1.80535792705008,
7.51860402984325));
#400805=CARTESIAN_POINT('Origin',(0.,0.,7.5));
#400806=CARTESIAN_POINT('Origin',(-1.86024642503783,-1.91217709997535,7.5));
#400807=CARTESIAN_POINT('',(-1.86024642503783,-1.91217709997535,7.59394543036555));
#400808=CARTESIAN_POINT('',(-1.86024642503783,-1.91217709997535,8.85049129520029));
#400809=CARTESIAN_POINT('',(-1.86024642503783,-1.91217709997535,7.5));
#400810=CARTESIAN_POINT('',(-1.92848201925696,-1.9335095747144,8.78727029226991));
#400811=CARTESIAN_POINT('Ctrl Pts',(-1.86024642503783,-1.91217709997535,
8.85049129520029));
#400812=CARTESIAN_POINT('Ctrl Pts',(-1.88302468545903,-1.91929826116103,
8.82945686509571));
#400813=CARTESIAN_POINT('Ctrl Pts',(-1.9057690832418,-1.92640883587952,
8.80838212259896));
#400814=CARTESIAN_POINT('Ctrl Pts',(-1.92848201925696,-1.9335095747144,
8.78727029226991));
#400815=CARTESIAN_POINT('',(-1.94186579781665,-1.93769374166282,8.75721825406948));
#400816=CARTESIAN_POINT('Origin',(-1.90158930505031,-1.92510232442672,8.7593767971313));
#400817=CARTESIAN_POINT('',(-1.94186579781665,-1.93769374166282,7.51860402984325));
#400818=CARTESIAN_POINT('',(-1.94186579781665,-1.93769374166282,7.5));
#400819=CARTESIAN_POINT('Ctrl Pts',(-1.94186579781665,-1.93769374166282,
7.51860402984325));
#400820=CARTESIAN_POINT('Ctrl Pts',(-1.93135492132931,-1.93440772928589,
7.52834476460825));
#400821=CARTESIAN_POINT('Ctrl Pts',(-1.92083722133263,-1.93111958367715,
7.53807742314407));
#400822=CARTESIAN_POINT('Ctrl Pts',(-1.9103124687182,-1.92782923321049,
7.54780169004674));
#400823=CARTESIAN_POINT('Ctrl Pts',(-1.89364182939128,-1.92261749589956,
7.5632044032688));
#400824=CARTESIAN_POINT('Ctrl Pts',(-1.87695347475875,-1.91740022025758,
7.57858609112103));
#400825=CARTESIAN_POINT('Ctrl Pts',(-1.86024642503783,-1.91217709997535,
7.59394543036555));
#400826=CARTESIAN_POINT('Origin',(-1.92517265250698,-2.18554644274946,7.5));
#400827=CARTESIAN_POINT('',(-1.87445832375784,-2.00297423990033,8.75721825406948));
#400828=CARTESIAN_POINT('',(-1.87070527778332,-1.98946322855772,8.78727029226991));
#400829=CARTESIAN_POINT('Origin',(-1.86117864728312,-1.95516724241237,8.75658640620986));
#400830=CARTESIAN_POINT('',(-1.85157082176546,-1.92057895321254,8.85049129520029));
#400831=CARTESIAN_POINT('Ctrl Pts',(-1.87070527778332,-1.98946322855772,
8.78727029226991));
#400832=CARTESIAN_POINT('Ctrl Pts',(-1.86433617262359,-1.96653437219954,
8.80838212259896));
#400833=CARTESIAN_POINT('Ctrl Pts',(-1.85795824503304,-1.9435737549827,
8.82945686509571));
#400834=CARTESIAN_POINT('Ctrl Pts',(-1.85157082176546,-1.92057895321254,
8.85049129520029));
#400835=CARTESIAN_POINT('',(-1.85157082176546,-1.92057895321254,7.59394543036555));
#400836=CARTESIAN_POINT('',(-1.85157082176546,-1.92057895321254,7.5));
#400837=CARTESIAN_POINT('',(-1.87445832375784,-2.00297423990033,7.51860402984325));
#400838=CARTESIAN_POINT('Ctrl Pts',(-1.85157082176546,-1.92057895321254,
7.59394543036555));
#400839=CARTESIAN_POINT('Ctrl Pts',(-1.85625577119297,-1.93744482836686,
7.57858609112103));
#400840=CARTESIAN_POINT('Ctrl Pts',(-1.86093547819015,-1.9542918307079,
7.56320440326857));
#400841=CARTESIAN_POINT('Ctrl Pts',(-1.86561021750532,-1.97112094933311,
7.54780169004651));
#400842=CARTESIAN_POINT('Ctrl Pts',(-1.86856154251838,-1.98174575542338,
7.53807742314383));
#400843=CARTESIAN_POINT('Ctrl Pts',(-1.87151088985391,-1.99236344185045,
7.52834476460825));
#400844=CARTESIAN_POINT('Ctrl Pts',(-1.87445832375784,-2.00297423990033,
7.51860402984325));
#400845=CARTESIAN_POINT('',(-1.87445832375784,-2.00297423990033,7.5));
#400846=CARTESIAN_POINT('Origin',(-1.85819500900388,-1.918738907444,7.5));
#400847=CARTESIAN_POINT('Ctrl Pts',(-1.85157082176546,-1.92057895321254,
8.85049129520029));
#400848=CARTESIAN_POINT('Ctrl Pts',(-1.85151898961498,-1.92039235683784,
8.85097269580138));
#400849=CARTESIAN_POINT('Ctrl Pts',(-1.85147591597155,-1.9202058634659,
8.85143669361005));
#400850=CARTESIAN_POINT('Ctrl Pts',(-1.8514404692925,-1.92001068892905,
8.8519052845931));
#400851=CARTESIAN_POINT('Ctrl Pts',(-1.85137113783624,-1.91962893991248,
8.85282181883899));
#400852=CARTESIAN_POINT('Ctrl Pts',(-1.85133296195825,-1.91922376460098,
8.85372622499635));
#400853=CARTESIAN_POINT('Ctrl Pts',(-1.85134069336431,-1.91878735874095,
8.85462257735071));
#400854=CARTESIAN_POINT('Ctrl Pts',(-1.85134711170302,-1.91842507009562,
8.85536669723986));
#400855=CARTESIAN_POINT('Ctrl Pts',(-1.8513851379691,-1.91804117502855,
8.85610498449051));
#400856=CARTESIAN_POINT('Ctrl Pts',(-1.85147117892724,-1.91763196469161,
8.85681338218371));
#400857=CARTESIAN_POINT('Ctrl Pts',(-1.85154926123187,-1.91726060566816,
8.85745625420284));
#400858=CARTESIAN_POINT('Ctrl Pts',(-1.85166728025086,-1.91686361656051,
8.85808743050666));
#400859=CARTESIAN_POINT('Ctrl Pts',(-1.85185348044153,-1.91643651442558,
8.8586680450841));
#400860=CARTESIAN_POINT('Ctrl Pts',(-1.85193938917318,-1.91623945875896,
8.85893592806395));
#400861=CARTESIAN_POINT('Ctrl Pts',(-1.85204005382136,-1.91603598377474,
8.85919241173848));
#400862=CARTESIAN_POINT('Ctrl Pts',(-1.85215983616256,-1.91582581219596,
8.85943017985534));
#400863=CARTESIAN_POINT('Ctrl Pts',(-1.85232157778255,-1.91554201834716,
8.8597512372));
#400864=CARTESIAN_POINT('Ctrl Pts',(-1.85252284994022,-1.91523910848121,
8.86004599534706));
#400865=CARTESIAN_POINT('Ctrl Pts',(-1.85276990912336,-1.91492648595462,
8.86026130871721));
#400866=CARTESIAN_POINT('Ctrl Pts',(-1.85286036445565,-1.91481202603387,
8.86034014101235));
#400867=CARTESIAN_POINT('Ctrl Pts',(-1.85295830659987,-1.91469453717766,
8.86040910639692));
#400868=CARTESIAN_POINT('Ctrl Pts',(-1.85306132555295,-1.91457743569342,
8.86046313645506));
#400869=CARTESIAN_POINT('Ctrl Pts',(-1.85322208576647,-1.91439469980799,
8.86054744990829));
#400870=CARTESIAN_POINT('Ctrl Pts',(-1.85339970735976,-1.91420801620861,
8.86059655985668));
#400871=CARTESIAN_POINT('Ctrl Pts',(-1.85358258667991,-1.914029155546,8.86059725258816));
#400872=CARTESIAN_POINT('Ctrl Pts',(-1.85376588852435,-1.91384988164381,
8.86059794692011));
#400873=CARTESIAN_POINT('Ctrl Pts',(-1.85395836289182,-1.91367837807428,
8.86056369958366));
#400874=CARTESIAN_POINT('Ctrl Pts',(-1.85414700868609,-1.91352118916219,
8.86048590497774));
#400875=CARTESIAN_POINT('Ctrl Pts',(-1.85419623962173,-1.91348016753622,
8.86046560290182));
#400876=CARTESIAN_POINT('Ctrl Pts',(-1.85424590826078,-1.91343965673616,
8.86044257503091));
#400877=CARTESIAN_POINT('Ctrl Pts',(-1.85429445905344,-1.91340088314132,
8.86041778462583));
#400878=CARTESIAN_POINT('Ctrl Pts',(-1.85462114564156,-1.9131399849621,
8.860250975962));
#400879=CARTESIAN_POINT('Ctrl Pts',(-1.85494126451144,-1.91292299108809,
8.8599848982295));
#400880=CARTESIAN_POINT('Ctrl Pts',(-1.85524071836528,-1.9127492218844,
8.85968173251462));
#400881=CARTESIAN_POINT('Ctrl Pts',(-1.8553991122973,-1.91265730793144,
8.85952137522077));
#400882=CARTESIAN_POINT('Ctrl Pts',(-1.85555468187754,-1.91257555051965,
8.85934740853961));
#400883=CARTESIAN_POINT('Ctrl Pts',(-1.8557045100443,-1.9125037265156,8.8591675900182));
#400884=CARTESIAN_POINT('Ctrl Pts',(-1.85630614801297,-1.91221531580599,
8.85844552518695));
#400885=CARTESIAN_POINT('Ctrl Pts',(-1.85684790431081,-1.91206804643514,
8.85759444184124));
#400886=CARTESIAN_POINT('Ctrl Pts',(-1.85730040856215,-1.91198764644738,
8.85683498915138));
#400887=CARTESIAN_POINT('Ctrl Pts',(-1.85734776192694,-1.91197923280278,
8.85675551444998));
#400888=CARTESIAN_POINT('Ctrl Pts',(-1.85739413746327,-1.91197157141331,
8.85667699793651));
#400889=CARTESIAN_POINT('Ctrl Pts',(-1.85743950055698,-1.91196459026259,
8.85659965593547));
#400890=CARTESIAN_POINT('Ctrl Pts',(-1.85805181391075,-1.91187035833396,
8.85555568965886));
#400891=CARTESIAN_POINT('Ctrl Pts',(-1.85865389393477,-1.91186822577661,
8.85434650606346));
#400892=CARTESIAN_POINT('Ctrl Pts',(-1.85924869496049,-1.91195196734977,
8.85297329937117));
#400893=CARTESIAN_POINT('Ctrl Pts',(-1.85958323429571,-1.91199906688222,
8.85220095427747));
#400894=CARTESIAN_POINT('Ctrl Pts',(-1.85991556375354,-1.91207366290457,
8.85137579139184));
#400895=CARTESIAN_POINT('Ctrl Pts',(-1.86024642503783,-1.91217709997535,
8.85049129520029));
#400896=CARTESIAN_POINT('Origin',(-1.85819500900388,-1.918738907444,7.59394543036555));
#400897=CARTESIAN_POINT('Ctrl Pts',(-1.85142033554723,-1.9200372009891,
7.59443877723642));
#400898=CARTESIAN_POINT('Ctrl Pts',(-1.84987047229342,-1.9144576743476,
7.58783886950016));
#400899=CARTESIAN_POINT('Ctrl Pts',(-1.85730292766809,-1.91035428688841,
7.58559994247159));
#400900=CARTESIAN_POINT('Ctrl Pts',(-1.85988099357869,-1.95049567322872,
7.56670252222139));
#400901=CARTESIAN_POINT('Ctrl Pts',(-1.85833337031734,-1.94492421058725,
7.5600487499903));
#400902=CARTESIAN_POINT('Ctrl Pts',(-1.86579953910258,-1.94077780480321,
7.55786368756704));
#400903=CARTESIAN_POINT('Ctrl Pts',(-1.86832585217658,-1.98089726731457,
7.53888913333561));
#400904=CARTESIAN_POINT('Ctrl Pts',(-1.86676903131439,-1.97529269319784,
7.53222002137278));
#400905=CARTESIAN_POINT('Ctrl Pts',(-1.87427946159672,-1.97114590146277,
7.53005029815327));
#400906=CARTESIAN_POINT('Ctrl Pts',(-1.87675452920536,-2.01124060755397,
7.51101258149734));
#400907=CARTESIAN_POINT('Ctrl Pts',(-1.87517883684549,-2.0055680958152,
7.5043616886572));
#400908=CARTESIAN_POINT('Ctrl Pts',(-1.88274235577551,-2.00145705422698,
7.50217374673251));
#400909=CARTESIAN_POINT('',(-1.88229076388121,-1.9998396124552,7.50366116523517));
#400910=CARTESIAN_POINT('Ctrl Pts',(-1.87445832375784,-2.00297423990033,
7.51860402984325));
#400911=CARTESIAN_POINT('Ctrl Pts',(-1.87457651791765,-2.0033997403191,
7.51734760759493));
#400912=CARTESIAN_POINT('Ctrl Pts',(-1.87474064949508,-2.00376831688545,
7.51608817408573));
#400913=CARTESIAN_POINT('Ctrl Pts',(-1.87496253976455,-2.00407368959407,
7.51481005913119));
#400914=CARTESIAN_POINT('Ctrl Pts',(-1.87516353327288,-2.00435030349066,
7.51365231206383));
#400915=CARTESIAN_POINT('Ctrl Pts',(-1.87541199969988,-2.00457559451801,
7.51247773061042));
#400916=CARTESIAN_POINT('Ctrl Pts',(-1.87572844271701,-2.00471830984543,
7.51129758471022));
#400917=CARTESIAN_POINT('Ctrl Pts',(-1.87612174524816,-2.0048956886987,
7.50983079813402));
#400918=CARTESIAN_POINT('Ctrl Pts',(-1.87661285822996,-2.00492797351969,
7.50839324291155));
#400919=CARTESIAN_POINT('Ctrl Pts',(-1.87721077373281,-2.00473313789105,
7.50715379678855));
#400920=CARTESIAN_POINT('Ctrl Pts',(-1.8774869934666,-2.00464312944468,
7.50658120839351));
#400921=CARTESIAN_POINT('Ctrl Pts',(-1.87782232998934,-2.00448281985078,
7.50598221009429));
#400922=CARTESIAN_POINT('Ctrl Pts',(-1.87819899209074,-2.00423550222563,
7.50545747549612));
#400923=CARTESIAN_POINT('Ctrl Pts',(-1.87839999064682,-2.00410352588565,
7.50517746087247));
#400924=CARTESIAN_POINT('Ctrl Pts',(-1.87861504784397,-2.00394551114248,
7.50491486231392));
#400925=CARTESIAN_POINT('Ctrl Pts',(-1.87883748095715,-2.00376429830917,
7.50468370960993));
#400926=CARTESIAN_POINT('Ctrl Pts',(-1.87917008862392,-2.00349332796302,
7.50433806340447));
#400927=CARTESIAN_POINT('Ctrl Pts',(-1.87952881064225,-2.00316193046716,
7.50405484070984));
#400928=CARTESIAN_POINT('Ctrl Pts',(-1.87988900162133,-2.00279189861426,
7.50385766036131));
#400929=CARTESIAN_POINT('Ctrl Pts',(-1.8799275184479,-2.00275232945919,
7.50383657498791));
#400930=CARTESIAN_POINT('Ctrl Pts',(-1.87996604537338,-2.00271234608088,
7.50381643264937));
#400931=CARTESIAN_POINT('Ctrl Pts',(-1.88000454770714,-2.00267199522525,
7.50379723213559));
#400932=CARTESIAN_POINT('Ctrl Pts',(-1.88026156337996,-2.00240264006418,
7.50366906242519));
#400933=CARTESIAN_POINT('Ctrl Pts',(-1.88052255371097,-2.00211055462659,
7.50358235568538));
#400934=CARTESIAN_POINT('Ctrl Pts',(-1.88076734876144,-2.00182297316665,
7.5035341175365));
#400935=CARTESIAN_POINT('Ctrl Pts',(-1.88113439123417,-2.0013917773154,
7.50346178989176));
#400936=CARTESIAN_POINT('Ctrl Pts',(-1.88151091146151,-2.00091230248073,
7.50346967198527));
#400937=CARTESIAN_POINT('Ctrl Pts',(-1.88186605434872,-2.0004302333364,
7.50354272648692));
#400938=CARTESIAN_POINT('Ctrl Pts',(-1.88201213196926,-2.00023194831909,
7.50357277531559));
#400939=CARTESIAN_POINT('Ctrl Pts',(-1.88215451294323,-2.00003357194373,
7.50361331098761));
#400940=CARTESIAN_POINT('Ctrl Pts',(-1.88229076388218,-1.99983961245623,
7.50366116523659));
#400941=CARTESIAN_POINT('',(-1.86023191546303,-1.92084218059593,7.57603338622103));
#400942=CARTESIAN_POINT('Origin',(-1.866381668932,-1.92718820469555,7.58486873427629));
#400943=CARTESIAN_POINT('Ctrl Pts',(-1.8822907638914,-1.99983961251163,
7.50366116529968));
#400944=CARTESIAN_POINT('Ctrl Pts',(-1.87495061796101,-1.97354987960083,
7.52783573079709));
#400945=CARTESIAN_POINT('Ctrl Pts',(-1.86759803291972,-1.94721864078629,
7.55196141284068));
#400946=CARTESIAN_POINT('Ctrl Pts',(-1.86023191544545,-1.92084218184786,
7.57603338728831));
#400947=CARTESIAN_POINT('Ctrl Pts',(-1.85201547038342,-1.92152278748123,
7.59639677331371));
#400948=CARTESIAN_POINT('Ctrl Pts',(-1.8444010537121,-1.90490675382385,
7.59959882295465));
#400949=CARTESIAN_POINT('Ctrl Pts',(-1.86101220389835,-1.9125734677282,
7.59642833564546));
#400950=CARTESIAN_POINT('Ctrl Pts',(-1.84984160606563,-1.9182840503799,
7.58707626057422));
#400951=CARTESIAN_POINT('Ctrl Pts',(-1.85118862591897,-1.91164343078902,
7.58809943920599));
#400952=CARTESIAN_POINT('Ctrl Pts',(-1.85783564952498,-1.91040590180985,
7.58710240504253));
#400953=CARTESIAN_POINT('Ctrl Pts',(-1.85581853271803,-1.91938039888897,
7.5801537675693));
#400954=CARTESIAN_POINT('Ctrl Pts',(-1.85601709593955,-1.91653613377419,
7.5820588065976));
#400955=CARTESIAN_POINT('Ctrl Pts',(-1.85882870182067,-1.91638798720131,
7.58020924244128));
#400956=CARTESIAN_POINT('Ctrl Pts',(-1.86023191488716,-1.92084218000158,
7.57603338509286));
#400957=CARTESIAN_POINT('Ctrl Pts',(-1.86023191488716,-1.92084218000158,
7.57603338509286));
#400958=CARTESIAN_POINT('Ctrl Pts',(-1.86023191488716,-1.92084218000158,
7.57603338509286));
#400959=CARTESIAN_POINT('Origin',(-1.86637756977769,-1.92719217450528,7.58486873427621));
#400960=CARTESIAN_POINT('Ctrl Pts',(-1.95008020177389,-1.94026180847486,
7.51098857897448));
#400961=CARTESIAN_POINT('Ctrl Pts',(-1.94446108228009,-1.93850510471887,
7.50433767179956));
#400962=CARTESIAN_POINT('Ctrl Pts',(-1.94010972714623,-1.94593300883656,
7.50214974420965));
#400963=CARTESIAN_POINT('Ctrl Pts',(-1.92001395850861,-1.93086220725069,
7.53887321589168));
#400964=CARTESIAN_POINT('Ctrl Pts',(-1.91446216603847,-1.92912655192329,
7.53220407452062));
#400965=CARTESIAN_POINT('Ctrl Pts',(-1.91007676036987,-1.93650023058753,
7.53003438070911));
#400966=CARTESIAN_POINT('Ctrl Pts',(-1.88988997696527,-1.92144455532479,
7.56669465659231));
#400967=CARTESIAN_POINT('Ctrl Pts',(-1.88437099455649,-1.91971915739764,
7.56004085833299));
#400968=CARTESIAN_POINT('Ctrl Pts',(-1.87998739246263,-1.92704859685846,
7.55785582193789));
#400969=CARTESIAN_POINT('Ctrl Pts',(-1.85970961953101,-1.91200927861987,
7.59443891967696));
#400970=CARTESIAN_POINT('Ctrl Pts',(-1.85418263528486,-1.91028137908059,
7.58783901202978));
#400971=CARTESIAN_POINT('Ctrl Pts',(-1.84984313418238,-1.917578495509,7.58560008491213));
#400972=CARTESIAN_POINT('',(-1.93848173883013,-1.94542168785063,7.50366116523517));
#400973=CARTESIAN_POINT('Ctrl Pts',(-1.93848173883039,-1.94542168785089,
7.50366116523554));
#400974=CARTESIAN_POINT('Ctrl Pts',(-1.93911531306414,-1.94500609044102,
7.50350835821027));
#400975=CARTESIAN_POINT('Ctrl Pts',(-1.93968420053049,-1.9446034428758,
7.50345484956));
#400976=CARTESIAN_POINT('Ctrl Pts',(-1.94020566163612,-1.94420226426758,
7.50349758195598));
#400977=CARTESIAN_POINT('Ctrl Pts',(-1.94047320985588,-1.94399642988938,
7.50351950684424));
#400978=CARTESIAN_POINT('Ctrl Pts',(-1.9407547228782,-1.94377079693832,
7.50357029184312));
#400979=CARTESIAN_POINT('Ctrl Pts',(-1.9410202019391,-1.94354575978781,
7.50365515313923));
#400980=CARTESIAN_POINT('Ctrl Pts',(-1.94142861623784,-1.94319956152377,
7.50378570417639));
#400981=CARTESIAN_POINT('Ctrl Pts',(-1.94181129617362,-1.94284487582416,
7.50400001621911));
#400982=CARTESIAN_POINT('Ctrl Pts',(-1.94213757088236,-1.94250703424478,
7.50428903009634));
#400983=CARTESIAN_POINT('Ctrl Pts',(-1.94217378486482,-1.94246953642866,
7.50432110841318));
#400984=CARTESIAN_POINT('Ctrl Pts',(-1.94220933369086,-1.94243224012205,
7.50435406373354));
#400985=CARTESIAN_POINT('Ctrl Pts',(-1.94224419729613,-1.94239517523651,
7.50438785222352));
#400986=CARTESIAN_POINT('Ctrl Pts',(-1.94245705636385,-1.94216887629467,
7.50459414719561));
#400987=CARTESIAN_POINT('Ctrl Pts',(-1.9426473857875,-1.94194724773844,
7.50483629897752));
#400988=CARTESIAN_POINT('Ctrl Pts',(-1.94280889250207,-1.94173963749441,
7.5050991045531));
#400989=CARTESIAN_POINT('Ctrl Pts',(-1.94316519253623,-1.9412816284436,
7.50567888004914));
#400990=CARTESIAN_POINT('Ctrl Pts',(-1.94339566683996,-1.94087411611104,
7.50637912803145));
#400991=CARTESIAN_POINT('Ctrl Pts',(-1.94353025984857,-1.94052476529617,
7.50710440483569));
#400992=CARTESIAN_POINT('Ctrl Pts',(-1.94356326472632,-1.94043909754077,
7.50728225710685));
#400993=CARTESIAN_POINT('Ctrl Pts',(-1.94359129721341,-1.94035527428432,
7.50746498566954));
#400994=CARTESIAN_POINT('Ctrl Pts',(-1.94361409802643,-1.9402753843589,
7.50764697238949));
#400995=CARTESIAN_POINT('Ctrl Pts',(-1.94373666892226,-1.93984591810612,
7.50862528291181));
#400996=CARTESIAN_POINT('Ctrl Pts',(-1.94372315950023,-1.93949226889329,
7.50965856837421));
#400997=CARTESIAN_POINT('Ctrl Pts',(-1.94363670254535,-1.93919419697488,
7.51067959873201));
#400998=CARTESIAN_POINT('Ctrl Pts',(-1.94358912517403,-1.93903016762221,
7.51124147302578));
#400999=CARTESIAN_POINT('Ctrl Pts',(-1.94351902817062,-1.93888304980718,
7.51180065547252));
#401000=CARTESIAN_POINT('Ctrl Pts',(-1.94343435338581,-1.93875032191858,
7.512351757165));
#401001=CARTESIAN_POINT('Ctrl Pts',(-1.94314176827386,-1.93829169419093,
7.51425603304535));
#401002=CARTESIAN_POINT('Ctrl Pts',(-1.94263512968855,-1.93795345792506,
7.5162690050518));
#401003=CARTESIAN_POINT('Ctrl Pts',(-1.94197444496732,-1.93772914884597,
7.51827788969243));
#401004=CARTESIAN_POINT('Ctrl Pts',(-1.94193868746169,-1.93771700881472,
7.51838661432545));
#401005=CARTESIAN_POINT('Ctrl Pts',(-1.94190246953308,-1.93770520633127,
7.51849533314856));
#401006=CARTESIAN_POINT('Ctrl Pts',(-1.94186579781665,-1.93769374166282,
7.51860402984325));
#401007=CARTESIAN_POINT('Ctrl Pts',(-1.86023191671588,-1.92084218061917,
7.57603338728984));
#401008=CARTESIAN_POINT('Ctrl Pts',(-1.88635872817725,-1.92904992062326,
7.55196141284921));
#401009=CARTESIAN_POINT('Ctrl Pts',(-1.91244077649953,-1.93724268577581,
7.52783573083105));
#401010=CARTESIAN_POINT('Ctrl Pts',(-1.93848173888798,-1.9454216878631,
7.50366116530176));
#401011=CARTESIAN_POINT('Origin',(-6.42796117143043E-16,-6.63739765492889E-16,
7.49482233047033));
#401012=CARTESIAN_POINT('Origin',(-1.87623278704648,-1.99340331564182,7.49482233047033));
#401013=CARTESIAN_POINT('Origin',(0.,0.,7.50366116523517));
#401014=CARTESIAN_POINT('Origin',(-1.93224291659623,-1.93916053003967,7.49482233047033));
#401015=CARTESIAN_POINT('Ctrl Pts',(-1.87445804062327,-2.00297322077964,
7.51860402984325));
#401016=CARTESIAN_POINT('Ctrl Pts',(-1.87649514626118,-2.01030442031656,
7.51860402984325));
#401017=CARTESIAN_POINT('Ctrl Pts',(-1.87091852206099,-2.01548105518488,
7.51860402984325));
#401018=CARTESIAN_POINT('Ctrl Pts',(-1.87521443062422,-2.00569534553861,
7.51041458714366));
#401019=CARTESIAN_POINT('Ctrl Pts',(-1.87517397337955,-2.01153081715378,
7.51004642900442));
#401020=CARTESIAN_POINT('Ctrl Pts',(-1.87091698409425,-2.0154824828393,
7.5072913648301));
#401021=CARTESIAN_POINT('Ctrl Pts',(-1.87802007521301,-2.0059235902333,
7.50215815450138));
#401022=CARTESIAN_POINT('Ctrl Pts',(-1.87786410871604,-2.00903385371624,
7.4987716367153));
#401023=CARTESIAN_POINT('Ctrl Pts',(-1.87535173527746,-2.01139857427044,
7.4948158853317));
#401024=CARTESIAN_POINT('Ctrl Pts',(-1.8822903865665,-1.99983921157654,
7.50366171572174));
#401025=CARTESIAN_POINT('Ctrl Pts',(-1.88480006004697,-2.0025056138865,
7.50000045605858));
#401026=CARTESIAN_POINT('Ctrl Pts',(-1.88480006004688,-2.00250561388658,
7.49482233047317));
#401027=CARTESIAN_POINT('Origin',(-1.86241434696071,-2.00631977766131,7.51860402984325));
#401028=CARTESIAN_POINT('Origin',(-1.86241434696071,-2.00631977766131,9.));
#401029=CARTESIAN_POINT('Origin',(-1.86241434696071,-2.00631977766131,8.75721825406948));
#401030=CARTESIAN_POINT('Ctrl Pts',(-1.86998861308145,-1.98688333975427,
8.78942910404913));
#401031=CARTESIAN_POINT('Ctrl Pts',(-1.87149950741743,-1.99224707231726,
8.7967269950169));
#401032=CARTESIAN_POINT('Ctrl Pts',(-1.86349840890978,-1.99620382713061,
8.79893251111267));
#401033=CARTESIAN_POINT('Ctrl Pts',(-1.87293117467996,-1.99747658052279,
8.78111911759583));
#401034=CARTESIAN_POINT('Ctrl Pts',(-1.87471519242254,-2.00383736591608,
8.78644465894814));
#401035=CARTESIAN_POINT('Ctrl Pts',(-1.86838843520263,-2.00890566492617,
8.78817647674132));
#401036=CARTESIAN_POINT('Ctrl Pts',(-1.87476504922421,-2.00407854085086,
8.76780923932029));
#401037=CARTESIAN_POINT('Ctrl Pts',(-1.87686610037958,-2.01158855555212,
8.76988516158373));
#401038=CARTESIAN_POINT('Ctrl Pts',(-1.87143223505307,-2.01684302869503,
8.77093053738833));
#401039=CARTESIAN_POINT('Ctrl Pts',(-1.87440746878475,-2.00279124894153,
8.75371302330492));
#401040=CARTESIAN_POINT('Ctrl Pts',(-1.8764576876754,-2.01011673895027,
8.75300828287559));
#401041=CARTESIAN_POINT('Ctrl Pts',(-1.87083814324369,-2.01529508421824,
8.75267964240738));
#401042=CARTESIAN_POINT('Origin',(-1.85866130098619,-1.9928087663187,8.78727029226991));
#401043=CARTESIAN_POINT('Ctrl Pts',(-1.85157082176546,-1.92057895321254,
8.85049129520029));
#401044=CARTESIAN_POINT('Ctrl Pts',(-1.8531337541682,-1.92620552894984,
8.85711686593484));
#401045=CARTESIAN_POINT('Ctrl Pts',(-1.84563514921931,-1.9303130447361,
8.85933012996512));
#401046=CARTESIAN_POINT('Ctrl Pts',(-1.8579582536052,-1.94357378584259,
8.82945683644724));
#401047=CARTESIAN_POINT('Ctrl Pts',(-1.85953415929186,-1.94924706556039,
8.8360746990239));
#401048=CARTESIAN_POINT('Ctrl Pts',(-1.85199552183797,-1.9533337497709,
8.8382956714852));
#401049=CARTESIAN_POINT('Ctrl Pts',(-1.86433616446271,-1.96653434282028,
8.80838214965003));
#401050=CARTESIAN_POINT('Ctrl Pts',(-1.86591828940898,-1.97223001194863,
8.81501364461986));
#401051=CARTESIAN_POINT('Ctrl Pts',(-1.85834689049523,-1.97631935554932,
8.81722098428721));
#401052=CARTESIAN_POINT('Ctrl Pts',(-1.87070527778332,-1.98946322855772,
8.78727029226991));
#401053=CARTESIAN_POINT('Ctrl Pts',(-1.87228766552574,-1.99515984375545,
8.79393457792714));
#401054=CARTESIAN_POINT('Ctrl Pts',(-1.86468995654685,-1.99927253550787,
8.79610912703474));
#401055=CARTESIAN_POINT('Origin',(-1.83952684496832,-1.92392449097352,8.85049129520029));
#401056=CARTESIAN_POINT('Ctrl Pts',(-1.86024642503783,-1.91217709997535,
8.85049129520029));
#401057=CARTESIAN_POINT('Ctrl Pts',(-1.86582001548252,-1.91391956999746,
8.85711686593484));
#401058=CARTESIAN_POINT('Ctrl Pts',(-1.87016576301192,-1.90655647007116,
8.85933012996512));
#401059=CARTESIAN_POINT('Ctrl Pts',(-1.85531555002704,-1.91063556189962,
8.86332496987232));
#401060=CARTESIAN_POINT('Ctrl Pts',(-1.85882508285509,-1.90762972196618,
8.86648636486738));
#401061=CARTESIAN_POINT('Ctrl Pts',(-1.8563663269405,-1.90226030661205,
8.87206031107457));
#401062=CARTESIAN_POINT('Ctrl Pts',(-1.85017872212212,-1.91556737749544,
8.86341338519876));
#401063=CARTESIAN_POINT('Ctrl Pts',(-1.84703128601865,-1.91896842389454,
8.86654584966058));
#401064=CARTESIAN_POINT('Ctrl Pts',(-1.84175139158006,-1.91627642324357,
8.87215952290715));
#401065=CARTESIAN_POINT('Ctrl Pts',(-1.85157082176546,-1.92057895321254,
8.85049129520029));
#401066=CARTESIAN_POINT('Ctrl Pts',(-1.8531337541682,-1.92620552894984,
8.85711686593484));
#401067=CARTESIAN_POINT('Ctrl Pts',(-1.84563514921931,-1.9303130447361,
8.85933012996512));
#401068=CARTESIAN_POINT('Origin',(-1.86397627237229,-1.90024654094144,8.85049129520029));
#401069=CARTESIAN_POINT('Ctrl Pts',(-1.92848201925696,-1.9335095747144,
8.78727029226991));
#401070=CARTESIAN_POINT('Ctrl Pts',(-1.93412498960262,-1.93527373495554,
8.79393457792714));
#401071=CARTESIAN_POINT('Ctrl Pts',(-1.93847908687934,-1.92781174781517,
8.79610912703474));
#401072=CARTESIAN_POINT('Ctrl Pts',(-1.90576905413921,-1.92640882678118,
8.80838214965002));
#401073=CARTESIAN_POINT('Ctrl Pts',(-1.91141108732466,-1.92817269403819,
8.81501364461993));
#401074=CARTESIAN_POINT('Ctrl Pts',(-1.91574100516639,-1.92073625510017,
8.81722098428721));
#401075=CARTESIAN_POINT('Ctrl Pts',(-1.88302471602829,-1.91929827071789,
8.82945683644722));
#401076=CARTESIAN_POINT('Ctrl Pts',(-1.88864457064352,-1.92105520429472,
8.83607469902389));
#401077=CARTESIAN_POINT('Ctrl Pts',(-1.89297078040505,-1.91365142474659,
8.83829567148519));
#401078=CARTESIAN_POINT('Ctrl Pts',(-1.86024642503783,-1.91217709997535,
8.85049129520029));
#401079=CARTESIAN_POINT('Ctrl Pts',(-1.86582001548252,-1.91391956999746,
8.85711686593484));
#401080=CARTESIAN_POINT('Ctrl Pts',(-1.87016576301192,-1.90655647007116,
8.85933012996512));
#401081=CARTESIAN_POINT('Origin',(-1.93221186659142,-1.92157901568049,8.78727029226991));
#401082=CARTESIAN_POINT('Ctrl Pts',(-1.94168907725774,-1.93763847423637,
8.75374538247848));
#401083=CARTESIAN_POINT('Ctrl Pts',(-1.94893794972875,-1.93991843614102,
8.75304829418601));
#401084=CARTESIAN_POINT('Ctrl Pts',(-1.95429209524045,-1.93447750156609,
8.75272238421917));
#401085=CARTESIAN_POINT('Ctrl Pts',(-1.9429489285874,-1.93803234165217,
8.76769408445021));
#401086=CARTESIAN_POINT('Ctrl Pts',(-1.95038042190973,-1.94036901920208,
8.76974318093969));
#401087=CARTESIAN_POINT('Ctrl Pts',(-1.95580304081854,-1.93511415845701,
8.7707786988043));
#401088=CARTESIAN_POINT('Ctrl Pts',(-1.9364916483571,-1.93601360166431,
8.78108014887988));
#401089=CARTESIAN_POINT('Ctrl Pts',(-1.9427884316051,-1.9379974761634,8.78639403366325));
#401090=CARTESIAN_POINT('Ctrl Pts',(-1.94806417781673,-1.9318583738154,
8.78812224174741));
#401091=CARTESIAN_POINT('Ctrl Pts',(-1.92590959152934,-1.93270533243208,
8.78944554828685));
#401092=CARTESIAN_POINT('Ctrl Pts',(-1.93121460487315,-1.93438260731681,
8.79673892988686));
#401093=CARTESIAN_POINT('Ctrl Pts',(-1.93542357110277,-1.92652206295941,
8.79894799272499));
#401094=CARTESIAN_POINT('Origin',(-1.94559564515111,-1.92576318262891,8.75721825406948));
#401095=CARTESIAN_POINT('Origin',(-1.94559564515111,-1.92576318262891,9.));
#401096=CARTESIAN_POINT('Origin',(-1.94559564515111,-1.92576318262891,7.51860402984325));
#401097=CARTESIAN_POINT('Ctrl Pts',(-1.93848118356972,-1.94542113060226,
7.50366195182966));
#401098=CARTESIAN_POINT('Ctrl Pts',(-1.94106594361275,-1.94801514433199,
7.50000065167735));
#401099=CARTESIAN_POINT('Ctrl Pts',(-1.94106594361283,-1.9480151443319,
7.49482233047108));
#401100=CARTESIAN_POINT('Ctrl Pts',(-1.94470436195012,-1.94134364970685,
7.50215800491337));
#401101=CARTESIAN_POINT('Ctrl Pts',(-1.94781906623355,-1.941286078871,7.49877273257268));
#401102=CARTESIAN_POINT('Ctrl Pts',(-1.95026446067573,-1.93884944135752,
7.49481816995647));
#401103=CARTESIAN_POINT('Ctrl Pts',(-1.94455588051516,-1.93853509676885,
7.51043025814041));
#401104=CARTESIAN_POINT('Ctrl Pts',(-1.95039284348443,-1.93868549717535,
7.51006209594513));
#401105=CARTESIAN_POINT('Ctrl Pts',(-1.95448142463543,-1.93455482237167,
7.50731281821699));
#401106=CARTESIAN_POINT('Ctrl Pts',(-1.94186435528907,-1.93769329059009,
7.51860402984325));
#401107=CARTESIAN_POINT('Ctrl Pts',(-1.9491267100195,-1.93996468248934,
7.51860402984324));
#401108=CARTESIAN_POINT('Ctrl Pts',(-1.9544796435308,-1.934556621819,7.51860402984325));
#401109=CARTESIAN_POINT('Origin',(0.,0.,7.5));
#401110=CARTESIAN_POINT('Origin',(-1.73391074180929,-2.02743472471361,7.5));
#401111=CARTESIAN_POINT('',(-1.73391074180929,-2.02743472471361,7.59394543036555));
#401112=CARTESIAN_POINT('',(-1.73391074180929,-2.02743472471361,8.85049129520029));
#401113=CARTESIAN_POINT('',(-1.73391074180929,-2.02743472471361,7.5));
#401114=CARTESIAN_POINT('',(-1.80063936233258,-2.05309523912754,8.78727029226991));
#401115=CARTESIAN_POINT('Ctrl Pts',(-1.73391074180929,-2.02743472471361,
8.85049129520029));
#401116=CARTESIAN_POINT('Ctrl Pts',(-1.7561859474878,-2.03600066286585,
8.82945686509571));
#401117=CARTESIAN_POINT('Ctrl Pts',(-1.7784280383796,-2.04455386671525,
8.80838212259896));
#401118=CARTESIAN_POINT('Ctrl Pts',(-1.80063936233259,-2.05309523912754,
8.78727029226991));
#401119=CARTESIAN_POINT('',(-1.813727561987,-2.05812831089271,8.75721825406948));
#401120=CARTESIAN_POINT('Origin',(-1.77434055646776,-2.0429822403225,8.75937679713164));
#401121=CARTESIAN_POINT('',(-1.813727561987,-2.05812831089271,7.51860402984325));
#401122=CARTESIAN_POINT('',(-1.813727561987,-2.05812831089271,7.5));
#401123=CARTESIAN_POINT('Ctrl Pts',(-1.813727561987,-2.05812831089271,7.51860402984325));
#401124=CARTESIAN_POINT('Ctrl Pts',(-1.80344881675854,-2.0541756158119,
7.52834476460825));
#401125=CARTESIAN_POINT('Ctrl Pts',(-1.793163398717,-2.05022035469848,7.53807742314407));
#401126=CARTESIAN_POINT('Ctrl Pts',(-1.7828710838138,-2.04626244139449,
7.54780169004674));
#401127=CARTESIAN_POINT('Ctrl Pts',(-1.76656861325929,-2.03999332062794,
7.5632044032688));
#401128=CARTESIAN_POINT('Ctrl Pts',(-1.75024881863925,-2.03371753788588,
7.57858609112103));
#401129=CARTESIAN_POINT('Ctrl Pts',(-1.73391074180929,-2.02743472471361,
7.59394543036555));
#401130=CARTESIAN_POINT('Origin',(-1.78118873745326,-2.30440223853068,7.5));
#401131=CARTESIAN_POINT('',(-1.74227604793054,-2.11895587165399,8.75721825406948));
#401132=CARTESIAN_POINT('',(-1.73939636646037,-2.10523216165204,8.78727029226991));
#401133=CARTESIAN_POINT('Origin',(-1.73208666082126,-2.07039626697765,8.75658640621007));
#401134=CARTESIAN_POINT('',(-1.72471465490914,-2.0352634676321,8.85049129520029));
#401135=CARTESIAN_POINT('Ctrl Pts',(-1.73939636646037,-2.10523216165204,
8.78727029226991));
#401136=CARTESIAN_POINT('Ctrl Pts',(-1.73450940418104,-2.08194234511969,
8.80838212259896));
#401137=CARTESIAN_POINT('Ctrl Pts',(-1.72961567252274,-2.0586202677297,
8.82945686509571));
#401138=CARTESIAN_POINT('Ctrl Pts',(-1.72471465490914,-2.0352634676321,
8.85049129520029));
#401139=CARTESIAN_POINT('',(-1.72471465490914,-2.0352634676321,7.59394543036555));
#401140=CARTESIAN_POINT('',(-1.72471465490914,-2.0352634676321,7.5));
#401141=CARTESIAN_POINT('',(-1.74227604793054,-2.11895587165399,7.51860402984325));
#401142=CARTESIAN_POINT('Ctrl Pts',(-1.72471465490914,-2.0352634676321,
7.59394543036555));
#401143=CARTESIAN_POINT('Ctrl Pts',(-1.72830937827429,-2.05239485577748,
7.57858609112103));
#401144=CARTESIAN_POINT('Ctrl Pts',(-1.73190007916554,-2.06950707400212,
7.56320440326857));
#401145=CARTESIAN_POINT('Ctrl Pts',(-1.73548696839503,-2.08660112697448,
7.54780169004651));
#401146=CARTESIAN_POINT('Ctrl Pts',(-1.73775149593086,-2.09739319530395,
7.53807742314383));
#401147=CARTESIAN_POINT('Ctrl Pts',(-1.74001450601091,-2.10817803188809,
7.52834476460825));
#401148=CARTESIAN_POINT('Ctrl Pts',(-1.74227604793054,-2.11895587165399,
7.51860402984325));
#401149=CARTESIAN_POINT('',(-1.74227604793054,-2.11895587165399,7.5));
#401150=CARTESIAN_POINT('Origin',(-1.7314431241816,-2.0338516155685,7.5));
#401151=CARTESIAN_POINT('Ctrl Pts',(-1.72471465490914,-2.0352634676321,
8.85049129520029));
#401152=CARTESIAN_POINT('Ctrl Pts',(-1.72467488452415,-2.03507393374238,
8.85097269580138));
#401153=CARTESIAN_POINT('Ctrl Pts',(-1.7246438480515,-2.03488506380326,
8.85143669361005));
#401154=CARTESIAN_POINT('Ctrl Pts',(-1.72462097907697,-2.03468801919691,
8.8519052845931));
#401155=CARTESIAN_POINT('Ctrl Pts',(-1.72457624881308,-2.03430261244298,
8.85282181883899));
#401156=CARTESIAN_POINT('Ctrl Pts',(-1.72456411104288,-2.03389582367071,
8.85372622499635));
#401157=CARTESIAN_POINT('Ctrl Pts',(-1.72459978718338,-2.03346080980621,
8.8546225773507));
#401158=CARTESIAN_POINT('Ctrl Pts',(-1.72462940424813,-2.03309967674613,
8.85536669723986));
#401159=CARTESIAN_POINT('Ctrl Pts',(-1.72469194862657,-2.03271900678389,
8.85610498449051));
#401160=CARTESIAN_POINT('Ctrl Pts',(-1.72480403100063,-2.03231614987659,
8.85681338218371));
#401161=CARTESIAN_POINT('Ctrl Pts',(-1.72490574593113,-2.03195055660051,
8.85745625420284));
#401162=CARTESIAN_POINT('Ctrl Pts',(-1.72504895764684,-2.03156194465407,
8.85808743050666));
#401163=CARTESIAN_POINT('Ctrl Pts',(-1.72526213979698,-2.03114764993346,
8.8586680450841));
#401164=CARTESIAN_POINT('Ctrl Pts',(-1.72536049741984,-2.03095650333018,
8.85893592806395));
#401165=CARTESIAN_POINT('Ctrl Pts',(-1.72547399192871,-2.03075989601328,
8.85919241173848));
#401166=CARTESIAN_POINT('Ctrl Pts',(-1.72560699390353,-2.0305578307355,
8.85943017985534));
#401167=CARTESIAN_POINT('Ctrl Pts',(-1.72578658594233,-2.03028498279278,
8.8597512372));
#401168=CARTESIAN_POINT('Ctrl Pts',(-1.72600685206651,-2.02999559083906,
8.86004599534706));
#401169=CARTESIAN_POINT('Ctrl Pts',(-1.72627343343412,-2.02969943976519,
8.86026130871721));
#401170=CARTESIAN_POINT('Ctrl Pts',(-1.72637103638852,-2.02959101050766,
8.86034014101235));
#401171=CARTESIAN_POINT('Ctrl Pts',(-1.72647630483696,-2.02948003821962,
8.86040910639692));
#401172=CARTESIAN_POINT('Ctrl Pts',(-1.72658661484442,-2.02936977777993,
8.86046313645506));
#401173=CARTESIAN_POINT('Ctrl Pts',(-1.72675875268721,-2.02919771728722,
8.86054744990829));
#401174=CARTESIAN_POINT('Ctrl Pts',(-1.72694797019717,-2.02902279750387,
8.86059655985668));
#401175=CARTESIAN_POINT('Ctrl Pts',(-1.72714193341414,-2.02885602144795,
8.86059725258816));
#401176=CARTESIAN_POINT('Ctrl Pts',(-1.72733634476364,-2.02868886007271,
8.86059794692011));
#401177=CARTESIAN_POINT('Ctrl Pts',(-1.7275394119433,-2.02853004075073,
8.86056369958366));
#401178=CARTESIAN_POINT('Ctrl Pts',(-1.72773774127272,-2.02838526137766,
8.86048590497774));
#401179=CARTESIAN_POINT('Ctrl Pts',(-1.72778949932273,-2.02834747827189,
8.86046560290182));
#401180=CARTESIAN_POINT('Ctrl Pts',(-1.7278416614481,-2.02831023298624,
8.86044257503091));
#401181=CARTESIAN_POINT('Ctrl Pts',(-1.72789259672071,-2.02827464971588,
8.86041778462583));
#401182=CARTESIAN_POINT('Ctrl Pts',(-1.72823532789993,-2.02803521846152,
8.86025097596201));
#401183=CARTESIAN_POINT('Ctrl Pts',(-1.7285686918965,-2.0278391805111,8.8599848982295));
#401184=CARTESIAN_POINT('Ctrl Pts',(-1.72887866392139,-2.02768495440917,
8.85968173251461));
#401185=CARTESIAN_POINT('Ctrl Pts',(-1.72904262136327,-2.02760337763735,
8.85952137522076));
#401186=CARTESIAN_POINT('Ctrl Pts',(-1.72920310952448,-2.02753175558216,
8.85934740853961));
#401187=CARTESIAN_POINT('Ctrl Pts',(-1.72935723163294,-2.02746967867184,
8.8591675900182));
#401188=CARTESIAN_POINT('Ctrl Pts',(-1.72997611200949,-2.02722040760996,
8.85844552518695));
#401189=CARTESIAN_POINT('Ctrl Pts',(-1.7305261907919,-2.02710815126501,
8.85759444184125));
#401190=CARTESIAN_POINT('Ctrl Pts',(-1.73098291656963,-2.02705690851457,
8.85683498915139));
#401191=CARTESIAN_POINT('Ctrl Pts',(-1.73103071170591,-2.02705154609721,
8.85675551444998));
#401192=CARTESIAN_POINT('Ctrl Pts',(-1.73107748282563,-2.02704687173969,
8.85667699793651));
#401193=CARTESIAN_POINT('Ctrl Pts',(-1.73112319999987,-2.02704281135589,
8.85659965593547));
#401194=CARTESIAN_POINT('Ctrl Pts',(-1.73174029275058,-2.02698800408813,
8.85555568965886));
#401195=CARTESIAN_POINT('Ctrl Pts',(-1.73234127237003,-2.02702445131194,
8.85434650606346));
#401196=CARTESIAN_POINT('Ctrl Pts',(-1.73292948597224,-2.02714612986161,
8.85297329937118));
#401197=CARTESIAN_POINT('Ctrl Pts',(-1.73326032028311,-2.02721456663182,
8.85220095427748));
#401198=CARTESIAN_POINT('Ctrl Pts',(-1.73358718755086,-2.02731030181011,
8.85137579139184));
#401199=CARTESIAN_POINT('Ctrl Pts',(-1.73391074180929,-2.02743472471361,
8.85049129520029));
#401200=CARTESIAN_POINT('Origin',(-1.7314431241816,-2.0338516155685,7.59394543036555));
#401201=CARTESIAN_POINT('Ctrl Pts',(-1.72459918806511,-2.0347131868116,
7.59443877723642));
#401202=CARTESIAN_POINT('Ctrl Pts',(-1.7234099906709,-2.02904582382637,
7.58783886950016));
#401203=CARTESIAN_POINT('Ctrl Pts',(-1.73109008020605,-2.02542706626766,
7.58559994247159));
#401204=CARTESIAN_POINT('Ctrl Pts',(-1.73109098175056,-2.06565115507454,
7.56670252222133));
#401205=CARTESIAN_POINT('Ctrl Pts',(-1.72990350308425,-2.05999198303778,
7.5600487499902));
#401206=CARTESIAN_POINT('Ctrl Pts',(-1.73761999295569,-2.05633245556569,
7.55786368756705));
#401207=CARTESIAN_POINT('Ctrl Pts',(-1.73757065265992,-2.09653134977288,
7.53888913333557));
#401208=CARTESIAN_POINT('Ctrl Pts',(-1.7363761167497,-2.09083854499964,
7.53222002137274));
#401209=CARTESIAN_POINT('Ctrl Pts',(-1.74413680190624,-2.08718146821332,
7.53005029815327));
#401210=CARTESIAN_POINT('Ctrl Pts',(-1.74403790758369,-2.12735237355686,
7.51101258149734));
#401211=CARTESIAN_POINT('Ctrl Pts',(-1.74282889172772,-2.12159056164571,
7.5043616886572));
#401212=CARTESIAN_POINT('Ctrl Pts',(-1.75064026593581,-2.11797256295502,
7.50217374673251));
#401213=CARTESIAN_POINT('',(-1.75029323173561,-2.11632951079882,7.50366116523517));
#401214=CARTESIAN_POINT('Ctrl Pts',(-1.74227604793054,-2.11895587165399,
7.51860402984325));
#401215=CARTESIAN_POINT('Ctrl Pts',(-1.74236673734234,-2.11938807056232,
7.51734760759494));
#401216=CARTESIAN_POINT('Ctrl Pts',(-1.74250691691215,-2.11976640579486,
7.51608817408573));
#401217=CARTESIAN_POINT('Ctrl Pts',(-1.74270878598765,-2.12008536764088,
7.5148100591312));
#401218=CARTESIAN_POINT('Ctrl Pts',(-1.74289164382005,-2.12037429090284,
7.51365231206384));
#401219=CARTESIAN_POINT('Ctrl Pts',(-1.74312516530045,-2.12061503834426,
7.51247773061043));
#401220=CARTESIAN_POINT('Ctrl Pts',(-1.74343181434905,-2.12077773502144,
7.51129758471022));
#401221=CARTESIAN_POINT('Ctrl Pts',(-1.74381294409581,-2.12097994841053,
7.50983079813402));
#401222=CARTESIAN_POINT('Ctrl Pts',(-1.74430097953774,-2.12104363261567,
7.50839324291155));
#401223=CARTESIAN_POINT('Ctrl Pts',(-1.74491014972064,-2.12088750587553,
7.50715379678855));
#401224=CARTESIAN_POINT('Ctrl Pts',(-1.74519156879233,-2.12081537982027,
7.50658120839351));
#401225=CARTESIAN_POINT('Ctrl Pts',(-1.74553648740116,-2.1206768846844,
7.50598221009429));
#401226=CARTESIAN_POINT('Ctrl Pts',(-1.74592822130452,-2.12045420802353,
7.50545747549611));
#401227=CARTESIAN_POINT('Ctrl Pts',(-1.74613726264066,-2.1203353808648,
7.50517746087247));
#401228=CARTESIAN_POINT('Ctrl Pts',(-1.74636200201908,-2.1201914695418,
7.50491486231392));
#401229=CARTESIAN_POINT('Ctrl Pts',(-1.74659558846567,-2.12002488036818,
7.50468370960992));
#401230=CARTESIAN_POINT('Ctrl Pts',(-1.74694487388399,-2.11977577700604,
7.50433806340446));
#401231=CARTESIAN_POINT('Ctrl Pts',(-1.74732409157993,-2.11946804380051,
7.50405484070984));
#401232=CARTESIAN_POINT('Ctrl Pts',(-1.74770725053022,-2.119121849733,7.50385766036131));
#401233=CARTESIAN_POINT('Ctrl Pts',(-1.74774822342432,-2.11908482965855,
7.50383657498791));
#401234=CARTESIAN_POINT('Ctrl Pts',(-1.74778923293594,-2.11904739685898,
7.50381643264937));
#401235=CARTESIAN_POINT('Ctrl Pts',(-1.74783024145072,-2.11900959576149,
7.50379723213559));
#401236=CARTESIAN_POINT('Ctrl Pts',(-1.7481039867017,-2.11875726107019,
7.50366906242519));
#401237=CARTESIAN_POINT('Ctrl Pts',(-1.74838315477833,-2.11848249746138,
7.50358235568538));
#401238=CARTESIAN_POINT('Ctrl Pts',(-1.74864587227851,-2.11821119094112,
7.5035341175365));
#401239=CARTESIAN_POINT('Ctrl Pts',(-1.74903978743616,-2.11780439751997,
7.50346178989176));
#401240=CARTESIAN_POINT('Ctrl Pts',(-1.74944625412045,-2.11735003155156,
7.50346967198527));
#401241=CARTESIAN_POINT('Ctrl Pts',(-1.74983155360463,-2.1168917069529,
7.50354272648692));
#401242=CARTESIAN_POINT('Ctrl Pts',(-1.7499900352577,-2.11670318855871,
7.50357277531559));
#401243=CARTESIAN_POINT('Ctrl Pts',(-1.7501448337127,-2.11651434214921,
7.50361331098761));
#401244=CARTESIAN_POINT('Ctrl Pts',(-1.75029323173652,-2.11632951079991,
7.50366116523659));
#401245=CARTESIAN_POINT('',(-1.73334108842445,-2.03608107236507,7.57603338622103));
#401246=CARTESIAN_POINT('Origin',(-1.73907161540567,-2.04280807393543,7.58486873427627));
#401247=CARTESIAN_POINT('Ctrl Pts',(-1.75029323174217,-2.11632951085579,
7.50366116529969));
#401248=CARTESIAN_POINT('Ctrl Pts',(-1.74465255589966,-2.08962350825637,
7.52783573079709));
#401249=CARTESIAN_POINT('Ctrl Pts',(-1.7390021257961,-2.06287528805497,
7.55196141284069));
#401250=CARTESIAN_POINT('Ctrl Pts',(-1.73334108832669,-2.03608107361331,
7.57603338728831));
#401251=CARTESIAN_POINT('Ctrl Pts',(-1.72509791827961,-2.03623385142682,
7.59639677331372));
#401252=CARTESIAN_POINT('Ctrl Pts',(-1.71825676553203,-2.01836216837368,
7.59974925422225));
#401253=CARTESIAN_POINT('Ctrl Pts',(-1.73480751822064,-2.02796794848296,
7.59639677331372));
#401254=CARTESIAN_POINT('Ctrl Pts',(-1.72313602699774,-2.03286248869316,
7.58707626057422));
#401255=CARTESIAN_POINT('Ctrl Pts',(-1.72493641503088,-2.02620846475785,
7.58811717123965));
#401256=CARTESIAN_POINT('Ctrl Pts',(-1.73179248798735,-2.02549313601007,
7.58707626057424));
#401257=CARTESIAN_POINT('Ctrl Pts',(-1.72903043012316,-2.03433952764208,
7.5801537675693));
#401258=CARTESIAN_POINT('Ctrl Pts',(-1.72941656890807,-2.03147110842989,
7.58208760766041));
#401259=CARTESIAN_POINT('Ctrl Pts',(-1.73230984781102,-2.03154771866078,
7.5801537675693));
#401260=CARTESIAN_POINT('Ctrl Pts',(-1.73334108788784,-2.03608107173505,
7.57603338509286));
#401261=CARTESIAN_POINT('Ctrl Pts',(-1.73334108788784,-2.03608107173505,
7.57603338509286));
#401262=CARTESIAN_POINT('Ctrl Pts',(-1.73334108788784,-2.03608107173505,
7.57603338509286));
#401263=CARTESIAN_POINT('Origin',(-1.73906727032637,-2.0428117729544,7.58486873427621));
#401264=CARTESIAN_POINT('Ctrl Pts',(-1.82176055196474,-2.06121740000461,
7.51098857897448));
#401265=CARTESIAN_POINT('Ctrl Pts',(-1.81626552995068,-2.05910428736283,
7.50433767179956));
#401266=CARTESIAN_POINT('Ctrl Pts',(-1.81144720769181,-2.06623813777422,
7.50214974420965));
#401267=CARTESIAN_POINT('Ctrl Pts',(-1.79235831753897,-2.04991076044924,
7.53887321589164));
#401268=CARTESIAN_POINT('Ctrl Pts',(-1.78692913564055,-2.04782296664701,
7.53220407452058));
#401269=CARTESIAN_POINT('Ctrl Pts',(-1.78208030704416,-2.05490052139174,
7.53003438070911));
#401270=CARTESIAN_POINT('Ctrl Pts',(-1.76289961997713,-2.0385824079751,
7.56669465659231));
#401271=CARTESIAN_POINT('Ctrl Pts',(-1.75750252353432,-2.03650695264607,
7.56004085833295));
#401272=CARTESIAN_POINT('Ctrl Pts',(-1.75265832922258,-2.04354047463692,
7.55785582193789));
#401273=CARTESIAN_POINT('Ctrl Pts',(-1.73338579157812,-2.02723285491819,
7.59443891967696));
#401274=CARTESIAN_POINT('Ctrl Pts',(-1.72798087001745,-2.02515439043735,
7.58783901202978));
#401275=CARTESIAN_POINT('Ctrl Pts',(-1.7231827570306,-2.0321584813672,7.58560008491213));
#401276=CARTESIAN_POINT('',(-1.80985532470035,-2.06562356178256,7.50366116523517));
#401277=CARTESIAN_POINT('Ctrl Pts',(-1.8098553247006,-2.06562356178284,
7.50366116523554));
#401278=CARTESIAN_POINT('Ctrl Pts',(-1.81051422460561,-2.06524941150295,
7.50350835821027));
#401279=CARTESIAN_POINT('Ctrl Pts',(-1.81110774094972,-2.06488403996545,
7.50345484956));
#401280=CARTESIAN_POINT('Ctrl Pts',(-1.81165383425926,-2.06451709574946,
7.50349758195598));
#401281=CARTESIAN_POINT('Ctrl Pts',(-1.8119340206264,-2.06432882615336,
7.50351950684424));
#401282=CARTESIAN_POINT('Ctrl Pts',(-1.81222941160284,-2.06412169339066,
7.50357029184312));
#401283=CARTESIAN_POINT('Ctrl Pts',(-1.81250876338827,-2.06391412790494,
7.50365515313924));
#401284=CARTESIAN_POINT('Ctrl Pts',(-1.81293851955496,-2.06359480813633,
7.50378570417639));
#401285=CARTESIAN_POINT('Ctrl Pts',(-1.81334313802457,-2.0632653695642,
7.50400001621911));
#401286=CARTESIAN_POINT('Ctrl Pts',(-1.81369038795123,-2.06294912660894,
7.50428903009634));
#401287=CARTESIAN_POINT('Ctrl Pts',(-1.81372893002152,-2.06291402607393,
7.50432110841318));
#401288=CARTESIAN_POINT('Ctrl Pts',(-1.81376679539125,-2.06287908401768,
7.50435406373354));
#401289=CARTESIAN_POINT('Ctrl Pts',(-1.81380396212087,-2.06284432900478,
7.50438785222352));
#401290=CARTESIAN_POINT('Ctrl Pts',(-1.8140308828698,-2.06263213294569,
7.50459414719561));
#401291=CARTESIAN_POINT('Ctrl Pts',(-1.81423502103158,-2.06242315419714,
7.50483629897752));
#401292=CARTESIAN_POINT('Ctrl Pts',(-1.81440949754729,-2.06222631828135,
7.5050991045531));
#401293=CARTESIAN_POINT('Ctrl Pts',(-1.81479441026545,-2.06179207848082,
7.50567888004914));
#401294=CARTESIAN_POINT('Ctrl Pts',(-1.8150505204398,-2.0614001699654,7.50637912803144));
#401295=CARTESIAN_POINT('Ctrl Pts',(-1.8152072198962,-2.06106016033291,
7.50710440483569));
#401296=CARTESIAN_POINT('Ctrl Pts',(-1.81524564571382,-2.06097678322089,
7.50728225710685));
#401297=CARTESIAN_POINT('Ctrl Pts',(-1.81527899117964,-2.06089492823592,
7.50746498566954));
#401298=CARTESIAN_POINT('Ctrl Pts',(-1.81530686371104,-2.06081666330602,
7.50764697238949));
#401299=CARTESIAN_POINT('Ctrl Pts',(-1.81545669876911,-2.06039593258197,
7.50862528291182));
#401300=CARTESIAN_POINT('Ctrl Pts',(-1.8154658754865,-2.06004214442774,
7.50965856837422));
#401301=CARTESIAN_POINT('Ctrl Pts',(-1.81539869370008,-2.05973914561394,
7.51067959873203));
#401302=CARTESIAN_POINT('Ctrl Pts',(-1.81536172347828,-2.05957240498452,
7.51124147302579));
#401303=CARTESIAN_POINT('Ctrl Pts',(-1.81530119636746,-2.05942109830839,
7.51180065547253));
#401304=CARTESIAN_POINT('Ctrl Pts',(-1.81522519946109,-2.05928321799138,
7.51235175716501));
#401305=CARTESIAN_POINT('Ctrl Pts',(-1.81496259987603,-2.0588067865711,
7.51425603304536));
#401306=CARTESIAN_POINT('Ctrl Pts',(-1.814478673106,-2.0584367848023,7.51626900505181));
#401307=CARTESIAN_POINT('Ctrl Pts',(-1.81383371736442,-2.05817060637484,
7.51827788969245));
#401308=CARTESIAN_POINT('Ctrl Pts',(-1.81379881114089,-2.05815620029534,
7.51838661432546));
#401309=CARTESIAN_POINT('Ctrl Pts',(-1.81376342381362,-2.0581421015707,
7.51849533314857));
#401310=CARTESIAN_POINT('Ctrl Pts',(-1.813727561987,-2.05812831089271,7.51860402984325));
#401311=CARTESIAN_POINT('Ctrl Pts',(-1.73334108967324,-2.03608107246854,
7.57603338728985));
#401312=CARTESIAN_POINT('Ctrl Pts',(-1.75888834909077,-2.04594589934822,
7.55196141284922));
#401313=CARTESIAN_POINT('Ctrl Pts',(-1.7843918967819,-2.05579291415967,
7.52783573083105));
#401314=CARTESIAN_POINT('Ctrl Pts',(-1.80985532475728,-2.06562356179871,
7.50366116530176));
#401315=CARTESIAN_POINT('Origin',(-5.98949470795629E-16,-7.0356012958692E-16,
7.49482233047033));
#401316=CARTESIAN_POINT('Origin',(-1.7446600766167,-2.1095183021391,7.49482233047033));
#401317=CARTESIAN_POINT('Origin',(0.,0.,7.50366116523517));
#401318=CARTESIAN_POINT('Origin',(-1.80403047455412,-2.05897554547888,7.49482233047033));
#401319=CARTESIAN_POINT('Ctrl Pts',(-1.74227583067299,-2.11895483648669,
7.51860402984325));
#401320=CARTESIAN_POINT('Ctrl Pts',(-1.74383903929183,-2.12640149109424,
7.51860402984325));
#401321=CARTESIAN_POINT('Ctrl Pts',(-1.73794220472938,-2.13121019447177,
7.51860402984325));
#401322=CARTESIAN_POINT('Ctrl Pts',(-1.74285625945743,-2.12171983042215,
7.51041458714365));
#401323=CARTESIAN_POINT('Ctrl Pts',(-1.74244200538642,-2.12754072033047,
7.51004642900441));
#401324=CARTESIAN_POINT('Ctrl Pts',(-1.73794057845242,-2.13121152065507,
7.50729136483009));
#401325=CARTESIAN_POINT('Ctrl Pts',(-1.74564151586071,-2.12212736442963,
7.50215815450138));
#401326=CARTESIAN_POINT('Ctrl Pts',(-1.74528659454811,-2.12522124473491,
7.49877163671531));
#401327=CARTESIAN_POINT('Ctrl Pts',(-1.74262787488409,-2.12742013839822,
7.49481588533172));
#401328=CARTESIAN_POINT('Ctrl Pts',(-1.75029288088052,-2.11632908656917,
7.50366171572174));
#401329=CARTESIAN_POINT('Ctrl Pts',(-1.75262656098511,-2.11915080580159,
7.50000045605858));
#401330=CARTESIAN_POINT('Ctrl Pts',(-1.75262656098502,-2.11915080580166,
7.49482233047317));
#401331=CARTESIAN_POINT('Origin',(-1.73004246743515,-2.12152287540599,7.51860402984325));
#401332=CARTESIAN_POINT('Origin',(-1.73004246743515,-2.12152287540599,9.));
#401333=CARTESIAN_POINT('Origin',(-1.73004246743515,-2.12152287540599,8.75721825406948));
#401334=CARTESIAN_POINT('Ctrl Pts',(-1.73884646826615,-2.10261165664174,
8.78942910404912));
#401335=CARTESIAN_POINT('Ctrl Pts',(-1.74001060278245,-2.10806117217338,
8.79672699501689));
#401336=CARTESIAN_POINT('Ctrl Pts',(-1.73177243323851,-2.11149716526814,
8.79893251111266));
#401337=CARTESIAN_POINT('Ctrl Pts',(-1.74110427278992,-2.11337166302987,
8.78111911759584));
#401338=CARTESIAN_POINT('Ctrl Pts',(-1.74247708815732,-2.11983368191661,
8.78644465894819));
#401339=CARTESIAN_POINT('Ctrl Pts',(-1.73583860290615,-2.12448621083597,
8.78817647674132));
#401340=CARTESIAN_POINT('Ctrl Pts',(-1.74251139039172,-2.1200775556679,
8.76780923932029));
#401341=CARTESIAN_POINT('Ctrl Pts',(-1.74412695641818,-2.12770675504822,
8.76988516158369));
#401342=CARTESIAN_POINT('Ctrl Pts',(-1.73836760030061,-2.13260228336569,
8.77093053738832));
#401343=CARTESIAN_POINT('Ctrl Pts',(-1.74223702171543,-2.11876999838042,
8.75371302330492));
#401344=CARTESIAN_POINT('Ctrl Pts',(-1.74381368245516,-2.1262117953596,
8.7530082828756));
#401345=CARTESIAN_POINT('Ctrl Pts',(-1.73787390625973,-2.13101945571392,
8.75267964240738));
#401346=CARTESIAN_POINT('Origin',(-1.72716278596498,-2.10779916540405,8.78727029226991));
#401347=CARTESIAN_POINT('Ctrl Pts',(-1.72471465490914,-2.0352634676321,
8.85049129520029));
#401348=CARTESIAN_POINT('Ctrl Pts',(-1.72591388015441,-2.04097862038896,
8.85711686593484));
#401349=CARTESIAN_POINT('Ctrl Pts',(-1.71816751245361,-2.04459725957488,
8.85933012996512));
#401350=CARTESIAN_POINT('Ctrl Pts',(-1.72961567910009,-2.05862029907538,
8.82945683644723));
#401351=CARTESIAN_POINT('Ctrl Pts',(-1.73082485863996,-2.06438289105558,
8.83607469902389));
#401352=CARTESIAN_POINT('Ctrl Pts',(-1.72303987536888,-2.06797817657507,
8.8382956714852));
#401353=CARTESIAN_POINT('Ctrl Pts',(-1.73450939791927,-2.08194231527794,
8.80838214965001));
#401354=CARTESIAN_POINT('Ctrl Pts',(-1.73572334944616,-2.08772764913656,
8.81501364461988));
#401355=CARTESIAN_POINT('Ctrl Pts',(-1.72790550163945,-2.09132348954826,
8.81722098428721));
#401356=CARTESIAN_POINT('Ctrl Pts',(-1.73939636646037,-2.10523216165204,
8.78727029226991));
#401357=CARTESIAN_POINT('Ctrl Pts',(-1.7406105196286,-2.11101845647365,
8.79393457792714));
#401358=CARTESIAN_POINT('Ctrl Pts',(-1.73276491989237,-2.11463591137414,
8.79610912703474));
#401359=CARTESIAN_POINT('Origin',(-1.71248107441375,-2.03783047138411,8.85049129520029));
#401360=CARTESIAN_POINT('Ctrl Pts',(-1.73391074180929,-2.02743472471361,
8.85049129520029));
#401361=CARTESIAN_POINT('Ctrl Pts',(-1.73936124027702,-2.02953071581005,
8.85711686593484));
#401362=CARTESIAN_POINT('Ctrl Pts',(-1.74416981443405,-2.02246117716243,
8.85933012996512));
#401363=CARTESIAN_POINT('Ctrl Pts',(-1.72908876449367,-2.02558043164655,
8.86332496987232));
#401364=CARTESIAN_POINT('Ctrl Pts',(-1.73278367143589,-2.02280562407395,
8.86648636486738));
#401365=CARTESIAN_POINT('Ctrl Pts',(-1.73067398692192,-2.0172897077272,
8.87206031107457));
#401366=CARTESIAN_POINT('Ctrl Pts',(-1.72364650824247,-2.03017299660442,
8.86341338519876));
#401367=CARTESIAN_POINT('Ctrl Pts',(-1.72028763309307,-2.03336539826539,
8.86654584966058));
#401368=CARTESIAN_POINT('Ctrl Pts',(-1.71519106383778,-2.03034064462033,
8.87215952290714));
#401369=CARTESIAN_POINT('Ctrl Pts',(-1.72471465490914,-2.0352634676321,
8.85049129520029));
#401370=CARTESIAN_POINT('Ctrl Pts',(-1.72591388015441,-2.04097862038896,
8.85711686593484));
#401371=CARTESIAN_POINT('Ctrl Pts',(-1.71816751245361,-2.04459725957488,
8.85933012996512));
#401372=CARTESIAN_POINT('Origin',(-1.73839731931417,-2.015767650432,8.85049129520029));
#401373=CARTESIAN_POINT('Ctrl Pts',(-1.80063936233259,-2.05309523912754,
8.78727029226991));
#401374=CARTESIAN_POINT('Ctrl Pts',(-1.80615770845573,-2.05521732106365,
8.79393457792714));
#401375=CARTESIAN_POINT('Ctrl Pts',(-1.8109809509302,-2.0480496333465,8.79610912703474));
#401376=CARTESIAN_POINT('Ctrl Pts',(-1.77842800991973,-2.044553855771,8.80838214965002));
#401377=CARTESIAN_POINT('Ctrl Pts',(-1.78394543957973,-2.04667558528088,
8.81501364461995));
#401378=CARTESIAN_POINT('Ctrl Pts',(-1.7887429154195,-2.03953184409284,
8.8172209842872));
#401379=CARTESIAN_POINT('Ctrl Pts',(-1.75618597738195,-2.03600067436165,
8.82945683644722));
#401380=CARTESIAN_POINT('Ctrl Pts',(-1.7616817182824,-2.03811406345147,
8.83607469902389));
#401381=CARTESIAN_POINT('Ctrl Pts',(-1.76647340116631,-2.03100267697358,
8.8382956714852));
#401382=CARTESIAN_POINT('Ctrl Pts',(-1.73391074180929,-2.02743472471361,
8.85049129520029));
#401383=CARTESIAN_POINT('Ctrl Pts',(-1.73936124027702,-2.02953071581005,
8.85711686593484));
#401384=CARTESIAN_POINT('Ctrl Pts',(-1.74416981443405,-2.02246117716243,
8.85933012996512));
#401385=CARTESIAN_POINT('Origin',(-1.80512593983747,-2.04142816484593,8.78727029226991));
#401386=CARTESIAN_POINT('Ctrl Pts',(-1.81355474551559,-2.05806183449402,
8.75374538247848));
#401387=CARTESIAN_POINT('Ctrl Pts',(-1.82064264673989,-2.06080154882625,
8.75304829418601));
#401388=CARTESIAN_POINT('Ctrl Pts',(-1.82633439346053,-2.05571483451569,
8.75272238421917));
#401389=CARTESIAN_POINT('Ctrl Pts',(-1.81478677317361,-2.05853561161882,
8.76769408445021));
#401390=CARTESIAN_POINT('Ctrl Pts',(-1.82205328625124,-2.06134362562603,
8.76974318093972));
#401391=CARTESIAN_POINT('Ctrl Pts',(-1.82780144389182,-2.0564469899423,
8.7707786988043));
#401392=CARTESIAN_POINT('Ctrl Pts',(-1.80847210123318,-2.05610729998394,
8.78108014887987));
#401393=CARTESIAN_POINT('Ctrl Pts',(-1.81462883978909,-2.05849053468797,
8.78639403366321));
#401394=CARTESIAN_POINT('Ctrl Pts',(-1.82028708005224,-2.05270206400449,
8.78812224174741));
#401395=CARTESIAN_POINT('Ctrl Pts',(-1.79812374791357,-2.05212783323685,
8.78944554828685));
#401396=CARTESIAN_POINT('Ctrl Pts',(-1.80331039816767,-2.05414155535238,
8.79673892988687));
#401397=CARTESIAN_POINT('Ctrl Pts',(-1.8080143434309,-2.04656683071863,
8.79894799272499));
#401398=CARTESIAN_POINT('Origin',(-1.81821413949188,-2.0464612366111,8.75721825406948));
#401399=CARTESIAN_POINT('Origin',(-1.81821413949188,-2.0464612366111,9.));
#401400=CARTESIAN_POINT('Origin',(-1.81821413949188,-2.0464612366111,7.51860402984325));
#401401=CARTESIAN_POINT('Ctrl Pts',(-1.80985480628381,-2.06562297010346,
7.50366195182966));
#401402=CARTESIAN_POINT('Ctrl Pts',(-1.81226805662981,-2.06837726029833,
7.50000065167735));
#401403=CARTESIAN_POINT('Ctrl Pts',(-1.8122680566299,-2.06837726029825,
7.49482233047108));
#401404=CARTESIAN_POINT('Ctrl Pts',(-1.81632644357473,-2.06195258723768,
7.50215800491337));
#401405=CARTESIAN_POINT('Ctrl Pts',(-1.81943843694026,-2.06209469447589,
7.49877273257264));
#401406=CARTESIAN_POINT('Ctrl Pts',(-1.82203492295881,-2.05981974025537,
7.49481816995649));
#401407=CARTESIAN_POINT('Ctrl Pts',(-1.81635821181536,-2.0591402915347,
7.51043025814042));
#401408=CARTESIAN_POINT('Ctrl Pts',(-1.82217354593106,-2.05966435842889,
7.51006209594515));
#401409=CARTESIAN_POINT('Ctrl Pts',(-1.82651837989694,-2.05580412683336,
7.50731281821698));
#401410=CARTESIAN_POINT('Ctrl Pts',(-1.81372615132356,-2.05812776832369,
7.51860402984325));
#401411=CARTESIAN_POINT('Ctrl Pts',(-1.82082805618867,-2.06085979406984,
7.51860402984325));
#401412=CARTESIAN_POINT('Ctrl Pts',(-1.8265164871608,-2.05580580846777,
7.51860402984325));
#401413=CARTESIAN_POINT('Origin',(0.,0.,7.5));
#401414=CARTESIAN_POINT('Origin',(-1.60045004741996,-2.13436118528464,7.5));
#401415=CARTESIAN_POINT('',(-1.60045004741996,-2.13436118528464,7.59394543036555));
#401416=CARTESIAN_POINT('',(-1.60045004741996,-2.13436118528464,8.85049129520029));
#401417=CARTESIAN_POINT('',(-1.60045004741996,-2.13436118528464,7.5));
#401418=CARTESIAN_POINT('',(-1.66539749203245,-2.16424429481556,8.78727029226991));
#401419=CARTESIAN_POINT('Ctrl Pts',(-1.60045004741996,-2.13436118528464,
8.85049129520029));
#401420=CARTESIAN_POINT('Ctrl Pts',(-1.62213066475764,-2.14433670112619,
8.82945686509571));
#401421=CARTESIAN_POINT('Ctrl Pts',(-1.64377905123609,-2.15429738715722,
8.80838212259897));
#401422=CARTESIAN_POINT('Ctrl Pts',(-1.66539749203245,-2.16424429481556,
8.78727029226991));
#401423=CARTESIAN_POINT('',(-1.67813633056179,-2.170105589426,8.75721825406948));
#401424=CARTESIAN_POINT('Origin',(-1.63980066194096,-2.15246710397329,8.75937679713085));
#401425=CARTESIAN_POINT('',(-1.67813633056179,-2.170105589426,7.51860402984325));
#401426=CARTESIAN_POINT('',(-1.67813633056179,-2.170105589426,7.5));
#401427=CARTESIAN_POINT('Ctrl Pts',(-1.67813633056179,-2.170105589426,7.51860402984325));
#401428=CARTESIAN_POINT('Ctrl Pts',(-1.66813195416114,-2.16550245411324,
7.52834476460825));
#401429=CARTESIAN_POINT('Ctrl Pts',(-1.6581210830637,-2.16089633051147,
7.53807742314407));
#401430=CARTESIAN_POINT('Ctrl Pts',(-1.64810349920137,-2.15628711828489,
7.54780169004674));
#401431=CARTESIAN_POINT('Ctrl Pts',(-1.63223618776764,-2.14898637522465,
7.5632044032688));
#401432=CARTESIAN_POINT('Ctrl Pts',(-1.61635201469678,-2.14167787391998,
7.57858609112103));
#401433=CARTESIAN_POINT('Ctrl Pts',(-1.60045004741996,-2.13436118528464,
7.59394543036555));
#401434=CARTESIAN_POINT('Origin',(-1.62988553581356,-2.41378875122106,7.5));
#401435=CARTESIAN_POINT('',(-1.60293438610525,-2.2262302592164,8.75721825406948));
#401436=CARTESIAN_POINT('',(-1.60093990236828,-2.21235024422326,8.78727029226991));
#401437=CARTESIAN_POINT('Origin',(-1.59587715873825,-2.17711758918138,8.75658640620972));
#401438=CARTESIAN_POINT('',(-1.59077126558566,-2.14158464790052,8.85049129520029));
#401439=CARTESIAN_POINT('Ctrl Pts',(-1.60093990236828,-2.21235024422326,
8.78727029226991));
#401440=CARTESIAN_POINT('Ctrl Pts',(-1.59755516454562,-2.18879517036853,
8.80838212259896));
#401441=CARTESIAN_POINT('Ctrl Pts',(-1.59416573821265,-2.16520746822394,
8.82945686509571));
#401442=CARTESIAN_POINT('Ctrl Pts',(-1.59077126558566,-2.14158464790052,
8.85049129520029));
#401443=CARTESIAN_POINT('',(-1.59077126558566,-2.14158464790052,7.59394543036555));
#401444=CARTESIAN_POINT('',(-1.59077126558566,-2.14158464790052,7.5));
#401445=CARTESIAN_POINT('',(-1.60293438610525,-2.2262302592164,7.51860402984325));
#401446=CARTESIAN_POINT('Ctrl Pts',(-1.59077126558566,-2.14158464790052,
7.59394543036555));
#401447=CARTESIAN_POINT('Ctrl Pts',(-1.59326099139908,-2.15891115248839,
7.57858609112103));
#401448=CARTESIAN_POINT('Ctrl Pts',(-1.59574793122424,-2.1762182688214,
7.56320440326857));
#401449=CARTESIAN_POINT('Ctrl Pts',(-1.59823223107081,-2.19350701301057,
7.54780169004651));
#401450=CARTESIAN_POINT('Ctrl Pts',(-1.59980065570003,-2.20442199665558,
7.53807742314383));
#401451=CARTESIAN_POINT('Ctrl Pts',(-1.60136802933076,-2.21532966618995,
7.52834476460825));
#401452=CARTESIAN_POINT('Ctrl Pts',(-1.60293438610525,-2.2262302592164,
7.51860402984325));
#401453=CARTESIAN_POINT('',(-1.60293438610525,-2.2262302592164,7.5));
#401454=CARTESIAN_POINT('Origin',(-1.59757636816867,-2.14060679114482,7.5));
#401455=CARTESIAN_POINT('Ctrl Pts',(-1.59077126558566,-2.14158464790052,
8.85049129520029));
#401456=CARTESIAN_POINT('Ctrl Pts',(-1.59074372039121,-2.14139295533119,
8.85097269580138));
#401457=CARTESIAN_POINT('Ctrl Pts',(-1.59072484862487,-2.14120248493199,
8.85143669361005));
#401458=CARTESIAN_POINT('Ctrl Pts',(-1.59071465132837,-2.14100437995467,
8.8519052845931));
#401459=CARTESIAN_POINT('Ctrl Pts',(-1.59069470606311,-2.14061689918241,
8.85282181883899));
#401460=CARTESIAN_POINT('Ctrl Pts',(-1.59070865627738,-2.1402101685317,
8.85372622499635));
#401461=CARTESIAN_POINT('Ctrl Pts',(-1.59077213055142,-2.13977833422801,
8.85462257735071));
#401462=CARTESIAN_POINT('Ctrl Pts',(-1.59082482463934,-2.13941984072639,
8.85536669723986));
#401463=CARTESIAN_POINT('Ctrl Pts',(-1.59091163012186,-2.13904396012349,
8.85610498449051));
#401464=CARTESIAN_POINT('Ctrl Pts',(-1.59104929334134,-2.13864911207127,
8.85681338218371));
#401465=CARTESIAN_POINT('Ctrl Pts',(-1.59117422292922,-2.13829078684376,
8.85745625420285));
#401466=CARTESIAN_POINT('Ctrl Pts',(-1.591342038854,-2.13791214894837,8.85808743050666));
#401467=CARTESIAN_POINT('Ctrl Pts',(-1.59158132695244,-2.13751236406794,
8.85866804508411));
#401468=CARTESIAN_POINT('Ctrl Pts',(-1.59169172929393,-2.1373279119904,
8.85893592806396));
#401469=CARTESIAN_POINT('Ctrl Pts',(-1.5918175872902,-2.13713898024247,
8.85919241173849));
#401470=CARTESIAN_POINT('Ctrl Pts',(-1.591963262365,-2.13694585159527,8.85943017985534));
#401471=CARTESIAN_POINT('Ctrl Pts',(-1.59215996684041,-2.13668507074933,
8.8597512372));
#401472=CARTESIAN_POINT('Ctrl Pts',(-1.59239832181035,-2.13641038588145,
8.86004599534706));
#401473=CARTESIAN_POINT('Ctrl Pts',(-1.59268332992239,-2.13613192320859,
8.86026130871721));
#401474=CARTESIAN_POINT('Ctrl Pts',(-1.59278767942744,-2.13602997017336,
8.86034014101235));
#401475=CARTESIAN_POINT('Ctrl Pts',(-1.59289984160947,-2.13592597046244,
8.86040910639692));
#401476=CARTESIAN_POINT('Ctrl Pts',(-1.59301698938381,-2.13582300415109,
8.86046313645506));
#401477=CARTESIAN_POINT('Ctrl Pts',(-1.59319979750456,-2.13566232608457,
8.86054744990829));
#401478=CARTESIAN_POINT('Ctrl Pts',(-1.59339983339585,-2.13549988890017,
8.86059655985669));
#401479=CARTESIAN_POINT('Ctrl Pts',(-1.59360408347319,-2.13534588276952,
8.86059725258816));
#401480=CARTESIAN_POINT('Ctrl Pts',(-1.59380880544979,-2.13519152082318,
8.86059794692011));
#401481=CARTESIAN_POINT('Ctrl Pts',(-1.59402163099506,-2.13504603837139,
8.86056369958366));
#401482=CARTESIAN_POINT('Ctrl Pts',(-1.59422882888188,-2.13491426346684,
8.86048590497774));
#401483=CARTESIAN_POINT('Ctrl Pts',(-1.59428290136132,-2.13487987414016,
8.86046560290182));
#401484=CARTESIAN_POINT('Ctrl Pts',(-1.59433734262766,-2.1348460474178,
8.86044257503091));
#401485=CARTESIAN_POINT('Ctrl Pts',(-1.59439045307624,-2.1348138006912,
8.86041778462583));
#401486=CARTESIAN_POINT('Ctrl Pts',(-1.59474782049063,-2.13459682023608,
8.86025097596201));
#401487=CARTESIAN_POINT('Ctrl Pts',(-1.59509305974973,-2.13442254377125,
8.8599848982295));
#401488=CARTESIAN_POINT('Ctrl Pts',(-1.59541227620413,-2.13428849451921,
8.85968173251462));
#401489=CARTESIAN_POINT('Ctrl Pts',(-1.59558112341958,-2.13421759014499,
8.85952137522077));
#401490=CARTESIAN_POINT('Ctrl Pts',(-1.59574587068148,-2.13415639775678,
8.85934740853961));
#401491=CARTESIAN_POINT('Ctrl Pts',(-1.59590365341084,-2.13410432302752,
8.8591675900182));
#401492=CARTESIAN_POINT('Ctrl Pts',(-1.59653723308305,-2.13389521592164,
8.85844552518695));
#401493=CARTESIAN_POINT('Ctrl Pts',(-1.59709337395832,-2.13381843388799,
8.85759444184124));
#401494=CARTESIAN_POINT('Ctrl Pts',(-1.59755244447825,-2.13379655894233,
8.85683498915138));
#401495=CARTESIAN_POINT('Ctrl Pts',(-1.59760048498555,-2.13379426978752,
8.85675551444998));
#401496=CARTESIAN_POINT('Ctrl Pts',(-1.59764745949611,-2.1337926016699,
8.85667699793651));
#401497=CARTESIAN_POINT('Ctrl Pts',(-1.59769334288919,-2.133791478738,8.85659965593547));
#401498=CARTESIAN_POINT('Ctrl Pts',(-1.59831267927036,-2.13377632134594,
8.85555568965886));
#401499=CARTESIAN_POINT('Ctrl Pts',(-1.59891008893109,-2.13385119858145,
8.85434650606346));
#401500=CARTESIAN_POINT('Ctrl Pts',(-1.59948929801393,-2.13401031410438,
8.85297329937117));
#401501=CARTESIAN_POINT('Ctrl Pts',(-1.59981506783129,-2.13409980689098,
8.85220095427747));
#401502=CARTESIAN_POINT('Ctrl Pts',(-1.60013512974126,-2.13421628782883,
8.85137579139183));
#401503=CARTESIAN_POINT('Ctrl Pts',(-1.60045004741996,-2.13436118528464,
8.85049129520029));
#401504=CARTESIAN_POINT('Origin',(-1.59757636816867,-2.14060679114482,7.59394543036555));
#401505=CARTESIAN_POINT('Ctrl Pts',(-1.59069129259387,-2.14102809970488,
7.59443877723642));
#401506=CARTESIAN_POINT('Ctrl Pts',(-1.58986764772642,-2.13529618878608,
7.58783886950016));
#401507=CARTESIAN_POINT('Ctrl Pts',(-1.59776381228678,-2.13217693137887,
7.58559994247159));
#401508=CARTESIAN_POINT('Ctrl Pts',(-1.5951875457606,-2.17231843324347,
7.56670252222137));
#401509=CARTESIAN_POINT('Ctrl Pts',(-1.59436509129382,-2.16659480656329,
7.56004874999029));
#401510=CARTESIAN_POINT('Ctrl Pts',(-1.60230019353943,-2.16343719518632,
7.55786368756705));
#401511=CARTESIAN_POINT('Ctrl Pts',(-1.59967540262376,-2.20355033521046,
7.53888913333558));
#401512=CARTESIAN_POINT('Ctrl Pts',(-1.59884806026982,-2.19779269273666,
7.53222002137279));
#401513=CARTESIAN_POINT('Ctrl Pts',(-1.60682710998053,-2.19464035861195,
7.53005029815326));
#401514=CARTESIAN_POINT('Ctrl Pts',(-1.6041546601048,-2.23472239234115,
7.51101258149734));
#401515=CARTESIAN_POINT('Ctrl Pts',(-1.6033172888582,-2.22889495677867,
7.5043616886572));
#401516=CARTESIAN_POINT('Ctrl Pts',(-1.61134441973222,-2.22578486811819,
7.50217374673251));
#401517=CARTESIAN_POINT('',(-1.6111033692641,-2.22412295723131,7.50366116523517));
#401518=CARTESIAN_POINT('Ctrl Pts',(-1.60293438610525,-2.2262302592164,
7.51860402984325));
#401519=CARTESIAN_POINT('Ctrl Pts',(-1.6029971981068,-2.22666738061629,
7.51734760759494));
#401520=CARTESIAN_POINT('Ctrl Pts',(-1.60311284964108,-2.2270539198544,
7.51608817408573));
#401521=CARTESIAN_POINT('Ctrl Pts',(-1.60329386799927,-2.22738516015517,
7.51481005913121));
#401522=CARTESIAN_POINT('Ctrl Pts',(-1.60345783875369,-2.22768520553485,
7.51365231206384));
#401523=CARTESIAN_POINT('Ctrl Pts',(-1.60367545569763,-2.22794042010745,
7.51247773061043));
#401524=CARTESIAN_POINT('Ctrl Pts',(-1.60397105069097,-2.22812242957886,
7.51129758471022));
#401525=CARTESIAN_POINT('Ctrl Pts',(-1.60433844150947,-2.22834864656557,
7.50983079813401));
#401526=CARTESIAN_POINT('Ctrl Pts',(-1.60482139396921,-2.2284434684628,
7.50839324291155));
#401527=CARTESIAN_POINT('Ctrl Pts',(-1.60543931562123,-2.22832669216941,
7.50715379678855));
#401528=CARTESIAN_POINT('Ctrl Pts',(-1.60572477761947,-2.2282727448867,
7.50658120839351));
#401529=CARTESIAN_POINT('Ctrl Pts',(-1.60607786096985,-2.22815663331509,
7.50598221009429));
#401530=CARTESIAN_POINT('Ctrl Pts',(-1.60648305695654,-2.22795951264466,
7.50545747549611));
#401531=CARTESIAN_POINT('Ctrl Pts',(-1.60669928207703,-2.22785432295346,
7.50517746087247));
#401532=CARTESIAN_POINT('Ctrl Pts',(-1.60693278013442,-2.22772510641312,
7.50491486231392));
#401533=CARTESIAN_POINT('Ctrl Pts',(-1.60717656005761,-2.22757382544985,
7.50468370960992));
#401534=CARTESIAN_POINT('Ctrl Pts',(-1.60754108793879,-2.22734761269087,
7.50433806340446));
#401535=CARTESIAN_POINT('Ctrl Pts',(-1.60793924302547,-2.22706480831741,
7.50405484070983));
#401536=CARTESIAN_POINT('Ctrl Pts',(-1.60834379546466,-2.22674387462097,
7.50385766036131));
#401537=CARTESIAN_POINT('Ctrl Pts',(-1.60838705605987,-2.22670955575058,
7.50383657498791));
#401538=CARTESIAN_POINT('Ctrl Pts',(-1.60843037964076,-2.22667482734914,
7.50381643264937));
#401539=CARTESIAN_POINT('Ctrl Pts',(-1.60847372582378,-2.22663973134263,
7.50379723213559));
#401540=CARTESIAN_POINT('Ctrl Pts',(-1.60876307577496,-2.22640545401846,
7.50366906242519));
#401541=CARTESIAN_POINT('Ctrl Pts',(-1.60905927443569,-2.22614914130103,
7.50358235568538));
#401542=CARTESIAN_POINT('Ctrl Pts',(-1.60933883482303,-2.22589522457715,
7.5035341175365));
#401543=CARTESIAN_POINT('Ctrl Pts',(-1.60975800398372,-2.22551450518751,
7.50346178989176));
#401544=CARTESIAN_POINT('Ctrl Pts',(-1.61019274686616,-2.22508711517259,
7.50346967198527));
#401545=CARTESIAN_POINT('Ctrl Pts',(-1.61060661966909,-2.22465441847368,
7.50354272648692));
#401546=CARTESIAN_POINT('Ctrl Pts',(-1.61077685411959,-2.22447644136512,
7.50357277531559));
#401547=CARTESIAN_POINT('Ctrl Pts',(-1.61094343395556,-2.22429790093189,
7.50361331098761));
#401548=CARTESIAN_POINT('Ctrl Pts',(-1.61110336926493,-2.22412295723246,
7.50366116523659));
#401549=CARTESIAN_POINT('',(-1.59932759105303,-2.14295327026985,7.57603338622103));
#401550=CARTESIAN_POINT('Origin',(-1.60461534358153,-2.15003360661828,7.58486873427627));
#401551=CARTESIAN_POINT('Ctrl Pts',(-1.61110336926699,-2.22412295728858,
7.50366116529968));
#401552=CARTESIAN_POINT('Ctrl Pts',(-1.6071853422593,-2.19711042569364,
7.52783573079709));
#401553=CARTESIAN_POINT('Ctrl Pts',(-1.6032602859228,-2.17005513827966,
7.55196141284069));
#401554=CARTESIAN_POINT('Ctrl Pts',(-1.5993275908755,-2.14295327150926,
7.57603338728831));
#401555=CARTESIAN_POINT('Ctrl Pts',(-1.59109156879725,-2.14257759370614,
7.59639677331371));
#401556=CARTESIAN_POINT('Ctrl Pts',(-1.58540951459622,-2.12430431578109,
7.59974925422226));
#401557=CARTESIAN_POINT('Ctrl Pts',(-1.60131081754378,-2.1349507701505,
7.59639677331372));
#401558=CARTESIAN_POINT('Ctrl Pts',(-1.58934971238339,-2.1390874589928,
7.58707626057422));
#401559=CARTESIAN_POINT('Ctrl Pts',(-1.5915727261035,-2.13256245772062,
7.58811717123965));
#401560=CARTESIAN_POINT('Ctrl Pts',(-1.598460543793,-2.13228786879498,7.58707626057424));
#401561=CARTESIAN_POINT('Ctrl Pts',(-1.59513737061506,-2.14093911891165,
7.58015376756929));
#401562=CARTESIAN_POINT('Ctrl Pts',(-1.59570649628635,-2.13810133317125,
7.58208760766041));
#401563=CARTESIAN_POINT('Ctrl Pts',(-1.59858892220314,-2.13836315901398,
7.5801537675693));
#401564=CARTESIAN_POINT('Ctrl Pts',(-1.59932759055789,-2.14295326960675,
7.57603338509286));
#401565=CARTESIAN_POINT('Ctrl Pts',(-1.59932759055789,-2.14295326960675,
7.57603338509286));
#401566=CARTESIAN_POINT('Ctrl Pts',(-1.59932759055789,-2.14295326960675,
7.57603338509286));
#401567=CARTESIAN_POINT('Origin',(-1.60461077043282,-2.15003701964728,7.58486873427622));
#401568=CARTESIAN_POINT('Ctrl Pts',(-1.68595489728115,-2.173703007108,7.51098857897448));
#401569=CARTESIAN_POINT('Ctrl Pts',(-1.68060655297096,-2.17124216881352,
7.50433767179956));
#401570=CARTESIAN_POINT('Ctrl Pts',(-1.67534106310677,-2.17805265099708,
7.50214974420965));
#401571=CARTESIAN_POINT('Ctrl Pts',(-1.65733749178295,-2.16053579062864,
7.53887321589163));
#401572=CARTESIAN_POINT('Ctrl Pts',(-1.65205323012919,-2.15810443754416,
7.5322040745206));
#401573=CARTESIAN_POINT('Ctrl Pts',(-1.64676090348176,-2.16485678517878,
7.53003438070911));
#401574=CARTESIAN_POINT('Ctrl Pts',(-1.62866513030972,-2.14734328823649,
7.56669465659233));
#401575=CARTESIAN_POINT('Ctrl Pts',(-1.6234120976599,-2.14492630399672,
7.56004085833299));
#401576=CARTESIAN_POINT('Ctrl Pts',(-1.61812721696367,-2.15163500626709,
7.55785582193789));
#401577=CARTESIAN_POINT('Ctrl Pts',(-1.59993910959754,-2.13412609657558,
7.59443891967696));
#401578=CARTESIAN_POINT('Ctrl Pts',(-1.5946784607044,-2.13170560800955,
7.58783901202978));
#401579=CARTESIAN_POINT('Ctrl Pts',(-1.58944145230864,-2.13838789212884,
7.58560008491213));
#401580=CARTESIAN_POINT('',(-1.67379182682863,-2.17733734542426,7.50366116523517));
#401581=CARTESIAN_POINT('Ctrl Pts',(-1.67379182682885,-2.17733734542456,
7.50366116523554));
#401582=CARTESIAN_POINT('Ctrl Pts',(-1.67447334484408,-2.1770061797384,
7.50350835821027));
#401583=CARTESIAN_POINT('Ctrl Pts',(-1.67508905117999,-2.17667958561864,
7.50345484956));
#401584=CARTESIAN_POINT('Ctrl Pts',(-1.6756575326789,-2.17634838364737,
7.50349758195598));
#401585=CARTESIAN_POINT('Ctrl Pts',(-1.67594920584753,-2.17617845247352,
7.50351950684424));
#401586=CARTESIAN_POINT('Ctrl Pts',(-1.6762572609532,-2.17599067105215,
7.50357029184312));
#401587=CARTESIAN_POINT('Ctrl Pts',(-1.67654933754676,-2.17580143016232,
7.50365515313923));
#401588=CARTESIAN_POINT('Ctrl Pts',(-1.67699866962114,-2.17551030104256,
7.50378570417639));
#401589=CARTESIAN_POINT('Ctrl Pts',(-1.6774235639605,-2.17520746333165,
7.50400001621911));
#401590=CARTESIAN_POINT('Ctrl Pts',(-1.67779036218066,-2.17491411851065,
7.50428903009635));
#401591=CARTESIAN_POINT('Ctrl Pts',(-1.67783107396112,-2.17488155949238,
7.50432110841318));
#401592=CARTESIAN_POINT('Ctrl Pts',(-1.67787110027762,-2.17484911527091,
7.50435406373354));
#401593=CARTESIAN_POINT('Ctrl Pts',(-1.67791041740552,-2.17481681294646,
7.50438785222352));
#401594=CARTESIAN_POINT('Ctrl Pts',(-1.67815046736962,-2.17461959172922,
7.50459414719561));
#401595=CARTESIAN_POINT('Ctrl Pts',(-1.67836757542204,-2.17442412152686,
7.50483629897752));
#401596=CARTESIAN_POINT('Ctrl Pts',(-1.67855430477747,-2.17423886878031,
7.5050991045531));
#401597=CARTESIAN_POINT('Ctrl Pts',(-1.67896624849071,-2.17383018261455,
7.50567888004914));
#401598=CARTESIAN_POINT('Ctrl Pts',(-1.67924694212404,-2.17345548835241,
7.50637912803144));
#401599=CARTESIAN_POINT('Ctrl Pts',(-1.67942510411654,-2.17312621707482,
7.50710440483569));
#401600=CARTESIAN_POINT('Ctrl Pts',(-1.67946879297412,-2.17304547322061,
7.50728225710685));
#401601=CARTESIAN_POINT('Ctrl Pts',(-1.67950731439499,-2.17296592286682,
7.50746498566954));
#401602=CARTESIAN_POINT('Ctrl Pts',(-1.67954014411056,-2.17288960453983,
7.50764697238949));
#401603=CARTESIAN_POINT('Ctrl Pts',(-1.67971662762648,-2.1724793382173,
7.50862528291182));
#401604=CARTESIAN_POINT('Ctrl Pts',(-1.67974845277418,-2.17212686491309,
7.50965856837423));
#401605=CARTESIAN_POINT('Ctrl Pts',(-1.67970082222061,-2.171820184291,7.51067959873204));
#401606=CARTESIAN_POINT('Ctrl Pts',(-1.6796746110669,-2.17165141755785,
7.5112414730258));
#401607=CARTESIAN_POINT('Ctrl Pts',(-1.67962390256754,-2.17149654377221,
7.51180065547253));
#401608=CARTESIAN_POINT('Ctrl Pts',(-1.67955689582721,-2.17135407760659,
7.51235175716501));
#401609=CARTESIAN_POINT('Ctrl Pts',(-1.67932536084707,-2.17086180025258,
7.51425603304536));
#401610=CARTESIAN_POINT('Ctrl Pts',(-1.6788661344512,-2.17046155339749,
7.5162690050518));
#401611=CARTESIAN_POINT('Ctrl Pts',(-1.67823955795078,-2.17015459940591,
7.51827788969243));
#401612=CARTESIAN_POINT('Ctrl Pts',(-1.67820564644651,-2.17013798647583,
7.51838661432545));
#401613=CARTESIAN_POINT('Ctrl Pts',(-1.67817123513467,-2.17012164944469,
7.51849533314856));
#401614=CARTESIAN_POINT('Ctrl Pts',(-1.67813633056179,-2.170105589426,7.51860402984325));
#401615=CARTESIAN_POINT('Ctrl Pts',(-1.59932759229263,-2.14295327045312,
7.57603338728985));
#401616=CARTESIAN_POINT('Ctrl Pts',(-1.62419032049749,-2.15443464751878,
7.55196141284921));
#401617=CARTESIAN_POINT('Ctrl Pts',(-1.64901056800952,-2.16589544849306,
7.52783573083104));
#401618=CARTESIAN_POINT('Ctrl Pts',(-1.67379182688441,-2.17733734544403,
7.50366116530176));
#401619=CARTESIAN_POINT('Origin',(-5.52641612598457E-16,-7.40489414195304E-16,
7.49482233047033));
#401620=CARTESIAN_POINT('Origin',(-1.6059181837037,-2.21696482544262,7.49482233047033));
#401621=CARTESIAN_POINT('Origin',(0.,0.,7.50366116523517));
#401622=CARTESIAN_POINT('Origin',(-1.66840488432875,-2.17032978875285,7.49482233047033));
#401623=CARTESIAN_POINT('Ctrl Pts',(-1.60293423561748,-2.22622921225624,
7.51860402984325));
#401624=CARTESIAN_POINT('Ctrl Pts',(-1.60401712365773,-2.23376072203332,
7.51860402984325));
#401625=CARTESIAN_POINT('Ctrl Pts',(-1.5978243100911,-2.23818173392643,
7.51860402984325));
#401626=CARTESIAN_POINT('Ctrl Pts',(-1.60333631807904,-2.22902571341501,
7.51041458714365));
#401627=CARTESIAN_POINT('Ctrl Pts',(-1.60254996944053,-2.23480810233128,
7.5100464290044));
#401628=CARTESIAN_POINT('Ctrl Pts',(-1.59782260218664,-2.23818295318902,
7.50729136483009));
#401629=CARTESIAN_POINT('Ctrl Pts',(-1.60608974108081,-2.22961086209062,
7.50215815450138));
#401630=CARTESIAN_POINT('Ctrl Pts',(-1.60553732340035,-2.2326756458004,
7.49877163671532));
#401631=CARTESIAN_POINT('Ctrl Pts',(-1.60274318276032,-2.23469967684713,
7.49481588533172));
#401632=CARTESIAN_POINT('Ctrl Pts',(-1.61110304631036,-2.22412251139392,
7.50366171572174));
#401633=CARTESIAN_POINT('Ctrl Pts',(-1.61325114344695,-2.22708795249921,
7.50000045605858));
#401634=CARTESIAN_POINT('Ctrl Pts',(-1.61325114344685,-2.22708795249928,
7.49482233047317));
#401635=CARTESIAN_POINT('Origin',(-1.59056147231796,-2.2280081805904,7.51860402984325));
#401636=CARTESIAN_POINT('Origin',(-1.59056147231796,-2.2280081805904,9.));
#401637=CARTESIAN_POINT('Origin',(-1.59056147231796,-2.2280081805904,8.75721825406948));
#401638=CARTESIAN_POINT('Ctrl Pts',(-1.60055903033135,-2.20969989122327,
8.78942910404913));
#401639=CARTESIAN_POINT('Ctrl Pts',(-1.60137162134954,-2.21521279649535,
8.79672699501692));
#401640=CARTESIAN_POINT('Ctrl Pts',(-1.59293023317501,-2.21811390863887,
8.79893251111267));
#401641=CARTESIAN_POINT('Ctrl Pts',(-1.6021227999773,-2.22058244805677,
8.78111911759578));
#401642=CARTESIAN_POINT('Ctrl Pts',(-1.60307877177671,-2.22711914661524,
8.7864446589481));
#401643=CARTESIAN_POINT('Ctrl Pts',(-1.59615583745414,-2.23133678720458,
8.78817647674132));
#401644=CARTESIAN_POINT('Ctrl Pts',(-1.60309737848858,-2.22736471705345,
8.76780923932033));
#401645=CARTESIAN_POINT('Ctrl Pts',(-1.60422082067881,-2.23508175109612,
8.76988516158376));
#401646=CARTESIAN_POINT('Ctrl Pts',(-1.59815964019984,-2.23959821781224,
8.77093053738833));
#401647=CARTESIAN_POINT('Ctrl Pts',(-1.60290734901521,-2.22604226742122,
8.75371302330491));
#401648=CARTESIAN_POINT('Ctrl Pts',(-1.60400397276686,-2.23356979143083,
8.75300828287559));
#401649=CARTESIAN_POINT('Ctrl Pts',(-1.59776837262215,-2.23798701116384,
8.75267964240738));
#401650=CARTESIAN_POINT('Origin',(-1.58856698858099,-2.21412816559725,8.78727029226991));
#401651=CARTESIAN_POINT('Ctrl Pts',(-1.59077126558566,-2.14158464790052,
8.85049129520029));
#401652=CARTESIAN_POINT('Ctrl Pts',(-1.59160185579969,-2.14736489288836,
8.85711686593484));
#401653=CARTESIAN_POINT('Ctrl Pts',(-1.58363955683346,-2.15047978570934,
8.85933012996512));
#401654=CARTESIAN_POINT('Ctrl Pts',(-1.59416574276816,-2.16520749992665,
8.82945683644722));
#401655=CARTESIAN_POINT('Ctrl Pts',(-1.59500322738315,-2.17103572444268,
8.83607469902388));
#401656=CARTESIAN_POINT('Ctrl Pts',(-1.58700388846102,-2.17412483747175,
8.8382956714852));
#401657=CARTESIAN_POINT('Ctrl Pts',(-1.59755516020868,-2.18879514018687,
8.80838214965003));
#401658=CARTESIAN_POINT('Ctrl Pts',(-1.59839594992901,-2.19464636559806,
8.81501364461995));
#401659=CARTESIAN_POINT('Ctrl Pts',(-1.59036377844286,-2.19773392674116,
8.81722098428721));
#401660=CARTESIAN_POINT('Ctrl Pts',(-1.60093990236828,-2.21235024422326,
8.78727029226991));
#401661=CARTESIAN_POINT('Ctrl Pts',(-1.60178083174652,-2.21820244154215,
8.79393457792714));
#401662=CARTESIAN_POINT('Ctrl Pts',(-1.59371958050514,-2.2213097946926,
8.79610912703474));
#401663=CARTESIAN_POINT('Origin',(-1.57839835179836,-2.14336256927451,8.85049129520029));
#401664=CARTESIAN_POINT('Ctrl Pts',(-1.60045004741996,-2.13436118528464,
8.85049129520029));
#401665=CARTESIAN_POINT('Ctrl Pts',(-1.6057550566434,-2.1368020845784,8.85711686593484));
#401666=CARTESIAN_POINT('Ctrl Pts',(-1.61100669796542,-2.13005515746017,
8.85933012996512));
#401667=CARTESIAN_POINT('Ctrl Pts',(-1.5957567823386,-2.1322017569142,8.86332496987232));
#401668=CARTESIAN_POINT('Ctrl Pts',(-1.59962188022982,-2.12966938398194,
8.86648636486737));
#401669=CARTESIAN_POINT('Ctrl Pts',(-1.59786993626268,-2.12402963272601,
8.87206031107457));
#401670=CARTESIAN_POINT('Ctrl Pts',(-1.59003146113943,-2.1364361993996,
8.86341338519876));
#401671=CARTESIAN_POINT('Ctrl Pts',(-1.58647494928258,-2.13940683805928,
8.86654584966058));
#401672=CARTESIAN_POINT('Ctrl Pts',(-1.58158264810685,-2.13606176078165,
8.87215952290714));
#401673=CARTESIAN_POINT('Ctrl Pts',(-1.59077126558566,-2.14158464790052,
8.85049129520029));
#401674=CARTESIAN_POINT('Ctrl Pts',(-1.59160185579969,-2.14736489288836,
8.85711686593484));
#401675=CARTESIAN_POINT('Ctrl Pts',(-1.58363955683346,-2.15047978570933,
8.85933012996512));
#401676=CARTESIAN_POINT('Origin',(-1.60567491878593,-2.12300553826612,8.85049129520029));
#401677=CARTESIAN_POINT('Ctrl Pts',(-1.66539749203245,-2.16424429481556,
8.78727029226991));
#401678=CARTESIAN_POINT('Ctrl Pts',(-1.67076853786518,-2.16671557835678,
8.79393457792714));
#401679=CARTESIAN_POINT('Ctrl Pts',(-1.67604110579949,-2.15987164362913,
8.79610912703474));
#401680=CARTESIAN_POINT('Ctrl Pts',(-1.64377902353589,-2.15429737441203,
8.80838214965003));
#401681=CARTESIAN_POINT('Ctrl Pts',(-1.64914917736846,-2.15676824753314,
8.81501364461995));
#401682=CARTESIAN_POINT('Ctrl Pts',(-1.65439449734899,-2.14994655925992,
8.81722098428721));
#401683=CARTESIAN_POINT('Ctrl Pts',(-1.62213069385384,-2.1443367145137,
8.82945683644723));
#401684=CARTESIAN_POINT('Ctrl Pts',(-1.62747973786129,-2.1467978747474,
8.83607469902389));
#401685=CARTESIAN_POINT('Ctrl Pts',(-1.63271720381481,-2.14000810355221,
8.83829567148519));
#401686=CARTESIAN_POINT('Ctrl Pts',(-1.60045004741996,-2.13436118528464,
8.85049129520029));
#401687=CARTESIAN_POINT('Ctrl Pts',(-1.6057550566434,-2.1368020845784,8.85711686593484));
#401688=CARTESIAN_POINT('Ctrl Pts',(-1.61100669796542,-2.13005515746017,
8.85933012996512));
#401689=CARTESIAN_POINT('Origin',(-1.67062236339842,-2.15288864779705,8.78727029226991));
#401690=CARTESIAN_POINT('Ctrl Pts',(-1.67796812831785,-2.17002817722086,
8.75374538247848));
#401691=CARTESIAN_POINT('Ctrl Pts',(-1.68486593258896,-2.1732163859068,
8.75304829418601));
#401692=CARTESIAN_POINT('Ctrl Pts',(-1.69087189191038,-2.16850479426081,
8.75272238421917));
#401693=CARTESIAN_POINT('Ctrl Pts',(-1.6791672696383,-2.17057991720282,
8.7676940844502));
#401694=CARTESIAN_POINT('Ctrl Pts',(-1.68623894281032,-2.17384772893549,
8.7697431809397));
#401695=CARTESIAN_POINT('Ctrl Pts',(-1.69228901876997,-2.16932943963944,
8.7707786988043));
#401696=CARTESIAN_POINT('Ctrl Pts',(-1.67302115432925,-2.1677520123743,
8.78108014887988));
#401697=CARTESIAN_POINT('Ctrl Pts',(-1.67901254883375,-2.17052481406068,
8.78639403366324));
#401698=CARTESIAN_POINT('Ctrl Pts',(-1.68503003222547,-2.16511076110939,
8.78812224174741));
#401699=CARTESIAN_POINT('Ctrl Pts',(-1.66294902812128,-2.16311770059481,
8.78944554828685));
#401700=CARTESIAN_POINT('Ctrl Pts',(-1.66799600222725,-2.16545959512503,
8.79673892988686));
#401701=CARTESIAN_POINT('Ctrl Pts',(-1.67317559700402,-2.15820181638322,
8.79894799272499));
#401702=CARTESIAN_POINT('Origin',(-1.68336120192776,-2.15874994240749,8.75721825406948));
#401703=CARTESIAN_POINT('Origin',(-1.68336120192776,-2.15874994240749,9.));
#401704=CARTESIAN_POINT('Origin',(-1.68336120192776,-2.15874994240749,7.51860402984325));
#401705=CARTESIAN_POINT('Ctrl Pts',(-1.67379134738624,-2.17733672174576,
7.50366195182966));
#401706=CARTESIAN_POINT('Ctrl Pts',(-1.67602317147191,-2.18023997043657,
7.50000065167735));
#401707=CARTESIAN_POINT('Ctrl Pts',(-1.676023171472,-2.1802399704365,7.49482233047108));
#401708=CARTESIAN_POINT('Ctrl Pts',(-1.68048485024188,-2.17408851930009,
7.50215800491337));
#401709=CARTESIAN_POINT('Ctrl Pts',(-1.6835813448413,-2.17442972066326,
7.49877273257265));
#401710=CARTESIAN_POINT('Ctrl Pts',(-1.68631825291818,-2.17232579801055,
7.49481816995647));
#401711=CARTESIAN_POINT('Ctrl Pts',(-1.6806967376156,-2.17128403715842,
7.51043025814042));
#401712=CARTESIAN_POINT('Ctrl Pts',(-1.68646654642247,-2.17217961703705,
7.51006209594514));
#401713=CARTESIAN_POINT('Ctrl Pts',(-1.69104977934849,-2.1686056911693,
7.50731281821699));
#401714=CARTESIAN_POINT('Ctrl Pts',(-1.67813495755924,-2.17010495759023,
7.51860402984325));
#401715=CARTESIAN_POINT('Ctrl Pts',(-1.68504722930857,-2.17328639070347,
7.51860402984324));
#401716=CARTESIAN_POINT('Ctrl Pts',(-1.69104778275849,-2.16860724808058,
7.51860402984325));
#401717=CARTESIAN_POINT('Origin',(0.,0.,7.5));
#401718=CARTESIAN_POINT('Origin',(-1.46041276049032,-2.23251709792629,7.5));
#401719=CARTESIAN_POINT('',(-1.46041276049032,-2.23251709792629,7.59394543036555));
#401720=CARTESIAN_POINT('',(-1.46041276049032,-2.23251709792629,8.85049129520029));
#401721=CARTESIAN_POINT('',(-1.46041276049032,-2.23251709792629,7.5));
#401722=CARTESIAN_POINT('',(-1.52331214621091,-2.26650000646724,8.78727029226991));
#401723=CARTESIAN_POINT('Ctrl Pts',(-1.46041276049032,-2.23251709792629,
8.85049129520029));
#401724=CARTESIAN_POINT('Ctrl Pts',(-1.48140969918006,-2.24386119992282,
8.82945686509571));
#401725=CARTESIAN_POINT('Ctrl Pts',(-1.50237542338152,-2.25518843754002,
8.80838212259896));
#401726=CARTESIAN_POINT('Ctrl Pts',(-1.52331214621091,-2.26650000646724,
8.78727029226991));
#401727=CARTESIAN_POINT('',(-1.5356492769952,-2.27316543860615,8.75721825406948));
#401728=CARTESIAN_POINT('Origin',(-1.49852247476105,-2.25310701859239,8.75937679713122));
#401729=CARTESIAN_POINT('',(-1.5356492769952,-2.27316543860615,7.51860402984325));
#401730=CARTESIAN_POINT('',(-1.5356492769952,-2.27316543860615,7.5));
#401731=CARTESIAN_POINT('Ctrl Pts',(-1.5356492769952,-2.27316543860615,
7.51860402984325));
#401732=CARTESIAN_POINT('Ctrl Pts',(-1.52596037955092,-2.26793077833182,
7.52834476460825));
#401733=CARTESIAN_POINT('Ctrl Pts',(-1.51626519221423,-2.26269271979158,
7.53807742314407));
#401734=CARTESIAN_POINT('Ctrl Pts',(-1.50656350379362,-2.25745114888412,
7.54780169004674));
#401735=CARTESIAN_POINT('Ctrl Pts',(-1.49119655366689,-2.24914878384944,
7.5632044032688));
#401736=CARTESIAN_POINT('Ctrl Pts',(-1.4758132736195,-2.24083759618167,
7.57858609112103));
#401737=CARTESIAN_POINT('Ctrl Pts',(-1.46041276049032,-2.23251709792629,
7.59394543036555));
#401738=CARTESIAN_POINT('Origin',(-1.47188478489785,-2.5132564881766,7.5));
#401739=CARTESIAN_POINT('',(-1.45700592305911,-2.32435658911881,8.75721825406948));
#401740=CARTESIAN_POINT('',(-1.45590483281683,-2.31037730509332,8.78727029226991));
#401741=CARTESIAN_POINT('Origin',(-1.45310985509581,-2.27489266822439,8.75658640621072));
#401742=CARTESIAN_POINT('',(-1.45029105591253,-2.23910559748224,8.85049129520029));
#401743=CARTESIAN_POINT('Ctrl Pts',(-1.45590483281683,-2.31037730509332,
8.78727029226991));
#401744=CARTESIAN_POINT('Ctrl Pts',(-1.45403622806458,-2.28665376676723,
8.80838212259897));
#401745=CARTESIAN_POINT('Ctrl Pts',(-1.45216503493676,-2.2628973667957,
8.82945686509571));
#401746=CARTESIAN_POINT('Ctrl Pts',(-1.45029105591253,-2.23910559748224,
8.85049129520029));
#401747=CARTESIAN_POINT('',(-1.45029105591253,-2.23910559748224,7.59394543036555));
#401748=CARTESIAN_POINT('',(-1.45029105591253,-2.23910559748224,7.5));
#401749=CARTESIAN_POINT('',(-1.45700592305911,-2.32435658911881,7.51860402984325));
#401750=CARTESIAN_POINT('Ctrl Pts',(-1.45029105591253,-2.23910559748224,
7.59394543036555));
#401751=CARTESIAN_POINT('Ctrl Pts',(-1.4516655533568,-2.25655602018874,
7.57858609112103));
#401752=CARTESIAN_POINT('Ctrl Pts',(-1.45303851274667,-2.27398691597673,
7.56320440326857));
#401753=CARTESIAN_POINT('Ctrl Pts',(-1.45441001468938,-2.29139930822442,
7.54780169004651));
#401754=CARTESIAN_POINT('Ctrl Pts',(-1.45527589141876,-2.30239235517593,
7.53807742314383));
#401755=CARTESIAN_POINT('Ctrl Pts',(-1.45614118792573,-2.3133780357067,
7.52834476460825));
#401756=CARTESIAN_POINT('Ctrl Pts',(-1.45700592305911,-2.32435658911881,
7.51860402984325));
#401757=CARTESIAN_POINT('',(-1.45700592305911,-2.32435658911881,7.5));
#401758=CARTESIAN_POINT('Origin',(-1.45714482817989,-2.23856575425761,7.5));
#401759=CARTESIAN_POINT('Ctrl Pts',(-1.45029105591253,-2.23910559748224,
8.85049129520029));
#401760=CARTESIAN_POINT('Ctrl Pts',(-1.45027584909771,-2.23891253393919,
8.85097269580139));
#401761=CARTESIAN_POINT('Ctrl Pts',(-1.45026921958582,-2.23872124576363,
8.85143669361005));
#401762=CARTESIAN_POINT('Ctrl Pts',(-1.45027173587024,-2.23852289447121,
8.8519052845931));
#401763=CARTESIAN_POINT('Ctrl Pts',(-1.45027665756298,-2.23813493192222,
8.852821818839));
#401764=CARTESIAN_POINT('Ctrl Pts',(-1.45031663843731,-2.23772993073654,
8.85372622499636));
#401765=CARTESIAN_POINT('Ctrl Pts',(-1.45040765001548,-2.23730305049344,
8.85462257735071));
#401766=CARTESIAN_POINT('Ctrl Pts',(-1.45048320459525,-2.23694866967697,
8.85536669723987));
#401767=CARTESIAN_POINT('Ctrl Pts',(-1.45059391447951,-2.23657912300745,
8.85610498449051));
#401768=CARTESIAN_POINT('Ctrl Pts',(-1.4507565928567,-2.23619390632566,
8.85681338218371));
#401769=CARTESIAN_POINT('Ctrl Pts',(-1.4509042237395,-2.23584432158194,
8.85745625420285));
#401770=CARTESIAN_POINT('Ctrl Pts',(-1.45109595428171,-2.23547721364192,
8.85808743050666));
#401771=CARTESIAN_POINT('Ctrl Pts',(-1.45136036504233,-2.23509358140352,
8.85866804508411));
#401772=CARTESIAN_POINT('Ctrl Pts',(-1.45148235843555,-2.23491658180486,
8.85893592806396));
#401773=CARTESIAN_POINT('Ctrl Pts',(-1.45162006274172,-2.23473610198698,
8.85919241173849));
#401774=CARTESIAN_POINT('Ctrl Pts',(-1.45177781230636,-2.23455270357738,
8.85943017985534));
#401775=CARTESIAN_POINT('Ctrl Pts',(-1.4519908209175,-2.23430506143267,
8.8597512372));
#401776=CARTESIAN_POINT('Ctrl Pts',(-1.4522462852815,-2.23404621238967,
8.86004599534706));
#401777=CARTESIAN_POINT('Ctrl Pts',(-1.45254854897852,-2.23378658238067,
8.86026130871721));
#401778=CARTESIAN_POINT('Ctrl Pts',(-1.45265921623971,-2.23369152451463,
8.86034014101236));
#401779=CARTESIAN_POINT('Ctrl Pts',(-1.45277781125687,-2.23359492473794,
8.86040910639692));
#401780=CARTESIAN_POINT('Ctrl Pts',(-1.45290131541276,-2.2334996756656,
8.86046313645506));
#401781=CARTESIAN_POINT('Ctrl Pts',(-1.45309404261369,-2.23335104028591,
8.86054744990829));
#401782=CARTESIAN_POINT('Ctrl Pts',(-1.45330407489592,-2.23320175318968,
8.86059655985668));
#401783=CARTESIAN_POINT('Ctrl Pts',(-1.45351777252623,-2.23306114982853,
8.86059725258816));
#401784=CARTESIAN_POINT('Ctrl Pts',(-1.45373196388344,-2.23292022161744,
8.86059794692011));
#401785=CARTESIAN_POINT('Ctrl Pts',(-1.45395367324849,-2.23278867385446,
8.86056369958366));
#401786=CARTESIAN_POINT('Ctrl Pts',(-1.45416888827215,-2.23267044490976,
8.86048590497774));
#401787=CARTESIAN_POINT('Ctrl Pts',(-1.45422505298561,-2.2326395906753,
8.86046560290182));
#401788=CARTESIAN_POINT('Ctrl Pts',(-1.45428154968207,-2.23260932151747,
8.86044257503091));
#401789=CARTESIAN_POINT('Ctrl Pts',(-1.45433661706441,-2.23258054384336,
8.86041778462583));
#401790=CARTESIAN_POINT('Ctrl Pts',(-1.45470715221461,-2.23238690580671,
8.86025097596201));
#401791=CARTESIAN_POINT('Ctrl Pts',(-1.45506284807406,-2.23223510696685,
8.8599848982295));
#401792=CARTESIAN_POINT('Ctrl Pts',(-1.45538999722908,-2.23212178540182,
8.85968173251461));
#401793=CARTESIAN_POINT('Ctrl Pts',(-1.45556304038868,-2.23206184478648,
8.85952137522076));
#401794=CARTESIAN_POINT('Ctrl Pts',(-1.45573136976944,-2.23201133351791,
8.85934740853961));
#401795=CARTESIAN_POINT('Ctrl Pts',(-1.45589216475661,-2.23196947495595,
8.8591675900182));
#401796=CARTESIAN_POINT('Ctrl Pts',(-1.4565378402097,-2.23180139107202,
8.85844552518696));
#401797=CARTESIAN_POINT('Ctrl Pts',(-1.45709775787568,-2.2317603988635,
8.85759444184126));
#401798=CARTESIAN_POINT('Ctrl Pts',(-1.45755728671856,-2.23176798161146,
8.85683498915141));
#401799=CARTESIAN_POINT('Ctrl Pts',(-1.45760537518815,-2.23176877512584,
8.85675551445));
#401800=CARTESIAN_POINT('Ctrl Pts',(-1.45765236006121,-2.23177012010277,
8.85667699793652));
#401801=CARTESIAN_POINT('Ctrl Pts',(-1.45769822112844,-2.23177193923715,
8.85659965593547));
#401802=CARTESIAN_POINT('Ctrl Pts',(-1.45831725615403,-2.23179649400576,
8.85555568965886));
#401803=CARTESIAN_POINT('Ctrl Pts',(-1.45890864097159,-2.23190949356633,
8.85434650606346));
#401804=CARTESIAN_POINT('Ctrl Pts',(-1.45947646544069,-2.23210539222271,
8.85297329937117));
#401805=CARTESIAN_POINT('Ctrl Pts',(-1.4597958321065,-2.23221557328064,
8.85220095427747));
#401806=CARTESIAN_POINT('Ctrl Pts',(-1.46010777345564,-2.23235232133289,
8.85137579139183));
#401807=CARTESIAN_POINT('Ctrl Pts',(-1.46041276049032,-2.23251709792629,
8.85049129520029));
#401808=CARTESIAN_POINT('Origin',(-1.45714482817989,-2.23856575425761,7.59394543036555));
#401809=CARTESIAN_POINT('Ctrl Pts',(-1.45024690539915,-2.23854506888738,
7.59443877723642));
#401810=CARTESIAN_POINT('Ctrl Pts',(-1.44979219759189,-2.23277216368647,
7.58783886950015));
#401811=CARTESIAN_POINT('Ctrl Pts',(-1.45787199014355,-2.23016522412853,
7.58559994247159));
#401812=CARTESIAN_POINT('Ctrl Pts',(-1.45272914197844,-2.27005918900933,
7.56670252222136));
#401813=CARTESIAN_POINT('Ctrl Pts',(-1.45227509135304,-2.26429462729539,
7.56004874999029));
#401814=CARTESIAN_POINT('Ctrl Pts',(-1.46039619893562,-2.26165190731611,
7.55786368756704));
#401815=CARTESIAN_POINT('Ctrl Pts',(-1.45520674322891,-2.30151445966057,
7.53888913333559));
#401816=CARTESIAN_POINT('Ctrl Pts',(-1.45474999415843,-2.29571563887414,
7.53222002137278));
#401817=CARTESIAN_POINT('Ctrl Pts',(-1.4629146207966,-2.29308100102817,
7.53005029815327));
#401818=CARTESIAN_POINT('Ctrl Pts',(-1.45767959703745,-2.33290945746886,
7.51101258149734));
#401819=CARTESIAN_POINT('Ctrl Pts',(-1.45721731133829,-2.32704034443776,
7.5043616886572));
#401820=CARTESIAN_POINT('Ctrl Pts',(-1.46542721367566,-2.3244509458289,
7.50217374673251));
#401821=CARTESIAN_POINT('',(-1.46529313746768,-2.32277700535966,7.50366116523517));
#401822=CARTESIAN_POINT('Ctrl Pts',(-1.45700592305911,-2.32435658911881,
7.51860402984325));
#401823=CARTESIAN_POINT('Ctrl Pts',(-1.45704059954241,-2.32479683678466,
7.51734760759493));
#401824=CARTESIAN_POINT('Ctrl Pts',(-1.45713124780419,-2.32518999165569,
7.51608817408572));
#401825=CARTESIAN_POINT('Ctrl Pts',(-1.45729067160182,-2.32553214927377,
7.51481005913119));
#401826=CARTESIAN_POINT('Ctrl Pts',(-1.45743508148726,-2.32584208382034,
7.51365231206383));
#401827=CARTESIAN_POINT('Ctrl Pts',(-1.45763589966004,-2.32611071679269,
7.51247773061042));
#401828=CARTESIAN_POINT('Ctrl Pts',(-1.45791922593489,-2.32631129114238,
7.51129758471022));
#401829=CARTESIAN_POINT('Ctrl Pts',(-1.45827136813745,-2.32656058215258,
7.50983079813402));
#401830=CARTESIAN_POINT('Ctrl Pts',(-1.45874725305975,-2.32668615209839,
7.50839324291155));
#401831=CARTESIAN_POINT('Ctrl Pts',(-1.45937138700827,-2.3266092061106,
7.50715379678855));
#401832=CARTESIAN_POINT('Ctrl Pts',(-1.4596597189085,-2.32657365928139,
7.50658120839351));
#401833=CARTESIAN_POINT('Ctrl Pts',(-1.4600195161052,-2.32648040840138,
7.50598221009429));
#401834=CARTESIAN_POINT('Ctrl Pts',(-1.46043650913799,-2.32630965373252,
7.50545747549611));
#401835=CARTESIAN_POINT('Ctrl Pts',(-1.46065902952744,-2.32621853375586,
7.50517746087247));
#401836=CARTESIAN_POINT('Ctrl Pts',(-1.46090032677019,-2.32610454297666,
7.50491486231392));
#401837=CARTESIAN_POINT('Ctrl Pts',(-1.46115329842597,-2.32596919186965,
7.50468370960992));
#401838=CARTESIAN_POINT('Ctrl Pts',(-1.46153157084676,-2.32576679927059,
7.50433806340446));
#401839=CARTESIAN_POINT('Ctrl Pts',(-1.46194702721954,-2.32551008583303,
7.50405484070983));
#401840=CARTESIAN_POINT('Ctrl Pts',(-1.46237131075489,-2.32521573129307,
7.5038576603613));
#401841=CARTESIAN_POINT('Ctrl Pts',(-1.46241668128413,-2.32518425465033,
7.50383657498791));
#401842=CARTESIAN_POINT('Ctrl Pts',(-1.46246214090839,-2.32515237335347,
7.50381643264937));
#401843=CARTESIAN_POINT('Ctrl Pts',(-1.46250764664089,-2.32512012665495,
7.50379723213559));
#401844=CARTESIAN_POINT('Ctrl Pts',(-1.46281141229126,-2.32490486939369,
7.50366906242519));
#401845=CARTESIAN_POINT('Ctrl Pts',(-1.46312342439227,-2.32466806081158,
7.50358235568538));
#401846=CARTESIAN_POINT('Ctrl Pts',(-1.46341867889316,-2.32443257728236,
7.5035341175365));
#401847=CARTESIAN_POINT('Ctrl Pts',(-1.4638613796009,-2.32407949638187,
7.50346178989176));
#401848=CARTESIAN_POINT('Ctrl Pts',(-1.46432261222973,-2.32368083855769,
7.50346967198527));
#401849=CARTESIAN_POINT('Ctrl Pts',(-1.46476335765928,-2.32327554780208,
7.50354272648692));
#401850=CARTESIAN_POINT('Ctrl Pts',(-1.46494464537735,-2.32310884332527,
7.50357277531559));
#401851=CARTESIAN_POINT('Ctrl Pts',(-1.46512232208201,-2.32294134252925,
7.50361331098761));
#401852=CARTESIAN_POINT('Ctrl Pts',(-1.46529313746844,-2.32277700536086,
7.50366116523658));
#401853=CARTESIAN_POINT('',(-1.45874211355529,-2.24101961352506,7.57603338622103));
#401854=CARTESIAN_POINT('Origin',(-1.46356536312152,-2.24842419003061,7.58486873427627));
#401855=CARTESIAN_POINT('Ctrl Pts',(-1.4652931374669,-2.322777005417,7.50366116529969));
#401856=CARTESIAN_POINT('Ctrl Pts',(-1.46311385930744,-2.29556894511303,
7.52783573079709));
#401857=CARTESIAN_POINT('Ctrl Pts',(-1.4609303056364,-2.26831776646579,
7.55196141284068));
#401858=CARTESIAN_POINT('Ctrl Pts',(-1.45874211329872,-2.24101961475054,
7.57603338728831));
#401859=CARTESIAN_POINT('Ctrl Pts',(-1.45054708277062,-2.24011702507145,
7.59639677331371));
#401860=CARTESIAN_POINT('Ctrl Pts',(-1.44624938057004,-2.22235184363283,
7.59959882295467));
#401861=CARTESIAN_POINT('Ctrl Pts',(-1.461088648627,-2.2330525415605,7.59642833564546));
#401862=CARTESIAN_POINT('Ctrl Pts',(-1.44903241888642,-2.23652246009058,
7.58707626057422));
#401863=CARTESIAN_POINT('Ctrl Pts',(-1.45162401029285,-2.23026179359102,
7.58809943920599));
#401864=CARTESIAN_POINT('Ctrl Pts',(-1.4583850215227,-2.23031772160695,
7.58710240504252));
#401865=CARTESIAN_POINT('Ctrl Pts',(-1.4546895494952,-2.2387411321116,7.58015376756929));
#401866=CARTESIAN_POINT('Ctrl Pts',(-1.45542815686251,-2.23598727471642,
7.5820588065976));
#401867=CARTESIAN_POINT('Ctrl Pts',(-1.45821623385673,-2.2363793228159,
7.58020924244127));
#401868=CARTESIAN_POINT('Ctrl Pts',(-1.45874211310365,-2.24101961283159,
7.57603338509286));
#401869=CARTESIAN_POINT('Ctrl Pts',(-1.45874211310365,-2.24101961283159,
7.57603338509286));
#401870=CARTESIAN_POINT('Ctrl Pts',(-1.45874211310365,-2.24101961283159,
7.57603338509286));
#401871=CARTESIAN_POINT('Origin',(-1.46356058069554,-2.24842730304479,7.58486873427621));
#401872=CARTESIAN_POINT('Ctrl Pts',(-1.54322129228844,-2.27725640229734,
7.51098857897448));
#401873=CARTESIAN_POINT('Ctrl Pts',(-1.53804160317611,-2.27445795046258,
7.50433767179956));
#401874=CARTESIAN_POINT('Ctrl Pts',(-1.53235058273389,-2.28091707868616,
7.50214974420965));
#401875=CARTESIAN_POINT('Ctrl Pts',(-1.51550631077548,-2.26228271581091,
7.53887321589173));
#401876=CARTESIAN_POINT('Ctrl Pts',(-1.51038868353099,-2.25951779439551,
7.53220407452067));
#401877=CARTESIAN_POINT('Ctrl Pts',(-1.50467460613786,-2.26591718807517,
7.53003438070911));
#401878=CARTESIAN_POINT('Ctrl Pts',(-1.48773810627429,-2.24728027432282,
7.56669465659231));
#401879=CARTESIAN_POINT('Ctrl Pts',(-1.48265072325536,-2.24453169307891,
7.56004085833298));
#401880=CARTESIAN_POINT('Ctrl Pts',(-1.4769468728831,-2.25088800813222,
7.55785582193789));
#401881=CARTESIAN_POINT('Ctrl Pts',(-1.45991793462976,-2.23224975633352,
7.59443891967696));
#401882=CARTESIAN_POINT('Ctrl Pts',(-1.45482317553887,-2.22949718998902,
7.58783901202978));
#401883=CARTESIAN_POINT('Ctrl Pts',(-1.44916879172502,-2.23583020835896,
7.58560008491213));
#401884=CARTESIAN_POINT('',(-1.53085035931324,-2.28010398287622,7.50366116523517));
#401885=CARTESIAN_POINT('Ctrl Pts',(-1.53085035931345,-2.28010398287653,
7.50366116523554));
#401886=CARTESIAN_POINT('Ctrl Pts',(-1.53155169493518,-2.27981716261495,
7.50350835821027));
#401887=CARTESIAN_POINT('Ctrl Pts',(-1.53218706119349,-2.27953068795822,
7.50345484955999));
#401888=CARTESIAN_POINT('Ctrl Pts',(-1.53277559486935,-2.27923658921161,
7.50349758195598));
#401889=CARTESIAN_POINT('Ctrl Pts',(-1.53307755629186,-2.27908569474366,
7.50351950684424));
#401890=CARTESIAN_POINT('Ctrl Pts',(-1.53339700966226,-2.27891803629774,
7.50357029184312));
#401891=CARTESIAN_POINT('Ctrl Pts',(-1.53370061085857,-2.27874789763522,
7.50365515313924));
#401892=CARTESIAN_POINT('Ctrl Pts',(-1.53416767243875,-2.27848615547631,
7.50378570417639));
#401893=CARTESIAN_POINT('Ctrl Pts',(-1.53461109666587,-2.27821116305176,
7.50400001621911));
#401894=CARTESIAN_POINT('Ctrl Pts',(-1.53499593592696,-2.27794192178181,
7.50428903009634));
#401895=CARTESIAN_POINT('Ctrl Pts',(-1.53503865012417,-2.27791203807226,
7.50432110841317));
#401896=CARTESIAN_POINT('Ctrl Pts',(-1.53508067291071,-2.27788222500581,
7.50435406373354));
#401897=CARTESIAN_POINT('Ctrl Pts',(-1.5351219788744,-2.27785250810699,
7.50438785222352));
#401898=CARTESIAN_POINT('Ctrl Pts',(-1.53537417163688,-2.2776710721559,
7.50459414719561));
#401899=CARTESIAN_POINT('Ctrl Pts',(-1.53560335743639,-2.27748991372871,
7.50483629897752));
#401900=CARTESIAN_POINT('Ctrl Pts',(-1.53580157232054,-2.27731700539468,
7.5050991045531));
#401901=CARTESIAN_POINT('Ctrl Pts',(-1.5362388542638,-2.27693555224281,
7.50567888004914));
#401902=CARTESIAN_POINT('Ctrl Pts',(-1.53654297792575,-2.27657961193305,
7.50637912803145));
#401903=CARTESIAN_POINT('Ctrl Pts',(-1.53674187034852,-2.27626243205666,
7.50710440483569));
#401904=CARTESIAN_POINT('Ctrl Pts',(-1.53679064271915,-2.27618465325407,
7.50728225710685));
#401905=CARTESIAN_POINT('Ctrl Pts',(-1.5368341818023,-2.27610773442093,
7.50746498566955));
#401906=CARTESIAN_POINT('Ctrl Pts',(-1.5368718337977,-2.27603367630522,
7.50764697238949));
#401907=CARTESIAN_POINT('Ctrl Pts',(-1.53707424056284,-2.27563556025655,
7.50862528291181));
#401908=CARTESIAN_POINT('Ctrl Pts',(-1.5371285833645,-2.27528585019075,
7.50965856837421));
#401909=CARTESIAN_POINT('Ctrl Pts',(-1.53710069976793,-2.27497674797686,
7.51067959873201));
#401910=CARTESIAN_POINT('Ctrl Pts',(-1.53708535538957,-2.27480664863867,
7.51124147302578));
#401911=CARTESIAN_POINT('Ctrl Pts',(-1.53704467387377,-2.27464884415312,
7.51180065547252));
#401912=CARTESIAN_POINT('Ctrl Pts',(-1.53698693264455,-2.27450237756292,
7.51235175716501));
#401913=CARTESIAN_POINT('Ctrl Pts',(-1.53678741369622,-2.27399627714842,
7.51425603304535));
#401914=CARTESIAN_POINT('Ctrl Pts',(-1.53635477473429,-2.27356742990722,
7.51626900505179));
#401915=CARTESIAN_POINT('Ctrl Pts',(-1.53574915221225,-2.27322096169132,
7.51827788969243));
#401916=CARTESIAN_POINT('Ctrl Pts',(-1.53571637477688,-2.27320221017675,
7.51838661432545));
#401917=CARTESIAN_POINT('Ctrl Pts',(-1.53568308088396,-2.27318370197147,
7.51849533314856));
#401918=CARTESIAN_POINT('Ctrl Pts',(-1.5356492769952,-2.27316543860615,
7.51860402984325));
#401919=CARTESIAN_POINT('Ctrl Pts',(-1.4587421147806,-2.24101961378737,
7.57603338728985));
#401920=CARTESIAN_POINT('Ctrl Pts',(-1.48281814548957,-2.25407036159787,
7.55196141284922));
#401921=CARTESIAN_POINT('Ctrl Pts',(-1.50685310110155,-2.26709785384546,
7.52783573083104));
#401922=CARTESIAN_POINT('Ctrl Pts',(-1.53085035936764,-2.28010398289952,
7.50366116530176));
#401923=CARTESIAN_POINT('Origin',(-5.04062831473864E-16,-7.74375868966278E-16,
7.49482233047033));
#401924=CARTESIAN_POINT('Origin',(-1.46057722850548,-2.31530136474094,7.49482233047033));
#401925=CARTESIAN_POINT('Origin',(0.,0.,7.50366116523517));
#401926=CARTESIAN_POINT('Origin',(-1.52592346056194,-2.27276568139056,7.49482233047033));
#401927=CARTESIAN_POINT('Ctrl Pts',(-1.4570058399595,-2.32435553466795,
7.51860402984325));
#401928=CARTESIAN_POINT('Ctrl Pts',(-1.45760395760193,-2.3319409510254,
7.51860402984325));
#401929=CARTESIAN_POINT('Ctrl Pts',(-1.45114061263041,-2.33595610454791,
7.51860402984325));
#401930=CARTESIAN_POINT('Ctrl Pts',(-1.4572279238551,-2.32717205162693,
7.51041458714366));
#401931=CARTESIAN_POINT('Ctrl Pts',(-1.45607271192434,-2.33289217847475,
7.51004642900444));
#401932=CARTESIAN_POINT('Ctrl Pts',(-1.45113883011662,-2.33595721187957,
7.50729136483011));
#401933=CARTESIAN_POINT('Ctrl Pts',(-1.45993819904965,-2.32793241046926,
7.50215815450137));
#401934=CARTESIAN_POINT('Ctrl Pts',(-1.45919055500407,-2.3309555037299,
7.49877163671527));
#401935=CARTESIAN_POINT('Ctrl Pts',(-1.45627247511124,-2.3327963549823,
7.49481588533168));
#401936=CARTESIAN_POINT('Ctrl Pts',(-1.46529284374239,-2.32277653974657,
7.50366171572174));
#401937=CARTESIAN_POINT('Ctrl Pts',(-1.46724653091907,-2.32587351709115,
7.50000045605858));
#401938=CARTESIAN_POINT('Ctrl Pts',(-1.46724653091897,-2.32587351709122,
7.49482233047317));
#401939=CARTESIAN_POINT('Origin',(-1.44454451893664,-2.32533812225451,7.51860402984325));
#401940=CARTESIAN_POINT('Origin',(-1.44454451893664,-2.32533812225451,9.));
#401941=CARTESIAN_POINT('Origin',(-1.44454451893664,-2.32533812225451,8.75721825406948));
#401942=CARTESIAN_POINT('Ctrl Pts',(-1.45569455202209,-2.30770799497263,
8.78942910404913));
#401943=CARTESIAN_POINT('Ctrl Pts',(-1.45615226043136,-2.31326163627486,
8.79672699501693));
#401944=CARTESIAN_POINT('Ctrl Pts',(-1.44754234110095,-2.31561594617505,
8.79893251111267));
#401945=CARTESIAN_POINT('Ctrl Pts',(-1.45655786092531,-2.31866838349119,
8.78111911759578));
#401946=CARTESIAN_POINT('Ctrl Pts',(-1.45709306086354,-2.32525290102489,
8.78644465894808));
#401947=CARTESIAN_POINT('Ctrl Pts',(-1.44991412529166,-2.32901832209435,
8.78817647674131));
#401948=CARTESIAN_POINT('Ctrl Pts',(-1.45709589559393,-2.32549915904842,
8.76780923932034));
#401949=CARTESIAN_POINT('Ctrl Pts',(-1.45772259748297,-2.33327231680526,
8.76988516158378));
#401950=CARTESIAN_POINT('Ctrl Pts',(-1.45138449933333,-2.33739116278949,
8.77093053738834));
#401951=CARTESIAN_POINT('Ctrl Pts',(-1.45699098619534,-2.32416725130063,
8.75371302330491));
#401952=CARTESIAN_POINT('Ctrl Pts',(-1.45760306669667,-2.33174957012983,
8.75300828287558));
#401953=CARTESIAN_POINT('Ctrl Pts',(-1.45109726602123,-2.33575819793818,
8.75267964240738));
#401954=CARTESIAN_POINT('Origin',(-1.44344342869436,-2.31135883822902,8.78727029226991));
#401955=CARTESIAN_POINT('Ctrl Pts',(-1.45029105591253,-2.23910559748224,
8.85049129520029));
#401956=CARTESIAN_POINT('Ctrl Pts',(-1.45074959802197,-2.24492718243455,
8.85711686593484));
#401957=CARTESIAN_POINT('Ctrl Pts',(-1.44260408658466,-2.24752552912784,
8.85933012996512));
#401958=CARTESIAN_POINT('Ctrl Pts',(-1.45216503745171,-2.26289739872513,
8.82945683644722));
#401959=CARTESIAN_POINT('Ctrl Pts',(-1.4526273857379,-2.26876730635234,
8.83607469902388));
#401960=CARTESIAN_POINT('Ctrl Pts',(-1.44444656216418,-2.27133755306296,
8.83829567148519));
#401961=CARTESIAN_POINT('Ctrl Pts',(-1.45403622567029,-2.28665373636973,
8.80838214965003));
#401962=CARTESIAN_POINT('Ctrl Pts',(-1.4545003985987,-2.29254680939303,
8.81501364461989));
#401963=CARTESIAN_POINT('Ctrl Pts',(-1.44628690934868,-2.29511340381663,
8.81722098428722));
#401964=CARTESIAN_POINT('Ctrl Pts',(-1.45590483281683,-2.31037730509332,
8.78727029226991));
#401965=CARTESIAN_POINT('Ctrl Pts',(-1.45636908284588,-2.31627135697542,
8.79393457792714));
#401966=CARTESIAN_POINT('Ctrl Pts',(-1.44812530550984,-2.31885583959521,
8.79610912703474));
#401967=CARTESIAN_POINT('Origin',(-1.43782965179006,-2.24008713061794,8.85049129520029));
#401968=CARTESIAN_POINT('Ctrl Pts',(-1.46041276049032,-2.23251709792629,
8.85049129520029));
#401969=CARTESIAN_POINT('Ctrl Pts',(-1.46555048104865,-2.23529287523862,
8.85711686593484));
#401970=CARTESIAN_POINT('Ctrl Pts',(-1.471223609415,-2.22889628422052,8.85933012996512));
#401971=CARTESIAN_POINT('Ctrl Pts',(-1.45586749327615,-2.23006140780684,
8.86332496987233));
#401972=CARTESIAN_POINT('Ctrl Pts',(-1.45988689960007,-2.22778187557852,
8.86648636486738));
#401973=CARTESIAN_POINT('Ctrl Pts',(-1.4584998952933,-2.22204146436104,
8.87206031107457));
#401974=CARTESIAN_POINT('Ctrl Pts',(-1.44988263370189,-2.23392032758733,
8.86341338519875));
#401975=CARTESIAN_POINT('Ctrl Pts',(-1.44614309960767,-2.23665699625423,
8.86654584966056));
#401976=CARTESIAN_POINT('Ctrl Pts',(-1.44147517002644,-2.2330053409841,
8.87215952290714));
#401977=CARTESIAN_POINT('Ctrl Pts',(-1.45029105591253,-2.23910559748224,
8.85049129520029));
#401978=CARTESIAN_POINT('Ctrl Pts',(-1.45074959802197,-2.24492718243455,
8.85711686593484));
#401979=CARTESIAN_POINT('Ctrl Pts',(-1.44260408658466,-2.24752552912784,
8.85933012996512));
#401980=CARTESIAN_POINT('Origin',(-1.4663544556002,-2.22151954096026,8.85049129520029));
#401981=CARTESIAN_POINT('Ctrl Pts',(-1.52331214621091,-2.26650000646724,
8.78727029226991));
#401982=CARTESIAN_POINT('Ctrl Pts',(-1.52851382097382,-2.26931033657941,
8.79393457792714));
#401983=CARTESIAN_POINT('Ctrl Pts',(-1.53421404825535,-2.26281827803708,
8.79610912703474));
#401984=CARTESIAN_POINT('Ctrl Pts',(-1.50237539655483,-2.25518842304625,
8.80838214965001));
#401985=CARTESIAN_POINT('Ctrl Pts',(-1.50757620744601,-2.25799828643088,
8.81501364461993));
#401986=CARTESIAN_POINT('Ctrl Pts',(-1.51324781742239,-2.25152668285288,
8.81722098428721));
#401987=CARTESIAN_POINT('Ctrl Pts',(-1.48140972735873,-2.24386121514702,
8.82945683644724));
#401988=CARTESIAN_POINT('Ctrl Pts',(-1.48659009410403,-2.24666003308931,
8.8360746990239));
#401989=CARTESIAN_POINT('Ctrl Pts',(-1.49225182125611,-2.24021977780301,
8.8382956714852));
#401990=CARTESIAN_POINT('Ctrl Pts',(-1.46041276049032,-2.23251709792629,
8.85049129520029));
#401991=CARTESIAN_POINT('Ctrl Pts',(-1.46555048104865,-2.23529287523862,
8.85711686593484));
#401992=CARTESIAN_POINT('Ctrl Pts',(-1.471223609415,-2.22889628422052,8.85933012996512));
#401993=CARTESIAN_POINT('Origin',(-1.52925384132079,-2.2555024495012,8.78727029226991));
#401994=CARTESIAN_POINT('Ctrl Pts',(-1.53548638015782,-2.27307740869792,
8.75374538247847));
#401995=CARTESIAN_POINT('Ctrl Pts',(-1.54216574291842,-2.27670101070421,
8.75304829418601));
#401996=CARTESIAN_POINT('Ctrl Pts',(-1.54846123506549,-2.27238390266349,
8.75272238421917));
#401997=CARTESIAN_POINT('Ctrl Pts',(-1.53664770761178,-2.27370484431909,
8.76769408445023));
#401998=CARTESIAN_POINT('Ctrl Pts',(-1.54349548185628,-2.27741902563785,
8.76974318093971));
#401999=CARTESIAN_POINT('Ctrl Pts',(-1.54982261507514,-2.27329764934939,
8.7707786988043));
#402000=CARTESIAN_POINT('Ctrl Pts',(-1.53069540464028,-2.27048896676447,
8.78108014887986));
#402001=CARTESIAN_POINT('Ctrl Pts',(-1.53649683516817,-2.27363994139627,
8.78639403366322));
#402002=CARTESIAN_POINT('Ctrl Pts',(-1.54284883455847,-2.26862255368208,
8.78812224174741));
#402003=CARTESIAN_POINT('Ctrl Pts',(-1.52094089407099,-2.26521885333373,
8.78944554828685));
#402004=CARTESIAN_POINT('Ctrl Pts',(-1.52582745292966,-2.26787929693168,
8.79673892988687));
#402005=CARTESIAN_POINT('Ctrl Pts',(-1.53146141315401,-2.26096828785145,
8.79894799272499));
#402006=CARTESIAN_POINT('Origin',(-1.54159097210508,-2.26216788164012,8.75721825406948));
#402007=CARTESIAN_POINT('Origin',(-1.54159097210508,-2.26216788164012,9.));
#402008=CARTESIAN_POINT('Origin',(-1.54159097210508,-2.26216788164012,7.51860402984325));
#402009=CARTESIAN_POINT('Ctrl Pts',(-1.53084992081514,-2.28010332976116,
7.50366195182966));
#402010=CARTESIAN_POINT('Ctrl Pts',(-1.53289114759659,-2.28314360687628,
7.50000065167735));
#402011=CARTESIAN_POINT('Ctrl Pts',(-1.53289114759668,-2.28314360687622,
7.49482233047108));
#402012=CARTESIAN_POINT('Ctrl Pts',(-1.53773778419653,-2.27729065529617,
7.50215800491337));
#402013=CARTESIAN_POINT('Ctrl Pts',(-1.54080605586929,-2.27782954871471,
7.49877273257264));
#402014=CARTESIAN_POINT('Ctrl Pts',(-1.54367213946218,-2.27590530309928,
7.49481816995647));
#402015=CARTESIAN_POINT('Ctrl Pts',(-1.53812892001266,-2.27450551093449,
7.51043025814041));
#402016=CARTESIAN_POINT('Ctrl Pts',(-1.54382949412869,-2.2757689236677,
7.51006209594514));
#402017=CARTESIAN_POINT('Ctrl Pts',(-1.54863229252765,-2.27249598955575,
7.50731281821699));
#402018=CARTESIAN_POINT('Ctrl Pts',(-1.53564794729548,-2.27316472009998,
7.51860402984325));
#402019=CARTESIAN_POINT('Ctrl Pts',(-1.54234218192175,-2.27678248738922,
7.51860402984324));
#402020=CARTESIAN_POINT('Ctrl Pts',(-1.54863020028821,-2.27249741534623,
7.51860402984325));
#402021=CARTESIAN_POINT('Origin',(0.,0.,7.5));
#402022=CARTESIAN_POINT('Origin',(-1.31437432427028,-2.32149911893915,7.5));
#402023=CARTESIAN_POINT('',(-1.31437432427028,-2.32149911893915,7.59394543036555));
#402024=CARTESIAN_POINT('',(-1.31437432427028,-2.32149911893915,8.85049129520029));
#402025=CARTESIAN_POINT('',(-1.31437432427028,-2.32149911893915,7.5));
#402026=CARTESIAN_POINT('',(-1.37496718403116,-2.35944218342961,8.78727029226991));
#402027=CARTESIAN_POINT('Ctrl Pts',(-1.31437432427028,-2.32149911893915,
8.85049129520029));
#402028=CARTESIAN_POINT('Ctrl Pts',(-1.33460130338716,-2.33416519174224,
8.82945686509571));
#402029=CARTESIAN_POINT('Ctrl Pts',(-1.35479821265378,-2.34681243489656,
8.80838212259897));
#402030=CARTESIAN_POINT('Ctrl Pts',(-1.37496718403116,-2.35944218342961,
8.78727029226991));
#402031=CARTESIAN_POINT('',(-1.38685191115369,-2.36688436340661,8.75721825406948));
#402032=CARTESIAN_POINT('Origin',(-1.35108653730004,-2.34448843318215,8.75937679713147));
#402033=CARTESIAN_POINT('',(-1.38685191115369,-2.36688436340661,7.51860402984325));
#402034=CARTESIAN_POINT('',(-1.38685191115369,-2.36688436340661,7.5));
#402035=CARTESIAN_POINT('Ctrl Pts',(-1.38685191115369,-2.36688436340661,
7.51860402984325));
#402036=CARTESIAN_POINT('Ctrl Pts',(-1.37751830642364,-2.3610396885126,
7.52834476460825));
#402037=CARTESIAN_POINT('Ctrl Pts',(-1.36817864245209,-2.35519121934,7.53807742314407));
#402038=CARTESIAN_POINT('Ctrl Pts',(-1.35883271579193,-2.34933882849083,
7.54780169004674));
#402039=CARTESIAN_POINT('Ctrl Pts',(-1.34402927306647,-2.34006895768049,
7.5632044032688));
#402040=CARTESIAN_POINT('Ctrl Pts',(-1.32921009923996,-2.33078923610249,
7.57858609112103));
#402041=CARTESIAN_POINT('Ctrl Pts',(-1.31437432427028,-2.32149911893915,
7.59394543036555));
#402042=CARTESIAN_POINT('Origin',(-1.3078357436827,-2.6023967151304,7.5));
#402043=CARTESIAN_POINT('',(-1.30509031014833,-2.4129316392236,8.75721825406948));
#402044=CARTESIAN_POINT('',(-1.30488713801673,-2.39891053004237,8.78727029226991));
#402045=CARTESIAN_POINT('Origin',(-1.30437141136731,-2.36331972532774,8.75658640621058));
#402046=CARTESIAN_POINT('',(-1.30385128920419,-2.32742558187727,8.85049129520029));
#402047=CARTESIAN_POINT('Ctrl Pts',(-1.30488713801673,-2.39891053004237,
8.78727029226991));
#402048=CARTESIAN_POINT('Ctrl Pts',(-1.30454234483262,-2.37511601235258,
8.80838212259897));
#402049=CARTESIAN_POINT('Ctrl Pts',(-1.30419707404389,-2.35128853469734,
8.82945686509571));
#402050=CARTESIAN_POINT('Ctrl Pts',(-1.30385128920419,-2.32742558187727,
8.85049129520029));
#402051=CARTESIAN_POINT('',(-1.30385128920419,-2.32742558187727,7.59394543036555));
#402052=CARTESIAN_POINT('',(-1.30385128920419,-2.32742558187727,7.5));
#402053=CARTESIAN_POINT('',(-1.30509031014833,-2.4129316392236,7.51860402984325));
#402054=CARTESIAN_POINT('Ctrl Pts',(-1.30385128920419,-2.32742558187727,
7.59394543036555));
#402055=CARTESIAN_POINT('Ctrl Pts',(-1.30410491017449,-2.34492821517238,
7.57858609112103));
#402056=CARTESIAN_POINT('Ctrl Pts',(-1.30435824734445,-2.36241126312565,
7.56320440326857));
#402057=CARTESIAN_POINT('Ctrl Pts',(-1.30461131558762,-2.37987575217717,
7.54780169004651));
#402058=CARTESIAN_POINT('Ctrl Pts',(-1.30477108634396,-2.39090168964724,
7.53807742314383));
#402059=CARTESIAN_POINT('Ctrl Pts',(-1.3049307500382,-2.4019202386567,7.52834476460825));
#402060=CARTESIAN_POINT('Ctrl Pts',(-1.30509031014833,-2.4129316392236,
7.51860402984325));
#402061=CARTESIAN_POINT('',(-1.30509031014833,-2.4129316392236,7.5));
#402062=CARTESIAN_POINT('Origin',(-1.31072556753552,-2.32732597051531,7.5));
#402063=CARTESIAN_POINT('Ctrl Pts',(-1.30385128920419,-2.32742558187727,
8.85049129520029));
#402064=CARTESIAN_POINT('Ctrl Pts',(-1.30384848325709,-2.3272319407,8.85097269580138));
#402065=CARTESIAN_POINT('Ctrl Pts',(-1.30385412324172,-2.32704062079223,
8.85143669361005));
#402066=CARTESIAN_POINT('Ctrl Pts',(-1.3038693427671,-2.32684283825271,
8.8519052845931));
#402067=CARTESIAN_POINT('Ctrl Pts',(-1.30389911119356,-2.32645598814832,
8.85282181883899));
#402068=CARTESIAN_POINT('Ctrl Pts',(-1.30396495843795,-2.32605438066443,
8.85372622499636));
#402069=CARTESIAN_POINT('Ctrl Pts',(-1.30408313333415,-2.32563420862441,
8.85462257735071));
#402070=CARTESIAN_POINT('Ctrl Pts',(-1.3041812379358,-2.32528539671988,
8.85536669723986));
#402071=CARTESIAN_POINT('Ctrl Pts',(-1.30431539729114,-2.32492370253026,
8.85610498449051));
#402072=CARTESIAN_POINT('Ctrl Pts',(-1.30450242234571,-2.32454970015687,
8.85681338218371));
#402073=CARTESIAN_POINT('Ctrl Pts',(-1.30467214787645,-2.32421029241564,
8.85745625420284));
#402074=CARTESIAN_POINT('Ctrl Pts',(-1.30488700517417,-2.32385622295628,
8.85808743050665));
#402075=CARTESIAN_POINT('Ctrl Pts',(-1.30517545207643,-2.32349031978706,
8.8586680450841));
#402076=CARTESIAN_POINT('Ctrl Pts',(-1.30530853522436,-2.32332149999658,
8.85893592806395));
#402077=CARTESIAN_POINT('Ctrl Pts',(-1.3054575199839,-2.32315021373903,
8.85919241173848));
#402078=CARTESIAN_POINT('Ctrl Pts',(-1.30562669581159,-2.32297729919044,
8.85943017985534));
#402079=CARTESIAN_POINT('Ctrl Pts',(-1.30585513326038,-2.32274381336165,
8.8597512372));
#402080=CARTESIAN_POINT('Ctrl Pts',(-1.30612665726057,-2.32250186380976,
8.86004599534705));
#402081=CARTESIAN_POINT('Ctrl Pts',(-1.3064449344762,-2.32226213334002,
8.86026130871721));
#402082=CARTESIAN_POINT('Ctrl Pts',(-1.30656146473803,-2.32217436125633,
8.86034014101235));
#402083=CARTESIAN_POINT('Ctrl Pts',(-1.30668600525794,-2.32208555836309,
8.86040910639692));
#402084=CARTESIAN_POINT('Ctrl Pts',(-1.30681535829032,-2.32199841792861,
8.86046313645506));
#402085=CARTESIAN_POINT('Ctrl Pts',(-1.30701721261402,-2.32186243601041,
8.86054744990829));
#402086=CARTESIAN_POINT('Ctrl Pts',(-1.3072363782195,-2.32172691245506,
8.86059655985669));
#402087=CARTESIAN_POINT('Ctrl Pts',(-1.30745864527339,-2.32160028963278,
8.86059725258816));
#402088=CARTESIAN_POINT('Ctrl Pts',(-1.30768142585297,-2.32147337426119,
8.86059794692011));
#402089=CARTESIAN_POINT('Ctrl Pts',(-1.30791110798646,-2.32135630174498,
8.86056369958366));
#402090=CARTESIAN_POINT('Ctrl Pts',(-1.30813345578227,-2.32125210458825,
8.86048590497774));
#402091=CARTESIAN_POINT('Ctrl Pts',(-1.30819148193688,-2.32122491223266,
8.86046560290182));
#402092=CARTESIAN_POINT('Ctrl Pts',(-1.30824980190643,-2.32119832502184,
8.86044257503091));
#402093=CARTESIAN_POINT('Ctrl Pts',(-1.30830659993883,-2.32117313465384,
8.86041778462583));
#402094=CARTESIAN_POINT('Ctrl Pts',(-1.30868878021643,-2.32100363473589,
8.86025097596201));
#402095=CARTESIAN_POINT('Ctrl Pts',(-1.30905347104566,-2.32087493729499,
8.8599848982295));
#402096=CARTESIAN_POINT('Ctrl Pts',(-1.30938720857525,-2.3207828090796,
8.85968173251461));
#402097=CARTESIAN_POINT('Ctrl Pts',(-1.30956373660753,-2.32073407853198,
8.85952137522076));
#402098=CARTESIAN_POINT('Ctrl Pts',(-1.30973495640561,-2.32069445594468,
8.85934740853961));
#402099=CARTESIAN_POINT('Ctrl Pts',(-1.30989810290951,-2.32066298555583,
8.8591675900182));
#402100=CARTESIAN_POINT('Ctrl Pts',(-1.31055322092456,-2.32053661558658,
8.85844552518695));
#402101=CARTESIAN_POINT('Ctrl Pts',(-1.31111461455946,-2.32053158164898,
8.85759444184125));
#402102=CARTESIAN_POINT('Ctrl Pts',(-1.31157271342272,-2.32056859093142,
8.85683498915139));
#402103=CARTESIAN_POINT('Ctrl Pts',(-1.31162065224875,-2.32057246385427,
8.85675551444998));
#402104=CARTESIAN_POINT('Ctrl Pts',(-1.31166745441337,-2.32057681639896,
8.85667699793651));
#402105=CARTESIAN_POINT('Ctrl Pts',(-1.31171310470178,-2.32058157012439,
8.85659965593547));
#402106=CARTESIAN_POINT('Ctrl Pts',(-1.3123292946241,-2.32064573615286,
8.85555568965886));
#402107=CARTESIAN_POINT('Ctrl Pts',(-1.31291222447142,-2.32079639369907,
8.85434650606346));
#402108=CARTESIAN_POINT('Ctrl Pts',(-1.31346633101424,-2.3210282704993,
8.85297329937117));
#402109=CARTESIAN_POINT('Ctrl Pts',(-1.31377798218236,-2.32115868707096,
8.85220095427747));
#402110=CARTESIAN_POINT('Ctrl Pts',(-1.31408052113675,-2.32131514031053,
8.85137579139183));
#402111=CARTESIAN_POINT('Ctrl Pts',(-1.31437432427028,-2.32149911893915,
8.85049129520029));
#402112=CARTESIAN_POINT('Origin',(-1.31072556753552,-2.32732597051531,7.59394543036555));
#402113=CARTESIAN_POINT('Ctrl Pts',(-1.30384314259316,-2.32686337621542,
7.59443877723642));
#402114=CARTESIAN_POINT('Ctrl Pts',(-1.30375924033801,-2.32107319883815,
7.58783886950016));
#402115=CARTESIAN_POINT('Ctrl Pts',(-1.31198945928027,-2.31898928960331,
7.58559994247159));
#402116=CARTESIAN_POINT('Ctrl Pts',(-1.30430116254246,-2.35847178464137,
7.56670252222136));
#402117=CARTESIAN_POINT('Ctrl Pts',(-1.30421738154994,-2.35268997571428,
7.56004874999027));
#402118=CARTESIAN_POINT('Ctrl Pts',(-1.31249112309637,-2.35057300663592,
7.55786368756704));
#402119=CARTESIAN_POINT('Ctrl Pts',(-1.30475832718527,-2.39002116752266,
7.53888913333561));
#402120=CARTESIAN_POINT('Ctrl Pts',(-1.30467404827816,-2.384204997022,7.53222002137279));
#402121=CARTESIAN_POINT('Ctrl Pts',(-1.3129907016416,-2.38209888174683,
7.53005029815327));
#402122=CARTESIAN_POINT('Ctrl Pts',(-1.30521461583457,-2.42151009722832,
7.51101258149734));
#402123=CARTESIAN_POINT('Ctrl Pts',(-1.30512931531396,-2.41562342417297,
7.5043616886572));
#402124=CARTESIAN_POINT('Ctrl Pts',(-1.31348825286495,-2.41356535601003,
7.50217374673251));
#402125=CARTESIAN_POINT('',(-1.31346170186502,-2.41188626453888,7.50366116523517));
#402126=CARTESIAN_POINT('Ctrl Pts',(-1.30509031014833,-2.4129316392236,
7.51860402984325));
#402127=CARTESIAN_POINT('Ctrl Pts',(-1.30509670862028,-2.41337320408332,
7.51734760759493));
#402128=CARTESIAN_POINT('Ctrl Pts',(-1.30516198111641,-2.41377135902957,
7.51608817408573));
#402129=CARTESIAN_POINT('Ctrl Pts',(-1.30529915524689,-2.41412302796591,
7.5148100591312));
#402130=CARTESIAN_POINT('Ctrl Pts',(-1.30542341085215,-2.41444157809184,
7.51365231206383));
#402131=CARTESIAN_POINT('Ctrl Pts',(-1.30560660504883,-2.41472252559345,
7.51247773061043));
#402132=CARTESIAN_POINT('Ctrl Pts',(-1.30587649835675,-2.41494084061838,
7.51129758471022));
#402133=CARTESIAN_POINT('Ctrl Pts',(-1.30621194491553,-2.41521218126185,
7.50983079813402));
#402134=CARTESIAN_POINT('Ctrl Pts',(-1.30667880678716,-2.4153679832624,
7.50839324291155));
#402135=CARTESIAN_POINT('Ctrl Pts',(-1.30730658833191,-2.41533118376777,
7.50715379678855));
#402136=CARTESIAN_POINT('Ctrl Pts',(-1.30759660531649,-2.41531418346161,
7.50658120839351));
#402137=CARTESIAN_POINT('Ctrl Pts',(-1.30796163787566,-2.41524417646108,
7.50598221009429));
#402138=CARTESIAN_POINT('Ctrl Pts',(-1.30838871444075,-2.41510048946133,
7.50545747549611));
#402139=CARTESIAN_POINT('Ctrl Pts',(-1.30861661571513,-2.41502381363074,
7.50517746087247));
#402140=CARTESIAN_POINT('Ctrl Pts',(-1.30886472060112,-2.41492551702525,
7.50491486231392));
#402141=CARTESIAN_POINT('Ctrl Pts',(-1.30912584447471,-2.41480665196124,
7.50468370960992));
#402142=CARTESIAN_POINT('Ctrl Pts',(-1.30951630703258,-2.41462891119669,
7.50433806340446));
#402143=CARTESIAN_POINT('Ctrl Pts',(-1.30994735749209,-2.41439934358562,
7.50405484070983));
#402144=CARTESIAN_POINT('Ctrl Pts',(-1.31038962865154,-2.41413277776807,
7.50385766036131));
#402145=CARTESIAN_POINT('Ctrl Pts',(-1.31043692267759,-2.41410427269726,
7.50383657498791));
#402146=CARTESIAN_POINT('Ctrl Pts',(-1.31048433154189,-2.41407536951207,
7.50381643264937));
#402147=CARTESIAN_POINT('Ctrl Pts',(-1.31053180983105,-2.41404610463014,
7.50379723213559));
#402148=CARTESIAN_POINT('Ctrl Pts',(-1.31084874294239,-2.41385075197005,
7.50366906242519));
#402149=CARTESIAN_POINT('Ctrl Pts',(-1.31117528635902,-2.41363442062052,
7.50358235568538));
#402150=CARTESIAN_POINT('Ctrl Pts',(-1.3114850217094,-2.41341833793829,
7.5035341175365));
#402151=CARTESIAN_POINT('Ctrl Pts',(-1.31194943481202,-2.41309434641211,
7.50346178989176));
#402152=CARTESIAN_POINT('Ctrl Pts',(-1.31243526188344,-2.41272605894918,
7.50346967198527));
#402153=CARTESIAN_POINT('Ctrl Pts',(-1.3129010688221,-2.41234983956352,
7.50354272648692));
#402154=CARTESIAN_POINT('Ctrl Pts',(-1.31309266485761,-2.41219509274291,
7.50357277531559));
#402155=CARTESIAN_POINT('Ctrl Pts',(-1.31328070831928,-2.41203931988079,
7.50361331098761));
#402156=CARTESIAN_POINT('Ctrl Pts',(-1.3134617018657,-2.41188626454012,
7.50366116523659));
#402157=CARTESIAN_POINT('',(-1.31216235181375,-2.32987712649109,7.57603338622103));
#402158=CARTESIAN_POINT('Origin',(-1.31650127865063,-2.33757551616054,7.58486873427627));
#402159=CARTESIAN_POINT('Ctrl Pts',(-1.31346170186057,-2.41188626459605,
7.50366116529969));
#402160=CARTESIAN_POINT('Ctrl Pts',(-1.31303012767074,-2.38459447933895,
7.52783573079709));
#402161=CARTESIAN_POINT('Ctrl Pts',(-1.31259704935557,-2.35725939039689,
7.55196141284068));
#402162=CARTESIAN_POINT('Ctrl Pts',(-1.31216235147919,-2.32987712769762,
7.57603338728831));
#402163=CARTESIAN_POINT('Ctrl Pts',(-1.30401338901575,-2.32827248701352,
7.59642833564546));
#402164=CARTESIAN_POINT('Ctrl Pts',(-1.30138988733093,-2.31016651972364,
7.5995988229546));
#402165=CARTESIAN_POINT('Ctrl Pts',(-1.31515263304405,-2.32219393616171,
7.59639677331372));
#402166=CARTESIAN_POINT('Ctrl Pts',(-1.30283923060014,-2.32461049415274,
7.58710240504252));
#402167=CARTESIAN_POINT('Ctrl Pts',(-1.30591687143453,-2.31859031743716,
7.58809943920598));
#402168=CARTESIAN_POINT('Ctrl Pts',(-1.31266628426856,-2.31918841227223,
7.58707626057424));
#402169=CARTESIAN_POINT('Ctrl Pts',(-1.308291512786,-2.32726456978442,7.58020924244129));
#402170=CARTESIAN_POINT('Ctrl Pts',(-1.30923351557898,-2.32461132539759,
7.5820588065976));
#402171=CARTESIAN_POINT('Ctrl Pts',(-1.31201671782412,-2.32523024110922,
7.5801537675693));
#402172=CARTESIAN_POINT('Ctrl Pts',(-1.31216235140747,-2.32987712577011,
7.57603338509286));
#402173=CARTESIAN_POINT('Ctrl Pts',(-1.31216235140747,-2.32987712577011,
7.57603338509286));
#402174=CARTESIAN_POINT('Ctrl Pts',(-1.31216235140747,-2.32987712577011,
7.57603338509286));
#402175=CARTESIAN_POINT('Origin',(-1.31649630659947,-2.33757831636809,7.58486873427622));
#402176=CARTESIAN_POINT('Ctrl Pts',(-1.39414625998579,-2.37145206245968,
7.51098857897448));
#402177=CARTESIAN_POINT('Ctrl Pts',(-1.38915651052492,-2.36832749652349,
7.50433767179956));
#402178=CARTESIAN_POINT('Ctrl Pts',(-1.38306334512839,-2.37440872884375,
7.50214974420965));
#402179=CARTESIAN_POINT('Ctrl Pts',(-1.36744758926186,-2.35473343605575,
7.5388732158917));
#402180=CARTESIAN_POINT('Ctrl Pts',(-1.36251762585473,-2.35164630796459,
7.53220407452064));
#402181=CARTESIAN_POINT('Ctrl Pts',(-1.35640527808569,-2.35766645120803,
7.53003438070912));
#402182=CARTESIAN_POINT('Ctrl Pts',(-1.34069764724134,-2.33798270372184,
7.5666946565923));
#402183=CARTESIAN_POINT('Ctrl Pts',(-1.33579681900136,-2.33491381998372,
7.56004085833294));
#402184=CARTESIAN_POINT('Ctrl Pts',(-1.32969743729772,-2.34089162835798,
7.55785582193789));
#402185=CARTESIAN_POINT('Ctrl Pts',(-1.31389764371717,-2.32120062302661,
7.59443891967696));
#402186=CARTESIAN_POINT('Ctrl Pts',(-1.30898970988645,-2.31812728978918,
7.58783901202978));
#402187=CARTESIAN_POINT('Ctrl Pts',(-1.30294118573047,-2.32408501867886,
7.58560008491213));
#402188=CARTESIAN_POINT('',(-1.38161829930507,-2.37350118398177,7.50366116523517));
#402189=CARTESIAN_POINT('Ctrl Pts',(-1.38161829930525,-2.37350118398209,
7.50366116523554));
#402190=CARTESIAN_POINT('Ctrl Pts',(-1.38233657059499,-2.37325988775106,
7.50350835821027));
#402191=CARTESIAN_POINT('Ctrl Pts',(-1.38298898591945,-2.37301470974318,
7.50345484956));
#402192=CARTESIAN_POINT('Ctrl Pts',(-1.38359515336115,-2.37275892273606,
7.50349758195598));
#402193=CARTESIAN_POINT('Ctrl Pts',(-1.38390616221329,-2.37262768503175,
7.50351950684424));
#402194=CARTESIAN_POINT('Ctrl Pts',(-1.38423570114598,-2.3724808385058,
7.50357029184312));
#402195=CARTESIAN_POINT('Ctrl Pts',(-1.38454957938261,-2.37233050120684,
7.50365515313924));
#402196=CARTESIAN_POINT('Ctrl Pts',(-1.38503245121239,-2.37209922156346,
7.50378570417639));
#402197=CARTESIAN_POINT('Ctrl Pts',(-1.38549258320202,-2.3718532044281,
7.50400001621911));
#402198=CARTESIAN_POINT('Ctrl Pts',(-1.38589388211697,-2.37160917307933,
7.50428903009635));
#402199=CARTESIAN_POINT('Ctrl Pts',(-1.38593842320912,-2.37158208747708,
7.50432110841318));
#402200=CARTESIAN_POINT('Ctrl Pts',(-1.38598226978506,-2.37155502807397,
7.50435406373354));
#402201=CARTESIAN_POINT('Ctrl Pts',(-1.38602539484945,-2.37152801871388,
7.50438785222351));
#402202=CARTESIAN_POINT('Ctrl Pts',(-1.38628869409615,-2.37136311358818,
7.50459414719561));
#402203=CARTESIAN_POINT('Ctrl Pts',(-1.38652901586914,-2.371197011355,7.50483629897752));
#402204=CARTESIAN_POINT('Ctrl Pts',(-1.38673790177455,-2.37103715795091,
7.5050991045531));
#402205=CARTESIAN_POINT('Ctrl Pts',(-1.38719872506251,-2.37068450528575,
7.50567888004914));
#402206=CARTESIAN_POINT('Ctrl Pts',(-1.38752502904372,-2.37034878156346,
7.50637912803144));
#402207=CARTESIAN_POINT('Ctrl Pts',(-1.38774383460514,-2.37004499644843,
7.50710440483569));
#402208=CARTESIAN_POINT('Ctrl Pts',(-1.38779749007269,-2.36997050230724,
7.50728225710685));
#402209=CARTESIAN_POINT('Ctrl Pts',(-1.38784586790669,-2.36989653107072,
7.50746498566954));
#402210=CARTESIAN_POINT('Ctrl Pts',(-1.38788818746179,-2.36982503748699,
7.50764697238949));
#402211=CARTESIAN_POINT('Ctrl Pts',(-1.38811568574333,-2.3694407076564,
7.50862528291182));
#402212=CARTESIAN_POINT('Ctrl Pts',(-1.38819232289273,-2.3690951978627,
7.50965856837421));
#402213=CARTESIAN_POINT('Ctrl Pts',(-1.38818430083284,-2.36878494422429,
7.51067959873202));
#402214=CARTESIAN_POINT('Ctrl Pts',(-1.38817988628316,-2.36861421125573,
7.51124147302578));
#402215=CARTESIAN_POINT('Ctrl Pts',(-1.38814939892001,-2.36845412452276,
7.51180065547253));
#402216=CARTESIAN_POINT('Ctrl Pts',(-1.38810116047299,-2.36830425937062,
7.51235175716501));
#402217=CARTESIAN_POINT('Ctrl Pts',(-1.38793447742262,-2.36778641557079,
7.51425603304536));
#402218=CARTESIAN_POINT('Ctrl Pts',(-1.38753020370092,-2.36733073016878,
7.51626900505179));
#402219=CARTESIAN_POINT('Ctrl Pts',(-1.38694802379011,-2.36694617144078,
7.51827788969243));
#402220=CARTESIAN_POINT('Ctrl Pts',(-1.38691651511317,-2.3669253583957,
7.51838661432545));
#402221=CARTESIAN_POINT('Ctrl Pts',(-1.38688447545091,-2.36690475507048,
7.51849533314856));
#402222=CARTESIAN_POINT('Ctrl Pts',(-1.38685191115369,-2.36688436340661,
7.51860402984325));
#402223=CARTESIAN_POINT('Ctrl Pts',(-1.31216235301973,-2.32987712683137,
7.57603338728985));
#402224=CARTESIAN_POINT('Ctrl Pts',(-1.33535275265834,-2.34444361706459,
7.55196141284922));
#402225=CARTESIAN_POINT('Ctrl Pts',(-1.3585036515822,-2.35898426782541,
7.52783573083106));
#402226=CARTESIAN_POINT('Ctrl Pts',(-1.38161829935786,-2.3735011840085,
7.50366116530176));
#402227=CARTESIAN_POINT('Origin',(-4.53412748053607E-16,-8.05080247188567E-16,
7.49482233047033));
#402228=CARTESIAN_POINT('Origin',(-1.3092344481825,-2.40412383410095,7.49482233047033));
#402229=CARTESIAN_POINT('Origin',(0.,0.,7.50366116523517));
#402230=CARTESIAN_POINT('Origin',(-1.37717168998613,-2.36586229233672,7.49482233047033));
#402231=CARTESIAN_POINT('Ctrl Pts',(-1.30509029477835,-2.41293058161501,
7.51860402984325));
#402232=CARTESIAN_POINT('Ctrl Pts',(-1.30520118422927,-2.42053873444995,
7.51860402984325));
#402233=CARTESIAN_POINT('Ctrl Pts',(-1.29849386712375,-2.42413153047479,
7.51860402984325));
#402234=CARTESIAN_POINT('Ctrl Pts',(-1.30513146751763,-2.41575554070188,
7.51041458714366));
#402235=CARTESIAN_POINT('Ctrl Pts',(-1.30361213930822,-2.42138990025308,
7.51004642900443));
#402236=CARTESIAN_POINT('Ctrl Pts',(-1.29849201732533,-2.42413252132527,
7.5072913648301));
#402237=CARTESIAN_POINT('Ctrl Pts',(-1.30778745780282,-2.41668798523334,
7.50215815450138));
#402238=CARTESIAN_POINT('Ctrl Pts',(-1.30684765962189,-2.41965696550619,
7.49877163671529));
#402239=CARTESIAN_POINT('Ctrl Pts',(-1.30381763149247,-2.4213070725116,
7.4948158853317));
#402240=CARTESIAN_POINT('Ctrl Pts',(-1.31346143857516,-2.4118857810634,
7.50366171572174));
#402241=CARTESIAN_POINT('Ctrl Pts',(-1.31521268767226,-2.41510156850306,
7.50000045605858));
#402242=CARTESIAN_POINT('Ctrl Pts',(-1.31521268767215,-2.41510156850312,
7.49482233047317));
#402243=CARTESIAN_POINT('Origin',(-1.29259162227319,-2.41311275079081,7.51860402984325));
#402244=CARTESIAN_POINT('Origin',(-1.29259162227319,-2.41311275079081,9.));
#402245=CARTESIAN_POINT('Origin',(-1.29259162227319,-2.41311275079081,8.75721825406948));
#402246=CARTESIAN_POINT('Ctrl Pts',(-1.30484831255306,-2.39623323156884,
8.78942910404912));
#402247=CARTESIAN_POINT('Ctrl Pts',(-1.30494925753138,-2.40180478779784,
8.7967269950169));
#402248=CARTESIAN_POINT('Ctrl Pts',(-1.29620618705045,-2.40360262109034,
8.79893251111266));
#402249=CARTESIAN_POINT('Ctrl Pts',(-1.30500761319209,-2.40722641318503,
8.78111911759583));
#402250=CARTESIAN_POINT('Ctrl Pts',(-1.30511984201779,-2.41383169249906,
8.78644465894817));
#402251=CARTESIAN_POINT('Ctrl Pts',(-1.29771440498274,-2.41712942112574,
8.78817647674132));
#402252=CARTESIAN_POINT('Ctrl Pts',(-1.30510689311819,-2.41407762618086,
8.76780923932028));
#402253=CARTESIAN_POINT('Ctrl Pts',(-1.30523427945356,-2.4218749660793,
8.76988516158371));
#402254=CARTESIAN_POINT('Ctrl Pts',(-1.29864530823805,-2.42557926611001,
8.77093053738833));
#402255=CARTESIAN_POINT('Ctrl Pts',(-1.30508753488961,-2.41274173341213,
8.75371302330492));
#402256=CARTESIAN_POINT('Ctrl Pts',(-1.30521255697054,-2.42034768968646,
8.7530082828756));
#402257=CARTESIAN_POINT('Ctrl Pts',(-1.29846328949484,-2.42393125325862,
8.75267964240738));
#402258=CARTESIAN_POINT('Origin',(-1.29238845014159,-2.39909164160958,8.78727029226991));
#402259=CARTESIAN_POINT('Ctrl Pts',(-1.30385128920419,-2.32742558187727,
8.85049129520029));
#402260=CARTESIAN_POINT('Ctrl Pts',(-1.30393589896117,-2.33326458465275,
8.85711686593484));
#402261=CARTESIAN_POINT('Ctrl Pts',(-1.29564064670648,-2.33533570805444,
8.85933012996512));
#402262=CARTESIAN_POINT('Ctrl Pts',(-1.30419707450795,-2.3512885667223,
8.82945683644722));
#402263=CARTESIAN_POINT('Ctrl Pts',(-1.30428238657706,-2.35717603675116,
8.83607469902389));
#402264=CARTESIAN_POINT('Ctrl Pts',(-1.29595369511063,-2.35921685544824,
8.8382956714852));
#402265=CARTESIAN_POINT('Ctrl Pts',(-1.30454234439083,-2.37511598186413,
8.80838214965003));
#402266=CARTESIAN_POINT('Ctrl Pts',(-1.30462799314121,-2.38102668659851,
8.8150136446199));
#402267=CARTESIAN_POINT('Ctrl Pts',(-1.29626693711643,-2.38306176761555,
8.81722098428721));
#402268=CARTESIAN_POINT('Ctrl Pts',(-1.30488713801673,-2.39891053004237,
8.78727029226991));
#402269=CARTESIAN_POINT('Ctrl Pts',(-1.30497280099364,-2.40482221656424,
8.79393457792714));
#402270=CARTESIAN_POINT('Ctrl Pts',(-1.29658037301229,-2.4068732084599,
8.79610912703474));
#402271=CARTESIAN_POINT('Origin',(-1.29135260132905,-2.32760669344448,8.85049129520029));
#402272=CARTESIAN_POINT('Ctrl Pts',(-1.31437432427028,-2.32149911893915,
8.85049129520029));
#402273=CARTESIAN_POINT('Ctrl Pts',(-1.31932364416768,-2.32459836800566,
8.85711686593484));
#402274=CARTESIAN_POINT('Ctrl Pts',(-1.32539494747702,-2.31857839805225,
8.85933012996512));
#402275=CARTESIAN_POINT('Ctrl Pts',(-1.30999573240122,-2.31875725802814,
8.86332496987232));
#402276=CARTESIAN_POINT('Ctrl Pts',(-1.3141529305551,-2.31673993359062,
8.86648636486737));
#402277=CARTESIAN_POINT('Ctrl Pts',(-1.31313656540692,-2.31092245099259,
8.87206031107457));
#402278=CARTESIAN_POINT('Ctrl Pts',(-1.30377592752361,-2.32222479797459,
8.86341338519876));
#402279=CARTESIAN_POINT('Ctrl Pts',(-1.29986873773977,-2.32471625109019,
8.86654584966059));
#402280=CARTESIAN_POINT('Ctrl Pts',(-1.29544436127693,-2.32077302326231,
8.87215952290714));
#402281=CARTESIAN_POINT('Ctrl Pts',(-1.30385128920419,-2.32742558187727,
8.85049129520029));
#402282=CARTESIAN_POINT('Ctrl Pts',(-1.30393589896117,-2.33326458465275,
8.85711686593484));
#402283=CARTESIAN_POINT('Ctrl Pts',(-1.29564064670648,-2.33533570805444,
8.85933012996512));
#402284=CARTESIAN_POINT('Origin',(-1.32100842742437,-2.31090484334613,8.85049129520029));
#402285=CARTESIAN_POINT('Ctrl Pts',(-1.37496718403116,-2.35944218342961,
8.78727029226991));
#402286=CARTESIAN_POINT('Ctrl Pts',(-1.37997811292689,-2.36258001186349,
8.79393457792714));
#402287=CARTESIAN_POINT('Ctrl Pts',(-1.38608257609906,-2.35646650676757,
8.79610912703474));
#402288=CARTESIAN_POINT('Ctrl Pts',(-1.35479818681082,-2.34681241871378,
8.80838214965003));
#402289=CARTESIAN_POINT('Ctrl Pts',(-1.35980828351301,-2.34994972603062,
8.81501364461989));
#402290=CARTESIAN_POINT('Ctrl Pts',(-1.36588287762334,-2.34385480035508,
8.81722098428721));
#402291=CARTESIAN_POINT('Ctrl Pts',(-1.33460133053251,-2.33416520874058,
8.8294568364472));
#402292=CARTESIAN_POINT('Ctrl Pts',(-1.33959173277746,-2.3372901834482,
8.83607469902387));
#402293=CARTESIAN_POINT('Ctrl Pts',(-1.34565445587685,-2.3312259084612,
8.8382956714852));
#402294=CARTESIAN_POINT('Ctrl Pts',(-1.31437432427028,-2.32149911893915,
8.85049129520029));
#402295=CARTESIAN_POINT('Ctrl Pts',(-1.31932364416768,-2.32459836800566,
8.85711686593484));
#402296=CARTESIAN_POINT('Ctrl Pts',(-1.32539494747702,-2.31857839805225,
8.85933012996512));
#402297=CARTESIAN_POINT('Origin',(-1.38160128718526,-2.3488479078366,8.78727029226991));
#402298=CARTESIAN_POINT('Ctrl Pts',(-1.38669498910092,-2.36678607752907,
8.75374538247848));
#402299=CARTESIAN_POINT('Ctrl Pts',(-1.3931284634167,-2.3708301826978,8.75304829418602));
#402300=CARTESIAN_POINT('Ctrl Pts',(-1.39968761886182,-2.36692529818531,
8.75272238421917));
#402301=CARTESIAN_POINT('Ctrl Pts',(-1.38781373054482,-2.36748663052191,
8.7676940844502));
#402302=CARTESIAN_POINT('Ctrl Pts',(-1.39440946688856,-2.37163191905902,
8.76974318093968));
#402303=CARTESIAN_POINT('Ctrl Pts',(-1.40098765781906,-2.36792439139734,
8.7707786988043));
#402304=CARTESIAN_POINT('Ctrl Pts',(-1.38207969920049,-2.36389599497184,
8.78108014887989));
#402305=CARTESIAN_POINT('Ctrl Pts',(-1.38766732642936,-2.36741219451847,
8.78639403366325));
#402306=CARTESIAN_POINT('Ctrl Pts',(-1.39432774009023,-2.36281208956369,
8.78812224174741));
#402307=CARTESIAN_POINT('Ctrl Pts',(-1.37268288764618,-2.35801173591639,
8.78944554828685));
#402308=CARTESIAN_POINT('Ctrl Pts',(-1.37738895133901,-2.36097979624865,
8.79673892988686));
#402309=CARTESIAN_POINT('Ctrl Pts',(-1.3834541258599,-2.35444395564872,
8.79894799272499));
#402310=CARTESIAN_POINT('Origin',(-1.39348601430779,-2.3562900878136,8.75721825406948));
#402311=CARTESIAN_POINT('Origin',(-1.39348601430779,-2.3562900878136,9.));
#402312=CARTESIAN_POINT('Origin',(-1.39348601430779,-2.3562900878136,7.51860402984325));
#402313=CARTESIAN_POINT('Ctrl Pts',(-1.38161790355313,-2.37350050411393,
7.50366195182966));
#402314=CARTESIAN_POINT('Ctrl Pts',(-1.38346014519167,-2.37666531650257,
7.50000065167735));
#402315=CARTESIAN_POINT('Ctrl Pts',(-1.38346014519177,-2.37666531650251,
7.49482233047108));
#402316=CARTESIAN_POINT('Ctrl Pts',(-1.38867182375219,-2.37113491551234,
7.50215800491337));
#402317=CARTESIAN_POINT('Ctrl Pts',(-1.39169926431185,-2.37186928655758,
7.49877273257265));
#402318=CARTESIAN_POINT('Ctrl Pts',(-1.39468274606848,-2.37013262511743,
7.49481816995649));
#402319=CARTESIAN_POINT('Ctrl Pts',(-1.38924060074977,-2.36838055368623,
7.51043025814041));
#402320=CARTESIAN_POINT('Ctrl Pts',(-1.39484851529315,-2.3700066076401,
7.51006209594514));
#402321=CARTESIAN_POINT('Ctrl Pts',(-1.39985114343625,-2.36704811447225,
7.50731281821697));
#402322=CARTESIAN_POINT('Ctrl Pts',(-1.38685063022083,-2.36688356118254,
7.51860402984325));
#402323=CARTESIAN_POINT('Ctrl Pts',(-1.39329931967805,-2.37092279646599,
7.51860402984324));
#402324=CARTESIAN_POINT('Ctrl Pts',(-1.39984896414482,-2.36704940328306,
7.51860402984325));
#402325=CARTESIAN_POINT('Origin',(0.,0.,7.5));
#402326=CARTESIAN_POINT('Origin',(-1.1629348420194,-2.40094160211229,7.5));
#402327=CARTESIAN_POINT('',(-1.1629348420194,-2.40094160211229,7.59394543036555));
#402328=CARTESIAN_POINT('',(-1.1629348420194,-2.40094160211229,8.85049129520029));
#402329=CARTESIAN_POINT('',(-1.1629348420194,-2.40094160211229,7.5));
#402330=CARTESIAN_POINT('',(-1.22097218676269,-2.44268890636151,8.78727029226991));
#402331=CARTESIAN_POINT('Ctrl Pts',(-1.1629348420194,-2.40094160211229,
8.85049129520029));
#402332=CARTESIAN_POINT('Ctrl Pts',(-1.18230874456756,-2.41487759811194,
8.82945686509571));
#402333=CARTESIAN_POINT('Ctrl Pts',(-1.20165384546694,-2.42879287656843,
8.80838212259897));
#402334=CARTESIAN_POINT('Ctrl Pts',(-1.22097218676269,-2.44268890636151,
8.78727029226991));
#402335=CARTESIAN_POINT('',(-1.23235567333045,-2.45087725266273,8.75721825406948));
#402336=CARTESIAN_POINT('Origin',(-1.19809869544859,-2.42623584190782,8.75937679713118));
#402337=CARTESIAN_POINT('',(-1.23235567333045,-2.45087725266273,7.51860402984325));
#402338=CARTESIAN_POINT('',(-1.23235567333045,-2.45087725266273,7.5));
#402339=CARTESIAN_POINT('Ctrl Pts',(-1.23235567333045,-2.45087725266273,
7.51860402984325));
#402340=CARTESIAN_POINT('Ctrl Pts',(-1.22341571509852,-2.44444658017186,
7.52834476460825));
#402341=CARTESIAN_POINT('Ctrl Pts',(-1.21446995317471,-2.43801173298122,
7.53807742314407));
#402342=CARTESIAN_POINT('Ctrl Pts',(-1.20551819269234,-2.43157257091968,
7.54780169004674));
#402343=CARTESIAN_POINT('Ctrl Pts',(-1.19133908788964,-2.42137328622121,
7.5632044032688));
#402344=CARTESIAN_POINT('Ctrl Pts',(-1.17714491544797,-2.41116316309945,
7.57858609112103));
#402345=CARTESIAN_POINT('Ctrl Pts',(-1.1629348420194,-2.40094160211229,
7.59394543036555));
#402346=CARTESIAN_POINT('Origin',(-1.13841252486687,-2.68084313576938,7.5));
#402347=CARTESIAN_POINT('',(-1.14781180121215,-2.49159143565061,8.75721825406948));
#402348=CARTESIAN_POINT('',(-1.14850738206911,-2.47758611705879,8.78727029226991));
#402349=CARTESIAN_POINT('Origin',(-1.15027302572279,-2.44203539474894,8.75658640621031));
#402350=CARTESIAN_POINT('',(-1.1520537178733,-2.40618167532514,8.85049129520029));
#402351=CARTESIAN_POINT('Ctrl Pts',(-1.14850738206911,-2.47758611705879,
8.78727029226991));
#402352=CARTESIAN_POINT('Ctrl Pts',(-1.14968781728229,-2.45381839678239,
8.80838212259896));
#402353=CARTESIAN_POINT('Ctrl Pts',(-1.15086988762439,-2.43001775366009,
8.82945686509571));
#402354=CARTESIAN_POINT('Ctrl Pts',(-1.1520537178733,-2.40618167532514,
8.85049129520029));
#402355=CARTESIAN_POINT('',(-1.1520537178733,-2.40618167532514,7.59394543036555));
#402356=CARTESIAN_POINT('',(-1.1520537178733,-2.40618167532514,7.5));
#402357=CARTESIAN_POINT('',(-1.14781180121215,-2.49159143565061,7.51860402984325));
#402358=CARTESIAN_POINT('Ctrl Pts',(-1.1520537178733,-2.40618167532514,
7.59394543036555));
#402359=CARTESIAN_POINT('Ctrl Pts',(-1.15118542018665,-2.42366459713435,
7.57858609112103));
#402360=CARTESIAN_POINT('Ctrl Pts',(-1.15031809411992,-2.44112795565877,
7.56320440326857));
#402361=CARTESIAN_POINT('Ctrl Pts',(-1.14945168875186,-2.45857277618247,
7.54780169004651));
#402362=CARTESIAN_POINT('Ctrl Pts',(-1.14890469700285,-2.46958629622899,
7.53807742314383));
#402363=CARTESIAN_POINT('Ctrl Pts',(-1.148358071792,-2.48059243613579,7.52834476460825));
#402364=CARTESIAN_POINT('Ctrl Pts',(-1.14781180121215,-2.49159143565061,
7.51860402984325));
#402365=CARTESIAN_POINT('',(-1.14781180121215,-2.49159143565061,7.5));
#402366=CARTESIAN_POINT('Origin',(-1.1589202543844,-2.4065227051503,7.5));
#402367=CARTESIAN_POINT('Ctrl Pts',(-1.1520537178733,-2.40618167532514,
8.85049129520029));
#402368=CARTESIAN_POINT('Ctrl Pts',(-1.15206332432413,-2.40598825222679,
8.85097269580138));
#402369=CARTESIAN_POINT('Ctrl Pts',(-1.15208121062939,-2.40579768676134,
8.85143669361005));
#402370=CARTESIAN_POINT('Ctrl Pts',(-1.15210907085544,-2.4056012857056,
8.8519052845931));
#402371=CARTESIAN_POINT('Ctrl Pts',(-1.15216356369076,-2.40521713769588,
8.85282181883899));
#402372=CARTESIAN_POINT('Ctrl Pts',(-1.15225500672476,-2.40482057420506,
8.85372622499636));
#402373=CARTESIAN_POINT('Ctrl Pts',(-1.152399859333,-2.40440883694516,8.85462257735071));
#402374=CARTESIAN_POINT('Ctrl Pts',(-1.15252011082368,-2.40406702729551,
8.85536669723987));
#402375=CARTESIAN_POINT('Ctrl Pts',(-1.15267716836054,-2.4037146718648,
8.85610498449051));
#402376=CARTESIAN_POINT('Ctrl Pts',(-1.1528877715664,-2.40335342065579,
8.85681338218371));
#402377=CARTESIAN_POINT('Ctrl Pts',(-1.15307889430648,-2.40302558461625,
8.85745625420285));
#402378=CARTESIAN_POINT('Ctrl Pts',(-1.153315995465,-2.4026860085849,8.85808743050666));
#402379=CARTESIAN_POINT('Ctrl Pts',(-1.1536272932187,-2.40233933805946,
8.8586680450841));
#402380=CARTESIAN_POINT('Ctrl Pts',(-1.15377091925415,-2.40217939179392,
8.85893592806395));
#402381=CARTESIAN_POINT('Ctrl Pts',(-1.15393057225672,-2.40201800294867,
8.85919241173848));
#402382=CARTESIAN_POINT('Ctrl Pts',(-1.15411047916769,-2.40185628280406,
8.85943017985535));
#402383=CARTESIAN_POINT('Ctrl Pts',(-1.15435340675565,-2.40163791273454,
8.85975123720001));
#402384=CARTESIAN_POINT('Ctrl Pts',(-1.15463987464168,-2.40141385689638,
8.86004599534706));
#402385=CARTESIAN_POINT('Ctrl Pts',(-1.15497285750656,-2.40119501106982,
8.86026130871721));
#402386=CARTESIAN_POINT('Ctrl Pts',(-1.15509477192118,-2.4011148854428,
8.86034014101236));
#402387=CARTESIAN_POINT('Ctrl Pts',(-1.15522474618014,-2.40103424434313,
8.86040910639693));
#402388=CARTESIAN_POINT('Ctrl Pts',(-1.15535941654965,-2.40095557062527,
8.86046313645507));
#402389=CARTESIAN_POINT('Ctrl Pts',(-1.1555695685334,-2.40083280094742,
8.8605474499083));
#402390=CARTESIAN_POINT('Ctrl Pts',(-1.15579696686364,-2.4007115978283,
8.86059655985669));
#402391=CARTESIAN_POINT('Ctrl Pts',(-1.15602688999811,-2.40059947586523,
8.86059725258816));
#402392=CARTESIAN_POINT('Ctrl Pts',(-1.15625734434688,-2.40048709485562,
8.86059794692011));
#402393=CARTESIAN_POINT('Ctrl Pts',(-1.15649405543566,-2.40038497866228,
8.86056369958366));
#402394=CARTESIAN_POINT('Ctrl Pts',(-1.15672262232883,-2.40029524146196,
8.86048590497774));
#402395=CARTESIAN_POINT('Ctrl Pts',(-1.15678227148269,-2.40027182272448,
8.86046560290182));
#402396=CARTESIAN_POINT('Ctrl Pts',(-1.15684217507605,-2.40024902671321,
8.86044257503091));
#402397=CARTESIAN_POINT('Ctrl Pts',(-1.15690047036322,-2.40022752716396,
8.86041778462584));
#402398=CARTESIAN_POINT('Ctrl Pts',(-1.15729272530748,-2.40008286187622,
8.86025097596201));
#402399=CARTESIAN_POINT('Ctrl Pts',(-1.15766491251364,-2.39997779467967,
8.8599848982295));
#402400=CARTESIAN_POINT('Ctrl Pts',(-1.15800386701871,-2.39990723838852,
8.85968173251461));
#402401=CARTESIAN_POINT('Ctrl Pts',(-1.15818315453212,-2.39986991815289,
8.85952137522076));
#402402=CARTESIAN_POINT('Ctrl Pts',(-1.15835656116864,-2.39984134706458,
8.85934740853961));
#402403=CARTESIAN_POINT('Ctrl Pts',(-1.15852138878529,-2.39982039416741,
8.8591675900182));
#402404=CARTESIAN_POINT('Ctrl Pts',(-1.15918325734184,-2.39973625739415,
8.85844552518696));
#402405=CARTESIAN_POINT('Ctrl Pts',(-1.1597438200588,-2.39976720241301,
8.85759444184126));
#402406=CARTESIAN_POINT('Ctrl Pts',(-1.16019860651595,-2.39983348615085,
8.85683498915141));
#402407=CARTESIAN_POINT('Ctrl Pts',(-1.1602461987075,-2.39984042256749,
8.85675551445));
#402408=CARTESIAN_POINT('Ctrl Pts',(-1.16029262584356,-2.39984776479439,
8.85667699793652));
#402409=CARTESIAN_POINT('Ctrl Pts',(-1.16033787776632,-2.3998554335768,
8.85659965593547));
#402410=CARTESIAN_POINT('Ctrl Pts',(-1.1609486905288,-2.39995894719316,
8.85555568965886));
#402411=CARTESIAN_POINT('Ctrl Pts',(-1.1615207700221,-2.40014664364083,
8.85434650606346));
#402412=CARTESIAN_POINT('Ctrl Pts',(-1.162058881696,-2.4004135457534,8.85297329937117));
#402413=CARTESIAN_POINT('Ctrl Pts',(-1.16236153672494,-2.40056366192913,
8.85220095427747));
#402414=CARTESIAN_POINT('Ctrl Pts',(-1.16265343008713,-2.4007391774561,
8.85137579139184));
#402415=CARTESIAN_POINT('Ctrl Pts',(-1.1629348420194,-2.40094160211229,
8.85049129520029));
#402416=CARTESIAN_POINT('Origin',(-1.1589202543844,-2.4065227051503,7.59394543036555));
#402417=CARTESIAN_POINT('Ctrl Pts',(-1.15208160864078,-2.40562010281996,
7.59443877723642));
#402418=CARTESIAN_POINT('Ctrl Pts',(-1.1523688567101,-2.39983644634716,
7.58783886950016));
#402419=CARTESIAN_POINT('Ctrl Pts',(-1.16071568230795,-2.39828413066546,
7.58559994247159));
#402420=CARTESIAN_POINT('Ctrl Pts',(-1.15051352985788,-2.43719291381971,
7.56670252222137));
#402421=CARTESIAN_POINT('Ctrl Pts',(-1.15080036277219,-2.43141761637255,
7.5600487499903));
#402422=CARTESIAN_POINT('Ctrl Pts',(-1.15919273970383,-2.42983509727514,
7.55786368756705));
#402423=CARTESIAN_POINT('Ctrl Pts',(-1.14894837930544,-2.46870676574944,
7.5388891333356));
#402424=CARTESIAN_POINT('Ctrl Pts',(-1.1492369168818,-2.46289714542674,
7.53222002137277));
#402425=CARTESIAN_POINT('Ctrl Pts',(-1.15767142205792,-2.46132820720179,
7.53005029815326));
#402426=CARTESIAN_POINT('Ctrl Pts',(-1.14738622780757,-2.50016023258599,
7.51101258149734));
#402427=CARTESIAN_POINT('Ctrl Pts',(-1.14767826298364,-2.49428018910865,
7.5043616886572));
#402428=CARTESIAN_POINT('Ctrl Pts',(-1.15615188708088,-2.49276190843518,
7.50217374673251));
#402429=CARTESIAN_POINT('',(-1.15623297039275,-2.49108456570912,7.50366116523517));
#402430=CARTESIAN_POINT('Ctrl Pts',(-1.14781180121215,-2.49159143565061,
7.51860402984325));
#402431=CARTESIAN_POINT('Ctrl Pts',(-1.14778989538006,-2.49203250321947,
7.51734760759494));
#402432=CARTESIAN_POINT('Ctrl Pts',(-1.14782952389185,-2.49243402213687,
7.51608817408573));
#402433=CARTESIAN_POINT('Ctrl Pts',(-1.14794388467726,-2.49279375730838,
7.5148100591312));
#402434=CARTESIAN_POINT('Ctrl Pts',(-1.14804747540941,-2.49311961402288,
7.51365231206384));
#402435=CARTESIAN_POINT('Ctrl Pts',(-1.14821229284573,-2.49341172158019,
7.51247773061043));
#402436=CARTESIAN_POINT('Ctrl Pts',(-1.14846764413724,-2.4936468801771,
7.51129758471022));
#402437=CARTESIAN_POINT('Ctrl Pts',(-1.14878501663036,-2.49393915545693,
7.50983079813401));
#402438=CARTESIAN_POINT('Ctrl Pts',(-1.14924093701577,-2.49412454928837,
7.50839324291155));
#402439=CARTESIAN_POINT('Ctrl Pts',(-1.14986978646771,-2.49412804750393,
7.50715379678855));
#402440=CARTESIAN_POINT('Ctrl Pts',(-1.15016029679465,-2.49412966357871,
7.50658120839351));
#402441=CARTESIAN_POINT('Ctrl Pts',(-1.1505290647192,-2.49408318813144,
7.50598221009429));
#402442=CARTESIAN_POINT('Ctrl Pts',(-1.15096446986736,-2.49396715924152,
7.50545747549611));
#402443=CARTESIAN_POINT('Ctrl Pts',(-1.15119681553147,-2.49390524263443,
7.50517746087247));
#402444=CARTESIAN_POINT('Ctrl Pts',(-1.1514507085445,-2.49382304412448,
7.50491486231392));
#402445=CARTESIAN_POINT('Ctrl Pts',(-1.15171891162188,-2.49372115354552,
7.50468370960992));
#402446=CARTESIAN_POINT('Ctrl Pts',(-1.15211995982243,-2.49356879499041,
7.50433806340447));
#402447=CARTESIAN_POINT('Ctrl Pts',(-1.15256483308989,-2.49336731654838,
7.50405484070984));
#402448=CARTESIAN_POINT('Ctrl Pts',(-1.15302327448637,-2.49312963482937,
7.50385766036131));
#402449=CARTESIAN_POINT('Ctrl Pts',(-1.15307229766794,-2.49310421846394,
7.50383657498791));
#402450=CARTESIAN_POINT('Ctrl Pts',(-1.15312146095907,-2.4930784121598,
7.50381643264937));
#402451=CARTESIAN_POINT('Ctrl Pts',(-1.15317071670641,-2.49305224935014,
7.50379723213559));
#402452=CARTESIAN_POINT('Ctrl Pts',(-1.1534995149326,-2.49287760403721,
7.50366906242519));
#402453=CARTESIAN_POINT('Ctrl Pts',(-1.15383924782791,-2.49268263887218,
7.50358235568538));
#402454=CARTESIAN_POINT('Ctrl Pts',(-1.15416219125878,-2.49248684496702,
7.5035341175365));
#402455=CARTESIAN_POINT('Ctrl Pts',(-1.15464640838322,-2.49219327416583,
7.50346178989176));
#402456=CARTESIAN_POINT('Ctrl Pts',(-1.15515483352959,-2.49185687043632,
7.50346967198527));
#402457=CARTESIAN_POINT('Ctrl Pts',(-1.15564378787674,-2.49151126838677,
7.50354272648693));
#402458=CARTESIAN_POINT('Ctrl Pts',(-1.15584490492048,-2.49136911511025,
7.50357277531559));
#402459=CARTESIAN_POINT('Ctrl Pts',(-1.15604254242823,-2.49122571028613,
7.50361331098761));
#402460=CARTESIAN_POINT('Ctrl Pts',(-1.15623297039335,-2.49108456571041,
7.50366116523658));
#402461=CARTESIAN_POINT('',(-1.16019063351066,-2.40916067458729,7.57603338622103));
#402462=CARTESIAN_POINT('Origin',(-1.16402740803746,-2.41712124308652,7.58486873427627));
#402463=CARTESIAN_POINT('Ctrl Pts',(-1.15623297038464,-2.49108456576589,
7.50366116529969));
#402464=CARTESIAN_POINT('Ctrl Pts',(-1.15755087359535,-2.46382120335537,
7.52783573079709));
#402465=CARTESIAN_POINT('Ctrl Pts',(-1.15887005024774,-2.43651452986229,
7.55196141284068));
#402466=CARTESIAN_POINT('Ctrl Pts',(-1.16019063309948,-2.4091606757699,
7.57603338728831));
#402467=CARTESIAN_POINT('Ctrl Pts',(-1.15217830426507,-2.40721753909579,
7.5963967733137));
#402468=CARTESIAN_POINT('Ctrl Pts',(-1.1501876471192,-2.38904863159187,
7.59959882295471));
#402469=CARTESIAN_POINT('Ctrl Pts',(-1.16353671011163,-2.40155908041819,
7.59642833564546));
#402470=CARTESIAN_POINT('Ctrl Pts',(-1.15113573851764,-2.4034587945253,
7.5870762605742));
#402471=CARTESIAN_POINT('Ctrl Pts',(-1.15450664925665,-2.39758093336444,
7.58809943920598));
#402472=CARTESIAN_POINT('Ctrl Pts',(-1.16120500076186,-2.39850098113831,
7.58710240504253));
#402473=CARTESIAN_POINT('Ctrl Pts',(-1.15646270668161,-2.40638266908519,
7.58015376756929));
#402474=CARTESIAN_POINT('Ctrl Pts',(-1.15754740556005,-2.40374587183485,
7.58205880659762));
#402475=CARTESIAN_POINT('Ctrl Pts',(-1.16026245848246,-2.40449123259747,
7.58020924244126));
#402476=CARTESIAN_POINT('Ctrl Pts',(-1.16019063315141,-2.40916067384176,
7.57603338509286));
#402477=CARTESIAN_POINT('Ctrl Pts',(-1.16019063315141,-2.40916067384176,
7.57603338509286));
#402478=CARTESIAN_POINT('Ctrl Pts',(-1.16019063315141,-2.40916067384176,
7.57603338509286));
#402479=CARTESIAN_POINT('Origin',(-1.16402226679189,-2.41712371898008,7.58486873427622));
#402480=CARTESIAN_POINT('Ctrl Pts',(-1.23934238165743,-2.4559029174225,
7.51098857897448));
#402481=CARTESIAN_POINT('Ctrl Pts',(-1.23456307579885,-2.45246507689652,
7.50433767179957));
#402482=CARTESIAN_POINT('Ctrl Pts',(-1.2280928035716,-2.45814342422544,
7.50214974420965));
#402483=CARTESIAN_POINT('Ctrl Pts',(-1.21376973228739,-2.4375080515231,
7.53887321589169));
#402484=CARTESIAN_POINT('Ctrl Pts',(-1.20904769099473,-2.43411140242769,
7.53220407452063));
#402485=CARTESIAN_POINT('Ctrl Pts',(-1.2025621897978,-2.43972755717505,
7.53003438070912));
#402486=CARTESIAN_POINT('Ctrl Pts',(-1.18814797399718,-2.41907786069558,
7.56669465659233));
#402487=CARTESIAN_POINT('Ctrl Pts',(-1.18345383909065,-2.41570128516483,
7.56004085833299));
#402488=CARTESIAN_POINT('Ctrl Pts',(-1.17698398972327,-2.42127602276314,
7.55785582193789));
#402489=CARTESIAN_POINT('Ctrl Pts',(-1.16247826555639,-2.40061317846372,
7.59443891967696));
#402490=CARTESIAN_POINT('Ctrl Pts',(-1.15777732473869,-2.39723170731885,
7.58783901202978));
#402491=CARTESIAN_POINT('Ctrl Pts',(-1.15135951492375,-2.40278966514233,
7.58560008491213));
#402492=CARTESIAN_POINT('',(-1.22670887334885,-2.45714515960792,7.50366116523517));
#402493=CARTESIAN_POINT('Ctrl Pts',(-1.22670887334902,-2.45714515960826,
7.50366116523554));
#402494=CARTESIAN_POINT('Ctrl Pts',(-1.22744112877596,-2.45695037894576,
7.50350835821027));
#402495=CARTESIAN_POINT('Ctrl Pts',(-1.22810791225206,-2.45674750507575,
7.50345484956));
#402496=CARTESIAN_POINT('Ctrl Pts',(-1.22872922258755,-2.4565310808918,
7.50349758195598));
#402497=CARTESIAN_POINT('Ctrl Pts',(-1.22904800086723,-2.456420039235,7.50351950684424));
#402498=CARTESIAN_POINT('Ctrl Pts',(-1.22938627121607,-2.4562946080529,
7.50357029184313));
#402499=CARTESIAN_POINT('Ctrl Pts',(-1.22970913670001,-2.45616468988571,
7.50365515313924));
#402500=CARTESIAN_POINT('Ctrl Pts',(-1.23020583455546,-2.45596482313552,
7.50378570417639));
#402501=CARTESIAN_POINT('Ctrl Pts',(-1.23068078352655,-2.45574879222655,
7.50400001621911));
#402502=CARTESIAN_POINT('Ctrl Pts',(-1.23109689307203,-2.45553097357611,
7.50428903009635));
#402503=CARTESIAN_POINT('Ctrl Pts',(-1.23114307803023,-2.45550679738171,
7.50432110841318));
#402504=CARTESIAN_POINT('Ctrl Pts',(-1.23118856822059,-2.45548260283481,
7.50435406373354));
#402505=CARTESIAN_POINT('Ctrl Pts',(-1.23123333517556,-2.45545841200071,
7.50438785222352));
#402506=CARTESIAN_POINT('Ctrl Pts',(-1.23150665895339,-2.45531071533093,
7.50459414719561));
#402507=CARTESIAN_POINT('Ctrl Pts',(-1.23175712916614,-2.45516035184146,
7.50483629897752));
#402508=CARTESIAN_POINT('Ctrl Pts',(-1.23197582773583,-2.45501421023925,
7.5050991045531));
#402509=CARTESIAN_POINT('Ctrl Pts',(-1.23245829874675,-2.45469180718625,
7.50567888004914));
#402510=CARTESIAN_POINT('Ctrl Pts',(-1.23280544219417,-2.4543776796122,
7.50637912803145));
#402511=CARTESIAN_POINT('Ctrl Pts',(-1.23304326177524,-2.45408853757672,
7.50710440483569));
#402512=CARTESIAN_POINT('Ctrl Pts',(-1.2331015798579,-2.45401763420935,
7.50728225710685));
#402513=CARTESIAN_POINT('Ctrl Pts',(-1.23315459764784,-2.45394691453314,
7.50746498566954));
#402514=CARTESIAN_POINT('Ctrl Pts',(-1.23320141086251,-2.45387827926384,
7.50764697238949));
#402515=CARTESIAN_POINT('Ctrl Pts',(-1.23345306582123,-2.45350931494506,
7.50862528291181));
#402516=CARTESIAN_POINT('Ctrl Pts',(-1.23355168239988,-2.4531694251973,
7.50965856837421));
#402517=CARTESIAN_POINT('Ctrl Pts',(-1.23356355484103,-2.45285929503312,
7.51067959873201));
#402518=CARTESIAN_POINT('Ctrl Pts',(-1.23357008826037,-2.45268863001259,
7.51124147302578));
#402519=CARTESIAN_POINT('Ctrl Pts',(-1.23354992032897,-2.45252691886292,
7.51180065547252));
#402520=CARTESIAN_POINT('Ctrl Pts',(-1.23351138288628,-2.4523742709769,
7.512351757165));
#402521=CARTESIAN_POINT('Ctrl Pts',(-1.23337822067029,-2.45184681172299,
7.51425603304535));
#402522=CARTESIAN_POINT('Ctrl Pts',(-1.23300397343626,-2.45136616066922,
7.51626900505179));
#402523=CARTESIAN_POINT('Ctrl Pts',(-1.23244762843881,-2.45094509166342,
7.51827788969243));
#402524=CARTESIAN_POINT('Ctrl Pts',(-1.2324175179962,-2.45092230261311,
7.51838661432545));
#402525=CARTESIAN_POINT('Ctrl Pts',(-1.23238686422244,-2.45089968883142,
7.51849533314856));
#402526=CARTESIAN_POINT('Ctrl Pts',(-1.23235567333046,-2.45087725266273,
7.51860402984325));
#402527=CARTESIAN_POINT('Ctrl Pts',(-1.16019063469236,-2.40916067500414,
7.57603338728984));
#402528=CARTESIAN_POINT('Ctrl Pts',(-1.18240010893415,-2.42518305082722,
7.55196141284921));
#402529=CARTESIAN_POINT('Ctrl Pts',(-1.20457181916034,-2.44117710944838,
7.52783573083105));
#402530=CARTESIAN_POINT('Ctrl Pts',(-1.22670887339983,-2.45714515963799,
7.50366116530176));
#402531=CARTESIAN_POINT('Origin',(-4.00899494394867E-16,-8.32476377985987E-16,
7.49482233047033));
#402532=CARTESIAN_POINT('Origin',(-1.15251174268203,-2.4830672429437,7.49482233047033));
#402533=CARTESIAN_POINT('Origin',(0.,0.,7.50366116523517));
#402534=CARTESIAN_POINT('Origin',(-1.22276082553376,-2.4492370676478,7.49482233047033));
#402535=CARTESIAN_POINT('Ctrl Pts',(-1.14781185363497,-2.49159037923024,
7.51860402984325));
#402536=CARTESIAN_POINT('Ctrl Pts',(-1.14743505922584,-2.49919000501071,
7.51860402984325));
#402537=CARTESIAN_POINT('Ctrl Pts',(-1.14051133179101,-2.50234567996836,
7.51860402984325));
#402538=CARTESIAN_POINT('Ctrl Pts',(-1.14767194603031,-2.49441217208215,
7.51041458714365));
#402539=CARTESIAN_POINT('Ctrl Pts',(-1.14579474478775,-2.49993761154477,
7.51004642900441));
#402540=CARTESIAN_POINT('Ctrl Pts',(-1.14050942230919,-2.50234655026605,
7.50729136483009));
#402541=CARTESIAN_POINT('Ctrl Pts',(-1.15026273737235,-2.49551287068815,
7.50215815450138));
#402542=CARTESIAN_POINT('Ctrl Pts',(-1.14913464688838,-2.49841553779643,
7.49877163671531));
#402543=CARTESIAN_POINT('Ctrl Pts',(-1.1460051215579,-2.49986811991121,
7.49481588533171));
#402544=CARTESIAN_POINT('Ctrl Pts',(-1.15623273862022,-2.49108406635796,
7.50366171572174));
#402545=CARTESIAN_POINT('Ctrl Pts',(-1.15777435337956,-2.49440544953232,
7.50000045605858));
#402546=CARTESIAN_POINT('Ctrl Pts',(-1.15777435337945,-2.49440544953238,
7.49482233047317));
#402547=CARTESIAN_POINT('Origin',(-1.13532718937378,-2.49097138142305,7.51860402984325));
#402548=CARTESIAN_POINT('Origin',(-1.13532718937378,-2.49097138142305,9.));
#402549=CARTESIAN_POINT('Origin',(-1.13532718937378,-2.49097138142305,8.75721825406948));
#402550=CARTESIAN_POINT('Ctrl Pts',(-1.14864017147867,-2.4749118318261,
8.78942910404913));
#402551=CARTESIAN_POINT('Ctrl Pts',(-1.14838393822148,-2.48047840826226,
8.79672699501689));
#402552=CARTESIAN_POINT('Ctrl Pts',(-1.13954364374201,-2.48171237726442,
8.79893251111267));
#402553=CARTESIAN_POINT('Ctrl Pts',(-1.14809480925301,-2.48589263319865,
8.78111911759581));
#402554=CARTESIAN_POINT('Ctrl Pts',(-1.14778360579387,-2.49249153178346,
8.78644465894816));
#402555=CARTESIAN_POINT('Ctrl Pts',(-1.14018209782489,-2.49530801689311,
8.78817647674132));
#402556=CARTESIAN_POINT('Ctrl Pts',(-1.14775492647408,-2.49273613052926,
8.7678092393203));
#402557=CARTESIAN_POINT('Ctrl Pts',(-1.14738247379801,-2.50052561162717,
8.76988516158372));
#402558=CARTESIAN_POINT('Ctrl Pts',(-1.14056970501268,-2.50380014394096,
8.77093053738833));
#402559=CARTESIAN_POINT('Ctrl Pts',(-1.14782119896262,-2.49140174220956,
8.75371302330492));
#402560=CARTESIAN_POINT('Ctrl Pts',(-1.14745864888062,-2.49900008142322,
8.7530082828756));
#402561=CARTESIAN_POINT('Ctrl Pts',(-1.14049364879242,-2.50214385512781,
8.75267964240737));
#402562=CARTESIAN_POINT('Origin',(-1.13602277023073,-2.47696606283122,8.78727029226991));
#402563=CARTESIAN_POINT('Ctrl Pts',(-1.1520537178733,-2.40618167532514,
8.85049129520029));
#402564=CARTESIAN_POINT('Ctrl Pts',(-1.15176404759815,-2.41201410220894,
8.85711686593484));
#402565=CARTESIAN_POINT('Ctrl Pts',(-1.14335314149693,-2.41354949162872,
8.85933012996512));
#402566=CARTESIAN_POINT('Ctrl Pts',(-1.15086988603564,-2.430017785649,8.82945683644723));
#402567=CARTESIAN_POINT('Ctrl Pts',(-1.15057781132208,-2.43589862520228,
8.8360746990239));
#402568=CARTESIAN_POINT('Ctrl Pts',(-1.14213547634264,-2.43740162972406,
8.8382956714852));
#402569=CARTESIAN_POINT('Ctrl Pts',(-1.14968781879481,-2.45381836632827,
8.80838214965003));
#402570=CARTESIAN_POINT('Ctrl Pts',(-1.14939459141806,-2.45972241442018,
8.81501364461993));
#402571=CARTESIAN_POINT('Ctrl Pts',(-1.14092032599118,-2.46121761944619,
8.81722098428721));
#402572=CARTESIAN_POINT('Ctrl Pts',(-1.14850738206911,-2.47758611705879,
8.78727029226991));
#402573=CARTESIAN_POINT('Ctrl Pts',(-1.14821410598632,-2.48349114583244,
8.79393457792714));
#402574=CARTESIAN_POINT('Ctrl Pts',(-1.13970751364641,-2.48500021903835,
8.79610912703474));
#402575=CARTESIAN_POINT('Origin',(-1.13956910603492,-2.40556162109758,8.85049129520029));
#402576=CARTESIAN_POINT('Ctrl Pts',(-1.1629348420194,-2.40094160211229,
8.85049129520029));
#402577=CARTESIAN_POINT('Ctrl Pts',(-1.16767542343879,-2.40435158745378,
8.85711686593484));
#402578=CARTESIAN_POINT('Ctrl Pts',(-1.17411995340352,-2.39873297591288,
8.85933012996512));
#402579=CARTESIAN_POINT('Ctrl Pts',(-1.15874091806867,-2.39792483730433,
8.86332496987231));
#402580=CARTESIAN_POINT('Ctrl Pts',(-1.16301882523356,-2.39617801027643,
8.86648636486737));
#402581=CARTESIAN_POINT('Ctrl Pts',(-1.16237727570637,-2.39030736158171,
8.87206031107457));
#402582=CARTESIAN_POINT('Ctrl Pts',(-1.15231172640009,-2.40098674855131,
8.86341338519876));
#402583=CARTESIAN_POINT('Ctrl Pts',(-1.1482529364075,-2.40322274820032,
8.86654584966058));
#402584=CARTESIAN_POINT('Ctrl Pts',(-1.144090293775,-2.39900415138368,8.87215952290714));
#402585=CARTESIAN_POINT('Ctrl Pts',(-1.1520537178733,-2.40618167532514,
8.85049129520029));
#402586=CARTESIAN_POINT('Ctrl Pts',(-1.15176404759815,-2.41201410220893,
8.85711686593484));
#402587=CARTESIAN_POINT('Ctrl Pts',(-1.14335314149693,-2.41354949162871,
8.85933012996512));
#402588=CARTESIAN_POINT('Origin',(-1.17023409226484,-2.39079414204317,8.85049129520029));
#402589=CARTESIAN_POINT('Ctrl Pts',(-1.22097218676269,-2.44268890636151,
8.78727029226991));
#402590=CARTESIAN_POINT('Ctrl Pts',(-1.22577177880956,-2.446141339107,8.79393457792714));
#402591=CARTESIAN_POINT('Ctrl Pts',(-1.23225539332379,-2.44043150916128,
8.79610912703474));
#402592=CARTESIAN_POINT('Ctrl Pts',(-1.20165382071392,-2.42879285876314,
8.80838214965003));
#402593=CARTESIAN_POINT('Ctrl Pts',(-1.20645261566517,-2.43224471814342,
8.81501364461989));
#402594=CARTESIAN_POINT('Ctrl Pts',(-1.2129052320992,-2.42655151572731,
8.81722098428722));
#402595=CARTESIAN_POINT('Ctrl Pts',(-1.18230877056806,-2.41487761681456,
8.82945683644724));
#402596=CARTESIAN_POINT('Ctrl Pts',(-1.18708870167944,-2.41831590709611,
8.8360746990239));
#402597=CARTESIAN_POINT('Ctrl Pts',(-1.19352750769642,-2.41265253181512,
8.8382956714852));
#402598=CARTESIAN_POINT('Ctrl Pts',(-1.1629348420194,-2.40094160211229,
8.85049129520029));
#402599=CARTESIAN_POINT('Ctrl Pts',(-1.16767542343879,-2.40435158745378,
8.85711686593484));
#402600=CARTESIAN_POINT('Ctrl Pts',(-1.17411995340352,-2.39873297591288,
8.85933012996512));
#402601=CARTESIAN_POINT('Origin',(-1.22827143700814,-2.43254144629239,8.78727029226991));
#402602=CARTESIAN_POINT('Ctrl Pts',(-1.23220537088867,-2.45076911469362,
8.75374538247848));
#402603=CARTESIAN_POINT('Ctrl Pts',(-1.2383665202337,-2.45521710492921,
8.75304829418601));
#402604=CARTESIAN_POINT('Ctrl Pts',(-1.24516238600019,-2.45174048995301,
8.75272238421917));
#402605=CARTESIAN_POINT('Ctrl Pts',(-1.23327692917392,-2.45153990633562,
8.76769408445022));
#402606=CARTESIAN_POINT('Ctrl Pts',(-1.2395935243215,-2.45609926821132,
8.76974318093971));
#402607=CARTESIAN_POINT('Ctrl Pts',(-1.2463957417661,-2.45282082420285,
8.7707786988043));
#402608=CARTESIAN_POINT('Ctrl Pts',(-1.22778473182153,-2.44758926748178,
8.78108014887988));
#402609=CARTESIAN_POINT('Ctrl Pts',(-1.23313559499255,-2.45145624312503,
8.78639403366323));
#402610=CARTESIAN_POINT('Ctrl Pts',(-1.2400770538556,-2.44729232374767,
8.78812224174741));
#402611=CARTESIAN_POINT('Ctrl Pts',(-1.21878423279646,-2.44111504248424,
8.78944554828686));
#402612=CARTESIAN_POINT('Ctrl Pts',(-1.22329046309831,-2.44437852315427,
8.79673892988686));
#402613=CARTESIAN_POINT('Ctrl Pts',(-1.22976192881266,-2.43824470820559,
8.79894799272499));
#402614=CARTESIAN_POINT('Origin',(-1.2396549235759,-2.44072979259361,8.75721825406948));
#402615=CARTESIAN_POINT('Origin',(-1.2396549235759,-2.44072979259361,9.));
#402616=CARTESIAN_POINT('Origin',(-1.2396549235759,-2.44072979259361,7.51860402984325));
#402617=CARTESIAN_POINT('Ctrl Pts',(-1.22670852196932,-2.45714445578104,
7.50366195182966));
#402618=CARTESIAN_POINT('Ctrl Pts',(-1.22834420829888,-2.46042079855024,
7.50000065167735));
#402619=CARTESIAN_POINT('Ctrl Pts',(-1.22834420829899,-2.46042079855019,
7.49482233047108));
#402620=CARTESIAN_POINT('Ctrl Pts',(-1.23389951291487,-2.45523567375381,
7.50215800491337));
#402621=CARTESIAN_POINT('Ctrl Pts',(-1.2368736819588,-2.45616250473761,
7.49877273257265));
#402622=CARTESIAN_POINT('Ctrl Pts',(-1.2399623021127,-2.45462056378711,
7.49481816995647));
#402623=CARTESIAN_POINT('Ctrl Pts',(-1.23464359386723,-2.45252341272685,
7.51043025814041));
#402624=CARTESIAN_POINT('Ctrl Pts',(-1.24013580471421,-2.45450542609691,
7.51006209594514));
#402625=CARTESIAN_POINT('Ctrl Pts',(-1.24531770572932,-2.45187353095617,
7.50731281821699));
#402626=CARTESIAN_POINT('Ctrl Pts',(-1.23235444642809,-2.45087637001726,
7.51860402984325));
#402627=CARTESIAN_POINT('Ctrl Pts',(-1.23853109166802,-2.45532047521073,
7.51860402984325));
#402628=CARTESIAN_POINT('Ctrl Pts',(-1.24531544834109,-2.4518746774913,
7.51860402984325));
#402629=CARTESIAN_POINT('Origin',(0.,0.,7.5));
#402630=CARTESIAN_POINT('Origin',(-1.00671661105392,-2.47051810124199,7.5));
#402631=CARTESIAN_POINT('',(-1.00671661105392,-2.47051810124199,7.59394543036555));
#402632=CARTESIAN_POINT('',(-1.00671661105392,-2.47051810124199,8.85049129520029));
#402633=CARTESIAN_POINT('',(-1.00671661105392,-2.47051810124199,7.5));
#402634=CARTESIAN_POINT('',(-1.0619599528811,-2.51589809662205,8.78727029226991));
#402635=CARTESIAN_POINT('Ctrl Pts',(-1.00671661105392,-2.47051810124199,
8.85049129520029));
#402636=CARTESIAN_POINT('Ctrl Pts',(-1.0251578255121,-2.48566675444137,
8.82945686509571));
#402637=CARTESIAN_POINT('Ctrl Pts',(-1.04357162487512,-2.50079288733603,
8.80838212259896));
#402638=CARTESIAN_POINT('Ctrl Pts',(-1.0619599528811,-2.51589809662205,
8.78727029226991));
#402639=CARTESIAN_POINT('',(-1.07279542170604,-2.52479896157614,8.75721825406948));
#402640=CARTESIAN_POINT('Origin',(-1.04018760906769,-2.49801332713423,8.75937679713151));
#402641=CARTESIAN_POINT('',(-1.07279542170604,-2.52479896157614,7.51860402984325));
#402642=CARTESIAN_POINT('',(-1.07279542170604,-2.52479896157614,7.5));
#402643=CARTESIAN_POINT('Ctrl Pts',(-1.07279542170604,-2.52479896157614,
7.51860402984325));
#402644=CARTESIAN_POINT('Ctrl Pts',(-1.06428584617822,-2.51780871650105,
7.52834476460825));
#402645=CARTESIAN_POINT('Ctrl Pts',(-1.05577074635675,-2.51081393345974,
7.53807742314407));
#402646=CARTESIAN_POINT('Ctrl Pts',(-1.04724993675614,-2.50381446008393,
7.54780169004674));
#402647=CARTESIAN_POINT('Ctrl Pts',(-1.03375343485924,-2.49272767254591,
7.5632044032688));
#402648=CARTESIAN_POINT('Ctrl Pts',(-1.02024259070161,-2.48162910346635,
7.57858609112102));
#402649=CARTESIAN_POINT('Ctrl Pts',(-1.00671661105392,-2.47051810124199,
7.59394543036555));
#402650=CARTESIAN_POINT('Origin',(-0.964311324797644,-2.74827339692444,
7.5));
#402651=CARTESIAN_POINT('',(-0.985816687379938,-2.56001274842385,8.75721825406948));
#402652=CARTESIAN_POINT('',(-0.987408162934497,-2.54608077127965,8.78727029226991));
#402653=CARTESIAN_POINT('Origin',(-0.991447921482891,-2.51071621691815,
8.75658640621013));
#402654=CARTESIAN_POINT('',(-0.995522110700908,-2.47505025214475,8.85049129520029));
#402655=CARTESIAN_POINT('Ctrl Pts',(-0.987408162934496,-2.54608077127965,
8.78727029226991));
#402656=CARTESIAN_POINT('Ctrl Pts',(-0.990108975883482,-2.52243751507743,
8.80838212259897));
#402657=CARTESIAN_POINT('Ctrl Pts',(-0.992813529975814,-2.49876150843588,
8.82945686509571));
#402658=CARTESIAN_POINT('Ctrl Pts',(-0.995522110700908,-2.47505025214475,
8.85049129520029));
#402659=CARTESIAN_POINT('',(-0.995522110700908,-2.47505025214475,7.59394543036555));
#402660=CARTESIAN_POINT('',(-0.995522110700908,-2.47505025214475,7.5));
#402661=CARTESIAN_POINT('',(-0.985816687379938,-2.56001274842385,7.51860402984325));
#402662=CARTESIAN_POINT('Ctrl Pts',(-0.995522110700909,-2.47505025214475,
7.59394543036555));
#402663=CARTESIAN_POINT('Ctrl Pts',(-0.993535462378759,-2.49244162139227,
7.57858609112103));
#402664=CARTESIAN_POINT('Ctrl Pts',(-0.991551037104199,-2.50981352980177,
7.56320440326857));
#402665=CARTESIAN_POINT('Ctrl Pts',(-0.989568718370413,-2.52716699728824,
7.54780169004651));
#402666=CARTESIAN_POINT('Ctrl Pts',(-0.988317211822469,-2.53812284299494,
7.53807742314383));
#402667=CARTESIAN_POINT('Ctrl Pts',(-0.987066543906777,-2.54907134720939,
7.52834476460825));
#402668=CARTESIAN_POINT('Ctrl Pts',(-0.985816687379938,-2.56001274842385,
7.51860402984325));
#402669=CARTESIAN_POINT('',(-0.985816687379938,-2.56001274842385,7.5));
#402670=CARTESIAN_POINT('Origin',(-1.0023526893204,-2.47583052179233,7.5));
#402671=CARTESIAN_POINT('Ctrl Pts',(-0.995522110700909,-2.47505025214475,
8.85049129520029));
#402672=CARTESIAN_POINT('Ctrl Pts',(-0.995544090074723,-2.47485784194232,
8.85097269580139));
#402673=CARTESIAN_POINT('Ctrl Pts',(-0.995574149201944,-2.47466881399357,
8.85143669361005));
#402674=CARTESIAN_POINT('Ctrl Pts',(-0.995614535645016,-2.47447460147567,
8.8519052845931));
#402675=CARTESIAN_POINT('Ctrl Pts',(-0.995693528966451,-2.47409473410718,
8.85282181883899));
#402676=CARTESIAN_POINT('Ctrl Pts',(-0.995810192031023,-2.4737048441739,
8.85372622499635));
#402677=CARTESIAN_POINT('Ctrl Pts',(-0.995981127120858,-2.47330323361082,
8.8546225773507));
#402678=CARTESIAN_POINT('Ctrl Pts',(-0.996123031361399,-2.47296983078522,
8.85536669723986));
#402679=CARTESIAN_POINT('Ctrl Pts',(-0.996302341696657,-2.47262826201747,
8.85610498449051));
#402680=CARTESIAN_POINT('Ctrl Pts',(-0.996535657640079,-2.47228124643154,
8.8568133821837));
#402681=CARTESIAN_POINT('Ctrl Pts',(-0.996747392225165,-2.47196632924231,
8.85745625420284));
#402682=CARTESIAN_POINT('Ctrl Pts',(-0.997005762944949,-2.47164264202971,
8.85808743050666));
#402683=CARTESIAN_POINT('Ctrl Pts',(-0.997338632360855,-2.47131662869161,
8.8586680450841));
#402684=CARTESIAN_POINT('Ctrl Pts',(-0.997492211093629,-2.47116621320451,
8.85893592806395));
#402685=CARTESIAN_POINT('Ctrl Pts',(-0.997661876290801,-2.47101538495295,
8.85919241173848));
#402686=CARTESIAN_POINT('Ctrl Pts',(-0.997851775008971,-2.47086552375508,
8.85943017985534));
#402687=CARTESIAN_POINT('Ctrl Pts',(-0.998108194494538,-2.4706631667743,
8.8597512372));
#402688=CARTESIAN_POINT('Ctrl Pts',(-0.998408429108412,-2.47045792534336,
8.86004599534705));
#402689=CARTESIAN_POINT('Ctrl Pts',(-0.998754749324536,-2.47026086344443,
8.86026130871721));
#402690=CARTESIAN_POINT('Ctrl Pts',(-0.99888154691946,-2.47018871352746,
8.86034014101235));
#402691=CARTESIAN_POINT('Ctrl Pts',(-0.999016420825366,-2.47011656559295,
8.86040910639692));
#402692=CARTESIAN_POINT('Ctrl Pts',(-0.999155855142562,-2.47004668187887,
8.86046313645506));
#402693=CARTESIAN_POINT('Ctrl Pts',(-0.999373441226795,-2.46993762892833,
8.86054744990829));
#402694=CARTESIAN_POINT('Ctrl Pts',(-0.999608137853282,-2.46983124429506,
8.86059655985668));
#402695=CARTESIAN_POINT('Ctrl Pts',(-0.99984477226485,-2.46973408392438,
8.86059725258816));
#402696=CARTESIAN_POINT('Ctrl Pts',(-1.00008195339645,-2.46963669907444,
8.86059794692011));
#402697=CARTESIAN_POINT('Ctrl Pts',(-1.00032472074388,-2.46954995882129,
8.86056369958366));
#402698=CARTESIAN_POINT('Ctrl Pts',(-1.00055856750402,-2.46947505032681,
8.86048590497774));
#402699=CARTESIAN_POINT('Ctrl Pts',(-1.00061959454596,-2.46945550144004,
8.86046560290182));
#402700=CARTESIAN_POINT('Ctrl Pts',(-1.00068083560641,-2.46943659030202,
8.86044257503091));
#402701=CARTESIAN_POINT('Ctrl Pts',(-1.00074038860052,-2.46941886991778,
8.86041778462583));
#402702=CARTESIAN_POINT('Ctrl Pts',(-1.00114110635174,-2.46929963372096,
8.86025097596201));
#402703=CARTESIAN_POINT('Ctrl Pts',(-1.00151926053775,-2.4692186285124,
8.8599848982295));
#402704=CARTESIAN_POINT('Ctrl Pts',(-1.00186203918154,-2.46916993407642,
8.85968173251461));
#402705=CARTESIAN_POINT('Ctrl Pts',(-1.00204334944522,-2.46914417750964,
8.85952137522076));
#402706=CARTESIAN_POINT('Ctrl Pts',(-1.00221823035513,-2.46912677532505,
8.85934740853961));
#402707=CARTESIAN_POINT('Ctrl Pts',(-1.0023840617725,-2.4691164260195,8.8591675900182));
#402708=CARTESIAN_POINT('Ctrl Pts',(-1.00304996111069,-2.46907486817829,
8.85844552518695));
#402709=CARTESIAN_POINT('Ctrl Pts',(-1.00360738943727,-2.46914166499387,
8.85759444184123));
#402710=CARTESIAN_POINT('Ctrl Pts',(-1.00405699467321,-2.46923695081302,
8.85683498915137));
#402711=CARTESIAN_POINT('Ctrl Pts',(-1.00410404466375,-2.46924692222023,
8.85675551444997));
#402712=CARTESIAN_POINT('Ctrl Pts',(-1.00414990599218,-2.46925722395855,
8.85667699793651));
#402713=CARTESIAN_POINT('Ctrl Pts',(-1.00419457359943,-2.46926777628528,
8.85659965593547));
#402714=CARTESIAN_POINT('Ctrl Pts',(-1.0047974992414,-2.46941021212986,
8.85555568965886));
#402715=CARTESIAN_POINT('Ctrl Pts',(-1.00535637758334,-2.46963417619404,
8.85434650606346));
#402716=CARTESIAN_POINT('Ctrl Pts',(-1.00587628317203,-2.4699350068609,
8.85297329937117));
#402717=CARTESIAN_POINT('Ctrl Pts',(-1.00616869838735,-2.47010420578113,
8.85220095427747));
#402718=CARTESIAN_POINT('Ctrl Pts',(-1.00644874670489,-2.47029806236456,
8.85137579139183));
#402719=CARTESIAN_POINT('Ctrl Pts',(-1.00671661105392,-2.47051810124199,
8.85049129520029));
#402720=CARTESIAN_POINT('Origin',(-1.0023526893204,-2.47583052179233,7.59394543036555));
#402721=CARTESIAN_POINT('Ctrl Pts',(-0.995585924237762,-2.47449162041812,
7.59443877723642));
#402722=CARTESIAN_POINT('Ctrl Pts',(-0.996243142267619,-2.46873825113483,
7.58783886950016));
#402723=CARTESIAN_POINT('Ctrl Pts',(-1.00467227562429,-2.46772390780438,
7.58559994247159));
#402724=CARTESIAN_POINT('Ctrl Pts',(-0.991998190294734,-2.50589909453893,
7.56670252222135));
#402725=CARTESIAN_POINT('Ctrl Pts',(-0.992654458457976,-2.50015404050765,
7.56004874999025));
#402726=CARTESIAN_POINT('Ctrl Pts',(-1.00113098469781,-2.49911247430166,
7.55786368756704));
#402727=CARTESIAN_POINT('Ctrl Pts',(-0.988417156086389,-2.53724791833978,
7.53888913333556));
#402728=CARTESIAN_POINT('Ctrl Pts',(-0.989077324483434,-2.53146872117112,
7.53222002137274));
#402729=CARTESIAN_POINT('Ctrl Pts',(-0.997595022281296,-2.5304434071001,
7.53005029815327));
#402730=CARTESIAN_POINT('Ctrl Pts',(-0.98484298365694,-2.56853667326526,
7.51101258149734));
#402731=CARTESIAN_POINT('Ctrl Pts',(-0.985511154494509,-2.56268742172586,
7.5043616886572));
#402732=CARTESIAN_POINT('Ctrl Pts',(-0.994064645198984,-2.56171516748281,
7.50217374673251));
#402733=CARTESIAN_POINT('',(-0.99425302963394,-2.56004646606291,7.50366116523517));
#402734=CARTESIAN_POINT('Ctrl Pts',(-0.985816687379937,-2.56001274842385,
7.51860402984325));
#402735=CARTESIAN_POINT('Ctrl Pts',(-0.985766567259559,-2.5604515062606,
7.51734760759493));
#402736=CARTESIAN_POINT('Ctrl Pts',(-0.985780388944966,-2.56085473922179,
7.51608817408572));
#402737=CARTESIAN_POINT('Ctrl Pts',(-0.985871466452295,-2.56122106239948,
7.51481005913119));
#402738=CARTESIAN_POINT('Ctrl Pts',(-0.985953966634802,-2.56155288668741,
7.51365231206383));
#402739=CARTESIAN_POINT('Ctrl Pts',(-0.986099730040565,-2.56185495396782,
7.51247773061042));
#402740=CARTESIAN_POINT('Ctrl Pts',(-0.986339490022423,-2.56210598981959,
7.51129758471022));
#402741=CARTESIAN_POINT('Ctrl Pts',(-0.98663748429825,-2.56241799871396,
7.50983079813402));
#402742=CARTESIAN_POINT('Ctrl Pts',(-0.987080589722761,-2.56263222255328,
7.50839324291155));
#402743=CARTESIAN_POINT('Ctrl Pts',(-0.987707923004627,-2.5626760041041,
7.50715379678855));
#402744=CARTESIAN_POINT('Ctrl Pts',(-0.987997732904675,-2.56269622991904,
7.50658120839351));
#402745=CARTESIAN_POINT('Ctrl Pts',(-0.988368720848104,-2.5626734770026,
7.50598221009429));
#402746=CARTESIAN_POINT('Ctrl Pts',(-0.988810665406192,-2.5625855830101,
7.50545747549611));
#402747=CARTESIAN_POINT('Ctrl Pts',(-0.989046500701851,-2.56253868005513,
7.50517746087247));
#402748=CARTESIAN_POINT('Ctrl Pts',(-0.989305138541066,-2.56247291741204,
7.50491486231392));
#402749=CARTESIAN_POINT('Ctrl Pts',(-0.989579318718269,-2.56238842000836,
7.50468370960993));
#402750=CARTESIAN_POINT('Ctrl Pts',(-0.989989304568424,-2.56226206973668,
7.50433806340447));
#402751=CARTESIAN_POINT('Ctrl Pts',(-0.990446172564147,-2.56208950838183,
7.50405484070984));
#402752=CARTESIAN_POINT('Ctrl Pts',(-0.990918900363643,-2.56188168744652,
7.50385766036131));
#402753=CARTESIAN_POINT('Ctrl Pts',(-0.990969451253942,-2.56185946422776,
7.50383657498791));
#402754=CARTESIAN_POINT('Ctrl Pts',(-0.9910201669494,-2.56183686084833,
7.50381643264937));
#402755=CARTESIAN_POINT('Ctrl Pts',(-0.991070997752494,-2.56181390761953,
7.50379723213559));
#402756=CARTESIAN_POINT('Ctrl Pts',(-0.991410309991077,-2.56166068730881,
7.50366906242519));
#402757=CARTESIAN_POINT('Ctrl Pts',(-0.991761836329731,-2.56148788948195,
7.50358235568538));
#402758=CARTESIAN_POINT('Ctrl Pts',(-0.992096660797257,-2.56131318891303,
7.5035341175365));
#402759=CARTESIAN_POINT('Ctrl Pts',(-0.992598692191497,-2.56105124518222,
7.50346178989176));
#402760=CARTESIAN_POINT('Ctrl Pts',(-0.993127626184824,-2.56074810754123,
7.50346967198527));
#402761=CARTESIAN_POINT('Ctrl Pts',(-0.99363771872217,-2.56043454298073,
7.50354272648692));
#402762=CARTESIAN_POINT('Ctrl Pts',(-0.993847530341072,-2.5603055673866,
7.50357277531559));
#402763=CARTESIAN_POINT('Ctrl Pts',(-0.994053949759997,-2.56017511988167,
7.50361331098761));
#402764=CARTESIAN_POINT('Ctrl Pts',(-0.994253029634453,-2.56004646606423,
7.50366116523659));
#402765=CARTESIAN_POINT('',(-1.00345144303437,-2.47854446470827,7.57603338622103));
#402766=CARTESIAN_POINT('Origin',(-1.00677029912175,-2.48673450035405,7.58486873427628));
#402767=CARTESIAN_POINT('Ctrl Pts',(-0.994253029622211,-2.56004646611904,
7.50366116529969));
#402768=CARTESIAN_POINT('Ctrl Pts',(-0.997314994686491,-2.5329235575592,
7.52783573079709));
#402769=CARTESIAN_POINT('Ctrl Pts',(-1.00038100552661,-2.50575750849375,
7.55196141284068));
#402770=CARTESIAN_POINT('Ctrl Pts',(-1.00345144254827,-2.47854446586211,
7.57603338728831));
#402771=CARTESIAN_POINT('Ctrl Pts',(-0.995580073096921,-2.47609196989964,
7.59639677331372));
#402772=CARTESIAN_POINT('Ctrl Pts',(-0.994718951965595,-2.45697504293775,
7.59974925422226));
#402773=CARTESIAN_POINT('Ctrl Pts',(-1.00739967866913,-2.47130674194168,
7.59639677331372));
#402774=CARTESIAN_POINT('Ctrl Pts',(-0.994780473004169,-2.47227415065623,
7.58707626057422));
#402775=CARTESIAN_POINT('Ctrl Pts',(-0.998585879238811,-2.46652642806453,
7.58811717123965));
#402776=CARTESIAN_POINT('Ctrl Pts',(-1.00531808064709,-2.4680079461374,
7.58707626057422));
#402777=CARTESIAN_POINT('Ctrl Pts',(-0.999909163054398,-2.47553331782441,
7.5801537675693));
#402778=CARTESIAN_POINT('Ctrl Pts',(-1.00117949275385,-2.47293270359068,
7.58208760766041));
#402779=CARTESIAN_POINT('Ctrl Pts',(-1.00390123521108,-2.47391710692992,
7.58015376756931));
#402780=CARTESIAN_POINT('Ctrl Pts',(-1.00345144272362,-2.47854446394126,
7.57603338509286));
#402781=CARTESIAN_POINT('Ctrl Pts',(-1.00345144272362,-2.47854446394126,
7.57603338509286));
#402782=CARTESIAN_POINT('Ctrl Pts',(-1.00345144272362,-2.47854446394126,
7.57603338509286));
#402783=CARTESIAN_POINT('Origin',(-1.00676500980816,-2.48673664175991,7.58486873427621));
#402784=CARTESIAN_POINT('Ctrl Pts',(-1.07944577964472,-2.5302619405081,
7.51098857897448));
#402785=CARTESIAN_POINT('Ctrl Pts',(-1.07489655658137,-2.52652495221648,
7.50433767179956));
#402786=CARTESIAN_POINT('Ctrl Pts',(-1.06807576525986,-2.53177708100687,
7.50214974420965));
#402787=CARTESIAN_POINT('Ctrl Pts',(-1.05510423513016,-2.51026642356291,
7.53887321589169));
#402788=CARTESIAN_POINT('Ctrl Pts',(-1.0506095198325,-2.50657421102301,
7.53220407452063));
#402789=CARTESIAN_POINT('Ctrl Pts',(-1.04377751552323,-2.51176329928973,
7.53003438070911));
#402790=CARTESIAN_POINT('Ctrl Pts',(-1.03071594587089,-2.49023250784913,
7.56669465659233));
#402791=CARTESIAN_POINT('Ctrl Pts',(-1.02624779350501,-2.48656211559887,
7.56004085833301));
#402792=CARTESIAN_POINT('Ctrl Pts',(-1.0194340624728,-2.49171087462867,
7.55785582193789));
#402793=CARTESIAN_POINT('Ctrl Pts',(-1.00628201485164,-2.4701610994206,
7.59443891967696));
#402794=CARTESIAN_POINT('Ctrl Pts',(-1.00180738422113,-2.46648538555856,
7.58783901202978));
#402795=CARTESIAN_POINT('Ctrl Pts',(-0.995046660904368,-2.47162073347496,
7.58560008491213));
#402796=CARTESIAN_POINT('',(-1.06675863750382,-2.53069219871727,7.50366116523517));
#402797=CARTESIAN_POINT('Ctrl Pts',(-1.06675863750396,-2.53069219871762,
7.50366116523554));
#402798=CARTESIAN_POINT('Ctrl Pts',(-1.06750186807349,-2.53054473401916,
7.50350835821027));
#402799=CARTESIAN_POINT('Ctrl Pts',(-1.06818027974491,-2.53038499793927,
7.50345484956));
#402800=CARTESIAN_POINT('Ctrl Pts',(-1.06881417987675,-2.53020882591189,
7.50349758195598));
#402801=CARTESIAN_POINT('Ctrl Pts',(-1.06913941765565,-2.53011843659659,
7.50351950684424));
#402802=CARTESIAN_POINT('Ctrl Pts',(-1.0694850293952,-2.53001493618197,
7.50357029184312));
#402803=CARTESIAN_POINT('Ctrl Pts',(-1.06981555540293,-2.52990597100817,
7.50365515313924));
#402804=CARTESIAN_POINT('Ctrl Pts',(-1.07032403824601,-2.52973833844651,
7.50378570417639));
#402805=CARTESIAN_POINT('Ctrl Pts',(-1.07081185253136,-2.52955318148127,
7.50400001621911));
#402806=CARTESIAN_POINT('Ctrl Pts',(-1.071241062824,-2.52936247059273,7.50428903009634));
#402807=CARTESIAN_POINT('Ctrl Pts',(-1.07128870186434,-2.52934130315135,
7.50432110841318));
#402808=CARTESIAN_POINT('Ctrl Pts',(-1.07133564874018,-2.52932007288123,
7.50435406373354));
#402809=CARTESIAN_POINT('Ctrl Pts',(-1.0713818736287,-2.52929879997845,
7.50438785222352));
#402810=CARTESIAN_POINT('Ctrl Pts',(-1.07166409879164,-2.52916891868189,
7.50459414719561));
#402811=CARTESIAN_POINT('Ctrl Pts',(-1.07192368820832,-2.52903491181197,
7.50483629897752));
#402812=CARTESIAN_POINT('Ctrl Pts',(-1.07215130076294,-2.52890308253883,
7.5050991045531));
#402813=CARTESIAN_POINT('Ctrl Pts',(-1.07265343691995,-2.52861225392127,
7.50567888004914));
#402814=CARTESIAN_POINT('Ctrl Pts',(-1.07301999334671,-2.52832101331306,
7.50637912803145));
#402815=CARTESIAN_POINT('Ctrl Pts',(-1.07327584969576,-2.52804770250378,
7.50710440483569));
#402816=CARTESIAN_POINT('Ctrl Pts',(-1.07333859075201,-2.52798068126736,
7.50728225710685));
#402817=CARTESIAN_POINT('Ctrl Pts',(-1.07339603063643,-2.52791350375377,
7.50746498566954));
#402818=CARTESIAN_POINT('Ctrl Pts',(-1.07344714514513,-2.52784800883596,
7.50764697238949));
#402819=CARTESIAN_POINT('Ctrl Pts',(-1.07372192267682,-2.52749592618251,
7.50862528291182));
#402820=CARTESIAN_POINT('Ctrl Pts',(-1.07384211344803,-2.52716305316058,
7.50965856837423));
#402821=CARTESIAN_POINT('Ctrl Pts',(-1.07387383160382,-2.52685432086199,
7.51067959873204));
#402822=CARTESIAN_POINT('Ctrl Pts',(-1.07389128614496,-2.52668442508867,
7.5112414730258));
#402823=CARTESIAN_POINT('Ctrl Pts',(-1.07388152051967,-2.5265217540281,
7.51180065547253));
#402824=CARTESIAN_POINT('Ctrl Pts',(-1.07385284243993,-2.5263669506711,
7.51235175716501));
#402825=CARTESIAN_POINT('Ctrl Pts',(-1.07375374825042,-2.52583204340632,
7.51425603304536));
#402826=CARTESIAN_POINT('Ctrl Pts',(-1.07341106536622,-2.52532840179909,
7.5162690050518));
#402827=CARTESIAN_POINT('Ctrl Pts',(-1.07288284142306,-2.52487255277834,
7.51827788969243));
#402828=CARTESIAN_POINT('Ctrl Pts',(-1.07285425294505,-2.5248478813679,
7.51838661432545));
#402829=CARTESIAN_POINT('Ctrl Pts',(-1.07282511102272,-2.52482335005462,
7.51849533314856));
#402830=CARTESIAN_POINT('Ctrl Pts',(-1.07279542170604,-2.52479896157613,
7.51860402984325));
#402831=CARTESIAN_POINT('Ctrl Pts',(-1.00345144418694,-2.47854446519997,
7.57603338728985));
#402832=CARTESIAN_POINT('Ctrl Pts',(-1.02458872953834,-2.49595688723385,
7.55196141284922));
#402833=CARTESIAN_POINT('Ctrl Pts',(-1.04569014275369,-2.51333863069778,
7.52783573083105));
#402834=CARTESIAN_POINT('Ctrl Pts',(-1.06675863755276,-2.53069219875054,
7.50366116530176));
#402835=CARTESIAN_POINT('Origin',(-3.46738858720988E-16,-8.56451684780639E-16,
7.49482233047033));
#402836=CARTESIAN_POINT('Origin',(-0.991053119217889,-2.55180719586894,
7.49482233047033));
#402837=CARTESIAN_POINT('Origin',(0.,0.,7.50366116523517));
#402838=CARTESIAN_POINT('Origin',(-1.06332537456791,-2.52254740248821,7.49482233047033));
#402839=CARTESIAN_POINT('Ctrl Pts',(-0.985816807380133,-2.56001169753273,
7.51860402984325));
#402840=CARTESIAN_POINT('Ctrl Pts',(-0.98495387744,-2.56757156776631,7.51860402984325));
#402841=CARTESIAN_POINT('Ctrl Pts',(-0.977842190757029,-2.57027715431148,
7.51860402984325));
#402842=CARTESIAN_POINT('Ctrl Pts',(-0.985496394341891,-2.56281872879758,
7.51041458714367));
#402843=CARTESIAN_POINT('Ctrl Pts',(-0.983269033888756,-2.56821254295568,
7.51004642900442));
#402844=CARTESIAN_POINT('Ctrl Pts',(-0.977840229438281,-2.57027790048012,
7.50729136483011));
#402845=CARTESIAN_POINT('Ctrl Pts',(-0.988011340623444,-2.56408315847147,
7.50215815450137));
#402846=CARTESIAN_POINT('Ctrl Pts',(-0.986699593402196,-2.56690758473339,
7.4987716367153));
#402847=CARTESIAN_POINT('Ctrl Pts',(-0.983483430761509,-2.56815667298608,
7.49481588533169));
#402848=CARTESIAN_POINT('Ctrl Pts',(-0.994252830331148,-2.560045952888,
7.50366171572174));
#402849=CARTESIAN_POINT('Ctrl Pts',(-0.995578475927007,-2.56345928352117,
7.50000045605858));
#402850=CARTESIAN_POINT('Ctrl Pts',(-0.995578475926891,-2.56345928352122,
7.49482233047317));
#402851=CARTESIAN_POINT('Origin',(-0.973397453526316,-2.55859407633733,
7.51860402984325));
#402852=CARTESIAN_POINT('Origin',(-0.973397453526316,-2.55859407633733,
9.));
#402853=CARTESIAN_POINT('Origin',(-0.973397453526316,-2.55859407633733,
8.75721825406948));
#402854=CARTESIAN_POINT('Ctrl Pts',(-0.987712021557121,-2.54342048849949,
8.78942910404912));
#402855=CARTESIAN_POINT('Ctrl Pts',(-0.987099662981832,-2.54895921088619,
8.7967269950169));
#402856=CARTESIAN_POINT('Ctrl Pts',(-0.978198471170077,-2.54962424495468,
8.79893251111267));
#402857=CARTESIAN_POINT('Ctrl Pts',(-0.986464237477146,-2.55434378716014,
8.78111911759585));
#402858=CARTESIAN_POINT('Ctrl Pts',(-0.985730880534933,-2.56090918872596,
8.78644465894816));
#402859=CARTESIAN_POINT('Ctrl Pts',(-0.97796453785879,-2.56323285677716,
8.78817647674132));
#402860=CARTESIAN_POINT('Ctrl Pts',(-0.985686588644423,-2.56115144742717,
8.76780923932029));
#402861=CARTESIAN_POINT('Ctrl Pts',(-0.984815827444824,-2.56890106107585,
8.76988516158371));
#402862=CARTESIAN_POINT('Ctrl Pts',(-0.977807256217964,-2.57173236991701,
8.77093053738832));
#402863=CARTESIAN_POINT('Ctrl Pts',(-0.985838219522211,-2.55982404684425,
8.75371302330492));
#402864=CARTESIAN_POINT('Ctrl Pts',(-0.984989587073333,-2.56738354579156,
8.7530082828756));
#402865=CARTESIAN_POINT('Ctrl Pts',(-0.977837475051993,-2.57007461118809,
8.75267964240738));
#402866=CARTESIAN_POINT('Origin',(-0.974988929080874,-2.54466209919314,
8.78727029226991));
#402867=CARTESIAN_POINT('Ctrl Pts',(-0.995522110700908,-2.47505025214475,
8.85049129520029));
#402868=CARTESIAN_POINT('Ctrl Pts',(-0.994859350710948,-2.48085213644374,
8.85711686593484));
#402869=CARTESIAN_POINT('Ctrl Pts',(-0.986367352980499,-2.48184548263714,
8.85933012996512));
#402870=CARTESIAN_POINT('Ctrl Pts',(-0.9928135263408,-2.49876154025725,
8.8294568364472));
#402871=CARTESIAN_POINT('Ctrl Pts',(-0.992145265042209,-2.5046115837038,
8.83607469902387));
#402872=CARTESIAN_POINT('Ctrl Pts',(-0.983623977915089,-2.50557059788234,
8.83829567148519));
#402873=CARTESIAN_POINT('Ctrl Pts',(-0.990108979344094,-2.52243748478279,
8.80838214965003));
#402874=CARTESIAN_POINT('Ctrl Pts',(-0.989438080774434,-2.52831061523216,
8.81501364461996));
#402875=CARTESIAN_POINT('Ctrl Pts',(-0.980885428519782,-2.52925980014899,
8.81722098428721));
#402876=CARTESIAN_POINT('Ctrl Pts',(-0.987408162934496,-2.54608077127965,
8.78727029226991));
#402877=CARTESIAN_POINT('Ctrl Pts',(-0.986737152926361,-2.55195487727524,
8.79393457792714));
#402878=CARTESIAN_POINT('Ctrl Pts',(-0.978151351640473,-2.5529158306859,
8.79610912703474));
#402879=CARTESIAN_POINT('Origin',(-0.983102876847287,-2.47363158005824,
8.85049129520029));
#402880=CARTESIAN_POINT('Ctrl Pts',(-1.00671661105392,-2.47051810124199,
8.85049129520029));
#402881=CARTESIAN_POINT('Ctrl Pts',(-1.0112289739294,-2.47422481049725,
8.85711686593484));
#402882=CARTESIAN_POINT('Ctrl Pts',(-1.01802024859356,-2.46903064544887,
8.85933012996512));
#402883=CARTESIAN_POINT('Ctrl Pts',(-1.00272458875463,-2.46723882907077,
8.86332496987232));
#402884=CARTESIAN_POINT('Ctrl Pts',(-1.00710562609237,-2.46576967753948,
8.86648636486737));
#402885=CARTESIAN_POINT('Ctrl Pts',(-1.0068415284508,-2.45986998650278,
8.87206031107456));
#402886=CARTESIAN_POINT('Ctrl Pts',(-0.996112429222693,-2.46988252956822,
8.86341338519877));
#402887=CARTESIAN_POINT('Ctrl Pts',(-0.991918717460054,-2.47185388754845,
8.8665458496606));
#402888=CARTESIAN_POINT('Ctrl Pts',(-0.988034913849338,-2.46737725686223,
8.87215952290715));
#402889=CARTESIAN_POINT('Ctrl Pts',(-0.995522110700908,-2.47505025214475,
8.85049129520029));
#402890=CARTESIAN_POINT('Ctrl Pts',(-0.994859350710948,-2.48085213644373,
8.85711686593484));
#402891=CARTESIAN_POINT('Ctrl Pts',(-0.986367352980499,-2.48184548263714,
8.85933012996512));
#402892=CARTESIAN_POINT('Origin',(-1.01465101420576,-2.46085915478681,8.85049129520029));
#402893=CARTESIAN_POINT('Ctrl Pts',(-1.0619599528811,-2.51589809662205,
8.78727029226991));
#402894=CARTESIAN_POINT('Ctrl Pts',(-1.06652848552588,-2.51965094689244,
8.79393457792714));
#402895=CARTESIAN_POINT('Ctrl Pts',(-1.07336460881941,-2.51436825501292,
8.79610912703474));
#402896=CARTESIAN_POINT('Ctrl Pts',(-1.04357160131374,-2.50079286798139,
8.80838214965003));
#402897=CARTESIAN_POINT('Ctrl Pts',(-1.0481393752363,-2.50454509499456,
8.81501364461993));
#402898=CARTESIAN_POINT('Ctrl Pts',(-1.05494349880899,-2.49927701042777,
8.81722098428722));
#402899=CARTESIAN_POINT('Ctrl Pts',(-1.02515785026093,-2.48566677477146,
8.82945683644728));
#402900=CARTESIAN_POINT('Ctrl Pts',(-1.02970766847652,-2.48940425195465,
8.83607469902396));
#402901=CARTESIAN_POINT('Ctrl Pts',(-1.03649609897604,-2.48416504840346,
8.8382956714852));
#402902=CARTESIAN_POINT('Ctrl Pts',(-1.00671661105392,-2.47051810124199,
8.85049129520029));
#402903=CARTESIAN_POINT('Ctrl Pts',(-1.0112289739294,-2.47422481049725,
8.85711686593484));
#402904=CARTESIAN_POINT('Ctrl Pts',(-1.01802024859356,-2.46903064544887,
8.85933012996512));
#402905=CARTESIAN_POINT('Origin',(-1.06989435603295,-2.50623915016687,8.78727029226991));
#402906=CARTESIAN_POINT('Ctrl Pts',(-1.07265235650021,-2.52468141587758,
8.75374538247848));
#402907=CARTESIAN_POINT('Ctrl Pts',(-1.07851586339026,-2.52951501343405,
8.75304829418602));
#402908=CARTESIAN_POINT('Ctrl Pts',(-1.08552051380799,-2.5264809541508,
8.75272238421917));
#402909=CARTESIAN_POINT('Ctrl Pts',(-1.07367232836399,-2.52551927882054,
8.76769408445019));
#402910=CARTESIAN_POINT('Ctrl Pts',(-1.07968382607105,-2.53047397863889,
8.76974318093968));
#402911=CARTESIAN_POINT('Ctrl Pts',(-1.08668211825917,-2.52763809011329,
8.7707786988043));
#402912=CARTESIAN_POINT('Ctrl Pts',(-1.06844453362053,-2.52122487068539,
8.78108014887992));
#402913=CARTESIAN_POINT('Ctrl Pts',(-1.07353664488914,-2.5254267321929,
8.78639403366326));
#402914=CARTESIAN_POINT('Ctrl Pts',(-1.08073062501099,-2.5217161088308,
8.78812224174741));
#402915=CARTESIAN_POINT('Ctrl Pts',(-1.05987733210579,-2.51418728372498,
8.78944554828685));
#402916=CARTESIAN_POINT('Ctrl Pts',(-1.06416521194977,-2.51773277439068,
8.79673892988685));
#402917=CARTESIAN_POINT('Ctrl Pts',(-1.07101637621682,-2.51202619025459,
8.79894799272499));
#402918=CARTESIAN_POINT('Origin',(-1.08072982485788,-2.51514001512096,8.75721825406948));
#402919=CARTESIAN_POINT('Origin',(-1.08072982485788,-2.51514001512096,9.));
#402920=CARTESIAN_POINT('Origin',(-1.08072982485788,-2.51514001512096,7.51860402984325));
#402921=CARTESIAN_POINT('Ctrl Pts',(-1.06675833194057,-2.53069147382351,
7.50366195182966));
#402922=CARTESIAN_POINT('Ctrl Pts',(-1.06818074157519,-2.53406588377806,
7.50000065167735));
#402923=CARTESIAN_POINT('Ctrl Pts',(-1.0681807415753,-2.53406588377801,
7.49482233047108));
#402924=CARTESIAN_POINT('Ctrl Pts',(-1.07405684430838,-2.52924734196545,
7.50215800491337));
#402925=CARTESIAN_POINT('Ctrl Pts',(-1.07696552033801,-2.5303628243405,
7.49877273257269));
#402926=CARTESIAN_POINT('Ctrl Pts',(-1.08014658708644,-2.52902194004573,
7.49481816995647));
#402927=CARTESIAN_POINT('Ctrl Pts',(-1.07497317162725,-2.52658832699994,
7.51043025814042));
#402928=CARTESIAN_POINT('Ctrl Pts',(-1.0803271101054,-2.52891815526811,
7.51006209594511));
#402929=CARTESIAN_POINT('Ctrl Pts',(-1.08566699044975,-2.52662367317616,
7.50731281821699));
#402930=CARTESIAN_POINT('Ctrl Pts',(-1.07279425387576,-2.52479800213625,
7.51860402984325));
#402931=CARTESIAN_POINT('Ctrl Pts',(-1.07867347373825,-2.52962871545823,
7.51860402984325));
#402932=CARTESIAN_POINT('Ctrl Pts',(-1.0856646642408,-2.52662467272425,
7.51860402984325));
#402933=CARTESIAN_POINT('Origin',(0.,0.,7.5));
#402934=CARTESIAN_POINT('Origin',(-0.84636156559358,-2.52994271156921,7.5));
#402935=CARTESIAN_POINT('',(-0.84636156559358,-2.52994271156921,7.59394543036555));
#402936=CARTESIAN_POINT('',(-0.84636156559358,-2.52994271156921,8.85049129520029));
#402937=CARTESIAN_POINT('',(-0.84636156559358,-2.52994271156921,7.5));
#402938=CARTESIAN_POINT('',(-0.89858389776343,-2.57876892194511,8.78727029226991));
#402939=CARTESIAN_POINT('Ctrl Pts',(-0.846361565593581,-2.52994271156921,
8.85049129520029));
#402940=CARTESIAN_POINT('Ctrl Pts',(-0.863794313055953,-2.54624177290296,
8.82945686509571));
#402941=CARTESIAN_POINT('Ctrl Pts',(-0.881201144631286,-2.56251660371118,
8.80838212259896));
#402942=CARTESIAN_POINT('Ctrl Pts',(-0.89858389776343,-2.57876892194511,
8.78727029226991));
#402943=CARTESIAN_POINT('',(-0.908826823579936,-2.58834572998875,8.75721825406948));
#402944=CARTESIAN_POINT('Origin',(-0.878002168679522,-2.55952593977548,
8.75937679713084));
#402945=CARTESIAN_POINT('',(-0.908826823579936,-2.58834572998875,7.51860402984325));
#402946=CARTESIAN_POINT('',(-0.908826823579936,-2.58834572998875,7.5));
#402947=CARTESIAN_POINT('Ctrl Pts',(-0.908826823579935,-2.58834572998875,
7.51860402984325));
#402948=CARTESIAN_POINT('Ctrl Pts',(-0.900782598427366,-2.58082463674586,
7.52834476460825));
#402949=CARTESIAN_POINT('Ctrl Pts',(-0.892733151079904,-2.57329866091778,
7.53807742314407));
#402950=CARTESIAN_POINT('Ctrl Pts',(-0.884678306195408,-2.56576763856519,
7.54780169004674));
#402951=CARTESIAN_POINT('Ctrl Pts',(-0.871919867225587,-2.55383890617572,
7.5632044032688));
#402952=CARTESIAN_POINT('Ctrl Pts',(-0.85914787030871,-2.54189749753934,
7.57858609112103));
#402953=CARTESIAN_POINT('Ctrl Pts',(-0.84636156559358,-2.52994271156921,
7.59394543036555));
#402954=CARTESIAN_POINT('Origin',(-0.786247562650692,-2.80441041318874,
7.5));
#402955=CARTESIAN_POINT('',(-0.819770641322262,-2.61791441969279,8.75721825406948));
#402956=CARTESIAN_POINT('',(-0.822251471860003,-2.60411303347872,8.78727029226991));
#402957=CARTESIAN_POINT('Origin',(-0.828548745068065,-2.56907996760912,
8.75658640621115));
#402958=CARTESIAN_POINT('',(-0.834899689636828,-2.53374831658168,8.85049129520029));
#402959=CARTESIAN_POINT('Ctrl Pts',(-0.822251471860003,-2.60411303347872,
8.78727029226991));
#402960=CARTESIAN_POINT('Ctrl Pts',(-0.826461564325062,-2.58069139656185,
8.80838212259896));
#402961=CARTESIAN_POINT('Ctrl Pts',(-0.830677488574736,-2.55723731619085,
8.82945686509571));
#402962=CARTESIAN_POINT('Ctrl Pts',(-0.834899689636828,-2.53374831658168,
8.85049129520029));
#402963=CARTESIAN_POINT('',(-0.834899689636828,-2.53374831658168,7.59394543036555));
#402964=CARTESIAN_POINT('',(-0.834899689636828,-2.53374831658168,7.5));
#402965=CARTESIAN_POINT('',(-0.819770641322262,-2.61791441969279,7.51860402984325));
#402966=CARTESIAN_POINT('Ctrl Pts',(-0.834899689636828,-2.53374831658168,
7.59394543036555));
#402967=CARTESIAN_POINT('Ctrl Pts',(-0.831802854243269,-2.55097666840084,
7.57858609112103));
#402968=CARTESIAN_POINT('Ctrl Pts',(-0.828709484189984,-2.56818574179751,
7.56320440326857));
#402969=CARTESIAN_POINT('Ctrl Pts',(-0.825619397863354,-2.58537654712652,
7.54780169004651));
#402970=CARTESIAN_POINT('Ctrl Pts',(-0.823668519225333,-2.59622969857337,
7.53807742314383));
#402971=CARTESIAN_POINT('Ctrl Pts',(-0.821718947867528,-2.60707557734321,
7.52834476460825));
#402972=CARTESIAN_POINT('Ctrl Pts',(-0.819770641322262,-2.61791441969279,
7.51860402984324));
#402973=CARTESIAN_POINT('',(-0.819770641322262,-2.61791441969279,7.5));
#402974=CARTESIAN_POINT('Origin',(-0.841666242052004,-2.53496461975634,
7.5));
#402975=CARTESIAN_POINT('Ctrl Pts',(-0.834899689636828,-2.53374831658168,
8.85049129520029));
#402976=CARTESIAN_POINT('Ctrl Pts',(-0.834933951615658,-2.53355770992996,
8.85097269580138));
#402977=CARTESIAN_POINT('Ctrl Pts',(-0.834976060045437,-2.5333709962543,
8.85143669361005));
#402978=CARTESIAN_POINT('Ctrl Pts',(-0.835028806748976,-2.53317977033515,
8.8519052845931));
#402979=CARTESIAN_POINT('Ctrl Pts',(-0.835131975956022,-2.53280574456438,
8.85282181883899));
#402980=CARTESIAN_POINT('Ctrl Pts',(-0.835273379657609,-2.53242413032999,
8.85372622499635));
#402981=CARTESIAN_POINT('Ctrl Pts',(-0.835469694820092,-2.5320342967677,
8.8546225773507));
#402982=CARTESIAN_POINT('Ctrl Pts',(-0.83563266869553,-2.53171067078987,
8.85536669723986));
#402983=CARTESIAN_POINT('Ctrl Pts',(-0.835833495004561,-2.53138129226441,
8.85610498449051));
#402984=CARTESIAN_POINT('Ctrl Pts',(-0.836088564940283,-2.53104993826304,
8.85681338218371));
#402985=CARTESIAN_POINT('Ctrl Pts',(-0.836320041307544,-2.53074923398639,
8.85745625420284));
#402986=CARTESIAN_POINT('Ctrl Pts',(-0.836598619887889,-2.53044276569274,
8.85808743050665));
#402987=CARTESIAN_POINT('Ctrl Pts',(-0.836951693134167,-2.53013874920071,
8.8586680450841));
#402988=CARTESIAN_POINT('Ctrl Pts',(-0.837114593476311,-2.52999848258155,
8.85893592806395));
#402989=CARTESIAN_POINT('Ctrl Pts',(-0.837293573677397,-2.52985883470932,
8.85919241173848));
#402990=CARTESIAN_POINT('Ctrl Pts',(-0.837492683868199,-2.52972144827,8.85943017985534));
#402991=CARTESIAN_POINT('Ctrl Pts',(-0.837761541568706,-2.52953593590618,
8.8597512372));
#402992=CARTESIAN_POINT('Ctrl Pts',(-0.838074309181994,-2.52935035226354,
8.86004599534706));
#402993=CARTESIAN_POINT('Ctrl Pts',(-0.838432543645307,-2.52917588406184,
8.86026130871721));
#402994=CARTESIAN_POINT('Ctrl Pts',(-0.838563703382024,-2.52911200633442,
8.86034014101235));
#402995=CARTESIAN_POINT('Ctrl Pts',(-0.838702922709061,-2.52904864803639,
8.86040910639693));
#402996=CARTESIAN_POINT('Ctrl Pts',(-0.838846548008433,-2.52898784149327,
8.86046313645507));
#402997=CARTESIAN_POINT('Ctrl Pts',(-0.83907067408525,-2.52889295339199,
8.8605474499083));
#402998=CARTESIAN_POINT('Ctrl Pts',(-0.839311704589203,-2.52880182440185,
8.86059655985668));
#402999=CARTESIAN_POINT('Ctrl Pts',(-0.839554077896316,-2.52872002487638,
8.86059725258815));
#403000=CARTESIAN_POINT('Ctrl Pts',(-0.839797011182598,-2.52863803636133,
8.86059794692011));
#403001=CARTESIAN_POINT('Ctrl Pts',(-0.840044837205576,-2.52856702848269,
8.86056369958366));
#403002=CARTESIAN_POINT('Ctrl Pts',(-0.84028300290619,-2.52850725650911,
8.86048590497774));
#403003=CARTESIAN_POINT('Ctrl Pts',(-0.840345157063002,-2.52849165780363,
8.86046560290182));
#403004=CARTESIAN_POINT('Ctrl Pts',(-0.840407483937903,-2.52847670924879,
8.86044257503091));
#403005=CARTESIAN_POINT('Ctrl Pts',(-0.840468049922912,-2.52846284084641,
8.86041778462583));
#403006=CARTESIAN_POINT('Ctrl Pts',(-0.840875583845895,-2.52836952370761,
8.86025097596201));
#403007=CARTESIAN_POINT('Ctrl Pts',(-0.841258151095109,-2.52831291335483,
8.8599848982295));
#403008=CARTESIAN_POINT('Ctrl Pts',(-0.841603345326632,-2.5282862808699,
8.85968173251461));
#403009=CARTESIAN_POINT('Ctrl Pts',(-0.841785933297837,-2.52827219381123,
8.85952137522076));
#403010=CARTESIAN_POINT('Ctrl Pts',(-0.841961569857954,-2.52826603203966,
8.85934740853961));
#403011=CARTESIAN_POINT('Ctrl Pts',(-0.842127723639171,-2.52826632885326,
8.8591675900182));
#403012=CARTESIAN_POINT('Ctrl Pts',(-0.842794917435792,-2.52826752071417,
8.85844552518694));
#403013=CARTESIAN_POINT('Ctrl Pts',(-0.843346920779428,-2.52836989484404,
8.8575944418412));
#403014=CARTESIAN_POINT('Ctrl Pts',(-0.843789497269798,-2.52849379119463,
8.85683498915134));
#403015=CARTESIAN_POINT('Ctrl Pts',(-0.843835811720827,-2.52850675661776,
8.85675551444995));
#403016=CARTESIAN_POINT('Ctrl Pts',(-0.843880918787595,-2.52851997553546,
8.8566769979365));
#403017=CARTESIAN_POINT('Ctrl Pts',(-0.843924818530555,-2.52853336804471,
8.85659965593547));
#403018=CARTESIAN_POINT('Ctrl Pts',(-0.844517379501239,-2.5287141408181,
8.85555568965886));
#403019=CARTESIAN_POINT('Ctrl Pts',(-0.845060760140823,-2.52897345218239,
8.85434650606346));
#403020=CARTESIAN_POINT('Ctrl Pts',(-0.845560323240718,-2.52930697522583,
8.85297329937117));
#403021=CARTESIAN_POINT('Ctrl Pts',(-0.845841297045581,-2.5294945616159,
8.85220095427747));
#403022=CARTESIAN_POINT('Ctrl Pts',(-0.846108349539873,-2.52970596265749,
8.85137579139183));
#403023=CARTESIAN_POINT('Ctrl Pts',(-0.84636156559358,-2.52994271156921,
8.85049129520029));
#403024=CARTESIAN_POINT('Origin',(-0.841666242052004,-2.53496461975634,
7.59394543036555));
#403025=CARTESIAN_POINT('Ctrl Pts',(-0.83499916371954,-2.53319492117119,
7.59443877723642));
#403026=CARTESIAN_POINT('Ctrl Pts',(-0.836023651060078,-2.52749548090589,
7.58783886950016));
#403027=CARTESIAN_POINT('Ctrl Pts',(-0.844500455058569,-2.52702327808101,
7.58559994247159));
#403028=CARTESIAN_POINT('Ctrl Pts',(-0.829406517384719,-2.56430799836504,
7.56670252222137));
#403029=CARTESIAN_POINT('Ctrl Pts',(-0.830429524050224,-2.55861679540901,
7.56004874999028));
#403030=CARTESIAN_POINT('Ctrl Pts',(-0.838955367733715,-2.55812046211334,
7.55786368756704));
#403031=CARTESIAN_POINT('Ctrl Pts',(-0.823824314758165,-2.59536297499574,
7.53888913333558));
#403032=CARTESIAN_POINT('Ctrl Pts',(-0.824853401202346,-2.5896379489419,
7.53222002137275));
#403033=CARTESIAN_POINT('Ctrl Pts',(-0.833419290574643,-2.58916047226024,
7.53005029815327));
#403034=CARTESIAN_POINT('Ctrl Pts',(-0.818252808438304,-2.62635844580471,
7.51101258149734));
#403035=CARTESIAN_POINT('Ctrl Pts',(-0.819294369280078,-2.62056402203247,
7.5043616886572));
#403036=CARTESIAN_POINT('Ctrl Pts',(-0.827892578463771,-2.62014178942107,
7.50217374673251));
#403037=CARTESIAN_POINT('',(-0.828187489909756,-2.6184885863594,7.50366116523517));
#403038=CARTESIAN_POINT('Ctrl Pts',(-0.819770641322261,-2.61791441969279,
7.51860402984325));
#403039=CARTESIAN_POINT('Ctrl Pts',(-0.819692512867927,-2.61834906484738,
7.51734760759493));
#403040=CARTESIAN_POINT('Ctrl Pts',(-0.819680470930672,-2.61875235488163,
7.51608817408572));
#403041=CARTESIAN_POINT('Ctrl Pts',(-0.819747890902916,-2.619123760765,
7.51481005913118));
#403042=CARTESIAN_POINT('Ctrl Pts',(-0.819808961524827,-2.61946018908918,
7.51365231206383));
#403043=CARTESIAN_POINT('Ctrl Pts',(-0.819935071926935,-2.61977097483344,
7.51247773061042));
#403044=CARTESIAN_POINT('Ctrl Pts',(-0.820158255373951,-2.6200368563799,
7.51129758471022));
#403045=CARTESIAN_POINT('Ctrl Pts',(-0.82043564691008,-2.62036731677734,
7.50983079813402));
#403046=CARTESIAN_POINT('Ctrl Pts',(-0.820864116558463,-2.62060949033283,
7.50839324291155));
#403047=CARTESIAN_POINT('Ctrl Pts',(-0.821487355823228,-2.62069337531113,
7.50715379678855));
#403048=CARTESIAN_POINT('Ctrl Pts',(-0.821775274405341,-2.62073212775401,
7.50658120839351));
#403049=CARTESIAN_POINT('Ctrl Pts',(-0.822146957898613,-2.62073319086503,
7.50598221009429));
#403050=CARTESIAN_POINT('Ctrl Pts',(-0.822593625821642,-2.62067379294522,
7.50545747549611));
#403051=CARTESIAN_POINT('Ctrl Pts',(-0.822831981651036,-2.62064209637667,
7.50517746087247));
#403052=CARTESIAN_POINT('Ctrl Pts',(-0.823094301518081,-2.62059303983323,
7.50491486231392));
#403053=CARTESIAN_POINT('Ctrl Pts',(-0.823373332129946,-2.62052628282281,
7.50468370960992));
#403054=CARTESIAN_POINT('Ctrl Pts',(-0.8237905709099,-2.62042646003491,
7.50433806340447));
#403055=CARTESIAN_POINT('Ctrl Pts',(-0.82425755626529,-2.62028352485886,
7.50405484070984));
#403056=CARTESIAN_POINT('Ctrl Pts',(-0.82474262792786,-2.62010641868806,
7.50385766036131));
#403057=CARTESIAN_POINT('Ctrl Pts',(-0.824794498802451,-2.62008747993595,
7.50383657498791));
#403058=CARTESIAN_POINT('Ctrl Pts',(-0.824846558500569,-2.62006817236335,
7.50381643264937));
#403059=CARTESIAN_POINT('Ctrl Pts',(-0.824898755484747,-2.62004852303516,
7.50379723213559));
#403060=CARTESIAN_POINT('Ctrl Pts',(-0.825247187428958,-2.61991735734176,
7.50366906242519));
#403061=CARTESIAN_POINT('Ctrl Pts',(-0.825609062713827,-2.61976743691642,
7.50358235568538));
#403062=CARTESIAN_POINT('Ctrl Pts',(-0.825954392352455,-2.61961454756584,
7.5035341175365));
#403063=CARTESIAN_POINT('Ctrl Pts',(-0.82647217506181,-2.61938530728838,
7.50346178989176));
#403064=CARTESIAN_POINT('Ctrl Pts',(-0.827019444398862,-2.61911668139349,
7.50346967198527));
#403065=CARTESIAN_POINT('Ctrl Pts',(-0.827548579046752,-2.6188364428261,
7.50354272648692));
#403066=CARTESIAN_POINT('Ctrl Pts',(-0.827766223079868,-2.61872117490273,
7.50357277531559));
#403067=CARTESIAN_POINT('Ctrl Pts',(-0.827980576188296,-2.61860422075377,
7.50361331098761));
#403068=CARTESIAN_POINT('Ctrl Pts',(-0.828187489910183,-2.61848858636075,
7.50366116523658));
#403069=CARTESIAN_POINT('',(-0.842588855338984,-2.53774338397764,7.57603338622103));
#403070=CARTESIAN_POINT('Origin',(-0.84537615509485,-2.546129232156,7.58486873427627));
#403071=CARTESIAN_POINT('Ctrl Pts',(-0.828187489894455,-2.61848858641467,
7.50366116529969));
#403072=CARTESIAN_POINT('Ctrl Pts',(-0.832980934541063,-2.59161758555462,
7.52783573079709));
#403073=CARTESIAN_POINT('Ctrl Pts',(-0.837781180672694,-2.56470379203952,
7.55196141284069));
#403074=CARTESIAN_POINT('Ctrl Pts',(-0.842588854779952,-2.53774338509797,
7.57603338728831));
#403075=CARTESIAN_POINT('Ctrl Pts',(-0.834890789857168,-2.53479160767929,
7.5963967733137));
#403076=CARTESIAN_POINT('Ctrl Pts',(-0.835239864301339,-2.51651730706895,
7.59959882295473));
#403077=CARTESIAN_POINT('Ctrl Pts',(-0.84687953098394,-2.53063208557011,
7.59642833564546));
#403078=CARTESIAN_POINT('Ctrl Pts',(-0.834337441147255,-2.53093040200112,
7.5870762605742));
#403079=CARTESIAN_POINT('Ctrl Pts',(-0.838432320957715,-2.52553186049669,
7.58809943920599));
#403080=CARTESIAN_POINT('Ctrl Pts',(-0.844958025991749,-2.52730092086952,
7.58710240504253));
#403081=CARTESIAN_POINT('Ctrl Pts',(-0.839246778196438,-2.53451146916045,
7.58015376756929));
#403082=CARTESIAN_POINT('Ctrl Pts',(-0.840659757860373,-2.53203502819294,
7.58205880659762));
#403083=CARTESIAN_POINT('Ctrl Pts',(-0.843257205617099,-2.53312146281555,
7.58020924244125));
#403084=CARTESIAN_POINT('Ctrl Pts',(-0.842588855078019,-2.5377433831923,
7.57603338509286));
#403085=CARTESIAN_POINT('Ctrl Pts',(-0.842588855078019,-2.5377433831923,
7.57603338509286));
#403086=CARTESIAN_POINT('Ctrl Pts',(-0.842588855078019,-2.5377433831923,
7.57603338509286));
#403087=CARTESIAN_POINT('Origin',(-0.84537073944863,-2.54613103027482,7.58486873427621));
#403088=CARTESIAN_POINT('Ctrl Pts',(-0.915113503383067,-2.59422357454067,
7.51098857897448));
#403089=CARTESIAN_POINT('Ctrl Pts',(-0.910813056848305,-2.59020279456988,
7.50433767179956));
#403090=CARTESIAN_POINT('Ctrl Pts',(-0.903669774527125,-2.59500712269797,
7.50214974420965));
#403091=CARTESIAN_POINT('Ctrl Pts',(-0.89210308835163,-2.57270957241784,
7.53887321589168));
#403092=CARTESIAN_POINT('Ctrl Pts',(-0.887854168798268,-2.56873696852669,
7.53220407452062));
#403093=CARTESIAN_POINT('Ctrl Pts',(-0.880703735547826,-2.57347766723606,
7.53003438070911));
#403094=CARTESIAN_POINT('Ctrl Pts',(-0.869048484835137,-2.55115425547473,
7.56669465659232));
#403095=CARTESIAN_POINT('Ctrl Pts',(-0.864824675606418,-2.54720512893398,
7.56004085833299));
#403096=CARTESIAN_POINT('Ctrl Pts',(-0.857695061991683,-2.55190675204006,
7.55785582193789));
#403097=CARTESIAN_POINT('Ctrl Pts',(-0.845950735501038,-2.52955859857208,
7.59443891967696));
#403098=CARTESIAN_POINT('Ctrl Pts',(-0.841720802274792,-2.52560374628955,
7.58783901202978));
#403099=CARTESIAN_POINT('Ctrl Pts',(-0.834644946718488,-2.53029538205276,
7.58560008491213));
#403100=CARTESIAN_POINT('',(-0.902424861598272,-2.59384008075032,7.50366116523517));
#403101=CARTESIAN_POINT('Ctrl Pts',(-0.902424861598394,-2.59384008075067,
7.50366116523554));
#403102=CARTESIAN_POINT('Ctrl Pts',(-0.903176013216671,-2.59374053798034,
7.50350835821027));
#403103=CARTESIAN_POINT('Ctrl Pts',(-0.903863265344334,-2.59362459608038,
7.50345484956));
#403104=CARTESIAN_POINT('Ctrl Pts',(-0.904507150440919,-2.59348940013822,
7.50349758195598));
#403105=CARTESIAN_POINT('Ctrl Pts',(-0.90483751124723,-2.5934200345935,
7.50351950684424));
#403106=CARTESIAN_POINT('Ctrl Pts',(-0.905189044184732,-2.59333889025176,
7.50357029184312));
#403107=CARTESIAN_POINT('Ctrl Pts',(-0.905525872513984,-2.59325132583262,
7.50365515313924));
#403108=CARTESIAN_POINT('Ctrl Pts',(-0.906044050879637,-2.59311661629765,
7.50378570417639));
#403109=CARTESIAN_POINT('Ctrl Pts',(-0.906542725945715,-2.59296309412583,
7.50400001621911));
#403110=CARTESIAN_POINT('Ctrl Pts',(-0.906983273268363,-2.59280027467113,
7.50428903009635));
#403111=CARTESIAN_POINT('Ctrl Pts',(-0.907032170631807,-2.59278220296432,
7.50432110841318));
#403112=CARTESIAN_POINT('Ctrl Pts',(-0.90708038127832,-2.59276402421073,
7.50435406373354));
#403113=CARTESIAN_POINT('Ctrl Pts',(-0.907127874152411,-2.59274575665419,
7.50438785222352));
#403114=CARTESIAN_POINT('Ctrl Pts',(-0.907417840976726,-2.59263422444096,
7.50459414719561));
#403115=CARTESIAN_POINT('Ctrl Pts',(-0.907685482888746,-2.59251712485355,
7.50483629897752));
#403116=CARTESIAN_POINT('Ctrl Pts',(-0.907921074119493,-2.59240014962423,
7.5050991045531));
#403117=CARTESIAN_POINT('Ctrl Pts',(-0.908440812037419,-2.59214209051931,
7.50567888004914));
#403118=CARTESIAN_POINT('Ctrl Pts',(-0.908825275184519,-2.59187493364706,
7.50637912803144));
#403119=CARTESIAN_POINT('Ctrl Pts',(-0.909098116932933,-2.59161857715671,
7.50710440483569));
#403120=CARTESIAN_POINT('Ctrl Pts',(-0.909165023146312,-2.59155571345589,
7.50728225710685));
#403121=CARTESIAN_POINT('Ctrl Pts',(-0.909226649092401,-2.59149235415174,
7.50746498566954));
#403122=CARTESIAN_POINT('Ctrl Pts',(-0.909281854854655,-2.59143026871808,
7.50764697238949));
#403123=CARTESIAN_POINT('Ctrl Pts',(-0.909578625839493,-2.59109651451309,
7.50862528291181));
#403124=CARTESIAN_POINT('Ctrl Pts',(-0.909719896913618,-2.59077202606364,
7.50965856837421));
#403125=CARTESIAN_POINT('Ctrl Pts',(-0.909771330447341,-2.5904659602779,
7.51067959873202));
#403126=CARTESIAN_POINT('Ctrl Pts',(-0.909799634385823,-2.59029753188995,
7.51124147302578));
#403127=CARTESIAN_POINT('Ctrl Pts',(-0.909800311195693,-2.59013456936876,
7.51180065547253));
#403128=CARTESIAN_POINT('Ctrl Pts',(-0.909781610323276,-2.58997824666098,
7.512351757165));
#403129=CARTESIAN_POINT('Ctrl Pts',(-0.909716991359532,-2.58943808943403,
7.51425603304535));
#403130=CARTESIAN_POINT('Ctrl Pts',(-0.909407280982637,-2.58891352684471,
7.51626900505179));
#403131=CARTESIAN_POINT('Ctrl Pts',(-0.908909348679264,-2.58842477099044,
7.51827788969243));
#403132=CARTESIAN_POINT('Ctrl Pts',(-0.908882399642043,-2.58839831859998,
7.51838661432545));
#403133=CARTESIAN_POINT('Ctrl Pts',(-0.908854889321556,-2.58837197055954,
7.51849533314856));
#403134=CARTESIAN_POINT('Ctrl Pts',(-0.908826823579939,-2.58834572998874,
7.51860402984325));
#403135=CARTESIAN_POINT('Ctrl Pts',(-0.84258885645768,-2.53774338454218,
7.57603338728984));
#403136=CARTESIAN_POINT('Ctrl Pts',(-0.862567095279249,-2.55647430140978,
7.55196141284921));
#403137=CARTESIAN_POINT('Ctrl Pts',(-0.882511501250651,-2.57517230440418,
7.52783573083105));
#403138=CARTESIAN_POINT('Ctrl Pts',(-0.902424861644981,-2.59384008078666,
7.50366116530176));
#403139=CARTESIAN_POINT('Origin',(-2.91153398701372E-16,-8.76907647894217E-16,
7.49482233047033));
#403140=CARTESIAN_POINT('Origin',(-0.825522045906653,-2.61006122566543,
7.49482233047033));
#403141=CARTESIAN_POINT('Origin',(0.,0.,7.50366116523517));
#403142=CARTESIAN_POINT('Origin',(-0.899520491555372,-2.58549204896708,
7.49482233047033));
#403143=CARTESIAN_POINT('Ctrl Pts',(-0.819770828406729,-2.61791337864929,
7.51860402984325));
#403144=CARTESIAN_POINT('Ctrl Pts',(-0.818425308899815,-2.62540242820759,
7.51860402984325));
#403145=CARTESIAN_POINT('Ctrl Pts',(-0.811154886414735,-2.62764680850481,
7.51860402984325));
#403146=CARTESIAN_POINT('Ctrl Pts',(-0.819271226580806,-2.62069411363351,
7.51041458714367));
#403147=CARTESIAN_POINT('Ctrl Pts',(-0.816702859618967,-2.62593413814771,
7.51004642900443));
#403148=CARTESIAN_POINT('Ctrl Pts',(-0.811152881318541,-2.62764742747825,
7.50729136483011));
#403149=CARTESIAN_POINT('Ctrl Pts',(-0.821699993348142,-2.62211707856253,
7.50215815450137));
#403150=CARTESIAN_POINT('Ctrl Pts',(-0.820209979640322,-2.62485165780475,
7.49877163671529));
#403151=CARTESIAN_POINT('Ctrl Pts',(-0.816920395591586,-2.62589211942377,
7.49481588533168));
#403152=CARTESIAN_POINT('Ctrl Pts',(-0.828187323895682,-2.61848806146948,
7.50366171572174));
#403153=CARTESIAN_POINT('Ctrl Pts',(-0.829291552965956,-2.62197931345374,
7.50000045605858));
#403154=CARTESIAN_POINT('Ctrl Pts',(-0.829291552965837,-2.62197931345377,
7.49482233047317));
#403155=CARTESIAN_POINT('Origin',(-0.807467818749214,-2.61570295937524,
7.51860402984325));
#403156=CARTESIAN_POINT('Origin',(-0.807467818749214,-2.61570295937524,
9.));
#403157=CARTESIAN_POINT('Origin',(-0.807467818749214,-2.61570295937524,
8.75721825406948));
#403158=CARTESIAN_POINT('Ctrl Pts',(-0.822725151075437,-2.60147768482362,
8.78942910404913));
#403159=CARTESIAN_POINT('Ctrl Pts',(-0.82175918349479,-2.60696579336252,
8.79672699501689));
#403160=CARTESIAN_POINT('Ctrl Pts',(-0.812833671257198,-2.60705915972975,
8.79893251111267));
#403161=CARTESIAN_POINT('Ctrl Pts',(-0.82078007255357,-2.6122985945952,
8.78111911759583));
#403162=CARTESIAN_POINT('Ctrl Pts',(-0.819627575649261,-2.61880352049878,
8.78644465894818));
#403163=CARTESIAN_POINT('Ctrl Pts',(-0.811728311833873,-2.620624823041,
8.78817647674133));
#403164=CARTESIAN_POINT('Ctrl Pts',(-0.819567853192924,-2.61904244366225,
8.7678092393203));
#403165=CARTESIAN_POINT('Ctrl Pts',(-0.818202361614366,-2.62672034503694,
8.7698851615837));
#403166=CARTESIAN_POINT('Ctrl Pts',(-0.811026787668476,-2.62909679595021,
8.77093053738833));
#403167=CARTESIAN_POINT('Ctrl Pts',(-0.819804219376154,-2.61772748538993,
8.75371302330492));
#403168=CARTESIAN_POINT('Ctrl Pts',(-0.81847299177316,-2.62521708046822,
8.7530082828756));
#403169=CARTESIAN_POINT('Ctrl Pts',(-0.811163157381088,-2.62744437939174,
8.75267964240738));
#403170=CARTESIAN_POINT('Origin',(-0.809948649286955,-2.60190157316117,
8.78727029226991));
#403171=CARTESIAN_POINT('Ctrl Pts',(-0.834899689636828,-2.53374831658168,
8.85049129520029));
#403172=CARTESIAN_POINT('Ctrl Pts',(-0.83386656335501,-2.53949581710878,
8.85711686593484));
#403173=CARTESIAN_POINT('Ctrl Pts',(-0.825328369435533,-2.53994303820322,
8.85933012996512));
#403174=CARTESIAN_POINT('Ctrl Pts',(-0.830677482908384,-2.55723734771397,
8.82945683644724));
#403175=CARTESIAN_POINT('Ctrl Pts',(-0.829635781053786,-2.56303255597043,
8.8360746990239));
#403176=CARTESIAN_POINT('Ctrl Pts',(-0.821070557575579,-2.56344363901071,
8.8382956714852));
#403177=CARTESIAN_POINT('Ctrl Pts',(-0.826461569719549,-2.58069136655118,
8.80838214965003));
#403178=CARTESIAN_POINT('Ctrl Pts',(-0.82541575682307,-2.58650944540522,
8.81501364461996));
#403179=CARTESIAN_POINT('Ctrl Pts',(-0.816819862423326,-2.58690870980847,
8.81722098428721));
#403180=CARTESIAN_POINT('Ctrl Pts',(-0.822251471860003,-2.60411303347872,
8.78727029226991));
#403181=CARTESIAN_POINT('Ctrl Pts',(-0.821205485250568,-2.60993207873471,
8.79393457792714));
#403182=CARTESIAN_POINT('Ctrl Pts',(-0.812575755917834,-2.61034096358643,
8.79610912703474));
#403183=CARTESIAN_POINT('Origin',(-0.822596867063781,-2.53153685626413,
8.85049129520029));
#403184=CARTESIAN_POINT('Ctrl Pts',(-0.84636156559358,-2.52994271156921,
8.85049129520029));
#403185=CARTESIAN_POINT('Ctrl Pts',(-0.850627167658196,-2.53393091307483,
8.85711686593484));
#403186=CARTESIAN_POINT('Ctrl Pts',(-0.857737280217463,-2.5291825384573,
8.85933012996512));
#403187=CARTESIAN_POINT('Ctrl Pts',(-0.842587849021636,-2.52641440726749,
8.8633249698723));
#403188=CARTESIAN_POINT('Ctrl Pts',(-0.847054013910112,-2.52522896829153,
8.86648636486736));
#403189=CARTESIAN_POINT('Ctrl Pts',(-0.847168453388,-2.51932447800883,8.87206031107457));
#403190=CARTESIAN_POINT('Ctrl Pts',(-0.835819892408176,-2.52862903348297,
8.86341338519878));
#403191=CARTESIAN_POINT('Ctrl Pts',(-0.831508491736669,-2.53032764906163,
8.86654584966058));
#403192=CARTESIAN_POINT('Ctrl Pts',(-0.827919486529851,-2.52561137994159,
8.87215952290714));
#403193=CARTESIAN_POINT('Ctrl Pts',(-0.834899689636828,-2.53374831658168,
8.85049129520029));
#403194=CARTESIAN_POINT('Ctrl Pts',(-0.83386656335501,-2.53949581710877,
8.85711686593484));
#403195=CARTESIAN_POINT('Ctrl Pts',(-0.825328369435533,-2.53994303820322,
8.85933012996512));
#403196=CARTESIAN_POINT('Origin',(-0.854898517487354,-2.5208119694108,8.85049129520029));
#403197=CARTESIAN_POINT('Ctrl Pts',(-0.89858389776343,-2.57876892194511,
8.78727029226991));
#403198=CARTESIAN_POINT('Ctrl Pts',(-0.902902597925538,-2.58280676847368,
8.79393457792714));
#403199=CARTESIAN_POINT('Ctrl Pts',(-0.910063138901394,-2.57797292237442,
8.79610912703474));
#403200=CARTESIAN_POINT('Ctrl Pts',(-0.881201122358369,-2.56251658288672,
8.80838214965003));
#403201=CARTESIAN_POINT('Ctrl Pts',(-0.885519105289315,-2.5665537588271,
8.81501364461988));
#403202=CARTESIAN_POINT('Ctrl Pts',(-0.892646776397478,-2.56173243979916,
8.81722098428721));
#403203=CARTESIAN_POINT('Ctrl Pts',(-0.863794336451352,-2.54624179477691,
8.82945683644723));
#403204=CARTESIAN_POINT('Ctrl Pts',(-0.86809534559213,-2.55026310076634,
8.83607469902389));
#403205=CARTESIAN_POINT('Ctrl Pts',(-0.875205505457217,-2.54546959795621,
8.83829567148519));
#403206=CARTESIAN_POINT('Ctrl Pts',(-0.846361565593581,-2.52994271156921,
8.85049129520029));
#403207=CARTESIAN_POINT('Ctrl Pts',(-0.850627167658196,-2.53393091307483,
8.85711686593484));
#403208=CARTESIAN_POINT('Ctrl Pts',(-0.857737280217463,-2.5291825384573,
8.85933012996512));
#403209=CARTESIAN_POINT('Origin',(-0.907120849657204,-2.5696381797867,8.78727029226991));
#403210=CARTESIAN_POINT('Ctrl Pts',(-0.908691583495682,-2.58821925958122,
8.75374538247848));
#403211=CARTESIAN_POINT('Ctrl Pts',(-0.914233353523221,-2.59341860216942,
8.75304829418602));
#403212=CARTESIAN_POINT('Ctrl Pts',(-0.921418004981141,-2.59083956617952,
8.75272238421917));
#403213=CARTESIAN_POINT('Ctrl Pts',(-0.909655777654809,-2.5891207508666,
8.76769408445019));
#403214=CARTESIAN_POINT('Ctrl Pts',(-0.915337475387793,-2.5944504287033,
8.76974318093968));
#403215=CARTESIAN_POINT('Ctrl Pts',(-0.922503084835728,-2.59206874893479,
8.7707786988043));
#403216=CARTESIAN_POINT('Ctrl Pts',(-0.904713867650227,-2.58450022009429,
8.78108014887992));
#403217=CARTESIAN_POINT('Ctrl Pts',(-0.909526302439,-2.58901970111583,8.78639403366326));
#403218=CARTESIAN_POINT('Ctrl Pts',(-0.916943242212213,-2.58577762151636,
8.78812224174741));
#403219=CARTESIAN_POINT('Ctrl Pts',(-0.896615168114524,-2.57692819012542,
8.78944554828685));
#403220=CARTESIAN_POINT('Ctrl Pts',(-0.900667077682591,-2.58074112160516,
8.79673892988686));
#403221=CARTESIAN_POINT('Ctrl Pts',(-0.907869787598809,-2.5754852178599,
8.79894799272499));
#403222=CARTESIAN_POINT('Origin',(-0.91736377547371,-2.57921498783034,8.75721825406948));
#403223=CARTESIAN_POINT('Origin',(-0.91736377547371,-2.57921498783034,9.));
#403224=CARTESIAN_POINT('Origin',(-0.91736377547371,-2.57921498783034,7.51860402984325));
#403225=CARTESIAN_POINT('Ctrl Pts',(-0.902424603106939,-2.59383933776842,
7.50366195182966));
#403226=CARTESIAN_POINT('Ctrl Pts',(-0.903627891060323,-2.59729794873401,
7.50000065167735));
#403227=CARTESIAN_POINT('Ctrl Pts',(-0.903627891060433,-2.59729794873397,
7.49482233047108));
#403228=CARTESIAN_POINT('Ctrl Pts',(-0.909800645744154,-2.59286579032708,
7.50215800491337));
#403229=CARTESIAN_POINT('Ctrl Pts',(-0.912631876385771,-2.59416534033701,
7.49877273257265));
#403230=CARTESIAN_POINT('Ctrl Pts',(-0.915892318043139,-2.5930310226792,
7.49481816995649));
#403231=CARTESIAN_POINT('Ctrl Pts',(-0.910885454044046,-2.59027094788589,
7.51043025814041));
#403232=CARTESIAN_POINT('Ctrl Pts',(-0.916079119671714,-2.59293901728808,
7.51006209594514));
#403233=CARTESIAN_POINT('Ctrl Pts',(-0.921555036631571,-2.590991376764,
7.50731281821697));
#403234=CARTESIAN_POINT('Ctrl Pts',(-0.908825719620616,-2.58834469769699,
7.51860402984325));
#403235=CARTESIAN_POINT('Ctrl Pts',(-0.914383355130147,-2.59354216871026,
7.51860402984324));
#403236=CARTESIAN_POINT('Ctrl Pts',(-0.92155265116081,-2.59099222521769,
7.51860402984325));
#403237=CARTESIAN_POINT('Origin',(0.,0.,7.5));
#403238=CARTESIAN_POINT('Origin',(-0.682528638916234,-2.57897124462359,
7.5));
#403239=CARTESIAN_POINT('',(-0.682528638916234,-2.57897124462359,7.59394543036555));
#403240=CARTESIAN_POINT('',(-0.682528638916234,-2.57897124462359,8.85049129520029));
#403241=CARTESIAN_POINT('',(-0.682528638916234,-2.57897124462359,7.5));
#403242=CARTESIAN_POINT('',(-0.731515368664204,-2.63104303262371,8.78727029226991));
#403243=CARTESIAN_POINT('Ctrl Pts',(-0.682528638916234,-2.57897124462359,
8.85049129520029));
#403244=CARTESIAN_POINT('Ctrl Pts',(-0.698881284484156,-2.59635373775254,
8.82945686509571));
#403245=CARTESIAN_POINT('Ctrl Pts',(-0.715209619867108,-2.61371038970359,
8.80838212259895));
#403246=CARTESIAN_POINT('Ctrl Pts',(-0.731515368664204,-2.63104303262371,
8.78727029226991));
#403247=CARTESIAN_POINT('',(-0.741123661093001,-2.64125643059841,8.75721825406948));
#403248=CARTESIAN_POINT('Origin',(-0.712208829051481,-2.6105209113155,8.75937679713132));
#403249=CARTESIAN_POINT('',(-0.741123661093001,-2.64125643059841,7.51860402984325));
#403250=CARTESIAN_POINT('',(-0.741123661093001,-2.64125643059841,7.5));
#403251=CARTESIAN_POINT('Ctrl Pts',(-0.741123661093001,-2.64125643059841,
7.51860402984325));
#403252=CARTESIAN_POINT('Ctrl Pts',(-0.733577841762315,-2.63323539497313,
7.52834476460825));
#403253=CARTESIAN_POINT('Ctrl Pts',(-0.726027123794601,-2.62520915220727,
7.53807742314407));
#403254=CARTESIAN_POINT('Ctrl Pts',(-0.71847134271161,-2.61717752746414,
7.54780169004674));
#403255=CARTESIAN_POINT('Ctrl Pts',(-0.706503393831275,-2.60445586794331,
7.5632044032688));
#403256=CARTESIAN_POINT('Ctrl Pts',(-0.694522727030071,-2.59172068955963,
7.57858609112103));
#403257=CARTESIAN_POINT('Ctrl Pts',(-0.682528638916234,-2.57897124462359,
7.59394543036555));
#403258=CARTESIAN_POINT('Origin',(-0.604952940619234,-2.8490235055211,7.5));
#403259=CARTESIAN_POINT('',(-0.650355981859141,-2.66505851907034,8.75721825406948));
#403260=CARTESIAN_POINT('',(-0.653715973115249,-2.65144443664273,8.78727029226991));
#403261=CARTESIAN_POINT('Origin',(-0.662244884137802,-2.61688681764065,
8.75658640621008));
#403262=CARTESIAN_POINT('',(-0.670846486662608,-2.58203466569847,8.85049129520029));
#403263=CARTESIAN_POINT('Ctrl Pts',(-0.653715973115249,-2.65144443664273,
8.78727029226991));
#403264=CARTESIAN_POINT('Ctrl Pts',(-0.659418044923381,-2.62834066354124,
8.80838212259896));
#403265=CARTESIAN_POINT('Ctrl Pts',(-0.665128015193342,-2.6052048872879,
8.82945686509571));
#403266=CARTESIAN_POINT('Ctrl Pts',(-0.670846486662608,-2.58203466569847,
8.85049129520029));
#403267=CARTESIAN_POINT('',(-0.670846486662608,-2.58203466569847,7.59394543036555));
#403268=CARTESIAN_POINT('',(-0.670846486662608,-2.58203466569847,7.5));
#403269=CARTESIAN_POINT('',(-0.650355981859141,-2.66505851907034,7.51860402984325));
#403270=CARTESIAN_POINT('Ctrl Pts',(-0.670846486662608,-2.58203466569847,
7.59394543036555));
#403271=CARTESIAN_POINT('Ctrl Pts',(-0.666652189758541,-2.59902920509618,
7.57858609112103));
#403272=CARTESIAN_POINT('Ctrl Pts',(-0.662462586247605,-2.61600472770608,
7.56320440326857));
#403273=CARTESIAN_POINT('Ctrl Pts',(-0.658277430155668,-2.63296223017113,
7.54780169004651));
#403274=CARTESIAN_POINT('Ctrl Pts',(-0.655635196006356,-2.64366808943085,
7.53807742314383));
#403275=CARTESIAN_POINT('Ctrl Pts',(-0.652994732413329,-2.65436677471377,
7.52834476460825));
#403276=CARTESIAN_POINT('Ctrl Pts',(-0.650355981859142,-2.66505851907034,
7.51860402984325));
#403277=CARTESIAN_POINT('',(-0.650355981859141,-2.66505851907034,7.5));
#403278=CARTESIAN_POINT('Origin',(-0.677521207658174,-2.58368200434956,
7.5));
#403279=CARTESIAN_POINT('Ctrl Pts',(-0.670846486662608,-2.58203466569847,
8.85049129520029));
#403280=CARTESIAN_POINT('Ctrl Pts',(-0.670892890456633,-2.58184664584108,
8.85097269580138));
#403281=CARTESIAN_POINT('Ctrl Pts',(-0.670946875156401,-2.58166301368505,
8.85143669361005));
#403282=CARTESIAN_POINT('Ctrl Pts',(-0.671011765372886,-2.58147556015295,
8.8519052845931));
#403283=CARTESIAN_POINT('Ctrl Pts',(-0.671138686521143,-2.58110891293204,
8.85282181883899));
#403284=CARTESIAN_POINT('Ctrl Pts',(-0.671304249801605,-2.58073714253129,
8.85372622499636));
#403285=CARTESIAN_POINT('Ctrl Pts',(-0.671525138335623,-2.58036068787951,
8.85462257735071));
#403286=CARTESIAN_POINT('Ctrl Pts',(-0.671708512151346,-2.58004816859801,
8.85536669723987));
#403287=CARTESIAN_POINT('Ctrl Pts',(-0.67193002919577,-2.57973233380185,
8.85610498449051));
#403288=CARTESIAN_POINT('Ctrl Pts',(-0.672205804986711,-2.5794180029897,
8.85681338218371));
#403289=CARTESIAN_POINT('Ctrl Pts',(-0.672456071950103,-2.57913274728401,
8.85745625420284));
#403290=CARTESIAN_POINT('Ctrl Pts',(-0.672753713651867,-2.57884475725327,
8.85808743050666));
#403291=CARTESIAN_POINT('Ctrl Pts',(-0.673125539874815,-2.57856398687628,
8.8586680450841));
#403292=CARTESIAN_POINT('Ctrl Pts',(-0.673297092433881,-2.57843444551069,
8.85893592806395));
#403293=CARTESIAN_POINT('Ctrl Pts',(-0.673484652170842,-2.57830655186085,
8.85919241173848));
#403294=CARTESIAN_POINT('Ctrl Pts',(-0.673692155647793,-2.57818220473043,
8.85943017985534));
#403295=CARTESIAN_POINT('Ctrl Pts',(-0.673972346769279,-2.57801429929367,
8.8597512372));
#403296=CARTESIAN_POINT('Ctrl Pts',(-0.67429636215277,-2.57784913604231,
8.86004599534706));
#403297=CARTESIAN_POINT('Ctrl Pts',(-0.67466503880102,-2.57769797846511,
8.86026130871721));
#403298=CARTESIAN_POINT('Ctrl Pts',(-0.674800021716039,-2.57764263541451,
8.86034014101235));
#403299=CARTESIAN_POINT('Ctrl Pts',(-0.674943014382129,-2.57758832710581,
8.86040910639692));
#403300=CARTESIAN_POINT('Ctrl Pts',(-0.675090240476513,-2.57753684760079,
8.86046313645506));
#403301=CARTESIAN_POINT('Ctrl Pts',(-0.675319985563791,-2.57745651426433,
8.86054744990829));
#403302=CARTESIAN_POINT('Ctrl Pts',(-0.675566359499169,-2.57738101538588,
8.86059655985668));
#403303=CARTESIAN_POINT('Ctrl Pts',(-0.67581347573792,-2.57731491283742,
8.86059725258816));
#403304=CARTESIAN_POINT('Ctrl Pts',(-0.676061162913906,-2.57724865756566,
8.86059794692011));
#403305=CARTESIAN_POINT('Ctrl Pts',(-0.676313029242146,-2.57719367384813,
8.86056369958366));
#403306=CARTESIAN_POINT('Ctrl Pts',(-0.67655453520928,-2.57714928401131,
8.86048590497774));
#403307=CARTESIAN_POINT('Ctrl Pts',(-0.676617561076204,-2.57713769958554,
8.86046560290182));
#403308=CARTESIAN_POINT('Ctrl Pts',(-0.676680717651053,-2.5771267750407,
8.86044257503091));
#403309=CARTESIAN_POINT('Ctrl Pts',(-0.676742047748341,-2.57711681560841,
8.86041778462584));
#403310=CARTESIAN_POINT('Ctrl Pts',(-0.677154723198782,-2.57704980098778,
8.86025097596201));
#403311=CARTESIAN_POINT('Ctrl Pts',(-0.677540131460308,-2.57701781811485,
8.8599848982295));
#403312=CARTESIAN_POINT('Ctrl Pts',(-0.677886322802429,-2.57701335701957,
8.85968173251461));
#403313=CARTESIAN_POINT('Ctrl Pts',(-0.678069438188012,-2.57701099735576,
8.85952137522076));
#403314=CARTESIAN_POINT('Ctrl Pts',(-0.67824510867004,-2.57701610131725,
8.85934740853961));
#403315=CARTESIAN_POINT('Ctrl Pts',(-0.678410902053581,-2.57702704303034,
8.8591675900182));
#403316=CARTESIAN_POINT('Ctrl Pts',(-0.679076648666189,-2.57707097969576,
8.85844552518695));
#403317=CARTESIAN_POINT('Ctrl Pts',(-0.679620958726725,-2.57720851046265,
8.85759444184123));
#403318=CARTESIAN_POINT('Ctrl Pts',(-0.680054687829788,-2.577360508228,
8.85683498915138));
#403319=CARTESIAN_POINT('Ctrl Pts',(-0.680100076425306,-2.57737641438933,
8.85675551444997));
#403320=CARTESIAN_POINT('Ctrl Pts',(-0.680144243875811,-2.57739249616704,
8.85667699793651));
#403321=CARTESIAN_POINT('Ctrl Pts',(-0.680187195361034,-2.57740867382615,
8.85659965593547));
#403322=CARTESIAN_POINT('Ctrl Pts',(-0.680766956700293,-2.57762704069422,
8.85555568965886));
#403323=CARTESIAN_POINT('Ctrl Pts',(-0.681292606769922,-2.57792063379262,
8.85434650606346));
#403324=CARTESIAN_POINT('Ctrl Pts',(-0.681769774569088,-2.5782854786949,
8.85297329937117));
#403325=CARTESIAN_POINT('Ctrl Pts',(-0.682038152381857,-2.5784906817221,
8.85220095427747));
#403326=CARTESIAN_POINT('Ctrl Pts',(-0.68229111167692,-2.57871875852963,
8.85137579139183));
#403327=CARTESIAN_POINT('Ctrl Pts',(-0.682528638916234,-2.57897124462359,
8.85049129520029));
#403328=CARTESIAN_POINT('Origin',(-0.677521207658174,-2.58368200434956,
7.59394543036555));
#403329=CARTESIAN_POINT('Ctrl Pts',(-0.670981212530835,-2.58148878062456,
7.59443877723642));
#403330=CARTESIAN_POINT('Ctrl Pts',(-0.672368759343822,-2.57586668959982,
7.58783886950016));
#403331=CARTESIAN_POINT('Ctrl Pts',(-0.680858400978228,-2.57593856766321,
7.58559994247159));
#403332=CARTESIAN_POINT('Ctrl Pts',(-0.663406635187641,-2.61217961058346,
7.56670252222133));
#403333=CARTESIAN_POINT('Ctrl Pts',(-0.664792176601553,-2.60656564507641,
7.56004874999027));
#403334=CARTESIAN_POINT('Ctrl Pts',(-0.67333230320828,-2.60661658423106,
7.55786368756704));
#403335=CARTESIAN_POINT('Ctrl Pts',(-0.655846202610834,-2.64281312848384,
7.53888913333559));
#403336=CARTESIAN_POINT('Ctrl Pts',(-0.657239978365184,-2.6371657989049,
7.53222002137279));
#403337=CARTESIAN_POINT('Ctrl Pts',(-0.665818860235125,-2.63723812166668,
7.53005029815327));
#403338=CARTESIAN_POINT('Ctrl Pts',(-0.648300256915117,-2.67338794813822,
7.51101258149734));
#403339=CARTESIAN_POINT('Ctrl Pts',(-0.649710927764185,-2.66767216266333,
7.5043616886572));
#403340=CARTESIAN_POINT('Ctrl Pts',(-0.658318523541249,-2.66780168672796,
7.50217374673251));
#403341=CARTESIAN_POINT('',(-0.658718750143873,-2.6661707753905,7.50366116523517));
#403342=CARTESIAN_POINT('Ctrl Pts',(-0.650355981859141,-2.66505851907034,
7.51860402984325));
#403343=CARTESIAN_POINT('Ctrl Pts',(-0.650250166117427,-2.66548726549259,
7.51734760759493));
#403344=CARTESIAN_POINT('Ctrl Pts',(-0.650212310040413,-2.66588895539464,
7.51608817408572));
#403345=CARTESIAN_POINT('Ctrl Pts',(-0.650255795434444,-2.66626391779723,
7.51481005913119));
#403346=CARTESIAN_POINT('Ctrl Pts',(-0.650295185543474,-2.66660356770152,
7.51365231206383));
#403347=CARTESIAN_POINT('Ctrl Pts',(-0.650401124727235,-2.66692179482434,
7.51247773061042));
#403348=CARTESIAN_POINT('Ctrl Pts',(-0.650606814530752,-2.6672014295012,
7.51129758471022));
#403349=CARTESIAN_POINT('Ctrl Pts',(-0.650862463465862,-2.66754898346906,
7.50983079813402));
#403350=CARTESIAN_POINT('Ctrl Pts',(-0.651274536664425,-2.66781811159763,
7.50839324291155));
#403351=CARTESIAN_POINT('Ctrl Pts',(-0.651891120888266,-2.66794175530204,
7.50715379678855));
#403352=CARTESIAN_POINT('Ctrl Pts',(-0.652175965033233,-2.66799887513076,
7.50658120839351));
#403353=CARTESIAN_POINT('Ctrl Pts',(-0.652546816749148,-2.66802374990068,
7.50598221009429));
#403354=CARTESIAN_POINT('Ctrl Pts',(-0.652996372582813,-2.66799309213236,
7.50545747549611));
#403355=CARTESIAN_POINT('Ctrl Pts',(-0.653236269490711,-2.66797673219823,
7.50517746087247));
#403356=CARTESIAN_POINT('Ctrl Pts',(-0.653501193456985,-2.66794458333831,
7.50491486231392));
#403357=CARTESIAN_POINT('Ctrl Pts',(-0.653783927906875,-2.66789584104,7.50468370960993));
#403358=CARTESIAN_POINT('Ctrl Pts',(-0.654206705092984,-2.66782295592915,
7.50433806340447));
#403359=CARTESIAN_POINT('Ctrl Pts',(-0.654681888865048,-2.6677102342832,
7.50405484070984));
#403360=CARTESIAN_POINT('Ctrl Pts',(-0.655177311127184,-2.66756457064415,
7.50385766036131));
#403361=CARTESIAN_POINT('Ctrl Pts',(-0.655230288837517,-2.66754899418207,
7.50383657498791));
#403362=CARTESIAN_POINT('Ctrl Pts',(-0.655283478613827,-2.66753306175526,
7.50381643264938));
#403363=CARTESIAN_POINT('Ctrl Pts',(-0.655336827290485,-2.66751679707098,
7.50379723213559));
#403364=CARTESIAN_POINT('Ctrl Pts',(-0.655692947158727,-2.66740822498289,
7.50366906242519));
#403365=CARTESIAN_POINT('Ctrl Pts',(-0.656063684366644,-2.66728179801424,
7.50358235568538));
#403366=CARTESIAN_POINT('Ctrl Pts',(-0.656418100142817,-2.66715134813715,
7.5035341175365));
#403367=CARTESIAN_POINT('Ctrl Pts',(-0.656949506487069,-2.66695575331051,
7.50346178989176));
#403368=CARTESIAN_POINT('Ctrl Pts',(-0.657512862320752,-2.66672274300315,
7.50346967198527));
#403369=CARTESIAN_POINT('Ctrl Pts',(-0.658058864751418,-2.66647698198924,
7.50354272648693));
#403370=CARTESIAN_POINT('Ctrl Pts',(-0.658283446852733,-2.66637589539726,
7.50357277531559));
#403371=CARTESIAN_POINT('Ctrl Pts',(-0.658504852827761,-2.66627291519395,
7.50361331098762));
#403372=CARTESIAN_POINT('Ctrl Pts',(-0.658718750144213,-2.66617077539187,
7.50366116523659));
#403373=CARTESIAN_POINT('',(-0.678263889302273,-2.586514171338,7.57603338622103));
#403374=CARTESIAN_POINT('Origin',(-0.680508179114217,-2.5950613728002,7.58486873427629));
#403375=CARTESIAN_POINT('Ctrl Pts',(-0.658718750125062,-2.66617077544467,
7.50366116529969));
#403376=CARTESIAN_POINT('Ctrl Pts',(-0.665223977061745,-2.63966210099077,
7.52783573079709));
#403377=CARTESIAN_POINT('Ctrl Pts',(-0.671738733243923,-2.61311115757656,
7.55196141284068));
#403378=CARTESIAN_POINT('Ctrl Pts',(-0.678263888672613,-2.58651417242021,
7.57603338728831));
#403379=CARTESIAN_POINT('Ctrl Pts',(-0.670770761278379,-2.58307524303168,
7.59639677331371));
#403380=CARTESIAN_POINT('Ctrl Pts',(-0.672361328299651,-2.56400514804977,
7.59974925422224));
#403381=CARTESIAN_POINT('Ctrl Pts',(-0.683105249421501,-2.57984075934191,
7.59639677331372));
#403382=CARTESIAN_POINT('Ctrl Pts',(-0.670465937780008,-2.57918651744113,
7.58707626057423));
#403383=CARTESIAN_POINT('Ctrl Pts',(-0.674975104133252,-2.5739726081208,
7.58811717123965));
#403384=CARTESIAN_POINT('Ctrl Pts',(-0.681462581934873,-2.57630285775876,
7.58707626057423));
#403385=CARTESIAN_POINT('Ctrl Pts',(-0.675135748308901,-2.58307476921871,
7.58015376756929));
#403386=CARTESIAN_POINT('Ctrl Pts',(-0.676728207785887,-2.58065795214827,
7.5820876076604));
#403387=CARTESIAN_POINT('Ctrl Pts',(-0.679301722070223,-2.58198232224996,
7.5801537675693));
#403388=CARTESIAN_POINT('Ctrl Pts',(-0.678263889092161,-2.58651417053755,
7.57603338509286));
#403389=CARTESIAN_POINT('Ctrl Pts',(-0.678263889092161,-2.58651417053755,
7.57603338509286));
#403390=CARTESIAN_POINT('Ctrl Pts',(-0.678263889092161,-2.58651417053755,
7.57603338509286));
#403391=CARTESIAN_POINT('Origin',(-0.680502659389277,-2.59506282024289,
7.58486873427622));
#403392=CARTESIAN_POINT('Ctrl Pts',(-0.747020829444778,-2.64752498744625,
7.51098857897448));
#403393=CARTESIAN_POINT('Ctrl Pts',(-0.742986830895866,-2.64323693804364,
7.50433767179957));
#403394=CARTESIAN_POINT('Ctrl Pts',(-0.735550410854303,-2.64757372349462,
7.50214974420965));
#403395=CARTESIAN_POINT('Ctrl Pts',(-0.725436098627555,-2.62458090579523,
7.53887321589168));
#403396=CARTESIAN_POINT('Ctrl Pts',(-0.721450434540312,-2.62034423483435,
7.5322040745206));
#403397=CARTESIAN_POINT('Ctrl Pts',(-0.714010955012724,-2.62461706343848,
7.53003438070912));
#403398=CARTESIAN_POINT('Ctrl Pts',(-0.70380991716486,-2.60159276304368,
7.56669465659227));
#403399=CARTESIAN_POINT('Ctrl Pts',(-0.699847807611344,-2.59738113002054,
7.56004085833293));
#403400=CARTESIAN_POINT('Ctrl Pts',(-0.69243160852584,-2.60161629722503,
7.55785582193789));
#403401=CARTESIAN_POINT('Ctrl Pts',(-0.682143263122402,-2.5785615988534,
7.59443891967696));
#403402=CARTESIAN_POINT('Ctrl Pts',(-0.678175409003361,-2.57434385948673,
7.58783901202978));
#403403=CARTESIAN_POINT('Ctrl Pts',(-0.670813497415762,-2.57857250415905,
7.58560008491213));
#403404=CARTESIAN_POINT('',(-0.734382828366891,-2.6463293175146,7.50366116523517));
#403405=CARTESIAN_POINT('Ctrl Pts',(-0.734382828366991,-2.64632931751496,
7.50366116523554));
#403406=CARTESIAN_POINT('Ctrl Pts',(-0.7351388143909,-2.64627810571535,
7.50350835821027));
#403407=CARTESIAN_POINT('Ctrl Pts',(-0.735832082908394,-2.64620643442547,
7.50345484956));
#403408=CARTESIAN_POINT('Ctrl Pts',(-0.736483307107746,-2.64611277011765,
7.50349758195598));
#403409=CARTESIAN_POINT('Ctrl Pts',(-0.73681743341806,-2.64606471338141,
7.50351950684424));
#403410=CARTESIAN_POINT('Ctrl Pts',(-0.737173443029265,-2.64600625855206,
7.50357029184312));
#403411=CARTESIAN_POINT('Ctrl Pts',(-0.737515189580187,-2.64594045470856,
7.50365515313923));
#403412=CARTESIAN_POINT('Ctrl Pts',(-0.738040934162347,-2.64583922175066,
7.50378570417639));
#403413=CARTESIAN_POINT('Ctrl Pts',(-0.738548420846335,-2.64571796522779,
7.50400001621911));
#403414=CARTESIAN_POINT('Ctrl Pts',(-0.738998494895536,-2.64558370626699,
7.50428903009634));
#403415=CARTESIAN_POINT('Ctrl Pts',(-0.739048449652339,-2.64556880455527,
7.50432110841318));
#403416=CARTESIAN_POINT('Ctrl Pts',(-0.739097725961653,-2.64555375201861,
7.50435406373354));
#403417=CARTESIAN_POINT('Ctrl Pts',(-0.739146291662912,-2.64553856487361,
7.50438785222352));
#403418=CARTESIAN_POINT('Ctrl Pts',(-0.739442808612724,-2.6454458400535,
7.50459414719561));
#403419=CARTESIAN_POINT('Ctrl Pts',(-0.739717403222056,-2.64534612893593,
7.50483629897752));
#403420=CARTESIAN_POINT('Ctrl Pts',(-0.739960005034027,-2.64524448842675,
7.5050991045531));
#403421=CARTESIAN_POINT('Ctrl Pts',(-0.740495208998279,-2.64502025925466,
7.50567888004914));
#403422=CARTESIAN_POINT('Ctrl Pts',(-0.740895999024185,-2.64477828392327,
7.50637912803144));
#403423=CARTESIAN_POINT('Ctrl Pts',(-0.741184705006695,-2.64453993517567,
7.50710440483569));
#403424=CARTESIAN_POINT('Ctrl Pts',(-0.741255501445223,-2.64448148733087,
7.50728225710685));
#403425=CARTESIAN_POINT('Ctrl Pts',(-0.741321060218752,-2.64442220659312,
7.50746498566954));
#403426=CARTESIAN_POINT('Ctrl Pts',(-0.741380130382238,-2.64436378576598,
7.50764697238949));
#403427=CARTESIAN_POINT('Ctrl Pts',(-0.741697675324592,-2.64404973147709,
7.50862528291181));
#403428=CARTESIAN_POINT('Ctrl Pts',(-0.741859446188481,-2.64373496099275,
7.50965856837421));
#403429=CARTESIAN_POINT('Ctrl Pts',(-0.741930383748714,-2.64343281940981,
7.51067959873201));
#403430=CARTESIAN_POINT('Ctrl Pts',(-0.741969420777586,-2.64326655051562,
7.51124147302578));
#403431=CARTESIAN_POINT('Ctrl Pts',(-0.741980537241458,-2.64310396618176,
7.51180065547252));
#403432=CARTESIAN_POINT('Ctrl Pts',(-0.741971890422264,-2.64294676648674,
7.51235175716501));
#403433=CARTESIAN_POINT('Ctrl Pts',(-0.741942012217466,-2.64240357891952,
7.51425603304535));
#403434=CARTESIAN_POINT('Ctrl Pts',(-0.741666547014249,-2.64186025088833,
7.51626900505179));
#403435=CARTESIAN_POINT('Ctrl Pts',(-0.741200952461297,-2.64134059660316,
7.51827788969242));
#403436=CARTESIAN_POINT('Ctrl Pts',(-0.741175753604239,-2.64131247193123,
7.51838661432544));
#403437=CARTESIAN_POINT('Ctrl Pts',(-0.741149987931403,-2.64128441543338,
7.51849533314856));
#403438=CARTESIAN_POINT('Ctrl Pts',(-0.741123661093005,-2.64125643059841,
7.51860402984325));
#403439=CARTESIAN_POINT('Ctrl Pts',(-0.678263890382501,-2.58651417197306,
7.57603338728985));
#403440=CARTESIAN_POINT('Ctrl Pts',(-0.697000987805607,-2.60648661431919,
7.55196141284922));
#403441=CARTESIAN_POINT('Ctrl Pts',(-0.715706430690877,-2.62642404273905,
7.52783573083105));
#403442=CARTESIAN_POINT('Ctrl Pts',(-0.734382828411178,-2.64632931755386,
7.50366116530176));
#403443=CARTESIAN_POINT('Origin',(-2.34371526914283E-16,-8.93760209386497E-16,
7.49482233047033));
#403444=CARTESIAN_POINT('Origin',(-0.656598725434862,-2.65758995402928,
7.49482233047033));
#403445=CARTESIAN_POINT('Origin',(0.,0.,7.50366116523517));
#403446=CARTESIAN_POINT('Origin',(-0.732019285896496,-2.63781235403044,
7.49482233047033));
#403447=CARTESIAN_POINT('Ctrl Pts',(-0.65035623525911,-2.66505749215231,
7.51860402984325));
#403448=CARTESIAN_POINT('Ctrl Pts',(-0.648533655213682,-2.6724449469243,
7.51860402984325));
#403449=CARTESIAN_POINT('Ctrl Pts',(-0.641134372651985,-2.67421889833352,
7.51860402984325));
#403450=CARTESIAN_POINT('Ctrl Pts',(-0.64967949761657,-2.66780050421939,
7.51041458714367));
#403451=CARTESIAN_POINT('Ctrl Pts',(-0.646780678116779,-2.67286520670501,
7.51004642900444));
#403452=CARTESIAN_POINT('Ctrl Pts',(-0.641132332017705,-2.67421938756826,
7.50729136483011));
#403453=CARTESIAN_POINT('Ctrl Pts',(-0.652012104546077,-2.66937615713541,
7.50215815450137));
#403454=CARTESIAN_POINT('Ctrl Pts',(-0.650349947137616,-2.67200965238524,
7.49877163671527));
#403455=CARTESIAN_POINT('Ctrl Pts',(-0.647000459287308,-2.67283721189065,
7.49481588533168));
#403456=CARTESIAN_POINT('Ctrl Pts',(-0.658718618100706,-2.66617024094247,
7.50366171572174));
#403457=CARTESIAN_POINT('Ctrl Pts',(-0.659596893131287,-2.66972506797452,
7.50000045605858));
#403458=CARTESIAN_POINT('Ctrl Pts',(-0.659596893131166,-2.66972506797455,
7.49482233047317));
#403459=CARTESIAN_POINT('Origin',(-0.638220125503567,-2.66206335788655,
7.51860402984325));
#403460=CARTESIAN_POINT('Origin',(-0.638220125503567,-2.66206335788655,
9.));
#403461=CARTESIAN_POINT('Origin',(-0.638220125503568,-2.66206335788655,
8.75721825406948));
#403462=CARTESIAN_POINT('Ctrl Pts',(-0.654357526473991,-2.64884485132562,
8.78942910404913));
#403463=CARTESIAN_POINT('Ctrl Pts',(-0.653041919255973,-2.65425979420155,
8.79672699501691));
#403464=CARTESIAN_POINT('Ctrl Pts',(-0.644128763436838,-2.65378110920504,
8.79893251111267));
#403465=CARTESIAN_POINT('Ctrl Pts',(-0.6517231462551,-2.65951890676874,
8.78111911759582));
#403466=CARTESIAN_POINT('Ctrl Pts',(-0.650156245245687,-2.66593662687421,
8.78644465894813));
#403467=CARTESIAN_POINT('Ctrl Pts',(-0.642156520060473,-2.66724807978471,
8.78817647674132));
#403468=CARTESIAN_POINT('Ctrl Pts',(-0.650081337635898,-2.66617123271351,
8.76780923932031));
#403469=CARTESIAN_POINT('Ctrl Pts',(-0.648226726776183,-2.67374587167056,
8.76988516158375));
#403470=CARTESIAN_POINT('Ctrl Pts',(-0.640913636083743,-2.67565769930935,
8.77093053738834));
#403471=CARTESIAN_POINT('Ctrl Pts',(-0.650401467845226,-2.66487412019735,
8.75371302330492));
#403472=CARTESIAN_POINT('Ctrl Pts',(-0.648593115387881,-2.67226303505393,
8.75300828287559));
#403473=CARTESIAN_POINT('Ctrl Pts',(-0.641155596302552,-2.67401741505541,
8.75267964240737));
#403474=CARTESIAN_POINT('Origin',(-0.641580116759675,-2.64844927545894,
8.78727029226991));
#403475=CARTESIAN_POINT('Ctrl Pts',(-0.670846486662608,-2.58203466569847,
8.85049129520029));
#403476=CARTESIAN_POINT('Ctrl Pts',(-0.669447239426428,-2.58770416474117,
8.85711686593484));
#403477=CARTESIAN_POINT('Ctrl Pts',(-0.660897934588176,-2.58760342300926,
8.85933012996512));
#403478=CARTESIAN_POINT('Ctrl Pts',(-0.665128007518938,-2.60520491838321,
8.82945683644723));
#403479=CARTESIAN_POINT('Ctrl Pts',(-0.663717145684703,-2.6109214776958,
8.83607469902391));
#403480=CARTESIAN_POINT('Ctrl Pts',(-0.655143182195925,-2.61078294036945,
8.8382956714852));
#403481=CARTESIAN_POINT('Ctrl Pts',(-0.659418052229574,-2.62834063393785,
8.80838214965003));
#403482=CARTESIAN_POINT('Ctrl Pts',(-0.658001622475826,-2.63407975346252,
8.81501364461989));
#403483=CARTESIAN_POINT('Ctrl Pts',(-0.649397808304884,-2.63392745668915,
8.81722098428721));
#403484=CARTESIAN_POINT('Ctrl Pts',(-0.653715973115249,-2.65144443664273,
8.78727029226991));
#403485=CARTESIAN_POINT('Ctrl Pts',(-0.652299308087855,-2.65718450945399,
8.79393457792714));
#403486=CARTESIAN_POINT('Ctrl Pts',(-0.643661112117175,-2.6570396455512,
8.79610912703474));
#403487=CARTESIAN_POINT('Origin',(-0.658710630307035,-2.57903950451468,
8.85049129520029));
#403488=CARTESIAN_POINT('Ctrl Pts',(-0.682528638916234,-2.57897124462359,
8.85049129520029));
#403489=CARTESIAN_POINT('Ctrl Pts',(-0.686529951896131,-2.58322455000411,
8.85711686593484));
#403490=CARTESIAN_POINT('Ctrl Pts',(-0.693929685372884,-2.57894147790725,
8.85933012996512));
#403491=CARTESIAN_POINT('Ctrl Pts',(-0.67898873508248,-2.57520840675055,
8.86332496987231));
#403492=CARTESIAN_POINT('Ctrl Pts',(-0.683521675092156,-2.57431155155301,
8.86648636486739));
#403493=CARTESIAN_POINT('Ctrl Pts',(-0.684014181433158,-2.56842652484136,
8.87206031107457));
#403494=CARTESIAN_POINT('Ctrl Pts',(-0.672092792372952,-2.5769848583099,
8.86341338519876));
#403495=CARTESIAN_POINT('Ctrl Pts',(-0.667681419262742,-2.57840375151124,
8.86654584966056));
#403496=CARTESIAN_POINT('Ctrl Pts',(-0.66440196045204,-2.5734672241188,
8.87215952290715));
#403497=CARTESIAN_POINT('Ctrl Pts',(-0.670846486662608,-2.58203466569847,
8.85049129520029));
#403498=CARTESIAN_POINT('Ctrl Pts',(-0.669447239426428,-2.58770416474117,
8.85711686593484));
#403499=CARTESIAN_POINT('Ctrl Pts',(-0.660897934588176,-2.58760342300926,
8.85933012996512));
#403500=CARTESIAN_POINT('Origin',(-0.691633059385434,-2.57040622694001,
8.85049129520029));
#403501=CARTESIAN_POINT('Ctrl Pts',(-0.731515368664204,-2.63104303262371,
8.78727029226991));
#403502=CARTESIAN_POINT('Ctrl Pts',(-0.735566489878316,-2.63534928303294,
8.79393457792714));
#403503=CARTESIAN_POINT('Ctrl Pts',(-0.743022024337704,-2.63098414602442,
8.79610912703474));
#403504=CARTESIAN_POINT('Ctrl Pts',(-0.715209598974184,-2.61371036749489,
8.80838214965002));
#403505=CARTESIAN_POINT('Ctrl Pts',(-0.719260047395506,-2.61801590274056,
8.81501364461988));
#403506=CARTESIAN_POINT('Ctrl Pts',(-0.726681976909647,-2.61366116108551,
8.81722098428721));
#403507=CARTESIAN_POINT('Ctrl Pts',(-0.698881306430013,-2.59635376108049,
8.82945683644723));
#403508=CARTESIAN_POINT('Ctrl Pts',(-0.702915832726872,-2.60064237146729,
8.83607469902389));
#403509=CARTESIAN_POINT('Ctrl Pts',(-0.710318504785465,-2.59631426692943,
8.83829567148519));
#403510=CARTESIAN_POINT('Ctrl Pts',(-0.682528638916234,-2.57897124462359,
8.85049129520029));
#403511=CARTESIAN_POINT('Ctrl Pts',(-0.686529951896131,-2.58322455000411,
8.85711686593484));
#403512=CARTESIAN_POINT('Ctrl Pts',(-0.693929685372884,-2.57894147790725,
8.85933012996512));
#403513=CARTESIAN_POINT('Origin',(-0.740619789133404,-2.62247801494013,
8.78727029226991));
#403514=CARTESIAN_POINT('Ctrl Pts',(-0.740996801860829,-2.64112155517595,
8.75374538247848));
#403515=CARTESIAN_POINT('Ctrl Pts',(-0.746194062704114,-2.64666527758192,
8.75304829418601));
#403516=CARTESIAN_POINT('Ctrl Pts',(-0.75352919192828,-2.64455186269746,
8.75272238421917));
#403517=CARTESIAN_POINT('Ctrl Pts',(-0.741901256234692,-2.64208297038268,
8.7676940844502));
#403518=CARTESIAN_POINT('Ctrl Pts',(-0.747229806678894,-2.64776572544829,
8.76974318093971));
#403519=CARTESIAN_POINT('Ctrl Pts',(-0.754533288360401,-2.64584804126991,
8.7707786988043));
#403520=CARTESIAN_POINT('Ctrl Pts',(-0.737265538337216,-2.63715530372526,
8.78108014887989));
#403521=CARTESIAN_POINT('Ctrl Pts',(-0.741778521319334,-2.6419738327439,
8.78639403366323));
#403522=CARTESIAN_POINT('Ctrl Pts',(-0.749387942947467,-2.63921361930754,
8.78812224174741));
#403523=CARTESIAN_POINT('Ctrl Pts',(-0.729668620074122,-2.62907994584327,
8.78944554828685));
#403524=CARTESIAN_POINT('Ctrl Pts',(-0.733467909200736,-2.63314464998371,
8.79673892988686));
#403525=CARTESIAN_POINT('Ctrl Pts',(-0.740992567286101,-2.62836102426519,
8.79894799272499));
#403526=CARTESIAN_POINT('Origin',(-0.750228081562201,-2.63269141291484,
8.75721825406948));
#403527=CARTESIAN_POINT('Origin',(-0.750228081562201,-2.63269141291484,
9.));
#403528=CARTESIAN_POINT('Origin',(-0.750228081562201,-2.63269141291484,
7.51860402984325));
#403529=CARTESIAN_POINT('Ctrl Pts',(-0.734382618009671,-2.64632855949765,
7.50366195182966));
#403530=CARTESIAN_POINT('Ctrl Pts',(-0.735361839713509,-2.64985715929995,
7.50000065167735));
#403531=CARTESIAN_POINT('Ctrl Pts',(-0.735361839713621,-2.64985715929991,
7.49482233047108));
#403532=CARTESIAN_POINT('Ctrl Pts',(-0.741805881174942,-2.64582959698829,
7.50215800491337));
#403533=CARTESIAN_POINT('Ctrl Pts',(-0.744548032294539,-2.64730787450337,
7.49877273257268));
#403534=CARTESIAN_POINT('Ctrl Pts',(-0.747874451006705,-2.64638478463707,
7.49481816995647));
#403535=CARTESIAN_POINT('Ctrl Pts',(-0.743054712745854,-2.64330958983561,
7.51043025814041));
#403536=CARTESIAN_POINT('Ctrl Pts',(-0.748066763636952,-2.64630493670231,
7.51006209594513));
#403537=CARTESIAN_POINT('Ctrl Pts',(-0.753656215494947,-2.6447121410188,
7.50731281821699));
#403538=CARTESIAN_POINT('Ctrl Pts',(-0.741122625541046,-2.6412553296967,
7.51860402984325));
#403539=CARTESIAN_POINT('Ctrl Pts',(-0.746335839181204,-2.64679820087801,
7.51860402984325));
#403540=CARTESIAN_POINT('Ctrl Pts',(-0.753653780564773,-2.64471283489161,
7.51860402984325));
#403541=CARTESIAN_POINT('Origin',(0.,0.,7.5));
#403542=CARTESIAN_POINT('Origin',(-0.515891055659646,-2.61740223164621,
7.5));
#403543=CARTESIAN_POINT('',(-0.515891055659646,-2.61740223164621,7.59394543036555));
#403544=CARTESIAN_POINT('',(-0.515891055659646,-2.61740223164621,8.85049129520029));
#403545=CARTESIAN_POINT('',(-0.515891055659646,-2.61740223164621,7.5));
#403546=CARTESIAN_POINT('',(-0.561440886005583,-2.67250562312429,8.78727029226991));
#403547=CARTESIAN_POINT('Ctrl Pts',(-0.515891055659647,-2.61740223164621,
8.85049129520029));
#403548=CARTESIAN_POINT('Ctrl Pts',(-0.531096402804849,-2.63579672817757,
8.82945686509571));
#403549=CARTESIAN_POINT('Ctrl Pts',(-0.546279145362919,-2.6541638790656,
8.80838212259896));
#403550=CARTESIAN_POINT('Ctrl Pts',(-0.561440886005583,-2.67250562312429,
8.78727029226991));
#403551=CARTESIAN_POINT('',(-0.570375062512109,-2.68331364198703,8.75721825406948));
#403552=CARTESIAN_POINT('Origin',(-0.543488870576429,-2.65078869247601,
8.75937679713158));
#403553=CARTESIAN_POINT('',(-0.570375062512109,-2.68331364198703,7.51860402984325));
#403554=CARTESIAN_POINT('',(-0.570375062512109,-2.68331364198703,7.5));
#403555=CARTESIAN_POINT('Ctrl Pts',(-0.570375062512109,-2.68331364198703,
7.51860402984325));
#403556=CARTESIAN_POINT('Ctrl Pts',(-0.563358656393509,-2.67482562413524,
7.52834476460825));
#403557=CARTESIAN_POINT('Ctrl Pts',(-0.556337695325301,-2.66633209598475,
7.53807742314407));
#403558=CARTESIAN_POINT('Ctrl Pts',(-0.549312026368994,-2.65783287251993,
7.54780169004674));
#403559=CARTESIAN_POINT('Ctrl Pts',(-0.538183746447212,-2.6443705618955,
7.5632044032688));
#403560=CARTESIAN_POINT('Ctrl Pts',(-0.527043640891408,-2.63089394534418,
7.57858609112103));
#403561=CARTESIAN_POINT('Ctrl Pts',(-0.515891055659647,-2.61740223164621,
7.59394543036555));
#403562=CARTESIAN_POINT('Origin',(-0.421172437192773,-2.88192934915564,
7.5));
#403563=CARTESIAN_POINT('',(-0.478268870165641,-2.70125132133977,8.75721825406948));
#403564=CARTESIAN_POINT('',(-0.482494215215328,-2.68788048588352,8.78727029226991));
#403565=CARTESIAN_POINT('Origin',(-0.493219716927205,-2.65394031842054,
8.75658640620967));
#403566=CARTESIAN_POINT('',(-0.504036631578572,-2.61971088052921,8.85049129520029));
#403567=CARTESIAN_POINT('Ctrl Pts',(-0.482494215215328,-2.68788048588352,
8.78727029226991));
#403568=CARTESIAN_POINT('Ctrl Pts',(-0.489664835330383,-2.66518951495683,
8.80838212259895));
#403569=CARTESIAN_POINT('Ctrl Pts',(-0.496845388128006,-2.64246711268839,
8.82945686509571));
#403570=CARTESIAN_POINT('Ctrl Pts',(-0.504036631578572,-2.61971088052921,
8.85049129520029));
#403571=CARTESIAN_POINT('',(-0.504036631578572,-2.61971088052921,7.59394543036555));
#403572=CARTESIAN_POINT('',(-0.504036631578572,-2.61971088052921,7.5));
#403573=CARTESIAN_POINT('',(-0.478268870165641,-2.70125132133977,7.51860402984325));
#403574=CARTESIAN_POINT('Ctrl Pts',(-0.504036631578572,-2.61971088052921,
7.59394543036555));
#403575=CARTESIAN_POINT('Ctrl Pts',(-0.49876210842965,-2.63640177329775,
7.57858609112103));
#403576=CARTESIAN_POINT('Ctrl Pts',(-0.493493487440555,-2.65307398905726,
7.56320440326857));
#403577=CARTESIAN_POINT('Ctrl Pts',(-0.488230459287406,-2.66972850664335,
7.54780169004651));
#403578=CARTESIAN_POINT('Ctrl Pts',(-0.484907727133681,-2.68024308104382,
7.53807742314383));
#403579=CARTESIAN_POINT('Ctrl Pts',(-0.481587221536713,-2.69075060964715,
7.52834476460825));
#403580=CARTESIAN_POINT('Ctrl Pts',(-0.478268870165641,-2.70125132133977,
7.51860402984325));
#403581=CARTESIAN_POINT('',(-0.478268870165641,-2.70125132133977,7.5));
#403582=CARTESIAN_POINT('Origin',(-0.510592093294233,-2.62178248538885,
7.5));
#403583=CARTESIAN_POINT('Ctrl Pts',(-0.504036631578572,-2.61971088052921,
8.85049129520029));
#403584=CARTESIAN_POINT('Ctrl Pts',(-0.504094986504649,-2.61952622008007,
8.85097269580138));
#403585=CARTESIAN_POINT('Ctrl Pts',(-0.504160625639693,-2.61934642402759,
8.85143669361005));
#403586=CARTESIAN_POINT('Ctrl Pts',(-0.504237392721307,-2.61916351316932,
8.8519052845931));
#403587=CARTESIAN_POINT('Ctrl Pts',(-0.504387544264551,-2.61880575113034,
8.85282181883899));
#403588=CARTESIAN_POINT('Ctrl Pts',(-0.504576586788855,-2.61844535224755,
8.85372622499635));
#403589=CARTESIAN_POINT('Ctrl Pts',(-0.504821141016042,-2.61808382343919,
8.8546225773507));
#403590=CARTESIAN_POINT('Ctrl Pts',(-0.505024161249708,-2.61778369506278,
8.85536669723986));
#403591=CARTESIAN_POINT('Ctrl Pts',(-0.505265458768475,-2.61748270182885,
8.85610498449051));
#403592=CARTESIAN_POINT('Ctrl Pts',(-0.505560807192758,-2.61718668585866,
8.85681338218371));
#403593=CARTESIAN_POINT('Ctrl Pts',(-0.50582883635165,-2.61691805090081,
8.85745625420284));
#403594=CARTESIAN_POINT('Ctrl Pts',(-0.506144318101241,-2.61664972254577,
8.85808743050666));
#403595=CARTESIAN_POINT('Ctrl Pts',(-0.506533369387157,-2.61639335202953,
8.85866804508411));
#403596=CARTESIAN_POINT('Ctrl Pts',(-0.506712869216879,-2.61627506823078,
8.85893592806396));
#403597=CARTESIAN_POINT('Ctrl Pts',(-0.506908237766522,-2.61615945434576,
8.85919241173848));
#403598=CARTESIAN_POINT('Ctrl Pts',(-0.507123281853322,-2.61604865749327,
8.85943017985534));
#403599=CARTESIAN_POINT('Ctrl Pts',(-0.507413655030366,-2.61589904894303,
8.8597512372));
#403600=CARTESIAN_POINT('Ctrl Pts',(-0.507747586735349,-2.61575498477418,
8.86004599534705));
#403601=CARTESIAN_POINT('Ctrl Pts',(-0.508125190597107,-2.61562775896039,
8.86026130871721));
#403602=CARTESIAN_POINT('Ctrl Pts',(-0.508263442016677,-2.61558117800309,
8.86034014101235));
#403603=CARTESIAN_POINT('Ctrl Pts',(-0.508409620434284,-2.61553614284821,
8.86040910639693));
#403604=CARTESIAN_POINT('Ctrl Pts',(-0.508559842340078,-2.6154942019216,
8.86046313645507));
#403605=CARTESIAN_POINT('Ctrl Pts',(-0.508794262365973,-2.61542875345688,
8.8605474499083));
#403606=CARTESIAN_POINT('Ctrl Pts',(-0.509044967329427,-2.61536919493121,
8.86059655985668));
#403607=CARTESIAN_POINT('Ctrl Pts',(-0.509295811046183,-2.6153190609893,
8.86059725258816));
#403608=CARTESIAN_POINT('Ctrl Pts',(-0.509547234312138,-2.61526881121795,
8.86059794692011));
#403609=CARTESIAN_POINT('Ctrl Pts',(-0.509802105972871,-2.61523007760143,
8.86056369958366));
#403610=CARTESIAN_POINT('Ctrl Pts',(-0.510045959806705,-2.61520125230872,
8.86048590497774));
#403611=CARTESIAN_POINT('Ctrl Pts',(-0.510109598396932,-2.61519372976556,
8.86046560290182));
#403612=CARTESIAN_POINT('Ctrl Pts',(-0.510173325147816,-2.61518687412201,
8.86044257503091));
#403613=CARTESIAN_POINT('Ctrl Pts',(-0.510235167338859,-2.61518086458527,
8.86041778462583));
#403614=CARTESIAN_POINT('Ctrl Pts',(-0.510651288544813,-2.61514042786026,
8.86025097596201));
#403615=CARTESIAN_POINT('Ctrl Pts',(-0.511037954093436,-2.61513320389167,
8.8599848982295));
#403616=CARTESIAN_POINT('Ctrl Pts',(-0.511383719971671,-2.61515093251763,
8.85968173251461));
#403617=CARTESIAN_POINT('Ctrl Pts',(-0.511566610311235,-2.61516030994504,
8.85952137522076));
#403618=CARTESIAN_POINT('Ctrl Pts',(-0.511741592847482,-2.61517665866632,
8.85934740853961));
#403619=CARTESIAN_POINT('Ctrl Pts',(-0.511906344552771,-2.61519820031704,
8.8591675900182));
#403620=CARTESIAN_POINT('Ctrl Pts',(-0.51256790828575,-2.61528470124179,
8.85844552518694));
#403621=CARTESIAN_POINT('Ctrl Pts',(-0.513102288376403,-2.61545682350229,
8.85759444184122));
#403622=CARTESIAN_POINT('Ctrl Pts',(-0.513525387806247,-2.61563629809097,
8.85683498915135));
#403623=CARTESIAN_POINT('Ctrl Pts',(-0.513569664034767,-2.61565507962869,
8.85675551444996));
#403624=CARTESIAN_POINT('Ctrl Pts',(-0.513612710375468,-2.61567395818293,
8.8566769979365));
#403625=CARTESIAN_POINT('Ctrl Pts',(-0.513654537106076,-2.6156928545144,
8.85659965593547));
#403626=CARTESIAN_POINT('Ctrl Pts',(-0.514219116450211,-2.61594791816087,
8.85555568965886));
#403627=CARTESIAN_POINT('Ctrl Pts',(-0.514724875940997,-2.61627458655635,
8.85434650606346));
#403628=CARTESIAN_POINT('Ctrl Pts',(-0.515177687654596,-2.61666925409151,
8.85297329937117));
#403629=CARTESIAN_POINT('Ctrl Pts',(-0.515432366653272,-2.61689123053259,
8.85220095427747));
#403630=CARTESIAN_POINT('Ctrl Pts',(-0.515670193285102,-2.61713504588954,
8.85137579139183));
#403631=CARTESIAN_POINT('Ctrl Pts',(-0.515891055659646,-2.61740223164621,
8.85049129520029));
#403632=CARTESIAN_POINT('Origin',(-0.510592093294233,-2.62178248538885,
7.59394543036555));
#403633=CARTESIAN_POINT('Ctrl Pts',(-0.504206055614823,-2.61917474895074,
7.59443877723642));
#403634=CARTESIAN_POINT('Ctrl Pts',(-0.505950960172775,-2.61365310954452,
7.58783886950016));
#403635=CARTESIAN_POINT('Ctrl Pts',(-0.514418553684599,-2.61426877313379,
7.58559994247159));
#403636=CARTESIAN_POINT('Ctrl Pts',(-0.494680672826292,-2.64931721647128,
7.56670252222134));
#403637=CARTESIAN_POINT('Ctrl Pts',(-0.496423055501789,-2.64380355740164,
7.56004874999026));
#403638=CARTESIAN_POINT('Ctrl Pts',(-0.504942371819622,-2.64440155968668,
7.55786368756704));
#403639=CARTESIAN_POINT('Ctrl Pts',(-0.485173077738411,-2.67940339594534,
7.53888913333558));
#403640=CARTESIAN_POINT('Ctrl Pts',(-0.486925815479463,-2.67385696892985,
7.53222002137275));
#403641=CARTESIAN_POINT('Ctrl Pts',(-0.495482437381228,-2.67447879394538,
7.53005029815327));
#403642=CARTESIAN_POINT('Ctrl Pts',(-0.475683700576297,-2.70943192595292,
7.51101258149734));
#403643=CARTESIAN_POINT('Ctrl Pts',(-0.47745768468355,-2.70381826616392,
7.5043616886572));
#403644=CARTESIAN_POINT('Ctrl Pts',(-0.486039296596616,-2.70449901466241,
7.50217374673251));
#403645=CARTESIAN_POINT('',(-0.486543193738921,-2.70289709681368,7.50366116523517));
#403646=CARTESIAN_POINT('Ctrl Pts',(-0.47826887016564,-2.70125132133977,
7.51860402984325));
#403647=CARTESIAN_POINT('Ctrl Pts',(-0.478135801956128,-2.70167240721866,
7.51734760759493));
#403648=CARTESIAN_POINT('Ctrl Pts',(-0.478072287298096,-2.70207084635854,
7.51608817408573));
#403649=CARTESIAN_POINT('Ctrl Pts',(-0.478091659423101,-2.70244782447943,
7.5148100591312));
#403650=CARTESIAN_POINT('Ctrl Pts',(-0.478109207156843,-2.70278930026951,
7.51365231206383));
#403651=CARTESIAN_POINT('Ctrl Pts',(-0.478194539795425,-2.70311366110739,
7.51247773061043));
#403652=CARTESIAN_POINT('Ctrl Pts',(-0.47838189073192,-2.70340589983577,
7.51129758471022));
#403653=CARTESIAN_POINT('Ctrl Pts',(-0.478614746549699,-2.70376911920023,
7.50983079813402));
#403654=CARTESIAN_POINT('Ctrl Pts',(-0.47900873000128,-2.70406409599668,
7.50839324291155));
#403655=CARTESIAN_POINT('Ctrl Pts',(-0.479616125507365,-2.70422699034869,
7.50715379678855));
#403656=CARTESIAN_POINT('Ctrl Pts',(-0.479896724729495,-2.70430224284564,
7.50658120839351));
#403657=CARTESIAN_POINT('Ctrl Pts',(-0.480265220758804,-2.70435082705869,
7.50598221009429));
#403658=CARTESIAN_POINT('Ctrl Pts',(-0.480715817181755,-2.7043490354212,
7.50545747549612));
#403659=CARTESIAN_POINT('Ctrl Pts',(-0.480956269380306,-2.70434807934797,
7.50517746087247));
#403660=CARTESIAN_POINT('Ctrl Pts',(-0.481222708816406,-2.70433297027813,
7.50491486231392));
#403661=CARTESIAN_POINT('Ctrl Pts',(-0.481507985287821,-2.7043024429845,
7.50468370960993));
#403662=CARTESIAN_POINT('Ctrl Pts',(-0.481934563597949,-2.70425679505124,
7.50433806340447));
#403663=CARTESIAN_POINT('Ctrl Pts',(-0.482415993154648,-2.70417475013281,
7.50405484070984));
#403664=CARTESIAN_POINT('Ctrl Pts',(-0.482919730220015,-2.70406112758864,
7.50385766036131));
#403665=CARTESIAN_POINT('Ctrl Pts',(-0.482973597069306,-2.70404897742364,
7.50383657498791));
#403666=CARTESIAN_POINT('Ctrl Pts',(-0.483027698355602,-2.70403648561238,
7.50381643264937));
#403667=CARTESIAN_POINT('Ctrl Pts',(-0.483081979503577,-2.70402367240709,
7.50379723213559));
#403668=CARTESIAN_POINT('Ctrl Pts',(-0.483444323922925,-2.70393814007029,
7.50366906242519));
#403669=CARTESIAN_POINT('Ctrl Pts',(-0.483822399615178,-2.70383572607388,
7.50358235568538));
#403670=CARTESIAN_POINT('Ctrl Pts',(-0.484184445158451,-2.70372825171679,
7.5035341175365));
#403671=CARTESIAN_POINT('Ctrl Pts',(-0.484727291474945,-2.70356710608208,
7.50346178989176));
#403672=CARTESIAN_POINT('Ctrl Pts',(-0.485304418855301,-2.70337066885157,
7.50346967198527));
#403673=CARTESIAN_POINT('Ctrl Pts',(-0.485865045427639,-2.70316039527586,
7.50354272648693));
#403674=CARTESIAN_POINT('Ctrl Pts',(-0.486095642741125,-2.70307390540177,
7.5035727753156));
#403675=CARTESIAN_POINT('Ctrl Pts',(-0.48632319177811,-2.70298532231186,
7.50361331098761));
#403676=CARTESIAN_POINT('Ctrl Pts',(-0.486543193739172,-2.70289709681507,
7.50366116523659));
#403677=CARTESIAN_POINT('',(-0.511151791457271,-2.62465641716278,7.57603338622103));
#403678=CARTESIAN_POINT('Origin',(-0.512843849057443,-2.63332984962537,
7.58486873427628));
#403679=CARTESIAN_POINT('Ctrl Pts',(-0.486543193716677,-2.70289709686653,
7.50366116529969));
#403680=CARTESIAN_POINT('Ctrl Pts',(-0.494733471570603,-2.6768596786482,
7.52783573079709));
#403681=CARTESIAN_POINT('Ctrl Pts',(-0.502935967272741,-2.65078068885653,
7.55196141284068));
#403682=CARTESIAN_POINT('Ctrl Pts',(-0.511151790759568,-2.62465641820242,
7.57603338728831));
#403683=CARTESIAN_POINT('Ctrl Pts',(-0.503894391761617,-2.62074446814268,
7.59639677331371));
#403684=CARTESIAN_POINT('Ctrl Pts',(-0.506703515972818,-2.60181546269509,
7.59974925422225));
#403685=CARTESIAN_POINT('Ctrl Pts',(-0.516410771457498,-2.61830690341518,
7.59639677331372));
#403686=CARTESIAN_POINT('Ctrl Pts',(-0.503839346059824,-2.61684420224733,
7.58707626057422));
#403687=CARTESIAN_POINT('Ctrl Pts',(-0.508673304164277,-2.61192990874306,
7.58811717123965));
#403688=CARTESIAN_POINT('Ctrl Pts',(-0.514998153140088,-2.61467102476307,
7.58707626057425));
#403689=CARTESIAN_POINT('Ctrl Pts',(-0.508250440815455,-2.62102366098244,
7.5801537675693));
#403690=CARTESIAN_POINT('Ctrl Pts',(-0.509994474415078,-2.61871383875086,
7.5820876076604));
#403691=CARTESIAN_POINT('Ctrl Pts',(-0.512477848454491,-2.62020037341847,
7.5801537675693));
#403692=CARTESIAN_POINT('Ctrl Pts',(-0.511151791298875,-2.62465641635051,
7.57603338509286));
#403693=CARTESIAN_POINT('Ctrl Pts',(-0.511151791298874,-2.62465641635051,
7.57603338509286));
#403694=CARTESIAN_POINT('Ctrl Pts',(-0.511151791298874,-2.62465641635051,
7.57603338509286));
#403695=CARTESIAN_POINT('Origin',(-0.512838247935145,-2.63333094044376,
7.58486873427623));
#403696=CARTESIAN_POINT('Ctrl Pts',(-0.575858486682835,-2.68994715228608,
7.51098857897448));
#403697=CARTESIAN_POINT('Ctrl Pts',(-0.572107512685101,-2.68540945396642,
7.50433767179956));
#403698=CARTESIAN_POINT('Ctrl Pts',(-0.564408512768212,-2.68926087595865,
7.50214974420965));
#403699=CARTESIAN_POINT('Ctrl Pts',(-0.55578813636867,-2.66566727325987,
7.53887321589168));
#403700=CARTESIAN_POINT('Ctrl Pts',(-0.552082105696198,-2.66118394461909,
7.53220407452066));
#403701=CARTESIAN_POINT('Ctrl Pts',(-0.544384150308563,-2.66497134514865,
7.53003438070912));
#403702=CARTESIAN_POINT('Ctrl Pts',(-0.535679243578268,-2.64134076790947,
7.56669465659234));
#403703=CARTESIAN_POINT('Ctrl Pts',(-0.531995114858089,-2.63688393490737,
7.56004085833301));
#403704=CARTESIAN_POINT('Ctrl Pts',(-0.524322805054464,-2.64063524299976,
7.55785582193788));
#403705=CARTESIAN_POINT('Ctrl Pts',(-0.515532717756325,-2.6169687364253,
7.59443891967696));
#403706=CARTESIAN_POINT('Ctrl Pts',(-0.511843247508166,-2.61250544157026,
7.58783901202978));
#403707=CARTESIAN_POINT('Ctrl Pts',(-0.504225531563111,-2.61625371874368,
7.58560008491213));
#403708=CARTESIAN_POINT('',(-0.563323058569129,-2.68794421947737,7.50366116523517));
#403709=CARTESIAN_POINT('Ctrl Pts',(-0.563323058569206,-2.68794421947773,
7.50366116523554));
#403710=CARTESIAN_POINT('Ctrl Pts',(-0.564080772490016,-2.68794154908911,
7.50350835821027));
#403711=CARTESIAN_POINT('Ctrl Pts',(-0.564777208608298,-2.687914442922,
7.50345484956));
#403712=CARTESIAN_POINT('Ctrl Pts',(-0.565433095890495,-2.68786269513525,
7.50349758195598));
#403713=CARTESIAN_POINT('Ctrl Pts',(-0.565769614708131,-2.68783614468294,
7.50351950684424));
#403714=CARTESIAN_POINT('Ctrl Pts',(-0.566128638073183,-2.68780061956941,
7.50357029184312));
#403715=CARTESIAN_POINT('Ctrl Pts',(-0.566473898535893,-2.68775684670366,
7.50365515313924));
#403716=CARTESIAN_POINT('Ctrl Pts',(-0.567005048937309,-2.68768950631076,
7.50378570417639));
#403717=CARTESIAN_POINT('Ctrl Pts',(-0.567519261867576,-2.6876010137059,
7.50400001621911));
#403718=CARTESIAN_POINT('Ctrl Pts',(-0.567977013192528,-2.68749586693788,
7.50428903009635));
#403719=CARTESIAN_POINT('Ctrl Pts',(-0.568027820067869,-2.68748419645558,
7.50432110841318));
#403720=CARTESIAN_POINT('Ctrl Pts',(-0.568077959553052,-2.68747233198995,
7.50435406373354));
#403721=CARTESIAN_POINT('Ctrl Pts',(-0.568127398514586,-2.68746028766373,
7.50438785222352));
#403722=CARTESIAN_POINT('Ctrl Pts',(-0.568429247138146,-2.68738675126291,
7.50459414719561));
#403723=CARTESIAN_POINT('Ctrl Pts',(-0.56870966607664,-2.68730483834955,
7.50483629897752));
#403724=CARTESIAN_POINT('Ctrl Pts',(-0.568958281566951,-2.68721895022315,
7.5050991045531));
#403725=CARTESIAN_POINT('Ctrl Pts',(-0.56950675230964,-2.68702947238968,
7.50567888004914));
#403726=CARTESIAN_POINT('Ctrl Pts',(-0.569922222282166,-2.68681367292768,
7.50637912803144));
#403727=CARTESIAN_POINT('Ctrl Pts',(-0.570225606143961,-2.68659431134895,
7.50710440483569));
#403728=CARTESIAN_POINT('Ctrl Pts',(-0.570300001889887,-2.68654051953491,
7.50728225710685));
#403729=CARTESIAN_POINT('Ctrl Pts',(-0.570369224095793,-2.68648556096084,
7.50746498566954));
#403730=CARTESIAN_POINT('Ctrl Pts',(-0.570431915928539,-2.68643104480392,
7.50764697238949));
#403731=CARTESIAN_POINT('Ctrl Pts',(-0.570768929968127,-2.68613798094756,
7.50862528291181));
#403732=CARTESIAN_POINT('Ctrl Pts',(-0.570950535870602,-2.68583422188777,
7.50965856837421));
#403733=CARTESIAN_POINT('Ctrl Pts',(-0.571040685959693,-2.68553724607221,
7.51067959873201));
#403734=CARTESIAN_POINT('Ctrl Pts',(-0.57109029566743,-2.68537381990632,
7.51124147302578));
#403735=CARTESIAN_POINT('Ctrl Pts',(-0.571111806105371,-2.6852122818537,
7.51180065547252));
#403736=CARTESIAN_POINT('Ctrl Pts',(-0.571113248871035,-2.6850548511387,
7.512351757165));
#403737=CARTESIAN_POINT('Ctrl Pts',(-0.571118234201136,-2.68451086530544,
7.51425603304536));
#403738=CARTESIAN_POINT('Ctrl Pts',(-0.570878146117201,-2.68395100448379,
7.51626900505181));
#403739=CARTESIAN_POINT('Ctrl Pts',(-0.570446802542556,-2.68340258713865,
7.51827788969244));
#403740=CARTESIAN_POINT('Ctrl Pts',(-0.57042345741317,-2.68337290575557,
7.51838661432546));
#403741=CARTESIAN_POINT('Ctrl Pts',(-0.570399542264663,-2.68334325609048,
7.51849533314857));
#403742=CARTESIAN_POINT('Ctrl Pts',(-0.570375062512112,-2.68331364198702,
7.51860402984325));
#403743=CARTESIAN_POINT('Ctrl Pts',(-0.511151792494592,-2.62465641786574,
7.57603338728984));
#403744=CARTESIAN_POINT('Ctrl Pts',(-0.528570753766828,-2.64578831464073,
7.55196141284922));
#403745=CARTESIAN_POINT('Ctrl Pts',(-0.545960368888816,-2.66688324131612,
7.52783573083105));
#403746=CARTESIAN_POINT('Ctrl Pts',(-0.56332305861081,-2.68794421951938,
7.50366116530176));
#403747=CARTESIAN_POINT('Origin',(-1.76626572250569E-16,-9.06940118467444E-16,
7.49482233047033));
#403748=CARTESIAN_POINT('Origin',(-0.484977299960275,-2.69419807522076,
7.49482233047033));
#403749=CARTESIAN_POINT('Origin',(0.,0.,7.50366116523517));
#403750=CARTESIAN_POINT('Origin',(-0.561510055974226,-2.67929332232211,
7.49482233047033));
#403751=CARTESIAN_POINT('Ctrl Pts',(-0.478269188839834,-2.70125031276705,
7.51860402984325));
#403752=CARTESIAN_POINT('Ctrl Pts',(-0.475977037628241,-2.70850581611646,
7.51860402984325));
#403753=CARTESIAN_POINT('Ctrl Pts',(-0.468479300229117,-2.70980204909083,
7.51860402984325));
#403754=CARTESIAN_POINT('Ctrl Pts',(-0.477418096240812,-2.70394433029203,
7.51041458714366));
#403755=CARTESIAN_POINT('Ctrl Pts',(-0.47420073607419,-2.70881289880017,
7.51004642900442));
#403756=CARTESIAN_POINT('Ctrl Pts',(-0.468477232442164,-2.70980240657649,
7.5072913648301));
#403757=CARTESIAN_POINT('Ctrl Pts',(-0.479644958150266,-2.70566619649922,
7.50215815450138));
#403758=CARTESIAN_POINT('Ctrl Pts',(-0.4778174872025,-2.70818778615984,
7.4987716367153));
#403759=CARTESIAN_POINT('Ctrl Pts',(-0.47442185931465,-2.70879904293209,
7.49481588533171));
#403760=CARTESIAN_POINT('Ctrl Pts',(-0.486543096209253,-2.7028965550037,
7.50366171572174));
#403761=CARTESIAN_POINT('Ctrl Pts',(-0.487191808179652,-2.70650034953677,
7.50000045605858));
#403762=CARTESIAN_POINT('Ctrl Pts',(-0.487191808179529,-2.70650034953679,
7.49482233047317));
#403763=CARTESIAN_POINT('Origin',(-0.466349848864439,-2.69748476704951,
7.51860402984325));
#403764=CARTESIAN_POINT('Origin',(-0.466349848864439,-2.69748476704951,
9.));
#403765=CARTESIAN_POINT('Origin',(-0.46634984886444,-2.69748476704951,8.75721825406948));
#403766=CARTESIAN_POINT('Ctrl Pts',(-0.483301006437013,-2.68532734615808,
8.78942910404913));
#403767=CARTESIAN_POINT('Ctrl Pts',(-0.481641165693878,-2.69064687220925,
8.7967269950169));
#403768=CARTESIAN_POINT('Ctrl Pts',(-0.472776992362339,-2.68959810286835,
8.79893251111267));
#403769=CARTESIAN_POINT('Ctrl Pts',(-0.479988149754494,-2.69581068528936,
8.78111911759583));
#403770=CARTESIAN_POINT('Ctrl Pts',(-0.478013283372321,-2.70211482780821,
8.78644465894815));
#403771=CARTESIAN_POINT('Ctrl Pts',(-0.469945969403999,-2.70291104204565,
8.78817647674132));
#403772=CARTESIAN_POINT('Ctrl Pts',(-0.477923498420511,-2.70234415227764,
8.7678092393203));
#403773=CARTESIAN_POINT('Ctrl Pts',(-0.47558738927346,-2.7097844030008,
8.76988516158372));
#403774=CARTESIAN_POINT('Ctrl Pts',(-0.468166832892793,-2.71122375125525,
8.77093053738833));
#403775=CARTESIAN_POINT('Ctrl Pts',(-0.478326077172247,-2.70107021563117,
8.75371302330492));
#403776=CARTESIAN_POINT('Ctrl Pts',(-0.476048030768691,-2.70832808762997,
8.75300828287559));
#403777=CARTESIAN_POINT('Ctrl Pts',(-0.468513389351372,-2.70960233958568,
8.75267964240738));
#403778=CARTESIAN_POINT('Origin',(-0.470575193914126,-2.68411393159326,
8.78727029226991));
#403779=CARTESIAN_POINT('Ctrl Pts',(-0.504036631578572,-2.61971088052921,
8.85049129520029));
#403780=CARTESIAN_POINT('Ctrl Pts',(-0.502277013195061,-2.62527908089984,
8.85711686593484));
#403781=CARTESIAN_POINT('Ctrl Pts',(-0.493751728365434,-2.62463079031095,
8.85933012996512));
#403782=CARTESIAN_POINT('Ctrl Pts',(-0.49684537847709,-2.6424671432281,
8.82945683644722));
#403783=CARTESIAN_POINT('Ctrl Pts',(-0.495071154197114,-2.64808156302841,
8.83607469902389));
#403784=CARTESIAN_POINT('Ctrl Pts',(-0.486523682952861,-2.64739397461503,
8.83829567148519));
#403785=CARTESIAN_POINT('Ctrl Pts',(-0.48966484451826,-2.66518948588238,
8.80838214965002));
#403786=CARTESIAN_POINT('Ctrl Pts',(-0.487883618320902,-2.67082606280457,
8.81501364461992));
#403787=CARTESIAN_POINT('Ctrl Pts',(-0.479307239296707,-2.67012283067464,
8.81722098428721));
#403788=CARTESIAN_POINT('Ctrl Pts',(-0.482494215215328,-2.68788048588352,
8.78727029226991));
#403789=CARTESIAN_POINT('Ctrl Pts',(-0.480712693150447,-2.69351799905962,
8.79393457792714));
#403790=CARTESIAN_POINT('Ctrl Pts',(-0.472101526741951,-2.69281998167918,
8.79610912703474));
#403791=CARTESIAN_POINT('Origin',(-0.49211761027737,-2.61594432623894,8.85049129520029));
#403792=CARTESIAN_POINT('Ctrl Pts',(-0.515891055659646,-2.61740223164621,
8.85049129520029));
#403793=CARTESIAN_POINT('Ctrl Pts',(-0.519611637301511,-2.6219031631575,
8.85711686593484));
#403794=CARTESIAN_POINT('Ctrl Pts',(-0.527270584603657,-2.61810299364327,
8.85933012996512));
#403795=CARTESIAN_POINT('Ctrl Pts',(-0.512599510788254,-2.61342032250981,
8.86332496987231));
#403796=CARTESIAN_POINT('Ctrl Pts',(-0.517180599096329,-2.61281573646103,
8.86648636486738));
#403797=CARTESIAN_POINT('Ctrl Pts',(-0.51804914848623,-2.60697435615754,
8.87206031107457));
#403798=CARTESIAN_POINT('Ctrl Pts',(-0.505603918890411,-2.61475129959254,
8.86341338519877));
#403799=CARTESIAN_POINT('Ctrl Pts',(-0.501110700619822,-2.61588463988002,
8.86654584966058));
#403800=CARTESIAN_POINT('Ctrl Pts',(-0.498154264204961,-2.61074813946514,
8.87215952290714));
#403801=CARTESIAN_POINT('Ctrl Pts',(-0.504036631578572,-2.61971088052921,
8.85049129520029));
#403802=CARTESIAN_POINT('Ctrl Pts',(-0.502277013195061,-2.62527908089984,
8.85711686593484));
#403803=CARTESIAN_POINT('Ctrl Pts',(-0.493751728365435,-2.62463079031095,
8.85933012996512));
#403804=CARTESIAN_POINT('Origin',(-0.525525532687672,-2.60943813393232,
8.85049129520029));
#403805=CARTESIAN_POINT('Ctrl Pts',(-0.561440886005583,-2.67250562312429,
8.78727029226991));
#403806=CARTESIAN_POINT('Ctrl Pts',(-0.565207781345668,-2.67706258210757,
8.79393457792714));
#403807=CARTESIAN_POINT('Ctrl Pts',(-0.572927672898287,-2.67318409147408,
8.79610912703474));
#403808=CARTESIAN_POINT('Ctrl Pts',(-0.546279125935841,-2.65416385556391,
8.80838214965003));
#403809=CARTESIAN_POINT('Ctrl Pts',(-0.550045395686168,-2.65872005774707,
8.81501364461994));
#403810=CARTESIAN_POINT('Ctrl Pts',(-0.557731085305896,-2.65484978803239,
8.81722098428722));
#403811=CARTESIAN_POINT('Ctrl Pts',(-0.531096423210991,-2.63579675286367,
8.82945683644724));
#403812=CARTESIAN_POINT('Ctrl Pts',(-0.534847887929972,-2.64033504482783,
8.8360746990239));
#403813=CARTESIAN_POINT('Ctrl Pts',(-0.542512653014741,-2.63649012367217,
8.83829567148519));
#403814=CARTESIAN_POINT('Ctrl Pts',(-0.515891055659647,-2.61740223164621,
8.85049129520029));
#403815=CARTESIAN_POINT('Ctrl Pts',(-0.519611637301512,-2.6219031631575,
8.85711686593484));
#403816=CARTESIAN_POINT('Ctrl Pts',(-0.527270584603657,-2.61810299364327,
8.85933012996512));
#403817=CARTESIAN_POINT('Origin',(-0.571075363033608,-2.6645415254104,8.78727029226991));
#403818=CARTESIAN_POINT('Ctrl Pts',(-0.570257105423824,-2.68317091578167,
8.75374538247847));
#403819=CARTESIAN_POINT('Ctrl Pts',(-0.57508850042324,-2.68903623766093,
8.75304829418601));
#403820=CARTESIAN_POINT('Ctrl Pts',(-0.582543965794282,-2.68739712835698,
8.75272238421917));
#403821=CARTESIAN_POINT('Ctrl Pts',(-0.571098103415368,-2.68418830424843,
8.76769408445022));
#403822=CARTESIAN_POINT('Ctrl Pts',(-0.576051610414045,-2.69020078488342,
8.76974318093972));
#403823=CARTESIAN_POINT('Ctrl Pts',(-0.583462952756313,-2.68875497647084,
8.7707786988043));
#403824=CARTESIAN_POINT('Ctrl Pts',(-0.566787626784249,-2.67897375054521,
8.78108014887986));
#403825=CARTESIAN_POINT('Ctrl Pts',(-0.5709826131446,-2.68407152719164,
8.78639403366322));
#403826=CARTESIAN_POINT('Ctrl Pts',(-0.578753247881951,-2.68180452222744,
8.78812224174741));
#403827=CARTESIAN_POINT('Ctrl Pts',(-0.559723707160403,-2.67042824812776,
8.78944554828686));
#403828=CARTESIAN_POINT('Ctrl Pts',(-0.5632547637516,-2.67472802218773,
8.79673892988686));
#403829=CARTESIAN_POINT('Ctrl Pts',(-0.571070449572005,-2.67043633144009,
8.79894799272499));
#403830=CARTESIAN_POINT('Origin',(-0.580009539540134,-2.67534954427313,
8.75721825406948));
#403831=CARTESIAN_POINT('Origin',(-0.580009539540134,-2.67534954427313,
9.));
#403832=CARTESIAN_POINT('Origin',(-0.580009539540134,-2.67534954427313,
7.51860402984325));
#403833=CARTESIAN_POINT('Ctrl Pts',(-0.563322897210423,-2.6879434495402,
7.50366195182966));
#403834=CARTESIAN_POINT('Ctrl Pts',(-0.564074028832693,-2.69152753840574,
7.50000065167735));
#403835=CARTESIAN_POINT('Ctrl Pts',(-0.564074028832807,-2.69152753840572,
7.49482233047108));
#403836=CARTESIAN_POINT('Ctrl Pts',(-0.57076287712312,-2.68792112230681,
7.50215800491337));
#403837=CARTESIAN_POINT('Ctrl Pts',(-0.573404680633563,-2.68957205276764,
7.49877273257264));
#403838=CARTESIAN_POINT('Ctrl Pts',(-0.576783407432534,-2.68886398386711,
7.49481816995649));
#403839=CARTESIAN_POINT('Ctrl Pts',(-0.572170600248251,-2.68548630569255,
7.51043025814043));
#403840=CARTESIAN_POINT('Ctrl Pts',(-0.576980440810586,-2.68879662150103,
7.51006209594516));
#403841=CARTESIAN_POINT('Ctrl Pts',(-0.582660459310099,-2.68756521579719,
7.50731281821699));
#403842=CARTESIAN_POINT('Ctrl Pts',(-0.570374099622813,-2.68331247699918,
7.51860402984326));
#403843=CARTESIAN_POINT('Ctrl Pts',(-0.57522146918052,-2.68917797150193,
7.51860402984326));
#403844=CARTESIAN_POINT('Ctrl Pts',(-0.582657984926167,-2.68756575223785,
7.51860402984327));
#403845=CARTESIAN_POINT('Origin',(0.,0.,7.5));
#403846=CARTESIAN_POINT('Origin',(-0.34713356539707,-2.64507775146798,7.5));
#403847=CARTESIAN_POINT('',(-0.34713356539707,-2.64507775146798,7.59394543036555));
#403848=CARTESIAN_POINT('',(-0.34713356539707,-2.64507775146798,8.85049129520029));
#403849=CARTESIAN_POINT('',(-0.34713356539707,-2.64507775146798,7.5));
#403850=CARTESIAN_POINT('',(-0.389059322317672,-2.7029863147688,8.78727029226991));
#403851=CARTESIAN_POINT('Ctrl Pts',(-0.34713356539707,-2.64507775146798,
8.85049129520029));
#403852=CARTESIAN_POINT('Ctrl Pts',(-0.361129132086595,-2.66440866446988,
8.82945686509571));
#403853=CARTESIAN_POINT('Ctrl Pts',(-0.37510389267392,-2.68371083973216,
8.80838212259896));
#403854=CARTESIAN_POINT('Ctrl Pts',(-0.389059322317672,-2.7029863147688,
8.78727029226991));
#403855=CARTESIAN_POINT('',(-0.397282670454287,-2.71434454205174,8.75721825406948));
#403856=CARTESIAN_POINT('Origin',(-0.372535599752971,-2.68016381430528,
8.75937679713133));
#403857=CARTESIAN_POINT('',(-0.397282670454287,-2.71434454205174,7.51860402984325));
#403858=CARTESIAN_POINT('',(-0.397282670454287,-2.71434454205174,7.5));
#403859=CARTESIAN_POINT('Ctrl Pts',(-0.397282670454287,-2.71434454205174,
7.51860402984325));
#403860=CARTESIAN_POINT('Ctrl Pts',(-0.39082450946553,-2.70542442105947,
7.52834476460825));
#403861=CARTESIAN_POINT('Ctrl Pts',(-0.384362155931846,-2.69649850925338,
7.53807742314407));
#403862=CARTESIAN_POINT('Ctrl Pts',(-0.377895469082967,-2.68756661219917,
7.54780169004674));
#403863=CARTESIAN_POINT('Ctrl Pts',(-0.367652586608945,-2.67341896999315,
7.5632044032688));
#403864=CARTESIAN_POINT('Ctrl Pts',(-0.357398819381816,-2.65925629358233,
7.57858609112103));
#403865=CARTESIAN_POINT('Ctrl Pts',(-0.34713356539707,-2.64507775146798,
7.59394543036555));
#403866=CARTESIAN_POINT('Origin',(-0.235661245880683,-2.9029927269226,7.5));
#403867=CARTESIAN_POINT('',(-0.304216449096279,-2.72634410251322,8.75721825406948));
#403868=CARTESIAN_POINT('',(-0.309289785090403,-2.71327145765926,8.78727029226991));
#403869=CARTESIAN_POINT('Origin',(-0.322167804103753,-2.68008820916575,
8.7565864062101));
#403870=CARTESIAN_POINT('',(-0.33515558185986,-2.64662214142563,8.85049129520029));
#403871=CARTESIAN_POINT('Ctrl Pts',(-0.309289785090403,-2.71327145765926,
8.78727029226991));
#403872=CARTESIAN_POINT('Ctrl Pts',(-0.317899487896232,-2.69108653097411,
8.80838212259896));
#403873=CARTESIAN_POINT('Ctrl Pts',(-0.326521116789851,-2.66887087391543,
8.82945686509571));
#403874=CARTESIAN_POINT('Ctrl Pts',(-0.33515558185986,-2.64662214142563,
8.85049129520029));
#403875=CARTESIAN_POINT('',(-0.33515558185986,-2.64662214142563,7.59394543036555));
#403876=CARTESIAN_POINT('',(-0.33515558185986,-2.64662214142563,7.5));
#403877=CARTESIAN_POINT('',(-0.304216449096279,-2.72634410251322,7.51860402984325));
#403878=CARTESIAN_POINT('Ctrl Pts',(-0.335155581859861,-2.64662214142562,
7.59394543036555));
#403879=CARTESIAN_POINT('Ctrl Pts',(-0.328822506613084,-2.66294080110644,
7.57858609112103));
#403880=CARTESIAN_POINT('Ctrl Pts',(-0.322496518039592,-2.67924120030481,
7.56320440326857));
#403881=CARTESIAN_POINT('Ctrl Pts',(-0.316177244736828,-2.69552429602679,
7.54780169004651));
#403882=CARTESIAN_POINT('Ctrl Pts',(-0.312187668397832,-2.70580437892645,
7.53807742314383));
#403883=CARTESIAN_POINT('Ctrl Pts',(-0.308200765466668,-2.71607757316128,
7.52834476460825));
#403884=CARTESIAN_POINT('Ctrl Pts',(-0.30421644909628,-2.72634410251322,
7.51860402984325));
#403885=CARTESIAN_POINT('',(-0.304216449096279,-2.72634410251322,7.5));
#403886=CARTESIAN_POINT('Origin',(-0.341564846497285,-2.64910949982511,
7.5));
#403887=CARTESIAN_POINT('Ctrl Pts',(-0.335155581859861,-2.64662214142563,
8.85049129520029));
#403888=CARTESIAN_POINT('Ctrl Pts',(-0.335225648125082,-2.64644159919414,
8.85097269580138));
#403889=CARTESIAN_POINT('Ctrl Pts',(-0.335302671970118,-2.64626637806575,
8.85143669361005));
#403890=CARTESIAN_POINT('Ctrl Pts',(-0.335391000464455,-2.64608876150126,
8.8519052845931));
#403891=CARTESIAN_POINT('Ctrl Pts',(-0.335563765397788,-2.64574135476517,
8.85282181883899));
#403892=CARTESIAN_POINT('Ctrl Pts',(-0.335775510349653,-2.64539380835665,
8.85372622499635));
#403893=CARTESIAN_POINT('Ctrl Pts',(-0.336042725344232,-2.64504869099114,
8.8546225773507));
#403894=CARTESIAN_POINT('Ctrl Pts',(-0.336264557742153,-2.64476218681169,
8.85536669723986));
#403895=CARTESIAN_POINT('Ctrl Pts',(-0.336524644191998,-2.64447727198575,
8.8561049844905));
#403896=CARTESIAN_POINT('Ctrl Pts',(-0.336838351599596,-2.64420078725064,
8.8568133821837));
#403897=CARTESIAN_POINT('Ctrl Pts',(-0.337123041564678,-2.64394987691929,
8.85745625420284));
#403898=CARTESIAN_POINT('Ctrl Pts',(-0.337455066979912,-2.64370231285873,
8.85808743050666));
#403899=CARTESIAN_POINT('Ctrl Pts',(-0.337859744633607,-2.64347139568469,
8.85866804508411));
#403900=CARTESIAN_POINT('Ctrl Pts',(-0.338046454130684,-2.64336485550626,
8.85893592806396));
#403901=CARTESIAN_POINT('Ctrl Pts',(-0.338248828681736,-2.64326199646832,
8.85919241173848));
#403902=CARTESIAN_POINT('Ctrl Pts',(-0.338470529716108,-2.64316520518179,
8.85943017985534));
#403903=CARTESIAN_POINT('Ctrl Pts',(-0.338769891743043,-2.6430345082917,
8.8597512372));
#403904=CARTESIAN_POINT('Ctrl Pts',(-0.339112367572514,-2.64291213519593,
8.86004599534706));
#403905=CARTESIAN_POINT('Ctrl Pts',(-0.339497346992517,-2.64280936394371,
8.86026130871721));
#403906=CARTESIAN_POINT('Ctrl Pts',(-0.339638298811899,-2.64277173649084,
8.86034014101236));
#403907=CARTESIAN_POINT('Ctrl Pts',(-0.339787062302549,-2.64273615954889,
8.86040910639693));
#403908=CARTESIAN_POINT('Ctrl Pts',(-0.339939662725721,-2.64270392954496,
8.86046313645507));
#403909=CARTESIAN_POINT('Ctrl Pts',(-0.340177794408063,-2.64265363489376,
8.8605474499083));
#403910=CARTESIAN_POINT('Ctrl Pts',(-0.340431800199123,-2.64261026145963,
8.86059655985668));
#403911=CARTESIAN_POINT('Ctrl Pts',(-0.340685340623247,-2.64257630213539,
8.86059725258816));
#403912=CARTESIAN_POINT('Ctrl Pts',(-0.340939466827042,-2.64254226435154,
8.86059794692011));
#403913=CARTESIAN_POINT('Ctrl Pts',(-0.341196296497944,-2.64251994000076,
8.86056369958366));
#403914=CARTESIAN_POINT('Ctrl Pts',(-0.341441496150768,-2.64250679770149,
8.86048590497774));
#403915=CARTESIAN_POINT('Ctrl Pts',(-0.341505485959682,-2.64250336795267,
8.86046560290182));
#403916=CARTESIAN_POINT('Ctrl Pts',(-0.341569521019712,-2.64250060938172,
8.86044257503091));
#403917=CARTESIAN_POINT('Ctrl Pts',(-0.341631621181681,-2.64249857443501,
8.86041778462583));
#403918=CARTESIAN_POINT('Ctrl Pts',(-0.342049478211856,-2.64248488176879,
8.86025097596201));
#403919=CARTESIAN_POINT('Ctrl Pts',(-0.342435812155897,-2.64250244638938,
8.8599848982295));
#403920=CARTESIAN_POINT('Ctrl Pts',(-0.342779731744087,-2.64254229188586,
8.85968173251461));
#403921=CARTESIAN_POINT('Ctrl Pts',(-0.342961645501996,-2.64256336787062,
8.85952137522076));
#403922=CARTESIAN_POINT('Ctrl Pts',(-0.343135221051685,-2.64259089417129,
8.85934740853961));
#403923=CARTESIAN_POINT('Ctrl Pts',(-0.343298254078627,-2.64262294724037,
8.8591675900182));
#403924=CARTESIAN_POINT('Ctrl Pts',(-0.343952916424673,-2.6427516569736,
8.85844552518696));
#403925=CARTESIAN_POINT('Ctrl Pts',(-0.344475170663018,-2.64295766344041,
8.85759444184125));
#403926=CARTESIAN_POINT('Ctrl Pts',(-0.344885901813324,-2.64316387735284,
8.8568349891514));
#403927=CARTESIAN_POINT('Ctrl Pts',(-0.34492888373434,-2.64318545708959,
8.85675551444999));
#403928=CARTESIAN_POINT('Ctrl Pts',(-0.344970632078601,-2.64320705484434,
8.85667699793652));
#403929=CARTESIAN_POINT('Ctrl Pts',(-0.345011162179599,-2.6432285921991,
8.85659965593547));
#403930=CARTESIAN_POINT('Ctrl Pts',(-0.345558239550983,-2.64351930451273,
8.85555568965886));
#403931=CARTESIAN_POINT('Ctrl Pts',(-0.346042030188692,-2.64387770585479,
8.85434650606346));
#403932=CARTESIAN_POINT('Ctrl Pts',(-0.346468625116265,-2.64430057424927,
8.85297329937117));
#403933=CARTESIAN_POINT('Ctrl Pts',(-0.346708558770214,-2.64453841195541,
8.85220095427747));
#403934=CARTESIAN_POINT('Ctrl Pts',(-0.346930275458167,-2.64479696397218,
8.85137579139183));
#403935=CARTESIAN_POINT('Ctrl Pts',(-0.347133565397069,-2.64507775146798,
8.85049129520029));
#403936=CARTESIAN_POINT('Origin',(-0.341564846497285,-2.64910949982511,
7.59394543036555));
#403937=CARTESIAN_POINT('Ctrl Pts',(-0.335359007864429,-2.64609796642226,
7.59443877723642));
#403938=CARTESIAN_POINT('Ctrl Pts',(-0.337454099980237,-2.64069946823527,
7.58783886950016));
#403939=CARTESIAN_POINT('Ctrl Pts',(-0.345864850211447,-2.64185638745667,
7.58559994247159));
#403940=CARTESIAN_POINT('Ctrl Pts',(-0.323921961471631,-2.67556820963984,
7.56670252222133));
#403941=CARTESIAN_POINT('Ctrl Pts',(-0.326014025584513,-2.67017751381542,
7.56004874999029));
#403942=CARTESIAN_POINT('Ctrl Pts',(-0.334477523915351,-2.6713201219112,
7.55786368756704));
#403943=CARTESIAN_POINT('Ctrl Pts',(-0.312506272620259,-2.70498342012268,
7.53888913333559));
#403944=CARTESIAN_POINT('Ctrl Pts',(-0.31461076997261,-2.699560687129,7.53222002137277));
#403945=CARTESIAN_POINT('Ctrl Pts',(-0.323109970911466,-2.70072945918586,
7.53005029815327));
#403946=CARTESIAN_POINT('Ctrl Pts',(-0.301112457877976,-2.73434226681255,
7.51101258149734));
#403947=CARTESIAN_POINT('Ctrl Pts',(-0.303242465562199,-2.72885380044164,
7.5043616886572));
#403948=CARTESIAN_POINT('Ctrl Pts',(-0.311762829927165,-2.73008297603239,
7.50217374673251));
#403949=CARTESIAN_POINT('',(-0.312368326987707,-2.72851663429644,7.50366116523517));
#403950=CARTESIAN_POINT('Ctrl Pts',(-0.304216449096279,-2.72634410251322,
7.51860402984325));
#403951=CARTESIAN_POINT('Ctrl Pts',(-0.304056675224784,-2.72675579751655,
7.51734760759494));
#403952=CARTESIAN_POINT('Ctrl Pts',(-0.303967762981087,-2.72714934862238,
7.51608817408573));
#403953=CARTESIAN_POINT('Ctrl Pts',(-0.30396294223285,-2.72752679337759,
7.5148100591312));
#403954=CARTESIAN_POINT('Ctrl Pts',(-0.303958575483901,-2.72786869185621,
7.51365231206384));
#403955=CARTESIAN_POINT('Ctrl Pts',(-0.304022950927189,-2.72819785354088,
7.51247773061043));
#403956=CARTESIAN_POINT('Ctrl Pts',(-0.304191193131477,-2.72850149544917,
7.51129758471022));
#403957=CARTESIAN_POINT('Ctrl Pts',(-0.304400298977422,-2.72887888766396,
7.50983079813402));
#403958=CARTESIAN_POINT('Ctrl Pts',(-0.30477457371951,-2.72919850100535,
7.50839324291155));
#403959=CARTESIAN_POINT('Ctrl Pts',(-0.305370284589417,-2.72939997663714,
7.50715379678855));
#403960=CARTESIAN_POINT('Ctrl Pts',(-0.305645485846318,-2.72949305257364,
7.50658120839351));
#403961=CARTESIAN_POINT('Ctrl Pts',(-0.306010111959797,-2.72956514658688,
7.50598221009429));
#403962=CARTESIAN_POINT('Ctrl Pts',(-0.306459897374679,-2.72959222844244,
7.50545747549611));
#403963=CARTESIAN_POINT('Ctrl Pts',(-0.306699916794221,-2.72960668015883,
7.50517746087247));
#403964=CARTESIAN_POINT('Ctrl Pts',(-0.306966776843353,-2.72960867296547,
7.50491486231392));
#403965=CARTESIAN_POINT('Ctrl Pts',(-0.307253423074079,-2.72959648611972,
7.50468370960992));
#403966=CARTESIAN_POINT('Ctrl Pts',(-0.30768204960644,-2.72957826294121,
7.50433806340447));
#403967=CARTESIAN_POINT('Ctrl Pts',(-0.30816774665045,-2.72952723189046,
7.50405484070984));
#403968=CARTESIAN_POINT('Ctrl Pts',(-0.308677728555385,-2.72944611734059,
7.50385766036131));
#403969=CARTESIAN_POINT('Ctrl Pts',(-0.308732263193207,-2.72943744340028,
7.50383657498791));
#403970=CARTESIAN_POINT('Ctrl Pts',(-0.308787053675708,-2.7294284435361,
7.50381643264937));
#403971=CARTESIAN_POINT('Ctrl Pts',(-0.308842044242128,-2.72941913446201,
7.50379723213559));
#403972=CARTESIAN_POINT('Ctrl Pts',(-0.30920912426164,-2.72935699334722,
7.50366906242519));
#403973=CARTESIAN_POINT('Ctrl Pts',(-0.309592984844114,-2.72927901316412,
7.50358235568538));
#403974=CARTESIAN_POINT('Ctrl Pts',(-0.30996117243169,-2.72919495596223,
7.5035341175365));
#403975=CARTESIAN_POINT('Ctrl Pts',(-0.310513228048472,-2.72906892170142,
7.50346178989176));
#403976=CARTESIAN_POINT('Ctrl Pts',(-0.311101755435299,-2.72890986475049,
7.50346967198527));
#403977=CARTESIAN_POINT('Ctrl Pts',(-0.31167470241447,-2.72873594267221,
7.50354272648692));
#403978=CARTESIAN_POINT('Ctrl Pts',(-0.311910367366302,-2.72866440492144,
7.50357277531559));
#403979=CARTESIAN_POINT('Ctrl Pts',(-0.312143124417443,-2.72859058295185,
7.50361331098761));
#403980=CARTESIAN_POINT('Ctrl Pts',(-0.312368326987868,-2.72851663429785,
7.50366116523658));
#403981=CARTESIAN_POINT('',(-0.341939261259455,-2.65201338678241,7.57603338622103));
#403982=CARTESIAN_POINT('Origin',(-0.343072133619649,-2.66077740924966,
7.58486873427626));
#403983=CARTESIAN_POINT('Ctrl Pts',(-0.312368326962123,-2.72851663434776,
7.50366116529969));
#403984=CARTESIAN_POINT('Ctrl Pts',(-0.322210000124767,-2.70305746570147,
7.52783573079709));
#403985=CARTESIAN_POINT('Ctrl Pts',(-0.3320665295326,-2.67755759369531,
7.55196141284068));
#403986=CARTESIAN_POINT('Ctrl Pts',(-0.341939260496575,-2.65201338777521,
7.57603338728831));
#403987=CARTESIAN_POINT('Ctrl Pts',(-0.334947412104101,-2.64764449208613,
7.59639677331371));
#403988=CARTESIAN_POINT('Ctrl Pts',(-0.338963550211403,-2.62893435951653,
7.59974925422225));
#403989=CARTESIAN_POINT('Ctrl Pts',(-0.347594250863831,-2.64601386279728,
7.59639677331372));
#403990=CARTESIAN_POINT('Ctrl Pts',(-0.335142370393516,-2.64374871291513,
7.58707626057422));
#403991=CARTESIAN_POINT('Ctrl Pts',(-0.34028125647849,-2.63915422911306,
7.58811717123965));
#403992=CARTESIAN_POINT('Ctrl Pts',(-0.346417486467326,-2.64229494768145,
7.58707626057424));
#403993=CARTESIAN_POINT('Ctrl Pts',(-0.339276623241309,-2.64820220431539,
7.58015376756929));
#403994=CARTESIAN_POINT('Ctrl Pts',(-0.341165064355278,-2.6460088684777,
7.5820876076604));
#403995=CARTESIAN_POINT('Ctrl Pts',(-0.343548093433292,-2.6476514592214,
7.5801537675693));
#403996=CARTESIAN_POINT('Ctrl Pts',(-0.341939261153426,-2.65201338596166,
7.57603338509286));
#403997=CARTESIAN_POINT('Ctrl Pts',(-0.341939261153426,-2.65201338596166,
7.57603338509286));
#403998=CARTESIAN_POINT('Ctrl Pts',(-0.341939261153426,-2.65201338596166,
7.57603338509286));
#403999=CARTESIAN_POINT('Origin',(-0.343066474116721,-2.66077813896297,
7.58486873427621));
#404000=CARTESIAN_POINT('Ctrl Pts',(-0.402329817877854,-2.72131574728531,
7.51098857897448));
#404001=CARTESIAN_POINT('Ctrl Pts',(-0.398877281988035,-2.71654704642434,
7.50433767179956));
#404002=CARTESIAN_POINT('Ctrl Pts',(-0.390947339037911,-2.71989727863872,
7.50214974420965));
#404003=CARTESIAN_POINT('Ctrl Pts',(-0.383856321441283,-2.69579984211488,
7.53887321589172));
#404004=CARTESIAN_POINT('Ctrl Pts',(-0.380445153058564,-2.69108827875315,
7.53220407452066));
#404005=CARTESIAN_POINT('Ctrl Pts',(-0.372520354360768,-2.69437468796705,
7.53003438070912));
#404006=CARTESIAN_POINT('Ctrl Pts',(-0.365347349076916,-2.67023493699403,
7.56669465659231));
#404007=CARTESIAN_POINT('Ctrl Pts',(-0.36195634006512,-2.66555121809578,
7.56004085833295));
#404008=CARTESIAN_POINT('Ctrl Pts',(-0.35405944671022,-2.66880325214652,
7.55785582193789));
#404009=CARTESIAN_POINT('Ctrl Pts',(-0.346803737871566,-2.6446221881212,
7.59443891967696));
#404010=CARTESIAN_POINT('Ctrl Pts',(-0.343407812318927,-2.63993167841372,
7.58783901202978));
#404011=CARTESIAN_POINT('Ctrl Pts',(-0.33556559484523,-2.64318418561333,
7.58560008491213));
#404012=CARTESIAN_POINT('',(-0.38994847349129,-2.71851378208007,7.50366116523517));
#404013=CARTESIAN_POINT('Ctrl Pts',(-0.389948473491343,-2.71851378208044,
7.50366116523554));
#404014=CARTESIAN_POINT('Ctrl Pts',(-0.390704801700024,-2.71855966407601,
7.50350835821027));
#404015=CARTESIAN_POINT('Ctrl Pts',(-0.391401543613698,-2.71857723441672,
7.50345484956));
#404016=CARTESIAN_POINT('Ctrl Pts',(-0.39205939879721,-2.71856761579381,
7.50349758195598));
#404017=CARTESIAN_POINT('Ctrl Pts',(-0.392396927294164,-2.71856268072692,
7.50351950684424));
#404018=CARTESIAN_POINT('Ctrl Pts',(-0.392757489109047,-2.71855023130952,
7.50357029184312));
#404019=CARTESIAN_POINT('Ctrl Pts',(-0.393104844734244,-2.71852866929362,
7.50365515313924));
#404020=CARTESIAN_POINT('Ctrl Pts',(-0.39363921834398,-2.71849549818184,
7.50378570417639));
#404021=CARTESIAN_POINT('Ctrl Pts',(-0.394158044509289,-2.71844013313008,
7.50400001621911));
#404022=CARTESIAN_POINT('Ctrl Pts',(-0.394621592111607,-2.71836453062546,
7.50428903009635));
#404023=CARTESIAN_POINT('Ctrl Pts',(-0.394673042329143,-2.7183561393291,
7.50432110841318));
#404024=CARTESIAN_POINT('Ctrl Pts',(-0.394723838956302,-2.71834751168813,
7.50435406373354));
#404025=CARTESIAN_POINT('Ctrl Pts',(-0.39477394802282,-2.71833865967341,
7.50438785222352));
#404026=CARTESIAN_POINT('Ctrl Pts',(-0.395079887959387,-2.71828461386872,
7.50459414719561));
#404027=CARTESIAN_POINT('Ctrl Pts',(-0.395364978925474,-2.71822083575731,
7.50483629897752));
#404028=CARTESIAN_POINT('Ctrl Pts',(-0.395618586479749,-2.71815105294643,
7.5050991045531));
#404029=CARTESIAN_POINT('Ctrl Pts',(-0.396178070216947,-2.71799710505662,
7.50567888004914));
#404030=CARTESIAN_POINT('Ctrl Pts',(-0.396606512880857,-2.7178083682303,
7.50637912803145));
#404031=CARTESIAN_POINT('Ctrl Pts',(-0.396923327952575,-2.71760889522423,
7.50710440483569));
#404032=CARTESIAN_POINT('Ctrl Pts',(-0.397001017297821,-2.71755998048304,
7.50728225710686));
#404033=CARTESIAN_POINT('Ctrl Pts',(-0.397073618487211,-2.71750956990922,
7.50746498566955));
#404034=CARTESIAN_POINT('Ctrl Pts',(-0.39713967437503,-2.7174591824411,
7.50764697238949));
#404035=CARTESIAN_POINT('Ctrl Pts',(-0.397494772648874,-2.71718831327952,
7.50862528291182));
#404036=CARTESIAN_POINT('Ctrl Pts',(-0.397695467332326,-2.71689681385543,
7.50965856837421));
#404037=CARTESIAN_POINT('Ctrl Pts',(-0.397804459504223,-2.71660622414456,
7.51067959873201));
#404038=CARTESIAN_POINT('Ctrl Pts',(-0.397864438033894,-2.71644631226014,
7.51124147302578));
#404039=CARTESIAN_POINT('Ctrl Pts',(-0.3978962540549,-2.71628648428327,
7.51180065547253));
#404040=CARTESIAN_POINT('Ctrl Pts',(-0.397907780476789,-2.71612946946487,
7.51235175716501));
#404041=CARTESIAN_POINT('Ctrl Pts',(-0.397947608855998,-2.71558692072005,
7.51425603304536));
#404042=CARTESIAN_POINT('Ctrl Pts',(-0.397743884464782,-2.71501282769615,
7.51626900505181));
#404043=CARTESIAN_POINT('Ctrl Pts',(-0.397348564351717,-2.71443790085555,
7.51827788969244));
#404044=CARTESIAN_POINT('Ctrl Pts',(-0.397327168880147,-2.71440678472847,
7.51838661432546));
#404045=CARTESIAN_POINT('Ctrl Pts',(-0.397305202528441,-2.71437566373297,
7.51849533314857));
#404046=CARTESIAN_POINT('Ctrl Pts',(-0.39728267045429,-2.71434454205174,
7.51860402984325));
#404047=CARTESIAN_POINT('Ctrl Pts',(-0.341939262249606,-2.65201338755038,
7.57603338728985));
#404048=CARTESIAN_POINT('Ctrl Pts',(-0.357968509122751,-2.67421790325761,
7.55196141284922));
#404049=CARTESIAN_POINT('Ctrl Pts',(-0.373970838822866,-2.69638364460996,
7.52783573083105));
#404050=CARTESIAN_POINT('Ctrl Pts',(-0.389948473530192,-2.71851378212467,
7.50366116530176));
#404051=CARTESIAN_POINT('Origin',(-1.18155821115197E-16,-9.16393216063564E-16,
7.49482233047033));
#404052=CARTESIAN_POINT('Origin',(-0.311362998732846,-2.71973515861749,
7.49482233047033));
#404053=CARTESIAN_POINT('Origin',(0.,0.,7.50366116523517));
#404054=CARTESIAN_POINT('Origin',(-0.388693460788429,-2.70976449964574,
7.49482233047033));
#404055=CARTESIAN_POINT('Ctrl Pts',(-0.304216831735198,-2.72634311643025,
7.51860402984325));
#404056=CARTESIAN_POINT('Ctrl Pts',(-0.301464528298434,-2.73343685393752,
7.51860402984325));
#404057=CARTESIAN_POINT('Ctrl Pts',(-0.293899145873112,-2.7342500419777,
7.51860402984325));
#404058=CARTESIAN_POINT('Ctrl Pts',(-0.303194881501745,-2.72897706911724,
7.51041458714365));
#404059=CARTESIAN_POINT('Ctrl Pts',(-0.299672201491327,-2.73362949765558,
7.51004642900442));
#404060=CARTESIAN_POINT('Ctrl Pts',(-0.293897059430465,-2.73425026624531,
7.50729136483009));
#404061=CARTESIAN_POINT('Ctrl Pts',(-0.305306847737899,-2.73083807309805,
7.50215815450138));
#404062=CARTESIAN_POINT('Ctrl Pts',(-0.303321572720941,-2.73323739541664,
7.4987716367153));
#404063=CARTESIAN_POINT('Ctrl Pts',(-0.299893758158899,-2.73362983767054,
7.49481588533172));
#404064=CARTESIAN_POINT('Ctrl Pts',(-0.312368264372309,-2.72851608735092,
7.50366171572174));
#404065=CARTESIAN_POINT('Ctrl Pts',(-0.312784747585891,-2.73215404062027,
7.50000045605858));
#404066=CARTESIAN_POINT('Ctrl Pts',(-0.312784747585768,-2.73215404062028,
7.49482233047317));
#404067=CARTESIAN_POINT('Origin',(-0.292563240664598,-2.72182163269599,
7.51860402984325));
#404068=CARTESIAN_POINT('Origin',(-0.292563240664598,-2.72182163269599,
9.));
#404069=CARTESIAN_POINT('Origin',(-0.292563240664598,-2.72182163269599,
8.75721825406948));
#404070=CARTESIAN_POINT('Ctrl Pts',(-0.310258498896846,-2.71077525492425,
8.78942910404912));
#404071=CARTESIAN_POINT('Ctrl Pts',(-0.308261245270244,-2.71597750507709,
8.7967269950169));
#404072=CARTESIAN_POINT('Ctrl Pts',(-0.299482479215875,-2.71436296100999,
8.79893251111267));
#404073=CARTESIAN_POINT('Ctrl Pts',(-0.306280778989409,-2.72102479945455,
8.78111911759584));
#404074=CARTESIAN_POINT('Ctrl Pts',(-0.303906062384054,-2.72718945931296,
8.78644465894814));
#404075=CARTESIAN_POINT('Ctrl Pts',(-0.295804309956148,-2.72746716306224,
8.78817647674132));
#404076=CARTESIAN_POINT('Ctrl Pts',(-0.303801769035854,-2.72741256006903,
8.76780923932029));
#404077=CARTESIAN_POINT('Ctrl Pts',(-0.300993761175047,-2.73468784897214,
8.76988516158373));
#404078=CARTESIAN_POINT('Ctrl Pts',(-0.293496231764021,-2.73564880325158,
8.77093053738833));
#404079=CARTESIAN_POINT('Ctrl Pts',(-0.304285142047544,-2.72616703417122,
8.75371302330492));
#404080=CARTESIAN_POINT('Ctrl Pts',(-0.30154676267909,-2.7332640391594,
8.75300828287559));
#404081=CARTESIAN_POINT('Ctrl Pts',(-0.293945960387538,-2.73405292689471,
8.75267964240738));
#404082=CARTESIAN_POINT('Origin',(-0.297636576658722,-2.70874898784203,
8.78727029226991));
#404083=CARTESIAN_POINT('Ctrl Pts',(-0.33515558185986,-2.64662214142563,
8.85049129520029));
#404084=CARTESIAN_POINT('Ctrl Pts',(-0.333042822978394,-2.6520661621945,
8.85711686593484));
#404085=CARTESIAN_POINT('Ctrl Pts',(-0.324576590381425,-2.65087298671372,
8.85933012996512));
#404086=CARTESIAN_POINT('Ctrl Pts',(-0.326521105202078,-2.66887090377406,
8.82945683644724));
#404087=CARTESIAN_POINT('Ctrl Pts',(-0.324390809144484,-2.67436011320682,
8.8360746990239));
#404088=CARTESIAN_POINT('Ctrl Pts',(-0.315904953537523,-2.67312629915468,
8.8382956714852));
#404089=CARTESIAN_POINT('Ctrl Pts',(-0.317899498928037,-2.69108650254807,
8.80838214965002));
#404090=CARTESIAN_POINT('Ctrl Pts',(-0.315760795727605,-2.69659737496413,
8.81501364461989));
#404091=CARTESIAN_POINT('Ctrl Pts',(-0.307247094031181,-2.69534609720933,
8.81722098428721));
#404092=CARTESIAN_POINT('Ctrl Pts',(-0.309289785090403,-2.71327145765926,
8.78727029226991));
#404093=CARTESIAN_POINT('Ctrl Pts',(-0.307150726644335,-2.71878324544933,
8.79393457792714));
#404094=CARTESIAN_POINT('Ctrl Pts',(-0.298601974927885,-2.71753494289437,
8.79610912703474));
#404095=CARTESIAN_POINT('Origin',(-0.32350237342818,-2.64209967160839,8.85049129520029));
#404096=CARTESIAN_POINT('Ctrl Pts',(-0.347133565397069,-2.64507775146798,
8.85049129520029));
#404097=CARTESIAN_POINT('Ctrl Pts',(-0.350558127032874,-2.64980781381701,
8.85711686593484));
#404098=CARTESIAN_POINT('Ctrl Pts',(-0.358444815903108,-2.64650616259708,
8.85933012996512));
#404099=CARTESIAN_POINT('Ctrl Pts',(-0.34410390515194,-2.64089313358697,
8.86332496987232));
#404100=CARTESIAN_POINT('Ctrl Pts',(-0.348714317083905,-2.64058330106072,
8.86648636486736));
#404101=CARTESIAN_POINT('Ctrl Pts',(-0.349955340466984,-2.63480957065002,
8.87206031107457));
#404102=CARTESIAN_POINT('Ctrl Pts',(-0.337037410453453,-2.64177316692274,
8.86341338519876));
#404103=CARTESIAN_POINT('Ctrl Pts',(-0.332480810620164,-2.64261629715804,
8.86654584966059));
#404104=CARTESIAN_POINT('Ctrl Pts',(-0.329859545232499,-2.63730093070269,
8.87215952290714));
#404105=CARTESIAN_POINT('Ctrl Pts',(-0.335155581859861,-2.64662214142563,
8.85049129520029));
#404106=CARTESIAN_POINT('Ctrl Pts',(-0.333042822978394,-2.65206616219449,
8.85711686593484));
#404107=CARTESIAN_POINT('Ctrl Pts',(-0.324576590381426,-2.65087298671372,
8.85933012996512));
#404108=CARTESIAN_POINT('Origin',(-0.357258508851223,-2.63774729990957,
8.85049129520029));
#404109=CARTESIAN_POINT('Ctrl Pts',(-0.389059322317672,-2.7029863147688,
8.78727029226991));
#404110=CARTESIAN_POINT('Ctrl Pts',(-0.392526512802782,-2.70777525680419,
8.79393457792714));
#404111=CARTESIAN_POINT('Ctrl Pts',(-0.40047903875833,-2.70439935009569,
8.79610912703474));
#404112=CARTESIAN_POINT('Ctrl Pts',(-0.375103874792512,-2.68371081503405,
8.80838214965003));
#404113=CARTESIAN_POINT('Ctrl Pts',(-0.378570489461523,-2.68849896174254,
8.81501364461988));
#404114=CARTESIAN_POINT('Ctrl Pts',(-0.386488357039691,-2.68512906773677,
8.81722098428721));
#404115=CARTESIAN_POINT('Ctrl Pts',(-0.361129150869165,-2.66440869041269,
8.82945683644722));
#404116=CARTESIAN_POINT('Ctrl Pts',(-0.364582138437075,-2.66917801513904,
8.83607469902387));
#404117=CARTESIAN_POINT('Ctrl Pts',(-0.372477500384171,-2.66583207697137,
8.8382956714852));
#404118=CARTESIAN_POINT('Ctrl Pts',(-0.34713356539707,-2.64507775146798,
8.85049129520029));
#404119=CARTESIAN_POINT('Ctrl Pts',(-0.350558127032874,-2.64980781381701,
8.85711686593484));
#404120=CARTESIAN_POINT('Ctrl Pts',(-0.358444815903108,-2.64650616259708,
8.85933012996512));
#404121=CARTESIAN_POINT('Origin',(-0.399184265771826,-2.69565586321039,
8.78727029226991));
#404122=CARTESIAN_POINT('Ctrl Pts',(-0.397174100220863,-2.71419455155609,
8.75374538247848));
#404123=CARTESIAN_POINT('Ctrl Pts',(-0.401619776138025,-2.72035737104291,
8.75304829418601));
#404124=CARTESIAN_POINT('Ctrl Pts',(-0.409164941549541,-2.71919930277121,
8.75272238421917));
#404125=CARTESIAN_POINT('Ctrl Pts',(-0.397948185988983,-2.71526373261547,
8.76769408445021));
#404126=CARTESIAN_POINT('Ctrl Pts',(-0.402506294519359,-2.72158123224724,
8.76974318093972));
#404127=CARTESIAN_POINT('Ctrl Pts',(-0.409995042726961,-2.7206132407373,
8.7707786988043));
#404128=CARTESIAN_POINT('Ctrl Pts',(-0.393980663297242,-2.70978371958609,
8.78108014887987));
#404129=CARTESIAN_POINT('Ctrl Pts',(-0.397840414937065,-2.71513979600257,
8.78639403366322));
#404130=CARTESIAN_POINT('Ctrl Pts',(-0.405740331578698,-2.71337531512024,
8.78812224174741));
#404131=CARTESIAN_POINT('Ctrl Pts',(-0.387478769473611,-2.70080318793564,
8.78944554828686));
#404132=CARTESIAN_POINT('Ctrl Pts',(-0.390727083660446,-2.70532036322122,
8.79673892988687));
#404133=CARTESIAN_POINT('Ctrl Pts',(-0.398801680886392,-2.70153824292231,
8.79894799272499));
#404134=CARTESIAN_POINT('Origin',(-0.407407613908441,-2.70701409049333,
8.75721825406948));
#404135=CARTESIAN_POINT('Origin',(-0.407407613908441,-2.70701409049333,
9.));
#404136=CARTESIAN_POINT('Origin',(-0.407407613908441,-2.70701409049333,
7.51860402984325));
#404137=CARTESIAN_POINT('Ctrl Pts',(-0.389948361794155,-2.71851300338654,
7.50366195182966));
#404138=CARTESIAN_POINT('Ctrl Pts',(-0.390468316773903,-2.72213785352538,
7.50000065167735));
#404139=CARTESIAN_POINT('Ctrl Pts',(-0.390468316774018,-2.72213785352537,
7.49482233047108));
#404140=CARTESIAN_POINT('Ctrl Pts',(-0.397374485980942,-2.7189674031765,
7.50215800491337));
#404141=CARTESIAN_POINT('Ctrl Pts',(-0.399905086144938,-2.72078420255571,
7.49877273257269));
#404142=CARTESIAN_POINT('Ctrl Pts',(-0.403322237117555,-2.72029406422792,
7.49481816995647));
#404143=CARTESIAN_POINT('Ctrl Pts',(-0.398935316024023,-2.7166277822844,
7.51043025814043));
#404144=CARTESIAN_POINT('Ctrl Pts',(-0.403523181591025,-2.72023946423692,
7.51006209594513));
#404145=CARTESIAN_POINT('Ctrl Pts',(-0.409270426317671,-2.71937450862293,
7.50731281821701));
#404146=CARTESIAN_POINT('Ctrl Pts',(-0.397281784184379,-2.71434331776496,
7.51860402984326));
#404147=CARTESIAN_POINT('Ctrl Pts',(-0.401743390778365,-2.72050733301407,
7.51860402984326));
#404148=CARTESIAN_POINT('Ctrl Pts',(-0.409267922647754,-2.71937488542709,
7.51860402984327));
#404149=CARTESIAN_POINT('Origin',(0.,0.,7.5));
#404150=CARTESIAN_POINT('Origin',(-0.17694962885436,-2.66188407944157,7.5));
#404151=CARTESIAN_POINT('',(-0.17694962885436,-2.66188407944157,7.59394543036555));
#404152=CARTESIAN_POINT('',(-0.17694962885436,-2.66188407944157,8.85049129520029));
#404153=CARTESIAN_POINT('',(-0.17694962885436,-2.66188407944157,7.5));
#404154=CARTESIAN_POINT('',(-0.215079030421395,-2.72235985585717,8.78727029226991));
#404155=CARTESIAN_POINT('Ctrl Pts',(-0.17694962885436,-2.66188407944157,
8.85049129520029));
#404156=CARTESIAN_POINT('Ctrl Pts',(-0.189677904302642,-2.68207197404603,
8.82945686509571));
#404157=CARTESIAN_POINT('Ctrl Pts',(-0.202387257630392,-2.70222985690408,
8.80838212259896));
#404158=CARTESIAN_POINT('Ctrl Pts',(-0.215079030421396,-2.72235985585717,
8.78727029226991));
#404159=CARTESIAN_POINT('',(-0.222557758686703,-2.73422161816809,8.75721825406948));
#404160=CARTESIAN_POINT('Origin',(-0.200051500241768,-2.69852556812846,
8.75937679713109));
#404161=CARTESIAN_POINT('',(-0.222557758686703,-2.73422161816809,7.51860402984325));
#404162=CARTESIAN_POINT('',(-0.222557758686703,-2.73422161816809,7.5));
#404163=CARTESIAN_POINT('Ctrl Pts',(-0.222557758686702,-2.73422161816809,
7.51860402984325));
#404164=CARTESIAN_POINT('Ctrl Pts',(-0.216684380796561,-2.72490604872586,
7.52834476460825));
#404165=CARTESIAN_POINT('Ctrl Pts',(-0.210807189994241,-2.71558443175037,
7.53807742314407));
#404166=CARTESIAN_POINT('Ctrl Pts',(-0.204926058256151,-2.70625656418765,
7.54780169004674));
#404167=CARTESIAN_POINT('Ctrl Pts',(-0.195610663431066,-2.69148172609652,
7.5632044032688));
#404168=CARTESIAN_POINT('Ctrl Pts',(-0.186285369461577,-2.67669118730146,
7.57858609112103));
#404169=CARTESIAN_POINT('Ctrl Pts',(-0.176949628854359,-2.66188407944157,
7.59394543036555));
#404170=CARTESIAN_POINT('Origin',(-0.0491816719600905,-2.91212708488465,
7.5));
#404171=CARTESIAN_POINT('',(-0.128913937383357,-2.74023375097047,8.75721825406948));
#404172=CARTESIAN_POINT('',(-0.13481441689609,-2.72751301502058,8.78727029226991));
#404173=CARTESIAN_POINT('Origin',(-0.149792034667995,-2.69522304258297,
8.7565864062109));
#404174=CARTESIAN_POINT('',(-0.16489730596464,-2.66265786424426,8.85049129520029));
#404175=CARTESIAN_POINT('Ctrl Pts',(-0.13481441689609,-2.72751301502058,
8.78727029226991));
#404176=CARTESIAN_POINT('Ctrl Pts',(-0.144827823277088,-2.70592529519938,
8.80838212259897));
#404177=CARTESIAN_POINT('Ctrl Pts',(-0.154855100144247,-2.68430767225054,
8.82945686509571));
#404178=CARTESIAN_POINT('Ctrl Pts',(-0.16489730596464,-2.66265786424426,
8.85049129520029));
#404179=CARTESIAN_POINT('',(-0.16489730596464,-2.66265786424426,7.59394543036555));
#404180=CARTESIAN_POINT('',(-0.16489730596464,-2.66265786424426,7.5));
#404181=CARTESIAN_POINT('',(-0.128913937383357,-2.74023375097047,7.51860402984325));
#404182=CARTESIAN_POINT('Ctrl Pts',(-0.16489730596464,-2.66265786424426,
7.59394543036555));
#404183=CARTESIAN_POINT('Ctrl Pts',(-0.157531702584637,-2.67853723396437,
7.57858609112103));
#404184=CARTESIAN_POINT('Ctrl Pts',(-0.150174341270717,-2.69439883476488,
7.56320440326857));
#404185=CARTESIAN_POINT('Ctrl Pts',(-0.142824790067819,-2.71024359788972,
7.54780169004651));
#404186=CARTESIAN_POINT('Ctrl Pts',(-0.138184763568491,-2.72024694622285,
7.53807742314383));
#404187=CARTESIAN_POINT('Ctrl Pts',(-0.133547846342464,-2.73024359133049,
7.52834476460825));
#404188=CARTESIAN_POINT('Ctrl Pts',(-0.128913937383358,-2.74023375097047,
7.51860402984324));
#404189=CARTESIAN_POINT('',(-0.128913937383357,-2.74023375097047,7.5));
#404190=CARTESIAN_POINT('Origin',(-0.17113403648065,-2.66555075509437,7.5));
#404191=CARTESIAN_POINT('Ctrl Pts',(-0.16489730596464,-2.66265786424426,
8.85049129520029));
#404192=CARTESIAN_POINT('Ctrl Pts',(-0.164978795651692,-2.66248218211717,
8.85097269580138));
#404193=CARTESIAN_POINT('Ctrl Pts',(-0.165066887699218,-2.66231225593408,
8.85143669361005));
#404194=CARTESIAN_POINT('Ctrl Pts',(-0.16516641464555,-2.66214066352794,
8.8519052845931));
#404195=CARTESIAN_POINT('Ctrl Pts',(-0.165361083040803,-2.66180503966352,
8.85282181883899));
#404196=CARTESIAN_POINT('Ctrl Pts',(-0.165594660314802,-2.66147177387202,
8.85372622499635));
#404197=CARTESIAN_POINT('Ctrl Pts',(-0.165883438033044,-2.66114448611064,
8.8546225773507));
#404198=CARTESIAN_POINT('Ctrl Pts',(-0.166123171038314,-2.66087278343529,
8.85536669723986));
#404199=CARTESIAN_POINT('Ctrl Pts',(-0.166400977668228,-2.66060511779347,
8.85610498449051));
#404200=CARTESIAN_POINT('Ctrl Pts',(-0.166731754968112,-2.66034930042851,
8.85681338218371));
#404201=CARTESIAN_POINT('Ctrl Pts',(-0.167031935887252,-2.66011714576804,
8.85745625420284));
#404202=CARTESIAN_POINT('Ctrl Pts',(-0.167379140604479,-2.65989136329579,
8.85808743050666));
#404203=CARTESIAN_POINT('Ctrl Pts',(-0.167797781718671,-2.65968684835214,
8.8586680450841));
#404204=CARTESIAN_POINT('Ctrl Pts',(-0.167990933653731,-2.65959248959048,
8.85893592806396));
#404205=CARTESIAN_POINT('Ctrl Pts',(-0.168199482605751,-2.65950280806947,
8.85919241173848));
#404206=CARTESIAN_POINT('Ctrl Pts',(-0.168426929570591,-2.65942042008507,
8.85943017985534));
#404207=CARTESIAN_POINT('Ctrl Pts',(-0.168734050304635,-2.65930917191667,
8.8597512372));
#404208=CARTESIAN_POINT('Ctrl Pts',(-0.16908366295195,-2.65920899275128,
8.86004599534705));
#404209=CARTESIAN_POINT('Ctrl Pts',(-0.169474435967183,-2.65913109836975,
8.86026130871721));
#404210=CARTESIAN_POINT('Ctrl Pts',(-0.169617508985118,-2.65910257904059,
8.86034014101235));
#404211=CARTESIAN_POINT('Ctrl Pts',(-0.169768246247719,-2.65907660650485,
8.86040910639692));
#404212=CARTESIAN_POINT('Ctrl Pts',(-0.169922598120396,-2.65905421986361,
8.86046313645506));
#404213=CARTESIAN_POINT('Ctrl Pts',(-0.170163462925023,-2.65901928569743,
8.86054744990829));
#404214=CARTESIAN_POINT('Ctrl Pts',(-0.17041972577941,-2.65899227558559,
8.86059655985669));
#404215=CARTESIAN_POINT('Ctrl Pts',(-0.170674921058915,-2.65897463042517,
8.86059725258816));
#404216=CARTESIAN_POINT('Ctrl Pts',(-0.170930705941467,-2.65895694449738,
8.86059794692011));
#404217=CARTESIAN_POINT('Ctrl Pts',(-0.171188438254332,-2.65895112114788,
8.86056369958366));
#404218=CARTESIAN_POINT('Ctrl Pts',(-0.171433976148177,-2.65895371584657,
8.86048590497774));
#404219=CARTESIAN_POINT('Ctrl Pts',(-0.171498054227927,-2.65895439298567,
8.86046560290182));
#404220=CARTESIAN_POINT('Ctrl Pts',(-0.171562134463306,-2.65895574282289,
8.86044257503091));
#404221=CARTESIAN_POINT('Ctrl Pts',(-0.171624237413315,-2.65895769082823,
8.86041778462584));
#404222=CARTESIAN_POINT('Ctrl Pts',(-0.172042113203544,-2.6589707984869,
8.86025097596201));
#404223=CARTESIAN_POINT('Ctrl Pts',(-0.172426528013957,-2.65901307951987,
8.8599848982295));
#404224=CARTESIAN_POINT('Ctrl Pts',(-0.172767188072743,-2.65907487815318,
8.85968173251462));
#404225=CARTESIAN_POINT('Ctrl Pts',(-0.172947377726346,-2.65910756608956,
8.85952137522077));
#404226=CARTESIAN_POINT('Ctrl Pts',(-0.173118833030314,-2.65914615685814,
8.85934740853961));
#404227=CARTESIAN_POINT('Ctrl Pts',(-0.173279477441229,-2.65918858963266,
8.8591675900182));
#404228=CARTESIAN_POINT('Ctrl Pts',(-0.17392454825235,-2.65935897927846,
8.85844552518696));
#404229=CARTESIAN_POINT('Ctrl Pts',(-0.174432530583701,-2.65959802342683,
8.85759444184126));
#404230=CARTESIAN_POINT('Ctrl Pts',(-0.174829205672076,-2.65983012928581,
8.85683498915141));
#404231=CARTESIAN_POINT('Ctrl Pts',(-0.174870716663646,-2.6598544185458,
8.85675551445));
#404232=CARTESIAN_POINT('Ctrl Pts',(-0.17491099545856,-2.65987864675125,
8.85667699793652));
#404233=CARTESIAN_POINT('Ctrl Pts',(-0.174950062383063,-2.6599027366277,
8.85659965593547));
#404234=CARTESIAN_POINT('Ctrl Pts',(-0.175477389723428,-2.66022790300923,
8.85555568965886));
#404235=CARTESIAN_POINT('Ctrl Pts',(-0.175937223508559,-2.66061656454988,
8.85434650606346));
#404236=CARTESIAN_POINT('Ctrl Pts',(-0.176335848680044,-2.66106589614674,
8.85297329937117));
#404237=CARTESIAN_POINT('Ctrl Pts',(-0.176560051050416,-2.6613186177918,
8.85220095427747));
#404238=CARTESIAN_POINT('Ctrl Pts',(-0.176764746713064,-2.66159084402269,
8.85137579139183));
#404239=CARTESIAN_POINT('Ctrl Pts',(-0.17694962885436,-2.66188407944157,
8.85049129520029));
#404240=CARTESIAN_POINT('Origin',(-0.17113403648065,-2.66555075509437,7.59394543036555));
#404241=CARTESIAN_POINT('Ctrl Pts',(-0.165133898016439,-2.66214779976352,
7.59443877723642));
#404242=CARTESIAN_POINT('Ctrl Pts',(-0.167570568507203,-2.65689462638278,
7.58783886950016));
#404243=CARTESIAN_POINT('Ctrl Pts',(-0.175889913880998,-2.65858804720708,
7.58559994247159));
#404244=CARTESIAN_POINT('Ctrl Pts',(-0.151832185296232,-2.69082471912743,
7.56670252222135));
#404245=CARTESIAN_POINT('Ctrl Pts',(-0.154265334106355,-2.68557913807363,
7.56004874999027));
#404246=CARTESIAN_POINT('Ctrl Pts',(-0.162638236120098,-2.6872616567584,
7.55786368756704));
#404247=CARTESIAN_POINT('Ctrl Pts',(-0.138555312195516,-2.71944808720963,
7.53888913333562));
#404248=CARTESIAN_POINT('Ctrl Pts',(-0.14100292132816,-2.71417133141079,
7.53222002137279));
#404249=CARTESIAN_POINT('Ctrl Pts',(-0.149409776264355,-2.7158822477739,
7.53005029815327));
#404250=CARTESIAN_POINT('Ctrl Pts',(-0.125303879501814,-2.74801660878327,
7.51101258149734));
#404251=CARTESIAN_POINT('Ctrl Pts',(-0.127781158104548,-2.74267588911605,
7.5043616886572));
#404252=CARTESIAN_POINT('Ctrl Pts',(-0.136205262916626,-2.74444844085289,
7.50217374673251));
#404253=CARTESIAN_POINT('',(-0.136909871778105,-2.7429241116639,7.50366116523517));
#404254=CARTESIAN_POINT('Ctrl Pts',(-0.128913937383357,-2.74023375097047,
7.51860402984325));
#404255=CARTESIAN_POINT('Ctrl Pts',(-0.128728114394988,-2.74063436335517,
7.51734760759494));
#404256=CARTESIAN_POINT('Ctrl Pts',(-0.128614169925107,-2.74102140924103,
7.51608817408573));
#404257=CARTESIAN_POINT('Ctrl Pts',(-0.128585176113117,-2.74139776962911,
7.5148100591312));
#404258=CARTESIAN_POINT('Ctrl Pts',(-0.128558912825387,-2.74173868586207,
7.51365231206384));
#404259=CARTESIAN_POINT('Ctrl Pts',(-0.128602066540877,-2.74207129579757,
7.51247773061043));
#404260=CARTESIAN_POINT('Ctrl Pts',(-0.128750508669652,-2.74238509315603,
7.51129758471022));
#404261=CARTESIAN_POINT('Ctrl Pts',(-0.128935005282989,-2.74277510743559,
7.50983079813402));
#404262=CARTESIAN_POINT('Ctrl Pts',(-0.129288033340387,-2.74311804396215,
7.50839324291155));
#404263=CARTESIAN_POINT('Ctrl Pts',(-0.129869611670373,-2.74335727296713,
7.50715379678855));
#404264=CARTESIAN_POINT('Ctrl Pts',(-0.130138284101049,-2.7434677898742,
7.50658120839351));
#404265=CARTESIAN_POINT('Ctrl Pts',(-0.130497541971785,-2.74356309743786,
7.50598221009429));
#404266=CARTESIAN_POINT('Ctrl Pts',(-0.13094466811385,-2.74361894150132,
7.50545747549611));
#404267=CARTESIAN_POINT('Ctrl Pts',(-0.131183268463104,-2.74364874162211,
7.50517746087247));
#404268=CARTESIAN_POINT('Ctrl Pts',(-0.131449452540084,-2.74366782811637,
7.50491486231392));
#404269=CARTESIAN_POINT('Ctrl Pts',(-0.131736290639274,-2.74367403179687,
7.50468370960992));
#404270=CARTESIAN_POINT('Ctrl Pts',(-0.132165204075514,-2.74368330825604,
7.50433806340446));
#404271=CARTESIAN_POINT('Ctrl Pts',(-0.132653172773507,-2.74366350077051,
7.50405484070983));
#404272=CARTESIAN_POINT('Ctrl Pts',(-0.133167303892982,-2.74361522753202,
7.50385766036131));
#404273=CARTESIAN_POINT('Ctrl Pts',(-0.133222282224801,-2.7436100654595,
7.50383657498791));
#404274=CARTESIAN_POINT('Ctrl Pts',(-0.133277536757653,-2.74360459452477,
7.50381643264937));
#404275=CARTESIAN_POINT('Ctrl Pts',(-0.133333010774479,-2.74359882783486,
7.50379723213559));
#404276=CARTESIAN_POINT('Ctrl Pts',(-0.133703317983615,-2.74356033329326,
7.50366906242519));
#404277=CARTESIAN_POINT('Ctrl Pts',(-0.134091386090839,-2.74350710736077,
7.50358235568538));
#404278=CARTESIAN_POINT('Ctrl Pts',(-0.134464202760945,-2.74344681272314,
7.5035341175365));
#404279=CARTESIAN_POINT('Ctrl Pts',(-0.13502319916307,-2.74335640773805,
7.50346178989176));
#404280=CARTESIAN_POINT('Ctrl Pts',(-0.135620708171097,-2.74323538466582,
7.50346967198527));
#404281=CARTESIAN_POINT('Ctrl Pts',(-0.136203621195066,-2.74309852876809,
7.50354272648692));
#404282=CARTESIAN_POINT('Ctrl Pts',(-0.136443385387408,-2.74304223710461,
7.50357277531559));
#404283=CARTESIAN_POINT('Ctrl Pts',(-0.136680394004056,-2.74298347960564,
7.50361331098761));
#404284=CARTESIAN_POINT('Ctrl Pts',(-0.136909871778176,-2.74292411166531,
7.50366116523658));
#404285=CARTESIAN_POINT('',(-0.171321629291381,-2.66847266454066,7.57603338622103));
#404286=CARTESIAN_POINT('Origin',(-0.171890661196624,-2.67729126376579,
7.58486873427628));
#404287=CARTESIAN_POINT('Ctrl Pts',(-0.136909871749285,-2.74292411171347,
7.50366116529968));
#404288=CARTESIAN_POINT('Ctrl Pts',(-0.148362498674589,-2.71814780982416,
7.52783573079709));
#404289=CARTESIAN_POINT('Ctrl Pts',(-0.159832559194555,-2.6933318400473,
7.55196141284068));
#404290=CARTESIAN_POINT('Ctrl Pts',(-0.171321628466457,-2.66847266548254,
7.57603338728831));
#404291=CARTESIAN_POINT('Ctrl Pts',(-0.164624061684239,-2.6636647768937,
7.5963967733137));
#404292=CARTESIAN_POINT('Ctrl Pts',(-0.169830710514483,-2.64525040115009,
7.59974925422226));
#404293=CARTESIAN_POINT('Ctrl Pts',(-0.177349390934601,-2.66284778364888,
7.59639677331373));
#404294=CARTESIAN_POINT('Ctrl Pts',(-0.165068222839374,-2.6597894930393,
7.5870762605742));
#404295=CARTESIAN_POINT('Ctrl Pts',(-0.170490920119603,-2.65553369865884,
7.58811717123965));
#404296=CARTESIAN_POINT('Ctrl Pts',(-0.176413316036275,-2.65906111388928,
7.58707626057426));
#404297=CARTESIAN_POINT('Ctrl Pts',(-0.168908645247684,-2.66449871675321,
7.58015376756929));
#404298=CARTESIAN_POINT('Ctrl Pts',(-0.170933733866522,-2.66243088019682,
7.58208760766041));
#404299=CARTESIAN_POINT('Ctrl Pts',(-0.173206625605373,-2.66422277725892,
7.5801537675693));
#404300=CARTESIAN_POINT('Ctrl Pts',(-0.171321629238156,-2.6684726637148,
7.57603338509286));
#404301=CARTESIAN_POINT('Ctrl Pts',(-0.171321629238156,-2.6684726637148,
7.57603338509286));
#404302=CARTESIAN_POINT('Ctrl Pts',(-0.171321629238156,-2.6684726637148,
7.57603338509286));
#404303=CARTESIAN_POINT('Origin',(-0.171884966568706,-2.6772916293733,7.58486873427622));
#404304=CARTESIAN_POINT('Ctrl Pts',(-0.227147889551738,-2.74150187215855,
7.51098857897448));
#404305=CARTESIAN_POINT('Ctrl Pts',(-0.224007978980372,-2.73652176437099,
7.50433767179956));
#404306=CARTESIAN_POINT('Ctrl Pts',(-0.215879678833561,-2.73935703998472,
7.50214974420965));
#404307=CARTESIAN_POINT('Ctrl Pts',(-0.210347158552128,-2.71485479117133,
7.53887321589167));
#404308=CARTESIAN_POINT('Ctrl Pts',(-0.207244869681734,-2.70993435391318,
7.53220407452062));
#404309=CARTESIAN_POINT('Ctrl Pts',(-0.199125792371522,-2.71270626725104,
7.53003438070911));
#404310=CARTESIAN_POINT('Ctrl Pts',(-0.193514163951469,-2.68815653795892,
7.56669465659233));
#404311=CARTESIAN_POINT('Ctrl Pts',(-0.190430209031565,-2.68326517957015,
7.56004085833302));
#404312=CARTESIAN_POINT('Ctrl Pts',(-0.182341182153933,-2.6860045762737,
7.55785582193789));
#404313=CARTESIAN_POINT('Ctrl Pts',(-0.176649667038724,-2.66140831997643,
7.59443891967696));
#404314=CARTESIAN_POINT('Ctrl Pts',(-0.173561240768126,-2.656509869727,
7.58783901202978));
#404315=CARTESIAN_POINT('Ctrl Pts',(-0.165526747119535,-2.65925324170307,
7.58560008491213));
#404316=CARTESIAN_POINT('',(-0.214971506492189,-2.73791238843283,7.50366116523517));
#404317=CARTESIAN_POINT('Ctrl Pts',(-0.214971506492218,-2.7379123884332,
7.50366116523554));
#404318=CARTESIAN_POINT('Ctrl Pts',(-0.21572334107393,-2.73800663427399,
7.50350835821027));
#404319=CARTESIAN_POINT('Ctrl Pts',(-0.216417525721022,-2.73806880892224,
7.50345484955999));
#404320=CARTESIAN_POINT('Ctrl Pts',(-0.217074645537791,-2.73810135898814,
7.50349758195598));
#404321=CARTESIAN_POINT('Ctrl Pts',(-0.217411796737069,-2.73811805958593,
7.50351950684424));
#404322=CARTESIAN_POINT('Ctrl Pts',(-0.217772415375944,-2.73812873702199,
7.50357029184312));
#404323=CARTESIAN_POINT('Ctrl Pts',(-0.218120438804858,-2.73812947445888,
7.50365515313923));
#404324=CARTESIAN_POINT('Ctrl Pts',(-0.218655839767129,-2.73813060893543,
7.50378570417639));
#404325=CARTESIAN_POINT('Ctrl Pts',(-0.219177147199483,-2.73810859894365,
7.50400001621911));
#404326=CARTESIAN_POINT('Ctrl Pts',(-0.219644586262637,-2.73806285136934,
7.50428903009634));
#404327=CARTESIAN_POINT('Ctrl Pts',(-0.219696468402389,-2.73805777374055,
7.50432110841318));
#404328=CARTESIAN_POINT('Ctrl Pts',(-0.219747713437285,-2.73805241837707,
7.50435406373354));
#404329=CARTESIAN_POINT('Ctrl Pts',(-0.219798286699883,-2.73804679504868,
7.50438785222352));
#404330=CARTESIAN_POINT('Ctrl Pts',(-0.220107060776633,-2.73801246192593,
7.50459414719561));
#404331=CARTESIAN_POINT('Ctrl Pts',(-0.220395652270383,-2.7379670806944,
7.50483629897752));
#404332=CARTESIAN_POINT('Ctrl Pts',(-0.220653209760782,-2.73791368995159,
7.50509910455309));
#404333=CARTESIAN_POINT('Ctrl Pts',(-0.221221407453803,-2.73779590461034,
7.50567888004914));
#404334=CARTESIAN_POINT('Ctrl Pts',(-0.221661062246291,-2.73763500597979,
7.50637912803144));
#404335=CARTESIAN_POINT('Ctrl Pts',(-0.221990006666845,-2.73745624122375,
7.50710440483569));
#404336=CARTESIAN_POINT('Ctrl Pts',(-0.222070670369226,-2.73741240455658,
7.50728225710685));
#404337=CARTESIAN_POINT('Ctrl Pts',(-0.22214635220824,-2.73736674913086,
7.50746498566954));
#404338=CARTESIAN_POINT('Ctrl Pts',(-0.22221550071332,-2.73732069740447,
7.50764697238949));
#404339=CARTESIAN_POINT('Ctrl Pts',(-0.222587224046446,-2.73707313599715,
7.50862528291181));
#404340=CARTESIAN_POINT('Ctrl Pts',(-0.222806182813372,-2.7367950940424,
7.50965856837421));
#404341=CARTESIAN_POINT('Ctrl Pts',(-0.222933569195861,-2.7365120845317,
7.51067959873201));
#404342=CARTESIAN_POINT('Ctrl Pts',(-0.223003670082823,-2.73635634404098,
7.51124147302578));
#404343=CARTESIAN_POINT('Ctrl Pts',(-0.223045660948038,-2.73619888290729,
7.51180065547252));
#404344=CARTESIAN_POINT('Ctrl Pts',(-0.223067223661612,-2.73604292919307,
7.512351757165));
#404345=CARTESIAN_POINT('Ctrl Pts',(-0.223141731426575,-2.73550404698584,
7.51425603304536));
#404346=CARTESIAN_POINT('Ctrl Pts',(-0.2229752078753,-2.73491808083107,
7.51626900505181));
#404347=CARTESIAN_POINT('Ctrl Pts',(-0.222617535678955,-2.73431900699272,
7.51827788969245));
#404348=CARTESIAN_POINT('Ctrl Pts',(-0.222598177783783,-2.7342865839845,
7.51838661432546));
#404349=CARTESIAN_POINT('Ctrl Pts',(-0.222578250493331,-2.73425411954143,
7.51849533314857));
#404350=CARTESIAN_POINT('Ctrl Pts',(-0.222557758686706,-2.73422161816809,
7.51860402984325));
#404351=CARTESIAN_POINT('Ctrl Pts',(-0.171321630230296,-2.66847266537049,
7.57603338728985));
#404352=CARTESIAN_POINT('Ctrl Pts',(-0.185895295090683,-2.69165855689206,
7.55196141284922));
#404353=CARTESIAN_POINT('Ctrl Pts',(-0.200444582363687,-2.71480402913563,
7.52783573083105));
#404354=CARTESIAN_POINT('Ctrl Pts',(-0.214971506528153,-2.73791238847983,
7.50366116530176));
#404355=CARTESIAN_POINT('Origin',(-5.91995423665181E-17,-9.22080657369149E-16,
7.49482233047033));
#404356=CARTESIAN_POINT('Origin',(-0.13646924015647,-2.7340962668661,7.49482233047033));
#404357=CARTESIAN_POINT('Origin',(0.,0.,7.50366116523517));
#404358=CARTESIAN_POINT('Origin',(-0.214279640797767,-2.72910067339767,
7.49482233047033));
#404359=CARTESIAN_POINT('Ctrl Pts',(-0.128914382414656,-2.74023279142927,
7.51860402984325));
#404360=CARTESIAN_POINT('Ctrl Pts',(-0.12571323655791,-2.74713561340538,
7.51860402984325));
#404361=CARTESIAN_POINT('Ctrl Pts',(-0.118111296885546,-2.7474624149473,
7.51860402984325));
#404362=CARTESIAN_POINT('Ctrl Pts',(-0.12772577395949,-2.7427958558017,
7.51041458714365));
#404363=CARTESIAN_POINT('Ctrl Pts',(-0.123912249553073,-2.74721302654344,
7.51004642900443));
#404364=CARTESIAN_POINT('Ctrl Pts',(-0.11810920036085,-2.74746250507528,
7.50729136483009));
#404365=CARTESIAN_POINT('Ctrl Pts',(-0.129714166000064,-2.74478835029159,
7.50215815450138));
#404366=CARTESIAN_POINT('Ctrl Pts',(-0.127579244834786,-2.74705554593811,
7.49877163671529));
#404367=CARTESIAN_POINT('Ctrl Pts',(-0.12413332922386,-2.74722756104425,
7.49481588533172));
#404368=CARTESIAN_POINT('Ctrl Pts',(-0.136909844334277,-2.74292356183035,
7.50366171572174));
#404369=CARTESIAN_POINT('Ctrl Pts',(-0.137092387372183,-2.74658072470565,
7.50000045605858));
#404370=CARTESIAN_POINT('Ctrl Pts',(-0.137092387372058,-2.74658072470566,
7.49482233047317));
#404371=CARTESIAN_POINT('Origin',(-0.117574427354248,-2.73497394942481,
7.51860402984325));
#404372=CARTESIAN_POINT('Origin',(-0.117574427354248,-2.73497394942481,
9.));
#404373=CARTESIAN_POINT('Origin',(-0.117574427354248,-2.73497394942481,
8.75721825406948));
#404374=CARTESIAN_POINT('Ctrl Pts',(-0.135941072634473,-2.72508400670848,
8.78942910404912));
#404375=CARTESIAN_POINT('Ctrl Pts',(-0.133614613267969,-2.73014760380123,
8.79672699501691));
#404376=CARTESIAN_POINT('Ctrl Pts',(-0.124957328323518,-2.72797391951581,
8.79893251111267));
#404377=CARTESIAN_POINT('Ctrl Pts',(-0.131314834806437,-2.73505763906079,
8.78111911759582));
#404378=CARTESIAN_POINT('Ctrl Pts',(-0.128550026197797,-2.74105748434906,
8.78644465894813));
#404379=CARTESIAN_POINT('Ctrl Pts',(-0.120447127148859,-2.74081553646593,
8.78817647674131));
#404380=CARTESIAN_POINT('Ctrl Pts',(-0.128431653016956,-2.74127344462293,
8.76780923932029));
#404381=CARTESIAN_POINT('Ctrl Pts',(-0.125163285149012,-2.74835387598339,
8.76988516158374));
#404382=CARTESIAN_POINT('Ctrl Pts',(-0.117619591664189,-2.74883248752051,
8.77093053738833));
#404383=CARTESIAN_POINT('Ctrl Pts',(-0.12899383400521,-2.74006144760687,
8.75371302330492));
#404384=CARTESIAN_POINT('Ctrl Pts',(-0.125806374260063,-2.74696842246862,
8.75300828287559));
#404385=CARTESIAN_POINT('Ctrl Pts',(-0.118170644421256,-2.74726870427462,
8.75267964240738));
#404386=CARTESIAN_POINT('Origin',(-0.123474906866981,-2.72225321347492,
8.78727029226991));
#404387=CARTESIAN_POINT('Ctrl Pts',(-0.16489730596464,-2.66265786424426,
8.85049129520029));
#404388=CARTESIAN_POINT('Ctrl Pts',(-0.162440088364647,-2.66795533476229,
8.85711686593484));
#404389=CARTESIAN_POINT('Ctrl Pts',(-0.154067697566079,-2.66622217740361,
8.85933012996512));
#404390=CARTESIAN_POINT('Ctrl Pts',(-0.154855086667233,-2.68430770130539,
8.82945683644723));
#404391=CARTESIAN_POINT('Ctrl Pts',(-0.152377472675502,-2.68964914403162,
8.83607469902388));
#404392=CARTESIAN_POINT('Ctrl Pts',(-0.14398810290671,-2.68787417434732,
8.8382956714852));
#404393=CARTESIAN_POINT('Ctrl Pts',(-0.14482783610749,-2.70592526753855,
8.80838214965003));
#404394=CARTESIAN_POINT('Ctrl Pts',(-0.142340444294174,-2.71128779009164,
8.81501364461989));
#404395=CARTESIAN_POINT('Ctrl Pts',(-0.133924404551986,-2.70949360848066,
8.81722098428721));
#404396=CARTESIAN_POINT('Ctrl Pts',(-0.13481441689609,-2.72751301502058,
8.78727029226991));
#404397=CARTESIAN_POINT('Ctrl Pts',(-0.132326611918816,-2.7328764283063,
8.79393457792714));
#404398=CARTESIAN_POINT('Ctrl Pts',(-0.123875403548917,-2.73108297011979,
8.79610912703474));
#404399=CARTESIAN_POINT('Origin',(-0.153557795935531,-2.6573980626986,8.85049129520029));
#404400=CARTESIAN_POINT('Ctrl Pts',(-0.17694962885436,-2.66188407944157,
8.85049129520029));
#404401=CARTESIAN_POINT('Ctrl Pts',(-0.180064098225775,-2.66682383578755,
8.85711686593484));
#404402=CARTESIAN_POINT('Ctrl Pts',(-0.188146120567841,-2.66403427005499,
8.85933012996512));
#404403=CARTESIAN_POINT('Ctrl Pts',(-0.174194302759305,-2.65751394830842,
8.8633249698723));
#404404=CARTESIAN_POINT('Ctrl Pts',(-0.178815093143622,-2.657500142473,
8.86648636486737));
#404405=CARTESIAN_POINT('Ctrl Pts',(-0.180423490888559,-2.65181778745183,
8.87206031107456));
#404406=CARTESIAN_POINT('Ctrl Pts',(-0.167085943002642,-2.6579394216515,
8.86341338519877));
#404407=CARTESIAN_POINT('Ctrl Pts',(-0.162484685652769,-2.65848887723162,
8.86654584966057));
#404408=CARTESIAN_POINT('Ctrl Pts',(-0.160209362634038,-2.65301648671671,
8.87215952290715));
#404409=CARTESIAN_POINT('Ctrl Pts',(-0.16489730596464,-2.66265786424426,
8.85049129520029));
#404410=CARTESIAN_POINT('Ctrl Pts',(-0.162440088364647,-2.66795533476229,
8.85711686593484));
#404411=CARTESIAN_POINT('Ctrl Pts',(-0.154067697566079,-2.66622217740361,
8.85933012996512));
#404412=CARTESIAN_POINT('Origin',(-0.187523433170195,-2.65521739643648,
8.85049129520029));
#404413=CARTESIAN_POINT('Ctrl Pts',(-0.215079030421396,-2.72235985585717,
8.78727029226991));
#404414=CARTESIAN_POINT('Ctrl Pts',(-0.218232268622115,-2.72736110215464,
8.79393457792714));
#404415=CARTESIAN_POINT('Ctrl Pts',(-0.22638475034563,-2.72450165169591,
8.79610912703474));
#404416=CARTESIAN_POINT('Ctrl Pts',(-0.202387241368133,-2.70222983111105,
8.80838214965003));
#404417=CARTESIAN_POINT('Ctrl Pts',(-0.205539955892626,-2.70723024682309,
8.81501364461993));
#404418=CARTESIAN_POINT('Ctrl Pts',(-0.213657465212903,-2.70437457614343,
8.81722098428721));
#404419=CARTESIAN_POINT('Ctrl Pts',(-0.189677921384463,-2.68207200113894,
8.82945683644722));
#404420=CARTESIAN_POINT('Ctrl Pts',(-0.192818242734711,-2.68705276044921,
8.83607469902389));
#404421=CARTESIAN_POINT('Ctrl Pts',(-0.200911757808346,-2.68421955444713,
8.8382956714852));
#404422=CARTESIAN_POINT('Ctrl Pts',(-0.17694962885436,-2.66188407944157,
8.85049129520029));
#404423=CARTESIAN_POINT('Ctrl Pts',(-0.180064098225775,-2.66682383578755,
8.85711686593484));
#404424=CARTESIAN_POINT('Ctrl Pts',(-0.188146120567841,-2.66403427005499,
8.85933012996512));
#404425=CARTESIAN_POINT('Origin',(-0.225652834737231,-2.71569317285208,
8.78727029226991));
#404426=CARTESIAN_POINT('Ctrl Pts',(-0.222459021446524,-2.73406497972526,
8.75374538247848));
#404427=CARTESIAN_POINT('Ctrl Pts',(-0.226500710045497,-2.74049997247247,
8.75304829418602));
#404428=CARTESIAN_POINT('Ctrl Pts',(-0.234104570794377,-2.73982770398393,
8.75272238421917));
#404429=CARTESIAN_POINT('Ctrl Pts',(-0.223163014106709,-2.73518155988289,
8.76769408445022));
#404430=CARTESIAN_POINT('Ctrl Pts',(-0.22730699392311,-2.74177811855035,
8.76974318093967));
#404431=CARTESIAN_POINT('Ctrl Pts',(-0.234842375123349,-2.74129192162787,
8.77077869880429));
#404432=CARTESIAN_POINT('Ctrl Pts',(-0.219554748756185,-2.72945860607643,
8.78108014887986));
#404433=CARTESIAN_POINT('Ctrl Pts',(-0.223063405128077,-2.73505097299613,
8.78639403366327));
#404434=CARTESIAN_POINT('Ctrl Pts',(-0.231060141221982,-2.73379626682602,
8.78812224174741));
#404435=CARTESIAN_POINT('Ctrl Pts',(-0.213641598409107,-2.72007994812382,
8.78944554828685));
#404436=CARTESIAN_POINT('Ctrl Pts',(-0.216593822171823,-2.72479596259281,
8.79673892988685));
#404437=CARTESIAN_POINT('Ctrl Pts',(-0.224894150551318,-2.72153895428623,
8.79894799272499));
#404438=CARTESIAN_POINT('Origin',(-0.233131563002538,-2.72755493516299,
8.75721825406948));
#404439=CARTESIAN_POINT('Origin',(-0.233131563002538,-2.72755493516299,
9.));
#404440=CARTESIAN_POINT('Origin',(-0.233131563002538,-2.72755493516299,
7.51860402984325));
#404441=CARTESIAN_POINT('Ctrl Pts',(-0.214971444915614,-2.73791160418274,
7.50366195182966));
#404442=CARTESIAN_POINT('Ctrl Pts',(-0.215258086646298,-2.74156232030815,
7.50000065167735));
#404443=CARTESIAN_POINT('Ctrl Pts',(-0.215258086646414,-2.74156232030814,
7.49482233047108));
#404444=CARTESIAN_POINT('Ctrl Pts',(-0.222353197839311,-2.73884086376986,
7.50215800491336));
#404445=CARTESIAN_POINT('Ctrl Pts',(-0.224762195877981,-2.74081606644907,
7.49877273257263));
#404446=CARTESIAN_POINT('Ctrl Pts',(-0.228203729217914,-2.74054587277758,
7.49481816995647));
#404447=CARTESIAN_POINT('Ctrl Pts',(-0.224060721014886,-2.73660605260401,
7.51043025814043));
#404448=CARTESIAN_POINT('Ctrl Pts',(-0.228407759062826,-2.74050425952473,
7.51006209594517));
#404449=CARTESIAN_POINT('Ctrl Pts',(-0.234198613355267,-2.74000930828873,
7.50731281821702));
#404450=CARTESIAN_POINT('Ctrl Pts',(-0.222556952678053,-2.73422033961323,
7.51860402984326));
#404451=CARTESIAN_POINT('Ctrl Pts',(-0.226614462609811,-2.74065754634786,
7.51860402984327));
#404452=CARTESIAN_POINT('Ctrl Pts',(-0.234196090687486,-2.74000952390803,
7.51860402984327));
#404453=CARTESIAN_POINT('Origin',(0.,0.,7.5));
#404454=CARTESIAN_POINT('Origin',(-0.00603856833113048,-2.66775215476039,
7.5));
#404455=CARTESIAN_POINT('',(-0.00603856833113048,-2.66775215476039,7.59394543036555));
#404456=CARTESIAN_POINT('',(-0.00603856833113048,-2.66775215476039,8.85049129520029));
#404457=CARTESIAN_POINT('',(-0.00603856833113048,-2.66775215476039,7.5));
#404458=CARTESIAN_POINT('',(-0.0402149326548299,-2.73054663635347,8.78727029226991));
#404459=CARTESIAN_POINT('Ctrl Pts',(-0.00603856833113057,-2.66775215476039,
8.85049129520029));
#404460=CARTESIAN_POINT('Ctrl Pts',(-0.0174472493241456,-2.68871407457819,
8.82945686509571));
#404461=CARTESIAN_POINT('Ctrl Pts',(-0.0288389699333437,-2.70964483196749,
8.80838212259895));
#404462=CARTESIAN_POINT('Ctrl Pts',(-0.0402149326548299,-2.73054663635347,
8.78727029226991));
#404463=CARTESIAN_POINT('',(-0.0469183093502055,-2.74286319116668,8.75721825406948));
#404464=CARTESIAN_POINT('Origin',(-0.0267453462054665,-2.70579850156065,
8.75937679713102));
#404465=CARTESIAN_POINT('',(-0.0469183093502055,-2.74286319116668,7.51860402984325));
#404466=CARTESIAN_POINT('',(-0.0469183093502055,-2.74286319116668,7.5));
#404467=CARTESIAN_POINT('Ctrl Pts',(-0.0469183093502053,-2.74286319116668,
7.51860402984325));
#404468=CARTESIAN_POINT('Ctrl Pts',(-0.041653849528267,-2.73319045294751,
7.52834476460825));
#404469=CARTESIAN_POINT('Ctrl Pts',(-0.0363859720949718,-2.72351143532627,
7.53807742314407));
#404470=CARTESIAN_POINT('Ctrl Pts',(-0.0311145622994817,-2.71382592746367,
7.54780169004674));
#404471=CARTESIAN_POINT('Ctrl Pts',(-0.0227649340788154,-2.69848460646635,
7.5632044032688));
#404472=CARTESIAN_POINT('Ctrl Pts',(-0.0144064330001542,-2.68312698278351,
7.57858609112103));
#404473=CARTESIAN_POINT('Ctrl Pts',(-0.00603856833113041,-2.66775215476039,
7.59394543036555));
#404474=CARTESIAN_POINT('Origin',(0.1375,-2.90929488800561,7.5));
#404475=CARTESIAN_POINT('',(0.0469183093502055,-2.74286319116668,8.75721825406948));
#404476=CARTESIAN_POINT('',(0.0402149326548299,-2.73054663635347,8.78727029226991));
#404477=CARTESIAN_POINT('Origin',(0.0231992623667671,-2.69928262639098,
8.75658640621021));
#404478=CARTESIAN_POINT('',(0.00603856833113048,-2.66775215476039,8.85049129520029));
#404479=CARTESIAN_POINT('Ctrl Pts',(0.04021493265483,-2.73054663635347,
8.78727029226991));
#404480=CARTESIAN_POINT('Ctrl Pts',(0.0288389699333486,-2.7096448319675,
8.80838212259896));
#404481=CARTESIAN_POINT('Ctrl Pts',(0.017447249324145,-2.68871407457819,
8.82945686509571));
#404482=CARTESIAN_POINT('Ctrl Pts',(0.00603856833113064,-2.66775215476039,
8.85049129520029));
#404483=CARTESIAN_POINT('',(0.00603856833113048,-2.66775215476039,7.59394543036555));
#404484=CARTESIAN_POINT('',(0.00603856833113048,-2.66775215476039,7.5));
#404485=CARTESIAN_POINT('',(0.0469183093502055,-2.74286319116668,7.51860402984325));
#404486=CARTESIAN_POINT('Ctrl Pts',(0.00603856833112958,-2.66775215476039,
7.59394543036555));
#404487=CARTESIAN_POINT('Ctrl Pts',(0.0144064330001523,-2.68312698278351,
7.57858609112103));
#404488=CARTESIAN_POINT('Ctrl Pts',(0.022764934078714,-2.69848460646616,
7.56320440326857));
#404489=CARTESIAN_POINT('Ctrl Pts',(0.031114562299379,-2.71382592746348,
7.54780169004651));
#404490=CARTESIAN_POINT('Ctrl Pts',(0.0363859720948704,-2.72351143532608,
7.53807742314383));
#404491=CARTESIAN_POINT('Ctrl Pts',(0.0416538495282657,-2.73319045294751,
7.52834476460825));
#404492=CARTESIAN_POINT('Ctrl Pts',(0.0469183093502052,-2.74286319116668,
7.51860402984325));
#404493=CARTESIAN_POINT('',(0.0469183093502055,-2.74286319116668,7.5));
#404494=CARTESIAN_POINT('Origin',(0.,-2.67103869055211,7.5));
#404495=CARTESIAN_POINT('Ctrl Pts',(0.0060385683311304,-2.66775215476039,
8.85049129520029));
#404496=CARTESIAN_POINT('Ctrl Pts',(0.0059459900808512,-2.66758205465325,
8.85097269580139));
#404497=CARTESIAN_POINT('Ctrl Pts',(0.00584719181995321,-2.66741812167859,
8.85143669361005));
#404498=CARTESIAN_POINT('Ctrl Pts',(0.00573687539919907,-2.6672532585408,
8.8519052845931));
#404499=CARTESIAN_POINT('Ctrl Pts',(0.00552110347621796,-2.66693079669851,
8.85282181883899));
#404500=CARTESIAN_POINT('Ctrl Pts',(0.00526665369920735,-2.66661318098465,
8.85372622499635));
#404501=CARTESIAN_POINT('Ctrl Pts',(0.00495749990689061,-2.66630506772301,
8.8546225773507));
#404502=CARTESIAN_POINT('Ctrl Pts',(0.00470085140861172,-2.66604928303633,
8.85536669723986));
#404503=CARTESIAN_POINT('Ctrl Pts',(0.00440646616566121,-2.66579996647417,
8.85610498449051));
#404504=CARTESIAN_POINT('Ctrl Pts',(0.00405997820836668,-2.66556586768779,
8.85681338218371));
#404505=CARTESIAN_POINT('Ctrl Pts',(0.00374553984295258,-2.66535342267149,
8.85745625420284));
#404506=CARTESIAN_POINT('Ctrl Pts',(0.00338458256238873,-2.66515034957616,
8.85808743050666));
#404507=CARTESIAN_POINT('Ctrl Pts',(0.00295369827383558,-2.66497307725867,
8.85866804508411));
#404508=CARTESIAN_POINT('Ctrl Pts',(0.00275489760352519,-2.66489128765418,
8.85893592806396));
#404509=CARTESIAN_POINT('Ctrl Pts',(0.00254103122291519,-2.6648151521707,
8.85919241173849));
#404510=CARTESIAN_POINT('Ctrl Pts',(0.00230877295597377,-2.66474750603832,
8.85943017985535));
#404511=CARTESIAN_POINT('Ctrl Pts',(0.00199515553979517,-2.66465616373421,
8.85975123720001));
#404512=CARTESIAN_POINT('Ctrl Pts',(0.00163984270799643,-2.66457859015688,
8.86004599534706));
#404513=CARTESIAN_POINT('Ctrl Pts',(0.00124488186767327,-2.66452589273075,
8.86026130871721));
#404514=CARTESIAN_POINT('Ctrl Pts',(0.00110027556890578,-2.66450659871735,
8.86034014101236));
#404515=CARTESIAN_POINT('Ctrl Pts',(0.000948183946098822,-2.66449033731455,
8.86040910639693));
#404516=CARTESIAN_POINT('Ctrl Pts',(0.000792714888868764,-2.6644778860275,
8.86046313645507));
#404517=CARTESIAN_POINT('Ctrl Pts',(0.000550106727103745,-2.66445845589833,
8.8605474499083));
#404518=CARTESIAN_POINT('Ctrl Pts',(0.000292639848427733,-2.66444792009911,
8.86059655985668));
#404519=CARTESIAN_POINT('Ctrl Pts',(3.68383656842663E-5,-2.66444666161026,
8.86059725258816));
#404520=CARTESIAN_POINT('Ctrl Pts',(-0.000219554120677806,-2.6644454002138,
8.86059794692011));
#404521=CARTESIAN_POINT('Ctrl Pts',(-0.000477129998147651,-2.66445610179498,
8.86056369958366));
#404522=CARTESIAN_POINT('Ctrl Pts',(-0.000721997165140026,-2.66447442282945,
8.86048590497774));
#404523=CARTESIAN_POINT('Ctrl Pts',(-0.000785900205151045,-2.66447920407396,
8.86046560290182));
#404524=CARTESIAN_POINT('Ctrl Pts',(-0.000849762296446932,-2.66448465677257,
8.86044257503091));
#404525=CARTESIAN_POINT('Ctrl Pts',(-0.000911612840154663,-2.66449057972519,
8.86041778462583));
#404526=CARTESIAN_POINT('Ctrl Pts',(-0.00132779024918037,-2.66453043384658,
8.860250975962));
#404527=CARTESIAN_POINT('Ctrl Pts',(-0.0017087062830535,-2.6645972575501,
8.8599848982295));
#404528=CARTESIAN_POINT('Ctrl Pts',(-0.00204470696718254,-2.6646807553764,
8.85968173251462));
#404529=CARTESIAN_POINT('Ctrl Pts',(-0.00222243207854282,-2.66472492094265,
8.85952137522077));
#404530=CARTESIAN_POINT('Ctrl Pts',(-0.00239106259016765,-2.6647744176014,
8.85934740853961));
#404531=CARTESIAN_POINT('Ctrl Pts',(-0.00254865826271333,-2.66482705571598,
8.8591675900182));
#404532=CARTESIAN_POINT('Ctrl Pts',(-0.00318148680458622,-2.66503842510675,
8.85844552518695));
#404533=CARTESIAN_POINT('Ctrl Pts',(-0.00367310982058979,-2.665309524653,
8.85759444184124));
#404534=CARTESIAN_POINT('Ctrl Pts',(-0.0040540988240094,-2.66556656868577,
8.85683498915139));
#404535=CARTESIAN_POINT('Ctrl Pts',(-0.00409396830856038,-2.66559346765924,
8.85675551444998));
#404536=CARTESIAN_POINT('Ctrl Pts',(-0.00413261203991475,-2.66562022675649,
8.85667699793651));
#404537=CARTESIAN_POINT('Ctrl Pts',(-0.00417005525354386,-2.66564677016415,
8.85659965593547));
#404538=CARTESIAN_POINT('Ctrl Pts',(-0.00467546566173685,-2.66600505443517,
8.85555568965886));
#404539=CARTESIAN_POINT('Ctrl Pts',(-0.00510945303863149,-2.66642237908077,
8.85434650606346));
#404540=CARTESIAN_POINT('Ctrl Pts',(-0.00547847041769397,-2.6668963274801,
8.85297329937117));
#404541=CARTESIAN_POINT('Ctrl Pts',(-0.00568602020885762,-2.66716289457662,
8.85220095427747));
#404542=CARTESIAN_POINT('Ctrl Pts',(-0.00587285370781608,-2.66744767638566,
8.85137579139183));
#404543=CARTESIAN_POINT('Ctrl Pts',(-0.00603856833113047,-2.66775215476039,
8.85049129520029));
#404544=CARTESIAN_POINT('Origin',(-2.28698895758661E-17,-2.67103869055211,
7.59394543036555));
#404545=CARTESIAN_POINT('Ctrl Pts',(0.00576978243959104,-2.66725829676663,
7.59443877723642));
#404546=CARTESIAN_POINT('Ctrl Pts',(0.00300154637558126,-2.66217203460837,
7.58783886950016));
#404547=CARTESIAN_POINT('Ctrl Pts',(-0.00519220816616302,-2.66439499840616,
7.58559994247159));
#404548=CARTESIAN_POINT('Ctrl Pts',(0.02088150189643,-2.69502405266403,
7.56670252222137));
#404549=CARTESIAN_POINT('Ctrl Pts',(0.0181172667194093,-2.68994514159859,
7.56004874999026));
#404550=CARTESIAN_POINT('Ctrl Pts',(0.00986936707313795,-2.69216065704217,
7.55786368756704));
#404551=CARTESIAN_POINT('Ctrl Pts',(0.0359650017270119,-2.72273795878639,
7.53888913333556));
#404552=CARTESIAN_POINT('Ctrl Pts',(0.0331843385650257,-2.71762886350384,
7.53222002137276));
#404553=CARTESIAN_POINT('Ctrl Pts',(0.0249043752016816,-2.71987489365092,
7.53005029815326));
#404554=CARTESIAN_POINT('Ctrl Pts',(0.0510195993927981,-2.75039876106078,
7.51101258149734));
#404555=CARTESIAN_POINT('Ctrl Pts',(0.0482052295407062,-2.74522773425994,
7.5043616886572));
#404556=CARTESIAN_POINT('Ctrl Pts',(0.0399120007351545,-2.74753637834759,
7.50217374673251));
#404557=CARTESIAN_POINT('',(0.0391111754616882,-2.74606032550115,7.50366116523517));
#404558=CARTESIAN_POINT('Ctrl Pts',(0.0469183093502058,-2.74286319116668,
7.51860402984325));
#404559=CARTESIAN_POINT('Ctrl Pts',(0.0471294178689308,-2.74325107473053,
7.51734760759493));
#404560=CARTESIAN_POINT('Ctrl Pts',(0.0472679263427267,-2.74363002494186,
7.51608817408573));
#404561=CARTESIAN_POINT('Ctrl Pts',(0.0473209740766766,-2.74400375441725,
7.5148100591312));
#404562=CARTESIAN_POINT('Ctrl Pts',(0.0473690259817052,-2.74434228750662,
7.51365231206384));
#404563=CARTESIAN_POINT('Ctrl Pts',(0.0473472713218873,-2.74467697892738,
7.51247773061042));
#404564=CARTESIAN_POINT('Ctrl Pts',(0.0472192392491715,-2.74499964227536,
7.51129758471022));
#404565=CARTESIAN_POINT('Ctrl Pts',(0.0470601100046003,-2.74540067596735,
7.50983079813402));
#404566=CARTESIAN_POINT('Ctrl Pts',(0.046729779299906,-2.74576552647934,
7.50839324291155));
#404567=CARTESIAN_POINT('Ctrl Pts',(0.0461647233399476,-2.7460415258142,
7.50715379678855));
#404568=CARTESIAN_POINT('Ctrl Pts',(0.0459036837681432,-2.74616902955418,
7.50658120839351));
#404569=CARTESIAN_POINT('Ctrl Pts',(0.0455512704078028,-2.74628715902903,
7.50598221009429));
#404570=CARTESIAN_POINT('Ctrl Pts',(0.0451086408757811,-2.74637153582515,
7.50545747549612));
#404571=CARTESIAN_POINT('Ctrl Pts',(0.0448724400568288,-2.74641656189527,
7.50517746087247));
#404572=CARTESIAN_POINT('Ctrl Pts',(0.0446080257594691,-2.74645266364665,
7.50491486231392));
#404573=CARTESIAN_POINT('Ctrl Pts',(0.0443221744710907,-2.74647723236113,
7.50468370960992));
#404574=CARTESIAN_POINT('Ctrl Pts',(0.0438947366282894,-2.74651397033903,
7.50433806340447));
#404575=CARTESIAN_POINT('Ctrl Pts',(0.0434065014443691,-2.74652546781193,
7.50405484070984));
#404576=CARTESIAN_POINT('Ctrl Pts',(0.0428903337854138,-2.74651023424991,
7.50385766036131));
#404577=CARTESIAN_POINT('Ctrl Pts',(0.0428351376773493,-2.74650860525724,
7.50383657498791));
#404578=CARTESIAN_POINT('Ctrl Pts',(0.0427796461468655,-2.7465066857332,
7.50381643264937));
#404579=CARTESIAN_POINT('Ctrl Pts',(0.0427239166342627,-2.74650448512403,
7.50379723213559));
#404580=CARTESIAN_POINT('Ctrl Pts',(0.0423519039072551,-2.74648979533795,
7.50366906242519));
#404581=CARTESIAN_POINT('Ctrl Pts',(0.041961222930374,-2.74646154237284,
7.50358235568538));
#404582=CARTESIAN_POINT('Ctrl Pts',(0.041585309161405,-2.74642525806308,
7.5035341175365));
#404583=CARTESIAN_POINT('Ctrl Pts',(0.0410216690100585,-2.74637085384718,
7.50346178989176));
#404584=CARTESIAN_POINT('Ctrl Pts',(0.0404176336735106,-2.74628836196342,
7.50346967198527));
#404585=CARTESIAN_POINT('Ctrl Pts',(0.0398271499193935,-2.74618913461648,
7.50354272648692));
#404586=CARTESIAN_POINT('Ctrl Pts',(0.0395842717290363,-2.74614832035481,
7.50357277531559));
#404587=CARTESIAN_POINT('Ctrl Pts',(0.0393439854661266,-2.74610486877363,
7.50361331098761));
#404588=CARTESIAN_POINT('Ctrl Pts',(0.0391111754617084,-2.74606032550256,
7.50366116523659));
#404589=CARTESIAN_POINT('',(-1.95335088339909E-13,-2.67396661573471,7.57603338622103));
#404590=CARTESIAN_POINT('Origin',(-2.85317610332501E-6,-2.68280355420138,
7.58486873427628));
#404591=CARTESIAN_POINT('Ctrl Pts',(0.039111175493625,-2.74606032554878,
7.50366116529969));
#404592=CARTESIAN_POINT('Ctrl Pts',(0.0260946561062611,-2.72206870155541,
7.52783573079709));
#404593=CARTESIAN_POINT('Ctrl Pts',(0.0130581974131689,-2.69803860815066,
7.55196141284069));
#404594=CARTESIAN_POINT('Ctrl Pts',(8.83381775932182E-10,-2.67396661662181,
7.57603338728831));
#404595=CARTESIAN_POINT('Ctrl Pts',(0.00637576431677354,-2.66873949177856,
7.59639677331371));
#404596=CARTESIAN_POINT('Ctrl Pts',(0.000286090908296224,-2.6515061579884,
7.59959882295465));
#404597=CARTESIAN_POINT('Ctrl Pts',(-0.00631291894862653,-2.66856962426893,
7.59642833564546));
#404598=CARTESIAN_POINT('Ctrl Pts',(0.00568422544926916,-2.66490062761342,
7.58707626057423));
#404599=CARTESIAN_POINT('Ctrl Pts',(9.68314384630046E-5,-2.66106744105337,
7.58809943920598));
#404600=CARTESIAN_POINT('Ctrl Pts',(-0.0055389809656482,-2.66480268125159,
7.58710240504252));
#404601=CARTESIAN_POINT('Ctrl Pts',(0.00215341460009478,-2.66984623243071,
7.58015376756929));
#404602=CARTESIAN_POINT('Ctrl Pts',(3.20712293815052E-5,-2.66794119340239,
7.58205880659761));
#404603=CARTESIAN_POINT('Ctrl Pts',(-0.00209070701379044,-2.66979075755872,
7.58020924244128));
#404604=CARTESIAN_POINT('Ctrl Pts',(7.55734230502141E-15,-2.67396661490714,
7.57603338509286));
#404605=CARTESIAN_POINT('Ctrl Pts',(7.55734230502141E-15,-2.67396661490714,
7.57603338509286));
#404606=CARTESIAN_POINT('Ctrl Pts',(7.55734230502141E-15,-2.67396661490714,
7.57603338509286));
#404607=CARTESIAN_POINT('Origin',(2.85317624624927E-6,-2.68280355420188,
7.58486873427622));
#404608=CARTESIAN_POINT('Ctrl Pts',(-0.0510325618244046,-2.75042257778878,
7.51098857897448));
#404609=CARTESIAN_POINT('Ctrl Pts',(-0.0482181791375388,-2.74525152740576,
7.50433767179956));
#404610=CARTESIAN_POINT('Ctrl Pts',(-0.0399249227228591,-2.74756019566318,
7.50214974420965));
#404611=CARTESIAN_POINT('Ctrl Pts',(-0.0359736340692041,-2.72275381955636,
7.53887321589169));
#404612=CARTESIAN_POINT('Ctrl Pts',(-0.0331929726815447,-2.71764472753391,
7.53220407452065));
#404613=CARTESIAN_POINT('Ctrl Pts',(-0.0249129797891101,-2.71989075460921,
7.53003438070911));
#404614=CARTESIAN_POINT('Ctrl Pts',(-0.0208857876177118,-2.69503192710157,
7.56669465659234));
#404615=CARTESIAN_POINT('Ctrl Pts',(-0.0181215594219111,-2.68995302886307,
7.56004085833303));
#404616=CARTESIAN_POINT('Ctrl Pts',(-0.00987363856813336,-2.6921685314508,
7.55785582193789));
#404617=CARTESIAN_POINT('Ctrl Pts',(-0.00576970483280572,-2.66725815417458,
7.59443891967696));
#404618=CARTESIAN_POINT('Ctrl Pts',(-0.00300146885025822,-2.66217189216599,
7.58783901202978));
#404619=CARTESIAN_POINT('Ctrl Pts',(0.00519228551543038,-2.66439485581461,
7.58560008491213));
#404620=CARTESIAN_POINT('',(-0.0391111754616882,-2.74606032550115,7.50366116523517));
#404621=CARTESIAN_POINT('Ctrl Pts',(-0.0391111754616935,-2.74606032550152,
7.50366116523554));
#404622=CARTESIAN_POINT('Ctrl Pts',(-0.0398554269668709,-2.74620254791117,
7.50350835821027));
#404623=CARTESIAN_POINT('Ctrl Pts',(-0.0405442017937647,-2.74630907137797,
7.50345484956));
#404624=CARTESIAN_POINT('Ctrl Pts',(-0.041197885997511,-2.74638365637749,
7.50349758195598));
#404625=CARTESIAN_POINT('Ctrl Pts',(-0.0415332744725173,-2.74642192401361,
7.50351950684424));
#404626=CARTESIAN_POINT('Ctrl Pts',(-0.0418924680760451,-2.74645568442726,
7.50357029184312));
#404627=CARTESIAN_POINT('Ctrl Pts',(-0.0422397292057554,-2.74647871828665,
7.50365515313923));
#404628=CARTESIAN_POINT('Ctrl Pts',(-0.0427739574431678,-2.74651415368973,
7.50378570417639));
#404629=CARTESIAN_POINT('Ctrl Pts',(-0.043295603978508,-2.74652558920171,
7.50400001621911));
#404630=CARTESIAN_POINT('Ctrl Pts',(-0.0437650136951257,-2.7465098845443,
7.50428903009635));
#404631=CARTESIAN_POINT('Ctrl Pts',(-0.0438171145622485,-2.74650814144815,
7.50432110841318));
#404632=CARTESIAN_POINT('Ctrl Pts',(-0.0438685974280384,-2.7465060803685,
7.50435406373354));
#404633=CARTESIAN_POINT('Ctrl Pts',(-0.0439194270703296,-2.7465037088339,
7.50438785222352));
#404634=CARTESIAN_POINT('Ctrl Pts',(-0.0442297664683503,-2.74648922947526,
7.50459414719561));
#404635=CARTESIAN_POINT('Ctrl Pts',(-0.0445206726054126,-2.74646243160482,
7.50483629897752));
#404636=CARTESIAN_POINT('Ctrl Pts',(-0.0447811216729617,-2.74642565232408,
7.5050991045531));
#404637=CARTESIAN_POINT('Ctrl Pts',(-0.0453556984756071,-2.74634451353664,
7.50567888004914));
#404638=CARTESIAN_POINT('Ctrl Pts',(-0.0458047587608244,-2.74621211426885,
7.50637912803145));
#404639=CARTESIAN_POINT('Ctrl Pts',(-0.0461444808270324,-2.74605479234555,
7.50710440483569));
#404640=CARTESIAN_POINT('Ctrl Pts',(-0.0462277874220943,-2.74601621388668,
7.50728225710685));
#404641=CARTESIAN_POINT('Ctrl Pts',(-0.0463062389178226,-2.74597550121701,
7.50746498566954));
#404642=CARTESIAN_POINT('Ctrl Pts',(-0.046378195894123,-2.74593397446876,
7.50764697238949));
#404643=CARTESIAN_POINT('Ctrl Pts',(-0.046765016795621,-2.74571073809862,
7.50862528291182));
#404644=CARTESIAN_POINT('Ctrl Pts',(-0.0470013398974825,-2.74544729614725,
7.50965856837422));
#404645=CARTESIAN_POINT('Ctrl Pts',(-0.0471465970325942,-2.74517302978349,
7.51067959873203));
#404646=CARTESIAN_POINT('Ctrl Pts',(-0.047226532217264,-2.74502210065757,
7.51124147302579));
#404647=CARTESIAN_POINT('Ctrl Pts',(-0.0472785253772167,-2.74486765340863,
7.51180065547253));
#404648=CARTESIAN_POINT('Ctrl Pts',(-0.0473100357766602,-2.74471340164584,
7.512351757165));
#404649=CARTESIAN_POINT('Ctrl Pts',(-0.0474189167589901,-2.7441804003588,
7.51425603304535));
#404650=CARTESIAN_POINT('Ctrl Pts',(-0.0472902783286503,-2.74358496893378,
7.51626900505179));
#404651=CARTESIAN_POINT('Ctrl Pts',(-0.0469717238008019,-2.74296420982058,
7.51827788969243));
#404652=CARTESIAN_POINT('Ctrl Pts',(-0.0469544830277697,-2.7429306131643,
7.51838661432545));
#404653=CARTESIAN_POINT('Ctrl Pts',(-0.046936676684081,-2.74289693867703,
7.51849533314856));
#404654=CARTESIAN_POINT('Ctrl Pts',(-0.0469183093502091,-2.74286319116668,
7.51860402984325));
#404655=CARTESIAN_POINT('Ctrl Pts',(-8.84014432836477E-10,-2.673966616623,
7.57603338728985));
#404656=CARTESIAN_POINT('Ctrl Pts',(-0.0130581974166911,-2.69803860815728,
7.55196141284922));
#404657=CARTESIAN_POINT('Ctrl Pts',(-0.0260946561203838,-2.72206870158194,
7.52783573083105));
#404658=CARTESIAN_POINT('Ctrl Pts',(-0.0391111754945677,-2.74606032555036,
7.50366116530176));
#404659=CARTESIAN_POINT('Origin',(0.,-9.23979071467924E-16,7.49482233047033));
#404660=CARTESIAN_POINT('Origin',(0.0389852998002483,-2.73722238709234,
7.49482233047033));
#404661=CARTESIAN_POINT('Origin',(0.,0.,7.50366116523517));
#404662=CARTESIAN_POINT('Origin',(-0.0389852998002483,-2.73722238709234,
7.49482233047033));
#404663=CARTESIAN_POINT('Ctrl Pts',(0.0469178037552554,-2.74286226211022,
7.51860402984325));
#404664=CARTESIAN_POINT('Ctrl Pts',(0.0505546378370144,-2.74954580337903,
7.51860402984325));
#404665=CARTESIAN_POINT('Ctrl Pts',(0.0581618967556967,-2.74938487552503,
7.51860402984325));
#404666=CARTESIAN_POINT('Ctrl Pts',(0.0482681861850447,-2.74534390598683,
7.51041458714366));
#404667=CARTESIAN_POINT('Ctrl Pts',(0.0523568843976852,-2.74950766782993,
7.51004642900441));
#404668=CARTESIAN_POINT('Ctrl Pts',(0.0581639947473825,-2.74938483114304,
7.50729136483008));
#404669=CARTESIAN_POINT('Ctrl Pts',(0.046411539069441,-2.74745970339853,
7.50215815450138));
#404670=CARTESIAN_POINT('Ctrl Pts',(0.0486873335340281,-2.74958545597972,
7.49877163671531));
#404671=CARTESIAN_POINT('Ctrl Pts',(0.0521371901874483,-2.74953633709117,
7.49481588533172));
#404672=CARTESIAN_POINT('Ctrl Pts',(0.0391111676211739,-2.74605977503896,
7.50366171572174));
#404673=CARTESIAN_POINT('Ctrl Pts',(0.0391633148674429,-2.7497211194535,
7.50000045605858));
#404674=CARTESIAN_POINT('Ctrl Pts',(0.0391633148675675,-2.7497211194535,
7.49482233047317));
#404675=CARTESIAN_POINT('Origin',(0.0578975244977156,-2.73688767154537,
7.51860402984325));
#404676=CARTESIAN_POINT('Origin',(0.0578975244977156,-2.73688767154537,
9.));
#404677=CARTESIAN_POINT('Origin',(0.0578975244977155,-2.73688767154537,
8.75721825406948));
#404678=CARTESIAN_POINT('Ctrl Pts',(0.0389349646546054,-2.72819480378046,
8.78942910404912));
#404679=CARTESIAN_POINT('Ctrl Pts',(0.0415810698404544,-2.73309894040653,
8.79672699501691));
#404680=CARTESIAN_POINT('Ctrl Pts',(0.0500812990341605,-2.73037504803777,
8.79893251111266));
#404681=CARTESIAN_POINT('Ctrl Pts',(0.0441907101996742,-2.7378515401601,
8.78111911759583));
#404682=CARTESIAN_POINT('Ctrl Pts',(0.0473342496199764,-2.74366191622698,
8.78644465894812));
#404683=CARTESIAN_POINT('Ctrl Pts',(0.0554049987396859,-2.74290131092718,
8.78817647674132));
#404684=CARTESIAN_POINT('Ctrl Pts',(0.0474662162126847,-2.74386984859159,
8.76780923932029));
#404685=CARTESIAN_POINT('Ctrl Pts',(0.0511815136631335,-2.75072632739817,
8.76988516158375));
#404686=CARTESIAN_POINT('Ctrl Pts',(0.0587403725670997,-2.75072062947551,
8.77093053738833));
#404687=CARTESIAN_POINT('Ctrl Pts',(0.0468275373701203,-2.74269636081296,
8.75371302330492));
#404688=CARTESIAN_POINT('Ctrl Pts',(0.0504509795361609,-2.74938492330704,
8.75300828287559));
#404689=CARTESIAN_POINT('Ctrl Pts',(0.058090260070451,-2.74919536526138,
8.75267964240738));
#404690=CARTESIAN_POINT('Origin',(0.0511941478023398,-2.72457111673216,
8.78727029226991));
#404691=CARTESIAN_POINT('Ctrl Pts',(0.00603856833113048,-2.66775215476039,
8.85049129520029));
#404692=CARTESIAN_POINT('Ctrl Pts',(0.00883014741545966,-2.67288130658491,
8.85711686593484));
#404693=CARTESIAN_POINT('Ctrl Pts',(0.0170742924659647,-2.67061528926368,
8.85933012996512));
#404694=CARTESIAN_POINT('Ctrl Pts',(0.0174472646350165,-2.68871410270986,
8.82945683644723));
#404695=CARTESIAN_POINT('Ctrl Pts',(0.0202620155135629,-2.69388582959568,
8.8360746990239));
#404696=CARTESIAN_POINT('Ctrl Pts',(0.0285204257242725,-2.69157699801036,
8.8382956714852));
#404697=CARTESIAN_POINT('Ctrl Pts',(0.0288389553570734,-2.70964480518555,
8.80838214965002));
#404698=CARTESIAN_POINT('Ctrl Pts',(0.0316648145567818,-2.71483694212032,
8.81501364461994));
#404699=CARTESIAN_POINT('Ctrl Pts',(0.0399486090321783,-2.71250722933019,
8.81722098428721));
#404700=CARTESIAN_POINT('Ctrl Pts',(0.04021493265483,-2.73054663635347,
8.78727029226991));
#404701=CARTESIAN_POINT('Ctrl Pts',(0.0430412612390256,-2.73573963571921,
8.79393457792714));
#404702=CARTESIAN_POINT('Ctrl Pts',(0.0513601984344042,-2.73340839160553,
8.79610912703474));
#404703=CARTESIAN_POINT('Origin',(0.0170177834786405,-2.66177663513908,
8.85049129520029));
#404704=CARTESIAN_POINT('Ctrl Pts',(-0.00603856833113047,-2.66775215476039,
8.85049129520029));
#404705=CARTESIAN_POINT('Ctrl Pts',(-0.00883014741545964,-2.67288130658491,
8.85711686593484));
#404706=CARTESIAN_POINT('Ctrl Pts',(-0.0170742924659647,-2.67061528926368,
8.85933012996512));
#404707=CARTESIAN_POINT('Ctrl Pts',(-0.0035688986120927,-2.66321446818132,
8.86332496987232));
#404708=CARTESIAN_POINT('Ctrl Pts',(-0.00818107962988514,-2.66349674576787,
8.86648636486738));
#404709=CARTESIAN_POINT('Ctrl Pts',(-0.0101502424853851,-2.65792911615186,
8.87206031107457));
#404710=CARTESIAN_POINT('Ctrl Pts',(0.00355211642776816,-2.66318363317047,
8.86341338519876));
#404711=CARTESIAN_POINT('Ctrl Pts',(0.0081791237408215,-2.6634371562646,
8.86654584966058));
#404712=CARTESIAN_POINT('Ctrl Pts',(0.0100991546002723,-2.65783022891655,
8.87215952290714));
#404713=CARTESIAN_POINT('Ctrl Pts',(0.0060385683311304,-2.66775215476039,
8.85049129520029));
#404714=CARTESIAN_POINT('Ctrl Pts',(0.00883014741545944,-2.67288130658491,
8.85711686593484));
#404715=CARTESIAN_POINT('Ctrl Pts',(0.0170742924659645,-2.67061528926368,
8.85933012996512));
#404716=CARTESIAN_POINT('Origin',(-0.0170177834786405,-2.66177663513908,
8.85049129520029));
#404717=CARTESIAN_POINT('Ctrl Pts',(-0.0402149326548301,-2.73054663635347,
8.78727029226991));
#404718=CARTESIAN_POINT('Ctrl Pts',(-0.0430412612390258,-2.73573963571921,
8.79393457792714));
#404719=CARTESIAN_POINT('Ctrl Pts',(-0.0513601984344043,-2.73340839160553,
8.79610912703474));
#404720=CARTESIAN_POINT('Ctrl Pts',(-0.0288389553570644,-2.70964480518553,
8.80838214965001));
#404721=CARTESIAN_POINT('Ctrl Pts',(-0.0316648145567926,-2.71483694212031,
8.81501364461994));
#404722=CARTESIAN_POINT('Ctrl Pts',(-0.0399486090321813,-2.71250722933019,
8.81722098428722));
#404723=CARTESIAN_POINT('Ctrl Pts',(-0.0174472646350206,-2.68871410270986,
8.82945683644722));
#404724=CARTESIAN_POINT('Ctrl Pts',(-0.0202620155135602,-2.69388582959568,
8.8360746990239));
#404725=CARTESIAN_POINT('Ctrl Pts',(-0.0285204257242735,-2.69157699801037,
8.83829567148519));
#404726=CARTESIAN_POINT('Ctrl Pts',(-0.00603856833113056,-2.66775215476039,
8.85049129520029));
#404727=CARTESIAN_POINT('Ctrl Pts',(-0.00883014741545973,-2.67288130658491,
8.85711686593484));
#404728=CARTESIAN_POINT('Ctrl Pts',(-0.0170742924659648,-2.67061528926368,
8.85933012996512));
#404729=CARTESIAN_POINT('Origin',(-0.05119414780234,-2.72457111673216,8.78727029226991));
#404730=CARTESIAN_POINT('Ctrl Pts',(-0.046829810835768,-2.74270054843765,
8.75374538247848));
#404731=CARTESIAN_POINT('Ctrl Pts',(-0.0504509039511556,-2.74938127167972,
8.75304829418601));
#404732=CARTESIAN_POINT('Ctrl Pts',(-0.0580822141425596,-2.74919756546978,
8.75272238421917));
#404733=CARTESIAN_POINT('Ctrl Pts',(-0.0474608175312104,-2.7438599394262,
8.7676940844502));
#404734=CARTESIAN_POINT('Ctrl Pts',(-0.0511736401317078,-2.75070845045484,
8.76974318093969));
#404735=CARTESIAN_POINT('Ctrl Pts',(-0.0587246898268686,-2.7507060460072,
8.77077869880429));
#404736=CARTESIAN_POINT('Ctrl Pts',(-0.0442266366581528,-2.73791756168736,
8.78108014887991));
#404737=CARTESIAN_POINT('Ctrl Pts',(-0.0473697799404577,-2.74372323887499,
8.78639403366324));
#404738=CARTESIAN_POINT('Ctrl Pts',(-0.0554304751827418,-2.74298346327396,
8.78812224174742));
#404739=CARTESIAN_POINT('Ctrl Pts',(-0.0389265281907873,-2.72817931634984,
8.78944554828685));
#404740=CARTESIAN_POINT('Ctrl Pts',(-0.041570530208704,-2.73307479088723,
8.79673892988686));
#404741=CARTESIAN_POINT('Ctrl Pts',(-0.0500624819120103,-2.73035627831871,
8.79894799272499));
#404742=CARTESIAN_POINT('Origin',(-0.0578975244977156,-2.73688767154537,
8.75721825406948));
#404743=CARTESIAN_POINT('Origin',(-0.0578975244977156,-2.73688767154537,
9.));
#404744=CARTESIAN_POINT('Origin',(-0.0578975244977155,-2.73688767154537,
7.51860402984325));
#404745=CARTESIAN_POINT('Ctrl Pts',(-0.0391111642587046,-2.74605953891717,
7.50366195182966));
#404746=CARTESIAN_POINT('Ctrl Pts',(-0.0391633148679688,-2.74972111945349,
7.50000065167735));
#404747=CARTESIAN_POINT('Ctrl Pts',(-0.0391633148680856,-2.74972111945349,
7.49482233047108));
#404748=CARTESIAN_POINT('Ctrl Pts',(-0.0464182127131561,-2.74745983977445,
7.50215800491338));
#404749=CARTESIAN_POINT('Ctrl Pts',(-0.0486957095368232,-2.74958532922222,
7.49877273257267));
#404750=CARTESIAN_POINT('Ctrl Pts',(-0.0521474832453746,-2.74953619049074,
7.49481816995647));
#404751=CARTESIAN_POINT('Ctrl Pts',(-0.0482654124422661,-2.74533902165334,
7.51043025814041));
#404752=CARTESIAN_POINT('Ctrl Pts',(-0.05235376005938,-2.74950773497384,
7.51006209594513));
#404753=CARTESIAN_POINT('Ctrl Pts',(-0.0581644280551635,-2.74938482197663,
7.50731281821699));
#404754=CARTESIAN_POINT('Ctrl Pts',(-0.0469175869148848,-2.74286186359761,
7.51860402984325));
#404755=CARTESIAN_POINT('Ctrl Pts',(-0.0505543270057747,-2.74954580995451,
7.51860402984325));
#404756=CARTESIAN_POINT('Ctrl Pts',(-0.0581618967557014,-2.74938487552503,
7.51860402984325));
#404757=CARTESIAN_POINT('Origin',(0.,0.,7.5));
#404758=CARTESIAN_POINT('Origin',(0.164897305964678,-2.66265786424426,7.5));
#404759=CARTESIAN_POINT('',(0.164897305964678,-2.66265786424426,7.59394543036555));
#404760=CARTESIAN_POINT('',(0.164897305964678,-2.66265786424426,8.85049129520029));
#404761=CARTESIAN_POINT('',(0.164897305964678,-2.66265786424426,7.5));
#404762=CARTESIAN_POINT('',(0.13481441689613,-2.72751301502058,8.78727029226991));
#404763=CARTESIAN_POINT('Ctrl Pts',(0.164897305964678,-2.66265786424426,
8.85049129520029));
#404764=CARTESIAN_POINT('Ctrl Pts',(0.154855100144285,-2.68430767225054,
8.82945686509571));
#404765=CARTESIAN_POINT('Ctrl Pts',(0.144827823277126,-2.70592529519937,
8.80838212259897));
#404766=CARTESIAN_POINT('Ctrl Pts',(0.13481441689613,-2.72751301502058,
8.78727029226991));
#404767=CARTESIAN_POINT('',(0.128913937383397,-2.74023375097047,8.75721825406948));
#404768=CARTESIAN_POINT('Origin',(0.146670710195346,-2.70195272855781,8.7593767971309));
#404769=CARTESIAN_POINT('',(0.128913937383397,-2.74023375097047,7.51860402984325));
#404770=CARTESIAN_POINT('',(0.128913937383397,-2.74023375097047,7.5));
#404771=CARTESIAN_POINT('Ctrl Pts',(0.128913937383397,-2.74023375097047,
7.51860402984325));
#404772=CARTESIAN_POINT('Ctrl Pts',(0.133547846342501,-2.73024359133049,
7.52834476460825));
#404773=CARTESIAN_POINT('Ctrl Pts',(0.138184763568441,-2.72024694622305,
7.53807742314407));
#404774=CARTESIAN_POINT('Ctrl Pts',(0.142824790067768,-2.71024359788991,
7.54780169004674));
#404775=CARTESIAN_POINT('Ctrl Pts',(0.150174341270667,-2.69439883476507,
7.5632044032688));
#404776=CARTESIAN_POINT('Ctrl Pts',(0.157531702584675,-2.67853723396437,
7.57858609112103));
#404777=CARTESIAN_POINT('Ctrl Pts',(0.164897305964679,-2.66265786424426,
7.59394543036555));
#404778=CARTESIAN_POINT('Origin',(0.323616654966475,-2.89450777438995,7.5));
#404779=CARTESIAN_POINT('',(0.222557758686742,-2.73422161816808,8.75721825406948));
#404780=CARTESIAN_POINT('',(0.215079030421435,-2.72235985585717,8.78727029226991));
#404781=CARTESIAN_POINT('Origin',(0.19609522865786,-2.69225027889583,8.75658640621063));
#404782=CARTESIAN_POINT('',(0.176949628854398,-2.66188407944157,8.85049129520029));
#404783=CARTESIAN_POINT('Ctrl Pts',(0.215079030421435,-2.72235985585717,
8.78727029226991));
#404784=CARTESIAN_POINT('Ctrl Pts',(0.202387257630427,-2.70222985690407,
8.80838212259895));
#404785=CARTESIAN_POINT('Ctrl Pts',(0.18967790430268,-2.68207197404603,
8.82945686509571));
#404786=CARTESIAN_POINT('Ctrl Pts',(0.176949628854398,-2.66188407944157,
8.85049129520029));
#404787=CARTESIAN_POINT('',(0.176949628854398,-2.66188407944157,7.59394543036555));
#404788=CARTESIAN_POINT('',(0.176949628854398,-2.66188407944157,7.5));
#404789=CARTESIAN_POINT('',(0.222557758686742,-2.73422161816808,7.51860402984325));
#404790=CARTESIAN_POINT('Ctrl Pts',(0.176949628854397,-2.66188407944157,
7.59394543036555));
#404791=CARTESIAN_POINT('Ctrl Pts',(0.186285369461614,-2.67669118730145,
7.57858609112103));
#404792=CARTESIAN_POINT('Ctrl Pts',(0.195610663430991,-2.69148172609634,
7.56320440326857));
#404793=CARTESIAN_POINT('Ctrl Pts',(0.204926058256075,-2.70625656418746,
7.54780169004651));
#404794=CARTESIAN_POINT('Ctrl Pts',(0.210807189994167,-2.71558443175019,
7.53807742314383));
#404795=CARTESIAN_POINT('Ctrl Pts',(0.2166843807966,-2.72490604872585,7.52834476460825));
#404796=CARTESIAN_POINT('Ctrl Pts',(0.222557758686742,-2.73422161816808,
7.51860402984325));
#404797=CARTESIAN_POINT('',(0.222557758686742,-2.73422161816808,7.5));
#404798=CARTESIAN_POINT('Origin',(0.171134036480688,-2.66555075509437,7.5));
#404799=CARTESIAN_POINT('Ctrl Pts',(0.176949628854398,-2.66188407944157,
8.85049129520029));
#404800=CARTESIAN_POINT('Ctrl Pts',(0.176846342464779,-2.6617202603322,
8.85097269580138));
#404801=CARTESIAN_POINT('Ctrl Pts',(0.176737243973756,-2.66156299420173,
8.85143669361005));
#404802=CARTESIAN_POINT('Ctrl Pts',(0.176616591392414,-2.66140553779028,
8.8519052845931));
#404803=CARTESIAN_POINT('Ctrl Pts',(0.176380602594819,-2.661097563035,8.85282181883899));
#404804=CARTESIAN_POINT('Ctrl Pts',(0.176106325903508,-2.66079690254988,
8.85372622499635));
#404805=CARTESIAN_POINT('Ctrl Pts',(0.175778066416361,-2.66050922989145,
8.8546225773507));
#404806=CARTESIAN_POINT('Ctrl Pts',(0.175505557048805,-2.6602704142676,
8.85536669723986));
#404807=CARTESIAN_POINT('Ctrl Pts',(0.175195802884927,-2.66004047128033,
8.85610498449051));
#404808=CARTESIAN_POINT('Ctrl Pts',(0.174835028063561,-2.65982905303466,
8.85681338218371));
#404809=CARTESIAN_POINT('Ctrl Pts',(0.174507624346565,-2.65963719064467,
8.85745625420285));
#404810=CARTESIAN_POINT('Ctrl Pts',(0.174134397753556,-2.65945766139716,
8.85808743050666));
#404811=CARTESIAN_POINT('Ctrl Pts',(0.173693040886609,-2.65930836015582,
8.85866804508411));
#404812=CARTESIAN_POINT('Ctrl Pts',(0.173489408395645,-2.65923947579952,
8.85893592806396));
#404813=CARTESIAN_POINT('Ctrl Pts',(0.173271103409276,-2.65917719921061,
8.85919241173848));
#404814=CARTESIAN_POINT('Ctrl Pts',(0.173034988239271,-2.65912457290272,
8.85943017985534));
#404815=CARTESIAN_POINT('Ctrl Pts',(0.172716162862191,-2.65905351180801,
8.8597512372));
#404816=CARTESIAN_POINT('Ctrl Pts',(0.172356609902548,-2.65899886258521,
8.86004599534705));
#404817=CARTESIAN_POINT('Ctrl Pts',(0.171959084215947,-2.65897157865952,
8.86026130871721));
#404818=CARTESIAN_POINT('Ctrl Pts',(0.171813538854646,-2.65896158924511,
8.86034014101235));
#404819=CARTESIAN_POINT('Ctrl Pts',(0.171660717848735,-2.65895510579683,
8.86040910639692));
#404820=CARTESIAN_POINT('Ctrl Pts',(0.171504770462657,-2.65895264102898,
8.86046313645506));
#404821=CARTESIAN_POINT('Ctrl Pts',(0.17126141587273,-2.6589487947794,8.86054744990829));
#404822=CARTESIAN_POINT('Ctrl Pts',(0.171003802956396,-2.65895477658666,
8.86059655985668));
#404823=CARTESIAN_POINT('Ctrl Pts',(0.170748446413576,-2.65896990994078,
8.86059725258816));
#404824=CARTESIAN_POINT('Ctrl Pts',(0.170492499895126,-2.658985078259,8.86059794692011));
#404825=CARTESIAN_POINT('Ctrl Pts',(0.170236138887582,-2.65901226079576,
8.86056369958366));
#404826=CARTESIAN_POINT('Ctrl Pts',(0.169992948659155,-2.65904623288096,
8.86048590497774));
#404827=CARTESIAN_POINT('Ctrl Pts',(0.169929483250181,-2.65905509858372,
8.86046560290182));
#404828=CARTESIAN_POINT('Ctrl Pts',(0.169866101726,-2.65906463173741,8.86044257503091));
#404829=CARTESIAN_POINT('Ctrl Pts',(0.169804757745746,-2.65907450529864,
8.86041778462583));
#404830=CARTESIAN_POINT('Ctrl Pts',(0.169391988880166,-2.6591409421136,
8.86025097596201));
#404831=CARTESIAN_POINT('Ctrl Pts',(0.169016136888523,-2.65923203389475,
8.8599848982295));
#404832=CARTESIAN_POINT('Ctrl Pts',(0.168686176277933,-2.65933688780354,
8.85968173251461));
#404833=CARTESIAN_POINT('Ctrl Pts',(0.168511646019421,-2.65939234951388,
8.85952137522076));
#404834=CARTESIAN_POINT('Ctrl Pts',(0.168346533239082,-2.65945254867042,
8.85934740853961));
#404835=CARTESIAN_POINT('Ctrl Pts',(0.168192633899328,-2.65951517582375,
8.8591675900182));
#404836=CARTESIAN_POINT('Ctrl Pts',(0.167574648054925,-2.65976665639733,
8.85844552518695));
#404837=CARTESIAN_POINT('Ctrl Pts',(0.167101404538696,-2.66006869733527,
8.85759444184123));
#404838=CARTESIAN_POINT('Ctrl Pts',(0.166737667185769,-2.66034962329277,
8.85683498915137));
#404839=CARTESIAN_POINT('Ctrl Pts',(0.1666996030405,-2.66037902144606,8.85675551444997));
#404840=CARTESIAN_POINT('Ctrl Pts',(0.166662753168086,-2.66040820147624,
8.85667699793651));
#404841=CARTESIAN_POINT('Ctrl Pts',(0.166627087527525,-2.66043708934255,
8.85659965593547));
#404842=CARTESIAN_POINT('Ctrl Pts',(0.16614567089128,-2.66082701923615,
8.85555568965886));
#404843=CARTESIAN_POINT('Ctrl Pts',(0.165739313269843,-2.66127129211021,
8.85434650606346));
#404844=CARTESIAN_POINT('Ctrl Pts',(0.165401420054767,-2.66176790975638,
8.85297329937117));
#404845=CARTESIAN_POINT('Ctrl Pts',(0.165211375709423,-2.66204722692299,
8.85220095427747));
#404846=CARTESIAN_POINT('Ctrl Pts',(0.165043172113078,-2.66234339408063,
8.85137579139183));
#404847=CARTESIAN_POINT('Ctrl Pts',(0.164897305964679,-2.66265786424426,
8.85049129520029));
#404848=CARTESIAN_POINT('Origin',(0.171134036480688,-2.66555075509437,7.59394543036555));
#404849=CARTESIAN_POINT('Ctrl Pts',(0.176649753622001,-2.66140845730323,
7.59443877723642));
#404850=CARTESIAN_POINT('Ctrl Pts',(0.173561327260517,-2.65651000690964,
7.58783886950016));
#404851=CARTESIAN_POINT('Ctrl Pts',(0.16552683344579,-2.65925337904586,
7.58559994247159));
#404852=CARTESIAN_POINT('Ctrl Pts',(0.193509382518766,-2.68814895428737,
7.56670252222136));
#404853=CARTESIAN_POINT('Ctrl Pts',(0.190425419810198,-2.68325758354531,
7.56004874999029));
#404854=CARTESIAN_POINT('Ctrl Pts',(0.182336414920134,-2.68599699171951,
7.55786368756704));
#404855=CARTESIAN_POINT('Ctrl Pts',(0.210337527743034,-2.71483951606508,
7.53888913333558));
#404856=CARTESIAN_POINT('Ctrl Pts',(0.207235236893097,-2.70991907566719,
7.53222002137275));
#404857=CARTESIAN_POINT('Ctrl Pts',(0.199116189248108,-2.71269099017859,
7.53005029815327));
#404858=CARTESIAN_POINT('Ctrl Pts',(0.227133427809875,-2.74147893487042,
7.51101258149734));
#404859=CARTESIAN_POINT('Ctrl Pts',(0.223993531557828,-2.73649884979426,
7.5043616886572));
#404860=CARTESIAN_POINT('Ctrl Pts',(0.215865257414856,-2.73933409951895,
7.50217374673251));
#404861=CARTESIAN_POINT('',(0.214971506492228,-2.73791238843282,7.50366116523517));
#404862=CARTESIAN_POINT('Ctrl Pts',(0.222557758686742,-2.73422161816808,
7.51860402984325));
#404863=CARTESIAN_POINT('Ctrl Pts',(0.222793285245637,-2.73459517901432,
7.51734760759493));
#404864=CARTESIAN_POINT('Ctrl Pts',(0.22295578856232,-2.7349644763634,7.51608817408572));
#404865=CARTESIAN_POINT('Ctrl Pts',(0.223032672233713,-2.73533403919153,
7.51481005913118));
#404866=CARTESIAN_POINT('Ctrl Pts',(0.223102315300454,-2.73566879803223,
7.51365231206383));
#404867=CARTESIAN_POINT('Ctrl Pts',(0.223102049090871,-2.73600419561941,
7.51247773061042));
#404868=CARTESIAN_POINT('Ctrl Pts',(0.222994953185465,-2.736334399064,7.51129758471022));
#404869=CARTESIAN_POINT('Ctrl Pts',(0.222861845205859,-2.73674480423496,
7.50983079813402));
#404870=CARTESIAN_POINT('Ctrl Pts',(0.222555569253588,-2.73713006948336,
7.50839324291155));
#404871=CARTESIAN_POINT('Ctrl Pts',(0.222009357599801,-2.73744170500765,
7.50715379678855));
#404872=CARTESIAN_POINT('Ctrl Pts',(0.221757023554462,-2.73758567164031,
7.50658120839351));
#404873=CARTESIAN_POINT('Ctrl Pts',(0.221412902846608,-2.73772613760701,
7.50598221009429));
#404874=CARTESIAN_POINT('Ctrl Pts',(0.22097658878432,-2.73783870041343,
7.50545747549612));
#404875=CARTESIAN_POINT('Ctrl Pts',(0.2207437580955,-2.73789876741109,7.50517746087247));
#404876=CARTESIAN_POINT('Ctrl Pts',(0.220482200112825,-2.73795173606975,
7.50491486231392));
#404877=CARTESIAN_POINT('Ctrl Pts',(0.220198510259517,-2.73799456886009,
7.50468370960992));
#404878=CARTESIAN_POINT('Ctrl Pts',(0.219774304443933,-2.7380586173925,
7.50433806340447));
#404879=CARTESIAN_POINT('Ctrl Pts',(0.219287809037178,-2.73810137257825,
7.50405484070984));
#404880=CARTESIAN_POINT('Ctrl Pts',(0.218771725882367,-2.73811924129067,
7.50385766036131));
#404881=CARTESIAN_POINT('Ctrl Pts',(0.218716538810708,-2.73812115207172,
7.50383657498791));
#404882=CARTESIAN_POINT('Ctrl Pts',(0.218661038309198,-2.73812279184612,
7.50381643264937));
#404883=CARTESIAN_POINT('Ctrl Pts',(0.218605282305343,-2.73812416636047,
7.50379723213559));
#404884=CARTESIAN_POINT('Ctrl Pts',(0.218233092740555,-2.73813334169338,
7.50366906242519));
#404885=CARTESIAN_POINT('Ctrl Pts',(0.217841404285952,-2.73813017779315,
7.50358235568538));
#404886=CARTESIAN_POINT('Ctrl Pts',(0.21746393812843,-2.73811805291127,
7.5035341175365));
#404887=CARTESIAN_POINT('Ctrl Pts',(0.216897970346147,-2.73809987302315,
7.50346178989176));
#404888=CARTESIAN_POINT('Ctrl Pts',(0.216289890791844,-2.7380562513047,
7.50346967198527));
#404889=CARTESIAN_POINT('Ctrl Pts',(0.215694262731985,-2.73799506025502,
7.50354272648692));
#404890=CARTESIAN_POINT('Ctrl Pts',(0.215449268582192,-2.7379698911097,
7.50357277531559));
#404891=CARTESIAN_POINT('Ctrl Pts',(0.215206692060812,-2.73794192399818,
7.50361331098761));
#404892=CARTESIAN_POINT('Ctrl Pts',(0.214971506492339,-2.73791238843424,
7.50366116523658));
#404893=CARTESIAN_POINT('',(0.171321629291032,-2.66847266454068,7.57603338622103));
#404894=CARTESIAN_POINT('Origin',(0.171884966568961,-2.67729162937223,7.5848687342763));
#404895=CARTESIAN_POINT('Ctrl Pts',(0.214971506527151,-2.73791238847831,
7.50366116529969));
#404896=CARTESIAN_POINT('Ctrl Pts',(0.200444582347945,-2.71480402911006,
7.52783573079709));
#404897=CARTESIAN_POINT('Ctrl Pts',(0.185895295086789,-2.69165855688567,
7.55196141284069));
#404898=CARTESIAN_POINT('Ctrl Pts',(0.171321630229629,-2.66847266536934,
7.57603338728831));
#404899=CARTESIAN_POINT('Ctrl Pts',(0.176949628854398,-2.66188407944157,
7.59394543036555));
#404900=CARTESIAN_POINT('Ctrl Pts',(0.170212604558692,-2.65119870914281,
7.59394543036555));
#404901=CARTESIAN_POINT('Ctrl Pts',(0.164897305964678,-2.66265786424426,
7.59394543036555));
#404902=CARTESIAN_POINT('Ctrl Pts',(0.175705296970942,-2.65991048600244,
7.58587155981959));
#404903=CARTESIAN_POINT('Ctrl Pts',(0.170587343070376,-2.65703556394579,
7.58685956158228));
#404904=CARTESIAN_POINT('Ctrl Pts',(0.165879044373256,-2.66054135235053,
7.58587155981959));
#404905=CARTESIAN_POINT('Ctrl Pts',(0.172975141359167,-2.66456245493304,
7.57982961904597));
#404906=CARTESIAN_POINT('Ctrl Pts',(0.170972652354739,-2.66303706706671,
7.58148017275036));
#404907=CARTESIAN_POINT('Ctrl Pts',(0.169181666028244,-2.66480600412994,
7.57982961904596));
#404908=CARTESIAN_POINT('Ctrl Pts',(0.17132162923821,-2.66847266371479,
7.57603338509286));
#404909=CARTESIAN_POINT('Ctrl Pts',(0.17132162923821,-2.66847266371479,
7.57603338509286));
#404910=CARTESIAN_POINT('Ctrl Pts',(0.17132162923821,-2.66847266371479,
7.57603338509286));
#404911=CARTESIAN_POINT('Origin',(0.171890661196855,-2.67729126376634,7.58486873427622));
#404912=CARTESIAN_POINT('Ctrl Pts',(0.125292469645955,-2.74804120708308,
7.51098857897448));
#404913=CARTESIAN_POINT('Ctrl Pts',(0.127769759546178,-2.74270046305981,
7.50433767179956));
#404914=CARTESIAN_POINT('Ctrl Pts',(0.13619389345922,-2.74447303714785,
7.50214974420965));
#404915=CARTESIAN_POINT('Ctrl Pts',(0.138547713792469,-2.71946446846798,
7.5388732158917));
#404916=CARTESIAN_POINT('Ctrl Pts',(0.140995321363304,-2.71418771603622,
7.53220407452064));
#404917=CARTESIAN_POINT('Ctrl Pts',(0.149402205571115,-2.71589862744197,
7.53003438070911));
#404918=CARTESIAN_POINT('Ctrl Pts',(0.151828412897425,-2.69083285197316,
7.56669465659229));
#404919=CARTESIAN_POINT('Ctrl Pts',(0.154261555562573,-2.68558728416721,
7.56004085833293));
#404920=CARTESIAN_POINT('Ctrl Pts',(0.162634477916496,-2.68726978866384,
7.55785582193789));
#404921=CARTESIAN_POINT('Ctrl Pts',(0.165133966327907,-2.66214765249215,
7.59443891967696));
#404922=CARTESIAN_POINT('Ctrl Pts',(0.167570636746966,-2.656894479266,7.58783901202978));
#404923=CARTESIAN_POINT('Ctrl Pts',(0.175889981935509,-2.65858789995271,
7.58560008491213));
#404924=CARTESIAN_POINT('',(0.136909871778145,-2.74292411166389,7.50366116523517));
#404925=CARTESIAN_POINT('Ctrl Pts',(0.136909871778163,-2.74292411166427,
7.50366116523554));
#404926=CARTESIAN_POINT('Ctrl Pts',(0.136176261638596,-2.74311372622038,
7.50350835821027));
#404927=CARTESIAN_POINT('Ctrl Pts',(0.135495726955406,-2.74326416077797,
7.50345484955999));
#404928=CARTESIAN_POINT('Ctrl Pts',(0.13484816449329,-2.74338047422534,
7.50349758195598));
#404929=CARTESIAN_POINT('Ctrl Pts',(0.134515916925741,-2.74344015164987,
7.50351950684424));
#404930=CARTESIAN_POINT('Ctrl Pts',(0.134159624361124,-2.74349685631232,
7.50357029184312));
#404931=CARTESIAN_POINT('Ctrl Pts',(0.133814552501086,-2.74354209194315,
7.50365515313923));
#404932=CARTESIAN_POINT('Ctrl Pts',(0.133283692246956,-2.74361168266108,
7.50378570417639));
#404933=CARTESIAN_POINT('Ctrl Pts',(0.132763850166139,-2.74365651668585,
7.50400001621911));
#404934=CARTESIAN_POINT('Ctrl Pts',(0.132294398701274,-2.74367091947915,
7.50428903009634));
#404935=CARTESIAN_POINT('Ctrl Pts',(0.132242293200415,-2.74367251807839,
7.50432110841318));
#404936=CARTESIAN_POINT('Ctrl Pts',(0.132190784057866,-2.74367375975199,
7.50435406373354));
#404937=CARTESIAN_POINT('Ctrl Pts',(0.132139906905781,-2.74367464975632,
7.50438785222352));
#404938=CARTESIAN_POINT('Ctrl Pts',(0.131829277437644,-2.74368008366058,
7.50459414719561));
#404939=CARTESIAN_POINT('Ctrl Pts',(0.131537252052987,-2.74367197926943,
7.50483629897752));
#404940=CARTESIAN_POINT('Ctrl Pts',(0.131274981649372,-2.74365196258472,
7.5050991045531));
#404941=CARTESIAN_POINT('Ctrl Pts',(0.130696386796431,-2.74360780376776,
7.50567888004914));
#404942=CARTESIAN_POINT('Ctrl Pts',(0.130239766303518,-2.74350444791973,
7.50637912803144));
#404943=CARTESIAN_POINT('Ctrl Pts',(0.129890662582497,-2.74336921529871,
7.50710440483569));
#404944=CARTESIAN_POINT('Ctrl Pts',(0.129805055419423,-2.74333605357529,
7.50728225710685));
#404945=CARTESIAN_POINT('Ctrl Pts',(0.129724156641004,-2.74330045095875,
7.50746498566954));
#404946=CARTESIAN_POINT('Ctrl Pts',(0.129649686880133,-2.74326361983096,
7.50764697238949));
#404947=CARTESIAN_POINT('Ctrl Pts',(0.129249357940325,-2.74306562582414,
7.50862528291181));
#404948=CARTESIAN_POINT('Ctrl Pts',(0.128996641605847,-2.74281786641564,
7.5096585683742));
#404949=CARTESIAN_POINT('Ctrl Pts',(0.128834110610838,-2.74255347021814,
7.510679598732));
#404950=CARTESIAN_POINT('Ctrl Pts',(0.128744669599277,-2.74240797265716,
7.51124147302577));
#404951=CARTESIAN_POINT('Ctrl Pts',(0.128682887795632,-2.74225717394986,
7.51180065547252));
#404952=CARTESIAN_POINT('Ctrl Pts',(0.128641559193309,-2.74210525799208,
7.512351757165));
#404953=CARTESIAN_POINT('Ctrl Pts',(0.128498752408923,-2.74158032784183,
7.51425603304536));
#404954=CARTESIAN_POINT('Ctrl Pts',(0.128588977115428,-2.740977877902,7.51626900505181));
#404955=CARTESIAN_POINT('Ctrl Pts',(0.128867104965898,-2.7403379843463,
7.51827788969244));
#404956=CARTESIAN_POINT('Ctrl Pts',(0.128882157770753,-2.74030335209783,
7.51838661432546));
#404957=CARTESIAN_POINT('Ctrl Pts',(0.128897769997591,-2.74026860594205,
7.51849533314857));
#404958=CARTESIAN_POINT('Ctrl Pts',(0.128913937383393,-2.74023375097046,
7.51860402984325));
#404959=CARTESIAN_POINT('Ctrl Pts',(0.171321628465944,-2.66847266548377,
7.57603338728985));
#404960=CARTESIAN_POINT('Ctrl Pts',(0.159832559191517,-2.69333184005413,
7.55196141284922));
#404961=CARTESIAN_POINT('Ctrl Pts',(0.148362498662249,-2.71814780985154,
7.52783573083105));
#404962=CARTESIAN_POINT('Ctrl Pts',(0.136909871748486,-2.74292411171511,
7.50366116530176));
#404963=CARTESIAN_POINT('Origin',(5.91995423665314E-17,-9.22080657369148E-16,
7.49482233047033));
#404964=CARTESIAN_POINT('Origin',(0.214279640797806,-2.72910067339766,7.49482233047033));
#404965=CARTESIAN_POINT('Origin',(0.,0.,7.50366116523517));
#404966=CARTESIAN_POINT('Origin',(0.13646924015651,-2.73409626686609,7.49482233047033));
#404967=CARTESIAN_POINT('Ctrl Pts',(0.222557194605735,-2.73422072341404,
7.51860402984325));
#404968=CARTESIAN_POINT('Ctrl Pts',(0.226614772381166,-2.74065751987086,
7.51860402984325));
#404969=CARTESIAN_POINT('Ctrl Pts',(0.234196090687522,-2.74000952390803,
7.51860402984325));
#404970=CARTESIAN_POINT('Ctrl Pts',(0.224063801999073,-2.7366107491878,
7.51041458714367));
#404971=CARTESIAN_POINT('Ctrl Pts',(0.228410872679967,-2.74050399234173,
7.51004642900443));
#404972=CARTESIAN_POINT('Ctrl Pts',(0.23419818152509,-2.74000934519844,
7.50729136483012));
#404973=CARTESIAN_POINT('Ctrl Pts',(0.22234652916971,-2.73884115525596,
7.50215815450136));
#404974=CARTESIAN_POINT('Ctrl Pts',(0.224753845205989,-2.74081672959849,
7.49877163671529));
#404975=CARTESIAN_POINT('Ctrl Pts',(0.22819346670093,-2.74054667855528,
7.49481588533168));
#404976=CARTESIAN_POINT('Ctrl Pts',(0.214971463399589,-2.73791183960396,
7.50366171572174));
#404977=CARTESIAN_POINT('Ctrl Pts',(0.215258086645813,-2.74156232030818,
7.50000045605858));
#404978=CARTESIAN_POINT('Ctrl Pts',(0.215258086645937,-2.74156232030817,
7.49482233047317));
#404979=CARTESIAN_POINT('Origin',(0.233131563002578,-2.72755493516299,7.51860402984325));
#404980=CARTESIAN_POINT('Origin',(0.233131563002578,-2.72755493516299,9.));
#404981=CARTESIAN_POINT('Origin',(0.233131563002578,-2.72755493516299,8.75721825406948));
#404982=CARTESIAN_POINT('Ctrl Pts',(0.213651009822431,-2.72009486320776,
8.78942910404912));
#404983=CARTESIAN_POINT('Ctrl Pts',(0.21660588741383,-2.72481938721781,
8.79672699501691));
#404984=CARTESIAN_POINT('Ctrl Pts',(0.22491413159174,-2.72155647982373,
8.79893251111267));
#404985=CARTESIAN_POINT('Ctrl Pts',(0.219514666098752,-2.7293950220136,
8.78111911759582));
#404986=CARTESIAN_POINT('Ctrl Pts',(0.223024018852947,-2.73499205277749,
8.78644465894813));
#404987=CARTESIAN_POINT('Ctrl Pts',(0.231029453604124,-2.73371591555135,
8.78817647674133));
#404988=CARTESIAN_POINT('Ctrl Pts',(0.22316903657846,-2.73519110279413,
8.7678092393203));
#404989=CARTESIAN_POINT('Ctrl Pts',(0.22731599665726,-2.74179545430472,
8.76988516158374));
#404990=CARTESIAN_POINT('Ctrl Pts',(0.234858960007768,-2.74130547033627,
8.77093053738832));
#404991=CARTESIAN_POINT('Ctrl Pts',(0.222456484349966,-2.73406094636595,
8.75371302330492));
#404992=CARTESIAN_POINT('Ctrl Pts',(0.226501019435815,-2.74050361175437,
8.75300828287559));
#404993=CARTESIAN_POINT('Ctrl Pts',(0.23411245922325,-2.73982499279172,
8.75267964240738));
#404994=CARTESIAN_POINT('Origin',(0.22565283473727,-2.71569317285207,8.78727029226991));
#404995=CARTESIAN_POINT('Ctrl Pts',(0.176949628854398,-2.66188407944157,
8.85049129520029));
#404996=CARTESIAN_POINT('Ctrl Pts',(0.180064098225814,-2.66682383578754,
8.85711686593484));
#404997=CARTESIAN_POINT('Ctrl Pts',(0.18814612056788,-2.66403427005498,
8.85933012996512));
#404998=CARTESIAN_POINT('Ctrl Pts',(0.189677921384504,-2.68207200113894,
8.82945683644723));
#404999=CARTESIAN_POINT('Ctrl Pts',(0.192818242734749,-2.68705276044921,
8.8360746990239));
#405000=CARTESIAN_POINT('Ctrl Pts',(0.200911757808383,-2.68421955444712,
8.8382956714852));
#405001=CARTESIAN_POINT('Ctrl Pts',(0.20238724136817,-2.70222983111105,
8.80838214965002));
#405002=CARTESIAN_POINT('Ctrl Pts',(0.205539955892651,-2.70723024682302,
8.81501364461987));
#405003=CARTESIAN_POINT('Ctrl Pts',(0.21365746521294,-2.70437457614343,
8.81722098428721));
#405004=CARTESIAN_POINT('Ctrl Pts',(0.215079030421435,-2.72235985585717,
8.78727029226991));
#405005=CARTESIAN_POINT('Ctrl Pts',(0.218232268622154,-2.72736110215464,
8.79393457792714));
#405006=CARTESIAN_POINT('Ctrl Pts',(0.226384750345669,-2.7245016516959,
8.79610912703474));
#405007=CARTESIAN_POINT('Origin',(0.187523433170234,-2.65521739643647,8.85049129520029));
#405008=CARTESIAN_POINT('Ctrl Pts',(0.164897305964679,-2.66265786424426,
8.85049129520029));
#405009=CARTESIAN_POINT('Ctrl Pts',(0.162440088364686,-2.66795533476228,
8.85711686593484));
#405010=CARTESIAN_POINT('Ctrl Pts',(0.154067697566117,-2.6662221774036,
8.85933012996512));
#405011=CARTESIAN_POINT('Ctrl Pts',(0.167071170905082,-2.65797126854675,
8.86332496987232));
#405012=CARTESIAN_POINT('Ctrl Pts',(0.162486551694914,-2.65854846961614,
8.86648636486737));
#405013=CARTESIAN_POINT('Ctrl Pts',(0.160164715441418,-2.65311844398962,
8.87206031107457));
#405014=CARTESIAN_POINT('Ctrl Pts',(0.174175579449892,-2.65748425188965,
8.86341338519876));
#405015=CARTESIAN_POINT('Ctrl Pts',(0.178809323360593,-2.65744080071698,
8.86654584966059));
#405016=CARTESIAN_POINT('Ctrl Pts',(0.180366172242112,-2.65172237660299,
8.87215952290714));
#405017=CARTESIAN_POINT('Ctrl Pts',(0.176949628854398,-2.66188407944157,
8.85049129520029));
#405018=CARTESIAN_POINT('Ctrl Pts',(0.180064098225814,-2.66682383578754,
8.85711686593484));
#405019=CARTESIAN_POINT('Ctrl Pts',(0.188146120567879,-2.66403427005498,
8.85933012996512));
#405020=CARTESIAN_POINT('Origin',(0.153557795935569,-2.65739806269859,8.85049129520029));
#405021=CARTESIAN_POINT('Ctrl Pts',(0.134814416896129,-2.72751301502058,
8.78727029226991));
#405022=CARTESIAN_POINT('Ctrl Pts',(0.132326611918855,-2.7328764283063,
8.79393457792714));
#405023=CARTESIAN_POINT('Ctrl Pts',(0.123875403548956,-2.73108297011979,
8.79610912703474));
#405024=CARTESIAN_POINT('Ctrl Pts',(0.14482783610753,-2.70592526753854,
8.80838214965003));
#405025=CARTESIAN_POINT('Ctrl Pts',(0.142340444294203,-2.71128779009168,
8.81501364461993));
#405026=CARTESIAN_POINT('Ctrl Pts',(0.133924404552021,-2.70949360848066,
8.81722098428721));
#405027=CARTESIAN_POINT('Ctrl Pts',(0.15485508666727,-2.68430770130539,
8.82945683644722));
#405028=CARTESIAN_POINT('Ctrl Pts',(0.152377472675528,-2.68964914403163,
8.83607469902389));
#405029=CARTESIAN_POINT('Ctrl Pts',(0.143988102906756,-2.68787417434732,
8.8382956714852));
#405030=CARTESIAN_POINT('Ctrl Pts',(0.164897305964678,-2.66265786424426,
8.85049129520029));
#405031=CARTESIAN_POINT('Ctrl Pts',(0.162440088364686,-2.66795533476228,
8.85711686593484));
#405032=CARTESIAN_POINT('Ctrl Pts',(0.154067697566117,-2.6662221774036,
8.85933012996512));
#405033=CARTESIAN_POINT('Origin',(0.123474906867021,-2.72225321347492,8.78727029226991));
#405034=CARTESIAN_POINT('Ctrl Pts',(0.128991833512721,-2.74006577228906,
8.75374538247847));
#405035=CARTESIAN_POINT('Ctrl Pts',(0.125806215729252,-2.74696477350121,
8.75304829418601));
#405036=CARTESIAN_POINT('Ctrl Pts',(0.118178814785805,-2.74727038445809,
8.75272238421917));
#405037=CARTESIAN_POINT('Ctrl Pts',(0.12843640572388,-2.74126320992229,
8.76769408445021));
#405038=CARTESIAN_POINT('Ctrl Pts',(0.12516999712376,-2.74833553131129,
8.7697431809397));
#405039=CARTESIAN_POINT('Ctrl Pts',(0.117634307816553,-2.74881692921888,
8.7707786988043));
#405040=CARTESIAN_POINT('Ctrl Pts',(0.131283212176553,-2.7351258267558,
8.78108014887987));
#405041=CARTESIAN_POINT('Ctrl Pts',(0.12851849783378,-2.74112095743854,
8.78639403366323));
#405042=CARTESIAN_POINT('Ctrl Pts',(0.120426966568877,-2.74089915230321,
8.78812224174741));
#405043=CARTESIAN_POINT('Ctrl Pts',(0.135948499481621,-2.72506801057236,
8.78944554828686));
#405044=CARTESIAN_POINT('Ctrl Pts',(0.13362358397994,-2.73012282862319,
8.79673892988687));
#405045=CARTESIAN_POINT('Ctrl Pts',(0.124974904203878,-2.72795398274399,
8.79894799272499));
#405046=CARTESIAN_POINT('Origin',(0.117574427354288,-2.73497394942481,8.75721825406948));
#405047=CARTESIAN_POINT('Origin',(0.117574427354288,-2.73497394942481,9.));
#405048=CARTESIAN_POINT('Origin',(0.117574427354288,-2.73497394942481,7.51860402984325));
#405049=CARTESIAN_POINT('Ctrl Pts',(0.136909832561502,-2.74292332597825,
7.50366195182966));
#405050=CARTESIAN_POINT('Ctrl Pts',(0.137092387371697,-2.74658072470567,
7.50000065167735));
#405051=CARTESIAN_POINT('Ctrl Pts',(0.13709238737158,-2.74658072470568,
7.49482233047108));
#405052=CARTESIAN_POINT('Ctrl Pts',(0.129707514805738,-2.74478891396914,
7.50215800491336));
#405053=CARTESIAN_POINT('Ctrl Pts',(0.127570877920035,-2.74705595609338,
7.49877273257266));
#405054=CARTESIAN_POINT('Ctrl Pts',(0.124123047921434,-2.74722807422352,
7.49481816995647));
#405055=CARTESIAN_POINT('Ctrl Pts',(0.127728229063037,-2.74279080378928,
7.51043025814043));
#405056=CARTESIAN_POINT('Ctrl Pts',(0.12391537177406,-2.74721289337237,
7.51006209594515));
#405057=CARTESIAN_POINT('Ctrl Pts',(0.118108767356082,-2.74746252368982,
7.50731281821701));
#405058=CARTESIAN_POINT('Ctrl Pts',(0.128914573276759,-2.74023237984243,
7.51860402984326));
#405059=CARTESIAN_POINT('Ctrl Pts',(0.125713547171854,-2.74713560005233,
7.51860402984326));
#405060=CARTESIAN_POINT('Ctrl Pts',(0.11811129688558,-2.74746241494729,
7.51860402984327));
#405061=CARTESIAN_POINT('Origin',(0.,0.,7.5));
#405062=CARTESIAN_POINT('Origin',(0.335155581859898,-2.64662214142562,7.5));
#405063=CARTESIAN_POINT('',(0.335155581859898,-2.64662214142562,7.59394543036555));
#405064=CARTESIAN_POINT('',(0.335155581859898,-2.64662214142562,8.85049129520029));
#405065=CARTESIAN_POINT('',(0.335155581859898,-2.64662214142562,7.5));
#405066=CARTESIAN_POINT('',(0.309289785090442,-2.71327145765926,8.78727029226991));
#405067=CARTESIAN_POINT('Ctrl Pts',(0.335155581859898,-2.64662214142562,
8.85049129520029));
#405068=CARTESIAN_POINT('Ctrl Pts',(0.326521116789889,-2.66887087391543,
8.82945686509571));
#405069=CARTESIAN_POINT('Ctrl Pts',(0.317899487896271,-2.69108653097411,
8.80838212259896));
#405070=CARTESIAN_POINT('Ctrl Pts',(0.309289785090442,-2.71327145765926,
8.78727029226991));
#405071=CARTESIAN_POINT('',(0.304216449096319,-2.72634410251322,8.75721825406948));
#405072=CARTESIAN_POINT('Origin',(0.319484065186767,-2.68700405222726,8.75937679713114));
#405073=CARTESIAN_POINT('',(0.304216449096319,-2.72634410251322,7.51860402984325));
#405074=CARTESIAN_POINT('',(0.304216449096319,-2.72634410251322,7.5));
#405075=CARTESIAN_POINT('Ctrl Pts',(0.304216449096319,-2.72634410251322,
7.51860402984325));
#405076=CARTESIAN_POINT('Ctrl Pts',(0.308200765466706,-2.71607757316128,
7.52834476460825));
#405077=CARTESIAN_POINT('Ctrl Pts',(0.312187668397793,-2.70580437892665,
7.53807742314407));
#405078=CARTESIAN_POINT('Ctrl Pts',(0.316177244736788,-2.69552429602699,
7.54780169004675));
#405079=CARTESIAN_POINT('Ctrl Pts',(0.322496518039553,-2.67924120030501,
7.5632044032688));
#405080=CARTESIAN_POINT('Ctrl Pts',(0.328822506613121,-2.66294080110644,
7.57858609112103));
#405081=CARTESIAN_POINT('Ctrl Pts',(0.335155581859899,-2.64662214142562,
7.59394543036555));
#405082=CARTESIAN_POINT('Origin',(0.508403499682117,-2.86782650745936,7.5));
#405083=CARTESIAN_POINT('',(0.397282670454326,-2.71434454205174,8.75721825406948));
#405084=CARTESIAN_POINT('',(0.389059322317711,-2.70298631476879,8.78727029226991));
#405085=CARTESIAN_POINT('Origin',(0.368185397592234,-2.67415489751875,8.7565864062112));
#405086=CARTESIAN_POINT('',(0.347133565397108,-2.64507775146798,8.85049129520029));
#405087=CARTESIAN_POINT('Ctrl Pts',(0.389059322317711,-2.70298631476879,
8.78727029226991));
#405088=CARTESIAN_POINT('Ctrl Pts',(0.375103892673955,-2.68371083973214,
8.80838212259895));
#405089=CARTESIAN_POINT('Ctrl Pts',(0.361129132086633,-2.66440866446988,
8.82945686509571));
#405090=CARTESIAN_POINT('Ctrl Pts',(0.347133565397108,-2.64507775146798,
8.85049129520029));
#405091=CARTESIAN_POINT('',(0.347133565397108,-2.64507775146798,7.59394543036555));
#405092=CARTESIAN_POINT('',(0.347133565397108,-2.64507775146798,7.5));
#405093=CARTESIAN_POINT('',(0.397282670454326,-2.71434454205174,7.51860402984325));
#405094=CARTESIAN_POINT('Ctrl Pts',(0.347133565397108,-2.64507775146798,
7.59394543036555));
#405095=CARTESIAN_POINT('Ctrl Pts',(0.357398819381853,-2.65925629358232,
7.57858609112103));
#405096=CARTESIAN_POINT('Ctrl Pts',(0.367652586608856,-2.67341896999297,
7.56320440326857));
#405097=CARTESIAN_POINT('Ctrl Pts',(0.377895469082877,-2.68756661219899,
7.54780169004651));
#405098=CARTESIAN_POINT('Ctrl Pts',(0.384362155931758,-2.6964985092532,
7.53807742314383));
#405099=CARTESIAN_POINT('Ctrl Pts',(0.390824509465566,-2.70542442105946,
7.52834476460825));
#405100=CARTESIAN_POINT('Ctrl Pts',(0.397282670454325,-2.71434454205173,
7.51860402984325));
#405101=CARTESIAN_POINT('',(0.397282670454326,-2.71434454205174,7.5));
#405102=CARTESIAN_POINT('Origin',(0.341564846497323,-2.6491094998251,7.5));
#405103=CARTESIAN_POINT('Ctrl Pts',(0.347133565397107,-2.64507775146798,
8.85049129520029));
#405104=CARTESIAN_POINT('Ctrl Pts',(0.34701999529408,-2.64492088652424,
8.85097269580138));
#405105=CARTESIAN_POINT('Ctrl Pts',(0.346901044882032,-2.64477093347822,
8.85143669361005));
#405106=CARTESIAN_POINT('Ctrl Pts',(0.34677055192744,-2.64462153081528,
8.8519052845931));
#405107=CARTESIAN_POINT('Ctrl Pts',(0.34651531598382,-2.64432930868135,
8.85282181883899));
#405108=CARTESIAN_POINT('Ctrl Pts',(0.346222339439965,-2.64404683890338,
8.85372622499636));
#405109=CARTESIAN_POINT('Ctrl Pts',(0.345876323146632,-2.64378078895684,
8.85462257735071));
#405110=CARTESIAN_POINT('Ctrl Pts',(0.345589072709243,-2.64355992374042,
8.85536669723986));
#405111=CARTESIAN_POINT('Ctrl Pts',(0.345265222470739,-2.6433502992131,
8.85610498449051));
#405112=CARTESIAN_POINT('Ctrl Pts',(0.344891643286429,-2.64316243027106,
8.85681338218371));
#405113=CARTESIAN_POINT('Ctrl Pts',(0.344552619589951,-2.6429919389111,
8.85745625420284));
#405114=CARTESIAN_POINT('Ctrl Pts',(0.344168657352627,-2.6428366912356,
8.85808743050666));
#405115=CARTESIAN_POINT('Ctrl Pts',(0.343718641537324,-2.64271597458123,
8.8586680450841));
#405116=CARTESIAN_POINT('Ctrl Pts',(0.343511013995289,-2.64266027853371,
8.85893592806396));
#405117=CARTESIAN_POINT('Ctrl Pts',(0.343289167465176,-2.64261211674724,
8.85919241173848));
#405118=CARTESIAN_POINT('Ctrl Pts',(0.343050165639986,-2.64257472651662,
8.85943017985534));
#405119=CARTESIAN_POINT('Ctrl Pts',(0.342727442423867,-2.6425242386366,
8.8597512372));
#405120=CARTESIAN_POINT('Ctrl Pts',(0.342365126816615,-2.64249273833371,
8.86004599534705));
#405121=CARTESIAN_POINT('Ctrl Pts',(0.34196666980205,-2.64249098002396,
8.86026130871721));
#405122=CARTESIAN_POINT('Ctrl Pts',(0.341820783455326,-2.64249033625719,
8.86034014101235));
#405123=CARTESIAN_POINT('Ctrl Pts',(0.341667861040604,-2.64249365740532,
8.86040910639692));
#405124=CARTESIAN_POINT('Ctrl Pts',(0.341512076146937,-2.64250118928493,
8.86046313645506));
#405125=CARTESIAN_POINT('Ctrl Pts',(0.341268975125058,-2.64251294271998,
8.86054744990829));
#405126=CARTESIAN_POINT('Ctrl Pts',(0.341012274757796,-2.6425354175532,
8.86059655985668));
#405127=CARTESIAN_POINT('Ctrl Pts',(0.340758412469709,-2.6425668805641,
8.86059725258815));
#405128=CARTESIAN_POINT('Ctrl Pts',(0.340503963658316,-2.64259841626712,
8.86059794692011));
#405129=CARTESIAN_POINT('Ctrl Pts',(0.340249870963067,-2.64264196806059,
8.86056369958366));
#405130=CARTESIAN_POINT('Ctrl Pts',(0.340009356994018,-2.64269145159793,
8.86048590497774));
#405131=CARTESIAN_POINT('Ctrl Pts',(0.33994659000906,-2.64270436532787,
8.86046560290182));
#405132=CARTESIAN_POINT('Ctrl Pts',(0.339883949500272,-2.64271793976287,
8.86044257503091));
#405133=CARTESIAN_POINT('Ctrl Pts',(0.339823364159044,-2.64273172336011,
8.86041778462583));
#405134=CARTESIAN_POINT('Ctrl Pts',(0.339415699992718,-2.64282446986554,
8.860250975962));
#405135=CARTESIAN_POINT('Ctrl Pts',(0.339046456499758,-2.64293945540863,
8.8599848982295));
#405136=CARTESIAN_POINT('Ctrl Pts',(0.338723891841634,-2.64306523453273,
8.85968173251461));
#405137=CARTESIAN_POINT('Ctrl Pts',(0.338553273618238,-2.6431317644831,
8.85952137522076));
#405138=CARTESIAN_POINT('Ctrl Pts',(0.338392357053016,-2.64320241876617,
8.85934740853961));
#405139=CARTESIAN_POINT('Ctrl Pts',(0.338242786451452,-2.64327477760985,
8.8591675900182));
#405140=CARTESIAN_POINT('Ctrl Pts',(0.337642182740921,-2.64356533597861,
8.85844552518695));
#405141=CARTESIAN_POINT('Ctrl Pts',(0.337189263383592,-2.64389707715724,
8.85759444184125));
#405142=CARTESIAN_POINT('Ctrl Pts',(0.336844272355963,-2.64420073065445,
8.85683498915139));
#405143=CARTESIAN_POINT('Ctrl Pts',(0.336808169963707,-2.64423250718423,
8.85675551444999));
#405144=CARTESIAN_POINT('Ctrl Pts',(0.336773265374257,-2.64426398824035,
8.85667699793651));
#405145=CARTESIAN_POINT('Ctrl Pts',(0.336739523864526,-2.64429510185888,
8.85659965593547));
#405146=CARTESIAN_POINT('Ctrl Pts',(0.336284079244452,-2.64471507506948,
8.85555568965886));
#405147=CARTESIAN_POINT('Ctrl Pts',(0.335907021189103,-2.64518447055947,
8.85434650606346));
#405148=CARTESIAN_POINT('Ctrl Pts',(0.335601640613713,-2.64570171674404,
8.85297329937118));
#405149=CARTESIAN_POINT('Ctrl Pts',(0.335429882647167,-2.64599263620658,
8.85220095427747));
#405150=CARTESIAN_POINT('Ctrl Pts',(0.335281000138092,-2.64629897169846,
8.85137579139184));
#405151=CARTESIAN_POINT('Ctrl Pts',(0.335155581859898,-2.64662214142562,
8.85049129520029));
#405152=CARTESIAN_POINT('Origin',(0.341564846497323,-2.6491094998251,7.59394543036555));
#405153=CARTESIAN_POINT('Ctrl Pts',(0.346803833075505,-2.64462231961843,
7.59443877723642));
#405154=CARTESIAN_POINT('Ctrl Pts',(0.343407907422933,-2.63993180977292,
7.58783886950016));
#405155=CARTESIAN_POINT('Ctrl Pts',(0.335565689793701,-2.64318431714299,
7.58559994247159));
#405156=CARTESIAN_POINT('Ctrl Pts',(0.365342091580689,-2.67022767525142,
7.56670252222137));
#405157=CARTESIAN_POINT('Ctrl Pts',(0.361951074004762,-2.66554394452431,
7.56004874999028));
#405158=CARTESIAN_POINT('Ctrl Pts',(0.354054203327156,-2.66879598861332,
7.55786368756704));
#405159=CARTESIAN_POINT('Ctrl Pts',(0.38384573174027,-2.69578521544099,
7.53888913333556));
#405160=CARTESIAN_POINT('Ctrl Pts',(0.380434561180908,-2.69107364907284,
7.53222002137276));
#405161=CARTESIAN_POINT('Ctrl Pts',(0.372509792162587,-2.69436005755723,
7.53005029815326));
#405162=CARTESIAN_POINT('Ctrl Pts',(0.402313916252095,-2.72129378369128,
7.51101258149734));
#405163=CARTESIAN_POINT('Ctrl Pts',(0.398861396107298,-2.7165251045776,
7.5043616886572));
#405164=CARTESIAN_POINT('Ctrl Pts',(0.390931477448869,-2.71987530929006,
7.50217374673251));
#405165=CARTESIAN_POINT('',(0.389948473491329,-2.71851378208006,7.50366116523517));
#405166=CARTESIAN_POINT('Ctrl Pts',(0.397282670454326,-2.71434454205174,
7.51860402984325));
#405167=CARTESIAN_POINT('Ctrl Pts',(0.397541647224239,-2.7147022451387,
7.51734760759494));
#405168=CARTESIAN_POINT('Ctrl Pts',(0.397727477622823,-2.71506037210353,
7.51608817408573));
#405169=CARTESIAN_POINT('Ctrl Pts',(0.397827881300162,-2.71542424967145,
7.5148100591312));
#405170=CARTESIAN_POINT('Ctrl Pts',(0.39791882935032,-2.7157538586676,7.51365231206384));
#405171=CARTESIAN_POINT('Ctrl Pts',(0.397940052684887,-2.71608858420057,
7.51247773061043));
#405172=CARTESIAN_POINT('Ctrl Pts',(0.397854333026837,-2.71642497086499,
7.51129758471022));
#405173=CARTESIAN_POINT('Ctrl Pts',(0.397747793281437,-2.71684306107205,
7.50983079813402));
#405174=CARTESIAN_POINT('Ctrl Pts',(0.397466830635174,-2.71724715791932,
7.50839324291155));
#405175=CARTESIAN_POINT('Ctrl Pts',(0.396941707788404,-2.71759314905581,
7.50715379678855));
#405176=CARTESIAN_POINT('Ctrl Pts',(0.396699116164248,-2.71775298699137,
7.5065812083935));
#405177=CARTESIAN_POINT('Ctrl Pts',(0.39636470217468,-2.71791521224513,
7.50598221009429));
#405178=CARTESIAN_POINT('Ctrl Pts',(0.395936496490198,-2.71805549851715,
7.50545747549611));
#405179=CARTESIAN_POINT('Ctrl Pts',(0.395707992682752,-2.71813035961417,
7.50517746087247));
#405180=CARTESIAN_POINT('Ctrl Pts',(0.395450365812616,-2.71819997752052,
7.50491486231392));
#405181=CARTESIAN_POINT('Ctrl Pts',(0.395170003136838,-2.71826089837762,
7.50468370960992));
#405182=CARTESIAN_POINT('Ctrl Pts',(0.394750772501156,-2.71835199427537,
7.50433806340446));
#405183=CARTESIAN_POINT('Ctrl Pts',(0.394268015985544,-2.71842583148373,
7.50405484070983));
#405184=CARTESIAN_POINT('Ctrl Pts',(0.393754138031257,-2.71847672904422,
7.5038576603613));
#405185=CARTESIAN_POINT('Ctrl Pts',(0.39369918677152,-2.71848217174719,
7.50383657498791));
#405186=CARTESIAN_POINT('Ctrl Pts',(0.393643905362452,-2.71848736408184,
7.50381643264937));
#405187=CARTESIAN_POINT('Ctrl Pts',(0.393588351980726,-2.71849230807153,
7.50379723213559));
#405188=CARTESIAN_POINT('Ctrl Pts',(0.393217514984914,-2.71852531082003,
7.50366906242518));
#405189=CARTESIAN_POINT('Ctrl Pts',(0.392826428584466,-2.71854724898582,
7.50358235568538));
#405190=CARTESIAN_POINT('Ctrl Pts',(0.392448961127797,-2.71855933335556,
7.5035341175365));
#405191=CARTESIAN_POINT('Ctrl Pts',(0.391882991397589,-2.71857745250028,
7.50346178989176));
#405192=CARTESIAN_POINT('Ctrl Pts',(0.391273366354846,-2.71857288019814,
7.50346967198527));
#405193=CARTESIAN_POINT('Ctrl Pts',(0.390675041552701,-2.71854997689285,
7.50354272648692));
#405194=CARTESIAN_POINT('Ctrl Pts',(0.39042893817699,-2.71854055628932,
7.50357277531559));
#405195=CARTESIAN_POINT('Ctrl Pts',(0.390185068196105,-2.71852818857031,
7.50361331098761));
#405196=CARTESIAN_POINT('Ctrl Pts',(0.38994847349153,-2.71851378208147,
7.50366116523658));
#405197=CARTESIAN_POINT('',(0.341939261259106,-2.65201338678245,7.57603338622103));
#405198=CARTESIAN_POINT('Origin',(0.343066474116874,-2.66077813896213,7.58486873427628));
#405199=CARTESIAN_POINT('Ctrl Pts',(0.389948473529094,-2.71851378212322,
7.50366116529969));
#405200=CARTESIAN_POINT('Ctrl Pts',(0.373970838805498,-2.69638364458546,
7.52783573079709));
#405201=CARTESIAN_POINT('Ctrl Pts',(0.357968509118452,-2.67421790325148,
7.55196141284068));
#405202=CARTESIAN_POINT('Ctrl Pts',(0.341939262248866,-2.65201338754928,
7.57603338728831));
#405203=CARTESIAN_POINT('Ctrl Pts',(0.347594250863872,-2.64601386279728,
7.59639677331372));
#405204=CARTESIAN_POINT('Ctrl Pts',(0.339350823778441,-2.62970074459047,
7.59959882295463));
#405205=CARTESIAN_POINT('Ctrl Pts',(0.334988019337696,-2.64746798269907,
7.59642833564546));
#405206=CARTESIAN_POINT('Ctrl Pts',(0.346417486467366,-2.64229494768145,
7.58707626057424));
#405207=CARTESIAN_POINT('Ctrl Pts',(0.340385787866657,-2.63920773161741,
7.58809943920598));
#405208=CARTESIAN_POINT('Ctrl Pts',(0.335273897319247,-2.64363299723925,
7.58710240504252));
#405209=CARTESIAN_POINT('Ctrl Pts',(0.343548093433333,-2.6476514592214,
7.5801537675693));
#405210=CARTESIAN_POINT('Ctrl Pts',(0.341200555278531,-2.64603333190638,
7.5820588065976));
#405211=CARTESIAN_POINT('Ctrl Pts',(0.33933172203006,-2.64813916602317,
7.58020924244129));
#405212=CARTESIAN_POINT('Ctrl Pts',(0.341939261153479,-2.65201338596165,
7.57603338509286));
#405213=CARTESIAN_POINT('Ctrl Pts',(0.341939261153479,-2.65201338596165,
7.57603338509286));
#405214=CARTESIAN_POINT('Ctrl Pts',(0.341939261153479,-2.65201338596165,
7.57603338509286));
#405215=CARTESIAN_POINT('Origin',(0.343072133619864,-2.66077740925008,7.58486873427621));
#405216=CARTESIAN_POINT('Ctrl Pts',(0.30110264748337,-2.73436754560449,
7.51098857897448));
#405217=CARTESIAN_POINT('Ctrl Pts',(0.303232664881372,-2.72887905420375,
7.50433767179956));
#405218=CARTESIAN_POINT('Ctrl Pts',(0.311753059719557,-2.73010825023526,
7.50214974420965));
#405219=CARTESIAN_POINT('Ctrl Pts',(0.312499739379771,-2.70500025455533,
7.53887321589168));
#405220=CARTESIAN_POINT('Ctrl Pts',(0.314604235389235,-2.69957752502187,
7.5322040745206));
#405221=CARTESIAN_POINT('Ctrl Pts',(0.323103465221949,-2.70074629025612,
7.53003438070912));
#405222=CARTESIAN_POINT('Ctrl Pts',(0.323918717896826,-2.67557656747421,
7.5666946565923));
#405223=CARTESIAN_POINT('Ctrl Pts',(0.326010776726132,-2.67018588526411,
7.56004085833297));
#405224=CARTESIAN_POINT('Ctrl Pts',(0.334474294446332,-2.67132847789769,
7.55785582193789));
#405225=CARTESIAN_POINT('Ctrl Pts',(0.335359066599835,-2.64609781507675,
7.59443891967696));
#405226=CARTESIAN_POINT('Ctrl Pts',(0.33745415865399,-2.64069931704862,
7.58783901202978));
#405227=CARTESIAN_POINT('Ctrl Pts',(0.345864908691513,-2.64185623614459,
7.58560008491213));
#405228=CARTESIAN_POINT('',(0.312368326987746,-2.72851663429643,7.50366116523517));
#405229=CARTESIAN_POINT('Ctrl Pts',(0.312368326987789,-2.7285166342968,
7.50366116523554));
#405230=CARTESIAN_POINT('Ctrl Pts',(0.311648372775254,-2.7287528618325,
7.50350835821027));
#405231=CARTESIAN_POINT('Ctrl Pts',(0.310978874698756,-2.72894658931301,
7.50345484956));
#405232=CARTESIAN_POINT('Ctrl Pts',(0.310340094951329,-2.72910415325133,
7.50349758195598));
#405233=CARTESIAN_POINT('Ctrl Pts',(0.310012353567758,-2.72918499523693,
7.50351950684424));
#405234=CARTESIAN_POINT('Ctrl Pts',(0.309660426124625,-2.72926441113656,
7.50357029184312));
#405235=CARTESIAN_POINT('Ctrl Pts',(0.309318961508551,-2.72933166265592,
7.50365515313924));
#405236=CARTESIAN_POINT('Ctrl Pts',(0.308793650656355,-2.72943512272552,
7.50378570417639));
#405237=CARTESIAN_POINT('Ctrl Pts',(0.308277749172678,-2.72951317103045,
7.50400001621911));
#405238=CARTESIAN_POINT('Ctrl Pts',(0.307810185036332,-2.72955762209029,
7.50428903009634));
#405239=CARTESIAN_POINT('Ctrl Pts',(0.307758289014417,-2.72956255581594,
7.50432110841318));
#405240=CARTESIAN_POINT('Ctrl Pts',(0.307706965257224,-2.72956709514048,
7.50435406373354));
#405241=CARTESIAN_POINT('Ctrl Pts',(0.307656249660477,-2.72957124302653,
7.50438785222352));
#405242=CARTESIAN_POINT('Ctrl Pts',(0.307346606565338,-2.7295965678646,
7.50459414719561));
#405243=CARTESIAN_POINT('Ctrl Pts',(0.307054661928029,-2.72960719025543,
7.50483629897752));
#405244=CARTESIAN_POINT('Ctrl Pts',(0.306791647913694,-2.7296040184196,
7.5050991045531));
#405245=CARTESIAN_POINT('Ctrl Pts',(0.306211412580815,-2.72959702103118,
7.50567888004914));
#405246=CARTESIAN_POINT('Ctrl Pts',(0.305749108231759,-2.72952313331425,
7.50637912803145));
#405247=CARTESIAN_POINT('Ctrl Pts',(0.305392057397997,-2.72941054569535,
7.50710440483569));
#405248=CARTESIAN_POINT('Ctrl Pts',(0.305304501445106,-2.72938293697602,
7.50728225710686));
#405249=CARTESIAN_POINT('Ctrl Pts',(0.305221487814431,-2.7293525907114,
7.50746498566955));
#405250=CARTESIAN_POINT('Ctrl Pts',(0.305144811281211,-2.72932060655107,
7.50764697238949));
#405251=CARTESIAN_POINT('Ctrl Pts',(0.304732619340569,-2.72914866850742,
7.50862528291182));
#405252=CARTESIAN_POINT('Ctrl Pts',(0.304464548239098,-2.72891760973833,
7.50965856837422));
#405253=CARTESIAN_POINT('Ctrl Pts',(0.304285411258914,-2.72866417016778,
7.51067959873203));
#405254=CARTESIAN_POINT('Ctrl Pts',(0.304186831952766,-2.72852470205243,
7.51124147302579));
#405255=CARTESIAN_POINT('Ctrl Pts',(0.304115515380115,-2.728378171551,7.51180065547253));
#405256=CARTESIAN_POINT('Ctrl Pts',(0.304064538403005,-2.72822921565349,
7.51235175716501));
#405257=CARTESIAN_POINT('Ctrl Pts',(0.303888392640273,-2.72771451369063,
7.51425603304536));
#405258=CARTESIAN_POINT('Ctrl Pts',(0.303939832870269,-2.72710752083202,
7.51626900505181));
#405259=CARTESIAN_POINT('Ctrl Pts',(0.304176391156363,-2.72645112229369,
7.51827788969245));
#405260=CARTESIAN_POINT('Ctrl Pts',(0.304189194137839,-2.72641559676438,
7.51838661432546));
#405261=CARTESIAN_POINT('Ctrl Pts',(0.304202548093838,-2.72637992171949,
7.51849533314857));
#405262=CARTESIAN_POINT('Ctrl Pts',(0.304216449096315,-2.72634410251322,
7.51860402984325));
#405263=CARTESIAN_POINT('Ctrl Pts',(0.341939260496137,-2.65201338777647,
7.57603338728985));
#405264=CARTESIAN_POINT('Ctrl Pts',(0.332066529529991,-2.67755759370233,
7.55196141284922));
#405265=CARTESIAN_POINT('Ctrl Pts',(0.322210000114193,-2.70305746572958,
7.52783573083105));
#405266=CARTESIAN_POINT('Ctrl Pts',(0.312368326961429,-2.72851663434944,
7.50366116530176));
#405267=CARTESIAN_POINT('Origin',(1.1815582111521E-16,-9.16393216063562E-16,
7.49482233047033));
#405268=CARTESIAN_POINT('Origin',(0.388693460788468,-2.70976449964573,7.49482233047033));
#405269=CARTESIAN_POINT('Origin',(0.,0.,7.50366116523517));
#405270=CARTESIAN_POINT('Origin',(0.311362998732885,-2.71973515861748,7.49482233047033));
#405271=CARTESIAN_POINT('Ctrl Pts',(0.397282050205201,-2.71434368527686,
7.51860402984325));
#405272=CARTESIAN_POINT('Ctrl Pts',(0.401743698216877,-2.72050728674434,
7.51860402984325));
#405273=CARTESIAN_POINT('Ctrl Pts',(0.409267922647788,-2.71937488542709,
7.51860402984325));
#405274=CARTESIAN_POINT('Ctrl Pts',(0.398938691589159,-2.71663227181923,
7.51041458714364));
#405275=CARTESIAN_POINT('Ctrl Pts',(0.403526271692425,-2.72023899811274,
7.5100464290044));
#405276=CARTESIAN_POINT('Ctrl Pts',(0.409269997739552,-2.71937457312425,
7.50729136483009));
#405277=CARTESIAN_POINT('Ctrl Pts',(0.397367849688418,-2.71896812132682,
7.50215815450138));
#405278=CARTESIAN_POINT('Ctrl Pts',(0.399896795118431,-2.72078539937199,
7.49877163671532));
#405279=CARTESIAN_POINT('Ctrl Pts',(0.403312047312363,-2.72029552587179,
7.49481588533172));
#405280=CARTESIAN_POINT('Ctrl Pts',(0.389948395323643,-2.71851323713979,
7.50366171572173));
#405281=CARTESIAN_POINT('Ctrl Pts',(0.390468316773421,-2.72213785352545,
7.50000045605858));
#405282=CARTESIAN_POINT('Ctrl Pts',(0.390468316773545,-2.72213785352543,
7.49482233047317));
#405283=CARTESIAN_POINT('Origin',(0.40740761390848,-2.70701409049333,7.51860402984325));
#405284=CARTESIAN_POINT('Origin',(0.40740761390848,-2.70701409049333,9.));
#405285=CARTESIAN_POINT('Origin',(0.40740761390848,-2.70701409049333,8.75721825406948));
#405286=CARTESIAN_POINT('Ctrl Pts',(0.387489117162883,-2.70081746938362,
8.78942910404912));
#405287=CARTESIAN_POINT('Ctrl Pts',(0.390740624933991,-2.70534296669508,
8.79672699501691));
#405288=CARTESIAN_POINT('Ctrl Pts',(0.398822743738664,-2.70155445226206,
8.79893251111267));
#405289=CARTESIAN_POINT('Ctrl Pts',(0.393936589149048,-2.70972283426823,
8.78111911759584));
#405290=CARTESIAN_POINT('Ctrl Pts',(0.39779733455391,-2.7150835203292,8.78644465894813));
#405291=CARTESIAN_POINT('Ctrl Pts',(0.40570455888801,-2.7132970950983,8.78817647674132));
#405292=CARTESIAN_POINT('Ctrl Pts',(0.397954807503326,-2.71527287005866,
8.76780923932029));
#405293=CARTESIAN_POINT('Ctrl Pts',(0.402516389461998,-2.72159795557623,
8.76988516158375));
#405294=CARTESIAN_POINT('Ctrl Pts',(0.410012461604671,-2.72062569901123,
8.77093053738833));
#405295=CARTESIAN_POINT('Ctrl Pts',(0.397171309918828,-2.71419068903609,
8.75371302330492));
#405296=CARTESIAN_POINT('Ctrl Pts',(0.401620318062267,-2.72036098302482,
8.75300828287558));
#405297=CARTESIAN_POINT('Ctrl Pts',(0.409172640064114,-2.71919609173606,
8.75267964240738));
#405298=CARTESIAN_POINT('Origin',(0.399184265771865,-2.69565586321038,8.78727029226991));
#405299=CARTESIAN_POINT('Ctrl Pts',(0.347133565397108,-2.64507775146798,
8.85049129520029));
#405300=CARTESIAN_POINT('Ctrl Pts',(0.350558127032912,-2.649807813817,8.85711686593484));
#405301=CARTESIAN_POINT('Ctrl Pts',(0.358444815903146,-2.64650616259708,
8.85933012996512));
#405302=CARTESIAN_POINT('Ctrl Pts',(0.361129150869197,-2.66440869041267,
8.82945683644721));
#405303=CARTESIAN_POINT('Ctrl Pts',(0.364582138437126,-2.66917801513903,
8.83607469902387));
#405304=CARTESIAN_POINT('Ctrl Pts',(0.372477500384207,-2.66583207697137,
8.8382956714852));
#405305=CARTESIAN_POINT('Ctrl Pts',(0.375103874792548,-2.68371081503404,
8.80838214965002));
#405306=CARTESIAN_POINT('Ctrl Pts',(0.378570489461554,-2.68849896174253,
8.81501364461987));
#405307=CARTESIAN_POINT('Ctrl Pts',(0.38648835703971,-2.68512906773677,
8.81722098428721));
#405308=CARTESIAN_POINT('Ctrl Pts',(0.389059322317711,-2.70298631476879,
8.78727029226991));
#405309=CARTESIAN_POINT('Ctrl Pts',(0.39252651280282,-2.70777525680419,
8.79393457792714));
#405310=CARTESIAN_POINT('Ctrl Pts',(0.400479038758368,-2.70439935009568,
8.79610912703474));
#405311=CARTESIAN_POINT('Origin',(0.357258508851261,-2.63774729990957,8.85049129520029));
#405312=CARTESIAN_POINT('Ctrl Pts',(0.335155581859898,-2.64662214142562,
8.85049129520029));
#405313=CARTESIAN_POINT('Ctrl Pts',(0.333042822978433,-2.65206616219449,
8.85711686593484));
#405314=CARTESIAN_POINT('Ctrl Pts',(0.324576590381463,-2.65087298671371,
8.85933012996512));
#405315=CARTESIAN_POINT('Ctrl Pts',(0.337024709144332,-2.64180589483668,
8.86332496987231));
#405316=CARTESIAN_POINT('Ctrl Pts',(0.332486490925516,-2.64267564754589,
8.86648636486738));
#405317=CARTESIAN_POINT('Ctrl Pts',(0.329821522197239,-2.6374055390489,
8.87206031107457));
#405318=CARTESIAN_POINT('Ctrl Pts',(0.344083317655487,-2.64086469778922,
8.86341338519877));
#405319=CARTESIAN_POINT('Ctrl Pts',(0.348704757116161,-2.64052445089995,
8.86654584966058));
#405320=CARTESIAN_POINT('Ctrl Pts',(0.349892026593758,-2.63471802825129,
8.87215952290715));
#405321=CARTESIAN_POINT('Ctrl Pts',(0.347133565397107,-2.64507775146798,
8.85049129520029));
#405322=CARTESIAN_POINT('Ctrl Pts',(0.350558127032912,-2.649807813817,8.85711686593484));
#405323=CARTESIAN_POINT('Ctrl Pts',(0.358444815903146,-2.64650616259708,
8.85933012996512));
#405324=CARTESIAN_POINT('Origin',(0.323502373428218,-2.64209967160839,8.85049129520029));
#405325=CARTESIAN_POINT('Ctrl Pts',(0.309289785090442,-2.71327145765926,
8.78727029226991));
#405326=CARTESIAN_POINT('Ctrl Pts',(0.307150726644374,-2.71878324544932,
8.79393457792714));
#405327=CARTESIAN_POINT('Ctrl Pts',(0.298601974927924,-2.71753494289437,
8.79610912703474));
#405328=CARTESIAN_POINT('Ctrl Pts',(0.317899498928076,-2.69108650254806,
8.80838214965002));
#405329=CARTESIAN_POINT('Ctrl Pts',(0.315760795727631,-2.6965973749641,
8.81501364461987));
#405330=CARTESIAN_POINT('Ctrl Pts',(0.307247094031223,-2.69534609720932,
8.81722098428721));
#405331=CARTESIAN_POINT('Ctrl Pts',(0.326521105202121,-2.66887090377404,
8.82945683644721));
#405332=CARTESIAN_POINT('Ctrl Pts',(0.324390809144546,-2.67436011320681,
8.83607469902389));
#405333=CARTESIAN_POINT('Ctrl Pts',(0.315904953537574,-2.67312629915468,
8.83829567148519));
#405334=CARTESIAN_POINT('Ctrl Pts',(0.335155581859898,-2.64662214142562,
8.85049129520029));
#405335=CARTESIAN_POINT('Ctrl Pts',(0.333042822978433,-2.65206616219449,
8.85711686593484));
#405336=CARTESIAN_POINT('Ctrl Pts',(0.324576590381463,-2.65087298671371,
8.85933012996512));
#405337=CARTESIAN_POINT('Origin',(0.297636576658761,-2.70874898784202,8.78727029226991));
#405338=CARTESIAN_POINT('Ctrl Pts',(0.304283422748619,-2.72617147813989,
8.75374538247849));
#405339=CARTESIAN_POINT('Ctrl Pts',(0.301546370683848,-2.7332604078463,
8.75304829418602));
#405340=CARTESIAN_POINT('Ctrl Pts',(0.293954221614916,-2.73405408014901,
8.75272238421917));
#405341=CARTESIAN_POINT('Ctrl Pts',(0.303805856238317,-2.72740204188969,
8.76769408445017));
#405342=CARTESIAN_POINT('Ctrl Pts',(0.300999284012165,-2.73466911195342,
8.76974318093968));
#405343=CARTESIAN_POINT('Ctrl Pts',(0.293509920856674,-2.73563233404902,
8.77077869880429));
#405344=CARTESIAN_POINT('Ctrl Pts',(0.306253590132223,-2.7210948731195,
8.78108014887993));
#405345=CARTESIAN_POINT('Ctrl Pts',(0.303878665533224,-2.72725482201941,
8.78639403366325));
#405346=CARTESIAN_POINT('Ctrl Pts',(0.295789548083311,-2.72755189879461,
8.78812224174741));
#405347=CARTESIAN_POINT('Ctrl Pts',(0.310264885608781,-2.71075881581417,
8.78944554828685));
#405348=CARTESIAN_POINT('Ctrl Pts',(0.308268610199825,-2.71595220604682,
8.79673892988686));
#405349=CARTESIAN_POINT('Ctrl Pts',(0.299498741631349,-2.71434193910989,
8.79894799272499));
#405350=CARTESIAN_POINT('Origin',(0.292563240664638,-2.72182163269598,8.75721825406948));
#405351=CARTESIAN_POINT('Origin',(0.292563240664638,-2.72182163269598,9.));
#405352=CARTESIAN_POINT('Origin',(0.292563240664638,-2.72182163269598,7.51860402984325));
#405353=CARTESIAN_POINT('Ctrl Pts',(0.312368237512627,-2.72851585273769,
7.50366195182966));
#405354=CARTESIAN_POINT('Ctrl Pts',(0.312784747585408,-2.73215404062032,
7.50000065167735));
#405355=CARTESIAN_POINT('Ctrl Pts',(0.312784747585292,-2.73215404062033,
7.49482233047108));
#405356=CARTESIAN_POINT('Ctrl Pts',(0.305300246324107,-2.73083906176094,
7.50215800491337));
#405357=CARTESIAN_POINT('Ctrl Pts',(0.303313249275647,-2.73323834079926,
7.49877273257269));
#405358=CARTESIAN_POINT('Ctrl Pts',(0.299883530860017,-2.73363100852074,
7.49481816995647));
#405359=CARTESIAN_POINT('Ctrl Pts',(0.30319700787747,-2.7289718701857,7.51043025814043));
#405360=CARTESIAN_POINT('Ctrl Pts',(0.299675308765078,-2.73362916471673,
7.51006209594513));
#405361=CARTESIAN_POINT('Ctrl Pts',(0.293896628507995,-2.73425031256432,
7.50731281821701));
#405362=CARTESIAN_POINT('Ctrl Pts',(0.304216995834693,-2.72634269346048,
7.51860402984326));
#405363=CARTESIAN_POINT('Ctrl Pts',(0.301464837418653,-2.7334368207108,
7.51860402984327));
#405364=CARTESIAN_POINT('Ctrl Pts',(0.293899145873147,-2.7342500419777,
7.51860402984327));
#405365=CARTESIAN_POINT('Origin',(0.,0.,7.5));
#405366=CARTESIAN_POINT('Origin',(0.50403663157861,-2.6197108805292,7.5));
#405367=CARTESIAN_POINT('',(0.50403663157861,-2.6197108805292,7.59394543036555));
#405368=CARTESIAN_POINT('',(0.50403663157861,-2.6197108805292,8.85049129520029));
#405369=CARTESIAN_POINT('',(0.50403663157861,-2.6197108805292,7.5));
#405370=CARTESIAN_POINT('',(0.482494215215367,-2.68788048588351,8.78727029226991));
#405371=CARTESIAN_POINT('Ctrl Pts',(0.50403663157861,-2.6197108805292,8.85049129520029));
#405372=CARTESIAN_POINT('Ctrl Pts',(0.496845388128044,-2.64246711268839,
8.82945686509571));
#405373=CARTESIAN_POINT('Ctrl Pts',(0.489664835330419,-2.66518951495683,
8.80838212259896));
#405374=CARTESIAN_POINT('Ctrl Pts',(0.482494215215367,-2.68788048588351,
8.78727029226991));
#405375=CARTESIAN_POINT('',(0.47826887016568,-2.70125132133976,8.75721825406948));
#405376=CARTESIAN_POINT('Origin',(0.490984591624991,-2.66101389988662,8.75937679713189));
#405377=CARTESIAN_POINT('',(0.47826887016568,-2.70125132133976,7.51860402984325));
#405378=CARTESIAN_POINT('',(0.47826887016568,-2.70125132133976,7.5));
#405379=CARTESIAN_POINT('Ctrl Pts',(0.47826887016568,-2.70125132133976,
7.51860402984325));
#405380=CARTESIAN_POINT('Ctrl Pts',(0.481587221536751,-2.69075060964714,
7.52834476460825));
#405381=CARTESIAN_POINT('Ctrl Pts',(0.484907727133655,-2.68024308104402,
7.53807742314407));
#405382=CARTESIAN_POINT('Ctrl Pts',(0.48823045928738,-2.66972850664355,
7.54780169004674));
#405383=CARTESIAN_POINT('Ctrl Pts',(0.49349348744053,-2.65307398905745,
7.5632044032688));
#405384=CARTESIAN_POINT('Ctrl Pts',(0.498762108429687,-2.63640177329775,
7.57858609112103));
#405385=CARTESIAN_POINT('Ctrl Pts',(0.50403663157861,-2.6197108805292,7.59394543036555));
#405386=CARTESIAN_POINT('Origin',(0.691101205365358,-2.82936072626276,7.5));
#405387=CARTESIAN_POINT('',(0.570375062512147,-2.68331364198702,8.75721825406948));
#405388=CARTESIAN_POINT('',(0.561440886005621,-2.67250562312428,8.78727029226991));
#405389=CARTESIAN_POINT('Origin',(0.538762613749665,-2.64507084005976,8.7565864062101));
#405390=CARTESIAN_POINT('',(0.515891055659684,-2.6174022316462,8.85049129520029));
#405391=CARTESIAN_POINT('Ctrl Pts',(0.561440886005621,-2.67250562312428,
8.78727029226991));
#405392=CARTESIAN_POINT('Ctrl Pts',(0.546279145362962,-2.6541638790656,
8.80838212259897));
#405393=CARTESIAN_POINT('Ctrl Pts',(0.531096402804887,-2.63579672817756,
8.82945686509571));
#405394=CARTESIAN_POINT('Ctrl Pts',(0.515891055659685,-2.6174022316462,
8.85049129520029));
#405395=CARTESIAN_POINT('',(0.515891055659684,-2.6174022316462,7.59394543036555));
#405396=CARTESIAN_POINT('',(0.515891055659684,-2.6174022316462,7.5));
#405397=CARTESIAN_POINT('',(0.570375062512147,-2.68331364198702,7.51860402984325));
#405398=CARTESIAN_POINT('Ctrl Pts',(0.515891055659684,-2.6174022316462,
7.59394543036555));
#405399=CARTESIAN_POINT('Ctrl Pts',(0.527043640891444,-2.63089394534417,
7.57858609112103));
#405400=CARTESIAN_POINT('Ctrl Pts',(0.538183746447113,-2.64437056189532,
7.56320440326857));
#405401=CARTESIAN_POINT('Ctrl Pts',(0.549312026368894,-2.65783287251976,
7.54780169004651));
#405402=CARTESIAN_POINT('Ctrl Pts',(0.556337695325203,-2.66633209598457,
7.53807742314383));
#405403=CARTESIAN_POINT('Ctrl Pts',(0.563358656393546,-2.67482562413523,
7.52834476460825));
#405404=CARTESIAN_POINT('Ctrl Pts',(0.570375062512147,-2.68331364198702,
7.51860402984325));
#405405=CARTESIAN_POINT('',(0.570375062512147,-2.68331364198702,7.5));
#405406=CARTESIAN_POINT('Origin',(0.510592093294271,-2.62178248538885,7.5));
#405407=CARTESIAN_POINT('Ctrl Pts',(0.515891055659684,-2.6174022316462,
8.85049129520029));
#405408=CARTESIAN_POINT('Ctrl Pts',(0.515767668527162,-2.61725296545981,
8.85097269580138));
#405409=CARTESIAN_POINT('Ctrl Pts',(0.515639354986848,-2.61711094168747,
8.85143669361005));
#405410=CARTESIAN_POINT('Ctrl Pts',(0.515499557882546,-2.61697020670063,
8.8519052845931));
#405411=CARTESIAN_POINT('Ctrl Pts',(0.515226123612142,-2.61669493799147,
8.85282181883899));
#405412=CARTESIAN_POINT('Ctrl Pts',(0.514915651119206,-2.61643181964957,
8.85372622499636));
#405413=CARTESIAN_POINT('Ctrl Pts',(0.514553299874856,-2.6161884856712,
8.85462257735071));
#405414=CARTESIAN_POINT('Ctrl Pts',(0.514252488741296,-2.61598647844477,
8.85536669723986));
#405415=CARTESIAN_POINT('Ctrl Pts',(0.513915873198261,-2.61579803376955,
8.85610498449051));
#405416=CARTESIAN_POINT('Ctrl Pts',(0.513531024768008,-2.61563448612491,
8.85681338218371));
#405417=CARTESIAN_POINT('Ctrl Pts',(0.513181774213136,-2.61548606638055,
8.85745625420285));
#405418=CARTESIAN_POINT('Ctrl Pts',(0.512788654114686,-2.61535573822306,
8.85808743050666));
#405419=CARTESIAN_POINT('Ctrl Pts',(0.512331828562537,-2.61526410220628,
8.85866804508411));
#405420=CARTESIAN_POINT('Ctrl Pts',(0.51212105915554,-2.61522182333456,
8.85893592806396));
#405421=CARTESIAN_POINT('Ctrl Pts',(0.511896582696664,-2.61518797425763,
8.85919241173849));
#405422=CARTESIAN_POINT('Ctrl Pts',(0.511655676326057,-2.61516597374877,
8.85943017985535));
#405423=CARTESIAN_POINT('Ctrl Pts',(0.511330381409818,-2.61513626654896,
8.85975123720001));
#405424=CARTESIAN_POINT('Ctrl Pts',(0.510966791987504,-2.61512804460748,
8.86004599534705));
#405425=CARTESIAN_POINT('Ctrl Pts',(0.510569040990318,-2.61515181913894,
8.86026130871721));
#405426=CARTESIAN_POINT('Ctrl Pts',(0.51042341313646,-2.61516052366518,
8.86034014101235));
#405427=CARTESIAN_POINT('Ctrl Pts',(0.510271017703931,-2.61517363576241,
8.86040910639693));
#405428=CARTESIAN_POINT('Ctrl Pts',(0.51011603545622,-2.61519113333937,
8.86046313645507));
#405429=CARTESIAN_POINT('Ctrl Pts',(0.509874186956632,-2.61521843816168,
8.8605474499083));
#405430=CARTESIAN_POINT('Ctrl Pts',(0.509619453975313,-2.61525731366694,
8.86059655985669));
#405431=CARTESIAN_POINT('Ctrl Pts',(0.509368129116552,-2.61530497704635,
8.86059725258816));
#405432=CARTESIAN_POINT('Ctrl Pts',(0.509116223596962,-2.61535275054721,
8.86059794692011));
#405433=CARTESIAN_POINT('Ctrl Pts',(0.508865443335394,-2.61541249263373,
8.86056369958366));
#405434=CARTESIAN_POINT('Ctrl Pts',(0.508628593949213,-2.61547728428474,
8.86048590497774));
#405435=CARTESIAN_POINT('Ctrl Pts',(0.508566783311275,-2.61549419297657,
8.86046560290182));
#405436=CARTESIAN_POINT('Ctrl Pts',(0.508505141221167,-2.61551175291262,
8.86044257503091));
#405437=CARTESIAN_POINT('Ctrl Pts',(0.508445563477128,-2.61552938990612,
8.86041778462583));
#405438=CARTESIAN_POINT('Ctrl Pts',(0.508044679189558,-2.61564806498672,
8.86025097596201));
#405439=CARTESIAN_POINT('Ctrl Pts',(0.507683561495995,-2.6157864717915,
8.8599848982295));
#405440=CARTESIAN_POINT('Ctrl Pts',(0.507369718277706,-2.61593265927751,
8.85968173251461));
#405441=CARTESIAN_POINT('Ctrl Pts',(0.507203713196304,-2.61600998408206,
8.85952137522076));
#405442=CARTESIAN_POINT('Ctrl Pts',(0.507047654086883,-2.61609080315806,
8.85934740853961));
#405443=CARTESIAN_POINT('Ctrl Pts',(0.506903026841193,-2.61617259635408,
8.8591675900182));
#405444=CARTESIAN_POINT('Ctrl Pts',(0.506322273274009,-2.61650103855136,
8.85844552518696));
#405445=CARTESIAN_POINT('Ctrl Pts',(0.50589153921837,-2.61686111677501,
8.85759444184127));
#405446=CARTESIAN_POINT('Ctrl Pts',(0.505566712158174,-2.61718625003458,
8.85683498915142));
#405447=CARTESIAN_POINT('Ctrl Pts',(0.505532719871405,-2.61722027436429,
8.85675551445));
#405448=CARTESIAN_POINT('Ctrl Pts',(0.505499903995364,-2.61725392708393,
8.85667699793652));
#405449=CARTESIAN_POINT('Ctrl Pts',(0.505468225267565,-2.61728713860215,
8.85659965593547));
#405450=CARTESIAN_POINT('Ctrl Pts',(0.505040624183298,-2.61773542936974,
8.85555568965886));
#405451=CARTESIAN_POINT('Ctrl Pts',(0.504694415106465,-2.61822801862891,
8.85434650606346));
#405452=CARTESIAN_POINT('Ctrl Pts',(0.504422802045048,-2.61876376787636,
8.85297329937117));
#405453=CARTESIAN_POINT('Ctrl Pts',(0.504270036247629,-2.61906509418437,
8.85220095427747));
#405454=CARTESIAN_POINT('Ctrl Pts',(0.504141086615989,-2.61938033921223,
8.85137579139183));
#405455=CARTESIAN_POINT('Ctrl Pts',(0.50403663157861,-2.6197108805292,8.85049129520029));
#405456=CARTESIAN_POINT('Origin',(0.510592093294271,-2.62178248538885,7.59394543036555));
#405457=CARTESIAN_POINT('Ctrl Pts',(0.515532821189714,-2.61696886155262,
7.59443877723642));
#405458=CARTESIAN_POINT('Ctrl Pts',(0.511843350832983,-2.61250556656624,
7.58783886950016));
#405459=CARTESIAN_POINT('Ctrl Pts',(0.504225634743635,-2.61625384391973,
7.58559994247159));
#405460=CARTESIAN_POINT('Ctrl Pts',(0.53567353162265,-2.64133385793579,
7.56670252222136));
#405461=CARTESIAN_POINT('Ctrl Pts',(0.531989393598045,-2.63687701367782,
7.56004874999028));
#405462=CARTESIAN_POINT('Ctrl Pts',(0.524317107068316,-2.64062833033498,
7.55786368756704));
#405463=CARTESIAN_POINT('Ctrl Pts',(0.555776631291165,-2.66565335512258,
7.53888913333559));
#405464=CARTESIAN_POINT('Ctrl Pts',(0.55207059825391,-2.66117002362098,
7.5322200213728));
#405465=CARTESIAN_POINT('Ctrl Pts',(0.544372672437995,-2.66495742152093,
7.53005029815327));
#405466=CARTESIAN_POINT('Ctrl Pts',(0.57584121051637,-2.68992625263927,
7.51101258149734));
#405467=CARTESIAN_POINT('Ctrl Pts',(0.572090253624662,-2.68538857501344,
7.5043616886572));
#405468=CARTESIAN_POINT('Ctrl Pts',(0.564391276187505,-2.68923996800388,
7.50217374673251));
#405469=CARTESIAN_POINT('',(0.563323058569168,-2.68794421947736,7.50366116523517));
#405470=CARTESIAN_POINT('Ctrl Pts',(0.570375062512147,-2.68331364198702,
7.51860402984325));
#405471=CARTESIAN_POINT('Ctrl Pts',(0.570656425301981,-2.68365401743601,
7.51734760759494));
#405472=CARTESIAN_POINT('Ctrl Pts',(0.570864819165499,-2.68399950239606,
7.51608817408573));
#405473=CARTESIAN_POINT('Ctrl Pts',(0.570988330268538,-2.6843561994528,
7.5148100591312));
#405474=CARTESIAN_POINT('Ctrl Pts',(0.571100209577064,-2.68467930417034,
7.51365231206384));
#405475=CARTESIAN_POINT('Ctrl Pts',(0.571142835244544,-2.68501198219009,
7.51247773061043));
#405476=CARTESIAN_POINT('Ctrl Pts',(0.571078844074313,-2.68535316978938,
7.51129758471022));
#405477=CARTESIAN_POINT('Ctrl Pts',(0.570999310357784,-2.68577722701019,
7.50983079813402));
#405478=CARTESIAN_POINT('Ctrl Pts',(0.570744815553309,-2.6861984949357,
7.50839324291155));
#405479=CARTESIAN_POINT('Ctrl Pts',(0.570242939355973,-2.6865774199326,
7.50715379678855));
#405480=CARTESIAN_POINT('Ctrl Pts',(0.57001108701402,-2.68675247236271,
7.50658120839351));
#405481=CARTESIAN_POINT('Ctrl Pts',(0.569687753921555,-2.68693579028516,
7.50598221009429));
#405482=CARTESIAN_POINT('Ctrl Pts',(0.569269416203884,-2.68710322355639,
7.50545747549611));
#405483=CARTESIAN_POINT('Ctrl Pts',(0.569046178248972,-2.68719257113246,
7.50517746087247));
#405484=CARTESIAN_POINT('Ctrl Pts',(0.568793541135446,-2.68727855221161,
7.50491486231392));
#405485=CARTESIAN_POINT('Ctrl Pts',(0.568517657707569,-2.68735731079858,
7.50468370960992));
#405486=CARTESIAN_POINT('Ctrl Pts',(0.568105124960397,-2.68747507972909,
7.50433806340446));
#405487=CARTESIAN_POINT('Ctrl Pts',(0.567628091086002,-2.68757969554714,
7.50405484070983));
#405488=CARTESIAN_POINT('Ctrl Pts',(0.567118529966979,-2.68766341280671,
7.5038576603613));
#405489=CARTESIAN_POINT('Ctrl Pts',(0.567064040325677,-2.68767236506636,
7.50383657498791));
#405490=CARTESIAN_POINT('Ctrl Pts',(0.567009205172219,-2.68768108862484,
7.50381643264937));
#405491=CARTESIAN_POINT('Ctrl Pts',(0.566954082693383,-2.68768958177396,
7.50379723213559));
#405492=CARTESIAN_POINT('Ctrl Pts',(0.566586122115307,-2.68774627632267,
7.50366906242519));
#405493=CARTESIAN_POINT('Ctrl Pts',(0.566197244826921,-2.68779322640586,
7.50358235568538));
#405494=CARTESIAN_POINT('Ctrl Pts',(0.565821327165852,-2.68782947036994,
7.5035341175365));
#405495=CARTESIAN_POINT('Ctrl Pts',(0.565257681178744,-2.68788381409206,
7.50346178989176));
#405496=CARTESIAN_POINT('Ctrl Pts',(0.564649015727631,-2.6879183099948,
7.50346967198527));
#405497=CARTESIAN_POINT('Ctrl Pts',(0.564050452828154,-2.6879337885485,
7.50354272648692));
#405498=CARTESIAN_POINT('Ctrl Pts',(0.563804251518082,-2.68794015519803,
7.50357277531559));
#405499=CARTESIAN_POINT('Ctrl Pts',(0.563560090191749,-2.68794343769315,
7.50361331098761));
#405500=CARTESIAN_POINT('Ctrl Pts',(0.563323058569459,-2.68794421947875,
7.50366116523658));
#405501=CARTESIAN_POINT('',(0.511151791456924,-2.62465641716285,7.57603338622103));
#405502=CARTESIAN_POINT('Origin',(0.512838247935187,-2.63333094044392,7.58486873427629));
#405503=CARTESIAN_POINT('Ctrl Pts',(0.563323058609621,-2.687944219518,7.50366116529969));
#405504=CARTESIAN_POINT('Ctrl Pts',(0.545960368869929,-2.66688324129277,
7.5278357307971));
#405505=CARTESIAN_POINT('Ctrl Pts',(0.528570753762145,-2.6457883146349,
7.55196141284068));
#405506=CARTESIAN_POINT('Ctrl Pts',(0.511151792493781,-2.62465641786469,
7.57603338728831));
#405507=CARTESIAN_POINT('Ctrl Pts',(0.51641077145758,-2.61830690341525,
7.5963967733137));
#405508=CARTESIAN_POINT('Ctrl Pts',(0.50713909630514,-2.60255546044574,
7.59959882295468));
#405509=CARTESIAN_POINT('Ctrl Pts',(0.503923606568037,-2.6205657196987,
7.59642833564546));
#405510=CARTESIAN_POINT('Ctrl Pts',(0.514998153140218,-2.61467102476309,
7.58707626057421));
#405511=CARTESIAN_POINT('Ctrl Pts',(0.508781048698791,-2.61197660397169,
7.58809943920599));
#405512=CARTESIAN_POINT('Ctrl Pts',(0.503963188820591,-2.61672029736263,
7.58710240504252));
#405513=CARTESIAN_POINT('Ctrl Pts',(0.5124778484545,-2.62020037341848,7.58015376756929));
#405514=CARTESIAN_POINT('Ctrl Pts',(0.510031459795584,-2.61873597800556,
7.58205880659761));
#405515=CARTESIAN_POINT('Ctrl Pts',(0.508301387520527,-2.62095722201766,
7.58020924244127));
#405516=CARTESIAN_POINT('Ctrl Pts',(0.511151791298927,-2.6246564163505,
7.57603338509286));
#405517=CARTESIAN_POINT('Ctrl Pts',(0.511151791298927,-2.6246564163505,
7.57603338509286));
#405518=CARTESIAN_POINT('Ctrl Pts',(0.511151791298927,-2.6246564163505,
7.57603338509286));
#405519=CARTESIAN_POINT('Origin',(0.512843849057621,-2.63332984962562,7.58486873427619));
#405520=CARTESIAN_POINT('Ctrl Pts',(0.47567552995596,-2.70945778136101,
7.51098857897448));
#405521=CARTESIAN_POINT('Ctrl Pts',(0.477449522153366,-2.70384409597124,
7.50433767179956));
#405522=CARTESIAN_POINT('Ctrl Pts',(0.486031165786685,-2.70452486291606,
7.50214974420965));
#405523=CARTESIAN_POINT('Ctrl Pts',(0.485167636506963,-2.67942061437602,
7.53887321589169));
#405524=CARTESIAN_POINT('Ctrl Pts',(0.486920373129621,-2.6738741908997,
7.53220407452062));
#405525=CARTESIAN_POINT('Ctrl Pts',(0.49547702342873,-2.67449600725536,
7.53003438070911));
#405526=CARTESIAN_POINT('Ctrl Pts',(0.494677971404042,-2.64932576495015,
7.56669465659233));
#405527=CARTESIAN_POINT('Ctrl Pts',(0.496420349679055,-2.64381211980541,
7.560040858333));
#405528=CARTESIAN_POINT('Ctrl Pts',(0.504939684355766,-2.6444101054177,
7.55785582193789));
#405529=CARTESIAN_POINT('Ctrl Pts',(0.504206104532811,-2.619174594153,7.59443891967696));
#405530=CARTESIAN_POINT('Ctrl Pts',(0.505951009039414,-2.61365295490927,
7.58783901202978));
#405531=CARTESIAN_POINT('Ctrl Pts',(0.514418602349914,-2.61426861838576,
7.58560008491213));
#405532=CARTESIAN_POINT('',(0.48654319373896,-2.70289709681367,7.50366116523517));
#405533=CARTESIAN_POINT('Ctrl Pts',(0.486543193739026,-2.70289709681404,
7.50366116523554));
#405534=CARTESIAN_POINT('Ctrl Pts',(0.485839853899813,-2.70317896661969,
7.50350835821027));
#405535=CARTESIAN_POINT('Ctrl Pts',(0.48518414354121,-2.70341519095536,
7.50345484956));
#405536=CARTESIAN_POINT('Ctrl Pts',(0.484556771391471,-2.70361335792061,
7.50349758195598));
#405537=CARTESIAN_POINT('Ctrl Pts',(0.484234882951524,-2.70371503227022,
7.50351950684424));
#405538=CARTESIAN_POINT('Ctrl Pts',(0.483888766775226,-2.70381683307007,
7.50357029184312));
#405539=CARTESIAN_POINT('Ctrl Pts',(0.483552312554467,-2.70390582412703,
7.50365515313923));
#405540=CARTESIAN_POINT('Ctrl Pts',(0.483034709719171,-2.70404272840868,
7.50378570417639));
#405541=CARTESIAN_POINT('Ctrl Pts',(0.482524868782483,-2.70415367027655,
7.50400001621911));
#405542=CARTESIAN_POINT('Ctrl Pts',(0.48206111329598,-2.70422798694398,
7.50428903009634));
#405543=CARTESIAN_POINT('Ctrl Pts',(0.4820096400049,-2.70423623552231,7.50432110841318));
#405544=CARTESIAN_POINT('Ctrl Pts',(0.481958712533397,-2.70424405384473,
7.50435406373354));
#405545=CARTESIAN_POINT('Ctrl Pts',(0.481908366893258,-2.70425144256795,
7.50438785222351));
#405546=CARTESIAN_POINT('Ctrl Pts',(0.481600982561012,-2.70429655427464,
7.50459414719561));
#405547=CARTESIAN_POINT('Ctrl Pts',(0.481310318334189,-2.70432585979777,
7.50483629897752));
#405548=CARTESIAN_POINT('Ctrl Pts',(0.481047641490135,-2.70433954584457,
7.50509910455309));
#405549=CARTESIAN_POINT('Ctrl Pts',(0.480468149988762,-2.70436973863845,
7.50567888004914));
#405550=CARTESIAN_POINT('Ctrl Pts',(0.480002061491295,-2.7043256226731,
7.50637912803144));
#405551=CARTESIAN_POINT('Ctrl Pts',(0.479638530743254,-2.704236142703,7.50710440483569));
#405552=CARTESIAN_POINT('Ctrl Pts',(0.479549385786738,-2.70421420043791,
7.50728225710685));
#405553=CARTESIAN_POINT('Ctrl Pts',(0.479464598424619,-2.70418923522453,
7.50746498566954));
#405554=CARTESIAN_POINT('Ctrl Pts',(0.479386030199372,-2.70416222946143,
7.50764697238949));
#405555=CARTESIAN_POINT('Ctrl Pts',(0.478963669043002,-2.70401705391124,
7.50862528291181));
#405556=CARTESIAN_POINT('Ctrl Pts',(0.478681344736196,-2.70380364525162,
7.50965856837421));
#405557=CARTESIAN_POINT('Ctrl Pts',(0.478486337883113,-2.70356220374557,
7.51067959873201));
#405558=CARTESIAN_POINT('Ctrl Pts',(0.478379025365891,-2.70342933818025,
7.51124147302578));
#405559=CARTESIAN_POINT('Ctrl Pts',(0.478298467079326,-2.70328767800995,
7.51180065547252));
#405560=CARTESIAN_POINT('Ctrl Pts',(0.478238051202762,-2.70314229426445,
7.512351757165));
#405561=CARTESIAN_POINT('Ctrl Pts',(0.478029290282408,-2.70263993550974,
7.51425603304535));
#405562=CARTESIAN_POINT('Ctrl Pts',(0.478041734656956,-2.70203089399621,
7.51626900505179));
#405563=CARTESIAN_POINT('Ctrl Pts',(0.478235751309932,-2.70136068775765,
7.51827788969242));
#405564=CARTESIAN_POINT('Ctrl Pts',(0.478246251857833,-2.70132441492951,
7.51838661432544));
#405565=CARTESIAN_POINT('Ctrl Pts',(0.478257292668725,-2.70128795759193,
7.51849533314856));
#405566=CARTESIAN_POINT('Ctrl Pts',(0.478268870165676,-2.70125132133976,
7.51860402984325));
#405567=CARTESIAN_POINT('Ctrl Pts',(0.511151790759207,-2.62465641820371,
7.57603338728985));
#405568=CARTESIAN_POINT('Ctrl Pts',(0.502935967270572,-2.65078068886369,
7.55196141284922));
#405569=CARTESIAN_POINT('Ctrl Pts',(0.494733471561858,-2.67685967867693,
7.52783573083104));
#405570=CARTESIAN_POINT('Ctrl Pts',(0.486543193716093,-2.70289709686825,
7.50366116530176));
#405571=CARTESIAN_POINT('Origin',(1.76626572250583E-16,-9.06940118467442E-16,
7.49482233047033));
#405572=CARTESIAN_POINT('Origin',(0.561510055974265,-2.6792933223221,7.49482233047033));
#405573=CARTESIAN_POINT('Origin',(0.,0.,7.50366116523517));
#405574=CARTESIAN_POINT('Origin',(0.484977299960314,-2.69419807522075,7.49482233047033));
#405575=CARTESIAN_POINT('Ctrl Pts',(0.570374388643635,-2.68331282671198,
7.51860402984325));
#405576=CARTESIAN_POINT('Ctrl Pts',(0.575221773022856,-2.68917790562962,
7.51860402984325));
#405577=CARTESIAN_POINT('Ctrl Pts',(0.582657984926202,-2.68756575223784,
7.51860402984325));
#405578=CARTESIAN_POINT('Ctrl Pts',(0.572174256523402,-2.68549056972994,
7.51041458714365));
#405579=CARTESIAN_POINT('Ctrl Pts',(0.576983494698361,-2.68879595835105,
7.5100464290044));
#405580=CARTESIAN_POINT('Ctrl Pts',(0.582660035745137,-2.68756530762508,
7.50729136483008));
#405581=CARTESIAN_POINT('Ctrl Pts',(0.570756300477624,-2.68792226417034,
7.50215815450138));
#405582=CARTESIAN_POINT('Ctrl Pts',(0.573396483322147,-2.68957377833285,
7.49877163671532));
#405583=CARTESIAN_POINT('Ctrl Pts',(0.576773332211246,-2.68886609537093,
7.49481588533172));
#405584=CARTESIAN_POINT('Ctrl Pts',(0.563322945647643,-2.68794368066494,
7.50366171572174));
#405585=CARTESIAN_POINT('Ctrl Pts',(0.564074028832216,-2.69152753840584,
7.50000045605858));
#405586=CARTESIAN_POINT('Ctrl Pts',(0.564074028832339,-2.69152753840582,
7.49482233047317));
#405587=CARTESIAN_POINT('Origin',(0.580009539540173,-2.67534954427312,7.51860402984325));
#405588=CARTESIAN_POINT('Origin',(0.580009539540173,-2.67534954427312,9.));
#405589=CARTESIAN_POINT('Origin',(0.580009539540173,-2.67534954427312,8.75721825406948));
#405590=CARTESIAN_POINT('Ctrl Pts',(0.559734948604752,-2.67044183725424,
8.78942910404913));
#405591=CARTESIAN_POINT('Ctrl Pts',(0.563269725412686,-2.67474971162796,
8.7967269950169));
#405592=CARTESIAN_POINT('Ctrl Pts',(0.571092507684352,-2.67045115797444,
8.79893251111267));
#405593=CARTESIAN_POINT('Ctrl Pts',(0.566739742255397,-2.67891581416313,
8.78111911759577));
#405594=CARTESIAN_POINT('Ctrl Pts',(0.570936015679932,-2.68401812731229,
8.78644465894813));
#405595=CARTESIAN_POINT('Ctrl Pts',(0.578712537116074,-2.68172875488109,
8.78817647674132));
#405596=CARTESIAN_POINT('Ctrl Pts',(0.571105296763092,-2.68419699867588,
8.76780923932034));
#405597=CARTESIAN_POINT('Ctrl Pts',(0.576062756082935,-2.69021682706735,
8.76988516158374));
#405598=CARTESIAN_POINT('Ctrl Pts',(0.58348113404944,-2.68876629311658,
8.77093053738833));
#405599=CARTESIAN_POINT('Ctrl Pts',(0.570254073382254,-2.68316723997289,
8.75371302330491));
#405600=CARTESIAN_POINT('Ctrl Pts',(0.575089272654503,-2.68903980750042,
8.75300828287559));
#405601=CARTESIAN_POINT('Ctrl Pts',(0.582551442759697,-2.68739343067373,
8.75267964240737));
#405602=CARTESIAN_POINT('Origin',(0.571075363033647,-2.66454152541039,8.78727029226991));
#405603=CARTESIAN_POINT('Ctrl Pts',(0.515891055659684,-2.6174022316462,
8.85049129520029));
#405604=CARTESIAN_POINT('Ctrl Pts',(0.51961163730155,-2.62190316315749,
8.85711686593484));
#405605=CARTESIAN_POINT('Ctrl Pts',(0.527270584603695,-2.61810299364326,
8.85933012996512));
#405606=CARTESIAN_POINT('Ctrl Pts',(0.531096423211032,-2.63579675286366,
8.82945683644723));
#405607=CARTESIAN_POINT('Ctrl Pts',(0.534847887930047,-2.64033504482779,
8.83607469902389));
#405608=CARTESIAN_POINT('Ctrl Pts',(0.542512653014795,-2.63649012367215,
8.8382956714852));
#405609=CARTESIAN_POINT('Ctrl Pts',(0.546279125935881,-2.65416385556391,
8.80838214965004));
#405610=CARTESIAN_POINT('Ctrl Pts',(0.550045395686181,-2.65872005774702,
8.81501364461989));
#405611=CARTESIAN_POINT('Ctrl Pts',(0.55773108530596,-2.65484978803238,
8.81722098428722));
#405612=CARTESIAN_POINT('Ctrl Pts',(0.561440886005621,-2.67250562312428,
8.78727029226991));
#405613=CARTESIAN_POINT('Ctrl Pts',(0.565207781345706,-2.67706258210756,
8.79393457792714));
#405614=CARTESIAN_POINT('Ctrl Pts',(0.572927672898325,-2.67318409147407,
8.79610912703474));
#405615=CARTESIAN_POINT('Origin',(0.52552553268771,-2.60943813393231,8.85049129520029));
#405616=CARTESIAN_POINT('Ctrl Pts',(0.50403663157861,-2.6197108805292,8.85049129520029));
#405617=CARTESIAN_POINT('Ctrl Pts',(0.502277013195099,-2.62527908089983,
8.85711686593484));
#405618=CARTESIAN_POINT('Ctrl Pts',(0.493751728365472,-2.62463079031094,
8.85933012996512));
#405619=CARTESIAN_POINT('Ctrl Pts',(0.505593340562145,-2.61478477403911,
8.86332496987232));
#405620=CARTESIAN_POINT('Ctrl Pts',(0.50112017184679,-2.61594350438771,
8.86648636486738));
#405621=CARTESIAN_POINT('Ctrl Pts',(0.498123021571862,-2.61085496902651,
8.87206031107457));
#405622=CARTESIAN_POINT('Ctrl Pts',(0.512577143703202,-2.61339326418189,
8.86341338519875));
#405623=CARTESIAN_POINT('Ctrl Pts',(0.517167288227797,-2.61275761972345,
8.86654584966055));
#405624=CARTESIAN_POINT('Ctrl Pts',(0.517980099556522,-2.60688705837627,
8.87215952290714));
#405625=CARTESIAN_POINT('Ctrl Pts',(0.515891055659684,-2.6174022316462,
8.85049129520029));
#405626=CARTESIAN_POINT('Ctrl Pts',(0.51961163730155,-2.62190316315749,
8.85711686593484));
#405627=CARTESIAN_POINT('Ctrl Pts',(0.527270584603694,-2.61810299364326,
8.85933012996512));
#405628=CARTESIAN_POINT('Origin',(0.492117610277408,-2.61594432623894,8.85049129520029));
#405629=CARTESIAN_POINT('Ctrl Pts',(0.482494215215367,-2.68788048588351,
8.78727029226991));
#405630=CARTESIAN_POINT('Ctrl Pts',(0.480712693150486,-2.69351799905962,
8.79393457792714));
#405631=CARTESIAN_POINT('Ctrl Pts',(0.47210152674199,-2.69281998167918,
8.79610912703474));
#405632=CARTESIAN_POINT('Ctrl Pts',(0.489664844518297,-2.66518948588238,
8.80838214965003));
#405633=CARTESIAN_POINT('Ctrl Pts',(0.48788361832092,-2.67082606280454,
8.81501364461989));
#405634=CARTESIAN_POINT('Ctrl Pts',(0.479307239296731,-2.67012283067463,
8.81722098428721));
#405635=CARTESIAN_POINT('Ctrl Pts',(0.496845378477128,-2.6424671432281,
8.82945683644723));
#405636=CARTESIAN_POINT('Ctrl Pts',(0.49507115419714,-2.64808156302841,
8.83607469902391));
#405637=CARTESIAN_POINT('Ctrl Pts',(0.486523682952896,-2.64739397461502,
8.8382956714852));
#405638=CARTESIAN_POINT('Ctrl Pts',(0.50403663157861,-2.6197108805292,8.85049129520029));
#405639=CARTESIAN_POINT('Ctrl Pts',(0.502277013195099,-2.62527908089983,
8.85711686593484));
#405640=CARTESIAN_POINT('Ctrl Pts',(0.493751728365472,-2.62463079031094,
8.85933012996512));
#405641=CARTESIAN_POINT('Origin',(0.470575193914165,-2.68411393159325,8.78727029226991));
#405642=CARTESIAN_POINT('Ctrl Pts',(0.478324646131857,-2.70107476062509,
8.75374538247847));
#405643=CARTESIAN_POINT('Ctrl Pts',(0.476047406919821,-2.70832448889302,
8.75304829418602));
#405644=CARTESIAN_POINT('Ctrl Pts',(0.46852170749443,-2.70960296117184,
8.75272238421917));
#405645=CARTESIAN_POINT('Ctrl Pts',(0.477926903323322,-2.70233339384104,
8.76769408445022));
#405646=CARTESIAN_POINT('Ctrl Pts',(0.475591700278409,-2.70976535062987,
8.76974318093968));
#405647=CARTESIAN_POINT('Ctrl Pts',(0.468179438674307,-2.71120643882727,
8.77077869880429));
#405648=CARTESIAN_POINT('Ctrl Pts',(0.479965506394863,-2.6958823569765,
8.78108014887987));
#405649=CARTESIAN_POINT('Ctrl Pts',(0.477990130614244,-2.70218181154225,
8.78639403366326));
#405650=CARTESIAN_POINT('Ctrl Pts',(0.469936666898026,-2.70299654947582,
8.78812224174742));
#405651=CARTESIAN_POINT('Ctrl Pts',(0.483306326769365,-2.68531053162587,
8.78944554828686));
#405652=CARTESIAN_POINT('Ctrl Pts',(0.481646894576993,-2.69062115328588,
8.79673892988685));
#405653=CARTESIAN_POINT('Ctrl Pts',(0.472791874487174,-2.68957608222346,
8.79894799272499));
#405654=CARTESIAN_POINT('Origin',(0.466349848864478,-2.6974847670495,8.75721825406948));
#405655=CARTESIAN_POINT('Origin',(0.466349848864478,-2.6974847670495,9.));
#405656=CARTESIAN_POINT('Origin',(0.466349848864479,-2.6974847670495,7.51860402984325));
#405657=CARTESIAN_POINT('Ctrl Pts',(0.486543054373036,-2.70289632259342,
7.50366195182966));
#405658=CARTESIAN_POINT('Ctrl Pts',(0.487191808179173,-2.70650034953686,
7.50000065167735));
#405659=CARTESIAN_POINT('Ctrl Pts',(0.487191808179058,-2.70650034953688,
7.49482233047108));
#405660=CARTESIAN_POINT('Ctrl Pts',(0.479638433643629,-2.70566760608482,
7.50215800491338));
#405661=CARTESIAN_POINT('Ctrl Pts',(0.477809241429477,-2.70818926288502,
7.49877273257264));
#405662=CARTESIAN_POINT('Ctrl Pts',(0.474411728045476,-2.70880086664193,
7.49481816995649));
#405663=CARTESIAN_POINT('Ctrl Pts',(0.477419885150982,-2.70393900580488,
7.51043025814042));
#405664=CARTESIAN_POINT('Ctrl Pts',(0.474203815632252,-2.70881236746162,
7.51006209594516));
#405665=CARTESIAN_POINT('Ctrl Pts',(0.468476805372746,-2.70980248040963,
7.50731281821699));
#405666=CARTESIAN_POINT('Ctrl Pts',(0.478269325502402,-2.70124988015243,
7.51860402984326));
#405667=CARTESIAN_POINT('Ctrl Pts',(0.475977343984493,-2.70850576315261,
7.51860402984326));
#405668=CARTESIAN_POINT('Ctrl Pts',(0.468479300229151,-2.70980204909082,
7.51860402984327));
#405669=CARTESIAN_POINT('Origin',(0.,0.,7.5));
#405670=CARTESIAN_POINT('Origin',(0.670846486662646,-2.58203466569846,7.5));
#405671=CARTESIAN_POINT('',(0.670846486662646,-2.58203466569846,7.59394543036555));
#405672=CARTESIAN_POINT('',(0.670846486662646,-2.58203466569846,8.85049129520029));
#405673=CARTESIAN_POINT('',(0.670846486662646,-2.58203466569846,7.5));
#405674=CARTESIAN_POINT('',(0.653715973115287,-2.65144443664272,8.78727029226991));
#405675=CARTESIAN_POINT('Ctrl Pts',(0.670846486662646,-2.58203466569846,
8.85049129520029));
#405676=CARTESIAN_POINT('Ctrl Pts',(0.665128015193379,-2.60520488728789,
8.82945686509571));
#405677=CARTESIAN_POINT('Ctrl Pts',(0.659418044923419,-2.62834066354123,
8.80838212259896));
#405678=CARTESIAN_POINT('Ctrl Pts',(0.653715973115287,-2.65144443664272,
8.78727029226991));
#405679=CARTESIAN_POINT('',(0.65035598185918,-2.66505851907033,8.75721825406948));
#405680=CARTESIAN_POINT('Origin',(0.660467557061559,-2.62408907064178,8.75937679713108));
#405681=CARTESIAN_POINT('',(0.65035598185918,-2.66505851907033,7.51860402984325));
#405682=CARTESIAN_POINT('',(0.65035598185918,-2.66505851907033,7.5));
#405683=CARTESIAN_POINT('Ctrl Pts',(0.65035598185918,-2.66505851907033,
7.51860402984325));
#405684=CARTESIAN_POINT('Ctrl Pts',(0.652994732413366,-2.65436677471377,
7.52834476460825));
#405685=CARTESIAN_POINT('Ctrl Pts',(0.655635196006342,-2.64366808943105,
7.53807742314407));
#405686=CARTESIAN_POINT('Ctrl Pts',(0.658277430155653,-2.63296223017134,
7.54780169004674));
#405687=CARTESIAN_POINT('Ctrl Pts',(0.662462586247591,-2.61600472770628,
7.5632044032688));
#405688=CARTESIAN_POINT('Ctrl Pts',(0.666652189758578,-2.59902920509617,
7.57858609112103));
#405689=CARTESIAN_POINT('Ctrl Pts',(0.670846486662646,-2.58203466569846,
7.59394543036555));
#405690=CARTESIAN_POINT('Origin',(0.870959027955008,-2.77926849494597,7.5));
#405691=CARTESIAN_POINT('',(0.741123661093039,-2.6412564305984,8.75721825406948));
#405692=CARTESIAN_POINT('',(0.731515368664242,-2.6310430326237,8.78727029226991));
#405693=CARTESIAN_POINT('Origin',(0.707125938766795,-2.60511761915769,8.75658640621103));
#405694=CARTESIAN_POINT('',(0.682528638916271,-2.57897124462358,8.85049129520029));
#405695=CARTESIAN_POINT('Ctrl Pts',(0.731515368664242,-2.6310430326237,
8.78727029226991));
#405696=CARTESIAN_POINT('Ctrl Pts',(0.715209619867144,-2.61371038970358,
8.80838212259895));
#405697=CARTESIAN_POINT('Ctrl Pts',(0.698881284484194,-2.59635373775253,
8.82945686509571));
#405698=CARTESIAN_POINT('Ctrl Pts',(0.682528638916271,-2.57897124462358,
8.85049129520029));
#405699=CARTESIAN_POINT('',(0.682528638916271,-2.57897124462358,7.59394543036555));
#405700=CARTESIAN_POINT('',(0.682528638916271,-2.57897124462358,7.5));
#405701=CARTESIAN_POINT('',(0.741123661093039,-2.6412564305984,7.51860402984325));
#405702=CARTESIAN_POINT('Ctrl Pts',(0.682528638916271,-2.57897124462358,
7.59394543036555));
#405703=CARTESIAN_POINT('Ctrl Pts',(0.694522727030107,-2.59172068955962,
7.57858609112103));
#405704=CARTESIAN_POINT('Ctrl Pts',(0.706503393831167,-2.60445586794314,
7.56320440326857));
#405705=CARTESIAN_POINT('Ctrl Pts',(0.7184713427115,-2.61717752746397,7.54780169004651));
#405706=CARTESIAN_POINT('Ctrl Pts',(0.726027123794494,-2.6252091522071,
7.53807742314383));
#405707=CARTESIAN_POINT('Ctrl Pts',(0.733577841762352,-2.63323539497312,
7.52834476460825));
#405708=CARTESIAN_POINT('Ctrl Pts',(0.74112366109304,-2.6412564305984,7.51860402984325));
#405709=CARTESIAN_POINT('',(0.741123661093039,-2.6412564305984,7.5));
#405710=CARTESIAN_POINT('Origin',(0.677521207658211,-2.58368200434955,7.5));
#405711=CARTESIAN_POINT('Ctrl Pts',(0.682528638916271,-2.57897124462358,
8.85049129520029));
#405712=CARTESIAN_POINT('Ctrl Pts',(0.682395941778447,-2.57883019056129,
8.85097269580138));
#405713=CARTESIAN_POINT('Ctrl Pts',(0.682258792377727,-2.57869667966878,
8.85143669361005));
#405714=CARTESIAN_POINT('Ctrl Pts',(0.682110265580004,-2.57856519066829,
8.8519052845931));
#405715=CARTESIAN_POINT('Ctrl Pts',(0.681819756582884,-2.57830800652207,
8.85282181883899));
#405716=CARTESIAN_POINT('Ctrl Pts',(0.681493063938937,-2.57806532082595,
8.85372622499636));
#405717=CARTESIAN_POINT('Ctrl Pts',(0.681115866722558,-2.57784570272727,
8.85462257735071));
#405718=CARTESIAN_POINT('Ctrl Pts',(0.680802730990299,-2.57766338358185,
8.85536669723986));
#405719=CARTESIAN_POINT('Ctrl Pts',(0.680454733368203,-2.57749689311832,
8.85610498449051));
#405720=CARTESIAN_POINT('Ctrl Pts',(0.680060197116754,-2.57735833882344,
8.85681338218371));
#405721=CARTESIAN_POINT('Ctrl Pts',(0.679702154848935,-2.57723260058324,
8.85745625420284));
#405722=CARTESIAN_POINT('Ctrl Pts',(0.679301492304172,-2.57712772749012,
8.85808743050665));
#405723=CARTESIAN_POINT('Ctrl Pts',(0.678839734209363,-2.57706554866298,
8.85866804508409));
#405724=CARTESIAN_POINT('Ctrl Pts',(0.678626689034105,-2.57703686070001,
8.85893592806395));
#405725=CARTESIAN_POINT('Ctrl Pts',(0.67840050506838,-2.57701746342574,
8.85919241173848));
#405726=CARTESIAN_POINT('Ctrl Pts',(0.678158684088304,-2.57701094304344,
8.85943017985534));
#405727=CARTESIAN_POINT('Ctrl Pts',(0.677832154178531,-2.5770021385971,
8.8597512372));
#405728=CARTESIAN_POINT('Ctrl Pts',(0.677468785008082,-2.57701722880275,
8.86004599534705));
#405729=CARTESIAN_POINT('Ctrl Pts',(0.677073374472439,-2.57706643848078,
8.86026130871721));
#405730=CARTESIAN_POINT('Ctrl Pts',(0.676928603527537,-2.57708445553127,
8.86034014101235));
#405731=CARTESIAN_POINT('Ctrl Pts',(0.676777361302722,-2.57710730469717,
8.86040910639692));
#405732=CARTESIAN_POINT('Ctrl Pts',(0.676623818556266,-2.57713469607019,
8.86046313645506));
#405733=CARTESIAN_POINT('Ctrl Pts',(0.676384216386331,-2.57717744007839,
8.86054744990829));
#405734=CARTESIAN_POINT('Ctrl Pts',(0.676132497543417,-2.5772325565079,
8.86059655985669));
#405735=CARTESIAN_POINT('Ctrl Pts',(0.675884742861737,-2.57729622439678,
8.86059725258816));
#405736=CARTESIAN_POINT('Ctrl Pts',(0.675636415767763,-2.57736003938391,
8.86059794692011));
#405737=CARTESIAN_POINT('Ctrl Pts',(0.675389978449765,-2.57743572627043,
8.86056369958366));
#405738=CARTESIAN_POINT('Ctrl Pts',(0.675157766911382,-2.57751555979232,
8.86048590497774));
#405739=CARTESIAN_POINT('Ctrl Pts',(0.675097166613635,-2.5775363939646,
8.86046560290182));
#405740=CARTESIAN_POINT('Ctrl Pts',(0.675036776242778,-2.57755786724414,
8.86044257503091));
#405741=CARTESIAN_POINT('Ctrl Pts',(0.674978450913656,-2.57757928515972,
8.86041778462583));
#405742=CARTESIAN_POINT('Ctrl Pts',(0.674585993824371,-2.57772340115413,
8.86025097596201));
#405743=CARTESIAN_POINT('Ctrl Pts',(0.674234485840269,-2.57788466047735,
8.8599848982295));
#405744=CARTESIAN_POINT('Ctrl Pts',(0.673930653710918,-2.57805065560952,
8.85968173251462));
#405745=CARTESIAN_POINT('Ctrl Pts',(0.673769943921998,-2.57813845752406,
8.85952137522077));
#405746=CARTESIAN_POINT('Ctrl Pts',(0.673619383548732,-2.57822910929007,
8.85934740853961));
#405747=CARTESIAN_POINT('Ctrl Pts',(0.673480293963292,-2.57832000073264,
8.8591675900182));
#405748=CARTESIAN_POINT('Ctrl Pts',(0.672921776980423,-2.57868497711901,
8.85844552518695));
#405749=CARTESIAN_POINT('Ctrl Pts',(0.672514998205092,-2.57907191274903,
8.85759444184125));
#405750=CARTESIAN_POINT('Ctrl Pts',(0.67221166989639,-2.57941718972865,
8.85683498915139));
#405751=CARTESIAN_POINT('Ctrl Pts',(0.672179927396713,-2.57945332204502,
8.85675551444998));
#405752=CARTESIAN_POINT('Ctrl Pts',(0.672149335081563,-2.57948900814192,
8.85667699793652));
#405753=CARTESIAN_POINT('Ctrl Pts',(0.672119849310388,-2.57952418108657,
8.85659965593547));
#405754=CARTESIAN_POINT('Ctrl Pts',(0.671721848866504,-2.57999894728824,
8.85555568965886));
#405755=CARTESIAN_POINT('Ctrl Pts',(0.671407911415544,-2.58051270616165,
8.85434650606346));
#405756=CARTESIAN_POINT('Ctrl Pts',(0.671171181984431,-2.58106475696341,
8.85297329937117));
#405757=CARTESIAN_POINT('Ctrl Pts',(0.671038036103566,-2.58137525190245,
8.85220095427747));
#405758=CARTESIAN_POINT('Ctrl Pts',(0.670929549231057,-2.58169811105686,
8.85137579139184));
#405759=CARTESIAN_POINT('Ctrl Pts',(0.670846486662646,-2.58203466569846,
8.85049129520029));
#405760=CARTESIAN_POINT('Origin',(0.677521207658211,-2.58368200434955,7.59394543036555));
#405761=CARTESIAN_POINT('Ctrl Pts',(0.682143374360212,-2.57856171709663,
7.59443877723642));
#405762=CARTESIAN_POINT('Ctrl Pts',(0.678175520124406,-2.57434397760585,
7.58783886950016));
#405763=CARTESIAN_POINT('Ctrl Pts',(0.670813608404349,-2.57857262246712,
7.58559994247159));
#405764=CARTESIAN_POINT('Ctrl Pts',(0.703803774221571,-2.60158623323358,
7.56670252222133));
#405765=CARTESIAN_POINT('Ctrl Pts',(0.699841654661642,-2.59737458957381,
7.56004874999028));
#405766=CARTESIAN_POINT('Ctrl Pts',(0.692425479350867,-2.60160976383429,
7.55786368756704));
#405767=CARTESIAN_POINT('Ctrl Pts',(0.725423725450355,-2.6245677533871,
7.53888913333561));
#405768=CARTESIAN_POINT('Ctrl Pts',(0.72143805881991,-2.62033107972281,
7.5322200213728));
#405769=CARTESIAN_POINT('Ctrl Pts',(0.713998608634764,-2.62460390380804,
7.53005029815326));
#405770=CARTESIAN_POINT('Ctrl Pts',(0.747002249729082,-2.64750523762779,
7.51101258149734));
#405771=CARTESIAN_POINT('Ctrl Pts',(0.742968269576908,-2.6432172077805,
7.5043616886572));
#405772=CARTESIAN_POINT('Ctrl Pts',(0.735531870110738,-2.647553962849,7.50217374673251));
#405773=CARTESIAN_POINT('',(0.73438282836693,-2.64632931751459,7.50366116523517));
#405774=CARTESIAN_POINT('Ctrl Pts',(0.74112366109304,-2.6412564305984,7.51860402984325));
#405775=CARTESIAN_POINT('Ctrl Pts',(0.741426253722739,-2.64157807973369,
7.51734760759494));
#405776=CARTESIAN_POINT('Ctrl Pts',(0.741656354716104,-2.64190950301716,
7.51608817408573));
#405777=CARTESIAN_POINT('Ctrl Pts',(0.741802465711226,-2.642257553818,7.5148100591312));
#405778=CARTESIAN_POINT('Ctrl Pts',(0.741934816542043,-2.64257282655033,
7.51365231206384));
#405779=CARTESIAN_POINT('Ctrl Pts',(0.741998669384426,-2.64290209001152,
7.51247773061043));
#405780=CARTESIAN_POINT('Ctrl Pts',(0.741956669655458,-2.64324667653265,
7.51129758471022));
#405781=CARTESIAN_POINT('Ctrl Pts',(0.741904468788902,-2.64367495822514,
7.50983079813401));
#405782=CARTESIAN_POINT('Ctrl Pts',(0.741677487599955,-2.64411166614862,
7.50839324291155));
#405783=CARTESIAN_POINT('Ctrl Pts',(0.741200920369,-2.64452196792184,7.50715379678855));
#405784=CARTESIAN_POINT('Ctrl Pts',(0.740980760040254,-2.64471151551851,
7.50658120839351));
#405785=CARTESIAN_POINT('Ctrl Pts',(0.740669836489923,-2.64491517281699,
7.50598221009429));
#405786=CARTESIAN_POINT('Ctrl Pts',(0.74026308577848,-2.6451090650682,7.50545747549611));
#405787=CARTESIAN_POINT('Ctrl Pts',(0.740046031008742,-2.64521253197498,
7.50517746087247));
#405788=CARTESIAN_POINT('Ctrl Pts',(0.739799421791916,-2.64531452291221,
7.50491486231392));
#405789=CARTESIAN_POINT('Ctrl Pts',(0.739529151276123,-2.64541079559313,
7.50468370960992));
#405790=CARTESIAN_POINT('Ctrl Pts',(0.739125011603008,-2.64555475361861,
7.50433806340446));
#405791=CARTESIAN_POINT('Ctrl Pts',(0.738655660604345,-2.64568971815751,
7.50405484070983));
#405792=CARTESIAN_POINT('Ctrl Pts',(0.738152510216528,-2.64580591110398,
7.5038576603613));
#405793=CARTESIAN_POINT('Ctrl Pts',(0.738098706103284,-2.64581833613356,
7.50383657498791));
#405794=CARTESIAN_POINT('Ctrl Pts',(0.738044542534841,-2.64583055506889,
7.50381643264937));
#405795=CARTESIAN_POINT('Ctrl Pts',(0.737990077468983,-2.64584256247728,
7.50379723213559));
#405796=CARTESIAN_POINT('Ctrl Pts',(0.737626505337586,-2.64592271585613,
7.50366906242519));
#405797=CARTESIAN_POINT('Ctrl Pts',(0.737241435141454,-2.64599448492876,
7.50358235568538));
#405798=CARTESIAN_POINT('Ctrl Pts',(0.736868612002289,-2.64605473955297,
7.5035341175365));
#405799=CARTESIAN_POINT('Ctrl Pts',(0.736309605900543,-2.64614508454246,
7.50346178989176));
#405800=CARTESIAN_POINT('Ctrl Pts',(0.735704401177955,-2.64621850689902,
7.50346967198527));
#405801=CARTESIAN_POINT('Ctrl Pts',(0.735108059804492,-2.64627230370701,
7.50354272648692));
#405802=CARTESIAN_POINT('Ctrl Pts',(0.734862772254051,-2.64629443144767,
7.50357277531559));
#405803=CARTESIAN_POINT('Ctrl Pts',(0.734619322893534,-2.64631335066844,
7.50361331098761));
#405804=CARTESIAN_POINT('Ctrl Pts',(0.734382828367309,-2.64632931751596,
7.50366116523658));
#405805=CARTESIAN_POINT('',(0.678263889301933,-2.58651417133809,7.57603338622103));
#405806=CARTESIAN_POINT('Origin',(0.680502659389328,-2.59506282024291,7.58486873427627));
#405807=CARTESIAN_POINT('Ctrl Pts',(0.734382828409904,-2.64632931755256,
7.50366116529968));
#405808=CARTESIAN_POINT('Ctrl Pts',(0.715706430670521,-2.62642404271696,
7.52783573079709));
#405809=CARTESIAN_POINT('Ctrl Pts',(0.697000987800557,-2.60648661431366,
7.55196141284068));
#405810=CARTESIAN_POINT('Ctrl Pts',(0.678263890381624,-2.58651417197205,
7.57603338728831));
#405811=CARTESIAN_POINT('Ctrl Pts',(0.683105249421544,-2.57984075934191,
7.59639677331371));
#405812=CARTESIAN_POINT('Ctrl Pts',(0.67284342550402,-2.56471571766823,
7.59959882295463));
#405813=CARTESIAN_POINT('Ctrl Pts',(0.670788463607718,-2.58289499004649,
7.59642833564546));
#405814=CARTESIAN_POINT('Ctrl Pts',(0.681462581934917,-2.57630285775875,
7.58707626057423));
#405815=CARTESIAN_POINT('Ctrl Pts',(0.675085619068564,-2.57401230419309,
7.58809943920599));
#405816=CARTESIAN_POINT('Ctrl Pts',(0.67058158747929,-2.57905493249942,
7.58710240504253));
#405817=CARTESIAN_POINT('Ctrl Pts',(0.679301722070263,-2.58198232224996,
7.58015376756929));
#405818=CARTESIAN_POINT('Ctrl Pts',(0.676766535642928,-2.58067767625402,
7.5820588065976));
#405819=CARTESIAN_POINT('Ctrl Pts',(0.675182333579464,-2.58300520259328,
7.58020924244128));
#405820=CARTESIAN_POINT('Ctrl Pts',(0.678263889092213,-2.58651417053753,
7.57603338509286));
#405821=CARTESIAN_POINT('Ctrl Pts',(0.678263889092213,-2.58651417053753,
7.57603338509286));
#405822=CARTESIAN_POINT('Ctrl Pts',(0.678263889092213,-2.58651417053753,
7.57603338509286));
#405823=CARTESIAN_POINT('Origin',(0.680508179114493,-2.59506137280058,7.58486873427621));
#405824=CARTESIAN_POINT('Ctrl Pts',(0.64829375964388,-2.67341427391705,
7.51098857897448));
#405825=CARTESIAN_POINT('Ctrl Pts',(0.649704436926231,-2.66769846237564,
7.50433767179956));
#405826=CARTESIAN_POINT('Ctrl Pts',(0.658312065540237,-2.66782800281639,
7.50214974420965));
#405827=CARTESIAN_POINT('Ctrl Pts',(0.655841875747635,-2.64283066015825,
7.53887321589163));
#405828=CARTESIAN_POINT('Ctrl Pts',(0.657235650612657,-2.63718333418287,
7.5322040745206));
#405829=CARTESIAN_POINT('Ctrl Pts',(0.66581456026676,-2.63725564648319,
7.53003438070911));
#405830=CARTESIAN_POINT('Ctrl Pts',(0.663404487018678,-2.61218831457927,
7.56669465659231));
#405831=CARTESIAN_POINT('Ctrl Pts',(0.664790024933336,-2.60657436325043,
7.56004085833297));
#405832=CARTESIAN_POINT('Ctrl Pts',(0.673330168792996,-2.60662528459036,
7.55785582193789));
#405833=CARTESIAN_POINT('Ctrl Pts',(0.67098125143039,-2.58148862301068,
7.59443891967696));
#405834=CARTESIAN_POINT('Ctrl Pts',(0.672368798202544,-2.57586653215138,
7.58783901202978));
#405835=CARTESIAN_POINT('Ctrl Pts',(0.680858439628815,-2.57593841011513,
7.58560008491213));
#405836=CARTESIAN_POINT('',(0.658718750143912,-2.66617077539049,7.50366116523517));
#405837=CARTESIAN_POINT('Ctrl Pts',(0.658718750144001,-2.66617077539085,
7.50366116523554));
#405838=CARTESIAN_POINT('Ctrl Pts',(0.658034914852376,-2.66649712920298,
7.50350835821027));
#405839=CARTESIAN_POINT('Ctrl Pts',(0.65739568666618,-2.66677487969734,
7.50345484956));
#405840=CARTESIAN_POINT('Ctrl Pts',(0.656782300120865,-2.66701283537894,
7.50349758195598));
#405841=CARTESIAN_POINT('Ctrl Pts',(0.656467587333186,-2.66713492429085,
7.50351950684424));
#405842=CARTESIAN_POINT('Ctrl Pts',(0.656128704689333,-2.66725869166959,
7.50357029184312));
#405843=CARTESIAN_POINT('Ctrl Pts',(0.655798643426452,-2.66736905658083,
7.50365515313923));
#405844=CARTESIAN_POINT('Ctrl Pts',(0.655290875549136,-2.66753884250547,
7.50378570417639));
#405845=CARTESIAN_POINT('Ctrl Pts',(0.654789190205213,-2.66768222205233,
7.50400001621911));
#405846=CARTESIAN_POINT('Ctrl Pts',(0.654331149039327,-2.66778609894424,
7.50428903009635));
#405847=CARTESIAN_POINT('Ctrl Pts',(0.654280309993871,-2.66779762848007,
7.50432110841318));
#405848=CARTESIAN_POINT('Ctrl Pts',(0.654229988079957,-2.66780869367321,
7.50435406373354));
#405849=CARTESIAN_POINT('Ctrl Pts',(0.654180219277456,-2.66781929287174,
7.50438785222352));
#405850=CARTESIAN_POINT('Ctrl Pts',(0.65387635681626,-2.66788400607338,
7.50459414719561));
#405851=CARTESIAN_POINT('Ctrl Pts',(0.653588167401578,-2.66793187430612,
7.50483629897752));
#405852=CARTESIAN_POINT('Ctrl Pts',(0.653326907123302,-2.66796236199665,
7.5050991045531));
#405853=CARTESIAN_POINT('Ctrl Pts',(0.652750540708314,-2.66802962090416,
7.50567888004914));
#405854=CARTESIAN_POINT('Ctrl Pts',(0.65228258332005,-2.66801545797236,
7.50637912803144));
#405855=CARTESIAN_POINT('Ctrl Pts',(0.651914066483551,-2.66794945334346,
7.50710440483569));
#405856=CARTESIAN_POINT('Ctrl Pts',(0.651823698839158,-2.66793326769808,
7.50728225710685));
#405857=CARTESIAN_POINT('Ctrl Pts',(0.651737486155056,-2.66791378612335,
7.50746498566954));
#405858=CARTESIAN_POINT('Ctrl Pts',(0.651657349091471,-2.66789186972997,
7.50764697238949));
#405859=CARTESIAN_POINT('Ctrl Pts',(0.651226554291956,-2.66777405323071,
7.50862528291182));
#405860=CARTESIAN_POINT('Ctrl Pts',(0.650931136910949,-2.66757917162251,
7.50965856837422));
#405861=CARTESIAN_POINT('Ctrl Pts',(0.650721061509954,-2.6673507203159,
7.51067959873203));
#405862=CARTESIAN_POINT('Ctrl Pts',(0.650605456751812,-2.66722500327372,
7.51124147302579));
#405863=CARTESIAN_POINT('Ctrl Pts',(0.650515987782613,-2.66708879554658,
7.51180065547253));
#405864=CARTESIAN_POINT('Ctrl Pts',(0.650446381268391,-2.66694758136607,
7.51235175716501));
#405865=CARTESIAN_POINT('Ctrl Pts',(0.650205863033812,-2.66645963011939,
7.51425603304536));
#405866=CARTESIAN_POINT('Ctrl Pts',(0.650179260416308,-2.66585104263315,
7.5162690050518));
#405867=CARTESIAN_POINT('Ctrl Pts',(0.650329938180127,-2.66516978271555,
7.51827788969243));
#405868=CARTESIAN_POINT('Ctrl Pts',(0.650338093145447,-2.66513291164141,
7.51838661432545));
#405869=CARTESIAN_POINT('Ctrl Pts',(0.65034677544217,-2.66509582182216,
7.51849533314856));
#405870=CARTESIAN_POINT('Ctrl Pts',(0.650355981859176,-2.66505851907033,
7.51860402984325));
#405871=CARTESIAN_POINT('Ctrl Pts',(0.678263888672342,-2.58651417242151,
7.57603338728985));
#405872=CARTESIAN_POINT('Ctrl Pts',(0.671738733242242,-2.61311115758385,
7.55196141284922));
#405873=CARTESIAN_POINT('Ctrl Pts',(0.665223977054884,-2.63966210102,7.52783573083104));
#405874=CARTESIAN_POINT('Ctrl Pts',(0.65871875012459,-2.66617077544642,
7.50366116530176));
#405875=CARTESIAN_POINT('Origin',(2.34371526914296E-16,-8.93760209386494E-16,
7.49482233047033));
#405876=CARTESIAN_POINT('Origin',(0.732019285896533,-2.63781235403043,7.49482233047033));
#405877=CARTESIAN_POINT('Origin',(0.,0.,7.50366116523517));
#405878=CARTESIAN_POINT('Origin',(0.6565987254349,-2.65758995402927,7.49482233047033));
#405879=CARTESIAN_POINT('Ctrl Pts',(0.74112293637421,-2.64125566017333,
7.51860402984325));
#405880=CARTESIAN_POINT('Ctrl Pts',(0.746336138178801,-2.6467981156738,
7.51860402984325));
#405881=CARTESIAN_POINT('Ctrl Pts',(0.753653780564807,-2.6447128348916,
7.51860402984325));
#405882=CARTESIAN_POINT('Ctrl Pts',(0.743058634706615,-2.64331361085372,
7.51041458714365));
#405883=CARTESIAN_POINT('Ctrl Pts',(0.748069768762033,-2.64630407925162,
7.51004642900442));
#405884=CARTESIAN_POINT('Ctrl Pts',(0.753655798683693,-2.64471225979592,
7.50729136483009));
#405885=CARTESIAN_POINT('Ctrl Pts',(0.741799391201317,-2.64583115787286,
7.50215815450138));
#405886=CARTESIAN_POINT('Ctrl Pts',(0.744539962382722,-2.64731012172677,
7.4987716367153));
#405887=CARTESIAN_POINT('Ctrl Pts',(0.747864531770558,-2.64638753732422,
7.49481588533172));
#405888=CARTESIAN_POINT('Ctrl Pts',(0.734382681155584,-2.64632878704413,
7.50366171572174));
#405889=CARTESIAN_POINT('Ctrl Pts',(0.735361839713041,-2.64985715930008,
7.50000045605858));
#405890=CARTESIAN_POINT('Ctrl Pts',(0.735361839713161,-2.64985715930004,
7.49482233047317));
#405891=CARTESIAN_POINT('Origin',(0.750228081562239,-2.63269141291482,7.51860402984325));
#405892=CARTESIAN_POINT('Origin',(0.750228081562239,-2.63269141291482,9.));
#405893=CARTESIAN_POINT('Origin',(0.750228081562239,-2.63269141291482,8.75721825406948));
#405894=CARTESIAN_POINT('Ctrl Pts',(0.729680709080038,-2.62909278680761,
8.78942910404913));
#405895=CARTESIAN_POINT('Ctrl Pts',(0.733484229768694,-2.63316533626375,
8.7967269950169));
#405896=CARTESIAN_POINT('Ctrl Pts',(0.741015530017009,-2.62837440706871,
8.79893251111267));
#405897=CARTESIAN_POINT('Ctrl Pts',(0.73721404019554,-2.637100554352,8.78111911759582));
#405898=CARTESIAN_POINT('Ctrl Pts',(0.741728598252154,-2.64192352809015,
8.78644465894813));
#405899=CARTESIAN_POINT('Ctrl Pts',(0.749342461395685,-2.63914061598106,
8.78817647674132));
#405900=CARTESIAN_POINT('Ctrl Pts',(0.741908991856784,-2.64209118606713,
8.76780923932031));
#405901=CARTESIAN_POINT('Ctrl Pts',(0.747241957274032,-2.64778102056637,
8.76988516158374));
#405902=CARTESIAN_POINT('Ctrl Pts',(0.754552157358074,-2.64585816978495,
8.77093053738833));
#405903=CARTESIAN_POINT('Ctrl Pts',(0.740993540539042,-2.64111808118309,
8.75371302330492));
#405904=CARTESIAN_POINT('Ctrl Pts',(0.746195062069161,-2.64666879060977,
8.75300828287559));
#405905=CARTESIAN_POINT('Ctrl Pts',(0.753536416620095,-2.64454769356067,
8.75267964240738));
#405906=CARTESIAN_POINT('Origin',(0.740619789133442,-2.62247801494012,8.78727029226991));
#405907=CARTESIAN_POINT('Ctrl Pts',(0.682528638916271,-2.57897124462358,
8.85049129520029));
#405908=CARTESIAN_POINT('Ctrl Pts',(0.686529951896168,-2.5832245500041,
8.85711686593484));
#405909=CARTESIAN_POINT('Ctrl Pts',(0.693929685372921,-2.57894147790724,
8.85933012996512));
#405910=CARTESIAN_POINT('Ctrl Pts',(0.698881306430053,-2.59635376108048,
8.82945683644722));
#405911=CARTESIAN_POINT('Ctrl Pts',(0.702915832726909,-2.60064237146728,
8.83607469902389));
#405912=CARTESIAN_POINT('Ctrl Pts',(0.710318504785506,-2.59631426692943,
8.83829567148519));
#405913=CARTESIAN_POINT('Ctrl Pts',(0.71520959897422,-2.61371036749488,
8.80838214965002));
#405914=CARTESIAN_POINT('Ctrl Pts',(0.719260047395548,-2.61801590274054,
8.81501364461988));
#405915=CARTESIAN_POINT('Ctrl Pts',(0.726681976909678,-2.6136611610855,
8.81722098428721));
#405916=CARTESIAN_POINT('Ctrl Pts',(0.731515368664242,-2.6310430326237,
8.78727029226991));
#405917=CARTESIAN_POINT('Ctrl Pts',(0.735566489878354,-2.63534928303293,
8.79393457792714));
#405918=CARTESIAN_POINT('Ctrl Pts',(0.743022024337742,-2.63098414602441,
8.79610912703474));
#405919=CARTESIAN_POINT('Origin',(0.69163305938547,-2.57040622694,8.85049129520029));
#405920=CARTESIAN_POINT('Ctrl Pts',(0.670846486662646,-2.58203466569846,
8.85049129520029));
#405921=CARTESIAN_POINT('Ctrl Pts',(0.669447239426466,-2.58770416474116,
8.85711686593484));
#405922=CARTESIAN_POINT('Ctrl Pts',(0.660897934588214,-2.58760342300925,
8.85933012996512));
#405923=CARTESIAN_POINT('Ctrl Pts',(0.672084380494145,-2.57701894173548,
8.86332496987231));
#405924=CARTESIAN_POINT('Ctrl Pts',(0.667694642491991,-2.57846188825189,
8.86648636486738));
#405925=CARTESIAN_POINT('Ctrl Pts',(0.664377626603774,-2.57357583590977,
8.87206031107456));
#405926=CARTESIAN_POINT('Ctrl Pts',(0.678964680319988,-2.57518283708093,
8.86341338519877));
#405927=CARTESIAN_POINT('Ctrl Pts',(0.683504668020099,-2.57425440705279,
8.86654584966058));
#405928=CARTESIAN_POINT('Ctrl Pts',(0.683939681183841,-2.56834383040285,
8.87215952290715));
#405929=CARTESIAN_POINT('Ctrl Pts',(0.682528638916271,-2.57897124462358,
8.85049129520029));
#405930=CARTESIAN_POINT('Ctrl Pts',(0.686529951896168,-2.5832245500041,
8.85711686593484));
#405931=CARTESIAN_POINT('Ctrl Pts',(0.693929685372921,-2.57894147790724,
8.85933012996512));
#405932=CARTESIAN_POINT('Origin',(0.658710630307072,-2.57903950451467,8.85049129520029));
#405933=CARTESIAN_POINT('Ctrl Pts',(0.653715973115287,-2.65144443664272,
8.78727029226991));
#405934=CARTESIAN_POINT('Ctrl Pts',(0.652299308087893,-2.65718450945398,
8.79393457792714));
#405935=CARTESIAN_POINT('Ctrl Pts',(0.643661112117213,-2.65703964555119,
8.79610912703474));
#405936=CARTESIAN_POINT('Ctrl Pts',(0.659418052229611,-2.62834063393785,
8.80838214965002));
#405937=CARTESIAN_POINT('Ctrl Pts',(0.658001622475823,-2.63407975346255,
8.81501364461996));
#405938=CARTESIAN_POINT('Ctrl Pts',(0.649397808304912,-2.63392745668914,
8.81722098428721));
#405939=CARTESIAN_POINT('Ctrl Pts',(0.665128007518977,-2.60520491838319,
8.82945683644723));
#405940=CARTESIAN_POINT('Ctrl Pts',(0.66371714568474,-2.61092147769581,
8.83607469902391));
#405941=CARTESIAN_POINT('Ctrl Pts',(0.655143182195968,-2.61078294036944,
8.83829567148519));
#405942=CARTESIAN_POINT('Ctrl Pts',(0.670846486662646,-2.58203466569846,
8.85049129520029));
#405943=CARTESIAN_POINT('Ctrl Pts',(0.669447239426466,-2.58770416474116,
8.85711686593484));
#405944=CARTESIAN_POINT('Ctrl Pts',(0.660897934588214,-2.58760342300925,
8.85933012996512));
#405945=CARTESIAN_POINT('Origin',(0.641580116759713,-2.64844927545893,8.78727029226991));
#405946=CARTESIAN_POINT('Ctrl Pts',(0.650400330943821,-2.66487874754016,
8.75374538247848));
#405947=CARTESIAN_POINT('Ctrl Pts',(0.648592262248902,-2.67225948368109,
8.75304829418603));
#405948=CARTESIAN_POINT('Ctrl Pts',(0.64116393718026,-2.6740175024192,8.75272238421917));
#405949=CARTESIAN_POINT('Ctrl Pts',(0.650084046247561,-2.66616027822844,
8.76769408445017));
#405950=CARTESIAN_POINT('Ctrl Pts',(0.648229808234099,-2.67372658223775,
8.76974318093967));
#405951=CARTESIAN_POINT('Ctrl Pts',(0.640925106754247,-2.67563961479641,
8.77077869880429));
#405952=CARTESIAN_POINT('Ctrl Pts',(0.651705141439437,-2.65959188196376,
8.78108014887994));
#405953=CARTESIAN_POINT('Ctrl Pts',(0.650137431720011,-2.66600495638528,
8.78639403366327));
#405954=CARTESIAN_POINT('Ctrl Pts',(0.642152715147357,-2.66733400754429,
8.78812224174742));
#405955=CARTESIAN_POINT('Ctrl Pts',(0.65436175856437,-2.64882773046581,
8.78944554828685));
#405956=CARTESIAN_POINT('Ctrl Pts',(0.653045988551392,-2.65423376106967,
8.79673892988685));
#405957=CARTESIAN_POINT('Ctrl Pts',(0.644142204117193,-2.65375818030291,
8.79894799272499));
#405958=CARTESIAN_POINT('Origin',(0.638220125503606,-2.66206335788654,8.75721825406948));
#405959=CARTESIAN_POINT('Origin',(0.638220125503606,-2.66206335788654,9.));
#405960=CARTESIAN_POINT('Origin',(0.638220125503606,-2.66206335788654,7.51860402984325));
#405961=CARTESIAN_POINT('Ctrl Pts',(0.658718561459868,-2.66617001169015,
7.50366195182966));
#405962=CARTESIAN_POINT('Ctrl Pts',(0.659596893130815,-2.66972506797464,
7.50000065167735));
#405963=CARTESIAN_POINT('Ctrl Pts',(0.659596893130701,-2.66972506797467,
7.49482233047108));
#405964=CARTESIAN_POINT('Ctrl Pts',(0.652005683757201,-2.66937798185144,
7.50215800491337));
#405965=CARTESIAN_POINT('Ctrl Pts',(0.65034181292054,-2.67201165438486,
7.49877273257267));
#405966=CARTESIAN_POINT('Ctrl Pts',(0.646990465679411,-2.67283968096613,
7.49481816995647));
#405967=CARTESIAN_POINT('Ctrl Pts',(0.649680941710166,-2.66779507605612,
7.51043025814043));
#405968=CARTESIAN_POINT('Ctrl Pts',(0.646783717304577,-2.67286447915022,
7.51006209594514));
#405969=CARTESIAN_POINT('Ctrl Pts',(0.641131910556243,-2.67421948861213,
7.50731281821701));
#405970=CARTESIAN_POINT('Ctrl Pts',(0.650356343923175,-2.66505705167055,
7.51860402984326));
#405971=CARTESIAN_POINT('Ctrl Pts',(0.648533957547086,-2.67244487444095,
7.51860402984326));
#405972=CARTESIAN_POINT('Ctrl Pts',(0.641134372652019,-2.67421889833351,
7.51860402984327));
#405973=CARTESIAN_POINT('Origin',(0.,0.,7.5));
#405974=CARTESIAN_POINT('Origin',(0.834899689636865,-2.53374831658167,7.5));
#405975=CARTESIAN_POINT('',(0.834899689636865,-2.53374831658167,7.59394543036555));
#405976=CARTESIAN_POINT('',(0.834899689636865,-2.53374831658167,8.85049129520029));
#405977=CARTESIAN_POINT('',(0.834899689636865,-2.53374831658167,7.5));
#405978=CARTESIAN_POINT('',(0.82225147186004,-2.60411303347871,8.78727029226991));
#405979=CARTESIAN_POINT('Ctrl Pts',(0.834899689636865,-2.53374831658167,
8.85049129520029));
#405980=CARTESIAN_POINT('Ctrl Pts',(0.830677488574773,-2.55723731619084,
8.82945686509571));
#405981=CARTESIAN_POINT('Ctrl Pts',(0.826461564325102,-2.58069139656183,
8.80838212259895));
#405982=CARTESIAN_POINT('Ctrl Pts',(0.82225147186004,-2.60411303347871,
8.78727029226991));
#405983=CARTESIAN_POINT('',(0.819770641322299,-2.61791441969278,8.75721825406948));
#405984=CARTESIAN_POINT('Origin',(0.827236519635628,-2.57638129654257,8.75937679713113));
#405985=CARTESIAN_POINT('',(0.819770641322299,-2.61791441969278,7.51860402984325));
#405986=CARTESIAN_POINT('',(0.819770641322299,-2.61791441969278,7.5));
#405987=CARTESIAN_POINT('Ctrl Pts',(0.819770641322299,-2.61791441969278,
7.51860402984325));
#405988=CARTESIAN_POINT('Ctrl Pts',(0.821718947867565,-2.6070755773432,
7.52834476460825));
#405989=CARTESIAN_POINT('Ctrl Pts',(0.823668519225332,-2.59622969857357,
7.53807742314407));
#405990=CARTESIAN_POINT('Ctrl Pts',(0.825619397863352,-2.58537654712672,
7.54780169004674));
#405991=CARTESIAN_POINT('Ctrl Pts',(0.828709484189983,-2.5681857417977,
7.5632044032688));
#405992=CARTESIAN_POINT('Ctrl Pts',(0.831802854243305,-2.55097666840083,
7.57858609112103));
#405993=CARTESIAN_POINT('Ctrl Pts',(0.834899689636865,-2.53374831658167,
7.59394543036555));
#405994=CARTESIAN_POINT('Origin',(1.04723789307866,-2.71775565323223,7.5));
#405995=CARTESIAN_POINT('',(0.908826823579973,-2.58834572998873,8.75721825406948));
#405996=CARTESIAN_POINT('',(0.898583897763467,-2.5787689219451,8.78727029226991));
#405997=CARTESIAN_POINT('Origin',(0.872583531618111,-2.55445941115698,8.7565864062094));
#405998=CARTESIAN_POINT('',(0.846361565593617,-2.5299427115692,8.85049129520029));
#405999=CARTESIAN_POINT('Ctrl Pts',(0.898583897763467,-2.5787689219451,
8.78727029226991));
#406000=CARTESIAN_POINT('Ctrl Pts',(0.881201144631321,-2.56251660371117,
8.80838212259895));
#406001=CARTESIAN_POINT('Ctrl Pts',(0.863794313055989,-2.54624177290295,
8.82945686509571));
#406002=CARTESIAN_POINT('Ctrl Pts',(0.846361565593617,-2.5299427115692,
8.85049129520029));
#406003=CARTESIAN_POINT('',(0.846361565593617,-2.5299427115692,7.59394543036555));
#406004=CARTESIAN_POINT('',(0.846361565593617,-2.5299427115692,7.5));
#406005=CARTESIAN_POINT('',(0.908826823579973,-2.58834572998873,7.51860402984325));
#406006=CARTESIAN_POINT('Ctrl Pts',(0.846361565593617,-2.5299427115692,
7.59394543036555));
#406007=CARTESIAN_POINT('Ctrl Pts',(0.859147870308745,-2.54189749753932,
7.57858609112103));
#406008=CARTESIAN_POINT('Ctrl Pts',(0.871919867225465,-2.55383890617555,
7.56320440326857));
#406009=CARTESIAN_POINT('Ctrl Pts',(0.884678306195284,-2.56576763856503,
7.54780169004651));
#406010=CARTESIAN_POINT('Ctrl Pts',(0.892733151079782,-2.57329866091762,
7.53807742314383));
#406011=CARTESIAN_POINT('Ctrl Pts',(0.9007825984274,-2.58082463674584,7.52834476460825));
#406012=CARTESIAN_POINT('Ctrl Pts',(0.908826823579971,-2.58834572998873,
7.51860402984325));
#406013=CARTESIAN_POINT('',(0.908826823579973,-2.58834572998873,7.5));
#406014=CARTESIAN_POINT('Origin',(0.841666242052041,-2.53496461975633,7.5));
#406015=CARTESIAN_POINT('Ctrl Pts',(0.846361565593617,-2.5299427115692,
8.85049129520029));
#406016=CARTESIAN_POINT('Ctrl Pts',(0.846220103731495,-2.52981044925243,
8.85097269580138));
#406017=CARTESIAN_POINT('Ctrl Pts',(0.846074682046675,-2.52968599986464,
8.85143669361005));
#406018=CARTESIAN_POINT('Ctrl Pts',(0.845918035884,-2.529564297167,8.8519052845931));
#406019=CARTESIAN_POINT('Ctrl Pts',(0.845611645923948,-2.52932625440854,
8.85282181883899));
#406020=CARTESIAN_POINT('Ctrl Pts',(0.845270075579139,-2.52910499860577,
8.85372622499635));
#406021=CARTESIAN_POINT('Ctrl Pts',(0.844879582375002,-2.52890999884467,
8.8546225773507));
#406022=CARTESIAN_POINT('Ctrl Pts',(0.844555408785934,-2.52874811696874,
8.85536669723986));
#406023=CARTESIAN_POINT('Ctrl Pts',(0.844197459081652,-2.52860426486191,
8.85610498449051));
#406024=CARTESIAN_POINT('Ctrl Pts',(0.843794856243094,-2.52849127326612,
8.85681338218371));
#406025=CARTESIAN_POINT('Ctrl Pts',(0.843429493534804,-2.52838873321548,
8.85745625420284));
#406026=CARTESIAN_POINT('Ctrl Pts',(0.843022934952063,-2.52830974613275,
8.85808743050665));
#406027=CARTESIAN_POINT('Ctrl Pts',(0.842558141777651,-2.5282772800014,
8.8586680450841));
#406028=CARTESIAN_POINT('Ctrl Pts',(0.842343696282456,-2.52826230083217,
8.85893592806395));
#406029=CARTESIAN_POINT('Ctrl Pts',(0.842116734248318,-2.52825743506811,
8.85919241173848));
#406030=CARTESIAN_POINT('Ctrl Pts',(0.841874992353052,-2.52826642160603,
8.85943017985534));
#406031=CARTESIAN_POINT('Ctrl Pts',(0.841548569231186,-2.52827855609252,
8.8597512372));
#406032=CARTESIAN_POINT('Ctrl Pts',(0.841186913474463,-2.52831689643641,
8.86004599534706));
#406033=CARTESIAN_POINT('Ctrl Pts',(0.84079546822707,-2.52839133904788,
8.86026130871721));
#406034=CARTESIAN_POINT('Ctrl Pts',(0.840652149085989,-2.5284185945867,
8.86034014101236));
#406035=CARTESIAN_POINT('Ctrl Pts',(0.840502681555632,-2.52845108692915,
8.86040910639693));
#406036=CARTESIAN_POINT('Ctrl Pts',(0.84035120925051,-2.5284882595412,8.86046313645507));
#406037=CARTESIAN_POINT('Ctrl Pts',(0.840114837986938,-2.52854626709098,
8.8605474499083));
#406038=CARTESIAN_POINT('Ctrl Pts',(0.839867167649147,-2.52861739795951,
8.86059655985669));
#406039=CARTESIAN_POINT('Ctrl Pts',(0.839624001221678,-2.52869680873284,
8.86059725258816));
#406040=CARTESIAN_POINT('Ctrl Pts',(0.839380272982615,-2.52877640297677,
8.86059794692011));
#406041=CARTESIAN_POINT('Ctrl Pts',(0.839139191271985,-2.52886772364964,
8.86056369958366));
#406042=CARTESIAN_POINT('Ctrl Pts',(0.838912571788422,-2.52896227098934,
8.86048590497774));
#406043=CARTESIAN_POINT('Ctrl Pts',(0.838853430850487,-2.52898694502999,
8.86046560290182));
#406044=CARTESIAN_POINT('Ctrl Pts',(0.838794540355868,-2.52901224341473,
8.86044257503091));
#406045=CARTESIAN_POINT('Ctrl Pts',(0.838737707112953,-2.52903735424157,
8.86041778462583));
#406046=CARTESIAN_POINT('Ctrl Pts',(0.838355289912312,-2.52920631894625,
8.860250975962));
#406047=CARTESIAN_POINT('Ctrl Pts',(0.838014836059376,-2.52938976813877,
8.8599848982295));
#406048=CARTESIAN_POINT('Ctrl Pts',(0.837722263530355,-2.5295748888075,
8.85968173251461));
#406049=CARTESIAN_POINT('Ctrl Pts',(0.837567509424911,-2.52967280703511,
8.85952137522076));
#406050=CARTESIAN_POINT('Ctrl Pts',(0.837423066472669,-2.52977291898358,
8.85934740853961));
#406051=CARTESIAN_POINT('Ctrl Pts',(0.83729008609642,-2.52987253518028,
8.8591675900182));
#406052=CARTESIAN_POINT('Ctrl Pts',(0.83675610076395,-2.53027254598948,
8.85844552518695));
#406053=CARTESIAN_POINT('Ctrl Pts',(0.836374948810173,-2.53068474902437,
8.85759444184123));
#406054=CARTESIAN_POINT('Ctrl Pts',(0.836094365694051,-2.53104875090687,
8.85683498915137));
#406055=CARTESIAN_POINT('Ctrl Pts',(0.836065003418205,-2.53108684273445,
8.85675551444997));
#406056=CARTESIAN_POINT('Ctrl Pts',(0.836036760374328,-2.5311244155668,
8.85667699793651));
#406057=CARTESIAN_POINT('Ctrl Pts',(0.836009588723137,-2.53116140540471,
8.85659965593547));
#406058=CARTESIAN_POINT('Ctrl Pts',(0.83564282438883,-2.53166069612428,
8.85555568965886));
#406059=CARTESIAN_POINT('Ctrl Pts',(0.835362448600069,-2.53219351346653,
8.85434650606346));
#406060=CARTESIAN_POINT('Ctrl Pts',(0.835161575571271,-2.53275959732744,
8.85297329937117));
#406061=CARTESIAN_POINT('Ctrl Pts',(0.835048596731946,-2.53307798500721,
8.85220095427747));
#406062=CARTESIAN_POINT('Ctrl Pts',(0.834961018414397,-2.53340713159064,
8.85137579139183));
#406063=CARTESIAN_POINT('Ctrl Pts',(0.834899689636865,-2.53374831658167,
8.85049129520029));
#406064=CARTESIAN_POINT('Origin',(0.841666242052041,-2.53496461975633,7.59394543036555));
#406065=CARTESIAN_POINT('Ctrl Pts',(0.845950854086167,-2.52955870944533,
7.59443877723642));
#406066=CARTESIAN_POINT('Ctrl Pts',(0.841720920735444,-2.52560385704642,
7.58783886950016));
#406067=CARTESIAN_POINT('Ctrl Pts',(0.83464506505906,-2.53029549300669,
7.58559994247159));
#406068=CARTESIAN_POINT('Ctrl Pts',(0.869041936146793,-2.55114813266053,
7.56670252222135));
#406069=CARTESIAN_POINT('Ctrl Pts',(0.864818116250616,-2.54719899614619,
7.56004874999028));
#406070=CARTESIAN_POINT('Ctrl Pts',(0.857688526813998,-2.55190062477045,
7.55786368756704));
#406071=CARTESIAN_POINT('Ctrl Pts',(0.892089897918742,-2.5726972397849,
7.53888913333557));
#406072=CARTESIAN_POINT('Ctrl Pts',(0.887840975654144,-2.56872463335888,
7.53222002137276));
#406073=CARTESIAN_POINT('Ctrl Pts',(0.88069057139642,-2.57346532567864,
7.53005029815327));
#406074=CARTESIAN_POINT('Ctrl Pts',(0.915093696466176,-2.59420505570681,
7.51101258149734));
#406075=CARTESIAN_POINT('Ctrl Pts',(0.910793269543267,-2.59018429407247,
7.5043616886572));
#406076=CARTESIAN_POINT('Ctrl Pts',(0.903650005808594,-2.59498859056224,
7.50217374673251));
#406077=CARTESIAN_POINT('',(0.902424861598309,-2.5938400807503,7.50366116523517));
#406078=CARTESIAN_POINT('Ctrl Pts',(0.908826823579973,-2.58834572998873,
7.51860402984325));
#406079=CARTESIAN_POINT('Ctrl Pts',(0.909149402631517,-2.58864733108503,
7.51734760759493));
#406080=CARTESIAN_POINT('Ctrl Pts',(0.909400265220393,-2.58896333080256,
7.51608817408572));
#406081=CARTESIAN_POINT('Ctrl Pts',(0.909568375706178,-2.58930130513209,
7.51481005913119));
#406082=CARTESIAN_POINT('Ctrl Pts',(0.909720654201332,-2.58960745035594,
7.51365231206383));
#406083=CARTESIAN_POINT('Ctrl Pts',(0.909805471833591,-2.58993194624438,
7.51247773061042));
#406084=CARTESIAN_POINT('Ctrl Pts',(0.909785636131782,-2.59027851570741,
7.51129758471022));
#406085=CARTESIAN_POINT('Ctrl Pts',(0.909760982619756,-2.59070926197024,
7.50983079813402));
#406086=CARTESIAN_POINT('Ctrl Pts',(0.90956244776073,-2.59115961536516,
7.50839324291155));
#406087=CARTESIAN_POINT('Ctrl Pts',(0.909113147813133,-2.5915996078967,
7.50715379678855));
#406088=CARTESIAN_POINT('Ctrl Pts',(0.90890558418361,-2.5918028717682,7.50658120839351));
#406089=CARTESIAN_POINT('Ctrl Pts',(0.908608347826973,-2.59202603157119,
7.50598221009429));
#406090=CARTESIAN_POINT('Ctrl Pts',(0.908214855547679,-2.59224558605754,
7.50545747549611));
#406091=CARTESIAN_POINT('Ctrl Pts',(0.908004875887722,-2.5923627471273,
7.50517746087247));
#406092=CARTESIAN_POINT('Ctrl Pts',(0.907765307937765,-2.59248032881998,
7.50491486231392));
#406093=CARTESIAN_POINT('Ctrl Pts',(0.907501760933578,-2.59259371998976,
7.50468370960993));
#406094=CARTESIAN_POINT('Ctrl Pts',(0.907107675031134,-2.59276327555579,
7.50433806340447));
#406095=CARTESIAN_POINT('Ctrl Pts',(0.906647935572143,-2.5929280342173,
7.50405484070984));
#406096=CARTESIAN_POINT('Ctrl Pts',(0.906153263468412,-2.59307622538893,
7.50385766036132));
#406097=CARTESIAN_POINT('Ctrl Pts',(0.906100365975858,-2.59309207213132,
7.50383657498791));
#406098=CARTESIAN_POINT('Ctrl Pts',(0.90604709656214,-2.59310773623329,
7.50381643264937));
#406099=CARTESIAN_POINT('Ctrl Pts',(0.905993512717888,-2.59312320855992,
7.50379723213559));
#406100=CARTESIAN_POINT('Ctrl Pts',(0.905635823029044,-2.5932264914015,
7.50366906242519));
#406101=CARTESIAN_POINT('Ctrl Pts',(0.905256142261199,-2.59332278454904,
7.50358235568538));
#406102=CARTESIAN_POINT('Ctrl Pts',(0.904887945654187,-2.59340680223421,
7.5035341175365));
#406103=CARTESIAN_POINT('Ctrl Pts',(0.904335876513782,-2.59353277724414,
7.50346178989176));
#406104=CARTESIAN_POINT('Ctrl Pts',(0.903736619435742,-2.5936448243463,
7.50346967198527));
#406105=CARTESIAN_POINT('Ctrl Pts',(0.903144950082912,-2.59373671834596,
7.50354272648692));
#406106=CARTESIAN_POINT('Ctrl Pts',(0.902901584231261,-2.59377451625012,
7.50357277531559));
#406107=CARTESIAN_POINT('Ctrl Pts',(0.9026598472222,-2.5938089944534,7.50361331098761));
#406108=CARTESIAN_POINT('Ctrl Pts',(0.902424861598775,-2.59384008075164,
7.50366116523658));
#406109=CARTESIAN_POINT('',(0.842588855338652,-2.53774338397775,7.57603338622103));
#406110=CARTESIAN_POINT('Origin',(0.845370739448648,-2.5461310302743,7.5848687342763));
#406111=CARTESIAN_POINT('Ctrl Pts',(0.902424861643628,-2.59384008078544,
7.50366116529969));
#406112=CARTESIAN_POINT('Ctrl Pts',(0.882511501228937,-2.57517230438344,
7.52783573079709));
#406113=CARTESIAN_POINT('Ctrl Pts',(0.862567095273873,-2.55647430140458,
7.55196141284069));
#406114=CARTESIAN_POINT('Ctrl Pts',(0.842588856456747,-2.53774338454123,
7.57603338728831));
#406115=CARTESIAN_POINT('Ctrl Pts',(0.846992701390038,-2.53077349621436,
7.59639677331372));
#406116=CARTESIAN_POINT('Ctrl Pts',(0.835782896743083,-2.5163370078768,
7.59959882295463));
#406117=CARTESIAN_POINT('Ctrl Pts',(0.83489690696676,-2.53461059085095,
7.59642833564546));
#406118=CARTESIAN_POINT('Ctrl Pts',(0.845126734807235,-2.52734810969668,
7.58707626057424));
#406119=CARTESIAN_POINT('Ctrl Pts',(0.83861611782419,-2.52547083573265,
7.58809943920598));
#406120=CARTESIAN_POINT('Ctrl Pts',(0.834444422555743,-2.53079167771301,
7.58710240504252));
#406121=CARTESIAN_POINT('Ctrl Pts',(0.84333419920026,-2.53315435188584,
7.5801537675693));
#406122=CARTESIAN_POINT('Ctrl Pts',(0.840720632629399,-2.53201481637711,
7.5820588065976));
#406123=CARTESIAN_POINT('Ctrl Pts',(0.839288810603534,-2.53443906073858,
7.58020924244128));
#406124=CARTESIAN_POINT('Ctrl Pts',(0.84258885507807,-2.53774338319228,
7.57603338509286));
#406125=CARTESIAN_POINT('Ctrl Pts',(0.84258885507807,-2.53774338319228,
7.57603338509286));
#406126=CARTESIAN_POINT('Ctrl Pts',(0.84258885507807,-2.53774338319228,
7.57603338509286));
#406127=CARTESIAN_POINT('Origin',(0.845376155095157,-2.54612923215639,7.5848687342762));
#406128=CARTESIAN_POINT('Ctrl Pts',(0.818248011214847,-2.626385133776,7.51098857897448));
#406129=CARTESIAN_POINT('Ctrl Pts',(0.819289576806601,-2.62059068357862,
7.50433767179956));
#406130=CARTESIAN_POINT('Ctrl Pts',(0.82788781980899,-2.62016846520582,
7.50214974420965));
#406131=CARTESIAN_POINT('Ctrl Pts',(0.823821120043198,-2.59538074787257,
7.53887321589166));
#406132=CARTESIAN_POINT('Ctrl Pts',(0.824850205830722,-2.58965572547184,
7.53220407452059));
#406133=CARTESIAN_POINT('Ctrl Pts',(0.83341612225984,-2.58917823657005,
7.53003438070911));
#406134=CARTESIAN_POINT('Ctrl Pts',(0.829404931296325,-2.56431682211121,
7.56669465659236));
#406135=CARTESIAN_POINT('Ctrl Pts',(0.830427935378149,-2.55862563352851,
7.56004085833304));
#406136=CARTESIAN_POINT('Ctrl Pts',(0.838953795137752,-2.55812928134927,
7.55785582193789));
#406137=CARTESIAN_POINT('Ctrl Pts',(0.834999192440815,-2.53319476138884,
7.59443891967696));
#406138=CARTESIAN_POINT('Ctrl Pts',(0.836023679751206,-2.52749532129125,
7.58783901202978));
#406139=CARTESIAN_POINT('Ctrl Pts',(0.844500483535603,-2.52702311838028,
7.58560008491213));
#406140=CARTESIAN_POINT('',(0.828187489909793,-2.61848858635939,7.50366116523517));
#406141=CARTESIAN_POINT('Ctrl Pts',(0.828187489909906,-2.61848858635974,
7.50366116523554));
#406142=CARTESIAN_POINT('Ctrl Pts',(0.827525969191762,-2.61885808312053,
7.50350835821027));
#406143=CARTESIAN_POINT('Ctrl Pts',(0.826905849903705,-2.61917621843721,
7.50345484955999));
#406144=CARTESIAN_POINT('Ctrl Pts',(0.826308969499699,-2.61945298502424,
7.50349758195598));
#406145=CARTESIAN_POINT('Ctrl Pts',(0.826002725586639,-2.61959498680893,
7.50351950684424));
#406146=CARTESIAN_POINT('Ctrl Pts',(0.825672469016706,-2.61974021217986,
7.50357029184312));
#406147=CARTESIAN_POINT('Ctrl Pts',(0.825350157004229,-2.61987149743226,
7.50365515313924));
#406148=CARTESIAN_POINT('Ctrl Pts',(0.824854310612016,-2.62007346731311,
7.50378570417639));
#406149=CARTESIAN_POINT('Ctrl Pts',(0.824362842393546,-2.62024869536167,
7.50400001621911));
#406150=CARTESIAN_POINT('Ctrl Pts',(0.823912397737676,-2.62038170562562,
7.50428903009635));
#406151=CARTESIAN_POINT('Ctrl Pts',(0.823862401846387,-2.6203964687416,
7.50432110841318));
#406152=CARTESIAN_POINT('Ctrl Pts',(0.823812892273602,-2.62041073533621,
7.50435406373354));
#406153=CARTESIAN_POINT('Ctrl Pts',(0.823763904819425,-2.62042450145567,
7.50438785222352));
#406154=CARTESIAN_POINT('Ctrl Pts',(0.823464812865309,-2.62050855023183,
7.50459414719561));
#406155=CARTESIAN_POINT('Ctrl Pts',(0.823180282494888,-2.62057478447335,
7.50483629897752));
#406156=CARTESIAN_POINT('Ctrl Pts',(0.822921512356913,-2.62062194852715,
7.5050991045531));
#406157=CARTESIAN_POINT('Ctrl Pts',(0.82235063944154,-2.62072599716703,
7.50567888004914));
#406158=CARTESIAN_POINT('Ctrl Pts',(0.821882736099762,-2.6207418454673,
7.50637912803145));
#406159=CARTESIAN_POINT('Ctrl Pts',(0.821510747489535,-2.62069958740676,
7.50710440483569));
#406160=CARTESIAN_POINT('Ctrl Pts',(0.821419528497299,-2.62068922489138,
7.50728225710685));
#406161=CARTESIAN_POINT('Ctrl Pts',(0.821332244757623,-2.62067530700927,
7.50746498566954));
#406162=CARTESIAN_POINT('Ctrl Pts',(0.821250868156086,-2.62065857004476,
7.50764697238949));
#406163=CARTESIAN_POINT('Ctrl Pts',(0.820813409941663,-2.62056859672971,
7.50862528291182));
#406164=CARTESIAN_POINT('Ctrl Pts',(0.820506113419842,-2.62039304298326,
7.50965856837422));
#406165=CARTESIAN_POINT('Ctrl Pts',(0.820281832715819,-2.62017852063152,
7.51067959873203));
#406166=CARTESIAN_POINT('Ctrl Pts',(0.820158410761503,-2.62006046871077,
7.51124147302579));
#406167=CARTESIAN_POINT('Ctrl Pts',(0.820060398756856,-2.61993027313354,
7.51180065547253));
#406168=CARTESIAN_POINT('Ctrl Pts',(0.819981887633074,-2.6197938087974,
7.51235175716501));
#406169=CARTESIAN_POINT('Ctrl Pts',(0.819710600425289,-2.61932227015509,
7.51425603304536));
#406170=CARTESIAN_POINT('Ctrl Pts',(0.819645060131596,-2.61871663751266,
7.5162690050518));
#406171=CARTESIAN_POINT('Ctrl Pts',(0.819751779839004,-2.61802712335916,
7.51827788969244));
#406172=CARTESIAN_POINT('Ctrl Pts',(0.819757555711242,-2.61798980555017,
7.51838661432545));
#406173=CARTESIAN_POINT('Ctrl Pts',(0.819763843816376,-2.61795223565927,
7.51849533314856));
#406174=CARTESIAN_POINT('Ctrl Pts',(0.819770641322295,-2.61791441969278,
7.51860402984325));
#406175=CARTESIAN_POINT('Ctrl Pts',(0.842588854779764,-2.53774338509928,
7.57603338728985));
#406176=CARTESIAN_POINT('Ctrl Pts',(0.837781180671478,-2.5647037920469,
7.55196141284922));
#406177=CARTESIAN_POINT('Ctrl Pts',(0.832980934536062,-2.59161758558423,
7.52783573083104));
#406178=CARTESIAN_POINT('Ctrl Pts',(0.828187489894095,-2.61848858641645,
7.50366116530176));
#406179=CARTESIAN_POINT('Origin',(2.91153398701384E-16,-8.76907647894213E-16,
7.49482233047033));
#406180=CARTESIAN_POINT('Origin',(0.899520491555409,-2.58549204896707,7.49482233047033));
#406181=CARTESIAN_POINT('Origin',(0.,0.,7.50366116523517));
#406182=CARTESIAN_POINT('Origin',(0.82552204590669,-2.61006122566541,7.49482233047033));
#406183=CARTESIAN_POINT('Ctrl Pts',(0.908826050988849,-2.58834500757948,
7.51860402984325));
#406184=CARTESIAN_POINT('Ctrl Pts',(0.914383648054368,-2.59354206452427,
7.51860402984325));
#406185=CARTESIAN_POINT('Ctrl Pts',(0.921552651160842,-2.59099222521767,
7.51860402984325));
#406186=CARTESIAN_POINT('Ctrl Pts',(0.910889625574226,-2.5902747093615,
7.51041458714367));
#406187=CARTESIAN_POINT('Ctrl Pts',(0.916082063685389,-2.59293796906005,
7.51004642900442));
#406188=CARTESIAN_POINT('Ctrl Pts',(0.921554628286784,-2.59099152200227,
7.5072913648301));
#406189=CARTESIAN_POINT('Ctrl Pts',(0.9097942691111,-2.5928677638187,7.50215815450137));
#406190=CARTESIAN_POINT('Ctrl Pts',(0.91262396703454,-2.59416809998427,
7.49877163671531));
#406191=CARTESIAN_POINT('Ctrl Pts',(0.915882595552394,-2.5930344052383,
7.4948158853317));
#406192=CARTESIAN_POINT('Ctrl Pts',(0.902424680702065,-2.59383956080161,
7.50366171572174));
#406193=CARTESIAN_POINT('Ctrl Pts',(0.903627891059863,-2.59729794873417,
7.50000045605858));
#406194=CARTESIAN_POINT('Ctrl Pts',(0.903627891059981,-2.59729794873413,
7.49482233047317));
#406195=CARTESIAN_POINT('Origin',(0.917363775473747,-2.57921498783032,7.51860402984325));
#406196=CARTESIAN_POINT('Origin',(0.917363775473747,-2.57921498783032,9.));
#406197=CARTESIAN_POINT('Origin',(0.917363775473747,-2.57921498783032,8.75721825406948));
#406198=CARTESIAN_POINT('Ctrl Pts',(0.896628055005695,-2.57694023016136,
8.78942910404912));
#406199=CARTESIAN_POINT('Ctrl Pts',(0.900684690092706,-2.58076071972063,
8.7967269950169));
#406200=CARTESIAN_POINT('Ctrl Pts',(0.90789356058949,-2.57549710193981,
8.79893251111266));
#406201=CARTESIAN_POINT('Ctrl Pts',(0.904658967512584,-2.58444888270673,
8.78111911759584));
#406202=CARTESIAN_POINT('Ctrl Pts',(0.909473258913846,-2.58897269840027,
8.78644465894814));
#406203=CARTESIAN_POINT('Ctrl Pts',(0.916893176767956,-2.58570768219606,
8.78817647674132));
#406204=CARTESIAN_POINT('Ctrl Pts',(0.909664023763959,-2.58912845404804,
8.76780923932029));
#406205=CARTESIAN_POINT('Ctrl Pts',(0.91535058097983,-2.59446491390464,
8.76988516158373));
#406206=CARTESIAN_POINT('Ctrl Pts',(0.922522564001213,-2.59207764769887,
8.77093053738833));
#406207=CARTESIAN_POINT('Ctrl Pts',(0.908688106295134,-2.58821600167965,
8.75371302330492));
#406208=CARTESIAN_POINT('Ctrl Pts',(0.91423457591542,-2.59342204394983,
8.75300828287559));
#406209=CARTESIAN_POINT('Ctrl Pts',(0.921424947711537,-2.59083494272107,
8.75267964240738));
#406210=CARTESIAN_POINT('Origin',(0.907120849657241,-2.56963817978669,8.78727029226991));
#406211=CARTESIAN_POINT('Ctrl Pts',(0.846361565593617,-2.5299427115692,
8.85049129520029));
#406212=CARTESIAN_POINT('Ctrl Pts',(0.850627167658232,-2.53393091307482,
8.85711686593484));
#406213=CARTESIAN_POINT('Ctrl Pts',(0.857737280217499,-2.52918253845728,
8.85933012996512));
#406214=CARTESIAN_POINT('Ctrl Pts',(0.863794336451385,-2.54624179477689,
8.82945683644722));
#406215=CARTESIAN_POINT('Ctrl Pts',(0.868095345592174,-2.55026310076631,
8.8360746990239));
#406216=CARTESIAN_POINT('Ctrl Pts',(0.875205505457256,-2.54546959795619,
8.8382956714852));
#406217=CARTESIAN_POINT('Ctrl Pts',(0.881201122358403,-2.5625165828867,
8.80838214965003));
#406218=CARTESIAN_POINT('Ctrl Pts',(0.885519105289387,-2.56655375882711,
8.81501364461992));
#406219=CARTESIAN_POINT('Ctrl Pts',(0.892646776397513,-2.56173243979915,
8.81722098428721));
#406220=CARTESIAN_POINT('Ctrl Pts',(0.898583897763467,-2.5787689219451,
8.78727029226991));
#406221=CARTESIAN_POINT('Ctrl Pts',(0.902902597925574,-2.58280676847366,
8.79393457792714));
#406222=CARTESIAN_POINT('Ctrl Pts',(0.91006313890143,-2.57797292237441,
8.79610912703474));
#406223=CARTESIAN_POINT('Origin',(0.854898517487391,-2.52081196941079,8.85049129520029));
#406224=CARTESIAN_POINT('Ctrl Pts',(0.834899689636865,-2.53374831658167,
8.85049129520029));
#406225=CARTESIAN_POINT('Ctrl Pts',(0.833866563355046,-2.53949581710876,
8.85711686593484));
#406226=CARTESIAN_POINT('Ctrl Pts',(0.82532836943557,-2.53994303820321,
8.85933012996512));
#406227=CARTESIAN_POINT('Ctrl Pts',(0.835813681545056,-2.52866358583139,
8.86332496987232));
#406228=CARTESIAN_POINT('Ctrl Pts',(0.83152541263115,-2.5303848191389,8.86648636486737));
#406229=CARTESIAN_POINT('Ctrl Pts',(0.827902161459422,-2.52572132765299,
8.87206031107457));
#406230=CARTESIAN_POINT('Ctrl Pts',(0.842562205427872,-2.52639043132742,
8.86341338519876));
#406231=CARTESIAN_POINT('Ctrl Pts',(0.8470333805202,-2.52517303084769,8.86654584966058));
#406232=CARTESIAN_POINT('Ctrl Pts',(0.847088807956572,-2.51924672672229,
8.87215952290715));
#406233=CARTESIAN_POINT('Ctrl Pts',(0.846361565593616,-2.5299427115692,
8.85049129520029));
#406234=CARTESIAN_POINT('Ctrl Pts',(0.850627167658232,-2.53393091307482,
8.85711686593484));
#406235=CARTESIAN_POINT('Ctrl Pts',(0.857737280217499,-2.52918253845728,
8.85933012996512));
#406236=CARTESIAN_POINT('Origin',(0.822596867063817,-2.53153685626412,8.85049129520029));
#406237=CARTESIAN_POINT('Ctrl Pts',(0.82225147186004,-2.60411303347871,
8.78727029226991));
#406238=CARTESIAN_POINT('Ctrl Pts',(0.821205485250605,-2.6099320787347,
8.79393457792714));
#406239=CARTESIAN_POINT('Ctrl Pts',(0.812575755917871,-2.61034096358642,
8.79610912703474));
#406240=CARTESIAN_POINT('Ctrl Pts',(0.826461569719588,-2.58069136655116,
8.80838214965001));
#406241=CARTESIAN_POINT('Ctrl Pts',(0.825415756823118,-2.58650944540513,
8.81501364461986));
#406242=CARTESIAN_POINT('Ctrl Pts',(0.816819862423375,-2.58690870980845,
8.81722098428722));
#406243=CARTESIAN_POINT('Ctrl Pts',(0.83067748290842,-2.55723734771396,
8.82945683644724));
#406244=CARTESIAN_POINT('Ctrl Pts',(0.829635781053824,-2.56303255597043,
8.83607469902391));
#406245=CARTESIAN_POINT('Ctrl Pts',(0.821070557575618,-2.56344363901071,
8.83829567148519));
#406246=CARTESIAN_POINT('Ctrl Pts',(0.834899689636865,-2.53374831658167,
8.85049129520029));
#406247=CARTESIAN_POINT('Ctrl Pts',(0.833866563355046,-2.53949581710876,
8.85711686593484));
#406248=CARTESIAN_POINT('Ctrl Pts',(0.82532836943557,-2.53994303820321,
8.85933012996512));
#406249=CARTESIAN_POINT('Origin',(0.809948649286992,-2.60190157316116,8.78727029226991));
#406250=CARTESIAN_POINT('Ctrl Pts',(0.819803381285507,-2.61773217606689,
8.75374538247848));
#406251=CARTESIAN_POINT('Ctrl Pts',(0.818471912849805,-2.62521359105286,
8.75304829418602));
#406252=CARTESIAN_POINT('Ctrl Pts',(0.811171486718982,-2.62744393217416,
8.75272238421917));
#406253=CARTESIAN_POINT('Ctrl Pts',(0.819569854383186,-2.619031338143,8.76769408445019));
#406254=CARTESIAN_POINT('Ctrl Pts',(0.818204200862904,-2.62670089780666,
8.76974318093968));
#406255=CARTESIAN_POINT('Ctrl Pts',(0.811037076092532,-2.62907801366545,
8.77077869880429));
#406256=CARTESIAN_POINT('Ctrl Pts',(0.820766780267531,-2.61237257342734,
8.78108014887992));
#406257=CARTESIAN_POINT('Ctrl Pts',(0.819613178664803,-2.61887291500624,
8.78639403366326));
#406258=CARTESIAN_POINT('Ctrl Pts',(0.811730020148829,-2.62071081803441,
8.78812224174742));
#406259=CARTESIAN_POINT('Ctrl Pts',(0.822728277533278,-2.6014603279895,
8.78944554828685));
#406260=CARTESIAN_POINT('Ctrl Pts',(0.821761576480921,-2.60693955299787,
8.79673892988686));
#406261=CARTESIAN_POINT('Ctrl Pts',(0.812845615262423,-2.60703541679016,
8.79894799272499));
#406262=CARTESIAN_POINT('Origin',(0.807467818749251,-2.61570295937523,8.75721825406948));
#406263=CARTESIAN_POINT('Origin',(0.807467818749251,-2.61570295937523,9.));
#406264=CARTESIAN_POINT('Origin',(0.807467818749251,-2.61570295937523,7.51860402984325));
#406265=CARTESIAN_POINT('Ctrl Pts',(0.828187252682973,-2.61848783631719,
7.50366195182966));
#406266=CARTESIAN_POINT('Ctrl Pts',(0.829291552965492,-2.62197931345388,
7.50000065167736));
#406267=CARTESIAN_POINT('Ctrl Pts',(0.82929155296538,-2.62197931345392,
7.49482233047108));
#406268=CARTESIAN_POINT('Ctrl Pts',(0.821693702661423,-2.62211931091083,
7.50215800491337));
#406269=CARTESIAN_POINT('Ctrl Pts',(0.820201990404422,-2.6248541768521,
7.49877273257264));
#406270=CARTESIAN_POINT('Ctrl Pts',(0.816910580710839,-2.62589522371893,
7.49481816995647));
#406271=CARTESIAN_POINT('Ctrl Pts',(0.819272319923741,-2.62068860409959,
7.51043025814043));
#406272=CARTESIAN_POINT('Ctrl Pts',(0.816705845947828,-2.62593321736634,
7.51006209594516));
#406273=CARTESIAN_POINT('Ctrl Pts',(0.811152467196917,-2.62764755531764,
7.50731281821702));
#406274=CARTESIAN_POINT('Ctrl Pts',(0.819770908625769,-2.61791293211041,
7.51860402984326));
#406275=CARTESIAN_POINT('Ctrl Pts',(0.818425605968019,-2.6254023365026,
7.51860402984327));
#406276=CARTESIAN_POINT('Ctrl Pts',(0.811154886414768,-2.6276468085048,
7.51860402984327));
#406277=CARTESIAN_POINT('Origin',(0.,0.,7.5));
#406278=CARTESIAN_POINT('Origin',(0.995522110700944,-2.47505025214474,7.5));
#406279=CARTESIAN_POINT('',(0.995522110700944,-2.47505025214474,7.59394543036555));
#406280=CARTESIAN_POINT('',(0.995522110700944,-2.47505025214474,8.85049129520029));
#406281=CARTESIAN_POINT('',(0.995522110700944,-2.47505025214474,7.5));
#406282=CARTESIAN_POINT('',(0.987408162934533,-2.54608077127964,8.78727029226991));
#406283=CARTESIAN_POINT('Ctrl Pts',(0.995522110700944,-2.47505025214474,
8.85049129520029));
#406284=CARTESIAN_POINT('Ctrl Pts',(0.99281352997585,-2.49876150843587,
8.82945686509571));
#406285=CARTESIAN_POINT('Ctrl Pts',(0.990108975883521,-2.5224375150774,
8.80838212259895));
#406286=CARTESIAN_POINT('Ctrl Pts',(0.987408162934533,-2.54608077127964,
8.78727029226991));
#406287=CARTESIAN_POINT('',(0.985816687379975,-2.56001274842383,8.75721825406948));
#406288=CARTESIAN_POINT('Origin',(0.990606189908979,-2.51808661906274,8.75937679713083));
#406289=CARTESIAN_POINT('',(0.985816687379975,-2.56001274842383,7.51860402984325));
#406290=CARTESIAN_POINT('',(0.985816687379975,-2.56001274842383,7.5));
#406291=CARTESIAN_POINT('Ctrl Pts',(0.985816687379975,-2.56001274842383,
7.51860402984325));
#406292=CARTESIAN_POINT('Ctrl Pts',(0.987066543906813,-2.54907134720937,
7.52834476460825));
#406293=CARTESIAN_POINT('Ctrl Pts',(0.988317211822481,-2.53812284299513,
7.53807742314407));
#406294=CARTESIAN_POINT('Ctrl Pts',(0.989568718370425,-2.52716699728844,
7.54780169004674));
#406295=CARTESIAN_POINT('Ctrl Pts',(0.991551037104211,-2.50981352980197,
7.5632044032688));
#406296=CARTESIAN_POINT('Ctrl Pts',(0.993535462378795,-2.49244162139226,
7.57858609112103));
#406297=CARTESIAN_POINT('Ctrl Pts',(0.995522110700944,-2.47505025214474,
7.59394543036555));
#406298=CARTESIAN_POINT('Origin',(1.21921343306784,-2.64507497058259,7.5));
#406299=CARTESIAN_POINT('',(1.07279542170607,-2.52479896157612,8.75721825406948));
#406300=CARTESIAN_POINT('',(1.06195995288114,-2.51589809662203,8.78727029226991));
#406301=CARTESIAN_POINT('Origin',(1.03445549157553,-2.49330438151181,8.75658640621066));
#406302=CARTESIAN_POINT('',(1.00671661105395,-2.47051810124197,8.85049129520029));
#406303=CARTESIAN_POINT('Ctrl Pts',(1.06195995288114,-2.51589809662203,
8.78727029226991));
#406304=CARTESIAN_POINT('Ctrl Pts',(1.04357162487516,-2.50079288733602,
8.80838212259896));
#406305=CARTESIAN_POINT('Ctrl Pts',(1.02515782551214,-2.48566675444136,
8.82945686509571));
#406306=CARTESIAN_POINT('Ctrl Pts',(1.00671661105395,-2.47051810124197,
8.85049129520029));
#406307=CARTESIAN_POINT('',(1.00671661105395,-2.47051810124197,7.59394543036555));
#406308=CARTESIAN_POINT('',(1.00671661105395,-2.47051810124197,7.5));
#406309=CARTESIAN_POINT('',(1.07279542170607,-2.52479896157612,7.51860402984325));
#406310=CARTESIAN_POINT('Ctrl Pts',(1.00671661105395,-2.47051810124197,
7.59394543036555));
#406311=CARTESIAN_POINT('Ctrl Pts',(1.02024259070164,-2.48162910346633,
7.57858609112103));
#406312=CARTESIAN_POINT('Ctrl Pts',(1.03375343485911,-2.49272767254576,
7.56320440326857));
#406313=CARTESIAN_POINT('Ctrl Pts',(1.04724993675601,-2.50381446008378,
7.54780169004651));
#406314=CARTESIAN_POINT('Ctrl Pts',(1.05577074635663,-2.51081393345959,
7.53807742314383));
#406315=CARTESIAN_POINT('Ctrl Pts',(1.06428584617825,-2.51780871650103,
7.52834476460825));
#406316=CARTESIAN_POINT('Ctrl Pts',(1.07279542170607,-2.52479896157612,
7.51860402984325));
#406317=CARTESIAN_POINT('',(1.07279542170607,-2.52479896157612,7.5));
#406318=CARTESIAN_POINT('Origin',(1.00235268932044,-2.47583052179232,7.5));
#406319=CARTESIAN_POINT('Ctrl Pts',(1.00671661105395,-2.47051810124197,
8.85049129520029));
#406320=CARTESIAN_POINT('Ctrl Pts',(1.00656696576467,-2.47039517416494,
8.85097269580138));
#406321=CARTESIAN_POINT('Ctrl Pts',(1.00641386936464,-2.4702802976711,8.85143669361005));
#406322=CARTESIAN_POINT('Ctrl Pts',(1.0062497475297,-2.47016888137881,8.8519052845931));
#406323=CARTESIAN_POINT('Ctrl Pts',(1.00592873562878,-2.46995095817687,
8.85282181883899));
#406324=CARTESIAN_POINT('Ctrl Pts',(1.00557369116892,-2.46975204145501,
8.85372622499635));
#406325=CARTESIAN_POINT('Ctrl Pts',(1.00517150659736,-2.46958246132731,
8.85462257735071));
#406326=CARTESIAN_POINT('Ctrl Pts',(1.0048376272503,-2.46944168192822,8.85536669723986));
#406327=CARTESIAN_POINT('Ctrl Pts',(1.00447119635595,-2.46932105929728,
8.85610498449051));
#406328=CARTESIAN_POINT('Ctrl Pts',(1.0040621813117,-2.46923409470727,8.85681338218371));
#406329=CARTESIAN_POINT('Ctrl Pts',(1.00369099951668,-2.46915517420525,
8.85745625420284));
#406330=CARTESIAN_POINT('Ctrl Pts',(1.00328021553239,-2.46910239770779,
8.85808743050665));
#406331=CARTESIAN_POINT('Ctrl Pts',(1.00281429721322,-2.46909977768251,
8.85866804508409));
#406332=CARTESIAN_POINT('Ctrl Pts',(1.00259933260063,-2.46909856885964,
8.85893592806395));
#406333=CARTESIAN_POINT('Ctrl Pts',(1.00237252513376,-2.46910825460028,
8.85919241173848));
#406334=CARTESIAN_POINT('Ctrl Pts',(1.0021318556926,-2.4691327111308,8.85943017985534));
#406335=CARTESIAN_POINT('Ctrl Pts',(1.00180688070127,-2.46916573468691,
8.8597512372));
#406336=CARTESIAN_POINT('Ctrl Pts',(1.00144842447935,-2.46922716762034,
8.86004599534706));
#406337=CARTESIAN_POINT('Ctrl Pts',(1.00106255305269,-2.46932653726459,
8.86026130871721));
#406338=CARTESIAN_POINT('Ctrl Pts',(1.00092127464453,-2.46936291929287,
8.86034014101235));
#406339=CARTESIAN_POINT('Ctrl Pts',(1.00077419600277,-2.46940492129387,
8.86040910639693));
#406340=CARTESIAN_POINT('Ctrl Pts',(1.00062541657118,-2.46945172239471,
8.86046313645507));
#406341=CARTESIAN_POINT('Ctrl Pts',(1.00039324751419,-2.46952475512062,
8.8605474499083));
#406342=CARTESIAN_POINT('Ctrl Pts',(1.00015064341207,-2.46961160813618,
8.86059655985669));
#406343=CARTESIAN_POINT('Ctrl Pts',(0.999913064461816,-2.46970643547805,
8.86059725258816));
#406344=CARTESIAN_POINT('Ctrl Pts',(0.999674936609278,-2.46980148190897,
8.86059794692011));
#406345=CARTESIAN_POINT('Ctrl Pts',(0.999440201162479,-2.46990806111196,
8.86056369958366));
#406346=CARTESIAN_POINT('Ctrl Pts',(0.999220104961803,-2.47001693375417,
8.86048590497774));
#406347=CARTESIAN_POINT('Ctrl Pts',(0.99916266640648,-2.47004534627226,
8.86046560290182));
#406348=CARTESIAN_POINT('Ctrl Pts',(0.999105517781774,-2.4700743658057,
8.86044257503091));
#406349=CARTESIAN_POINT('Ctrl Pts',(0.999050410165051,-2.47010306635803,
8.86041778462584));
#406350=CARTESIAN_POINT('Ctrl Pts',(0.998679604287361,-2.47029618546077,
8.86025097596201));
#406351=CARTESIAN_POINT('Ctrl Pts',(0.998351603563499,-2.4705010706905,
8.8599848982295));
#406352=CARTESIAN_POINT('Ctrl Pts',(0.998071492878086,-2.47070455619526,
8.85968173251461));
#406353=CARTESIAN_POINT('Ctrl Pts',(0.997923330373931,-2.47081218836895,
8.85952137522076));
#406354=CARTESIAN_POINT('Ctrl Pts',(0.997785598389788,-2.47092134911841,
8.85934740853961));
#406355=CARTESIAN_POINT('Ctrl Pts',(0.99765927366762,-2.4710292807249,8.8591675900182));
#406356=CARTESIAN_POINT('Ctrl Pts',(0.997152014245821,-2.47146268222672,
8.85844552518694));
#406357=CARTESIAN_POINT('Ctrl Pts',(0.996798055348731,-2.4718984588358,
8.85759444184121));
#406358=CARTESIAN_POINT('Ctrl Pts',(0.996541370401398,-2.47227968985936,
8.85683498915135));
#406359=CARTESIAN_POINT('Ctrl Pts',(0.996514509005272,-2.47231958467067,
8.85675551444995));
#406360=CARTESIAN_POINT('Ctrl Pts',(0.996488731289395,-2.47235888984364,
8.8566769979365));
#406361=CARTESIAN_POINT('Ctrl Pts',(0.996463985412329,-2.47239754457562,
8.85659965593547));
#406362=CARTESIAN_POINT('Ctrl Pts',(0.99612996430092,-2.47291930812044,
8.85555568965886));
#406363=CARTESIAN_POINT('Ctrl Pts',(0.995884302298615,-2.47346899447078,
8.85434650606346));
#406364=CARTESIAN_POINT('Ctrl Pts',(0.995720111102494,-2.47404678523083,
8.85297329937117));
#406365=CARTESIAN_POINT('Ctrl Pts',(0.995627763558993,-2.47437175732804,
8.85220095427747));
#406366=CARTESIAN_POINT('Ctrl Pts',(0.995561453674497,-2.4747058388066,
8.85137579139184));
#406367=CARTESIAN_POINT('Ctrl Pts',(0.995522110700944,-2.47505025214474,
8.85049129520029));
#406368=CARTESIAN_POINT('Origin',(1.00235268932044,-2.47583052179232,7.59394543036555));
#406369=CARTESIAN_POINT('Ctrl Pts',(1.00628214029679,-2.47016120246828,
7.59443877723642));
#406370=CARTESIAN_POINT('Ctrl Pts',(1.00180750953461,-2.46648548849807,
7.58783886950016));
#406371=CARTESIAN_POINT('Ctrl Pts',(0.995046786110639,-2.47162083661881,
7.58559994247159));
#406372=CARTESIAN_POINT('Ctrl Pts',(1.03070901834745,-2.49022681719079,
7.56670252222132));
#406373=CARTESIAN_POINT('Ctrl Pts',(1.02624085469712,-2.48655641567082,
7.56004874999026));
#406374=CARTESIAN_POINT('Ctrl Pts',(1.0194271481468,-2.49170517865848,7.55786368756704));
#406375=CARTESIAN_POINT('Ctrl Pts',(1.05509028164394,-2.51025496138264,
7.5388891333356));
#406376=CARTESIAN_POINT('Ctrl Pts',(1.05059556347821,-2.50656274648674,
7.53222002137279));
#406377=CARTESIAN_POINT('Ctrl Pts',(1.0437635876927,-2.51175182651942,7.53005029815327));
#406378=CARTESIAN_POINT('Ctrl Pts',(1.07942482691751,-2.53024472875669,
7.51101258149734));
#406379=CARTESIAN_POINT('Ctrl Pts',(1.07487562460053,-2.52650775750732,
7.5043616886572));
#406380=CARTESIAN_POINT('Ctrl Pts',(1.06805484980026,-2.53175985353354,
7.50217374673251));
#406381=CARTESIAN_POINT('',(1.06675863750385,-2.53069219871726,7.50366116523517));
#406382=CARTESIAN_POINT('Ctrl Pts',(1.07279542170607,-2.52479896157612,
7.51860402984325));
#406383=CARTESIAN_POINT('Ctrl Pts',(1.07313666163295,-2.52507927528982,
7.51734760759494));
#406384=CARTESIAN_POINT('Ctrl Pts',(1.07340725496914,-2.52537855293079,
7.51608817408573));
#406385=CARTESIAN_POINT('Ctrl Pts',(1.07359667414355,-2.52570506198001,
7.5148100591312));
#406386=CARTESIAN_POINT('Ctrl Pts',(1.07376825455804,-2.52600082167898,
7.51365231206384));
#406387=CARTESIAN_POINT('Ctrl Pts',(1.07387368844633,-2.52631921657145,
7.51247773061043));
#406388=CARTESIAN_POINT('Ctrl Pts',(1.07387609828084,-2.52666634484814,
7.51129758471022));
#406389=CARTESIAN_POINT('Ctrl Pts',(1.07387909342991,-2.5270977856525,7.50983079813402));
#406390=CARTESIAN_POINT('Ctrl Pts',(1.07370982072313,-2.52755993392016,
7.50839324291155));
#406391=CARTESIAN_POINT('Ctrl Pts',(1.07328963432874,-2.52802780918635,
7.50715379678855));
#406392=CARTESIAN_POINT('Ctrl Pts',(1.07309552032192,-2.52824395407782,
7.50658120839351));
#406393=CARTESIAN_POINT('Ctrl Pts',(1.07281319256692,-2.52848569937381,
7.50598221009429));
#406394=CARTESIAN_POINT('Ctrl Pts',(1.07243457566396,-2.52873001389882,
7.50545747549611));
#406395=CARTESIAN_POINT('Ctrl Pts',(1.07223253396525,-2.52886038769161,
7.50517746087247));
#406396=CARTESIAN_POINT('Ctrl Pts',(1.07200099171825,-2.52899307697135,
7.50491486231392));
#406397=CARTESIAN_POINT('Ctrl Pts',(1.07174525119684,-2.52912312068133,
7.50468370960992));
#406398=CARTESIAN_POINT('Ctrl Pts',(1.07136283844856,-2.52931757704773,
7.50433806340447));
#406399=CARTESIAN_POINT('Ctrl Pts',(1.07091459969728,-2.52951145280317,
7.50405484070984));
#406400=CARTESIAN_POINT('Ctrl Pts',(1.0704304385914,-2.52969103325065,7.50385766036131));
#406401=CARTESIAN_POINT('Ctrl Pts',(1.07037866508669,-2.5297102365882,7.50383657498791));
#406402=CARTESIAN_POINT('Ctrl Pts',(1.07032650872316,-2.52972928148965,
7.50381643264937));
#406403=CARTESIAN_POINT('Ctrl Pts',(1.07027402628804,-2.52974815515541,
7.50379723213559));
#406404=CARTESIAN_POINT('Ctrl Pts',(1.0699236888654,-2.52987414304837,7.50366906242519));
#406405=CARTESIAN_POINT('Ctrl Pts',(1.06955095771556,-2.52999456458162,
7.50358235568538));
#406406=CARTESIAN_POINT('Ctrl Pts',(1.06918890063954,-2.53010200008105,
7.5035341175365));
#406407=CARTESIAN_POINT('Ctrl Pts',(1.06864603703099,-2.53026308745309,
7.50346178989176));
#406408=CARTESIAN_POINT('Ctrl Pts',(1.06805519007336,-2.53041329887527,
7.50346967198527));
#406409=CARTESIAN_POINT('Ctrl Pts',(1.06747062403745,-2.53054291245445,
7.50354272648692));
#406410=CARTESIAN_POINT('Ctrl Pts',(1.06723017992708,-2.53059622520241,
7.50357277531559));
#406411=CARTESIAN_POINT('Ctrl Pts',(1.0669911486187,-2.53064612070987,7.50361331098761));
#406412=CARTESIAN_POINT('Ctrl Pts',(1.06675863750441,-2.53069219871856,
7.50366116523659));
#406413=CARTESIAN_POINT('',(1.00345144303404,-2.4785444647084,7.57603338622103));
#406414=CARTESIAN_POINT('Origin',(1.00676500980812,-2.48673664175929,7.58486873427625));
#406415=CARTESIAN_POINT('Ctrl Pts',(1.06675863755133,-2.53069219874942,
7.50366116529969));
#406416=CARTESIAN_POINT('Ctrl Pts',(1.0456901427307,-2.51333863067846,7.5278357307971));
#406417=CARTESIAN_POINT('Ctrl Pts',(1.02458872953262,-2.49595688722902,
7.55196141284068));
#406418=CARTESIAN_POINT('Ctrl Pts',(1.00345144418594,-2.47854446519909,
7.57603338728831));
#406419=CARTESIAN_POINT('Ctrl Pts',(1.00739967866916,-2.47130674194166,
7.59639677331372));
#406420=CARTESIAN_POINT('Ctrl Pts',(0.995287956784576,-2.45761812956736,
7.59959882295463));
#406421=CARTESIAN_POINT('Ctrl Pts',(0.99557457985025,-2.47591093306534,
7.59642833564546));
#406422=CARTESIAN_POINT('Ctrl Pts',(1.00531808064712,-2.46800794613739,
7.58707626057423));
#406423=CARTESIAN_POINT('Ctrl Pts',(0.998700563069069,-2.46655166589637,
7.58809943920599));
#406424=CARTESIAN_POINT('Ctrl Pts',(0.994878346512149,-2.47212885706977,
7.58710240504253));
#406425=CARTESIAN_POINT('Ctrl Pts',(1.00390123521112,-2.47391710692992,
7.58015376756929));
#406426=CARTESIAN_POINT('Ctrl Pts',(1.00122002820245,-2.4729473645042,7.5820588065976));
#406427=CARTESIAN_POINT('Ctrl Pts',(0.999946469877937,-2.47545836514784,
7.58020924244128));
#406428=CARTESIAN_POINT('Ctrl Pts',(1.00345144272367,-2.47854446394124,
7.57603338509286));
#406429=CARTESIAN_POINT('Ctrl Pts',(1.00345144272367,-2.47854446394124,
7.57603338509286));
#406430=CARTESIAN_POINT('Ctrl Pts',(1.00345144272367,-2.47854446394124,
7.57603338509286));
#406431=CARTESIAN_POINT('Origin',(1.00677029912178,-2.48673450035402,7.58486873427622));
#406432=CARTESIAN_POINT('Ctrl Pts',(0.984839906194085,-2.56856361376242,
7.51098857897448));
#406433=CARTESIAN_POINT('Ctrl Pts',(0.98550808007881,-2.56271433554783,
7.50433767179956));
#406434=CARTESIAN_POINT('Ctrl Pts',(0.994061605444767,-2.56174209334736,
7.50214974420965));
#406435=CARTESIAN_POINT('Ctrl Pts',(0.988415106647427,-2.53726585938649,
7.53887321589173));
#406436=CARTESIAN_POINT('Ctrl Pts',(0.989075274623224,-2.53148666590551,
7.53220407452067));
#406437=CARTESIAN_POINT('Ctrl Pts',(0.997592998639344,-2.53046133790587,
7.53003438070912));
#406438=CARTESIAN_POINT('Ctrl Pts',(0.991997172804488,-2.5059080017768,
7.56669465659233));
#406439=CARTESIAN_POINT('Ctrl Pts',(0.99265343931025,-2.50016296225485,
7.56004085833301));
#406440=CARTESIAN_POINT('Ctrl Pts',(1.00112998038329,-2.4991213761741,7.55785582193789));
#406441=CARTESIAN_POINT('Ctrl Pts',(0.995585942662736,-2.47449145912388,
7.59443891967696));
#406442=CARTESIAN_POINT('Ctrl Pts',(0.996243160673252,-2.46873809000989,
7.58783901202978));
#406443=CARTESIAN_POINT('Ctrl Pts',(1.00467229381076,-2.46772374660724,
7.58560008491213));
#406444=CARTESIAN_POINT('',(0.994253029633976,-2.5600464660629,7.50366116523517));
#406445=CARTESIAN_POINT('Ctrl Pts',(0.994253029634111,-2.56004646606324,
7.50366116523554));
#406446=CARTESIAN_POINT('Ctrl Pts',(0.993616541819977,-2.56045758743124,
7.50350835821026));
#406447=CARTESIAN_POINT('Ctrl Pts',(0.993018079633229,-2.560814800284,7.50345484956));
#406448=CARTESIAN_POINT('Ctrl Pts',(0.992440158080142,-2.56112924048317,
7.50349758195598));
#406449=CARTESIAN_POINT('Ctrl Pts',(0.992143641463629,-2.56129057162485,
7.50351950684424));
#406450=CARTESIAN_POINT('Ctrl Pts',(0.991823368062701,-2.56145665822576,
7.50357029184312));
#406451=CARTESIAN_POINT('Ctrl Pts',(0.991510129749823,-2.56160832434007,
7.50365515313923));
#406452=CARTESIAN_POINT('Ctrl Pts',(0.9910282423819,-2.56184164823956,7.50378570417639));
#406453=CARTESIAN_POINT('Ctrl Pts',(0.990549010837215,-2.56204800474017,
7.50400001621911));
#406454=CARTESIAN_POINT('Ctrl Pts',(0.990108013665073,-2.56220960180846,
7.50428903009634));
#406455=CARTESIAN_POINT('Ctrl Pts',(0.990059066371791,-2.56222753783979,
7.50432110841318));
#406456=CARTESIAN_POINT('Ctrl Pts',(0.990010572585586,-2.56224494721138,
7.50435406373354));
#406457=CARTESIAN_POINT('Ctrl Pts',(0.989962567779687,-2.56226182368384,
7.50438785222352));
#406458=CARTESIAN_POINT('Ctrl Pts',(0.989669475365647,-2.56236486266006,
7.50459414719561));
#406459=CARTESIAN_POINT('Ctrl Pts',(0.989389773235812,-2.56244919073965,
7.50483629897752));
#406460=CARTESIAN_POINT('Ctrl Pts',(0.989134556580141,-2.56251283734951,
7.5050991045531));
#406461=CARTESIAN_POINT('Ctrl Pts',(0.988571523003644,-2.56265324816356,
7.50567888004914));
#406462=CARTESIAN_POINT('Ctrl Pts',(0.988105596423548,-2.56269904257184,
7.50637912803145));
#406463=CARTESIAN_POINT('Ctrl Pts',(0.987731664620582,-2.56268070472711,
7.50710440483569));
#406464=CARTESIAN_POINT('Ctrl Pts',(0.987639969118908,-2.56267620792353,
7.50728225710685));
#406465=CARTESIAN_POINT('Ctrl Pts',(0.987551972991268,-2.5626679109256,
7.50746498566955));
#406466=CARTESIAN_POINT('Ctrl Pts',(0.987469691245689,-2.56265642216574,
7.50764697238949));
#406467=CARTESIAN_POINT('Ctrl Pts',(0.987027367225998,-2.56259466175454,
7.50862528291182));
#406468=CARTESIAN_POINT('Ctrl Pts',(0.986709454310686,-2.56243915725785,
7.50965856837422));
#406469=CARTESIAN_POINT('Ctrl Pts',(0.986471889921157,-2.56223944537933,
7.51067959873203));
#406470=CARTESIAN_POINT('Ctrl Pts',(0.986341157937951,-2.56212954368068,
7.51124147302579));
#406471=CARTESIAN_POINT('Ctrl Pts',(0.986235005650205,-2.56200589525493,
7.51180065547253));
#406472=CARTESIAN_POINT('Ctrl Pts',(0.98614791253591,-2.56187474152437,
7.51235175716501));
#406473=CARTESIAN_POINT('Ctrl Pts',(0.985846971132247,-2.56142155313985,
7.51425603304536));
#406474=CARTESIAN_POINT('Ctrl Pts',(0.985742762481488,-2.56082136401568,
7.5162690050518));
#406475=CARTESIAN_POINT('Ctrl Pts',(0.985805085598317,-2.56012642898782,
7.51827788969243));
#406476=CARTESIAN_POINT('Ctrl Pts',(0.985808458643174,-2.56008881779087,
7.51838661432545));
#406477=CARTESIAN_POINT('Ctrl Pts',(0.985812326717548,-2.56005092221106,
7.51849533314857));
#406478=CARTESIAN_POINT('Ctrl Pts',(0.98581668737997,-2.56001274842383,
7.51860402984325));
#406479=CARTESIAN_POINT('Ctrl Pts',(1.00345144254816,-2.47854446586344,
7.57603338728985));
#406480=CARTESIAN_POINT('Ctrl Pts',(1.00038100552585,-2.5057575085012,7.55196141284922));
#406481=CARTESIAN_POINT('Ctrl Pts',(0.997314994683372,-2.53292355758907,
7.52783573083105));
#406482=CARTESIAN_POINT('Ctrl Pts',(0.994253029621964,-2.56004646612085,
7.50366116530176));
#406483=CARTESIAN_POINT('Origin',(3.46738858721E-16,-8.56451684780634E-16,
7.49482233047033));
#406484=CARTESIAN_POINT('Origin',(1.06332537456794,-2.5225474024882,7.49482233047033));
#406485=CARTESIAN_POINT('Origin',(0.,0.,7.50366116523517));
#406486=CARTESIAN_POINT('Origin',(0.991053119217926,-2.55180719586893,7.49482233047033));
#406487=CARTESIAN_POINT('Ctrl Pts',(1.07279460441741,-2.52479829015122,
7.51860402984325));
#406488=CARTESIAN_POINT('Ctrl Pts',(1.07867375938541,-2.52962859271858,
7.51860402984325));
#406489=CARTESIAN_POINT('Ctrl Pts',(1.08566466424083,-2.52662467272424,
7.51860402984325));
#406490=CARTESIAN_POINT('Ctrl Pts',(1.07497757558516,-2.52659181347634,
7.51041458714365));
#406491=CARTESIAN_POINT('Ctrl Pts',(1.08032998091007,-2.5289169205702,7.5100464290044));
#406492=CARTESIAN_POINT('Ctrl Pts',(1.08566659224939,-2.52662384427877,
7.50729136483009));
#406493=CARTESIAN_POINT('Ctrl Pts',(1.07405060721884,-2.52924971995458,
7.50215815450138));
#406494=CARTESIAN_POINT('Ctrl Pts',(1.0769578040486,-2.5303660850716,7.49877163671533));
#406495=CARTESIAN_POINT('Ctrl Pts',(1.08013710129291,-2.52902593857712,
7.49481588533172));
#406496=CARTESIAN_POINT('Ctrl Pts',(1.06675842366606,-2.53069169142692,
7.50366171572174));
#406497=CARTESIAN_POINT('Ctrl Pts',(1.06818074157475,-2.53406588377825,
7.50000045605858));
#406498=CARTESIAN_POINT('Ctrl Pts',(1.06818074157486,-2.5340658837782,7.49482233047317));
#406499=CARTESIAN_POINT('Origin',(1.08072982485792,-2.51514001512094,7.51860402984325));
#406500=CARTESIAN_POINT('Origin',(1.08072982485792,-2.51514001512094,9.));
#406501=CARTESIAN_POINT('Origin',(1.08072982485792,-2.51514001512094,8.75721825406948));
#406502=CARTESIAN_POINT('Ctrl Pts',(1.05989096392722,-2.51419847335743,
8.78942910404913));
#406503=CARTESIAN_POINT('Ctrl Pts',(1.06418404382886,-2.51775120380875,
8.7967269950169));
#406504=CARTESIAN_POINT('Ctrl Pts',(1.07104086177895,-2.51203652677664,
8.79893251111267));
#406505=CARTESIAN_POINT('Ctrl Pts',(1.06838645708339,-2.52117715623988,
8.78111911759584));
#406506=CARTESIAN_POINT('Ctrl Pts',(1.07348069887328,-2.52538322455977,
8.78644465894813));
#406507=CARTESIAN_POINT('Ctrl Pts',(1.08067618140392,-2.52164952091238,
8.78817647674133));
#406508=CARTESIAN_POINT('Ctrl Pts',(1.07368105107517,-2.52552643784495,
8.76780923932029));
#406509=CARTESIAN_POINT('Ctrl Pts',(1.07969783280627,-2.53048759440067,
8.76988516158373));
#406510=CARTESIAN_POINT('Ctrl Pts',(1.0867021275484,-2.52764572255948,8.77093053738832));
#406511=CARTESIAN_POINT('Ctrl Pts',(1.07264867770947,-2.52467838745471,
8.75371302330492));
#406512=CARTESIAN_POINT('Ctrl Pts',(1.07851730378655,-2.52951836982402,
8.75300828287559));
#406513=CARTESIAN_POINT('Ctrl Pts',(1.0855271460478,-2.52647589536948,8.75267964240738));
#406514=CARTESIAN_POINT('Origin',(1.06989435603299,-2.50623915016686,8.78727029226991));
#406515=CARTESIAN_POINT('Ctrl Pts',(1.00671661105395,-2.47051810124197,
8.85049129520029));
#406516=CARTESIAN_POINT('Ctrl Pts',(1.01122897392943,-2.47422481049724,
8.85711686593484));
#406517=CARTESIAN_POINT('Ctrl Pts',(1.01802024859359,-2.46903064544885,
8.85933012996512));
#406518=CARTESIAN_POINT('Ctrl Pts',(1.02515785026094,-2.48566677477142,
8.82945683644723));
#406519=CARTESIAN_POINT('Ctrl Pts',(1.02970766847652,-2.48940425195461,
8.83607469902389));
#406520=CARTESIAN_POINT('Ctrl Pts',(1.03649609897605,-2.48416504840347,
8.83829567148519));
#406521=CARTESIAN_POINT('Ctrl Pts',(1.04357160131378,-2.50079286798137,
8.80838214965003));
#406522=CARTESIAN_POINT('Ctrl Pts',(1.0481393752363,-2.50454509499454,8.81501364461989));
#406523=CARTESIAN_POINT('Ctrl Pts',(1.05494349880901,-2.49927701042776,
8.81722098428721));
#406524=CARTESIAN_POINT('Ctrl Pts',(1.06195995288114,-2.51589809662203,
8.78727029226991));
#406525=CARTESIAN_POINT('Ctrl Pts',(1.06652848552592,-2.51965094689243,
8.79393457792714));
#406526=CARTESIAN_POINT('Ctrl Pts',(1.07336460881944,-2.51436825501291,
8.79610912703474));
#406527=CARTESIAN_POINT('Origin',(1.0146510142058,-2.4608591547868,8.85049129520029));
#406528=CARTESIAN_POINT('Ctrl Pts',(0.995522110700944,-2.47505025214474,
8.85049129520029));
#406529=CARTESIAN_POINT('Ctrl Pts',(0.994859350710984,-2.48085213644372,
8.85711686593484));
#406530=CARTESIAN_POINT('Ctrl Pts',(0.986367352980535,-2.48184548263713,
8.85933012996512));
#406531=CARTESIAN_POINT('Ctrl Pts',(0.996108444897021,-2.46991740885651,
8.86332496987232));
#406532=CARTESIAN_POINT('Ctrl Pts',(0.991939266488174,-2.47190985603824,
8.86648636486737));
#406533=CARTESIAN_POINT('Ctrl Pts',(0.988024668749186,-2.46748808869534,
8.87206031107457));
#406534=CARTESIAN_POINT('Ctrl Pts',(1.00269746170462,-2.46721654538254,
8.86341338519876));
#406535=CARTESIAN_POINT('Ctrl Pts',(1.00708145117165,-2.4657151770109,8.86654584966058));
#406536=CARTESIAN_POINT('Ctrl Pts',(1.00675706511742,-2.4597974978649,8.87215952290714));
#406537=CARTESIAN_POINT('Ctrl Pts',(1.00671661105395,-2.47051810124197,
8.85049129520029));
#406538=CARTESIAN_POINT('Ctrl Pts',(1.01122897392943,-2.47422481049724,
8.85711686593484));
#406539=CARTESIAN_POINT('Ctrl Pts',(1.01802024859359,-2.46903064544885,
8.85933012996512));
#406540=CARTESIAN_POINT('Origin',(0.983102876847322,-2.47363158005823,8.85049129520029));
#406541=CARTESIAN_POINT('Ctrl Pts',(0.987408162934533,-2.54608077127964,
8.78727029226991));
#406542=CARTESIAN_POINT('Ctrl Pts',(0.986737152926397,-2.55195487727523,
8.79393457792714));
#406543=CARTESIAN_POINT('Ctrl Pts',(0.97815135164051,-2.55291583068589,
8.79610912703474));
#406544=CARTESIAN_POINT('Ctrl Pts',(0.990108979344133,-2.52243748478276,
8.80838214965001));
#406545=CARTESIAN_POINT('Ctrl Pts',(0.989438080774451,-2.52831061523213,
8.81501364461994));
#406546=CARTESIAN_POINT('Ctrl Pts',(0.980885428519814,-2.52925980014898,
8.81722098428721));
#406547=CARTESIAN_POINT('Ctrl Pts',(0.992813526340833,-2.49876154025726,
8.82945683644724));
#406548=CARTESIAN_POINT('Ctrl Pts',(0.992145265042246,-2.50461158370382,
8.8360746990239));
#406549=CARTESIAN_POINT('Ctrl Pts',(0.983623977915115,-2.50557059788233,
8.8382956714852));
#406550=CARTESIAN_POINT('Ctrl Pts',(0.995522110700944,-2.47505025214474,
8.85049129520029));
#406551=CARTESIAN_POINT('Ctrl Pts',(0.994859350710984,-2.48085213644372,
8.85711686593484));
#406552=CARTESIAN_POINT('Ctrl Pts',(0.986367352980535,-2.48184548263713,
8.85933012996512));
#406553=CARTESIAN_POINT('Origin',(0.974988929080911,-2.54466209919313,8.78727029226991));
#406554=CARTESIAN_POINT('Ctrl Pts',(0.985837683686217,-2.55982878158036,
8.75374538247848));
#406555=CARTESIAN_POINT('Ctrl Pts',(0.98498828679914,-2.56738013267245,
8.75304829418601));
#406556=CARTESIAN_POINT('Ctrl Pts',(0.977845758623038,-2.57007363122686,
8.75272238421917));
#406557=CARTESIAN_POINT('Ctrl Pts',(0.985687874189968,-2.56114023650866,
8.76769408445021));
#406558=CARTESIAN_POINT('Ctrl Pts',(0.98481641692612,-2.5688815359609,8.76974318093971));
#406559=CARTESIAN_POINT('Ctrl Pts',(0.977816320118244,-2.57171296704088,
8.77077869880429));
#406560=CARTESIAN_POINT('Ctrl Pts',(0.986455712341585,-2.55441846563452,
8.78108014887987));
#406561=CARTESIAN_POINT('Ctrl Pts',(0.985720959251978,-2.56097936307296,
8.78639403366322));
#406562=CARTESIAN_POINT('Ctrl Pts',(0.977971752381973,-2.56331856563252,
8.78812224174741));
#406563=CARTESIAN_POINT('Ctrl Pts',(0.987714029535141,-2.54340296701399,
8.78944554828685));
#406564=CARTESIAN_POINT('Ctrl Pts',(0.987100369825394,-2.54893287111602,
8.79673892988687));
#406565=CARTESIAN_POINT('Ctrl Pts',(0.9782088694197,-2.54959978554247,8.79894799272499));
#406566=CARTESIAN_POINT('Origin',(0.973397453526352,-2.55859407633732,8.75721825406948));
#406567=CARTESIAN_POINT('Origin',(0.973397453526352,-2.55859407633732,9.));
#406568=CARTESIAN_POINT('Origin',(0.973397453526352,-2.55859407633732,7.51860402984325));
#406569=CARTESIAN_POINT('Ctrl Pts',(0.994252744839196,-2.56004573276091,
7.50366195182966));
#406570=CARTESIAN_POINT('Ctrl Pts',(0.995578475926554,-2.56345928352135,
7.50000065167735));
#406571=CARTESIAN_POINT('Ctrl Pts',(0.995578475926445,-2.56345928352139,
7.49482233047108));
#406572=CARTESIAN_POINT('Ctrl Pts',(0.988005205888665,-2.56408578927886,
7.50215800491337));
#406573=CARTESIAN_POINT('Ctrl Pts',(0.986691781976957,-2.5669106104772,
7.49877273257268));
#406574=CARTESIAN_POINT('Ctrl Pts',(0.983473834939363,-2.5681603997447,
7.49481816995647));
#406575=CARTESIAN_POINT('Ctrl Pts',(0.985497132441383,-2.56281316053288,
7.51043025814043));
#406576=CARTESIAN_POINT('Ctrl Pts',(0.983271955087221,-2.5682114327314,
7.51006209594514));
#406577=CARTESIAN_POINT('Ctrl Pts',(0.97783982435821,-2.57027805458972,
7.50731281821702));
#406578=CARTESIAN_POINT('Ctrl Pts',(0.98581685882451,-2.56001124677167,
7.51860402984326));
#406579=CARTESIAN_POINT('Ctrl Pts',(0.984954168022284,-2.56757145721651,
7.51860402984326));
#406580=CARTESIAN_POINT('Ctrl Pts',(0.977842190757062,-2.57027715431147,
7.51860402984327));
#406581=CARTESIAN_POINT('Origin',(0.,0.,7.5));
#406582=CARTESIAN_POINT('Origin',(1.15205371787333,-2.40618167532513,7.5));
#406583=CARTESIAN_POINT('',(1.15205371787333,-2.40618167532513,7.59394543036555));
#406584=CARTESIAN_POINT('',(1.15205371787333,-2.40618167532513,8.85049129520029));
#406585=CARTESIAN_POINT('',(1.15205371787333,-2.40618167532513,7.5));
#406586=CARTESIAN_POINT('',(1.14850738206914,-2.47758611705877,8.78727029226991));
#406587=CARTESIAN_POINT('Ctrl Pts',(1.15205371787333,-2.40618167532513,
8.85049129520029));
#406588=CARTESIAN_POINT('Ctrl Pts',(1.15086988762442,-2.43001775366008,
8.82945686509571));
#406589=CARTESIAN_POINT('Ctrl Pts',(1.14968781728233,-2.45381839678236,
8.80838212259895));
#406590=CARTESIAN_POINT('Ctrl Pts',(1.14850738206914,-2.47758611705877,
8.78727029226991));
#406591=CARTESIAN_POINT('',(1.14781180121219,-2.4915914356506,8.75721825406948));
#406592=CARTESIAN_POINT('Origin',(1.14990524686342,-2.44944458353935,8.7593767971312));
#406593=CARTESIAN_POINT('',(1.14781180121219,-2.4915914356506,7.51860402984325));
#406594=CARTESIAN_POINT('',(1.14781180121219,-2.4915914356506,7.5));
#406595=CARTESIAN_POINT('Ctrl Pts',(1.14781180121219,-2.4915914356506,7.51860402984325));
#406596=CARTESIAN_POINT('Ctrl Pts',(1.14835807179204,-2.48059243613578,
7.52834476460825));
#406597=CARTESIAN_POINT('Ctrl Pts',(1.14890469700287,-2.46958629622919,
7.53807742314407));
#406598=CARTESIAN_POINT('Ctrl Pts',(1.14945168875189,-2.45857277618267,
7.54780169004674));
#406599=CARTESIAN_POINT('Ctrl Pts',(1.15031809411995,-2.44112795565896,
7.5632044032688));
#406600=CARTESIAN_POINT('Ctrl Pts',(1.15118542018668,-2.42366459713434,
7.57858609112103));
#406601=CARTESIAN_POINT('Ctrl Pts',(1.15205371787333,-2.40618167532513,
7.59394543036555));
#406602=CARTESIAN_POINT('Origin',(1.38617896354007,-2.56152510751203,7.5));
#406603=CARTESIAN_POINT('',(1.23235567333049,-2.45087725266271,8.75721825406948));
#406604=CARTESIAN_POINT('',(1.22097218676273,-2.4426889063615,8.78727029226991));
#406605=CARTESIAN_POINT('Origin',(1.19207665202558,-2.42190382934856,8.75658640621066));
#406606=CARTESIAN_POINT('',(1.16293484201943,-2.40094160211227,8.85049129520029));
#406607=CARTESIAN_POINT('Ctrl Pts',(1.22097218676273,-2.44268890636149,
8.78727029226991));
#406608=CARTESIAN_POINT('Ctrl Pts',(1.20165384546697,-2.42879287656841,
8.80838212259896));
#406609=CARTESIAN_POINT('Ctrl Pts',(1.1823087445676,-2.41487759811192,8.82945686509571));
#406610=CARTESIAN_POINT('Ctrl Pts',(1.16293484201943,-2.40094160211227,
8.85049129520029));
#406611=CARTESIAN_POINT('',(1.16293484201943,-2.40094160211227,7.59394543036555));
#406612=CARTESIAN_POINT('',(1.16293484201943,-2.40094160211227,7.5));
#406613=CARTESIAN_POINT('',(1.23235567333049,-2.45087725266271,7.51860402984325));
#406614=CARTESIAN_POINT('Ctrl Pts',(1.16293484201943,-2.40094160211227,
7.59394543036555));
#406615=CARTESIAN_POINT('Ctrl Pts',(1.177144915448,-2.41116316309943,7.57858609112103));
#406616=CARTESIAN_POINT('Ctrl Pts',(1.1913390878895,-2.42137328622107,7.56320440326857));
#406617=CARTESIAN_POINT('Ctrl Pts',(1.2055181926922,-2.43157257091954,7.54780169004651));
#406618=CARTESIAN_POINT('Ctrl Pts',(1.21446995317457,-2.43801173298108,
7.53807742314383));
#406619=CARTESIAN_POINT('Ctrl Pts',(1.22341571509856,-2.44444658017184,
7.52834476460825));
#406620=CARTESIAN_POINT('Ctrl Pts',(1.23235567333049,-2.45087725266271,
7.51860402984325));
#406621=CARTESIAN_POINT('',(1.23235567333049,-2.45087725266271,7.5));
#406622=CARTESIAN_POINT('Origin',(1.15892025438444,-2.40652270515029,7.5));
#406623=CARTESIAN_POINT('Ctrl Pts',(1.16293484201943,-2.40094160211227,
8.85049129520029));
#406624=CARTESIAN_POINT('Ctrl Pts',(1.16277762822757,-2.4008285154087,8.85097269580138));
#406625=CARTESIAN_POINT('Ctrl Pts',(1.16261748621829,-2.40072368386097,
8.85143669361005));
#406626=CARTESIAN_POINT('Ctrl Pts',(1.16244656312291,-2.40062301180747,
8.8519052845931));
#406627=CARTESIAN_POINT('Ctrl Pts',(1.16211224838788,-2.40042610365523,
8.85282181883899));
#406628=CARTESIAN_POINT('Ctrl Pts',(1.16174518876681,-2.40025034340575,
8.85372622499635));
#406629=CARTESIAN_POINT('Ctrl Pts',(1.16133296549051,-2.40010687975259,
8.8546225773507));
#406630=CARTESIAN_POINT('Ctrl Pts',(1.1609907523673,-2.39998778132309,8.85536669723986));
#406631=CARTESIAN_POINT('Ctrl Pts',(1.16061734602602,-2.39989088383228,
8.85610498449051));
#406632=CARTESIAN_POINT('Ctrl Pts',(1.16020359950664,-2.39983030360421,
8.85681338218371));
#406633=CARTESIAN_POINT('Ctrl Pts',(1.1598281238905,-2.39977532695209,8.85745625420284));
#406634=CARTESIAN_POINT('Ctrl Pts',(1.15941480250415,-2.39974897790984,
8.85808743050665));
#406635=CARTESIAN_POINT('Ctrl Pts',(1.15894967359855,-2.39977621475689,
8.8586680450841));
#406636=CARTESIAN_POINT('Ctrl Pts',(1.15873507320426,-2.39978878124769,
8.85893592806395));
#406637=CARTESIAN_POINT('Ctrl Pts',(1.15850935230519,-2.39981297869223,
8.85919241173848));
#406638=CARTESIAN_POINT('Ctrl Pts',(1.1582707442805,-2.39985280471822,8.85943017985534));
#406639=CARTESIAN_POINT('Ctrl Pts',(1.15794855281164,-2.39990658164308,
8.8597512372));
#406640=CARTESIAN_POINT('Ctrl Pts',(1.15759476909804,-2.39999085472495,
8.86004599534705));
#406641=CARTESIAN_POINT('Ctrl Pts',(1.15721605712058,-2.4001147430708,8.86026130871721));
#406642=CARTESIAN_POINT('Ctrl Pts',(1.15707739998861,-2.40016010208699,
8.86034014101235));
#406643=CARTESIAN_POINT('Ctrl Pts',(1.15693331461314,-2.40021144115131,
8.86040910639692));
#406644=CARTESIAN_POINT('Ctrl Pts',(1.15678783942167,-2.40026767842518,
8.86046313645507));
#406645=CARTESIAN_POINT('Ctrl Pts',(1.15656082660373,-2.40035543622007,
8.8605474499083));
#406646=CARTESIAN_POINT('Ctrl Pts',(1.15632428564956,-2.40045765448499,
8.86059655985669));
#406647=CARTESIAN_POINT('Ctrl Pts',(1.1560932704394,-2.40056750872952,8.86059725258816));
#406648=CARTESIAN_POINT('Ctrl Pts',(1.15586172149181,-2.40067761678125,
8.86059794692011));
#406649=CARTESIAN_POINT('Ctrl Pts',(1.15563429688715,-2.40079901655755,
8.86056369958366));
#406650=CARTESIAN_POINT('Ctrl Pts',(1.15542162839186,-2.40092176712124,
8.86048590497774));
#406651=CARTESIAN_POINT('Ctrl Pts',(1.15536612824649,-2.40095380136364,
8.86046560290182));
#406652=CARTESIAN_POINT('Ctrl Pts',(1.15531095632765,-2.40098642279828,
8.86044257503091));
#406653=CARTESIAN_POINT('Ctrl Pts',(1.15525780078614,-2.40101859513937,
8.86041778462583));
#406654=CARTESIAN_POINT('Ctrl Pts',(1.15490012995229,-2.40123507507237,
8.860250975962));
#406655=CARTESIAN_POINT('Ctrl Pts',(1.15458593018283,-2.40146055442195,
8.8599848982295));
#406656=CARTESIAN_POINT('Ctrl Pts',(1.15431943237592,-2.40168156859715,
8.85968173251462));
#406657=CARTESIAN_POINT('Ctrl Pts',(1.15417847030456,-2.40179847243323,
8.85952137522077));
#406658=CARTESIAN_POINT('Ctrl Pts',(1.15404801525878,-2.40191623341874,
8.85934740853961));
#406659=CARTESIAN_POINT('Ctrl Pts',(1.15392886528608,-2.40203203692091,
8.8591675900182));
#406660=CARTESIAN_POINT('Ctrl Pts',(1.15345041621273,-2.40249704817559,
8.85844552518695));
#406661=CARTESIAN_POINT('Ctrl Pts',(1.15312510486536,-2.40295460765929,
8.85759444184123));
#406662=CARTESIAN_POINT('Ctrl Pts',(1.15289337286033,-2.40335150126387,
8.85683498915137));
#406663=CARTESIAN_POINT('Ctrl Pts',(1.15286912272316,-2.40339303512257,
8.85675551444997));
#406664=CARTESIAN_POINT('Ctrl Pts',(1.15284591626144,-2.40343391112278,
8.85667699793651));
#406665=CARTESIAN_POINT('Ctrl Pts',(1.15282369784461,-2.40347407190826,
8.85659965593547));
#406666=CARTESIAN_POINT('Ctrl Pts',(1.15252379252049,-2.40401616424,8.85555568965886));
#406667=CARTESIAN_POINT('Ctrl Pts',(1.1523138537825,-2.40458046081931,8.85434650606346));
#406668=CARTESIAN_POINT('Ctrl Pts',(1.1521870191159,-2.40516758421233,8.85297329937117));
#406669=CARTESIAN_POINT('Ctrl Pts',(1.15211568234409,-2.40549780534694,
8.85220095427747));
#406670=CARTESIAN_POINT('Ctrl Pts',(1.15207091337418,-2.40583544890816,
8.85137579139183));
#406671=CARTESIAN_POINT('Ctrl Pts',(1.15205371787333,-2.40618167532513,
8.85049129520029));
#406672=CARTESIAN_POINT('Origin',(1.15892025438444,-2.40652270515029,7.59394543036555));
#406673=CARTESIAN_POINT('Ctrl Pts',(1.1624783973461,-2.40061327326238,7.59443877723642));
#406674=CARTESIAN_POINT('Ctrl Pts',(1.15777745639006,-2.397231802018,7.58783886950016));
#406675=CARTESIAN_POINT('Ctrl Pts',(1.15135964648122,-2.40278976005227,
7.58559994247159));
#406676=CARTESIAN_POINT('Ctrl Pts',(1.18814069610536,-2.41907262557727,
7.56670252222135));
#406677=CARTESIAN_POINT('Ctrl Pts',(1.1834465493436,-2.41569604151888,7.56004874999026));
#406678=CARTESIAN_POINT('Ctrl Pts',(1.17697672466145,-2.4212707814983,7.55786368756704));
#406679=CARTESIAN_POINT('Ctrl Pts',(1.21375507308567,-2.43749750689603,
7.53888913333558));
#406680=CARTESIAN_POINT('Ctrl Pts',(1.2090330287799,-2.43410085563323,7.53222002137276));
#406681=CARTESIAN_POINT('Ctrl Pts',(1.20254755552053,-2.43971700033598,
7.53005029815327));
#406682=CARTESIAN_POINT('Ctrl Pts',(1.23932036921914,-2.45588708348031,
7.51101258149734));
#406683=CARTESIAN_POINT('Ctrl Pts',(1.23454108515621,-2.45244925863235,
7.5043616886572));
#406684=CARTESIAN_POINT('Ctrl Pts',(1.22807082731706,-2.4581275722059,7.50217374673251));
#406685=CARTESIAN_POINT('',(1.22670887334889,-2.45714515960791,7.50366116523517));
#406686=CARTESIAN_POINT('Ctrl Pts',(1.23235567333049,-2.45087725266271,
7.51860402984325));
#406687=CARTESIAN_POINT('Ctrl Pts',(1.23271417190463,-2.45113512712465,
7.51734760759493));
#406688=CARTESIAN_POINT('Ctrl Pts',(1.23300338406209,-2.45141645289302,
7.51608817408573));
#406689=CARTESIAN_POINT('Ctrl Pts',(1.2332133335611,-2.45173015496621,7.5148100591312));
#406690=CARTESIAN_POINT('Ctrl Pts',(1.2334035108342,-2.45201431380026,7.51365231206384));
#406691=CARTESIAN_POINT('Ctrl Pts',(1.23352912772806,-2.45232529934387,
7.51247773061042));
#406692=CARTESIAN_POINT('Ctrl Pts',(1.23355377319635,-2.45267156000965,
7.51129758471022));
#406693=CARTESIAN_POINT('Ctrl Pts',(1.23358440469881,-2.45310192247275,
7.50983079813402));
#406694=CARTESIAN_POINT('Ctrl Pts',(1.23344508972213,-2.45357396654679,
7.50839324291155));
#406695=CARTESIAN_POINT('Ctrl Pts',(1.23305574351699,-2.45406780194778,
7.50715379678855));
#406696=CARTESIAN_POINT('Ctrl Pts',(1.23287587678896,-2.45429593967351,
7.50658120839351));
#406697=CARTESIAN_POINT('Ctrl Pts',(1.23260961778091,-2.45455527707924,
7.50598221009429));
#406698=CARTESIAN_POINT('Ctrl Pts',(1.23224743207234,-2.45482334770211,
7.50545747549611));
#406699=CARTESIAN_POINT('Ctrl Pts',(1.23205415856755,-2.45496639848404,
7.50517746087247));
#406700=CARTESIAN_POINT('Ctrl Pts',(1.23183159348028,-2.45511365010212,
7.50491486231392));
#406701=CARTESIAN_POINT('Ctrl Pts',(1.2315847103343,-2.45525981197482,7.50468370960992));
#406702=CARTESIAN_POINT('Ctrl Pts',(1.23121554215619,-2.45547837007867,
7.50433806340446));
#406703=CARTESIAN_POINT('Ctrl Pts',(1.23078064602179,-2.45570056625098,
7.50405484070983));
#406704=CARTESIAN_POINT('Ctrl Pts',(1.2303089854356,-2.45591079803973,7.50385766036131));
#406705=CARTESIAN_POINT('Ctrl Pts',(1.23025854866718,-2.45593327906179,
7.50383657498791));
#406706=CARTESIAN_POINT('Ctrl Pts',(1.23020771967552,-2.45595562650313,
7.50381643264937));
#406707=CARTESIAN_POINT('Ctrl Pts',(1.23015655431111,-2.45597782395208,
7.50379723213559));
#406708=CARTESIAN_POINT('Ctrl Pts',(1.2298150087663,-2.45612599918514,7.50366906242519));
#406709=CARTESIAN_POINT('Ctrl Pts',(1.22945075886671,-2.45627005426621,
7.50358235568538));
#406710=CARTESIAN_POINT('Ctrl Pts',(1.22909632909186,-2.45640046610438,
7.5035341175365));
#406711=CARTESIAN_POINT('Ctrl Pts',(1.22856490175818,-2.45659600389596,
7.50346178989176));
#406712=CARTESIAN_POINT('Ctrl Pts',(1.22798489283786,-2.45678376238721,
7.50346967198527));
#406713=CARTESIAN_POINT('Ctrl Pts',(1.22740983222609,-2.45695056293591,
7.50354272648692));
#406714=CARTESIAN_POINT('Ctrl Pts',(1.22717329789342,-2.45701917145415,
7.50357277531559));
#406715=CARTESIAN_POINT('Ctrl Pts',(1.22693795451664,-2.45708427923446,
7.50361331098761));
#406716=CARTESIAN_POINT('Ctrl Pts',(1.22670887334952,-2.45714515960918,
7.50366116523659));
#406717=CARTESIAN_POINT('',(1.16019063351034,-2.40916067458744,7.57603338622103));
#406718=CARTESIAN_POINT('Origin',(1.16402226679194,-2.41712371898013,7.58486873427627));
#406719=CARTESIAN_POINT('Ctrl Pts',(1.22670887339833,-2.45714515963696,
7.50366116529969));
#406720=CARTESIAN_POINT('Ctrl Pts',(1.20457181913612,-2.4411771094306,7.52783573079709));
#406721=CARTESIAN_POINT('Ctrl Pts',(1.18240010892814,-2.42518305082275,
7.55196141284068));
#406722=CARTESIAN_POINT('Ctrl Pts',(1.16019063469131,-2.40916067500332,
7.57603338728831));
#406723=CARTESIAN_POINT('Ctrl Pts',(1.16366703458207,-2.40168485817268,
7.59639677331372));
#406724=CARTESIAN_POINT('Ctrl Pts',(1.15070316512304,-2.38880037120621,
7.59959882295461));
#406725=CARTESIAN_POINT('Ctrl Pts',(1.15216122323506,-2.40703722617453,
7.59642833564546));
#406726=CARTESIAN_POINT('Ctrl Pts',(1.16137835885355,-2.39852620854137,
7.58707626057423));
#406727=CARTESIAN_POINT('Ctrl Pts',(1.15468113347971,-2.39749690619127,
7.58809943920598));
#406728=CARTESIAN_POINT('Ctrl Pts',(1.151224101942,-2.40330752868284,7.58710240504251));
#406729=CARTESIAN_POINT('Ctrl Pts',(1.16034302571037,-2.40451400592806,
7.5801537675693));
#406730=CARTESIAN_POINT('Ctrl Pts',(1.15760519591849,-2.40371804146504,
7.5820588065976));
#406731=CARTESIAN_POINT('Ctrl Pts',(1.15649513461978,-2.40630548015053,
7.58020924244129));
#406732=CARTESIAN_POINT('Ctrl Pts',(1.16019063315146,-2.40916067384174,
7.57603338509286));
#406733=CARTESIAN_POINT('Ctrl Pts',(1.16019063315146,-2.40916067384174,
7.57603338509286));
#406734=CARTESIAN_POINT('Ctrl Pts',(1.16019063315146,-2.40916067384174,
7.57603338509286));
#406735=CARTESIAN_POINT('Origin',(1.16402740803763,-2.41712124308664,7.58486873427621));
#406736=CARTESIAN_POINT('Ctrl Pts',(1.14738488275127,-2.50018731490472,
7.51098857897448));
#406737=CARTESIAN_POINT('Ctrl Pts',(1.14767691925915,-2.49430724461178,
7.50433767179956));
#406738=CARTESIAN_POINT('Ctrl Pts',(1.15615057871823,-2.49278897373537,
7.50214974420965));
#406739=CARTESIAN_POINT('Ctrl Pts',(1.14894748356408,-2.46872480124225,
7.53887321589167));
#406740=CARTESIAN_POINT('Ctrl Pts',(1.14923602095633,-2.46291518462664,
7.53220407452059));
#406741=CARTESIAN_POINT('Ctrl Pts',(1.15767055140447,-2.46134623082197,
7.53003438070911));
#406742=CARTESIAN_POINT('Ctrl Pts',(1.15051308514687,-2.43720186794752,
7.56669465659231));
#406743=CARTESIAN_POINT('Ctrl Pts',(1.15079991733674,-2.43142658508602,
7.56004085833299));
#406744=CARTESIAN_POINT('Ctrl Pts',(1.15919230779771,-2.42984404520438,
7.55785582193789));
#406745=CARTESIAN_POINT('Ctrl Pts',(1.15208161669374,-2.40561994067662,
7.59443891967696));
#406746=CARTESIAN_POINT('Ctrl Pts',(1.1523688647546,-2.39983628437402,7.58783901202978));
#406747=CARTESIAN_POINT('Ctrl Pts',(1.16071569012911,-2.39828396863431,
7.58560008491213));
#406748=CARTESIAN_POINT('',(1.15623297039279,-2.49108456570911,7.50366116523517));
#406749=CARTESIAN_POINT('Ctrl Pts',(1.15623297039294,-2.49108456570945,
7.50366116523554));
#406750=CARTESIAN_POINT('Ctrl Pts',(1.15562413094777,-2.49153562229877,
7.50350835821027));
#406751=CARTESIAN_POINT('Ctrl Pts',(1.15504978507183,-2.49193044482336,
7.50345484956));
#406752=CARTESIAN_POINT('Ctrl Pts',(1.15449319717329,-2.49228126653246,
7.50349758195598));
#406753=CARTESIAN_POINT('Ctrl Pts',(1.1542076263037,-2.49246126408685,7.50351950684424));
#406754=CARTESIAN_POINT('Ctrl Pts',(1.15389865214388,-2.49264752943228,
7.50357029184312));
#406755=CARTESIAN_POINT('Ctrl Pts',(1.15359577469402,-2.49281895317991,
7.50365515313923));
#406756=CARTESIAN_POINT('Ctrl Pts',(1.15312982652894,-2.49308267232009,
7.50378570417639));
#406757=CARTESIAN_POINT('Ctrl Pts',(1.15266480092325,-2.49331930930963,
7.50400001621911));
#406758=CARTESIAN_POINT('Ctrl Pts',(1.1522350633868,-2.49350882914524,7.50428903009635));
#406759=CARTESIAN_POINT('Ctrl Pts',(1.15218736582646,-2.49352986438892,
7.50432110841318));
#406760=CARTESIAN_POINT('Ctrl Pts',(1.15214008709821,-2.49355034499863,
7.50435406373354));
#406761=CARTESIAN_POINT('Ctrl Pts',(1.15209326220264,-2.49357026247504,
7.50438785222352));
#406762=CARTESIAN_POINT('Ctrl Pts',(1.15180737370827,-2.49369186824209,
7.50459414719561));
#406763=CARTESIAN_POINT('Ctrl Pts',(1.15153364917507,-2.49379394363758,
7.50483629897752));
#406764=CARTESIAN_POINT('Ctrl Pts',(1.15128303474168,-2.49387381126592,
7.5050991045531));
#406765=CARTESIAN_POINT('Ctrl Pts',(1.1507301541298,-2.494050007276,7.50567888004914));
#406766=CARTESIAN_POINT('Ctrl Pts',(1.15026811890364,-2.49412555961323,
7.50637912803145));
#406767=CARTESIAN_POINT('Ctrl Pts',(1.14989378047392,-2.49413121733845,
7.50710440483569));
#406768=CARTESIAN_POINT('Ctrl Pts',(1.1498019852593,-2.49413260472499,7.50728225710685));
#406769=CARTESIAN_POINT('Ctrl Pts',(1.14971363833866,-2.49412996270539,
7.50746498566955));
#406770=CARTESIAN_POINT('Ctrl Pts',(1.14963078956238,-2.49412376935996,
7.50764697238949));
#406771=CARTESIAN_POINT('Ctrl Pts',(1.14918541734169,-2.4940904756394,7.50862528291181));
#406772=CARTESIAN_POINT('Ctrl Pts',(1.14885819440525,-2.49395565939379,
7.50965856837421));
#406773=CARTESIAN_POINT('Ctrl Pts',(1.14860832253325,-2.49377157864745,
7.51067959873201));
#406774=CARTESIAN_POINT('Ctrl Pts',(1.14847081772692,-2.49367027878054,
7.51124147302578));
#406775=CARTESIAN_POINT('Ctrl Pts',(1.14835696135859,-2.49355368560417,
7.51180065547253));
#406776=CARTESIAN_POINT('Ctrl Pts',(1.14826164413807,-2.49342838141801,
7.51235175716501));
#406777=CARTESIAN_POINT('Ctrl Pts',(1.14793228517131,-2.49299540553956,
7.51425603304536));
#406778=CARTESIAN_POINT('Ctrl Pts',(1.14778983637918,-2.49240312623949,
7.51626900505181));
#406779=CARTESIAN_POINT('Ctrl Pts',(1.14780750680638,-2.49170562597437,
7.51827788969244));
#406780=CARTESIAN_POINT('Ctrl Pts',(1.14780846316329,-2.49166787594193,
7.51838661432546));
#406781=CARTESIAN_POINT('Ctrl Pts',(1.14780989531216,-2.49162981039429,
7.51849533314857));
#406782=CARTESIAN_POINT('Ctrl Pts',(1.14781180121218,-2.4915914356506,7.51860402984325));
#406783=CARTESIAN_POINT('Ctrl Pts',(1.16019063309946,-2.40916067577124,
7.57603338728985));
#406784=CARTESIAN_POINT('Ctrl Pts',(1.15887005024747,-2.43651452986977,
7.55196141284922));
#406785=CARTESIAN_POINT('Ctrl Pts',(1.15755087359419,-2.46382120338538,
7.52783573083105));
#406786=CARTESIAN_POINT('Ctrl Pts',(1.15623297038451,-2.49108456576771,
7.50366116530176));
#406787=CARTESIAN_POINT('Origin',(4.00899494394879E-16,-8.32476377985981E-16,
7.49482233047033));
#406788=CARTESIAN_POINT('Origin',(1.2227608255338,-2.44923706764778,7.49482233047033));
#406789=CARTESIAN_POINT('Origin',(0.,0.,7.50366116523517));
#406790=CARTESIAN_POINT('Origin',(1.15251174268207,-2.48306724294369,7.49482233047033));
#406791=CARTESIAN_POINT('Ctrl Pts',(1.23235481470268,-2.45087663498119,
7.51860402984325));
#406792=CARTESIAN_POINT('Ctrl Pts',(1.23853136886433,-2.45532033442178,
7.51860402984325));
#406793=CARTESIAN_POINT('Ctrl Pts',(1.24531544834112,-2.45187467749128,
7.51860402984325));
#406794=CARTESIAN_POINT('Ctrl Pts',(1.23464821215602,-2.45252660987735,
7.51041458714366));
#406795=CARTESIAN_POINT('Ctrl Pts',(1.24013859051314,-2.45450401000272,
7.51004642900443));
#406796=CARTESIAN_POINT('Ctrl Pts',(1.24531731930969,-2.45187372722001,
7.5072913648301));
#406797=CARTESIAN_POINT('Ctrl Pts',(1.2338934409984,-2.45523844646883,7.50215815450137));
#406798=CARTESIAN_POINT('Ctrl Pts',(1.2368661904391,-2.4561662531536,7.49877163671529));
#406799=CARTESIAN_POINT('Ctrl Pts',(1.23995309199553,-2.45462516185997,
7.4948158853317));
#406800=CARTESIAN_POINT('Ctrl Pts',(1.22670862744824,-2.45714466706049,
7.50366171572174));
#406801=CARTESIAN_POINT('Ctrl Pts',(1.22834420829845,-2.46042079855046,
7.50000045605858));
#406802=CARTESIAN_POINT('Ctrl Pts',(1.22834420829856,-2.4604207985504,7.49482233047317));
#406803=CARTESIAN_POINT('Origin',(1.23965492357593,-2.44072979259359,7.51860402984325));
#406804=CARTESIAN_POINT('Origin',(1.23965492357593,-2.44072979259359,9.));
#406805=CARTESIAN_POINT('Origin',(1.23965492357593,-2.44072979259359,8.75721825406948));
#406806=CARTESIAN_POINT('Ctrl Pts',(1.21879855353206,-2.44112533573259,
8.78942910404913));
#406807=CARTESIAN_POINT('Ctrl Pts',(1.22331043706217,-2.44439570814448,
8.79672699501692));
#406808=CARTESIAN_POINT('Ctrl Pts',(1.22978702632982,-2.43825345469478,
8.79893251111267));
#406809=CARTESIAN_POINT('Ctrl Pts',(1.22772371753385,-2.44754537204723,
8.7811191175958));
#406810=CARTESIAN_POINT('Ctrl Pts',(1.23307697638015,-2.45141640935655,
8.7864446589481));
#406811=CARTESIAN_POINT('Ctrl Pts',(1.24001845580619,-2.44722936085514,
8.78817647674131));
#406812=CARTESIAN_POINT('Ctrl Pts',(1.23328609264361,-2.45154649178501,
8.76780923932032));
#406813=CARTESIAN_POINT('Ctrl Pts',(1.23960837464324,-2.45611195858344,
8.76988516158377));
#406814=CARTESIAN_POINT('Ctrl Pts',(1.2464161989566,-2.4528271589678,8.77093053738834));
#406815=CARTESIAN_POINT('Ctrl Pts',(1.23220150562468,-2.45076632819391,
8.75371302330492));
#406816=CARTESIAN_POINT('Ctrl Pts',(1.23836817271518,-2.45522036213662,
8.75300828287558));
#406817=CARTESIAN_POINT('Ctrl Pts',(1.24516868049613,-2.45173501663643,
8.75267964240738));
#406818=CARTESIAN_POINT('Origin',(1.22827143700817,-2.43254144629237,8.78727029226991));
#406819=CARTESIAN_POINT('Ctrl Pts',(1.16293484201943,-2.40094160211227,
8.85049129520029));
#406820=CARTESIAN_POINT('Ctrl Pts',(1.16767542343882,-2.40435158745376,
8.85711686593484));
#406821=CARTESIAN_POINT('Ctrl Pts',(1.17411995340356,-2.39873297591286,
8.85933012996512));
#406822=CARTESIAN_POINT('Ctrl Pts',(1.18230877056809,-2.41487761681454,
8.82945683644721));
#406823=CARTESIAN_POINT('Ctrl Pts',(1.18708870167946,-2.41831590709608,
8.83607469902387));
#406824=CARTESIAN_POINT('Ctrl Pts',(1.19352750769644,-2.41265253181512,
8.83829567148519));
#406825=CARTESIAN_POINT('Ctrl Pts',(1.20165382071394,-2.42879285876311,
8.80838214965003));
#406826=CARTESIAN_POINT('Ctrl Pts',(1.20645261566523,-2.43224471814344,
8.81501364461995));
#406827=CARTESIAN_POINT('Ctrl Pts',(1.21290523209922,-2.42655151572731,
8.81722098428721));
#406828=CARTESIAN_POINT('Ctrl Pts',(1.22097218676273,-2.44268890636149,
8.78727029226991));
#406829=CARTESIAN_POINT('Ctrl Pts',(1.22577177880959,-2.44614133910698,
8.79393457792714));
#406830=CARTESIAN_POINT('Ctrl Pts',(1.23225539332383,-2.44043150916126,
8.79610912703474));
#406831=CARTESIAN_POINT('Origin',(1.17023409226487,-2.39079414204315,8.85049129520029));
#406832=CARTESIAN_POINT('Ctrl Pts',(1.15205371787333,-2.40618167532513,
8.85049129520029));
#406833=CARTESIAN_POINT('Ctrl Pts',(1.15176404759819,-2.41201410220892,
8.85711686593484));
#406834=CARTESIAN_POINT('Ctrl Pts',(1.14335314149697,-2.4135494916287,8.85933012996512));
#406835=CARTESIAN_POINT('Ctrl Pts',(1.15230998498431,-2.40102181145301,
8.86332496987232));
#406836=CARTESIAN_POINT('Ctrl Pts',(1.14827702912889,-2.40327728511609,
8.86648636486737));
#406837=CARTESIAN_POINT('Ctrl Pts',(1.14408717074443,-2.39911541190671,
8.87206031107457));
#406838=CARTESIAN_POINT('Ctrl Pts',(1.1587124190333,-2.39790433743638,8.86341338519876));
#406839=CARTESIAN_POINT('Ctrl Pts',(1.16299120812194,-2.39612517061756,
8.86654584966059));
#406840=CARTESIAN_POINT('Ctrl Pts',(1.16228834154898,-2.39024043346388,
8.87215952290714));
#406841=CARTESIAN_POINT('Ctrl Pts',(1.16293484201943,-2.40094160211227,
8.85049129520029));
#406842=CARTESIAN_POINT('Ctrl Pts',(1.16767542343882,-2.40435158745376,
8.85711686593484));
#406843=CARTESIAN_POINT('Ctrl Pts',(1.17411995340356,-2.39873297591286,
8.85933012996512));
#406844=CARTESIAN_POINT('Origin',(1.13956910603496,-2.40556162109756,8.85049129520029));
#406845=CARTESIAN_POINT('Ctrl Pts',(1.14850738206914,-2.47758611705877,
8.78727029226991));
#406846=CARTESIAN_POINT('Ctrl Pts',(1.14821410598636,-2.48349114583243,
8.79393457792714));
#406847=CARTESIAN_POINT('Ctrl Pts',(1.13970751364645,-2.48500021903834,
8.79610912703474));
#406848=CARTESIAN_POINT('Ctrl Pts',(1.14968781879484,-2.45381836632824,
8.80838214965001));
#406849=CARTESIAN_POINT('Ctrl Pts',(1.14939459141809,-2.45972241442015,
8.81501364461992));
#406850=CARTESIAN_POINT('Ctrl Pts',(1.1409203259912,-2.46121761944617,8.81722098428721));
#406851=CARTESIAN_POINT('Ctrl Pts',(1.15086988603568,-2.43001778564902,
8.82945683644727));
#406852=CARTESIAN_POINT('Ctrl Pts',(1.15057781132211,-2.4358986252023,8.83607469902394));
#406853=CARTESIAN_POINT('Ctrl Pts',(1.14213547634265,-2.43740162972406,
8.8382956714852));
#406854=CARTESIAN_POINT('Ctrl Pts',(1.15205371787333,-2.40618167532513,
8.85049129520029));
#406855=CARTESIAN_POINT('Ctrl Pts',(1.15176404759819,-2.41201410220892,
8.85711686593484));
#406856=CARTESIAN_POINT('Ctrl Pts',(1.14335314149697,-2.4135494916287,8.85933012996512));
#406857=CARTESIAN_POINT('Origin',(1.13602277023077,-2.47696606283121,8.78727029226991));
#406858=CARTESIAN_POINT('Ctrl Pts',(1.14782096758314,-2.49140650154879,
8.75374538247848));
#406859=CARTESIAN_POINT('Ctrl Pts',(1.14745713259868,-2.49899675862557,
8.75304829418601));
#406860=CARTESIAN_POINT('Ctrl Pts',(1.14050185255765,-2.50214234644979,
8.75272238421917));
#406861=CARTESIAN_POINT('Ctrl Pts',(1.14775549109232,-2.49272486027965,
8.76769408445019));
#406862=CARTESIAN_POINT('Ctrl Pts',(1.14738181108972,-2.50050608886051,
8.76974318093969));
#406863=CARTESIAN_POINT('Ctrl Pts',(1.14057750714366,-2.50378020020404,
8.7707786988043));
#406864=CARTESIAN_POINT('Ctrl Pts',(1.14809108629953,-2.48596770444542,
8.78108014887992));
#406865=CARTESIAN_POINT('Ctrl Pts',(1.14777820098111,-2.4925621976085,8.78639403366325));
#406866=CARTESIAN_POINT('Ctrl Pts',(1.14019478891027,-2.49539308741434,
8.78812224174741));
#406867=CARTESIAN_POINT('Ctrl Pts',(1.14864105272565,-2.47489421768879,
8.78944554828685));
#406868=CARTESIAN_POINT('Ctrl Pts',(1.14838295601787,-2.48045207732235,
8.79673892988686));
#406869=CARTESIAN_POINT('Ctrl Pts',(1.13955245350739,-2.48168730188855,
8.79894799272499));
#406870=CARTESIAN_POINT('Origin',(1.13532718937381,-2.49097138142303,8.75721825406948));
#406871=CARTESIAN_POINT('Origin',(1.13532718937381,-2.49097138142303,9.));
#406872=CARTESIAN_POINT('Origin',(1.13532718937381,-2.49097138142303,7.51860402984325));
#406873=CARTESIAN_POINT('Ctrl Pts',(1.15623263920033,-2.49108385216064,
7.50366195182966));
#406874=CARTESIAN_POINT('Ctrl Pts',(1.15777435337912,-2.49440544953253,
7.50000065167736));
#406875=CARTESIAN_POINT('Ctrl Pts',(1.15777435337901,-2.49440544953258,
7.49482233047108));
#406876=CARTESIAN_POINT('Ctrl Pts',(1.15025678379846,-2.49551588914408,
7.50215800491337));
#406877=CARTESIAN_POINT('Ctrl Pts',(1.14912704537263,-2.49841905780325,
7.49877273257265));
#406878=CARTESIAN_POINT('Ctrl Pts',(1.14599578422564,-2.49987245381924,
7.49481816995649));
#406879=CARTESIAN_POINT('Ctrl Pts',(1.14767232585336,-2.49440656796782,
7.51043025814043));
#406880=CARTESIAN_POINT('Ctrl Pts',(1.14579758885199,-2.49993631643975,
7.51006209594516));
#406881=CARTESIAN_POINT('Ctrl Pts',(1.14050902793524,-2.50234673001258,
7.50731281821699));
#406882=CARTESIAN_POINT('Ctrl Pts',(1.14781187609329,-2.49158992609924,
7.51860402984326));
#406883=CARTESIAN_POINT('Ctrl Pts',(1.14743534212814,-2.49918987607038,
7.51860402984326));
#406884=CARTESIAN_POINT('Ctrl Pts',(1.14051133179104,-2.50234567996835,
7.51860402984327));
#406885=CARTESIAN_POINT('Origin',(0.,0.,7.5));
#406886=CARTESIAN_POINT('Origin',(1.30385128920423,-2.32742558187725,7.5));
#406887=CARTESIAN_POINT('',(1.30385128920423,-2.32742558187725,7.59394543036555));
#406888=CARTESIAN_POINT('',(1.30385128920423,-2.32742558187725,8.85049129520029));
#406889=CARTESIAN_POINT('',(1.30385128920423,-2.32742558187725,7.5));
#406890=CARTESIAN_POINT('',(1.30488713801677,-2.39891053004235,8.78727029226991));
#406891=CARTESIAN_POINT('Ctrl Pts',(1.30385128920423,-2.32742558187725,
8.85049129520029));
#406892=CARTESIAN_POINT('Ctrl Pts',(1.30419707404393,-2.35128853469732,
8.82945686509571));
#406893=CARTESIAN_POINT('Ctrl Pts',(1.30454234483265,-2.37511601235255,
8.80838212259895));
#406894=CARTESIAN_POINT('Ctrl Pts',(1.30488713801677,-2.39891053004236,
8.78727029226991));
#406895=CARTESIAN_POINT('',(1.30509031014836,-2.41293163922358,8.75721825406948));
#406896=CARTESIAN_POINT('Origin',(1.30447909650471,-2.37073725481645,8.75937679713112));
#406897=CARTESIAN_POINT('',(1.30509031014836,-2.41293163922358,7.51860402984325));
#406898=CARTESIAN_POINT('',(1.30509031014836,-2.41293163922358,7.5));
#406899=CARTESIAN_POINT('Ctrl Pts',(1.30509031014836,-2.41293163922358,
7.51860402984325));
#406900=CARTESIAN_POINT('Ctrl Pts',(1.30493075003824,-2.40192023865669,
7.52834476460825));
#406901=CARTESIAN_POINT('Ctrl Pts',(1.304771086344,-2.39090168964744,7.53807742314407));
#406902=CARTESIAN_POINT('Ctrl Pts',(1.30461131558766,-2.37987575217737,
7.54780169004674));
#406903=CARTESIAN_POINT('Ctrl Pts',(1.30435824734449,-2.36241126312585,
7.5632044032688));
#406904=CARTESIAN_POINT('Ctrl Pts',(1.30410491017452,-2.34492821517236,
7.57858609112103));
#406905=CARTESIAN_POINT('Ctrl Pts',(1.30385128920423,-2.32742558187725,
7.59394543036555));
#406906=CARTESIAN_POINT('Origin',(1.54744838731667,-2.46744938832929,7.5));
#406907=CARTESIAN_POINT('',(1.38685191115373,-2.36688436340659,8.75721825406948));
#406908=CARTESIAN_POINT('',(1.3749671840312,-2.35944218342959,8.78727029226991));
#406909=CARTESIAN_POINT('Origin',(1.34479931381015,-2.34055115485206,8.75658640620957));
#406910=CARTESIAN_POINT('',(1.31437432427031,-2.32149911893913,8.85049129520029));
#406911=CARTESIAN_POINT('Ctrl Pts',(1.3749671840312,-2.35944218342959,8.78727029226991));
#406912=CARTESIAN_POINT('Ctrl Pts',(1.35479821265381,-2.34681243489654,
8.80838212259896));
#406913=CARTESIAN_POINT('Ctrl Pts',(1.33460130338719,-2.33416519174222,
8.82945686509571));
#406914=CARTESIAN_POINT('Ctrl Pts',(1.31437432427031,-2.32149911893913,
8.85049129520029));
#406915=CARTESIAN_POINT('',(1.31437432427031,-2.32149911893913,7.59394543036555));
#406916=CARTESIAN_POINT('',(1.31437432427031,-2.32149911893913,7.5));
#406917=CARTESIAN_POINT('',(1.38685191115373,-2.36688436340659,7.51860402984325));
#406918=CARTESIAN_POINT('Ctrl Pts',(1.31437432427031,-2.32149911893913,
7.59394543036555));
#406919=CARTESIAN_POINT('Ctrl Pts',(1.32921009923999,-2.33078923610247,
7.57858609112103));
#406920=CARTESIAN_POINT('Ctrl Pts',(1.34402927306632,-2.34006895768036,
7.56320440326857));
#406921=CARTESIAN_POINT('Ctrl Pts',(1.35883271579178,-2.3493388284907,7.54780169004651));
#406922=CARTESIAN_POINT('Ctrl Pts',(1.36817864245194,-2.35519121933987,
7.53807742314383));
#406923=CARTESIAN_POINT('Ctrl Pts',(1.37751830642368,-2.36103968851258,
7.52834476460825));
#406924=CARTESIAN_POINT('Ctrl Pts',(1.38685191115373,-2.36688436340659,
7.51860402984325));
#406925=CARTESIAN_POINT('',(1.38685191115373,-2.36688436340659,7.5));
#406926=CARTESIAN_POINT('Origin',(1.31072556753556,-2.32732597051529,7.5));
#406927=CARTESIAN_POINT('Ctrl Pts',(1.31437432427031,-2.32149911893913,
8.85049129520029));
#406928=CARTESIAN_POINT('Ctrl Pts',(1.31421018800108,-2.32139633730655,
8.85097269580138));
#406929=CARTESIAN_POINT('Ctrl Pts',(1.3140436584404,-2.32130198148024,8.85143669361005));
#406930=CARTESIAN_POINT('Ctrl Pts',(1.31386663644423,-2.3212124673486,8.8519052845931));
#406931=CARTESIAN_POINT('Ctrl Pts',(1.31352039264605,-2.32103738338388,
8.85282181883899));
#406932=CARTESIAN_POINT('Ctrl Pts',(1.3131428261905,-2.32088550184336,8.85372622499635));
#406933=CARTESIAN_POINT('Ctrl Pts',(1.31272225812331,-2.32076874418765,
8.85462257735071));
#406934=CARTESIAN_POINT('Ctrl Pts',(1.31237311745109,-2.32067181612873,
8.85536669723986));
#406935=CARTESIAN_POINT('Ctrl Pts',(1.31199427006963,-2.32059904195064,
8.85610498449051));
#406936=CARTESIAN_POINT('Ctrl Pts',(1.31157749224831,-2.32056509502165,
8.85681338218371));
#406937=CARTESIAN_POINT('Ctrl Pts',(1.31119926572089,-2.32053428813029,
8.85745625420284));
#406938=CARTESIAN_POINT('Ctrl Pts',(1.31078510535873,-2.32053447481711,
8.85808743050666));
#406939=CARTESIAN_POINT('Ctrl Pts',(1.31032267718113,-2.32059145661444,
8.85866804508411));
#406940=CARTESIAN_POINT('Ctrl Pts',(1.3101093228442,-2.32061774678051,8.85893592806396));
#406941=CARTESIAN_POINT('Ctrl Pts',(1.30988561604852,-2.32065635649647,
8.85919241173848));
#406942=CARTESIAN_POINT('Ctrl Pts',(1.30965004993186,-2.32071138836425,
8.85943017985534));
#406943=CARTESIAN_POINT('Ctrl Pts',(1.30933196593933,-2.32078569767693,
8.8597512372));
#406944=CARTESIAN_POINT('Ctrl Pts',(1.30898430850721,-2.32089246461107,
8.86004599534706));
#406945=CARTESIAN_POINT('Ctrl Pts',(1.30861431218769,-2.32104036257473,
8.86026130871721));
#406946=CARTESIAN_POINT('Ctrl Pts',(1.30847884610382,-2.32109451218891,
8.86034014101235));
#406947=CARTESIAN_POINT('Ctrl Pts',(1.30833834607235,-2.32115497735332,
8.86040910639692));
#406948=CARTESIAN_POINT('Ctrl Pts',(1.30819677290977,-2.32122041970919,
8.86046313645506));
#406949=CARTESIAN_POINT('Ctrl Pts',(1.30797584917523,-2.32132254195747,
8.86054744990829));
#406950=CARTESIAN_POINT('Ctrl Pts',(1.30774634336655,-2.32143970543497,
8.86059655985669));
#406951=CARTESIAN_POINT('Ctrl Pts',(1.30752284118752,-2.32156413516751,
8.86059725258816));
#406952=CARTESIAN_POINT('Ctrl Pts',(1.30729882262918,-2.32168885238244,
8.86059794692012));
#406953=CARTESIAN_POINT('Ctrl Pts',(1.30707964340312,-2.32182457387433,
8.86056369958366));
#406954=CARTESIAN_POINT('Ctrl Pts',(1.30687527651368,-2.3219606979511,8.86048590497774));
#406955=CARTESIAN_POINT('Ctrl Pts',(1.30682194284028,-2.32199622228223,
8.86046560290182));
#406956=CARTESIAN_POINT('Ctrl Pts',(1.30676897434056,-2.32203231156962,
8.86044257503091));
#406957=CARTESIAN_POINT('Ctrl Pts',(1.30671798930178,-2.32206782349642,
8.86041778462583));
#406958=CARTESIAN_POINT('Ctrl Pts',(1.30637492325794,-2.32230677469718,
8.86025097596201));
#406959=CARTESIAN_POINT('Ctrl Pts',(1.30607581555714,-2.3225519216236,8.8599848982295));
#406960=CARTESIAN_POINT('Ctrl Pts',(1.30582402572537,-2.32278955627459,
8.85968173251461));
#406961=CARTESIAN_POINT('Ctrl Pts',(1.30569084333021,-2.32291525139012,
8.85952137522076));
#406962=CARTESIAN_POINT('Ctrl Pts',(1.30556820129056,-2.32304112870654,
8.85934740853961));
#406963=CARTESIAN_POINT('Ctrl Pts',(1.30545671568011,-2.32316432824296,
8.8591675900182));
#406964=CARTESIAN_POINT('Ctrl Pts',(1.30500904300508,-2.32365903841951,
8.85844552518696));
#406965=CARTESIAN_POINT('Ctrl Pts',(1.30471371598155,-2.32413650056776,
8.85759444184126));
#406966=CARTESIAN_POINT('Ctrl Pts',(1.30450788915532,-2.32454742583239,
8.85683498915141));
#406967=CARTESIAN_POINT('Ctrl Pts',(1.30448634992612,-2.32459042806696,
8.85675551445));
#406968=CARTESIAN_POINT('Ctrl Pts',(1.30446581007889,-2.32463270692615,
8.85667699793652));
#406969=CARTESIAN_POINT('Ctrl Pts',(1.30444621042253,-2.32467420873585,
8.85659965593547));
#406970=CARTESIAN_POINT('Ctrl Pts',(1.30418165326101,-2.32523440228085,
8.85555568965886));
#406971=CARTESIAN_POINT('Ctrl Pts',(1.30400830047065,-2.32581099027345,
8.85434650606346));
#406972=CARTESIAN_POINT('Ctrl Pts',(1.30391934352442,-2.32640503368347,
8.85297329937117));
#406973=CARTESIAN_POINT('Ctrl Pts',(1.3038693106624,-2.32673914690601,8.85220095427747));
#406974=CARTESIAN_POINT('Ctrl Pts',(1.30384626657238,-2.32707896510007,
8.85137579139183));
#406975=CARTESIAN_POINT('Ctrl Pts',(1.30385128920423,-2.32742558187725,
8.85049129520029));
#406976=CARTESIAN_POINT('Origin',(1.31072556753556,-2.32732597051529,7.59394543036555));
#406977=CARTESIAN_POINT('Ctrl Pts',(1.31389778130987,-2.3212007091867,7.59443877723642));
#406978=CARTESIAN_POINT('Ctrl Pts',(1.30898984733472,-2.31812737585883,
7.58783886950016));
#406979=CARTESIAN_POINT('Ctrl Pts',(1.30294132309855,-2.32408510496488,
7.58559994247159));
#406980=CARTESIAN_POINT('Ctrl Pts',(1.34069004888756,-2.33797794565578,
7.56670252222133));
#406981=CARTESIAN_POINT('Ctrl Pts',(1.33578920827041,-2.33490905416709,
7.56004874999026));
#406982=CARTESIAN_POINT('Ctrl Pts',(1.32968985135374,-2.340886863336,7.55786368756704));
#406983=CARTESIAN_POINT('Ctrl Pts',(1.36743228458249,-2.35472385231203,
7.53888913333561));
#406984=CARTESIAN_POINT('Ctrl Pts',(1.36250231802957,-2.35163672225099,
7.53222002137281));
#406985=CARTESIAN_POINT('Ctrl Pts',(1.35638999749712,-2.35765685368048,
7.53005029815327));
#406986=CARTESIAN_POINT('Ctrl Pts',(1.39412327829026,-2.37143767139179,
7.51101258149734));
#406987=CARTESIAN_POINT('Ctrl Pts',(1.38913355158475,-2.36831311970494,
7.5043616886572));
#406988=CARTESIAN_POINT('Ctrl Pts',(1.38304039838404,-2.37439431741734,
7.50217374673251));
#406989=CARTESIAN_POINT('',(1.3816182993051,-2.37350118398174,7.50366116523517));
#406990=CARTESIAN_POINT('Ctrl Pts',(1.38685191115373,-2.36688436340659,
7.51860402984325));
#406991=CARTESIAN_POINT('Ctrl Pts',(1.3872261952276,-2.36711873895528,7.51734760759493));
#406992=CARTESIAN_POINT('Ctrl Pts',(1.38753283777153,-2.36738095682314,
7.51608817408573));
#406993=CARTESIAN_POINT('Ctrl Pts',(1.38776245486761,-2.36768056285119,
7.5148100591312));
#406994=CARTESIAN_POINT('Ctrl Pts',(1.38797044752012,-2.36795195315072,
7.51365231206384));
#406995=CARTESIAN_POINT('Ctrl Pts',(1.38811573123279,-2.36825425143914,
7.51247773061043));
#406996=CARTESIAN_POINT('Ctrl Pts',(1.38816251106135,-2.36859822163467,
7.51129758471022));
#406997=CARTESIAN_POINT('Ctrl Pts',(1.38822065304579,-2.36902573730484,
7.50983079813401));
#406998=CARTESIAN_POINT('Ctrl Pts',(1.38811186827433,-2.36950573745491,
7.50839324291155));
#406999=CARTESIAN_POINT('Ctrl Pts',(1.3877549621655,-2.37002350371511,7.50715379678855));
#407000=CARTESIAN_POINT('Ctrl Pts',(1.38759008182723,-2.37026269680825,
7.50658120839351));
#407001=CARTESIAN_POINT('Ctrl Pts',(1.3873409856815,-2.37053856065068,7.50598221009429));
#407002=CARTESIAN_POINT('Ctrl Pts',(1.38699671946609,-2.37082928581173,
7.50545747549611));
#407003=CARTESIAN_POINT('Ctrl Pts',(1.38681300835751,-2.37098442575645,
7.50517746087247));
#407004=CARTESIAN_POINT('Ctrl Pts',(1.38660033499764,-2.3711456346244,7.50491486231392));
#407005=CARTESIAN_POINT('Ctrl Pts',(1.3863633237229,-2.37130731404933,7.50468370960992));
#407006=CARTESIAN_POINT('Ctrl Pts',(1.3860089171062,-2.37154907578849,7.50433806340446));
#407007=CARTESIAN_POINT('Ctrl Pts',(1.38558915067019,-2.37179867932594,
7.50405484070983));
#407008=CARTESIAN_POINT('Ctrl Pts',(1.3851319287582,-2.37203869856845,7.5038576603613));
#407009=CARTESIAN_POINT('Ctrl Pts',(1.38508303598156,-2.37206436489568,
7.50383657498791));
#407010=CARTESIAN_POINT('Ctrl Pts',(1.385033743229,-2.37208992304648,7.50381643264937));
#407011=CARTESIAN_POINT('Ctrl Pts',(1.38498410518476,-2.37211535306455,
7.50379723213559));
#407012=CARTESIAN_POINT('Ctrl Pts',(1.38465275500168,-2.37228510675388,
7.50366906242519));
#407013=CARTESIAN_POINT('Ctrl Pts',(1.38429848313331,-2.37245220342953,
7.50358235568538));
#407014=CARTESIAN_POINT('Ctrl Pts',(1.3839531370876,-2.37260505571624,7.5035341175365));
#407015=CARTESIAN_POINT('Ctrl Pts',(1.3834353297777,-2.37283424042062,7.50346178989176));
#407016=CARTESIAN_POINT('Ctrl Pts',(1.38286854227575,-2.37305877444104,
7.50346967198527));
#407017=CARTESIAN_POINT('Ctrl Pts',(1.38230535013553,-2.37326207654002,
7.50354272648692));
#407018=CARTESIAN_POINT('Ctrl Pts',(1.38207369755087,-2.37334569890143,
7.50357277531559));
#407019=CARTESIAN_POINT('Ctrl Pts',(1.38184300918211,-2.37342575141274,
7.50361331098761));
#407020=CARTESIAN_POINT('Ctrl Pts',(1.38161829930581,-2.37350118398297,
7.50366116523659));
#407021=CARTESIAN_POINT('',(1.31216235181344,-2.32987712649126,7.57603338622103));
#407022=CARTESIAN_POINT('Origin',(1.31649630659949,-2.33757831636798,7.58486873427628));
#407023=CARTESIAN_POINT('Ctrl Pts',(1.3816182993563,-2.37350118400757,7.50366116529969));
#407024=CARTESIAN_POINT('Ctrl Pts',(1.3585036515569,-2.35898426780922,7.5278357307971));
#407025=CARTESIAN_POINT('Ctrl Pts',(1.33535275265204,-2.34444361706053,
7.55196141284068));
#407026=CARTESIAN_POINT('Ctrl Pts',(1.31216235301863,-2.32987712683062,
7.57603338728831));
#407027=CARTESIAN_POINT('Ctrl Pts',(1.3151526330441,-2.3221939361617,7.59639677331372));
#407028=CARTESIAN_POINT('Ctrl Pts',(1.30074331794073,-2.30960147554746,
7.59974925422225));
#407029=CARTESIAN_POINT('Ctrl Pts',(1.30404198763954,-2.3284513350771,7.59639677331371));
#407030=CARTESIAN_POINT('Ctrl Pts',(1.31266628426861,-2.31918841227221,
7.58707626057423));
#407031=CARTESIAN_POINT('Ctrl Pts',(1.30579990181469,-2.31857995225022,
7.58811717123966));
#407032=CARTESIAN_POINT('Ctrl Pts',(1.30276074036381,-2.32476711066725,
7.58707626057422));
#407033=CARTESIAN_POINT('Ctrl Pts',(1.31201671782416,-2.32523024110921,
7.5801537675693));
#407034=CARTESIAN_POINT('Ctrl Pts',(1.30919143812989,-2.32460196840805,
7.5820876076604));
#407035=CARTESIAN_POINT('Ctrl Pts',(1.30826409698657,-2.32734367779122,
7.58015376756929));
#407036=CARTESIAN_POINT('Ctrl Pts',(1.31216235140752,-2.32987712577008,
7.57603338509286));
#407037=CARTESIAN_POINT('Ctrl Pts',(1.31216235140752,-2.32987712577008,
7.57603338509286));
#407038=CARTESIAN_POINT('Ctrl Pts',(1.31216235140752,-2.32987712577008,
7.57603338509286));
#407039=CARTESIAN_POINT('Origin',(1.31650127865133,-2.3375755161612,7.58486873427622));
#407040=CARTESIAN_POINT('Ctrl Pts',(1.30521500871195,-2.42153721008158,
7.51098857897448));
#407041=CARTESIAN_POINT('Ctrl Pts',(1.30512970780234,-2.41565051018039,
7.50433767179956));
#407042=CARTESIAN_POINT('Ctrl Pts',(1.31348868127021,-2.41359244952874,
7.50214974420965));
#407043=CARTESIAN_POINT('Ctrl Pts',(1.3047585888223,-2.39003922334996,7.53887321589166));
#407044=CARTESIAN_POINT('Ctrl Pts',(1.30467430996897,-2.38422305656059,
7.53220407452061));
#407045=CARTESIAN_POINT('Ctrl Pts',(1.31299098755429,-2.38211692411852,
7.53003438070911));
#407046=CARTESIAN_POINT('Ctrl Pts',(1.30430129243809,-2.35848074886471,
7.56669465659234));
#407047=CARTESIAN_POINT('Ctrl Pts',(1.30421751165708,-2.35269895453973,
7.56004085833299));
#407048=CARTESIAN_POINT('Ctrl Pts',(1.31249126537343,-2.350581963853,7.55785582193789));
#407049=CARTESIAN_POINT('Ctrl Pts',(1.30384314024102,-2.32686321388927,
7.59443891967696));
#407050=CARTESIAN_POINT('Ctrl Pts',(1.30375923798833,-2.32107303668239,
7.58783901202978));
#407051=CARTESIAN_POINT('Ctrl Pts',(1.31198945670399,-2.31898912740396,
7.58560008491213));
#407052=CARTESIAN_POINT('',(1.31346170186506,-2.41188626453886,7.50366116523517));
#407053=CARTESIAN_POINT('Ctrl Pts',(1.31346170186524,-2.41188626453919,
7.50366116523554));
#407054=CARTESIAN_POINT('Ctrl Pts',(1.31288301264091,-2.41237540286155,
7.50350835821027));
#407055=CARTESIAN_POINT('Ctrl Pts',(1.31233514318617,-2.41280621264754,
7.50345484956));
#407056=CARTESIAN_POINT('Ctrl Pts',(1.31180217608123,-2.41319197426492,
7.50349758195598));
#407057=CARTESIAN_POINT('Ctrl Pts',(1.31152872443053,-2.41338989858346,
7.50351950684424));
#407058=CARTESIAN_POINT('Ctrl Pts',(1.31123231915291,-2.41359557726914,
7.50357029184312));
#407059=CARTESIAN_POINT('Ctrl Pts',(1.31094104715448,-2.41378605423314,
7.50365515313923));
#407060=CARTESIAN_POINT('Ctrl Pts',(1.3104929528732,-2.4140790849355,7.50378570417639));
#407061=CARTESIAN_POINT('Ctrl Pts',(1.31004404409646,-2.41434503002182,
7.50400001621911));
#407062=CARTESIAN_POINT('Ctrl Pts',(1.30962733207943,-2.4145616938471,7.50428903009635));
#407063=CARTESIAN_POINT('Ctrl Pts',(1.30958108025154,-2.4145857418648,7.50432110841318));
#407064=CARTESIAN_POINT('Ctrl Pts',(1.30953521085967,-2.41460920955342,
7.50435406373355));
#407065=CARTESIAN_POINT('Ctrl Pts',(1.30948975828797,-2.4146320861886,7.50438785222352));
#407066=CARTESIAN_POINT('Ctrl Pts',(1.30921224849042,-2.41477175904227,
7.50459414719561));
#407067=CARTESIAN_POINT('Ctrl Pts',(1.30894562634667,-2.41489116230397,
7.50483629897752));
#407068=CARTESIAN_POINT('Ctrl Pts',(1.30870064396404,-2.41498692275759,
7.5050991045531));
#407069=CARTESIAN_POINT('Ctrl Pts',(1.30816018822179,-2.41519817993649,
7.50567888004914));
#407070=CARTESIAN_POINT('Ctrl Pts',(1.30770394295143,-2.41530317974192,
7.50637912803145));
#407071=CARTESIAN_POINT('Ctrl Pts',(1.30733073613186,-2.41533280978828,
7.50710440483569));
#407072=CARTESIAN_POINT('Ctrl Pts',(1.30723921841051,-2.41534007566388,
7.50728225710685));
#407073=CARTESIAN_POINT('Ctrl Pts',(1.30715088373331,-2.41534309947923,
7.50746498566954));
#407074=CARTESIAN_POINT('Ctrl Pts',(1.30706780836973,-2.41534222699802,
7.50764697238949));
#407075=CARTESIAN_POINT('Ctrl Pts',(1.30662121807804,-2.41533753677912,
7.50862528291181));
#407076=CARTESIAN_POINT('Ctrl Pts',(1.3062860297497,-2.41522396277347,7.50965856837421));
#407077=CARTESIAN_POINT('Ctrl Pts',(1.30602487717234,-2.41505626958657,
7.51067959873201));
#407078=CARTESIAN_POINT('Ctrl Pts',(1.30588116457962,-2.4149639878143,7.51124147302578));
#407079=CARTESIAN_POINT('Ctrl Pts',(1.30576007199096,-2.41485492899367,
7.51180065547252));
#407080=CARTESIAN_POINT('Ctrl Pts',(1.30565692234312,-2.41473598925369,
7.512351757165));
#407081=CARTESIAN_POINT('Ctrl Pts',(1.3053004992199,-2.41432500507207,7.51425603304536));
#407082=CARTESIAN_POINT('Ctrl Pts',(1.30512039563905,-2.4137430693988,7.51626900505181));
#407083=CARTESIAN_POINT('Ctrl Pts',(1.30509334076503,-2.41304587007462,
7.51827788969244));
#407084=CARTESIAN_POINT('Ctrl Pts',(1.30509187650413,-2.41300813632967,
7.51838661432546));
#407085=CARTESIAN_POINT('Ctrl Pts',(1.30509086684248,-2.41297005723368,
7.51849533314857));
#407086=CARTESIAN_POINT('Ctrl Pts',(1.30509031014836,-2.41293163922358,
7.51860402984325));
#407087=CARTESIAN_POINT('Ctrl Pts',(1.31216235147925,-2.32987712769895,
7.57603338728985));
#407088=CARTESIAN_POINT('Ctrl Pts',(1.31259704935578,-2.35725939040437,
7.55196141284922));
#407089=CARTESIAN_POINT('Ctrl Pts',(1.31303012767148,-2.38459447936898,
7.52783573083105));
#407090=CARTESIAN_POINT('Ctrl Pts',(1.31346170186056,-2.41188626459787,
7.50366116530176));
#407091=CARTESIAN_POINT('Origin',(4.53412748053618E-16,-8.0508024718856E-16,
7.49482233047033));
#407092=CARTESIAN_POINT('Origin',(1.37717168998616,-2.3658622923367,7.49482233047033));
#407093=CARTESIAN_POINT('Origin',(0.,0.,7.50366116523517));
#407094=CARTESIAN_POINT('Origin',(1.30923444818254,-2.40412383410094,7.49482233047033));
#407095=CARTESIAN_POINT('Ctrl Pts',(1.38685101471507,-2.36688380200663,
7.51860402984325));
#407096=CARTESIAN_POINT('Ctrl Pts',(1.39329958728445,-2.37092263820628,
7.51860402984325));
#407097=CARTESIAN_POINT('Ctrl Pts',(1.39984896414485,-2.36704940328304,
7.51860402984325));
#407098=CARTESIAN_POINT('Ctrl Pts',(1.38924541439193,-2.36838344837307,
7.51041458714365));
#407099=CARTESIAN_POINT('Ctrl Pts',(1.39485120463891,-2.37000501596869,
7.51004642900441));
#407100=CARTESIAN_POINT('Ctrl Pts',(1.39985077038522,-2.36704833509084,
7.50729136483009));
#407101=CARTESIAN_POINT('Ctrl Pts',(1.38866594195957,-2.37113807155953,
7.50215815450138));
#407102=CARTESIAN_POINT('Ctrl Pts',(1.39169202834611,-2.37187350725535,
7.49877163671532));
#407103=CARTESIAN_POINT('Ctrl Pts',(1.39467384947403,-2.37013780383728,
7.49481588533172));
#407104=CARTESIAN_POINT('Ctrl Pts',(1.38161802235206,-2.37350070820122,
7.50366171572174));
#407105=CARTESIAN_POINT('Ctrl Pts',(1.38346014519125,-2.37666531650282,
7.50000045605858));
#407106=CARTESIAN_POINT('Ctrl Pts',(1.38346014519135,-2.37666531650275,
7.49482233047317));
#407107=CARTESIAN_POINT('Origin',(1.39348601430782,-2.35629008781358,7.51860402984325));
#407108=CARTESIAN_POINT('Origin',(1.39348601430782,-2.35629008781358,9.));
#407109=CARTESIAN_POINT('Origin',(1.39348601430782,-2.35629008781358,8.75721825406948));
#407110=CARTESIAN_POINT('Ctrl Pts',(1.37269783844897,-2.35802109048348,
8.78942910404912));
#407111=CARTESIAN_POINT('Ctrl Pts',(1.37740998531032,-2.3609956661942,8.79672699501691));
#407112=CARTESIAN_POINT('Ctrl Pts',(1.38347973220101,-2.35445107616387,
8.79893251111267));
#407113=CARTESIAN_POINT('Ctrl Pts',(1.38201599788308,-2.36385609892402,
8.78111911759583));
#407114=CARTESIAN_POINT('Ctrl Pts',(1.38760627609689,-2.36737619830013,
8.78644465894813));
#407115=CARTESIAN_POINT('Ctrl Pts',(1.39426522839043,-2.36275301042509,
8.78817647674131));
#407116=CARTESIAN_POINT('Ctrl Pts',(1.38782329711837,-2.36749261533527,
8.76780923932029));
#407117=CARTESIAN_POINT('Ctrl Pts',(1.39442509977367,-2.37164363189401,
8.76988516158374));
#407118=CARTESIAN_POINT('Ctrl Pts',(1.40100847884786,-2.36792940245014,
8.77093053738833));
#407119=CARTESIAN_POINT('Ctrl Pts',(1.38669095324689,-2.36678354440284,
8.75371302330492));
#407120=CARTESIAN_POINT('Ctrl Pts',(1.39313032119299,-2.37083332733808,
8.75300828287559));
#407121=CARTESIAN_POINT('Ctrl Pts',(1.39969354974844,-2.36691943282451,
8.75267964240738));
#407122=CARTESIAN_POINT('Origin',(1.3816012871853,-2.34884790783658,8.78727029226991));
#407123=CARTESIAN_POINT('Ctrl Pts',(1.31437432427031,-2.32149911893913,
8.85049129520029));
#407124=CARTESIAN_POINT('Ctrl Pts',(1.31932364416771,-2.32459836800564,
8.85711686593484));
#407125=CARTESIAN_POINT('Ctrl Pts',(1.32539494747705,-2.31857839805223,
8.85933012996512));
#407126=CARTESIAN_POINT('Ctrl Pts',(1.33460133053255,-2.33416520874056,
8.82945683644721));
#407127=CARTESIAN_POINT('Ctrl Pts',(1.33959173277752,-2.33729018344815,
8.83607469902389));
#407128=CARTESIAN_POINT('Ctrl Pts',(1.34565445587691,-2.33122590846116,
8.8382956714852));
#407129=CARTESIAN_POINT('Ctrl Pts',(1.35479818681085,-2.34681241871376,
8.80838214965003));
#407130=CARTESIAN_POINT('Ctrl Pts',(1.35980828351311,-2.34994972603058,
8.81501364461993));
#407131=CARTESIAN_POINT('Ctrl Pts',(1.36588287762337,-2.34385480035506,
8.81722098428721));
#407132=CARTESIAN_POINT('Ctrl Pts',(1.3749671840312,-2.35944218342959,8.78727029226991));
#407133=CARTESIAN_POINT('Ctrl Pts',(1.37997811292692,-2.36258001186347,
8.79393457792714));
#407134=CARTESIAN_POINT('Ctrl Pts',(1.38608257609909,-2.35646650676755,
8.79610912703474));
#407135=CARTESIAN_POINT('Origin',(1.32100842742441,-2.31090484334611,8.85049129520029));
#407136=CARTESIAN_POINT('Ctrl Pts',(1.30385128920423,-2.32742558187725,
8.85049129520029));
#407137=CARTESIAN_POINT('Ctrl Pts',(1.3039358989612,-2.33326458465274,8.85711686593484));
#407138=CARTESIAN_POINT('Ctrl Pts',(1.29564064670651,-2.33533570805443,
8.85933012996512));
#407139=CARTESIAN_POINT('Ctrl Pts',(1.30377643617359,-2.32225990040868,
8.86332496987232));
#407140=CARTESIAN_POINT('Ctrl Pts',(1.29989627515225,-2.32476913232805,
8.86648636486736));
#407141=CARTESIAN_POINT('Ctrl Pts',(1.29544837314915,-2.32088425528192,
8.87206031107457));
#407142=CARTESIAN_POINT('Ctrl Pts',(1.30996597848913,-2.31873862621884,
8.86341338519877));
#407143=CARTESIAN_POINT('Ctrl Pts',(1.31412198473723,-2.31668897193089,
8.86654584966059));
#407144=CARTESIAN_POINT('Ctrl Pts',(1.31304352587506,-2.31086135841679,
8.87215952290714));
#407145=CARTESIAN_POINT('Ctrl Pts',(1.31437432427031,-2.32149911893913,
8.85049129520029));
#407146=CARTESIAN_POINT('Ctrl Pts',(1.31932364416771,-2.32459836800564,
8.85711686593484));
#407147=CARTESIAN_POINT('Ctrl Pts',(1.32539494747705,-2.31857839805223,
8.85933012996512));
#407148=CARTESIAN_POINT('Origin',(1.29135260132909,-2.32760669344446,8.85049129520029));
#407149=CARTESIAN_POINT('Ctrl Pts',(1.30488713801677,-2.39891053004235,
8.78727029226991));
#407150=CARTESIAN_POINT('Ctrl Pts',(1.30497280099367,-2.40482221656422,
8.79393457792714));
#407151=CARTESIAN_POINT('Ctrl Pts',(1.29658037301232,-2.40687320845989,
8.79610912703474));
#407152=CARTESIAN_POINT('Ctrl Pts',(1.30454234439086,-2.3751159818641,8.80838214965001));
#407153=CARTESIAN_POINT('Ctrl Pts',(1.30462799314122,-2.38102668659853,
8.81501364461992));
#407154=CARTESIAN_POINT('Ctrl Pts',(1.29626693711645,-2.38306176761555,
8.8172209842872));
#407155=CARTESIAN_POINT('Ctrl Pts',(1.30419707450798,-2.35128856672228,
8.82945683644722));
#407156=CARTESIAN_POINT('Ctrl Pts',(1.3042823865771,-2.35717603675113,8.83607469902389));
#407157=CARTESIAN_POINT('Ctrl Pts',(1.29595369511065,-2.35921685544822,
8.83829567148521));
#407158=CARTESIAN_POINT('Ctrl Pts',(1.30385128920423,-2.32742558187725,
8.85049129520029));
#407159=CARTESIAN_POINT('Ctrl Pts',(1.3039358989612,-2.33326458465274,8.85711686593484));
#407160=CARTESIAN_POINT('Ctrl Pts',(1.29564064670651,-2.33533570805443,
8.85933012996512));
#407161=CARTESIAN_POINT('Origin',(1.29238845014162,-2.39909164160956,8.78727029226991));
#407162=CARTESIAN_POINT('Ctrl Pts',(1.30508760891743,-2.41274649779731,
8.75374538247848));
#407163=CARTESIAN_POINT('Ctrl Pts',(1.3052108309116,-2.42034447086437,8.75304829418602));
#407164=CARTESIAN_POINT('Ctrl Pts',(1.29847137974323,-2.4239292220633,8.75272238421917));
#407165=CARTESIAN_POINT('Ctrl Pts',(1.30510673448899,-2.41406634291195,
8.76769408445019));
#407166=CARTESIAN_POINT('Ctrl Pts',(1.30523236727893,-2.42185552588413,
8.76974318093968));
#407167=CARTESIAN_POINT('Ctrl Pts',(1.2986518165391,-2.42555886346539,8.7707786988043));
#407168=CARTESIAN_POINT('Ctrl Pts',(1.30500870771911,-2.4073015687203,8.78108014887989));
#407169=CARTESIAN_POINT('Ctrl Pts',(1.30511897588475,-2.41390255942111,
8.78639403366326));
#407170=CARTESIAN_POINT('Ctrl Pts',(1.29773252047994,-2.41721350373984,
8.78812224174741));
#407171=CARTESIAN_POINT('Ctrl Pts',(1.30484806344777,-2.39621559715997,
8.78944554828685));
#407172=CARTESIAN_POINT('Ctrl Pts',(1.30494659031671,-2.40177857388768,
8.79673892988685));
#407173=CARTESIAN_POINT('Ctrl Pts',(1.29621337213039,-2.40357703279091,
8.79894799272499));
#407174=CARTESIAN_POINT('Origin',(1.29259162227322,-2.41311275079079,8.75721825406948));
#407175=CARTESIAN_POINT('Origin',(1.29259162227322,-2.41311275079079,9.));
#407176=CARTESIAN_POINT('Origin',(1.29259162227322,-2.41311275079079,7.51860402984325));
#407177=CARTESIAN_POINT('Ctrl Pts',(1.31346132563586,-2.41188557367602,
7.50366195182966));
#407178=CARTESIAN_POINT('Ctrl Pts',(1.31521268767183,-2.41510156850329,
7.50000065167735));
#407179=CARTESIAN_POINT('Ctrl Pts',(1.31521268767173,-2.41510156850335,
7.49482233047108));
#407180=CARTESIAN_POINT('Ctrl Pts',(1.30778170985432,-2.41669137893432,
7.50215800491337));
#407181=CARTESIAN_POINT('Ctrl Pts',(1.30684029925188,-2.41966096531158,
7.49877273257265));
#407182=CARTESIAN_POINT('Ctrl Pts',(1.30380859101921,-2.42131199576008,
7.49481816995649));
#407183=CARTESIAN_POINT('Ctrl Pts',(1.30513148750345,-2.41574992376647,
7.51043025814043));
#407184=CARTESIAN_POINT('Ctrl Pts',(1.30361489455136,-2.42138842558917,
7.51006209594515));
#407185=CARTESIAN_POINT('Ctrl Pts',(1.29849163527805,-2.42413272597012,
7.50731281821699));
#407186=CARTESIAN_POINT('Ctrl Pts',(1.30509028815832,-2.41293012797612,
7.51860402984326));
#407187=CARTESIAN_POINT('Ctrl Pts',(1.30520145828909,-2.42053858764892,
7.51860402984326));
#407188=CARTESIAN_POINT('Ctrl Pts',(1.29849386712378,-2.42413153047477,
7.51860402984327));
#407189=CARTESIAN_POINT('Origin',(0.,0.,7.5));
#407190=CARTESIAN_POINT('Origin',(1.45029105591256,-2.23910559748222,7.5));
#407191=CARTESIAN_POINT('',(1.45029105591256,-2.23910559748222,7.59394543036555));
#407192=CARTESIAN_POINT('',(1.45029105591256,-2.23910559748222,8.85049129520029));
#407193=CARTESIAN_POINT('',(1.45029105591256,-2.23910559748222,7.5));
#407194=CARTESIAN_POINT('',(1.45590483281687,-2.3103773050933,8.78727029226991));
#407195=CARTESIAN_POINT('Ctrl Pts',(1.45029105591256,-2.23910559748222,
8.85049129520029));
#407196=CARTESIAN_POINT('Ctrl Pts',(1.45216503493679,-2.26289736679568,
8.82945686509571));
#407197=CARTESIAN_POINT('Ctrl Pts',(1.45403622806461,-2.2866537667672,8.80838212259896));
#407198=CARTESIAN_POINT('Ctrl Pts',(1.45590483281687,-2.3103773050933,8.78727029226991));
#407199=CARTESIAN_POINT('',(1.45700592305914,-2.32435658911879,8.75721825406948));
#407200=CARTESIAN_POINT('Origin',(1.45369256172862,-2.28228805819315,8.75937679713143));
#407201=CARTESIAN_POINT('',(1.45700592305914,-2.32435658911879,7.51860402984325));
#407202=CARTESIAN_POINT('',(1.45700592305914,-2.32435658911879,7.5));
#407203=CARTESIAN_POINT('Ctrl Pts',(1.45700592305915,-2.32435658911879,
7.51860402984325));
#407204=CARTESIAN_POINT('Ctrl Pts',(1.45614118792576,-2.31337803570668,
7.52834476460825));
#407205=CARTESIAN_POINT('Ctrl Pts',(1.45527589141882,-2.30239235517612,
7.53807742314407));
#407206=CARTESIAN_POINT('Ctrl Pts',(1.45441001468943,-2.29139930822462,
7.54780169004674));
#407207=CARTESIAN_POINT('Ctrl Pts',(1.45303851274672,-2.27398691597693,
7.5632044032688));
#407208=CARTESIAN_POINT('Ctrl Pts',(1.45166555335683,-2.25655602018872,
7.57858609112103));
#407209=CARTESIAN_POINT('Ctrl Pts',(1.45029105591256,-2.23910559748222,
7.59394543036555));
#407210=CARTESIAN_POINT('Origin',(1.70235901374314,-2.36323439034367,7.5));
#407211=CARTESIAN_POINT('',(1.53564927699523,-2.27316543860613,8.75721825406948));
#407212=CARTESIAN_POINT('',(1.52331214621094,-2.26650000646721,8.78727029226991));
#407213=CARTESIAN_POINT('Origin',(1.49199590675922,-2.24958065361595,8.75658640621018));
#407214=CARTESIAN_POINT('',(1.46041276049035,-2.23251709792627,8.85049129520029));
#407215=CARTESIAN_POINT('Ctrl Pts',(1.52331214621094,-2.26650000646721,
8.78727029226991));
#407216=CARTESIAN_POINT('Ctrl Pts',(1.50237542338155,-2.25518843753999,
8.80838212259896));
#407217=CARTESIAN_POINT('Ctrl Pts',(1.48140969918009,-2.2438611999228,8.82945686509571));
#407218=CARTESIAN_POINT('Ctrl Pts',(1.46041276049035,-2.23251709792627,
8.85049129520029));
#407219=CARTESIAN_POINT('',(1.46041276049035,-2.23251709792627,7.59394543036555));
#407220=CARTESIAN_POINT('',(1.46041276049035,-2.23251709792627,7.5));
#407221=CARTESIAN_POINT('',(1.53564927699523,-2.27316543860613,7.51860402984325));
#407222=CARTESIAN_POINT('Ctrl Pts',(1.46041276049035,-2.23251709792627,
7.59394543036555));
#407223=CARTESIAN_POINT('Ctrl Pts',(1.47581327361953,-2.24083759618164,
7.57858609112103));
#407224=CARTESIAN_POINT('Ctrl Pts',(1.49119655366674,-2.24914878384932,
7.56320440326857));
#407225=CARTESIAN_POINT('Ctrl Pts',(1.50656350379346,-2.257451148884,7.54780169004651));
#407226=CARTESIAN_POINT('Ctrl Pts',(1.51626519221407,-2.26269271979146,
7.53807742314383));
#407227=CARTESIAN_POINT('Ctrl Pts',(1.52596037955095,-2.2679307783318,7.52834476460825));
#407228=CARTESIAN_POINT('Ctrl Pts',(1.53564927699523,-2.27316543860613,
7.51860402984325));
#407229=CARTESIAN_POINT('',(1.53564927699523,-2.27316543860613,7.5));
#407230=CARTESIAN_POINT('Origin',(1.45714482817992,-2.23856575425759,7.5));
#407231=CARTESIAN_POINT('Ctrl Pts',(1.46041276049035,-2.23251709792627,
8.85049129520029));
#407232=CARTESIAN_POINT('Ctrl Pts',(1.46024237621488,-2.23242504371646,
8.85097269580138));
#407233=CARTESIAN_POINT('Ctrl Pts',(1.4600701434085,-2.23234155133989,8.85143669361005));
#407234=CARTESIAN_POINT('Ctrl Pts',(1.4598877499329,-2.23226356296287,8.8519052845931));
#407235=CARTESIAN_POINT('Ctrl Pts',(1.45953099986161,-2.23211102264326,
8.85282181883899));
#407236=CARTESIAN_POINT('Ctrl Pts',(1.45914447807312,-2.23198364392551,
8.85372622499635));
#407237=CARTESIAN_POINT('Ctrl Pts',(1.45871729341944,-2.23189407204951,
8.85462257735071));
#407238=CARTESIAN_POINT('Ctrl Pts',(1.45836265989212,-2.23181971265935,
8.85536669723986));
#407239=CARTESIAN_POINT('Ctrl Pts',(1.45797992823564,-2.23177136083869,
8.85610498449051));
#407240=CARTESIAN_POINT('Ctrl Pts',(1.45756183174184,-2.231764186704,8.85681338218371));
#407241=CARTESIAN_POINT('Ctrl Pts',(1.45718240851709,-2.23175767616551,
8.85745625420284));
#407242=CARTESIAN_POINT('Ctrl Pts',(1.45676911105288,-2.23178439781428,
8.85808743050665));
#407243=CARTESIAN_POINT('Ctrl Pts',(1.45631128381985,-2.23187089041146,
8.85866804508409));
#407244=CARTESIAN_POINT('Ctrl Pts',(1.45610005225901,-2.23191079622087,
8.85893592806395));
#407245=CARTESIAN_POINT('Ctrl Pts',(1.45587927882592,-2.23196365955263,
8.85919241173848));
#407246=CARTESIAN_POINT('Ctrl Pts',(1.45564772260899,-2.23203367112445,
8.85943017985534));
#407247=CARTESIAN_POINT('Ctrl Pts',(1.45533505316815,-2.23212820747205,
8.8597512372));
#407248=CARTESIAN_POINT('Ctrl Pts',(1.45499495061646,-2.23225702953023,
8.86004599534706));
#407249=CARTESIAN_POINT('Ctrl Pts',(1.45463519034913,-2.23242832936725,
8.86026130871721));
#407250=CARTESIAN_POINT('Ctrl Pts',(1.45450347197255,-2.23249104706703,
8.86034014101236));
#407251=CARTESIAN_POINT('Ctrl Pts',(1.45436713462985,-2.23256038986719,
8.86040910639693));
#407252=CARTESIAN_POINT('Ctrl Pts',(1.45423004525065,-2.2326347683884,8.86046313645507));
#407253=CARTESIAN_POINT('Ctrl Pts',(1.45401611842253,-2.23275083544783,
8.8605474499083));
#407254=CARTESIAN_POINT('Ctrl Pts',(1.45379459084792,-2.23288246268805,
8.86059655985668));
#407255=CARTESIAN_POINT('Ctrl Pts',(1.45357952011843,-2.23302095660014,
8.86059725258816));
#407256=CARTESIAN_POINT('Ctrl Pts',(1.45336395248964,-2.23315977048849,
8.86059794692011));
#407257=CARTESIAN_POINT('Ctrl Pts',(1.45315391929665,-2.23330925598724,
8.86056369958366));
#407258=CARTESIAN_POINT('Ctrl Pts',(1.45295869380045,-2.23345819421406,
8.86048590497774));
#407259=CARTESIAN_POINT('Ctrl Pts',(1.4529077457585,-2.23349706265684,8.86046560290182));
#407260=CARTESIAN_POINT('Ctrl Pts',(1.45285719833683,-2.23353647149834,
8.86044257503091));
#407261=CARTESIAN_POINT('Ctrl Pts',(1.45280859330924,-2.23357517708473,
8.86041778462583));
#407262=CARTESIAN_POINT('Ctrl Pts',(1.45248154178738,-2.23383561765152,
8.86025097596201));
#407263=CARTESIAN_POINT('Ctrl Pts',(1.45219875525293,-2.23409942479347,
8.8599848982295));
#407264=CARTESIAN_POINT('Ctrl Pts',(1.45196270805475,-2.23435270342849,
8.85968173251461));
#407265=CARTESIAN_POINT('Ctrl Pts',(1.4518378526108,-2.23448667331529,8.85952137522076));
#407266=CARTESIAN_POINT('Ctrl Pts',(1.45172352753973,-2.23462014970572,
8.85934740853961));
#407267=CARTESIAN_POINT('Ctrl Pts',(1.45162016440982,-2.23475023902306,
8.8591675900182));
#407268=CARTESIAN_POINT('Ctrl Pts',(1.45120510771616,-2.23527261525127,
8.85844552518697));
#407269=CARTESIAN_POINT('Ctrl Pts',(1.45094097857854,-2.23576801806967,
8.85759444184129));
#407270=CARTESIAN_POINT('Ctrl Pts',(1.45076190271771,-2.23619128641431,
8.85683498915145));
#407271=CARTESIAN_POINT('Ctrl Pts',(1.45074316290579,-2.23623558031934,
8.85675551445002));
#407272=CARTESIAN_POINT('Ctrl Pts',(1.45072537407568,-2.23627908830462,
8.85667699793653));
#407273=CARTESIAN_POINT('Ctrl Pts',(1.450708473719,-2.2363217605987,8.85659965593547));
#407274=CARTESIAN_POINT('Ctrl Pts',(1.4504803518422,-2.23689775340152,8.85555568965886));
#407275=CARTESIAN_POINT('Ctrl Pts',(1.45034429734326,-2.23748426348365,
8.85434650606346));
#407276=CARTESIAN_POINT('Ctrl Pts',(1.45029358366058,-2.23808278585889,
8.85297329937117));
#407277=CARTESIAN_POINT('Ctrl Pts',(1.4502650603041,-2.23841941822646,8.85220095427747));
#407278=CARTESIAN_POINT('Ctrl Pts',(1.45026383578709,-2.23876001466751,
8.85137579139183));
#407279=CARTESIAN_POINT('Ctrl Pts',(1.45029105591256,-2.23910559748222,
8.85049129520029));
#407280=CARTESIAN_POINT('Origin',(1.45714482817992,-2.23856575425759,7.59394543036555));
#407281=CARTESIAN_POINT('Ctrl Pts',(1.45991807746006,-2.23224983350099,
7.59443877723642));
#407282=CARTESIAN_POINT('Ctrl Pts',(1.45482331821924,-2.22949726707549,
7.58783886950016));
#407283=CARTESIAN_POINT('Ctrl Pts',(1.44916893433922,-2.2358302856665,7.58559994247159));
#407284=CARTESIAN_POINT('Ctrl Pts',(1.48773021868178,-2.2472760128609,7.56670252222132));
#407285=CARTESIAN_POINT('Ctrl Pts',(1.48264282281451,-2.24452742467538,
7.56004874999026));
#407286=CARTESIAN_POINT('Ctrl Pts',(1.47693899722923,-2.2508837389336,7.55786368756704));
#407287=CARTESIAN_POINT('Ctrl Pts',(1.51549042350862,-2.26227413233219,
7.53888913333561));
#407288=CARTESIAN_POINT('Ctrl Pts',(1.51037279299857,-2.25950920915251,
7.53222002137279));
#407289=CARTESIAN_POINT('Ctrl Pts',(1.50465874202924,-2.26590858929742,
7.53005029815326));
#407290=CARTESIAN_POINT('Ctrl Pts',(1.54319743577238,-2.27724351323973,
7.51101258149734));
#407291=CARTESIAN_POINT('Ctrl Pts',(1.53801777028162,-2.2744450741671,7.5043616886572));
#407292=CARTESIAN_POINT('Ctrl Pts',(1.53232675979283,-2.28090416707254,
7.50217374673251));
#407293=CARTESIAN_POINT('',(1.53085035931327,-2.28010398287619,7.50366116523517));
#407294=CARTESIAN_POINT('Ctrl Pts',(1.53564927699523,-2.27316543860613,
7.51860402984325));
#407295=CARTESIAN_POINT('Ctrl Pts',(1.5360378085553,-2.27337535214216,7.51734760759494));
#407296=CARTESIAN_POINT('Ctrl Pts',(1.53636062142571,-2.27361738460005,
7.51608817408573));
#407297=CARTESIAN_POINT('Ctrl Pts',(1.53660896257297,-2.27390166343753,
7.5148100591312));
#407298=CARTESIAN_POINT('Ctrl Pts',(1.53683391591845,-2.27415917000158,
7.51365231206384));
#407299=CARTESIAN_POINT('Ctrl Pts',(1.53699826944799,-2.27445153882632,
7.51247773061043));
#407300=CARTESIAN_POINT('Ctrl Pts',(1.53706699140847,-2.27479180510429,
7.51129758471022));
#407301=CARTESIAN_POINT('Ctrl Pts',(1.537152404957,-2.27521471722792,7.50983079813402));
#407302=CARTESIAN_POINT('Ctrl Pts',(1.53707459741073,-2.27570070103044,
7.50839324291155));
#407303=CARTESIAN_POINT('Ctrl Pts',(1.53675159800197,-2.27624027053724,
7.50715379678855));
#407304=CARTESIAN_POINT('Ctrl Pts',(1.53660238158212,-2.27648953610206,
7.50658120839351));
#407305=CARTESIAN_POINT('Ctrl Pts',(1.53637147188821,-2.27678079279749,
7.50598221009429));
#407306=CARTESIAN_POINT('Ctrl Pts',(1.53604653982969,-2.27709297784467,
7.50545747549611));
#407307=CARTESIAN_POINT('Ctrl Pts',(1.53587314602567,-2.27725956944888,
7.50517746087247));
#407308=CARTESIAN_POINT('Ctrl Pts',(1.53567123831366,-2.27743407312486,
7.50491486231392));
#407309=CARTESIAN_POINT('Ctrl Pts',(1.53544507284033,-2.27761060572659,
7.50468370960992));
#407310=CARTESIAN_POINT('Ctrl Pts',(1.53510688411784,-2.27787457765022,
7.50433806340446));
#407311=CARTESIAN_POINT('Ctrl Pts',(1.53470397229055,-2.27815056287832,
7.50405484070983));
#407312=CARTESIAN_POINT('Ctrl Pts',(1.53426306787569,-2.27841938328404,
7.5038576603613));
#407313=CARTESIAN_POINT('Ctrl Pts',(1.53421592000173,-2.27844812944801,
7.50383657498791));
#407314=CARTESIAN_POINT('Ctrl Pts',(1.53416836604276,-2.27847679328435,
7.50381643264937));
#407315=CARTESIAN_POINT('Ctrl Pts',(1.53412045929205,-2.27850535137413,
7.50379723213559));
#407316=CARTESIAN_POINT('Ctrl Pts',(1.53380066605968,-2.27869598596542,
7.50366906242519));
#407317=CARTESIAN_POINT('Ctrl Pts',(1.53345782800162,-2.27888543759957,
7.50358235568538));
#407318=CARTESIAN_POINT('Ctrl Pts',(1.53312298478604,-2.27906010223198,
7.5035341175365));
#407319=CARTESIAN_POINT('Ctrl Pts',(1.53262092528121,-2.27932199208006,
7.50346178989176));
#407320=CARTESIAN_POINT('Ctrl Pts',(1.53206968824905,-2.27958237897118,
7.50346967198527));
#407321=CARTESIAN_POINT('Ctrl Pts',(1.53152067885769,-2.27982134720851,
7.50354272648692));
#407322=CARTESIAN_POINT('Ctrl Pts',(1.5312948599312,-2.27991963979087,7.50357277531559));
#407323=CARTESIAN_POINT('Ctrl Pts',(1.53106977451844,-2.28001430808024,
7.50361331098761));
#407324=CARTESIAN_POINT('Ctrl Pts',(1.53085035931406,-2.28010398287737,
7.50366116523658));
#407325=CARTESIAN_POINT('',(1.458742113555,-2.24101961352525,7.57603338622103));
#407326=CARTESIAN_POINT('Origin',(1.46356058069564,-2.24842730304492,7.58486873427628));
#407327=CARTESIAN_POINT('Ctrl Pts',(1.53085035936602,-2.28010398289869,
7.50366116529969));
#407328=CARTESIAN_POINT('Ctrl Pts',(1.50685310107529,-2.26709785383089,
7.52783573079709));
#407329=CARTESIAN_POINT('Ctrl Pts',(1.48281814548303,-2.25407036159423,
7.55196141284068));
#407330=CARTESIAN_POINT('Ctrl Pts',(1.45874211477945,-2.2410196137867,7.57603338728831));
#407331=CARTESIAN_POINT('Ctrl Pts',(1.4612339872377,-2.23316062115808,7.5963967733137));
#407332=CARTESIAN_POINT('Ctrl Pts',(1.44672891934441,-2.2220396984816,7.59959882295473));
#407333=CARTESIAN_POINT('Ctrl Pts',(1.45050708407105,-2.23994037679046,
7.59642833564546));
#407334=CARTESIAN_POINT('Ctrl Pts',(1.45856018235572,-2.23032057335266,
7.58707626057419));
#407335=CARTESIAN_POINT('Ctrl Pts',(1.4517863168465,-2.23015614373247,7.58809943920599));
#407336=CARTESIAN_POINT('Ctrl Pts',(1.44910071340169,-2.23636113647472,
7.58710240504253));
#407337=CARTESIAN_POINT('Ctrl Pts',(1.45829905181767,-2.23639160646937,
7.58015376756929));
#407338=CARTESIAN_POINT('Ctrl Pts',(1.45548191389407,-2.23595228276659,
7.58205880659762));
#407339=CARTESIAN_POINT('Ctrl Pts',(1.45471184049851,-2.23866043010443,
7.58020924244126));
#407340=CARTESIAN_POINT('Ctrl Pts',(1.4587421131037,-2.24101961283156,7.57603338509286));
#407341=CARTESIAN_POINT('Ctrl Pts',(1.4587421131037,-2.24101961283156,7.57603338509286));
#407342=CARTESIAN_POINT('Ctrl Pts',(1.4587421131037,-2.24101961283156,7.57603338509286));
#407343=CARTESIAN_POINT('Origin',(1.46356536312188,-2.24842419003088,7.58486873427622));
#407344=CARTESIAN_POINT('Ctrl Pts',(1.45768172623409,-2.33293648944411,
7.51098857897448));
#407345=CARTESIAN_POINT('Ctrl Pts',(1.45721943842671,-2.32706734964726,
7.50433767179956));
#407346=CARTESIAN_POINT('Ctrl Pts',(1.46542937708842,-2.32447795623305,
7.50214974420965));
#407347=CARTESIAN_POINT('Ctrl Pts',(1.45520816116921,-2.30153246162714,
7.5388732158917));
#407348=CARTESIAN_POINT('Ctrl Pts',(1.45475141239017,-2.29573364454088,
7.53220407452063));
#407349=CARTESIAN_POINT('Ctrl Pts',(1.46291606210059,-2.29309898801137,
7.53003438070911));
#407350=CARTESIAN_POINT('Ctrl Pts',(1.45272984594694,-2.27006812649224,
7.56669465659231));
#407351=CARTESIAN_POINT('Ctrl Pts',(1.45227579646826,-2.26430357933689,
7.56004085833298));
#407352=CARTESIAN_POINT('Ctrl Pts',(1.46039691481123,-2.2616608370139,7.55785582193789));
#407353=CARTESIAN_POINT('Ctrl Pts',(1.45024689265157,-2.23854490704545,
7.59443891967696));
#407354=CARTESIAN_POINT('Ctrl Pts',(1.44979218485769,-2.23277200201442,
7.58783901202978));
#407355=CARTESIAN_POINT('Ctrl Pts',(1.45787197718042,-2.23016506242751,
7.58560008491213));
#407356=CARTESIAN_POINT('',(1.46529313746772,-2.32277700535964,7.50366116523517));
#407357=CARTESIAN_POINT('Ctrl Pts',(1.46529313746792,-2.32277700535995,
7.50366116523554));
#407358=CARTESIAN_POINT('Ctrl Pts',(1.46474697642258,-2.32330221544108,
7.50350835821027));
#407359=CARTESIAN_POINT('Ctrl Pts',(1.46422783470215,-2.32376724219865,
7.50345484955999));
#407360=CARTESIAN_POINT('Ctrl Pts',(1.46372067846698,-2.32418635854706,
7.50349758195598));
#407361=CARTESIAN_POINT('Ctrl Pts',(1.46346046970665,-2.32440139631627,
7.50351950684424));
#407362=CARTESIAN_POINT('Ctrl Pts',(1.4631778513041,-2.32462564316438,7.50357029184312));
#407363=CARTESIAN_POINT('Ctrl Pts',(1.46289938165621,-2.32483439063404,
7.50365515313924));
#407364=CARTESIAN_POINT('Ctrl Pts',(1.46247098257425,-2.32515552877257,
7.50378570417639));
#407365=CARTESIAN_POINT('Ctrl Pts',(1.46204003528892,-2.32544968913026,
7.50400001621911));
#407366=CARTESIAN_POINT('Ctrl Pts',(1.46163806115038,-2.32569260662708,
7.50428903009635));
#407367=CARTESIAN_POINT('Ctrl Pts',(1.4615934451136,-2.32571956860033,7.50432110841318));
#407368=CARTESIAN_POINT('Ctrl Pts',(1.4615491735453,-2.32574592693409,7.50435406373354));
#407369=CARTESIAN_POINT('Ctrl Pts',(1.46150528007182,-2.32577166872304,
7.50438785222352));
#407370=CARTESIAN_POINT('Ctrl Pts',(1.46123728931837,-2.32592883471764,
7.50459414719561));
#407371=CARTESIAN_POINT('Ctrl Pts',(1.46097886517166,-2.32606507519193,
7.50483629897752));
#407372=CARTESIAN_POINT('Ctrl Pts',(1.46074052152493,-2.32617633497057,
7.5050991045531));
#407373=CARTESIAN_POINT('Ctrl Pts',(1.4602147115009,-2.32642178521724,7.50567888004914));
#407374=CARTESIAN_POINT('Ctrl Pts',(1.45976613099601,-2.32655580102415,
7.50637912803145));
#407375=CARTESIAN_POINT('Ctrl Pts',(1.45939558937346,-2.32660928163542,
7.50710440483569));
#407376=CARTESIAN_POINT('Ctrl Pts',(1.45930472521133,-2.32662239614304,
7.50728225710685));
#407377=CARTESIAN_POINT('Ctrl Pts',(1.45921676576372,-2.32663107336784,
7.50746498566954));
#407378=CARTESIAN_POINT('Ctrl Pts',(1.45913380518732,-2.32663552533605,
7.50764697238949));
#407379=CARTESIAN_POINT('Ctrl Pts',(1.45868783195992,-2.32665945789195,
7.50862528291182));
#407380=CARTESIAN_POINT('Ctrl Pts',(1.45834605560042,-2.3265675928262,7.50965856837423));
#407381=CARTESIAN_POINT('Ctrl Pts',(1.45807469544967,-2.32641697628601,
7.51067959873204));
#407382=CARTESIAN_POINT('Ctrl Pts',(1.45792536561644,-2.32633409181397,
7.5112414730258));
#407383=CARTESIAN_POINT('Ctrl Pts',(1.45779753440286,-2.32623301549518,
7.51180065547253));
#407384=CARTESIAN_POINT('Ctrl Pts',(1.45768697619173,-2.32612092895028,
7.51235175716501));
#407385=CARTESIAN_POINT('Ctrl Pts',(1.45730495353112,-2.32573362528765,
7.51425603304537));
#407386=CARTESIAN_POINT('Ctrl Pts',(1.45708793524579,-2.32516442453967,
7.51626900505183));
#407387=CARTESIAN_POINT('Ctrl Pts',(1.45701626624484,-2.32447039109801,
7.51827788969247));
#407388=CARTESIAN_POINT('Ctrl Pts',(1.45701238738308,-2.32443282869661,
7.51838661432547));
#407389=CARTESIAN_POINT('Ctrl Pts',(1.45700894005983,-2.32439489252745,
7.51849533314857));
#407390=CARTESIAN_POINT('Ctrl Pts',(1.45700592305914,-2.32435658911879,
7.51860402984325));
#407391=CARTESIAN_POINT('Ctrl Pts',(1.45874211329887,-2.24101961475187,
7.57603338728985));
#407392=CARTESIAN_POINT('Ctrl Pts',(1.46093030563709,-2.26831776647325,
7.55196141284922));
#407393=CARTESIAN_POINT('Ctrl Pts',(1.46311385931012,-2.29556894514294,
7.52783573083104));
#407394=CARTESIAN_POINT('Ctrl Pts',(1.46529313746701,-2.32277700541881,
7.50366116530176));
#407395=CARTESIAN_POINT('Origin',(5.04062831473875E-16,-7.74375868966271E-16,
7.49482233047033));
#407396=CARTESIAN_POINT('Origin',(1.52592346056197,-2.27276568139054,7.49482233047033));
#407397=CARTESIAN_POINT('Origin',(0.,0.,7.50366116523517));
#407398=CARTESIAN_POINT('Origin',(1.46057722850551,-2.31530136474092,7.49482233047033));
#407399=CARTESIAN_POINT('Ctrl Pts',(1.53564834642939,-2.27316493579465,
7.51860402984325));
#407400=CARTESIAN_POINT('Ctrl Pts',(1.54234243883859,-2.27678231230908,
7.51860402984325));
#407401=CARTESIAN_POINT('Ctrl Pts',(1.54863020028824,-2.27249741534621,
7.51860402984325));
#407402=CARTESIAN_POINT('Ctrl Pts',(1.53813390922792,-2.27450809126278,
7.51041458714365));
#407403=CARTESIAN_POINT('Ctrl Pts',(1.54383207597018,-2.27576716295959,
7.51004642900442));
#407404=CARTESIAN_POINT('Ctrl Pts',(1.5486319343782,-2.2724962336225,7.5072913648301));
#407405=CARTESIAN_POINT('Ctrl Pts',(1.53773211669732,-2.27729418170668,
7.50215815450138));
#407406=CARTESIAN_POINT('Ctrl Pts',(1.54079910519163,-2.27783422435049,
7.4987716367153));
#407407=CARTESIAN_POINT('Ctrl Pts',(1.54366359294844,-2.27591104118567,
7.4948158853317));
#407408=CARTESIAN_POINT('Ctrl Pts',(1.5308500524459,-2.28010352581766,7.50366171572173));
#407409=CARTESIAN_POINT('Ctrl Pts',(1.53289114759618,-2.28314360687655,
7.50000045605858));
#407410=CARTESIAN_POINT('Ctrl Pts',(1.53289114759628,-2.28314360687648,
7.49482233047317));
#407411=CARTESIAN_POINT('Origin',(1.54159097210511,-2.26216788164009,7.51860402984325));
#407412=CARTESIAN_POINT('Origin',(1.54159097210511,-2.26216788164009,9.));
#407413=CARTESIAN_POINT('Origin',(1.54159097210511,-2.26216788164009,8.75721825406948));
#407414=CARTESIAN_POINT('Ctrl Pts',(1.52095641350494,-2.26522723077964,
8.78942910404912));
#407415=CARTESIAN_POINT('Ctrl Pts',(1.52584946047531,-2.26789378661955,
8.79672699501691));
#407416=CARTESIAN_POINT('Ctrl Pts',(1.53148742309712,-2.26097375313283,
8.79893251111267));
#407417=CARTESIAN_POINT('Ctrl Pts',(1.53062927805548,-2.27045323404477,
8.78111911759583));
#407418=CARTESIAN_POINT('Ctrl Pts',(1.53643360398454,-2.27360793064426,
8.78644465894813));
#407419=CARTESIAN_POINT('Ctrl Pts',(1.54278266608224,-2.26856760106627,
8.78817647674131));
#407420=CARTESIAN_POINT('Ctrl Pts',(1.53665763797811,-2.27371020390355,
8.76780923932029));
#407421=CARTESIAN_POINT('Ctrl Pts',(1.54351183306588,-2.27742971280518,
8.76988516158374));
#407422=CARTESIAN_POINT('Ctrl Pts',(1.54984371438416,-2.27330131609855,
8.77093053738832));
#407423=CARTESIAN_POINT('Ctrl Pts',(1.53548219029793,-2.27307513935433,
8.75371302330492));
#407424=CARTESIAN_POINT('Ctrl Pts',(1.54216779835549,-2.27670402985534,
8.75300828287558));
#407425=CARTESIAN_POINT('Ctrl Pts',(1.54846677797151,-2.2723776693605,8.75267964240737));
#407426=CARTESIAN_POINT('Origin',(1.52925384132083,-2.25550244950118,8.78727029226991));
#407427=CARTESIAN_POINT('Ctrl Pts',(1.46041276049035,-2.23251709792627,
8.85049129520029));
#407428=CARTESIAN_POINT('Ctrl Pts',(1.46555048104868,-2.2352928752386,8.85711686593484));
#407429=CARTESIAN_POINT('Ctrl Pts',(1.47122360941503,-2.2288962842205,8.85933012996512));
#407430=CARTESIAN_POINT('Ctrl Pts',(1.48140972735875,-2.243861215147,8.82945683644721));
#407431=CARTESIAN_POINT('Ctrl Pts',(1.48659009410405,-2.24666003308928,
8.83607469902388));
#407432=CARTESIAN_POINT('Ctrl Pts',(1.49225182125615,-2.24021977780299,
8.8382956714852));
#407433=CARTESIAN_POINT('Ctrl Pts',(1.50237539655486,-2.25518842304623,
8.80838214965002));
#407434=CARTESIAN_POINT('Ctrl Pts',(1.50757620744598,-2.25799828643083,
8.81501364461988));
#407435=CARTESIAN_POINT('Ctrl Pts',(1.51324781742242,-2.25152668285287,
8.81722098428721));
#407436=CARTESIAN_POINT('Ctrl Pts',(1.52331214621094,-2.26650000646721,
8.78727029226991));
#407437=CARTESIAN_POINT('Ctrl Pts',(1.52851382097385,-2.26931033657938,
8.79393457792714));
#407438=CARTESIAN_POINT('Ctrl Pts',(1.53421404825539,-2.26281827803705,
8.79610912703474));
#407439=CARTESIAN_POINT('Origin',(1.46635445560024,-2.22151954096023,8.85049129520029));
#407440=CARTESIAN_POINT('Ctrl Pts',(1.45029105591256,-2.23910559748222,
8.85049129520029));
#407441=CARTESIAN_POINT('Ctrl Pts',(1.45074959802201,-2.24492718243453,
8.85711686593484));
#407442=CARTESIAN_POINT('Ctrl Pts',(1.44260408658469,-2.24752552912782,
8.85933012996512));
#407443=CARTESIAN_POINT('Ctrl Pts',(1.44988539032746,-2.23395532531037,
8.86332496987232));
#407444=CARTESIAN_POINT('Ctrl Pts',(1.44617396855413,-2.23670800451386,
8.86648636486737));
#407445=CARTESIAN_POINT('Ctrl Pts',(1.44148630031579,-2.23311608742407,
8.87206031107458));
#407446=CARTESIAN_POINT('Ctrl Pts',(1.45583660675253,-2.23004472061829,
8.86341338519876));
#407447=CARTESIAN_POINT('Ctrl Pts',(1.45985275223894,-2.22773300133033,
8.86654584966057));
#407448=CARTESIAN_POINT('Ctrl Pts',(1.45840313270637,-2.22198645836975,
8.87215952290713));
#407449=CARTESIAN_POINT('Ctrl Pts',(1.46041276049035,-2.23251709792627,
8.85049129520029));
#407450=CARTESIAN_POINT('Ctrl Pts',(1.46555048104868,-2.2352928752386,8.85711686593484));
#407451=CARTESIAN_POINT('Ctrl Pts',(1.47122360941503,-2.2288962842205,8.85933012996512));
#407452=CARTESIAN_POINT('Origin',(1.43782965179009,-2.24008713061792,8.85049129520029));
#407453=CARTESIAN_POINT('Ctrl Pts',(1.45590483281687,-2.3103773050933,8.78727029226991));
#407454=CARTESIAN_POINT('Ctrl Pts',(1.45636908284591,-2.3162713569754,8.79393457792714));
#407455=CARTESIAN_POINT('Ctrl Pts',(1.44812530550987,-2.31885583959519,
8.79610912703474));
#407456=CARTESIAN_POINT('Ctrl Pts',(1.45403622567033,-2.2866537363697,8.80838214965002));
#407457=CARTESIAN_POINT('Ctrl Pts',(1.45450039859872,-2.29254680939304,
8.81501364461991));
#407458=CARTESIAN_POINT('Ctrl Pts',(1.44628690934872,-2.29511340381661,
8.81722098428722));
#407459=CARTESIAN_POINT('Ctrl Pts',(1.45216503745174,-2.26289739872511,
8.82945683644722));
#407460=CARTESIAN_POINT('Ctrl Pts',(1.45262738573792,-2.26876730635232,
8.83607469902389));
#407461=CARTESIAN_POINT('Ctrl Pts',(1.44444656216423,-2.27133755306294,
8.83829567148519));
#407462=CARTESIAN_POINT('Ctrl Pts',(1.45029105591256,-2.23910559748222,
8.85049129520029));
#407463=CARTESIAN_POINT('Ctrl Pts',(1.45074959802201,-2.24492718243453,
8.85711686593484));
#407464=CARTESIAN_POINT('Ctrl Pts',(1.44260408658469,-2.24752552912782,
8.85933012996512));
#407465=CARTESIAN_POINT('Origin',(1.4434434286944,-2.31135883822899,8.78727029226991));
#407466=CARTESIAN_POINT('Ctrl Pts',(1.45699136532628,-2.3241720011539,8.75374538247848));
#407467=CARTESIAN_POINT('Ctrl Pts',(1.45760113795345,-2.33174646851014,
8.75304829418601));
#407468=CARTESIAN_POINT('Ctrl Pts',(1.4511052095082,-2.33575565257217,8.75272238421917));
#407469=CARTESIAN_POINT('Ctrl Pts',(1.45709501436912,-2.3254879091256,8.76769408445022));
#407470=CARTESIAN_POINT('Ctrl Pts',(1.45771944369952,-2.33325303906549,
8.76974318093971));
#407471=CARTESIAN_POINT('Ctrl Pts',(1.45138968706045,-2.33737038507601,
8.7707786988043));
#407472=CARTESIAN_POINT('Ctrl Pts',(1.45656376843519,-2.31874331448478,
8.78108014887987));
#407473=CARTESIAN_POINT('Ctrl Pts',(1.45709673696933,-2.32532367783662,
8.78639403366323));
#407474=CARTESIAN_POINT('Ctrl Pts',(1.4499375907602,-2.32910107128779,8.78812224174741));
#407475=CARTESIAN_POINT('Ctrl Pts',(1.45569317358816,-2.30769041275578,
8.78944554828686));
#407476=CARTESIAN_POINT('Ctrl Pts',(1.45614791916577,-2.31323564711301,
8.79673892988686));
#407477=CARTESIAN_POINT('Ctrl Pts',(1.4475478719704,-2.31558995009988,8.79894799272499));
#407478=CARTESIAN_POINT('Origin',(1.44454451893667,-2.32533812225449,8.75721825406948));
#407479=CARTESIAN_POINT('Origin',(1.44454451893667,-2.32533812225449,9.));
#407480=CARTESIAN_POINT('Origin',(1.44454451893667,-2.32533812225449,7.51860402984325));
#407481=CARTESIAN_POINT('Ctrl Pts',(1.46529271774779,-2.32277634002134,
7.50366195182966));
#407482=CARTESIAN_POINT('Ctrl Pts',(1.46724653091866,-2.32587351709141,
7.50000065167736));
#407483=CARTESIAN_POINT('Ctrl Pts',(1.46724653091856,-2.32587351709147,
7.49482233047108));
#407484=CARTESIAN_POINT('Ctrl Pts',(1.4599326803461,-2.32793616546985,7.50215800491336));
#407485=CARTESIAN_POINT('Ctrl Pts',(1.45918346602515,-2.33095996689781,
7.49877273257263));
#407486=CARTESIAN_POINT('Ctrl Pts',(1.45626376864621,-2.33280184734056,
7.49481816995647));
#407487=CARTESIAN_POINT('Ctrl Pts',(1.45722758392157,-2.32716644495161,
7.51043025814044));
#407488=CARTESIAN_POINT('Ctrl Pts',(1.4560753670245,-2.33289053031165,7.51006209594517));
#407489=CARTESIAN_POINT('Ctrl Pts',(1.45113846196595,-2.33595744058181,
7.50731281821701));
#407490=CARTESIAN_POINT('Ctrl Pts',(1.45700580428833,-2.32435508238524,
7.51860402984326));
#407491=CARTESIAN_POINT('Ctrl Pts',(1.45760422169309,-2.33194078696692,
7.51860402984326));
#407492=CARTESIAN_POINT('Ctrl Pts',(1.45114061263044,-2.33595610454789,
7.51860402984327));
#407493=CARTESIAN_POINT('Origin',(0.,0.,7.5));
#407494=CARTESIAN_POINT('Origin',(1.59077126558569,-2.1415846479005,7.5));
#407495=CARTESIAN_POINT('',(1.59077126558569,-2.1415846479005,7.59394543036555));
#407496=CARTESIAN_POINT('',(1.59077126558569,-2.1415846479005,8.85049129520029));
#407497=CARTESIAN_POINT('',(1.59077126558569,-2.1415846479005,7.5));
#407498=CARTESIAN_POINT('',(1.60093990236831,-2.21235024422324,8.78727029226991));
#407499=CARTESIAN_POINT('Ctrl Pts',(1.59077126558569,-2.1415846479005,8.85049129520029));
#407500=CARTESIAN_POINT('Ctrl Pts',(1.59416573821268,-2.16520746822392,
8.82945686509571));
#407501=CARTESIAN_POINT('Ctrl Pts',(1.59755516454566,-2.18879517036851,
8.80838212259896));
#407502=CARTESIAN_POINT('Ctrl Pts',(1.60093990236831,-2.21235024422324,
8.78727029226991));
#407503=CARTESIAN_POINT('',(1.60293438610528,-2.22623025921638,8.75721825406948));
#407504=CARTESIAN_POINT('Origin',(1.59693249240026,-2.18446045038842,8.75937679713133));
#407505=CARTESIAN_POINT('',(1.60293438610528,-2.22623025921638,7.51860402984325));
#407506=CARTESIAN_POINT('',(1.60293438610528,-2.22623025921638,7.5));
#407507=CARTESIAN_POINT('Ctrl Pts',(1.60293438610528,-2.22623025921638,
7.51860402984325));
#407508=CARTESIAN_POINT('Ctrl Pts',(1.60136802933079,-2.21532966618993,
7.52834476460825));
#407509=CARTESIAN_POINT('Ctrl Pts',(1.59980065570009,-2.20442199665577,
7.53807742314407));
#407510=CARTESIAN_POINT('Ctrl Pts',(1.59823223107087,-2.19350701301076,
7.54780169004674));
#407511=CARTESIAN_POINT('Ctrl Pts',(1.5957479312243,-2.17621826882159,7.5632044032688));
#407512=CARTESIAN_POINT('Ctrl Pts',(1.59326099139911,-2.15891115248837,
7.57858609112102));
#407513=CARTESIAN_POINT('Ctrl Pts',(1.59077126558569,-2.1415846479005,7.59394543036555));
#407514=CARTESIAN_POINT('Origin',(1.85027428182728,-2.24930835533595,7.5));
#407515=CARTESIAN_POINT('',(1.67813633056182,-2.17010558942598,8.75721825406948));
#407516=CARTESIAN_POINT('',(1.66539749203248,-2.16424429481554,8.78727029226991));
#407517=CARTESIAN_POINT('Origin',(1.63306156849261,-2.14936614293919,8.75658640620944));
#407518=CARTESIAN_POINT('',(1.60045004741999,-2.13436118528462,8.85049129520029));
#407519=CARTESIAN_POINT('Ctrl Pts',(1.66539749203248,-2.16424429481554,
8.78727029226991));
#407520=CARTESIAN_POINT('Ctrl Pts',(1.6437790512361,-2.15429738715719,8.80838212259895));
#407521=CARTESIAN_POINT('Ctrl Pts',(1.62213066475767,-2.14433670112617,
8.82945686509571));
#407522=CARTESIAN_POINT('Ctrl Pts',(1.60045004741999,-2.13436118528462,
8.85049129520029));
#407523=CARTESIAN_POINT('',(1.60045004741999,-2.13436118528462,7.59394543036555));
#407524=CARTESIAN_POINT('',(1.60045004741999,-2.13436118528462,7.5));
#407525=CARTESIAN_POINT('',(1.67813633056182,-2.17010558942598,7.51860402984325));
#407526=CARTESIAN_POINT('Ctrl Pts',(1.60045004741999,-2.13436118528462,
7.59394543036555));
#407527=CARTESIAN_POINT('Ctrl Pts',(1.61635201469681,-2.14167787391995,
7.57858609112103));
#407528=CARTESIAN_POINT('Ctrl Pts',(1.63223618776748,-2.14898637522454,
7.56320440326857));
#407529=CARTESIAN_POINT('Ctrl Pts',(1.6481034992012,-2.15628711828478,7.54780169004651));
#407530=CARTESIAN_POINT('Ctrl Pts',(1.65812108306353,-2.16089633051136,
7.53807742314383));
#407531=CARTESIAN_POINT('Ctrl Pts',(1.66813195416117,-2.16550245411322,
7.52834476460825));
#407532=CARTESIAN_POINT('Ctrl Pts',(1.67813633056182,-2.17010558942598,
7.51860402984325));
#407533=CARTESIAN_POINT('',(1.67813633056182,-2.17010558942598,7.5));
#407534=CARTESIAN_POINT('Origin',(1.5975763681687,-2.1406067911448,7.5));
#407535=CARTESIAN_POINT('Ctrl Pts',(1.60045004741999,-2.13436118528462,
8.85049129520029));
#407536=CARTESIAN_POINT('Ctrl Pts',(1.60027411528381,-2.13428023676806,
8.85097269580138));
#407537=CARTESIAN_POINT('Ctrl Pts',(1.60009688697327,-2.13420795092933,
8.85143669361005));
#407538=CARTESIAN_POINT('Ctrl Pts',(1.59990987151216,-2.1341418087779,8.8519052845931));
#407539=CARTESIAN_POINT('Ctrl Pts',(1.59954408113031,-2.13401243892428,
8.85282181883899));
#407540=CARTESIAN_POINT('Ctrl Pts',(1.59915019230982,-2.13391008645578,
8.85372622499635));
#407541=CARTESIAN_POINT('Ctrl Pts',(1.59871814646303,-2.13384806842955,
8.8546225773507));
#407542=CARTESIAN_POINT('Ctrl Pts',(1.59835947734584,-2.13379658326684,
8.85536669723986));
#407543=CARTESIAN_POINT('Ctrl Pts',(1.59797443414081,-2.1337728524916,8.85610498449051));
#407544=CARTESIAN_POINT('Ctrl Pts',(1.59755673702271,-2.13379248063127,
8.8568133821837));
#407545=CARTESIAN_POINT('Ctrl Pts',(1.59717767623203,-2.13381029319885,
8.85745625420284));
#407546=CARTESIAN_POINT('Ctrl Pts',(1.5967669399937,-2.13386344000458,8.85808743050665));
#407547=CARTESIAN_POINT('Ctrl Pts',(1.59631559501555,-2.13397908798497,
8.8586680450841));
#407548=CARTESIAN_POINT('Ctrl Pts',(1.5961073542266,-2.13403244545619,8.85893592806395));
#407549=CARTESIAN_POINT('Ctrl Pts',(1.59589042136151,-2.13409934517698,
8.85919241173848));
#407550=CARTESIAN_POINT('Ctrl Pts',(1.59566382655846,-2.13418404876028,
8.85943017985534));
#407551=CARTESIAN_POINT('Ctrl Pts',(1.59535785649511,-2.13429842367267,
8.8597512372));
#407552=CARTESIAN_POINT('Ctrl Pts',(1.59502670637819,-2.13444877149742,
8.86004599534705));
#407553=CARTESIAN_POINT('Ctrl Pts',(1.59467866049516,-2.13464276930002,
8.86026130871721));
#407554=CARTESIAN_POINT('Ctrl Pts',(1.59455123108493,-2.13471379736492,
8.86034014101235));
#407555=CARTESIAN_POINT('Ctrl Pts',(1.59441961667038,-2.1347917328564,8.86040910639693));
#407556=CARTESIAN_POINT('Ctrl Pts',(1.59428757440423,-2.13487474190565,
8.86046313645507));
#407557=CARTESIAN_POINT('Ctrl Pts',(1.59408152355376,-2.13500427683179,
8.8605474499083));
#407558=CARTESIAN_POINT('Ctrl Pts',(1.59386888451754,-2.13514982695017,
8.86059655985669));
#407559=CARTESIAN_POINT('Ctrl Pts',(1.59366312900935,-2.13530181594061,
8.86059725258816));
#407560=CARTESIAN_POINT('Ctrl Pts',(1.59345689812372,-2.13545415608633,
8.86059794692012));
#407561=CARTESIAN_POINT('Ctrl Pts',(1.59325687403525,-2.13561679132398,
8.86056369958366));
#407562=CARTESIAN_POINT('Ctrl Pts',(1.59307159215572,-2.13577793168172,
8.86048590497774));
#407563=CARTESIAN_POINT('Ctrl Pts',(1.59302323910167,-2.13581998451737,
8.86046560290182));
#407564=CARTESIAN_POINT('Ctrl Pts',(1.59297532046824,-2.13586255097361,
8.86044257503091));
#407565=CARTESIAN_POINT('Ctrl Pts',(1.59292929518033,-2.13590429117003,
8.86041778462584));
#407566=CARTESIAN_POINT('Ctrl Pts',(1.59261960210531,-2.13618515089669,
8.86025097596201));
#407567=CARTESIAN_POINT('Ctrl Pts',(1.59235429876774,-2.13646653421405,
8.8599848982295));
#407568=CARTESIAN_POINT('Ctrl Pts',(1.5921349641717,-2.13673441605687,8.85968173251461));
#407569=CARTESIAN_POINT('Ctrl Pts',(1.59201894873677,-2.13687611020392,
8.85952137522076));
#407570=CARTESIAN_POINT('Ctrl Pts',(1.59191341042051,-2.13701663718524,
8.85934740853961));
#407571=CARTESIAN_POINT('Ctrl Pts',(1.59181859451242,-2.1371530817186,8.8591675900182));
#407572=CARTESIAN_POINT('Ctrl Pts',(1.5914378593571,-2.1377009774425,8.85844552518695));
#407573=CARTESIAN_POINT('Ctrl Pts',(1.59120601346868,-2.13821228521465,
8.85759444184125));
#407574=CARTESIAN_POINT('Ctrl Pts',(1.59105442443436,-2.13864615733888,
8.8568349891514));
#407575=CARTESIAN_POINT('Ctrl Pts',(1.59103856104563,-2.13869156090119,
8.85675551444999));
#407576=CARTESIAN_POINT('Ctrl Pts',(1.59102359633077,-2.13873611922889,
8.85667699793652));
#407577=CARTESIAN_POINT('Ctrl Pts',(1.59100946472096,-2.13877978665773,
8.85659965593547));
#407578=CARTESIAN_POINT('Ctrl Pts',(1.59081871553061,-2.13936921184039,
8.85555568965886));
#407579=CARTESIAN_POINT('Ctrl Pts',(1.59072051840021,-2.13996323391634,
8.85434650606346));
#407580=CARTESIAN_POINT('Ctrl Pts',(1.59070825637447,-2.14056377579997,
8.85297329937117));
#407581=CARTESIAN_POINT('Ctrl Pts',(1.59070135973213,-2.14090154401796,
8.85220095427747));
#407582=CARTESIAN_POINT('Ctrl Pts',(1.59072195981993,-2.14124151912216,
8.85137579139183));
#407583=CARTESIAN_POINT('Ctrl Pts',(1.59077126558569,-2.1415846479005,8.85049129520029));
#407584=CARTESIAN_POINT('Origin',(1.5975763681687,-2.1406067911448,7.59394543036555));
#407585=CARTESIAN_POINT('Ctrl Pts',(1.59993925707851,-2.13412616443333,
7.59443877723642));
#407586=CARTESIAN_POINT('Ctrl Pts',(1.59467860803057,-2.13170567579607,
7.58783886950016));
#407587=CARTESIAN_POINT('Ctrl Pts',(1.58944159958293,-2.13838796014022,
7.58559994247159));
#407588=CARTESIAN_POINT('Ctrl Pts',(1.62865698589034,-2.14733954089,7.56670252222137));
#407589=CARTESIAN_POINT('Ctrl Pts',(1.62340393997382,-2.14492255054604,
7.56004874999031));
#407590=CARTESIAN_POINT('Ctrl Pts',(1.61811908396272,-2.15163125043485,
7.55786368756704));
#407591=CARTESIAN_POINT('Ctrl Pts',(1.65732108721284,-2.16052824268629,
7.53888913333555));
#407592=CARTESIAN_POINT('Ctrl Pts',(1.65203682218725,-2.15809688805033,
7.53222002137276));
#407593=CARTESIAN_POINT('Ctrl Pts',(1.64674452104206,-2.16484922048506,
7.53005029815326));
#407594=CARTESIAN_POINT('Ctrl Pts',(1.6859302639761,-2.17369167302457,7.51101258149734));
#407595=CARTESIAN_POINT('Ctrl Pts',(1.68058194405662,-2.17123084595257,
7.5043616886572));
#407596=CARTESIAN_POINT('Ctrl Pts',(1.67531646186256,-2.17804129225283,
7.50217374673251));
#407597=CARTESIAN_POINT('',(1.67379182682866,-2.17733734542424,7.50366116523517));
#407598=CARTESIAN_POINT('Ctrl Pts',(1.67813633056182,-2.17010558942598,
7.51860402984325));
#407599=CARTESIAN_POINT('Ctrl Pts',(1.67853751304856,-2.17029017836962,
7.51734760759494));
#407600=CARTESIAN_POINT('Ctrl Pts',(1.67887516973813,-2.17051103085424,
7.51608817408573));
#407601=CARTESIAN_POINT('Ctrl Pts',(1.67914121444952,-2.17077881433842,
7.5148100591312));
#407602=CARTESIAN_POINT('Ctrl Pts',(1.67938220410643,-2.17102137901729,
7.51365231206384));
#407603=CARTESIAN_POINT('Ctrl Pts',(1.67956495208894,-2.17130261697213,
7.51247773061042));
#407604=CARTESIAN_POINT('Ctrl Pts',(1.67965533378806,-2.17163778110541,
7.51129758471022));
#407605=CARTESIAN_POINT('Ctrl Pts',(1.67976766791808,-2.17205435184589,
7.50983079813402));
#407606=CARTESIAN_POINT('Ctrl Pts',(1.6797211573249,-2.17254432228916,7.50839324291155));
#407607=CARTESIAN_POINT('Ctrl Pts',(1.67943339189006,-2.17310347783572,
7.50715379678855));
#407608=CARTESIAN_POINT('Ctrl Pts',(1.67930045255092,-2.17336179158654,
7.50658120839351));
#407609=CARTESIAN_POINT('Ctrl Pts',(1.67908867816629,-2.17366724429874,
7.50598221009429));
#407610=CARTESIAN_POINT('Ctrl Pts',(1.67878441548018,-2.17399960639673,
7.50545747549611));
#407611=CARTESIAN_POINT('Ctrl Pts',(1.67862205149305,-2.17417696509979,
7.50517746087247));
#407612=CARTESIAN_POINT('Ctrl Pts',(1.678431739111,-2.17436404651078,7.50491486231392));
#407613=CARTESIAN_POINT('Ctrl Pts',(1.67821734880152,-2.17455470687897,
7.50468370960992));
#407614=CARTESIAN_POINT('Ctrl Pts',(1.67789676766325,-2.17483980426981,
7.50433806340447));
#407615=CARTESIAN_POINT('Ctrl Pts',(1.6775123660958,-2.17514103710607,7.50405484070984));
#407616=CARTESIAN_POINT('Ctrl Pts',(1.67708959094888,-2.17543755403427,
7.50385766036131));
#407617=CARTESIAN_POINT('Ctrl Pts',(1.67704438171833,-2.17546926191083,
7.50383657498791));
#407618=CARTESIAN_POINT('Ctrl Pts',(1.67699876196236,-2.17550091364686,
7.50381643264937));
#407619=CARTESIAN_POINT('Ctrl Pts',(1.67695278336431,-2.17553248245704,
7.50379723213559));
#407620=CARTESIAN_POINT('Ctrl Pts',(1.67664586118162,-2.17574321459187,
7.50366906242519));
#407621=CARTESIAN_POINT('Ctrl Pts',(1.676315865729,-2.17595424268711,7.50358235568538));
#407622=CARTESIAN_POINT('Ctrl Pts',(1.67599290128614,-2.17615000193079,
7.5035341175365));
#407623=CARTESIAN_POINT('Ctrl Pts',(1.67550865265659,-2.176443520761,7.50346178989176));
#407624=CARTESIAN_POINT('Ctrl Pts',(1.67497523124543,-2.17673869053724,
7.50346967198527));
#407625=CARTESIAN_POINT('Ctrl Pts',(1.67444266060028,-2.17701234294117,
7.50354272648692));
#407626=CARTESIAN_POINT('Ctrl Pts',(1.67422360327037,-2.17712490183918,
7.50357277531559));
#407627=CARTESIAN_POINT('Ctrl Pts',(1.67400504573785,-2.1772337968943,7.50361331098761));
#407628=CARTESIAN_POINT('Ctrl Pts',(1.67379182682952,-2.17733734542536,
7.50366116523659));
#407629=CARTESIAN_POINT('',(1.59932759105275,-2.14295327027006,7.57603338622103));
#407630=CARTESIAN_POINT('Origin',(1.60461077043291,-2.15003701964738,7.58486873427624));
#407631=CARTESIAN_POINT('Ctrl Pts',(1.67379182688274,-2.17733734544331,
7.50366116529968));
#407632=CARTESIAN_POINT('Ctrl Pts',(1.64901056798238,-2.16589544848021,
7.52783573079709));
#407633=CARTESIAN_POINT('Ctrl Pts',(1.62419032049075,-2.15443464751554,
7.55196141284069));
#407634=CARTESIAN_POINT('Ctrl Pts',(1.59932759229144,-2.14295327045252,
7.57603338728831));
#407635=CARTESIAN_POINT('Ctrl Pts',(1.60045004741999,-2.13436118528462,
7.59394543036555));
#407636=CARTESIAN_POINT('Ctrl Pts',(1.58897458506506,-2.12908118542448,
7.59394543036555));
#407637=CARTESIAN_POINT('Ctrl Pts',(1.59077126558569,-2.1415846479005,7.59394543036555));
#407638=CARTESIAN_POINT('Ctrl Pts',(1.59833052356808,-2.1333859665705,7.58587155981958));
#407639=CARTESIAN_POINT('Ctrl Pts',(1.59247285696246,-2.13376855106787,
7.58685956158229));
#407640=CARTESIAN_POINT('Ctrl Pts',(1.59043941776118,-2.13927525189277,
7.58587155981959));
#407641=CARTESIAN_POINT('Ctrl Pts',(1.59858022403627,-2.13877412156755,
7.579829619046));
#407642=CARTESIAN_POINT('Ctrl Pts',(1.59606980950254,-2.13858813978266,
7.58148017275035));
#407643=CARTESIAN_POINT('Ctrl Pts',(1.59553382207232,-2.14104771044236,
7.57982961904594));
#407644=CARTESIAN_POINT('Ctrl Pts',(1.59932759055794,-2.14295326960672,
7.57603338509286));
#407645=CARTESIAN_POINT('Ctrl Pts',(1.59932759055794,-2.14295326960672,
7.57603338509286));
#407646=CARTESIAN_POINT('Ctrl Pts',(1.59932759055794,-2.14295326960672,
7.57603338509286));
#407647=CARTESIAN_POINT('Origin',(1.60461534358175,-2.1500336066184,7.58486873427624));
#407648=CARTESIAN_POINT('Ctrl Pts',(1.60415851687139,-2.23474923235821,
7.51098857897448));
#407649=CARTESIAN_POINT('Ctrl Pts',(1.60332114180601,-2.22892177022005,
7.50433767179956));
#407650=CARTESIAN_POINT('Ctrl Pts',(1.61134830926255,-2.22581168441624,
7.50214974420965));
#407651=CARTESIAN_POINT('Ctrl Pts',(1.5996779710407,-2.20356820934228,7.53887321589168));
#407652=CARTESIAN_POINT('Ctrl Pts',(1.59885062921467,-2.19781057054241,
7.53220407452061));
#407653=CARTESIAN_POINT('Ctrl Pts',(1.60682970075317,-2.19465821629431,
7.53003438070911));
#407654=CARTESIAN_POINT('Ctrl Pts',(1.59518882090922,-2.17232730725995,
7.56669465659231));
#407655=CARTESIAN_POINT('Ctrl Pts',(1.59436636851955,-2.16660369503496,
7.56004085833299));
#407656=CARTESIAN_POINT('Ctrl Pts',(1.60230148007192,-2.16344606067077,
7.55785582193789));
#407657=CARTESIAN_POINT('Ctrl Pts',(1.59069126950323,-2.14102793901221,
7.59443891967696));
#407658=CARTESIAN_POINT('Ctrl Pts',(1.58986762466002,-2.13529602826209,
7.58783901202978));
#407659=CARTESIAN_POINT('Ctrl Pts',(1.59776378899006,-2.13217677084063,
7.58560008491213));
#407660=CARTESIAN_POINT('',(1.61110336926413,-2.22412295723129,7.50366116523517));
#407661=CARTESIAN_POINT('Ctrl Pts',(1.61110336926435,-2.22412295723159,
7.50366116523554));
#407662=CARTESIAN_POINT('Ctrl Pts',(1.61059198069088,-2.22468208087059,
7.50350835821027));
#407663=CARTESIAN_POINT('Ctrl Pts',(1.61010369996945,-2.22517941370504,
7.50345484955999));
#407664=CARTESIAN_POINT('Ctrl Pts',(1.6096244386178,-2.22563016254552,7.50349758195598));
#407665=CARTESIAN_POINT('Ctrl Pts',(1.60937854200145,-2.22586143012909,
7.50351950684424));
#407666=CARTESIAN_POINT('Ctrl Pts',(1.60911087181361,-2.22610332366122,
7.50357029184312));
#407667=CARTESIAN_POINT('Ctrl Pts',(1.60884634880778,-2.22632948384842,
7.50365515313923));
#407668=CARTESIAN_POINT('Ctrl Pts',(1.60843940530886,-2.22667740979762,
7.50378570417639));
#407669=CARTESIAN_POINT('Ctrl Pts',(1.60802819036978,-2.22699857665867,
7.50400001621911));
#407670=CARTESIAN_POINT('Ctrl Pts',(1.60764260590767,-2.22726674962692,
7.50428903009634));
#407671=CARTESIAN_POINT('Ctrl Pts',(1.60759980899889,-2.2272965147632,7.50432110841318));
#407672=CARTESIAN_POINT('Ctrl Pts',(1.60755731717551,-2.22732565543006,
7.50435406373354));
#407673=CARTESIAN_POINT('Ctrl Pts',(1.60751516316796,-2.22735415659424,
7.50438785222352));
#407674=CARTESIAN_POINT('Ctrl Pts',(1.6072577926901,-2.22752816990097,7.50459414719561));
#407675=CARTESIAN_POINT('Ctrl Pts',(1.60700862846067,-2.22768068774653,
7.50483629897752));
#407676=CARTESIAN_POINT('Ctrl Pts',(1.60677790295502,-2.2278069896599,7.5050991045531));
#407677=CARTESIAN_POINT('Ctrl Pts',(1.60626889931537,-2.22808562436662,
7.50567888004914));
#407678=CARTESIAN_POINT('Ctrl Pts',(1.60582982688947,-2.22824810547531,
7.50637912803145));
#407679=CARTESIAN_POINT('Ctrl Pts',(1.60546347309896,-2.2283252168882,7.50710440483569));
#407680=CARTESIAN_POINT('Ctrl Pts',(1.60537363587638,-2.22834412613751,
7.50728225710685));
#407681=CARTESIAN_POINT('Ctrl Pts',(1.60528641310259,-2.22835842111518,
7.50746498566955));
#407682=CARTESIAN_POINT('Ctrl Pts',(1.60520390821617,-2.22836817923873,
7.50764697238949));
#407683=CARTESIAN_POINT('Ctrl Pts',(1.60476038465272,-2.2284206362254,7.50862528291182));
#407684=CARTESIAN_POINT('Ctrl Pts',(1.60441342469444,-2.22835085759283,
7.50965856837421));
#407685=CARTESIAN_POINT('Ctrl Pts',(1.60413297204736,-2.22821793661503,
7.51067959873201));
#407686=CARTESIAN_POINT('Ctrl Pts',(1.60397863860193,-2.22814479003328,
7.51124147302578));
#407687=CARTESIAN_POINT('Ctrl Pts',(1.60384459404931,-2.22805211156061,
7.51180065547252));
#407688=CARTESIAN_POINT('Ctrl Pts',(1.60372708158229,-2.22794733879844,
7.512351757165));
#407689=CARTESIAN_POINT('Ctrl Pts',(1.60332102919734,-2.22758530716863,
7.51425603304535));
#407690=CARTESIAN_POINT('Ctrl Pts',(1.60306798798222,-2.22703118031392,
7.5162690050518));
#407691=CARTESIAN_POINT('Ctrl Pts',(1.60295199935764,-2.22634316468706,
7.51827788969243));
#407692=CARTESIAN_POINT('Ctrl Pts',(1.60294572183409,-2.22630592798116,
7.51838661432545));
#407693=CARTESIAN_POINT('Ctrl Pts',(1.60293985101504,-2.22626829062669,
7.51849533314856));
#407694=CARTESIAN_POINT('Ctrl Pts',(1.60293438610528,-2.22623025921638,
7.51860402984325));
#407695=CARTESIAN_POINT('Ctrl Pts',(1.59932759087574,-2.14295327151057,
7.57603338728985));
#407696=CARTESIAN_POINT('Ctrl Pts',(1.60326028592398,-2.17005513828705,
7.55196141284922));
#407697=CARTESIAN_POINT('Ctrl Pts',(1.60718534226389,-2.19711042572332,
7.52783573083105));
#407698=CARTESIAN_POINT('Ctrl Pts',(1.61110336926721,-2.22412295729039,
7.50366116530176));
#407699=CARTESIAN_POINT('Origin',(5.52641612598468E-16,-7.40489414195296E-16,
7.49482233047033));
#407700=CARTESIAN_POINT('Origin',(1.66840488432878,-2.17032978875283,7.49482233047033));
#407701=CARTESIAN_POINT('Origin',(0.,0.,7.50366116523517));
#407702=CARTESIAN_POINT('Origin',(1.60591818370373,-2.2169648254426,7.49482233047033));
#407703=CARTESIAN_POINT('Ctrl Pts',(1.67813536969269,-2.17010514726914,
7.51860402984325));
#407704=CARTESIAN_POINT('Ctrl Pts',(1.68504747448013,-2.17328619952233,
7.51860402984325));
#407705=CARTESIAN_POINT('Ctrl Pts',(1.69104778275851,-2.16860724808056,
7.51860402984325));
#407706=CARTESIAN_POINT('Ctrl Pts',(1.68070188190216,-2.17128629252502,
7.51041458714365));
#407707=CARTESIAN_POINT('Ctrl Pts',(1.6864690101503,-2.17217769452731,7.51004642900442));
#407708=CARTESIAN_POINT('Ctrl Pts',(1.69104943757229,-2.16860595768131,
7.50729136483009));
#407709=CARTESIAN_POINT('Ctrl Pts',(1.68047942032506,-2.17409240158313,
7.50215815450137));
#407710=CARTESIAN_POINT('Ctrl Pts',(1.68357470801357,-2.1744348320239,7.49877163671531));
#407711=CARTESIAN_POINT('Ctrl Pts',(1.68631009160464,-2.17233207188443,
7.49481588533172));
#407712=CARTESIAN_POINT('Ctrl Pts',(1.67379149130793,-2.17733690896584,
7.50366171572174));
#407713=CARTESIAN_POINT('Ctrl Pts',(1.67602317147152,-2.18023997043687,
7.50000045605858));
#407714=CARTESIAN_POINT('Ctrl Pts',(1.67602317147162,-2.18023997043679,
7.49482233047317));
#407715=CARTESIAN_POINT('Origin',(1.68336120192779,-2.15874994240746,7.51860402984325));
#407716=CARTESIAN_POINT('Origin',(1.68336120192779,-2.15874994240746,9.));
#407717=CARTESIAN_POINT('Origin',(1.68336120192779,-2.15874994240746,8.75721825406948));
#407718=CARTESIAN_POINT('Ctrl Pts',(1.66296505241367,-2.1631250664948,8.78942910404913));
#407719=CARTESIAN_POINT('Ctrl Pts',(1.66801889291353,-2.16547264501399,
8.79672699501691));
#407720=CARTESIAN_POINT('Ctrl Pts',(1.67320190366869,-2.15820560397282,
8.79893251111267));
#407721=CARTESIAN_POINT('Ctrl Pts',(1.67295287420541,-2.16772058981614,
8.78111911759576));
#407722=CARTESIAN_POINT('Ctrl Pts',(1.67894739662943,-2.17049692031404,
8.78644465894812));
#407723=CARTESIAN_POINT('Ctrl Pts',(1.6849604788733,-2.16506016082844,8.78817647674131));
#407724=CARTESIAN_POINT('Ctrl Pts',(1.67917752299134,-2.17058462953467,
8.76780923932034));
#407725=CARTESIAN_POINT('Ctrl Pts',(1.68625594515373,-2.17385734651929,
8.76988516158375));
#407726=CARTESIAN_POINT('Ctrl Pts',(1.69231030965761,-2.16933174701751,
8.77093053738834));
#407727=CARTESIAN_POINT('Ctrl Pts',(1.67796380166913,-2.17002618098512,
8.75371302330491));
#407728=CARTESIAN_POINT('Ctrl Pts',(1.6848681772406,-2.17321926716246,8.75300828287559));
#407729=CARTESIAN_POINT('Ctrl Pts',(1.69087702405881,-2.16849821862959,
8.75267964240738));
#407730=CARTESIAN_POINT('Origin',(1.67062236339845,-2.15288864779702,8.78727029226991));
#407731=CARTESIAN_POINT('Ctrl Pts',(1.60045004741999,-2.13436118528462,
8.85049129520029));
#407732=CARTESIAN_POINT('Ctrl Pts',(1.60575505664343,-2.13680208457838,
8.85711686593484));
#407733=CARTESIAN_POINT('Ctrl Pts',(1.61100669796545,-2.13005515746015,
8.85933012996512));
#407734=CARTESIAN_POINT('Ctrl Pts',(1.62213069385386,-2.14433671451368,
8.82945683644722));
#407735=CARTESIAN_POINT('Ctrl Pts',(1.62747973786134,-2.14679787474736,
8.83607469902389));
#407736=CARTESIAN_POINT('Ctrl Pts',(1.63271720381485,-2.14000810355218,
8.83829567148519));
#407737=CARTESIAN_POINT('Ctrl Pts',(1.64377902353591,-2.154297374412,8.80838214965002));
#407738=CARTESIAN_POINT('Ctrl Pts',(1.64914917736847,-2.15676824753308,
8.81501364461992));
#407739=CARTESIAN_POINT('Ctrl Pts',(1.65439449734903,-2.14994655925988,
8.81722098428722));
#407740=CARTESIAN_POINT('Ctrl Pts',(1.66539749203248,-2.16424429481554,
8.78727029226991));
#407741=CARTESIAN_POINT('Ctrl Pts',(1.67076853786521,-2.16671557835676,
8.79393457792714));
#407742=CARTESIAN_POINT('Ctrl Pts',(1.67604110579952,-2.15987164362911,
8.79610912703474));
#407743=CARTESIAN_POINT('Origin',(1.60567491878596,-2.1230055382661,8.85049129520029));
#407744=CARTESIAN_POINT('Ctrl Pts',(1.59077126558569,-2.1415846479005,8.85049129520029));
#407745=CARTESIAN_POINT('Ctrl Pts',(1.59160185579972,-2.14736489288834,
8.85711686593484));
#407746=CARTESIAN_POINT('Ctrl Pts',(1.58363955683349,-2.15047978570931,
8.85933012996512));
#407747=CARTESIAN_POINT('Ctrl Pts',(1.59003645441303,-2.13647094859846,
8.86332496987231));
#407748=CARTESIAN_POINT('Ctrl Pts',(1.58650902291591,-2.13945576373675,
8.86648636486736));
#407749=CARTESIAN_POINT('Ctrl Pts',(1.58160085107661,-2.13617156656108,
8.87206031107458));
#407750=CARTESIAN_POINT('Ctrl Pts',(1.5957248901228,-2.13218708291762,8.86341338519877));
#407751=CARTESIAN_POINT('Ctrl Pts',(1.59958467164427,-2.1296227979801,8.86654584966057));
#407752=CARTESIAN_POINT('Ctrl Pts',(1.59776984823889,-2.12398093935068,
8.87215952290713));
#407753=CARTESIAN_POINT('Ctrl Pts',(1.60045004741999,-2.13436118528462,
8.85049129520029));
#407754=CARTESIAN_POINT('Ctrl Pts',(1.60575505664343,-2.13680208457838,
8.85711686593484));
#407755=CARTESIAN_POINT('Ctrl Pts',(1.61100669796545,-2.13005515746015,
8.85933012996512));
#407756=CARTESIAN_POINT('Origin',(1.57839835179839,-2.14336256927449,8.85049129520029));
#407757=CARTESIAN_POINT('Ctrl Pts',(1.60093990236831,-2.21235024422324,
8.78727029226991));
#407758=CARTESIAN_POINT('Ctrl Pts',(1.60178083174655,-2.21820244154213,
8.79393457792714));
#407759=CARTESIAN_POINT('Ctrl Pts',(1.59371958050517,-2.22130979469258,
8.79610912703474));
#407760=CARTESIAN_POINT('Ctrl Pts',(1.59755516020871,-2.18879514018686,
8.80838214965003));
#407761=CARTESIAN_POINT('Ctrl Pts',(1.598395949929,-2.19464636559799,8.8150136446199));
#407762=CARTESIAN_POINT('Ctrl Pts',(1.59036377844287,-2.19773392674114,
8.81722098428722));
#407763=CARTESIAN_POINT('Ctrl Pts',(1.59416574276819,-2.16520749992663,
8.82945683644723));
#407764=CARTESIAN_POINT('Ctrl Pts',(1.59500322738317,-2.17103572444266,
8.83607469902388));
#407765=CARTESIAN_POINT('Ctrl Pts',(1.58700388846104,-2.17412483747174,
8.8382956714852));
#407766=CARTESIAN_POINT('Ctrl Pts',(1.59077126558569,-2.1415846479005,8.85049129520029));
#407767=CARTESIAN_POINT('Ctrl Pts',(1.59160185579972,-2.14736489288834,
8.85711686593484));
#407768=CARTESIAN_POINT('Ctrl Pts',(1.58363955683349,-2.15047978570931,
8.85933012996512));
#407769=CARTESIAN_POINT('Origin',(1.58856698858102,-2.21412816559723,8.78727029226991));
#407770=CARTESIAN_POINT('Ctrl Pts',(1.60290803169132,-2.22604698322441,
8.75374538247847));
#407771=CARTESIAN_POINT('Ctrl Pts',(1.60400184926499,-2.23356681975875,
8.75304829418601));
#407772=CARTESIAN_POINT('Ctrl Pts',(1.59777613670621,-2.23798396208661,
8.75272238421917));
#407773=CARTESIAN_POINT('Ctrl Pts',(1.60309577828932,-2.22735354670507,
8.76769408445022));
#407774=CARTESIAN_POINT('Ctrl Pts',(1.60421643824611,-2.23506271502813,
8.7697431809397));
#407775=CARTESIAN_POINT('Ctrl Pts',(1.59816348603556,-2.23957715040998,
8.77077869880429));
#407776=CARTESIAN_POINT('Ctrl Pts',(1.60213349619481,-2.22065684660117,
8.78108014887987));
#407777=CARTESIAN_POINT('Ctrl Pts',(1.60308697501545,-2.22718954247952,
8.78639403366323));
#407778=CARTESIAN_POINT('Ctrl Pts',(1.59618455646938,-2.23141786294321,
8.78812224174742));
#407779=CARTESIAN_POINT('Ctrl Pts',(1.60055652823306,-2.20968243344753,
8.78944554828686));
#407780=CARTESIAN_POINT('Ctrl Pts',(1.60136562387223,-2.21518713887686,
8.79673892988686));
#407781=CARTESIAN_POINT('Ctrl Pts',(1.59293408710644,-2.2180876116114,8.79894799272499));
#407782=CARTESIAN_POINT('Origin',(1.59056147231799,-2.22800818059038,8.75721825406948));
#407783=CARTESIAN_POINT('Origin',(1.59056147231799,-2.22800818059038,9.));
#407784=CARTESIAN_POINT('Origin',(1.59056147231799,-2.22800818059038,7.51860402984325));
#407785=CARTESIAN_POINT('Ctrl Pts',(1.61110290777819,-2.22412232015155,
7.50366195182966));
#407786=CARTESIAN_POINT('Ctrl Pts',(1.61325114344655,-2.2270879524995,7.50000065167735));
#407787=CARTESIAN_POINT('Ctrl Pts',(1.61325114344646,-2.22708795249957,
7.49482233047108));
#407788=CARTESIAN_POINT('Ctrl Pts',(1.60608447429974,-2.2296149629607,7.50215800491337));
#407789=CARTESIAN_POINT('Ctrl Pts',(1.60553053494263,-2.23268055399066,
7.49877273257264));
#407790=CARTESIAN_POINT('Ctrl Pts',(1.60273484608026,-2.23470571574587,
7.49481816995649));
#407791=CARTESIAN_POINT('Ctrl Pts',(1.60333561962302,-2.22902014003884,
7.51043025814043));
#407792=CARTESIAN_POINT('Ctrl Pts',(1.60255251348734,-2.23480628744168,
7.51006209594517));
#407793=CARTESIAN_POINT('Ctrl Pts',(1.59782224944538,-2.23818320500886,
7.50731281821699));
#407794=CARTESIAN_POINT('Ctrl Pts',(1.60293417104175,-2.22622876318826,
7.51860402984326));
#407795=CARTESIAN_POINT('Ctrl Pts',(1.60401737669502,-2.23376054139154,
7.51860402984327));
#407796=CARTESIAN_POINT('Ctrl Pts',(1.59782431009112,-2.23818173392641,
7.51860402984327));
#407797=CARTESIAN_POINT('Origin',(0.,0.,7.5));
#407798=CARTESIAN_POINT('Origin',(1.72471465490916,-2.03526346763208,7.5));
#407799=CARTESIAN_POINT('',(1.72471465490916,-2.03526346763208,7.59394543036555));
#407800=CARTESIAN_POINT('',(1.72471465490916,-2.03526346763208,8.85049129520029));
#407801=CARTESIAN_POINT('',(1.72471465490916,-2.03526346763208,7.5));
#407802=CARTESIAN_POINT('',(1.7393963664604,-2.10523216165202,8.78727029226991));
#407803=CARTESIAN_POINT('Ctrl Pts',(1.72471465490916,-2.03526346763208,
8.85049129520029));
#407804=CARTESIAN_POINT('Ctrl Pts',(1.72961567252277,-2.05862026772968,
8.82945686509571));
#407805=CARTESIAN_POINT('Ctrl Pts',(1.73450940418107,-2.08194234511967,
8.80838212259896));
#407806=CARTESIAN_POINT('Ctrl Pts',(1.7393963664604,-2.10523216165202,8.78727029226991));
#407807=CARTESIAN_POINT('',(1.74227604793057,-2.11895587165396,8.75721825406948));
#407808=CARTESIAN_POINT('Origin',(1.73361028491986,-2.07765642602876,8.75937679713156));
#407809=CARTESIAN_POINT('',(1.74227604793057,-2.11895587165396,7.51860402984325));
#407810=CARTESIAN_POINT('',(1.74227604793057,-2.11895587165396,7.5));
#407811=CARTESIAN_POINT('Ctrl Pts',(1.74227604793057,-2.11895587165396,
7.51860402984325));
#407812=CARTESIAN_POINT('Ctrl Pts',(1.74001450601094,-2.10817803188807,
7.52834476460825));
#407813=CARTESIAN_POINT('Ctrl Pts',(1.73775149593093,-2.09739319530413,
7.53807742314407));
#407814=CARTESIAN_POINT('Ctrl Pts',(1.7354869683951,-2.08660112697466,7.54780169004674));
#407815=CARTESIAN_POINT('Ctrl Pts',(1.73190007916561,-2.06950707400231,
7.5632044032688));
#407816=CARTESIAN_POINT('Ctrl Pts',(1.72830937827432,-2.05239485577746,
7.57858609112103));
#407817=CARTESIAN_POINT('Ctrl Pts',(1.72471465490916,-2.03526346763208,
7.59394543036555));
#407818=CARTESIAN_POINT('Origin',(1.9905863760048,-2.12613942982102,7.5));
#407819=CARTESIAN_POINT('',(1.81372756198702,-2.05812831089268,8.75721825406948));
#407820=CARTESIAN_POINT('',(1.80063936233261,-2.05309523912752,8.78727029226991));
#407821=CARTESIAN_POINT('Origin',(1.76741662995361,-2.04031942574495,8.75658640621003));
#407822=CARTESIAN_POINT('',(1.73391074180931,-2.02743472471359,8.85049129520029));
#407823=CARTESIAN_POINT('Ctrl Pts',(1.80063936233261,-2.05309523912752,
8.78727029226991));
#407824=CARTESIAN_POINT('Ctrl Pts',(1.77842803837963,-2.04455386671523,
8.80838212259896));
#407825=CARTESIAN_POINT('Ctrl Pts',(1.75618594748783,-2.03600066286583,
8.82945686509571));
#407826=CARTESIAN_POINT('Ctrl Pts',(1.73391074180931,-2.02743472471359,
8.85049129520029));
#407827=CARTESIAN_POINT('',(1.73391074180931,-2.02743472471359,7.59394543036555));
#407828=CARTESIAN_POINT('',(1.73391074180931,-2.02743472471359,7.5));
#407829=CARTESIAN_POINT('',(1.81372756198702,-2.05812831089268,7.51860402984325));
#407830=CARTESIAN_POINT('Ctrl Pts',(1.73391074180931,-2.02743472471359,
7.59394543036555));
#407831=CARTESIAN_POINT('Ctrl Pts',(1.75024881863928,-2.03371753788586,
7.57858609112103));
#407832=CARTESIAN_POINT('Ctrl Pts',(1.76656861325912,-2.03999332062783,
7.56320440326857));
#407833=CARTESIAN_POINT('Ctrl Pts',(1.78287108381363,-2.04626244139439,
7.54780169004651));
#407834=CARTESIAN_POINT('Ctrl Pts',(1.79316339871683,-2.05022035469838,
7.53807742314383));
#407835=CARTESIAN_POINT('Ctrl Pts',(1.80344881675856,-2.05417561581187,
7.52834476460825));
#407836=CARTESIAN_POINT('Ctrl Pts',(1.81372756198702,-2.05812831089268,
7.51860402984324));
#407837=CARTESIAN_POINT('',(1.81372756198702,-2.05812831089268,7.5));
#407838=CARTESIAN_POINT('Origin',(1.73144312418163,-2.03385161556848,7.5));
#407839=CARTESIAN_POINT('Ctrl Pts',(1.73391074180931,-2.02743472471359,
8.85049129520029));
#407840=CARTESIAN_POINT('Ctrl Pts',(1.73372998475531,-2.02736521452511,
8.85097269580138));
#407841=CARTESIAN_POINT('Ctrl Pts',(1.73354848920976,-2.02730443226223,
8.85143669361005));
#407842=CARTESIAN_POINT('Ctrl Pts',(1.73335762024977,-2.02725040812867,
8.8519052845931));
#407843=CARTESIAN_POINT('Ctrl Pts',(1.73298429266852,-2.02714474034953,
8.85282181883899));
#407844=CARTESIAN_POINT('Ctrl Pts',(1.73258465538969,-2.02706783471853,
8.85372622499635));
#407845=CARTESIAN_POINT('Ctrl Pts',(1.73214952371884,-2.02703362538743,
8.8546225773507));
#407846=CARTESIAN_POINT('Ctrl Pts',(1.73178829286012,-2.02700522601574,
8.85536669723986));
#407847=CARTESIAN_POINT('Ctrl Pts',(1.73140252033166,-2.02700621380077,
8.85610498449051));
#407848=CARTESIAN_POINT('Ctrl Pts',(1.73098693899631,-2.02705256355857,
8.85681338218371));
#407849=CARTESIAN_POINT('Ctrl Pts',(1.7306097982818,-2.02709462603657,8.85745625420285));
#407850=CARTESIAN_POINT('Ctrl Pts',(1.73020331107266,-2.02717397960763,
8.85808743050666));
#407851=CARTESIAN_POINT('Ctrl Pts',(1.72976030302272,-2.02731830774888,
8.85866804508411));
#407852=CARTESIAN_POINT('Ctrl Pts',(1.72955590871172,-2.02738489762461,
8.85893592806396));
#407853=CARTESIAN_POINT('Ctrl Pts',(1.72934370783829,-2.02746555882914,
8.85919241173848));
#407854=CARTESIAN_POINT('Ctrl Pts',(1.72912300557579,-2.02756460635871,
8.85943017985534));
#407855=CARTESIAN_POINT('Ctrl Pts',(1.72882499218654,-2.02769834984485,
8.8597512372));
#407856=CARTESIAN_POINT('Ctrl Pts',(1.72850415527126,-2.02786960562471,
8.86004599534705));
#407857=CARTESIAN_POINT('Ctrl Pts',(1.72816925396771,-2.0280855042143,8.86026130871721));
#407858=CARTESIAN_POINT('Ctrl Pts',(1.72804663715862,-2.02816455077478,
8.86034014101235));
#407859=CARTESIAN_POINT('Ctrl Pts',(1.72792028650408,-2.02825075870392,
8.86040910639692));
#407860=CARTESIAN_POINT('Ctrl Pts',(1.72779383394098,-2.02834205717921,
8.86046313645506));
#407861=CARTESIAN_POINT('Ctrl Pts',(1.72759650577529,-2.02848452768528,
8.86054744990829));
#407862=CARTESIAN_POINT('Ctrl Pts',(1.72739362905688,-2.02864340258515,
8.86059655985669));
#407863=CARTESIAN_POINT('Ctrl Pts',(1.72719803426349,-2.02880826209858,
8.86059725258816));
#407864=CARTESIAN_POINT('Ctrl Pts',(1.727001987568,-2.02897350250335,8.86059794692012));
#407865=CARTESIAN_POINT('Ctrl Pts',(1.72681279452592,-2.0291486191768,8.86056369958366));
#407866=CARTESIAN_POINT('Ctrl Pts',(1.72663821762605,-2.02932129950518,
8.86048590497774));
#407867=CARTESIAN_POINT('Ctrl Pts',(1.72659265825296,-2.02936636392957,
8.86046560290182));
#407868=CARTESIAN_POINT('Ctrl Pts',(1.72654756531572,-2.02941191308585,
8.86044257503091));
#407869=CARTESIAN_POINT('Ctrl Pts',(1.72650430889527,-2.02945651637288,
8.86041778462583));
#407870=CARTESIAN_POINT('Ctrl Pts',(1.72621324686235,-2.02975664114655,
8.86025097596201));
#407871=CARTESIAN_POINT('Ctrl Pts',(1.72596651690999,-2.03005444437491,
8.8599848982295));
#407872=CARTESIAN_POINT('Ctrl Pts',(1.72576479620899,-2.03033582864157,
8.85968173251462));
#407873=CARTESIAN_POINT('Ctrl Pts',(1.72565809751539,-2.03048466479723,
8.85952137522077));
#407874=CARTESIAN_POINT('Ctrl Pts',(1.72556177963353,-2.03063166491394,
8.85934740853961));
#407875=CARTESIAN_POINT('Ctrl Pts',(1.72547590056616,-2.03077390398346,
8.8591675900182));
#407876=CARTESIAN_POINT('Ctrl Pts',(1.72513105147161,-2.03134506778199,
8.85844552518696));
#407877=CARTESIAN_POINT('Ctrl Pts',(1.72493244153686,-2.03187017943455,
8.85759444184125));
#407878=CARTESIAN_POINT('Ctrl Pts',(1.72480896224092,-2.03231287246475,
8.8568349891514));
#407879=CARTESIAN_POINT('Ctrl Pts',(1.72479604046145,-2.03235919911137,
8.85675551444999));
#407880=CARTESIAN_POINT('Ctrl Pts',(1.72478396135506,-2.03240462468179,
8.85667699793652));
#407881=CARTESIAN_POINT('Ctrl Pts',(1.72477265656193,-2.03244910780656,
8.85659965593547));
#407882=CARTESIAN_POINT('Ctrl Pts',(1.72462006388736,-2.03304954329455,
8.85555568965886));
#407883=CARTESIAN_POINT('Ctrl Pts',(1.72456012763858,-2.03364863640018,
8.85434650606346));
#407884=CARTESIAN_POINT('Ctrl Pts',(1.72458636765708,-2.0342487300368,8.85297329937117));
#407885=CARTESIAN_POINT('Ctrl Pts',(1.72460112606866,-2.03458624614315,
8.85220095427747));
#407886=CARTESIAN_POINT('Ctrl Pts',(1.72464346611107,-2.03492420287988,
8.85137579139183));
#407887=CARTESIAN_POINT('Ctrl Pts',(1.72471465490916,-2.03526346763208,
8.85049129520029));
#407888=CARTESIAN_POINT('Origin',(1.73144312418163,-2.03385161556848,7.59394543036555));
#407889=CARTESIAN_POINT('Ctrl Pts',(1.73338594310373,-2.02723291318739,
7.59443877723642));
#407890=CARTESIAN_POINT('Ctrl Pts',(1.72798102138401,-2.02515444864538,
7.58783886950016));
#407891=CARTESIAN_POINT('Ctrl Pts',(1.7231829083598,-2.03215853980295,7.58559994247159));
#407892=CARTESIAN_POINT('Ctrl Pts',(1.76289125219805,-2.03857919014268,
7.5667025222214));
#407893=CARTESIAN_POINT('Ctrl Pts',(1.75749414212467,-2.03650372957208,
7.5600487499903));
#407894=CARTESIAN_POINT('Ctrl Pts',(1.75264997229473,-2.04353724760462,
7.55786368756704));
#407895=CARTESIAN_POINT('Ctrl Pts',(1.79234146307551,-2.04990427905937,
7.53888913333558));
#407896=CARTESIAN_POINT('Ctrl Pts',(1.78691227771274,-2.04781648392493,
7.53222002137277));
#407897=CARTESIAN_POINT('Ctrl Pts',(1.78206347359233,-2.05489402186702,
7.53005029815327));
#407898=CARTESIAN_POINT('Ctrl Pts',(1.82173524309424,-2.06120766746955,
7.51101258149734));
#407899=CARTESIAN_POINT('Ctrl Pts',(1.8162402461398,-2.05909456446446,7.5043616886572));
#407900=CARTESIAN_POINT('Ctrl Pts',(1.81142192923626,-2.06622837857485,
7.50217374673251));
#407901=CARTESIAN_POINT('',(1.80985532470038,-2.06562356178253,7.50366116523517));
#407902=CARTESIAN_POINT('Ctrl Pts',(1.81372756198702,-2.05812831089268,
7.51860402984325));
#407903=CARTESIAN_POINT('Ctrl Pts',(1.81413974685554,-2.05828681672836,
7.51734760759493));
#407904=CARTESIAN_POINT('Ctrl Pts',(1.8144908598605,-2.05848558170949,7.51608817408573));
#407905=CARTESIAN_POINT('Ctrl Pts',(1.81477351490123,-2.0587357694606,7.5148100591312));
#407906=CARTESIAN_POINT('Ctrl Pts',(1.81502955059139,-2.05896239550399,
7.51365231206384));
#407907=CARTESIAN_POINT('Ctrl Pts',(1.8152299420762,-2.05923134692185,7.51247773061042));
#407908=CARTESIAN_POINT('Ctrl Pts',(1.81534161211617,-2.05956003164913,
7.51129758471022));
#407909=CARTESIAN_POINT('Ctrl Pts',(1.81548040522266,-2.05996854922792,
7.50983079813402));
#407910=CARTESIAN_POINT('Ctrl Pts',(1.81546538270456,-2.06046049291831,
7.50839324291155));
#407911=CARTESIAN_POINT('Ctrl Pts',(1.81521403373354,-2.06103693681454,
7.50715379678855));
#407912=CARTESIAN_POINT('Ctrl Pts',(1.81509791775138,-2.06130323728476,
7.50658120839351));
#407913=CARTESIAN_POINT('Ctrl Pts',(1.81490614890239,-2.06162163084301,
7.50598221009429));
#407914=CARTESIAN_POINT('Ctrl Pts',(1.81462380586933,-2.06197280424466,
7.50545747549611));
#407915=CARTESIAN_POINT('Ctrl Pts',(1.81447313888755,-2.06216020124161,
7.50517746087247));
#407916=CARTESIAN_POINT('Ctrl Pts',(1.81429520386986,-2.06235909162996,
7.50491486231392));
#407917=CARTESIAN_POINT('Ctrl Pts',(1.81409346969999,-2.06256309630026,
7.50468370960992));
#407918=CARTESIAN_POINT('Ctrl Pts',(1.8137918134826,-2.06286814763199,7.50433806340447));
#407919=CARTESIAN_POINT('Ctrl Pts',(1.81342750176348,-2.06319339024607,
7.50405484070984));
#407920=CARTESIAN_POINT('Ctrl Pts',(1.81302459315826,-2.06351638524511,
7.50385766036131));
#407921=CARTESIAN_POINT('Ctrl Pts',(1.81298150834555,-2.06355092453978,
7.50383657498791));
#407922=CARTESIAN_POINT('Ctrl Pts',(1.81293801025395,-2.06358543411172,
7.50381643264937));
#407923=CARTESIAN_POINT('Ctrl Pts',(1.81289414874447,-2.06361988391929,
7.50379723213559));
#407924=CARTESIAN_POINT('Ctrl Pts',(1.81260135882057,-2.0638498476541,7.50366906242519));
#407925=CARTESIAN_POINT('Ctrl Pts',(1.81228556199548,-2.06408158505074,
7.50358235568538));
#407926=CARTESIAN_POINT('Ctrl Pts',(1.81197580345551,-2.06429763448895,
7.5035341175365));
#407927=CARTESIAN_POINT('Ctrl Pts',(1.81151135558272,-2.06462157616947,
7.50346178989177));
#407928=CARTESIAN_POINT('Ctrl Pts',(1.81099794173556,-2.0649503159149,7.50346967198527));
#407929=CARTESIAN_POINT('Ctrl Pts',(1.81048399828363,-2.06525752798901,
7.50354272648693));
#407930=CARTESIAN_POINT('Ctrl Pts',(1.81027260270386,-2.065383890674,7.50357277531559));
#407931=CARTESIAN_POINT('Ctrl Pts',(1.81006147115137,-2.06550656502174,
7.50361331098761));
#407932=CARTESIAN_POINT('Ctrl Pts',(1.80985532470131,-2.0656235617836,7.50366116523659));
#407933=CARTESIAN_POINT('',(1.73334108842418,-2.0360810723653,7.57603338622103));
#407934=CARTESIAN_POINT('Origin',(1.73906727032635,-2.04281177295423,7.58486873427629));
#407935=CARTESIAN_POINT('Ctrl Pts',(1.80985532475557,-2.0656235617981,7.50366116529968));
#407936=CARTESIAN_POINT('Ctrl Pts',(1.78439189675399,-2.05579291414859,
7.52783573079709));
#407937=CARTESIAN_POINT('Ctrl Pts',(1.75888834908382,-2.04594589934544,
7.55196141284069));
#407938=CARTESIAN_POINT('Ctrl Pts',(1.73334108967202,-2.03608107246802,
7.57603338728831));
#407939=CARTESIAN_POINT('Ctrl Pts',(1.73480751822065,-2.02796794848293,
7.59639677331372));
#407940=CARTESIAN_POINT('Ctrl Pts',(1.71899942470746,-2.01879319534087,
7.5995988229546));
#407941=CARTESIAN_POINT('Ctrl Pts',(1.72503565868803,-2.03606376834598,
7.59642833564546));
#407942=CARTESIAN_POINT('Ctrl Pts',(1.73179248798734,-2.02549313601005,
7.58707626057424));
#407943=CARTESIAN_POINT('Ctrl Pts',(1.72505320902729,-2.02619627904982,
7.58809943920598));
#407944=CARTESIAN_POINT('Ctrl Pts',(1.72318313120985,-2.03269375623325,
7.58710240504251));
#407945=CARTESIAN_POINT('Ctrl Pts',(1.73230984781107,-2.03154771866075,
7.5801537675693));
#407946=CARTESIAN_POINT('Ctrl Pts',(1.72945965908282,-2.0314722494012,7.58205880659759));
#407947=CARTESIAN_POINT('Ctrl Pts',(1.7290422181741,-2.03425663768693,7.58020924244129));
#407948=CARTESIAN_POINT('Ctrl Pts',(1.73334108788788,-2.03608107173502,
7.57603338509286));
#407949=CARTESIAN_POINT('Ctrl Pts',(1.73334108788788,-2.03608107173502,
7.57603338509286));
#407950=CARTESIAN_POINT('Ctrl Pts',(1.73334108788788,-2.03608107173502,
7.57603338509286));
#407951=CARTESIAN_POINT('Origin',(1.73907161540585,-2.04280807393549,7.5848687342762));
#407952=CARTESIAN_POINT('Ctrl Pts',(1.74404347607193,-2.12737891132435,
7.51098857897448));
#407953=CARTESIAN_POINT('Ctrl Pts',(1.74283445470231,-2.12161707313678,
7.50433767179957));
#407954=CARTESIAN_POINT('Ctrl Pts',(1.75064586560079,-2.11799907495305,
7.50214974420965));
#407955=CARTESIAN_POINT('Ctrl Pts',(1.73757436099934,-2.09654902262137,
7.53887321589169));
#407956=CARTESIAN_POINT('Ctrl Pts',(1.73637982585136,-2.09085622148072,
7.53220407452065));
#407957=CARTESIAN_POINT('Ctrl Pts',(1.74414053150149,-2.08719912321377,
7.53003438070911));
#407958=CARTESIAN_POINT('Ctrl Pts',(1.73109282283946,-2.0656599291594,7.56669465659233));
#407959=CARTESIAN_POINT('Ctrl Pts',(1.72990534717208,-2.06000077141512,
7.56004085833302));
#407960=CARTESIAN_POINT('Ctrl Pts',(1.7376218448584,-2.05634122040663,7.55785582193789));
#407961=CARTESIAN_POINT('Ctrl Pts',(1.7245991547263,-2.03471302792851,7.59443891967696));
#407962=CARTESIAN_POINT('Ctrl Pts',(1.72340995736708,-2.02904566511006,
7.58783901202978));
#407963=CARTESIAN_POINT('Ctrl Pts',(1.73109004667147,-2.02542690755189,
7.58560008491213));
#407964=CARTESIAN_POINT('',(1.75029323173564,-2.1163295107988,7.50366116523517));
#407965=CARTESIAN_POINT('Ctrl Pts',(1.75029323173588,-2.11632951079908,
7.50366116523554));
#407966=CARTESIAN_POINT('Ctrl Pts',(1.74981871703963,-2.116920250437,7.50350835821027));
#407967=CARTESIAN_POINT('Ctrl Pts',(1.74936330376742,-2.11744784570104,
7.50345484956));
#407968=CARTESIAN_POINT('Ctrl Pts',(1.74891390668698,-2.11792837480991,
7.50349758195598));
#407969=CARTESIAN_POINT('Ctrl Pts',(1.74868333265656,-2.11817492187973,
7.50351950684424));
#407970=CARTESIAN_POINT('Ctrl Pts',(1.74843171059764,-2.11843346810347,
7.50357029184312));
#407971=CARTESIAN_POINT('Ctrl Pts',(1.74818222121564,-2.11867611166748,
7.50365515313923));
#407972=CARTESIAN_POINT('Ctrl Pts',(1.74779840551789,-2.119049395725,7.50378570417639));
#407973=CARTESIAN_POINT('Ctrl Pts',(1.74740861269544,-2.1193962493459,7.50400001621911));
#407974=CARTESIAN_POINT('Ctrl Pts',(1.74704100235903,-2.11968857580533,
7.50428903009634));
#407975=CARTESIAN_POINT('Ctrl Pts',(1.74700020043991,-2.1197210217933,7.50432110841318));
#407976=CARTESIAN_POINT('Ctrl Pts',(1.74695966296948,-2.11975282504801,
7.50435406373354));
#407977=CARTESIAN_POINT('Ctrl Pts',(1.74691942164772,-2.11978396847003,
7.50438785222352));
#407978=CARTESIAN_POINT('Ctrl Pts',(1.74667372903595,-2.11997411403089,
7.50459414719561));
#407979=CARTESIAN_POINT('Ctrl Pts',(1.74643484859307,-2.12014228251917,
7.50483629897752));
#407980=CARTESIAN_POINT('Ctrl Pts',(1.74621268932909,-2.12028310756562,
7.5050991045531));
#407981=CARTESIAN_POINT('Ctrl Pts',(1.74572258367896,-2.12059378176261,
7.50567888004914));
#407982=CARTESIAN_POINT('Ctrl Pts',(1.74529482357482,-2.12078406050335,
7.50637912803144));
#407983=CARTESIAN_POINT('Ctrl Pts',(1.74493416304265,-2.12088448585052,
7.50710440483569));
#407984=CARTESIAN_POINT('Ctrl Pts',(1.74484572192005,-2.12090911213937,
7.50728225710685));
#407985=CARTESIAN_POINT('Ctrl Pts',(1.74475959423717,-2.12092896612877,
7.50746498566954));
#407986=CARTESIAN_POINT('Ctrl Pts',(1.744677884071,-2.12094399030943,7.50764697238949));
#407987=CARTESIAN_POINT('Ctrl Pts',(1.74423863270496,-2.12102475616988,
7.50862528291182));
#407988=CARTESIAN_POINT('Ctrl Pts',(1.74388791488079,-2.12097735070584,
7.50965856837421));
#407989=CARTESIAN_POINT('Ctrl Pts',(1.74359952217746,-2.12086267149124,
7.51067959873202));
#407990=CARTESIAN_POINT('Ctrl Pts',(1.74344081930906,-2.12079956337479,
7.51124147302578));
#407991=CARTESIAN_POINT('Ctrl Pts',(1.74330111223522,-2.12071566358395,
7.51180065547253));
#407992=CARTESIAN_POINT('Ctrl Pts',(1.74317712839625,-2.12061863513827,
7.512351757165));
#407993=CARTESIAN_POINT('Ctrl Pts',(1.74274871484331,-2.1202833632069,7.51425603304535));
#407994=CARTESIAN_POINT('Ctrl Pts',(1.74246069049903,-2.11974658727156,
7.5162690050518));
#407995=CARTESIAN_POINT('Ctrl Pts',(1.74230085887296,-2.11906741666329,
7.51827788969243));
#407996=CARTESIAN_POINT('Ctrl Pts',(1.74229220848331,-2.11903065866651,
7.51838661432545));
#407997=CARTESIAN_POINT('Ctrl Pts',(1.7422839382929,-2.11899347478669,7.51849533314857));
#407998=CARTESIAN_POINT('Ctrl Pts',(1.74227604793057,-2.11895587165396,
7.51860402984325));
#407999=CARTESIAN_POINT('Ctrl Pts',(1.73334108832701,-2.0360810736146,7.57603338728985));
#408000=CARTESIAN_POINT('Ctrl Pts',(1.73900212579776,-2.06287528806226,
7.55196141284922));
#408001=CARTESIAN_POINT('Ctrl Pts',(1.74465255590614,-2.08962350828569,
7.52783573083105));
#408002=CARTESIAN_POINT('Ctrl Pts',(1.7502932317425,-2.11632951085758,7.50366116530176));
#408003=CARTESIAN_POINT('Origin',(5.98949470795639E-16,-7.03560129586911E-16,
7.49482233047033));
#408004=CARTESIAN_POINT('Origin',(1.80403047455415,-2.05897554547885,7.49482233047033));
#408005=CARTESIAN_POINT('Origin',(0.,0.,7.50366116523517));
#408006=CARTESIAN_POINT('Origin',(1.74466007661673,-2.10951830213907,7.49482233047033));
#408007=CARTESIAN_POINT('Ctrl Pts',(1.81372657476301,-2.0581279312074,7.51860402984325));
#408008=CARTESIAN_POINT('Ctrl Pts',(1.82082828860748,-2.06085958757331,
7.51860402984325));
#408009=CARTESIAN_POINT('Ctrl Pts',(1.82651648716082,-2.05580580846774,
7.51860402984325));
#408010=CARTESIAN_POINT('Ctrl Pts',(1.81636349003428,-2.05914221267183,
7.51041458714366));
#408011=CARTESIAN_POINT('Ctrl Pts',(1.82217588142129,-2.0596622820176,7.51004642900441));
#408012=CARTESIAN_POINT('Ctrl Pts',(1.82651805589845,-2.05580441469547,
7.5072913648301));
#408013=CARTESIAN_POINT('Ctrl Pts',(1.81632127355298,-2.06195680944011,
7.50215815450138));
#408014=CARTESIAN_POINT('Ctrl Pts',(1.81943214123463,-2.06210022055771,
7.49877163671531));
#408015=CARTESIAN_POINT('Ctrl Pts',(1.82202718038203,-2.05982652413606,
7.49481588533171));
#408016=CARTESIAN_POINT('Ctrl Pts',(1.80985496190503,-2.06562314771777,
7.50366171572174));
#408017=CARTESIAN_POINT('Ctrl Pts',(1.81226805662945,-2.06837726029865,
7.50000045605858));
#408018=CARTESIAN_POINT('Ctrl Pts',(1.81226805662954,-2.06837726029857,
7.49482233047317));
#408019=CARTESIAN_POINT('Origin',(1.81821413949191,-2.04646123661107,7.51860402984325));
#408020=CARTESIAN_POINT('Origin',(1.81821413949191,-2.04646123661107,9.));
#408021=CARTESIAN_POINT('Origin',(1.81821413949191,-2.04646123661107,8.75721825406948));
#408022=CARTESIAN_POINT('Ctrl Pts',(1.79814021121717,-2.05213415732287,
8.78942910404913));
#408023=CARTESIAN_POINT('Ctrl Pts',(1.80333407793184,-2.05415311181764,
8.79672699501691));
#408024=CARTESIAN_POINT('Ctrl Pts',(1.8080408387174,-2.04656892505244,8.79893251111267));
#408025=CARTESIAN_POINT('Ctrl Pts',(1.80840194814797,-2.05608031670936,
8.78111911759583));
#408026=CARTESIAN_POINT('Ctrl Pts',(1.81456203428848,-2.05846687256808,
8.78644465894813));
#408027=CARTESIAN_POINT('Ctrl Pts',(1.82021442763375,-2.05265602398582,
8.78817647674133));
#408028=CARTESIAN_POINT('Ctrl Pts',(1.8147973073802,-2.0585396573341,8.7678092393203));
#408029=CARTESIAN_POINT('Ctrl Pts',(1.82207086986224,-2.06135213410561,
8.76988516158373));
#408030=CARTESIAN_POINT('Ctrl Pts',(1.82782283886928,-2.05644792846776,
8.77093053738832));
#408031=CARTESIAN_POINT('Ctrl Pts',(1.81355029985717,-2.0580601195691,8.75371302330492));
#408032=CARTESIAN_POINT('Ctrl Pts',(1.82064507138233,-2.06080428034673,
8.75300828287559));
#408033=CARTESIAN_POINT('Ctrl Pts',(1.82633909376226,-2.05570794357694,
8.75267964240738));
#408034=CARTESIAN_POINT('Origin',(1.8051259398375,-2.0414281648459,8.78727029226991));
#408035=CARTESIAN_POINT('Ctrl Pts',(1.73391074180931,-2.02743472471359,
8.85049129520029));
#408036=CARTESIAN_POINT('Ctrl Pts',(1.73936124027705,-2.02953071581002,
8.85711686593484));
#408037=CARTESIAN_POINT('Ctrl Pts',(1.74416981443408,-2.0224611771624,8.85933012996512));
#408038=CARTESIAN_POINT('Ctrl Pts',(1.75618597738197,-2.03600067436163,
8.82945683644721));
#408039=CARTESIAN_POINT('Ctrl Pts',(1.76168171828244,-2.0381140634514,8.83607469902389));
#408040=CARTESIAN_POINT('Ctrl Pts',(1.76647340116635,-2.03100267697354,
8.8382956714852));
#408041=CARTESIAN_POINT('Ctrl Pts',(1.77842800991976,-2.04455385577097,
8.80838214965003));
#408042=CARTESIAN_POINT('Ctrl Pts',(1.78394543957975,-2.04667558528086,
8.81501364461993));
#408043=CARTESIAN_POINT('Ctrl Pts',(1.78874291541953,-2.03953184409282,
8.8172209842872));
#408044=CARTESIAN_POINT('Ctrl Pts',(1.80063936233261,-2.05309523912752,
8.78727029226991));
#408045=CARTESIAN_POINT('Ctrl Pts',(1.80615770845576,-2.05521732106363,
8.79393457792714));
#408046=CARTESIAN_POINT('Ctrl Pts',(1.81098095093023,-2.04804963334647,
8.79610912703474));
#408047=CARTESIAN_POINT('Origin',(1.7383973193142,-2.01576765043198,8.85049129520029));
#408048=CARTESIAN_POINT('Ctrl Pts',(1.72471465490916,-2.03526346763208,
8.85049129520029));
#408049=CARTESIAN_POINT('Ctrl Pts',(1.72591388015444,-2.04097862038893,
8.85711686593484));
#408050=CARTESIAN_POINT('Ctrl Pts',(1.71816751245364,-2.04459725957486,
8.85933012996512));
#408051=CARTESIAN_POINT('Ctrl Pts',(1.72365371764567,-2.0302073544872,8.86332496987231));
#408052=CARTESIAN_POINT('Ctrl Pts',(1.72032477139737,-2.03341204031464,
8.86648636486737));
#408053=CARTESIAN_POINT('Ctrl Pts',(1.71521626468802,-2.03044905852375,
8.87206031107457));
#408054=CARTESIAN_POINT('Ctrl Pts',(1.72905599763766,-2.02556783114055,
8.86341338519877));
#408055=CARTESIAN_POINT('Ctrl Pts',(1.732743554524,-2.0227615177503,8.86654584966058));
#408056=CARTESIAN_POINT('Ctrl Pts',(1.73057098474445,-2.01724752705931,
8.87215952290714));
#408057=CARTESIAN_POINT('Ctrl Pts',(1.73391074180931,-2.02743472471359,
8.85049129520029));
#408058=CARTESIAN_POINT('Ctrl Pts',(1.73936124027705,-2.02953071581002,
8.85711686593484));
#408059=CARTESIAN_POINT('Ctrl Pts',(1.74416981443408,-2.0224611771624,8.85933012996512));
#408060=CARTESIAN_POINT('Origin',(1.71248107441377,-2.03783047138408,8.85049129520029));
#408061=CARTESIAN_POINT('Ctrl Pts',(1.7393963664604,-2.10523216165202,8.78727029226991));
#408062=CARTESIAN_POINT('Ctrl Pts',(1.74061051962863,-2.11101845647362,
8.79393457792714));
#408063=CARTESIAN_POINT('Ctrl Pts',(1.7327649198924,-2.11463591137412,8.79610912703474));
#408064=CARTESIAN_POINT('Ctrl Pts',(1.7345093979193,-2.0819423152779,8.80838214965003));
#408065=CARTESIAN_POINT('Ctrl Pts',(1.73572334944618,-2.08772764913654,
8.81501364461988));
#408066=CARTESIAN_POINT('Ctrl Pts',(1.72790550163947,-2.09132348954823,
8.81722098428722));
#408067=CARTESIAN_POINT('Ctrl Pts',(1.72961567910012,-2.05862029907537,
8.82945683644722));
#408068=CARTESIAN_POINT('Ctrl Pts',(1.73082485863999,-2.06438289105554,
8.83607469902389));
#408069=CARTESIAN_POINT('Ctrl Pts',(1.72303987536893,-2.06797817657504,
8.83829567148518));
#408070=CARTESIAN_POINT('Ctrl Pts',(1.72471465490916,-2.03526346763208,
8.85049129520029));
#408071=CARTESIAN_POINT('Ctrl Pts',(1.72591388015444,-2.04097862038893,
8.85711686593484));
#408072=CARTESIAN_POINT('Ctrl Pts',(1.71816751245364,-2.04459725957486,
8.85933012996512));
#408073=CARTESIAN_POINT('Origin',(1.72716278596501,-2.10779916540403,8.78727029226991));
#408074=CARTESIAN_POINT('Ctrl Pts',(1.74223800513146,-2.11877466075527,
8.75374538247848));
#408075=CARTESIAN_POINT('Ctrl Pts',(1.74381137292058,-2.12620896584639,
8.75304829418602));
#408076=CARTESIAN_POINT('Ctrl Pts',(1.73788145903659,-2.13101591545477,
8.75272238421917));
#408077=CARTESIAN_POINT('Ctrl Pts',(1.74250907779356,-2.12006651079531,
8.76769408445017));
#408078=CARTESIAN_POINT('Ctrl Pts',(1.7441213633446,-2.12768803887529,8.76974318093967));
#408079=CARTESIAN_POINT('Ctrl Pts',(1.73837008844154,-2.13258101284513,
8.7707786988043));
#408080=CARTESIAN_POINT('Ctrl Pts',(1.74111971376202,-2.11344522340546,
8.78108014887993));
#408081=CARTESIAN_POINT('Ctrl Pts',(1.74248978482015,-2.11990340756171,
8.78639403366328));
#408082=CARTESIAN_POINT('Ctrl Pts',(1.73587245745552,-2.12456527996217,
8.78812224174742));
#408083=CARTESIAN_POINT('Ctrl Pts',(1.73884285278516,-2.10259439504486,
8.78944554828685));
#408084=CARTESIAN_POINT('Ctrl Pts',(1.74000297373834,-2.10803595153092,
8.79673892988685));
#408085=CARTESIAN_POINT('Ctrl Pts',(1.73177459439527,-2.11147067534851,
8.79894799272499));
#408086=CARTESIAN_POINT('Origin',(1.73004246743518,-2.12152287540597,8.75721825406948));
#408087=CARTESIAN_POINT('Origin',(1.73004246743518,-2.12152287540597,9.));
#408088=CARTESIAN_POINT('Origin',(1.73004246743518,-2.12152287540597,7.51860402984325));
#408089=CARTESIAN_POINT('Ctrl Pts',(1.75029273038004,-2.11632890459551,
7.50366195182966));
#408090=CARTESIAN_POINT('Ctrl Pts',(1.75262656098474,-2.1191508058019,7.50000065167735));
#408091=CARTESIAN_POINT('Ctrl Pts',(1.75262656098465,-2.11915080580197,
7.49482233047108));
#408092=CARTESIAN_POINT('Ctrl Pts',(1.74563652264445,-2.12213179431785,
7.50215800491337));
#408093=CARTESIAN_POINT('Ctrl Pts',(1.74528013450683,-2.12522657777872,
7.49877273257269));
#408094=CARTESIAN_POINT('Ctrl Pts',(1.74261994224621,-2.12742669902232,
7.49481816995647));
#408095=CARTESIAN_POINT('Ctrl Pts',(1.74285520534903,-2.1217143132473,7.51043025814041));
#408096=CARTESIAN_POINT('Ctrl Pts',(1.74244442792581,-2.1275387461721,7.51006209594511));
#408097=CARTESIAN_POINT('Ctrl Pts',(1.73794024257006,-2.13121179455772,
7.50731281821699));
#408098=CARTESIAN_POINT('Ctrl Pts',(1.74227573745806,-2.11895439247877,
7.51860402984325));
#408099=CARTESIAN_POINT('Ctrl Pts',(1.74383928023547,-2.12640129461145,
7.51860402984325));
#408100=CARTESIAN_POINT('Ctrl Pts',(1.7379422047294,-2.13121019447175,7.51860402984325));
#408101=CARTESIAN_POINT('Origin',(0.,0.,7.5));
#408102=CARTESIAN_POINT('Origin',(1.85157082176548,-1.92057895321252,7.5));
#408103=CARTESIAN_POINT('',(1.85157082176548,-1.92057895321252,7.59394543036555));
#408104=CARTESIAN_POINT('',(1.85157082176548,-1.92057895321252,8.85049129520029));
#408105=CARTESIAN_POINT('',(1.85157082176548,-1.92057895321252,7.5));
#408106=CARTESIAN_POINT('',(1.87070527778335,-1.98946322855769,8.78727029226991));
#408107=CARTESIAN_POINT('Ctrl Pts',(1.85157082176548,-1.92057895321252,
8.85049129520029));
#408108=CARTESIAN_POINT('Ctrl Pts',(1.85795824503307,-1.94357375498267,
8.82945686509571));
#408109=CARTESIAN_POINT('Ctrl Pts',(1.86433617262361,-1.9665343721995,8.80838212259895));
#408110=CARTESIAN_POINT('Ctrl Pts',(1.87070527778335,-1.98946322855769,
8.78727029226991));
#408111=CARTESIAN_POINT('',(1.87445832375787,-2.0029742399003,8.75721825406948));
#408112=CARTESIAN_POINT('Origin',(1.86316430091954,-1.96231486575488,8.75937679713047));
#408113=CARTESIAN_POINT('',(1.87445832375787,-2.0029742399003,7.51860402984325));
#408114=CARTESIAN_POINT('',(1.87445832375787,-2.0029742399003,7.5));
#408115=CARTESIAN_POINT('Ctrl Pts',(1.87445832375787,-2.0029742399003,7.51860402984325));
#408116=CARTESIAN_POINT('Ctrl Pts',(1.87151088985394,-1.99236344185042,
7.52834476460825));
#408117=CARTESIAN_POINT('Ctrl Pts',(1.86856154251846,-1.98174575542356,
7.53807742314407));
#408118=CARTESIAN_POINT('Ctrl Pts',(1.86561021750541,-1.97112094933329,
7.54780169004674));
#408119=CARTESIAN_POINT('Ctrl Pts',(1.86093547819024,-1.95429183070808,
7.5632044032688));
#408120=CARTESIAN_POINT('Ctrl Pts',(1.856255771193,-1.93744482836684,7.57858609112103));
#408121=CARTESIAN_POINT('Ctrl Pts',(1.85157082176548,-1.92057895321252,
7.59394543036555));
#408122=CARTESIAN_POINT('Origin',(2.12271872378388,-1.99423374133347,7.5));
#408123=CARTESIAN_POINT('',(1.94186579781668,-1.9376937416628,8.75721825406948));
#408124=CARTESIAN_POINT('',(1.92848201925699,-1.93350957471437,8.78727029226991));
#408125=CARTESIAN_POINT('Origin',(1.89450899737204,-1.92288859838283,8.75658640621046));
#408126=CARTESIAN_POINT('',(1.86024642503786,-1.91217709997533,8.85049129520029));
#408127=CARTESIAN_POINT('Ctrl Pts',(1.92848201925699,-1.93350957471437,
8.78727029226991));
#408128=CARTESIAN_POINT('Ctrl Pts',(1.90576908324183,-1.92640883587949,
8.80838212259896));
#408129=CARTESIAN_POINT('Ctrl Pts',(1.88302468545905,-1.919298261161,8.82945686509571));
#408130=CARTESIAN_POINT('Ctrl Pts',(1.86024642503786,-1.91217709997533,
8.85049129520029));
#408131=CARTESIAN_POINT('',(1.86024642503786,-1.91217709997533,7.59394543036555));
#408132=CARTESIAN_POINT('',(1.86024642503786,-1.91217709997533,7.5));
#408133=CARTESIAN_POINT('',(1.94186579781668,-1.9376937416628,7.51860402984325));
#408134=CARTESIAN_POINT('Ctrl Pts',(1.86024642503786,-1.91217709997533,
7.59394543036555));
#408135=CARTESIAN_POINT('Ctrl Pts',(1.87695347475877,-1.91740022025755,
7.57858609112103));
#408136=CARTESIAN_POINT('Ctrl Pts',(1.8936418293911,-1.92261749589947,7.56320440326857));
#408137=CARTESIAN_POINT('Ctrl Pts',(1.91031246871802,-1.9278292332104,7.54780169004651));
#408138=CARTESIAN_POINT('Ctrl Pts',(1.92083722133245,-1.93111958367706,
7.53807742314383));
#408139=CARTESIAN_POINT('Ctrl Pts',(1.93135492132934,-1.93440772928586,
7.52834476460825));
#408140=CARTESIAN_POINT('Ctrl Pts',(1.94186579781668,-1.93769374166279,
7.51860402984324));
#408141=CARTESIAN_POINT('',(1.94186579781668,-1.9376937416628,7.5));
#408142=CARTESIAN_POINT('Origin',(1.85819500900391,-1.91873890744398,7.5));
#408143=CARTESIAN_POINT('Ctrl Pts',(1.86024642503786,-1.91217709997533,
8.85049129520029));
#408144=CARTESIAN_POINT('Ctrl Pts',(1.86006158583555,-1.9121193137472,8.85097269580138));
#408145=CARTESIAN_POINT('Ctrl Pts',(1.8598765688591,-1.91207028482753,8.85143669361005));
#408146=CARTESIAN_POINT('Ctrl Pts',(1.85968263072174,-1.9120286007086,8.8519052845931));
#408147=CARTESIAN_POINT('Ctrl Pts',(1.85930330002419,-1.91194706921549,
8.85282181883899));
#408148=CARTESIAN_POINT('Ctrl Pts',(1.85889955648231,-1.91189592644373,
8.85372622499635));
#408149=CARTESIAN_POINT('Ctrl Pts',(1.85846312703678,-1.91188966638124,
8.8546225773507));
#408150=CARTESIAN_POINT('Ctrl Pts',(1.85810081881161,-1.91188446949969,
8.85536669723986));
#408151=CARTESIAN_POINT('Ctrl Pts',(1.85771590218179,-1.91191017178598,
8.85610498449051));
#408152=CARTESIAN_POINT('Ctrl Pts',(1.85730414434205,-1.9119830527008,8.85681338218371));
#408153=CARTESIAN_POINT('Ctrl Pts',(1.8569304734558,-1.91204919224547,8.85745625420285));
#408154=CARTESIAN_POINT('Ctrl Pts',(1.85652990561897,-1.91215442650102,
8.85808743050666));
#408155=CARTESIAN_POINT('Ctrl Pts',(1.85609705491235,-1.91232684172784,
8.85866804508411));
#408156=CARTESIAN_POINT('Ctrl Pts',(1.85589734697936,-1.91240639037599,
8.85893592806396));
#408157=CARTESIAN_POINT('Ctrl Pts',(1.85569075007651,-1.91250048161007,
8.85919241173848));
#408158=CARTESIAN_POINT('Ctrl Pts',(1.85547684726748,-1.91261346607838,
8.85943017985534));
#408159=CARTESIAN_POINT('Ctrl Pts',(1.85518801515329,-1.91276602855758,
8.8597512372));
#408160=CARTESIAN_POINT('Ctrl Pts',(1.85487880982735,-1.91295748856581,
8.86004599534706));
#408161=CARTESIAN_POINT('Ctrl Pts',(1.85455842928457,-1.91319440076879,
8.86026130871721));
#408162=CARTESIAN_POINT('Ctrl Pts',(1.85444112893538,-1.91328114100556,
8.86034014101236));
#408163=CARTESIAN_POINT('Ctrl Pts',(1.8543205612428,-1.9133752671255,8.86040910639693));
#408164=CARTESIAN_POINT('Ctrl Pts',(1.85420021800344,-1.91347447986182,
8.86046313645507));
#408165=CARTESIAN_POINT('Ctrl Pts',(1.8540124233863,-1.91362930050593,8.8605474499083));
#408166=CARTESIAN_POINT('Ctrl Pts',(1.85382014264965,-1.91380084733626,
8.86059655985668));
#408167=CARTESIAN_POINT('Ctrl Pts',(1.85363551231204,-1.91397789992958,
8.86059725258816));
#408168=CARTESIAN_POINT('Ctrl Pts',(1.85345045540458,-1.91415536158512,
8.86059794692011));
#408169=CARTESIAN_POINT('Ctrl Pts',(1.85327287084369,-1.91434224010241,
8.86056369958366));
#408170=CARTESIAN_POINT('Ctrl Pts',(1.85310971629741,-1.91452575082091,
8.86048590497774));
#408171=CARTESIAN_POINT('Ctrl Pts',(1.85306713781853,-1.91457364165467,
8.86046560290182));
#408172=CARTESIAN_POINT('Ctrl Pts',(1.85302505587403,-1.91462198633973,
8.86044257503091));
#408173=CARTESIAN_POINT('Ctrl Pts',(1.85298474607094,-1.9146692694329,8.86041778462584));
#408174=CARTESIAN_POINT('Ctrl Pts',(1.85271351111646,-1.91498742597651,
8.86025097596201));
#408175=CARTESIAN_POINT('Ctrl Pts',(1.85248636841559,-1.91530042537852,
8.8599848982295));
#408176=CARTESIAN_POINT('Ctrl Pts',(1.85230309052328,-1.91559415580071,
8.85968173251461));
#408177=CARTESIAN_POINT('Ctrl Pts',(1.85220614701882,-1.9157495223653,8.85952137522076));
#408178=CARTESIAN_POINT('Ctrl Pts',(1.85211944536219,-1.91590239156238,
8.85934740853961));
#408179=CARTESIAN_POINT('Ctrl Pts',(1.85204285603105,-1.91604984067722,
8.8591675900182));
#408180=CARTESIAN_POINT('Ctrl Pts',(1.85173531005616,-1.91664192551581,
8.85844552518695));
#408181=CARTESIAN_POINT('Ctrl Pts',(1.85157075220592,-1.91717868325238,
8.85759444184125));
#408182=CARTESIAN_POINT('Ctrl Pts',(1.85147589005126,-1.91762837806792,
8.85683498915139));
#408183=CARTESIAN_POINT('Ctrl Pts',(1.85146596297942,-1.91767543743273,
8.85675551444998));
#408184=CARTESIAN_POINT('Ctrl Pts',(1.85145681911714,-1.91772154358245,
8.85667699793651));
#408185=CARTESIAN_POINT('Ctrl Pts',(1.8514483875945,-1.91776665961245,8.85659965593547));
#408186=CARTESIAN_POINT('Ctrl Pts',(1.85133457847175,-1.91837563808756,
8.85555568965886));
#408187=CARTESIAN_POINT('Ctrl Pts',(1.85131314939549,-1.91897734042079,
8.85434650606346));
#408188=CARTESIAN_POINT('Ctrl Pts',(1.85137778363236,-1.91957451989692,
8.85297329937117));
#408189=CARTESIAN_POINT('Ctrl Pts',(1.85141413645238,-1.91991039696556,
8.85220095427747));
#408190=CARTESIAN_POINT('Ctrl Pts',(1.85147804246511,-1.92024494659809,
8.85137579139183));
#408191=CARTESIAN_POINT('Ctrl Pts',(1.85157082176548,-1.92057895321252,
8.85049129520029));
#408192=CARTESIAN_POINT('Origin',(1.85819500900391,-1.91873890744398,7.59394543036555));
#408193=CARTESIAN_POINT('Ctrl Pts',(1.85970977447863,-1.91200932706107,
7.59443877723642));
#408194=CARTESIAN_POINT('Ctrl Pts',(1.85418279006983,-1.91028142747093,
7.58783886950016));
#408195=CARTESIAN_POINT('Ctrl Pts',(1.84984328894465,-1.91757854412898,
7.58559994247159));
#408196=CARTESIAN_POINT('Ctrl Pts',(1.88988142021141,-1.92144188022918,
7.56670252222134));
#408197=CARTESIAN_POINT('Ctrl Pts',(1.88436242386425,-1.9197164779445,7.56004874999027));
#408198=CARTESIAN_POINT('Ctrl Pts',(1.87997884594833,-1.92704591188663,
7.55786368756704));
#408199=CARTESIAN_POINT('Ctrl Pts',(1.91999672341034,-1.9308568190467,7.53888913333558));
#408200=CARTESIAN_POINT('Ctrl Pts',(1.91444492739765,-1.92912116261176,
7.53222002137278));
#408201=CARTESIAN_POINT('Ctrl Pts',(1.9100595450782,-1.93649482293976,7.53005029815326));
#408202=CARTESIAN_POINT('Ctrl Pts',(1.95005432133752,-1.94025371748124,
7.51101258149734));
#408203=CARTESIAN_POINT('Ctrl Pts',(1.94443522746928,-1.93849702173656,
7.5043616886572));
#408204=CARTESIAN_POINT('Ctrl Pts',(1.94008387535393,-1.94592488928472,
7.50217374673251));
#408205=CARTESIAN_POINT('',(1.93848173883016,-1.9454216878506,7.50366116523517));
#408206=CARTESIAN_POINT('Ctrl Pts',(1.94186579781668,-1.93769374166279,
7.51860402984325));
#408207=CARTESIAN_POINT('Ctrl Pts',(1.94228729131094,-1.93782551305604,
7.51734760759494));
#408208=CARTESIAN_POINT('Ctrl Pts',(1.94265041783264,-1.93800137376573,
7.51608817408573));
#408209=CARTESIAN_POINT('Ctrl Pts',(1.94294852171252,-1.93823293770863,
7.5148100591312));
#408210=CARTESIAN_POINT('Ctrl Pts',(1.94321855133035,-1.93844269386152,
7.51365231206384));
#408211=CARTESIAN_POINT('Ctrl Pts',(1.94343576286587,-1.93869825356333,
7.51247773061043));
#408212=CARTESIAN_POINT('Ctrl Pts',(1.94356826237055,-1.93901910824856,
7.51129758471022));
#408213=CARTESIAN_POINT('Ctrl Pts',(1.94373294412285,-1.93941789397931,
7.50983079813402));
#408214=CARTESIAN_POINT('Ctrl Pts',(1.94374947141059,-1.93990978941467,
7.50839324291155));
#408215=CARTESIAN_POINT('Ctrl Pts',(1.94353557175022,-1.94050115292895,
7.50715379678855));
#408216=CARTESIAN_POINT('Ctrl Pts',(1.94343675627051,-1.94077434583282,
7.50658120839351));
#408217=CARTESIAN_POINT('Ctrl Pts',(1.94326578097651,-1.94110437188969,
7.50598221009429));
#408218=CARTESIAN_POINT('Ctrl Pts',(1.94300651780458,-1.94147291354816,
7.50545747549611));
#408219=CARTESIAN_POINT('Ctrl Pts',(1.9428681669511,-1.94166957878455,7.50517746087247));
#408220=CARTESIAN_POINT('Ctrl Pts',(1.94270334047091,-1.94187946086699,
7.50491486231392));
#408221=CARTESIAN_POINT('Ctrl Pts',(1.94251509140964,-1.94209597154046,
7.50468370960992));
#408222=CARTESIAN_POINT('Ctrl Pts',(1.94223359968323,-1.94241972329172,
7.50433806340447));
#408223=CARTESIAN_POINT('Ctrl Pts',(1.94189087484744,-1.94276763919195,
7.50405484070984));
#408224=CARTESIAN_POINT('Ctrl Pts',(1.9415094884218,-1.94311578500609,7.50385766036131));
#408225=CARTESIAN_POINT('Ctrl Pts',(1.94146870507166,-1.94315301378951,
7.50383657498791));
#408226=CARTESIAN_POINT('Ctrl Pts',(1.94142750738743,-1.94319023939013,
7.50381643264937));
#408227=CARTESIAN_POINT('Ctrl Pts',(1.94138594320287,-1.94322742863343,
7.50379723213559));
#408228=CARTESIAN_POINT('Ctrl Pts',(1.94110848867435,-1.94347567899792,
7.50366906242519));
#408229=CARTESIAN_POINT('Ctrl Pts',(1.94080818815368,-1.94372717343727,
7.50358235568538));
#408230=CARTESIAN_POINT('Ctrl Pts',(1.94051290838089,-1.94396262527654,
7.5035341175365));
#408231=CARTESIAN_POINT('Ctrl Pts',(1.9400701697808,-1.94431565866151,7.50346178989176));
#408232=CARTESIAN_POINT('Ctrl Pts',(1.93957887322525,-1.94467661751401,
7.50346967198527));
#408233=CARTESIAN_POINT('Ctrl Pts',(1.93908566887044,-1.94501612685798,
7.50354272648692));
#408234=CARTESIAN_POINT('Ctrl Pts',(1.93888280371058,-1.94515577407859,
7.50357277531559));
#408235=CARTESIAN_POINT('Ctrl Pts',(1.93867996572295,-1.94529172362374,
7.50361331098761));
#408236=CARTESIAN_POINT('Ctrl Pts',(1.93848173883116,-1.9454216878516,7.50366116523658));
#408237=CARTESIAN_POINT('',(1.86023191546278,-1.92084218059617,7.57603338622103));
#408238=CARTESIAN_POINT('Origin',(1.8663775697776,-1.92719217450502,7.58486873427627));
#408239=CARTESIAN_POINT('Ctrl Pts',(1.93848173888624,-1.9454216878626,7.50366116529968));
#408240=CARTESIAN_POINT('Ctrl Pts',(1.91244077647096,-1.93724268576655,
7.52783573079709));
#408241=CARTESIAN_POINT('Ctrl Pts',(1.88635872817014,-1.92904992062092,
7.55196141284068));
#408242=CARTESIAN_POINT('Ctrl Pts',(1.86023191671463,-1.92084218061873,
7.57603338728831));
#408243=CARTESIAN_POINT('Ctrl Pts',(1.8611755226901,-1.91265177151731,7.59639677331372));
#408244=CARTESIAN_POINT('Ctrl Pts',(1.84481208014828,-1.9045086969183,7.59959882295463));
#408245=CARTESIAN_POINT('Ctrl Pts',(1.85194244145045,-1.92135704284004,
7.59642833564546));
#408246=CARTESIAN_POINT('Ctrl Pts',(1.85800812538024,-1.91037521746235,
7.58707626057423));
#408247=CARTESIAN_POINT('Ctrl Pts',(1.85132774352081,-1.9115087029048,7.58809943920598));
#408248=CARTESIAN_POINT('Ctrl Pts',(1.84987780277126,-1.91811264662167,
7.58710240504252));
#408249=CARTESIAN_POINT('Ctrl Pts',(1.85891234067499,-1.91638421296595,
7.5801537675693));
#408250=CARTESIAN_POINT('Ctrl Pts',(1.85606317263307,-1.91649151098492,
7.5820588065976));
#408251=CARTESIAN_POINT('Ctrl Pts',(1.85582498577148,-1.91929692397712,
7.58020924244128));
#408252=CARTESIAN_POINT('Ctrl Pts',(1.86023191488719,-1.92084218000155,
7.57603338509286));
#408253=CARTESIAN_POINT('Ctrl Pts',(1.86023191488719,-1.92084218000155,
7.57603338509286));
#408254=CARTESIAN_POINT('Ctrl Pts',(1.86023191488719,-1.92084218000155,
7.57603338509286));
#408255=CARTESIAN_POINT('Origin',(1.86638166893217,-1.9271882046956,7.58486873427621));
#408256=CARTESIAN_POINT('Ctrl Pts',(1.87676178653315,-2.0112667340225,7.51098857897448));
#408257=CARTESIAN_POINT('Ctrl Pts',(1.87518608698743,-2.00559419641456,
7.50433767179956));
#408258=CARTESIAN_POINT('Ctrl Pts',(1.88274964256493,-2.0014831529815,7.50214974420965));
#408259=CARTESIAN_POINT('Ctrl Pts',(1.86833068520011,-1.98091466625817,
7.53887321589171));
#408260=CARTESIAN_POINT('Ctrl Pts',(1.86677386533131,-1.97531009571771,
7.53220407452065));
#408261=CARTESIAN_POINT('Ctrl Pts',(1.87428431468889,-1.97116328123316,
7.53003438070911));
#408262=CARTESIAN_POINT('Ctrl Pts',(1.85988339304239,-1.95050431132724,
7.56669465659232));
#408263=CARTESIAN_POINT('Ctrl Pts',(1.85833577368955,-1.94493286275669,
7.56004085833297));
#408264=CARTESIAN_POINT('Ctrl Pts',(1.86580194876566,-1.94078643298402,
7.55785582193789));
#408265=CARTESIAN_POINT('Ctrl Pts',(1.85142029209724,-1.92003704456848,
7.59443891967696));
#408266=CARTESIAN_POINT('Ctrl Pts',(1.84987042888904,-1.91445751809117,
7.58783901202978));
#408267=CARTESIAN_POINT('Ctrl Pts',(1.85730288403347,-1.9103541306473,7.58560008491213));
#408268=CARTESIAN_POINT('',(1.88229076388123,-1.99983961245518,7.50366116523517));
#408269=CARTESIAN_POINT('Ctrl Pts',(1.88229076388149,-1.99983961245545,
7.50366116523554));
#408270=CARTESIAN_POINT('Ctrl Pts',(1.88185507294513,-2.0004595406164,7.50350835821027));
#408271=CARTESIAN_POINT('Ctrl Pts',(1.88143439851296,-2.00101523030791,
7.50345484956));
#408272=CARTESIAN_POINT('Ctrl Pts',(1.88101671237273,-2.001523565088,7.50349758195598));
#408273=CARTESIAN_POINT('Ctrl Pts',(1.88080240840638,-2.00178437852927,
7.50351950684424));
#408274=CARTESIAN_POINT('Ctrl Pts',(1.8805678684454,-2.00205851502273,7.50357029184312));
#408275=CARTESIAN_POINT('Ctrl Pts',(1.88033443789261,-2.0023166448891,7.50365515313923));
#408276=CARTESIAN_POINT('Ctrl Pts',(1.87997532717706,-2.00271375315068,
7.50378570417639));
#408277=CARTESIAN_POINT('Ctrl Pts',(1.87960855821356,-2.00308486823549,
7.50400001621911));
#408278=CARTESIAN_POINT('Ctrl Pts',(1.87926043259258,-2.00340014695398,
7.50428903009634));
#408279=CARTESIAN_POINT('Ctrl Pts',(1.87922179332696,-2.00343514046613,
7.50432110841318));
#408280=CARTESIAN_POINT('Ctrl Pts',(1.87918337678663,-2.00346947562229,
7.50435406373354));
#408281=CARTESIAN_POINT('Ctrl Pts',(1.87914521351089,-2.00350313332715,
7.50438785222352));
#408282=CARTESIAN_POINT('Ctrl Pts',(1.87891220836886,-2.00370862979324,
7.50459414719561));
#408283=CARTESIAN_POINT('Ctrl Pts',(1.8786845933235,-2.00389175788385,7.50483629897752));
#408284=CARTESIAN_POINT('Ctrl Pts',(1.87847191320126,-2.00404652738305,
7.5050991045531));
#408285=CARTESIAN_POINT('Ctrl Pts',(1.8780027194899,-2.0043879644434,7.50567888004914));
#408286=CARTESIAN_POINT('Ctrl Pts',(1.87758802946555,-2.00460525892003,
7.50637912803145));
#408287=CARTESIAN_POINT('Ctrl Pts',(1.87723454422321,-2.00472858553219,
7.50710440483569));
#408288=CARTESIAN_POINT('Ctrl Pts',(1.87714786262412,-2.00475882766586,
7.50728225710685));
#408289=CARTESIAN_POINT('Ctrl Pts',(1.87706318394926,-2.00478415908271,
7.50746498566954));
#408290=CARTESIAN_POINT('Ctrl Pts',(1.87698260426796,-2.0048043875829,7.50764697238949));
#408291=CARTESIAN_POINT('Ctrl Pts',(1.87654943007741,-2.00491313043287,
7.50862528291181));
#408292=CARTESIAN_POINT('Ctrl Pts',(1.87619639556211,-2.00488829293659,
7.5096585683742));
#408293=CARTESIAN_POINT('Ctrl Pts',(1.87590124787002,-2.00479232672667,
7.510679598732));
#408294=CARTESIAN_POINT('Ctrl Pts',(1.87573882772278,-2.00473951640031,
7.51124147302577));
#408295=CARTESIAN_POINT('Ctrl Pts',(1.87559403221404,-2.00466474005354,
7.51180065547252));
#408296=CARTESIAN_POINT('Ctrl Pts',(1.87546408647931,-2.00457585463505,
7.51235175716501));
#408297=CARTESIAN_POINT('Ctrl Pts',(1.87501507220157,-2.0042687201064,7.51425603304536));
#408298=CARTESIAN_POINT('Ctrl Pts',(1.87469324828193,-2.00375150081788,
7.51626900505181));
#408299=CARTESIAN_POINT('Ctrl Pts',(1.8744902304368,-2.0030839660859,7.51827788969245));
#408300=CARTESIAN_POINT('Ctrl Pts',(1.87447924272737,-2.00304783784474,
7.51838661432546));
#408301=CARTESIAN_POINT('Ctrl Pts',(1.87446860714959,-2.00301126023611,
7.51849533314857));
#408302=CARTESIAN_POINT('Ctrl Pts',(1.87445832375787,-2.00297423990031,
7.51860402984325));
#408303=CARTESIAN_POINT('Ctrl Pts',(1.86023191544585,-1.92084218184913,
7.57603338728984));
#408304=CARTESIAN_POINT('Ctrl Pts',(1.86759803292184,-1.94721864079347,
7.55196141284921));
#408305=CARTESIAN_POINT('Ctrl Pts',(1.87495061796935,-1.97354987962968,
7.52783573083105));
#408306=CARTESIAN_POINT('Ctrl Pts',(1.88229076389185,-1.9998396125134,7.50366116530176));
#408307=CARTESIAN_POINT('Origin',(6.42796117143052E-16,-6.6373976549288E-16,
7.49482233047033));
#408308=CARTESIAN_POINT('Origin',(1.93224291659625,-1.93916053003964,7.49482233047033));
#408309=CARTESIAN_POINT('Origin',(0.,0.,7.50366116523517));
#408310=CARTESIAN_POINT('Origin',(1.87623278704651,-1.9934033156418,7.49482233047033));
#408311=CARTESIAN_POINT('Ctrl Pts',(1.9418647882945,-1.93769342600927,7.51860402984325));
#408312=CARTESIAN_POINT('Ctrl Pts',(1.9491269287305,-1.93996446152595,7.51860402984325));
#408313=CARTESIAN_POINT('Ctrl Pts',(1.95447964353083,-1.93455662181897,
7.51860402984325));
#408314=CARTESIAN_POINT('Ctrl Pts',(1.9445612709771,-1.93853667578216,7.51041458714365));
#408315=CARTESIAN_POINT('Ctrl Pts',(1.95039504114,-1.93868327539489,7.51004642900441));
#408316=CARTESIAN_POINT('Ctrl Pts',(1.95448111974601,-1.93455513040099,
7.50729136483009));
#408317=CARTESIAN_POINT('Ctrl Pts',(1.94469947306817,-1.94134819447875,
7.50215815450138));
#408318=CARTESIAN_POINT('Ctrl Pts',(1.9478131375204,-1.94129199696614,7.49877163671531));
#408319=CARTESIAN_POINT('Ctrl Pts',(1.95025716865164,-1.9388567073686,7.49481588533172));
#408320=CARTESIAN_POINT('Ctrl Pts',(1.93848135025099,-1.94542129788096,
7.50366171572174));
#408321=CARTESIAN_POINT('Ctrl Pts',(1.9410659436124,-1.94801514433233,7.50000045605858));
#408322=CARTESIAN_POINT('Ctrl Pts',(1.94106594361249,-1.94801514433224,
7.49482233047317));
#408323=CARTESIAN_POINT('Origin',(1.94559564515114,-1.92576318262889,7.51860402984325));
#408324=CARTESIAN_POINT('Origin',(1.94559564515114,-1.92576318262889,9.));
#408325=CARTESIAN_POINT('Origin',(1.94559564515114,-1.92576318262889,8.75721825406948));
#408326=CARTESIAN_POINT('Ctrl Pts',(1.9259264261929,-1.9327105887171,8.78942910404912));
#408327=CARTESIAN_POINT('Ctrl Pts',(1.93123897640997,-1.93439262287037,
8.79672699501691));
#408328=CARTESIAN_POINT('Ctrl Pts',(1.93545014613629,-1.92652245543134,
8.79893251111267));
#408329=CARTESIAN_POINT('Ctrl Pts',(1.93641991058458,-1.93599116855337,
8.78111911759582));
#408330=CARTESIAN_POINT('Ctrl Pts',(1.94272024732633,-1.93797814290299,
8.78644465894813));
#408331=CARTESIAN_POINT('Ctrl Pts',(1.94798872487631,-1.93181708324732,
8.78817647674132));
#408332=CARTESIAN_POINT('Ctrl Pts',(1.94295970036019,-1.93803570412616,
8.76780923932029));
#408333=CARTESIAN_POINT('Ctrl Pts',(1.95039851453346,-1.94037638361425,
8.76988516158373));
#408334=CARTESIAN_POINT('Ctrl Pts',(1.95582445196924,-1.93511372427326,
8.77093053738833));
#408335=CARTESIAN_POINT('Ctrl Pts',(1.94168453085778,-1.93763704766925,
8.75371302330492));
#408336=CARTESIAN_POINT('Ctrl Pts',(1.94894054439862,-1.93992100670192,
8.75300828287559));
#408337=CARTESIAN_POINT('Ctrl Pts',(1.95429634438096,-1.93447032363614,
8.75267964240738));
#408338=CARTESIAN_POINT('Origin',(1.93221186659145,-1.92157901568046,8.78727029226991));
#408339=CARTESIAN_POINT('Ctrl Pts',(1.86024642503786,-1.91217709997533,
8.85049129520029));
#408340=CARTESIAN_POINT('Ctrl Pts',(1.86582001548255,-1.91391956999743,
8.85711686593484));
#408341=CARTESIAN_POINT('Ctrl Pts',(1.87016576301195,-1.90655647007113,
8.85933012996512));
#408342=CARTESIAN_POINT('Ctrl Pts',(1.88302471602833,-1.91929827071787,
8.82945683644723));
#408343=CARTESIAN_POINT('Ctrl Pts',(1.88864457064357,-1.92105520429467,
8.83607469902389));
#408344=CARTESIAN_POINT('Ctrl Pts',(1.89297078040509,-1.91365142474655,
8.8382956714852));
#408345=CARTESIAN_POINT('Ctrl Pts',(1.90576905413923,-1.92640882678116,
8.80838214965003));
#408346=CARTESIAN_POINT('Ctrl Pts',(1.91141108732463,-1.92817269403816,
8.81501364461988));
#408347=CARTESIAN_POINT('Ctrl Pts',(1.91574100516642,-1.92073625510015,
8.81722098428721));
#408348=CARTESIAN_POINT('Ctrl Pts',(1.92848201925699,-1.93350957471437,
8.78727029226991));
#408349=CARTESIAN_POINT('Ctrl Pts',(1.93412498960265,-1.93527373495551,
8.79393457792714));
#408350=CARTESIAN_POINT('Ctrl Pts',(1.93847908687937,-1.92781174781514,
8.79610912703474));
#408351=CARTESIAN_POINT('Origin',(1.86397627237232,-1.90024654094142,8.85049129520029));
#408352=CARTESIAN_POINT('Ctrl Pts',(1.85157082176548,-1.92057895321252,
8.85049129520029));
#408353=CARTESIAN_POINT('Ctrl Pts',(1.85313375416823,-1.92620552894981,
8.85711686593484));
#408354=CARTESIAN_POINT('Ctrl Pts',(1.84563514921934,-1.93031304473608,
8.85933012996512));
#408355=CARTESIAN_POINT('Ctrl Pts',(1.85018811802994,-1.91560120287821,
8.86332496987231));
#408356=CARTESIAN_POINT('Ctrl Pts',(1.84707133638469,-1.91901259065336,
8.86648636486738));
#408357=CARTESIAN_POINT('Ctrl Pts',(1.8417834867551,-1.91638299977497,8.87206031107458));
#408358=CARTESIAN_POINT('Ctrl Pts',(1.85528204317687,-1.91062508666239,
8.86341338519876));
#408359=CARTESIAN_POINT('Ctrl Pts',(1.85878222246585,-1.90758827656308,
8.86654584966059));
#408360=CARTESIAN_POINT('Ctrl Pts',(1.85626083386738,-1.90222481198104,
8.87215952290713));
#408361=CARTESIAN_POINT('Ctrl Pts',(1.86024642503786,-1.91217709997533,
8.85049129520029));
#408362=CARTESIAN_POINT('Ctrl Pts',(1.86582001548255,-1.91391956999743,
8.85711686593484));
#408363=CARTESIAN_POINT('Ctrl Pts',(1.87016576301195,-1.90655647007113,
8.85933012996512));
#408364=CARTESIAN_POINT('Origin',(1.83952684496835,-1.92392449097349,8.85049129520029));
#408365=CARTESIAN_POINT('Ctrl Pts',(1.87070527778335,-1.98946322855769,
8.78727029226991));
#408366=CARTESIAN_POINT('Ctrl Pts',(1.87228766552577,-1.99515984375543,
8.79393457792714));
#408367=CARTESIAN_POINT('Ctrl Pts',(1.86468995654688,-1.99927253550784,
8.79610912703474));
#408368=CARTESIAN_POINT('Ctrl Pts',(1.86433616446273,-1.96653434282024,
8.80838214965002));
#408369=CARTESIAN_POINT('Ctrl Pts',(1.865918289409,-1.97223001194861,8.81501364461986));
#408370=CARTESIAN_POINT('Ctrl Pts',(1.85834689049528,-1.97631935554928,
8.81722098428721));
#408371=CARTESIAN_POINT('Ctrl Pts',(1.85795825360523,-1.94357378584256,
8.82945683644723));
#408372=CARTESIAN_POINT('Ctrl Pts',(1.85953415929191,-1.94924706556034,
8.83607469902388));
#408373=CARTESIAN_POINT('Ctrl Pts',(1.851995521838,-1.95333374977088,8.8382956714852));
#408374=CARTESIAN_POINT('Ctrl Pts',(1.85157082176548,-1.92057895321252,
8.85049129520029));
#408375=CARTESIAN_POINT('Ctrl Pts',(1.85313375416823,-1.92620552894981,
8.85711686593484));
#408376=CARTESIAN_POINT('Ctrl Pts',(1.84563514921934,-1.93031304473608,
8.85933012996512));
#408377=CARTESIAN_POINT('Origin',(1.85866130098622,-1.99280876631867,8.78727029226991));
#408378=CARTESIAN_POINT('Ctrl Pts',(1.87440874889962,-2.00279583872934,
8.75374538247847));
#408379=CARTESIAN_POINT('Ctrl Pts',(1.87645520159847,-2.01011406322296,
8.75304829418601));
#408380=CARTESIAN_POINT('Ctrl Pts',(1.87084545367739,-2.01529106732485,
8.75272238421917));
#408381=CARTESIAN_POINT('Ctrl Pts',(1.87476203373011,-2.00406766683984,
8.76769408445023));
#408382=CARTESIAN_POINT('Ctrl Pts',(1.87685931964825,-2.01157023618304,
8.76974318093971));
#408383=CARTESIAN_POINT('Ctrl Pts',(1.87143335527491,-2.0168216424613,8.7707786988043));
#408384=CARTESIAN_POINT('Ctrl Pts',(1.87295129695636,-1.99754900045418,
8.78108014887986));
#408385=CARTESIAN_POINT('Ctrl Pts',(1.87473233033614,-2.00390613482436,
8.78639403366322));
#408386=CARTESIAN_POINT('Ctrl Pts',(1.86842728617051,-2.00898240252794,
8.78812224174741));
#408387=CARTESIAN_POINT('Ctrl Pts',(1.86998389907454,-1.98686634526786,
8.78944554828686));
#408388=CARTESIAN_POINT('Ctrl Pts',(1.8714902781559,-1.99222239228784,8.79673892988687));
#408389=CARTESIAN_POINT('Ctrl Pts',(1.86349886841125,-1.99617725317157,
8.79894799272499));
#408390=CARTESIAN_POINT('Origin',(1.86241434696074,-2.00631977766128,8.75721825406948));
#408391=CARTESIAN_POINT('Origin',(1.86241434696074,-2.00631977766128,9.));
#408392=CARTESIAN_POINT('Origin',(1.86241434696074,-2.00631977766128,7.51860402984325));
#408393=CARTESIAN_POINT('Ctrl Pts',(1.88229022471614,-1.99983903961936,
7.50366195182966));
#408394=CARTESIAN_POINT('Ctrl Pts',(1.88480006004662,-2.00250561388683,
7.50000065167735));
#408395=CARTESIAN_POINT('Ctrl Pts',(1.88480006004653,-2.00250561388691,
7.49482233047108));
#408396=CARTESIAN_POINT('Ctrl Pts',(1.87801537607976,-2.00592833093631,
7.50215800491337));
#408397=CARTESIAN_POINT('Ctrl Pts',(1.87785800363692,-2.00903958969902,
7.49877273257263));
#408398=CARTESIAN_POINT('Ctrl Pts',(1.87534423927866,-2.01140562966089,
7.49481816995647));
#408399=CARTESIAN_POINT('Ctrl Pts',(1.87521302519499,-2.00568990723634,
7.51043025814042));
#408400=CARTESIAN_POINT('Ctrl Pts',(1.87517626445681,-2.0115286918389,7.51006209594516));
#408401=CARTESIAN_POINT('Ctrl Pts',(1.870916666451,-2.01548277769926,7.50731281821699));
#408402=CARTESIAN_POINT('Ctrl Pts',(1.87445791915217,-2.00297278365627,
7.51860402984325));
#408403=CARTESIAN_POINT('Ctrl Pts',(1.87649537412108,-2.01030420880015,
7.51860402984324));
#408404=CARTESIAN_POINT('Ctrl Pts',(1.87091852206101,-2.01548105518485,
7.51860402984325));
#408405=CARTESIAN_POINT('Origin',(0.,0.,7.5));
#408406=CARTESIAN_POINT('Origin',(1.97081848695447,-1.79800236791131,7.5));
#408407=CARTESIAN_POINT('',(1.97081848695447,-1.79800236791131,7.59394543036555));
#408408=CARTESIAN_POINT('',(1.97081848695447,-1.79800236791131,8.85049129520029));
#408409=CARTESIAN_POINT('',(1.97081848695447,-1.79800236791131,7.5));
#408410=CARTESIAN_POINT('',(1.99432705985486,-1.8655191643187,8.78727029226991));
#408411=CARTESIAN_POINT('Ctrl Pts',(1.97081848695447,-1.79800236791131,
8.85049129520029));
#408412=CARTESIAN_POINT('Ctrl Pts',(1.97866606858373,-1.82054068078118,
8.82945686509571));
#408413=CARTESIAN_POINT('Ctrl Pts',(1.98650198383398,-1.84304548772368,
8.80838212259895));
#408414=CARTESIAN_POINT('Ctrl Pts',(1.99432705985486,-1.8655191643187,8.78727029226991));
#408415=CARTESIAN_POINT('',(1.9989380482628,-1.87876195735827,8.75721825406948));
#408416=CARTESIAN_POINT('Origin',(1.98506217516105,-1.83890973278876,8.75937679713163));
#408417=CARTESIAN_POINT('',(1.9989380482628,-1.87876195735827,7.51860402984325));
#408418=CARTESIAN_POINT('',(1.9989380482628,-1.87876195735827,7.5));
#408419=CARTESIAN_POINT('Ctrl Pts',(1.9989380482628,-1.87876195735827,7.51860402984325));
#408420=CARTESIAN_POINT('Ctrl Pts',(1.99531683401271,-1.86836180306959,
7.52834476460825));
#408421=CARTESIAN_POINT('Ctrl Pts',(1.99169326892259,-1.85795489715082,
7.53807742314407));
#408422=CARTESIAN_POINT('Ctrl Pts',(1.98806727405985,-1.84754101290699,
7.54780169004674));
#408423=CARTESIAN_POINT('Ctrl Pts',(1.98232389416557,-1.83104598308719,
7.5632044032688));
#408424=CARTESIAN_POINT('Ctrl Pts',(1.97657441098223,-1.81453342457585,
7.57858609112103));
#408425=CARTESIAN_POINT('Ctrl Pts',(1.97081848695447,-1.79800236791131,
7.59394543036555));
#408426=CARTESIAN_POINT('Origin',(2.24612836500519,-1.85413331864099,7.5));
#408427=CARTESIAN_POINT('',(2.0620244905542,-1.80929677321441,8.75721825406948));
#408428=CARTESIAN_POINT('',(2.04840012990614,-1.80597870472223,8.78727029226991));
#408429=CARTESIAN_POINT('Origin',(2.01381642095027,-1.79755620931172,8.75658640621115));
#408430=CARTESIAN_POINT('',(1.97893795668432,-1.78906192937257,8.85049129520029));
#408431=CARTESIAN_POINT('Ctrl Pts',(2.04840012990614,-1.80597870472223,
8.78727029226991));
#408432=CARTESIAN_POINT('Ctrl Pts',(2.02527891415481,-1.80034777792373,
8.80838212259896));
#408433=CARTESIAN_POINT('Ctrl Pts',(2.0021256710902,-1.79470905121288,8.82945686509571));
#408434=CARTESIAN_POINT('Ctrl Pts',(1.97893795668432,-1.78906192937257,
8.85049129520029));
#408435=CARTESIAN_POINT('',(1.97893795668432,-1.78906192937257,7.59394543036555));
#408436=CARTESIAN_POINT('',(1.97893795668432,-1.78906192937257,7.5));
#408437=CARTESIAN_POINT('',(2.0620244905542,-1.80929677321441,7.51860402984325));
#408438=CARTESIAN_POINT('Ctrl Pts',(1.97893795668431,-1.78906192937257,
7.59394543036555));
#408439=CARTESIAN_POINT('Ctrl Pts',(1.99594532644522,-1.79320389384314,
7.57858609112103));
#408440=CARTESIAN_POINT('Ctrl Pts',(2.01293366506122,-1.7973412234803,7.56320440326857));
#408441=CARTESIAN_POINT('Ctrl Pts',(2.02990396992771,-1.80147416118906,
7.54780169004651));
#408442=CARTESIAN_POINT('Ctrl Pts',(2.04061791178733,-1.80408342806256,
7.53807742314383));
#408443=CARTESIAN_POINT('Ctrl Pts',(2.05132467425404,-1.80669094647106,
7.52834476460825));
#408444=CARTESIAN_POINT('Ctrl Pts',(2.0620244905542,-1.80929677321441,7.51860402984325));
#408445=CARTESIAN_POINT('',(2.0620244905542,-1.80929677321441,7.5));
#408446=CARTESIAN_POINT('Origin',(1.97731117195261,-1.79574168958059,7.5));
#408447=CARTESIAN_POINT('Ctrl Pts',(1.97893795668432,-1.78906192937257,
8.85049129520029));
#408448=CARTESIAN_POINT('Ctrl Pts',(1.97874979487762,-1.78901610456079,
8.85097269580138));
#408449=CARTESIAN_POINT('Ctrl Pts',(1.97856201674473,-1.78897903045468,
8.85143669361005));
#408450=CARTESIAN_POINT('Ctrl Pts',(1.9783658063634,-1.78894985763937,8.8519052845931));
#408451=CARTESIAN_POINT('Ctrl Pts',(1.97798203130075,-1.78889279746269,
8.85282181883899));
#408452=CARTESIAN_POINT('Ctrl Pts',(1.97757584056464,-1.78886762770679,
8.85372622499635));
#408453=CARTESIAN_POINT('Ctrl Pts',(1.97713990672663,-1.78888934263685,
8.85462257735071));
#408454=CARTESIAN_POINT('Ctrl Pts',(1.97677800993722,-1.78890736960054,
8.85536669723986));
#408455=CARTESIAN_POINT('Ctrl Pts',(1.97639553091104,-1.78895768077186,
8.85610498449051));
#408456=CARTESIAN_POINT('Ctrl Pts',(1.97598928856819,-1.7890567933604,8.85681338218371));
#408457=CARTESIAN_POINT('Ctrl Pts',(1.97562062300403,-1.78914673819017,
8.85745625420284));
#408458=CARTESIAN_POINT('Ctrl Pts',(1.97522762055869,-1.78927742070007,
8.85808743050665));
#408459=CARTESIAN_POINT('Ctrl Pts',(1.97480670587177,-1.78947721452131,
8.8586680450841));
#408460=CARTESIAN_POINT('Ctrl Pts',(1.97461250495954,-1.78956939505943,
8.85893592806395));
#408461=CARTESIAN_POINT('Ctrl Pts',(1.97441236097825,-1.78967652968199,
8.85919241173848));
#408462=CARTESIAN_POINT('Ctrl Pts',(1.97420613659522,-1.78980298681162,
8.85943017985534));
#408463=CARTESIAN_POINT('Ctrl Pts',(1.97392767262918,-1.78997374137194,
8.8597512372));
#408464=CARTESIAN_POINT('Ctrl Pts',(1.97363136948359,-1.7901846188583,8.86004599534706));
#408465=CARTESIAN_POINT('Ctrl Pts',(1.97332682621396,-1.7904415711516,8.86026130871722));
#408466=CARTESIAN_POINT('Ctrl Pts',(1.97321532433697,-1.79053564863043,
8.86034014101236));
#408467=CARTESIAN_POINT('Ctrl Pts',(1.97310103504486,-1.79063730615675,
8.86040910639693));
#408468=CARTESIAN_POINT('Ctrl Pts',(1.97298729564543,-1.79074402546768,
8.86046313645507));
#408469=CARTESIAN_POINT('Ctrl Pts',(1.97280980626519,-1.79091056005861,
8.8605474499083));
#408470=CARTESIAN_POINT('Ctrl Pts',(1.9726289116331,-1.79109407389667,8.86059655985669));
#408471=CARTESIAN_POINT('Ctrl Pts',(1.97245600443692,-1.79128259202279,
8.86059725258816));
#408472=CARTESIAN_POINT('Ctrl Pts',(1.97228269775604,-1.7914715457011,8.86059794692012));
#408473=CARTESIAN_POINT('Ctrl Pts',(1.97211745140938,-1.79166941813832,
8.86056369958366));
#408474=CARTESIAN_POINT('Ctrl Pts',(1.97196638965372,-1.79186300516204,
8.86048590497774));
#408475=CARTESIAN_POINT('Ctrl Pts',(1.97192696703314,-1.79191352561145,
8.86046560290182));
#408476=CARTESIAN_POINT('Ctrl Pts',(1.97188806900511,-1.7919644671666,8.86044257503091));
#408477=CARTESIAN_POINT('Ctrl Pts',(1.97185087146102,-1.79201423576954,
8.86041778462583));
#408478=CARTESIAN_POINT('Ctrl Pts',(1.97160057814758,-1.79234911670961,
8.86025097596201));
#408479=CARTESIAN_POINT('Ctrl Pts',(1.9713939560763,-1.79267602610359,8.8599848982295));
#408480=CARTESIAN_POINT('Ctrl Pts',(1.97122987412083,-1.79298089568,8.85968173251461));
#408481=CARTESIAN_POINT('Ctrl Pts',(1.97114308416717,-1.79314215421898,
8.85952137522076));
#408482=CARTESIAN_POINT('Ctrl Pts',(1.97106635501148,-1.79330026432412,
8.85934740853961));
#408483=CARTESIAN_POINT('Ctrl Pts',(1.97099937013856,-1.79345231758423,
8.8591675900182));
#408484=CARTESIAN_POINT('Ctrl Pts',(1.97073039105572,-1.79406289045929,
8.85844552518695));
#408485=CARTESIAN_POINT('Ctrl Pts',(1.97060056149349,-1.79460908862718,
8.85759444184124));
#408486=CARTESIAN_POINT('Ctrl Pts',(1.97053470628905,-1.79506393733561,
8.85683498915138));
#408487=CARTESIAN_POINT('Ctrl Pts',(1.9705278147173,-1.79511153604159,8.85675551444998));
#408488=CARTESIAN_POINT('Ctrl Pts',(1.97052164367322,-1.79515813331054,
8.85667699793651));
#408489=CARTESIAN_POINT('Ctrl Pts',(1.97051612006802,-1.79520369685433,
8.85659965593547));
#408490=CARTESIAN_POINT('Ctrl Pts',(1.97044156216318,-1.79581871589338,
8.85555568965886));
#408491=CARTESIAN_POINT('Ctrl Pts',(1.9704587283161,-1.79642055493027,8.85434650606346));
#408492=CARTESIAN_POINT('Ctrl Pts',(1.97056149117541,-1.79701236630734,
8.85297329937117));
#408493=CARTESIAN_POINT('Ctrl Pts',(1.97061928902234,-1.79734522414734,
8.85220095427747));
#408494=CARTESIAN_POINT('Ctrl Pts',(1.97070449840186,-1.79767499193948,
8.85137579139183));
#408495=CARTESIAN_POINT('Ctrl Pts',(1.97081848695447,-1.79800236791131,
8.85049129520029));
#408496=CARTESIAN_POINT('Origin',(1.97731117195261,-1.79574168958059,7.59394543036555));
#408497=CARTESIAN_POINT('Ctrl Pts',(1.97839165948369,-1.78892888448513,
7.59443877723642));
#408498=CARTESIAN_POINT('Ctrl Pts',(1.97276532395028,-1.78755865015692,
7.58783886950016));
#408499=CARTESIAN_POINT('Ctrl Pts',(1.96890226666508,-1.79511880689789,
7.58559994247159));
#408500=CARTESIAN_POINT('Ctrl Pts',(2.0091056600909,-1.79640895348185,7.56670252222136));
#408501=CARTESIAN_POINT('Ctrl Pts',(2.00348745620967,-1.7950406995313,7.56004874999026));
#408502=CARTESIAN_POINT('Ctrl Pts',(1.99958248326974,-1.80263593116663,
7.55786368756704));
#408503=CARTESIAN_POINT('Ctrl Pts',(2.03976230537068,-1.80387505419708,
7.53888913333559));
#408504=CARTESIAN_POINT('Ctrl Pts',(2.03411071222872,-1.80249866864629,
7.53222002137279));
#408505=CARTESIAN_POINT('Ctrl Pts',(2.03020677218686,-1.81013815140818,
7.53005029815326));
#408506=CARTESIAN_POINT('Ctrl Pts',(2.07036020808908,-1.81132684878468,
7.51101258149734));
#408507=CARTESIAN_POINT('Ctrl Pts',(2.06464010736904,-1.80993377894005,
7.5043616886572));
#408508=CARTESIAN_POINT('Ctrl Pts',(2.06077360068109,-1.81762517722493,
7.50217374673251));
#408509=CARTESIAN_POINT('',(2.05914251569205,-1.81722565891164,7.50366116523517));
#408510=CARTESIAN_POINT('Ctrl Pts',(2.0620244905542,-1.80929677321441,7.51860402984325));
#408511=CARTESIAN_POINT('Ctrl Pts',(2.06245356066702,-1.80940126868829,
7.51734760759494));
#408512=CARTESIAN_POINT('Ctrl Pts',(2.06282720854069,-1.80955350247717,
7.51608817408573));
#408513=CARTESIAN_POINT('Ctrl Pts',(2.06313953628695,-1.80976549106596,
7.5148100591312));
#408514=CARTESIAN_POINT('Ctrl Pts',(2.06342245022282,-1.80995751539531,
7.51365231206384));
#408515=CARTESIAN_POINT('Ctrl Pts',(2.06365558924025,-1.81019863323145,
7.51247773061043));
#408516=CARTESIAN_POINT('Ctrl Pts',(2.06380837374076,-1.8105103394139,7.51129758471022));
#408517=CARTESIAN_POINT('Ctrl Pts',(2.06399826742623,-1.8108977546005,7.50983079813402));
#408518=CARTESIAN_POINT('Ctrl Pts',(2.06404627660563,-1.81138758047697,
7.50839324291155));
#408519=CARTESIAN_POINT('Ctrl Pts',(2.06387070521551,-1.81199143356978,
7.50715379678855));
#408520=CARTESIAN_POINT('Ctrl Pts',(2.06378959629224,-1.81227039629905,
7.50658120839351));
#408521=CARTESIAN_POINT('Ctrl Pts',(2.06364011712739,-1.8126106987067,7.50598221009429));
#408522=CARTESIAN_POINT('Ctrl Pts',(2.06340499918458,-1.81299509420526,
7.50545747549612));
#408523=CARTESIAN_POINT('Ctrl Pts',(2.06327953297272,-1.81320021954144,
7.50517746087247));
#408524=CARTESIAN_POINT('Ctrl Pts',(2.06312849233741,-1.81342023086748,
7.50491486231392));
#408525=CARTESIAN_POINT('Ctrl Pts',(2.0629545019405,-1.81364835785532,7.50468370960992));
#408526=CARTESIAN_POINT('Ctrl Pts',(2.06269433141495,-1.81398947966072,
7.50433806340446));
#408527=CARTESIAN_POINT('Ctrl Pts',(2.06237460179235,-1.81435863918605,
7.50405484070983));
#408528=CARTESIAN_POINT('Ctrl Pts',(2.06201630474492,-1.81473050520947,
7.5038576603613));
#408529=CARTESIAN_POINT('Ctrl Pts',(2.0619779904449,-1.81477027050056,7.50383657498791));
#408530=CARTESIAN_POINT('Ctrl Pts',(2.06193926245815,-1.81481005916188,
7.50381643264937));
#408531=CARTESIAN_POINT('Ctrl Pts',(2.06190016639467,-1.81484983502234,
7.50379723213559));
#408532=CARTESIAN_POINT('Ctrl Pts',(2.06163918738169,-1.81511535190252,
7.50366906242519));
#408533=CARTESIAN_POINT('Ctrl Pts',(2.06135561716471,-1.81538556993998,
7.50358235568538));
#408534=CARTESIAN_POINT('Ctrl Pts',(2.06107602952701,-1.81563945665819,
7.5035341175365));
#408535=CARTESIAN_POINT('Ctrl Pts',(2.0606568195075,-1.81602013105772,7.50346178989176));
#408536=CARTESIAN_POINT('Ctrl Pts',(2.0601896590865,-1.81641182575993,7.50346967198527));
#408537=CARTESIAN_POINT('Ctrl Pts',(2.05971922051128,-1.81678223725705,
7.50354272648692));
#408538=CARTESIAN_POINT('Ctrl Pts',(2.05952571938779,-1.81693459517288,
7.50357277531559));
#408539=CARTESIAN_POINT('Ctrl Pts',(2.05933200846983,-1.8170832612696,7.50361331098761));
#408540=CARTESIAN_POINT('Ctrl Pts',(2.05914251569312,-1.81722565891258,
7.50366116523659));
#408541=CARTESIAN_POINT('',(1.97947865054224,-1.79771013628761,7.57603338622103));
#408542=CARTESIAN_POINT('Origin',(1.98601852345805,-1.80365333002949,7.58486873427628));
#408543=CARTESIAN_POINT('Ctrl Pts',(2.05914251574879,-1.81722565892002,
7.50366116529968));
#408544=CARTESIAN_POINT('Ctrl Pts',(2.03263102682017,-1.81073191165143,
7.52783573079709));
#408545=CARTESIAN_POINT('Ctrl Pts',(2.00607765461974,-1.80422706199264,
7.55196141284068));
#408546=CARTESIAN_POINT('Ctrl Pts',(1.97947865179297,-1.79771013622992,
7.57603338728831));
#408547=CARTESIAN_POINT('Ctrl Pts',(1.97989555771598,-1.78947609816003,
7.5963967733137));
#408548=CARTESIAN_POINT('Ctrl Pts',(1.96304400704071,-1.78239816374406,
7.5995988229547));
#408549=CARTESIAN_POINT('Ctrl Pts',(1.97123919548054,-1.79875504911528,
7.59642833564546));
#408550=CARTESIAN_POINT('Ctrl Pts',(1.9765888088445,-1.78740715737189,7.58707626057421));
#408551=CARTESIAN_POINT('Ctrl Pts',(1.96999477520764,-1.78896632748219,
7.58809943920599));
#408552=CARTESIAN_POINT('Ctrl Pts',(1.96897092964353,-1.79564960071125,
7.58710240504253));
#408553=CARTESIAN_POINT('Ctrl Pts',(1.97787616399563,-1.79334587347696,
7.58015376756929));
#408554=CARTESIAN_POINT('Ctrl Pts',(1.9750397244827,-1.79363549786383,7.58205880659761));
#408555=CARTESIAN_POINT('Ctrl Pts',(1.9749817704291,-1.79645040751884,7.58020924244126));
#408556=CARTESIAN_POINT('Ctrl Pts',(1.97947864992974,-1.79771013573109,
7.57603338509286));
#408557=CARTESIAN_POINT('Ctrl Pts',(1.97947864992974,-1.79771013573109,
7.57603338509286));
#408558=CARTESIAN_POINT('Ctrl Pts',(1.97947864992974,-1.79771013573109,
7.57603338509286));
#408559=CARTESIAN_POINT('Origin',(1.98602235984358,-1.80364910574229,7.58486873427622));
#408560=CARTESIAN_POINT('Ctrl Pts',(2.00176808024936,-1.8868898302952,7.51098857897448));
#408561=CARTESIAN_POINT('Ctrl Pts',(1.99983217741496,-1.88132990294067,
7.50433767179956));
#408562=CARTESIAN_POINT('Ctrl Pts',(2.00711679739923,-1.87674270741756,
7.50214974420965));
#408563=CARTESIAN_POINT('Ctrl Pts',(1.99140963785971,-1.85714030662641,
7.53887321589171));
#408564=CARTESIAN_POINT('Ctrl Pts',(1.98949693057689,-1.85164699706867,
7.53220407452065));
#408565=CARTESIAN_POINT('Ctrl Pts',(1.99672626159454,-1.84702750651672,
7.53003438070911));
#408566=CARTESIAN_POINT('Ctrl Pts',(1.98103130343959,-1.82733365289799,
7.56669465659232));
#408567=CARTESIAN_POINT('Ctrl Pts',(1.97912989990116,-1.82187280777845,
7.56004085833298));
#408568=CARTESIAN_POINT('Ctrl Pts',(1.98631507225217,-1.8172565378109,7.55785582193788));
#408569=CARTESIAN_POINT('Ctrl Pts',(1.97063354635954,-1.79747121714566,
7.59443891967696));
#408570=CARTESIAN_POINT('Ctrl Pts',(1.96872938602274,-1.79200245448059,
7.58783901202978));
#408571=CARTESIAN_POINT('Ctrl Pts',(1.97588366545475,-1.78743129885021,
7.58560008491213));
#408572=CARTESIAN_POINT('',(2.00655355952794,-1.87513194417972,7.50366116523517));
#408573=CARTESIAN_POINT('Ctrl Pts',(2.00655355952821,-1.87513194417998,
7.50366116523554));
#408574=CARTESIAN_POINT('Ctrl Pts',(2.00615848269925,-1.87577851344617,
7.50350835821027));
#408575=CARTESIAN_POINT('Ctrl Pts',(2.00577427574859,-1.87636001411703,
7.50345484956));
#408576=CARTESIAN_POINT('Ctrl Pts',(2.00539001691052,-1.87689406571167,
7.50349758195598));
#408577=CARTESIAN_POINT('Ctrl Pts',(2.00519286362921,-1.87716807378603,
7.50351950684424));
#408578=CARTESIAN_POINT('Ctrl Pts',(2.00497636954117,-1.87745667406356,
7.50357029184312));
#408579=CARTESIAN_POINT('Ctrl Pts',(2.00475995703381,-1.8777292295213,7.50365515313924));
#408580=CARTESIAN_POINT('Ctrl Pts',(2.00442702696342,-1.8781485301839,7.50378570417639));
#408581=CARTESIAN_POINT('Ctrl Pts',(2.00408478899121,-1.87854238174115,
7.50400001621911));
#408582=CARTESIAN_POINT('Ctrl Pts',(2.0037575786085,-1.87887931717082,7.50428903009634));
#408583=CARTESIAN_POINT('Ctrl Pts',(2.00372126077342,-1.87891671441129,
7.50432110841318));
#408584=CARTESIAN_POINT('Ctrl Pts',(2.003685123025,-1.87895344037837,7.50435406373354));
#408585=CARTESIAN_POINT('Ctrl Pts',(2.00364919461635,-1.87898947405934,
7.50438785222352));
#408586=CARTESIAN_POINT('Ctrl Pts',(2.00342983441216,-1.87920947700161,
7.50459414719561));
#408587=CARTESIAN_POINT('Ctrl Pts',(2.00321442008338,-1.87940681218195,
7.50483629897752));
#408588=CARTESIAN_POINT('Ctrl Pts',(2.00301209305112,-1.87957489015283,
7.5050991045531));
#408589=CARTESIAN_POINT('Ctrl Pts',(2.00256573929613,-1.87994568703842,
7.50567888004914));
#408590=CARTESIAN_POINT('Ctrl Pts',(2.00216582340183,-1.88018910434133,
7.50637912803144));
#408591=CARTESIAN_POINT('Ctrl Pts',(2.001820965996,-1.88033482544297,7.50710440483569));
#408592=CARTESIAN_POINT('Ctrl Pts',(2.00173640011371,-1.88037055915006,
7.50728225710685));
#408593=CARTESIAN_POINT('Ctrl Pts',(2.00165351840972,-1.88040126390212,
7.50746498566954));
#408594=CARTESIAN_POINT('Ctrl Pts',(2.00157440033248,-1.88042661359859,
7.50764697238949));
#408595=CARTESIAN_POINT('Ctrl Pts',(2.00114908332307,-1.8805628865904,7.50862528291181));
#408596=CARTESIAN_POINT('Ctrl Pts',(2.00079518281119,-1.88056071912447,
7.50965856837421));
#408597=CARTESIAN_POINT('Ctrl Pts',(2.00049449295551,-1.88048386026498,
7.51067959873202));
#408598=CARTESIAN_POINT('Ctrl Pts',(2.00032902294865,-1.88044156473766,
7.51124147302578));
#408599=CARTESIAN_POINT('Ctrl Pts',(2.00017973400084,-1.88037621910702,
7.51180065547253));
#408600=CARTESIAN_POINT('Ctrl Pts',(2.00004436034524,-1.88029584196496,
7.51235175716501));
#408601=CARTESIAN_POINT('Ctrl Pts',(1.99957659043867,-1.88001810692069,
7.51425603304536));
#408602=CARTESIAN_POINT('Ctrl Pts',(1.9992222893872,-1.879522569644,7.5162690050518));
#408603=CARTESIAN_POINT('Ctrl Pts',(1.99897691956688,-1.87886941383172,
7.51827788969243));
#408604=CARTESIAN_POINT('Ctrl Pts',(1.99896363968852,-1.87883406380486,
7.51838661432545));
#408605=CARTESIAN_POINT('Ctrl Pts',(1.99895068242725,-1.87879824277265,
7.51849533314856));
#408606=CARTESIAN_POINT('Ctrl Pts',(1.99893804826279,-1.87876195735827,
7.51860402984325));
#408607=CARTESIAN_POINT('Ctrl Pts',(1.97947865060564,-1.79771013753908,
7.57603338728984));
#408608=CARTESIAN_POINT('Ctrl Pts',(1.98851957913015,-1.82356045445255,
7.55196141284921));
#408609=CARTESIAN_POINT('Ctrl Pts',(1.99754410576772,-1.84936651119314,
7.52783573083104));
#408610=CARTESIAN_POINT('Ctrl Pts',(2.00655355954226,-1.87513194423715,
7.50366116530176));
#408611=CARTESIAN_POINT('Origin',(6.8400137636579E-16,-6.21191952330704E-16,
7.49482233047033));
#408612=CARTESIAN_POINT('Origin',(2.05251535802926,-1.81137708803386,7.49482233047033));
#408613=CARTESIAN_POINT('Origin',(0.,0.,7.50366116523517));
#408614=CARTESIAN_POINT('Origin',(2.00009565450364,-1.86909700733688,7.49482233047033));
#408615=CARTESIAN_POINT('Ctrl Pts',(2.0620234628822,-1.80929652288974,7.51860402984325));
#408616=CARTESIAN_POINT('Ctrl Pts',(2.06941618821694,-1.81109760538512,
7.51860402984325));
#408617=CARTESIAN_POINT('Ctrl Pts',(2.07441142381099,-1.80535792705005,
7.51860402984325));
#408618=CARTESIAN_POINT('Ctrl Pts',(2.06476843255037,-1.80996527587688,
7.51041458714366));
#408619=CARTESIAN_POINT('Ctrl Pts',(2.07059960927626,-1.80973780334733,
7.51004642900442));
#408620=CARTESIAN_POINT('Ctrl Pts',(2.07441280143767,-1.80535634411491,
7.50729136483009));
#408621=CARTESIAN_POINT('Ctrl Pts',(2.0650864853118,-1.8127621633684,7.50215815450138));
#408622=CARTESIAN_POINT('Ctrl Pts',(2.06819015181947,-1.81250658815321,
7.4987716367153));
#408623=CARTESIAN_POINT('Ctrl Pts',(2.07047313188641,-1.80991971250712,
7.49481588533171));
#408624=CARTESIAN_POINT('Ctrl Pts',(2.05914210292583,-1.81722529463959,
7.50366171572174));
#408625=CARTESIAN_POINT('Ctrl Pts',(2.06188757427571,-1.81964821629001,
7.50000045605858));
#408626=CARTESIAN_POINT('Ctrl Pts',(2.0618875742758,-1.81964821628992,7.49482233047317));
#408627=CARTESIAN_POINT('Origin',(2.06498228097549,-1.79715175465437,7.51860402984325));
#408628=CARTESIAN_POINT('Origin',(2.06498228097549,-1.79715175465437,9.));
#408629=CARTESIAN_POINT('Origin',(2.06498228097549,-1.79715175465437,8.75721825406948));
#408630=CARTESIAN_POINT('Ctrl Pts',(2.04579859637349,-1.80534509773718,
8.78942910404913));
#408631=CARTESIAN_POINT('Ctrl Pts',(2.05120799968458,-1.80668329970981,
8.7967269950169));
#408632=CARTESIAN_POINT('Ctrl Pts',(2.05490627375195,-1.79855949180312,
8.79893251111266));
#408633=CARTESIAN_POINT('Ctrl Pts',(2.05648070824781,-1.80794661741698,
8.78111911759577));
#408634=CARTESIAN_POINT('Ctrl Pts',(2.0628954061557,-1.80952584535372,8.78644465894812));
#408635=CARTESIAN_POINT('Ctrl Pts',(2.06775831860606,-1.80303989174028,
8.78817647674132));
#408636=CARTESIAN_POINT('Ctrl Pts',(2.06313805516787,-1.80956794650262,
8.76780923932035));
#408637=CARTESIAN_POINT('Ctrl Pts',(2.07071155334932,-1.81142721035319,
8.76988516158375));
#408638=CARTESIAN_POINT('Ctrl Pts',(2.07578916287304,-1.8058277227051,8.77093053738833));
#408639=CARTESIAN_POINT('Ctrl Pts',(2.06183996363106,-1.80925180951868,
8.75371302330491));
#408640=CARTESIAN_POINT('Ctrl Pts',(2.06922740267153,-1.81106618152883,
8.75300828287558));
#408641=CARTESIAN_POINT('Ctrl Pts',(2.07422297212532,-1.80528355019295,
8.75267964240738));
#408642=CARTESIAN_POINT('Origin',(2.05135792032744,-1.79383368616219,8.78727029226991));
#408643=CARTESIAN_POINT('Ctrl Pts',(1.97893795668432,-1.78906192937257,
8.85049129520029));
#408644=CARTESIAN_POINT('Ctrl Pts',(1.9846117360273,-1.79044371813726,8.85711686593484));
#408645=CARTESIAN_POINT('Ctrl Pts',(1.9884767993203,-1.78281731348926,8.85933012996512));
#408646=CARTESIAN_POINT('Ctrl Pts',(2.00212570220898,-1.79470905879152,
8.82945683644723));
#408647=CARTESIAN_POINT('Ctrl Pts',(2.00784657735092,-1.79610231723841,
8.83607469902389));
#408648=CARTESIAN_POINT('Ctrl Pts',(2.01168953666617,-1.78843656833835,
8.83829567148519));
#408649=CARTESIAN_POINT('Ctrl Pts',(2.02527888452907,-1.8003477707087,8.80838214965003));
#408650=CARTESIAN_POINT('Ctrl Pts',(2.03102233691534,-1.80174652760393,
8.81501364461986));
#408651=CARTESIAN_POINT('Ctrl Pts',(2.03486690419791,-1.79404794883865,
8.81722098428721));
#408652=CARTESIAN_POINT('Ctrl Pts',(2.04840012990614,-1.80597870472223,
8.78727029226991));
#408653=CARTESIAN_POINT('Ctrl Pts',(2.05414453629875,-1.80737769395556,
8.79393457792714));
#408654=CARTESIAN_POINT('Ctrl Pts',(2.05801159645807,-1.79965207029772,
8.79610912703474));
#408655=CARTESIAN_POINT('Origin',(1.98189574710561,-1.77691691081253,8.85049129520029));
#408656=CARTESIAN_POINT('Ctrl Pts',(1.97081848695447,-1.79800236791131,
8.85049129520029));
#408657=CARTESIAN_POINT('Ctrl Pts',(1.9727387040902,-1.80351724582245,8.85711686593484));
#408658=CARTESIAN_POINT('Ctrl Pts',(1.9655186752694,-1.80809675954562,8.85933012996512));
#408659=CARTESIAN_POINT('Ctrl Pts',(1.96911969857312,-1.79312343503143,
8.86332496987233));
#408660=CARTESIAN_POINT('Ctrl Pts',(1.96622788905522,-1.79672750663017,
8.86648636486738));
#408661=CARTESIAN_POINT('Ctrl Pts',(1.9607824254138,-1.79444211221725,8.87206031107456));
#408662=CARTESIAN_POINT('Ctrl Pts',(1.97388433684392,-1.78783117387533,
8.86341338519875));
#408663=CARTESIAN_POINT('Ctrl Pts',(1.97718275554805,-1.78457634597106,
8.86654584966058));
#408664=CARTESIAN_POINT('Ctrl Pts',(1.97432290905723,-1.77938544712438,
8.87215952290715));
#408665=CARTESIAN_POINT('Ctrl Pts',(1.97893795668432,-1.78906192937257,
8.85049129520029));
#408666=CARTESIAN_POINT('Ctrl Pts',(1.9846117360273,-1.79044371813726,8.85711686593484));
#408667=CARTESIAN_POINT('Ctrl Pts',(1.9884767993203,-1.78281731348926,8.85933012996512));
#408668=CARTESIAN_POINT('Origin',(1.95901360513968,-1.80211269214899,8.85049129520029));
#408669=CARTESIAN_POINT('Ctrl Pts',(1.99432705985486,-1.8655191643187,8.78727029226991));
#408670=CARTESIAN_POINT('Ctrl Pts',(1.99627117980082,-1.8711026912788,8.79393457792714));
#408671=CARTESIAN_POINT('Ctrl Pts',(1.98895258219517,-1.87569371995055,
8.79610912703474));
#408672=CARTESIAN_POINT('Ctrl Pts',(1.98650197380754,-1.84304545892765,
8.80838214965002));
#408673=CARTESIAN_POINT('Ctrl Pts',(1.98844577088239,-1.84862805859965,
8.81501364461993));
#408674=CARTESIAN_POINT('Ctrl Pts',(1.98115193336384,-1.85319410139922,
8.81722098428721));
#408675=CARTESIAN_POINT('Ctrl Pts',(1.97866607911547,-1.82054071102842,
8.82945683644721));
#408676=CARTESIAN_POINT('Ctrl Pts',(1.9806022352144,-1.82610136576058,8.83607469902388));
#408677=CARTESIAN_POINT('Ctrl Pts',(1.97334092145606,-1.83066265560013,
8.83829567148519));
#408678=CARTESIAN_POINT('Ctrl Pts',(1.97081848695447,-1.79800236791131,
8.85049129520029));
#408679=CARTESIAN_POINT('Ctrl Pts',(1.9727387040902,-1.80351724582245,8.85711686593484));
#408680=CARTESIAN_POINT('Ctrl Pts',(1.9655186752694,-1.80809675954562,8.85933012996512));
#408681=CARTESIAN_POINT('Origin',(1.98252217804007,-1.86962948855638,8.78727029226991));
#408682=CARTESIAN_POINT('Ctrl Pts',(1.99887714505915,-1.87858709900373,
8.75374538247848));
#408683=CARTESIAN_POINT('Ctrl Pts',(2.00138827335462,-1.88575917074565,
8.75304829418601));
#408684=CARTESIAN_POINT('Ctrl Pts',(1.99612174305393,-1.89128495592071,
8.75272238421917));
#408685=CARTESIAN_POINT('Ctrl Pts',(1.99931119033488,-1.87983367897014,
8.76769408445018));
#408686=CARTESIAN_POINT('Ctrl Pts',(2.00188485842239,-1.88718645990986,
8.76974318093969));
#408687=CARTESIAN_POINT('Ctrl Pts',(1.99680650103025,-1.89277471934172,
8.77077869880429));
#408688=CARTESIAN_POINT('Ctrl Pts',(1.99708652152473,-1.87344442018716,
8.78108014887992));
#408689=CARTESIAN_POINT('Ctrl Pts',(1.99927119857793,-1.87967438194253,
8.78639403366325));
#408690=CARTESIAN_POINT('Ctrl Pts',(1.9933043463902,-1.88514418547636,8.78812224174742));
#408691=CARTESIAN_POINT('Ctrl Pts',(1.99344078041233,-1.86297383549666,
8.78944554828685));
#408692=CARTESIAN_POINT('Ctrl Pts',(1.99528722758711,-1.86822236390449,
8.79673892988686));
#408693=CARTESIAN_POINT('Ctrl Pts',(1.98756562585767,-1.87268111048267,
8.79894799272499));
#408694=CARTESIAN_POINT('Origin',(1.98713316644801,-1.88287228159595,8.75721825406948));
#408695=CARTESIAN_POINT('Origin',(1.98713316644801,-1.88287228159595,9.));
#408696=CARTESIAN_POINT('Origin',(1.98713316644801,-1.88287228159595,7.51860402984325));
#408697=CARTESIAN_POINT('Ctrl Pts',(2.0065529847689,-1.87513140706529,7.50366195182966));
#408698=CARTESIAN_POINT('Ctrl Pts',(2.00922851137342,-1.8776316968682,7.50000065167735));
#408699=CARTESIAN_POINT('Ctrl Pts',(2.00922851137334,-1.87763169686828,
7.49482233047108));
#408700=CARTESIAN_POINT('Ctrl Pts',(2.00267706150172,-1.88148207777267,
7.50215800491337));
#408701=CARTESIAN_POINT('Ctrl Pts',(2.0027193514308,-1.88459702700761,7.49877273257264));
#408702=CARTESIAN_POINT('Ctrl Pts',(2.00036234457185,-1.88711926312202,
7.49481816995647));
#408703=CARTESIAN_POINT('Ctrl Pts',(1.99986519248849,-1.88142369117742,
7.51043025814041));
#408704=CARTESIAN_POINT('Ctrl Pts',(2.00020259949308,-1.88725283463937,
7.51006209594515));
#408705=CARTESIAN_POINT('Ctrl Pts',(1.99620509243912,-1.89147170978753,
7.50731281821699));
#408706=CARTESIAN_POINT('Ctrl Pts',(1.99893755118653,-1.87876053002942,
7.51860402984325));
#408707=CARTESIAN_POINT('Ctrl Pts',(2.00144054600743,-1.885946351786,7.51860402984325));
#408708=CARTESIAN_POINT('Ctrl Pts',(1.99620683387471,-1.89146987192287,
7.51860402984325));
#408709=CARTESIAN_POINT('Origin',(0.,0.,7.5));
#408710=CARTESIAN_POINT('Origin',(2.08196763624133,-1.66803740521006,7.5));
#408711=CARTESIAN_POINT('',(2.08196763624133,-1.66803740521006,7.59394543036555));
#408712=CARTESIAN_POINT('',(2.08196763624133,-1.66803740521006,8.85049129520029));
#408713=CARTESIAN_POINT('',(2.08196763624133,-1.66803740521006,7.5));
#408714=CARTESIAN_POINT('',(2.10975372425562,-1.73390928168091,8.78727029226991));
#408715=CARTESIAN_POINT('Ctrl Pts',(2.08196763624133,-1.66803740521006,
8.85049129520029));
#408716=CARTESIAN_POINT('Ctrl Pts',(2.09124312883604,-1.69002661441761,
8.82945686509571));
#408717=CARTESIAN_POINT('Ctrl Pts',(2.10050483228945,-1.71198313400677,
8.80838212259895));
#408718=CARTESIAN_POINT('Ctrl Pts',(2.10975372425562,-1.73390928168091,
8.78727029226991));
#408719=CARTESIAN_POINT('',(2.11520370755655,-1.74682943894027,8.75721825406948));
#408720=CARTESIAN_POINT('Origin',(2.09880300312937,-1.70794812528232,8.75937679713171));
#408721=CARTESIAN_POINT('',(2.11520370755655,-1.74682943894027,7.51860402984325));
#408722=CARTESIAN_POINT('',(2.11520370755655,-1.74682943894027,7.5));
#408723=CARTESIAN_POINT('Ctrl Pts',(2.11520370755655,-1.74682943894027,
7.51860402984325));
#408724=CARTESIAN_POINT('Ctrl Pts',(2.1109235933064,-1.73668266487759,7.52834476460825));
#408725=CARTESIAN_POINT('Ctrl Pts',(2.10664070046786,-1.7265293036756,7.53807742314407));
#408726=CARTESIAN_POINT('Ctrl Pts',(2.10235493574609,-1.71636913416235,
7.54780169004674));
#408727=CARTESIAN_POINT('Ctrl Pts',(2.09556651605263,-1.70027597476365,
7.5632044032688));
#408728=CARTESIAN_POINT('Ctrl Pts',(2.08877088254286,-1.68416571372708,
7.57858609112103));
#408729=CARTESIAN_POINT('Ctrl Pts',(2.08196763624133,-1.66803740521006,
7.59394543036555));
#408730=CARTESIAN_POINT('Origin',(2.36030818298168,-1.70641386443187,7.5));
#408731=CARTESIAN_POINT('',(2.17370988235716,-1.67346501623194,8.75721825406948));
#408732=CARTESIAN_POINT('',(2.15990092504106,-1.67102668085116,8.78727029226991));
#408733=CARTESIAN_POINT('Origin',(2.12484864088931,-1.6648372762011,8.75658640621081));
#408734=CARTESIAN_POINT('',(2.0894976077859,-1.65859511954943,8.85049129520029));
#408735=CARTESIAN_POINT('Ctrl Pts',(2.15990092504106,-1.67102668085116,
8.78727029226991));
#408736=CARTESIAN_POINT('Ctrl Pts',(2.13646643958855,-1.66688870477509,
8.80838212259895));
#408737=CARTESIAN_POINT('Ctrl Pts',(2.11299949288423,-1.66274499680943,
8.82945686509571));
#408738=CARTESIAN_POINT('Ctrl Pts',(2.0894976077859,-1.65859511954943,8.85049129520029));
#408739=CARTESIAN_POINT('',(2.0894976077859,-1.65859511954943,7.59394543036555));
#408740=CARTESIAN_POINT('',(2.0894976077859,-1.65859511954943,7.5));
#408741=CARTESIAN_POINT('',(2.17370988235716,-1.67346501623194,7.51860402984325));
#408742=CARTESIAN_POINT('Ctrl Pts',(2.0894976077859,-1.65859511954943,7.59394543036555));
#408743=CARTESIAN_POINT('Ctrl Pts',(2.10673541065637,-1.6616389079879,7.57858609112103));
#408744=CARTESIAN_POINT('Ctrl Pts',(2.12395392452868,-1.66467929044536,
7.56320440326857));
#408745=CARTESIAN_POINT('Ctrl Pts',(2.14115416031193,-1.66771644542441,
7.54780169004651));
#408746=CARTESIAN_POINT('Ctrl Pts',(2.15201326553151,-1.66963390666746,
7.53807742314383));
#408747=CARTESIAN_POINT('Ctrl Pts',(2.16286509408447,-1.67155008302322,
7.52834476460825));
#408748=CARTESIAN_POINT('Ctrl Pts',(2.17370988235716,-1.67346501623194,
7.51860402984325));
#408749=CARTESIAN_POINT('',(2.17370988235716,-1.67346501623194,7.5));
#408750=CARTESIAN_POINT('Origin',(2.08830213916384,-1.66536538392933,7.5));
#408751=CARTESIAN_POINT('Ctrl Pts',(2.0894976077859,-1.65859511954943,8.85049129520029));
#408752=CARTESIAN_POINT('Ctrl Pts',(2.08930689657204,-1.658561444458,8.85097269580138));
#408753=CARTESIAN_POINT('Ctrl Pts',(2.08911712890333,-1.65853647751089,
8.85143669361005));
#408754=CARTESIAN_POINT('Ctrl Pts',(2.08891945254858,-1.65851993587655,
8.8519052845931));
#408755=CARTESIAN_POINT('Ctrl Pts',(2.08853281013488,-1.65848758148882,
8.85282181883899));
#408756=CARTESIAN_POINT('Ctrl Pts',(2.08812584132941,-1.65848848817669,
8.85372622499636));
#408757=CARTESIAN_POINT('Ctrl Pts',(2.08769219444457,-1.658538088868,8.85462257735071));
#408758=CARTESIAN_POINT('Ctrl Pts',(2.08733219620246,-1.65857926560027,
8.85536669723987));
#408759=CARTESIAN_POINT('Ctrl Pts',(2.08695372646827,-1.65865397891724,
8.85610498449051));
#408760=CARTESIAN_POINT('Ctrl Pts',(2.08655466895923,-1.65877891590461,
8.85681338218371));
#408761=CARTESIAN_POINT('Ctrl Pts',(2.08619252364304,-1.65889229641687,
8.85745625420285));
#408762=CARTESIAN_POINT('Ctrl Pts',(2.08580870152052,-1.65904789017867,
8.85808743050667));
#408763=CARTESIAN_POINT('Ctrl Pts',(2.08540145248205,-1.65927424159866,
8.85866804508412));
#408764=CARTESIAN_POINT('Ctrl Pts',(2.08521355660378,-1.65937867523714,
8.85893592806396));
#408765=CARTESIAN_POINT('Ctrl Pts',(2.0850206879786,-1.65949841300904,8.85919241173849));
#408766=CARTESIAN_POINT('Ctrl Pts',(2.0848229894418,-1.65963782316052,8.85943017985534));
#408767=CARTESIAN_POINT('Ctrl Pts',(2.08455603789209,-1.65982606813484,
8.8597512372));
#408768=CARTESIAN_POINT('Ctrl Pts',(2.08427385450003,-1.66005549655851,
8.86004599534705));
#408769=CARTESIAN_POINT('Ctrl Pts',(2.08398639993717,-1.66033143307005,
8.86026130871721));
#408770=CARTESIAN_POINT('Ctrl Pts',(2.0838811547175,-1.66043246120639,8.86034014101235));
#408771=CARTESIAN_POINT('Ctrl Pts',(2.08377361346507,-1.66054123240651,
8.86040910639692));
#408772=CARTESIAN_POINT('Ctrl Pts',(2.08366694528517,-1.66065501975951,
8.86046313645506));
#408773=CARTESIAN_POINT('Ctrl Pts',(2.08350049048377,-1.66083258397089,
8.86054744990829));
#408774=CARTESIAN_POINT('Ctrl Pts',(2.08333172529108,-1.66102731071897,
8.86059655985668));
#408775=CARTESIAN_POINT('Ctrl Pts',(2.08317125174908,-1.66122651971647,
8.86059725258816));
#408776=CARTESIAN_POINT('Ctrl Pts',(2.0830104074491,-1.66142618896635,8.86059794692011));
#408777=CARTESIAN_POINT('Ctrl Pts',(2.08285817834937,-1.66163424222321,
8.86056369958365));
#408778=CARTESIAN_POINT('Ctrl Pts',(2.08271983012948,-1.66183711006154,
8.86048590497774));
#408779=CARTESIAN_POINT('Ctrl Pts',(2.08268372536321,-1.66189005252724,
8.86046560290182));
#408780=CARTESIAN_POINT('Ctrl Pts',(2.082648171092,-1.66194338162272,8.86044257503091));
#408781=CARTESIAN_POINT('Ctrl Pts',(2.08261423865959,-1.66199543122556,
8.86041778462583));
#408782=CARTESIAN_POINT('Ctrl Pts',(2.0823859154961,-1.66234566046448,8.86025097596201));
#408783=CARTESIAN_POINT('Ctrl Pts',(2.08220066310881,-1.6626851365096,8.8599848982295));
#408784=CARTESIAN_POINT('Ctrl Pts',(2.08205645133815,-1.66299989246576,
8.85968173251461));
#408785=CARTESIAN_POINT('Ctrl Pts',(2.08198017157382,-1.66316638033319,
8.85952137522076));
#408786=CARTESIAN_POINT('Ctrl Pts',(2.08191373021563,-1.66332908163805,
8.85934740853961));
#408787=CARTESIAN_POINT('Ctrl Pts',(2.08185662505613,-1.66348511422397,
8.8591675900182));
#408788=CARTESIAN_POINT('Ctrl Pts',(2.08162731815808,-1.66411166616059,
8.85844552518695));
#408789=CARTESIAN_POINT('Ctrl Pts',(2.08153275038139,-1.66466506031438,
8.85759444184123));
#408790=CARTESIAN_POINT('Ctrl Pts',(2.08149617274034,-1.6651231938448,8.85683498915137));
#408791=CARTESIAN_POINT('Ctrl Pts',(2.08149234498762,-1.66517113629864,
8.85675551444997));
#408792=CARTESIAN_POINT('Ctrl Pts',(2.08148917211988,-1.66521803320865,
8.85667699793651));
#408793=CARTESIAN_POINT('Ctrl Pts',(2.0814865791298,-1.66526385703585,8.85659965593547));
#408794=CARTESIAN_POINT('Ctrl Pts',(2.08145157881729,-1.66588238939369,
8.85555568965886));
#408795=CARTESIAN_POINT('Ctrl Pts',(2.08150726966,-1.66648189204854,8.85434650606346));
#408796=CARTESIAN_POINT('Ctrl Pts',(2.08164773886711,-1.66706590344665,
8.85297329937117));
#408797=CARTESIAN_POINT('Ctrl Pts',(2.08172674423719,-1.66739437427376,
8.85220095427747));
#408798=CARTESIAN_POINT('Ctrl Pts',(2.08183290683989,-1.66771800513891,
8.85137579139183));
#408799=CARTESIAN_POINT('Ctrl Pts',(2.08196763624133,-1.66803740521006,
8.85049129520029));
#408800=CARTESIAN_POINT('Origin',(2.08830213916384,-1.66536538392933,7.59394543036555));
#408801=CARTESIAN_POINT('Ctrl Pts',(2.08894390879625,-1.65849734939881,
7.59443877723642));
#408802=CARTESIAN_POINT('Ctrl Pts',(2.08324134195779,-1.6574904109193,7.58783886950016));
#408803=CARTESIAN_POINT('Ctrl Pts',(2.07987060264358,-1.66528254143747,
7.58559994247159));
#408804=CARTESIAN_POINT('Ctrl Pts',(2.12007405386126,-1.66399419701615,
7.56670252222138));
#408805=CARTESIAN_POINT('Ctrl Pts',(2.11437972885085,-1.66298871384865,
7.56004874999029));
#408806=CARTESIAN_POINT('Ctrl Pts',(2.1109694072583,-1.67081853274127,7.55786368756705));
#408807=CARTESIAN_POINT('Ctrl Pts',(2.15114606649061,-1.66948077981977,
7.5388891333356));
#408808=CARTESIAN_POINT('Ctrl Pts',(2.14541789982785,-1.66846932101654,
7.53222002137277));
#408809=CARTESIAN_POINT('Ctrl Pts',(2.14201144419061,-1.67634323393906,
7.53005029815326));
#408810=CARTESIAN_POINT('Ctrl Pts',(2.18215854065473,-1.67495684953808,
7.51101258149734));
#408811=CARTESIAN_POINT('Ctrl Pts',(2.1763609382037,-1.67393313001629,7.5043616886572));
#408812=CARTESIAN_POINT('Ctrl Pts',(2.1729951652485,-1.68185645343255,7.50217374673251));
#408813=CARTESIAN_POINT('',(2.17134183427229,-1.68156225994654,7.50366116523517));
#408814=CARTESIAN_POINT('Ctrl Pts',(2.17370988235716,-1.67346501623194,
7.51860402984325));
#408815=CARTESIAN_POINT('Ctrl Pts',(2.17414476594742,-1.67354180639215,
7.51734760759493));
#408816=CARTESIAN_POINT('Ctrl Pts',(2.1745273997738,-1.67366978769892,7.51608817408573));
#408817=CARTESIAN_POINT('Ctrl Pts',(2.17485266796472,-1.67386132982701,
7.5148100591312));
#408818=CARTESIAN_POINT('Ctrl Pts',(2.17514730366459,-1.67403483326368,
7.51365231206384));
#408819=CARTESIAN_POINT('Ctrl Pts',(2.17539541214572,-1.67426051842923,
7.51247773061043));
#408820=CARTESIAN_POINT('Ctrl Pts',(2.17556785381776,-1.67456179524134,
7.51129758471022));
#408821=CARTESIAN_POINT('Ctrl Pts',(2.17578217912252,-1.67493624791169,
7.50983079813401));
#408822=CARTESIAN_POINT('Ctrl Pts',(2.17586147291357,-1.67542199142967,
7.50839324291155));
#408823=CARTESIAN_POINT('Ctrl Pts',(2.17572495125419,-1.67603585273913,
7.50715379678855));
#408824=CARTESIAN_POINT('Ctrl Pts',(2.17566188218133,-1.67631943897611,
7.50658120839351));
#408825=CARTESIAN_POINT('Ctrl Pts',(2.17553451338757,-1.67666861935894,
7.50598221009429));
#408826=CARTESIAN_POINT('Ctrl Pts',(2.17532450682395,-1.67706728913404,
7.50545747549611));
#408827=CARTESIAN_POINT('Ctrl Pts',(2.17521244082129,-1.67728003166601,
7.50517746087247));
#408828=CARTESIAN_POINT('Ctrl Pts',(2.17507580668922,-1.67750926816192,
7.50491486231392));
#408829=CARTESIAN_POINT('Ctrl Pts',(2.17491678992053,-1.6777480740414,7.50468370960992));
#408830=CARTESIAN_POINT('Ctrl Pts',(2.17467900969235,-1.67810516415827,
7.50433806340446));
#408831=CARTESIAN_POINT('Ctrl Pts',(2.17438358912055,-1.67849405035301,
7.50405484070983));
#408832=CARTESIAN_POINT('Ctrl Pts',(2.17404985377076,-1.67888810850845,
7.50385766036131));
#408833=CARTESIAN_POINT('Ctrl Pts',(2.17401416596252,-1.67893024690312,
7.50383657498791));
#408834=CARTESIAN_POINT('Ctrl Pts',(2.17397806681485,-1.678972435125,7.50381643264937));
#408835=CARTESIAN_POINT('Ctrl Pts',(2.17394159952656,-1.67901463415508,
7.50379723213559));
#408836=CARTESIAN_POINT('Ctrl Pts',(2.17369816844787,-1.67929632648512,
7.50366906242519));
#408837=CARTESIAN_POINT('Ctrl Pts',(2.17343249378542,-1.67958415773683,
7.50358235568538));
#408838=CARTESIAN_POINT('Ctrl Pts',(2.17316974716839,-1.679855436059,7.5035341175365));
#408839=CARTESIAN_POINT('Ctrl Pts',(2.17277578835334,-1.68026218720031,
7.50346178989176));
#408840=CARTESIAN_POINT('Ctrl Pts',(2.17233468372927,-1.68068300819468,
7.50346967198527));
#408841=CARTESIAN_POINT('Ctrl Pts',(2.17188894406666,-1.68108279974466,
7.50354272648692));
#408842=CARTESIAN_POINT('Ctrl Pts',(2.17170560211717,-1.68124724228436,
7.50357277531559));
#408843=CARTESIAN_POINT('Ctrl Pts',(2.17152181426858,-1.68140801403177,
7.50361331098761));
#408844=CARTESIAN_POINT('Ctrl Pts',(2.17134183427341,-1.68156225994741,
7.50366116523659));
#408845=CARTESIAN_POINT('',(2.09059128324979,-1.66719091542144,7.57603338622103));
#408846=CARTESIAN_POINT('Origin',(2.09749850102558,-1.67270288713781,7.58486873427625));
#408847=CARTESIAN_POINT('Ctrl Pts',(2.17134183432944,-1.68156225995127,
7.50366116529969));
#408848=CARTESIAN_POINT('Ctrl Pts',(2.14446876028218,-1.67678045171056,
7.52783573079709));
#408849=CARTESIAN_POINT('Ctrl Pts',(2.1175531776842,-1.67199024736115,7.55196141284068));
#408850=CARTESIAN_POINT('Ctrl Pts',(2.09059128449425,-1.66719091528372,
7.57603338728831));
#408851=CARTESIAN_POINT('Ctrl Pts',(2.09047977720881,-1.65894708367393,
7.59639677331371));
#408852=CARTESIAN_POINT('Ctrl Pts',(2.07320936503687,-1.65296337419233,
7.59959882295466));
#408853=CARTESIAN_POINT('Ctrl Pts',(2.08243570482692,-1.66876158506196,
7.59642833564546));
#408854=CARTESIAN_POINT('Ctrl Pts',(2.0870472649161,-1.65709425787419,7.58707626057422));
#408855=CARTESIAN_POINT('Ctrl Pts',(2.08056667580056,-1.65907270568797,
7.58809943920599));
#408856=CARTESIAN_POINT('Ctrl Pts',(2.07997313262296,-1.66580784542589,
7.58710240504252));
#408857=CARTESIAN_POINT('Ctrl Pts',(2.08871246990533,-1.66293829112234,
7.58015376756929));
#408858=CARTESIAN_POINT('Ctrl Pts',(2.08590041445979,-1.66340905174838,
7.5820588065976));
#408859=CARTESIAN_POINT('Ctrl Pts',(2.08602293135981,-1.66622189099856,
7.58020924244128));
#408860=CARTESIAN_POINT('Ctrl Pts',(2.09059128260289,-1.6671909149053,7.57603338509286));
#408861=CARTESIAN_POINT('Ctrl Pts',(2.09059128260289,-1.6671909149053,7.57603338509286));
#408862=CARTESIAN_POINT('Ctrl Pts',(2.09059128260289,-1.6671909149053,7.57603338509286));
#408863=CARTESIAN_POINT('Origin',(2.09750205887835,-1.67269842573215,7.58486873427623));
#408864=CARTESIAN_POINT('Ctrl Pts',(2.11854867954592,-1.75475929151861,
7.51098857897448));
#408865=CARTESIAN_POINT('Ctrl Pts',(2.11626052846283,-1.74933482135159,
7.50433767179956));
#408866=CARTESIAN_POINT('Ctrl Pts',(2.12323627878781,-1.74429032350879,
7.50214974420965));
#408867=CARTESIAN_POINT('Ctrl Pts',(2.10630546116131,-1.72573455911936,
7.53887321589167));
#408868=CARTESIAN_POINT('Ctrl Pts',(2.10404472618893,-1.72037508373164,
7.53220407452062));
#408869=CARTESIAN_POINT('Ctrl Pts',(2.11096323199481,-1.71530189958989,
7.53003438070911));
#408870=CARTESIAN_POINT('Ctrl Pts',(2.09403873128106,-1.69665408852713,
7.56669465659231));
#408871=CARTESIAN_POINT('Ctrl Pts',(2.09179135683201,-1.69132628664256,
7.56004085833298));
#408872=CARTESIAN_POINT('Ctrl Pts',(2.0986660010435,-1.68625914572364,7.5578558219379));
#408873=CARTESIAN_POINT('Ctrl Pts',(2.08174904468028,-1.66751919493522,
7.59443891967696));
#408874=CARTESIAN_POINT('Ctrl Pts',(2.07949841181814,-1.66218366840122,
7.58783901202978));
#408875=CARTESIAN_POINT('Ctrl Pts',(2.08634511706896,-1.65716352844334,
7.58560008491213));
#408876=CARTESIAN_POINT('',(2.12257099619415,-1.7427189565311,7.50366116523517));
#408877=CARTESIAN_POINT('Ctrl Pts',(2.12257099619444,-1.74271895653134,
7.50366116523554));
#408878=CARTESIAN_POINT('Ctrl Pts',(2.12221815692832,-1.74338951001097,
7.50350835821027));
#408879=CARTESIAN_POINT('Ctrl Pts',(2.12187199624794,-1.74399443215018,
7.50345484956));
#408880=CARTESIAN_POINT('Ctrl Pts',(2.12152274371401,-1.74455200602683,
7.50349758195598));
#408881=CARTESIAN_POINT('Ctrl Pts',(2.12134355126286,-1.74483808277631,
7.50351950684424));
#408882=CARTESIAN_POINT('Ctrl Pts',(2.12114599266842,-1.74513996091746,
7.50357029184312));
#408883=CARTESIAN_POINT('Ctrl Pts',(2.1209474874919,-1.74542582197774,7.50365515313924));
#408884=CARTESIAN_POINT('Ctrl Pts',(2.12064210614773,-1.74586559204501,
7.50378570417639));
#408885=CARTESIAN_POINT('Ctrl Pts',(2.12032580549606,-1.74628056165416,
7.50400001621911));
#408886=CARTESIAN_POINT('Ctrl Pts',(2.12002085492926,-1.74663776925505,
7.50428903009635));
#408887=CARTESIAN_POINT('Ctrl Pts',(2.1199870077625,-1.74667741655056,7.50432110841318));
#408888=CARTESIAN_POINT('Ctrl Pts',(2.11995329730375,-1.7467163824137,7.50435406373354));
#408889=CARTESIAN_POINT('Ctrl Pts',(2.11991975139974,-1.74675464400065,
7.50438785222352));
#408890=CARTESIAN_POINT('Ctrl Pts',(2.11971493753152,-1.74698824937982,
7.50459414719561));
#408891=CARTESIAN_POINT('Ctrl Pts',(2.119512609103,-1.74719898075729,7.50483629897752));
#408892=CARTESIAN_POINT('Ctrl Pts',(2.11932146656589,-1.74737967653142,
7.5050991045531));
#408893=CARTESIAN_POINT('Ctrl Pts',(2.11889978693059,-1.74777830955832,
7.50567888004914));
#408894=CARTESIAN_POINT('Ctrl Pts',(2.11851628850652,-1.74804684943359,
7.50637912803144));
#408895=CARTESIAN_POINT('Ctrl Pts',(2.11818147603026,-1.74821436622545,
7.50710440483569));
#408896=CARTESIAN_POINT('Ctrl Pts',(2.11809937336412,-1.74825544466849,
7.50728225710685));
#408897=CARTESIAN_POINT('Ctrl Pts',(2.1180186292097,-1.74829139658335,7.50746498566954));
#408898=CARTESIAN_POINT('Ctrl Pts',(2.11794129784966,-1.74832176330876,
7.50764697238949));
#408899=CARTESIAN_POINT('Ctrl Pts',(2.11752558574023,-1.74848500646745,
7.50862528291181));
#408900=CARTESIAN_POINT('Ctrl Pts',(2.11717227348489,-1.74850551793846,
7.50965856837421));
#408901=CARTESIAN_POINT('Ctrl Pts',(2.11686727706473,-1.74844808225894,
7.51067959873201));
#408902=CARTESIAN_POINT('Ctrl Pts',(2.11669943715001,-1.74841647533206,
7.51124147302578));
#408903=CARTESIAN_POINT('Ctrl Pts',(2.11654626822342,-1.74836082893675,
7.51180065547252));
#408904=CARTESIAN_POINT('Ctrl Pts',(2.11640602292634,-1.74828929035804,
7.512351757165));
#408905=CARTESIAN_POINT('Ctrl Pts',(2.11592141955783,-1.74804209607102,
7.51425603304536));
#408906=CARTESIAN_POINT('Ctrl Pts',(2.11553609727354,-1.74757027707511,
7.5162690050518));
#408907=CARTESIAN_POINT('Ctrl Pts',(2.11524938375526,-1.74693418413987,
7.51827788969244));
#408908=CARTESIAN_POINT('Ctrl Pts',(2.11523386627784,-1.74689975758816,
7.51838661432545));
#408909=CARTESIAN_POINT('Ctrl Pts',(2.11521864057724,-1.74686484032868,
7.51849533314856));
#408910=CARTESIAN_POINT('Ctrl Pts',(2.11520370755655,-1.74682943894028,
7.51860402984325));
#408911=CARTESIAN_POINT('Ctrl Pts',(2.09059128339322,-1.66719091666627,
7.57603338728985));
#408912=CARTESIAN_POINT('Ctrl Pts',(2.10126987185163,-1.69240886705183,
7.55196141284922));
#408913=CARTESIAN_POINT('Ctrl Pts',(2.11192925636358,-1.71758369907425,
7.52783573083104));
#408914=CARTESIAN_POINT('Ctrl Pts',(2.12257099621212,-1.74271895658749,
7.50366116530176));
#408915=CARTESIAN_POINT('Origin',(7.22395927215206E-16,-5.76091528191146E-16,
7.49482233047033));
#408916=CARTESIAN_POINT('Origin',(2.16435357359296,-1.67615030903418,7.49482233047033));
#408917=CARTESIAN_POINT('Origin',(0.,0.,7.50366116523517));
#408918=CARTESIAN_POINT('Origin',(2.11573969989724,-1.73711017850876,7.49482233047033));
#408919=CARTESIAN_POINT('Ctrl Pts',(2.17370884075828,-1.67346483226476,
7.51860402984325));
#408920=CARTESIAN_POINT('Ctrl Pts',(2.18120177269763,-1.67478856070453,
7.51860402984325));
#408921=CARTESIAN_POINT('Ctrl Pts',(2.18581900259087,-1.66874062931082,
7.51860402984325));
#408922=CARTESIAN_POINT('Ctrl Pts',(2.17649101774286,-1.67395634041669,
7.51041458714365));
#408923=CARTESIAN_POINT('Ctrl Pts',(2.18229563947575,-1.67335573047827,
7.51004642900441));
#408924=CARTESIAN_POINT('Ctrl Pts',(2.18582027596805,-1.66873896136315,
7.50729136483009));
#408925=CARTESIAN_POINT('Ctrl Pts',(2.17698761422762,-1.6767271036925,7.50215815450138));
#408926=CARTESIAN_POINT('Ctrl Pts',(2.18006852915933,-1.67627320098811,
7.49877163671531));
#408927=CARTESIAN_POINT('Ctrl Pts',(2.18218107690716,-1.67354536932037,
7.49481588533172));
#408928=CARTESIAN_POINT('Ctrl Pts',(2.17134139901514,-1.68156192286894,
7.50366171572174));
#408929=CARTESIAN_POINT('Ctrl Pts',(2.17423646662283,-1.68380396341364,
7.50000045605858));
#408930=CARTESIAN_POINT('Ctrl Pts',(2.17423646662291,-1.68380396341354,
7.49482233047317));
#408931=CARTESIAN_POINT('Origin',(2.17588346167,-1.66115544463214,7.51860402984325));
#408932=CARTESIAN_POINT('Origin',(2.17588346167,-1.66115544463214,9.));
#408933=CARTESIAN_POINT('Origin',(2.17588346167,-1.66115544463214,8.75721825406948));
#408934=CARTESIAN_POINT('Ctrl Pts',(2.15726414129915,-1.67056105650534,
8.78942910404913));
#408935=CARTESIAN_POINT('Ctrl Pts',(2.16274816930576,-1.6715499273384,8.79672699501691));
#408936=CARTESIAN_POINT('Ctrl Pts',(2.16591835071274,-1.66320586143327,
8.79893251111267));
#408937=CARTESIAN_POINT('Ctrl Pts',(2.16809098556714,-1.6724728258263,8.78111911759577));
#408938=CARTESIAN_POINT('Ctrl Pts',(2.17459368527149,-1.67363781796379,
8.7864446589481));
#408939=CARTESIAN_POINT('Ctrl Pts',(2.1790310498719,-1.66685362256725,8.78817647674132));
#408940=CARTESIAN_POINT('Ctrl Pts',(2.17483853316514,-1.67366428603579,
8.76780923932034));
#408941=CARTESIAN_POINT('Ctrl Pts',(2.18251559422625,-1.67503449413487,
8.76988516158376));
#408942=CARTESIAN_POINT('Ctrl Pts',(2.18722401085122,-1.66912118767553,
8.77093053738833));
#408943=CARTESIAN_POINT('Ctrl Pts',(2.1735228537305,-1.67343196759951,8.75371302330491));
#408944=CARTESIAN_POINT('Ctrl Pts',(2.18101136169898,-1.67476929694335,
8.75300828287558));
#408945=CARTESIAN_POINT('Ctrl Pts',(2.1856261727578,-1.66867847940991,8.75267964240738));
#408946=CARTESIAN_POINT('Origin',(2.1620745043539,-1.65871710925135,8.78727029226991));
#408947=CARTESIAN_POINT('Ctrl Pts',(2.0894976077859,-1.65859511954943,8.85049129520029));
#408948=CARTESIAN_POINT('Ctrl Pts',(2.09524826125083,-1.65961054899028,
8.85711686593484));
#408949=CARTESIAN_POINT('Ctrl Pts',(2.09861675793331,-1.65175217815314,
8.85933012996512));
#408950=CARTESIAN_POINT('Ctrl Pts',(2.11299952442464,-1.66274500237873,
8.82945683644724));
#408951=CARTESIAN_POINT('Ctrl Pts',(2.11879791179024,-1.66376886049788,
8.83607469902391));
#408952=CARTESIAN_POINT('Ctrl Pts',(2.12214182911506,-1.65587264245236,
8.83829567148519));
#408953=CARTESIAN_POINT('Ctrl Pts',(2.13646640956141,-1.66688869947301,
8.80838214965002));
#408954=CARTESIAN_POINT('Ctrl Pts',(2.14228768007077,-1.66791659821434,
8.81501364461988));
#408955=CARTESIAN_POINT('Ctrl Pts',(2.14563109864249,-1.65998751473328,
8.81722098428721));
#408956=CARTESIAN_POINT('Ctrl Pts',(2.15990092504106,-1.67102668085116,
8.78727029226991));
#408957=CARTESIAN_POINT('Ctrl Pts',(2.16572316248258,-1.67205475032983,
8.79393457792714));
#408958=CARTESIAN_POINT('Ctrl Pts',(2.16908729494481,-1.66409723639929,
8.79610912703474));
#408959=CARTESIAN_POINT('Origin',(2.09167118709874,-1.64628554794962,8.85049129520029));
#408960=CARTESIAN_POINT('Ctrl Pts',(2.08196763624133,-1.66803740521006,
8.85049129520029));
#408961=CARTESIAN_POINT('Ctrl Pts',(2.08423724752594,-1.67341792347876,
8.85711686593484));
#408962=CARTESIAN_POINT('Ctrl Pts',(2.07732546348034,-1.67845061693465,
8.85933012996512));
#408963=CARTESIAN_POINT('Ctrl Pts',(2.07995974390002,-1.66327733836634,
8.86332496987231));
#408964=CARTESIAN_POINT('Ctrl Pts',(2.07730478957507,-1.66705928388541,
8.86648636486738));
#408965=CARTESIAN_POINT('Ctrl Pts',(2.07172408849994,-1.66512747711382,
8.87206031107456));
#408966=CARTESIAN_POINT('Ctrl Pts',(2.08437551637402,-1.65769067930624,
8.86341338519877));
#408967=CARTESIAN_POINT('Ctrl Pts',(2.08745862058335,-1.654231208383,8.86654584966059));
#408968=CARTESIAN_POINT('Ctrl Pts',(2.08427206792285,-1.6492342057885,8.87215952290715));
#408969=CARTESIAN_POINT('Ctrl Pts',(2.0894976077859,-1.65859511954943,8.85049129520029));
#408970=CARTESIAN_POINT('Ctrl Pts',(2.09524826125083,-1.65961054899028,
8.85711686593484));
#408971=CARTESIAN_POINT('Ctrl Pts',(2.09861675793331,-1.65175217815314,
8.85933012996512));
#408972=CARTESIAN_POINT('Origin',(2.07045035820039,-1.67289562572048,8.85049129520029));
#408973=CARTESIAN_POINT('Ctrl Pts',(2.10975372425562,-1.73390928168091,
8.78727029226991));
#408974=CARTESIAN_POINT('Ctrl Pts',(2.11205158759924,-1.73935677649344,
8.79393457792714));
#408975=CARTESIAN_POINT('Ctrl Pts',(2.10504217505423,-1.74440727656294,
8.79610912703474));
#408976=CARTESIAN_POINT('Ctrl Pts',(2.10050482043863,-1.7119831059123,8.80838214965002));
#408977=CARTESIAN_POINT('Ctrl Pts',(2.10280230216297,-1.7174296960283,8.81501364461987));
#408978=CARTESIAN_POINT('Ctrl Pts',(2.09581599798248,-1.72245367517762,
8.81722098428721));
#408979=CARTESIAN_POINT('Ctrl Pts',(2.0912431412841,-1.69002664392795,8.82945683644722));
#408980=CARTESIAN_POINT('Ctrl Pts',(2.09353159171462,-1.69545182375141,
8.8360746990239));
#408981=CARTESIAN_POINT('Ctrl Pts',(2.08657743994755,-1.70046897590161,
8.8382956714852));
#408982=CARTESIAN_POINT('Ctrl Pts',(2.08196763624133,-1.66803740521006,
8.85049129520029));
#408983=CARTESIAN_POINT('Ctrl Pts',(2.08423724752594,-1.67341792347876,
8.85711686593484));
#408984=CARTESIAN_POINT('Ctrl Pts',(2.07732546348034,-1.67845061693465,
8.85933012996512));
#408985=CARTESIAN_POINT('Origin',(2.09823644621469,-1.73876750219133,8.78727029226991));
#408986=CARTESIAN_POINT('Ctrl Pts',(2.11513172627182,-1.74665884193262,
8.75374538247848));
#408987=CARTESIAN_POINT('Ctrl Pts',(2.11809721139911,-1.75365528934166,
8.75304829418601));
#408988=CARTESIAN_POINT('Ctrl Pts',(2.1131955400215,-1.75950714895335,8.75272238421917));
#408989=CARTESIAN_POINT('Ctrl Pts',(2.11564474840766,-1.74787505129053,
8.7676940844502));
#408990=CARTESIAN_POINT('Ctrl Pts',(2.11868422291036,-1.75504782967268,
8.76974318093972));
#408991=CARTESIAN_POINT('Ctrl Pts',(2.11397434055922,-1.76094997890145,
8.7707786988043));
#408992=CARTESIAN_POINT('Ctrl Pts',(2.11301528920241,-1.74164145494495,
8.78108014887988));
#408993=CARTESIAN_POINT('Ctrl Pts',(2.11559463262245,-1.74771864383637,
8.78639403366322));
#408994=CARTESIAN_POINT('Ctrl Pts',(2.10999049148817,-1.75355950660447,
8.78812224174741));
#408995=CARTESIAN_POINT('Ctrl Pts',(2.10870618599171,-1.73142596662878,
8.78944554828685));
#408996=CARTESIAN_POINT('Ctrl Pts',(2.11088511381241,-1.73654540909541,
8.79673892988686));
#408997=CARTESIAN_POINT('Ctrl Pts',(2.10346504981595,-1.74148971942196,
8.79894799272499));
#408998=CARTESIAN_POINT('Origin',(2.10368642951562,-1.75168765945069,8.75721825406948));
#408999=CARTESIAN_POINT('Origin',(2.10368642951562,-1.75168765945069,9.));
#409000=CARTESIAN_POINT('Origin',(2.10368642951562,-1.75168765945069,7.51860402984325));
#409001=CARTESIAN_POINT('Ctrl Pts',(2.12257038820298,-1.74271845734516,
7.50366195182966));
#409002=CARTESIAN_POINT('Ctrl Pts',(2.12540061176883,-1.7450421884564,7.50000065167736));
#409003=CARTESIAN_POINT('Ctrl Pts',(2.12540061176876,-1.74504218845649,
7.49482233047108));
#409004=CARTESIAN_POINT('Ctrl Pts',(2.11910931730509,-1.74930441117483,
7.50215800491336));
#409005=CARTESIAN_POINT('Ctrl Pts',(2.11935109582767,-1.75241025088743,
7.49877273257264));
#409006=CARTESIAN_POINT('Ctrl Pts',(2.11716053191481,-1.75507831874518,
7.49481816995647));
#409007=CARTESIAN_POINT('Ctrl Pts',(2.11629948473631,-1.74942630160732,
7.51043025814042));
#409008=CARTESIAN_POINT('Ctrl Pts',(2.11700967300596,-1.75522185072786,
7.51006209594515));
#409009=CARTESIAN_POINT('Ctrl Pts',(2.11329068351776,-1.75968817890087,
7.50731281821699));
#409010=CARTESIAN_POINT('Ctrl Pts',(2.11520312005231,-1.74682804639181,
7.51860402984325));
#409011=CARTESIAN_POINT('Ctrl Pts',(2.11816136938258,-1.75383873667812,
7.51860402984324));
#409012=CARTESIAN_POINT('Ctrl Pts',(2.11329230362299,-1.75968623323814,
7.51860402984325));
#409013=CARTESIAN_POINT('Origin',(0.,0.,7.5));
#409014=CARTESIAN_POINT('Origin',(2.1845615339302,-1.5312181190179,7.5));
#409015=CARTESIAN_POINT('',(2.1845615339302,-1.5312181190179,7.59394543036555));
#409016=CARTESIAN_POINT('',(2.1845615339302,-1.5312181190179,8.85049129520029));
#409017=CARTESIAN_POINT('',(2.1845615339302,-1.5312181190179,7.5));
#409018=CARTESIAN_POINT('',(2.21651095806265,-1.59517439388233,8.78727029226991));
#409019=CARTESIAN_POINT('Ctrl Pts',(2.1845615339302,-1.5312181190179,8.85049129520029));
#409020=CARTESIAN_POINT('Ctrl Pts',(2.19522682250172,-1.55256786618582,
8.82945686509571));
#409021=CARTESIAN_POINT('Ctrl Pts',(2.20587625583215,-1.573885874373,8.80838212259895));
#409022=CARTESIAN_POINT('Ctrl Pts',(2.21651095806265,-1.59517439388233,
8.78727029226991));
#409023=CARTESIAN_POINT('',(2.22277754110618,-1.60771882366393,8.75721825406948));
#409024=CARTESIAN_POINT('Origin',(2.20391939936576,-1.56996819257488,8.75937679713147));
#409025=CARTESIAN_POINT('',(2.22277754110618,-1.60771882366393,7.51860402984325));
#409026=CARTESIAN_POINT('',(2.22277754110618,-1.60771882366393,7.5));
#409027=CARTESIAN_POINT('Ctrl Pts',(2.22277754110618,-1.60771882366393,
7.51860402984325));
#409028=CARTESIAN_POINT('Ctrl Pts',(2.21785611476351,-1.59786712509835,
7.52834476460825));
#409029=CARTESIAN_POINT('Ctrl Pts',(2.21293149350188,-1.58800903095222,
7.53807742314407));
#409030=CARTESIAN_POINT('Ctrl Pts',(2.20800357004763,-1.57814432648541,
7.54780169004674));
#409031=CARTESIAN_POINT('Ctrl Pts',(2.20019800562762,-1.56251916775177,
7.5632044032688));
#409032=CARTESIAN_POINT('Ctrl Pts',(2.19238414650717,-1.54687740470819,
7.57858609112103));
#409033=CARTESIAN_POINT('Ctrl Pts',(2.1845615339302,-1.5312181190179,7.59394543036555));
#409034=CARTESIAN_POINT('Origin',(2.46478898834977,-1.55168238962917,7.5));
#409035=CARTESIAN_POINT('',(2.27646303399421,-1.53075663254066,8.75721825406948));
#409036=CARTESIAN_POINT('',(2.26252622397769,-1.52920804991437,8.78727029226991));
#409037=CARTESIAN_POINT('Origin',(2.22714940198636,-1.5252771696165,8.75658640621103));
#409038=CARTESIAN_POINT('',(2.19147106502126,-1.52131278661253,8.85049129520029));
#409039=CARTESIAN_POINT('Ctrl Pts',(2.26252622397769,-1.52920804991437,
8.78727029226991));
#409040=CARTESIAN_POINT('Ctrl Pts',(2.23887476615141,-1.52658002839203,
8.80838212259895));
#409041=CARTESIAN_POINT('Ctrl Pts',(2.21519054652502,-1.52394836655642,
8.82945686509571));
#409042=CARTESIAN_POINT('Ctrl Pts',(2.19147106502126,-1.52131278661253,
8.85049129520029));
#409043=CARTESIAN_POINT('',(2.19147106502126,-1.52131278661253,7.59394543036555));
#409044=CARTESIAN_POINT('',(2.19147106502126,-1.52131278661253,7.5));
#409045=CARTESIAN_POINT('',(2.27646303399421,-1.53075663254066,7.51860402984325));
#409046=CARTESIAN_POINT('Ctrl Pts',(2.19147106502125,-1.52131278661253,
7.59394543036555));
#409047=CARTESIAN_POINT('Ctrl Pts',(2.20886846717181,-1.52324589143932,
7.57858609112103));
#409048=CARTESIAN_POINT('Ctrl Pts',(2.22624640173356,-1.5251768331334,7.56320440326857));
#409049=CARTESIAN_POINT('Ctrl Pts',(2.2436058889753,-1.52710572506146,7.54780169004651));
#409050=CARTESIAN_POINT('Ctrl Pts',(2.25456553516222,-1.52832350141452,
7.53807742314383));
#409051=CARTESIAN_POINT('Ctrl Pts',(2.26551783731019,-1.52954046173787,
7.52834476460825));
#409052=CARTESIAN_POINT('Ctrl Pts',(2.27646303399421,-1.53075663254066,
7.51860402984325));
#409053=CARTESIAN_POINT('',(2.27646303399421,-1.53075663254066,7.5));
#409054=CARTESIAN_POINT('Origin',(2.19071182494584,-1.52814573469575,7.5));
#409055=CARTESIAN_POINT('Ctrl Pts',(2.19147106502126,-1.52131278661253,
8.85049129520029));
#409056=CARTESIAN_POINT('Ctrl Pts',(2.19127858807353,-1.52129139961961,
8.85097269580138));
#409057=CARTESIAN_POINT('Ctrl Pts',(2.19108761066505,-1.52127864242605,
8.85143669361005));
#409058=CARTESIAN_POINT('Ctrl Pts',(2.19088928063142,-1.52127479994581,
8.8519052845931));
#409059=CARTESIAN_POINT('Ctrl Pts',(2.19050135966329,-1.52126728429814,
8.85282181883899));
#409060=CARTESIAN_POINT('Ctrl Pts',(2.19009528511056,-1.52129426370401,
8.85372622499636));
#409061=CARTESIAN_POINT('Ctrl Pts',(2.18966570712696,-1.52137154633668,
8.85462257735071));
#409062=CARTESIAN_POINT('Ctrl Pts',(2.18930908674214,-1.52143570363351,
8.85536669723986));
#409063=CARTESIAN_POINT('Ctrl Pts',(2.18893618151326,-1.52153451208308,
8.85610498449051));
#409064=CARTESIAN_POINT('Ctrl Pts',(2.18854594865094,-1.5216847600764,8.85681338218371));
#409065=CARTESIAN_POINT('Ctrl Pts',(2.18819181171551,-1.52182111036631,
8.85745625420284));
#409066=CARTESIAN_POINT('Ctrl Pts',(2.18781874712326,-1.52200097601186,
8.85808743050666));
#409067=CARTESIAN_POINT('Ctrl Pts',(2.18742683720688,-1.52225295490406,
8.85866804508411));
#409068=CARTESIAN_POINT('Ctrl Pts',(2.18724601846703,-1.52236921250269,
8.85893592806396));
#409069=CARTESIAN_POINT('Ctrl Pts',(2.18706121773651,-1.52250106139574,
8.85919241173848));
#409070=CARTESIAN_POINT('Ctrl Pts',(2.18687285743163,-1.52265285170285,
8.85943017985534));
#409071=CARTESIAN_POINT('Ctrl Pts',(2.18661851525943,-1.5228578135522,8.8597512372));
#409072=CARTESIAN_POINT('Ctrl Pts',(2.18635161117299,-1.52310485014257,
8.86004599534706));
#409073=CARTESIAN_POINT('Ctrl Pts',(2.18608242652935,-1.52339863699003,
8.86026130871721));
#409074=CARTESIAN_POINT('Ctrl Pts',(2.18598387044219,-1.52350620063761,
8.86034014101235));
#409075=CARTESIAN_POINT('Ctrl Pts',(2.18588351913952,-1.52362163854733,
8.86040910639692));
#409076=CARTESIAN_POINT('Ctrl Pts',(2.18578436050157,-1.52374202636576,
8.86046313645506));
#409077=CARTESIAN_POINT('Ctrl Pts',(2.1856296242775,-1.52392989054817,8.86054744990829));
#409078=CARTESIAN_POINT('Ctrl Pts',(2.18547368201657,-1.52413503003227,
8.86059655985668));
#409079=CARTESIAN_POINT('Ctrl Pts',(2.18532630154898,-1.52434411130867,
8.86059725258815));
#409080=CARTESIAN_POINT('Ctrl Pts',(2.18517858057362,-1.52455367564634,
8.86059794692011));
#409081=CARTESIAN_POINT('Ctrl Pts',(2.18503999426283,-1.52477105478738,
8.86056369958366));
#409082=CARTESIAN_POINT('Ctrl Pts',(2.18491492808123,-1.52498236981286,
8.86048590497774));
#409083=CARTESIAN_POINT('Ctrl Pts',(2.1848822895315,-1.5250375167429,8.86046560290182));
#409084=CARTESIAN_POINT('Ctrl Pts',(2.18485022511723,-1.52509301423802,
8.86044257503091));
#409085=CARTESIAN_POINT('Ctrl Pts',(2.18481969723215,-1.52514713095777,
8.86041778462583));
#409086=CARTESIAN_POINT('Ctrl Pts',(2.18461428244747,-1.52551126932846,
8.86025097596201));
#409087=CARTESIAN_POINT('Ctrl Pts',(2.18445116098596,-1.52586191704486,
8.8599848982295));
#409088=CARTESIAN_POINT('Ctrl Pts',(2.1843274119972,-1.52618526598101,8.85968173251462));
#409089=CARTESIAN_POINT('Ctrl Pts',(2.18426195587212,-1.52635629904255,
8.85952137522077));
#409090=CARTESIAN_POINT('Ctrl Pts',(2.18420607533322,-1.52652292297255,
8.85934740853961));
#409091=CARTESIAN_POINT('Ctrl Pts',(2.1841590845445,-1.52668229371293,8.8591675900182));
#409092=CARTESIAN_POINT('Ctrl Pts',(2.18397039210248,-1.52732225007479,
8.85844552518694));
#409093=CARTESIAN_POINT('Ctrl Pts',(2.18391147471059,-1.52788056619921,
8.85759444184122));
#409094=CARTESIAN_POINT('Ctrl Pts',(2.1839043249383,-1.52834010198266,8.85683498915136));
#409095=CARTESIAN_POINT('Ctrl Pts',(2.18390357673367,-1.52838819117855,
8.85675551444997));
#409096=CARTESIAN_POINT('Ctrl Pts',(2.18390341508028,-1.52843519502016,
8.8566769979365));
#409097=CARTESIAN_POINT('Ctrl Pts',(2.18390376336045,-1.52848109083083,
8.85659965593547));
#409098=CARTESIAN_POINT('Ctrl Pts',(2.18390846446408,-1.52910059482533,
8.85555568965886));
#409099=CARTESIAN_POINT('Ctrl Pts',(2.18400245115095,-1.52969529761313,
8.85434650606346));
#409100=CARTESIAN_POINT('Ctrl Pts',(2.18418004948776,-1.5302691092042,8.85297329937117));
#409101=CARTESIAN_POINT('Ctrl Pts',(2.18427993773099,-1.53059184326132,
8.85220095427747));
#409102=CARTESIAN_POINT('Ctrl Pts',(2.18440661731195,-1.53090800733084,
8.85137579139183));
#409103=CARTESIAN_POINT('Ctrl Pts',(2.1845615339302,-1.5312181190179,8.85049129520029));
#409104=CARTESIAN_POINT('Origin',(2.19071182494584,-1.52814573469575,7.59394543036555));
#409105=CARTESIAN_POINT('Ctrl Pts',(2.19091223951051,-1.52125069295724,
7.59443877723642));
#409106=CARTESIAN_POINT('Ctrl Pts',(2.18515687443732,-1.52061118805262,
7.58783886950016));
#409107=CARTESIAN_POINT('Ctrl Pts',(2.18229230418496,-1.5286032728123,7.58559994247159));
#409108=CARTESIAN_POINT('Ctrl Pts',(2.22233060858982,-1.52474173146927,
7.56670252222138));
#409109=CARTESIAN_POINT('Ctrl Pts',(2.21658356165311,-1.52410315083086,
7.56004874999025));
#409110=CARTESIAN_POINT('Ctrl Pts',(2.21368190515091,-1.53213538257544,
7.55786368756704));
#409111=CARTESIAN_POINT('Ctrl Pts',(2.25369030700393,-1.52822625081568,
7.53888913333558));
#409112=CARTESIAN_POINT('Ctrl Pts',(2.24790910508592,-1.52758387506119,
7.53222002137278));
#409113=CARTESIAN_POINT('Ctrl Pts',(2.24501413171017,-1.53565986254719,
7.53005029815327));
#409114=CARTESIAN_POINT('Ctrl Pts',(2.28498991570529,-1.5317040933196,7.51101258149734));
#409115=CARTESIAN_POINT('Ctrl Pts',(2.27913863511533,-1.53105393080376,
7.5043616886572));
#409116=CARTESIAN_POINT('Ctrl Pts',(2.2762874265759,-1.53917662071594,7.50217374673251));
#409117=CARTESIAN_POINT('',(2.27461864350413,-1.53898896096134,7.50366116523517));
#409118=CARTESIAN_POINT('Ctrl Pts',(2.27646303399421,-1.53075663254066,
7.51860402984325));
#409119=CARTESIAN_POINT('Ctrl Pts',(2.27690194403195,-1.53080540183996,
7.51734760759493));
#409120=CARTESIAN_POINT('Ctrl Pts',(2.27729199148658,-1.53090860476198,
7.51608817408573));
#409121=CARTESIAN_POINT('Ctrl Pts',(2.2776288635254,-1.53107891334168,7.51481005913119));
#409122=CARTESIAN_POINT('Ctrl Pts',(2.27793401026798,-1.53123318292282,
7.51365231206383));
#409123=CARTESIAN_POINT('Ctrl Pts',(2.27819606868182,-1.53144250802903,
7.51247773061042));
#409124=CARTESIAN_POINT('Ctrl Pts',(2.27838745892558,-1.53173211745976,
7.51129758471022));
#409125=CARTESIAN_POINT('Ctrl Pts',(2.27862533514098,-1.53209206890751,
7.50983079813402));
#409126=CARTESIAN_POINT('Ctrl Pts',(2.27873558770848,-1.53257173404271,
7.50839324291155));
#409127=CARTESIAN_POINT('Ctrl Pts',(2.27863867677663,-1.53319308108102,
7.50715379678855));
#409128=CARTESIAN_POINT('Ctrl Pts',(2.27859390671853,-1.53348012550903,
7.50658120839351));
#409129=CARTESIAN_POINT('Ctrl Pts',(2.27848917168156,-1.53383674900995,
7.50598221009429));
#409130=CARTESIAN_POINT('Ctrl Pts',(2.27830513945914,-1.53424805484197,
7.50545747549611));
#409131=CARTESIAN_POINT('Ctrl Pts',(2.27820693416892,-1.53446754036504,
7.50517746087247));
#409132=CARTESIAN_POINT('Ctrl Pts',(2.27808526799905,-1.53470506004887,
7.50491486231392));
#409133=CARTESIAN_POINT('Ctrl Pts',(2.2779418782926,-1.53495356351541,7.50468370960992));
#409134=CARTESIAN_POINT('Ctrl Pts',(2.27772746545173,-1.53532515458387,
7.50433806340446));
#409135=CARTESIAN_POINT('Ctrl Pts',(2.27745756787722,-1.53573216943124,
7.50405484070983));
#409136=CARTESIAN_POINT('Ctrl Pts',(2.2771497656152,-1.53614680044922,7.5038576603613));
#409137=CARTESIAN_POINT('Ctrl Pts',(2.27711685094761,-1.53619113879176,
7.5038365749879));
#409138=CARTESIAN_POINT('Ctrl Pts',(2.27708352897818,-1.53623555321374,
7.50381643264937));
#409139=CARTESIAN_POINT('Ctrl Pts',(2.27704984031698,-1.53628000200856,
7.50379723213559));
#409140=CARTESIAN_POINT('Ctrl Pts',(2.2768249574831,-1.53657671225426,7.50366906242519));
#409141=CARTESIAN_POINT('Ctrl Pts',(2.27657827008935,-1.53688097395986,
7.50358235568538));
#409142=CARTESIAN_POINT('Ctrl Pts',(2.27633344417521,-1.53716852914518,
7.5035341175365));
#409143=CARTESIAN_POINT('Ctrl Pts',(2.2759663554259,-1.53759968560059,7.50346178989176));
#409144=CARTESIAN_POINT('Ctrl Pts',(2.27555311919226,-1.53804790364339,
7.50346967198527));
#409145=CARTESIAN_POINT('Ctrl Pts',(2.27513391008215,-1.53847543241699,
7.50354272648692));
#409146=CARTESIAN_POINT('Ctrl Pts',(2.27496148069805,-1.53865128385089,
7.50357277531559));
#409147=CARTESIAN_POINT('Ctrl Pts',(2.27478837114253,-1.53882350060339,
7.50361331098761));
#409148=CARTESIAN_POINT('Ctrl Pts',(2.27461864350531,-1.53898896096214,
7.50366116523659));
#409149=CARTESIAN_POINT('',(2.19311322794403,-1.52982084947247,7.57603338622103));
#409150=CARTESIAN_POINT('Origin',(2.20035940734052,-1.53487894928946,7.58486873427628));
#409151=CARTESIAN_POINT('Ctrl Pts',(2.27461864356147,-1.5389889609624,7.50366116529968));
#409152=CARTESIAN_POINT('Ctrl Pts',(2.24749441162108,-1.53593874122534,
7.52783573079709));
#409153=CARTESIAN_POINT('Ctrl Pts',(2.22032722052781,-1.53288286616248,
7.55196141284068));
#409154=CARTESIAN_POINT('Ctrl Pts',(2.19311322917711,-1.5298208492553,7.57603338728831));
#409155=CARTESIAN_POINT('Ctrl Pts',(2.19247376689065,-1.52160109977801,
7.59639677331371));
#409156=CARTESIAN_POINT('Ctrl Pts',(2.1748554610499,-1.51673620357623,7.59959882295466));
#409157=CARTESIAN_POINT('Ctrl Pts',(2.1850750391811,-1.53191082170738,7.59642833564546));
#409158=CARTESIAN_POINT('Ctrl Pts',(2.18892959610601,-1.51997200262526,
7.58707626057423));
#409159=CARTESIAN_POINT('Ctrl Pts',(2.18258908164249,-1.52236159827603,
7.58809943920599));
#409160=CARTESIAN_POINT('Ctrl Pts',(2.1824282798476,-1.529120928389,7.58710240504253));
#409161=CARTESIAN_POINT('Ctrl Pts',(2.19096580824876,-1.52569733863037,
7.5801537675693));
#409162=CARTESIAN_POINT('Ctrl Pts',(2.18818969220951,-1.5263473010393,7.58205880659762));
#409163=CARTESIAN_POINT('Ctrl Pts',(2.18849217661503,-1.52914651132475,
7.58020924244127));
#409164=CARTESIAN_POINT('Ctrl Pts',(2.1931132272654,-1.52982084899883,7.57603338509286));
#409165=CARTESIAN_POINT('Ctrl Pts',(2.1931132272654,-1.52982084899883,7.57603338509286));
#409166=CARTESIAN_POINT('Ctrl Pts',(2.1931132272654,-1.52982084899883,7.57603338509286));
#409167=CARTESIAN_POINT('Origin',(2.20036267204003,-1.5348742690978,7.58486873427622));
#409168=CARTESIAN_POINT('Ctrl Pts',(2.22662370789095,-1.61541807041848,
7.51098857897448));
#409169=CARTESIAN_POINT('Ctrl Pts',(2.22399271106279,-1.61015134775044,
7.50433767179956));
#409170=CARTESIAN_POINT('Ctrl Pts',(2.2306309268741,-1.60467027651163,7.50214974420965));
#409171=CARTESIAN_POINT('Ctrl Pts',(2.21254602352189,-1.58723739814,7.53887321589165));
#409172=CARTESIAN_POINT('Ctrl Pts',(2.20994655070493,-1.58203378015628,
7.53220407452062));
#409173=CARTESIAN_POINT('Ctrl Pts',(2.21652580167462,-1.57652774922653,
7.53003438070912));
#409174=CARTESIAN_POINT('Ctrl Pts',(2.19844130480581,-1.55900260857537,
7.56669465659232));
#409175=CARTESIAN_POINT('Ctrl Pts',(2.19585719438983,-1.55382974300651,
7.56004085833299));
#409176=CARTESIAN_POINT('Ctrl Pts',(2.20239306107413,-1.54833255310514,
7.55785582193789));
#409177=CARTESIAN_POINT('Ctrl Pts',(2.18431018964266,-1.53071497867105,
7.59443891967696));
#409178=CARTESIAN_POINT('Ctrl Pts',(2.18172233258837,-1.52553461309112,
7.58783901202978));
#409179=CARTESIAN_POINT('Ctrl Pts',(2.1882333290775,-1.52008611763762,7.58560008491213));
#409180=CARTESIAN_POINT('',(2.22986633334695,-1.60314476287804,7.50366116523517));
#409181=CARTESIAN_POINT('Ctrl Pts',(2.22986633334725,-1.60314476287826,
7.50366116523554));
#409182=CARTESIAN_POINT('Ctrl Pts',(2.22955718153619,-1.60383654512325,
7.50350835821027));
#409183=CARTESIAN_POINT('Ctrl Pts',(2.22925048957459,-1.60446240297599,
7.50345484956));
#409184=CARTESIAN_POINT('Ctrl Pts',(2.22893767849838,-1.60504120794399,
7.50349758195598));
#409185=CARTESIAN_POINT('Ctrl Pts',(2.22877718321761,-1.60533817781787,
7.50351950684424));
#409186=CARTESIAN_POINT('Ctrl Pts',(2.2285993719274,-1.60565209334061,7.50357029184312));
#409187=CARTESIAN_POINT('Ctrl Pts',(2.22841958978207,-1.605950085339,7.50365515313924));
#409188=CARTESIAN_POINT('Ctrl Pts',(2.22814301204158,-1.60640851770141,
7.50378570417639));
#409189=CARTESIAN_POINT('Ctrl Pts',(2.22785394845766,-1.60684290016333,
7.50400001621911));
#409190=CARTESIAN_POINT('Ctrl Pts',(2.22757251081408,-1.60721891209279,
7.50428903009635));
#409191=CARTESIAN_POINT('Ctrl Pts',(2.2275412734009,-1.6072606465241,7.50432110841318));
#409192=CARTESIAN_POINT('Ctrl Pts',(2.22751012875532,-1.6073016921642,7.50435406373354));
#409193=CARTESIAN_POINT('Ctrl Pts',(2.22747910320326,-1.60734202443206,
7.50438785222352));
#409194=CARTESIAN_POINT('Ctrl Pts',(2.22728967729514,-1.60758827231352,
7.50459414719561));
#409195=CARTESIAN_POINT('Ctrl Pts',(2.22710126617778,-1.6078115339477,7.50483629897752));
#409196=CARTESIAN_POINT('Ctrl Pts',(2.22692209358151,-1.60800410500738,
7.5050991045531));
#409197=CARTESIAN_POINT('Ctrl Pts',(2.22652682083797,-1.60842893610696,
7.50567888004914));
#409198=CARTESIAN_POINT('Ctrl Pts',(2.22616131576143,-1.60872149506665,
7.50637912803144));
#409199=CARTESIAN_POINT('Ctrl Pts',(2.22583792403101,-1.60891011918631,
7.50710440483569));
#409200=CARTESIAN_POINT('Ctrl Pts',(2.22575862195849,-1.60895637356516,
7.50728225710685));
#409201=CARTESIAN_POINT('Ctrl Pts',(2.22568034714869,-1.60899742490869,
7.50746498566954));
#409202=CARTESIAN_POINT('Ctrl Pts',(2.225605120277,-1.60903268387966,7.50764697238949));
#409203=CARTESIAN_POINT('Ctrl Pts',(2.22520072131776,-1.60922222640407,
7.50862528291182));
#409204=CARTESIAN_POINT('Ctrl Pts',(2.22484944915481,-1.60926533252598,
7.50965856837421));
#409205=CARTESIAN_POINT('Ctrl Pts',(2.22454139946588,-1.60922755604196,
7.51067959873202));
#409206=CARTESIAN_POINT('Ctrl Pts',(2.22437187933351,-1.60920676759516,
7.51124147302578));
#409207=CARTESIAN_POINT('Ctrl Pts',(2.22421545983212,-1.60916104909815,
7.51180065547253));
#409208=CARTESIAN_POINT('Ctrl Pts',(2.22407091919156,-1.60909864305016,
7.512351757165));
#409209=CARTESIAN_POINT('Ctrl Pts',(2.2235714737003,-1.60888300529474,7.51425603304536));
#409210=CARTESIAN_POINT('Ctrl Pts',(2.22315671355512,-1.60843684338508,
7.51626900505181));
#409211=CARTESIAN_POINT('Ctrl Pts',(2.22282983450622,-1.60782042716918,
7.51827788969244));
#409212=CARTESIAN_POINT('Ctrl Pts',(2.22281214319438,-1.60778706555871,
7.51838661432546));
#409213=CARTESIAN_POINT('Ctrl Pts',(2.22279471162011,-1.60775319555448,
7.51849533314857));
#409214=CARTESIAN_POINT('Ctrl Pts',(2.22277754110617,-1.60771882366394,
7.51860402984325));
#409215=CARTESIAN_POINT('Ctrl Pts',(2.19311322816693,-1.52982085070556,
7.57603338728985));
#409216=CARTESIAN_POINT('Ctrl Pts',(2.20538559594874,-1.55430280859582,
7.55196141284922));
#409217=CARTESIAN_POINT('Ctrl Pts',(2.21763603663764,-1.57874296711532,
7.52783573083105));
#409218=CARTESIAN_POINT('Ctrl Pts',(2.2298663333685,-1.60314476293316,7.50366116530176));
#409219=CARTESIAN_POINT('Origin',(7.57821998246254E-16,-5.28623820391005E-16,
7.49482233047033));
#409220=CARTESIAN_POINT('Origin',(2.26729799607038,-1.53403586888157,7.49482233047033));
#409221=CARTESIAN_POINT('Origin',(0.,0.,7.50366116523517));
#409222=CARTESIAN_POINT('Origin',(2.22268971703922,-1.59798519134819,7.49482233047033));
#409223=CARTESIAN_POINT('Ctrl Pts',(2.27646198274858,-1.53075651568693,
7.51860402984325));
#409224=CARTESIAN_POINT('Ctrl Pts',(2.28402433122799,-1.531597450587,7.51860402984325));
#409225=CARTESIAN_POINT('Ctrl Pts',(2.28824458223239,-1.52526611838201,
7.51860402984325));
#409226=CARTESIAN_POINT('Ctrl Pts',(2.27926993448757,-1.53106875929122,
7.51041458714366));
#409227=CARTESIAN_POINT('Ctrl Pts',(2.2850241487917,-1.53009747997901,7.51004642900442));
#409228=CARTESIAN_POINT('Ctrl Pts',(2.28824574612751,-1.52526437227577,
7.5072913648301));
#409229=CARTESIAN_POINT('Ctrl Pts',(2.27994303407421,-1.5338020126907,7.50215815450137));
#409230=CARTESIAN_POINT('Ctrl Pts',(2.28298853728965,-1.53315164768067,
7.4987716367153));
#409231=CARTESIAN_POINT('Ctrl Pts',(2.28492197180653,-1.53029406923673,
7.4948158853317));
#409232=CARTESIAN_POINT('Ctrl Pts',(2.27461818754463,-1.53898865246333,
7.50366171572174));
#409233=CARTESIAN_POINT('Ctrl Pts',(2.27765095495633,-1.54104059887679,
7.50000045605858));
#409234=CARTESIAN_POINT('Ctrl Pts',(2.2776509549564,-1.54104059887668,7.49482233047317));
#409235=CARTESIAN_POINT('Origin',(2.27784347049497,-1.51833309057118,7.51860402984325));
#409236=CARTESIAN_POINT('Origin',(2.27784347049497,-1.51833309057118,9.));
#409237=CARTESIAN_POINT('Origin',(2.27784347049497,-1.51833309057118,8.75721825406948));
#409238=CARTESIAN_POINT('Ctrl Pts',(2.2598650251365,-1.5289123215581,8.78942910404912));
#409239=CARTESIAN_POINT('Ctrl Pts',(2.26540114279122,-1.5295477977692,8.79672699501691));
#409240=CARTESIAN_POINT('Ctrl Pts',(2.26803020458243,-1.52101776142226,
8.79893251111267));
#409241=CARTESIAN_POINT('Ctrl Pts',(2.27079211197274,-1.53012648465001,
8.78111911759582));
#409242=CARTESIAN_POINT('Ctrl Pts',(2.27735609248566,-1.53087245378568,
8.78644465894813));
#409243=CARTESIAN_POINT('Ctrl Pts',(2.28134967515313,-1.52381789432009,
8.78817647674132));
#409244=CARTESIAN_POINT('Ctrl Pts',(2.27760213312822,-1.53088318001778,
8.76780923932029));
#409245=CARTESIAN_POINT('Ctrl Pts',(2.28535121037834,-1.53175870188637,
8.76988516158373));
#409246=CARTESIAN_POINT('Ctrl Pts',(2.28967108621072,-1.52555587566044,
8.77093053738833));
#409247=CARTESIAN_POINT('Ctrl Pts',(2.27627427220479,-1.53073563477544,
8.75371302330492));
#409248=CARTESIAN_POINT('Ctrl Pts',(2.28383307721574,-1.53159042607985,
8.75300828287559));
#409249=CARTESIAN_POINT('Ctrl Pts',(2.28804816663108,-1.52521645082456,
8.75267964240738));
#409250=CARTESIAN_POINT('Origin',(2.26390666047845,-1.5167845079449,8.78727029226991));
#409251=CARTESIAN_POINT('Ctrl Pts',(2.19147106502126,-1.52131278661253,
8.85049129520029));
#409252=CARTESIAN_POINT('Ctrl Pts',(2.19727496193954,-1.52195768411216,
8.85711686593484));
#409253=CARTESIAN_POINT('Ctrl Pts',(2.20013305013608,-1.51389963881726,
8.85933012996512));
#409254=CARTESIAN_POINT('Ctrl Pts',(2.21519057835743,-1.52394837009347,
8.82945683644721));
#409255=CARTESIAN_POINT('Ctrl Pts',(2.22104265112921,-1.52459862063228,
8.83607469902385));
#409256=CARTESIAN_POINT('Ctrl Pts',(2.2238737855901,-1.516504380695,8.83829567148519));
#409257=CARTESIAN_POINT('Ctrl Pts',(2.23887473584627,-1.52658002502469,
8.80838214965001));
#409258=CARTESIAN_POINT('Ctrl Pts',(2.24474990362954,-1.5272328417557,8.81501364461993));
#409259=CARTESIAN_POINT('Ctrl Pts',(2.24757843466632,-1.51910583586367,
8.81722098428721));
#409260=CARTESIAN_POINT('Ctrl Pts',(2.26252622397769,-1.52920804991437,
8.78727029226991));
#409261=CARTESIAN_POINT('Ctrl Pts',(2.26840236764561,-1.52986097508039,
8.79393457792714));
#409262=CARTESIAN_POINT('Ctrl Pts',(2.27124974846887,-1.52170427000876,
8.79610912703474));
#409263=CARTESIAN_POINT('Origin',(2.19285150152201,-1.50888924464306,8.85049129520029));
#409264=CARTESIAN_POINT('Ctrl Pts',(2.1845615339302,-1.5312181190179,8.85049129520029));
#409265=CARTESIAN_POINT('Ctrl Pts',(2.1871712130441,-1.53644216794048,8.85711686593484));
#409266=CARTESIAN_POINT('Ctrl Pts',(2.18059607577693,-1.54190736071218,
8.85933012996512));
#409267=CARTESIAN_POINT('Ctrl Pts',(2.18225278848926,-1.52659647834603,
8.86332496987231));
#409268=CARTESIAN_POINT('Ctrl Pts',(2.1798455991341,-1.53054075696004,8.86648636486738));
#409269=CARTESIAN_POINT('Ctrl Pts',(2.17415259292302,-1.52897047603819,
8.87206031107456));
#409270=CARTESIAN_POINT('Ctrl Pts',(2.18630154981017,-1.52073837816234,
8.86341338519876));
#409271=CARTESIAN_POINT('Ctrl Pts',(2.18915667038817,-1.51708847992823,
8.86654584966059));
#409272=CARTESIAN_POINT('Ctrl Pts',(2.18565650578641,-1.51230590734143,
8.87215952290715));
#409273=CARTESIAN_POINT('Ctrl Pts',(2.19147106502126,-1.52131278661253,
8.85049129520029));
#409274=CARTESIAN_POINT('Ctrl Pts',(2.19727496193954,-1.52195768411216,
8.85711686593484));
#409275=CARTESIAN_POINT('Ctrl Pts',(2.20013305013608,-1.51389963881726,
8.85933012996512));
#409276=CARTESIAN_POINT('Origin',(2.17337918662905,-1.5368042723309,8.85049129520029));
#409277=CARTESIAN_POINT('Ctrl Pts',(2.21651095806265,-1.59517439388233,
8.78727029226991));
#409278=CARTESIAN_POINT('Ctrl Pts',(2.21915312239058,-1.6004634716226,8.79393457792714));
#409279=CARTESIAN_POINT('Ctrl Pts',(2.21248169808586,-1.60595268950174,
8.79610912703474));
#409280=CARTESIAN_POINT('Ctrl Pts',(2.20587624220566,-1.57388584709553,
8.80838214965002));
#409281=CARTESIAN_POINT('Ctrl Pts',(2.20851796773431,-1.57917404644858,
8.81501364461994));
#409282=CARTESIAN_POINT('Ctrl Pts',(2.20186790511426,-1.58463531733956,
8.81722098428722));
#409283=CARTESIAN_POINT('Ctrl Pts',(2.19522683681494,-1.55256789483797,
8.8294568364472));
#409284=CARTESIAN_POINT('Ctrl Pts',(2.19785817784332,-1.55783530652512,
8.83607469902386));
#409285=CARTESIAN_POINT('Ctrl Pts',(2.19123976416885,-1.56328770443167,
8.83829567148519));
#409286=CARTESIAN_POINT('Ctrl Pts',(2.1845615339302,-1.5312181190179,8.85049129520029));
#409287=CARTESIAN_POINT('Ctrl Pts',(2.1871712130441,-1.53644216794048,8.85711686593484));
#409288=CARTESIAN_POINT('Ctrl Pts',(2.18059607577693,-1.54190736071218,
8.85933012996512));
#409289=CARTESIAN_POINT('Origin',(2.2053286107615,-1.60076054719533,8.78727029226991));
#409290=CARTESIAN_POINT('Ctrl Pts',(2.22269477752691,-1.60755318902288,
8.75374538247849));
#409291=CARTESIAN_POINT('Ctrl Pts',(2.22610243367153,-1.61434526219589,
8.75304829418602));
#409292=CARTESIAN_POINT('Ctrl Pts',(2.22158576323609,-1.62049914969784,
8.75272238421917));
#409293=CARTESIAN_POINT('Ctrl Pts',(2.22328466840486,-1.60873403010713,
8.76769408445016));
#409294=CARTESIAN_POINT('Ctrl Pts',(2.22677745947003,-1.61569733144681,
8.76974318093967));
#409295=CARTESIAN_POINT('Ctrl Pts',(2.22245540607675,-1.6218891172753,8.77077869880429));
#409296=CARTESIAN_POINT('Ctrl Pts',(2.22026122381642,-1.60268171138352,
8.78108014887993));
#409297=CARTESIAN_POINT('Ctrl Pts',(2.22322463452794,-1.60858115493823,
8.78639403366327));
#409298=CARTESIAN_POINT('Ctrl Pts',(2.21800623306506,-1.61476907558262,
8.78812224174741));
#409299=CARTESIAN_POINT('Ctrl Pts',(2.21530646553678,-1.59276329707431,
8.78944554828684));
#409300=CARTESIAN_POINT('Ctrl Pts',(2.21780892032158,-1.59773261671255,
8.79673892988686));
#409301=CARTESIAN_POINT('Ctrl Pts',(2.2107208846927,-1.60314217355577,8.79894799272499));
#409302=CARTESIAN_POINT('Origin',(2.21159519380502,-1.61330497697693,8.75721825406948));
#409303=CARTESIAN_POINT('Origin',(2.21159519380502,-1.61330497697693,9.));
#409304=CARTESIAN_POINT('Origin',(2.21159519380502,-1.61330497697693,7.51860402984325));
#409305=CARTESIAN_POINT('Ctrl Pts',(2.22986569462201,-1.60314430367187,
7.50366195182966));
#409306=CARTESIAN_POINT('Ctrl Pts',(2.23283898515348,-1.60528192738186,
7.50000065167735));
#409307=CARTESIAN_POINT('Ctrl Pts',(2.23283898515341,-1.60528192738195,
7.49482233047108));
#409308=CARTESIAN_POINT('Ctrl Pts',(2.22683369837613,-1.60993847752684,
7.50215800491337));
#409309=CARTESIAN_POINT('Ctrl Pts',(2.22727397197242,-1.61302244515553,
7.49877273257266));
#409310=CARTESIAN_POINT('Ctrl Pts',(2.22525885250261,-1.6158253810935,7.49481816995647));
#409311=CARTESIAN_POINT('Ctrl Pts',(2.22403744845654,-1.61024014411316,
7.51043025814042));
#409312=CARTESIAN_POINT('Ctrl Pts',(2.22511749967528,-1.6159782837378,7.51006209594513));
#409313=CARTESIAN_POINT('Ctrl Pts',(2.2216923098784,-1.62067371183517,7.50731281821699));
#409314=CARTESIAN_POINT('Ctrl Pts',(2.22277686558814,-1.60771747161814,
7.51860402984325));
#409315=CARTESIAN_POINT('Ctrl Pts',(2.22617821334675,-1.61452422200402,
7.51860402984324));
#409316=CARTESIAN_POINT('Ctrl Pts',(2.22169380199591,-1.62067166636953,
7.51860402984325));
#409317=CARTESIAN_POINT('Origin',(0.,0.,7.5));
#409318=CARTESIAN_POINT('Origin',(2.27817859968918,-1.38810672912943,7.5));
#409319=CARTESIAN_POINT('',(2.27817859968918,-1.38810672912943,7.59394543036555));
#409320=CARTESIAN_POINT('',(2.27817859968918,-1.38810672912943,8.85049129520029));
#409321=CARTESIAN_POINT('',(2.27817859968918,-1.38810672912943,7.5));
#409322=CARTESIAN_POINT('',(2.3141600729029,-1.44988459233544,8.78727029226991));
#409323=CARTESIAN_POINT('Ctrl Pts',(2.27817859968918,-1.38810672912943,
8.85049129520029));
#409324=CARTESIAN_POINT('Ctrl Pts',(2.29018985827907,-1.40872928356711,
8.82945686509571));
#409325=CARTESIAN_POINT('Ctrl Pts',(2.30218326068068,-1.42932118008398,
8.80838212259896));
#409326=CARTESIAN_POINT('Ctrl Pts',(2.3141600729029,-1.44988459233544,8.78727029226991));
#409327=CARTESIAN_POINT('',(2.32121750495511,-1.46200174688655,8.75721825406948));
#409328=CARTESIAN_POINT('Origin',(2.29997941805042,-1.42553692380631,8.75937679713093));
#409329=CARTESIAN_POINT('',(2.32121750495511,-1.46200174688655,7.51860402984325));
#409330=CARTESIAN_POINT('',(2.32121750495511,-1.46200174688655,7.5));
#409331=CARTESIAN_POINT('Ctrl Pts',(2.32121750495511,-1.46200174688655,
7.51860402984325));
#409332=CARTESIAN_POINT('Ctrl Pts',(2.3156749897164,-1.45248560656066,7.52834476460825));
#409333=CARTESIAN_POINT('Ctrl Pts',(2.31012887635679,-1.44296328849378,
7.53807742314407));
#409334=CARTESIAN_POINT('Ctrl Pts',(2.30457904406456,-1.43343458526004,
7.54780169004674));
#409335=CARTESIAN_POINT('Ctrl Pts',(2.2957884096565,-1.41834163432028,7.5632044032688));
#409336=CARTESIAN_POINT('Ctrl Pts',(2.28698843374856,-1.4032326446292,7.57858609112103));
#409337=CARTESIAN_POINT('Ctrl Pts',(2.27817859968918,-1.38810672912943,
7.59394543036555));
#409338=CARTESIAN_POINT('Origin',(2.55914144706916,-1.39057471905265,7.5));
#409339=CARTESIAN_POINT('',(2.36986171072479,-1.3817580415,8.75721825406948));
#409340=CARTESIAN_POINT('',(2.35585431734964,-1.38110557508639,8.78727029226991));
#409341=CARTESIAN_POINT('Origin',(2.32029832846392,-1.3794493719707,8.7565864062096));
#409342=CARTESIAN_POINT('',(2.28443929758137,-1.37777905311488,8.85049129520029));
#409343=CARTESIAN_POINT('Ctrl Pts',(2.35585431734964,-1.38110557508639,
8.78727029226991));
#409344=CARTESIAN_POINT('Ctrl Pts',(2.33208307606304,-1.37999830722192,
8.80838212259897));
#409345=CARTESIAN_POINT('Ctrl Pts',(2.30827890705326,-1.37888950557933,
8.82945686509571));
#409346=CARTESIAN_POINT('Ctrl Pts',(2.28443929758137,-1.37777905311488,
8.85049129520029));
#409347=CARTESIAN_POINT('',(2.28443929758137,-1.37777905311488,7.59394543036555));
#409348=CARTESIAN_POINT('',(2.28443929758137,-1.37777905311488,7.5));
#409349=CARTESIAN_POINT('',(2.36986171072479,-1.3817580415,7.51860402984325));
#409350=CARTESIAN_POINT('Ctrl Pts',(2.28443929758137,-1.37777905311488,
7.59394543036555));
#409351=CARTESIAN_POINT('Ctrl Pts',(2.30192480935484,-1.37859353078759,
7.57858609112103));
#409352=CARTESIAN_POINT('Ctrl Pts',(2.31939075494536,-1.37940709706468,
7.56320440326856));
#409353=CARTESIAN_POINT('Ctrl Pts',(2.33683815978891,-1.38021979971107,
7.54780169004651));
#409354=CARTESIAN_POINT('Ctrl Pts',(2.34785331140615,-1.38073288706991,
7.53807742314383));
#409355=CARTESIAN_POINT('Ctrl Pts',(2.35886108179036,-1.38124563060984,
7.52834476460825));
#409356=CARTESIAN_POINT('Ctrl Pts',(2.36986171072479,-1.3817580415,7.51860402984325));
#409357=CARTESIAN_POINT('',(2.36986171072479,-1.3817580415,7.5));
#409358=CARTESIAN_POINT('Origin',(2.28411940593293,-1.38464660685207,7.5));
#409359=CARTESIAN_POINT('Ctrl Pts',(2.28443929758137,-1.37777905311488,
8.85049129520029));
#409360=CARTESIAN_POINT('Ctrl Pts',(2.28424584582883,-1.3777700421042,8.85097269580138));
#409361=CARTESIAN_POINT('Ctrl Pts',(2.28405444344772,-1.37776954708624,
8.85143669361005));
#409362=CARTESIAN_POINT('Ctrl Pts',(2.28385627471587,-1.37777841954967,
8.8519052845931));
#409363=CARTESIAN_POINT('Ctrl Pts',(2.28346866924377,-1.37779577352546,
8.85282181883899));
#409364=CARTESIAN_POINT('Ctrl Pts',(2.28306515759124,-1.37784871478518,
8.85372622499635));
#409365=CARTESIAN_POINT('Ctrl Pts',(2.28264141373695,-1.3779533617883,8.8546225773507));
#409366=CARTESIAN_POINT('Ctrl Pts',(2.28228963663908,-1.37804023601358,
8.85536669723986));
#409367=CARTESIAN_POINT('Ctrl Pts',(2.28192382826309,-1.37816273357065,
8.85610498449051));
#409368=CARTESIAN_POINT('Ctrl Pts',(2.28154402359801,-1.37833767516868,
8.85681338218371));
#409369=CARTESIAN_POINT('Ctrl Pts',(2.28119935026796,-1.37849643494365,
8.85745625420285));
#409370=CARTESIAN_POINT('Ctrl Pts',(2.28083857620841,-1.37869983336644,
8.85808743050666));
#409371=CARTESIAN_POINT('Ctrl Pts',(2.28046361585604,-1.37897640429554,
8.85866804508411));
#409372=CARTESIAN_POINT('Ctrl Pts',(2.2802906172776,-1.3791040081269,8.85893592806396));
#409373=CARTESIAN_POINT('Ctrl Pts',(2.28011464382758,-1.37924742634571,
8.85919241173848));
#409374=CARTESIAN_POINT('Ctrl Pts',(2.27993639576752,-1.37941097306953,
8.85943017985534));
#409375=CARTESIAN_POINT('Ctrl Pts',(2.27969570811936,-1.3796318095617,8.8597512372));
#409376=CARTESIAN_POINT('Ctrl Pts',(2.27944518010468,-1.37989543919243,
8.86004599534705));
#409377=CARTESIAN_POINT('Ctrl Pts',(2.2791953715177,-1.38020586914263,8.86026130871721));
#409378=CARTESIAN_POINT('Ctrl Pts',(2.27910390955116,-1.38031952629935,
8.86034014101235));
#409379=CARTESIAN_POINT('Ctrl Pts',(2.27901116056327,-1.38044115655954,
8.86040910639692));
#409380=CARTESIAN_POINT('Ctrl Pts',(2.27891991893139,-1.38056765014403,
8.86046313645506));
#409381=CARTESIAN_POINT('Ctrl Pts',(2.27877753712898,-1.38076504232325,
8.86054744990829));
#409382=CARTESIAN_POINT('Ctrl Pts',(2.27863505860003,-1.38097975158124,
8.86059655985668));
#409383=CARTESIAN_POINT('Ctrl Pts',(2.27850137682478,-1.38119784597671,
8.86059725258816));
#409384=CARTESIAN_POINT('Ctrl Pts',(2.27836738619123,-1.38141644425736,
8.86059794692011));
#409385=CARTESIAN_POINT('Ctrl Pts',(2.27824301215027,-1.38164225602506,
8.86056369958366));
#409386=CARTESIAN_POINT('Ctrl Pts',(2.27813174193072,-1.38186114989892,
8.86048590497774));
#409387=CARTESIAN_POINT('Ctrl Pts',(2.27810270371633,-1.38191827468275,
8.86046560290182));
#409388=CARTESIAN_POINT('Ctrl Pts',(2.27807426091855,-1.38197571252638,
8.86044257503091));
#409389=CARTESIAN_POINT('Ctrl Pts',(2.27804726302642,-1.38203167398584,
8.86041778462583));
#409390=CARTESIAN_POINT('Ctrl Pts',(2.27786560071396,-1.38240822516564,
8.86025097596201));
#409391=CARTESIAN_POINT('Ctrl Pts',(2.27772528047932,-1.38276860366661,
8.8599848982295));
#409392=CARTESIAN_POINT('Ctrl Pts',(2.2776225027836,-1.38309921687263,8.85968173251461));
#409393=CARTESIAN_POINT('Ctrl Pts',(2.27756813927102,-1.38327409231674,
8.85952137522076));
#409394=CARTESIAN_POINT('Ctrl Pts',(2.27752304917653,-1.38344395417843,
8.85934740853961));
#409395=CARTESIAN_POINT('Ctrl Pts',(2.27748636585382,-1.38360600818469,
8.8591675900182));
#409396=CARTESIAN_POINT('Ctrl Pts',(2.27733906324554,-1.38425673925384,
8.85844552518695));
#409397=CARTESIAN_POINT('Ctrl Pts',(2.27731603834266,-1.38481768310816,
8.85759444184124));
#409398=CARTESIAN_POINT('Ctrl Pts',(2.27733834581908,-1.38527673281353,
8.85683498915138));
#409399=CARTESIAN_POINT('Ctrl Pts',(2.27734068023708,-1.38532477114265,
8.85675551444998));
#409400=CARTESIAN_POINT('Ctrl Pts',(2.27734353046229,-1.385371688767,8.85667699793651));
#409401=CARTESIAN_POINT('Ctrl Pts',(2.27734681858158,-1.38541746796543,
8.85659965593547));
#409402=CARTESIAN_POINT('Ctrl Pts',(2.27739120178349,-1.38603539792178,
8.85555568965886));
#409403=CARTESIAN_POINT('Ctrl Pts',(2.27752309810307,-1.38662285708122,
8.85434650606346));
#409404=CARTESIAN_POINT('Ctrl Pts',(2.27773709577991,-1.38718411095032,
8.85297329937117));
#409405=CARTESIAN_POINT('Ctrl Pts',(2.27785745643407,-1.38749978205399,
8.85220095427747));
#409406=CARTESIAN_POINT('Ctrl Pts',(2.27800413243973,-1.38780718014191,
8.85137579139183));
#409407=CARTESIAN_POINT('Ctrl Pts',(2.27817859968918,-1.38810672912943,
8.85049129520029));
#409408=CARTESIAN_POINT('Origin',(2.28411940593293,-1.38464660685207,7.59394543036555));
#409409=CARTESIAN_POINT('Ctrl Pts',(2.28387764188342,-1.37775289111106,
7.59443877723642));
#409410=CARTESIAN_POINT('Ctrl Pts',(2.27809312860512,-1.37748344764416,
7.58783886950016));
#409411=CARTESIAN_POINT('Ctrl Pts',(2.27574649854822,-1.38564264545478,
7.58559994247159));
#409412=CARTESIAN_POINT('Ctrl Pts',(2.31545513015925,-1.37922377509171,
7.56670252222136));
#409413=CARTESIAN_POINT('Ctrl Pts',(2.30967897714493,-1.37895472104715,
7.5600487499903));
#409414=CARTESIAN_POINT('Ctrl Pts',(2.30729790926198,-1.38715635948058,
7.55786368756705));
#409415=CARTESIAN_POINT('Ctrl Pts',(2.34697365063072,-1.38069191234348,
7.53888913333557));
#409416=CARTESIAN_POINT('Ctrl Pts',(2.34116316965616,-1.38042125929753,
7.53222002137276));
#409417=CARTESIAN_POINT('Ctrl Pts',(2.33879157460851,-1.38866613538211,
7.53005029815326));
#409418=CARTESIAN_POINT('Ctrl Pts',(2.37843177706342,-1.38215723643218,
7.51101258149734));
#409419=CARTESIAN_POINT('Ctrl Pts',(2.37255086250157,-1.38188330257953,
7.5043616886572));
#409420=CARTESIAN_POINT('Ctrl Pts',(2.37022593460538,-1.39017198111245,
7.50217374673251));
#409421=CARTESIAN_POINT('',(2.36854855682565,-1.39009162622346,7.50366116523517));
#409422=CARTESIAN_POINT('Ctrl Pts',(2.36986171072479,-1.3817580415,7.51860402984325));
#409423=CARTESIAN_POINT('Ctrl Pts',(2.37030284363452,-1.38177858953488,
7.51734760759493));
#409424=CARTESIAN_POINT('Ctrl Pts',(2.37069870192874,-1.3818565899892,7.51608817408572));
#409425=CARTESIAN_POINT('Ctrl Pts',(2.37104579353599,-1.38200496518603,
7.51481005913119));
#409426=CARTESIAN_POINT('Ctrl Pts',(2.37136019740786,-1.38213936698485,
7.51365231206383));
#409427=CARTESIAN_POINT('Ctrl Pts',(2.37163512890018,-1.38233147186995,
7.51247773061042));
#409428=CARTESIAN_POINT('Ctrl Pts',(2.37184468125209,-1.38260822385203,
7.51129758471022));
#409429=CARTESIAN_POINT('Ctrl Pts',(2.37210513089374,-1.38295219495948,
7.50983079813402));
#409430=CARTESIAN_POINT('Ctrl Pts',(2.37224588918625,-1.38342381066495,
7.50839324291155));
#409431=CARTESIAN_POINT('Ctrl Pts',(2.37218898720973,-1.38405009018386,
7.50715379678855));
#409432=CARTESIAN_POINT('Ctrl Pts',(2.37216270013616,-1.38433941327578,
7.50658120839351));
#409433=CARTESIAN_POINT('Ctrl Pts',(2.37208102923471,-1.38470201445232,
7.50598221009429));
#409434=CARTESIAN_POINT('Ctrl Pts',(2.37192372758136,-1.38512426619737,
7.50545747549611));
#409435=CARTESIAN_POINT('Ctrl Pts',(2.37183978655019,-1.38534959279844,
7.50517746087247));
#409436=CARTESIAN_POINT('Ctrl Pts',(2.37173358829491,-1.38559441965088,
7.50491486231392));
#409437=CARTESIAN_POINT('Ctrl Pts',(2.37160641486976,-1.38585159955043,
7.50468370960993));
#409438=CARTESIAN_POINT('Ctrl Pts',(2.37141625048457,-1.38623616462306,
7.50433806340447));
#409439=CARTESIAN_POINT('Ctrl Pts',(2.37117298497438,-1.38665963561174,
7.50405484070984));
#409440=CARTESIAN_POINT('Ctrl Pts',(2.37089238062566,-1.38709313568445,
7.50385766036131));
#409441=CARTESIAN_POINT('Ctrl Pts',(2.37086237435214,-1.38713949177911,
7.50383657498791));
#409442=CARTESIAN_POINT('Ctrl Pts',(2.37083196648805,-1.38718594989282,
7.50381643264937));
#409443=CARTESIAN_POINT('Ctrl Pts',(2.37080119488787,-1.38723246580277,
7.50379723213559));
#409444=CARTESIAN_POINT('Ctrl Pts',(2.37059578439061,-1.38754297471808,
7.50366906242519));
#409445=CARTESIAN_POINT('Ctrl Pts',(2.37036909795698,-1.38786241660096,
7.50358235568538));
#409446=CARTESIAN_POINT('Ctrl Pts',(2.37014319878791,-1.38816506702348,
7.5035341175365));
#409447=CARTESIAN_POINT('Ctrl Pts',(2.36980448855075,-1.38861885707863,
7.50346178989176));
#409448=CARTESIAN_POINT('Ctrl Pts',(2.36942081878388,-1.38909263034579,
7.50346967198527));
#409449=CARTESIAN_POINT('Ctrl Pts',(2.36902986284642,-1.38954613953558,
7.50354272648692));
#409450=CARTESIAN_POINT('Ctrl Pts',(2.36886905457703,-1.38973267725242,
7.50357277531559));
#409451=CARTESIAN_POINT('Ctrl Pts',(2.36870733465888,-1.38991563133443,
7.50361331098761));
#409452=CARTESIAN_POINT('Ctrl Pts',(2.36854855682688,-1.39009162622418,
7.50366116523659));
#409453=CARTESIAN_POINT('',(2.28662319996335,-1.38616442150747,7.57603338622103));
#409454=CARTESIAN_POINT('Origin',(2.294178564875,-1.39074786460788,7.58486873427628));
#409455=CARTESIAN_POINT('Ctrl Pts',(2.36854855688294,-1.39009162622084,
7.50366116529968));
#409456=CARTESIAN_POINT('Ctrl Pts',(2.34128462633659,-1.3887855289946,7.52783573079709));
#409457=CARTESIAN_POINT('Ctrl Pts',(2.31397746256358,-1.38747654046439,
7.55196141284068));
#409458=CARTESIAN_POINT('Ctrl Pts',(2.28662320117998,-1.38616442121175,
7.57603338728831));
#409459=CARTESIAN_POINT('Ctrl Pts',(2.28545841158025,-1.3780025305807,7.5963967733137));
#409460=CARTESIAN_POINT('Ctrl Pts',(2.26756460946825,-1.3742764385605,7.59959882295475));
#409461=CARTESIAN_POINT('Ctrl Pts',(2.27873543150217,-1.38876510819256,
7.59642833564546));
#409462=CARTESIAN_POINT('Ctrl Pts',(2.28181714606166,-1.37660385638453,
7.58707626057419));
#409463=CARTESIAN_POINT('Ctrl Pts',(2.27564276078405,-1.3793947805112,7.58809943920599));
#409464=CARTESIAN_POINT('Ctrl Pts',(2.27591536114095,-1.38615052546194,
7.58710240504253));
#409465=CARTESIAN_POINT('Ctrl Pts',(2.28421599812538,-1.38218696851294,
7.58015376756929));
#409466=CARTESIAN_POINT('Ctrl Pts',(2.28148722914879,-1.3830134618697,7.58205880659763));
#409467=CARTESIAN_POINT('Ctrl Pts',(2.28196843808642,-1.38578754063506,
7.58020924244125));
#409468=CARTESIAN_POINT('Ctrl Pts',(2.28662319925576,-1.38616442107829,
7.57603338509286));
#409469=CARTESIAN_POINT('Ctrl Pts',(2.28662319925576,-1.38616442107829,
7.57603338509286));
#409470=CARTESIAN_POINT('Ctrl Pts',(2.28662319925576,-1.38616442107829,
7.57603338509286));
#409471=CARTESIAN_POINT('Origin',(2.29418152300587,-1.3907429848622,7.58486873427622));
#409472=CARTESIAN_POINT('Ctrl Pts',(2.32554906181098,-1.46943874996092,
7.51098857897448));
#409473=CARTESIAN_POINT('Ctrl Pts',(2.32258603056805,-1.464351416885,7.50433767179956));
#409474=CARTESIAN_POINT('Ctrl Pts',(2.32885943401303,-1.45845629514758,
7.50214974420965));
#409475=CARTESIAN_POINT('Ctrl Pts',(2.30969475968219,-1.44221793823036,
7.53887321589167));
#409476=CARTESIAN_POINT('Ctrl Pts',(2.30676723081195,-1.43719156043309,
7.5322040745206));
#409477=CARTESIAN_POINT('Ctrl Pts',(2.31298019139209,-1.43127530817745,
7.53003438070911));
#409478=CARTESIAN_POINT('Ctrl Pts',(2.29381001144492,-1.41494485249995,
7.56669465659232));
#409479=CARTESIAN_POINT('Ctrl Pts',(2.29089978372603,-1.40994817966098,
7.56004085833297));
#409480=CARTESIAN_POINT('Ctrl Pts',(2.297070015605,-1.4040435299096,7.55785582193789));
#409481=CARTESIAN_POINT('Ctrl Pts',(2.27789553550273,-1.38762072622218,
7.59443891967696));
#409482=CARTESIAN_POINT('Ctrl Pts',(2.27498108831602,-1.38261680882968,
7.58783901202978));
#409483=CARTESIAN_POINT('Ctrl Pts',(2.2811296209623,-1.37676234691709,7.58560008491213));
#409484=CARTESIAN_POINT('',(2.3279986714312,-1.45698290352085,7.50366116523517));
#409485=CARTESIAN_POINT('Ctrl Pts',(2.32799867143151,-1.45698290352105,
7.50366116523554));
#409486=CARTESIAN_POINT('Ctrl Pts',(2.32773447744662,-1.45769307184976,
7.50350835821027));
#409487=CARTESIAN_POINT('Ctrl Pts',(2.32746851446685,-1.45833729363187,
7.50345484956));
#409488=CARTESIAN_POINT('Ctrl Pts',(2.32719343025617,-1.45893495125745,
7.50349758195598));
#409489=CARTESIAN_POINT('Ctrl Pts',(2.32705229165532,-1.45924159394282,
7.50351950684424));
#409490=CARTESIAN_POINT('Ctrl Pts',(2.32689495833407,-1.45956625690093,
7.50357029184312));
#409491=CARTESIAN_POINT('Ctrl Pts',(2.32673463798333,-1.4598751553244,7.50365515313923));
#409492=CARTESIAN_POINT('Ctrl Pts',(2.32648800036377,-1.46035036618503,
7.50378570417639));
#409493=CARTESIAN_POINT('Ctrl Pts',(2.32622736167188,-1.460802376529,7.50400001621911));
#409494=CARTESIAN_POINT('Ctrl Pts',(2.32597059343916,-1.46119564767336,
7.50428903009635));
#409495=CARTESIAN_POINT('Ctrl Pts',(2.32594209414078,-1.46123929774474,
7.50432110841318));
#409496=CARTESIAN_POINT('Ctrl Pts',(2.32591364328842,-1.46128225449646,
7.50435406373354));
#409497=CARTESIAN_POINT('Ctrl Pts',(2.32588526557895,-1.4613244917113,7.50438785222352));
#409498=CARTESIAN_POINT('Ctrl Pts',(2.32571200602261,-1.46158237020968,
7.50459414719561));
#409499=CARTESIAN_POINT('Ctrl Pts',(2.32553828643811,-1.46181724467062,
7.50483629897752));
#409500=CARTESIAN_POINT('Ctrl Pts',(2.32537182004132,-1.46202089970006,
7.5050991045531));
#409501=CARTESIAN_POINT('Ctrl Pts',(2.32500457845002,-1.46247018315022,
7.50567888004914));
#409502=CARTESIAN_POINT('Ctrl Pts',(2.32465856865977,-1.46278555900681,
7.50637912803144));
#409503=CARTESIAN_POINT('Ctrl Pts',(2.32434792656118,-1.46299451535729,
7.50710440483569));
#409504=CARTESIAN_POINT('Ctrl Pts',(2.3242717509515,-1.46304575560279,7.50728225710685));
#409505=CARTESIAN_POINT('Ctrl Pts',(2.3241962671343,-1.46309173768622,7.50746498566954));
#409506=CARTESIAN_POINT('Ctrl Pts',(2.32412345387431,-1.46313174401607,
7.50764697238949));
#409507=CARTESIAN_POINT('Ctrl Pts',(2.32373202982735,-1.46334680703531,
7.50862528291182));
#409508=CARTESIAN_POINT('Ctrl Pts',(2.32338424120944,-1.46341233067583,
7.50965856837422));
#409509=CARTESIAN_POINT('Ctrl Pts',(2.32307440409399,-1.46339436861898,
7.51067959873203));
#409510=CARTESIAN_POINT('Ctrl Pts',(2.32290390033856,-1.46338448407644,
7.51124147302579));
#409511=CARTESIAN_POINT('Ctrl Pts',(2.32274487302364,-1.46334888134486,
7.51180065547253));
#409512=CARTESIAN_POINT('Ctrl Pts',(2.32259663098812,-1.46329586426742,
7.51235175716501));
#409513=CARTESIAN_POINT('Ctrl Pts',(2.32208439570276,-1.46311266914538,
7.51425603304536));
#409514=CARTESIAN_POINT('Ctrl Pts',(2.32164190203507,-1.46269399769696,
7.51626900505181));
#409515=CARTESIAN_POINT('Ctrl Pts',(2.32127620067169,-1.46209979118686,
7.51827788969245));
#409516=CARTESIAN_POINT('Ctrl Pts',(2.32125640822282,-1.46206763160763,
7.51838661432546));
#409517=CARTESIAN_POINT('Ctrl Pts',(2.32123684240497,-1.46203494803775,
7.51849533314857));
#409518=CARTESIAN_POINT('Ctrl Pts',(2.32121750495511,-1.46200174688656,
7.51860402984325));
#409519=CARTESIAN_POINT('Ctrl Pts',(2.2866232002648,-1.38616442272374,7.57603338728985));
#409520=CARTESIAN_POINT('Ctrl Pts',(2.30043891757839,-1.40980978650236,
7.55196141284922));
#409521=CARTESIAN_POINT('Ctrl Pts',(2.31423007475575,-1.43341484166519,
7.52783573083105));
#409522=CARTESIAN_POINT('Ctrl Pts',(2.32799867145623,-1.45698290357448,
7.50366116530176));
#409523=CARTESIAN_POINT('Origin',(7.90134016134199E-16,-4.78983883923424E-16,
7.49482233047033));
#409524=CARTESIAN_POINT('Origin',(2.36092560474805,-1.38561774629407,7.49482233047033));
#409525=CARTESIAN_POINT('Origin',(0.,0.,7.50366116523517));
#409526=CARTESIAN_POINT('Origin',(2.32050622536844,-1.45229374026962,7.49482233047033));
#409527=CARTESIAN_POINT('Ctrl Pts',(2.36986065415221,-1.3817579922399,7.51860402984325));
#409528=CARTESIAN_POINT('Ctrl Pts',(2.37746134385964,-1.38211267801838,
7.51860402984325));
#409529=CARTESIAN_POINT('Ctrl Pts',(2.38126727405859,-1.37552396180421,
7.51860402984325));
#409530=CARTESIAN_POINT('Ctrl Pts',(2.37268284216962,-1.3818896882206,7.51041458714366));
#409531=CARTESIAN_POINT('Ctrl Pts',(2.37836300374412,-1.38055173072963,
7.51004642900443));
#409532=CARTESIAN_POINT('Ctrl Pts',(2.38126832368895,-1.37552214471451,
7.5072913648301));
#409533=CARTESIAN_POINT('Ctrl Pts',(2.37352967894753,-1.38457420021925,
7.50215815450137));
#409534=CARTESIAN_POINT('Ctrl Pts',(2.37652725582072,-1.38373004539292,
7.49877163671529));
#409535=CARTESIAN_POINT('Ctrl Pts',(2.37827363220952,-1.38075446257555,
7.4948158853317));
#409536=CARTESIAN_POINT('Ctrl Pts',(2.36854808203743,-1.39009134757271,
7.50366171572174));
#409537=CARTESIAN_POINT('Ctrl Pts',(2.37170608696132,-1.39194476796698,
7.50000045605858));
#409538=CARTESIAN_POINT('Ctrl Pts',(2.37170608696138,-1.39194476796687,
7.49482233047317));
#409539=CARTESIAN_POINT('Origin',(2.37044333190378,-1.36927158015965,7.51860402984325));
#409540=CARTESIAN_POINT('Origin',(2.37044333190378,-1.36927158015965,9.));
#409541=CARTESIAN_POINT('Origin',(2.37044333190378,-1.36927158015965,8.75721825406948));
#409542=CARTESIAN_POINT('Ctrl Pts',(2.35317963884605,-1.38098095793091,
8.78942910404912));
#409543=CARTESIAN_POINT('Ctrl Pts',(2.35874509705393,-1.38126042821201,
8.7967269950169));
#409544=CARTESIAN_POINT('Ctrl Pts',(2.36082223585053,-1.37257947317229,
8.79893251111266));
#409545=CARTESIAN_POINT('Ctrl Pts',(2.36416206650685,-1.38149252553718,
8.78111911759584));
#409546=CARTESIAN_POINT('Ctrl Pts',(2.37076035502444,-1.38181640632384,
8.78644465894815));
#409547=CARTESIAN_POINT('Ctrl Pts',(2.37429374527117,-1.37452047148726,
8.78817647674132));
#409548=CARTESIAN_POINT('Ctrl Pts',(2.37100657738217,-1.38181134663966,
8.76780923932029));
#409549=CARTESIAN_POINT('Ctrl Pts',(2.37879582820069,-1.38218858457061,
8.76988516158373));
#409550=CARTESIAN_POINT('Ctrl Pts',(2.38270941194408,-1.37572172732154,
8.77093053738833));
#409551=CARTESIAN_POINT('Ctrl Pts',(2.36967199143527,-1.38174918088632,
8.75371302330492));
#409552=CARTESIAN_POINT('Ctrl Pts',(2.37727003273756,-1.38211792163047,
8.75300828287559));
#409553=CARTESIAN_POINT('Ctrl Pts',(2.38106807980287,-1.37548698068487,
8.75267964240738));
#409554=CARTESIAN_POINT('Origin',(2.35643593852863,-1.36861911374604,8.78727029226991));
#409555=CARTESIAN_POINT('Ctrl Pts',(2.28443929758137,-1.37777905311488,
8.85049129520029));
#409556=CARTESIAN_POINT('Ctrl Pts',(2.29027258849564,-1.37805076865112,
8.85711686593484));
#409557=CARTESIAN_POINT('Ctrl Pts',(2.29260852370879,-1.36982616113503,
8.85933012996512));
#409558=CARTESIAN_POINT('Ctrl Pts',(2.3082789390469,-1.3788895070696,8.82945683644722));
#409559=CARTESIAN_POINT('Ctrl Pts',(2.31416064980263,-1.37916347800908,
8.83607469902389));
#409560=CARTESIAN_POINT('Ctrl Pts',(2.31646736766074,-1.37090447714816,
8.8382956714852));
#409561=CARTESIAN_POINT('Ctrl Pts',(2.33208304560441,-1.37999830580315,
8.80838214965003));
#409562=CARTESIAN_POINT('Ctrl Pts',(2.33798796833692,-1.38027335795988,
8.81501364461991));
#409563=CARTESIAN_POINT('Ctrl Pts',(2.34028998879804,-1.37198182526731,
8.81722098428721));
#409564=CARTESIAN_POINT('Ctrl Pts',(2.35585431734964,-1.38110557508639,
8.78727029226991));
#409565=CARTESIAN_POINT('Ctrl Pts',(2.3617602209092,-1.38138067293018,8.79393457792714));
#409566=CARTESIAN_POINT('Ctrl Pts',(2.36407914959491,-1.37305829436821,
8.79610912703474));
#409567=CARTESIAN_POINT('Origin',(2.28502091876036,-1.36529259177452,8.85049129520029));
#409568=CARTESIAN_POINT('Ctrl Pts',(2.27817859968918,-1.38810672912943,
8.85049129520029));
#409569=CARTESIAN_POINT('Ctrl Pts',(2.28111762290111,-1.39315284196833,
8.85711686593484));
#409570=CARTESIAN_POINT('Ctrl Pts',(2.27490615106176,-1.39902807640644,
8.85933012996512));
#409571=CARTESIAN_POINT('Ctrl Pts',(2.27557848827884,-1.38364250594227,
8.86332496987233));
#409572=CARTESIAN_POINT('Ctrl Pts',(2.27342895555082,-1.38773290976438,
8.86648636486737));
#409573=CARTESIAN_POINT('Ctrl Pts',(2.2676470379875,-1.38653060731339,8.87206031107456));
#409574=CARTESIAN_POINT('Ctrl Pts',(2.27924360121797,-1.37753703682522,
8.86341338519876));
#409575=CARTESIAN_POINT('Ctrl Pts',(2.28185900586176,-1.37371170949497,
8.86654584966059));
#409576=CARTESIAN_POINT('Ctrl Pts',(2.27805961224584,-1.36916321953248,
8.87215952290715));
#409577=CARTESIAN_POINT('Ctrl Pts',(2.28443929758137,-1.37777905311488,
8.85049129520029));
#409578=CARTESIAN_POINT('Ctrl Pts',(2.29027258849564,-1.37805076865112,
8.85711686593484));
#409579=CARTESIAN_POINT('Ctrl Pts',(2.29260852370879,-1.36982616113503,
8.85933012996512));
#409580=CARTESIAN_POINT('Origin',(2.26737713379147,-1.39439786054282,8.85049129520029));
#409581=CARTESIAN_POINT('Ctrl Pts',(2.3141600729029,-1.44988459233544,8.78727029226991));
#409582=CARTESIAN_POINT('Ctrl Pts',(2.31713568099515,-1.45499351904854,
8.79393457792714));
#409583=CARTESIAN_POINT('Ctrl Pts',(2.31082965924422,-1.46089889836361,
8.79610912703474));
#409584=CARTESIAN_POINT('Ctrl Pts',(2.30218324533452,-1.42932115373562,
8.80838214965003));
#409585=CARTESIAN_POINT('Ctrl Pts',(2.30515835925059,-1.43442923198012,
8.81501364461989));
#409586=CARTESIAN_POINT('Ctrl Pts',(2.29887186472478,-1.44030535307933,
8.81722098428721));
#409587=CARTESIAN_POINT('Ctrl Pts',(2.29018987439862,-1.40872931124334,
8.82945683644721));
#409588=CARTESIAN_POINT('Ctrl Pts',(2.29315329328017,-1.41381730986973,
8.83607469902388));
#409589=CARTESIAN_POINT('Ctrl Pts',(2.2868978141797,-1.41968254846006,8.8382956714852));
#409590=CARTESIAN_POINT('Ctrl Pts',(2.27817859968918,-1.38810672912943,
8.85049129520029));
#409591=CARTESIAN_POINT('Ctrl Pts',(2.28111762290111,-1.39315284196833,
8.85711686593484));
#409592=CARTESIAN_POINT('Ctrl Pts',(2.27490615106176,-1.39902807640644,
8.85933012996512));
#409593=CARTESIAN_POINT('Origin',(2.30335860700519,-1.45617572374883,8.78727029226991));
#409594=CARTESIAN_POINT('Ctrl Pts',(2.32112429917461,-1.46184175524037,
8.75374538247849));
#409595=CARTESIAN_POINT('Ctrl Pts',(2.32496012354654,-1.46840154409179,
8.75304829418602));
#409596=CARTESIAN_POINT('Ctrl Pts',(2.32084701402089,-1.47483217184024,
8.75272238421917));
#409597=CARTESIAN_POINT('Ctrl Pts',(2.32178863480649,-1.46298237572162,
8.76769408445018));
#409598=CARTESIAN_POINT('Ctrl Pts',(2.32572038980644,-1.46970758632,8.76974318093968));
#409599=CARTESIAN_POINT('Ctrl Pts',(2.32180392561553,-1.47616356537213,
8.77077869880429));
#409600=CARTESIAN_POINT('Ctrl Pts',(2.31838362881724,-1.45713620489586,
8.78108014887992));
#409601=CARTESIAN_POINT('Ctrl Pts',(2.32171892952992,-1.4628336610349,8.78639403366326));
#409602=CARTESIAN_POINT('Ctrl Pts',(2.31690771126943,-1.46934321206233,
8.78812224174742));
#409603=CARTESIAN_POINT('Ctrl Pts',(2.31280357563322,-1.4475556214855,8.78944554828685));
#409604=CARTESIAN_POINT('Ctrl Pts',(2.31561927425866,-1.45235439829503,
8.79673892988685));
#409605=CARTESIAN_POINT('Ctrl Pts',(2.3088923932561,-1.45820697262553,8.79894799272499));
#409606=CARTESIAN_POINT('Origin',(2.3104160390574,-1.46829287829994,8.75721825406948));
#409607=CARTESIAN_POINT('Origin',(2.3104160390574,-1.46829287829994,9.));
#409608=CARTESIAN_POINT('Origin',(2.3104160390574,-1.46829287829994,7.51860402984325));
#409609=CARTESIAN_POINT('Ctrl Pts',(2.32799800459714,-1.45698248618141,
7.50366195182966));
#409610=CARTESIAN_POINT('Ctrl Pts',(2.33110214420567,-1.45892521853581,
7.50000065167735));
#409611=CARTESIAN_POINT('Ctrl Pts',(2.3311021442056,-1.45892521853591,7.49482233047108));
#409612=CARTESIAN_POINT('Ctrl Pts',(2.32540754212621,-1.46395696134398,
7.50215800491337));
#409613=CARTESIAN_POINT('Ctrl Pts',(2.32604450161756,-1.46700638420423,
7.49877273257267));
#409614=CARTESIAN_POINT('Ctrl Pts',(2.32421310714897,-1.46993267035743,
7.49481816995649));
#409615=CARTESIAN_POINT('Ctrl Pts',(2.32263636524652,-1.46443716447142,
7.51043025814042));
#409616=CARTESIAN_POINT('Ctrl Pts',(2.32408184125221,-1.47009431535362,
7.51006209594513));
#409617=CARTESIAN_POINT('Ctrl Pts',(2.32096452598623,-1.47499954885414,
7.50731281821698));
#409618=CARTESIAN_POINT('Ctrl Pts',(2.32121674419913,-1.46200044089927,
7.51860402984325));
#409619=CARTESIAN_POINT('Ctrl Pts',(2.32504721351855,-1.46857528098733,
7.51860402984325));
#409620=CARTESIAN_POINT('Ctrl Pts',(2.3209658839846,-1.47499741199082,7.51860402984325));
#409621=CARTESIAN_POINT('Origin',(0.,0.,7.5));
#459208=UNCERTAINTY_MEASURE_WITH_UNIT(LENGTH_MEASURE(0.01),#459243,
'DISTANCE_ACCURACY_VALUE',
'Maximum model space distance between geometric entities at asserted c
onnectivities');
#459216=UNCERTAINTY_MEASURE_WITH_UNIT(LENGTH_MEASURE(0.01),#459243,
'DISTANCE_ACCURACY_VALUE',
'Maximum model space distance between geometric entities at asserted c
onnectivities');
#459234=(
GEOMETRIC_REPRESENTATION_CONTEXT(3)
GLOBAL_UNCERTAINTY_ASSIGNED_CONTEXT((#459208))
GLOBAL_UNIT_ASSIGNED_CONTEXT((#459243,#459245,#459246))
REPRESENTATION_CONTEXT('','3D')
);
#459242=(
GEOMETRIC_REPRESENTATION_CONTEXT(3)
GLOBAL_UNCERTAINTY_ASSIGNED_CONTEXT((#459216))
GLOBAL_UNIT_ASSIGNED_CONTEXT((#459243,#459245,#459246))
REPRESENTATION_CONTEXT('','3D')
);
#459243=(
LENGTH_UNIT()
NAMED_UNIT(*)
SI_UNIT(.MILLI.,.METRE.)
);
#459245=(
NAMED_UNIT(*)
PLANE_ANGLE_UNIT()
SI_UNIT($,.RADIAN.)
);
#459246=(
NAMED_UNIT(*)
SI_UNIT($,.STERADIAN.)
SOLID_ANGLE_UNIT()
);
#459264=SHAPE_DEFINITION_REPRESENTATION(#459291,#459345);
#459291=PRODUCT_DEFINITION_SHAPE('',$,#459371);
#459345=SHAPE_REPRESENTATION('',(#99385),#459234);
#459353=PRODUCT_DEFINITION_CONTEXT('part definition',#459430,'design');
#459371=PRODUCT_DEFINITION('Assembly Screw 2','Assembly Screw 2',#459396,
#459353);
#459396=PRODUCT_DEFINITION_FORMATION('',$,#459449);
#459430=APPLICATION_CONTEXT(
'Core Data for Automotive Mechanical Design Process');
#459431=PRODUCT_CONTEXT('part definition',#459430,'mechanical');
#459449=PRODUCT('Assembly Screw 2','Assembly Screw 2',$,(#459431));
#459527=COLOUR_RGB('Black',0.12,0.14,0.17);
#459528=FILL_AREA_STYLE_COLOUR('',#459527);
#459529=FILL_AREA_STYLE('',(#459528));
#459530=SURFACE_STYLE_FILL_AREA(#459529);
#459531=SURFACE_SIDE_STYLE('',(#459530));
#459532=SURFACE_STYLE_USAGE(.BOTH.,#459531);
#459533=PRESENTATION_STYLE_ASSIGNMENT((#459532));
ENDSEC;
END-ISO-10303-21;
